ISO-10303-21;
HEADER;
/* Generated by software containing ST-Developer
 * from STEP Tools, Inc. (www.steptools.com) 
 */

FILE_DESCRIPTION(
/* description */ (''),
/* implementation_level */ '2;1');

FILE_NAME(
/* name */ 'Screw.step',
/* time_stamp */ '2026-10-06T13:41:14-07:00',
/* author */ (''),
/* organization */ (''),
/* preprocessor_version */ 'ST-DEVELOPER v20.2',
/* originating_system */ 'Autodesk Translation Framework v15.15.0.0',
/* authorisation */ '');

FILE_SCHEMA (('AUTOMOTIVE_DESIGN { 1 0 10303 214 3 1 1 }'));
ENDSEC;

DATA;
#10=MECHANICAL_DESIGN_GEOMETRIC_PRESENTATION_REPRESENTATION('',(#1961),#279266);
#47=B_SPLINE_SURFACE_WITH_KNOTS('',3,3,((#188642,#188643,#188644,#188645,
#188646,#188647,#188648,#188649,#188650,#188651,#188652,#188653,#188654,
#188655,#188656,#188657,#188658,#188659,#188660,#188661,#188662,#188663,
#188664,#188665,#188666,#188667,#188668,#188669,#188670,#188671,#188672,
#188673,#188674,#188675,#188676,#188677,#188678,#188679,#188680,#188681,
#188682,#188683,#188684,#188685,#188686,#188687,#188688,#188689,#188690,
#188691,#188692,#188693,#188694,#188695,#188696,#188697,#188698,#188699,
#188700,#188701,#188702,#188703,#188704,#188705,#188706,#188707,#188708,
#188709,#188710,#188711,#188712,#188713,#188714,#188715,#188716,#188717,
#188718,#188719,#188720,#188721,#188722,#188723,#188724,#188725,#188726,
#188727,#188728,#188729,#188730,#188731,#188732,#188733,#188734,#188735,
#188736,#188737,#188738,#188739,#188740,#188741,#188742,#188743,#188744,
#188745,#188746,#188747,#188748,#188749,#188750,#188751,#188752,#188753,
#188754,#188755,#188756,#188757,#188758,#188759,#188760,#188761,#188762,
#188763,#188764,#188765,#188766,#188767,#188768,#188769,#188770,#188771,
#188772,#188773,#188774,#188775,#188776,#188777,#188778,#188779,#188780,
#188781,#188782,#188783,#188784,#188785,#188786,#188787,#188788,#188789,
#188790,#188791,#188792,#188793,#188794,#188795,#188796,#188797,#188798,
#188799,#188800,#188801,#188802,#188803,#188804,#188805,#188806,#188807,
#188808,#188809,#188810,#188811,#188812,#188813,#188814,#188815,#188816,
#188817,#188818,#188819,#188820,#188821,#188822,#188823,#188824,#188825,
#188826,#188827,#188828,#188829,#188830,#188831,#188832,#188833,#188834,
#188835,#188836,#188837,#188838,#188839,#188840,#188841,#188842,#188843,
#188844,#188845,#188846,#188847,#188848,#188849,#188850,#188851,#188852,
#188853,#188854,#188855,#188856,#188857,#188858,#188859,#188860,#188861,
#188862,#188863,#188864,#188865,#188866,#188867,#188868,#188869,#188870,
#188871,#188872,#188873,#188874,#188875,#188876,#188877,#188878,#188879,
#188880,#188881,#188882,#188883,#188884,#188885,#188886,#188887,#188888,
#188889,#188890,#188891,#188892,#188893,#188894,#188895,#188896,#188897,
#188898,#188899,#188900,#188901,#188902,#188903,#188904,#188905,#188906,
#188907,#188908,#188909,#188910,#188911,#188912,#188913,#188914,#188915,
#188916,#188917,#188918,#188919,#188920,#188921,#188922,#188923,#188924,
#188925,#188926,#188927,#188928,#188929,#188930,#188931,#188932,#188933,
#188934,#188935,#188936,#188937,#188938,#188939,#188940,#188941,#188942,
#188943,#188944,#188945,#188946,#188947,#188948,#188949,#188950,#188951,
#188952,#188953,#188954,#188955,#188956,#188957,#188958,#188959,#188960,
#188961,#188962,#188963,#188964,#188965,#188966,#188967,#188968,#188969,
#188970,#188971,#188972,#188973,#188974,#188975,#188976,#188977,#188978,
#188979,#188980,#188981,#188982,#188983,#188984,#188985,#188986,#188987,
#188988,#188989,#188990,#188991,#188992,#188993,#188994,#188995,#188996,
#188997,#188998,#188999,#189000,#189001,#189002,#189003,#189004,#189005,
#189006,#189007,#189008,#189009,#189010,#189011,#189012,#189013,#189014,
#189015,#189016,#189017,#189018,#189019,#189020,#189021,#189022,#189023,
#189024,#189025,#189026,#189027,#189028,#189029,#189030,#189031,#189032,
#189033,#189034,#189035,#189036,#189037,#189038,#189039,#189040,#189041,
#189042,#189043,#189044,#189045,#189046,#189047,#189048,#189049,#189050,
#189051,#189052,#189053,#189054,#189055,#189056,#189057,#189058,#189059,
#189060,#189061,#189062,#189063,#189064,#189065,#189066,#189067,#189068,
#189069,#189070,#189071,#189072,#189073,#189074,#189075,#189076,#189077,
#189078,#189079,#189080,#189081,#189082,#189083,#189084,#189085,#189086,
#189087,#189088,#189089,#189090,#189091,#189092,#189093,#189094,#189095,
#189096,#189097,#189098,#189099,#189100,#189101,#189102,#189103,#189104,
#189105,#189106,#189107,#189108,#189109,#189110,#189111,#189112,#189113,
#189114,#189115,#189116,#189117,#189118,#189119,#189120,#189121,#189122,
#189123,#189124,#189125,#189126,#189127,#189128,#189129,#189130,#189131,
#189132,#189133,#189134,#189135,#189136,#189137,#189138,#189139,#189140,
#189141,#189142,#189143,#189144,#189145,#189146,#189147,#189148,#189149,
#189150,#189151,#189152,#189153,#189154,#189155,#189156,#189157,#189158,
#189159,#189160,#189161,#189162,#189163,#189164,#189165,#189166,#189167,
#189168,#189169,#189170,#189171,#189172,#189173,#189174,#189175,#189176,
#189177,#189178,#189179,#189180,#189181,#189182,#189183,#189184,#189185,
#189186,#189187,#189188,#189189,#189190,#189191,#189192,#189193,#189194,
#189195,#189196,#189197,#189198,#189199,#189200,#189201,#189202,#189203,
#189204,#189205,#189206,#189207,#189208,#189209,#189210,#189211,#189212,
#189213,#189214,#189215,#189216,#189217,#189218,#189219,#189220,#189221,
#189222,#189223,#189224,#189225,#189226,#189227,#189228,#189229,#189230,
#189231,#189232,#189233,#189234,#189235,#189236,#189237,#189238,#189239,
#189240,#189241,#189242,#189243,#189244,#189245,#189246,#189247,#189248,
#189249,#189250,#189251,#189252,#189253,#189254,#189255,#189256,#189257,
#189258,#189259,#189260,#189261,#189262,#189263,#189264,#189265,#189266,
#189267,#189268,#189269,#189270,#189271,#189272,#189273,#189274,#189275,
#189276,#189277,#189278,#189279,#189280,#189281,#189282,#189283,#189284,
#189285,#189286,#189287,#189288,#189289,#189290,#189291,#189292,#189293,
#189294,#189295,#189296,#189297,#189298,#189299,#189300,#189301,#189302,
#189303,#189304,#189305,#189306,#189307,#189308,#189309,#189310,#189311,
#189312,#189313,#189314,#189315,#189316,#189317,#189318,#189319,#189320,
#189321,#189322,#189323,#189324,#189325,#189326,#189327,#189328,#189329,
#189330,#189331,#189332,#189333,#189334,#189335,#189336,#189337,#189338,
#189339,#189340,#189341,#189342,#189343,#189344,#189345,#189346,#189347,
#189348,#189349,#189350,#189351,#189352,#189353,#189354,#189355,#189356,
#189357,#189358,#189359,#189360,#189361,#189362,#189363,#189364,#189365,
#189366,#189367,#189368,#189369,#189370,#189371,#189372,#189373,#189374,
#189375,#189376,#189377,#189378,#189379,#189380,#189381,#189382,#189383,
#189384,#189385,#189386,#189387,#189388,#189389,#189390,#189391,#189392,
#189393,#189394,#189395,#189396,#189397,#189398,#189399,#189400,#189401,
#189402,#189403,#189404,#189405,#189406,#189407,#189408,#189409,#189410,
#189411,#189412,#189413,#189414,#189415,#189416,#189417,#189418,#189419,
#189420,#189421,#189422,#189423,#189424,#189425,#189426,#189427,#189428,
#189429,#189430,#189431,#189432,#189433,#189434,#189435,#189436,#189437,
#189438,#189439,#189440,#189441,#189442,#189443,#189444,#189445,#189446,
#189447,#189448,#189449,#189450,#189451,#189452,#189453,#189454,#189455,
#189456,#189457,#189458,#189459,#189460,#189461,#189462,#189463,#189464,
#189465,#189466,#189467,#189468,#189469,#189470,#189471,#189472,#189473,
#189474,#189475,#189476,#189477,#189478,#189479,#189480,#189481,#189482,
#189483,#189484,#189485,#189486,#189487,#189488,#189489,#189490,#189491,
#189492,#189493,#189494,#189495,#189496,#189497,#189498,#189499,#189500,
#189501,#189502,#189503,#189504,#189505,#189506,#189507,#189508,#189509,
#189510,#189511,#189512,#189513,#189514,#189515,#189516,#189517,#189518,
#189519,#189520,#189521,#189522,#189523,#189524,#189525,#189526,#189527,
#189528,#189529,#189530,#189531,#189532,#189533,#189534,#189535,#189536,
#189537,#189538,#189539,#189540,#189541,#189542,#189543,#189544,#189545,
#189546,#189547,#189548,#189549,#189550,#189551,#189552,#189553,#189554,
#189555,#189556,#189557,#189558,#189559,#189560,#189561,#189562,#189563,
#189564,#189565,#189566,#189567,#189568,#189569,#189570,#189571,#189572,
#189573,#189574,#189575,#189576,#189577,#189578,#189579,#189580,#189581,
#189582,#189583,#189584,#189585,#189586,#189587,#189588,#189589,#189590,
#189591,#189592,#189593,#189594,#189595,#189596,#189597,#189598,#189599,
#189600,#189601,#189602,#189603,#189604,#189605,#189606,#189607,#189608,
#189609,#189610,#189611,#189612,#189613,#189614,#189615,#189616,#189617,
#189618,#189619,#189620,#189621,#189622,#189623,#189624,#189625,#189626,
#189627,#189628,#189629,#189630,#189631,#189632,#189633,#189634,#189635,
#189636,#189637,#189638,#189639,#189640,#189641,#189642,#189643,#189644,
#189645,#189646,#189647,#189648,#189649,#189650,#189651,#189652,#189653,
#189654,#189655,#189656,#189657,#189658,#189659,#189660,#189661,#189662,
#189663,#189664,#189665,#189666,#189667,#189668,#189669,#189670,#189671,
#189672,#189673,#189674,#189675,#189676,#189677,#189678,#189679,#189680,
#189681,#189682,#189683,#189684,#189685,#189686,#189687,#189688,#189689,
#189690,#189691,#189692,#189693,#189694,#189695,#189696,#189697,#189698,
#189699,#189700,#189701,#189702,#189703,#189704,#189705,#189706,#189707,
#189708,#189709,#189710,#189711,#189712,#189713,#189714,#189715,#189716,
#189717,#189718,#189719,#189720,#189721,#189722,#189723,#189724,#189725,
#189726,#189727,#189728,#189729,#189730,#189731,#189732,#189733,#189734,
#189735,#189736,#189737,#189738,#189739,#189740,#189741,#189742,#189743,
#189744,#189745,#189746,#189747,#189748,#189749,#189750,#189751,#189752,
#189753,#189754,#189755,#189756,#189757,#189758,#189759,#189760,#189761,
#189762,#189763,#189764,#189765,#189766,#189767,#189768,#189769,#189770,
#189771,#189772,#189773,#189774,#189775,#189776,#189777,#189778,#189779,
#189780,#189781,#189782,#189783,#189784,#189785,#189786,#189787,#189788,
#189789,#189790,#189791,#189792,#189793,#189794,#189795,#189796,#189797,
#189798,#189799,#189800,#189801,#189802,#189803,#189804,#189805,#189806,
#189807,#189808,#189809,#189810,#189811,#189812,#189813,#189814,#189815,
#189816,#189817,#189818,#189819,#189820,#189821,#189822,#189823,#189824,
#189825,#189826,#189827,#189828,#189829,#189830,#189831,#189832,#189833,
#189834,#189835,#189836,#189837,#189838,#189839,#189840,#189841,#189842,
#189843,#189844,#189845,#189846,#189847,#189848,#189849,#189850,#189851,
#189852,#189853,#189854,#189855,#189856,#189857,#189858,#189859,#189860,
#189861,#189862,#189863,#189864,#189865,#189866,#189867,#189868,#189869,
#189870,#189871,#189872,#189873,#189874,#189875,#189876,#189877,#189878,
#189879,#189880,#189881,#189882,#189883,#189884,#189885,#189886,#189887,
#189888,#189889,#189890,#189891,#189892,#189893,#189894,#189895,#189896,
#189897,#189898,#189899,#189900,#189901,#189902,#189903,#189904,#189905,
#189906,#189907,#189908,#189909,#189910,#189911,#189912,#189913,#189914,
#189915,#189916,#189917,#189918,#189919,#189920,#189921,#189922,#189923,
#189924,#189925,#189926,#189927,#189928,#189929,#189930,#189931,#189932,
#189933,#189934,#189935,#189936,#189937,#189938,#189939,#189940,#189941,
#189942,#189943,#189944,#189945,#189946,#189947,#189948,#189949,#189950,
#189951,#189952,#189953,#189954,#189955,#189956,#189957,#189958,#189959,
#189960,#189961,#189962,#189963,#189964,#189965,#189966,#189967,#189968,
#189969,#189970,#189971,#189972,#189973,#189974,#189975,#189976,#189977,
#189978,#189979,#189980,#189981,#189982,#189983,#189984,#189985,#189986,
#189987,#189988,#189989,#189990,#189991,#189992,#189993,#189994,#189995,
#189996,#189997,#189998,#189999,#190000,#190001,#190002,#190003,#190004,
#190005,#190006,#190007,#190008,#190009,#190010,#190011,#190012,#190013,
#190014,#190015,#190016,#190017,#190018,#190019,#190020,#190021,#190022,
#190023,#190024,#190025,#190026,#190027,#190028,#190029,#190030,#190031,
#190032,#190033,#190034,#190035,#190036,#190037,#190038,#190039,#190040,
#190041,#190042,#190043,#190044,#190045,#190046,#190047,#190048,#190049,
#190050,#190051,#190052,#190053,#190054,#190055,#190056,#190057,#190058,
#190059,#190060,#190061,#190062,#190063,#190064,#190065,#190066,#190067,
#190068,#190069,#190070,#190071,#190072,#190073,#190074,#190075,#190076,
#190077,#190078,#190079,#190080,#190081,#190082,#190083,#190084,#190085,
#190086,#190087,#190088,#190089,#190090,#190091,#190092,#190093,#190094,
#190095,#190096,#190097,#190098,#190099,#190100,#190101,#190102,#190103,
#190104,#190105,#190106,#190107,#190108,#190109,#190110,#190111,#190112,
#190113,#190114,#190115,#190116,#190117,#190118,#190119,#190120,#190121,
#190122,#190123,#190124,#190125,#190126,#190127,#190128,#190129,#190130,
#190131,#190132,#190133,#190134,#190135,#190136,#190137,#190138,#190139,
#190140,#190141,#190142,#190143,#190144,#190145,#190146,#190147,#190148,
#190149,#190150,#190151,#190152,#190153,#190154,#190155,#190156,#190157,
#190158,#190159,#190160,#190161,#190162,#190163,#190164,#190165,#190166,
#190167,#190168,#190169,#190170,#190171,#190172,#190173,#190174,#190175,
#190176,#190177,#190178,#190179,#190180,#190181,#190182,#190183,#190184,
#190185,#190186,#190187,#190188,#190189,#190190,#190191,#190192,#190193,
#190194,#190195,#190196,#190197,#190198,#190199,#190200,#190201,#190202,
#190203,#190204,#190205,#190206,#190207,#190208,#190209,#190210,#190211,
#190212,#190213,#190214,#190215,#190216,#190217,#190218,#190219,#190220,
#190221,#190222,#190223,#190224,#190225,#190226,#190227,#190228,#190229,
#190230,#190231,#190232,#190233,#190234,#190235,#190236,#190237,#190238,
#190239,#190240,#190241,#190242,#190243,#190244,#190245,#190246,#190247,
#190248,#190249,#190250,#190251,#190252,#190253,#190254,#190255,#190256,
#190257,#190258,#190259,#190260,#190261,#190262,#190263,#190264,#190265,
#190266,#190267,#190268,#190269,#190270,#190271,#190272,#190273,#190274,
#190275,#190276,#190277,#190278,#190279,#190280,#190281,#190282,#190283,
#190284,#190285,#190286,#190287,#190288,#190289,#190290,#190291,#190292,
#190293,#190294,#190295,#190296,#190297,#190298,#190299,#190300,#190301,
#190302,#190303,#190304,#190305,#190306,#190307,#190308,#190309,#190310,
#190311,#190312,#190313,#190314,#190315,#190316,#190317,#190318,#190319,
#190320,#190321,#190322,#190323,#190324,#190325,#190326,#190327,#190328,
#190329,#190330,#190331,#190332,#190333,#190334,#190335,#190336),(#190337,
#190338,#190339,#190340,#190341,#190342,#190343,#190344,#190345,#190346,
#190347,#190348,#190349,#190350,#190351,#190352,#190353,#190354,#190355,
#190356,#190357,#190358,#190359,#190360,#190361,#190362,#190363,#190364,
#190365,#190366,#190367,#190368,#190369,#190370,#190371,#190372,#190373,
#190374,#190375,#190376,#190377,#190378,#190379,#190380,#190381,#190382,
#190383,#190384,#190385,#190386,#190387,#190388,#190389,#190390,#190391,
#190392,#190393,#190394,#190395,#190396,#190397,#190398,#190399,#190400,
#190401,#190402,#190403,#190404,#190405,#190406,#190407,#190408,#190409,
#190410,#190411,#190412,#190413,#190414,#190415,#190416,#190417,#190418,
#190419,#190420,#190421,#190422,#190423,#190424,#190425,#190426,#190427,
#190428,#190429,#190430,#190431,#190432,#190433,#190434,#190435,#190436,
#190437,#190438,#190439,#190440,#190441,#190442,#190443,#190444,#190445,
#190446,#190447,#190448,#190449,#190450,#190451,#190452,#190453,#190454,
#190455,#190456,#190457,#190458,#190459,#190460,#190461,#190462,#190463,
#190464,#190465,#190466,#190467,#190468,#190469,#190470,#190471,#190472,
#190473,#190474,#190475,#190476,#190477,#190478,#190479,#190480,#190481,
#190482,#190483,#190484,#190485,#190486,#190487,#190488,#190489,#190490,
#190491,#190492,#190493,#190494,#190495,#190496,#190497,#190498,#190499,
#190500,#190501,#190502,#190503,#190504,#190505,#190506,#190507,#190508,
#190509,#190510,#190511,#190512,#190513,#190514,#190515,#190516,#190517,
#190518,#190519,#190520,#190521,#190522,#190523,#190524,#190525,#190526,
#190527,#190528,#190529,#190530,#190531,#190532,#190533,#190534,#190535,
#190536,#190537,#190538,#190539,#190540,#190541,#190542,#190543,#190544,
#190545,#190546,#190547,#190548,#190549,#190550,#190551,#190552,#190553,
#190554,#190555,#190556,#190557,#190558,#190559,#190560,#190561,#190562,
#190563,#190564,#190565,#190566,#190567,#190568,#190569,#190570,#190571,
#190572,#190573,#190574,#190575,#190576,#190577,#190578,#190579,#190580,
#190581,#190582,#190583,#190584,#190585,#190586,#190587,#190588,#190589,
#190590,#190591,#190592,#190593,#190594,#190595,#190596,#190597,#190598,
#190599,#190600,#190601,#190602,#190603,#190604,#190605,#190606,#190607,
#190608,#190609,#190610,#190611,#190612,#190613,#190614,#190615,#190616,
#190617,#190618,#190619,#190620,#190621,#190622,#190623,#190624,#190625,
#190626,#190627,#190628,#190629,#190630,#190631,#190632,#190633,#190634,
#190635,#190636,#190637,#190638,#190639,#190640,#190641,#190642,#190643,
#190644,#190645,#190646,#190647,#190648,#190649,#190650,#190651,#190652,
#190653,#190654,#190655,#190656,#190657,#190658,#190659,#190660,#190661,
#190662,#190663,#190664,#190665,#190666,#190667,#190668,#190669,#190670,
#190671,#190672,#190673,#190674,#190675,#190676,#190677,#190678,#190679,
#190680,#190681,#190682,#190683,#190684,#190685,#190686,#190687,#190688,
#190689,#190690,#190691,#190692,#190693,#190694,#190695,#190696,#190697,
#190698,#190699,#190700,#190701,#190702,#190703,#190704,#190705,#190706,
#190707,#190708,#190709,#190710,#190711,#190712,#190713,#190714,#190715,
#190716,#190717,#190718,#190719,#190720,#190721,#190722,#190723,#190724,
#190725,#190726,#190727,#190728,#190729,#190730,#190731,#190732,#190733,
#190734,#190735,#190736,#190737,#190738,#190739,#190740,#190741,#190742,
#190743,#190744,#190745,#190746,#190747,#190748,#190749,#190750,#190751,
#190752,#190753,#190754,#190755,#190756,#190757,#190758,#190759,#190760,
#190761,#190762,#190763,#190764,#190765,#190766,#190767,#190768,#190769,
#190770,#190771,#190772,#190773,#190774,#190775,#190776,#190777,#190778,
#190779,#190780,#190781,#190782,#190783,#190784,#190785,#190786,#190787,
#190788,#190789,#190790,#190791,#190792,#190793,#190794,#190795,#190796,
#190797,#190798,#190799,#190800,#190801,#190802,#190803,#190804,#190805,
#190806,#190807,#190808,#190809,#190810,#190811,#190812,#190813,#190814,
#190815,#190816,#190817,#190818,#190819,#190820,#190821,#190822,#190823,
#190824,#190825,#190826,#190827,#190828,#190829,#190830,#190831,#190832,
#190833,#190834,#190835,#190836,#190837,#190838,#190839,#190840,#190841,
#190842,#190843,#190844,#190845,#190846,#190847,#190848,#190849,#190850,
#190851,#190852,#190853,#190854,#190855,#190856,#190857,#190858,#190859,
#190860,#190861,#190862,#190863,#190864,#190865,#190866,#190867,#190868,
#190869,#190870,#190871,#190872,#190873,#190874,#190875,#190876,#190877,
#190878,#190879,#190880,#190881,#190882,#190883,#190884,#190885,#190886,
#190887,#190888,#190889,#190890,#190891,#190892,#190893,#190894,#190895,
#190896,#190897,#190898,#190899,#190900,#190901,#190902,#190903,#190904,
#190905,#190906,#190907,#190908,#190909,#190910,#190911,#190912,#190913,
#190914,#190915,#190916,#190917,#190918,#190919,#190920,#190921,#190922,
#190923,#190924,#190925,#190926,#190927,#190928,#190929,#190930,#190931,
#190932,#190933,#190934,#190935,#190936,#190937,#190938,#190939,#190940,
#190941,#190942,#190943,#190944,#190945,#190946,#190947,#190948,#190949,
#190950,#190951,#190952,#190953,#190954,#190955,#190956,#190957,#190958,
#190959,#190960,#190961,#190962,#190963,#190964,#190965,#190966,#190967,
#190968,#190969,#190970,#190971,#190972,#190973,#190974,#190975,#190976,
#190977,#190978,#190979,#190980,#190981,#190982,#190983,#190984,#190985,
#190986,#190987,#190988,#190989,#190990,#190991,#190992,#190993,#190994,
#190995,#190996,#190997,#190998,#190999,#191000,#191001,#191002,#191003,
#191004,#191005,#191006,#191007,#191008,#191009,#191010,#191011,#191012,
#191013,#191014,#191015,#191016,#191017,#191018,#191019,#191020,#191021,
#191022,#191023,#191024,#191025,#191026,#191027,#191028,#191029,#191030,
#191031,#191032,#191033,#191034,#191035,#191036,#191037,#191038,#191039,
#191040,#191041,#191042,#191043,#191044,#191045,#191046,#191047,#191048,
#191049,#191050,#191051,#191052,#191053,#191054,#191055,#191056,#191057,
#191058,#191059,#191060,#191061,#191062,#191063,#191064,#191065,#191066,
#191067,#191068,#191069,#191070,#191071,#191072,#191073,#191074,#191075,
#191076,#191077,#191078,#191079,#191080,#191081,#191082,#191083,#191084,
#191085,#191086,#191087,#191088,#191089,#191090,#191091,#191092,#191093,
#191094,#191095,#191096,#191097,#191098,#191099,#191100,#191101,#191102,
#191103,#191104,#191105,#191106,#191107,#191108,#191109,#191110,#191111,
#191112,#191113,#191114,#191115,#191116,#191117,#191118,#191119,#191120,
#191121,#191122,#191123,#191124,#191125,#191126,#191127,#191128,#191129,
#191130,#191131,#191132,#191133,#191134,#191135,#191136,#191137,#191138,
#191139,#191140,#191141,#191142,#191143,#191144,#191145,#191146,#191147,
#191148,#191149,#191150,#191151,#191152,#191153,#191154,#191155,#191156,
#191157,#191158,#191159,#191160,#191161,#191162,#191163,#191164,#191165,
#191166,#191167,#191168,#191169,#191170,#191171,#191172,#191173,#191174,
#191175,#191176,#191177,#191178,#191179,#191180,#191181,#191182,#191183,
#191184,#191185,#191186,#191187,#191188,#191189,#191190,#191191,#191192,
#191193,#191194,#191195,#191196,#191197,#191198,#191199,#191200,#191201,
#191202,#191203,#191204,#191205,#191206,#191207,#191208,#191209,#191210,
#191211,#191212,#191213,#191214,#191215,#191216,#191217,#191218,#191219,
#191220,#191221,#191222,#191223,#191224,#191225,#191226,#191227,#191228,
#191229,#191230,#191231,#191232,#191233,#191234,#191235,#191236,#191237,
#191238,#191239,#191240,#191241,#191242,#191243,#191244,#191245,#191246,
#191247,#191248,#191249,#191250,#191251,#191252,#191253,#191254,#191255,
#191256,#191257,#191258,#191259,#191260,#191261,#191262,#191263,#191264,
#191265,#191266,#191267,#191268,#191269,#191270,#191271,#191272,#191273,
#191274,#191275,#191276,#191277,#191278,#191279,#191280,#191281,#191282,
#191283,#191284,#191285,#191286,#191287,#191288,#191289,#191290,#191291,
#191292,#191293,#191294,#191295,#191296,#191297,#191298,#191299,#191300,
#191301,#191302,#191303,#191304,#191305,#191306,#191307,#191308,#191309,
#191310,#191311,#191312,#191313,#191314,#191315,#191316,#191317,#191318,
#191319,#191320,#191321,#191322,#191323,#191324,#191325,#191326,#191327,
#191328,#191329,#191330,#191331,#191332,#191333,#191334,#191335,#191336,
#191337,#191338,#191339,#191340,#191341,#191342,#191343,#191344,#191345,
#191346,#191347,#191348,#191349,#191350,#191351,#191352,#191353,#191354,
#191355,#191356,#191357,#191358,#191359,#191360,#191361,#191362,#191363,
#191364,#191365,#191366,#191367,#191368,#191369,#191370,#191371,#191372,
#191373,#191374,#191375,#191376,#191377,#191378,#191379,#191380,#191381,
#191382,#191383,#191384,#191385,#191386,#191387,#191388,#191389,#191390,
#191391,#191392,#191393,#191394,#191395,#191396,#191397,#191398,#191399,
#191400,#191401,#191402,#191403,#191404,#191405,#191406,#191407,#191408,
#191409,#191410,#191411,#191412,#191413,#191414,#191415,#191416,#191417,
#191418,#191419,#191420,#191421,#191422,#191423,#191424,#191425,#191426,
#191427,#191428,#191429,#191430,#191431,#191432,#191433,#191434,#191435,
#191436,#191437,#191438,#191439,#191440,#191441,#191442,#191443,#191444,
#191445,#191446,#191447,#191448,#191449,#191450,#191451,#191452,#191453,
#191454,#191455,#191456,#191457,#191458,#191459,#191460,#191461,#191462,
#191463,#191464,#191465,#191466,#191467,#191468,#191469,#191470,#191471,
#191472,#191473,#191474,#191475,#191476,#191477,#191478,#191479,#191480,
#191481,#191482,#191483,#191484,#191485,#191486,#191487,#191488,#191489,
#191490,#191491,#191492,#191493,#191494,#191495,#191496,#191497,#191498,
#191499,#191500,#191501,#191502,#191503,#191504,#191505,#191506,#191507,
#191508,#191509,#191510,#191511,#191512,#191513,#191514,#191515,#191516,
#191517,#191518,#191519,#191520,#191521,#191522,#191523,#191524,#191525,
#191526,#191527,#191528,#191529,#191530,#191531,#191532,#191533,#191534,
#191535,#191536,#191537,#191538,#191539,#191540,#191541,#191542,#191543,
#191544,#191545,#191546,#191547,#191548,#191549,#191550,#191551,#191552,
#191553,#191554,#191555,#191556,#191557,#191558,#191559,#191560,#191561,
#191562,#191563,#191564,#191565,#191566,#191567,#191568,#191569,#191570,
#191571,#191572,#191573,#191574,#191575,#191576,#191577,#191578,#191579,
#191580,#191581,#191582,#191583,#191584,#191585,#191586,#191587,#191588,
#191589,#191590,#191591,#191592,#191593,#191594,#191595,#191596,#191597,
#191598,#191599,#191600,#191601,#191602,#191603,#191604,#191605,#191606,
#191607,#191608,#191609,#191610,#191611,#191612,#191613,#191614,#191615,
#191616,#191617,#191618,#191619,#191620,#191621,#191622,#191623,#191624,
#191625,#191626,#191627,#191628,#191629,#191630,#191631,#191632,#191633,
#191634,#191635,#191636,#191637,#191638,#191639,#191640,#191641,#191642,
#191643,#191644,#191645,#191646,#191647,#191648,#191649,#191650,#191651,
#191652,#191653,#191654,#191655,#191656,#191657,#191658,#191659,#191660,
#191661,#191662,#191663,#191664,#191665,#191666,#191667,#191668,#191669,
#191670,#191671,#191672,#191673,#191674,#191675,#191676,#191677,#191678,
#191679,#191680,#191681,#191682,#191683,#191684,#191685,#191686,#191687,
#191688,#191689,#191690,#191691,#191692,#191693,#191694,#191695,#191696,
#191697,#191698,#191699,#191700,#191701,#191702,#191703,#191704,#191705,
#191706,#191707,#191708,#191709,#191710,#191711,#191712,#191713,#191714,
#191715,#191716,#191717,#191718,#191719,#191720,#191721,#191722,#191723,
#191724,#191725,#191726,#191727,#191728,#191729,#191730,#191731,#191732,
#191733,#191734,#191735,#191736,#191737,#191738,#191739,#191740,#191741,
#191742,#191743,#191744,#191745,#191746,#191747,#191748,#191749,#191750,
#191751,#191752,#191753,#191754,#191755,#191756,#191757,#191758,#191759,
#191760,#191761,#191762,#191763,#191764,#191765,#191766,#191767,#191768,
#191769,#191770,#191771,#191772,#191773,#191774,#191775,#191776,#191777,
#191778,#191779,#191780,#191781,#191782,#191783,#191784,#191785,#191786,
#191787,#191788,#191789,#191790,#191791,#191792,#191793,#191794,#191795,
#191796,#191797,#191798,#191799,#191800,#191801,#191802,#191803,#191804,
#191805,#191806,#191807,#191808,#191809,#191810,#191811,#191812,#191813,
#191814,#191815,#191816,#191817,#191818,#191819,#191820,#191821,#191822,
#191823,#191824,#191825,#191826,#191827,#191828,#191829,#191830,#191831,
#191832,#191833,#191834,#191835,#191836,#191837,#191838,#191839,#191840,
#191841,#191842,#191843,#191844,#191845,#191846,#191847,#191848,#191849,
#191850,#191851,#191852,#191853,#191854,#191855,#191856,#191857,#191858,
#191859,#191860,#191861,#191862,#191863,#191864,#191865,#191866,#191867,
#191868,#191869,#191870,#191871,#191872,#191873,#191874,#191875,#191876,
#191877,#191878,#191879,#191880,#191881,#191882,#191883,#191884,#191885,
#191886,#191887,#191888,#191889,#191890,#191891,#191892,#191893,#191894,
#191895,#191896,#191897,#191898,#191899,#191900,#191901,#191902,#191903,
#191904,#191905,#191906,#191907,#191908,#191909,#191910,#191911,#191912,
#191913,#191914,#191915,#191916,#191917,#191918,#191919,#191920,#191921,
#191922,#191923,#191924,#191925,#191926,#191927,#191928,#191929,#191930,
#191931,#191932,#191933,#191934,#191935,#191936,#191937,#191938,#191939,
#191940,#191941,#191942,#191943,#191944,#191945,#191946,#191947,#191948,
#191949,#191950,#191951,#191952,#191953,#191954,#191955,#191956,#191957,
#191958,#191959,#191960,#191961,#191962,#191963,#191964,#191965,#191966,
#191967,#191968,#191969,#191970,#191971,#191972,#191973,#191974,#191975,
#191976,#191977,#191978,#191979,#191980,#191981,#191982,#191983,#191984,
#191985,#191986,#191987,#191988,#191989,#191990,#191991,#191992,#191993,
#191994,#191995,#191996,#191997,#191998,#191999,#192000,#192001,#192002,
#192003,#192004,#192005,#192006,#192007,#192008,#192009,#192010,#192011,
#192012,#192013,#192014,#192015,#192016,#192017,#192018,#192019,#192020,
#192021,#192022,#192023,#192024,#192025,#192026,#192027,#192028,#192029,
#192030,#192031),(#192032,#192033,#192034,#192035,#192036,#192037,#192038,
#192039,#192040,#192041,#192042,#192043,#192044,#192045,#192046,#192047,
#192048,#192049,#192050,#192051,#192052,#192053,#192054,#192055,#192056,
#192057,#192058,#192059,#192060,#192061,#192062,#192063,#192064,#192065,
#192066,#192067,#192068,#192069,#192070,#192071,#192072,#192073,#192074,
#192075,#192076,#192077,#192078,#192079,#192080,#192081,#192082,#192083,
#192084,#192085,#192086,#192087,#192088,#192089,#192090,#192091,#192092,
#192093,#192094,#192095,#192096,#192097,#192098,#192099,#192100,#192101,
#192102,#192103,#192104,#192105,#192106,#192107,#192108,#192109,#192110,
#192111,#192112,#192113,#192114,#192115,#192116,#192117,#192118,#192119,
#192120,#192121,#192122,#192123,#192124,#192125,#192126,#192127,#192128,
#192129,#192130,#192131,#192132,#192133,#192134,#192135,#192136,#192137,
#192138,#192139,#192140,#192141,#192142,#192143,#192144,#192145,#192146,
#192147,#192148,#192149,#192150,#192151,#192152,#192153,#192154,#192155,
#192156,#192157,#192158,#192159,#192160,#192161,#192162,#192163,#192164,
#192165,#192166,#192167,#192168,#192169,#192170,#192171,#192172,#192173,
#192174,#192175,#192176,#192177,#192178,#192179,#192180,#192181,#192182,
#192183,#192184,#192185,#192186,#192187,#192188,#192189,#192190,#192191,
#192192,#192193,#192194,#192195,#192196,#192197,#192198,#192199,#192200,
#192201,#192202,#192203,#192204,#192205,#192206,#192207,#192208,#192209,
#192210,#192211,#192212,#192213,#192214,#192215,#192216,#192217,#192218,
#192219,#192220,#192221,#192222,#192223,#192224,#192225,#192226,#192227,
#192228,#192229,#192230,#192231,#192232,#192233,#192234,#192235,#192236,
#192237,#192238,#192239,#192240,#192241,#192242,#192243,#192244,#192245,
#192246,#192247,#192248,#192249,#192250,#192251,#192252,#192253,#192254,
#192255,#192256,#192257,#192258,#192259,#192260,#192261,#192262,#192263,
#192264,#192265,#192266,#192267,#192268,#192269,#192270,#192271,#192272,
#192273,#192274,#192275,#192276,#192277,#192278,#192279,#192280,#192281,
#192282,#192283,#192284,#192285,#192286,#192287,#192288,#192289,#192290,
#192291,#192292,#192293,#192294,#192295,#192296,#192297,#192298,#192299,
#192300,#192301,#192302,#192303,#192304,#192305,#192306,#192307,#192308,
#192309,#192310,#192311,#192312,#192313,#192314,#192315,#192316,#192317,
#192318,#192319,#192320,#192321,#192322,#192323,#192324,#192325,#192326,
#192327,#192328,#192329,#192330,#192331,#192332,#192333,#192334,#192335,
#192336,#192337,#192338,#192339,#192340,#192341,#192342,#192343,#192344,
#192345,#192346,#192347,#192348,#192349,#192350,#192351,#192352,#192353,
#192354,#192355,#192356,#192357,#192358,#192359,#192360,#192361,#192362,
#192363,#192364,#192365,#192366,#192367,#192368,#192369,#192370,#192371,
#192372,#192373,#192374,#192375,#192376,#192377,#192378,#192379,#192380,
#192381,#192382,#192383,#192384,#192385,#192386,#192387,#192388,#192389,
#192390,#192391,#192392,#192393,#192394,#192395,#192396,#192397,#192398,
#192399,#192400,#192401,#192402,#192403,#192404,#192405,#192406,#192407,
#192408,#192409,#192410,#192411,#192412,#192413,#192414,#192415,#192416,
#192417,#192418,#192419,#192420,#192421,#192422,#192423,#192424,#192425,
#192426,#192427,#192428,#192429,#192430,#192431,#192432,#192433,#192434,
#192435,#192436,#192437,#192438,#192439,#192440,#192441,#192442,#192443,
#192444,#192445,#192446,#192447,#192448,#192449,#192450,#192451,#192452,
#192453,#192454,#192455,#192456,#192457,#192458,#192459,#192460,#192461,
#192462,#192463,#192464,#192465,#192466,#192467,#192468,#192469,#192470,
#192471,#192472,#192473,#192474,#192475,#192476,#192477,#192478,#192479,
#192480,#192481,#192482,#192483,#192484,#192485,#192486,#192487,#192488,
#192489,#192490,#192491,#192492,#192493,#192494,#192495,#192496,#192497,
#192498,#192499,#192500,#192501,#192502,#192503,#192504,#192505,#192506,
#192507,#192508,#192509,#192510,#192511,#192512,#192513,#192514,#192515,
#192516,#192517,#192518,#192519,#192520,#192521,#192522,#192523,#192524,
#192525,#192526,#192527,#192528,#192529,#192530,#192531,#192532,#192533,
#192534,#192535,#192536,#192537,#192538,#192539,#192540,#192541,#192542,
#192543,#192544,#192545,#192546,#192547,#192548,#192549,#192550,#192551,
#192552,#192553,#192554,#192555,#192556,#192557,#192558,#192559,#192560,
#192561,#192562,#192563,#192564,#192565,#192566,#192567,#192568,#192569,
#192570,#192571,#192572,#192573,#192574,#192575,#192576,#192577,#192578,
#192579,#192580,#192581,#192582,#192583,#192584,#192585,#192586,#192587,
#192588,#192589,#192590,#192591,#192592,#192593,#192594,#192595,#192596,
#192597,#192598,#192599,#192600,#192601,#192602,#192603,#192604,#192605,
#192606,#192607,#192608,#192609,#192610,#192611,#192612,#192613,#192614,
#192615,#192616,#192617,#192618,#192619,#192620,#192621,#192622,#192623,
#192624,#192625,#192626,#192627,#192628,#192629,#192630,#192631,#192632,
#192633,#192634,#192635,#192636,#192637,#192638,#192639,#192640,#192641,
#192642,#192643,#192644,#192645,#192646,#192647,#192648,#192649,#192650,
#192651,#192652,#192653,#192654,#192655,#192656,#192657,#192658,#192659,
#192660,#192661,#192662,#192663,#192664,#192665,#192666,#192667,#192668,
#192669,#192670,#192671,#192672,#192673,#192674,#192675,#192676,#192677,
#192678,#192679,#192680,#192681,#192682,#192683,#192684,#192685,#192686,
#192687,#192688,#192689,#192690,#192691,#192692,#192693,#192694,#192695,
#192696,#192697,#192698,#192699,#192700,#192701,#192702,#192703,#192704,
#192705,#192706,#192707,#192708,#192709,#192710,#192711,#192712,#192713,
#192714,#192715,#192716,#192717,#192718,#192719,#192720,#192721,#192722,
#192723,#192724,#192725,#192726,#192727,#192728,#192729,#192730,#192731,
#192732,#192733,#192734,#192735,#192736,#192737,#192738,#192739,#192740,
#192741,#192742,#192743,#192744,#192745,#192746,#192747,#192748,#192749,
#192750,#192751,#192752,#192753,#192754,#192755,#192756,#192757,#192758,
#192759,#192760,#192761,#192762,#192763,#192764,#192765,#192766,#192767,
#192768,#192769,#192770,#192771,#192772,#192773,#192774,#192775,#192776,
#192777,#192778,#192779,#192780,#192781,#192782,#192783,#192784,#192785,
#192786,#192787,#192788,#192789,#192790,#192791,#192792,#192793,#192794,
#192795,#192796,#192797,#192798,#192799,#192800,#192801,#192802,#192803,
#192804,#192805,#192806,#192807,#192808,#192809,#192810,#192811,#192812,
#192813,#192814,#192815,#192816,#192817,#192818,#192819,#192820,#192821,
#192822,#192823,#192824,#192825,#192826,#192827,#192828,#192829,#192830,
#192831,#192832,#192833,#192834,#192835,#192836,#192837,#192838,#192839,
#192840,#192841,#192842,#192843,#192844,#192845,#192846,#192847,#192848,
#192849,#192850,#192851,#192852,#192853,#192854,#192855,#192856,#192857,
#192858,#192859,#192860,#192861,#192862,#192863,#192864,#192865,#192866,
#192867,#192868,#192869,#192870,#192871,#192872,#192873,#192874,#192875,
#192876,#192877,#192878,#192879,#192880,#192881,#192882,#192883,#192884,
#192885,#192886,#192887,#192888,#192889,#192890,#192891,#192892,#192893,
#192894,#192895,#192896,#192897,#192898,#192899,#192900,#192901,#192902,
#192903,#192904,#192905,#192906,#192907,#192908,#192909,#192910,#192911,
#192912,#192913,#192914,#192915,#192916,#192917,#192918,#192919,#192920,
#192921,#192922,#192923,#192924,#192925,#192926,#192927,#192928,#192929,
#192930,#192931,#192932,#192933,#192934,#192935,#192936,#192937,#192938,
#192939,#192940,#192941,#192942,#192943,#192944,#192945,#192946,#192947,
#192948,#192949,#192950,#192951,#192952,#192953,#192954,#192955,#192956,
#192957,#192958,#192959,#192960,#192961,#192962,#192963,#192964,#192965,
#192966,#192967,#192968,#192969,#192970,#192971,#192972,#192973,#192974,
#192975,#192976,#192977,#192978,#192979,#192980,#192981,#192982,#192983,
#192984,#192985,#192986,#192987,#192988,#192989,#192990,#192991,#192992,
#192993,#192994,#192995,#192996,#192997,#192998,#192999,#193000,#193001,
#193002,#193003,#193004,#193005,#193006,#193007,#193008,#193009,#193010,
#193011,#193012,#193013,#193014,#193015,#193016,#193017,#193018,#193019,
#193020,#193021,#193022,#193023,#193024,#193025,#193026,#193027,#193028,
#193029,#193030,#193031,#193032,#193033,#193034,#193035,#193036,#193037,
#193038,#193039,#193040,#193041,#193042,#193043,#193044,#193045,#193046,
#193047,#193048,#193049,#193050,#193051,#193052,#193053,#193054,#193055,
#193056,#193057,#193058,#193059,#193060,#193061,#193062,#193063,#193064,
#193065,#193066,#193067,#193068,#193069,#193070,#193071,#193072,#193073,
#193074,#193075,#193076,#193077,#193078,#193079,#193080,#193081,#193082,
#193083,#193084,#193085,#193086,#193087,#193088,#193089,#193090,#193091,
#193092,#193093,#193094,#193095,#193096,#193097,#193098,#193099,#193100,
#193101,#193102,#193103,#193104,#193105,#193106,#193107,#193108,#193109,
#193110,#193111,#193112,#193113,#193114,#193115,#193116,#193117,#193118,
#193119,#193120,#193121,#193122,#193123,#193124,#193125,#193126,#193127,
#193128,#193129,#193130,#193131,#193132,#193133,#193134,#193135,#193136,
#193137,#193138,#193139,#193140,#193141,#193142,#193143,#193144,#193145,
#193146,#193147,#193148,#193149,#193150,#193151,#193152,#193153,#193154,
#193155,#193156,#193157,#193158,#193159,#193160,#193161,#193162,#193163,
#193164,#193165,#193166,#193167,#193168,#193169,#193170,#193171,#193172,
#193173,#193174,#193175,#193176,#193177,#193178,#193179,#193180,#193181,
#193182,#193183,#193184,#193185,#193186,#193187,#193188,#193189,#193190,
#193191,#193192,#193193,#193194,#193195,#193196,#193197,#193198,#193199,
#193200,#193201,#193202,#193203,#193204,#193205,#193206,#193207,#193208,
#193209,#193210,#193211,#193212,#193213,#193214,#193215,#193216,#193217,
#193218,#193219,#193220,#193221,#193222,#193223,#193224,#193225,#193226,
#193227,#193228,#193229,#193230,#193231,#193232,#193233,#193234,#193235,
#193236,#193237,#193238,#193239,#193240,#193241,#193242,#193243,#193244,
#193245,#193246,#193247,#193248,#193249,#193250,#193251,#193252,#193253,
#193254,#193255,#193256,#193257,#193258,#193259,#193260,#193261,#193262,
#193263,#193264,#193265,#193266,#193267,#193268,#193269,#193270,#193271,
#193272,#193273,#193274,#193275,#193276,#193277,#193278,#193279,#193280,
#193281,#193282,#193283,#193284,#193285,#193286,#193287,#193288,#193289,
#193290,#193291,#193292,#193293,#193294,#193295,#193296,#193297,#193298,
#193299,#193300,#193301,#193302,#193303,#193304,#193305,#193306,#193307,
#193308,#193309,#193310,#193311,#193312,#193313,#193314,#193315,#193316,
#193317,#193318,#193319,#193320,#193321,#193322,#193323,#193324,#193325,
#193326,#193327,#193328,#193329,#193330,#193331,#193332,#193333,#193334,
#193335,#193336,#193337,#193338,#193339,#193340,#193341,#193342,#193343,
#193344,#193345,#193346,#193347,#193348,#193349,#193350,#193351,#193352,
#193353,#193354,#193355,#193356,#193357,#193358,#193359,#193360,#193361,
#193362,#193363,#193364,#193365,#193366,#193367,#193368,#193369,#193370,
#193371,#193372,#193373,#193374,#193375,#193376,#193377,#193378,#193379,
#193380,#193381,#193382,#193383,#193384,#193385,#193386,#193387,#193388,
#193389,#193390,#193391,#193392,#193393,#193394,#193395,#193396,#193397,
#193398,#193399,#193400,#193401,#193402,#193403,#193404,#193405,#193406,
#193407,#193408,#193409,#193410,#193411,#193412,#193413,#193414,#193415,
#193416,#193417,#193418,#193419,#193420,#193421,#193422,#193423,#193424,
#193425,#193426,#193427,#193428,#193429,#193430,#193431,#193432,#193433,
#193434,#193435,#193436,#193437,#193438,#193439,#193440,#193441,#193442,
#193443,#193444,#193445,#193446,#193447,#193448,#193449,#193450,#193451,
#193452,#193453,#193454,#193455,#193456,#193457,#193458,#193459,#193460,
#193461,#193462,#193463,#193464,#193465,#193466,#193467,#193468,#193469,
#193470,#193471,#193472,#193473,#193474,#193475,#193476,#193477,#193478,
#193479,#193480,#193481,#193482,#193483,#193484,#193485,#193486,#193487,
#193488,#193489,#193490,#193491,#193492,#193493,#193494,#193495,#193496,
#193497,#193498,#193499,#193500,#193501,#193502,#193503,#193504,#193505,
#193506,#193507,#193508,#193509,#193510,#193511,#193512,#193513,#193514,
#193515,#193516,#193517,#193518,#193519,#193520,#193521,#193522,#193523,
#193524,#193525,#193526,#193527,#193528,#193529,#193530,#193531,#193532,
#193533,#193534,#193535,#193536,#193537,#193538,#193539,#193540,#193541,
#193542,#193543,#193544,#193545,#193546,#193547,#193548,#193549,#193550,
#193551,#193552,#193553,#193554,#193555,#193556,#193557,#193558,#193559,
#193560,#193561,#193562,#193563,#193564,#193565,#193566,#193567,#193568,
#193569,#193570,#193571,#193572,#193573,#193574,#193575,#193576,#193577,
#193578,#193579,#193580,#193581,#193582,#193583,#193584,#193585,#193586,
#193587,#193588,#193589,#193590,#193591,#193592,#193593,#193594,#193595,
#193596,#193597,#193598,#193599,#193600,#193601,#193602,#193603,#193604,
#193605,#193606,#193607,#193608,#193609,#193610,#193611,#193612,#193613,
#193614,#193615,#193616,#193617,#193618,#193619,#193620,#193621,#193622,
#193623,#193624,#193625,#193626,#193627,#193628,#193629,#193630,#193631,
#193632,#193633,#193634,#193635,#193636,#193637,#193638,#193639,#193640,
#193641,#193642,#193643,#193644,#193645,#193646,#193647,#193648,#193649,
#193650,#193651,#193652,#193653,#193654,#193655,#193656,#193657,#193658,
#193659,#193660,#193661,#193662,#193663,#193664,#193665,#193666,#193667,
#193668,#193669,#193670,#193671,#193672,#193673,#193674,#193675,#193676,
#193677,#193678,#193679,#193680,#193681,#193682,#193683,#193684,#193685,
#193686,#193687,#193688,#193689,#193690,#193691,#193692,#193693,#193694,
#193695,#193696,#193697,#193698,#193699,#193700,#193701,#193702,#193703,
#193704,#193705,#193706,#193707,#193708,#193709,#193710,#193711,#193712,
#193713,#193714,#193715,#193716,#193717,#193718,#193719,#193720,#193721,
#193722,#193723,#193724,#193725,#193726),(#193727,#193728,#193729,#193730,
#193731,#193732,#193733,#193734,#193735,#193736,#193737,#193738,#193739,
#193740,#193741,#193742,#193743,#193744,#193745,#193746,#193747,#193748,
#193749,#193750,#193751,#193752,#193753,#193754,#193755,#193756,#193757,
#193758,#193759,#193760,#193761,#193762,#193763,#193764,#193765,#193766,
#193767,#193768,#193769,#193770,#193771,#193772,#193773,#193774,#193775,
#193776,#193777,#193778,#193779,#193780,#193781,#193782,#193783,#193784,
#193785,#193786,#193787,#193788,#193789,#193790,#193791,#193792,#193793,
#193794,#193795,#193796,#193797,#193798,#193799,#193800,#193801,#193802,
#193803,#193804,#193805,#193806,#193807,#193808,#193809,#193810,#193811,
#193812,#193813,#193814,#193815,#193816,#193817,#193818,#193819,#193820,
#193821,#193822,#193823,#193824,#193825,#193826,#193827,#193828,#193829,
#193830,#193831,#193832,#193833,#193834,#193835,#193836,#193837,#193838,
#193839,#193840,#193841,#193842,#193843,#193844,#193845,#193846,#193847,
#193848,#193849,#193850,#193851,#193852,#193853,#193854,#193855,#193856,
#193857,#193858,#193859,#193860,#193861,#193862,#193863,#193864,#193865,
#193866,#193867,#193868,#193869,#193870,#193871,#193872,#193873,#193874,
#193875,#193876,#193877,#193878,#193879,#193880,#193881,#193882,#193883,
#193884,#193885,#193886,#193887,#193888,#193889,#193890,#193891,#193892,
#193893,#193894,#193895,#193896,#193897,#193898,#193899,#193900,#193901,
#193902,#193903,#193904,#193905,#193906,#193907,#193908,#193909,#193910,
#193911,#193912,#193913,#193914,#193915,#193916,#193917,#193918,#193919,
#193920,#193921,#193922,#193923,#193924,#193925,#193926,#193927,#193928,
#193929,#193930,#193931,#193932,#193933,#193934,#193935,#193936,#193937,
#193938,#193939,#193940,#193941,#193942,#193943,#193944,#193945,#193946,
#193947,#193948,#193949,#193950,#193951,#193952,#193953,#193954,#193955,
#193956,#193957,#193958,#193959,#193960,#193961,#193962,#193963,#193964,
#193965,#193966,#193967,#193968,#193969,#193970,#193971,#193972,#193973,
#193974,#193975,#193976,#193977,#193978,#193979,#193980,#193981,#193982,
#193983,#193984,#193985,#193986,#193987,#193988,#193989,#193990,#193991,
#193992,#193993,#193994,#193995,#193996,#193997,#193998,#193999,#194000,
#194001,#194002,#194003,#194004,#194005,#194006,#194007,#194008,#194009,
#194010,#194011,#194012,#194013,#194014,#194015,#194016,#194017,#194018,
#194019,#194020,#194021,#194022,#194023,#194024,#194025,#194026,#194027,
#194028,#194029,#194030,#194031,#194032,#194033,#194034,#194035,#194036,
#194037,#194038,#194039,#194040,#194041,#194042,#194043,#194044,#194045,
#194046,#194047,#194048,#194049,#194050,#194051,#194052,#194053,#194054,
#194055,#194056,#194057,#194058,#194059,#194060,#194061,#194062,#194063,
#194064,#194065,#194066,#194067,#194068,#194069,#194070,#194071,#194072,
#194073,#194074,#194075,#194076,#194077,#194078,#194079,#194080,#194081,
#194082,#194083,#194084,#194085,#194086,#194087,#194088,#194089,#194090,
#194091,#194092,#194093,#194094,#194095,#194096,#194097,#194098,#194099,
#194100,#194101,#194102,#194103,#194104,#194105,#194106,#194107,#194108,
#194109,#194110,#194111,#194112,#194113,#194114,#194115,#194116,#194117,
#194118,#194119,#194120,#194121,#194122,#194123,#194124,#194125,#194126,
#194127,#194128,#194129,#194130,#194131,#194132,#194133,#194134,#194135,
#194136,#194137,#194138,#194139,#194140,#194141,#194142,#194143,#194144,
#194145,#194146,#194147,#194148,#194149,#194150,#194151,#194152,#194153,
#194154,#194155,#194156,#194157,#194158,#194159,#194160,#194161,#194162,
#194163,#194164,#194165,#194166,#194167,#194168,#194169,#194170,#194171,
#194172,#194173,#194174,#194175,#194176,#194177,#194178,#194179,#194180,
#194181,#194182,#194183,#194184,#194185,#194186,#194187,#194188,#194189,
#194190,#194191,#194192,#194193,#194194,#194195,#194196,#194197,#194198,
#194199,#194200,#194201,#194202,#194203,#194204,#194205,#194206,#194207,
#194208,#194209,#194210,#194211,#194212,#194213,#194214,#194215,#194216,
#194217,#194218,#194219,#194220,#194221,#194222,#194223,#194224,#194225,
#194226,#194227,#194228,#194229,#194230,#194231,#194232,#194233,#194234,
#194235,#194236,#194237,#194238,#194239,#194240,#194241,#194242,#194243,
#194244,#194245,#194246,#194247,#194248,#194249,#194250,#194251,#194252,
#194253,#194254,#194255,#194256,#194257,#194258,#194259,#194260,#194261,
#194262,#194263,#194264,#194265,#194266,#194267,#194268,#194269,#194270,
#194271,#194272,#194273,#194274,#194275,#194276,#194277,#194278,#194279,
#194280,#194281,#194282,#194283,#194284,#194285,#194286,#194287,#194288,
#194289,#194290,#194291,#194292,#194293,#194294,#194295,#194296,#194297,
#194298,#194299,#194300,#194301,#194302,#194303,#194304,#194305,#194306,
#194307,#194308,#194309,#194310,#194311,#194312,#194313,#194314,#194315,
#194316,#194317,#194318,#194319,#194320,#194321,#194322,#194323,#194324,
#194325,#194326,#194327,#194328,#194329,#194330,#194331,#194332,#194333,
#194334,#194335,#194336,#194337,#194338,#194339,#194340,#194341,#194342,
#194343,#194344,#194345,#194346,#194347,#194348,#194349,#194350,#194351,
#194352,#194353,#194354,#194355,#194356,#194357,#194358,#194359,#194360,
#194361,#194362,#194363,#194364,#194365,#194366,#194367,#194368,#194369,
#194370,#194371,#194372,#194373,#194374,#194375,#194376,#194377,#194378,
#194379,#194380,#194381,#194382,#194383,#194384,#194385,#194386,#194387,
#194388,#194389,#194390,#194391,#194392,#194393,#194394,#194395,#194396,
#194397,#194398,#194399,#194400,#194401,#194402,#194403,#194404,#194405,
#194406,#194407,#194408,#194409,#194410,#194411,#194412,#194413,#194414,
#194415,#194416,#194417,#194418,#194419,#194420,#194421,#194422,#194423,
#194424,#194425,#194426,#194427,#194428,#194429,#194430,#194431,#194432,
#194433,#194434,#194435,#194436,#194437,#194438,#194439,#194440,#194441,
#194442,#194443,#194444,#194445,#194446,#194447,#194448,#194449,#194450,
#194451,#194452,#194453,#194454,#194455,#194456,#194457,#194458,#194459,
#194460,#194461,#194462,#194463,#194464,#194465,#194466,#194467,#194468,
#194469,#194470,#194471,#194472,#194473,#194474,#194475,#194476,#194477,
#194478,#194479,#194480,#194481,#194482,#194483,#194484,#194485,#194486,
#194487,#194488,#194489,#194490,#194491,#194492,#194493,#194494,#194495,
#194496,#194497,#194498,#194499,#194500,#194501,#194502,#194503,#194504,
#194505,#194506,#194507,#194508,#194509,#194510,#194511,#194512,#194513,
#194514,#194515,#194516,#194517,#194518,#194519,#194520,#194521,#194522,
#194523,#194524,#194525,#194526,#194527,#194528,#194529,#194530,#194531,
#194532,#194533,#194534,#194535,#194536,#194537,#194538,#194539,#194540,
#194541,#194542,#194543,#194544,#194545,#194546,#194547,#194548,#194549,
#194550,#194551,#194552,#194553,#194554,#194555,#194556,#194557,#194558,
#194559,#194560,#194561,#194562,#194563,#194564,#194565,#194566,#194567,
#194568,#194569,#194570,#194571,#194572,#194573,#194574,#194575,#194576,
#194577,#194578,#194579,#194580,#194581,#194582,#194583,#194584,#194585,
#194586,#194587,#194588,#194589,#194590,#194591,#194592,#194593,#194594,
#194595,#194596,#194597,#194598,#194599,#194600,#194601,#194602,#194603,
#194604,#194605,#194606,#194607,#194608,#194609,#194610,#194611,#194612,
#194613,#194614,#194615,#194616,#194617,#194618,#194619,#194620,#194621,
#194622,#194623,#194624,#194625,#194626,#194627,#194628,#194629,#194630,
#194631,#194632,#194633,#194634,#194635,#194636,#194637,#194638,#194639,
#194640,#194641,#194642,#194643,#194644,#194645,#194646,#194647,#194648,
#194649,#194650,#194651,#194652,#194653,#194654,#194655,#194656,#194657,
#194658,#194659,#194660,#194661,#194662,#194663,#194664,#194665,#194666,
#194667,#194668,#194669,#194670,#194671,#194672,#194673,#194674,#194675,
#194676,#194677,#194678,#194679,#194680,#194681,#194682,#194683,#194684,
#194685,#194686,#194687,#194688,#194689,#194690,#194691,#194692,#194693,
#194694,#194695,#194696,#194697,#194698,#194699,#194700,#194701,#194702,
#194703,#194704,#194705,#194706,#194707,#194708,#194709,#194710,#194711,
#194712,#194713,#194714,#194715,#194716,#194717,#194718,#194719,#194720,
#194721,#194722,#194723,#194724,#194725,#194726,#194727,#194728,#194729,
#194730,#194731,#194732,#194733,#194734,#194735,#194736,#194737,#194738,
#194739,#194740,#194741,#194742,#194743,#194744,#194745,#194746,#194747,
#194748,#194749,#194750,#194751,#194752,#194753,#194754,#194755,#194756,
#194757,#194758,#194759,#194760,#194761,#194762,#194763,#194764,#194765,
#194766,#194767,#194768,#194769,#194770,#194771,#194772,#194773,#194774,
#194775,#194776,#194777,#194778,#194779,#194780,#194781,#194782,#194783,
#194784,#194785,#194786,#194787,#194788,#194789,#194790,#194791,#194792,
#194793,#194794,#194795,#194796,#194797,#194798,#194799,#194800,#194801,
#194802,#194803,#194804,#194805,#194806,#194807,#194808,#194809,#194810,
#194811,#194812,#194813,#194814,#194815,#194816,#194817,#194818,#194819,
#194820,#194821,#194822,#194823,#194824,#194825,#194826,#194827,#194828,
#194829,#194830,#194831,#194832,#194833,#194834,#194835,#194836,#194837,
#194838,#194839,#194840,#194841,#194842,#194843,#194844,#194845,#194846,
#194847,#194848,#194849,#194850,#194851,#194852,#194853,#194854,#194855,
#194856,#194857,#194858,#194859,#194860,#194861,#194862,#194863,#194864,
#194865,#194866,#194867,#194868,#194869,#194870,#194871,#194872,#194873,
#194874,#194875,#194876,#194877,#194878,#194879,#194880,#194881,#194882,
#194883,#194884,#194885,#194886,#194887,#194888,#194889,#194890,#194891,
#194892,#194893,#194894,#194895,#194896,#194897,#194898,#194899,#194900,
#194901,#194902,#194903,#194904,#194905,#194906,#194907,#194908,#194909,
#194910,#194911,#194912,#194913,#194914,#194915,#194916,#194917,#194918,
#194919,#194920,#194921,#194922,#194923,#194924,#194925,#194926,#194927,
#194928,#194929,#194930,#194931,#194932,#194933,#194934,#194935,#194936,
#194937,#194938,#194939,#194940,#194941,#194942,#194943,#194944,#194945,
#194946,#194947,#194948,#194949,#194950,#194951,#194952,#194953,#194954,
#194955,#194956,#194957,#194958,#194959,#194960,#194961,#194962,#194963,
#194964,#194965,#194966,#194967,#194968,#194969,#194970,#194971,#194972,
#194973,#194974,#194975,#194976,#194977,#194978,#194979,#194980,#194981,
#194982,#194983,#194984,#194985,#194986,#194987,#194988,#194989,#194990,
#194991,#194992,#194993,#194994,#194995,#194996,#194997,#194998,#194999,
#195000,#195001,#195002,#195003,#195004,#195005,#195006,#195007,#195008,
#195009,#195010,#195011,#195012,#195013,#195014,#195015,#195016,#195017,
#195018,#195019,#195020,#195021,#195022,#195023,#195024,#195025,#195026,
#195027,#195028,#195029,#195030,#195031,#195032,#195033,#195034,#195035,
#195036,#195037,#195038,#195039,#195040,#195041,#195042,#195043,#195044,
#195045,#195046,#195047,#195048,#195049,#195050,#195051,#195052,#195053,
#195054,#195055,#195056,#195057,#195058,#195059,#195060,#195061,#195062,
#195063,#195064,#195065,#195066,#195067,#195068,#195069,#195070,#195071,
#195072,#195073,#195074,#195075,#195076,#195077,#195078,#195079,#195080,
#195081,#195082,#195083,#195084,#195085,#195086,#195087,#195088,#195089,
#195090,#195091,#195092,#195093,#195094,#195095,#195096,#195097,#195098,
#195099,#195100,#195101,#195102,#195103,#195104,#195105,#195106,#195107,
#195108,#195109,#195110,#195111,#195112,#195113,#195114,#195115,#195116,
#195117,#195118,#195119,#195120,#195121,#195122,#195123,#195124,#195125,
#195126,#195127,#195128,#195129,#195130,#195131,#195132,#195133,#195134,
#195135,#195136,#195137,#195138,#195139,#195140,#195141,#195142,#195143,
#195144,#195145,#195146,#195147,#195148,#195149,#195150,#195151,#195152,
#195153,#195154,#195155,#195156,#195157,#195158,#195159,#195160,#195161,
#195162,#195163,#195164,#195165,#195166,#195167,#195168,#195169,#195170,
#195171,#195172,#195173,#195174,#195175,#195176,#195177,#195178,#195179,
#195180,#195181,#195182,#195183,#195184,#195185,#195186,#195187,#195188,
#195189,#195190,#195191,#195192,#195193,#195194,#195195,#195196,#195197,
#195198,#195199,#195200,#195201,#195202,#195203,#195204,#195205,#195206,
#195207,#195208,#195209,#195210,#195211,#195212,#195213,#195214,#195215,
#195216,#195217,#195218,#195219,#195220,#195221,#195222,#195223,#195224,
#195225,#195226,#195227,#195228,#195229,#195230,#195231,#195232,#195233,
#195234,#195235,#195236,#195237,#195238,#195239,#195240,#195241,#195242,
#195243,#195244,#195245,#195246,#195247,#195248,#195249,#195250,#195251,
#195252,#195253,#195254,#195255,#195256,#195257,#195258,#195259,#195260,
#195261,#195262,#195263,#195264,#195265,#195266,#195267,#195268,#195269,
#195270,#195271,#195272,#195273,#195274,#195275,#195276,#195277,#195278,
#195279,#195280,#195281,#195282,#195283,#195284,#195285,#195286,#195287,
#195288,#195289,#195290,#195291,#195292,#195293,#195294,#195295,#195296,
#195297,#195298,#195299,#195300,#195301,#195302,#195303,#195304,#195305,
#195306,#195307,#195308,#195309,#195310,#195311,#195312,#195313,#195314,
#195315,#195316,#195317,#195318,#195319,#195320,#195321,#195322,#195323,
#195324,#195325,#195326,#195327,#195328,#195329,#195330,#195331,#195332,
#195333,#195334,#195335,#195336,#195337,#195338,#195339,#195340,#195341,
#195342,#195343,#195344,#195345,#195346,#195347,#195348,#195349,#195350,
#195351,#195352,#195353,#195354,#195355,#195356,#195357,#195358,#195359,
#195360,#195361,#195362,#195363,#195364,#195365,#195366,#195367,#195368,
#195369,#195370,#195371,#195372,#195373,#195374,#195375,#195376,#195377,
#195378,#195379,#195380,#195381,#195382,#195383,#195384,#195385,#195386,
#195387,#195388,#195389,#195390,#195391,#195392,#195393,#195394,#195395,
#195396,#195397,#195398,#195399,#195400,#195401,#195402,#195403,#195404,
#195405,#195406,#195407,#195408,#195409,#195410,#195411,#195412,#195413,
#195414,#195415,#195416,#195417,#195418,#195419,#195420,#195421)),
 .UNSPECIFIED.,.F.,.F.,.F.,(4,4),(4,1,1,1,1,1,1,1,1,1,1,1,1,1,1,1,1,1,1,
1,1,1,1,1,1,1,1,1,1,1,1,1,1,1,1,1,1,1,1,1,1,1,1,1,1,1,1,1,1,1,1,1,1,1,1,
1,1,1,1,1,1,1,1,1,1,1,1,1,1,1,1,1,1,1,1,1,1,1,1,1,1,1,1,1,1,1,1,1,1,1,1,
1,1,1,1,1,1,1,1,1,1,1,1,1,1,1,1,1,1,1,1,1,1,1,1,1,1,1,1,1,1,1,1,1,1,1,1,
1,1,1,1,1,1,1,1,1,1,1,1,1,1,1,1,1,1,1,1,1,1,1,1,1,1,1,1,1,1,1,1,1,1,1,1,
1,1,1,1,1,1,1,1,1,1,1,1,1,1,1,1,1,1,1,1,1,1,1,1,1,1,1,1,1,1,1,1,1,1,1,1,
1,1,1,1,1,1,1,1,1,1,1,1,1,1,1,1,1,1,1,1,1,1,1,1,1,1,1,1,1,1,1,1,1,1,1,1,
1,1,1,1,1,1,1,1,1,1,1,1,1,1,1,1,1,1,1,1,1,1,1,1,1,1,1,1,1,1,1,1,1,1,1,1,
1,1,1,1,1,1,1,1,1,1,1,1,1,1,1,1,1,1,1,1,1,1,1,1,1,1,1,1,1,1,1,1,1,1,1,1,
1,1,1,1,1,1,1,1,1,1,1,1,1,1,1,1,1,1,1,1,1,1,1,1,1,1,1,1,1,1,1,1,1,1,1,1,
1,1,1,1,1,1,1,1,1,1,1,1,1,1,1,1,1,1,1,1,1,1,1,1,1,1,1,1,1,1,1,1,1,1,1,1,
1,1,1,1,1,1,1,1,1,1,1,1,1,1,1,1,1,1,1,1,1,1,1,1,1,1,1,1,1,1,1,1,1,1,1,1,
1,1,1,1,1,1,1,1,1,1,1,1,1,1,1,1,1,1,1,1,1,1,1,1,1,1,1,1,1,1,1,1,1,1,1,1,
1,1,1,1,1,1,1,1,1,1,1,1,1,1,1,1,1,1,1,1,1,1,1,1,1,1,1,1,1,1,1,1,1,1,1,1,
1,1,1,1,1,1,1,1,1,1,1,1,1,1,1,1,1,1,1,1,1,1,1,1,1,1,1,1,1,1,1,1,1,1,1,1,
1,1,1,1,1,1,1,1,1,1,1,1,1,1,1,1,1,1,1,1,1,1,1,1,1,1,1,1,1,1,1,1,1,1,1,1,
1,1,1,1,1,1,1,1,1,1,1,1,1,1,1,1,1,1,1,1,1,1,1,1,1,1,1,1,1,1,1,1,1,1,1,1,
1,1,1,1,1,1,1,1,1,1,1,1,1,1,1,1,1,1,1,1,1,1,1,1,1,1,1,1,1,1,1,1,1,1,1,1,
1,1,1,1,1,1,1,1,1,1,1,1,1,1,1,1,1,1,1,1,1,1,1,1,1,1,1,1,1,1,1,1,1,1,1,1,
1,1,1,1,1,1,1,1,1,1,1,1,1,1,1,1,1,1,1,1,1,1,1,1,1,1,1,1,1,1,1,1,1,1,1,1,
1,1,1,1,1,1,1,1,1,1,1,1,1,1,1,1,1,1,1,1,1,1,1,1,1,1,1,1,1,1,1,1,1,1,1,1,
1,1,1,1,1,1,1,1,1,1,1,1,1,1,1,1,1,1,1,1,1,1,1,1,1,1,1,1,1,1,1,1,1,1,1,1,
1,1,1,1,1,1,1,1,1,1,1,1,1,1,1,1,1,1,1,1,1,1,1,1,1,1,1,1,1,1,1,1,1,1,1,1,
1,1,1,1,1,1,1,1,1,1,1,1,1,1,1,1,1,1,1,1,1,1,1,1,1,1,1,1,1,1,1,1,1,1,1,1,
1,1,1,1,1,1,1,1,1,1,1,1,1,1,1,1,1,1,1,1,1,1,1,1,1,1,1,1,1,1,1,1,1,1,1,1,
1,1,1,1,1,1,1,1,1,1,1,1,1,1,1,1,1,1,1,1,1,1,1,1,1,1,1,1,1,1,1,1,1,1,1,1,
1,1,1,1,1,1,1,1,1,1,1,1,1,1,1,1,1,1,1,1,1,1,1,1,1,1,1,1,1,1,1,1,1,1,1,1,
1,1,1,1,1,1,1,1,1,1,1,1,1,1,1,1,1,1,1,1,1,1,1,1,1,1,1,1,1,1,1,1,1,1,1,1,
1,1,1,1,1,1,1,1,1,1,1,1,1,1,1,1,1,1,1,1,1,1,1,1,1,1,1,1,1,1,1,1,1,1,1,1,
1,1,1,1,1,1,1,1,1,1,1,1,1,1,1,1,1,1,1,1,1,1,1,1,1,1,1,1,1,1,1,1,1,1,1,1,
1,1,1,1,1,1,1,1,1,1,1,1,1,1,1,1,1,1,1,1,1,1,1,1,1,1,1,1,1,1,1,1,1,1,1,1,
1,1,1,1,1,1,1,1,1,1,1,1,1,1,1,1,1,1,1,1,1,1,1,1,1,1,1,1,1,1,1,1,1,1,1,1,
1,1,1,1,1,1,1,1,1,1,1,1,1,1,1,1,1,1,1,1,1,1,1,1,1,1,1,1,1,1,1,1,1,1,1,1,
1,1,1,1,1,1,1,1,1,1,1,1,1,1,1,1,1,1,1,1,1,1,1,1,1,1,1,1,1,1,1,1,1,1,1,1,
1,1,1,1,1,1,1,1,1,1,1,1,1,1,1,1,1,1,1,1,1,1,1,1,1,1,1,1,1,1,1,1,1,1,1,1,
1,1,1,1,1,1,1,1,1,1,1,1,1,1,1,1,1,1,1,1,1,1,1,1,1,1,1,1,1,1,1,1,1,1,1,1,
1,1,1,1,1,1,1,1,1,1,1,1,1,1,1,1,1,1,1,1,1,1,1,1,1,1,1,1,1,1,1,1,1,1,1,1,
1,1,1,1,1,1,1,1,1,1,1,1,1,1,1,1,1,1,1,1,1,1,1,1,1,1,1,1,1,1,1,1,1,1,1,1,
1,1,1,1,1,1,1,1,1,1,1,1,1,1,1,1,1,1,1,1,1,1,1,1,1,1,1,1,1,1,1,1,1,1,1,1,
1,1,1,1,1,1,1,1,1,1,1,1,1,1,1,1,1,1,1,1,1,1,1,1,1,1,1,1,1,1,1,1,1,1,1,1,
1,1,1,1,1,1,1,1,1,1,1,1,1,1,1,1,1,1,1,1,1,1,1,1,1,1,1,1,1,1,1,1,1,1,1,1,
1,1,1,1,1,1,1,1,1,1,1,1,1,1,1,1,1,1,1,1,1,1,1,1,1,1,1,1,1,1,1,1,1,1,1,1,
1,1,1,1,1,1,1,1,1,1,1,1,1,1,1,1,1,1,1,1,1,1,1,1,1,1,1,1,1,1,1,1,1,1,1,1,
1,1,1,1,1,1,1,1,1,1,1,1,1,1,1,1,1,1,1,1,1,1,1,1,1,1,1,1,1,1,1,1,1,1,1,1,
1,1,1,1,1,1,1,1,1,1,1,1,1,1,1,1,1,1,1,1,1,1,1,1,1,1,1,1,1,1,1,1,1,1,1,1,
1,1,1,1,1,1,1,1,1,1,1,1,1,1,1,1,1,1,1,1,1,1,1,1,1,1,1,1,1,1,1,1,1,1,1,1,
1,1,1,1,1,1,1,1,1,1,1,1,1,1,1,1,1,1,1,1,1,1,1,1,1,1,1,1,1,1,1,1,1,1,1,1,
1,1,1,1,1,1,1,1,1,1,1,1,1,1,1,1,1,4),(-0.000587328099657093,0.1157205948422),
(8.30590413559005,8.80579087257276,9.30565887793282,10.305394888653,11.3051308993731,
12.3048669100932,13.3046029208133,14.3043389315335,15.3040749422536,16.3038109529737,
17.3035469636939,18.303282974414,19.3030189851341,20.3027549958542,21.3024910065744,
22.3022270172945,23.3019630280146,24.3016990387348,25.3014350494549,26.301171060175,
27.3009070708951,28.3006430816153,29.3003790923354,30.3001151030555,31.2998511137757,
32.2995871244958,33.2993231352159,34.299059145936,35.2987951566562,36.2985311673763,
37.2982671780964,38.2980031888166,39.2977391995367,40.2974752102568,41.2972112209769,
42.2969472316971,43.2966832424172,44.2964192531373,45.2961552638575,46.2958912745776,
47.2956272852977,48.2953632960178,49.295099306738,50.2948353174581,51.2945713281782,
52.2943073388984,53.2940433496185,54.2937793603386,55.2935153710587,56.2932513817789,
57.292987392499,58.2927234032191,59.2924594139393,60.2921954246594,61.2919314353795,
62.2916674460996,63.2914034568198,64.2911394675399,65.29087547826,66.2906114889802,
67.2903474997003,68.2900835104204,69.2898195211405,70.2895555318607,71.2892915425808,
72.2890275533009,73.2887635640211,74.2884995747412,75.2882355854613,76.2879715961814,
77.2877076069016,78.2874436176217,79.2871796283418,80.286915639062,81.2866516497821,
82.2863876605022,83.2861236712224,84.2858596819425,85.2855956926626,86.2853317033827,
87.2850677141029,88.284803724823,89.2845397355431,90.2842757462633,91.2840117569834,
92.2837477677035,93.2834837784236,94.2832197891438,95.2829557998639,96.282691810584,
97.2824278213041,98.2821638320243,99.2818998427444,100.281635853465,101.281371864185,
102.281107874905,103.280843885625,104.280579896345,105.280315907065,106.280051917785,
107.279787928505,108.279523939226,109.279259949946,110.278995960666,111.278731971386,
112.278467982106,113.278203992826,114.277940003546,115.277676014266,116.277412024987,
117.277148035707,118.276884046427,119.276620057147,120.276356067867,121.276092078587,
122.275828089307,123.275564100028,124.275300110748,125.275036121468,126.274772132188,
127.274508142908,128.274244153628,129.273980164348,130.273716175068,131.273452185789,
132.273188196509,133.272924207229,134.272660217949,135.272396228669,136.272132239389,
137.271868250109,138.271604260829,139.27134027155,140.27107628227,141.27081229299,
142.27054830371,143.27028431443,144.27002032515,145.26975633587,146.26949234659,
147.269228357311,148.268964368031,149.268700378751,150.268436389471,151.268172400191,
152.267908410911,153.267644421631,154.267380432352,155.267116443072,156.266852453792,
157.266588464512,158.266324475232,159.266060485952,160.265796496672,161.265532507392,
162.265268518113,163.265004528833,164.264740539553,165.264476550273,166.264212560993,
167.263948571713,168.263684582433,169.263420593153,170.263156603874,171.262892614594,
172.262628625314,173.262364636034,174.262100646754,175.261836657474,176.261572668194,
177.261308678914,178.261044689635,179.260780700355,180.260516711075,181.260252721795,
182.259988732515,183.259724743235,184.259460753955,185.259196764675,186.258932775396,
187.258668786116,188.258404796836,189.258140807556,190.257876818276,191.257612828996,
192.257348839716,193.257084850437,194.256820861157,195.256556871877,196.256292882597,
197.256028893317,198.255764904037,199.255500914757,200.255236925477,201.254972936198,
202.254708946918,203.254444957638,204.254180968358,205.253916979078,206.253652989798,
207.253389000518,208.253125011238,209.252861021959,210.252597032679,211.252333043399,
212.252069054119,213.251805064839,214.251541075559,215.251277086279,216.251013096999,
217.25074910772,218.25048511844,219.25022112916,220.24995713988,221.2496931506,
222.24942916132,223.24916517204,224.248901182761,225.248637193481,226.248373204201,
227.248109214921,228.247845225641,229.247581236361,230.247317247081,231.247053257801,
232.246789268522,233.246525279242,234.246261289962,235.245997300682,236.245733311402,
237.245469322122,238.245205332842,239.244941343562,240.244677354283,241.244413365003,
242.244149375723,243.243885386443,244.243621397163,245.243357407883,246.243093418603,
247.242829429323,248.242565440044,249.242301450764,250.242037461484,251.241773472204,
252.241509482924,253.241245493644,254.240981504364,255.240717515084,256.240453525805,
257.240189536525,258.239925547245,259.239661557965,260.239397568685,261.239133579405,
262.238869590125,263.238605600846,264.238341611566,265.238077622286,266.237813633006,
267.237549643726,268.237285654446,269.237021665166,270.236757675886,271.236493686607,
272.236229697327,273.235965708047,274.235701718767,275.235437729487,276.235173740207,
277.234909750927,278.234645761647,279.234381772368,280.234117783088,281.233853793808,
282.233589804528,283.233325815248,284.233061825968,285.232797836688,286.232533847408,
287.232269858129,288.232005868849,289.231741879569,290.231477890289,291.231213901009,
292.230949911729,293.230685922449,294.23042193317,295.23015794389,296.22989395461,
297.22962996533,298.22936597605,299.22910198677,300.22883799749,301.22857400821,
302.228310018931,303.228046029651,304.227782040371,305.227518051091,306.227254061811,
307.226990072531,308.226726083251,309.226462093971,310.226198104692,311.225934115412,
312.225670126132,313.225406136852,314.225142147572,315.224878158292,316.224614169012,
317.224350179732,318.224086190453,319.223822201173,320.223558211893,321.223294222613,
322.223030233333,323.222766244053,324.222502254773,325.222238265494,326.221974276214,
327.221710286934,328.221446297654,329.221182308374,330.220918319094,331.220654329814,
332.220390340534,333.220126351255,334.219862361975,335.219598372695,336.219334383415,
337.219070394135,338.218806404855,339.218542415575,340.218278426295,341.218014437016,
342.217750447736,343.217486458456,344.217222469176,345.216958479896,346.216694490616,
347.216430501336,348.216166512056,349.215902522777,350.215638533497,351.215374544217,
352.215110554937,353.214846565657,354.214582576377,355.214318587097,356.214054597817,
357.213790608538,358.213526619258,359.213262629978,360.212998640698,361.212734651418,
362.212470662138,363.212206672858,364.211942683579,365.211678694299,366.211414705019,
367.211150715739,368.210886726459,369.210622737179,370.210358747899,371.210094758619,
372.20983076934,373.20956678006,374.20930279078,375.2090388015,376.20877481222,
377.20851082294,378.20824683366,379.20798284438,380.207718855101,381.207454865821,
382.207190876541,383.206926887261,384.206662897981,385.206398908701,386.206134919421,
387.205870930141,388.205606940862,389.205342951582,390.205078962302,391.204814973022,
392.204550983742,393.204286994462,394.204023005182,395.203759015903,396.203495026623,
397.203231037343,398.202967048063,399.202703058783,400.202439069503,401.202175080223,
402.201911090943,403.201647101664,404.201383112384,405.201119123104,406.200855133824,
407.200591144544,408.200327155264,409.200063165984,410.199799176704,411.199535187425,
412.199271198145,413.199007208865,414.198743219585,415.198479230305,416.198215241025,
417.197951251745,418.197687262465,419.197423273186,420.197159283906,421.196895294626,
422.196631305346,423.196367316066,424.196103326786,425.195839337506,426.195575348226,
427.195311358947,428.195047369667,429.194783380387,430.194519391107,431.194255401827,
432.193991412547,433.193727423267,434.193463433988,435.193199444708,436.192935455428,
437.192671466148,438.192407476868,439.192143487588,440.191879498308,441.191615509028,
442.191351519749,443.191087530469,444.190823541189,445.190559551909,446.190295562629,
447.190031573349,448.189767584069,449.189503594789,450.18923960551,451.18897561623,
452.18871162695,453.18844763767,454.18818364839,455.18791965911,456.18765566983,
457.18739168055,458.187127691271,459.186863701991,460.186599712711,461.186335723431,
462.186071734151,463.185807744871,464.185543755591,465.185279766312,466.185015777032,
467.184751787752,468.184487798472,469.184223809192,470.183959819912,471.183695830632,
472.183431841352,473.183167852073,474.182903862793,475.182639873513,476.182375884233,
477.182111894953,478.181847905673,479.181583916393,480.181319927113,481.181055937834,
482.180791948554,483.180527959274,484.180263969994,485.179999980714,486.179735991434,
487.179472002154,488.179208012874,489.178944023595,490.178680034315,491.178416045035,
492.178152055755,493.177888066475,494.177624077195,495.177360087915,496.177096098636,
497.176832109356,498.176568120076,499.176304130796,500.176040141516,501.175776152236,
502.175512162956,503.175248173676,504.174984184397,505.174720195117,506.174456205837,
507.174192216557,508.173928227277,509.173664237997,510.173400248717,511.173136259437,
512.172872270158,513.172608280878,514.172344291598,515.172080302318,516.171816313038,
517.171552323758,518.171288334478,519.171024345198,520.170760355919,521.170496366639,
522.170232377359,523.169968388079,524.169704398799,525.169440409519,526.169176420239,
527.168912430959,528.16864844168,529.1683844524,530.16812046312,531.16785647384,
532.16759248456,533.16732849528,534.167064506,535.166800516721,536.166536527441,
537.166272538161,538.166008548881,539.165744559601,540.165480570321,541.165216581041,
542.164952591761,543.164688602482,544.164424613202,545.164160623922,546.163896634642,
547.163632645362,548.163368656082,549.163104666802,550.162840677522,551.162576688243,
552.162312698963,553.162048709683,554.161784720403,555.161520731123,556.161256741843,
557.160992752563,558.160728763283,559.160464774004,560.160200784724,561.159936795444,
562.159672806164,563.159408816884,564.159144827604,565.158880838324,566.158616849045,
567.158352859765,568.158088870485,569.157824881205,570.157560891925,571.157296902645,
572.157032913365,573.156768924085,574.156504934806,575.156240945526,576.155976956246,
577.155712966966,578.155448977686,579.155184988406,580.154920999126,581.154657009846,
582.154393020567,583.154129031287,584.153865042007,585.153601052727,586.153337063447,
587.153073074167,588.152809084887,589.152545095607,590.152281106328,591.152017117048,
592.151753127768,593.151489138488,594.151225149208,595.150961159928,596.150697170648,
597.150433181368,598.150169192089,599.149905202809,600.149641213529,601.149377224249,
602.149113234969,603.148849245689,604.148585256409,605.14832126713,606.14805727785,
607.14779328857,608.14752929929,609.14726531001,610.14700132073,611.14673733145,
612.14647334217,613.146209352891,614.145945363611,615.145681374331,616.145417385051,
617.145153395771,618.144889406491,619.144625417211,620.144361427931,621.144097438652,
622.143833449372,623.143569460092,624.143305470812,625.143041481532,626.142777492252,
627.142513502972,628.142249513692,629.141985524413,630.141721535133,631.141457545853,
632.141193556573,633.140929567293,634.140665578013,635.140401588733,636.140137599454,
637.139873610174,638.139609620894,639.139345631614,640.139081642334,641.138817653054,
642.138553663774,643.138289674494,644.138025685215,645.137761695935,646.137497706655,
647.137233717375,648.136969728095,649.136705738815,650.136441749535,651.136177760255,
652.135913770976,653.135649781696,654.135385792416,655.135121803136,656.134857813856,
657.134593824576,658.134329835296,659.134065846016,660.133801856737,661.133537867457,
662.133273878177,663.133009888897,664.132745899617,665.132481910337,666.132217921057,
667.131953931778,668.131689942498,669.131425953218,670.131161963938,671.130897974658,
672.130633985378,673.130369996098,674.130106006818,675.129842017539,676.129578028259,
677.129314038979,678.129050049699,679.128786060419,680.128522071139,681.128258081859,
682.127994092579,683.1277301033,684.12746611402,685.12720212474,686.12693813546,
687.12667414618,688.1264101569,689.12614616762,690.12588217834,691.125618189061,
692.125354199781,693.125090210501,694.124826221221,695.124562231941,696.124298242661,
697.124034253381,698.123770264101,699.123506274822,700.123242285542,701.122978296262,
702.122714306982,703.122450317702,704.122186328422,705.121922339142,706.121658349863,
707.121394360583,708.121130371303,709.120866382023,710.120602392743,711.120338403463,
712.120074414183,713.119810424903,714.119546435624,715.119282446344,716.119018457064,
717.118754467784,718.118490478504,719.118226489224,720.117962499944,721.117698510664,
722.117434521385,723.117170532105,724.116906542825,725.116642553545,726.116378564265,
727.116114574985,728.115850585705,729.115586596425,730.115322607146,731.115058617866,
732.114794628586,733.114530639306,734.114266650026,735.114002660746,736.113738671466,
737.113474682187,738.113210692907,739.112946703627,740.112682714347,741.112418725067,
742.112154735787,743.111890746507,744.111626757227,745.111362767948,746.111098778668,
747.110834789388,748.110570800108,749.110306810828,750.110042821548,751.109778832268,
752.109514842988,753.109250853709,754.108986864429,755.108722875149,756.108458885869,
757.108194896589,758.107930907309,759.107666918029,760.107402928749,761.10713893947,
762.10687495019,763.10661096091,764.10634697163,765.10608298235,766.10581899307,
767.10555500379,768.10529101451,769.105027025231,770.104763035951,771.104499046671,
772.104235057391,773.103971068111,774.103707078831,775.103443089551,776.103179100272,
777.102915110992,778.102651121712,779.102387132432,780.102123143152,781.101859153872,
782.101595164592,783.101331175312,784.101067186033,785.100803196753,786.100539207473,
787.100275218193,788.100011228913,789.099747239633,790.099483250353,791.099219261073,
792.098955271794,793.098691282514,794.098427293234,795.098163303954,796.097899314674,
797.097635325394,798.097371336114,799.097107346834,800.096843357555,801.096579368275,
802.096315378995,803.096051389715,804.095787400435,805.095523411155,806.095259421875,
807.094995432596,808.094731443316,809.094467454036,810.094203464756,811.093939475476,
812.093675486196,813.093411496916,814.093147507636,815.092883518357,816.092619529077,
817.092355539797,818.092091550517,819.091827561237,820.091563571957,821.091299582677,
822.091035593397,823.090771604118,824.090507614838,825.090243625558,826.089979636278,
827.089715646998,828.089451657718,829.089187668438,830.088923679158,831.088659689879,
832.088395700599,833.088131711319,834.087867722039,835.087603732759,836.087339743479,
837.087075754199,838.08681176492,839.08654777564,840.08628378636,841.08601979708,
842.0857558078,843.08549181852,844.08522782924,845.08496383996,846.084699850681,
847.084435861401,848.084171872121,849.083907882841,850.083643893561,851.083379904281,
852.083115915001,853.082851925721,854.082587936442,855.082323947162,856.082059957882,
857.081795968602,858.081531979322,859.081267990042,860.081004000762,861.080740011482,
862.080476022203,863.080212032923,864.079948043643,865.079684054363,866.079420065083,
867.079156075803,868.078892086523,869.078628097243,870.078364107964,871.078100118684,
872.077836129404,873.077572140124,874.077308150844,875.077044161564,876.076780172284,
877.076516183005,878.076252193725,879.075988204445,880.075724215165,881.075460225885,
882.075196236605,883.074932247325,884.074668258045,885.074404268766,886.074140279486,
887.073876290206,888.073612300926,889.073348311646,890.073084322366,891.072820333086,
892.072556343806,893.072292354527,894.072028365247,895.071764375967,896.071500386687,
897.071236397407,898.070972408127,899.070708418847,900.070444429567,901.070180440288,
902.069916451008,903.069652461728,904.069388472448,905.069124483168,906.068860493888,
907.068596504608,908.068332515329,909.068068526049,910.067804536769,911.067540547489,
912.067276558209,913.067012568929,914.066748579649,915.066484590369,916.06622060109,
917.06595661181,918.06569262253,919.06542863325,920.06516464397,921.06490065469,
922.06463666541,923.06437267613,924.064108686851,925.063844697571,926.063580708291,
927.063316719011,928.063052729731,929.062788740451,930.062524751171,931.062260761891,
932.061996772612,933.061732783332,934.061468794052,935.061204804772,936.060940815492,
937.060676826212,938.060412836932,939.060148847652,940.059884858373,941.059620869093,
942.059356879813,943.059092890533,944.058828901253,945.058564911973,946.058300922693,
947.058036933414,948.057772944134,949.057508954854,950.057244965574,951.056980976294,
952.056716987014,953.056452997734,954.056189008454,955.055925019175,956.055661029895,
957.055397040615,958.055133051335,959.054869062055,960.054605072775,961.054341083495,
962.054077094215,963.053813104936,964.053549115656,965.053285126376,966.053021137096,
967.052757147816,968.052493158536,969.052229169256,970.051965179976,971.051701190697,
972.051437201417,973.051173212137,974.050909222857,975.050645233577,976.050381244297,
977.050117255017,978.049853265738,979.049589276458,980.049325287178,981.049061297898,
982.048797308618,983.048533319338,984.048269330058,985.048005340778,986.047741351499,
987.047477362219,988.047213372939,989.046949383659,990.046685394379,991.046421405099,
992.046157415819,993.045893426539,994.04562943726,995.04536544798,996.0451014587,
997.04483746942,998.04457348014,999.04430949086,1000.04404550158,1001.0437815123,
1002.04351752302,1003.04325353374,1004.04298954446,1005.04272555518,1006.0424615659,
1007.04219757662,1008.04193358734,1009.04166959806,1010.04140560878,1011.0411416195,
1012.04087763022,1013.04061364094,1014.04034965166,1015.04008566238,1016.0398216731,
1017.03955768382,1018.03929369454,1019.03902970526,1020.03876571598,1021.0385017267,
1022.03823773742,1023.03797374814,1024.03770975886,1025.03744576958,1026.0371817803,
1027.03691779102,1028.03665380174,1029.03638981246,1030.03612582318,1031.0358618339,
1032.03559784462,1033.03533385534,1034.03506986606,1035.03480587678,1036.03454188751,
1037.03427789823,1038.03401390895,1039.03374991967,1040.03348593039,1041.03322194111,
1042.03295795183,1043.03269396255,1044.03242997327,1045.03216598399,1046.03190199471,
1047.03163800543,1048.03137401615,1049.03111002687,1050.03084603759,1051.03058204831,
1052.03031805903,1053.03005406975,1054.02979008047,1055.02952609119,1056.02926210191,
1057.02899811263,1058.02873412335,1059.02847013407,1060.02820614479,1061.02794215551,
1062.02767816623,1063.02741417695,1064.02715018767,1065.02688619839,1066.02662220911,
1067.02635821983,1068.02609423055,1069.02583024127,1070.02556625199,1071.02530226271,
1072.02503827343,1073.02477428415,1074.02451029487,1075.02424630559,1076.02398231631,
1077.02371832703,1078.02345433775,1079.02319034847,1080.02292635919,1081.02266236991,
1082.02239838063,1083.02213439135,1084.02187040207,1085.02160641279,1086.02134242351,
1087.02107843423,1088.02081444495,1089.02055045567,1090.02028646639,1091.02002247711,
1092.01975848783,1093.01949449855,1094.01923050927,1095.01896651999,1096.01870253071,
1097.01843854143,1098.01817455215,1099.01791056287,1100.01764657359,1101.01738258431,
1102.01711859503,1103.01685460575,1104.01659061647,1105.01632662719,1106.01606263791,
1107.01579864863,1108.01553465935,1109.01527067007,1110.01500668079,1111.01474269151,
1112.01447870223,1113.01421471295,1114.01395072368,1115.0136867344,1116.01342274512,
1117.01315875584,1118.01289476656,1119.01263077728,1120.012366788,1121.01210279872,
1122.01183880944,1123.01157482016,1124.01131083088,1125.0110468416,1126.01078285232,
1127.01051886304,1128.01025487376,1129.00999088448,1130.0097268952,1131.00946290592,
1132.00919891664,1133.00893492736,1134.00867093808,1135.0084069488,1136.00814295952,
1137.00787897024,1138.00761498096,1139.00735099168,1140.0070870024,1141.00682301312,
1142.00655902384,1143.00629503456,1144.00603104528,1145.005767056,1146.00550306672,
1147.00523907744,1148.00497508816,1149.00471109888,1150.0044471096,1151.00418312032,
1152.00391913104,1153.00365514176,1154.00339115248,1155.0031271632,1156.00286317392,
1157.00259918464,1158.00233519536,1159.00207120608,1160.0018072168,1161.00154322752,
1162.00127923824,1163.00101524896,1164.00075125968,1165.0004872704,1166.00022328112,
1166.99995929184,1167.99969530256,1168.99943131328,1169.999167324,1170.99890333472,
1171.99863934544,1172.99837535616,1173.99811136688,1174.9978473776,1175.99758338832,
1176.99731939904,1177.99705540976,1178.99679142048,1179.9965274312,1180.99626344192,
1181.99599945264,1182.99573546336,1183.99547147408,1184.9952074848,1185.99494349552,
1186.99467950624,1187.99441551696,1188.99415152768,1189.99388753841,1190.99362354913,
1191.99335955985,1192.99309557057,1193.99283158129,1194.99256759201,1195.99230360273,
1196.99203961345,1197.99177562417,1198.99151163489,1199.99124764561,1200.99098365633,
1201.99071966705,1202.99045567777,1203.99019168849,1204.98992769921,1205.98966370993,
1206.98939972065,1207.98913573137,1208.98887174209,1209.98860775281,1210.98834376353,
1211.98807977425,1212.98781578497,1213.98755179569,1214.98728780641,1215.98702381713,
1216.98675982785,1217.98649583857,1218.98623184929,1219.98596786001,1220.98570387073,
1221.98543988145,1222.98517589217,1223.98491190289,1224.98464791361,1225.98438392433,
1226.98411993505,1227.98385594577,1228.98359195649,1229.98332796721,1230.98306397793,
1231.98279998865,1232.98253599937,1233.98227201009,1234.98200802081,1235.98174403153,
1236.98148004225,1237.98121605297,1238.98095206369,1239.98068807441,1240.98042408513,
1241.98016009585,1242.97989610657,1243.97963211729,1244.97936812801,1245.97910413873,
1246.97884014945,1247.97857616017,1248.97831217089,1249.97804818161,1250.97778419233,
1251.97752020305,1252.97725621377,1253.97699222449,1254.97672823521,1255.97646424593,
1256.97620025665,1257.97593626737,1258.97567227809,1259.97540828881,1260.97514429953,
1261.97488031025,1262.97461632097,1263.97435233169,1264.97408834241,1265.97382435313,
1266.97356036385,1267.97329637458,1268.9730323853,1269.97276839602,1270.97250440674,
1271.97224041746,1272.97197642818,1273.9717124389,1274.97144844962,1275.97118446034,
1276.97092047106,1277.97065648178,1278.9703924925,1279.97012850322,1280.96986451394,
1281.96960052466,1282.96933653538,1283.9690725461,1284.96880855682,1285.96854456754,
1286.96828057826,1287.96801658898,1288.9677525997,1289.96748861042,1290.96722462114,
1291.96696063186,1292.96669664258,1293.9664326533,1294.96616866402,1295.96590467474,
1296.96564068546,1297.96537669618,1298.9651127069,1299.96484871762,1300.96458472834,
1301.96432073906,1302.96405674978,1303.9637927605,1304.96352877122,1305.96326478194,
1306.96300079266,1307.96273680338,1308.9624728141,1309.96220882482,1310.96194483554,
1311.96168084626,1312.96141685698,1313.9611528677,1314.96088887842,1315.96062488914,
1316.96036089986,1317.96009691058,1318.9598329213,1319.95956893202,1320.95930494274,
1321.95904095346,1322.95877696418,1323.9585129749,1324.95824898562,1325.95798499634,
1326.95772100706,1327.95745701778,1328.9571930285,1329.95692903922,1330.95666504994,
1331.95640106066,1332.95613707138,1333.9558730821,1334.95560909282,1335.95534510354,
1336.95508111426,1337.95481712498,1338.9545531357,1339.95428914642,1340.95402515714,
1341.95376116786,1342.95349717858,1343.9532331893,1344.95296920002,1345.95270521075,
1346.95244122147,1347.95217723219,1348.95191324291,1349.95164925363,1350.95138526435,
1351.95112127507,1352.95085728579,1353.95059329651,1354.95032930723,1355.95006531795,
1356.94980132867,1357.94953733939,1358.94927335011,1359.94900936083,1360.94874537155,
1361.94848138227,1362.94821739299,1363.94795340371,1364.94768941443,1365.94742542515,
1366.94716143587,1367.94689744659,1368.94663345731,1369.94636946803,1370.94610547875,
1371.94584148947,1372.94557750019,1373.94531351091,1374.94504952163,1375.94478553235,
1376.94452154307,1377.94425755379,1378.94399356451,1379.94372957523,1380.94346558595,
1381.94320159667,1382.94293760739,1383.94267361811,1384.94240962883,1385.94214563955,
1386.94188165027,1387.94161766099,1388.94135367171,1389.94108968243,1390.94082569315,
1391.94056170387,1392.94029771459,1393.94003372531,1394.93976973603,1395.93950574675,
1396.93924175747,1397.93897776819,1398.93871377891,1399.93844978963,1400.93818580035,
1401.93792181107,1402.93765782179,1403.93739383251,1404.93712984323,1405.93686585395,
1406.93660186467,1407.93633787539,1408.93607388611,1409.93580989683,1410.93554590755,
1411.93528191827,1412.93501792899,1413.93475393971,1414.93448995043,1415.93422596115,
1416.93396197187,1417.93369798259,1418.93343399331,1419.93317000403,1420.93290601475,
1421.93264202547,1422.93237803619,1423.93211404692,1424.93185005764,1425.93158606836,
1426.93132207908,1427.9310580898,1428.93079410052,1429.93053011124,1430.93026612196,
1431.93000213268,1432.9297381434,1433.92947415412,1434.92921016484,1435.92894617556,
1436.92868218628,1437.928418197,1438.92815420772,1439.92789021844,1440.92762622916,
1441.92736223988,1442.9270982506,1443.92683426132,1444.92657027204,1445.92630628276,
1446.92604229348,1447.9257783042,1448.92551431492,1449.92525032564,1450.92498633636,
1451.92472234708,1452.9244583578,1453.92419436852,1454.92393037924,1455.92366638996,
1456.92340240068,1457.9231384114,1458.92287442212,1459.92261043284,1460.92234644356,
1461.92208245428,1462.921818465,1463.92155447572,1464.92129048644,1465.92102649716,
1466.92076250788,1467.9204985186,1468.92023452932,1469.91997054004,1470.91970655076,
1471.91944256148,1472.9191785722,1473.91891458292,1474.91865059364,1475.91838660436,
1476.91812261508,1477.9178586258,1478.91759463652,1479.91733064724,1480.91706665796,
1481.91680266868,1482.9165386794,1483.91627469012,1484.91601070084,1485.91574671156,
1486.91548272228,1487.915218733,1488.91495474372,1489.91469075444,1490.91442676516,
1491.91416277588,1492.9138987866,1493.91363479732,1494.91337080804,1495.91310681876,
1496.91284282948,1497.9125788402,1498.91231485092,1499.91205086164,1500.91178687236,
1501.91152288309,1502.91125889381,1503.91099490453,1504.91073091525,1505.91046692597,
1506.91020293669,1507.90993894741,1508.90967495813,1509.90941096885,1510.90914697957,
1511.90888299029,1512.90861900101,1513.90835501173,1514.90809102245,1515.90782703317,
1516.90756304389,1517.90729905461,1518.90703506533,1519.90677107605,1520.90650708677,
1521.90624309749,1522.90597910821,1523.90571511893,1524.90545112965,1525.90518714037,
1526.90492315109,1527.90465916181,1528.90439517253,1529.90413118325,1530.90386719397,
1531.90360320469,1532.90333921541,1533.90307522613,1534.90281123685,1535.90254724757,
1536.90228325829,1537.90201926901,1538.90175527973,1539.90149129045,1540.90122730117,
1541.90096331189,1542.90069932261,1543.90043533333,1544.90017134405,1545.89990735477,
1546.89964336549,1547.89937937621,1548.89911538693,1549.89885139765,1550.89858740837,
1551.89832341909,1552.89805942981,1553.89779544053,1554.89753145125,1555.89726746197,
1556.89700347269,1557.89673948341,1558.89647549413,1559.89621150485,1560.89594751557,
1561.89568352629,1562.89541953701,1563.89515554773,1564.89489155845,1565.89462756917,
1566.89436357989,1567.89409959061,1568.89383560133,1569.89357161205,1570.89330762277,
1571.89304363349,1572.89277964421,1573.89251565493,1574.89225166565,1575.89198767637,
1576.89172368709,1577.89145969781,1578.89119570853,1579.89093171926,1580.89066772998,
1581.8904037407,1582.89013975142,1583.88987576214,1584.88961177286,1585.88934778358,
1586.8890837943,1587.88881980502,1588.88855581574,1589.88829182646,1590.88802783718,
1591.8877638479,1592.88749985862,1593.88723586934,1594.88697188006,1595.88670789078,
1596.8864439015,1597.88617991222,1598.88591592294,1599.88565193366,1600.88538794438,
1601.8851239551,1602.88485996582,1603.88459597654,1604.88433198726,1605.88406799798,
1606.8838040087,1607.88354001942,1608.88327603014,1609.88301204086,1610.88274805158,
1611.8824840623,1612.88222007302,1613.88195608374,1614.88169209446,1615.88142810518,
1616.8811641159,1617.88090012662,1618.88063613734,1619.88037214806,1620.88010815878,
1621.8798441695,1622.87958018022,1623.87931619094,1624.87905220166,1625.87878821238,
1626.8785242231,1627.87826023382,1628.87799624454,1629.87773225526,1630.87746826598,
1631.8772042767,1632.87694028742,1633.87667629814,1634.87641230886,1635.87614831958,
1636.8758843303,1637.87562034102,1638.87535635174,1639.87509236246,1640.87482837318,
1641.8745643839,1642.87430039462,1643.87403640534,1644.87377241606,1645.87350842678,
1646.8732444375,1647.87298044822,1648.87271645894,1649.87245246966,1650.87218848038,
1651.8719244911,1652.87166050182,1653.87139651254,1654.87113252326,1655.87086853399,
1656.8706045447,1657.87034055543,1658.87007656615,1659.86981257687,1660.86954858759,
1661.86928459831,1662.86902060903,1663.86875661975,1664.86849263047,1665.86822864119,
1666.86796465191,1667.86770066263,1668.86743667335,1669.86717268407,1670.86690869479,
1671.86664470551,1672.86638071623,1673.86611672695,1674.86585273767,1675.86558874839,
1676.86532475911,1677.86506076983,1678.86479678055,1679.86453279127,1680.86426880199,
1681.86400481271,1682.86374082343,1683.86347683415,1684.86321284487,1685.86294885559,
1686.86268486631,1687.86242087703,1688.86215688775,1689.86189289847,1690.86162890919,
1691.86136491991,1692.86110093063,1693.86083694135,1694.86057295207,1695.86030896279,
1696.86004497351,1697.35991297887,1697.85988790214),.UNSPECIFIED.);
#48=B_SPLINE_SURFACE_WITH_KNOTS('',3,3,((#195534,#195535,#195536,#195537,
#195538,#195539,#195540,#195541,#195542,#195543,#195544,#195545,#195546,
#195547,#195548,#195549,#195550,#195551,#195552,#195553,#195554,#195555,
#195556,#195557,#195558,#195559,#195560,#195561,#195562,#195563,#195564,
#195565,#195566,#195567,#195568,#195569,#195570,#195571,#195572,#195573,
#195574,#195575,#195576,#195577,#195578,#195579,#195580,#195581,#195582,
#195583,#195584,#195585,#195586,#195587,#195588,#195589,#195590,#195591,
#195592,#195593,#195594,#195595,#195596,#195597,#195598,#195599,#195600,
#195601,#195602,#195603,#195604,#195605,#195606,#195607,#195608,#195609,
#195610,#195611,#195612,#195613,#195614,#195615,#195616,#195617,#195618,
#195619,#195620,#195621,#195622,#195623,#195624,#195625,#195626,#195627,
#195628,#195629,#195630,#195631,#195632,#195633,#195634,#195635,#195636,
#195637,#195638,#195639,#195640,#195641,#195642,#195643,#195644,#195645,
#195646,#195647,#195648,#195649,#195650,#195651,#195652,#195653,#195654,
#195655,#195656,#195657,#195658,#195659,#195660,#195661,#195662,#195663,
#195664,#195665,#195666,#195667,#195668,#195669,#195670,#195671,#195672,
#195673,#195674,#195675,#195676,#195677,#195678,#195679,#195680,#195681,
#195682,#195683,#195684,#195685,#195686,#195687,#195688,#195689,#195690,
#195691,#195692,#195693,#195694,#195695,#195696,#195697,#195698,#195699,
#195700,#195701,#195702,#195703,#195704,#195705,#195706,#195707,#195708,
#195709,#195710,#195711,#195712,#195713,#195714,#195715,#195716,#195717,
#195718,#195719,#195720,#195721,#195722,#195723,#195724,#195725,#195726,
#195727,#195728,#195729,#195730,#195731,#195732,#195733,#195734,#195735,
#195736,#195737,#195738,#195739,#195740,#195741,#195742,#195743,#195744,
#195745,#195746,#195747,#195748,#195749,#195750,#195751,#195752,#195753,
#195754,#195755,#195756,#195757,#195758,#195759,#195760,#195761,#195762,
#195763,#195764,#195765,#195766,#195767,#195768,#195769,#195770,#195771,
#195772,#195773,#195774,#195775,#195776,#195777,#195778,#195779,#195780,
#195781,#195782,#195783,#195784,#195785,#195786,#195787,#195788,#195789,
#195790,#195791,#195792,#195793,#195794,#195795,#195796,#195797,#195798,
#195799,#195800,#195801,#195802,#195803,#195804,#195805,#195806,#195807,
#195808,#195809,#195810,#195811,#195812,#195813,#195814,#195815,#195816,
#195817,#195818,#195819,#195820,#195821,#195822,#195823,#195824,#195825,
#195826,#195827,#195828,#195829,#195830,#195831,#195832,#195833,#195834,
#195835,#195836,#195837,#195838,#195839,#195840,#195841,#195842,#195843,
#195844,#195845,#195846,#195847,#195848,#195849,#195850,#195851,#195852,
#195853,#195854,#195855,#195856,#195857,#195858,#195859,#195860,#195861,
#195862,#195863,#195864,#195865,#195866,#195867,#195868,#195869,#195870,
#195871,#195872,#195873,#195874,#195875,#195876,#195877,#195878,#195879,
#195880,#195881,#195882,#195883,#195884,#195885,#195886,#195887,#195888,
#195889,#195890,#195891,#195892,#195893,#195894,#195895,#195896,#195897,
#195898,#195899,#195900,#195901,#195902,#195903,#195904,#195905,#195906,
#195907,#195908,#195909,#195910,#195911,#195912,#195913,#195914,#195915,
#195916,#195917,#195918,#195919,#195920,#195921,#195922,#195923,#195924,
#195925,#195926,#195927,#195928,#195929,#195930,#195931,#195932,#195933,
#195934,#195935,#195936,#195937,#195938,#195939,#195940,#195941,#195942,
#195943,#195944,#195945,#195946,#195947,#195948,#195949,#195950,#195951,
#195952,#195953,#195954,#195955,#195956,#195957,#195958,#195959,#195960,
#195961,#195962,#195963,#195964,#195965,#195966,#195967,#195968,#195969,
#195970,#195971,#195972,#195973,#195974,#195975,#195976,#195977,#195978,
#195979,#195980,#195981,#195982,#195983,#195984,#195985,#195986,#195987,
#195988,#195989,#195990,#195991,#195992,#195993,#195994,#195995,#195996,
#195997,#195998,#195999,#196000,#196001,#196002,#196003,#196004,#196005,
#196006,#196007,#196008,#196009,#196010,#196011,#196012,#196013,#196014,
#196015,#196016,#196017,#196018,#196019,#196020,#196021,#196022,#196023,
#196024,#196025,#196026,#196027,#196028,#196029,#196030,#196031,#196032,
#196033,#196034,#196035,#196036,#196037,#196038,#196039,#196040,#196041,
#196042,#196043,#196044,#196045,#196046,#196047,#196048,#196049,#196050,
#196051,#196052,#196053,#196054,#196055,#196056,#196057,#196058,#196059,
#196060,#196061,#196062,#196063,#196064,#196065,#196066,#196067,#196068,
#196069,#196070,#196071,#196072,#196073,#196074,#196075,#196076,#196077,
#196078,#196079,#196080,#196081,#196082,#196083,#196084,#196085,#196086,
#196087,#196088,#196089,#196090,#196091,#196092,#196093,#196094,#196095,
#196096,#196097,#196098,#196099,#196100,#196101,#196102,#196103,#196104,
#196105,#196106,#196107,#196108,#196109,#196110,#196111,#196112,#196113,
#196114,#196115,#196116,#196117,#196118,#196119,#196120,#196121,#196122,
#196123,#196124,#196125,#196126,#196127,#196128,#196129,#196130,#196131,
#196132,#196133,#196134,#196135,#196136,#196137,#196138,#196139,#196140,
#196141,#196142,#196143,#196144,#196145,#196146,#196147,#196148,#196149,
#196150,#196151,#196152,#196153,#196154,#196155,#196156,#196157,#196158,
#196159,#196160,#196161,#196162,#196163,#196164,#196165,#196166,#196167,
#196168,#196169,#196170,#196171,#196172,#196173,#196174,#196175,#196176,
#196177,#196178,#196179,#196180,#196181,#196182,#196183,#196184,#196185,
#196186,#196187,#196188,#196189,#196190,#196191,#196192,#196193,#196194,
#196195,#196196,#196197,#196198,#196199,#196200,#196201,#196202,#196203,
#196204,#196205,#196206,#196207,#196208,#196209,#196210,#196211,#196212,
#196213,#196214,#196215,#196216,#196217,#196218,#196219,#196220,#196221,
#196222,#196223,#196224,#196225,#196226,#196227,#196228,#196229,#196230,
#196231,#196232,#196233,#196234,#196235,#196236,#196237,#196238,#196239,
#196240,#196241,#196242,#196243,#196244,#196245,#196246,#196247,#196248,
#196249,#196250,#196251,#196252,#196253,#196254,#196255,#196256,#196257,
#196258,#196259,#196260,#196261,#196262,#196263,#196264,#196265,#196266,
#196267,#196268,#196269,#196270,#196271,#196272,#196273,#196274,#196275,
#196276,#196277,#196278,#196279,#196280,#196281,#196282,#196283,#196284,
#196285,#196286,#196287,#196288,#196289,#196290,#196291,#196292,#196293,
#196294,#196295,#196296,#196297,#196298,#196299,#196300,#196301,#196302,
#196303,#196304,#196305,#196306,#196307,#196308,#196309,#196310,#196311,
#196312,#196313,#196314,#196315,#196316,#196317,#196318,#196319,#196320,
#196321,#196322,#196323,#196324,#196325,#196326,#196327,#196328,#196329,
#196330,#196331,#196332,#196333,#196334,#196335,#196336,#196337,#196338,
#196339,#196340,#196341,#196342,#196343,#196344,#196345,#196346,#196347,
#196348,#196349,#196350,#196351,#196352,#196353,#196354,#196355,#196356,
#196357,#196358,#196359,#196360,#196361,#196362,#196363,#196364,#196365,
#196366,#196367,#196368,#196369,#196370,#196371,#196372,#196373,#196374,
#196375,#196376,#196377,#196378,#196379,#196380,#196381,#196382,#196383,
#196384,#196385,#196386,#196387,#196388,#196389,#196390,#196391,#196392,
#196393,#196394,#196395,#196396,#196397,#196398,#196399,#196400,#196401,
#196402,#196403,#196404,#196405,#196406,#196407,#196408,#196409,#196410,
#196411,#196412,#196413,#196414,#196415,#196416,#196417,#196418,#196419,
#196420,#196421,#196422,#196423,#196424,#196425,#196426,#196427,#196428,
#196429,#196430,#196431,#196432,#196433,#196434,#196435,#196436,#196437,
#196438,#196439,#196440,#196441,#196442,#196443,#196444,#196445,#196446,
#196447,#196448,#196449,#196450,#196451,#196452,#196453,#196454,#196455,
#196456,#196457,#196458,#196459,#196460,#196461,#196462,#196463,#196464,
#196465,#196466,#196467,#196468,#196469,#196470,#196471,#196472,#196473,
#196474,#196475,#196476,#196477,#196478,#196479,#196480,#196481,#196482,
#196483,#196484,#196485,#196486,#196487,#196488,#196489,#196490,#196491,
#196492,#196493,#196494,#196495,#196496,#196497,#196498,#196499,#196500,
#196501,#196502,#196503,#196504,#196505,#196506,#196507,#196508,#196509,
#196510,#196511,#196512,#196513,#196514,#196515,#196516,#196517,#196518,
#196519,#196520,#196521,#196522,#196523,#196524,#196525,#196526,#196527,
#196528,#196529,#196530,#196531,#196532,#196533,#196534,#196535,#196536,
#196537,#196538,#196539,#196540,#196541,#196542,#196543,#196544,#196545,
#196546,#196547,#196548,#196549,#196550,#196551,#196552,#196553,#196554,
#196555,#196556,#196557,#196558,#196559,#196560,#196561,#196562,#196563,
#196564,#196565,#196566,#196567,#196568,#196569,#196570,#196571,#196572,
#196573,#196574,#196575,#196576,#196577,#196578,#196579,#196580,#196581,
#196582,#196583,#196584,#196585,#196586,#196587,#196588,#196589,#196590,
#196591,#196592,#196593,#196594,#196595,#196596,#196597,#196598,#196599,
#196600,#196601,#196602,#196603,#196604,#196605,#196606,#196607,#196608,
#196609,#196610,#196611,#196612,#196613,#196614,#196615,#196616,#196617,
#196618,#196619,#196620,#196621,#196622,#196623,#196624,#196625,#196626,
#196627,#196628,#196629,#196630,#196631,#196632,#196633,#196634,#196635,
#196636,#196637,#196638,#196639,#196640,#196641,#196642,#196643,#196644,
#196645,#196646,#196647,#196648,#196649,#196650,#196651,#196652,#196653,
#196654,#196655,#196656,#196657,#196658,#196659,#196660,#196661,#196662,
#196663,#196664,#196665,#196666,#196667,#196668,#196669,#196670,#196671,
#196672,#196673,#196674,#196675,#196676,#196677,#196678,#196679,#196680,
#196681,#196682,#196683,#196684,#196685,#196686,#196687,#196688,#196689,
#196690,#196691,#196692,#196693,#196694,#196695,#196696,#196697,#196698,
#196699,#196700,#196701,#196702,#196703,#196704,#196705,#196706,#196707,
#196708,#196709,#196710,#196711,#196712,#196713,#196714,#196715,#196716,
#196717,#196718,#196719,#196720,#196721,#196722,#196723,#196724,#196725,
#196726,#196727,#196728,#196729,#196730,#196731,#196732,#196733,#196734,
#196735,#196736,#196737,#196738,#196739,#196740,#196741,#196742,#196743,
#196744,#196745,#196746,#196747,#196748,#196749,#196750,#196751,#196752,
#196753,#196754,#196755,#196756,#196757,#196758,#196759,#196760,#196761,
#196762,#196763,#196764,#196765,#196766,#196767,#196768,#196769,#196770,
#196771,#196772,#196773,#196774,#196775,#196776,#196777,#196778,#196779,
#196780,#196781,#196782,#196783,#196784,#196785,#196786,#196787,#196788,
#196789,#196790,#196791,#196792,#196793,#196794,#196795,#196796,#196797,
#196798,#196799,#196800,#196801,#196802,#196803,#196804,#196805,#196806,
#196807,#196808,#196809,#196810,#196811,#196812,#196813,#196814,#196815,
#196816,#196817,#196818,#196819,#196820,#196821,#196822,#196823,#196824,
#196825,#196826,#196827,#196828,#196829,#196830,#196831,#196832,#196833,
#196834,#196835,#196836,#196837,#196838,#196839,#196840,#196841,#196842,
#196843,#196844,#196845,#196846,#196847,#196848,#196849,#196850,#196851,
#196852,#196853,#196854,#196855,#196856,#196857,#196858,#196859,#196860,
#196861,#196862,#196863,#196864,#196865,#196866,#196867,#196868,#196869,
#196870,#196871,#196872,#196873,#196874,#196875,#196876,#196877,#196878,
#196879,#196880,#196881,#196882,#196883,#196884,#196885,#196886,#196887,
#196888,#196889,#196890,#196891,#196892,#196893,#196894,#196895,#196896,
#196897,#196898,#196899,#196900,#196901,#196902,#196903,#196904,#196905,
#196906,#196907,#196908,#196909,#196910,#196911,#196912,#196913,#196914,
#196915,#196916,#196917,#196918,#196919,#196920,#196921,#196922,#196923,
#196924,#196925,#196926,#196927,#196928,#196929,#196930,#196931,#196932,
#196933,#196934,#196935,#196936,#196937,#196938,#196939,#196940,#196941,
#196942,#196943,#196944,#196945,#196946,#196947,#196948,#196949,#196950,
#196951,#196952,#196953,#196954,#196955,#196956,#196957,#196958,#196959,
#196960,#196961,#196962,#196963,#196964,#196965,#196966,#196967,#196968,
#196969,#196970,#196971,#196972,#196973,#196974,#196975,#196976,#196977,
#196978,#196979,#196980,#196981,#196982,#196983,#196984,#196985,#196986,
#196987,#196988,#196989,#196990,#196991,#196992,#196993,#196994,#196995,
#196996,#196997,#196998,#196999,#197000,#197001,#197002,#197003,#197004,
#197005,#197006,#197007,#197008,#197009,#197010,#197011,#197012,#197013,
#197014,#197015,#197016,#197017,#197018,#197019,#197020,#197021,#197022,
#197023,#197024,#197025,#197026,#197027,#197028,#197029,#197030,#197031,
#197032,#197033,#197034,#197035,#197036,#197037,#197038,#197039,#197040,
#197041,#197042,#197043,#197044,#197045,#197046,#197047,#197048,#197049,
#197050,#197051,#197052,#197053,#197054,#197055,#197056,#197057,#197058,
#197059,#197060,#197061,#197062,#197063,#197064,#197065,#197066,#197067,
#197068,#197069,#197070,#197071,#197072,#197073,#197074,#197075,#197076,
#197077,#197078,#197079,#197080,#197081,#197082,#197083,#197084,#197085,
#197086,#197087,#197088,#197089,#197090,#197091,#197092,#197093,#197094,
#197095,#197096,#197097,#197098,#197099,#197100,#197101,#197102,#197103,
#197104,#197105,#197106,#197107,#197108,#197109,#197110,#197111,#197112,
#197113,#197114,#197115,#197116,#197117,#197118,#197119,#197120,#197121,
#197122,#197123,#197124,#197125,#197126,#197127,#197128,#197129,#197130,
#197131,#197132,#197133,#197134,#197135,#197136,#197137,#197138,#197139,
#197140,#197141,#197142,#197143,#197144,#197145,#197146,#197147,#197148,
#197149,#197150,#197151,#197152,#197153,#197154,#197155,#197156,#197157,
#197158,#197159,#197160,#197161,#197162,#197163,#197164,#197165,#197166,
#197167,#197168,#197169,#197170,#197171,#197172,#197173,#197174,#197175,
#197176,#197177,#197178,#197179,#197180,#197181,#197182,#197183,#197184,
#197185,#197186,#197187,#197188,#197189,#197190,#197191,#197192,#197193,
#197194,#197195,#197196,#197197,#197198,#197199,#197200,#197201,#197202,
#197203,#197204,#197205,#197206,#197207,#197208,#197209,#197210,#197211,
#197212,#197213,#197214,#197215,#197216,#197217,#197218,#197219,#197220,
#197221,#197222,#197223,#197224,#197225,#197226,#197227,#197228),(#197229,
#197230,#197231,#197232,#197233,#197234,#197235,#197236,#197237,#197238,
#197239,#197240,#197241,#197242,#197243,#197244,#197245,#197246,#197247,
#197248,#197249,#197250,#197251,#197252,#197253,#197254,#197255,#197256,
#197257,#197258,#197259,#197260,#197261,#197262,#197263,#197264,#197265,
#197266,#197267,#197268,#197269,#197270,#197271,#197272,#197273,#197274,
#197275,#197276,#197277,#197278,#197279,#197280,#197281,#197282,#197283,
#197284,#197285,#197286,#197287,#197288,#197289,#197290,#197291,#197292,
#197293,#197294,#197295,#197296,#197297,#197298,#197299,#197300,#197301,
#197302,#197303,#197304,#197305,#197306,#197307,#197308,#197309,#197310,
#197311,#197312,#197313,#197314,#197315,#197316,#197317,#197318,#197319,
#197320,#197321,#197322,#197323,#197324,#197325,#197326,#197327,#197328,
#197329,#197330,#197331,#197332,#197333,#197334,#197335,#197336,#197337,
#197338,#197339,#197340,#197341,#197342,#197343,#197344,#197345,#197346,
#197347,#197348,#197349,#197350,#197351,#197352,#197353,#197354,#197355,
#197356,#197357,#197358,#197359,#197360,#197361,#197362,#197363,#197364,
#197365,#197366,#197367,#197368,#197369,#197370,#197371,#197372,#197373,
#197374,#197375,#197376,#197377,#197378,#197379,#197380,#197381,#197382,
#197383,#197384,#197385,#197386,#197387,#197388,#197389,#197390,#197391,
#197392,#197393,#197394,#197395,#197396,#197397,#197398,#197399,#197400,
#197401,#197402,#197403,#197404,#197405,#197406,#197407,#197408,#197409,
#197410,#197411,#197412,#197413,#197414,#197415,#197416,#197417,#197418,
#197419,#197420,#197421,#197422,#197423,#197424,#197425,#197426,#197427,
#197428,#197429,#197430,#197431,#197432,#197433,#197434,#197435,#197436,
#197437,#197438,#197439,#197440,#197441,#197442,#197443,#197444,#197445,
#197446,#197447,#197448,#197449,#197450,#197451,#197452,#197453,#197454,
#197455,#197456,#197457,#197458,#197459,#197460,#197461,#197462,#197463,
#197464,#197465,#197466,#197467,#197468,#197469,#197470,#197471,#197472,
#197473,#197474,#197475,#197476,#197477,#197478,#197479,#197480,#197481,
#197482,#197483,#197484,#197485,#197486,#197487,#197488,#197489,#197490,
#197491,#197492,#197493,#197494,#197495,#197496,#197497,#197498,#197499,
#197500,#197501,#197502,#197503,#197504,#197505,#197506,#197507,#197508,
#197509,#197510,#197511,#197512,#197513,#197514,#197515,#197516,#197517,
#197518,#197519,#197520,#197521,#197522,#197523,#197524,#197525,#197526,
#197527,#197528,#197529,#197530,#197531,#197532,#197533,#197534,#197535,
#197536,#197537,#197538,#197539,#197540,#197541,#197542,#197543,#197544,
#197545,#197546,#197547,#197548,#197549,#197550,#197551,#197552,#197553,
#197554,#197555,#197556,#197557,#197558,#197559,#197560,#197561,#197562,
#197563,#197564,#197565,#197566,#197567,#197568,#197569,#197570,#197571,
#197572,#197573,#197574,#197575,#197576,#197577,#197578,#197579,#197580,
#197581,#197582,#197583,#197584,#197585,#197586,#197587,#197588,#197589,
#197590,#197591,#197592,#197593,#197594,#197595,#197596,#197597,#197598,
#197599,#197600,#197601,#197602,#197603,#197604,#197605,#197606,#197607,
#197608,#197609,#197610,#197611,#197612,#197613,#197614,#197615,#197616,
#197617,#197618,#197619,#197620,#197621,#197622,#197623,#197624,#197625,
#197626,#197627,#197628,#197629,#197630,#197631,#197632,#197633,#197634,
#197635,#197636,#197637,#197638,#197639,#197640,#197641,#197642,#197643,
#197644,#197645,#197646,#197647,#197648,#197649,#197650,#197651,#197652,
#197653,#197654,#197655,#197656,#197657,#197658,#197659,#197660,#197661,
#197662,#197663,#197664,#197665,#197666,#197667,#197668,#197669,#197670,
#197671,#197672,#197673,#197674,#197675,#197676,#197677,#197678,#197679,
#197680,#197681,#197682,#197683,#197684,#197685,#197686,#197687,#197688,
#197689,#197690,#197691,#197692,#197693,#197694,#197695,#197696,#197697,
#197698,#197699,#197700,#197701,#197702,#197703,#197704,#197705,#197706,
#197707,#197708,#197709,#197710,#197711,#197712,#197713,#197714,#197715,
#197716,#197717,#197718,#197719,#197720,#197721,#197722,#197723,#197724,
#197725,#197726,#197727,#197728,#197729,#197730,#197731,#197732,#197733,
#197734,#197735,#197736,#197737,#197738,#197739,#197740,#197741,#197742,
#197743,#197744,#197745,#197746,#197747,#197748,#197749,#197750,#197751,
#197752,#197753,#197754,#197755,#197756,#197757,#197758,#197759,#197760,
#197761,#197762,#197763,#197764,#197765,#197766,#197767,#197768,#197769,
#197770,#197771,#197772,#197773,#197774,#197775,#197776,#197777,#197778,
#197779,#197780,#197781,#197782,#197783,#197784,#197785,#197786,#197787,
#197788,#197789,#197790,#197791,#197792,#197793,#197794,#197795,#197796,
#197797,#197798,#197799,#197800,#197801,#197802,#197803,#197804,#197805,
#197806,#197807,#197808,#197809,#197810,#197811,#197812,#197813,#197814,
#197815,#197816,#197817,#197818,#197819,#197820,#197821,#197822,#197823,
#197824,#197825,#197826,#197827,#197828,#197829,#197830,#197831,#197832,
#197833,#197834,#197835,#197836,#197837,#197838,#197839,#197840,#197841,
#197842,#197843,#197844,#197845,#197846,#197847,#197848,#197849,#197850,
#197851,#197852,#197853,#197854,#197855,#197856,#197857,#197858,#197859,
#197860,#197861,#197862,#197863,#197864,#197865,#197866,#197867,#197868,
#197869,#197870,#197871,#197872,#197873,#197874,#197875,#197876,#197877,
#197878,#197879,#197880,#197881,#197882,#197883,#197884,#197885,#197886,
#197887,#197888,#197889,#197890,#197891,#197892,#197893,#197894,#197895,
#197896,#197897,#197898,#197899,#197900,#197901,#197902,#197903,#197904,
#197905,#197906,#197907,#197908,#197909,#197910,#197911,#197912,#197913,
#197914,#197915,#197916,#197917,#197918,#197919,#197920,#197921,#197922,
#197923,#197924,#197925,#197926,#197927,#197928,#197929,#197930,#197931,
#197932,#197933,#197934,#197935,#197936,#197937,#197938,#197939,#197940,
#197941,#197942,#197943,#197944,#197945,#197946,#197947,#197948,#197949,
#197950,#197951,#197952,#197953,#197954,#197955,#197956,#197957,#197958,
#197959,#197960,#197961,#197962,#197963,#197964,#197965,#197966,#197967,
#197968,#197969,#197970,#197971,#197972,#197973,#197974,#197975,#197976,
#197977,#197978,#197979,#197980,#197981,#197982,#197983,#197984,#197985,
#197986,#197987,#197988,#197989,#197990,#197991,#197992,#197993,#197994,
#197995,#197996,#197997,#197998,#197999,#198000,#198001,#198002,#198003,
#198004,#198005,#198006,#198007,#198008,#198009,#198010,#198011,#198012,
#198013,#198014,#198015,#198016,#198017,#198018,#198019,#198020,#198021,
#198022,#198023,#198024,#198025,#198026,#198027,#198028,#198029,#198030,
#198031,#198032,#198033,#198034,#198035,#198036,#198037,#198038,#198039,
#198040,#198041,#198042,#198043,#198044,#198045,#198046,#198047,#198048,
#198049,#198050,#198051,#198052,#198053,#198054,#198055,#198056,#198057,
#198058,#198059,#198060,#198061,#198062,#198063,#198064,#198065,#198066,
#198067,#198068,#198069,#198070,#198071,#198072,#198073,#198074,#198075,
#198076,#198077,#198078,#198079,#198080,#198081,#198082,#198083,#198084,
#198085,#198086,#198087,#198088,#198089,#198090,#198091,#198092,#198093,
#198094,#198095,#198096,#198097,#198098,#198099,#198100,#198101,#198102,
#198103,#198104,#198105,#198106,#198107,#198108,#198109,#198110,#198111,
#198112,#198113,#198114,#198115,#198116,#198117,#198118,#198119,#198120,
#198121,#198122,#198123,#198124,#198125,#198126,#198127,#198128,#198129,
#198130,#198131,#198132,#198133,#198134,#198135,#198136,#198137,#198138,
#198139,#198140,#198141,#198142,#198143,#198144,#198145,#198146,#198147,
#198148,#198149,#198150,#198151,#198152,#198153,#198154,#198155,#198156,
#198157,#198158,#198159,#198160,#198161,#198162,#198163,#198164,#198165,
#198166,#198167,#198168,#198169,#198170,#198171,#198172,#198173,#198174,
#198175,#198176,#198177,#198178,#198179,#198180,#198181,#198182,#198183,
#198184,#198185,#198186,#198187,#198188,#198189,#198190,#198191,#198192,
#198193,#198194,#198195,#198196,#198197,#198198,#198199,#198200,#198201,
#198202,#198203,#198204,#198205,#198206,#198207,#198208,#198209,#198210,
#198211,#198212,#198213,#198214,#198215,#198216,#198217,#198218,#198219,
#198220,#198221,#198222,#198223,#198224,#198225,#198226,#198227,#198228,
#198229,#198230,#198231,#198232,#198233,#198234,#198235,#198236,#198237,
#198238,#198239,#198240,#198241,#198242,#198243,#198244,#198245,#198246,
#198247,#198248,#198249,#198250,#198251,#198252,#198253,#198254,#198255,
#198256,#198257,#198258,#198259,#198260,#198261,#198262,#198263,#198264,
#198265,#198266,#198267,#198268,#198269,#198270,#198271,#198272,#198273,
#198274,#198275,#198276,#198277,#198278,#198279,#198280,#198281,#198282,
#198283,#198284,#198285,#198286,#198287,#198288,#198289,#198290,#198291,
#198292,#198293,#198294,#198295,#198296,#198297,#198298,#198299,#198300,
#198301,#198302,#198303,#198304,#198305,#198306,#198307,#198308,#198309,
#198310,#198311,#198312,#198313,#198314,#198315,#198316,#198317,#198318,
#198319,#198320,#198321,#198322,#198323,#198324,#198325,#198326,#198327,
#198328,#198329,#198330,#198331,#198332,#198333,#198334,#198335,#198336,
#198337,#198338,#198339,#198340,#198341,#198342,#198343,#198344,#198345,
#198346,#198347,#198348,#198349,#198350,#198351,#198352,#198353,#198354,
#198355,#198356,#198357,#198358,#198359,#198360,#198361,#198362,#198363,
#198364,#198365,#198366,#198367,#198368,#198369,#198370,#198371,#198372,
#198373,#198374,#198375,#198376,#198377,#198378,#198379,#198380,#198381,
#198382,#198383,#198384,#198385,#198386,#198387,#198388,#198389,#198390,
#198391,#198392,#198393,#198394,#198395,#198396,#198397,#198398,#198399,
#198400,#198401,#198402,#198403,#198404,#198405,#198406,#198407,#198408,
#198409,#198410,#198411,#198412,#198413,#198414,#198415,#198416,#198417,
#198418,#198419,#198420,#198421,#198422,#198423,#198424,#198425,#198426,
#198427,#198428,#198429,#198430,#198431,#198432,#198433,#198434,#198435,
#198436,#198437,#198438,#198439,#198440,#198441,#198442,#198443,#198444,
#198445,#198446,#198447,#198448,#198449,#198450,#198451,#198452,#198453,
#198454,#198455,#198456,#198457,#198458,#198459,#198460,#198461,#198462,
#198463,#198464,#198465,#198466,#198467,#198468,#198469,#198470,#198471,
#198472,#198473,#198474,#198475,#198476,#198477,#198478,#198479,#198480,
#198481,#198482,#198483,#198484,#198485,#198486,#198487,#198488,#198489,
#198490,#198491,#198492,#198493,#198494,#198495,#198496,#198497,#198498,
#198499,#198500,#198501,#198502,#198503,#198504,#198505,#198506,#198507,
#198508,#198509,#198510,#198511,#198512,#198513,#198514,#198515,#198516,
#198517,#198518,#198519,#198520,#198521,#198522,#198523,#198524,#198525,
#198526,#198527,#198528,#198529,#198530,#198531,#198532,#198533,#198534,
#198535,#198536,#198537,#198538,#198539,#198540,#198541,#198542,#198543,
#198544,#198545,#198546,#198547,#198548,#198549,#198550,#198551,#198552,
#198553,#198554,#198555,#198556,#198557,#198558,#198559,#198560,#198561,
#198562,#198563,#198564,#198565,#198566,#198567,#198568,#198569,#198570,
#198571,#198572,#198573,#198574,#198575,#198576,#198577,#198578,#198579,
#198580,#198581,#198582,#198583,#198584,#198585,#198586,#198587,#198588,
#198589,#198590,#198591,#198592,#198593,#198594,#198595,#198596,#198597,
#198598,#198599,#198600,#198601,#198602,#198603,#198604,#198605,#198606,
#198607,#198608,#198609,#198610,#198611,#198612,#198613,#198614,#198615,
#198616,#198617,#198618,#198619,#198620,#198621,#198622,#198623,#198624,
#198625,#198626,#198627,#198628,#198629,#198630,#198631,#198632,#198633,
#198634,#198635,#198636,#198637,#198638,#198639,#198640,#198641,#198642,
#198643,#198644,#198645,#198646,#198647,#198648,#198649,#198650,#198651,
#198652,#198653,#198654,#198655,#198656,#198657,#198658,#198659,#198660,
#198661,#198662,#198663,#198664,#198665,#198666,#198667,#198668,#198669,
#198670,#198671,#198672,#198673,#198674,#198675,#198676,#198677,#198678,
#198679,#198680,#198681,#198682,#198683,#198684,#198685,#198686,#198687,
#198688,#198689,#198690,#198691,#198692,#198693,#198694,#198695,#198696,
#198697,#198698,#198699,#198700,#198701,#198702,#198703,#198704,#198705,
#198706,#198707,#198708,#198709,#198710,#198711,#198712,#198713,#198714,
#198715,#198716,#198717,#198718,#198719,#198720,#198721,#198722,#198723,
#198724,#198725,#198726,#198727,#198728,#198729,#198730,#198731,#198732,
#198733,#198734,#198735,#198736,#198737,#198738,#198739,#198740,#198741,
#198742,#198743,#198744,#198745,#198746,#198747,#198748,#198749,#198750,
#198751,#198752,#198753,#198754,#198755,#198756,#198757,#198758,#198759,
#198760,#198761,#198762,#198763,#198764,#198765,#198766,#198767,#198768,
#198769,#198770,#198771,#198772,#198773,#198774,#198775,#198776,#198777,
#198778,#198779,#198780,#198781,#198782,#198783,#198784,#198785,#198786,
#198787,#198788,#198789,#198790,#198791,#198792,#198793,#198794,#198795,
#198796,#198797,#198798,#198799,#198800,#198801,#198802,#198803,#198804,
#198805,#198806,#198807,#198808,#198809,#198810,#198811,#198812,#198813,
#198814,#198815,#198816,#198817,#198818,#198819,#198820,#198821,#198822,
#198823,#198824,#198825,#198826,#198827,#198828,#198829,#198830,#198831,
#198832,#198833,#198834,#198835,#198836,#198837,#198838,#198839,#198840,
#198841,#198842,#198843,#198844,#198845,#198846,#198847,#198848,#198849,
#198850,#198851,#198852,#198853,#198854,#198855,#198856,#198857,#198858,
#198859,#198860,#198861,#198862,#198863,#198864,#198865,#198866,#198867,
#198868,#198869,#198870,#198871,#198872,#198873,#198874,#198875,#198876,
#198877,#198878,#198879,#198880,#198881,#198882,#198883,#198884,#198885,
#198886,#198887,#198888,#198889,#198890,#198891,#198892,#198893,#198894,
#198895,#198896,#198897,#198898,#198899,#198900,#198901,#198902,#198903,
#198904,#198905,#198906,#198907,#198908,#198909,#198910,#198911,#198912,
#198913,#198914,#198915,#198916,#198917,#198918,#198919,#198920,#198921,
#198922,#198923),(#198924,#198925,#198926,#198927,#198928,#198929,#198930,
#198931,#198932,#198933,#198934,#198935,#198936,#198937,#198938,#198939,
#198940,#198941,#198942,#198943,#198944,#198945,#198946,#198947,#198948,
#198949,#198950,#198951,#198952,#198953,#198954,#198955,#198956,#198957,
#198958,#198959,#198960,#198961,#198962,#198963,#198964,#198965,#198966,
#198967,#198968,#198969,#198970,#198971,#198972,#198973,#198974,#198975,
#198976,#198977,#198978,#198979,#198980,#198981,#198982,#198983,#198984,
#198985,#198986,#198987,#198988,#198989,#198990,#198991,#198992,#198993,
#198994,#198995,#198996,#198997,#198998,#198999,#199000,#199001,#199002,
#199003,#199004,#199005,#199006,#199007,#199008,#199009,#199010,#199011,
#199012,#199013,#199014,#199015,#199016,#199017,#199018,#199019,#199020,
#199021,#199022,#199023,#199024,#199025,#199026,#199027,#199028,#199029,
#199030,#199031,#199032,#199033,#199034,#199035,#199036,#199037,#199038,
#199039,#199040,#199041,#199042,#199043,#199044,#199045,#199046,#199047,
#199048,#199049,#199050,#199051,#199052,#199053,#199054,#199055,#199056,
#199057,#199058,#199059,#199060,#199061,#199062,#199063,#199064,#199065,
#199066,#199067,#199068,#199069,#199070,#199071,#199072,#199073,#199074,
#199075,#199076,#199077,#199078,#199079,#199080,#199081,#199082,#199083,
#199084,#199085,#199086,#199087,#199088,#199089,#199090,#199091,#199092,
#199093,#199094,#199095,#199096,#199097,#199098,#199099,#199100,#199101,
#199102,#199103,#199104,#199105,#199106,#199107,#199108,#199109,#199110,
#199111,#199112,#199113,#199114,#199115,#199116,#199117,#199118,#199119,
#199120,#199121,#199122,#199123,#199124,#199125,#199126,#199127,#199128,
#199129,#199130,#199131,#199132,#199133,#199134,#199135,#199136,#199137,
#199138,#199139,#199140,#199141,#199142,#199143,#199144,#199145,#199146,
#199147,#199148,#199149,#199150,#199151,#199152,#199153,#199154,#199155,
#199156,#199157,#199158,#199159,#199160,#199161,#199162,#199163,#199164,
#199165,#199166,#199167,#199168,#199169,#199170,#199171,#199172,#199173,
#199174,#199175,#199176,#199177,#199178,#199179,#199180,#199181,#199182,
#199183,#199184,#199185,#199186,#199187,#199188,#199189,#199190,#199191,
#199192,#199193,#199194,#199195,#199196,#199197,#199198,#199199,#199200,
#199201,#199202,#199203,#199204,#199205,#199206,#199207,#199208,#199209,
#199210,#199211,#199212,#199213,#199214,#199215,#199216,#199217,#199218,
#199219,#199220,#199221,#199222,#199223,#199224,#199225,#199226,#199227,
#199228,#199229,#199230,#199231,#199232,#199233,#199234,#199235,#199236,
#199237,#199238,#199239,#199240,#199241,#199242,#199243,#199244,#199245,
#199246,#199247,#199248,#199249,#199250,#199251,#199252,#199253,#199254,
#199255,#199256,#199257,#199258,#199259,#199260,#199261,#199262,#199263,
#199264,#199265,#199266,#199267,#199268,#199269,#199270,#199271,#199272,
#199273,#199274,#199275,#199276,#199277,#199278,#199279,#199280,#199281,
#199282,#199283,#199284,#199285,#199286,#199287,#199288,#199289,#199290,
#199291,#199292,#199293,#199294,#199295,#199296,#199297,#199298,#199299,
#199300,#199301,#199302,#199303,#199304,#199305,#199306,#199307,#199308,
#199309,#199310,#199311,#199312,#199313,#199314,#199315,#199316,#199317,
#199318,#199319,#199320,#199321,#199322,#199323,#199324,#199325,#199326,
#199327,#199328,#199329,#199330,#199331,#199332,#199333,#199334,#199335,
#199336,#199337,#199338,#199339,#199340,#199341,#199342,#199343,#199344,
#199345,#199346,#199347,#199348,#199349,#199350,#199351,#199352,#199353,
#199354,#199355,#199356,#199357,#199358,#199359,#199360,#199361,#199362,
#199363,#199364,#199365,#199366,#199367,#199368,#199369,#199370,#199371,
#199372,#199373,#199374,#199375,#199376,#199377,#199378,#199379,#199380,
#199381,#199382,#199383,#199384,#199385,#199386,#199387,#199388,#199389,
#199390,#199391,#199392,#199393,#199394,#199395,#199396,#199397,#199398,
#199399,#199400,#199401,#199402,#199403,#199404,#199405,#199406,#199407,
#199408,#199409,#199410,#199411,#199412,#199413,#199414,#199415,#199416,
#199417,#199418,#199419,#199420,#199421,#199422,#199423,#199424,#199425,
#199426,#199427,#199428,#199429,#199430,#199431,#199432,#199433,#199434,
#199435,#199436,#199437,#199438,#199439,#199440,#199441,#199442,#199443,
#199444,#199445,#199446,#199447,#199448,#199449,#199450,#199451,#199452,
#199453,#199454,#199455,#199456,#199457,#199458,#199459,#199460,#199461,
#199462,#199463,#199464,#199465,#199466,#199467,#199468,#199469,#199470,
#199471,#199472,#199473,#199474,#199475,#199476,#199477,#199478,#199479,
#199480,#199481,#199482,#199483,#199484,#199485,#199486,#199487,#199488,
#199489,#199490,#199491,#199492,#199493,#199494,#199495,#199496,#199497,
#199498,#199499,#199500,#199501,#199502,#199503,#199504,#199505,#199506,
#199507,#199508,#199509,#199510,#199511,#199512,#199513,#199514,#199515,
#199516,#199517,#199518,#199519,#199520,#199521,#199522,#199523,#199524,
#199525,#199526,#199527,#199528,#199529,#199530,#199531,#199532,#199533,
#199534,#199535,#199536,#199537,#199538,#199539,#199540,#199541,#199542,
#199543,#199544,#199545,#199546,#199547,#199548,#199549,#199550,#199551,
#199552,#199553,#199554,#199555,#199556,#199557,#199558,#199559,#199560,
#199561,#199562,#199563,#199564,#199565,#199566,#199567,#199568,#199569,
#199570,#199571,#199572,#199573,#199574,#199575,#199576,#199577,#199578,
#199579,#199580,#199581,#199582,#199583,#199584,#199585,#199586,#199587,
#199588,#199589,#199590,#199591,#199592,#199593,#199594,#199595,#199596,
#199597,#199598,#199599,#199600,#199601,#199602,#199603,#199604,#199605,
#199606,#199607,#199608,#199609,#199610,#199611,#199612,#199613,#199614,
#199615,#199616,#199617,#199618,#199619,#199620,#199621,#199622,#199623,
#199624,#199625,#199626,#199627,#199628,#199629,#199630,#199631,#199632,
#199633,#199634,#199635,#199636,#199637,#199638,#199639,#199640,#199641,
#199642,#199643,#199644,#199645,#199646,#199647,#199648,#199649,#199650,
#199651,#199652,#199653,#199654,#199655,#199656,#199657,#199658,#199659,
#199660,#199661,#199662,#199663,#199664,#199665,#199666,#199667,#199668,
#199669,#199670,#199671,#199672,#199673,#199674,#199675,#199676,#199677,
#199678,#199679,#199680,#199681,#199682,#199683,#199684,#199685,#199686,
#199687,#199688,#199689,#199690,#199691,#199692,#199693,#199694,#199695,
#199696,#199697,#199698,#199699,#199700,#199701,#199702,#199703,#199704,
#199705,#199706,#199707,#199708,#199709,#199710,#199711,#199712,#199713,
#199714,#199715,#199716,#199717,#199718,#199719,#199720,#199721,#199722,
#199723,#199724,#199725,#199726,#199727,#199728,#199729,#199730,#199731,
#199732,#199733,#199734,#199735,#199736,#199737,#199738,#199739,#199740,
#199741,#199742,#199743,#199744,#199745,#199746,#199747,#199748,#199749,
#199750,#199751,#199752,#199753,#199754,#199755,#199756,#199757,#199758,
#199759,#199760,#199761,#199762,#199763,#199764,#199765,#199766,#199767,
#199768,#199769,#199770,#199771,#199772,#199773,#199774,#199775,#199776,
#199777,#199778,#199779,#199780,#199781,#199782,#199783,#199784,#199785,
#199786,#199787,#199788,#199789,#199790,#199791,#199792,#199793,#199794,
#199795,#199796,#199797,#199798,#199799,#199800,#199801,#199802,#199803,
#199804,#199805,#199806,#199807,#199808,#199809,#199810,#199811,#199812,
#199813,#199814,#199815,#199816,#199817,#199818,#199819,#199820,#199821,
#199822,#199823,#199824,#199825,#199826,#199827,#199828,#199829,#199830,
#199831,#199832,#199833,#199834,#199835,#199836,#199837,#199838,#199839,
#199840,#199841,#199842,#199843,#199844,#199845,#199846,#199847,#199848,
#199849,#199850,#199851,#199852,#199853,#199854,#199855,#199856,#199857,
#199858,#199859,#199860,#199861,#199862,#199863,#199864,#199865,#199866,
#199867,#199868,#199869,#199870,#199871,#199872,#199873,#199874,#199875,
#199876,#199877,#199878,#199879,#199880,#199881,#199882,#199883,#199884,
#199885,#199886,#199887,#199888,#199889,#199890,#199891,#199892,#199893,
#199894,#199895,#199896,#199897,#199898,#199899,#199900,#199901,#199902,
#199903,#199904,#199905,#199906,#199907,#199908,#199909,#199910,#199911,
#199912,#199913,#199914,#199915,#199916,#199917,#199918,#199919,#199920,
#199921,#199922,#199923,#199924,#199925,#199926,#199927,#199928,#199929,
#199930,#199931,#199932,#199933,#199934,#199935,#199936,#199937,#199938,
#199939,#199940,#199941,#199942,#199943,#199944,#199945,#199946,#199947,
#199948,#199949,#199950,#199951,#199952,#199953,#199954,#199955,#199956,
#199957,#199958,#199959,#199960,#199961,#199962,#199963,#199964,#199965,
#199966,#199967,#199968,#199969,#199970,#199971,#199972,#199973,#199974,
#199975,#199976,#199977,#199978,#199979,#199980,#199981,#199982,#199983,
#199984,#199985,#199986,#199987,#199988,#199989,#199990,#199991,#199992,
#199993,#199994,#199995,#199996,#199997,#199998,#199999,#200000,#200001,
#200002,#200003,#200004,#200005,#200006,#200007,#200008,#200009,#200010,
#200011,#200012,#200013,#200014,#200015,#200016,#200017,#200018,#200019,
#200020,#200021,#200022,#200023,#200024,#200025,#200026,#200027,#200028,
#200029,#200030,#200031,#200032,#200033,#200034,#200035,#200036,#200037,
#200038,#200039,#200040,#200041,#200042,#200043,#200044,#200045,#200046,
#200047,#200048,#200049,#200050,#200051,#200052,#200053,#200054,#200055,
#200056,#200057,#200058,#200059,#200060,#200061,#200062,#200063,#200064,
#200065,#200066,#200067,#200068,#200069,#200070,#200071,#200072,#200073,
#200074,#200075,#200076,#200077,#200078,#200079,#200080,#200081,#200082,
#200083,#200084,#200085,#200086,#200087,#200088,#200089,#200090,#200091,
#200092,#200093,#200094,#200095,#200096,#200097,#200098,#200099,#200100,
#200101,#200102,#200103,#200104,#200105,#200106,#200107,#200108,#200109,
#200110,#200111,#200112,#200113,#200114,#200115,#200116,#200117,#200118,
#200119,#200120,#200121,#200122,#200123,#200124,#200125,#200126,#200127,
#200128,#200129,#200130,#200131,#200132,#200133,#200134,#200135,#200136,
#200137,#200138,#200139,#200140,#200141,#200142,#200143,#200144,#200145,
#200146,#200147,#200148,#200149,#200150,#200151,#200152,#200153,#200154,
#200155,#200156,#200157,#200158,#200159,#200160,#200161,#200162,#200163,
#200164,#200165,#200166,#200167,#200168,#200169,#200170,#200171,#200172,
#200173,#200174,#200175,#200176,#200177,#200178,#200179,#200180,#200181,
#200182,#200183,#200184,#200185,#200186,#200187,#200188,#200189,#200190,
#200191,#200192,#200193,#200194,#200195,#200196,#200197,#200198,#200199,
#200200,#200201,#200202,#200203,#200204,#200205,#200206,#200207,#200208,
#200209,#200210,#200211,#200212,#200213,#200214,#200215,#200216,#200217,
#200218,#200219,#200220,#200221,#200222,#200223,#200224,#200225,#200226,
#200227,#200228,#200229,#200230,#200231,#200232,#200233,#200234,#200235,
#200236,#200237,#200238,#200239,#200240,#200241,#200242,#200243,#200244,
#200245,#200246,#200247,#200248,#200249,#200250,#200251,#200252,#200253,
#200254,#200255,#200256,#200257,#200258,#200259,#200260,#200261,#200262,
#200263,#200264,#200265,#200266,#200267,#200268,#200269,#200270,#200271,
#200272,#200273,#200274,#200275,#200276,#200277,#200278,#200279,#200280,
#200281,#200282,#200283,#200284,#200285,#200286,#200287,#200288,#200289,
#200290,#200291,#200292,#200293,#200294,#200295,#200296,#200297,#200298,
#200299,#200300,#200301,#200302,#200303,#200304,#200305,#200306,#200307,
#200308,#200309,#200310,#200311,#200312,#200313,#200314,#200315,#200316,
#200317,#200318,#200319,#200320,#200321,#200322,#200323,#200324,#200325,
#200326,#200327,#200328,#200329,#200330,#200331,#200332,#200333,#200334,
#200335,#200336,#200337,#200338,#200339,#200340,#200341,#200342,#200343,
#200344,#200345,#200346,#200347,#200348,#200349,#200350,#200351,#200352,
#200353,#200354,#200355,#200356,#200357,#200358,#200359,#200360,#200361,
#200362,#200363,#200364,#200365,#200366,#200367,#200368,#200369,#200370,
#200371,#200372,#200373,#200374,#200375,#200376,#200377,#200378,#200379,
#200380,#200381,#200382,#200383,#200384,#200385,#200386,#200387,#200388,
#200389,#200390,#200391,#200392,#200393,#200394,#200395,#200396,#200397,
#200398,#200399,#200400,#200401,#200402,#200403,#200404,#200405,#200406,
#200407,#200408,#200409,#200410,#200411,#200412,#200413,#200414,#200415,
#200416,#200417,#200418,#200419,#200420,#200421,#200422,#200423,#200424,
#200425,#200426,#200427,#200428,#200429,#200430,#200431,#200432,#200433,
#200434,#200435,#200436,#200437,#200438,#200439,#200440,#200441,#200442,
#200443,#200444,#200445,#200446,#200447,#200448,#200449,#200450,#200451,
#200452,#200453,#200454,#200455,#200456,#200457,#200458,#200459,#200460,
#200461,#200462,#200463,#200464,#200465,#200466,#200467,#200468,#200469,
#200470,#200471,#200472,#200473,#200474,#200475,#200476,#200477,#200478,
#200479,#200480,#200481,#200482,#200483,#200484,#200485,#200486,#200487,
#200488,#200489,#200490,#200491,#200492,#200493,#200494,#200495,#200496,
#200497,#200498,#200499,#200500,#200501,#200502,#200503,#200504,#200505,
#200506,#200507,#200508,#200509,#200510,#200511,#200512,#200513,#200514,
#200515,#200516,#200517,#200518,#200519,#200520,#200521,#200522,#200523,
#200524,#200525,#200526,#200527,#200528,#200529,#200530,#200531,#200532,
#200533,#200534,#200535,#200536,#200537,#200538,#200539,#200540,#200541,
#200542,#200543,#200544,#200545,#200546,#200547,#200548,#200549,#200550,
#200551,#200552,#200553,#200554,#200555,#200556,#200557,#200558,#200559,
#200560,#200561,#200562,#200563,#200564,#200565,#200566,#200567,#200568,
#200569,#200570,#200571,#200572,#200573,#200574,#200575,#200576,#200577,
#200578,#200579,#200580,#200581,#200582,#200583,#200584,#200585,#200586,
#200587,#200588,#200589,#200590,#200591,#200592,#200593,#200594,#200595,
#200596,#200597,#200598,#200599,#200600,#200601,#200602,#200603,#200604,
#200605,#200606,#200607,#200608,#200609,#200610,#200611,#200612,#200613,
#200614,#200615,#200616,#200617,#200618),(#200619,#200620,#200621,#200622,
#200623,#200624,#200625,#200626,#200627,#200628,#200629,#200630,#200631,
#200632,#200633,#200634,#200635,#200636,#200637,#200638,#200639,#200640,
#200641,#200642,#200643,#200644,#200645,#200646,#200647,#200648,#200649,
#200650,#200651,#200652,#200653,#200654,#200655,#200656,#200657,#200658,
#200659,#200660,#200661,#200662,#200663,#200664,#200665,#200666,#200667,
#200668,#200669,#200670,#200671,#200672,#200673,#200674,#200675,#200676,
#200677,#200678,#200679,#200680,#200681,#200682,#200683,#200684,#200685,
#200686,#200687,#200688,#200689,#200690,#200691,#200692,#200693,#200694,
#200695,#200696,#200697,#200698,#200699,#200700,#200701,#200702,#200703,
#200704,#200705,#200706,#200707,#200708,#200709,#200710,#200711,#200712,
#200713,#200714,#200715,#200716,#200717,#200718,#200719,#200720,#200721,
#200722,#200723,#200724,#200725,#200726,#200727,#200728,#200729,#200730,
#200731,#200732,#200733,#200734,#200735,#200736,#200737,#200738,#200739,
#200740,#200741,#200742,#200743,#200744,#200745,#200746,#200747,#200748,
#200749,#200750,#200751,#200752,#200753,#200754,#200755,#200756,#200757,
#200758,#200759,#200760,#200761,#200762,#200763,#200764,#200765,#200766,
#200767,#200768,#200769,#200770,#200771,#200772,#200773,#200774,#200775,
#200776,#200777,#200778,#200779,#200780,#200781,#200782,#200783,#200784,
#200785,#200786,#200787,#200788,#200789,#200790,#200791,#200792,#200793,
#200794,#200795,#200796,#200797,#200798,#200799,#200800,#200801,#200802,
#200803,#200804,#200805,#200806,#200807,#200808,#200809,#200810,#200811,
#200812,#200813,#200814,#200815,#200816,#200817,#200818,#200819,#200820,
#200821,#200822,#200823,#200824,#200825,#200826,#200827,#200828,#200829,
#200830,#200831,#200832,#200833,#200834,#200835,#200836,#200837,#200838,
#200839,#200840,#200841,#200842,#200843,#200844,#200845,#200846,#200847,
#200848,#200849,#200850,#200851,#200852,#200853,#200854,#200855,#200856,
#200857,#200858,#200859,#200860,#200861,#200862,#200863,#200864,#200865,
#200866,#200867,#200868,#200869,#200870,#200871,#200872,#200873,#200874,
#200875,#200876,#200877,#200878,#200879,#200880,#200881,#200882,#200883,
#200884,#200885,#200886,#200887,#200888,#200889,#200890,#200891,#200892,
#200893,#200894,#200895,#200896,#200897,#200898,#200899,#200900,#200901,
#200902,#200903,#200904,#200905,#200906,#200907,#200908,#200909,#200910,
#200911,#200912,#200913,#200914,#200915,#200916,#200917,#200918,#200919,
#200920,#200921,#200922,#200923,#200924,#200925,#200926,#200927,#200928,
#200929,#200930,#200931,#200932,#200933,#200934,#200935,#200936,#200937,
#200938,#200939,#200940,#200941,#200942,#200943,#200944,#200945,#200946,
#200947,#200948,#200949,#200950,#200951,#200952,#200953,#200954,#200955,
#200956,#200957,#200958,#200959,#200960,#200961,#200962,#200963,#200964,
#200965,#200966,#200967,#200968,#200969,#200970,#200971,#200972,#200973,
#200974,#200975,#200976,#200977,#200978,#200979,#200980,#200981,#200982,
#200983,#200984,#200985,#200986,#200987,#200988,#200989,#200990,#200991,
#200992,#200993,#200994,#200995,#200996,#200997,#200998,#200999,#201000,
#201001,#201002,#201003,#201004,#201005,#201006,#201007,#201008,#201009,
#201010,#201011,#201012,#201013,#201014,#201015,#201016,#201017,#201018,
#201019,#201020,#201021,#201022,#201023,#201024,#201025,#201026,#201027,
#201028,#201029,#201030,#201031,#201032,#201033,#201034,#201035,#201036,
#201037,#201038,#201039,#201040,#201041,#201042,#201043,#201044,#201045,
#201046,#201047,#201048,#201049,#201050,#201051,#201052,#201053,#201054,
#201055,#201056,#201057,#201058,#201059,#201060,#201061,#201062,#201063,
#201064,#201065,#201066,#201067,#201068,#201069,#201070,#201071,#201072,
#201073,#201074,#201075,#201076,#201077,#201078,#201079,#201080,#201081,
#201082,#201083,#201084,#201085,#201086,#201087,#201088,#201089,#201090,
#201091,#201092,#201093,#201094,#201095,#201096,#201097,#201098,#201099,
#201100,#201101,#201102,#201103,#201104,#201105,#201106,#201107,#201108,
#201109,#201110,#201111,#201112,#201113,#201114,#201115,#201116,#201117,
#201118,#201119,#201120,#201121,#201122,#201123,#201124,#201125,#201126,
#201127,#201128,#201129,#201130,#201131,#201132,#201133,#201134,#201135,
#201136,#201137,#201138,#201139,#201140,#201141,#201142,#201143,#201144,
#201145,#201146,#201147,#201148,#201149,#201150,#201151,#201152,#201153,
#201154,#201155,#201156,#201157,#201158,#201159,#201160,#201161,#201162,
#201163,#201164,#201165,#201166,#201167,#201168,#201169,#201170,#201171,
#201172,#201173,#201174,#201175,#201176,#201177,#201178,#201179,#201180,
#201181,#201182,#201183,#201184,#201185,#201186,#201187,#201188,#201189,
#201190,#201191,#201192,#201193,#201194,#201195,#201196,#201197,#201198,
#201199,#201200,#201201,#201202,#201203,#201204,#201205,#201206,#201207,
#201208,#201209,#201210,#201211,#201212,#201213,#201214,#201215,#201216,
#201217,#201218,#201219,#201220,#201221,#201222,#201223,#201224,#201225,
#201226,#201227,#201228,#201229,#201230,#201231,#201232,#201233,#201234,
#201235,#201236,#201237,#201238,#201239,#201240,#201241,#201242,#201243,
#201244,#201245,#201246,#201247,#201248,#201249,#201250,#201251,#201252,
#201253,#201254,#201255,#201256,#201257,#201258,#201259,#201260,#201261,
#201262,#201263,#201264,#201265,#201266,#201267,#201268,#201269,#201270,
#201271,#201272,#201273,#201274,#201275,#201276,#201277,#201278,#201279,
#201280,#201281,#201282,#201283,#201284,#201285,#201286,#201287,#201288,
#201289,#201290,#201291,#201292,#201293,#201294,#201295,#201296,#201297,
#201298,#201299,#201300,#201301,#201302,#201303,#201304,#201305,#201306,
#201307,#201308,#201309,#201310,#201311,#201312,#201313,#201314,#201315,
#201316,#201317,#201318,#201319,#201320,#201321,#201322,#201323,#201324,
#201325,#201326,#201327,#201328,#201329,#201330,#201331,#201332,#201333,
#201334,#201335,#201336,#201337,#201338,#201339,#201340,#201341,#201342,
#201343,#201344,#201345,#201346,#201347,#201348,#201349,#201350,#201351,
#201352,#201353,#201354,#201355,#201356,#201357,#201358,#201359,#201360,
#201361,#201362,#201363,#201364,#201365,#201366,#201367,#201368,#201369,
#201370,#201371,#201372,#201373,#201374,#201375,#201376,#201377,#201378,
#201379,#201380,#201381,#201382,#201383,#201384,#201385,#201386,#201387,
#201388,#201389,#201390,#201391,#201392,#201393,#201394,#201395,#201396,
#201397,#201398,#201399,#201400,#201401,#201402,#201403,#201404,#201405,
#201406,#201407,#201408,#201409,#201410,#201411,#201412,#201413,#201414,
#201415,#201416,#201417,#201418,#201419,#201420,#201421,#201422,#201423,
#201424,#201425,#201426,#201427,#201428,#201429,#201430,#201431,#201432,
#201433,#201434,#201435,#201436,#201437,#201438,#201439,#201440,#201441,
#201442,#201443,#201444,#201445,#201446,#201447,#201448,#201449,#201450,
#201451,#201452,#201453,#201454,#201455,#201456,#201457,#201458,#201459,
#201460,#201461,#201462,#201463,#201464,#201465,#201466,#201467,#201468,
#201469,#201470,#201471,#201472,#201473,#201474,#201475,#201476,#201477,
#201478,#201479,#201480,#201481,#201482,#201483,#201484,#201485,#201486,
#201487,#201488,#201489,#201490,#201491,#201492,#201493,#201494,#201495,
#201496,#201497,#201498,#201499,#201500,#201501,#201502,#201503,#201504,
#201505,#201506,#201507,#201508,#201509,#201510,#201511,#201512,#201513,
#201514,#201515,#201516,#201517,#201518,#201519,#201520,#201521,#201522,
#201523,#201524,#201525,#201526,#201527,#201528,#201529,#201530,#201531,
#201532,#201533,#201534,#201535,#201536,#201537,#201538,#201539,#201540,
#201541,#201542,#201543,#201544,#201545,#201546,#201547,#201548,#201549,
#201550,#201551,#201552,#201553,#201554,#201555,#201556,#201557,#201558,
#201559,#201560,#201561,#201562,#201563,#201564,#201565,#201566,#201567,
#201568,#201569,#201570,#201571,#201572,#201573,#201574,#201575,#201576,
#201577,#201578,#201579,#201580,#201581,#201582,#201583,#201584,#201585,
#201586,#201587,#201588,#201589,#201590,#201591,#201592,#201593,#201594,
#201595,#201596,#201597,#201598,#201599,#201600,#201601,#201602,#201603,
#201604,#201605,#201606,#201607,#201608,#201609,#201610,#201611,#201612,
#201613,#201614,#201615,#201616,#201617,#201618,#201619,#201620,#201621,
#201622,#201623,#201624,#201625,#201626,#201627,#201628,#201629,#201630,
#201631,#201632,#201633,#201634,#201635,#201636,#201637,#201638,#201639,
#201640,#201641,#201642,#201643,#201644,#201645,#201646,#201647,#201648,
#201649,#201650,#201651,#201652,#201653,#201654,#201655,#201656,#201657,
#201658,#201659,#201660,#201661,#201662,#201663,#201664,#201665,#201666,
#201667,#201668,#201669,#201670,#201671,#201672,#201673,#201674,#201675,
#201676,#201677,#201678,#201679,#201680,#201681,#201682,#201683,#201684,
#201685,#201686,#201687,#201688,#201689,#201690,#201691,#201692,#201693,
#201694,#201695,#201696,#201697,#201698,#201699,#201700,#201701,#201702,
#201703,#201704,#201705,#201706,#201707,#201708,#201709,#201710,#201711,
#201712,#201713,#201714,#201715,#201716,#201717,#201718,#201719,#201720,
#201721,#201722,#201723,#201724,#201725,#201726,#201727,#201728,#201729,
#201730,#201731,#201732,#201733,#201734,#201735,#201736,#201737,#201738,
#201739,#201740,#201741,#201742,#201743,#201744,#201745,#201746,#201747,
#201748,#201749,#201750,#201751,#201752,#201753,#201754,#201755,#201756,
#201757,#201758,#201759,#201760,#201761,#201762,#201763,#201764,#201765,
#201766,#201767,#201768,#201769,#201770,#201771,#201772,#201773,#201774,
#201775,#201776,#201777,#201778,#201779,#201780,#201781,#201782,#201783,
#201784,#201785,#201786,#201787,#201788,#201789,#201790,#201791,#201792,
#201793,#201794,#201795,#201796,#201797,#201798,#201799,#201800,#201801,
#201802,#201803,#201804,#201805,#201806,#201807,#201808,#201809,#201810,
#201811,#201812,#201813,#201814,#201815,#201816,#201817,#201818,#201819,
#201820,#201821,#201822,#201823,#201824,#201825,#201826,#201827,#201828,
#201829,#201830,#201831,#201832,#201833,#201834,#201835,#201836,#201837,
#201838,#201839,#201840,#201841,#201842,#201843,#201844,#201845,#201846,
#201847,#201848,#201849,#201850,#201851,#201852,#201853,#201854,#201855,
#201856,#201857,#201858,#201859,#201860,#201861,#201862,#201863,#201864,
#201865,#201866,#201867,#201868,#201869,#201870,#201871,#201872,#201873,
#201874,#201875,#201876,#201877,#201878,#201879,#201880,#201881,#201882,
#201883,#201884,#201885,#201886,#201887,#201888,#201889,#201890,#201891,
#201892,#201893,#201894,#201895,#201896,#201897,#201898,#201899,#201900,
#201901,#201902,#201903,#201904,#201905,#201906,#201907,#201908,#201909,
#201910,#201911,#201912,#201913,#201914,#201915,#201916,#201917,#201918,
#201919,#201920,#201921,#201922,#201923,#201924,#201925,#201926,#201927,
#201928,#201929,#201930,#201931,#201932,#201933,#201934,#201935,#201936,
#201937,#201938,#201939,#201940,#201941,#201942,#201943,#201944,#201945,
#201946,#201947,#201948,#201949,#201950,#201951,#201952,#201953,#201954,
#201955,#201956,#201957,#201958,#201959,#201960,#201961,#201962,#201963,
#201964,#201965,#201966,#201967,#201968,#201969,#201970,#201971,#201972,
#201973,#201974,#201975,#201976,#201977,#201978,#201979,#201980,#201981,
#201982,#201983,#201984,#201985,#201986,#201987,#201988,#201989,#201990,
#201991,#201992,#201993,#201994,#201995,#201996,#201997,#201998,#201999,
#202000,#202001,#202002,#202003,#202004,#202005,#202006,#202007,#202008,
#202009,#202010,#202011,#202012,#202013,#202014,#202015,#202016,#202017,
#202018,#202019,#202020,#202021,#202022,#202023,#202024,#202025,#202026,
#202027,#202028,#202029,#202030,#202031,#202032,#202033,#202034,#202035,
#202036,#202037,#202038,#202039,#202040,#202041,#202042,#202043,#202044,
#202045,#202046,#202047,#202048,#202049,#202050,#202051,#202052,#202053,
#202054,#202055,#202056,#202057,#202058,#202059,#202060,#202061,#202062,
#202063,#202064,#202065,#202066,#202067,#202068,#202069,#202070,#202071,
#202072,#202073,#202074,#202075,#202076,#202077,#202078,#202079,#202080,
#202081,#202082,#202083,#202084,#202085,#202086,#202087,#202088,#202089,
#202090,#202091,#202092,#202093,#202094,#202095,#202096,#202097,#202098,
#202099,#202100,#202101,#202102,#202103,#202104,#202105,#202106,#202107,
#202108,#202109,#202110,#202111,#202112,#202113,#202114,#202115,#202116,
#202117,#202118,#202119,#202120,#202121,#202122,#202123,#202124,#202125,
#202126,#202127,#202128,#202129,#202130,#202131,#202132,#202133,#202134,
#202135,#202136,#202137,#202138,#202139,#202140,#202141,#202142,#202143,
#202144,#202145,#202146,#202147,#202148,#202149,#202150,#202151,#202152,
#202153,#202154,#202155,#202156,#202157,#202158,#202159,#202160,#202161,
#202162,#202163,#202164,#202165,#202166,#202167,#202168,#202169,#202170,
#202171,#202172,#202173,#202174,#202175,#202176,#202177,#202178,#202179,
#202180,#202181,#202182,#202183,#202184,#202185,#202186,#202187,#202188,
#202189,#202190,#202191,#202192,#202193,#202194,#202195,#202196,#202197,
#202198,#202199,#202200,#202201,#202202,#202203,#202204,#202205,#202206,
#202207,#202208,#202209,#202210,#202211,#202212,#202213,#202214,#202215,
#202216,#202217,#202218,#202219,#202220,#202221,#202222,#202223,#202224,
#202225,#202226,#202227,#202228,#202229,#202230,#202231,#202232,#202233,
#202234,#202235,#202236,#202237,#202238,#202239,#202240,#202241,#202242,
#202243,#202244,#202245,#202246,#202247,#202248,#202249,#202250,#202251,
#202252,#202253,#202254,#202255,#202256,#202257,#202258,#202259,#202260,
#202261,#202262,#202263,#202264,#202265,#202266,#202267,#202268,#202269,
#202270,#202271,#202272,#202273,#202274,#202275,#202276,#202277,#202278,
#202279,#202280,#202281,#202282,#202283,#202284,#202285,#202286,#202287,
#202288,#202289,#202290,#202291,#202292,#202293,#202294,#202295,#202296,
#202297,#202298,#202299,#202300,#202301,#202302,#202303,#202304,#202305,
#202306,#202307,#202308,#202309,#202310,#202311,#202312,#202313)),
 .UNSPECIFIED.,.F.,.F.,.F.,(4,4),(4,1,1,1,1,1,1,1,1,1,1,1,1,1,1,1,1,1,1,
1,1,1,1,1,1,1,1,1,1,1,1,1,1,1,1,1,1,1,1,1,1,1,1,1,1,1,1,1,1,1,1,1,1,1,1,
1,1,1,1,1,1,1,1,1,1,1,1,1,1,1,1,1,1,1,1,1,1,1,1,1,1,1,1,1,1,1,1,1,1,1,1,
1,1,1,1,1,1,1,1,1,1,1,1,1,1,1,1,1,1,1,1,1,1,1,1,1,1,1,1,1,1,1,1,1,1,1,1,
1,1,1,1,1,1,1,1,1,1,1,1,1,1,1,1,1,1,1,1,1,1,1,1,1,1,1,1,1,1,1,1,1,1,1,1,
1,1,1,1,1,1,1,1,1,1,1,1,1,1,1,1,1,1,1,1,1,1,1,1,1,1,1,1,1,1,1,1,1,1,1,1,
1,1,1,1,1,1,1,1,1,1,1,1,1,1,1,1,1,1,1,1,1,1,1,1,1,1,1,1,1,1,1,1,1,1,1,1,
1,1,1,1,1,1,1,1,1,1,1,1,1,1,1,1,1,1,1,1,1,1,1,1,1,1,1,1,1,1,1,1,1,1,1,1,
1,1,1,1,1,1,1,1,1,1,1,1,1,1,1,1,1,1,1,1,1,1,1,1,1,1,1,1,1,1,1,1,1,1,1,1,
1,1,1,1,1,1,1,1,1,1,1,1,1,1,1,1,1,1,1,1,1,1,1,1,1,1,1,1,1,1,1,1,1,1,1,1,
1,1,1,1,1,1,1,1,1,1,1,1,1,1,1,1,1,1,1,1,1,1,1,1,1,1,1,1,1,1,1,1,1,1,1,1,
1,1,1,1,1,1,1,1,1,1,1,1,1,1,1,1,1,1,1,1,1,1,1,1,1,1,1,1,1,1,1,1,1,1,1,1,
1,1,1,1,1,1,1,1,1,1,1,1,1,1,1,1,1,1,1,1,1,1,1,1,1,1,1,1,1,1,1,1,1,1,1,1,
1,1,1,1,1,1,1,1,1,1,1,1,1,1,1,1,1,1,1,1,1,1,1,1,1,1,1,1,1,1,1,1,1,1,1,1,
1,1,1,1,1,1,1,1,1,1,1,1,1,1,1,1,1,1,1,1,1,1,1,1,1,1,1,1,1,1,1,1,1,1,1,1,
1,1,1,1,1,1,1,1,1,1,1,1,1,1,1,1,1,1,1,1,1,1,1,1,1,1,1,1,1,1,1,1,1,1,1,1,
1,1,1,1,1,1,1,1,1,1,1,1,1,1,1,1,1,1,1,1,1,1,1,1,1,1,1,1,1,1,1,1,1,1,1,1,
1,1,1,1,1,1,1,1,1,1,1,1,1,1,1,1,1,1,1,1,1,1,1,1,1,1,1,1,1,1,1,1,1,1,1,1,
1,1,1,1,1,1,1,1,1,1,1,1,1,1,1,1,1,1,1,1,1,1,1,1,1,1,1,1,1,1,1,1,1,1,1,1,
1,1,1,1,1,1,1,1,1,1,1,1,1,1,1,1,1,1,1,1,1,1,1,1,1,1,1,1,1,1,1,1,1,1,1,1,
1,1,1,1,1,1,1,1,1,1,1,1,1,1,1,1,1,1,1,1,1,1,1,1,1,1,1,1,1,1,1,1,1,1,1,1,
1,1,1,1,1,1,1,1,1,1,1,1,1,1,1,1,1,1,1,1,1,1,1,1,1,1,1,1,1,1,1,1,1,1,1,1,
1,1,1,1,1,1,1,1,1,1,1,1,1,1,1,1,1,1,1,1,1,1,1,1,1,1,1,1,1,1,1,1,1,1,1,1,
1,1,1,1,1,1,1,1,1,1,1,1,1,1,1,1,1,1,1,1,1,1,1,1,1,1,1,1,1,1,1,1,1,1,1,1,
1,1,1,1,1,1,1,1,1,1,1,1,1,1,1,1,1,1,1,1,1,1,1,1,1,1,1,1,1,1,1,1,1,1,1,1,
1,1,1,1,1,1,1,1,1,1,1,1,1,1,1,1,1,1,1,1,1,1,1,1,1,1,1,1,1,1,1,1,1,1,1,1,
1,1,1,1,1,1,1,1,1,1,1,1,1,1,1,1,1,1,1,1,1,1,1,1,1,1,1,1,1,1,1,1,1,1,1,1,
1,1,1,1,1,1,1,1,1,1,1,1,1,1,1,1,1,1,1,1,1,1,1,1,1,1,1,1,1,1,1,1,1,1,1,1,
1,1,1,1,1,1,1,1,1,1,1,1,1,1,1,1,1,1,1,1,1,1,1,1,1,1,1,1,1,1,1,1,1,1,1,1,
1,1,1,1,1,1,1,1,1,1,1,1,1,1,1,1,1,1,1,1,1,1,1,1,1,1,1,1,1,1,1,1,1,1,1,1,
1,1,1,1,1,1,1,1,1,1,1,1,1,1,1,1,1,1,1,1,1,1,1,1,1,1,1,1,1,1,1,1,1,1,1,1,
1,1,1,1,1,1,1,1,1,1,1,1,1,1,1,1,1,1,1,1,1,1,1,1,1,1,1,1,1,1,1,1,1,1,1,1,
1,1,1,1,1,1,1,1,1,1,1,1,1,1,1,1,1,1,1,1,1,1,1,1,1,1,1,1,1,1,1,1,1,1,1,1,
1,1,1,1,1,1,1,1,1,1,1,1,1,1,1,1,1,1,1,1,1,1,1,1,1,1,1,1,1,1,1,1,1,1,1,1,
1,1,1,1,1,1,1,1,1,1,1,1,1,1,1,1,1,1,1,1,1,1,1,1,1,1,1,1,1,1,1,1,1,1,1,1,
1,1,1,1,1,1,1,1,1,1,1,1,1,1,1,1,1,1,1,1,1,1,1,1,1,1,1,1,1,1,1,1,1,1,1,1,
1,1,1,1,1,1,1,1,1,1,1,1,1,1,1,1,1,1,1,1,1,1,1,1,1,1,1,1,1,1,1,1,1,1,1,1,
1,1,1,1,1,1,1,1,1,1,1,1,1,1,1,1,1,1,1,1,1,1,1,1,1,1,1,1,1,1,1,1,1,1,1,1,
1,1,1,1,1,1,1,1,1,1,1,1,1,1,1,1,1,1,1,1,1,1,1,1,1,1,1,1,1,1,1,1,1,1,1,1,
1,1,1,1,1,1,1,1,1,1,1,1,1,1,1,1,1,1,1,1,1,1,1,1,1,1,1,1,1,1,1,1,1,1,1,1,
1,1,1,1,1,1,1,1,1,1,1,1,1,1,1,1,1,1,1,1,1,1,1,1,1,1,1,1,1,1,1,1,1,1,1,1,
1,1,1,1,1,1,1,1,1,1,1,1,1,1,1,1,1,1,1,1,1,1,1,1,1,1,1,1,1,1,1,1,1,1,1,1,
1,1,1,1,1,1,1,1,1,1,1,1,1,1,1,1,1,1,1,1,1,1,1,1,1,1,1,1,1,1,1,1,1,1,1,1,
1,1,1,1,1,1,1,1,1,1,1,1,1,1,1,1,1,1,1,1,1,1,1,1,1,1,1,1,1,1,1,1,1,1,1,1,
1,1,1,1,1,1,1,1,1,1,1,1,1,1,1,1,1,1,1,1,1,1,1,1,1,1,1,1,1,1,1,1,1,1,1,1,
1,1,1,1,1,1,1,1,1,1,1,1,1,1,1,1,1,1,1,1,1,1,1,1,1,1,1,1,1,1,1,1,1,1,1,1,
1,1,1,1,1,1,1,1,1,1,1,1,1,1,1,1,1,1,1,1,1,1,1,1,1,1,1,1,1,1,1,1,1,1,1,1,
1,1,1,1,1,1,1,1,1,1,1,1,1,1,1,1,1,4),(-0.000423095957202541,0.115881565465356),
(11.6153146011728,12.1152895244478,12.6151575298078,13.614893540528,14.6146295512481,
15.6143655619682,16.6141015726884,17.6138375834085,18.6135735941286,19.6133096048488,
20.6130456155689,21.612781626289,22.6125176370092,23.6122536477293,24.6119896584494,
25.6117256691696,26.6114616798897,27.6111976906098,28.6109337013299,29.6106697120501,
30.6104057227702,31.6101417334903,32.6098777442105,33.6096137549306,34.6093497656507,
35.6090857763709,36.608821787091,37.6085577978111,38.6082938085313,39.6080298192514,
40.6077658299715,41.6075018406916,42.6072378514118,43.6069738621319,44.606709872852,
45.6064458835722,46.6061818942923,47.6059179050124,48.6056539157326,49.6053899264527,
50.6051259371728,51.604861947893,52.6045979586131,53.6043339693332,54.6040699800534,
55.6038059907735,56.6035420014936,57.6032780122137,58.6030140229339,59.602750033654,
60.6024860443741,61.6022220550943,62.6019580658144,63.6016940765345,64.6014300872547,
65.6011660979748,66.6009021086949,67.6006381194151,68.6003741301352,69.6001101408553,
70.5998461515754,71.5995821622956,72.5993181730157,73.5990541837358,74.598790194456,
75.5985262051761,76.5982622158962,77.5979982266164,78.5977342373365,79.5974702480566,
80.5972062587768,81.5969422694969,82.596678280217,83.5964142909372,84.5961503016573,
85.5958863123774,86.5956223230975,87.5953583338177,88.5950943445378,89.5948303552579,
90.5945663659781,91.5943023766982,92.5940383874183,93.5937743981385,94.5935104088586,
95.5932464195787,96.5929824302989,97.592718441019,98.5924544517391,99.5921904624593,
100.591926473179,101.5916624839,102.59139849462,103.59113450534,104.59087051606,
105.59060652678,106.5903425375,107.59007854822,108.58981455894,109.589550569661,
110.589286580381,111.589022591101,112.588758601821,113.588494612541,114.588230623261,
115.587966633981,116.587702644701,117.587438655422,118.587174666142,119.586910676862,
120.586646687582,121.586382698302,122.586118709022,123.585854719742,124.585590730463,
125.585326741183,126.585062751903,127.584798762623,128.584534773343,129.584270784063,
130.584006794783,131.583742805503,132.583478816224,133.583214826944,134.582950837664,
135.582686848384,136.582422859104,137.582158869824,138.581894880544,139.581630891264,
140.581366901985,141.581102912705,142.580838923425,143.580574934145,144.580310944865,
145.580046955585,146.579782966305,147.579518977026,148.579254987746,149.578990998466,
150.578727009186,151.578463019906,152.578199030626,153.577935041346,154.577671052066,
155.577407062787,156.577143073507,157.576879084227,158.576615094947,159.576351105667,
160.576087116387,161.575823127107,162.575559137827,163.575295148548,164.575031159268,
165.574767169988,166.574503180708,167.574239191428,168.573975202148,169.573711212868,
170.573447223589,171.573183234309,172.572919245029,173.572655255749,174.572391266469,
175.572127277189,176.571863287909,177.571599298629,178.57133530935,179.57107132007,
180.57080733079,181.57054334151,182.57027935223,183.57001536295,184.56975137367,
185.56948738439,186.569223395111,187.568959405831,188.568695416551,189.568431427271,
190.568167437991,191.567903448711,192.567639459431,193.567375470152,194.567111480872,
195.566847491592,196.566583502312,197.566319513032,198.566055523752,199.565791534472,
200.565527545192,201.565263555913,202.564999566633,203.564735577353,204.564471588073,
205.564207598793,206.563943609513,207.563679620233,208.563415630954,209.563151641674,
210.562887652394,211.562623663114,212.562359673834,213.562095684554,214.561831695274,
215.561567705994,216.561303716715,217.561039727435,218.560775738155,219.560511748875,
220.560247759595,221.559983770315,222.559719781035,223.559455791755,224.559191802476,
225.558927813196,226.558663823916,227.558399834636,228.558135845356,229.557871856076,
230.557607866796,231.557343877517,232.557079888237,233.556815898957,234.556551909677,
235.556287920397,236.556023931117,237.555759941837,238.555495952557,239.555231963278,
240.554967973998,241.554703984718,242.554439995438,243.554176006158,244.553912016878,
245.553648027598,246.553384038319,247.553120049039,248.552856059759,249.552592070479,
250.552328081199,251.552064091919,252.551800102639,253.551536113359,254.55127212408,
255.5510081348,256.55074414552,257.55048015624,258.55021616696,259.54995217768,
260.5496881884,261.54942419912,262.549160209841,263.548896220561,264.548632231281,
265.548368242001,266.548104252721,267.547840263441,268.547576274161,269.547312284882,
270.547048295602,271.546784306322,272.546520317042,273.546256327762,274.545992338482,
275.545728349202,276.545464359922,277.545200370643,278.544936381363,279.544672392083,
280.544408402803,281.544144413523,282.543880424243,283.543616434963,284.543352445683,
285.543088456404,286.542824467124,287.542560477844,288.542296488564,289.542032499284,
290.541768510004,291.541504520724,292.541240531445,293.540976542165,294.540712552885,
295.540448563605,296.540184574325,297.539920585045,298.539656595765,299.539392606485,
300.539128617206,301.538864627926,302.538600638646,303.538336649366,304.538072660086,
305.537808670806,306.537544681526,307.537280692246,308.537016702967,309.536752713687,
310.536488724407,311.536224735127,312.535960745847,313.535696756567,314.535432767287,
315.535168778008,316.534904788728,317.534640799448,318.534376810168,319.534112820888,
320.533848831608,321.533584842328,322.533320853048,323.533056863769,324.532792874489,
325.532528885209,326.532264895929,327.532000906649,328.531736917369,329.531472928089,
330.53120893881,331.53094494953,332.53068096025,333.53041697097,334.53015298169,
335.52988899241,336.52962500313,337.52936101385,338.529097024571,339.528833035291,
340.528569046011,341.528305056731,342.528041067451,343.527777078171,344.527513088891,
345.527249099611,346.526985110332,347.526721121052,348.526457131772,349.526193142492,
350.525929153212,351.525665163932,352.525401174652,353.525137185373,354.524873196093,
355.524609206813,356.524345217533,357.524081228253,358.523817238973,359.523553249693,
360.523289260413,361.523025271134,362.522761281854,363.522497292574,364.522233303294,
365.521969314014,366.521705324734,367.521441335454,368.521177346175,369.520913356895,
370.520649367615,371.520385378335,372.520121389055,373.519857399775,374.519593410495,
375.519329421215,376.519065431936,377.518801442656,378.518537453376,379.518273464096,
380.518009474816,381.517745485536,382.517481496256,383.517217506976,384.516953517697,
385.516689528417,386.516425539137,387.516161549857,388.515897560577,389.515633571297,
390.515369582017,391.515105592737,392.514841603458,393.514577614178,394.514313624898,
395.514049635618,396.513785646338,397.513521657058,398.513257667778,399.512993678499,
400.512729689219,401.512465699939,402.512201710659,403.511937721379,404.511673732099,
405.511409742819,406.511145753539,407.51088176426,408.51061777498,409.5103537857,
410.51008979642,411.50982580714,412.50956181786,413.50929782858,414.509033839301,
415.508769850021,416.508505860741,417.508241871461,418.507977882181,419.507713892901,
420.507449903621,421.507185914341,422.506921925062,423.506657935782,424.506393946502,
425.506129957222,426.505865967942,427.505601978662,428.505337989382,429.505074000102,
430.504810010823,431.504546021543,432.504282032263,433.504018042983,434.503754053703,
435.503490064423,436.503226075143,437.502962085864,438.502698096584,439.502434107304,
440.502170118024,441.501906128744,442.501642139464,443.501378150184,444.501114160904,
445.500850171625,446.500586182345,447.500322193065,448.500058203785,449.499794214505,
450.499530225225,451.499266235945,452.499002246665,453.498738257386,454.498474268106,
455.498210278826,456.497946289546,457.497682300266,458.497418310986,459.497154321706,
460.496890332427,461.496626343147,462.496362353867,463.496098364587,464.495834375307,
465.495570386027,466.495306396747,467.495042407467,468.494778418188,469.494514428908,
470.494250439628,471.493986450348,472.493722461068,473.493458471788,474.493194482508,
475.492930493229,476.492666503949,477.492402514669,478.492138525389,479.491874536109,
480.491610546829,481.491346557549,482.491082568269,483.49081857899,484.49055458971,
485.49029060043,486.49002661115,487.48976262187,488.48949863259,489.48923464331,
490.48897065403,491.488706664751,492.488442675471,493.488178686191,494.487914696911,
495.487650707631,496.487386718351,497.487122729071,498.486858739792,499.486594750512,
500.486330761232,501.486066771952,502.485802782672,503.485538793392,504.485274804112,
505.485010814832,506.484746825553,507.484482836273,508.484218846993,509.483954857713,
510.483690868433,511.483426879153,512.483162889873,513.482898900594,514.482634911314,
515.482370922034,516.482106932754,517.481842943474,518.481578954194,519.481314964914,
520.481050975635,521.480786986355,522.480522997075,523.480259007795,524.479995018515,
525.479731029235,526.479467039955,527.479203050675,528.478939061396,529.478675072116,
530.478411082836,531.478147093556,532.477883104276,533.477619114996,534.477355125716,
535.477091136436,536.476827147157,537.476563157877,538.476299168597,539.476035179317,
540.475771190037,541.475507200757,542.475243211477,543.474979222197,544.474715232918,
545.474451243638,546.474187254358,547.473923265078,548.473659275798,549.473395286518,
550.473131297238,551.472867307958,552.472603318679,553.472339329399,554.472075340119,
555.471811350839,556.471547361559,557.471283372279,558.471019382999,559.47075539372,
560.47049140444,561.47022741516,562.46996342588,563.4696994366,564.46943544732,
565.46917145804,566.46890746876,567.468643479481,568.468379490201,569.468115500921,
570.467851511641,571.467587522361,572.467323533081,573.467059543801,574.466795554521,
575.466531565242,576.466267575962,577.466003586682,578.465739597402,579.465475608122,
580.465211618842,581.464947629562,582.464683640283,583.464419651003,584.464155661723,
585.463891672443,586.463627683163,587.463363693883,588.463099704603,589.462835715323,
590.462571726044,591.462307736764,592.462043747484,593.461779758204,594.461515768924,
595.461251779644,596.460987790364,597.460723801085,598.460459811805,599.460195822525,
600.459931833245,601.459667843965,602.459403854685,603.459139865405,604.458875876125,
605.458611886846,606.458347897566,607.458083908286,608.457819919006,609.457555929726,
610.457291940446,611.457027951166,612.456763961887,613.456499972607,614.456235983327,
615.455971994047,616.455708004767,617.455444015487,618.455180026207,619.454916036927,
620.454652047648,621.454388058368,622.454124069088,623.453860079808,624.453596090528,
625.453332101248,626.453068111968,627.452804122688,628.452540133409,629.452276144129,
630.452012154849,631.451748165569,632.451484176289,633.451220187009,634.450956197729,
635.450692208449,636.45042821917,637.45016422989,638.44990024061,639.44963625133,
640.44937226205,641.44910827277,642.44884428349,643.448580294211,644.448316304931,
645.448052315651,646.447788326371,647.447524337091,648.447260347811,649.446996358531,
650.446732369251,651.446468379972,652.446204390692,653.445940401412,654.445676412132,
655.445412422852,656.445148433572,657.444884444292,658.444620455012,659.444356465733,
660.444092476453,661.443828487173,662.443564497893,663.443300508613,664.443036519333,
665.442772530053,666.442508540774,667.442244551494,668.441980562214,669.441716572934,
670.441452583654,671.441188594374,672.440924605094,673.440660615815,674.440396626535,
675.440132637255,676.439868647975,677.439604658695,678.439340669415,679.439076680135,
680.438812690855,681.438548701576,682.438284712296,683.438020723016,684.437756733736,
685.437492744456,686.437228755176,687.436964765896,688.436700776616,689.436436787337,
690.436172798057,691.435908808777,692.435644819497,693.435380830217,694.435116840937,
695.434852851657,696.434588862377,697.434324873098,698.434060883818,699.433796894538,
700.433532905258,701.433268915978,702.433004926698,703.432740937418,704.432476948139,
705.432212958859,706.431948969579,707.431684980299,708.431420991019,709.431157001739,
710.430893012459,711.430629023179,712.4303650339,713.43010104462,714.42983705534,
715.42957306606,716.42930907678,717.4290450875,718.42878109822,719.42851710894,
720.428253119661,721.427989130381,722.427725141101,723.427461151821,724.427197162541,
725.426933173261,726.426669183981,727.426405194702,728.426141205422,729.425877216142,
730.425613226862,731.425349237582,732.425085248302,733.424821259022,734.424557269742,
735.424293280463,736.424029291183,737.423765301903,738.423501312623,739.423237323343,
740.422973334063,741.422709344783,742.422445355504,743.422181366224,744.421917376944,
745.421653387664,746.421389398384,747.421125409104,748.420861419824,749.420597430544,
750.420333441265,751.420069451985,752.419805462705,753.419541473425,754.419277484145,
755.419013494865,756.418749505585,757.418485516306,758.418221527026,759.417957537746,
760.417693548466,761.417429559186,762.417165569906,763.416901580626,764.416637591346,
765.416373602067,766.416109612787,767.415845623507,768.415581634227,769.415317644947,
770.415053655667,771.414789666387,772.414525677107,773.414261687828,774.413997698548,
775.413733709268,776.413469719988,777.413205730708,778.412941741428,779.412677752148,
780.412413762868,781.412149773589,782.411885784309,783.411621795029,784.411357805749,
785.411093816469,786.410829827189,787.410565837909,788.41030184863,789.41003785935,
790.40977387007,791.40950988079,792.40924589151,793.40898190223,794.40871791295,
795.40845392367,796.408189934391,797.407925945111,798.407661955831,799.407397966551,
800.407133977271,801.406869987991,802.406605998711,803.406342009432,804.406078020152,
805.405814030872,806.405550041592,807.405286052312,808.405022063032,809.404758073752,
810.404494084472,811.404230095193,812.403966105913,813.403702116633,814.403438127353,
815.403174138073,816.402910148793,817.402646159513,818.402382170234,819.402118180954,
820.401854191674,821.401590202394,822.401326213114,823.401062223834,824.400798234554,
825.400534245274,826.400270255995,827.400006266715,828.399742277435,829.399478288155,
830.399214298875,831.398950309595,832.398686320315,833.398422331035,834.398158341756,
835.397894352476,836.397630363196,837.397366373916,838.397102384636,839.396838395356,
840.396574406076,841.396310416796,842.396046427517,843.395782438237,844.395518448957,
845.395254459677,846.394990470397,847.394726481117,848.394462491837,849.394198502558,
850.393934513278,851.393670523998,852.393406534718,853.393142545438,854.392878556158,
855.392614566878,856.392350577598,857.392086588319,858.391822599039,859.391558609759,
860.391294620479,861.391030631199,862.390766641919,863.390502652639,864.390238663359,
865.38997467408,866.3897106848,867.38944669552,868.38918270624,869.38891871696,
870.38865472768,871.3883907384,872.388126749121,873.387862759841,874.387598770561,
875.387334781281,876.387070792001,877.386806802721,878.386542813441,879.386278824161,
880.386014834882,881.385750845602,882.385486856322,883.385222867042,884.384958877762,
885.384694888482,886.384430899202,887.384166909923,888.383902920643,889.383638931363,
890.383374942083,891.383110952803,892.382846963523,893.382582974243,894.382318984963,
895.382054995684,896.381791006404,897.381527017124,898.381263027844,899.380999038564,
900.380735049284,901.380471060004,902.380207070725,903.379943081445,904.379679092165,
905.379415102885,906.379151113605,907.378887124325,908.378623135045,909.378359145765,
910.378095156486,911.377831167206,912.377567177926,913.377303188646,914.377039199366,
915.376775210086,916.376511220806,917.376247231526,918.375983242247,919.375719252967,
920.375455263687,921.375191274407,922.374927285127,923.374663295847,924.374399306567,
925.374135317287,926.373871328008,927.373607338728,928.373343349448,929.373079360168,
930.372815370888,931.372551381608,932.372287392328,933.372023403049,934.371759413769,
935.371495424489,936.371231435209,937.370967445929,938.370703456649,939.370439467369,
940.370175478089,941.36991148881,942.36964749953,943.36938351025,944.36911952097,
945.36885553169,946.36859154241,947.36832755313,948.368063563851,949.367799574571,
950.367535585291,951.367271596011,952.367007606731,953.366743617451,954.366479628171,
955.366215638891,956.365951649612,957.365687660332,958.365423671052,959.365159681772,
960.364895692492,961.364631703212,962.364367713932,963.364103724653,964.363839735373,
965.363575746093,966.363311756813,967.363047767533,968.362783778253,969.362519788973,
970.362255799693,971.361991810414,972.361727821134,973.361463831854,974.361199842574,
975.360935853294,976.360671864014,977.360407874734,978.360143885454,979.359879896175,
980.359615906895,981.359351917615,982.359087928335,983.358823939055,984.358559949775,
985.358295960495,986.358031971215,987.357767981936,988.357503992656,989.357240003376,
990.356976014096,991.356712024816,992.356448035536,993.356184046256,994.355920056977,
995.355656067697,996.355392078417,997.355128089137,998.354864099857,999.354600110577,
1000.3543361213,1001.35407213202,1002.35380814274,1003.35354415346,1004.35328016418,
1005.3530161749,1006.35275218562,1007.35248819634,1008.35222420706,1009.35196021778,
1010.3516962285,1011.35143223922,1012.35116824994,1013.35090426066,1014.35064027138,
1015.3503762821,1016.35011229282,1017.34984830354,1018.34958431426,1019.34932032498,
1020.3490563357,1021.34879234642,1022.34852835714,1023.34826436786,1024.34800037858,
1025.3477363893,1026.34747240002,1027.34720841074,1028.34694442146,1029.34668043218,
1030.3464164429,1031.34615245362,1032.34588846434,1033.34562447506,1034.34536048578,
1035.3450964965,1036.34483250722,1037.34456851794,1038.34430452866,1039.34404053938,
1040.3437765501,1041.34351256082,1042.34324857154,1043.34298458226,1044.34272059298,
1045.3424566037,1046.34219261442,1047.34192862514,1048.34166463586,1049.34140064658,
1050.3411366573,1051.34087266802,1052.34060867874,1053.34034468946,1054.34008070018,
1055.3398167109,1056.33955272162,1057.33928873234,1058.33902474307,1059.33876075378,
1060.33849676451,1061.33823277523,1062.33796878595,1063.33770479667,1064.33744080739,
1065.33717681811,1066.33691282883,1067.33664883955,1068.33638485027,1069.33612086099,
1070.33585687171,1071.33559288243,1072.33532889315,1073.33506490387,1074.33480091459,
1075.33453692531,1076.33427293603,1077.33400894675,1078.33374495747,1079.33348096819,
1080.33321697891,1081.33295298963,1082.33268900035,1083.33242501107,1084.33216102179,
1085.33189703251,1086.33163304323,1087.33136905395,1088.33110506467,1089.33084107539,
1090.33057708611,1091.33031309683,1092.33004910755,1093.32978511827,1094.32952112899,
1095.32925713971,1096.32899315043,1097.32872916115,1098.32846517187,1099.32820118259,
1100.32793719331,1101.32767320403,1102.32740921475,1103.32714522547,1104.32688123619,
1105.32661724691,1106.32635325763,1107.32608926835,1108.32582527907,1109.32556128979,
1110.32529730051,1111.32503331123,1112.32476932195,1113.32450533267,1114.32424134339,
1115.32397735411,1116.32371336483,1117.32344937555,1118.32318538627,1119.32292139699,
1120.32265740771,1121.32239341843,1122.32212942915,1123.32186543987,1124.32160145059,
1125.32133746131,1126.32107347203,1127.32080948275,1128.32054549347,1129.32028150419,
1130.32001751491,1131.31975352563,1132.31948953635,1133.31922554707,1134.31896155779,
1135.31869756852,1136.31843357924,1137.31816958996,1138.31790560068,1139.3176416114,
1140.31737762212,1141.31711363284,1142.31684964356,1143.31658565428,1144.316321665,
1145.31605767572,1146.31579368644,1147.31552969716,1148.31526570788,1149.3150017186,
1150.31473772932,1151.31447374004,1152.31420975076,1153.31394576148,1154.3136817722,
1155.31341778292,1156.31315379364,1157.31288980436,1158.31262581508,1159.3123618258,
1160.31209783652,1161.31183384724,1162.31156985796,1163.31130586868,1164.3110418794,
1165.31077789012,1166.31051390084,1167.31024991156,1168.30998592228,1169.309721933,
1170.30945794372,1171.30919395444,1172.30892996516,1173.30866597588,1174.3084019866,
1175.30813799732,1176.30787400804,1177.30761001876,1178.30734602948,1179.3070820402,
1180.30681805092,1181.30655406164,1182.30629007236,1183.30602608308,1184.3057620938,
1185.30549810452,1186.30523411524,1187.30497012596,1188.30470613668,1189.3044421474,
1190.30417815812,1191.30391416884,1192.30365017956,1193.30338619028,1194.303122201,
1195.30285821172,1196.30259422244,1197.30233023316,1198.30206624388,1199.3018022546,
1200.30153826532,1201.30127427604,1202.30101028676,1203.30074629748,1204.3004823082,
1205.30021831892,1206.29995432964,1207.29969034036,1208.29942635108,1209.2991623618,
1210.29889837252,1211.29863438324,1212.29837039397,1213.29810640469,1214.29784241541,
1215.29757842613,1216.29731443685,1217.29705044757,1218.29678645829,1219.29652246901,
1220.29625847973,1221.29599449045,1222.29573050117,1223.29546651189,1224.29520252261,
1225.29493853333,1226.29467454405,1227.29441055477,1228.29414656549,1229.29388257621,
1230.29361858693,1231.29335459765,1232.29309060837,1233.29282661909,1234.29256262981,
1235.29229864053,1236.29203465125,1237.29177066197,1238.29150667269,1239.29124268341,
1240.29097869413,1241.29071470485,1242.29045071557,1243.29018672629,1244.28992273701,
1245.28965874773,1246.28939475845,1247.28913076917,1248.28886677989,1249.28860279061,
1250.28833880133,1251.28807481205,1252.28781082277,1253.28754683349,1254.28728284421,
1255.28701885493,1256.28675486565,1257.28649087637,1258.28622688709,1259.28596289781,
1260.28569890853,1261.28543491925,1262.28517092997,1263.28490694069,1264.28464295141,
1265.28437896213,1266.28411497285,1267.28385098357,1268.28358699429,1269.28332300501,
1270.28305901573,1271.28279502645,1272.28253103717,1273.28226704789,1274.28200305861,
1275.28173906933,1276.28147508005,1277.28121109077,1278.28094710149,1279.28068311221,
1280.28041912293,1281.28015513365,1282.27989114437,1283.27962715509,1284.27936316581,
1285.27909917653,1286.27883518725,1287.27857119797,1288.2783072087,1289.27804321942,
1290.27777923014,1291.27751524086,1292.27725125158,1293.2769872623,1294.27672327302,
1295.27645928374,1296.27619529446,1297.27593130518,1298.2756673159,1299.27540332662,
1300.27513933734,1301.27487534806,1302.27461135878,1303.2743473695,1304.27408338022,
1305.27381939094,1306.27355540166,1307.27329141238,1308.2730274231,1309.27276343382,
1310.27249944454,1311.27223545526,1312.27197146598,1313.2717074767,1314.27144348742,
1315.27117949814,1316.27091550886,1317.27065151958,1318.2703875303,1319.27012354102,
1320.26985955174,1321.26959556246,1322.26933157318,1323.2690675839,1324.26880359462,
1325.26853960534,1326.26827561606,1327.26801162678,1328.2677476375,1329.26748364822,
1330.26721965894,1331.26695566966,1332.26669168038,1333.2664276911,1334.26616370182,
1335.26589971254,1336.26563572326,1337.26537173398,1338.2651077447,1339.26484375542,
1340.26457976614,1341.26431577686,1342.26405178758,1343.2637877983,1344.26352380902,
1345.26325981974,1346.26299583046,1347.26273184118,1348.2624678519,1349.26220386262,
1350.26193987334,1351.26167588406,1352.26141189478,1353.2611479055,1354.26088391622,
1355.26061992694,1356.26035593766,1357.26009194838,1358.2598279591,1359.25956396982,
1360.25929998054,1361.25903599126,1362.25877200198,1363.2585080127,1364.25824402343,
1365.25798003415,1366.25771604487,1367.25745205559,1368.25718806631,1369.25692407703,
1370.25666008775,1371.25639609847,1372.25613210919,1373.25586811991,1374.25560413063,
1375.25534014135,1376.25507615207,1377.25481216279,1378.25454817351,1379.25428418423,
1380.25402019495,1381.25375620567,1382.25349221639,1383.25322822711,1384.25296423783,
1385.25270024855,1386.25243625927,1387.25217226999,1388.25190828071,1389.25164429143,
1390.25138030215,1391.25111631287,1392.25085232359,1393.25058833431,1394.25032434503,
1395.25006035575,1396.24979636647,1397.24953237719,1398.24926838791,1399.24900439863,
1400.24874040935,1401.24847642007,1402.24821243079,1403.24794844151,1404.24768445223,
1405.24742046295,1406.24715647367,1407.24689248439,1408.24662849511,1409.24636450583,
1410.24610051655,1411.24583652727,1412.24557253799,1413.24530854871,1414.24504455943,
1415.24478057015,1416.24451658087,1417.24425259159,1418.24398860231,1419.24372461303,
1420.24346062375,1421.24319663447,1422.24293264519,1423.24266865591,1424.24240466663,
1425.24214067735,1426.24187668807,1427.24161269879,1428.24134870951,1429.24108472023,
1430.24082073095,1431.24055674167,1432.24029275239,1433.24002876311,1434.23976477383,
1435.23950078455,1436.23923679527,1437.23897280599,1438.23870881671,1439.23844482743,
1440.23818083815,1441.23791684888,1442.2376528596,1443.23738887032,1444.23712488104,
1445.23686089176,1446.23659690248,1447.2363329132,1448.23606892392,1449.23580493464,
1450.23554094536,1451.23527695608,1452.2350129668,1453.23474897752,1454.23448498824,
1455.23422099896,1456.23395700968,1457.2336930204,1458.23342903112,1459.23316504184,
1460.23290105256,1461.23263706328,1462.232373074,1463.23210908472,1464.23184509544,
1465.23158110616,1466.23131711688,1467.2310531276,1468.23078913832,1469.23052514904,
1470.23026115976,1471.22999717048,1472.2297331812,1473.22946919192,1474.22920520264,
1475.22894121336,1476.22867722408,1477.2284132348,1478.22814924552,1479.22788525624,
1480.22762126696,1481.22735727768,1482.2270932884,1483.22682929912,1484.22656530984,
1485.22630132056,1486.22603733128,1487.225773342,1488.22550935272,1489.22524536344,
1490.22498137416,1491.22471738488,1492.2244533956,1493.22418940632,1494.22392541704,
1495.22366142776,1496.22339743848,1497.2231334492,1498.22286945992,1499.22260547064,
1500.22234148136,1501.22207749208,1502.2218135028,1503.22154951352,1504.22128552424,
1505.22102153496,1506.22075754568,1507.2204935564,1508.22022956712,1509.21996557784,
1510.21970158856,1511.21943759928,1512.21917361,1513.21890962072,1514.21864563144,
1515.21838164216,1516.21811765288,1517.21785366361,1518.21758967433,1519.21732568505,
1520.21706169577,1521.21679770649,1522.21653371721,1523.21626972793,1524.21600573865,
1525.21574174937,1526.21547776009,1527.21521377081,1528.21494978153,1529.21468579225,
1530.21442180297,1531.21415781369,1532.21389382441,1533.21362983513,1534.21336584585,
1535.21310185657,1536.21283786729,1537.21257387801,1538.21230988873,1539.21204589945,
1540.21178191017,1541.21151792089,1542.21125393161,1543.21098994233,1544.21072595305,
1545.21046196377,1546.21019797449,1547.20993398521,1548.20966999593,1549.20940600665,
1550.20914201737,1551.20887802809,1552.20861403881,1553.20835004953,1554.20808606025,
1555.20782207097,1556.20755808169,1557.20729409241,1558.20703010313,1559.20676611385,
1560.20650212457,1561.20623813529,1562.20597414601,1563.20571015673,1564.20544616745,
1565.20518217817,1566.20491818889,1567.20465419961,1568.20439021033,1569.20412622105,
1570.20386223177,1571.20359824249,1572.20333425321,1573.20307026393,1574.20280627465,
1575.20254228537,1576.20227829609,1577.20201430681,1578.20175031753,1579.20148632825,
1580.20122233897,1581.20095834969,1582.20069436041,1583.20043037113,1584.20016638185,
1585.19990239257,1586.19963840329,1587.19937441401,1588.19911042473,1589.19884643545,
1590.19858244617,1591.19831845689,1592.19805446761,1593.19779047834,1594.19752648906,
1595.19726249978,1596.1969985105,1597.19673452122,1598.19647053194,1599.19620654266,
1600.19594255338,1601.1956785641,1602.19541457482,1603.19515058554,1604.19488659626,
1605.19462260698,1606.1943586177,1607.19409462842,1608.19383063914,1609.19356664986,
1610.19330266058,1611.1930386713,1612.19277468202,1613.19251069274,1614.19224670346,
1615.19198271418,1616.1917187249,1617.19145473562,1618.19119074634,1619.19092675706,
1620.19066276778,1621.1903987785,1622.19013478922,1623.18987079994,1624.18960681066,
1625.18934282138,1626.1890788321,1627.18881484282,1628.18855085354,1629.18828686426,
1630.18802287498,1631.1877588857,1632.18749489642,1633.18723090714,1634.18696691786,
1635.18670292858,1636.1864389393,1637.18617495002,1638.18591096074,1639.18564697146,
1640.18538298218,1641.1851189929,1642.18485500362,1643.18459101434,1644.18432702506,
1645.18406303578,1646.1837990465,1647.18353505722,1648.18327106794,1649.18300707866,
1650.18274308938,1651.1824791001,1652.18221511082,1653.18195112154,1654.18168713226,
1655.18142314298,1656.1811591537,1657.18089516442,1658.18063117514,1659.18036718586,
1660.18010319658,1661.1798392073,1662.17957521802,1663.17931122874,1664.17904723946,
1665.17878325018,1666.1785192609,1667.17825527162,1668.17799128234,1669.17772729307,
1670.17746330379,1671.17719931451,1672.17693532523,1673.17667133595,1674.17640734667,
1675.17614335739,1676.17587936811,1677.17561537883,1678.17535138955,1679.17508740027,
1680.17482341099,1681.17455942171,1682.17429543243,1683.17403144315,1684.17376745387,
1685.17350346459,1686.17323947531,1687.17297548603,1688.17271149675,1689.17244750747,
1690.17218351819,1691.17191952891,1692.17165553963,1693.17139155035,1694.17112756107,
1695.17086357179,1696.17059958251,1697.17033559323,1698.17007160395,1699.16980761467,
1700.16954362539,1700.66941163075,1701.16959429301),.UNSPECIFIED.);
#57=B_SPLINE_CURVE_WITH_KNOTS('',3,(#17635,#17636,#17637,#17638,#17639,
#17640,#17641,#17642,#17643,#17644,#17645,#17646,#17647,#17648,#17649,#17650,
#17651,#17652,#17653,#17654,#17655,#17656,#17657,#17658,#17659,#17660,#17661,
#17662,#17663,#17664,#17665,#17666,#17667,#17668,#17669,#17670,#17671,#17672,
#17673,#17674,#17675,#17676,#17677,#17678,#17679,#17680,#17681,#17682,#17683,
#17684,#17685,#17686,#17687,#17688,#17689,#17690,#17691,#17692,#17693,#17694,
#17695,#17696,#17697,#17698,#17699,#17700,#17701,#17702,#17703,#17704,#17705,
#17706,#17707,#17708,#17709,#17710,#17711,#17712,#17713,#17714,#17715,#17716,
#17717,#17718,#17719,#17720,#17721,#17722,#17723,#17724,#17725,#17726,#17727,
#17728,#17729,#17730,#17731,#17732,#17733,#17734,#17735,#17736,#17737,#17738,
#17739,#17740,#17741,#17742,#17743,#17744,#17745,#17746,#17747,#17748,#17749,
#17750,#17751,#17752,#17753,#17754,#17755,#17756,#17757,#17758,#17759,#17760,
#17761,#17762,#17763,#17764,#17765,#17766,#17767,#17768,#17769,#17770,#17771,
#17772,#17773,#17774,#17775,#17776,#17777,#17778,#17779,#17780,#17781,#17782,
#17783,#17784,#17785,#17786,#17787,#17788,#17789,#17790,#17791,#17792,#17793,
#17794,#17795,#17796,#17797,#17798,#17799,#17800,#17801,#17802,#17803,#17804,
#17805,#17806,#17807,#17808,#17809,#17810,#17811,#17812,#17813,#17814,#17815,
#17816,#17817,#17818,#17819,#17820,#17821),.UNSPECIFIED.,.F.,.F.,(4,3,3,
3,3,3,3,3,3,3,3,3,3,3,3,3,3,3,3,3,3,3,3,3,3,3,3,3,3,3,3,3,3,3,3,3,3,3,3,
3,3,3,3,3,3,3,3,3,3,3,3,3,3,3,3,3,3,3,3,3,3,3,4),(10.376533854396,10.4587496980149,
10.5408628620149,10.6228947330942,10.708174253879,10.7901150713661,10.8720441195327,
10.9539805511138,11.0359435241432,11.1179969429654,11.2001039925654,11.2823284670145,
11.3051308993731,11.3890132354057,11.4727929338235,11.5564899638666,11.6401242241457,
11.7237228276305,11.8073038438104,11.8908852014556,11.9744848256528,12.0581716556972,
12.1419024849746,12.2257650432031,12.3048669100932,12.3887095503942,12.4724509163694,
12.556111015579,12.6397097858981,12.7232752401318,12.8068245416396,12.8903756577647,
12.9739465531604,13.0576072322501,13.1413132752236,13.2251536490027,13.3046029208133,
13.3882436530409,13.4717799864317,13.5552321639106,13.6386203543971,13.7219719209224,
13.8053053499079,13.8886388083069,13.9719904593266,14.0554306107815,14.1389150776764,
14.2225343171068,14.3043389315335,14.3881048144593,14.4717676646521,14.5553475841518,
14.638864603264,14.7223462009019,14.8058103764429,14.8892751759554,14.9727586420724,
15.0563306187544,15.1399471272635,15.2236974410639,15.3040749422536,15.3969223262202,
15.4575905445046),.UNSPECIFIED.);
#58=B_SPLINE_CURVE_WITH_KNOTS('',3,(#17824,#17825,#17826,#17827,#17828,
#17829,#17830,#17831,#17832,#17833,#17834,#17835,#17836,#17837,#17838,#17839,
#17840,#17841,#17842,#17843,#17844,#17845,#17846,#17847,#17848,#17849,#17850,
#17851,#17852,#17853,#17854,#17855,#17856,#17857,#17858,#17859,#17860,#17861,
#17862,#17863,#17864,#17865,#17866,#17867,#17868,#17869,#17870,#17871,#17872,
#17873,#17874,#17875,#17876,#17877,#17878,#17879,#17880,#17881,#17882,#17883,
#17884,#17885,#17886,#17887,#17888,#17889,#17890,#17891,#17892,#17893,#17894,
#17895,#17896,#17897,#17898,#17899,#17900,#17901,#17902,#17903,#17904,#17905,
#17906,#17907,#17908,#17909,#17910,#17911,#17912,#17913,#17914,#17915,#17916,
#17917,#17918,#17919,#17920,#17921,#17922,#17923,#17924,#17925,#17926,#17927,
#17928,#17929,#17930,#17931,#17932,#17933,#17934,#17935,#17936,#17937,#17938,
#17939,#17940,#17941,#17942,#17943,#17944,#17945,#17946,#17947,#17948,#17949,
#17950,#17951,#17952,#17953,#17954,#17955,#17956,#17957,#17958,#17959),
 .UNSPECIFIED.,.F.,.F.,(4,3,3,3,3,3,3,3,3,3,3,3,3,3,3,3,3,3,3,3,3,3,3,3,
3,3,3,3,3,3,3,3,3,3,3,3,3,3,3,3,3,3,3,3,3,4),(11.6154215190877,11.7134290666772,
11.8138941811199,11.9120721012973,12.0136808128725,12.1152895244478,12.1990316872646,
12.2827632483713,12.3665368506524,12.4503294937948,12.5342132456109,12.6151575298078,
12.6999655671363,12.7846980365675,12.8693733302146,12.9540097909809,13.0386424107133,
13.1232764318659,13.2079284449498,13.2926150490975,13.3774076283761,13.4622560147635,
13.5472444041499,13.614893540528,13.6979395377845,13.7808742160161,13.8637184213379,
13.9464929096598,14.0300099898584,14.1127187343178,14.1954240856934,14.2781447082332,
14.362265918987,14.4451170212129,14.5298732862305,14.6146295512481,14.6985212370077,
14.7823082215908,14.8665574653667,14.9501883058671,15.0337808140819,15.117352935138,
15.2020902443029,15.2857015431039,15.3710018574507,15.4563021717976),
 .UNSPECIFIED.);
#59=B_SPLINE_CURVE_WITH_KNOTS('',3,(#17965,#17966,#17967,#17968,#17969,
#17970,#17971,#17972,#17973,#17974,#17975,#17976,#17977,#17978,#17979,#17980,
#17981,#17982,#17983,#17984,#17985,#17986,#17987,#17988,#17989,#17990,#17991,
#17992,#17993,#17994,#17995,#17996,#17997,#17998,#17999,#18000,#18001,#18002,
#18003,#18004,#18005,#18006,#18007,#18008,#18009,#18010,#18011,#18012,#18013,
#18014,#18015,#18016,#18017,#18018,#18019,#18020,#18021,#18022,#18023,#18024,
#18025,#18026,#18027,#18028,#18029,#18030,#18031,#18032,#18033,#18034,#18035,
#18036,#18037,#18038,#18039,#18040,#18041,#18042,#18043,#18044,#18045,#18046,
#18047,#18048,#18049,#18050,#18051,#18052,#18053,#18054,#18055,#18056,#18057,
#18058,#18059,#18060,#18061,#18062,#18063,#18064,#18065,#18066,#18067,#18068,
#18069,#18070,#18071,#18072,#18073,#18074,#18075,#18076,#18077,#18078,#18079,
#18080,#18081,#18082,#18083,#18084,#18085,#18086,#18087,#18088,#18089,#18090,
#18091,#18092,#18093,#18094,#18095,#18096,#18097,#18098,#18099,#18100,#18101,
#18102,#18103,#18104,#18105,#18106,#18107,#18108,#18109,#18110,#18111,#18112,
#18113,#18114,#18115,#18116,#18117,#18118,#18119,#18120,#18121,#18122,#18123,
#18124,#18125,#18126,#18127,#18128,#18129,#18130,#18131,#18132,#18133,#18134,
#18135,#18136,#18137,#18138,#18139,#18140,#18141,#18142,#18143,#18144,#18145,
#18146,#18147,#18148,#18149,#18150,#18151,#18152,#18153,#18154,#18155,#18156,
#18157,#18158,#18159,#18160,#18161,#18162,#18163,#18164,#18165,#18166,#18167,
#18168,#18169,#18170,#18171,#18172,#18173,#18174,#18175,#18176,#18177,#18178,
#18179,#18180,#18181,#18182,#18183,#18184),.UNSPECIFIED.,.F.,.F.,(4,3,3,
3,3,3,3,3,3,3,3,3,3,3,3,3,3,3,3,3,3,3,3,3,3,3,3,3,3,3,3,3,3,3,3,3,3,3,3,
3,3,3,3,3,3,3,3,3,3,3,3,3,3,3,3,3,3,3,3,3,3,3,3,3,3,3,3,3,3,3,3,3,3,4),
(15.7079632679298,15.7926435804918,15.8773492161091,15.9620963337644,16.0475249885667,
16.132453607754,16.2181322803638,16.3038109529737,16.3875351972687,16.471156054379,
16.5546936734092,16.6381681310957,16.7216069220662,16.805028147841,16.8884498952704,
16.9718902477285,17.0554192578422,17.138992811707,17.2227006276309,17.3035469636939,
17.3872906015743,17.4709310773888,17.5544885181045,17.6379829786723,17.7214419777467,
17.804883533783,17.8883257146451,17.9717865847761,18.0553361303936,18.1389302620967,
18.2226585200042,18.303282974414,18.3870229255899,18.4706597068039,18.5542134490663,
18.6377042113358,18.7211595257893,18.8045974060827,18.8880359236554,18.9714931465372,
19.0550390912698,19.1386296415935,19.222354388209,19.3030189851341,19.3867556060725,
19.4703889983084,19.5539392967613,19.6374265642217,19.7208783183761,19.8043125989766,
19.8877474807551,19.9712010350115,20.0547432795759,20.1383301067002,20.2220511281309,
20.3027549958542,20.3864945572802,20.4701309258356,20.5536842330696,20.6371745384566,
20.7206293641871,20.8040667364236,20.8875047270122,20.9709614043765,21.0545067771072,
21.1380967401163,21.2218208789181,21.3024910065744,21.3858830961904,21.469172262834,
21.5523598572504,21.6354890394002,21.7185738574777,21.7400988072349),
 .UNSPECIFIED.);
#60=B_SPLINE_CURVE_WITH_KNOTS('',3,(#18185,#18186,#18187,#18188,#18189,
#18190,#18191,#18192,#18193,#18194),.UNSPECIFIED.,.F.,.F.,(4,3,3,4),(15.4575905445046,
15.5499665865835,15.6419244349656,15.7079632677523),.UNSPECIFIED.);
#61=B_SPLINE_CURVE_WITH_KNOTS('',3,(#18196,#18197,#18198,#18199,#18200,
#18201,#18202,#18203,#18204,#18205),.UNSPECIFIED.,.F.,.F.,(4,3,3,4),(15.4563021717976,
15.5401663906876,15.6143655619682,15.7079632679337),.UNSPECIFIED.);
#62=B_SPLINE_CURVE_WITH_KNOTS('',3,(#18206,#18207,#18208,#18209,#18210,
#18211,#18212,#18213,#18214,#18215,#18216,#18217,#18218,#18219,#18220,#18221,
#18222,#18223,#18224,#18225,#18226,#18227,#18228,#18229,#18230,#18231,#18232,
#18233,#18234,#18235,#18236,#18237,#18238,#18239,#18240,#18241,#18242,#18243,
#18244,#18245,#18246,#18247,#18248,#18249,#18250,#18251,#18252,#18253,#18254,
#18255,#18256,#18257,#18258,#18259,#18260,#18261,#18262,#18263,#18264,#18265,
#18266,#18267,#18268,#18269,#18270,#18271,#18272,#18273,#18274,#18275,#18276,
#18277,#18278,#18279,#18280,#18281,#18282,#18283,#18284,#18285,#18286,#18287,
#18288,#18289,#18290,#18291,#18292,#18293,#18294,#18295,#18296,#18297,#18298,
#18299,#18300,#18301,#18302,#18303,#18304,#18305,#18306,#18307,#18308,#18309,
#18310,#18311,#18312,#18313,#18314,#18315,#18316,#18317,#18318,#18319,#18320,
#18321,#18322,#18323,#18324,#18325,#18326,#18327,#18328,#18329,#18330,#18331,
#18332,#18333,#18334,#18335,#18336,#18337,#18338,#18339,#18340,#18341,#18342,
#18343,#18344,#18345,#18346,#18347,#18348,#18349,#18350,#18351,#18352,#18353,
#18354,#18355,#18356,#18357,#18358,#18359,#18360,#18361,#18362,#18363,#18364,
#18365,#18366,#18367,#18368,#18369,#18370,#18371,#18372,#18373,#18374,#18375,
#18376,#18377,#18378,#18379,#18380,#18381,#18382,#18383,#18384,#18385,#18386,
#18387,#18388,#18389,#18390,#18391,#18392,#18393,#18394,#18395,#18396,#18397,
#18398,#18399,#18400,#18401,#18402,#18403,#18404,#18405,#18406,#18407,#18408,
#18409,#18410,#18411,#18412,#18413,#18414,#18415,#18416,#18417,#18418,#18419,
#18420,#18421,#18422,#18423,#18424,#18425),.UNSPECIFIED.,.F.,.F.,(4,3,3,
3,3,3,3,3,3,3,3,3,3,3,3,3,3,3,3,3,3,3,3,3,3,3,3,3,3,3,3,3,3,3,3,3,3,3,3,
3,3,3,3,3,3,3,3,3,3,3,3,3,3,3,3,3,3,3,3,3,3,3,3,3,3,3,3,3,3,3,3,3,3,4),
(15.7079632680592,15.7907745344394,15.8734936731201,15.956141602808,16.0387439060103,
16.1213228371711,16.2038972033411,16.2864858052991,16.3691583325617,16.4518728357758,
16.5347192332603,16.6141015726884,16.697742304916,16.781278638307,16.8647308157857,
16.9481190062724,17.0314705727976,17.1148040017831,17.1981374601819,17.2814891112015,
17.3649292626563,17.4484137295512,17.5320329689815,17.6138375834085,17.6976034663343,
17.781266316527,17.8648462360265,17.9483632551386,18.0318448527766,18.1153090283176,
18.19877382783,18.2822572939469,18.365829270629,18.449445779138,18.5331960929383,
18.6135735941286,18.6973242901216,18.7809720312271,18.86453693568,18.9480390499362,
19.0315059660048,19.1149555983376,19.1984060076848,19.2818752514727,19.365433354798,
19.44903615789,19.5327731955315,19.6133096048488,19.6970338491438,19.780654706254,
19.8641923252842,19.9476667829708,20.0311055739413,20.1145267997161,20.1979485471458,
20.2813888996038,20.3649179097175,20.4484914635823,20.5321992795062,20.6130456155689,
20.6967892534494,20.7804297292639,20.8639871699793,20.9474816305479,21.0309406296223,
21.1143821856589,21.1978243665211,21.2812852366525,21.3648347822701,21.4484289139732,
21.5321571718807,21.612781626289,21.7074539497444,21.740715980233),
 .UNSPECIFIED.);
#63=B_SPLINE_CURVE_WITH_KNOTS('',3,(#18431,#18432,#18433,#18434,#18435,
#18436,#18437,#18438,#18439,#18440,#18441,#18442,#18443,#18444,#18445,#18446,
#18447,#18448,#18449,#18450,#18451,#18452,#18453,#18454,#18455,#18456,#18457,
#18458,#18459,#18460,#18461,#18462,#18463,#18464,#18465,#18466,#18467,#18468,
#18469,#18470,#18471,#18472,#18473,#18474,#18475,#18476,#18477,#18478,#18479,
#18480,#18481,#18482,#18483,#18484,#18485,#18486,#18487,#18488,#18489,#18490,
#18491,#18492,#18493,#18494,#18495,#18496,#18497,#18498,#18499,#18500,#18501,
#18502,#18503,#18504,#18505,#18506,#18507,#18508,#18509,#18510,#18511,#18512,
#18513,#18514,#18515,#18516,#18517,#18518,#18519,#18520,#18521,#18522,#18523,
#18524,#18525,#18526,#18527,#18528,#18529,#18530,#18531,#18532,#18533,#18534,
#18535,#18536,#18537,#18538,#18539,#18540,#18541,#18542,#18543,#18544,#18545,
#18546,#18547,#18548,#18549,#18550,#18551,#18552,#18553,#18554,#18555,#18556,
#18557,#18558,#18559,#18560,#18561,#18562,#18563,#18564,#18565,#18566,#18567,
#18568,#18569,#18570,#18571,#18572,#18573,#18574,#18575,#18576,#18577,#18578,
#18579,#18580,#18581,#18582,#18583,#18584,#18585,#18586,#18587,#18588,#18589,
#18590,#18591,#18592,#18593,#18594,#18595,#18596,#18597,#18598,#18599,#18600,
#18601,#18602,#18603,#18604,#18605,#18606,#18607,#18608,#18609,#18610,#18611,
#18612,#18613,#18614,#18615,#18616,#18617,#18618,#18619,#18620,#18621,#18622,
#18623,#18624,#18625,#18626,#18627,#18628,#18629,#18630,#18631,#18632,#18633,
#18634,#18635,#18636,#18637,#18638,#18639,#18640,#18641,#18642,#18643,#18644,
#18645,#18646,#18647,#18648,#18649,#18650),.UNSPECIFIED.,.F.,.F.,(4,3,3,
3,3,3,3,3,3,3,3,3,3,3,3,3,3,3,3,3,3,3,3,3,3,3,3,3,3,3,3,3,3,3,3,3,3,3,3,
3,3,3,3,3,3,3,3,3,3,3,3,3,3,3,3,3,3,3,3,3,3,3,3,3,3,3,3,3,3,3,3,3,3,4),
(21.9911485752722,22.0905199443307,22.1906522436346,22.2915864234119,22.3022270172945,
22.3859654335529,22.4696006451592,22.5531527849645,22.6366419137261,22.7200955530059,
22.8035317329769,22.8869685266068,22.9704240034381,23.0539681767605,23.1375569390688,
23.2212798871326,23.3019630280146,23.385701881021,23.4693375349391,23.5528901221183,
23.6363797028221,23.719833799406,23.8032704398822,23.8867076967894,23.9701636392423,
24.0537082792805,24.1372975096405,24.2210209233106,24.3016990387348,24.3854377526698,
24.4690732665012,24.5526257127343,24.6361151517867,24.7195691061525,24.803005604086,
24.8864427182613,24.9698985179291,25.0534430159093,25.1370321043811,25.2207553778982,
25.3014350494549,25.3851737205122,25.4688091904866,25.5523615919349,25.6358509853249,
25.7193048928488,25.8027413432284,25.8861784091806,25.9696341599982,26.0531786084049,
26.1367676468314,26.2204908699956,26.301171060175,26.3849097947876,26.4685453291628,
26.5520977957841,26.6355872550472,26.7190412292786,26.8024777468644,26.8859148804588,
26.9693706992928,27.052915215926,27.1365043228015,27.2202276141041,27.3009070708951,
27.3842944828408,27.4675500501445,27.550729511587,27.633851366961,27.7169340711784,
27.8000126126222,27.8830868940955,27.9662056561429,28.0225858316167),
 .UNSPECIFIED.);
#64=B_SPLINE_CURVE_WITH_KNOTS('',3,(#18651,#18652,#18653,#18654,#18655,
#18656,#18657,#18658,#18659,#18660),.UNSPECIFIED.,.F.,.F.,(4,3,3,4),(21.7400988072349,
21.8231667809187,21.907157678014,21.9911485751093),.UNSPECIFIED.);
#65=B_SPLINE_CURVE_WITH_KNOTS('',3,(#18662,#18663,#18664,#18665,#18666,
#18667,#18668,#18669,#18670,#18671),.UNSPECIFIED.,.F.,.F.,(4,3,3,4),(21.740715980233,
21.8348722215429,21.9284884766943,21.9911485749198),.UNSPECIFIED.);
#66=B_SPLINE_CURVE_WITH_KNOTS('',3,(#18672,#18673,#18674,#18675,#18676,
#18677,#18678,#18679,#18680,#18681,#18682,#18683,#18684,#18685,#18686,#18687,
#18688,#18689,#18690,#18691,#18692,#18693,#18694,#18695,#18696,#18697,#18698,
#18699,#18700,#18701,#18702,#18703,#18704,#18705,#18706,#18707,#18708,#18709,
#18710,#18711,#18712,#18713,#18714,#18715,#18716,#18717,#18718,#18719,#18720,
#18721,#18722,#18723,#18724,#18725,#18726,#18727,#18728,#18729,#18730,#18731,
#18732,#18733,#18734,#18735,#18736,#18737,#18738,#18739,#18740,#18741,#18742,
#18743,#18744,#18745,#18746,#18747,#18748,#18749,#18750,#18751,#18752,#18753,
#18754,#18755,#18756,#18757,#18758,#18759,#18760,#18761,#18762,#18763,#18764,
#18765,#18766,#18767,#18768,#18769,#18770,#18771,#18772,#18773,#18774,#18775,
#18776,#18777,#18778,#18779,#18780,#18781,#18782,#18783,#18784,#18785,#18786,
#18787,#18788,#18789,#18790,#18791,#18792,#18793,#18794,#18795,#18796,#18797,
#18798,#18799,#18800,#18801,#18802,#18803,#18804,#18805,#18806,#18807,#18808,
#18809,#18810,#18811,#18812,#18813,#18814,#18815,#18816,#18817,#18818,#18819,
#18820,#18821,#18822,#18823,#18824,#18825,#18826,#18827,#18828,#18829,#18830,
#18831,#18832,#18833,#18834,#18835,#18836,#18837,#18838,#18839,#18840,#18841,
#18842,#18843,#18844,#18845,#18846,#18847,#18848,#18849,#18850,#18851,#18852,
#18853,#18854,#18855,#18856,#18857,#18858,#18859,#18860,#18861,#18862,#18863,
#18864,#18865,#18866,#18867,#18868,#18869,#18870,#18871,#18872,#18873,#18874,
#18875,#18876,#18877,#18878,#18879,#18880,#18881,#18882,#18883,#18884,#18885,
#18886,#18887,#18888,#18889,#18890,#18891),.UNSPECIFIED.,.F.,.F.,(4,3,3,
3,3,3,3,3,3,3,3,3,3,3,3,3,3,3,3,3,3,3,3,3,3,3,3,3,3,3,3,3,3,3,3,3,3,3,3,
3,3,3,3,3,3,3,3,3,3,3,3,3,3,3,3,3,3,3,3,3,3,3,3,3,3,3,3,3,3,3,3,3,3,4),
(21.9911485751133,22.0752803066499,22.1594213519125,22.2435887880297,22.327799705763,
22.412122635211,22.496510193649,22.5810312627201,22.6125176370092,22.6962542579476,
22.7798876501835,22.8634379486364,22.9469252160963,23.0303769702507,23.1138112508511,
23.1972461326295,23.2806996868859,23.3642419314503,23.4478287585743,23.531549780005,
23.6122536477293,23.6959932091553,23.7796295777105,23.8631828849443,23.946673190331,
24.0301280160616,24.113565388298,24.1970033788866,24.2804600562506,24.3640054289813,
24.4475953919903,24.5313195307922,24.6119896584494,24.6957284703853,24.7793640854067,
24.8629166358964,24.9464061821532,25.0298602478526,25.11329685962,25.1967340900312,
25.2801900082394,25.3637346277638,25.4473238396068,25.5310472383997,25.6117256691696,
25.6954640854281,25.7790992970342,25.8626514368397,25.9461405656013,26.0295942048811,
26.1130303848521,26.196467178482,26.2799226553132,26.3634668286356,26.4470555909439,
26.5307785390076,26.6114616798897,26.6952005328961,26.7788361868141,26.8623887739932,
26.9458783546974,27.0293324512814,27.1127690917577,27.1962063486646,27.2796622911176,
27.3632069311557,27.4467961615158,27.530519575186,27.6111976906098,27.6949624620804,
27.7785925584211,27.8621451536583,27.9456293039383,28.0234162092491),
 .UNSPECIFIED.);
#67=B_SPLINE_CURVE_WITH_KNOTS('',3,(#18897,#18898,#18899,#18900,#18901,
#18902,#18903,#18904,#18905,#18906,#18907,#18908,#18909,#18910,#18911,#18912,
#18913,#18914,#18915,#18916,#18917,#18918,#18919,#18920,#18921,#18922,#18923,
#18924,#18925,#18926,#18927,#18928,#18929,#18930,#18931,#18932,#18933,#18934,
#18935,#18936,#18937,#18938,#18939,#18940,#18941,#18942,#18943,#18944,#18945,
#18946,#18947,#18948,#18949,#18950,#18951,#18952,#18953,#18954,#18955,#18956,
#18957,#18958,#18959,#18960,#18961,#18962,#18963,#18964,#18965,#18966,#18967,
#18968,#18969,#18970,#18971,#18972,#18973,#18974,#18975,#18976,#18977,#18978,
#18979,#18980,#18981,#18982,#18983,#18984,#18985,#18986,#18987,#18988,#18989,
#18990,#18991,#18992,#18993,#18994,#18995,#18996,#18997,#18998,#18999,#19000,
#19001,#19002,#19003,#19004,#19005,#19006,#19007,#19008,#19009,#19010,#19011,
#19012,#19013,#19014,#19015,#19016,#19017,#19018,#19019,#19020,#19021,#19022,
#19023,#19024,#19025,#19026,#19027,#19028,#19029,#19030,#19031,#19032,#19033,
#19034,#19035,#19036,#19037,#19038,#19039,#19040,#19041,#19042,#19043,#19044,
#19045,#19046,#19047,#19048,#19049,#19050,#19051,#19052,#19053,#19054,#19055,
#19056,#19057,#19058,#19059,#19060,#19061,#19062,#19063,#19064,#19065,#19066,
#19067,#19068,#19069,#19070,#19071,#19072,#19073,#19074,#19075,#19076,#19077,
#19078,#19079,#19080,#19081,#19082,#19083,#19084,#19085,#19086,#19087,#19088,
#19089,#19090,#19091,#19092,#19093,#19094,#19095,#19096,#19097,#19098,#19099,
#19100,#19101,#19102,#19103,#19104,#19105,#19106,#19107,#19108,#19109,#19110,
#19111,#19112,#19113,#19114,#19115,#19116,#19117,#19118,#19119),
 .UNSPECIFIED.,.F.,.F.,(4,3,3,3,3,3,3,3,3,3,3,3,3,3,3,3,3,3,3,3,3,3,3,3,
3,3,3,3,3,3,3,3,3,3,3,3,3,3,3,3,3,3,3,3,3,3,3,3,3,3,3,3,3,3,3,3,3,3,3,3,
3,3,3,3,3,3,3,3,3,3,3,3,3,3,4),(28.2743338822889,28.3006430816153,28.3843817879882,
28.468017293797,28.5515697315575,28.6350591616976,28.7185131065089,28.8019495944981,
28.8853866983471,28.9688424873144,29.0523869740573,29.1359760509821,29.2196993125341,
29.3003790923354,29.3841178077619,29.4677533227502,29.5513057698054,29.6347952093454,
29.7182491636837,29.801685661276,29.8851227747951,29.9685785734908,30.0521230699997,
30.1357121567266,30.2194354280432,30.3001151030555,30.3838538143865,30.4674893252401,
30.5510417681263,30.6345312034672,30.7179851535757,30.80142164692,30.8848587561773,
30.9683145506009,31.051859042846,31.1354481253068,31.2191713923966,31.2998511137757,
31.3835898249122,31.4672253355584,31.5507777782246,31.6342672133331,31.7177211631913,
31.8011576562743,31.8845947652594,31.9680505594003,32.0515950513474,32.1351841335015,
32.2189074002725,32.2995871244958,32.3833258368923,32.466961348817,32.5505137927785,
32.6340032291978,32.7174571803857,32.8008936748098,32.884330785146,32.967786580647,
33.0513310739606,33.1349201574868,33.2186434256259,33.2993231352159,33.3830618469456,
33.4666973581966,33.5502498014783,33.6337392372124,33.7171931877092,33.8006296814388,
33.8840667910778,33.9675225858795,34.0510670784944,34.1346561613211,34.2183794287664,
34.299059145936,34.3065000825424),.UNSPECIFIED.);
#68=B_SPLINE_CURVE_WITH_KNOTS('',3,(#19120,#19121,#19122,#19123,#19124,
#19125,#19126,#19127,#19128,#19129),.UNSPECIFIED.,.F.,.F.,(4,3,3,4),(28.0225858316167,
28.1058018123903,28.1900678472803,28.2743338821704),.UNSPECIFIED.);
#69=B_SPLINE_CURVE_WITH_KNOTS('',3,(#19131,#19132,#19133,#19134,#19135,
#19136,#19137,#19138,#19139,#19140),.UNSPECIFIED.,.F.,.F.,(4,3,3,4),(28.0234162092491,
28.1068355155373,28.190584698915,28.2743338822928),.UNSPECIFIED.);
#70=B_SPLINE_CURVE_WITH_KNOTS('',3,(#19141,#19142,#19143,#19144,#19145,
#19146,#19147,#19148,#19149,#19150,#19151,#19152,#19153,#19154,#19155,#19156,
#19157,#19158,#19159,#19160,#19161,#19162,#19163,#19164,#19165,#19166,#19167,
#19168,#19169,#19170,#19171,#19172,#19173,#19174,#19175,#19176,#19177,#19178,
#19179,#19180,#19181,#19182,#19183,#19184,#19185,#19186,#19187,#19188,#19189,
#19190,#19191,#19192,#19193,#19194,#19195,#19196,#19197,#19198,#19199,#19200,
#19201,#19202,#19203,#19204,#19205,#19206,#19207,#19208,#19209,#19210,#19211,
#19212,#19213,#19214,#19215,#19216,#19217,#19218,#19219,#19220,#19221,#19222,
#19223,#19224,#19225,#19226,#19227,#19228,#19229,#19230,#19231,#19232,#19233,
#19234,#19235,#19236,#19237,#19238,#19239,#19240,#19241,#19242,#19243,#19244,
#19245,#19246,#19247,#19248,#19249,#19250,#19251,#19252,#19253,#19254,#19255,
#19256,#19257,#19258,#19259,#19260,#19261,#19262,#19263,#19264,#19265,#19266,
#19267,#19268,#19269,#19270,#19271,#19272,#19273,#19274,#19275,#19276,#19277,
#19278,#19279,#19280,#19281,#19282,#19283,#19284,#19285,#19286,#19287,#19288,
#19289,#19290,#19291,#19292,#19293,#19294,#19295,#19296,#19297,#19298,#19299,
#19300,#19301,#19302,#19303,#19304,#19305,#19306,#19307,#19308,#19309,#19310,
#19311,#19312,#19313,#19314,#19315,#19316,#19317,#19318,#19319,#19320,#19321,
#19322,#19323,#19324,#19325,#19326,#19327,#19328,#19329,#19330,#19331,#19332,
#19333,#19334,#19335,#19336,#19337,#19338,#19339,#19340,#19341,#19342,#19343,
#19344,#19345,#19346,#19347,#19348,#19349,#19350,#19351,#19352,#19353,#19354,
#19355,#19356,#19357,#19358,#19359,#19360),.UNSPECIFIED.,.F.,.F.,(4,3,3,
3,3,3,3,3,3,3,3,3,3,3,3,3,3,3,3,3,3,3,3,3,3,3,3,3,3,3,3,3,3,3,3,3,3,3,3,
3,3,3,3,3,3,3,3,3,3,3,3,3,3,3,3,3,3,3,3,3,3,3,3,3,3,3,3,3,3,3,3,3,3,4),
(28.2743338824827,28.3712824055307,28.4687879362423,28.5669577034657,28.6109337013299,
28.6946723723872,28.7783078423616,28.8618602438099,28.9453496371999,29.0288035447238,
29.1122399951033,29.1956770610554,29.2791328118729,29.3626772602797,29.4462662987062,
29.5299895218703,29.6106697120501,29.6944084466627,29.7780439810379,29.8615964476591,
29.9450859069223,30.0285398811537,30.1119763987395,30.1954135323339,30.2788693511678,
30.362413867801,30.4460029746765,30.5297262659791,30.6104057227702,30.694144433022,
30.777779942827,30.8613323846962,30.9448218190526,31.0282757682304,31.1117122606767,
31.1951493690697,31.2786051626639,31.3621496541399,31.4457387358632,31.5294620022777,
31.6101417334903,31.6938804398633,31.7775159456722,31.8610683834328,31.9445578135729,
32.0280117583843,32.1114482463736,32.1948853502228,32.2783411391901,32.3618856259331,
32.4454747028581,32.5291979644102,32.6098777442105,32.693616459637,32.7772519746252,
32.8608044216806,32.9442938612206,33.0277478155589,33.1111843131511,33.1946214266703,
33.2780772253658,33.3616217218747,33.4452108086016,33.5289340799181,33.6096137549306,
33.696625903061,33.7795858721787,33.8624709514653,33.9452998737482,34.0280913257695,
34.1108784301918,34.1936633276373,34.2764866832596,34.3057109399742),
 .UNSPECIFIED.);
#71=B_SPLINE_CURVE_WITH_KNOTS('',3,(#19366,#19367,#19368,#19369,#19370,
#19371,#19372,#19373,#19374,#19375,#19376,#19377,#19378,#19379,#19380,#19381,
#19382,#19383,#19384,#19385,#19386,#19387,#19388,#19389,#19390,#19391,#19392,
#19393,#19394,#19395,#19396,#19397,#19398,#19399,#19400,#19401,#19402,#19403,
#19404,#19405,#19406,#19407,#19408,#19409,#19410,#19411,#19412,#19413,#19414,
#19415,#19416,#19417,#19418,#19419,#19420,#19421,#19422,#19423,#19424,#19425,
#19426,#19427,#19428,#19429,#19430,#19431,#19432,#19433,#19434,#19435,#19436,
#19437,#19438,#19439,#19440,#19441,#19442,#19443,#19444,#19445,#19446,#19447,
#19448,#19449,#19450,#19451,#19452,#19453,#19454,#19455,#19456,#19457,#19458,
#19459,#19460,#19461,#19462,#19463,#19464,#19465,#19466,#19467,#19468,#19469,
#19470,#19471,#19472,#19473,#19474,#19475,#19476,#19477,#19478,#19479,#19480,
#19481,#19482,#19483,#19484,#19485,#19486,#19487,#19488,#19489,#19490,#19491,
#19492,#19493,#19494,#19495,#19496,#19497,#19498,#19499,#19500,#19501,#19502,
#19503,#19504,#19505,#19506,#19507,#19508,#19509,#19510,#19511,#19512,#19513,
#19514,#19515,#19516,#19517,#19518,#19519,#19520,#19521,#19522,#19523,#19524,
#19525,#19526,#19527,#19528,#19529,#19530,#19531,#19532,#19533,#19534,#19535,
#19536,#19537,#19538,#19539,#19540,#19541,#19542,#19543,#19544,#19545,#19546,
#19547,#19548,#19549,#19550,#19551,#19552,#19553,#19554,#19555,#19556,#19557,
#19558,#19559,#19560,#19561,#19562,#19563,#19564,#19565,#19566,#19567,#19568,
#19569,#19570,#19571,#19572,#19573,#19574,#19575,#19576,#19577,#19578,#19579,
#19580,#19581,#19582,#19583,#19584,#19585),.UNSPECIFIED.,.F.,.F.,(4,3,3,
3,3,3,3,3,3,3,3,3,3,3,3,3,3,3,3,3,3,3,3,3,3,3,3,3,3,3,3,3,3,3,3,3,3,3,3,
3,3,3,3,3,3,3,3,3,3,3,3,3,3,3,3,3,3,3,3,3,3,3,3,3,3,3,3,3,3,3,3,3,3,4),
(34.5575191894685,34.6401346660436,34.7227049790521,34.8052521817043,34.8877950853622,
34.9703524953451,35.0529944964819,35.1356787053279,35.2184958070966,35.2987951566562,
35.3825338685851,35.4661693800365,35.5497218235198,35.6332112594563,35.7166652101566,
35.8001017040901,35.8835388139334,35.9669946089394,36.0505391017574,36.134128184787,
36.2178514524327,36.2985311673763,36.3822698791994,36.465905390544,36.5494578339196,
36.6329472697474,36.7164012203379,36.7998377141608,36.8832748238929,36.9667306187873,
37.0502751114939,37.1338641944118,37.2175874619467,37.2982671780964,37.3820058899321,
37.4656414012895,37.5491938446774,37.632683280518,37.7161372311207,37.7995737249558,
37.8830108347001,37.9664666296065,38.0500111223246,38.1336002052539,38.2173234727998,
38.2980031888166,38.3817419006748,38.4653774120547,38.548929855466,38.6324192913301,
38.7158732419566,38.7993097358158,38.8827468455844,38.9662026405151,39.049747133258,
39.133336216212,39.2170594837827,39.2977391995367,39.3814779113784,39.4651134227418,
39.5486658661357,39.6321553019831,39.7156092525924,39.7990457464345,39.8824828561857,
39.9659386510992,40.0494831438246,40.1330722267613,40.2167954943148,40.2974752102568,
40.3839889562121,40.4703860712489,40.5566452121474,40.5902857429648),
 .UNSPECIFIED.);
#72=B_SPLINE_CURVE_WITH_KNOTS('',3,(#19586,#19587,#19588,#19589,#19590,
#19591,#19592,#19593,#19594,#19595),.UNSPECIFIED.,.F.,.F.,(4,3,3,4),(34.3065000825424,
34.4146795617861,34.5207421559751,34.557519189341),.UNSPECIFIED.);
#73=B_SPLINE_CURVE_WITH_KNOTS('',3,(#19597,#19598,#19599,#19600,#19601,
#19602,#19603,#19604,#19605,#19606),.UNSPECIFIED.,.F.,.F.,(4,3,3,4),(34.3057109399742,
34.3886262459297,34.4730727175991,34.5575191892685),.UNSPECIFIED.);
#74=B_SPLINE_CURVE_WITH_KNOTS('',3,(#19607,#19608,#19609,#19610,#19611,
#19612,#19613,#19614,#19615,#19616,#19617,#19618,#19619,#19620,#19621,#19622,
#19623,#19624,#19625,#19626,#19627,#19628,#19629,#19630,#19631,#19632,#19633,
#19634,#19635,#19636,#19637,#19638,#19639,#19640,#19641,#19642,#19643,#19644,
#19645,#19646,#19647,#19648,#19649,#19650,#19651,#19652,#19653,#19654,#19655,
#19656,#19657,#19658,#19659,#19660,#19661,#19662,#19663,#19664,#19665,#19666,
#19667,#19668,#19669,#19670,#19671,#19672,#19673,#19674,#19675,#19676,#19677,
#19678,#19679,#19680,#19681,#19682,#19683,#19684,#19685,#19686,#19687,#19688,
#19689,#19690,#19691,#19692,#19693,#19694,#19695,#19696,#19697,#19698,#19699,
#19700,#19701,#19702,#19703,#19704,#19705,#19706,#19707,#19708,#19709,#19710,
#19711,#19712,#19713,#19714,#19715,#19716,#19717,#19718,#19719,#19720,#19721,
#19722,#19723,#19724,#19725,#19726,#19727,#19728,#19729,#19730,#19731,#19732,
#19733,#19734,#19735,#19736,#19737,#19738,#19739,#19740,#19741,#19742,#19743,
#19744,#19745,#19746,#19747,#19748,#19749,#19750,#19751,#19752,#19753,#19754,
#19755,#19756,#19757,#19758,#19759,#19760,#19761,#19762,#19763,#19764,#19765,
#19766,#19767,#19768,#19769,#19770,#19771,#19772,#19773,#19774,#19775,#19776,
#19777,#19778,#19779,#19780,#19781,#19782,#19783,#19784,#19785,#19786,#19787,
#19788,#19789,#19790,#19791,#19792,#19793,#19794,#19795,#19796,#19797,#19798,
#19799,#19800,#19801,#19802,#19803,#19804,#19805,#19806,#19807,#19808,#19809,
#19810,#19811,#19812,#19813,#19814,#19815,#19816,#19817,#19818,#19819,#19820,
#19821,#19822,#19823,#19824,#19825,#19826),.UNSPECIFIED.,.F.,.F.,(4,3,3,
3,3,3,3,3,3,3,3,3,3,3,3,3,3,3,3,3,3,3,3,3,3,3,3,3,3,3,3,3,3,3,3,3,3,3,3,
3,3,3,3,3,3,3,3,3,3,3,3,3,3,3,3,3,3,3,3,3,3,3,3,3,3,3,3,3,3,3,3,3,3,4),
(34.5575191894724,34.6093497656507,34.6930884767872,34.7767239874333,34.8602764300995,
34.9437658652082,35.0272198150664,35.1106563081493,35.1940934171344,35.2775492112753,
35.3610937032224,35.4446827853765,35.5284060521475,35.6090857763709,35.6928244887674,
35.776460000692,35.8600124446535,35.9435018810726,36.0269558322605,36.1103923266845,
36.1938294370208,36.2772852325218,36.3608297258354,36.4444188093616,36.5281420775006,
36.608821787091,36.6925604988207,36.7761960100715,36.8597484533532,36.9432378890873,
37.0266918395841,37.1101283333137,37.1935654429527,37.2770212377544,37.3605657303692,
37.4441548131959,37.5278780806412,37.6085577978111,37.6922965095691,37.7759320208472,
37.8594844641547,37.9429738999134,38.0264278504329,38.1098643441839,38.1933014538431,
38.2767572486637,38.3603017412953,38.4438908241376,38.5276140915964,38.6082938085313,
38.6920325204602,38.7756680319116,38.859220475395,38.9427099113317,39.026163862032,
39.1096003559656,39.1930374658088,39.2764932608146,39.3600377536327,39.4436268366622,
39.5273501043079,39.6080298192514,39.6917695595991,39.7754058589717,39.8589588508911,
39.9424485965472,40.0259016212374,40.109336849158,40.1927723527529,40.2762262007468,
40.3597640184065,40.4433462857643,40.5270516189311,40.5895313989693),
 .UNSPECIFIED.);
#75=B_SPLINE_CURVE_WITH_KNOTS('',3,(#19832,#19833,#19834,#19835,#19836,
#19837,#19838,#19839,#19840,#19841,#19842,#19843,#19844,#19845,#19846,#19847,
#19848,#19849,#19850,#19851,#19852,#19853,#19854,#19855,#19856,#19857,#19858,
#19859,#19860,#19861,#19862,#19863,#19864,#19865,#19866,#19867,#19868,#19869,
#19870,#19871,#19872,#19873,#19874,#19875,#19876,#19877,#19878,#19879,#19880,
#19881,#19882,#19883,#19884,#19885,#19886,#19887,#19888,#19889,#19890,#19891,
#19892,#19893,#19894,#19895,#19896,#19897,#19898,#19899,#19900,#19901,#19902,
#19903,#19904,#19905,#19906,#19907,#19908,#19909,#19910,#19911,#19912,#19913,
#19914,#19915,#19916,#19917,#19918,#19919,#19920,#19921,#19922,#19923,#19924,
#19925,#19926,#19927,#19928,#19929,#19930,#19931,#19932,#19933,#19934,#19935,
#19936,#19937,#19938,#19939,#19940,#19941,#19942,#19943,#19944,#19945,#19946,
#19947,#19948,#19949,#19950,#19951,#19952,#19953,#19954,#19955,#19956,#19957,
#19958,#19959,#19960,#19961,#19962,#19963,#19964,#19965,#19966,#19967,#19968,
#19969,#19970,#19971,#19972,#19973,#19974,#19975,#19976,#19977,#19978,#19979,
#19980,#19981,#19982,#19983,#19984,#19985,#19986,#19987,#19988,#19989,#19990,
#19991,#19992,#19993,#19994,#19995,#19996,#19997,#19998,#19999,#20000,#20001,
#20002,#20003,#20004,#20005,#20006,#20007,#20008,#20009,#20010,#20011,#20012,
#20013,#20014,#20015,#20016,#20017,#20018,#20019,#20020,#20021,#20022,#20023,
#20024,#20025,#20026,#20027,#20028,#20029,#20030,#20031,#20032,#20033,#20034,
#20035,#20036,#20037,#20038,#20039,#20040,#20041,#20042,#20043,#20044,#20045,
#20046,#20047,#20048),.UNSPECIFIED.,.F.,.F.,(4,3,3,3,3,3,3,3,3,3,3,3,3,
3,3,3,3,3,3,3,3,3,3,3,3,3,3,3,3,3,3,3,3,3,3,3,3,3,3,3,3,3,3,3,3,3,3,3,3,
3,3,3,3,3,3,3,3,3,3,3,3,3,3,3,3,3,3,3,3,3,3,3,4),(40.8407044968307,40.9298601171088,
41.0216978930758,41.1113188688309,41.2042650449039,41.2972112209769,41.3809499328246,
41.4645854441938,41.5481378875942,41.631627323447,41.7150812740625,41.7985177679105,
41.8819548776678,41.9654106725873,42.0489551653189,42.1325442482617,42.2162675158211,
42.2969472316971,42.3806859435423,42.4643214549091,42.547873898307,42.6313633341573,
42.7148172847703,42.7982537786158,42.8816908883705,42.9651466832875,43.0486911760164,
43.1322802589567,43.2160035265135,43.2966832424172,43.380421954263,43.4640574656304,
43.5476099090288,43.6310993448798,43.7145532954933,43.7979897893395,43.8814268990948,
43.9648826940124,44.0484271867419,44.1320162696828,44.2157395372403,44.2964192531373,
44.3801579649835,44.4637934763512,44.54734591975,44.6308353556013,44.7142893062153,
44.7977258000618,44.8811629098175,44.9646187047355,45.0481631974655,45.1317522804067,
45.2154755479646,45.2961552638575,45.3798939757033,45.4635294870707,45.5470819304692,
45.6305713663201,45.7140253169337,45.7974618107799,45.8808989205352,45.9643547154527,
46.0478992081823,46.1314882911231,46.2152115586806,46.2958912745776,46.3783624320973,
46.4607382036819,46.5430378108789,46.625328127725,46.7075361957602,46.7898676370116,
46.872199078263),.UNSPECIFIED.);
#76=B_SPLINE_CURVE_WITH_KNOTS('',3,(#20049,#20050,#20051,#20052,#20053,
#20054,#20055,#20056,#20057,#20058),.UNSPECIFIED.,.F.,.F.,(4,3,3,4),(40.5902857429648,
40.6763925853647,40.7624026469278,40.8407044966482),.UNSPECIFIED.);
#77=B_SPLINE_CURVE_WITH_KNOTS('',3,(#20060,#20061,#20062,#20063,#20064,
#20065,#20066,#20067,#20068,#20069,#20070,#20071,#20072),.UNSPECIFIED.,
 .F.,.F.,(4,3,3,3,4),(40.5895313989693,40.6077658299715,40.7242351632557,
40.8344463524574,40.8407044965399),.UNSPECIFIED.);
#78=B_SPLINE_CURVE_WITH_KNOTS('',3,(#20073,#20074,#20075,#20076,#20077,
#20078,#20079,#20080,#20081,#20082,#20083,#20084,#20085,#20086,#20087,#20088,
#20089,#20090,#20091,#20092,#20093,#20094,#20095,#20096,#20097,#20098,#20099,
#20100,#20101,#20102,#20103,#20104,#20105,#20106,#20107,#20108,#20109,#20110,
#20111,#20112,#20113,#20114,#20115,#20116,#20117,#20118,#20119,#20120,#20121,
#20122,#20123,#20124,#20125,#20126,#20127,#20128,#20129,#20130,#20131,#20132,
#20133,#20134,#20135,#20136,#20137,#20138,#20139,#20140,#20141,#20142,#20143,
#20144,#20145,#20146,#20147,#20148,#20149,#20150,#20151,#20152,#20153,#20154,
#20155,#20156,#20157,#20158,#20159,#20160,#20161,#20162,#20163,#20164,#20165,
#20166,#20167,#20168,#20169,#20170,#20171,#20172,#20173,#20174,#20175,#20176,
#20177,#20178,#20179,#20180,#20181,#20182,#20183,#20184,#20185,#20186,#20187,
#20188,#20189,#20190,#20191,#20192,#20193,#20194,#20195,#20196,#20197,#20198,
#20199,#20200,#20201,#20202,#20203,#20204,#20205,#20206,#20207,#20208,#20209,
#20210,#20211,#20212,#20213,#20214,#20215,#20216,#20217,#20218,#20219,#20220,
#20221,#20222,#20223,#20224,#20225,#20226,#20227,#20228,#20229,#20230,#20231,
#20232,#20233,#20234,#20235,#20236,#20237,#20238,#20239,#20240,#20241,#20242,
#20243,#20244,#20245,#20246,#20247,#20248,#20249,#20250,#20251,#20252,#20253,
#20254,#20255,#20256,#20257,#20258,#20259,#20260,#20261,#20262,#20263,#20264,
#20265,#20266,#20267,#20268,#20269,#20270,#20271,#20272,#20273,#20274,#20275,
#20276,#20277,#20278,#20279,#20280,#20281,#20282,#20283,#20284,#20285,#20286,
#20287,#20288,#20289,#20290,#20291,#20292),.UNSPECIFIED.,.F.,.F.,(4,3,3,
3,3,3,3,3,3,3,3,3,3,3,3,3,3,3,3,3,3,3,3,3,3,3,3,3,3,3,3,3,3,3,3,3,3,3,3,
3,3,3,3,3,3,3,3,3,3,3,3,3,3,3,3,3,3,3,3,3,3,3,3,3,3,3,3,3,3,3,3,3,3,4),
(40.840704496652,40.9231791511788,41.0087194873679,41.0911052472321,41.1734797508196,
41.2558619211434,41.3382706848019,41.4207689799329,41.5033205891009,41.5859878354084,
41.6075018406916,41.6912405525498,41.7748760639297,41.8584285073409,41.9419179432047,
42.0253718938312,42.1088083876904,42.1922454974588,42.2757012923896,42.3592457851324,
42.4428348680864,42.526558135657,42.6072378514118,42.6909765632536,42.7746120746171,
42.8581645180118,42.9416539538587,43.0251079044681,43.1085443983101,43.1919815080613,
43.2754373029746,43.3589817957001,43.4425708786367,43.5262941461901,43.6069738621319,
43.6907125739767,43.774348085343,43.8579005287403,43.9413899645904,44.0248439152029,
44.1082804090481,44.1917175188026,44.2751733137188,44.3587178064472,44.442306889387,
44.5260301569433,44.606709872852,44.6904485846998,44.7740840960691,44.8576365394695,
44.9411259753222,45.0245799259379,45.1080164197859,45.191453529543,45.2749093244626,
45.3584538171943,45.4420429001373,45.5257661676968,45.6064458835722,45.6901845954174,
45.7738201067842,45.8573725501822,45.9408619860327,46.0243159366455,46.1077524304912,
46.1911895402463,46.2746453351632,46.3581898278923,46.4417789108326,46.5255021783895,
46.6061818942923,46.6935617353949,46.7835468238829,46.873531912371),
 .UNSPECIFIED.);
#79=B_SPLINE_CURVE_WITH_KNOTS('',3,(#20298,#20299,#20300,#20301,#20302,
#20303,#20304,#20305,#20306,#20307,#20308,#20309,#20310,#20311,#20312,#20313,
#20314,#20315,#20316,#20317,#20318,#20319,#20320,#20321,#20322,#20323,#20324,
#20325,#20326,#20327,#20328,#20329,#20330,#20331,#20332,#20333,#20334,#20335,
#20336,#20337,#20338,#20339,#20340,#20341,#20342,#20343,#20344,#20345,#20346,
#20347,#20348,#20349,#20350,#20351,#20352,#20353,#20354,#20355,#20356,#20357,
#20358,#20359,#20360,#20361,#20362,#20363,#20364,#20365,#20366,#20367,#20368,
#20369,#20370,#20371,#20372,#20373,#20374,#20375,#20376,#20377,#20378,#20379,
#20380,#20381,#20382,#20383,#20384,#20385,#20386,#20387,#20388,#20389,#20390,
#20391,#20392,#20393,#20394,#20395,#20396,#20397,#20398,#20399,#20400,#20401,
#20402,#20403,#20404,#20405,#20406,#20407,#20408,#20409,#20410,#20411,#20412,
#20413,#20414,#20415,#20416,#20417,#20418,#20419,#20420,#20421,#20422,#20423,
#20424,#20425,#20426,#20427,#20428,#20429,#20430,#20431,#20432,#20433,#20434,
#20435,#20436,#20437,#20438,#20439,#20440,#20441,#20442,#20443,#20444,#20445,
#20446,#20447,#20448,#20449,#20450,#20451,#20452,#20453,#20454,#20455,#20456,
#20457,#20458,#20459,#20460,#20461,#20462,#20463,#20464,#20465,#20466,#20467,
#20468,#20469,#20470,#20471,#20472,#20473,#20474,#20475,#20476,#20477,#20478,
#20479,#20480,#20481,#20482,#20483,#20484,#20485,#20486,#20487,#20488,#20489,
#20490,#20491,#20492,#20493,#20494,#20495,#20496,#20497,#20498,#20499,#20500,
#20501,#20502,#20503,#20504,#20505,#20506,#20507,#20508,#20509,#20510,#20511,
#20512,#20513,#20514,#20515,#20516,#20517),.UNSPECIFIED.,.F.,.F.,(4,3,3,
3,3,3,3,3,3,3,3,3,3,3,3,3,3,3,3,3,3,3,3,3,3,3,3,3,3,3,3,3,3,3,3,3,3,3,3,
3,3,3,3,3,3,3,3,3,3,3,3,3,3,3,3,3,3,3,3,3,3,3,3,3,3,3,3,3,3,3,3,3,3,4),
(47.1238898038278,47.2546038085429,47.2956272852977,47.3793659971438,47.4630015085113,
47.54655395191,47.6300433877611,47.7134973383749,47.7969338322212,47.8803709419768,
47.9638267368945,48.0473712296243,48.1309603125654,48.2146835801231,48.2953632960178,
48.3791020078637,48.4627375192312,48.5462899626297,48.6297793984807,48.7132333490943,
48.7966698429405,48.880106952696,48.9635627476137,49.0471072403433,49.1306963232843,
49.2144195908419,49.295099306738,49.3788380185839,49.4624735299514,49.54602597335,
49.6295154092011,49.7129693598147,49.796405853661,49.8798429634164,49.9632987583341,
50.0468432510638,50.1304323340048,50.2141556015624,50.2948353174581,50.3785740293041,
50.4622095406716,50.5457619840702,50.6292514199212,50.7127053705349,50.7961418643812,
50.8795789741367,50.9630347690544,51.0465792617841,51.1301683447251,51.2138916122827,
51.2945713281782,51.3783100400241,51.4619455513916,51.5454979947902,51.6289874306412,
51.7124413812548,51.795877875101,51.8793149848565,51.9627707797741,52.0463152725038,
52.1299043554448,52.2136276230024,52.2943073388984,52.3780542392129,52.4616961110549,
52.548417940162,52.6319027033865,52.7153500216485,52.7987779830063,52.8822046585315,
52.9656778285902,53.0491789172906,53.1327580827016,53.1554707439118),
 .UNSPECIFIED.);
#80=B_SPLINE_CURVE_WITH_KNOTS('',3,(#20518,#20519,#20520,#20521,#20522,
#20523,#20524,#20525,#20526,#20527),.UNSPECIFIED.,.F.,.F.,(4,3,3,4),(46.872199078263,
46.9544540684318,47.039171936041,47.1238898036503),.UNSPECIFIED.);
#81=B_SPLINE_CURVE_WITH_KNOTS('',3,(#20529,#20530,#20531,#20532,#20533,
#20534,#20535,#20536,#20537,#20538),.UNSPECIFIED.,.F.,.F.,(4,3,3,4),(46.873531912371,
46.960478001365,47.047291421921,47.1238898038316),.UNSPECIFIED.);
#82=B_SPLINE_CURVE_WITH_KNOTS('',3,(#20539,#20540,#20541,#20542,#20543,
#20544,#20545,#20546,#20547,#20548,#20549,#20550,#20551,#20552,#20553,#20554,
#20555,#20556,#20557,#20558,#20559,#20560,#20561,#20562,#20563,#20564,#20565,
#20566,#20567,#20568,#20569,#20570,#20571,#20572,#20573,#20574,#20575,#20576,
#20577,#20578,#20579,#20580,#20581,#20582,#20583,#20584,#20585,#20586,#20587,
#20588,#20589,#20590,#20591,#20592,#20593,#20594,#20595,#20596,#20597,#20598,
#20599,#20600,#20601,#20602,#20603,#20604,#20605,#20606,#20607,#20608,#20609,
#20610,#20611,#20612,#20613,#20614,#20615,#20616,#20617,#20618,#20619,#20620,
#20621,#20622,#20623,#20624,#20625,#20626,#20627,#20628,#20629,#20630,#20631,
#20632,#20633,#20634,#20635,#20636,#20637,#20638,#20639,#20640,#20641,#20642,
#20643,#20644,#20645,#20646,#20647,#20648,#20649,#20650,#20651,#20652,#20653,
#20654,#20655,#20656,#20657,#20658,#20659,#20660,#20661,#20662,#20663,#20664,
#20665,#20666,#20667,#20668,#20669,#20670,#20671,#20672,#20673,#20674,#20675,
#20676,#20677,#20678,#20679,#20680,#20681,#20682,#20683,#20684,#20685,#20686,
#20687,#20688,#20689,#20690,#20691,#20692,#20693,#20694,#20695,#20696,#20697,
#20698,#20699,#20700,#20701,#20702,#20703,#20704,#20705,#20706,#20707,#20708,
#20709,#20710,#20711,#20712,#20713,#20714,#20715,#20716,#20717,#20718,#20719,
#20720,#20721,#20722,#20723,#20724,#20725,#20726,#20727,#20728,#20729,#20730,
#20731,#20732,#20733,#20734,#20735,#20736,#20737,#20738,#20739,#20740,#20741,
#20742,#20743,#20744,#20745,#20746,#20747,#20748,#20749,#20750,#20751,#20752,
#20753,#20754,#20755,#20756,#20757,#20758),.UNSPECIFIED.,.F.,.F.,(4,3,3,
3,3,3,3,3,3,3,3,3,3,3,3,3,3,3,3,3,3,3,3,3,3,3,3,3,3,3,3,3,3,3,3,3,3,3,3,
3,3,3,3,3,3,3,3,3,3,3,3,3,3,3,3,3,3,3,3,3,3,3,3,3,3,3,3,3,3,3,3,3,3,4),
(47.123889804,47.2119695169777,47.3001901238871,47.3886427955167,47.4772210930821,
47.5660058086749,47.6059179050124,47.6896566168586,47.7732921282264,47.8568445716251,
47.9403340074762,48.0237879580902,48.1072244519367,48.1906615616924,48.2741173566102,
48.3576618493402,48.4412509322814,48.5249741998393,48.6056539157326,48.6893926275784,
48.7730281389457,48.8565805823441,48.940070018195,49.0235239688085,49.1069604626546,
49.1903975724099,49.2738533673274,49.3573978600569,49.4409869429977,49.5247102105551,
49.6053899264527,49.6891286382987,49.7727641496662,49.8563165930648,49.9398060289159,
50.0232599795296,50.1066964733759,50.1901335831314,50.2735893780492,50.3571338707789,
50.4407229537199,50.5244462212776,50.6051259371728,50.6888646490187,50.7725001603863,
50.8560526037849,50.9395420396359,51.0229959902495,51.1064324840958,51.1898695938513,
51.273325388769,51.3568698814987,51.4404589644397,51.5241822319973,51.604861947893,
51.688600659739,51.7722361711065,51.8557886145051,51.939278050356,52.0227320009698,
52.1061684948161,52.1896056045716,52.2730613994893,52.356605892219,52.44019497516,
52.5239182427177,52.6045979586131,52.6871060320478,52.7695180670308,52.8518532668798,
52.934128908709,53.0163690882775,53.0986070875677,53.1554762266557),
 .UNSPECIFIED.);
#83=B_SPLINE_CURVE_WITH_KNOTS('',3,(#20764,#20765,#20766,#20767,#20768,
#20769,#20770,#20771,#20772,#20773,#20774,#20775,#20776,#20777,#20778,#20779,
#20780,#20781,#20782,#20783,#20784,#20785,#20786,#20787,#20788,#20789,#20790,
#20791,#20792,#20793,#20794,#20795,#20796,#20797,#20798,#20799,#20800,#20801,
#20802,#20803,#20804,#20805,#20806,#20807,#20808,#20809,#20810,#20811,#20812,
#20813,#20814,#20815,#20816,#20817,#20818,#20819,#20820,#20821,#20822,#20823,
#20824,#20825,#20826,#20827,#20828,#20829,#20830,#20831,#20832,#20833,#20834,
#20835,#20836,#20837,#20838,#20839,#20840,#20841,#20842,#20843,#20844,#20845,
#20846,#20847,#20848,#20849,#20850,#20851,#20852,#20853,#20854,#20855,#20856,
#20857,#20858,#20859,#20860,#20861,#20862,#20863,#20864,#20865,#20866,#20867,
#20868,#20869,#20870,#20871,#20872,#20873,#20874,#20875,#20876,#20877,#20878,
#20879,#20880,#20881,#20882,#20883,#20884,#20885,#20886,#20887,#20888,#20889,
#20890,#20891,#20892,#20893,#20894,#20895,#20896,#20897,#20898,#20899,#20900,
#20901,#20902,#20903,#20904,#20905,#20906,#20907,#20908,#20909,#20910,#20911,
#20912,#20913,#20914,#20915,#20916,#20917,#20918,#20919,#20920,#20921,#20922,
#20923,#20924,#20925,#20926,#20927,#20928,#20929,#20930,#20931,#20932,#20933,
#20934,#20935,#20936,#20937,#20938,#20939,#20940,#20941,#20942,#20943,#20944,
#20945,#20946,#20947,#20948,#20949,#20950,#20951,#20952,#20953,#20954,#20955,
#20956,#20957,#20958,#20959,#20960,#20961,#20962,#20963,#20964,#20965,#20966,
#20967,#20968,#20969,#20970,#20971,#20972,#20973,#20974,#20975,#20976,#20977,
#20978,#20979,#20980,#20981,#20982,#20983),.UNSPECIFIED.,.F.,.F.,(4,3,3,
3,3,3,3,3,3,3,3,3,3,3,3,3,3,3,3,3,3,3,3,3,3,3,3,3,3,3,3,3,3,3,3,3,3,3,3,
3,3,3,3,3,3,3,3,3,3,3,3,3,3,3,3,3,3,3,3,3,3,3,3,3,3,3,3,3,3,3,3,3,3,4),
(53.4070751111425,53.4896343762135,53.5721034786018,53.6545035043015,53.7368608751334,
53.819197084156,53.9015310878447,53.9838818385131,54.066316941824,54.1487965694145,
54.2314023405145,54.2937793603386,54.3775180721845,54.4611535835521,54.5447060269508,
54.6281954628017,54.7116494134154,54.7950859072616,54.8785230170172,54.9619788119348,
55.0455233046645,55.1291123876056,55.2128356551632,55.2935153710587,55.3772540829047,
55.4608895942722,55.5444420376709,55.627931473522,55.7113854241356,55.7948219179819,
55.8782590277374,55.961714822655,56.0452593153847,56.1288483983257,56.2125716658834,
56.2932513817789,56.3769900936248,56.4606256049923,56.5441780483911,56.6276674842419,
56.7111214348556,56.7945579287019,56.8779950384574,56.9614508333752,57.0449953261048,
57.1285844090459,57.2123076766035,57.292987392499,57.376726104345,57.4603616157126,
57.5439140591111,57.6274034949616,57.7108574455754,57.7942939394216,57.8777310491771,
57.9611868440946,58.0447313368243,58.1283204197652,58.2120436873228,58.2927234032191,
58.3764621150651,58.4600976264325,58.5436500698315,58.6271395056821,58.7105934562957,
58.7940299501419,58.8774670598972,58.9609228548147,59.0444673475445,59.1280564304858,
59.2117796980434,59.2924594139393,59.3857393267099,59.4398822683535),
 .UNSPECIFIED.);
#84=B_SPLINE_CURVE_WITH_KNOTS('',3,(#20984,#20985,#20986,#20987,#20988,
#20989,#20990,#20991,#20992,#20993),.UNSPECIFIED.,.F.,.F.,(4,3,3,4),(53.1554707439118,
53.2392036250967,53.2940433496185,53.4070751110074),.UNSPECIFIED.);
#85=B_SPLINE_CURVE_WITH_KNOTS('',3,(#20995,#20996,#20997,#20998,#20999,
#21000,#21001,#21002,#21003,#21004),.UNSPECIFIED.,.F.,.F.,(4,3,3,4),(53.1554762266557,
53.2377493943412,53.3224122526225,53.4070751109039),.UNSPECIFIED.);
#86=B_SPLINE_CURVE_WITH_KNOTS('',3,(#21005,#21006,#21007,#21008,#21009,
#21010,#21011,#21012,#21013,#21014,#21015,#21016,#21017,#21018,#21019,#21020,
#21021,#21022,#21023,#21024,#21025,#21026,#21027,#21028,#21029,#21030,#21031,
#21032,#21033,#21034,#21035,#21036,#21037,#21038,#21039,#21040,#21041,#21042,
#21043,#21044,#21045,#21046,#21047,#21048,#21049,#21050,#21051,#21052,#21053,
#21054,#21055,#21056,#21057,#21058,#21059,#21060,#21061,#21062,#21063,#21064,
#21065,#21066,#21067,#21068,#21069,#21070,#21071,#21072,#21073,#21074,#21075,
#21076,#21077,#21078,#21079,#21080,#21081,#21082,#21083,#21084,#21085,#21086,
#21087,#21088,#21089,#21090,#21091,#21092,#21093,#21094,#21095,#21096,#21097,
#21098,#21099,#21100,#21101,#21102,#21103,#21104,#21105,#21106,#21107,#21108,
#21109,#21110,#21111,#21112,#21113,#21114,#21115,#21116,#21117,#21118,#21119,
#21120,#21121,#21122,#21123,#21124,#21125,#21126,#21127,#21128,#21129,#21130,
#21131,#21132,#21133,#21134,#21135,#21136,#21137,#21138,#21139,#21140,#21141,
#21142,#21143,#21144,#21145,#21146,#21147,#21148,#21149,#21150,#21151,#21152,
#21153,#21154,#21155,#21156,#21157,#21158,#21159,#21160,#21161,#21162,#21163,
#21164,#21165,#21166,#21167,#21168,#21169,#21170,#21171,#21172,#21173,#21174,
#21175,#21176,#21177,#21178,#21179,#21180,#21181,#21182,#21183,#21184,#21185,
#21186,#21187,#21188,#21189,#21190,#21191,#21192,#21193,#21194,#21195,#21196,
#21197,#21198,#21199,#21200,#21201,#21202,#21203,#21204,#21205,#21206,#21207,
#21208,#21209,#21210,#21211,#21212,#21213,#21214,#21215,#21216,#21217,#21218,
#21219,#21220,#21221),.UNSPECIFIED.,.F.,.F.,(4,3,3,3,3,3,3,3,3,3,3,3,3,
3,3,3,3,3,3,3,3,3,3,3,3,3,3,3,3,3,3,3,3,3,3,3,3,3,3,3,3,3,3,3,3,3,3,3,3,
3,3,3,3,3,3,3,3,3,3,3,3,3,3,3,3,3,3,3,3,3,3,3,4),(53.4070751110112,53.5281266875687,
53.6043339693332,53.6880726811791,53.7717081925466,53.8552606359451,53.9387500717959,
54.0222040224095,54.1056405162557,54.1890776260112,54.2725334209287,54.3560779136583,
54.4396669965993,54.5233902641568,54.6040699800534,54.6878086918993,54.7714442032668,
54.8549966466653,54.9384860825163,55.02194003313,55.1053765269762,55.1888136367316,
55.2722694316493,55.3558139243789,55.4394030073199,55.5231262748775,55.6038059907735,
55.6875447026194,55.771180213987,55.8547326573855,55.9382220932365,56.0216760438502,
56.1051125376965,56.188549647452,56.2720054423696,56.3555499350993,56.4391390180403,
56.522862285598,56.6035420014936,56.6872807133395,56.7709162247071,56.8544686681056,
56.9379581039566,57.0214120545703,57.1048485484165,57.188285658172,57.2717414530897,
57.3552859458194,57.4388750287604,57.522598296318,57.6032780122137,57.6870167240596,
57.7706522354271,57.8542046788257,57.9376941146768,58.0211480652904,58.1045845591367,
58.1880216688921,58.2714774638097,58.3550219565394,58.4386110394804,58.522334307038,
58.6030140229339,58.6867625271259,58.7704056656083,58.8539487725955,58.9374351492175,
59.0208829145339,59.1043101578345,59.1878874695081,59.2713533662358,59.3549863853822,
59.4386194045287),.UNSPECIFIED.);
#87=B_SPLINE_CURVE_WITH_KNOTS('',3,(#21227,#21228,#21229,#21230,#21231,
#21232,#21233,#21234,#21235,#21236,#21237,#21238,#21239,#21240,#21241,#21242,
#21243,#21244,#21245,#21246,#21247,#21248,#21249,#21250,#21251,#21252,#21253,
#21254,#21255,#21256,#21257,#21258,#21259,#21260,#21261,#21262,#21263,#21264,
#21265,#21266,#21267,#21268,#21269,#21270,#21271,#21272,#21273,#21274,#21275,
#21276,#21277,#21278,#21279,#21280,#21281,#21282,#21283,#21284,#21285,#21286,
#21287,#21288,#21289,#21290,#21291,#21292,#21293,#21294,#21295,#21296,#21297,
#21298,#21299,#21300,#21301,#21302,#21303,#21304,#21305,#21306,#21307,#21308,
#21309,#21310,#21311,#21312,#21313,#21314,#21315,#21316,#21317,#21318,#21319,
#21320,#21321,#21322,#21323,#21324,#21325,#21326,#21327,#21328,#21329,#21330,
#21331,#21332,#21333,#21334,#21335,#21336,#21337,#21338,#21339,#21340,#21341,
#21342,#21343,#21344,#21345,#21346,#21347,#21348,#21349,#21350,#21351,#21352,
#21353,#21354,#21355,#21356,#21357,#21358,#21359,#21360,#21361,#21362,#21363,
#21364,#21365,#21366,#21367,#21368,#21369,#21370,#21371,#21372,#21373,#21374,
#21375,#21376,#21377,#21378,#21379,#21380,#21381,#21382,#21383,#21384,#21385,
#21386,#21387,#21388,#21389,#21390,#21391,#21392,#21393,#21394,#21395,#21396,
#21397,#21398,#21399,#21400,#21401,#21402,#21403,#21404,#21405,#21406,#21407,
#21408,#21409,#21410,#21411,#21412,#21413,#21414,#21415,#21416,#21417,#21418,
#21419,#21420,#21421,#21422,#21423,#21424,#21425,#21426,#21427,#21428,#21429,
#21430,#21431,#21432,#21433,#21434,#21435,#21436,#21437,#21438,#21439,#21440,
#21441,#21442,#21443,#21444,#21445,#21446),.UNSPECIFIED.,.F.,.F.,(4,3,3,
3,3,3,3,3,3,3,3,3,3,3,3,3,3,3,3,3,3,3,3,3,3,3,3,3,3,3,3,3,3,3,3,3,3,3,3,
3,3,3,3,3,3,3,3,3,3,3,3,3,3,3,3,3,3,3,3,3,3,3,3,3,3,3,3,3,3,3,3,3,3,4),
(59.6902604181869,59.7747787530522,59.8593179788568,59.9438945410883,60.0309697619811,
60.1157222054673,60.2039588150634,60.2921954246594,60.3759341365053,60.4595696478729,
60.5431220912715,60.6266115271223,60.710065477736,60.7935019715823,60.8769390813379,
60.9603948762555,61.0439393689852,61.1275284519262,61.2112517194837,61.2919314353795,
61.3756701472254,61.4593056585929,61.5428581019914,61.6263475378422,61.7098014884559,
61.7932379823021,61.8766750920576,61.9601308869752,62.0436753797049,62.1272644626459,
62.2109877302035,62.2916674460996,62.3754061579455,62.459041669313,62.5425941127115,
62.6260835485626,62.7095374991762,62.7929739930223,62.8764111027777,62.959866897695,
63.0434113904248,63.1270004733656,63.2107237409232,63.2914034568198,63.3751421686657,
63.4587776800333,63.5423301234322,63.6258195592835,63.7092735098971,63.7927100037433,
63.8761471134986,63.9596029084161,64.0431474011459,64.1267364840869,64.2104597516445,
64.2911394675399,64.3748781793858,64.4585136907535,64.5420661341521,64.625555570003,
64.7090095206166,64.792446014463,64.8758831242186,64.9593389191362,65.0428834118659,
65.1264724948068,65.2101957623644,65.29087547826,65.3743504055609,65.4613697556974,
65.544635511258,65.6278429630006,65.7110052807257,65.7224278061069),
 .UNSPECIFIED.);
#88=B_SPLINE_CURVE_WITH_KNOTS('',3,(#21447,#21448,#21449,#21450,#21451,
#21452,#21453,#21454,#21455,#21456),.UNSPECIFIED.,.F.,.F.,(4,3,3,4),(59.4398822683535,
59.5326783695403,59.6250277789513,59.6902604180037),.UNSPECIFIED.);
#89=B_SPLINE_CURVE_WITH_KNOTS('',3,(#21458,#21459,#21460,#21461,#21462,
#21463,#21464,#21465,#21466,#21467),.UNSPECIFIED.,.F.,.F.,(4,3,3,4),(59.4386194045287,
59.5223427634998,59.602750033654,59.6902604181908),.UNSPECIFIED.);
#90=B_SPLINE_CURVE_WITH_KNOTS('',3,(#21468,#21469,#21470,#21471,#21472,
#21473,#21474,#21475,#21476,#21477,#21478,#21479,#21480,#21481,#21482,#21483,
#21484,#21485,#21486,#21487,#21488,#21489,#21490,#21491,#21492,#21493,#21494,
#21495,#21496,#21497,#21498,#21499,#21500,#21501,#21502,#21503,#21504,#21505,
#21506,#21507,#21508,#21509,#21510,#21511,#21512,#21513,#21514,#21515,#21516,
#21517,#21518,#21519,#21520,#21521,#21522,#21523,#21524,#21525,#21526,#21527,
#21528,#21529,#21530,#21531,#21532,#21533,#21534,#21535,#21536,#21537,#21538,
#21539,#21540,#21541,#21542,#21543,#21544,#21545,#21546,#21547,#21548,#21549,
#21550,#21551,#21552,#21553,#21554,#21555,#21556,#21557,#21558,#21559,#21560,
#21561,#21562,#21563,#21564,#21565,#21566,#21567,#21568,#21569,#21570,#21571,
#21572,#21573,#21574,#21575,#21576,#21577,#21578,#21579,#21580,#21581,#21582,
#21583,#21584,#21585,#21586,#21587,#21588,#21589,#21590,#21591,#21592,#21593,
#21594,#21595,#21596,#21597,#21598,#21599,#21600,#21601,#21602,#21603,#21604,
#21605,#21606,#21607,#21608,#21609,#21610,#21611,#21612,#21613,#21614,#21615,
#21616,#21617,#21618,#21619,#21620,#21621,#21622,#21623,#21624,#21625,#21626,
#21627,#21628,#21629,#21630,#21631,#21632,#21633,#21634,#21635,#21636,#21637,
#21638,#21639,#21640,#21641,#21642,#21643,#21644,#21645,#21646,#21647,#21648,
#21649,#21650,#21651,#21652,#21653,#21654,#21655,#21656,#21657,#21658,#21659,
#21660,#21661,#21662,#21663,#21664,#21665,#21666,#21667,#21668,#21669,#21670,
#21671,#21672,#21673,#21674,#21675,#21676,#21677,#21678,#21679,#21680,#21681,
#21682,#21683,#21684,#21685,#21686,#21687),.UNSPECIFIED.,.F.,.F.,(4,3,3,
3,3,3,3,3,3,3,3,3,3,3,3,3,3,3,3,3,3,3,3,3,3,3,3,3,3,3,3,3,3,3,3,3,3,3,3,
3,3,3,3,3,3,3,3,3,3,3,3,3,3,3,3,3,3,3,3,3,3,3,3,3,3,3,3,3,3,3,3,3,3,4),
(59.690260418325,59.7729922509435,59.8556292811794,59.9381925013212,60.0212291942028,
60.1037176127869,60.1861993999656,60.2686934103523,60.3521415688578,60.4347588661806,
60.5186224552774,60.6024860443741,60.68622475622,60.7698602675875,60.8534127109862,
60.936902146837,61.0203560974506,61.1037925912969,61.1872297010523,61.2706854959699,
61.3542299886996,61.4378190716406,61.5215423391982,61.6022220550943,61.6859607669403,
61.7695962783077,61.8531487217063,61.9366381575571,62.0200921081707,62.1035286020169,
62.1869657117725,62.2704215066901,62.3539659994198,62.4375550823607,62.5212783499182,
62.6019580658144,62.6856967776603,62.7693322890281,62.8528847324265,62.9363741682772,
63.0198281188909,63.1032646127372,63.1867017224929,63.2701575174107,63.3537020101404,
63.4372910930814,63.521014360639,63.6016940765345,63.6854327883804,63.7690682997479,
63.8526207431468,63.9361101789976,64.0195641296113,64.1030006234575,64.1864377332125,
64.2698935281301,64.3534380208598,64.4370271038007,64.5207503713583,64.6014300872547,
64.6851687991007,64.7688043104682,64.8523567538665,64.9358461897175,65.0193001403312,
65.1027366341774,65.186173743933,65.269629538851,65.3531740315807,65.4367631145216,
65.5204863820792,65.6011660979748,65.6963168570349,65.7229944280855),
 .UNSPECIFIED.);
#91=B_SPLINE_CURVE_WITH_KNOTS('',3,(#21693,#21694,#21695,#21696,#21697,
#21698,#21699,#21700,#21701,#21702,#21703,#21704,#21705,#21706,#21707,#21708,
#21709,#21710,#21711,#21712,#21713,#21714,#21715,#21716,#21717,#21718,#21719,
#21720,#21721,#21722,#21723,#21724,#21725,#21726,#21727,#21728,#21729,#21730,
#21731,#21732,#21733,#21734,#21735,#21736,#21737,#21738,#21739,#21740,#21741,
#21742,#21743,#21744,#21745,#21746,#21747,#21748,#21749,#21750,#21751,#21752,
#21753,#21754,#21755,#21756,#21757,#21758,#21759,#21760,#21761,#21762,#21763,
#21764,#21765,#21766,#21767,#21768,#21769,#21770,#21771,#21772,#21773,#21774,
#21775,#21776,#21777,#21778,#21779,#21780,#21781,#21782,#21783,#21784,#21785,
#21786,#21787,#21788,#21789,#21790,#21791,#21792,#21793,#21794,#21795,#21796,
#21797,#21798,#21799,#21800,#21801,#21802,#21803,#21804,#21805,#21806,#21807,
#21808,#21809,#21810,#21811,#21812,#21813,#21814,#21815,#21816,#21817,#21818,
#21819,#21820,#21821,#21822,#21823,#21824,#21825,#21826,#21827,#21828,#21829,
#21830,#21831,#21832,#21833,#21834,#21835,#21836,#21837,#21838,#21839,#21840,
#21841,#21842,#21843,#21844,#21845,#21846,#21847,#21848,#21849,#21850,#21851,
#21852,#21853,#21854,#21855,#21856,#21857,#21858,#21859,#21860,#21861,#21862,
#21863,#21864,#21865,#21866,#21867,#21868,#21869,#21870,#21871,#21872,#21873,
#21874,#21875,#21876,#21877,#21878,#21879,#21880,#21881,#21882,#21883,#21884,
#21885,#21886,#21887,#21888,#21889,#21890,#21891,#21892,#21893,#21894,#21895,
#21896,#21897,#21898,#21899,#21900,#21901,#21902,#21903,#21904,#21905,#21906,
#21907,#21908,#21909,#21910,#21911,#21912),.UNSPECIFIED.,.F.,.F.,(4,3,3,
3,3,3,3,3,3,3,3,3,3,3,3,3,3,3,3,3,3,3,3,3,3,3,3,3,3,3,3,3,3,3,3,3,3,3,3,
3,3,3,3,3,3,3,3,3,3,3,3,3,3,3,3,3,3,3,3,3,3,3,3,3,3,3,3,3,3,3,3,3,3,4),
(65.973445725537,66.0722016376632,66.1716623230831,66.2718883360919,66.2906114889802,
66.3743502008262,66.4579857121937,66.5415381555923,66.6250275914434,66.7084815420572,
66.7919180359034,66.875355145659,66.9588109405769,67.0423554333066,67.1259445162477,
67.2096677838053,67.2903474997003,67.3740862115462,67.4577217229137,67.5412741663122,
67.6247636021632,67.7082175527769,67.7916540466231,67.8750911563786,67.9585469512962,
68.0420914440259,68.1256805269669,68.2094037945244,68.2900835104204,68.3738222222663,
68.4574577336338,68.5410101770324,68.6244996128835,68.7079535634972,68.7913900573434,
68.8748271670989,68.9582829620166,69.0418274547463,69.1254165376873,69.2091398052449,
69.2898195211405,69.3735582329864,69.4571937443539,69.5407461877524,69.6242356236035,
69.7076895742171,69.7911260680634,69.8745631778188,69.9580189727365,70.0415634654662,
70.1251525484071,70.2088758159647,70.2895555318607,70.3732942437067,70.4569297550742,
70.5404821984727,70.6239716343238,70.7074255849375,70.7908620787838,70.8742991885393,
70.957754983457,71.0412994761868,71.1248885591278,71.2086118266854,71.2892915425808,
71.3726036548392,71.4557840971122,71.5388885214543,71.6219354908015,71.7049435228024,
71.7879472022301,71.8709469547149,71.9539898147039,72.0048655224089),
 .UNSPECIFIED.);
#92=B_SPLINE_CURVE_WITH_KNOTS('',3,(#21913,#21914,#21915,#21916,#21917,
#21918,#21919,#21920,#21921,#21922),.UNSPECIFIED.,.F.,.F.,(4,3,3,4),(65.7224278061069,
65.8055735571319,65.8895096412492,65.9734457253665),.UNSPECIFIED.);
#93=B_SPLINE_CURVE_WITH_KNOTS('',3,(#21924,#21925,#21926,#21927,#21928,
#21929,#21930,#21931,#21932,#21933),.UNSPECIFIED.,.F.,.F.,(4,3,3,4),(65.7229944280855,
65.8176176411345,65.9116665109351,65.9734457253704),.UNSPECIFIED.);
#94=B_SPLINE_CURVE_WITH_KNOTS('',3,(#21934,#21935,#21936,#21937,#21938,
#21939,#21940,#21941,#21942,#21943),.UNSPECIFIED.,.F.,.F.,(4,1,1,1,1,1,
1,4),(65.9734457253704,66.6009021086949,67.6006381194151,68.6003741301352,
69.6001101408553,70.5998461515754,71.5995821622956,72.0060503087704),
 .UNSPECIFIED.);
#95=B_SPLINE_CURVE_WITH_KNOTS('',3,(#21949,#21950,#21951,#21952,#21953,
#21954,#21955,#21956,#21957,#21958,#21959,#21960,#21961,#21962,#21963,#21964,
#21965,#21966,#21967,#21968,#21969,#21970,#21971,#21972,#21973,#21974,#21975,
#21976,#21977,#21978,#21979,#21980,#21981,#21982,#21983,#21984,#21985,#21986,
#21987,#21988,#21989,#21990,#21991,#21992,#21993,#21994,#21995,#21996,#21997,
#21998,#21999,#22000,#22001,#22002,#22003,#22004,#22005,#22006,#22007,#22008,
#22009,#22010,#22011,#22012,#22013,#22014,#22015,#22016,#22017,#22018,#22019,
#22020,#22021,#22022,#22023,#22024,#22025,#22026,#22027,#22028,#22029,#22030,
#22031,#22032,#22033,#22034,#22035,#22036,#22037,#22038,#22039,#22040,#22041,
#22042,#22043,#22044,#22045,#22046,#22047,#22048,#22049,#22050,#22051,#22052,
#22053,#22054,#22055,#22056,#22057,#22058,#22059,#22060,#22061,#22062,#22063,
#22064,#22065,#22066,#22067,#22068,#22069,#22070,#22071,#22072,#22073,#22074,
#22075,#22076,#22077,#22078,#22079,#22080,#22081,#22082,#22083,#22084,#22085,
#22086,#22087,#22088,#22089,#22090,#22091,#22092,#22093,#22094,#22095,#22096,
#22097,#22098,#22099,#22100,#22101,#22102,#22103,#22104,#22105,#22106,#22107,
#22108,#22109,#22110,#22111,#22112,#22113,#22114,#22115,#22116,#22117,#22118,
#22119,#22120,#22121,#22122,#22123,#22124,#22125,#22126,#22127,#22128,#22129,
#22130,#22131,#22132,#22133,#22134,#22135,#22136,#22137,#22138,#22139,#22140,
#22141,#22142,#22143,#22144,#22145,#22146,#22147,#22148,#22149,#22150,#22151,
#22152,#22153,#22154,#22155,#22156,#22157,#22158,#22159,#22160,#22161,#22162,
#22163,#22164,#22165,#22166,#22167,#22168,#22169,#22170,#22171),
 .UNSPECIFIED.,.F.,.F.,(4,3,3,3,3,3,3,3,3,3,3,3,3,3,3,3,3,3,3,3,3,3,3,3,
3,3,3,3,3,3,3,3,3,3,3,3,3,3,3,3,3,3,3,3,3,3,3,3,3,3,3,3,3,3,3,3,3,3,3,3,
3,3,3,3,3,3,3,3,3,3,3,3,3,3,4),(72.2566310325461,72.2890275533009,72.3727662651468,
72.4564017765142,72.5399542199127,72.6234436557635,72.7068976063771,72.7903341002233,
72.8737712099786,72.9572270048961,73.0407714976257,73.1243605805666,73.2080838481241,
73.2887635640211,73.372502275867,73.4561377872345,73.539690230633,73.6231796664841,
73.7066336170977,73.790070110944,73.8735072206994,73.956963015617,74.0405075083467,
74.1240965912877,74.2078198588453,74.2884995747412,74.3722382865871,74.4558737979546,
74.5394262413532,74.6229156772043,74.7063696278179,74.7898061216642,74.8732432314197,
74.9566990263373,75.0402435190669,75.1238326020079,75.2075558695655,75.2882355854613,
75.3719742973073,75.4556098086748,75.5391622520734,75.6226516879244,75.7061056385381,
75.7895421323844,75.87297924214,75.9564350370577,76.0399795297874,76.1235686127284,
76.207291880286,76.2879715961814,76.3717103080273,76.4553458193948,76.5388982627933,
76.6223876986444,76.7058416492581,76.7892781431043,76.8727152528598,76.9561710477774,
77.0397155405071,77.1233046234481,77.2070278910057,77.2877076069016,77.3714463187476,
77.4550818301151,77.5386342735135,77.6221237093646,77.7055776599783,77.7890141538246,
77.8724512635801,77.9559070584978,78.0394515512275,78.1230406341685,78.2067639017261,
78.2874436176217,78.2887592231474),.UNSPECIFIED.);
#96=B_SPLINE_CURVE_WITH_KNOTS('',3,(#22172,#22173,#22174,#22175,#22176,
#22177,#22178,#22179,#22180,#22181),.UNSPECIFIED.,.F.,.F.,(4,3,3,4),(72.0048655224089,
72.0880045572239,72.172317794814,72.256631032404),.UNSPECIFIED.);
#97=B_SPLINE_CURVE_WITH_KNOTS('',3,(#22183,#22184,#22185,#22186),
 .UNSPECIFIED.,.F.,.F.,(4,4),(72.0060503087704,72.2566310325499),
 .UNSPECIFIED.);
#98=B_SPLINE_CURVE_WITH_KNOTS('',3,(#22187,#22188,#22189,#22190,#22191,
#22192,#22193,#22194,#22195,#22196),.UNSPECIFIED.,.F.,.F.,(4,1,1,1,1,1,
1,4),(72.2566310325499,72.5993181730157,73.5990541837358,74.598790194456,
75.5985262051761,76.5982622158962,77.5979982266164,78.2879140477243),
 .UNSPECIFIED.);
#99=B_SPLINE_CURVE_WITH_KNOTS('',3,(#22202,#22203,#22204,#22205,#22206,
#22207,#22208,#22209,#22210,#22211,#22212,#22213,#22214,#22215,#22216,#22217,
#22218,#22219,#22220,#22221,#22222,#22223,#22224,#22225,#22226,#22227,#22228,
#22229,#22230,#22231,#22232,#22233,#22234,#22235,#22236,#22237,#22238,#22239,
#22240,#22241,#22242,#22243,#22244,#22245,#22246,#22247,#22248,#22249,#22250,
#22251,#22252,#22253,#22254,#22255,#22256,#22257,#22258,#22259,#22260,#22261,
#22262,#22263,#22264,#22265,#22266,#22267,#22268,#22269,#22270,#22271,#22272,
#22273,#22274,#22275,#22276,#22277,#22278,#22279,#22280,#22281,#22282,#22283,
#22284,#22285,#22286,#22287,#22288,#22289,#22290,#22291,#22292,#22293,#22294,
#22295,#22296,#22297,#22298,#22299,#22300,#22301,#22302,#22303,#22304,#22305,
#22306,#22307,#22308,#22309,#22310,#22311,#22312,#22313,#22314,#22315,#22316,
#22317,#22318,#22319,#22320,#22321,#22322,#22323,#22324,#22325,#22326,#22327,
#22328,#22329,#22330,#22331,#22332,#22333,#22334,#22335,#22336,#22337,#22338,
#22339,#22340,#22341,#22342,#22343,#22344,#22345,#22346,#22347,#22348,#22349,
#22350,#22351,#22352,#22353,#22354,#22355,#22356,#22357,#22358,#22359,#22360,
#22361,#22362,#22363,#22364,#22365,#22366,#22367,#22368,#22369,#22370,#22371,
#22372,#22373,#22374,#22375,#22376,#22377,#22378,#22379,#22380,#22381,#22382,
#22383,#22384,#22385,#22386,#22387,#22388,#22389,#22390,#22391,#22392,#22393,
#22394,#22395,#22396,#22397,#22398,#22399,#22400,#22401,#22402,#22403,#22404,
#22405,#22406,#22407,#22408,#22409,#22410,#22411,#22412,#22413,#22414,#22415,
#22416,#22417,#22418,#22419,#22420,#22421),.UNSPECIFIED.,.F.,.F.,(4,3,3,
3,3,3,3,3,3,3,3,3,3,3,3,3,3,3,3,3,3,3,3,3,3,3,3,3,3,3,3,3,3,3,3,3,3,3,3,
3,3,3,3,3,3,3,3,3,3,3,3,3,3,3,3,3,3,3,3,3,3,3,3,3,3,3,3,3,3,3,3,3,3,4),
(78.5398163397257,78.62239295459,78.705491288809,78.7879946449525,78.8704919407165,
78.9530020139644,79.0365464175588,79.1191811714259,79.2031803998838,79.2871796283418,
79.3709183401877,79.4545538515552,79.5381062949538,79.6215957308051,79.7050496814187,
79.788486175265,79.8719232850204,79.955379079938,80.0389235726677,80.1225126556086,
80.2062359231661,80.286915639062,80.3706543509079,80.4542898622755,80.5378423056737,
80.6213317415248,80.7047856921384,80.7882221859847,80.8716592957401,80.9551150906578,
81.0386595833875,81.1222486663285,81.2059719338861,81.2866516497821,81.370390361628,
81.4540258729957,81.5375783163942,81.6210677522452,81.7045217028589,81.7879581967051,
81.8713953064607,81.9548511013783,82.038395594108,82.121984677049,82.2057079446065,
82.2863876605022,82.3701263723481,82.4537618837154,82.5373143271138,82.6208037629648,
82.7042577135786,82.787694207425,82.8711313171803,82.9545871120976,83.0381316048273,
83.1217206877683,83.2054439553258,83.2861236712224,83.3698623830682,83.4534978944356,
83.5370503378342,83.6205397736848,83.7039937242985,83.7874302181448,83.8708673279002,
83.9543231228179,84.0378676155475,84.1214566984884,84.2051799660461,84.2858596819425,
84.3725698184977,84.4591613046955,84.5456123157065,84.5725992439732),
 .UNSPECIFIED.);
#100=B_SPLINE_CURVE_WITH_KNOTS('',3,(#22422,#22423,#22424,#22425,#22426,
#22427,#22428,#22429,#22430,#22431),.UNSPECIFIED.,.F.,.F.,(4,3,3,4),(78.2887592231474,
78.3981054868849,78.5051444124938,78.5398163395285),.UNSPECIFIED.);
#101=B_SPLINE_CURVE_WITH_KNOTS('',3,(#22433,#22434,#22435,#22436),
 .UNSPECIFIED.,.F.,.F.,(4,4),(78.2879140477243,78.5398092039209),
 .UNSPECIFIED.);
#102=B_SPLINE_CURVE_WITH_KNOTS('',3,(#22437,#22438,#22439,#22440,#22441,
#22442,#22443,#22444,#22445,#22446,#22447,#22448,#22449,#22450,#22451,#22452,
#22453,#22454,#22455,#22456,#22457,#22458,#22459,#22460,#22461,#22462,#22463,
#22464,#22465,#22466,#22467,#22468,#22469,#22470,#22471,#22472,#22473,#22474,
#22475,#22476,#22477,#22478,#22479,#22480,#22481,#22482,#22483,#22484,#22485,
#22486,#22487,#22488,#22489,#22490,#22491,#22492,#22493,#22494,#22495,#22496,
#22497,#22498,#22499,#22500,#22501,#22502,#22503,#22504,#22505,#22506,#22507,
#22508,#22509,#22510,#22511,#22512,#22513,#22514,#22515,#22516,#22517,#22518,
#22519,#22520,#22521,#22522,#22523,#22524,#22525,#22526,#22527,#22528,#22529,
#22530,#22531,#22532,#22533,#22534,#22535,#22536,#22537,#22538,#22539,#22540,
#22541,#22542,#22543,#22544,#22545,#22546,#22547,#22548,#22549,#22550,#22551,
#22552,#22553,#22554,#22555,#22556,#22557,#22558,#22559,#22560,#22561,#22562,
#22563,#22564,#22565,#22566,#22567,#22568,#22569,#22570,#22571,#22572,#22573,
#22574,#22575,#22576,#22577,#22578,#22579,#22580,#22581,#22582,#22583,#22584,
#22585,#22586,#22587,#22588,#22589,#22590,#22591,#22592,#22593,#22594,#22595,
#22596,#22597,#22598,#22599,#22600,#22601,#22602,#22603,#22604,#22605,#22606,
#22607,#22608,#22609,#22610,#22611,#22612,#22613,#22614,#22615,#22616,#22617,
#22618,#22619,#22620,#22621,#22622,#22623,#22624,#22625,#22626,#22627,#22628,
#22629,#22630,#22631,#22632,#22633,#22634,#22635,#22636,#22637,#22638,#22639,
#22640,#22641,#22642,#22643,#22644,#22645,#22646,#22647,#22648,#22649,#22650,
#22651,#22652,#22653,#22654,#22655,#22656),.UNSPECIFIED.,.F.,.F.,(4,3,3,
3,3,3,3,3,3,3,3,3,3,3,3,3,3,3,3,3,3,3,3,3,3,3,3,3,3,3,3,3,3,3,3,3,3,3,3,
3,3,3,3,3,3,3,3,3,3,3,3,3,3,3,3,3,3,3,3,3,3,3,3,3,3,3,3,3,3,3,3,3,3,4),
(78.5398163397295,78.5977342373365,78.6814729491824,78.7651084605499,78.8486609039486,
78.9321503397996,79.0156042904133,79.0990407842595,79.1824778940149,79.2659336889324,
79.3494781816621,79.4330672646031,79.5167905321606,79.5974702480566,79.6812089599025,
79.76484447127,79.8483969146685,79.9318863505195,80.0153403011332,80.0987767949795,
80.1822139047349,80.2656696996526,80.3492141923823,80.4328032753233,80.5165265428808,
80.5972062587768,80.6809449706228,80.7645804819903,80.8481329253889,80.93162236124,
81.0150763118536,81.0985128056999,81.1819499154554,81.2654057103731,81.3489502031028,
81.4325392860438,81.5162625536014,81.5969422694969,81.6806809813428,81.7643164927103,
81.8478689361088,81.9313583719598,82.0148123225734,82.0982488164197,82.1816859261751,
82.2651417210928,82.3486862138224,82.4322752967634,82.5159985643209,82.596678280217,
82.680416992063,82.7640525034305,82.8476049468291,82.9310943826802,83.0145483332938,
83.0979848271401,83.1814219368956,83.2648777318133,83.348422224543,83.432011307484,
83.5157345750416,83.5964142909372,83.6801543798819,83.7637909471208,83.847344126517,
83.9308339795196,84.0142867067674,84.0977215231147,84.1811565009327,84.264609708774,
84.3481453391041,84.4317253719729,84.5154248974244,84.571795089726),
 .UNSPECIFIED.);
#103=B_SPLINE_CURVE_WITH_KNOTS('',3,(#22662,#22663,#22664,#22665,#22666,
#22667,#22668,#22669,#22670,#22671,#22672,#22673,#22674,#22675,#22676,#22677,
#22678,#22679,#22680,#22681,#22682,#22683,#22684,#22685,#22686,#22687,#22688,
#22689,#22690,#22691,#22692,#22693,#22694,#22695,#22696,#22697,#22698,#22699,
#22700,#22701,#22702,#22703,#22704,#22705,#22706,#22707,#22708,#22709,#22710,
#22711,#22712,#22713,#22714,#22715,#22716,#22717,#22718,#22719,#22720,#22721,
#22722,#22723,#22724,#22725,#22726,#22727,#22728,#22729,#22730,#22731,#22732,
#22733,#22734,#22735,#22736,#22737,#22738,#22739,#22740,#22741,#22742,#22743,
#22744,#22745,#22746,#22747,#22748,#22749,#22750,#22751,#22752,#22753,#22754,
#22755,#22756,#22757,#22758,#22759,#22760,#22761,#22762,#22763,#22764,#22765,
#22766,#22767,#22768,#22769,#22770,#22771,#22772,#22773,#22774,#22775,#22776,
#22777,#22778,#22779,#22780,#22781,#22782,#22783,#22784,#22785,#22786,#22787,
#22788,#22789,#22790,#22791,#22792,#22793,#22794,#22795,#22796,#22797,#22798,
#22799,#22800,#22801,#22802,#22803,#22804,#22805,#22806,#22807,#22808,#22809,
#22810,#22811,#22812,#22813,#22814,#22815,#22816,#22817,#22818,#22819,#22820,
#22821,#22822,#22823,#22824,#22825,#22826,#22827,#22828,#22829,#22830,#22831,
#22832,#22833,#22834,#22835,#22836,#22837,#22838,#22839,#22840,#22841,#22842,
#22843,#22844,#22845,#22846,#22847,#22848,#22849,#22850,#22851,#22852,#22853,
#22854,#22855,#22856,#22857,#22858,#22859,#22860,#22861,#22862,#22863,#22864,
#22865,#22866,#22867,#22868,#22869,#22870,#22871,#22872,#22873,#22874,#22875,
#22876,#22877,#22878,#22879,#22880,#22881),.UNSPECIFIED.,.F.,.F.,(4,3,3,
3,3,3,3,3,3,3,3,3,3,3,3,3,3,3,3,3,3,3,3,3,3,3,3,3,3,3,3,3,3,3,3,3,3,3,3,
3,3,3,3,3,3,3,3,3,3,3,3,3,3,3,3,3,3,3,3,3,3,3,3,3,3,3,3,3,3,3,3,3,3,4),
(84.8230016470632,84.9118882294179,85.0053150952291,85.0946470022648,85.1841250841541,
85.2738132970661,85.2855956926626,85.3693344045085,85.452969915876,85.5365223592745,
85.6200117951256,85.7034657457393,85.7869022395855,85.8703393493409,85.9537951442584,
86.0373396369881,86.1209287199291,86.2046519874867,86.2853317033827,86.3690704152286,
86.4527059265962,86.5362583699947,86.6197478058457,86.7032017564594,86.7866382503057,
86.8700753600612,86.9535311549789,87.0370756477086,87.1206647306495,87.2043879982071,
87.2850677141029,87.3688064259488,87.4524419373163,87.5359943807148,87.6194838165659,
87.7029377671795,87.7863742610257,87.8698113707812,87.9532671656989,88.0368116584285,
88.1204007413695,88.2041240089271,88.284803724823,88.368542436669,88.4521779480365,
88.535730391435,88.619219827286,88.7026737778997,88.786110271746,88.8695473815015,
88.9530031764193,89.036547669149,89.12013675209,89.2038600196476,89.2845397355431,
89.368278447389,89.4519139587565,89.5354664021551,89.6189558380062,89.7024097886198,
89.7858462824661,89.8692833922215,89.9527391871391,90.0362836798687,90.1198727628097,
90.2035960303673,90.2842757462633,90.3667505459319,90.4491298248377,90.5314328034189,
90.6136786176278,90.69588927706,90.7781041156691,90.8545165002977),
 .UNSPECIFIED.);
#104=B_SPLINE_CURVE_WITH_KNOTS('',3,(#22882,#22883,#22884,#22885,#22886,
#22887,#22888,#22889,#22890,#22891),.UNSPECIFIED.,.F.,.F.,(4,3,3,4),(84.5725992439732,
84.6588962802708,84.7450885344468,84.8230016469053),.UNSPECIFIED.);
#105=B_SPLINE_CURVE_WITH_KNOTS('',3,(#22893,#22894,#22895,#22896,#22897,
#22898,#22899,#22900,#22901,#22902),.UNSPECIFIED.,.F.,.F.,(4,3,3,4),(84.571795089726,
84.5961503016573,84.7095759742832,84.8230016469091),.UNSPECIFIED.);
#106=B_SPLINE_CURVE_WITH_KNOTS('',3,(#22903,#22904,#22905,#22906,#22907,
#22908,#22909,#22910,#22911,#22912,#22913,#22914,#22915,#22916,#22917,#22918,
#22919,#22920,#22921,#22922,#22923,#22924,#22925,#22926,#22927,#22928,#22929,
#22930,#22931,#22932,#22933,#22934,#22935,#22936,#22937,#22938,#22939,#22940,
#22941,#22942,#22943,#22944,#22945,#22946,#22947,#22948,#22949,#22950,#22951,
#22952,#22953,#22954,#22955,#22956,#22957,#22958,#22959,#22960,#22961,#22962,
#22963,#22964,#22965,#22966,#22967,#22968,#22969,#22970,#22971,#22972,#22973,
#22974,#22975,#22976,#22977,#22978,#22979,#22980,#22981,#22982,#22983,#22984,
#22985,#22986,#22987,#22988,#22989,#22990,#22991,#22992,#22993,#22994,#22995,
#22996,#22997,#22998,#22999,#23000,#23001,#23002,#23003,#23004,#23005,#23006,
#23007,#23008,#23009,#23010,#23011,#23012,#23013,#23014,#23015,#23016,#23017,
#23018,#23019,#23020,#23021,#23022,#23023,#23024,#23025,#23026,#23027,#23028,
#23029,#23030,#23031,#23032,#23033,#23034,#23035,#23036,#23037,#23038,#23039,
#23040,#23041,#23042,#23043,#23044,#23045,#23046,#23047,#23048,#23049,#23050,
#23051,#23052,#23053,#23054,#23055,#23056,#23057,#23058,#23059,#23060,#23061,
#23062,#23063,#23064,#23065,#23066,#23067,#23068,#23069,#23070,#23071,#23072,
#23073,#23074,#23075,#23076,#23077,#23078,#23079,#23080,#23081,#23082,#23083,
#23084,#23085,#23086,#23087,#23088,#23089,#23090,#23091,#23092,#23093,#23094,
#23095,#23096,#23097,#23098,#23099,#23100,#23101,#23102,#23103,#23104,#23105,
#23106,#23107,#23108,#23109,#23110,#23111,#23112,#23113,#23114,#23115,#23116,
#23117,#23118,#23119,#23120,#23121,#23122),.UNSPECIFIED.,.F.,.F.,(4,3,3,
3,3,3,3,3,3,3,3,3,3,3,3,3,3,3,3,3,3,3,3,3,3,3,3,3,3,3,3,3,3,3,3,3,3,3,3,
3,3,3,3,3,3,3,3,3,3,3,3,3,3,3,3,3,3,3,3,3,3,3,3,3,3,3,3,3,3,3,3,3,3,4),
(84.8230016470494,84.9054512045182,84.9917555930006,85.0741114802006,85.1564545594353,
85.2388037750452,85.3211780738551,85.4036410329863,85.4861559906397,85.5687878473739,
85.5958863123774,85.6796250242234,85.763260535591,85.8468129789896,85.9303024148405,
86.0137563654542,86.0971928593005,86.180629969056,86.2640857639739,86.3476302567036,
86.4312193396445,86.5149426072021,86.5956223230975,86.6793610349434,86.762996546311,
86.8465489897096,86.9300384255609,87.0134923761746,87.0969288700208,87.1803659797762,
87.2638217746938,87.3473662674234,87.4309553503644,87.514678617922,87.5953583338177,
87.6790970456637,87.7627325570311,87.8462850004296,87.9297744362802,88.0132283868939,
88.0966648807401,88.1801019904954,88.2635577854131,88.3471022781427,88.4306913610839,
88.5144146286414,88.5950943445378,88.6788330563837,88.7624685677512,88.8460210111494,
88.9295104470006,89.0129643976143,89.0964008914605,89.1798380012159,89.2632937961336,
89.3468382888634,89.4304273718043,89.5141506393619,89.5948303552579,89.6785690671039,
89.7622045784714,89.8457570218702,89.929246457721,90.0127004083347,90.0961369021807,
90.1795740119362,90.2630298068536,90.3465742995832,90.430163382524,90.5138866500815,
90.5945663659781,90.6821700263414,90.7695849001495,90.8558404966185),
 .UNSPECIFIED.);
#107=B_SPLINE_CURVE_WITH_KNOTS('',3,(#23128,#23129,#23130,#23131,#23132,
#23133,#23134,#23135,#23136,#23137,#23138,#23139,#23140,#23141,#23142,#23143,
#23144,#23145,#23146,#23147,#23148,#23149,#23150,#23151,#23152,#23153,#23154,
#23155,#23156,#23157,#23158,#23159,#23160,#23161,#23162,#23163,#23164,#23165,
#23166,#23167,#23168,#23169,#23170,#23171,#23172,#23173,#23174,#23175,#23176,
#23177,#23178,#23179,#23180,#23181,#23182,#23183,#23184,#23185,#23186,#23187,
#23188,#23189,#23190,#23191,#23192,#23193,#23194,#23195,#23196,#23197,#23198,
#23199,#23200,#23201,#23202,#23203,#23204,#23205,#23206,#23207,#23208,#23209,
#23210,#23211,#23212,#23213,#23214,#23215,#23216,#23217,#23218,#23219,#23220,
#23221,#23222,#23223,#23224,#23225,#23226,#23227,#23228,#23229,#23230,#23231,
#23232,#23233,#23234,#23235,#23236,#23237,#23238,#23239,#23240,#23241,#23242,
#23243,#23244,#23245,#23246,#23247,#23248,#23249,#23250,#23251,#23252,#23253,
#23254,#23255,#23256,#23257,#23258,#23259,#23260,#23261,#23262,#23263,#23264,
#23265,#23266,#23267,#23268,#23269,#23270,#23271,#23272,#23273,#23274,#23275,
#23276,#23277,#23278,#23279,#23280,#23281,#23282,#23283,#23284,#23285,#23286,
#23287,#23288,#23289,#23290,#23291,#23292,#23293,#23294,#23295,#23296,#23297,
#23298,#23299,#23300,#23301,#23302,#23303,#23304,#23305,#23306,#23307,#23308,
#23309,#23310,#23311,#23312,#23313,#23314,#23315,#23316,#23317,#23318,#23319,
#23320,#23321,#23322,#23323,#23324,#23325,#23326,#23327,#23328,#23329,#23330,
#23331,#23332,#23333,#23334,#23335,#23336,#23337,#23338,#23339,#23340,#23341,
#23342,#23343,#23344,#23345,#23346,#23347),.UNSPECIFIED.,.F.,.F.,(4,3,3,
3,3,3,3,3,3,3,3,3,3,3,3,3,3,3,3,3,3,3,3,3,3,3,3,3,3,3,3,3,3,3,3,3,3,3,3,
3,3,3,3,3,3,3,3,3,3,3,3,3,3,3,3,3,3,3,3,3,3,3,3,3,3,3,3,3,3,3,3,3,3,4),
(91.1061869540849,91.2342698388801,91.2840117569834,91.3677504688293,91.4513859801969,
91.5349384235956,91.6184278594466,91.7018818100603,91.7853183039066,91.8687554136621,
91.95221120858,92.0357557013097,92.1193447842506,92.2030680518082,92.2837477677035,
92.3674864795494,92.4511219909169,92.5346744343155,92.6181638701666,92.7016178207802,
92.7850543146265,92.8684914243819,92.9519472192995,93.0354917120292,93.1190807949702,
93.2028040625277,93.2834837784236,93.3672224902695,93.450858001637,93.5344104450355,
93.6178998808865,93.7013538315002,93.7847903253464,93.8682274351018,93.9516832300195,
94.0352277227491,94.1188168056901,94.2025400732476,94.2832197891438,94.3669585009898,
94.4505940123573,94.5341464557559,94.6176358916069,94.7010898422206,94.7845263360669,
94.8679634458224,94.9514192407401,95.0349637334698,95.1185528164108,95.2022760839684,
95.2829557998639,95.3666945117099,95.4503300230774,95.5338824664759,95.6173719023269,
95.7008258529406,95.7842623467869,95.8676994565424,95.9511552514601,96.0346997441898,
96.1182888271308,96.2020120946884,96.282691810584,96.3664390909035,96.4500812622947,
96.5360408032565,96.6195259372999,96.7029733472777,96.7864011215343,96.8698273312194,
96.9532987109112,97.0367978149355,97.120372459563,97.1377575899893),
 .UNSPECIFIED.);
#108=B_SPLINE_CURVE_WITH_KNOTS('',3,(#23348,#23349,#23350,#23351,#23352,
#23353,#23354,#23355,#23356,#23357),.UNSPECIFIED.,.F.,.F.,(4,3,3,4),(90.8545165002977,
90.9367707195664,91.0214788367447,91.106186953923),.UNSPECIFIED.);
#109=B_SPLINE_CURVE_WITH_KNOTS('',3,(#23359,#23360,#23361,#23362,#23363,
#23364,#23365,#23366,#23367,#23368),.UNSPECIFIED.,.F.,.F.,(4,3,3,4),(90.8558404966185,
90.943003649067,91.0300245809721,91.1061869540887),.UNSPECIFIED.);
#110=B_SPLINE_CURVE_WITH_KNOTS('',3,(#23369,#23370,#23371,#23372,#23373,
#23374,#23375,#23376,#23377,#23378,#23379,#23380,#23381,#23382,#23383,#23384,
#23385,#23386,#23387,#23388,#23389,#23390,#23391,#23392,#23393,#23394,#23395,
#23396,#23397,#23398,#23399,#23400,#23401,#23402,#23403,#23404,#23405,#23406,
#23407,#23408,#23409,#23410,#23411,#23412,#23413,#23414,#23415,#23416,#23417,
#23418,#23419,#23420,#23421,#23422,#23423,#23424,#23425,#23426,#23427,#23428,
#23429,#23430,#23431,#23432,#23433,#23434,#23435,#23436,#23437,#23438,#23439,
#23440,#23441,#23442,#23443,#23444,#23445,#23446,#23447,#23448,#23449,#23450,
#23451,#23452,#23453,#23454,#23455,#23456,#23457,#23458,#23459,#23460,#23461,
#23462,#23463,#23464,#23465,#23466,#23467,#23468,#23469,#23470,#23471,#23472,
#23473,#23474,#23475,#23476,#23477,#23478,#23479,#23480,#23481,#23482,#23483,
#23484,#23485,#23486,#23487,#23488,#23489,#23490,#23491,#23492,#23493,#23494,
#23495,#23496,#23497,#23498,#23499,#23500,#23501,#23502,#23503,#23504,#23505,
#23506,#23507,#23508,#23509,#23510,#23511,#23512,#23513,#23514,#23515,#23516,
#23517,#23518,#23519,#23520,#23521,#23522,#23523,#23524,#23525,#23526,#23527,
#23528,#23529,#23530,#23531,#23532,#23533,#23534,#23535,#23536,#23537,#23538,
#23539,#23540,#23541,#23542,#23543,#23544,#23545,#23546,#23547,#23548,#23549,
#23550,#23551,#23552,#23553,#23554,#23555,#23556,#23557,#23558,#23559,#23560,
#23561,#23562,#23563,#23564,#23565,#23566,#23567,#23568,#23569,#23570,#23571,
#23572,#23573,#23574,#23575,#23576,#23577,#23578,#23579,#23580,#23581,#23582,
#23583,#23584,#23585,#23586,#23587,#23588),.UNSPECIFIED.,.F.,.F.,(4,3,3,
3,3,3,3,3,3,3,3,3,3,3,3,3,3,3,3,3,3,3,3,3,3,3,3,3,3,3,3,3,3,3,3,3,3,3,3,
3,3,3,3,3,3,3,3,3,3,3,3,3,3,3,3,3,3,3,3,3,3,3,3,3,3,3,3,3,3,3,3,3,3,4),
(91.1061869542033,91.1940293877261,91.2820034417824,91.3702005362681,91.4585174044926,
91.5470388628258,91.5943023766982,91.6780410885441,91.7616765999115,91.8452290433101,
91.9287184791611,92.0121724297747,92.095608923621,92.1790460333764,92.262501828294,
92.3460463210237,92.4296354039646,92.5133586715222,92.5940383874183,92.6777770992642,
92.7614126106318,92.8449650540303,92.9284544898813,93.011908440495,93.0953449343413,
93.1787820440968,93.2622378390145,93.3457823317442,93.4293714146852,93.5130946822428,
93.5937743981385,93.6775131099844,93.7611486213519,93.8447010647504,93.9281905006014,
94.0116444512151,94.0950809450613,94.1785180548168,94.2619738497344,94.3455183424641,
94.429107425405,94.5128306929626,94.5935104088586,94.6772491207046,94.7608846320721,
94.8444370754706,94.9279265113217,95.0113804619354,95.0948169557816,95.1782540655371,
95.2617098604549,95.3452543531846,95.4288434361256,95.5125667036832,95.5932464195787,
95.6769851314246,95.7606206427921,95.8441730861908,95.927662522042,96.0111164726556,
96.0945529665019,96.1779900762574,96.2614458711751,96.3449903639048,96.4285794468458,
96.5123027144034,96.5929824302989,96.6755077426029,96.7579368247763,96.8402888703964,
96.9225805906639,97.0048367170366,97.0870887865323,97.1377977613825),
 .UNSPECIFIED.);
#111=B_SPLINE_CURVE_WITH_KNOTS('',3,(#23594,#23595,#23596,#23597,#23598,
#23599,#23600,#23601,#23602,#23603,#23604,#23605,#23606,#23607,#23608,#23609,
#23610,#23611,#23612,#23613,#23614,#23615,#23616,#23617,#23618,#23619,#23620,
#23621,#23622,#23623,#23624,#23625,#23626,#23627,#23628,#23629,#23630,#23631,
#23632,#23633,#23634,#23635,#23636,#23637,#23638,#23639,#23640,#23641,#23642,
#23643,#23644,#23645,#23646,#23647,#23648,#23649,#23650,#23651,#23652,#23653,
#23654,#23655,#23656,#23657,#23658,#23659,#23660,#23661,#23662,#23663,#23664,
#23665,#23666,#23667,#23668,#23669,#23670,#23671,#23672,#23673,#23674,#23675,
#23676,#23677,#23678,#23679,#23680,#23681,#23682,#23683,#23684,#23685,#23686,
#23687,#23688,#23689,#23690,#23691,#23692,#23693,#23694,#23695,#23696,#23697,
#23698,#23699,#23700,#23701,#23702,#23703,#23704,#23705,#23706,#23707,#23708,
#23709,#23710,#23711,#23712,#23713,#23714,#23715,#23716,#23717,#23718,#23719,
#23720,#23721,#23722,#23723,#23724,#23725,#23726,#23727,#23728,#23729,#23730,
#23731,#23732,#23733,#23734,#23735,#23736,#23737,#23738,#23739,#23740,#23741,
#23742,#23743,#23744,#23745,#23746,#23747,#23748,#23749,#23750,#23751,#23752,
#23753,#23754,#23755,#23756,#23757,#23758,#23759,#23760,#23761,#23762,#23763,
#23764,#23765,#23766,#23767,#23768,#23769,#23770,#23771,#23772,#23773,#23774,
#23775,#23776,#23777,#23778,#23779,#23780,#23781,#23782,#23783,#23784,#23785,
#23786,#23787,#23788,#23789,#23790,#23791,#23792,#23793,#23794,#23795,#23796,
#23797,#23798,#23799,#23800,#23801,#23802,#23803,#23804,#23805,#23806,#23807,
#23808,#23809,#23810,#23811,#23812,#23813),.UNSPECIFIED.,.F.,.F.,(4,3,3,
3,3,3,3,3,3,3,3,3,3,3,3,3,3,3,3,3,3,3,3,3,3,3,3,3,3,3,3,3,3,3,3,3,3,3,3,
3,3,3,3,3,3,3,3,3,3,3,3,3,3,3,3,3,3,3,3,3,3,3,3,3,3,3,3,3,3,3,3,3,3,4),
(97.3893722614005,97.4719677846863,97.5544719674218,97.6369058779297,97.7192955269354,
97.8016628999257,97.884026934726,97.9664065640542,98.0488700592945,98.1313770056035,
98.2140118307161,98.2821638320243,98.3659025438702,98.4495380552377,98.5330904986362,
98.6165799344873,98.7000338851009,98.7834703789472,98.8669074887027,98.9503632836207,
99.0339077763503,99.1174968592912,99.2012201268488,99.2818998427444,99.3656385545902,
99.449274065958,99.5328265093568,99.6163159452077,99.6997698958214,99.7832063896676,
99.8666434994231,99.9500992943405,100.03364378707,100.117232870011,100.200956137569,
100.281635853465,100.365374565311,100.449010076678,100.532562520077,100.616051955928,
100.699505906542,100.782942400388,100.866379510144,100.949835305062,101.033379797791,
101.116968880732,101.20069214829,101.281371864185,101.365110576031,101.448746087398,
101.532298530797,101.615787966648,101.699241917262,101.782678411108,101.866115520863,
101.949571315781,102.033115808511,102.116704891452,102.200428159009,102.281107874905,
102.364846586751,102.448482098118,102.532034541517,102.615523977367,102.698977927981,
102.782414421827,102.865851531583,102.949307326501,103.03285181923,103.116440902171,
103.200164169729,103.280843885625,103.374544855062,103.422164115585),
 .UNSPECIFIED.);
#112=B_SPLINE_CURVE_WITH_KNOTS('',3,(#23814,#23815,#23816,#23817,#23818,
#23819,#23820,#23821,#23822,#23823),.UNSPECIFIED.,.F.,.F.,(4,3,3,4),(97.1377575899893,
97.2214880297379,97.2824278213041,97.3893722612645),.UNSPECIFIED.);
#113=B_SPLINE_CURVE_WITH_KNOTS('',3,(#23825,#23826,#23827,#23828,#23829,
#23830,#23831,#23832,#23833,#23834),.UNSPECIFIED.,.F.,.F.,(4,3,3,4),(97.1377977613825,
97.2200836147453,97.3047279379176,97.3893722610898),.UNSPECIFIED.);
#114=B_SPLINE_CURVE_WITH_KNOTS('',3,(#23835,#23836,#23837,#23838,#23839,
#23840,#23841,#23842,#23843,#23844,#23845,#23846,#23847,#23848,#23849,#23850,
#23851,#23852,#23853,#23854,#23855,#23856,#23857,#23858,#23859,#23860,#23861,
#23862,#23863,#23864,#23865,#23866,#23867,#23868,#23869,#23870,#23871,#23872,
#23873,#23874,#23875,#23876,#23877,#23878,#23879,#23880,#23881,#23882,#23883,
#23884,#23885,#23886,#23887,#23888,#23889,#23890,#23891,#23892,#23893,#23894,
#23895,#23896,#23897,#23898,#23899,#23900,#23901,#23902,#23903,#23904,#23905,
#23906,#23907,#23908,#23909,#23910,#23911,#23912,#23913,#23914,#23915,#23916,
#23917,#23918,#23919,#23920,#23921,#23922,#23923,#23924,#23925,#23926,#23927,
#23928,#23929,#23930,#23931,#23932,#23933,#23934,#23935,#23936,#23937,#23938,
#23939,#23940,#23941,#23942,#23943,#23944,#23945,#23946,#23947,#23948,#23949,
#23950,#23951,#23952,#23953,#23954,#23955,#23956,#23957,#23958,#23959,#23960,
#23961,#23962,#23963,#23964,#23965,#23966,#23967,#23968,#23969,#23970,#23971,
#23972,#23973,#23974,#23975,#23976,#23977,#23978,#23979,#23980,#23981,#23982,
#23983,#23984,#23985,#23986,#23987,#23988,#23989,#23990,#23991,#23992,#23993,
#23994,#23995,#23996,#23997,#23998,#23999,#24000,#24001,#24002,#24003,#24004,
#24005,#24006,#24007,#24008,#24009,#24010,#24011,#24012,#24013,#24014,#24015,
#24016,#24017,#24018,#24019,#24020,#24021,#24022,#24023,#24024,#24025,#24026,
#24027,#24028,#24029,#24030,#24031,#24032,#24033,#24034,#24035,#24036,#24037,
#24038,#24039,#24040,#24041,#24042,#24043,#24044,#24045,#24046,#24047,#24048,
#24049,#24050,#24051),.UNSPECIFIED.,.F.,.F.,(4,3,3,3,3,3,3,3,3,3,3,3,3,
3,3,3,3,3,3,3,3,3,3,3,3,3,3,3,3,3,3,3,3,3,3,3,3,3,3,3,3,3,3,3,3,3,3,3,3,
3,3,3,3,3,3,3,3,3,3,3,3,3,3,3,3,3,3,3,3,3,3,3,4),(97.3893722612683,97.5085709008744,
97.592718441019,97.676457152865,97.7600926642325,97.8436451076312,97.9271345434824,
98.0105884940961,98.0940249879424,98.177462097698,98.2609178926158,98.3444623853455,
98.4280514682866,98.5117747358442,98.5924544517391,98.676193163585,98.7598286749525,
98.843381118351,98.926870554202,99.0103245048157,99.0937609986619,99.1771981084174,
99.2606539033351,99.3441983960647,99.4277874790057,99.5115107465633,99.5921904624593,
99.6759291743052,99.7595646856727,99.8431171290711,99.9266065649221,100.010060515536,
100.093497009382,100.176934119137,100.260389914055,100.343934406785,100.427523489726,
100.511246757283,100.591926473179,100.675665185025,100.759300696393,100.842853139791,
100.926342575642,101.009796526256,101.093233020102,101.176670129858,101.260125924776,
101.343670417505,101.427259500446,101.510982768004,101.5916624839,101.675401195746,
101.759036707114,101.842589150512,101.926078586363,102.009532536977,102.092969030823,
102.176406140579,102.259861935497,102.343406428226,102.426995511167,102.510718778725,
102.59139849462,102.675147385514,102.758790830291,102.84233402803,102.925820381412,
103.009268009692,103.09269500225,103.176148517115,103.2596128892,103.3431540916,
103.420910293148),.UNSPECIFIED.);
#115=B_SPLINE_CURVE_WITH_KNOTS('',3,(#24057,#24058,#24059,#24060,#24061,
#24062,#24063,#24064,#24065,#24066,#24067,#24068,#24069,#24070,#24071,#24072,
#24073,#24074,#24075,#24076,#24077,#24078,#24079,#24080,#24081,#24082,#24083,
#24084,#24085,#24086,#24087,#24088,#24089,#24090,#24091,#24092,#24093,#24094,
#24095,#24096,#24097,#24098,#24099,#24100,#24101,#24102,#24103,#24104,#24105,
#24106,#24107,#24108,#24109,#24110,#24111,#24112,#24113,#24114,#24115,#24116,
#24117,#24118,#24119,#24120,#24121,#24122,#24123,#24124,#24125,#24126,#24127,
#24128,#24129,#24130,#24131,#24132,#24133,#24134,#24135,#24136,#24137,#24138,
#24139,#24140,#24141,#24142,#24143,#24144,#24145,#24146,#24147,#24148,#24149,
#24150,#24151,#24152,#24153,#24154,#24155,#24156,#24157,#24158,#24159,#24160,
#24161,#24162,#24163,#24164,#24165,#24166,#24167,#24168,#24169,#24170,#24171,
#24172,#24173,#24174,#24175,#24176,#24177,#24178,#24179,#24180,#24181,#24182,
#24183,#24184,#24185,#24186,#24187,#24188,#24189,#24190,#24191,#24192,#24193,
#24194,#24195,#24196,#24197,#24198,#24199,#24200,#24201,#24202,#24203,#24204,
#24205,#24206,#24207,#24208,#24209,#24210,#24211,#24212,#24213,#24214,#24215,
#24216,#24217,#24218,#24219,#24220,#24221,#24222,#24223,#24224,#24225,#24226,
#24227,#24228,#24229,#24230,#24231,#24232,#24233,#24234,#24235,#24236,#24237,
#24238,#24239,#24240,#24241,#24242,#24243,#24244,#24245,#24246,#24247,#24248,
#24249,#24250,#24251,#24252,#24253,#24254,#24255,#24256,#24257,#24258,#24259,
#24260,#24261,#24262,#24263,#24264,#24265,#24266,#24267,#24268,#24269,#24270,
#24271,#24272,#24273,#24274,#24275,#24276),.UNSPECIFIED.,.F.,.F.,(4,3,3,
3,3,3,3,3,3,3,3,3,3,3,3,3,3,3,3,3,3,3,3,3,3,3,3,3,3,3,3,3,3,3,3,3,3,3,3,
3,3,3,3,3,3,3,3,3,3,3,3,3,3,3,3,3,3,3,3,3,3,3,3,3,3,3,3,3,3,3,3,3,3,4),
(103.672557568444,103.756948747136,103.841357026278,103.925799068812,104.014494275695,
104.099107419003,104.18379133639,104.268605737223,104.280579896345,104.364318608191,
104.447954119558,104.531506562957,104.614995998808,104.698449949422,104.781886443268,
104.865323553023,104.948779347941,105.03232384067,105.115912923611,105.199636191169,
105.280315907065,105.364054618911,105.447690130278,105.531242573677,105.614732009527,
105.698185960141,105.781622453987,105.865059563743,105.94851535866,106.03205985139,
106.115648934331,106.199372201889,106.280051917785,106.363790629631,106.447426140998,
106.530978584397,106.614468020248,106.697921970862,106.781358464708,106.864795574464,
106.948251369382,107.031795862111,107.115384945052,107.19910821261,107.279787928505,
107.363526640351,107.447162151719,107.530714595117,107.614204030968,107.697657981582,
107.781094475428,107.864531585183,107.947987380101,108.031531872831,108.115120955772,
108.198844223329,108.279523939226,108.363262651072,108.44689816244,108.530450605838,
108.613940041689,108.697393992303,108.780830486149,108.864267595905,108.947723390823,
109.031267883552,109.114856966493,109.198580234051,109.279259949946,109.362821357527,
109.448305160013,109.531656885119,109.618206726296,109.704756567473),
 .UNSPECIFIED.);
#116=B_SPLINE_CURVE_WITH_KNOTS('',3,(#24277,#24278,#24279,#24280,#24281,
#24282,#24283,#24284,#24285,#24286),.UNSPECIFIED.,.F.,.F.,(4,3,3,4),(103.422164115585,
103.515371370637,103.608104590454,103.672557568256),.UNSPECIFIED.);
#117=B_SPLINE_CURVE_WITH_KNOTS('',3,(#24288,#24289,#24290,#24291,#24292,
#24293,#24294,#24295,#24296,#24297),.UNSPECIFIED.,.F.,.F.,(4,3,3,4),(103.420910293148,
103.506022399244,103.59113450534,103.672557568448),.UNSPECIFIED.);
#118=B_SPLINE_CURVE_WITH_KNOTS('',3,(#24298,#24299,#24300,#24301,#24302,
#24303,#24304,#24305,#24306,#24307,#24308,#24309,#24310,#24311,#24312,#24313,
#24314,#24315,#24316,#24317,#24318,#24319,#24320,#24321,#24322,#24323,#24324,
#24325,#24326,#24327,#24328,#24329,#24330,#24331,#24332,#24333,#24334,#24335,
#24336,#24337,#24338,#24339,#24340,#24341,#24342,#24343,#24344,#24345,#24346,
#24347,#24348,#24349,#24350,#24351,#24352,#24353,#24354,#24355,#24356,#24357,
#24358,#24359,#24360,#24361,#24362,#24363,#24364,#24365,#24366,#24367,#24368,
#24369,#24370,#24371,#24372,#24373,#24374,#24375,#24376,#24377,#24378,#24379,
#24380,#24381,#24382,#24383,#24384,#24385,#24386,#24387,#24388,#24389,#24390,
#24391,#24392,#24393,#24394,#24395,#24396,#24397,#24398,#24399,#24400,#24401,
#24402,#24403,#24404,#24405,#24406,#24407,#24408,#24409,#24410,#24411,#24412,
#24413,#24414,#24415,#24416,#24417,#24418,#24419,#24420,#24421,#24422,#24423,
#24424,#24425,#24426,#24427,#24428,#24429,#24430,#24431,#24432,#24433,#24434,
#24435,#24436,#24437,#24438,#24439,#24440,#24441,#24442,#24443,#24444,#24445,
#24446,#24447,#24448,#24449,#24450,#24451,#24452,#24453,#24454,#24455,#24456,
#24457,#24458,#24459,#24460,#24461,#24462,#24463,#24464,#24465,#24466,#24467,
#24468,#24469,#24470,#24471,#24472,#24473,#24474,#24475,#24476,#24477,#24478,
#24479,#24480,#24481,#24482,#24483,#24484,#24485,#24486,#24487,#24488,#24489,
#24490,#24491,#24492,#24493,#24494,#24495,#24496,#24497,#24498,#24499,#24500,
#24501,#24502,#24503,#24504,#24505,#24506,#24507,#24508,#24509,#24510,#24511,
#24512,#24513,#24514,#24515,#24516,#24517),.UNSPECIFIED.,.F.,.F.,(4,3,3,
3,3,3,3,3,3,3,3,3,3,3,3,3,3,3,3,3,3,3,3,3,3,3,3,3,3,3,3,3,3,3,3,3,3,3,3,
3,3,3,3,3,3,3,3,3,3,3,3,3,3,3,3,3,3,3,3,3,3,3,3,3,3,3,3,3,3,3,3,3,3,4),
(103.672557568579,103.755338549975,103.838023743102,103.920634109801,104.004413660583,
104.086946693849,104.169472251958,104.252009159745,104.336724498823,104.419384236231,
104.505127376145,104.59087051606,104.674609227906,104.758244739273,104.841797182672,
104.925286618523,105.008740569137,105.092177062983,105.175614172739,105.259069967657,
105.342614460386,105.426203543327,105.509926810885,105.59060652678,105.674345238626,
105.757980749993,105.841533193392,105.925022629242,106.008476579856,106.091913073702,
106.175350183458,106.258805978375,106.342350471105,106.425939554046,106.509662821604,
106.5903425375,106.674081249346,106.757716760713,106.841269204112,106.924758639964,
107.008212590577,107.091649084424,107.175086194179,107.258541989097,107.342086481826,
107.425675564767,107.509398832325,107.59007854822,107.673817260066,107.757452771433,
107.841005214832,107.924494650683,108.007948601297,108.091385095143,108.174822204899,
108.258277999817,108.341822492546,108.425411575487,108.509134843045,108.58981455894,
108.673553270786,108.757188782154,108.840741225552,108.924230661404,109.007684612017,
109.091121105864,109.174558215619,109.258014010538,109.341558503267,109.425147586208,
109.508870853766,109.589550569661,109.68519153841,109.705270710528),
 .UNSPECIFIED.);
#119=B_SPLINE_CURVE_WITH_KNOTS('',3,(#24523,#24524,#24525,#24526,#24527,
#24528,#24529,#24530,#24531,#24532,#24533,#24534,#24535,#24536,#24537,#24538,
#24539,#24540,#24541,#24542,#24543,#24544,#24545,#24546,#24547,#24548,#24549,
#24550,#24551,#24552,#24553,#24554,#24555,#24556,#24557,#24558,#24559,#24560,
#24561,#24562,#24563,#24564,#24565,#24566,#24567,#24568,#24569,#24570,#24571,
#24572,#24573,#24574,#24575,#24576,#24577,#24578,#24579,#24580,#24581,#24582,
#24583,#24584,#24585,#24586,#24587,#24588,#24589,#24590,#24591,#24592,#24593,
#24594,#24595,#24596,#24597,#24598,#24599,#24600,#24601,#24602,#24603,#24604,
#24605,#24606,#24607,#24608,#24609,#24610,#24611,#24612,#24613,#24614,#24615,
#24616,#24617,#24618,#24619,#24620,#24621,#24622,#24623,#24624,#24625,#24626,
#24627,#24628,#24629,#24630,#24631,#24632,#24633,#24634,#24635,#24636,#24637,
#24638,#24639,#24640,#24641,#24642,#24643,#24644,#24645,#24646,#24647,#24648,
#24649,#24650,#24651,#24652,#24653,#24654,#24655,#24656,#24657,#24658,#24659,
#24660,#24661,#24662,#24663,#24664,#24665,#24666,#24667,#24668,#24669,#24670,
#24671,#24672,#24673,#24674,#24675,#24676,#24677,#24678,#24679,#24680,#24681,
#24682,#24683,#24684,#24685,#24686,#24687,#24688,#24689,#24690,#24691,#24692,
#24693,#24694,#24695,#24696,#24697,#24698,#24699,#24700,#24701,#24702,#24703,
#24704,#24705,#24706,#24707,#24708,#24709,#24710,#24711,#24712,#24713,#24714,
#24715,#24716,#24717,#24718,#24719,#24720,#24721,#24722,#24723,#24724,#24725,
#24726,#24727,#24728,#24729,#24730,#24731,#24732,#24733,#24734,#24735,#24736,
#24737,#24738,#24739,#24740,#24741,#24742),.UNSPECIFIED.,.F.,.F.,(4,3,3,
3,3,3,3,3,3,3,3,3,3,3,3,3,3,3,3,3,3,3,3,3,3,3,3,3,3,3,3,3,3,3,3,3,3,3,3,
3,3,3,3,3,3,3,3,3,3,3,3,3,3,3,3,3,3,3,3,3,3,3,3,3,3,3,3,3,3,3,3,3,3,4),
(109.955742875801,110.053908632085,110.152728187028,110.252279042651,110.278995960666,
110.362734672512,110.446370183879,110.529922627278,110.613412063129,110.696866013743,
110.780302507589,110.863739617344,110.947195412262,111.030739904991,111.114328987932,
111.19805225549,111.278731971386,111.362470683232,111.446106194599,111.529658637998,
111.613148073849,111.696602024463,111.780038518309,111.863475628064,111.946931422982,
112.030475915712,112.114064998653,112.19778826621,112.278467982106,112.362206693952,
112.445842205319,112.529394648718,112.612884084569,112.696338035182,112.779774529029,
112.863211638784,112.946667433702,113.030211926431,113.113801009372,113.19752427693,
113.278203992826,113.361942704672,113.445578216039,113.529130659438,113.612620095289,
113.696074045903,113.779510539749,113.862947649505,113.946403444422,114.029947937152,
114.113537020093,114.197260287651,114.277940003546,114.361678715392,114.44531422676,
114.528866670158,114.612356106009,114.695810056623,114.779246550469,114.862683660225,
114.946139455142,115.029683947872,115.113273030813,115.196996298371,115.277676014266,
115.360916343682,115.444025174985,115.527058070878,115.610033652872,115.692970496751,
115.775902763453,115.858831416099,115.94180178495,115.987147173825),
 .UNSPECIFIED.);
#120=B_SPLINE_CURVE_WITH_KNOTS('',3,(#24743,#24744,#24745,#24746,#24747,
#24748,#24749,#24750,#24751,#24752),.UNSPECIFIED.,.F.,.F.,(4,3,3,4),(109.704756567473,
109.787983735154,109.871863305389,109.955742875624),.UNSPECIFIED.);
#121=B_SPLINE_CURVE_WITH_KNOTS('',3,(#24754,#24755,#24756,#24757,#24758,
#24759,#24760,#24761,#24762,#24763),.UNSPECIFIED.,.F.,.F.,(4,3,3,4),(109.705270710528,
109.800372858636,109.894864507288,109.955742875431),.UNSPECIFIED.);
#122=B_SPLINE_CURVE_WITH_KNOTS('',3,(#24764,#24765,#24766,#24767,#24768,
#24769,#24770,#24771,#24772,#24773,#24774,#24775,#24776,#24777,#24778,#24779,
#24780,#24781,#24782,#24783,#24784,#24785,#24786,#24787,#24788,#24789,#24790,
#24791,#24792,#24793,#24794,#24795,#24796,#24797,#24798,#24799,#24800,#24801,
#24802,#24803,#24804,#24805,#24806,#24807,#24808,#24809,#24810,#24811,#24812,
#24813,#24814,#24815,#24816,#24817,#24818,#24819,#24820,#24821,#24822,#24823,
#24824,#24825,#24826,#24827,#24828,#24829,#24830,#24831,#24832,#24833,#24834,
#24835,#24836,#24837,#24838,#24839,#24840,#24841,#24842,#24843,#24844,#24845,
#24846,#24847,#24848,#24849,#24850,#24851,#24852,#24853,#24854,#24855,#24856,
#24857,#24858,#24859,#24860,#24861,#24862,#24863,#24864,#24865,#24866,#24867,
#24868,#24869,#24870,#24871,#24872,#24873,#24874,#24875,#24876,#24877,#24878,
#24879,#24880,#24881,#24882,#24883,#24884,#24885,#24886,#24887,#24888,#24889,
#24890,#24891,#24892,#24893,#24894,#24895,#24896,#24897,#24898,#24899,#24900,
#24901,#24902,#24903,#24904,#24905,#24906,#24907,#24908,#24909,#24910,#24911,
#24912,#24913,#24914,#24915,#24916,#24917,#24918,#24919,#24920,#24921,#24922,
#24923,#24924,#24925,#24926,#24927,#24928,#24929,#24930,#24931,#24932,#24933,
#24934,#24935,#24936,#24937,#24938,#24939,#24940,#24941,#24942,#24943,#24944,
#24945,#24946,#24947,#24948,#24949,#24950,#24951,#24952,#24953,#24954,#24955,
#24956,#24957,#24958,#24959,#24960,#24961,#24962,#24963,#24964,#24965,#24966,
#24967,#24968,#24969,#24970,#24971,#24972,#24973,#24974,#24975,#24976,#24977,
#24978,#24979,#24980,#24981,#24982,#24983),.UNSPECIFIED.,.F.,.F.,(4,3,3,
3,3,3,3,3,3,3,3,3,3,3,3,3,3,3,3,3,3,3,3,3,3,3,3,3,3,3,3,3,3,3,3,3,3,3,3,
3,3,3,3,3,3,3,3,3,3,3,3,3,3,3,3,3,3,3,3,3,3,3,3,3,3,3,3,3,3,3,3,3,3,4),
(109.955742875628,110.039648469011,110.123556652528,110.207484832012,110.291450422462,
110.375523162037,110.459655763239,110.543923584594,110.589286580381,110.673025292227,
110.756660803595,110.840213246993,110.923702682844,111.007156633458,111.090593127304,
111.17403023706,111.257486031977,111.341030524707,111.424619607648,111.508342875206,
111.589022591101,111.672761302947,111.756396814314,111.839949257713,111.923438693564,
112.006892644178,112.090329138024,112.173766247779,112.257222042697,112.340766535426,
112.424355618367,112.508078885925,112.588758601821,112.672497313667,112.756132825034,
112.839685268433,112.923174704284,113.006628654898,113.090065148744,113.173502258499,
113.256958053417,113.340502546147,113.424091629088,113.507814896646,113.588494612541,
113.672233324387,113.755868835754,113.839421279153,113.922910715004,114.006364665617,
114.089801159464,114.173238269219,114.256694064136,114.340238556866,114.423827639807,
114.507550907365,114.588230623261,114.671969335107,114.755604846474,114.839157289873,
114.922646725724,115.006100676337,115.089537170184,115.172974279939,115.256430074857,
115.339974567586,115.423563650527,115.507286918084,115.587966633981,115.671933979496,
115.755764025857,115.839515095663,115.923193376346,115.988071988884),
 .UNSPECIFIED.);
#123=B_SPLINE_CURVE_WITH_KNOTS('',3,(#24989,#24990,#24991,#24992,#24993,
#24994,#24995,#24996,#24997,#24998,#24999,#25000,#25001,#25002,#25003,#25004,
#25005,#25006,#25007,#25008,#25009,#25010,#25011,#25012,#25013,#25014,#25015,
#25016,#25017,#25018,#25019,#25020,#25021,#25022,#25023,#25024,#25025,#25026,
#25027,#25028,#25029,#25030,#25031,#25032,#25033,#25034,#25035,#25036,#25037,
#25038,#25039,#25040,#25041,#25042,#25043,#25044,#25045,#25046,#25047,#25048,
#25049,#25050,#25051,#25052,#25053,#25054,#25055,#25056,#25057,#25058,#25059,
#25060,#25061,#25062,#25063,#25064,#25065,#25066,#25067,#25068,#25069,#25070,
#25071,#25072,#25073,#25074,#25075,#25076,#25077,#25078,#25079,#25080,#25081,
#25082,#25083,#25084,#25085,#25086,#25087,#25088,#25089,#25090,#25091,#25092,
#25093,#25094,#25095,#25096,#25097,#25098,#25099,#25100,#25101,#25102,#25103,
#25104,#25105,#25106,#25107,#25108,#25109,#25110,#25111,#25112,#25113,#25114,
#25115,#25116,#25117,#25118,#25119,#25120,#25121,#25122,#25123,#25124,#25125,
#25126,#25127,#25128,#25129,#25130,#25131,#25132,#25133,#25134,#25135,#25136,
#25137,#25138,#25139,#25140,#25141,#25142,#25143,#25144,#25145,#25146,#25147,
#25148,#25149,#25150,#25151,#25152,#25153,#25154,#25155,#25156,#25157,#25158,
#25159,#25160,#25161,#25162,#25163,#25164,#25165,#25166,#25167,#25168,#25169,
#25170,#25171,#25172,#25173,#25174,#25175,#25176,#25177,#25178,#25179,#25180,
#25181,#25182,#25183,#25184,#25185,#25186,#25187,#25188,#25189,#25190,#25191,
#25192,#25193,#25194,#25195,#25196,#25197,#25198,#25199,#25200,#25201,#25202,
#25203,#25204,#25205,#25206,#25207,#25208),.UNSPECIFIED.,.F.,.F.,(4,3,3,
3,3,3,3,3,3,3,3,3,3,3,3,3,3,3,3,3,3,3,3,3,3,3,3,3,3,3,3,3,3,3,3,3,3,3,3,
3,3,3,3,3,3,3,3,3,3,3,3,3,3,3,3,3,3,3,3,3,3,3,3,3,3,3,3,3,3,3,3,3,3,4),
(116.238928182803,116.277412024987,116.361150736833,116.4447862482,116.528338691599,
116.61182812745,116.695282078063,116.778718571909,116.862155681664,116.945611476582,
117.029155969311,117.112745052252,117.19646831981,117.277148035707,117.360886747553,
117.44452225892,117.528074702319,117.61156413817,117.695018088784,117.77845458263,
117.861891692385,117.945347487303,118.028891980033,118.112481062974,118.196204330531,
118.276884046427,118.360622758273,118.44425826964,118.527810713039,118.61130014889,
118.694754099503,118.77819059335,118.861627703105,118.945083498023,119.028627990752,
119.112217073693,119.195940341251,119.276620057147,119.360358768993,119.44399428036,
119.527546723759,119.61103615961,119.694490110224,119.77792660407,119.861363713826,
119.944819508743,120.028364001473,120.111953084414,120.195676351972,120.276356067867,
120.360094779713,120.44373029108,120.527282734479,120.61077217033,120.694226120944,
120.77766261479,120.861099724545,120.944555519463,121.028100012192,121.111689095133,
121.195412362691,121.276092078587,121.359831060277,121.443466778056,121.5270193647,
121.610508880833,121.693962581455,121.77739873563,121.860835415973,121.944290691593,
122.027833400628,122.111420662809,122.195139108014,122.271018544109),
 .UNSPECIFIED.);
#124=B_SPLINE_CURVE_WITH_KNOTS('',3,(#25209,#25210,#25211,#25212,#25213,
#25214,#25215,#25216,#25217,#25218),.UNSPECIFIED.,.F.,.F.,(4,3,3,4),(115.987147173825,
116.070212549419,116.154570366029,116.238928182639),.UNSPECIFIED.);
#125=B_SPLINE_CURVE_WITH_KNOTS('',3,(#25220,#25221,#25222,#25223,#25224,
#25225,#25226,#25227,#25228,#25229),.UNSPECIFIED.,.F.,.F.,(4,3,3,4),(115.988071988884,
116.071683453257,116.155305818032,116.238928182807),.UNSPECIFIED.);
#126=B_SPLINE_CURVE_WITH_KNOTS('',3,(#25230,#25231,#25232,#25233,#25234,
#25235,#25236,#25237,#25238,#25239,#25240,#25241,#25242,#25243,#25244,#25245,
#25246,#25247,#25248,#25249,#25250,#25251,#25252,#25253,#25254,#25255,#25256,
#25257,#25258,#25259,#25260,#25261,#25262,#25263,#25264,#25265,#25266,#25267,
#25268,#25269,#25270,#25271,#25272,#25273,#25274,#25275,#25276,#25277,#25278,
#25279,#25280,#25281,#25282,#25283,#25284,#25285,#25286,#25287,#25288,#25289,
#25290,#25291,#25292,#25293,#25294,#25295,#25296,#25297,#25298,#25299,#25300,
#25301,#25302,#25303,#25304,#25305,#25306,#25307,#25308,#25309,#25310,#25311,
#25312,#25313,#25314,#25315,#25316,#25317,#25318,#25319,#25320,#25321,#25322,
#25323,#25324,#25325,#25326,#25327,#25328,#25329,#25330,#25331,#25332,#25333,
#25334,#25335,#25336,#25337,#25338,#25339,#25340,#25341,#25342,#25343,#25344,
#25345,#25346,#25347,#25348,#25349,#25350,#25351,#25352,#25353,#25354,#25355,
#25356,#25357,#25358,#25359,#25360,#25361,#25362,#25363,#25364,#25365,#25366,
#25367,#25368,#25369,#25370,#25371,#25372,#25373,#25374,#25375,#25376,#25377,
#25378,#25379,#25380,#25381,#25382,#25383,#25384,#25385,#25386,#25387,#25388,
#25389,#25390,#25391,#25392,#25393,#25394,#25395,#25396,#25397,#25398,#25399,
#25400,#25401,#25402,#25403,#25404,#25405,#25406,#25407,#25408,#25409,#25410,
#25411,#25412,#25413,#25414,#25415,#25416,#25417,#25418,#25419,#25420,#25421,
#25422,#25423,#25424,#25425,#25426,#25427,#25428,#25429,#25430,#25431,#25432,
#25433,#25434,#25435,#25436,#25437,#25438,#25439,#25440,#25441,#25442,#25443,
#25444,#25445,#25446,#25447,#25448,#25449),.UNSPECIFIED.,.F.,.F.,(4,3,3,
3,3,3,3,3,3,3,3,3,3,3,3,3,3,3,3,3,3,3,3,3,3,3,3,3,3,3,3,3,3,3,3,3,3,3,3,
3,3,3,3,3,3,3,3,3,3,3,3,3,3,3,3,3,3,3,3,3,3,3,3,3,3,3,3,3,3,3,3,3,3,4),
(116.238928183003,116.334849321083,116.431253899856,116.528269407277,116.587702644701,
116.671441356547,116.755076867914,116.838629311313,116.922118747164,117.005572697778,
117.089009191624,117.17244630138,117.255902096297,117.339446589027,117.423035671968,
117.506758939526,117.587438655422,117.671177367268,117.754812878636,117.838365322034,
117.921854757885,118.005308708499,118.088745202345,118.172182312101,118.255638107018,
118.339182599748,118.422771682689,118.506494950247,118.587174666142,118.670913377988,
118.754548889355,118.838101332754,118.921590768605,119.005044719218,119.088481213064,
119.17191832282,119.255374117737,119.338918610467,119.422507693408,119.506230960966,
119.586910676862,119.670649388708,119.754284900075,119.837837343474,119.921326779325,
120.004780729939,120.088217223785,120.17165433354,120.255110128458,120.338654621188,
120.422243704129,120.505966971687,120.586646687582,120.670385399428,120.754020910795,
120.837573354194,120.921062790045,121.004516740659,121.087953234505,121.17139034426,
121.254846139178,121.338390631908,121.421979714849,121.505702982407,121.586382698302,
121.671870895413,121.754714488921,121.837482997203,121.920195242189,122.002869998466,
122.085539448033,122.168206900628,122.250910091201,122.27028827519),
 .UNSPECIFIED.);
#127=B_SPLINE_CURVE_WITH_KNOTS('',3,(#25455,#25456,#25457,#25458,#25459,
#25460,#25461,#25462,#25463,#25464,#25465,#25466,#25467,#25468,#25469,#25470,
#25471,#25472,#25473,#25474,#25475,#25476,#25477,#25478,#25479,#25480,#25481,
#25482,#25483,#25484,#25485,#25486,#25487,#25488,#25489,#25490,#25491,#25492,
#25493,#25494,#25495,#25496,#25497,#25498,#25499,#25500,#25501,#25502,#25503,
#25504,#25505,#25506,#25507,#25508,#25509,#25510,#25511,#25512,#25513,#25514,
#25515,#25516,#25517,#25518,#25519,#25520,#25521,#25522,#25523,#25524,#25525,
#25526,#25527,#25528,#25529,#25530,#25531,#25532,#25533,#25534,#25535,#25536,
#25537,#25538,#25539,#25540,#25541,#25542,#25543,#25544,#25545,#25546,#25547,
#25548,#25549,#25550,#25551,#25552,#25553,#25554,#25555,#25556,#25557,#25558,
#25559,#25560,#25561,#25562,#25563,#25564,#25565,#25566,#25567,#25568,#25569,
#25570,#25571,#25572,#25573,#25574,#25575,#25576,#25577,#25578,#25579,#25580,
#25581,#25582,#25583,#25584,#25585,#25586,#25587,#25588,#25589,#25590,#25591,
#25592,#25593,#25594,#25595,#25596,#25597,#25598,#25599,#25600,#25601,#25602,
#25603,#25604,#25605,#25606,#25607,#25608,#25609,#25610,#25611,#25612,#25613,
#25614,#25615,#25616,#25617,#25618,#25619,#25620,#25621,#25622,#25623,#25624,
#25625,#25626,#25627,#25628,#25629,#25630,#25631,#25632,#25633,#25634,#25635,
#25636,#25637,#25638,#25639,#25640,#25641,#25642,#25643,#25644,#25645,#25646,
#25647,#25648,#25649,#25650,#25651,#25652,#25653,#25654,#25655,#25656,#25657,
#25658,#25659,#25660,#25661,#25662,#25663,#25664,#25665,#25666,#25667,#25668,
#25669,#25670,#25671,#25672,#25673,#25674),.UNSPECIFIED.,.F.,.F.,(4,3,3,
3,3,3,3,3,3,3,3,3,3,3,3,3,3,3,3,3,3,3,3,3,3,3,3,3,3,3,3,3,3,3,3,3,3,3,3,
3,3,3,3,3,3,3,3,3,3,3,3,3,3,3,3,3,3,3,3,3,3,3,3,3,3,3,3,3,3,3,3,3,3,4),
(122.522113489983,122.604654564358,122.688518256317,122.770981109149,122.853436233243,
122.93590249609,123.020817897075,123.103407097541,123.189485598785,123.275564100028,
123.359302811874,123.442938323242,123.52649076664,123.609980202491,123.693434153104,
123.77687064695,123.860307756706,123.943763551624,124.027308044353,124.110897127294,
124.194620394852,124.275300110748,124.359038822594,124.442674333961,124.52622677736,
124.609716213211,124.693170163825,124.776606657671,124.860043767427,124.943499562344,
125.027044055074,125.110633138015,125.194356405572,125.275036121468,125.358774833314,
125.442410344681,125.52596278808,125.609452223931,125.692906174545,125.776342668391,
125.859779778146,125.943235573064,126.026780065794,126.110369148735,126.194092416292,
126.274772132188,126.358510844034,126.442146355402,126.5256987988,126.609188234651,
126.692642185265,126.776078679111,126.859515788866,126.942971583784,127.026516076514,
127.110105159455,127.193828427013,127.274508142908,127.358246854754,127.441882366121,
127.525434809519,127.60892424537,127.692378195984,127.77581468983,127.859251799586,
127.942707594504,128.026252087233,128.109841170174,128.193564437732,128.274244153628,
128.361156935022,128.44794892309,128.534597940399,128.554911617023),
 .UNSPECIFIED.);
#128=B_SPLINE_CURVE_WITH_KNOTS('',3,(#25675,#25676,#25677,#25678,#25679,
#25680,#25681,#25682,#25683,#25684,#25685,#25686,#25687),.UNSPECIFIED.,
 .F.,.F.,(4,3,3,3,4),(122.271018544109,122.275828089307,122.386363683307,
122.494373601401,122.522113489845),.UNSPECIFIED.);
#129=B_SPLINE_CURVE_WITH_KNOTS('',3,(#25689,#25690,#25691,#25692,#25693,
#25694,#25695,#25696,#25697,#25698),.UNSPECIFIED.,.F.,.F.,(4,3,3,4),(122.27028827519,
122.35308028165,122.43759688576,122.52211348987),.UNSPECIFIED.);
#130=B_SPLINE_CURVE_WITH_KNOTS('',3,(#25699,#25700,#25701,#25702,#25703,
#25704,#25705,#25706,#25707,#25708,#25709,#25710,#25711,#25712,#25713,#25714,
#25715,#25716,#25717,#25718,#25719,#25720,#25721,#25722,#25723,#25724,#25725,
#25726,#25727,#25728,#25729,#25730,#25731,#25732,#25733,#25734,#25735,#25736,
#25737,#25738,#25739,#25740,#25741,#25742,#25743,#25744,#25745,#25746,#25747,
#25748,#25749,#25750,#25751,#25752,#25753,#25754,#25755,#25756,#25757,#25758,
#25759,#25760,#25761,#25762,#25763,#25764,#25765,#25766,#25767,#25768,#25769,
#25770,#25771,#25772,#25773,#25774,#25775,#25776,#25777,#25778,#25779,#25780,
#25781,#25782,#25783,#25784,#25785,#25786,#25787,#25788,#25789,#25790,#25791,
#25792,#25793,#25794,#25795,#25796,#25797,#25798,#25799,#25800,#25801,#25802,
#25803,#25804,#25805,#25806,#25807,#25808,#25809,#25810,#25811,#25812,#25813,
#25814,#25815,#25816,#25817,#25818,#25819,#25820,#25821,#25822,#25823,#25824,
#25825,#25826,#25827,#25828,#25829,#25830,#25831,#25832,#25833,#25834,#25835,
#25836,#25837,#25838,#25839,#25840,#25841,#25842,#25843,#25844,#25845,#25846,
#25847,#25848,#25849,#25850,#25851,#25852,#25853,#25854,#25855,#25856,#25857,
#25858,#25859,#25860,#25861,#25862,#25863,#25864,#25865,#25866,#25867,#25868,
#25869,#25870,#25871,#25872,#25873,#25874,#25875,#25876,#25877,#25878,#25879,
#25880,#25881,#25882,#25883,#25884,#25885,#25886,#25887,#25888,#25889,#25890,
#25891,#25892,#25893,#25894,#25895,#25896,#25897,#25898,#25899,#25900,#25901,
#25902,#25903,#25904,#25905,#25906,#25907,#25908,#25909,#25910,#25911,#25912,
#25913,#25914,#25915,#25916,#25917,#25918),.UNSPECIFIED.,.F.,.F.,(4,3,3,
3,3,3,3,3,3,3,3,3,3,3,3,3,3,3,3,3,3,3,3,3,3,3,3,3,3,3,3,3,3,3,3,3,3,3,3,
3,3,3,3,3,3,3,3,3,3,3,3,3,3,3,3,3,3,3,3,3,3,3,3,3,3,3,3,3,3,3,3,3,3,4),
(122.522113489987,122.586118709022,122.669857420868,122.753492932236,122.837045375634,
122.920534811485,123.003988762099,123.087425255945,123.170862365701,123.254318160619,
123.337862653349,123.42145173629,123.505175003848,123.585854719742,123.669593431588,
123.753228942956,123.836781386354,123.920270822205,124.003724772819,124.087161266665,
124.170598376421,124.254054171338,124.337598664068,124.421187747009,124.504911014567,
124.585590730463,124.669329442309,124.752964953677,124.836517397075,124.920006832926,
125.00346078354,125.086897277386,125.170334387142,125.25379018206,125.337334674789,
125.42092375773,125.504647025288,125.585326741183,125.669065453029,125.752700964396,
125.836253407795,125.919742843646,126.003196794259,126.086633288106,126.170070397861,
126.253526192779,126.337070685508,126.420659768449,126.504383036007,126.585062751903,
126.668801463749,126.752436975116,126.835989418515,126.919478854366,127.00293280498,
127.086369298826,127.169806408581,127.253262203499,127.336806696229,127.42039577917,
127.504119046727,127.584798762623,127.668539201737,127.752176038431,127.835729406909,
127.919219368881,128.002671805427,128.086106216966,128.169540675799,128.252993250309,
128.336526720534,128.420104546152,128.503798371839,128.554060123745),
 .UNSPECIFIED.);
#131=B_SPLINE_CURVE_WITH_KNOTS('',3,(#25924,#25925,#25926,#25927,#25928,
#25929,#25930,#25931,#25932,#25933,#25934,#25935,#25936,#25937,#25938,#25939,
#25940,#25941,#25942,#25943,#25944,#25945,#25946,#25947,#25948,#25949,#25950,
#25951,#25952,#25953,#25954,#25955,#25956,#25957,#25958,#25959,#25960,#25961,
#25962,#25963,#25964,#25965,#25966,#25967,#25968,#25969,#25970,#25971,#25972,
#25973,#25974,#25975,#25976,#25977,#25978,#25979,#25980,#25981,#25982,#25983,
#25984,#25985,#25986,#25987,#25988,#25989,#25990,#25991,#25992,#25993,#25994,
#25995,#25996,#25997,#25998,#25999,#26000,#26001,#26002,#26003,#26004,#26005,
#26006,#26007,#26008,#26009,#26010,#26011,#26012,#26013,#26014,#26015,#26016,
#26017,#26018,#26019,#26020,#26021,#26022,#26023,#26024,#26025,#26026,#26027,
#26028,#26029,#26030,#26031,#26032,#26033,#26034,#26035,#26036,#26037,#26038,
#26039,#26040,#26041,#26042,#26043,#26044,#26045,#26046,#26047,#26048,#26049,
#26050,#26051,#26052,#26053,#26054,#26055,#26056,#26057,#26058,#26059,#26060,
#26061,#26062,#26063,#26064,#26065,#26066,#26067,#26068,#26069,#26070,#26071,
#26072,#26073,#26074,#26075,#26076,#26077,#26078,#26079,#26080,#26081,#26082,
#26083,#26084,#26085,#26086,#26087,#26088,#26089,#26090,#26091,#26092,#26093,
#26094,#26095,#26096,#26097,#26098,#26099,#26100,#26101,#26102,#26103,#26104,
#26105,#26106,#26107,#26108,#26109,#26110,#26111,#26112,#26113,#26114,#26115,
#26116,#26117,#26118,#26119,#26120,#26121,#26122,#26123,#26124,#26125,#26126,
#26127,#26128,#26129,#26130,#26131,#26132,#26133,#26134,#26135,#26136,#26137,
#26138,#26139,#26140,#26141,#26142,#26143),.UNSPECIFIED.,.F.,.F.,(4,3,3,
3,3,3,3,3,3,3,3,3,3,3,3,3,3,3,3,3,3,3,3,3,3,3,3,3,3,3,3,3,3,3,3,3,3,3,3,
3,3,3,3,3,3,3,3,3,3,3,3,3,3,3,3,3,3,3,3,3,3,3,3,3,3,3,3,3,3,3,3,3,3,4),
(128.805298797295,128.8939242966,128.982712920427,129.07175499949,129.160936434563,
129.250328626049,129.273980164348,129.357718876194,129.441354387561,129.52490683096,
129.608396266811,129.691850217425,129.775286711271,129.858723821027,129.942179615945,
130.025724108675,130.109313191616,130.193036459173,130.273716175068,130.357454886914,
130.441090398282,130.52464284168,130.608132277531,130.691586228145,130.775022721991,
130.858459831747,130.941915626664,131.025460119394,131.109049202335,131.192772469893,
131.273452185789,131.357190897635,131.440826409003,131.524378852401,131.607868288252,
131.691322238866,131.774758732712,131.858195842468,131.941651637385,132.025196130115,
132.108785213056,132.192508480614,132.273188196509,132.356926908355,132.440562419722,
132.524114863121,132.607604298972,132.691058249585,132.774494743432,132.857931853187,
132.941387648105,133.024932140834,133.108521223775,133.192244491333,133.272924207229,
133.356662919075,133.440298430442,133.523850873841,133.607340309692,133.690794260306,
133.774230754152,133.857667863907,133.941123658825,134.024668151555,134.108257234496,
134.191980502053,134.272660217949,134.355141887779,134.43752788941,134.519837440161,
134.602089086034,134.684305498508,134.766524040057,134.836834981773),
 .UNSPECIFIED.);
#132=B_SPLINE_CURVE_WITH_KNOTS('',3,(#26144,#26145,#26146,#26147,#26148,
#26149,#26150,#26151,#26152,#26153),.UNSPECIFIED.,.F.,.F.,(4,3,3,4),(128.554911617023,
128.641404974725,128.727785214999,128.805298797162),.UNSPECIFIED.);
#133=B_SPLINE_CURVE_WITH_KNOTS('',3,(#26155,#26156,#26157,#26158,#26159,
#26160,#26161,#26162,#26163,#26164),.UNSPECIFIED.,.F.,.F.,(4,3,3,4),(128.554060123745,
128.584534773343,128.699129012509,128.805298797166),.UNSPECIFIED.);
#134=B_SPLINE_CURVE_WITH_KNOTS('',3,(#26165,#26166,#26167,#26168,#26169,
#26170,#26171,#26172,#26173,#26174,#26175,#26176,#26177,#26178,#26179,#26180,
#26181,#26182,#26183,#26184,#26185,#26186,#26187,#26188,#26189,#26190,#26191,
#26192,#26193,#26194,#26195,#26196,#26197,#26198,#26199,#26200,#26201,#26202,
#26203,#26204,#26205,#26206,#26207,#26208,#26209,#26210,#26211,#26212,#26213,
#26214,#26215,#26216,#26217,#26218,#26219,#26220,#26221,#26222,#26223,#26224,
#26225,#26226,#26227,#26228,#26229,#26230,#26231,#26232,#26233,#26234,#26235,
#26236,#26237,#26238,#26239,#26240,#26241,#26242,#26243,#26244,#26245,#26246,
#26247,#26248,#26249,#26250,#26251,#26252,#26253,#26254,#26255,#26256,#26257,
#26258,#26259,#26260,#26261,#26262,#26263,#26264,#26265,#26266,#26267,#26268,
#26269,#26270,#26271,#26272,#26273,#26274,#26275,#26276,#26277,#26278,#26279,
#26280,#26281,#26282,#26283,#26284,#26285,#26286,#26287,#26288,#26289,#26290,
#26291,#26292,#26293,#26294,#26295,#26296,#26297,#26298,#26299,#26300,#26301,
#26302,#26303,#26304,#26305,#26306,#26307,#26308,#26309,#26310,#26311,#26312,
#26313,#26314,#26315,#26316,#26317,#26318,#26319,#26320,#26321,#26322,#26323,
#26324,#26325,#26326,#26327,#26328,#26329,#26330,#26331,#26332,#26333,#26334,
#26335,#26336,#26337,#26338,#26339,#26340,#26341,#26342,#26343,#26344,#26345,
#26346,#26347,#26348,#26349,#26350,#26351,#26352,#26353,#26354,#26355,#26356,
#26357,#26358,#26359,#26360,#26361,#26362,#26363,#26364,#26365,#26366,#26367,
#26368,#26369,#26370,#26371,#26372,#26373,#26374,#26375,#26376,#26377,#26378,
#26379,#26380,#26381,#26382,#26383,#26384),.UNSPECIFIED.,.F.,.F.,(4,3,3,
3,3,3,3,3,3,3,3,3,3,3,3,3,3,3,3,3,3,3,3,3,3,3,3,3,3,3,3,3,3,3,3,3,3,3,3,
3,3,3,3,3,3,3,3,3,3,3,3,3,3,3,3,3,3,3,3,3,3,3,3,3,3,3,3,3,3,3,3,3,3,4),
(128.805298797311,128.887726483839,128.970091451098,129.052422139225,129.134737418886,
129.217056253792,129.299397608162,129.381826252758,129.464304627651,129.546902434122,
129.584270784063,129.668009495909,129.751645007276,129.835197450675,129.918686886526,
130.002140837139,130.085577330985,130.169014440741,130.252470235658,130.336014728388,
130.419603811329,130.503327078886,130.584006794783,130.667745506629,130.751381017996,
130.834933461395,130.918422897246,131.00187684786,131.085313341706,131.168750451462,
131.252206246379,131.335750739109,131.41933982205,131.503063089608,131.583742805503,
131.667481517349,131.751117028716,131.834669472115,131.918158907966,132.00161285858,
132.085049352426,132.168486462181,132.251942257099,132.335486749829,132.41907583277,
132.502799100327,132.583478816224,132.66721752807,132.750853039438,132.834405482836,
132.917894918687,133.001348869301,133.084785363147,133.168222472903,133.25167826782,
133.33522276055,133.418811843492,133.502535111049,133.583214826944,133.66695353879,
133.750589050157,133.834141493555,133.917630929406,134.00108488002,134.084521373866,
134.167958483622,134.251414278539,134.334958771269,134.41854785421,134.502271121768,
134.582950837664,134.670785363976,134.758427403399,134.838147840597),
 .UNSPECIFIED.);
#135=B_SPLINE_CURVE_WITH_KNOTS('',3,(#26390,#26391,#26392,#26393,#26394,
#26395,#26396,#26397,#26398,#26399,#26400,#26401,#26402,#26403,#26404,#26405,
#26406,#26407,#26408,#26409,#26410,#26411,#26412,#26413,#26414,#26415,#26416,
#26417,#26418,#26419,#26420,#26421,#26422,#26423,#26424,#26425,#26426,#26427,
#26428,#26429,#26430,#26431,#26432,#26433,#26434,#26435,#26436,#26437,#26438,
#26439,#26440,#26441,#26442,#26443,#26444,#26445,#26446,#26447,#26448,#26449,
#26450,#26451,#26452,#26453,#26454,#26455,#26456,#26457,#26458,#26459,#26460,
#26461,#26462,#26463,#26464,#26465,#26466,#26467,#26468,#26469,#26470,#26471,
#26472,#26473,#26474,#26475,#26476,#26477,#26478,#26479,#26480,#26481,#26482,
#26483,#26484,#26485,#26486,#26487,#26488,#26489,#26490,#26491,#26492,#26493,
#26494,#26495,#26496,#26497,#26498,#26499,#26500,#26501,#26502,#26503,#26504,
#26505,#26506,#26507,#26508,#26509,#26510,#26511,#26512,#26513,#26514,#26515,
#26516,#26517,#26518,#26519,#26520,#26521,#26522,#26523,#26524,#26525,#26526,
#26527,#26528,#26529,#26530,#26531,#26532,#26533,#26534,#26535,#26536,#26537,
#26538,#26539,#26540,#26541,#26542,#26543,#26544,#26545,#26546,#26547,#26548,
#26549,#26550,#26551,#26552,#26553,#26554,#26555,#26556,#26557,#26558,#26559,
#26560,#26561,#26562,#26563,#26564,#26565,#26566,#26567,#26568,#26569,#26570,
#26571,#26572,#26573,#26574,#26575,#26576,#26577,#26578,#26579,#26580,#26581,
#26582,#26583,#26584,#26585,#26586,#26587,#26588,#26589,#26590,#26591,#26592,
#26593,#26594,#26595,#26596,#26597,#26598,#26599,#26600,#26601,#26602,#26603,
#26604,#26605,#26606,#26607,#26608,#26609),.UNSPECIFIED.,.F.,.F.,(4,3,3,
3,3,3,3,3,3,3,3,3,3,3,3,3,3,3,3,3,3,3,3,3,3,3,3,3,3,3,3,3,3,3,3,3,3,3,3,
3,3,3,3,3,3,3,3,3,3,3,3,3,3,3,3,3,3,3,3,3,3,3,3,3,3,3,3,3,3,3,3,3,3,4),
(135.088484104342,135.214157566306,135.272396228669,135.356134940515,135.439770451882,
135.523322895281,135.606812331132,135.690266281746,135.773702775592,135.857139885347,
135.940595680265,136.024140172995,136.107729255936,136.191452523493,136.272132239389,
136.355870951235,136.439506462602,136.523058906001,136.606548341852,136.690002292465,
136.773438786311,136.856875896067,136.940331690984,137.023876183714,137.107465266655,
137.191188534212,137.271868250109,137.355606961955,137.439242473323,137.522794916721,
137.606284352572,137.689738303186,137.773174797032,137.856611906788,137.940067701705,
138.023612194435,138.107201277376,138.190924544934,138.271604260829,138.355342972675,
138.438978484043,138.522530927441,138.606020363292,138.689474313906,138.772910807752,
138.856347917508,138.939803712425,139.023348205155,139.106937288096,139.190660555654,
139.27134027155,139.355078983396,139.438714494763,139.522266938162,139.605756374013,
139.689210324627,139.772646818473,139.856083928229,139.939539723146,140.023084215876,
140.106673298817,140.190396566375,140.27107628227,140.354823944191,140.43846641674,
140.523663793172,140.607149308209,140.690596820117,140.774024417531,140.860529670196,
140.944000016269,141.027498490743,141.111069615446,141.120045428192),
 .UNSPECIFIED.);
#136=B_SPLINE_CURVE_WITH_KNOTS('',3,(#26610,#26611,#26612,#26613,#26614,
#26615,#26616,#26617,#26618,#26619),.UNSPECIFIED.,.F.,.F.,(4,3,3,4),(134.836834981773,
134.919091621056,135.003787862626,135.088484104197),.UNSPECIFIED.);
#137=B_SPLINE_CURVE_WITH_KNOTS('',3,(#26621,#26622,#26623,#26624,#26625,
#26626,#26627,#26628,#26629,#26630),.UNSPECIFIED.,.F.,.F.,(4,3,3,4),(134.838147840597,
134.925534959382,135.012769870911,135.088484104346),.UNSPECIFIED.);
#138=B_SPLINE_CURVE_WITH_KNOTS('',3,(#26631,#26632,#26633,#26634,#26635,
#26636,#26637,#26638,#26639,#26640,#26641,#26642,#26643,#26644,#26645,#26646,
#26647,#26648,#26649,#26650,#26651,#26652,#26653,#26654,#26655,#26656,#26657,
#26658,#26659,#26660,#26661,#26662,#26663,#26664,#26665,#26666,#26667,#26668,
#26669,#26670,#26671,#26672,#26673,#26674,#26675,#26676,#26677,#26678,#26679,
#26680,#26681,#26682,#26683,#26684,#26685,#26686,#26687,#26688,#26689,#26690,
#26691,#26692,#26693,#26694,#26695,#26696,#26697,#26698,#26699,#26700,#26701,
#26702,#26703,#26704,#26705,#26706,#26707,#26708,#26709,#26710,#26711,#26712,
#26713,#26714,#26715,#26716,#26717,#26718,#26719,#26720,#26721,#26722,#26723,
#26724,#26725,#26726,#26727,#26728,#26729,#26730,#26731,#26732,#26733,#26734,
#26735,#26736,#26737,#26738,#26739,#26740,#26741,#26742,#26743,#26744,#26745,
#26746,#26747,#26748,#26749,#26750,#26751,#26752,#26753,#26754,#26755,#26756,
#26757,#26758,#26759,#26760,#26761,#26762,#26763,#26764,#26765,#26766,#26767,
#26768,#26769,#26770,#26771,#26772,#26773,#26774,#26775,#26776,#26777,#26778,
#26779,#26780,#26781,#26782,#26783,#26784,#26785,#26786,#26787,#26788,#26789,
#26790,#26791,#26792,#26793,#26794,#26795,#26796,#26797,#26798,#26799,#26800,
#26801,#26802,#26803,#26804,#26805,#26806,#26807,#26808,#26809,#26810,#26811,
#26812,#26813,#26814,#26815,#26816,#26817,#26818,#26819,#26820,#26821,#26822,
#26823,#26824,#26825,#26826,#26827,#26828,#26829,#26830,#26831,#26832,#26833,
#26834,#26835,#26836,#26837,#26838,#26839,#26840,#26841,#26842,#26843,#26844,
#26845,#26846,#26847,#26848,#26849,#26850),.UNSPECIFIED.,.F.,.F.,(4,3,3,
3,3,3,3,3,3,3,3,3,3,3,3,3,3,3,3,3,3,3,3,3,3,3,3,3,3,3,3,3,3,3,3,3,3,3,3,
3,3,3,3,3,3,3,3,3,3,3,3,3,3,3,3,3,3,3,3,3,3,3,3,3,3,3,3,3,3,3,3,3,3,4),
(135.088484104467,135.176096259964,135.26383125192,135.351780680477,135.439844267785,
135.52811071901,135.582686848384,135.66642556023,135.750061071597,135.833613514996,
135.917102950847,136.00055690146,136.083993395307,136.167430505062,136.25088629998,
136.334430792709,136.41801987565,136.501743143208,136.582422859104,136.66616157095,
136.749797082317,136.833349525716,136.916838961567,137.000292912181,137.083729406027,
137.167166515782,137.2506223107,137.33416680343,137.417755886371,137.501479153928,
137.582158869824,137.66589758167,137.749533093037,137.833085536436,137.916574972287,
138.000028922901,138.083465416747,138.166902526502,138.25035832142,138.33390281415,
138.417491897091,138.501215164648,138.581894880544,138.66563359239,138.749269103757,
138.832821547156,138.916310983007,138.999764933621,139.083201427467,139.166638537223,
139.25009433214,139.33363882487,139.417227907811,139.500951175369,139.581630891264,
139.66536960311,139.749005114477,139.832557557876,139.916046993727,139.999500944341,
140.082937438187,140.166374547942,140.24983034286,140.33337483559,140.416963918531,
140.500687186089,140.581366901985,140.6639127266,140.7463621142,140.82873424645,
140.911045277623,140.993320565168,141.075589977367,141.120120147634),
 .UNSPECIFIED.);
#139=B_SPLINE_CURVE_WITH_KNOTS('',3,(#26856,#26857,#26858,#26859,#26860,
#26861,#26862,#26863,#26864,#26865,#26866,#26867,#26868,#26869,#26870,#26871,
#26872,#26873,#26874,#26875,#26876,#26877,#26878,#26879,#26880,#26881,#26882,
#26883,#26884,#26885,#26886,#26887,#26888,#26889,#26890,#26891,#26892,#26893,
#26894,#26895,#26896,#26897,#26898,#26899,#26900,#26901,#26902,#26903,#26904,
#26905,#26906,#26907,#26908,#26909,#26910,#26911,#26912,#26913,#26914,#26915,
#26916,#26917,#26918,#26919,#26920,#26921,#26922,#26923,#26924,#26925,#26926,
#26927,#26928,#26929,#26930,#26931,#26932,#26933,#26934,#26935,#26936,#26937,
#26938,#26939,#26940,#26941,#26942,#26943,#26944,#26945,#26946,#26947,#26948,
#26949,#26950,#26951,#26952,#26953,#26954,#26955,#26956,#26957,#26958,#26959,
#26960,#26961,#26962,#26963,#26964,#26965,#26966,#26967,#26968,#26969,#26970,
#26971,#26972,#26973,#26974,#26975,#26976,#26977,#26978,#26979,#26980,#26981,
#26982,#26983,#26984,#26985,#26986,#26987,#26988,#26989,#26990,#26991,#26992,
#26993,#26994,#26995,#26996,#26997,#26998,#26999,#27000,#27001,#27002,#27003,
#27004,#27005,#27006,#27007,#27008,#27009,#27010,#27011,#27012,#27013,#27014,
#27015,#27016,#27017,#27018,#27019,#27020,#27021,#27022,#27023,#27024,#27025,
#27026,#27027,#27028,#27029,#27030,#27031,#27032,#27033,#27034,#27035,#27036,
#27037,#27038,#27039,#27040,#27041,#27042,#27043,#27044,#27045,#27046,#27047,
#27048,#27049,#27050,#27051,#27052,#27053,#27054,#27055,#27056,#27057,#27058,
#27059,#27060,#27061,#27062,#27063,#27064,#27065,#27066,#27067,#27068,#27069,
#27070,#27071,#27072,#27073,#27074,#27075),.UNSPECIFIED.,.F.,.F.,(4,3,3,
3,3,3,3,3,3,3,3,3,3,3,3,3,3,3,3,3,3,3,3,3,3,3,3,3,3,3,3,3,3,3,3,3,3,3,3,
3,3,3,3,3,3,3,3,3,3,3,3,3,3,3,3,3,3,3,3,3,3,3,3,3,3,3,3,3,3,3,3,3,3,4),
(141.371669411658,141.454304261838,141.536846637303,141.619317585863,141.701742710514,
141.784144477249,141.866541802964,141.948953598539,142.031448791127,142.113986382401,
142.196653608407,142.27054830371,142.354287015556,142.437922526923,142.521474970322,
142.604964406173,142.688418356786,142.771854850632,142.855291960388,142.938747755305,
143.022292248035,143.105881330976,143.189604598533,143.27028431443,143.354023026276,
143.437658537643,143.521210981042,143.604700416893,143.688154367507,143.771590861353,
143.855027971109,143.938483766026,144.022028258756,144.105617341697,144.189340609254,
144.27002032515,144.353759036996,144.437394548363,144.520946991762,144.604436427613,
144.687890378227,144.771326872073,144.854763981828,144.938219776746,145.021764269475,
145.105353352416,145.189076619974,145.26975633587,145.353495047716,145.437130559084,
145.520683002482,145.604172438333,145.687626388947,145.771062882794,145.854499992549,
145.937955787467,146.021500280197,146.105089363138,146.188812630696,146.26949234659,
146.353231058436,146.436866569804,146.520419013202,146.603908449053,146.687362399667,
146.770798893513,146.854236003269,146.937691798186,147.021236290916,147.104825373857,
147.188548641414,147.269228357311,147.363365580996,147.404444607709),
 .UNSPECIFIED.);
#140=B_SPLINE_CURVE_WITH_KNOTS('',3,(#27076,#27077,#27078,#27079,#27080,
#27081,#27082,#27083,#27084,#27085),.UNSPECIFIED.,.F.,.F.,(4,3,3,4),(141.120045428192,
141.203773533166,141.27081229299,141.371669411522),.UNSPECIFIED.);
#141=B_SPLINE_CURVE_WITH_KNOTS('',3,(#27087,#27088,#27089,#27090,#27091,
#27092,#27093,#27094,#27095,#27096),.UNSPECIFIED.,.F.,.F.,(4,3,3,4),(141.120120147634,
141.20242193175,141.287045671566,141.371669411383),.UNSPECIFIED.);
#142=B_SPLINE_CURVE_WITH_KNOTS('',3,(#27097,#27098,#27099,#27100,#27101,
#27102,#27103,#27104,#27105,#27106,#27107,#27108,#27109,#27110,#27111,#27112,
#27113,#27114,#27115,#27116,#27117,#27118,#27119,#27120,#27121,#27122,#27123,
#27124,#27125,#27126,#27127,#27128,#27129,#27130,#27131,#27132,#27133,#27134,
#27135,#27136,#27137,#27138,#27139,#27140,#27141,#27142,#27143,#27144,#27145,
#27146,#27147,#27148,#27149,#27150,#27151,#27152,#27153,#27154,#27155,#27156,
#27157,#27158,#27159,#27160,#27161,#27162,#27163,#27164,#27165,#27166,#27167,
#27168,#27169,#27170,#27171,#27172,#27173,#27174,#27175,#27176,#27177,#27178,
#27179,#27180,#27181,#27182,#27183,#27184,#27185,#27186,#27187,#27188,#27189,
#27190,#27191,#27192,#27193,#27194,#27195,#27196,#27197,#27198,#27199,#27200,
#27201,#27202,#27203,#27204,#27205,#27206,#27207,#27208,#27209,#27210,#27211,
#27212,#27213,#27214,#27215,#27216,#27217,#27218,#27219,#27220,#27221,#27222,
#27223,#27224,#27225,#27226,#27227,#27228,#27229,#27230,#27231,#27232,#27233,
#27234,#27235,#27236,#27237,#27238,#27239,#27240,#27241,#27242,#27243,#27244,
#27245,#27246,#27247,#27248,#27249,#27250,#27251,#27252,#27253,#27254,#27255,
#27256,#27257,#27258,#27259,#27260,#27261,#27262,#27263,#27264,#27265,#27266,
#27267,#27268,#27269,#27270,#27271,#27272,#27273,#27274,#27275,#27276,#27277,
#27278,#27279,#27280,#27281,#27282,#27283,#27284,#27285,#27286,#27287,#27288,
#27289,#27290,#27291,#27292,#27293,#27294,#27295,#27296,#27297,#27298,#27299,
#27300,#27301,#27302,#27303,#27304,#27305,#27306,#27307,#27308,#27309,#27310,
#27311,#27312,#27313),.UNSPECIFIED.,.F.,.F.,(4,3,3,3,3,3,3,3,3,3,3,3,3,
3,3,3,3,3,3,3,3,3,3,3,3,3,3,3,3,3,3,3,3,3,3,3,3,3,3,3,3,3,3,3,3,3,3,3,3,
3,3,3,3,3,3,3,3,3,3,3,3,3,3,3,3,3,3,3,3,3,3,3,4),(141.371669411525,141.489150236208,
141.581102912705,141.664841624551,141.748477135919,141.832029579317,141.915519015168,
141.998972965782,142.082409459628,142.165846569383,142.249302364301,142.332846857031,
142.416435939972,142.50015920753,142.580838923425,142.664577635271,142.748213146638,
142.831765590037,142.915255025888,142.998708976501,143.082145470347,143.165582580103,
143.24903837502,143.33258286775,143.416171950691,143.499895218248,143.580574934145,
143.664313645991,143.747949157358,143.831501600757,143.914991036608,143.998444987222,
144.081881481068,144.165318590823,144.248774385741,144.332318878471,144.415907961412,
144.499631228969,144.580310944865,144.664049656711,144.747685168078,144.831237611477,
144.914727047328,144.998180997942,145.081617491788,145.165054601543,145.248510396461,
145.332054889191,145.415643972132,145.499367239689,145.580046955585,145.663785667431,
145.747421178799,145.830973622197,145.914463058048,145.997917008662,146.081353502508,
146.164790612264,146.248246407181,146.331790899911,146.415379982852,146.49910325041,
146.579782966305,146.6635322455,146.747175998179,146.830719293296,146.914205630078,
146.997653127976,147.081079876464,147.164531967087,147.247994869194,147.331531662987,
147.403202100703),.UNSPECIFIED.);
#143=B_SPLINE_CURVE_WITH_KNOTS('',3,(#27319,#27320,#27321,#27322,#27323,
#27324,#27325,#27326,#27327,#27328,#27329,#27330,#27331,#27332,#27333,#27334,
#27335,#27336,#27337,#27338,#27339,#27340,#27341,#27342,#27343,#27344,#27345,
#27346,#27347,#27348,#27349,#27350,#27351,#27352,#27353,#27354,#27355,#27356,
#27357,#27358,#27359,#27360,#27361,#27362,#27363,#27364,#27365,#27366,#27367,
#27368,#27369,#27370,#27371,#27372,#27373,#27374,#27375,#27376,#27377,#27378,
#27379,#27380,#27381,#27382,#27383,#27384,#27385,#27386,#27387,#27388,#27389,
#27390,#27391,#27392,#27393,#27394,#27395,#27396,#27397,#27398,#27399,#27400,
#27401,#27402,#27403,#27404,#27405,#27406,#27407,#27408,#27409,#27410,#27411,
#27412,#27413,#27414,#27415,#27416,#27417,#27418,#27419,#27420,#27421,#27422,
#27423,#27424,#27425,#27426,#27427,#27428,#27429,#27430,#27431,#27432,#27433,
#27434,#27435,#27436,#27437,#27438,#27439,#27440,#27441,#27442,#27443,#27444,
#27445,#27446,#27447,#27448,#27449,#27450,#27451,#27452,#27453,#27454,#27455,
#27456,#27457,#27458,#27459,#27460,#27461,#27462,#27463,#27464,#27465,#27466,
#27467,#27468,#27469,#27470,#27471,#27472,#27473,#27474,#27475,#27476,#27477,
#27478,#27479,#27480,#27481,#27482,#27483,#27484,#27485,#27486,#27487,#27488,
#27489,#27490,#27491,#27492,#27493,#27494,#27495,#27496,#27497,#27498,#27499,
#27500,#27501,#27502,#27503,#27504,#27505,#27506,#27507,#27508,#27509,#27510,
#27511,#27512,#27513,#27514,#27515,#27516,#27517,#27518,#27519,#27520,#27521,
#27522,#27523,#27524,#27525,#27526,#27527,#27528,#27529,#27530,#27531,#27532,
#27533,#27534,#27535,#27536,#27537,#27538),.UNSPECIFIED.,.F.,.F.,(4,3,3,
3,3,3,3,3,3,3,3,3,3,3,3,3,3,3,3,3,3,3,3,3,3,3,3,3,3,3,3,3,3,3,3,3,3,3,3,
3,3,3,3,3,3,3,3,3,3,3,3,3,3,3,3,3,3,3,3,3,3,3,3,3,3,3,3,3,3,3,3,3,3,4),
(147.654854718701,147.739123187276,147.823405100597,147.907717322165,147.992076731998,
148.07655108834,148.161092958481,148.245767361688,148.268964368031,148.352703079877,
148.436338591245,148.519891034643,148.603380470494,148.686834421108,148.770270914954,
148.85370802471,148.937163819627,149.020708312357,149.104297395298,149.188020662856,
149.268700378751,149.352439090597,149.436074601964,149.519627045363,149.603116481214,
149.686570431827,149.770006925673,149.853444035429,149.936899830347,150.020444323076,
150.104033406017,150.187756673575,150.268436389471,150.352175101317,150.435810612684,
150.519363056083,150.602852491934,150.686306442548,150.769742936394,150.85318004615,
150.936635841067,151.020180333797,151.103769416738,151.187492684296,151.268172400191,
151.351911112037,151.435546623404,151.519099066803,151.602588502654,151.686042453268,
151.769478947114,151.85291605687,151.936371851788,152.019916344517,152.103505427458,
152.187228695016,152.267908410911,152.351647122757,152.435282634124,152.518835077523,
152.602324513373,152.685778463987,152.769214957833,152.852652067589,152.936107862506,
153.019652355236,153.103241438177,153.186964705735,153.267644421631,153.351296231555,
153.435243463639,153.518685048359,153.602885104126,153.687085159892),
 .UNSPECIFIED.);
#144=B_SPLINE_CURVE_WITH_KNOTS('',3,(#27539,#27540,#27541,#27542,#27543,
#27544,#27545,#27546,#27547,#27548),.UNSPECIFIED.,.F.,.F.,(4,3,3,4),(147.404444607709,
147.498077880791,147.591207952791,147.654854718509),.UNSPECIFIED.);
#145=B_SPLINE_CURVE_WITH_KNOTS('',3,(#27550,#27551,#27552,#27553,#27554,
#27555,#27556,#27557,#27558,#27559,#27560,#27561,#27562),.UNSPECIFIED.,
 .F.,.F.,(4,3,3,3,4),(147.403202100703,147.486842374459,147.570597041304,
147.579518977026,147.654854718705),.UNSPECIFIED.);
#146=B_SPLINE_CURVE_WITH_KNOTS('',3,(#27563,#27564,#27565,#27566,#27567,
#27568,#27569,#27570,#27571,#27572,#27573,#27574,#27575,#27576,#27577,#27578,
#27579,#27580,#27581,#27582,#27583,#27584,#27585,#27586,#27587,#27588,#27589,
#27590,#27591,#27592,#27593,#27594,#27595,#27596,#27597,#27598,#27599,#27600,
#27601,#27602,#27603,#27604,#27605,#27606,#27607,#27608,#27609,#27610,#27611,
#27612,#27613,#27614,#27615,#27616,#27617,#27618,#27619,#27620,#27621,#27622,
#27623,#27624,#27625,#27626,#27627,#27628,#27629,#27630,#27631,#27632,#27633,
#27634,#27635,#27636,#27637,#27638,#27639,#27640,#27641,#27642,#27643,#27644,
#27645,#27646,#27647,#27648,#27649,#27650,#27651,#27652,#27653,#27654,#27655,
#27656,#27657,#27658,#27659,#27660,#27661,#27662,#27663,#27664,#27665,#27666,
#27667,#27668,#27669,#27670,#27671,#27672,#27673,#27674,#27675,#27676,#27677,
#27678,#27679,#27680,#27681,#27682,#27683,#27684,#27685,#27686,#27687,#27688,
#27689,#27690,#27691,#27692,#27693,#27694,#27695,#27696,#27697,#27698,#27699,
#27700,#27701,#27702,#27703,#27704,#27705,#27706,#27707,#27708,#27709,#27710,
#27711,#27712,#27713,#27714,#27715,#27716,#27717,#27718,#27719,#27720,#27721,
#27722,#27723,#27724,#27725,#27726,#27727,#27728,#27729,#27730,#27731,#27732,
#27733,#27734,#27735,#27736,#27737,#27738,#27739,#27740,#27741,#27742,#27743,
#27744,#27745,#27746,#27747,#27748,#27749,#27750,#27751,#27752,#27753,#27754,
#27755,#27756,#27757,#27758,#27759,#27760,#27761,#27762,#27763,#27764,#27765,
#27766,#27767,#27768,#27769,#27770,#27771,#27772,#27773,#27774,#27775,#27776,
#27777,#27778,#27779,#27780,#27781,#27782,#27783,#27784,#27785),
 .UNSPECIFIED.,.F.,.F.,(4,3,3,3,3,3,3,3,3,3,3,3,3,3,3,3,3,3,3,3,3,3,3,3,
3,3,3,3,3,3,3,3,3,3,3,3,3,3,3,3,3,3,3,3,3,3,3,3,3,3,3,3,3,3,3,3,3,3,3,3,
3,3,3,3,3,3,3,3,3,3,3,3,3,3,4),(147.654854718832,147.737687936593,147.820424429939,
147.903085126839,147.987606359453,148.070187266232,148.15275988548,148.235343009465,
148.321321004035,148.404026515879,148.486788223612,148.569662852917,148.579254987746,
148.662993699592,148.746629210959,148.830181654358,148.913671090209,148.997125040823,
149.080561534669,149.163998644425,149.247454439342,149.330998932072,149.414588015013,
149.498311282571,149.578990998466,149.662729710312,149.746365221679,149.829917665078,
149.913407100929,149.996861051543,150.080297545389,150.163734655145,150.247190450062,
150.330734942792,150.414324025733,150.498047293291,150.578727009186,150.662465721032,
150.746101232399,150.829653675798,150.913143111649,150.996597062262,151.080033556109,
151.163470665864,151.246926460781,151.330470953511,151.414060036452,151.497783304009,
151.578463019906,151.662201731752,151.745837243119,151.829389686518,151.91287912237,
151.996333072983,152.079769566829,152.163206676585,152.246662471503,152.330206964232,
152.413796047173,152.497519314731,152.578199030626,152.661937742472,152.745573253839,
152.829125697238,152.912615133089,152.996069083703,153.079505577549,153.162942687305,
153.246398482222,153.329942974952,153.413532057893,153.497255325451,153.577935041346,
153.674085070861,153.687545719545),.UNSPECIFIED.);
#147=B_SPLINE_CURVE_WITH_KNOTS('',3,(#27791,#27792,#27793,#27794,#27795,
#27796,#27797,#27798,#27799,#27800,#27801,#27802,#27803,#27804,#27805,#27806,
#27807,#27808,#27809,#27810,#27811,#27812,#27813,#27814,#27815,#27816,#27817,
#27818,#27819,#27820,#27821,#27822,#27823,#27824,#27825,#27826,#27827,#27828,
#27829,#27830,#27831,#27832,#27833,#27834,#27835,#27836,#27837,#27838,#27839,
#27840,#27841,#27842,#27843,#27844,#27845,#27846,#27847,#27848,#27849,#27850,
#27851,#27852,#27853,#27854,#27855,#27856,#27857,#27858,#27859,#27860,#27861,
#27862,#27863,#27864,#27865,#27866,#27867,#27868,#27869,#27870,#27871,#27872,
#27873,#27874,#27875,#27876,#27877,#27878,#27879,#27880,#27881,#27882,#27883,
#27884,#27885,#27886,#27887,#27888,#27889,#27890,#27891,#27892,#27893,#27894,
#27895,#27896,#27897,#27898,#27899,#27900,#27901,#27902,#27903,#27904,#27905,
#27906,#27907,#27908,#27909,#27910,#27911,#27912,#27913,#27914,#27915,#27916,
#27917,#27918,#27919,#27920,#27921,#27922,#27923,#27924,#27925,#27926,#27927,
#27928,#27929,#27930,#27931,#27932,#27933,#27934,#27935,#27936,#27937,#27938,
#27939,#27940,#27941,#27942,#27943,#27944,#27945,#27946,#27947,#27948,#27949,
#27950,#27951,#27952,#27953,#27954,#27955,#27956,#27957,#27958,#27959,#27960,
#27961,#27962,#27963,#27964,#27965,#27966,#27967,#27968,#27969,#27970,#27971,
#27972,#27973,#27974,#27975,#27976,#27977,#27978,#27979,#27980,#27981,#27982,
#27983,#27984,#27985,#27986,#27987,#27988,#27989,#27990,#27991,#27992,#27993,
#27994,#27995,#27996,#27997,#27998,#27999,#28000,#28001,#28002,#28003,#28004,
#28005,#28006,#28007,#28008,#28009,#28010),.UNSPECIFIED.,.F.,.F.,(4,3,3,
3,3,3,3,3,3,3,3,3,3,3,3,3,3,3,3,3,3,3,3,3,3,3,3,3,3,3,3,3,3,3,3,3,3,3,3,
3,3,3,3,3,3,3,3,3,3,3,3,3,3,3,3,3,3,3,3,3,3,3,3,3,3,3,3,3,3,3,3,3,3,4),
(153.938040026064,154.035637973361,154.133843211017,154.232747939408,154.267380432352,
154.351119144198,154.434754655565,154.518307098964,154.601796534815,154.685250485428,
154.768686979275,154.85212408903,154.935579883948,155.019124376677,155.102713459618,
155.186436727176,155.267116443072,155.350855154918,155.434490666285,155.518043109684,
155.601532545535,155.684986496149,155.768422989995,155.85186009975,155.935315894668,
156.018860387398,156.102449470339,156.186172737896,156.266852453792,156.350591165638,
156.434226677005,156.517779120404,156.601268556255,156.684722506869,156.768159000715,
156.85159611047,156.935051905388,157.018596398118,157.102185481059,157.185908748616,
157.266588464512,157.350327176358,157.433962687725,157.517515131124,157.601004566975,
157.684458517588,157.767895011435,157.85133212119,157.934787916108,158.018332408837,
158.101921491778,158.185644759336,158.266324475232,158.350063187078,158.433698698445,
158.517251141844,158.600740577695,158.684194528309,158.767631022155,158.85106813191,
158.934523926828,159.018068419558,159.101657502499,159.185380770056,159.266060485952,
159.349232519083,159.432273222354,159.515238066942,159.598145728663,159.681014837138,
159.76387911148,159.846740065297,159.929641331942,159.96943076146),
 .UNSPECIFIED.);
#148=B_SPLINE_CURVE_WITH_KNOTS('',3,(#28011,#28012,#28013,#28014,#28015,
#28016,#28017,#28018,#28019,#28020),.UNSPECIFIED.,.F.,.F.,(4,3,3,4),(153.687085159892,
153.770397630781,153.854218828331,153.938040025881),.UNSPECIFIED.);
#149=B_SPLINE_CURVE_WITH_KNOTS('',3,(#28022,#28023,#28024,#28025,#28026,
#28027,#28028,#28029,#28030,#28031),.UNSPECIFIED.,.F.,.F.,(4,3,3,4),(153.687545719545,
153.783145344568,153.87809568214,153.938040025688),.UNSPECIFIED.);
#150=B_SPLINE_CURVE_WITH_KNOTS('',3,(#28032,#28033,#28034,#28035,#28036,
#28037,#28038,#28039,#28040,#28041,#28042,#28043,#28044,#28045,#28046,#28047,
#28048,#28049,#28050,#28051,#28052,#28053,#28054,#28055,#28056,#28057,#28058,
#28059,#28060,#28061,#28062,#28063,#28064,#28065,#28066,#28067,#28068,#28069,
#28070,#28071,#28072,#28073,#28074,#28075,#28076,#28077,#28078,#28079,#28080,
#28081,#28082,#28083,#28084,#28085,#28086,#28087,#28088,#28089,#28090,#28091,
#28092,#28093,#28094,#28095,#28096,#28097,#28098,#28099,#28100,#28101,#28102,
#28103,#28104,#28105,#28106,#28107,#28108,#28109,#28110,#28111,#28112,#28113,
#28114,#28115,#28116,#28117,#28118,#28119,#28120,#28121,#28122,#28123,#28124,
#28125,#28126,#28127,#28128,#28129,#28130,#28131,#28132,#28133,#28134,#28135,
#28136,#28137,#28138,#28139,#28140,#28141,#28142,#28143,#28144,#28145,#28146,
#28147,#28148,#28149,#28150,#28151,#28152,#28153,#28154,#28155,#28156,#28157,
#28158,#28159,#28160,#28161,#28162,#28163,#28164,#28165,#28166,#28167,#28168,
#28169,#28170,#28171,#28172,#28173,#28174,#28175,#28176,#28177,#28178,#28179,
#28180,#28181,#28182,#28183,#28184,#28185,#28186,#28187,#28188,#28189,#28190,
#28191,#28192,#28193,#28194,#28195,#28196,#28197,#28198,#28199,#28200,#28201,
#28202,#28203,#28204,#28205,#28206,#28207,#28208,#28209,#28210,#28211,#28212,
#28213,#28214,#28215,#28216,#28217,#28218,#28219,#28220,#28221,#28222,#28223,
#28224,#28225,#28226,#28227,#28228,#28229,#28230,#28231,#28232,#28233,#28234,
#28235,#28236,#28237,#28238,#28239,#28240,#28241,#28242,#28243,#28244,#28245,
#28246,#28247,#28248,#28249,#28250,#28251),.UNSPECIFIED.,.F.,.F.,(4,3,3,
3,3,3,3,3,3,3,3,3,3,3,3,3,3,3,3,3,3,3,3,3,3,3,3,3,3,3,3,3,3,3,3,3,3,3,3,
3,3,3,3,3,3,3,3,3,3,3,3,3,3,3,3,3,3,3,3,3,3,3,3,3,3,3,3,3,3,3,3,3,3,4),
(153.938040025885,154.021840747954,154.105640891805,154.189458006602,154.273309648661,
154.357266132484,154.441280186974,154.525430396561,154.577671052066,154.661409763912,
154.745045275279,154.828597718678,154.912087154529,154.995541105143,155.078977598989,
155.162414708745,155.245870503662,155.329414996392,155.413004079333,155.496727346891,
155.577407062787,155.661145774633,155.744781286001,155.828333729399,155.91182316525,
155.995277115864,156.07871360971,156.162150719466,156.245606514383,156.329151007113,
156.412740090054,156.496463357612,156.577143073507,156.660881785353,156.74451729672,
156.828069740119,156.91155917597,156.995013126584,157.07844962043,157.161886730185,
157.245342525102,157.328887017832,157.412476100773,157.496199368331,157.576879084227,
157.660617796073,157.74425330744,157.827805750839,157.911295186691,157.994749137304,
158.078185631151,158.161622740906,158.245078535824,158.328623028554,158.412212111495,
158.495935379053,158.576615094947,158.660353806793,158.74398931816,158.827541761559,
158.91103119741,158.994485148024,159.07792164187,159.161358751626,159.244814546543,
159.328359039273,159.411948122214,159.495671389771,159.576351105667,159.660425946794,
159.744362130889,159.828218528182,159.91200005122,159.970399332816),
 .UNSPECIFIED.);
#151=B_SPLINE_CURVE_WITH_KNOTS('',3,(#28257,#28258,#28259,#28260,#28261,
#28262,#28263,#28264,#28265,#28266,#28267,#28268,#28269,#28270,#28271,#28272,
#28273,#28274,#28275,#28276,#28277,#28278,#28279,#28280,#28281,#28282,#28283,
#28284,#28285,#28286,#28287,#28288,#28289,#28290,#28291,#28292,#28293,#28294,
#28295,#28296,#28297,#28298,#28299,#28300,#28301,#28302,#28303,#28304,#28305,
#28306,#28307,#28308,#28309,#28310,#28311,#28312,#28313,#28314,#28315,#28316,
#28317,#28318,#28319,#28320,#28321,#28322,#28323,#28324,#28325,#28326,#28327,
#28328,#28329,#28330,#28331,#28332,#28333,#28334,#28335,#28336,#28337,#28338,
#28339,#28340,#28341,#28342,#28343,#28344,#28345,#28346,#28347,#28348,#28349,
#28350,#28351,#28352,#28353,#28354,#28355,#28356,#28357,#28358,#28359,#28360,
#28361,#28362,#28363,#28364,#28365,#28366,#28367,#28368,#28369,#28370,#28371,
#28372,#28373,#28374,#28375,#28376,#28377,#28378,#28379,#28380,#28381,#28382,
#28383,#28384,#28385,#28386,#28387,#28388,#28389,#28390,#28391,#28392,#28393,
#28394,#28395,#28396,#28397,#28398,#28399,#28400,#28401,#28402,#28403,#28404,
#28405,#28406,#28407,#28408,#28409,#28410,#28411,#28412,#28413,#28414,#28415,
#28416,#28417,#28418,#28419,#28420,#28421,#28422,#28423,#28424,#28425,#28426,
#28427,#28428,#28429,#28430,#28431,#28432,#28433,#28434,#28435,#28436,#28437,
#28438,#28439,#28440,#28441,#28442,#28443,#28444,#28445,#28446,#28447,#28448,
#28449,#28450,#28451,#28452,#28453,#28454,#28455,#28456,#28457,#28458,#28459,
#28460,#28461,#28462,#28463,#28464,#28465,#28466,#28467,#28468,#28469,#28470,
#28471,#28472,#28473,#28474,#28475,#28476),.UNSPECIFIED.,.F.,.F.,(4,3,3,
3,3,3,3,3,3,3,3,3,3,3,3,3,3,3,3,3,3,3,3,3,3,3,3,3,3,3,3,3,3,3,3,3,3,3,3,
3,3,3,3,3,3,3,3,3,3,3,3,3,3,3,3,3,3,3,3,3,3,3,3,3,3,3,3,3,3,3,3,3,3,4),
(160.22122533306,160.265796496672,160.349535208518,160.433170719886,160.516723163284,
160.600212599136,160.683666549749,160.767103043596,160.850540153351,160.933995948269,
161.017540440999,161.10112952394,161.184852791498,161.265532507392,161.349271219238,
161.432906730605,161.516459174004,161.599948609855,161.683402560469,161.766839054315,
161.85027616407,161.933731958988,162.017276451718,162.100865534659,162.184588802216,
162.265268518113,162.349007229959,162.432642741327,162.516195184725,162.599684620576,
162.68313857119,162.766575065036,162.850012174792,162.933467969709,163.017012462439,
163.10060154538,163.184324812938,163.265004528833,163.348743240679,163.432378752046,
163.515931195445,163.599420631296,163.68287458191,163.766311075756,163.849748185511,
163.933203980429,164.016748473159,164.1003375561,164.184060823657,164.264740539553,
164.348479251399,164.432114762766,164.515667206165,164.599156642016,164.68261059263,
164.766047086476,164.849484196231,164.932939991149,165.016484483878,165.100073566819,
165.183796834377,165.264476550273,165.348215877039,165.431851859126,165.515404629652,
165.598894249496,165.682347637802,165.765783365477,165.849219505055,165.932674125469,
166.016214587326,166.09979955514,166.183511955595,166.253279225986),
 .UNSPECIFIED.);
#152=B_SPLINE_CURVE_WITH_KNOTS('',3,(#28477,#28478,#28479,#28480,#28481,
#28482,#28483,#28484,#28485,#28486),.UNSPECIFIED.,.F.,.F.,(4,3,3,4),(159.96943076146,
160.052425750303,160.13682554159,160.221225332876),.UNSPECIFIED.);
#153=B_SPLINE_CURVE_WITH_KNOTS('',3,(#28488,#28489,#28490,#28491,#28492,
#28493,#28494,#28495,#28496,#28497),.UNSPECIFIED.,.F.,.F.,(4,3,3,4),(159.970399332816,
160.054113020307,160.137828429699,160.221225333064),.UNSPECIFIED.);
#154=B_SPLINE_CURVE_WITH_KNOTS('',3,(#28498,#28499,#28500,#28501,#28502,
#28503,#28504,#28505,#28506,#28507,#28508,#28509,#28510,#28511,#28512,#28513,
#28514,#28515,#28516,#28517,#28518,#28519,#28520,#28521,#28522,#28523,#28524,
#28525,#28526,#28527,#28528,#28529,#28530,#28531,#28532,#28533,#28534,#28535,
#28536,#28537,#28538,#28539,#28540,#28541,#28542,#28543,#28544,#28545,#28546,
#28547,#28548,#28549,#28550,#28551,#28552,#28553,#28554,#28555,#28556,#28557,
#28558,#28559,#28560,#28561,#28562,#28563,#28564,#28565,#28566,#28567,#28568,
#28569,#28570,#28571,#28572,#28573,#28574,#28575,#28576,#28577,#28578,#28579,
#28580,#28581,#28582,#28583,#28584,#28585,#28586,#28587,#28588,#28589,#28590,
#28591,#28592,#28593,#28594,#28595,#28596,#28597,#28598,#28599,#28600,#28601,
#28602,#28603,#28604,#28605,#28606,#28607,#28608,#28609,#28610,#28611,#28612,
#28613,#28614,#28615,#28616,#28617,#28618,#28619,#28620,#28621,#28622,#28623,
#28624,#28625,#28626,#28627,#28628,#28629,#28630,#28631,#28632,#28633,#28634,
#28635,#28636,#28637,#28638,#28639,#28640,#28641,#28642,#28643,#28644,#28645,
#28646,#28647,#28648,#28649,#28650,#28651,#28652,#28653,#28654,#28655,#28656,
#28657,#28658,#28659,#28660,#28661,#28662,#28663,#28664,#28665,#28666,#28667,
#28668,#28669,#28670,#28671,#28672,#28673,#28674,#28675,#28676,#28677,#28678,
#28679,#28680,#28681,#28682,#28683,#28684,#28685,#28686,#28687,#28688,#28689,
#28690,#28691,#28692,#28693,#28694,#28695,#28696,#28697,#28698,#28699,#28700,
#28701,#28702,#28703,#28704,#28705,#28706,#28707,#28708,#28709,#28710,#28711,
#28712,#28713,#28714,#28715,#28716,#28717),.UNSPECIFIED.,.F.,.F.,(4,3,3,
3,3,3,3,3,3,3,3,3,3,3,3,3,3,3,3,3,3,3,3,3,3,3,3,3,3,3,3,3,3,3,3,3,3,3,3,
3,3,3,3,3,3,3,3,3,3,3,3,3,3,3,3,3,3,3,3,3,3,3,3,3,3,3,3,3,3,3,3,3,3,4),
(160.221225333262,160.316660060154,160.412545812793,160.509018326866,160.576087116387,
160.659825828233,160.7434613396,160.827013782999,160.91050321885,160.993957169463,
161.077393663309,161.160830773065,161.244286567983,161.327831060712,161.411420143653,
161.495143411211,161.575823127107,161.659561838953,161.74319735032,161.826749793719,
161.91023922957,161.993693180184,162.07712967403,162.160566783786,162.244022578703,
162.327567071433,162.411156154374,162.494879421932,162.575559137827,162.659297849673,
162.74293336104,162.826485804439,162.90997524029,162.993429190904,163.07686568475,
163.160302794506,163.243758589423,163.327303082153,163.410892165094,163.494615432652,
163.575295148548,163.659033860394,163.742669371762,163.82622181516,163.909711251011,
163.993165201625,164.076601695471,164.160038805227,164.243494600144,164.327039092874,
164.410628175815,164.494351443373,164.575031159268,164.658769871114,164.742405382481,
164.82595782588,164.909447261731,164.992901212345,165.076337706191,165.159774815947,
165.243230610864,165.326775103594,165.410364186535,165.494087454093,165.574767169988,
165.659493734827,165.742284208432,165.824999485849,165.907658428563,165.993888743597,
166.076503904695,166.159117880116,166.241766148672,166.252579688701),
 .UNSPECIFIED.);
#155=B_SPLINE_CURVE_WITH_KNOTS('',3,(#28723,#28724,#28725,#28726,#28727,
#28728,#28729,#28730,#28731,#28732,#28733,#28734,#28735,#28736,#28737,#28738,
#28739,#28740,#28741,#28742,#28743,#28744,#28745,#28746,#28747,#28748,#28749,
#28750,#28751,#28752,#28753,#28754,#28755,#28756,#28757,#28758,#28759,#28760,
#28761,#28762,#28763,#28764,#28765,#28766,#28767,#28768,#28769,#28770,#28771,
#28772,#28773,#28774,#28775,#28776,#28777,#28778,#28779,#28780,#28781,#28782,
#28783,#28784,#28785,#28786,#28787,#28788,#28789,#28790,#28791,#28792,#28793,
#28794,#28795,#28796,#28797,#28798,#28799,#28800,#28801,#28802,#28803,#28804,
#28805,#28806,#28807,#28808,#28809,#28810,#28811,#28812,#28813,#28814,#28815,
#28816,#28817,#28818,#28819,#28820,#28821,#28822,#28823,#28824,#28825,#28826,
#28827,#28828,#28829,#28830,#28831,#28832,#28833,#28834,#28835,#28836,#28837,
#28838,#28839,#28840,#28841,#28842,#28843,#28844,#28845,#28846,#28847,#28848,
#28849,#28850,#28851,#28852,#28853,#28854,#28855,#28856,#28857,#28858,#28859,
#28860,#28861,#28862,#28863,#28864,#28865,#28866,#28867,#28868,#28869,#28870,
#28871,#28872,#28873,#28874,#28875,#28876,#28877,#28878,#28879,#28880,#28881,
#28882,#28883,#28884,#28885,#28886,#28887,#28888,#28889,#28890,#28891,#28892,
#28893,#28894,#28895,#28896,#28897,#28898,#28899,#28900,#28901,#28902,#28903,
#28904,#28905,#28906,#28907,#28908,#28909,#28910,#28911,#28912,#28913,#28914,
#28915,#28916,#28917,#28918,#28919,#28920,#28921,#28922,#28923,#28924,#28925,
#28926,#28927,#28928,#28929,#28930,#28931,#28932,#28933,#28934,#28935,#28936,
#28937,#28938,#28939,#28940,#28941,#28942,#28943,#28944,#28945),
 .UNSPECIFIED.,.F.,.F.,(4,3,3,3,3,3,3,3,3,3,3,3,3,3,3,3,3,3,3,3,3,3,3,3,
3,3,3,3,3,3,3,3,3,3,3,3,3,3,3,3,3,3,3,3,3,3,3,3,3,3,3,3,3,3,3,3,3,3,3,3,
3,3,3,3,3,3,3,3,3,3,3,3,3,3,4),(166.50441064024,166.5869194705,166.671548108151,
166.753973814019,166.836390160482,166.918816041903,167.005099174355,167.087646260185,
167.170249047393,167.252965034704,167.263948571713,167.347687283559,167.431322794926,
167.514875238325,167.598364674176,167.68181862479,167.765255118636,167.848692228391,
167.932148023309,168.015692516039,168.09928159898,168.183004866537,168.263684582433,
168.347423294279,168.431058805647,168.514611249045,168.598100684896,168.68155463551,
168.764991129356,168.848428239112,168.931884034029,169.015428526759,169.0990176097,
169.182740877258,169.263420593153,169.347159304999,169.430794816366,169.514347259765,
169.597836695616,169.68129064623,169.764727140076,169.848164249832,169.93162004475,
170.015164537479,170.09875362042,170.182476887978,170.263156603874,170.34689531572,
170.430530827087,170.514083270486,170.597572706337,170.681026656951,170.764463150797,
170.847900260553,170.931356055471,171.014900548201,171.098489631142,171.182212898699,
171.262892614594,171.34663132644,171.430266837807,171.513819281205,171.597308717056,
171.68076266767,171.764199161516,171.847636271271,171.931092066188,172.014636558918,
172.098225641859,172.181948909417,172.262628625314,172.349750479316,172.436749265431,
172.523602585952,172.537222833018),.UNSPECIFIED.);
#156=B_SPLINE_CURVE_WITH_KNOTS('',3,(#28946,#28947,#28948,#28949,#28950,
#28951,#28952,#28953,#28954,#28955,#28956,#28957,#28958),.UNSPECIFIED.,
 .F.,.F.,(4,3,3,3,4),(166.253279225986,166.264212560993,166.375998781252,
166.485008013926,166.504410640086),.UNSPECIFIED.);
#157=B_SPLINE_CURVE_WITH_KNOTS('',3,(#28960,#28961,#28962,#28963,#28964,
#28965,#28966,#28967,#28968,#28969),.UNSPECIFIED.,.F.,.F.,(4,3,3,4),(166.252579688701,
166.33531487359,166.419862756856,166.504410640121),.UNSPECIFIED.);
#158=B_SPLINE_CURVE_WITH_KNOTS('',3,(#28970,#28971,#28972,#28973,#28974,
#28975,#28976,#28977,#28978,#28979,#28980,#28981,#28982,#28983,#28984,#28985,
#28986,#28987,#28988,#28989,#28990,#28991,#28992,#28993,#28994,#28995,#28996,
#28997,#28998,#28999,#29000,#29001,#29002,#29003,#29004,#29005,#29006,#29007,
#29008,#29009,#29010,#29011,#29012,#29013,#29014,#29015,#29016,#29017,#29018,
#29019,#29020,#29021,#29022,#29023,#29024,#29025,#29026,#29027,#29028,#29029,
#29030,#29031,#29032,#29033,#29034,#29035,#29036,#29037,#29038,#29039,#29040,
#29041,#29042,#29043,#29044,#29045,#29046,#29047,#29048,#29049,#29050,#29051,
#29052,#29053,#29054,#29055,#29056,#29057,#29058,#29059,#29060,#29061,#29062,
#29063,#29064,#29065,#29066,#29067,#29068,#29069,#29070,#29071,#29072,#29073,
#29074,#29075,#29076,#29077,#29078,#29079,#29080,#29081,#29082,#29083,#29084,
#29085,#29086,#29087,#29088,#29089,#29090,#29091,#29092,#29093,#29094,#29095,
#29096,#29097,#29098,#29099,#29100,#29101,#29102,#29103,#29104,#29105,#29106,
#29107,#29108,#29109,#29110,#29111,#29112,#29113,#29114,#29115,#29116,#29117,
#29118,#29119,#29120,#29121,#29122,#29123,#29124,#29125,#29126,#29127,#29128,
#29129,#29130,#29131,#29132,#29133,#29134,#29135,#29136,#29137,#29138,#29139,
#29140,#29141,#29142,#29143,#29144,#29145,#29146,#29147,#29148,#29149,#29150,
#29151,#29152,#29153,#29154,#29155,#29156,#29157,#29158,#29159,#29160,#29161,
#29162,#29163,#29164,#29165,#29166,#29167,#29168,#29169,#29170,#29171,#29172,
#29173,#29174,#29175,#29176,#29177,#29178,#29179,#29180,#29181,#29182,#29183,
#29184,#29185,#29186,#29187,#29188,#29189),.UNSPECIFIED.,.F.,.F.,(4,3,3,
3,3,3,3,3,3,3,3,3,3,3,3,3,3,3,3,3,3,3,3,3,3,3,3,3,3,3,3,3,3,3,3,3,3,3,3,
3,3,3,3,3,3,3,3,3,3,3,3,3,3,3,3,3,3,3,3,3,3,3,3,3,3,3,3,3,3,3,3,3,3,4),
(166.504410640244,166.574503180708,166.658241892554,166.741877403921,166.82542984732,
166.908919283171,166.992373233784,167.075809727631,167.159246837386,167.242702632304,
167.326247125034,167.409836207974,167.493559475532,167.574239191428,167.657977903274,
167.741613414641,167.82516585804,167.908655293891,167.992109244504,168.075545738351,
168.158982848106,168.242438643024,168.325983135753,168.409572218694,168.493295486252,
168.573975202148,168.657713913994,168.741349425361,168.82490186876,168.908391304611,
168.991845255225,169.075281749071,169.158718858827,169.242174653744,169.325719146474,
169.409308229415,169.493031496973,169.573711212868,169.657449924714,169.741085436082,
169.82463787948,169.908127315331,169.991581265945,170.075017759791,170.158454869547,
170.241910664464,170.325455157194,170.409044240135,170.492767507693,170.573447223589,
170.657185935435,170.740821446803,170.824373890201,170.907863326052,170.991317276666,
171.074753770512,171.158190880268,171.241646675186,171.325191167915,171.408780250856,
171.492503518414,171.573183234309,171.656924025188,171.740561132948,171.824114692136,
171.907604764723,171.991056917326,172.07449093084,172.157924877497,172.241376825514,
172.324908162857,172.408483808463,172.492172042282,172.536326482869),
 .UNSPECIFIED.);
#159=B_SPLINE_CURVE_WITH_KNOTS('',3,(#29195,#29196,#29197,#29198,#29199,
#29200,#29201,#29202,#29203,#29204,#29205,#29206,#29207,#29208,#29209,#29210,
#29211,#29212,#29213,#29214,#29215,#29216,#29217,#29218,#29219,#29220,#29221,
#29222,#29223,#29224,#29225,#29226,#29227,#29228,#29229,#29230,#29231,#29232,
#29233,#29234,#29235,#29236,#29237,#29238,#29239,#29240,#29241,#29242,#29243,
#29244,#29245,#29246,#29247,#29248,#29249,#29250,#29251,#29252,#29253,#29254,
#29255,#29256,#29257,#29258,#29259,#29260,#29261,#29262,#29263,#29264,#29265,
#29266,#29267,#29268,#29269,#29270,#29271,#29272,#29273,#29274,#29275,#29276,
#29277,#29278,#29279,#29280,#29281,#29282,#29283,#29284,#29285,#29286,#29287,
#29288,#29289,#29290,#29291,#29292,#29293,#29294,#29295,#29296,#29297,#29298,
#29299,#29300,#29301,#29302,#29303,#29304,#29305,#29306,#29307,#29308,#29309,
#29310,#29311,#29312,#29313,#29314,#29315,#29316,#29317,#29318,#29319,#29320,
#29321,#29322,#29323,#29324,#29325,#29326,#29327,#29328,#29329,#29330,#29331,
#29332,#29333,#29334,#29335,#29336,#29337,#29338,#29339,#29340,#29341,#29342,
#29343,#29344,#29345,#29346,#29347,#29348,#29349,#29350,#29351,#29352,#29353,
#29354,#29355,#29356,#29357,#29358,#29359,#29360,#29361,#29362,#29363,#29364,
#29365,#29366,#29367,#29368,#29369,#29370,#29371,#29372,#29373,#29374,#29375,
#29376,#29377,#29378,#29379,#29380,#29381,#29382,#29383,#29384,#29385,#29386,
#29387,#29388,#29389,#29390,#29391,#29392,#29393,#29394,#29395,#29396,#29397,
#29398,#29399,#29400,#29401,#29402,#29403,#29404,#29405,#29406,#29407,#29408,
#29409,#29410,#29411,#29412,#29413,#29414),.UNSPECIFIED.,.F.,.F.,(4,3,3,
3,3,3,3,3,3,3,3,3,3,3,3,3,3,3,3,3,3,3,3,3,3,3,3,3,3,3,3,3,3,3,3,3,3,3,3,
3,3,3,3,3,3,3,3,3,3,3,3,3,3,3,3,3,3,3,3,3,3,3,3,3,3,3,3,3,3,3,3,3,3,4),
(172.787595947525,172.875968071268,172.964492839275,173.053261020649,173.142162136332,
173.231271976019,173.262364636034,173.34610334788,173.429738859247,173.513291302646,
173.596780738497,173.680234689111,173.763671182957,173.847108292712,173.93056408763,
174.01410858036,174.097697663301,174.181420930858,174.262100646754,174.3458393586,
174.429474869967,174.513027313366,174.596516749217,174.67997069983,174.763407193677,
174.846844303432,174.93030009835,175.01384459108,175.09743367402,175.181156941578,
175.261836657474,175.34557536932,175.429210880687,175.512763324086,175.596252759937,
175.67970671055,175.763143204397,175.846580314152,175.93003610907,176.013580601799,
176.09716968474,176.180892952298,176.261572668194,176.34531138004,176.428946891407,
176.512499334806,176.595988770657,176.679442721271,176.762879215117,176.846316324873,
176.92977211979,177.01331661252,177.096905695461,177.180628963019,177.261308678914,
177.34504739076,177.428682902128,177.512235345526,177.595724781377,177.679178731991,
177.762615225837,177.846052335593,177.92950813051,178.01305262324,178.096641706181,
178.180364973739,178.261044689635,178.343536465897,178.425932413336,178.50825174412,
178.590512421042,178.672737770061,178.754963250308,178.819154473902),
 .UNSPECIFIED.);
#160=B_SPLINE_CURVE_WITH_KNOTS('',3,(#29415,#29416,#29417,#29418,#29419,
#29420,#29421,#29422,#29423,#29424),.UNSPECIFIED.,.F.,.F.,(4,3,3,4),(172.537222833018,
172.623918808965,172.710492976874,172.787595947419),.UNSPECIFIED.);
#161=B_SPLINE_CURVE_WITH_KNOTS('',3,(#29426,#29427,#29428,#29429,#29430,
#29431,#29432,#29433,#29434,#29435),.UNSPECIFIED.,.F.,.F.,(4,3,3,4),(172.536326482869,
172.572919245029,172.689017473637,172.787595947423),.UNSPECIFIED.);
#162=B_SPLINE_CURVE_WITH_KNOTS('',3,(#29436,#29437,#29438,#29439,#29440,
#29441,#29442,#29443,#29444,#29445,#29446,#29447,#29448,#29449,#29450,#29451,
#29452,#29453,#29454,#29455,#29456,#29457,#29458,#29459,#29460,#29461,#29462,
#29463,#29464,#29465,#29466,#29467,#29468,#29469,#29470,#29471,#29472,#29473,
#29474,#29475,#29476,#29477,#29478,#29479,#29480,#29481,#29482,#29483,#29484,
#29485,#29486,#29487,#29488,#29489,#29490,#29491,#29492,#29493,#29494,#29495,
#29496,#29497,#29498,#29499,#29500,#29501,#29502,#29503,#29504,#29505,#29506,
#29507,#29508,#29509,#29510,#29511,#29512,#29513,#29514,#29515,#29516,#29517,
#29518,#29519,#29520,#29521,#29522,#29523,#29524,#29525,#29526,#29527,#29528,
#29529,#29530,#29531,#29532,#29533,#29534,#29535,#29536,#29537,#29538,#29539,
#29540,#29541,#29542,#29543,#29544,#29545,#29546,#29547,#29548,#29549,#29550,
#29551,#29552,#29553,#29554,#29555,#29556,#29557,#29558,#29559,#29560,#29561,
#29562,#29563,#29564,#29565,#29566,#29567,#29568,#29569,#29570,#29571,#29572,
#29573,#29574,#29575,#29576,#29577,#29578,#29579,#29580,#29581,#29582,#29583,
#29584,#29585,#29586,#29587,#29588,#29589,#29590,#29591,#29592,#29593,#29594,
#29595,#29596,#29597,#29598,#29599,#29600,#29601,#29602,#29603,#29604,#29605,
#29606,#29607,#29608,#29609,#29610,#29611,#29612,#29613,#29614,#29615,#29616,
#29617,#29618,#29619,#29620,#29621,#29622,#29623,#29624,#29625,#29626,#29627,
#29628,#29629,#29630,#29631,#29632,#29633,#29634,#29635,#29636,#29637,#29638,
#29639,#29640,#29641,#29642,#29643,#29644,#29645,#29646,#29647,#29648,#29649,
#29650,#29651,#29652,#29653,#29654,#29655),.UNSPECIFIED.,.F.,.F.,(4,3,3,
3,3,3,3,3,3,3,3,3,3,3,3,3,3,3,3,3,3,3,3,3,3,3,3,3,3,3,3,3,3,3,3,3,3,3,3,
3,3,3,3,3,3,3,3,3,3,3,3,3,3,3,3,3,3,3,3,3,3,3,3,3,3,3,3,3,3,3,3,3,3,4),
(172.787595947533,172.870004970122,172.952349393634,173.034657092611,173.116947717683,
173.199240249463,173.281553667809,173.363953449252,173.446401525226,173.528970574567,
173.572655255749,173.656393967595,173.740029478962,173.823581922361,173.907071358212,
173.990525308826,174.073961802672,174.157398912427,174.240854707345,174.324399200075,
174.407988283016,174.491711550574,174.572391266469,174.656129978315,174.739765489682,
174.823317933081,174.906807368932,174.990261319546,175.073697813392,175.157134923148,
175.240590718065,175.324135210795,175.407724293736,175.491447561294,175.572127277189,
175.655865989035,175.739501500402,175.823053943801,175.906543379652,175.989997330266,
176.073433824112,176.156870933867,176.240326728785,176.323871221514,176.407460304455,
176.491183572013,176.571863287909,176.655601999755,176.739237511123,176.822789954522,
176.906279390372,176.989733340986,177.073169834833,177.156606944588,177.240062739506,
177.323607232235,177.407196315176,177.490919582734,177.571599298629,177.655338010475,
177.738973521842,177.822525965241,177.906015401092,177.989469351706,178.072905845552,
178.156342955308,178.239798750226,178.323343242955,178.406932325897,178.490655593454,
178.57133530935,178.659407964876,178.747284406029,178.820453921422),
 .UNSPECIFIED.);
#163=B_SPLINE_CURVE_WITH_KNOTS('',3,(#29661,#29662,#29663,#29664,#29665,
#29666,#29667,#29668,#29669,#29670,#29671,#29672,#29673,#29674,#29675,#29676,
#29677,#29678,#29679,#29680,#29681,#29682,#29683,#29684,#29685,#29686,#29687,
#29688,#29689,#29690,#29691,#29692,#29693,#29694,#29695,#29696,#29697,#29698,
#29699,#29700,#29701,#29702,#29703,#29704,#29705,#29706,#29707,#29708,#29709,
#29710,#29711,#29712,#29713,#29714,#29715,#29716,#29717,#29718,#29719,#29720,
#29721,#29722,#29723,#29724,#29725,#29726,#29727,#29728,#29729,#29730,#29731,
#29732,#29733,#29734,#29735,#29736,#29737,#29738,#29739,#29740,#29741,#29742,
#29743,#29744,#29745,#29746,#29747,#29748,#29749,#29750,#29751,#29752,#29753,
#29754,#29755,#29756,#29757,#29758,#29759,#29760,#29761,#29762,#29763,#29764,
#29765,#29766,#29767,#29768,#29769,#29770,#29771,#29772,#29773,#29774,#29775,
#29776,#29777,#29778,#29779,#29780,#29781,#29782,#29783,#29784,#29785,#29786,
#29787,#29788,#29789,#29790,#29791,#29792,#29793,#29794,#29795,#29796,#29797,
#29798,#29799,#29800,#29801,#29802,#29803,#29804,#29805,#29806,#29807,#29808,
#29809,#29810,#29811,#29812,#29813,#29814,#29815,#29816,#29817,#29818,#29819,
#29820,#29821,#29822,#29823,#29824,#29825,#29826,#29827,#29828,#29829,#29830,
#29831,#29832,#29833,#29834,#29835,#29836,#29837,#29838,#29839,#29840,#29841,
#29842,#29843,#29844,#29845,#29846,#29847,#29848,#29849,#29850,#29851,#29852,
#29853,#29854,#29855,#29856,#29857,#29858,#29859,#29860,#29861,#29862,#29863,
#29864,#29865,#29866,#29867,#29868,#29869,#29870,#29871,#29872,#29873,#29874,
#29875,#29876,#29877),.UNSPECIFIED.,.F.,.F.,(4,3,3,3,3,3,3,3,3,3,3,3,3,
3,3,3,3,3,3,3,3,3,3,3,3,3,3,3,3,3,3,3,3,3,3,3,3,3,3,3,3,3,3,3,3,3,3,3,3,
3,3,3,3,3,3,3,3,3,3,3,3,3,3,3,3,3,3,3,3,3,3,3,4),(179.070781254599,179.194242909084,
179.260780700355,179.344519412201,179.428154923568,179.511707366967,179.595196802818,
179.678650753431,179.762087247277,179.845524357033,179.928980151951,180.01252464468,
180.096113727621,180.179836995179,180.260516711075,180.344255422921,180.427890934288,
180.511443377687,180.594932813538,180.678386764152,180.761823257998,180.845260367753,
180.928716162671,181.012260655401,181.095849738342,181.179573005899,181.260252721795,
181.343991433641,181.427626945008,181.511179388407,181.594668824258,181.678122774871,
181.761559268718,181.844996378473,181.928452173391,182.01199666612,182.095585749061,
182.179309016619,182.259988732515,182.343727444361,182.427362955728,182.510915399127,
182.594404834978,182.677858785592,182.761295279438,182.844732389193,182.928188184111,
183.011732676841,183.095321759782,183.179045027339,183.259724743235,183.343463455081,
183.427098966448,183.510651409847,183.594140845698,183.677594796312,183.761031290158,
183.844468399913,183.927924194831,184.01146868756,184.095057770501,184.178781038059,
184.259460753955,184.343208799076,184.426851574391,184.51128690772,184.594772813922,
184.678220437969,184.761647868793,184.84681946185,184.93028775386,185.016310997439,
185.102334241018),.UNSPECIFIED.);
#164=B_SPLINE_CURVE_WITH_KNOTS('',3,(#29878,#29879,#29880,#29881,#29882,
#29883,#29884,#29885,#29886,#29887),.UNSPECIFIED.,.F.,.F.,(4,3,3,4),(178.819154473902,
178.901416734859,178.986098994665,179.070781254471),.UNSPECIFIED.);
#165=B_SPLINE_CURVE_WITH_KNOTS('',3,(#29889,#29890,#29891,#29892,#29893,
#29894,#29895,#29896,#29897,#29898),.UNSPECIFIED.,.F.,.F.,(4,3,3,4),(178.820453921422,
178.908072122234,178.995527665515,179.070781254524),.UNSPECIFIED.);
#166=B_SPLINE_CURVE_WITH_KNOTS('',3,(#29899,#29900,#29901,#29902,#29903,
#29904,#29905,#29906,#29907,#29908,#29909,#29910,#29911,#29912,#29913,#29914,
#29915,#29916,#29917,#29918,#29919,#29920,#29921,#29922,#29923,#29924,#29925,
#29926,#29927,#29928,#29929,#29930,#29931,#29932,#29933,#29934,#29935,#29936,
#29937,#29938,#29939,#29940,#29941,#29942,#29943,#29944,#29945,#29946,#29947,
#29948,#29949,#29950,#29951,#29952,#29953,#29954,#29955,#29956,#29957,#29958,
#29959,#29960,#29961,#29962,#29963,#29964,#29965,#29966,#29967,#29968,#29969,
#29970,#29971,#29972,#29973,#29974,#29975,#29976,#29977,#29978,#29979,#29980,
#29981,#29982,#29983,#29984,#29985,#29986,#29987,#29988,#29989,#29990,#29991,
#29992,#29993,#29994,#29995,#29996,#29997,#29998,#29999,#30000,#30001,#30002,
#30003,#30004,#30005,#30006,#30007,#30008,#30009,#30010,#30011,#30012,#30013,
#30014,#30015,#30016,#30017,#30018,#30019,#30020,#30021,#30022,#30023,#30024,
#30025,#30026,#30027,#30028,#30029,#30030,#30031,#30032,#30033,#30034,#30035,
#30036,#30037,#30038,#30039,#30040,#30041,#30042,#30043,#30044,#30045,#30046,
#30047,#30048,#30049,#30050,#30051,#30052,#30053,#30054,#30055,#30056,#30057,
#30058,#30059,#30060,#30061,#30062,#30063,#30064,#30065,#30066,#30067,#30068,
#30069,#30070,#30071,#30072,#30073,#30074,#30075,#30076,#30077,#30078,#30079,
#30080,#30081,#30082,#30083,#30084,#30085,#30086,#30087,#30088,#30089,#30090,
#30091,#30092,#30093,#30094,#30095,#30096,#30097,#30098,#30099,#30100,#30101,
#30102,#30103,#30104,#30105,#30106,#30107,#30108,#30109,#30110,#30111,#30112,
#30113,#30114,#30115,#30116,#30117,#30118),.UNSPECIFIED.,.F.,.F.,(4,3,3,
3,3,3,3,3,3,3,3,3,3,3,3,3,3,3,3,3,3,3,3,3,3,3,3,3,3,3,3,3,3,3,3,3,3,3,3,
3,3,3,3,3,3,3,3,3,3,3,3,3,3,3,3,3,3,3,3,3,3,3,3,3,3,3,3,3,3,3,3,3,3,4),
(179.070781254603,179.158169935777,179.245673124652,179.333382542047,179.421200727411,
179.509220156274,179.57107132007,179.654810031916,179.738445543283,179.821997986682,
179.905487422533,179.988941373147,180.072377866993,180.155814976749,180.239270771666,
180.322815264396,180.406404347337,180.490127614894,180.57080733079,180.654546042636,
180.738181554003,180.821733997402,180.905223433253,180.988677383867,181.072113877713,
181.155550987468,181.239006782386,181.322551275116,181.406140358057,181.489863625614,
181.57054334151,181.654282053356,181.737917564723,181.821470008122,181.904959443973,
181.988413394587,182.071849888433,182.155286998188,182.238742793106,182.322287285835,
182.405876368776,182.489599636334,182.57027935223,182.654018064076,182.737653575443,
182.821206018842,182.904695454694,182.988149405307,183.071585899154,183.155023008909,
183.238478803827,183.322023296557,183.405612379498,183.489335647055,183.57001536295,
183.653754074796,183.737389586164,183.820942029562,183.904431465413,183.987885416027,
184.071321909873,184.154759019628,184.238214814546,184.321759307275,184.405348390217,
184.489071657774,184.56975137367,184.652320999124,184.73479396478,184.817189438157,
184.899523026234,184.981820702053,185.064110743829,185.102443334662),
 .UNSPECIFIED.);
#167=B_SPLINE_CURVE_WITH_KNOTS('',3,(#30124,#30125,#30126,#30127,#30128,
#30129,#30130,#30131,#30132,#30133,#30134,#30135,#30136,#30137,#30138,#30139,
#30140,#30141,#30142,#30143,#30144,#30145,#30146,#30147,#30148,#30149,#30150,
#30151,#30152,#30153,#30154,#30155,#30156,#30157,#30158,#30159,#30160,#30161,
#30162,#30163,#30164,#30165,#30166,#30167,#30168,#30169,#30170,#30171,#30172,
#30173,#30174,#30175,#30176,#30177,#30178,#30179,#30180,#30181,#30182,#30183,
#30184,#30185,#30186,#30187,#30188,#30189,#30190,#30191,#30192,#30193,#30194,
#30195,#30196,#30197,#30198,#30199,#30200,#30201,#30202,#30203,#30204,#30205,
#30206,#30207,#30208,#30209,#30210,#30211,#30212,#30213,#30214,#30215,#30216,
#30217,#30218,#30219,#30220,#30221,#30222,#30223,#30224,#30225,#30226,#30227,
#30228,#30229,#30230,#30231,#30232,#30233,#30234,#30235,#30236,#30237,#30238,
#30239,#30240,#30241,#30242,#30243,#30244,#30245,#30246,#30247,#30248,#30249,
#30250,#30251,#30252,#30253,#30254,#30255,#30256,#30257,#30258,#30259,#30260,
#30261,#30262,#30263,#30264,#30265,#30266,#30267,#30268,#30269,#30270,#30271,
#30272,#30273,#30274,#30275,#30276,#30277,#30278,#30279,#30280,#30281,#30282,
#30283,#30284,#30285,#30286,#30287,#30288,#30289,#30290,#30291,#30292,#30293,
#30294,#30295,#30296,#30297,#30298,#30299,#30300,#30301,#30302,#30303,#30304,
#30305,#30306,#30307,#30308,#30309,#30310,#30311,#30312,#30313,#30314,#30315,
#30316,#30317,#30318,#30319,#30320,#30321,#30322,#30323,#30324,#30325,#30326,
#30327,#30328,#30329,#30330,#30331,#30332,#30333,#30334,#30335,#30336,#30337,
#30338,#30339,#30340,#30341,#30342,#30343),.UNSPECIFIED.,.F.,.F.,(4,3,3,
3,3,3,3,3,3,3,3,3,3,3,3,3,3,3,3,3,3,3,3,3,3,3,3,3,3,3,3,3,3,3,3,3,3,3,3,
3,3,3,3,3,3,3,3,3,3,3,3,3,3,3,3,3,3,3,3,3,3,3,3,3,3,3,3,3,3,3,3,3,3,4),
(185.353966561914,185.436643810729,185.519227495568,185.601738640769,185.684202445595,
185.766641843628,185.849075728445,185.93152298674,186.0140531916,186.096624763862,
186.179327746526,186.258932775396,186.342671487242,186.426306998609,186.509859442008,
186.593348877859,186.676802828473,186.760239322319,186.843676432075,186.927132226992,
187.010676719722,187.094265802663,187.17798907022,187.258668786116,187.342407497962,
187.42604300933,187.509595452728,187.593084888579,187.676538839193,187.759975333039,
187.843412442794,187.926868237712,188.010412730442,188.094001813383,188.177725080941,
188.258404796836,188.342143508682,188.425779020049,188.509331463448,188.592820899299,
188.676274849913,188.759711343759,188.843148453515,188.926604248432,189.010148741162,
189.093737824103,189.177461091661,189.258140807556,189.341879519402,189.425515030769,
189.509067474168,189.592556910019,189.676010860633,189.759447354479,189.842884464234,
189.926340259152,190.009884751882,190.093473834823,190.17719710238,190.257876818276,
190.341615530122,190.425251041489,190.508803484888,190.592292920739,190.675746871353,
190.759183365199,190.842620474954,190.926076269872,191.009620762602,191.093209845543,
191.1769331131,191.257612828996,191.352202270869,191.386723760419),
 .UNSPECIFIED.);
#168=B_SPLINE_CURVE_WITH_KNOTS('',3,(#30344,#30345,#30346,#30347,#30348,
#30349,#30350,#30351,#30352,#30353),.UNSPECIFIED.,.F.,.F.,(4,3,3,4),(185.102334241018,
185.186060117836,185.259196764675,185.353966561779),.UNSPECIFIED.);
#169=B_SPLINE_CURVE_WITH_KNOTS('',3,(#30355,#30356,#30357,#30358,#30359,
#30360,#30361,#30362,#30363,#30364),.UNSPECIFIED.,.F.,.F.,(4,3,3,4),(185.102443334662,
185.184764311148,185.269365436413,185.353966561677),.UNSPECIFIED.);
#170=B_SPLINE_CURVE_WITH_KNOTS('',3,(#30365,#30366,#30367,#30368,#30369,
#30370,#30371,#30372,#30373,#30374,#30375,#30376,#30377,#30378,#30379,#30380,
#30381,#30382,#30383,#30384,#30385,#30386,#30387,#30388,#30389,#30390,#30391,
#30392,#30393,#30394,#30395,#30396,#30397,#30398,#30399,#30400,#30401,#30402,
#30403,#30404,#30405,#30406,#30407,#30408,#30409,#30410,#30411,#30412,#30413,
#30414,#30415,#30416,#30417,#30418,#30419,#30420,#30421,#30422,#30423,#30424,
#30425,#30426,#30427,#30428,#30429,#30430,#30431,#30432,#30433,#30434,#30435,
#30436,#30437,#30438,#30439,#30440,#30441,#30442,#30443,#30444,#30445,#30446,
#30447,#30448,#30449,#30450,#30451,#30452,#30453,#30454,#30455,#30456,#30457,
#30458,#30459,#30460,#30461,#30462,#30463,#30464,#30465,#30466,#30467,#30468,
#30469,#30470,#30471,#30472,#30473,#30474,#30475,#30476,#30477,#30478,#30479,
#30480,#30481,#30482,#30483,#30484,#30485,#30486,#30487,#30488,#30489,#30490,
#30491,#30492,#30493,#30494,#30495,#30496,#30497,#30498,#30499,#30500,#30501,
#30502,#30503,#30504,#30505,#30506,#30507,#30508,#30509,#30510,#30511,#30512,
#30513,#30514,#30515,#30516,#30517,#30518,#30519,#30520,#30521,#30522,#30523,
#30524,#30525,#30526,#30527,#30528,#30529,#30530,#30531,#30532,#30533,#30534,
#30535,#30536,#30537,#30538,#30539,#30540,#30541,#30542,#30543,#30544,#30545,
#30546,#30547,#30548,#30549,#30550,#30551,#30552,#30553,#30554,#30555,#30556,
#30557,#30558,#30559,#30560,#30561,#30562,#30563,#30564,#30565,#30566,#30567,
#30568,#30569,#30570,#30571,#30572,#30573,#30574,#30575,#30576,#30577,#30578,
#30579,#30580,#30581),.UNSPECIFIED.,.F.,.F.,(4,3,3,3,3,3,3,3,3,3,3,3,3,
3,3,3,3,3,3,3,3,3,3,3,3,3,3,3,3,3,3,3,3,3,3,3,3,3,3,3,3,3,3,3,3,3,3,3,3,
3,3,3,3,3,3,3,3,3,3,3,3,3,3,3,3,3,3,3,3,3,3,3,4),(185.353966561782,185.469849979115,
185.56948738439,185.653226096236,185.736861607603,185.820414051002,185.903903486853,
185.987357437466,186.070793931313,186.154231041068,186.237686835986,186.321231328715,
186.404820411656,186.488543679214,186.569223395111,186.652962106957,186.736597618325,
186.820150061723,186.903639497574,186.987093448188,187.070529942034,187.15396705179,
187.237422846707,187.320967339437,187.404556422378,187.488279689936,187.568959405831,
187.652698117677,187.736333629044,187.819886072443,187.903375508294,187.986829458907,
188.070265952754,188.153703062509,188.237158857427,188.320703350156,188.404292433097,
188.488015700655,188.568695416551,188.652434128397,188.736069639764,188.819622083163,
188.903111519014,188.986565469628,189.070001963474,189.153439073229,189.236894868147,
189.320439360877,189.404028443818,189.487751711375,189.568431427271,189.652170139117,
189.735805650484,189.819358093883,189.902847529734,189.986301480348,190.069737974194,
190.153175083949,190.236630878867,190.320175371597,190.403764454538,190.487487722095,
190.568167437991,190.651917107085,190.735561169276,190.819104568393,190.90259089521,
190.986038269379,191.069464780467,191.152915473613,191.236376932508,191.319909424351,
191.385494809803),.UNSPECIFIED.);
#171=B_SPLINE_CURVE_WITH_KNOTS('',3,(#30587,#30588,#30589,#30590,#30591,
#30592,#30593,#30594,#30595,#30596,#30597,#30598,#30599,#30600,#30601,#30602,
#30603,#30604,#30605,#30606,#30607,#30608,#30609,#30610,#30611,#30612,#30613,
#30614,#30615,#30616,#30617,#30618,#30619,#30620,#30621,#30622,#30623,#30624,
#30625,#30626,#30627,#30628,#30629,#30630,#30631,#30632,#30633,#30634,#30635,
#30636,#30637,#30638,#30639,#30640,#30641,#30642,#30643,#30644,#30645,#30646,
#30647,#30648,#30649,#30650,#30651,#30652,#30653,#30654,#30655,#30656,#30657,
#30658,#30659,#30660,#30661,#30662,#30663,#30664,#30665,#30666,#30667,#30668,
#30669,#30670,#30671,#30672,#30673,#30674,#30675,#30676,#30677,#30678,#30679,
#30680,#30681,#30682,#30683,#30684,#30685,#30686,#30687,#30688,#30689,#30690,
#30691,#30692,#30693,#30694,#30695,#30696,#30697,#30698,#30699,#30700,#30701,
#30702,#30703,#30704,#30705,#30706,#30707,#30708,#30709,#30710,#30711,#30712,
#30713,#30714,#30715,#30716,#30717,#30718,#30719,#30720,#30721,#30722,#30723,
#30724,#30725,#30726,#30727,#30728,#30729,#30730,#30731,#30732,#30733,#30734,
#30735,#30736,#30737,#30738,#30739,#30740,#30741,#30742,#30743,#30744,#30745,
#30746,#30747,#30748,#30749,#30750,#30751,#30752,#30753,#30754,#30755,#30756,
#30757,#30758,#30759,#30760,#30761,#30762,#30763,#30764,#30765,#30766,#30767,
#30768,#30769,#30770,#30771,#30772,#30773,#30774,#30775,#30776,#30777,#30778,
#30779,#30780,#30781,#30782,#30783,#30784,#30785,#30786,#30787,#30788,#30789,
#30790,#30791,#30792,#30793,#30794,#30795,#30796,#30797,#30798,#30799,#30800,
#30801,#30802,#30803,#30804,#30805,#30806),.UNSPECIFIED.,.F.,.F.,(4,3,3,
3,3,3,3,3,3,3,3,3,3,3,3,3,3,3,3,3,3,3,3,3,3,3,3,3,3,3,3,3,3,3,3,3,3,3,3,
3,3,3,3,3,3,3,3,3,3,3,3,3,3,3,3,3,3,3,3,3,3,3,3,3,3,3,3,3,3,3,3,3,3,4),
(191.637151868958,191.72130199631,191.805462039817,191.889649048006,191.973880083454,
192.058223549659,192.14263207536,192.227173928829,192.257348839716,192.341087551562,
192.424723062929,192.508275506328,192.591764942179,192.675218892793,192.758655386639,
192.842092496395,192.925548291313,193.009092784042,193.092681866983,193.176405134541,
193.257084850437,193.340823562283,193.42445907365,193.508011517049,193.5915009529,
193.674954903514,193.75839139736,193.841828507116,193.925284302033,194.008828794763,
194.092417877704,194.176141145262,194.256820861157,194.340559573003,194.42419508437,
194.507747527769,194.59123696362,194.674690914234,194.75812740808,194.841564517836,
194.925020312753,195.008564805483,195.092153888424,195.175877155981,195.256556871877,
195.340295583723,195.42393109509,195.507483538489,195.59097297434,195.674426924954,
195.7578634188,195.841300528555,195.924756323473,196.008300816203,196.091889899144,
196.175613166701,196.256292882597,196.340031594443,196.423667105811,196.507219549209,
196.59070898506,196.674162935674,196.75759942952,196.841036539275,196.924492334193,
197.008036826923,197.091625909864,197.175349177421,197.256028893317,197.339775084216,
197.423386845421,197.506921237328,197.590387613573,197.669413533224),
 .UNSPECIFIED.);
#172=B_SPLINE_CURVE_WITH_KNOTS('',3,(#30807,#30808,#30809,#30810,#30811,
#30812,#30813,#30814,#30815,#30816),.UNSPECIFIED.,.F.,.F.,(4,3,3,4),(191.386723760419,
191.480798684565,191.574339257805,191.637151868763),.UNSPECIFIED.);
#173=B_SPLINE_CURVE_WITH_KNOTS('',3,(#30818,#30819,#30820,#30821,#30822,
#30823,#30824,#30825,#30826,#30827,#30828,#30829,#30830),.UNSPECIFIED.,
 .F.,.F.,(4,3,3,3,4),(191.385494809803,191.469130268462,191.552881694883,
191.567903448711,191.637151868962),.UNSPECIFIED.);
#174=B_SPLINE_CURVE_WITH_KNOTS('',3,(#30831,#30832,#30833,#30834,#30835,
#30836,#30837,#30838,#30839,#30840,#30841,#30842,#30843,#30844,#30845,#30846,
#30847,#30848,#30849,#30850,#30851,#30852,#30853,#30854,#30855,#30856,#30857,
#30858,#30859,#30860,#30861,#30862,#30863,#30864,#30865,#30866,#30867,#30868,
#30869,#30870,#30871,#30872,#30873,#30874,#30875,#30876,#30877,#30878,#30879,
#30880,#30881,#30882,#30883,#30884,#30885,#30886,#30887,#30888,#30889,#30890,
#30891,#30892,#30893,#30894,#30895,#30896,#30897,#30898,#30899,#30900,#30901,
#30902,#30903,#30904,#30905,#30906,#30907,#30908,#30909,#30910,#30911,#30912,
#30913,#30914,#30915,#30916,#30917,#30918,#30919,#30920,#30921,#30922,#30923,
#30924,#30925,#30926,#30927,#30928,#30929,#30930,#30931,#30932,#30933,#30934,
#30935,#30936,#30937,#30938,#30939,#30940,#30941,#30942,#30943,#30944,#30945,
#30946,#30947,#30948,#30949,#30950,#30951,#30952,#30953,#30954,#30955,#30956,
#30957,#30958,#30959,#30960,#30961,#30962,#30963,#30964,#30965,#30966,#30967,
#30968,#30969,#30970,#30971,#30972,#30973,#30974,#30975,#30976,#30977,#30978,
#30979,#30980,#30981,#30982,#30983,#30984,#30985,#30986,#30987,#30988,#30989,
#30990,#30991,#30992,#30993,#30994,#30995,#30996,#30997,#30998,#30999,#31000,
#31001,#31002,#31003,#31004,#31005,#31006,#31007,#31008,#31009,#31010,#31011,
#31012,#31013,#31014,#31015,#31016,#31017,#31018,#31019,#31020,#31021,#31022,
#31023,#31024,#31025,#31026,#31027,#31028,#31029,#31030,#31031,#31032,#31033,
#31034,#31035,#31036,#31037,#31038,#31039,#31040,#31041,#31042,#31043,#31044,
#31045,#31046,#31047,#31048,#31049,#31050,#31051,#31052,#31053),
 .UNSPECIFIED.,.F.,.F.,(4,3,3,3,3,3,3,3,3,3,3,3,3,3,3,3,3,3,3,3,3,3,3,3,
3,3,3,3,3,3,3,3,3,3,3,3,3,3,3,3,3,3,3,3,3,3,3,3,3,3,3,3,3,3,3,3,3,3,3,3,
3,3,3,3,3,3,3,3,3,3,3,3,3,3,4),(191.637151869084,191.720040417558,191.802831357082,
191.885545578145,191.970807313306,192.053439367496,192.136062354038,192.218695029689,
192.30135615543,192.384108212342,192.466914941915,192.5498368084,192.567639459431,
192.651378171277,192.735013682644,192.818566126043,192.902055561894,192.985509512508,
193.068946006354,193.15238311611,193.235838911027,193.319383403757,193.402972486698,
193.486695754256,193.567375470152,193.651114181998,193.734749693366,193.818302136764,
193.901791572616,193.985245523229,194.068682017076,194.152119126831,194.235574921749,
194.319119414479,194.40270849742,194.486431764978,194.567111480872,194.650850192718,
194.734485704085,194.818038147484,194.901527583335,194.984981533949,195.068418027795,
195.151855137551,195.235310932468,195.318855425198,195.402444508139,195.486167775696,
195.566847491592,195.650586203438,195.734221714805,195.817774158204,195.901263594055,
195.984717544669,196.068154038515,196.151591148271,196.235046943188,196.318591435918,
196.402180518859,196.485903786417,196.566583502312,196.650322214158,196.733957725526,
196.817510168924,196.900999604776,196.984453555389,197.067890049236,197.151327158991,
197.234782953909,197.318327446638,197.401916529579,197.485639797137,197.566319513032,
197.662998523347,197.669819480909),.UNSPECIFIED.);
#175=B_SPLINE_CURVE_WITH_KNOTS('',3,(#31059,#31060,#31061,#31062,#31063,
#31064,#31065,#31066,#31067,#31068,#31069,#31070,#31071,#31072,#31073,#31074,
#31075,#31076,#31077,#31078,#31079,#31080,#31081,#31082,#31083,#31084,#31085,
#31086,#31087,#31088,#31089,#31090,#31091,#31092,#31093,#31094,#31095,#31096,
#31097,#31098,#31099,#31100,#31101,#31102,#31103,#31104,#31105,#31106,#31107,
#31108,#31109,#31110,#31111,#31112,#31113,#31114,#31115,#31116,#31117,#31118,
#31119,#31120,#31121,#31122,#31123,#31124,#31125,#31126,#31127,#31128,#31129,
#31130,#31131,#31132,#31133,#31134,#31135,#31136,#31137,#31138,#31139,#31140,
#31141,#31142,#31143,#31144,#31145,#31146,#31147,#31148,#31149,#31150,#31151,
#31152,#31153,#31154,#31155,#31156,#31157,#31158,#31159,#31160,#31161,#31162,
#31163,#31164,#31165,#31166,#31167,#31168,#31169,#31170,#31171,#31172,#31173,
#31174,#31175,#31176,#31177,#31178,#31179,#31180,#31181,#31182,#31183,#31184,
#31185,#31186,#31187,#31188,#31189,#31190,#31191,#31192,#31193,#31194,#31195,
#31196,#31197,#31198,#31199,#31200,#31201,#31202,#31203,#31204,#31205,#31206,
#31207,#31208,#31209,#31210,#31211,#31212,#31213,#31214,#31215,#31216,#31217,
#31218,#31219,#31220,#31221,#31222,#31223,#31224,#31225,#31226,#31227,#31228,
#31229,#31230,#31231,#31232,#31233,#31234,#31235,#31236,#31237,#31238,#31239,
#31240,#31241,#31242,#31243,#31244,#31245,#31246,#31247,#31248,#31249,#31250,
#31251,#31252,#31253,#31254,#31255,#31256,#31257,#31258,#31259,#31260,#31261,
#31262,#31263,#31264,#31265,#31266,#31267,#31268,#31269,#31270,#31271,#31272,
#31273,#31274,#31275,#31276,#31277,#31278),.UNSPECIFIED.,.F.,.F.,(4,3,3,
3,3,3,3,3,3,3,3,3,3,3,3,3,3,3,3,3,3,3,3,3,3,3,3,3,3,3,3,3,3,3,3,3,3,3,3,
3,3,3,3,3,3,3,3,3,3,3,3,3,3,3,3,3,3,3,3,3,3,3,3,3,3,3,3,3,3,3,3,3,3,4),
(197.920337176326,198.017388435386,198.115004455218,198.213290205117,198.255764904037,
198.339503615883,198.42313912725,198.506691570649,198.5901810065,198.673634957114,
198.75707145096,198.840508560715,198.923964355633,199.007508848363,199.091097931304,
199.174821198861,199.255500914757,199.339239626603,199.42287513797,199.506427581369,
199.58991701722,199.673370967834,199.75680746168,199.840244571436,199.923700366353,
200.007244859083,200.090833942024,200.174557209581,200.255236925477,200.338975637323,
200.422611148691,200.506163592089,200.58965302794,200.673106978554,200.7565434724,
200.839980582156,200.923436377074,201.006980869803,201.090569952744,201.174293220302,
201.254972936198,201.338711648044,201.422347159412,201.50589960281,201.589389038661,
201.672842989275,201.756279483121,201.839716592877,201.923172387794,202.006716880524,
202.090305963465,202.174029231023,202.254708946918,202.338447658764,202.422083170131,
202.50563561353,202.589125049381,202.672578999995,202.756015493841,202.839452603596,
202.922908398514,203.006452891243,203.090041974184,203.173765241742,203.254444957638,
203.341603870439,203.424575763055,203.507472782828,203.590313653258,203.673117051873,
203.755916189265,203.838713095402,203.921548720593,203.95171626005),
 .UNSPECIFIED.);
#176=B_SPLINE_CURVE_WITH_KNOTS('',3,(#31279,#31280,#31281,#31282,#31283,
#31284,#31285,#31286,#31287,#31288),.UNSPECIFIED.,.F.,.F.,(4,3,3,4),(197.669413533224,
197.75281524834,197.836576212239,197.920337176138),.UNSPECIFIED.);
#177=B_SPLINE_CURVE_WITH_KNOTS('',3,(#31290,#31291,#31292,#31293,#31294,
#31295,#31296,#31297,#31298,#31299),.UNSPECIFIED.,.F.,.F.,(4,3,3,4),(197.669819480909,
197.765936206161,197.861361969395,197.920337175945),.UNSPECIFIED.);
#178=B_SPLINE_CURVE_WITH_KNOTS('',3,(#31300,#31301,#31302,#31303,#31304,
#31305,#31306,#31307,#31308,#31309,#31310,#31311,#31312,#31313,#31314,#31315,
#31316,#31317,#31318,#31319,#31320,#31321,#31322,#31323,#31324,#31325,#31326,
#31327,#31328,#31329,#31330,#31331,#31332,#31333,#31334,#31335,#31336,#31337,
#31338,#31339,#31340,#31341,#31342,#31343,#31344,#31345,#31346,#31347,#31348,
#31349,#31350,#31351,#31352,#31353,#31354,#31355,#31356,#31357,#31358,#31359,
#31360,#31361,#31362,#31363,#31364,#31365,#31366,#31367,#31368,#31369,#31370,
#31371,#31372,#31373,#31374,#31375,#31376,#31377,#31378,#31379,#31380,#31381,
#31382,#31383,#31384,#31385,#31386,#31387,#31388,#31389,#31390,#31391,#31392,
#31393,#31394,#31395,#31396,#31397,#31398,#31399,#31400,#31401,#31402,#31403,
#31404,#31405,#31406,#31407,#31408,#31409,#31410,#31411,#31412,#31413,#31414,
#31415,#31416,#31417,#31418,#31419,#31420,#31421,#31422,#31423,#31424,#31425,
#31426,#31427,#31428,#31429,#31430,#31431,#31432,#31433,#31434,#31435,#31436,
#31437,#31438,#31439,#31440,#31441,#31442,#31443,#31444,#31445,#31446,#31447,
#31448,#31449,#31450,#31451,#31452,#31453,#31454,#31455,#31456,#31457,#31458,
#31459,#31460,#31461,#31462,#31463,#31464,#31465,#31466,#31467,#31468,#31469,
#31470,#31471,#31472,#31473,#31474,#31475,#31476,#31477,#31478,#31479,#31480,
#31481,#31482,#31483,#31484,#31485,#31486,#31487,#31488,#31489,#31490,#31491,
#31492,#31493,#31494,#31495,#31496,#31497,#31498,#31499,#31500,#31501,#31502,
#31503,#31504,#31505,#31506,#31507,#31508,#31509,#31510,#31511,#31512,#31513,
#31514,#31515,#31516,#31517,#31518,#31519),.UNSPECIFIED.,.F.,.F.,(4,3,3,
3,3,3,3,3,3,3,3,3,3,3,3,3,3,3,3,3,3,3,3,3,3,3,3,3,3,3,3,3,3,3,3,3,3,3,3,
3,3,3,3,3,3,3,3,3,3,3,3,3,3,3,3,3,3,3,3,3,3,3,3,3,3,3,3,3,3,3,3,3,3,4),
(197.920337176141,198.004037107572,198.087733392622,198.171443712856,198.255185755071,
198.339030392134,198.422930356544,198.506967457774,198.566055523752,198.649794235598,
198.733429746965,198.816982190364,198.900471626215,198.983925576829,199.067362070675,
199.15079918043,199.234254975348,199.317799468078,199.401388551019,199.485111818576,
199.565791534472,199.649530246318,199.733165757685,199.816718201084,199.900207636935,
199.983661587549,200.067098081395,200.150535191151,200.233990986069,200.317535478798,
200.401124561739,200.484847829297,200.565527545192,200.649266257038,200.732901768406,
200.816454211804,200.899943647655,200.983397598269,201.066834092115,201.150271201871,
201.233726996788,201.317271489518,201.400860572459,201.484583840017,201.565263555913,
201.649002267759,201.732637779126,201.816190222525,201.899679658377,201.98313360899,
202.066570102837,202.150007212592,202.23346300751,202.31700750024,202.40059658318,
202.484319850738,202.564999566633,202.648738278479,202.732373789846,202.815926233245,
202.899415669096,202.98286961971,203.066306113556,203.149743223311,203.233199018228,
203.316743510958,203.400332593899,203.484055861457,203.564735577353,203.648922162625,
203.732968699384,203.816934586732,203.900823571561,203.952726252955),
 .UNSPECIFIED.);
#179=B_SPLINE_CURVE_WITH_KNOTS('',3,(#31525,#31526,#31527,#31528,#31529,
#31530,#31531,#31532,#31533,#31534,#31535,#31536,#31537,#31538,#31539,#31540,
#31541,#31542,#31543,#31544,#31545,#31546,#31547,#31548,#31549,#31550,#31551,
#31552,#31553,#31554,#31555,#31556,#31557,#31558,#31559,#31560,#31561,#31562,
#31563,#31564,#31565,#31566,#31567,#31568,#31569,#31570,#31571,#31572,#31573,
#31574,#31575,#31576,#31577,#31578,#31579,#31580,#31581,#31582,#31583,#31584,
#31585,#31586,#31587,#31588,#31589,#31590,#31591,#31592,#31593,#31594,#31595,
#31596,#31597,#31598,#31599,#31600,#31601,#31602,#31603,#31604,#31605,#31606,
#31607,#31608,#31609,#31610,#31611,#31612,#31613,#31614,#31615,#31616,#31617,
#31618,#31619,#31620,#31621,#31622,#31623,#31624,#31625,#31626,#31627,#31628,
#31629,#31630,#31631,#31632,#31633,#31634,#31635,#31636,#31637,#31638,#31639,
#31640,#31641,#31642,#31643,#31644,#31645,#31646,#31647,#31648,#31649,#31650,
#31651,#31652,#31653,#31654,#31655,#31656,#31657,#31658,#31659,#31660,#31661,
#31662,#31663,#31664,#31665,#31666,#31667,#31668,#31669,#31670,#31671,#31672,
#31673,#31674,#31675,#31676,#31677,#31678,#31679,#31680,#31681,#31682,#31683,
#31684,#31685,#31686,#31687,#31688,#31689,#31690,#31691,#31692,#31693,#31694,
#31695,#31696,#31697,#31698,#31699,#31700,#31701,#31702,#31703,#31704,#31705,
#31706,#31707,#31708,#31709,#31710,#31711,#31712,#31713,#31714,#31715,#31716,
#31717,#31718,#31719,#31720,#31721,#31722,#31723,#31724,#31725,#31726,#31727,
#31728,#31729,#31730,#31731,#31732,#31733,#31734,#31735,#31736,#31737,#31738,
#31739,#31740,#31741,#31742,#31743,#31744),.UNSPECIFIED.,.F.,.F.,(4,3,3,
3,3,3,3,3,3,3,3,3,3,3,3,3,3,3,3,3,3,3,3,3,3,3,3,3,3,3,3,3,3,3,3,3,3,3,3,
3,3,3,3,3,3,3,3,3,3,3,3,3,3,3,3,3,3,3,3,3,3,3,3,3,3,3,3,3,3,3,3,3,3,4),
(204.203522483317,204.254180968358,204.337919680204,204.421555191571,204.50510763497,
204.588597070821,204.672051021435,204.755487515281,204.838924625037,204.922380419955,
205.005924912684,205.089513995625,205.173237263183,205.253916979078,205.337655690924,
205.421291202291,205.50484364569,205.588333081541,205.671787032155,205.755223526001,
205.838660635756,205.922116430674,206.005660923404,206.089250006344,206.172973273902,
206.253652989798,206.337391701644,206.421027213011,206.50457965641,206.588069092261,
206.671523042874,206.75495953672,206.838396646476,206.921852441393,207.005396934123,
207.088986017064,207.172709284621,207.253389000518,207.337127712364,207.420763223732,
207.50431566713,207.587805102981,207.671259053595,207.754695547441,207.838132657197,
207.921588452115,208.005132944845,208.088722027786,208.172445295343,208.253125011238,
208.336863723084,208.420499234451,208.50405167785,208.587541113701,208.670995064315,
208.754431558161,208.837868667916,208.921324462834,209.004868955564,209.088458038505,
209.172181306062,209.252861021959,209.336600695396,209.420236943405,209.503789899441,
209.587279624644,209.670732707411,209.754168015386,209.837603621028,209.921057593095,
210.004595835075,210.088178535835,210.171884999686,210.235541291062),
 .UNSPECIFIED.);
#180=B_SPLINE_CURVE_WITH_KNOTS('',3,(#31745,#31746,#31747,#31748,#31749,
#31750,#31751,#31752,#31753,#31754),.UNSPECIFIED.,.F.,.F.,(4,3,3,4),(203.95171626005,
204.034644119421,204.119083301269,204.203522483116),.UNSPECIFIED.);
#181=B_SPLINE_CURVE_WITH_KNOTS('',3,(#31756,#31757,#31758,#31759,#31760,
#31761,#31762,#31763,#31764,#31765),.UNSPECIFIED.,.F.,.F.,(4,3,3,4),(203.952726252955,
204.036546364182,204.120363659949,204.203522483321),.UNSPECIFIED.);
#182=B_SPLINE_CURVE_WITH_KNOTS('',3,(#31766,#31767,#31768,#31769,#31770,
#31771,#31772,#31773,#31774,#31775,#31776,#31777,#31778,#31779,#31780,#31781,
#31782,#31783,#31784,#31785,#31786,#31787,#31788,#31789,#31790,#31791,#31792,
#31793,#31794,#31795,#31796,#31797,#31798,#31799,#31800,#31801,#31802,#31803,
#31804,#31805,#31806,#31807,#31808,#31809,#31810,#31811,#31812,#31813,#31814,
#31815,#31816,#31817,#31818,#31819,#31820,#31821,#31822,#31823,#31824,#31825,
#31826,#31827,#31828,#31829,#31830,#31831,#31832,#31833,#31834,#31835,#31836,
#31837,#31838,#31839,#31840,#31841,#31842,#31843,#31844,#31845,#31846,#31847,
#31848,#31849,#31850,#31851,#31852,#31853,#31854,#31855,#31856,#31857,#31858,
#31859,#31860,#31861,#31862,#31863,#31864,#31865,#31866,#31867,#31868,#31869,
#31870,#31871,#31872,#31873,#31874,#31875,#31876,#31877,#31878,#31879,#31880,
#31881,#31882,#31883,#31884,#31885,#31886,#31887,#31888,#31889,#31890,#31891,
#31892,#31893,#31894,#31895,#31896,#31897,#31898,#31899,#31900,#31901,#31902,
#31903,#31904,#31905,#31906,#31907,#31908,#31909,#31910,#31911,#31912,#31913,
#31914,#31915,#31916,#31917,#31918,#31919,#31920,#31921,#31922,#31923,#31924,
#31925,#31926,#31927,#31928,#31929,#31930,#31931,#31932,#31933,#31934,#31935,
#31936,#31937,#31938,#31939,#31940,#31941,#31942,#31943,#31944,#31945,#31946,
#31947,#31948,#31949,#31950,#31951,#31952,#31953,#31954,#31955,#31956,#31957,
#31958,#31959,#31960,#31961,#31962,#31963,#31964,#31965,#31966,#31967,#31968,
#31969,#31970,#31971,#31972,#31973,#31974,#31975,#31976,#31977,#31978,#31979,
#31980,#31981,#31982),.UNSPECIFIED.,.F.,.F.,(4,3,3,3,3,3,3,3,3,3,3,3,3,
3,3,3,3,3,3,3,3,3,3,3,3,3,3,3,3,3,3,3,3,3,3,3,3,3,3,3,3,3,3,3,3,3,3,3,3,
3,3,3,3,3,3,3,3,3,3,3,3,3,3,3,3,3,3,3,3,3,3,3,4),(204.20352248352,204.298487723003,
204.393874096607,204.489824564911,204.564471588073,204.648210299919,204.731845811287,
204.815398254685,204.898887690536,204.98234164115,205.065778134996,205.149215244751,
205.232671039669,205.316215532399,205.39980461534,205.483527882897,205.564207598793,
205.647946310639,205.731581822006,205.815134265405,205.898623701256,205.982077651869,
206.065514145716,206.148951255471,206.232407050389,206.315951543118,206.399540626059,
206.483263893617,206.563943609513,206.647682321359,206.731317832726,206.814870276125,
206.898359711976,206.98181366259,207.065250156436,207.148687266191,207.232143061109,
207.315687553839,207.39927663678,207.482999904337,207.563679620233,207.647418332079,
207.731053843447,207.814606286845,207.898095722696,207.98154967331,208.064986167156,
208.148423276912,208.23187907183,208.31542356456,208.399012647501,208.482735915058,
208.563415630954,208.6471543428,208.730789854168,208.814342297566,208.897831733417,
208.981285684031,209.064722177877,209.148159287633,209.23161508255,209.31515957528,
209.398748658221,209.482471925779,209.563151641674,209.647116797923,209.729857499283,
209.812522884371,209.89513185114,209.980067111272,210.062631853633,210.148752372651,
210.234872891669),.UNSPECIFIED.);
#183=B_SPLINE_CURVE_WITH_KNOTS('',3,(#31988,#31989,#31990,#31991,#31992,
#31993,#31994,#31995,#31996,#31997,#31998,#31999,#32000,#32001,#32002,#32003,
#32004,#32005,#32006,#32007,#32008,#32009,#32010,#32011,#32012,#32013,#32014,
#32015,#32016,#32017,#32018,#32019,#32020,#32021,#32022,#32023,#32024,#32025,
#32026,#32027,#32028,#32029,#32030,#32031,#32032,#32033,#32034,#32035,#32036,
#32037,#32038,#32039,#32040,#32041,#32042,#32043,#32044,#32045,#32046,#32047,
#32048,#32049,#32050,#32051,#32052,#32053,#32054,#32055,#32056,#32057,#32058,
#32059,#32060,#32061,#32062,#32063,#32064,#32065,#32066,#32067,#32068,#32069,
#32070,#32071,#32072,#32073,#32074,#32075,#32076,#32077,#32078,#32079,#32080,
#32081,#32082,#32083,#32084,#32085,#32086,#32087,#32088,#32089,#32090,#32091,
#32092,#32093,#32094,#32095,#32096,#32097,#32098,#32099,#32100,#32101,#32102,
#32103,#32104,#32105,#32106,#32107,#32108,#32109,#32110,#32111,#32112,#32113,
#32114,#32115,#32116,#32117,#32118,#32119,#32120,#32121,#32122,#32123,#32124,
#32125,#32126,#32127,#32128,#32129,#32130,#32131,#32132,#32133,#32134,#32135,
#32136,#32137,#32138,#32139,#32140,#32141,#32142,#32143,#32144,#32145,#32146,
#32147,#32148,#32149,#32150,#32151,#32152,#32153,#32154,#32155,#32156,#32157,
#32158,#32159,#32160,#32161,#32162,#32163,#32164,#32165,#32166,#32167,#32168,
#32169,#32170,#32171,#32172,#32173,#32174,#32175,#32176,#32177,#32178,#32179,
#32180,#32181,#32182,#32183,#32184,#32185,#32186,#32187,#32188,#32189,#32190,
#32191,#32192,#32193,#32194,#32195,#32196,#32197,#32198,#32199,#32200,#32201,
#32202,#32203,#32204,#32205,#32206,#32207),.UNSPECIFIED.,.F.,.F.,(4,3,3,
3,3,3,3,3,3,3,3,3,3,3,3,3,3,3,3,3,3,3,3,3,3,3,3,3,3,3,3,3,3,3,3,3,3,3,3,
3,3,3,3,3,3,3,3,3,3,3,3,3,3,3,3,3,3,3,3,3,3,3,3,3,3,3,3,3,3,3,3,3,3,4),
(210.486707790497,210.569187649479,210.654580823719,210.736972714126,210.819353651069,
210.901742553176,210.984158342872,211.066663834264,211.149222895521,211.231897354181,
211.252333043399,211.336071755245,211.419707266612,211.503259710011,211.586749145862,
211.670203096476,211.753639590322,211.837076700078,211.920532494996,212.004076987725,
212.087666070666,212.171389338224,212.252069054119,212.335807765965,212.419443277332,
212.502995720731,212.586485156582,212.669939107196,212.753375601042,212.836812710797,
212.920268505715,213.003812998444,213.087402081385,213.171125348943,213.251805064839,
213.335543776685,213.419179288052,213.502731731451,213.586221167302,213.669675117916,
213.753111611762,213.836548721517,213.920004516435,214.003549009165,214.087138092106,
214.170861359663,214.251541075559,214.335279787405,214.418915298773,214.502467742171,
214.585957178022,214.669411128636,214.752847622482,214.836284732238,214.919740527155,
215.003285019885,215.086874102826,215.170597370384,215.251277086279,215.335015798125,
215.418651309492,215.502203752891,215.585693188742,215.669147139356,215.752583633203,
215.836020742958,215.919476537876,216.003021030605,216.086610113546,216.170333381104,
216.251013096999,216.338350634161,216.428941749218,216.519532864276),
 .UNSPECIFIED.);
#184=B_SPLINE_CURVE_WITH_KNOTS('',3,(#32208,#32209,#32210,#32211,#32212,
#32213,#32214,#32215,#32216,#32217,#32218,#32219,#32220),.UNSPECIFIED.,
 .F.,.F.,(4,3,3,3,4),(210.235541291062,210.252597032679,210.369652411526,
210.479644992553,210.486707790373),.UNSPECIFIED.);
#185=B_SPLINE_CURVE_WITH_KNOTS('',3,(#32222,#32223,#32224,#32225,#32226,
#32227,#32228,#32229,#32230,#32231),.UNSPECIFIED.,.F.,.F.,(4,3,3,4),(210.234872891669,
210.317554458692,210.402131124533,210.486707790373),.UNSPECIFIED.);
#186=B_SPLINE_CURVE_WITH_KNOTS('',3,(#32232,#32233,#32234,#32235,#32236,
#32237,#32238,#32239,#32240,#32241,#32242,#32243,#32244,#32245,#32246,#32247,
#32248,#32249,#32250,#32251,#32252,#32253,#32254,#32255,#32256,#32257,#32258,
#32259,#32260,#32261,#32262,#32263,#32264,#32265,#32266,#32267,#32268,#32269,
#32270,#32271,#32272,#32273,#32274,#32275,#32276,#32277,#32278,#32279,#32280,
#32281,#32282,#32283,#32284,#32285,#32286,#32287,#32288,#32289,#32290,#32291,
#32292,#32293,#32294,#32295,#32296,#32297,#32298,#32299,#32300,#32301,#32302,
#32303,#32304,#32305,#32306,#32307,#32308,#32309,#32310,#32311,#32312,#32313,
#32314,#32315,#32316,#32317,#32318,#32319,#32320,#32321,#32322,#32323,#32324,
#32325,#32326,#32327,#32328,#32329,#32330,#32331,#32332,#32333,#32334,#32335,
#32336,#32337,#32338,#32339,#32340,#32341,#32342,#32343,#32344,#32345,#32346,
#32347,#32348,#32349,#32350,#32351,#32352,#32353,#32354,#32355,#32356,#32357,
#32358,#32359,#32360,#32361,#32362,#32363,#32364,#32365,#32366,#32367,#32368,
#32369,#32370,#32371,#32372,#32373,#32374,#32375,#32376,#32377,#32378,#32379,
#32380,#32381,#32382,#32383,#32384,#32385,#32386,#32387,#32388,#32389,#32390,
#32391,#32392,#32393,#32394,#32395,#32396,#32397,#32398,#32399,#32400,#32401,
#32402,#32403,#32404,#32405,#32406,#32407,#32408,#32409,#32410,#32411,#32412,
#32413,#32414,#32415,#32416,#32417,#32418,#32419,#32420,#32421,#32422,#32423,
#32424,#32425,#32426,#32427,#32428,#32429,#32430,#32431,#32432,#32433,#32434,
#32435,#32436,#32437,#32438,#32439,#32440,#32441,#32442,#32443,#32444,#32445,
#32446,#32447,#32448,#32449,#32450,#32451),.UNSPECIFIED.,.F.,.F.,(4,3,3,
3,3,3,3,3,3,3,3,3,3,3,3,3,3,3,3,3,3,3,3,3,3,3,3,3,3,3,3,3,3,3,3,3,3,3,3,
3,3,3,3,3,3,3,3,3,3,3,3,3,3,3,3,3,3,3,3,3,3,3,3,3,3,3,3,3,3,3,3,3,3,4),
(210.486707790501,210.562887652394,210.64662636424,210.730261875607,210.813814319006,
210.897303754857,210.98075770547,211.064194199317,211.147631309072,211.23108710399,
211.31463159672,211.398220679661,211.481943947218,211.562623663114,211.64636237496,
211.729997886327,211.813550329726,211.897039765577,211.980493716191,212.063930210037,
212.147367319792,212.23082311471,212.31436760744,212.397956690381,212.481679957938,
212.562359673834,212.64609838568,212.729733897047,212.813286340446,212.896775776297,
212.98022972691,213.063666220757,213.147103330512,213.23055912543,213.314103618159,
213.3976927011,213.481415968658,213.562095684554,213.6458343964,213.729469907767,
213.813022351166,213.896511787017,213.979965737631,214.063402231477,214.146839341232,
214.23029513615,214.313839628879,214.39742871182,214.481151979378,214.561831695274,
214.64557040712,214.729205918488,214.812758361886,214.896247797737,214.979701748351,
215.063138242197,215.146575351953,215.230031146871,215.3135756396,215.397164722542,
215.480887990099,215.561567705994,215.645308850233,215.72894623067,215.812499982196,
215.895990167042,215.979442042456,216.062875664721,216.146309106006,216.229760434362,
216.313289666024,216.396863158832,216.480545908606,216.518594148983),
 .UNSPECIFIED.);
#187=B_SPLINE_CURVE_WITH_KNOTS('',3,(#32457,#32458,#32459,#32460,#32461,
#32462,#32463,#32464,#32465,#32466,#32467,#32468,#32469,#32470,#32471,#32472,
#32473,#32474,#32475,#32476,#32477,#32478,#32479,#32480,#32481,#32482,#32483,
#32484,#32485,#32486,#32487,#32488,#32489,#32490,#32491,#32492,#32493,#32494,
#32495,#32496,#32497,#32498,#32499,#32500,#32501,#32502,#32503,#32504,#32505,
#32506,#32507,#32508,#32509,#32510,#32511,#32512,#32513,#32514,#32515,#32516,
#32517,#32518,#32519,#32520,#32521,#32522,#32523,#32524,#32525,#32526,#32527,
#32528,#32529,#32530,#32531,#32532,#32533,#32534,#32535,#32536,#32537,#32538,
#32539,#32540,#32541,#32542,#32543,#32544,#32545,#32546,#32547,#32548,#32549,
#32550,#32551,#32552,#32553,#32554,#32555,#32556,#32557,#32558,#32559,#32560,
#32561,#32562,#32563,#32564,#32565,#32566,#32567,#32568,#32569,#32570,#32571,
#32572,#32573,#32574,#32575,#32576,#32577,#32578,#32579,#32580,#32581,#32582,
#32583,#32584,#32585,#32586,#32587,#32588,#32589,#32590,#32591,#32592,#32593,
#32594,#32595,#32596,#32597,#32598,#32599,#32600,#32601,#32602,#32603,#32604,
#32605,#32606,#32607,#32608,#32609,#32610,#32611,#32612,#32613,#32614,#32615,
#32616,#32617,#32618,#32619,#32620,#32621,#32622,#32623,#32624,#32625,#32626,
#32627,#32628,#32629,#32630,#32631,#32632,#32633,#32634,#32635,#32636,#32637,
#32638,#32639,#32640,#32641,#32642,#32643,#32644,#32645,#32646,#32647,#32648,
#32649,#32650,#32651,#32652,#32653,#32654,#32655,#32656,#32657,#32658,#32659,
#32660,#32661,#32662,#32663,#32664,#32665,#32666,#32667,#32668,#32669,#32670,
#32671,#32672,#32673,#32674,#32675,#32676),.UNSPECIFIED.,.F.,.F.,(4,3,3,
3,3,3,3,3,3,3,3,3,3,3,3,3,3,3,3,3,3,3,3,3,3,3,3,3,3,3,3,3,3,3,3,3,3,3,3,
3,3,3,3,3,3,3,3,3,3,3,3,3,3,3,3,3,3,3,3,3,3,3,3,3,3,3,3,3,3,3,3,3,3,4),
(216.769893097836,216.858019319225,216.946288279332,217.034791092222,217.123420686244,
217.212257061535,217.25074910772,217.334487819566,217.418123330933,217.501675774332,
217.585165210183,217.668619160797,217.752055654643,217.835492764398,217.918948559316,
218.002493052046,218.086082134987,218.169805402545,218.25048511844,218.334223830286,
218.417859341653,218.501411785052,218.584901220903,218.668355171516,218.751791665363,
218.835228775118,218.918684570036,219.002229062765,219.085818145706,219.169541413264,
219.25022112916,219.333959841006,219.417595352373,219.501147795772,219.584637231623,
219.668091182237,219.751527676083,219.834964785838,219.918420580756,220.001965073486,
220.085554156426,220.169277423984,220.24995713988,220.333695851726,220.417331363093,
220.500883806492,220.584373242343,220.667827192957,220.751263686803,220.834700796558,
220.918156591476,221.001701084206,221.085290167147,221.169013434704,221.2496931506,
221.333431862446,221.417067373813,221.500619817212,221.584109253063,221.667563203677,
221.750999697523,221.834436807278,221.917892602196,222.001437094926,222.085026177867,
222.168749445424,222.24942916132,222.331934290144,222.414343415733,222.496675743037,
222.578948659109,222.661186136252,222.743421800978,222.801474927361),
 .UNSPECIFIED.);
#188=B_SPLINE_CURVE_WITH_KNOTS('',3,(#32677,#32678,#32679,#32680,#32681,
#32682,#32683,#32684,#32685,#32686),.UNSPECIFIED.,.F.,.F.,(4,3,3,4),(216.519532864276,
216.606437933948,216.693212126797,216.769893097676),.UNSPECIFIED.);
#189=B_SPLINE_CURVE_WITH_KNOTS('',3,(#32688,#32689,#32690,#32691,#32692,
#32693,#32694,#32695,#32696,#32697),.UNSPECIFIED.,.F.,.F.,(4,3,3,4),(216.518594148983,
216.561303716715,216.679015246047,216.76989309768),.UNSPECIFIED.);
#190=B_SPLINE_CURVE_WITH_KNOTS('',3,(#32698,#32699,#32700,#32701,#32702,
#32703,#32704,#32705,#32706,#32707,#32708,#32709,#32710,#32711,#32712,#32713,
#32714,#32715,#32716,#32717,#32718,#32719,#32720,#32721,#32722,#32723,#32724,
#32725,#32726,#32727,#32728,#32729,#32730,#32731,#32732,#32733,#32734,#32735,
#32736,#32737,#32738,#32739,#32740,#32741,#32742,#32743,#32744,#32745,#32746,
#32747,#32748,#32749,#32750,#32751,#32752,#32753,#32754,#32755,#32756,#32757,
#32758,#32759,#32760,#32761,#32762,#32763,#32764,#32765,#32766,#32767,#32768,
#32769,#32770,#32771,#32772,#32773,#32774,#32775,#32776,#32777,#32778,#32779,
#32780,#32781,#32782,#32783,#32784,#32785,#32786,#32787,#32788,#32789,#32790,
#32791,#32792,#32793,#32794,#32795,#32796,#32797,#32798,#32799,#32800,#32801,
#32802,#32803,#32804,#32805,#32806,#32807,#32808,#32809,#32810,#32811,#32812,
#32813,#32814,#32815,#32816,#32817,#32818,#32819,#32820,#32821,#32822,#32823,
#32824,#32825,#32826,#32827,#32828,#32829,#32830,#32831,#32832,#32833,#32834,
#32835,#32836,#32837,#32838,#32839,#32840,#32841,#32842,#32843,#32844,#32845,
#32846,#32847,#32848,#32849,#32850,#32851,#32852,#32853,#32854,#32855,#32856,
#32857,#32858,#32859,#32860,#32861,#32862,#32863,#32864,#32865,#32866,#32867,
#32868,#32869,#32870,#32871,#32872,#32873,#32874,#32875,#32876,#32877,#32878,
#32879,#32880,#32881,#32882,#32883,#32884,#32885,#32886,#32887,#32888,#32889,
#32890,#32891,#32892,#32893,#32894,#32895,#32896,#32897,#32898,#32899,#32900,
#32901,#32902,#32903,#32904,#32905,#32906,#32907,#32908,#32909,#32910,#32911,
#32912,#32913,#32914,#32915,#32916,#32917),.UNSPECIFIED.,.F.,.F.,(4,3,3,
3,3,3,3,3,3,3,3,3,3,3,3,3,3,3,3,3,3,3,3,3,3,3,3,3,3,3,3,3,3,3,3,3,3,3,3,
3,3,3,3,3,3,3,3,3,3,3,3,3,3,3,3,3,3,3,3,3,3,3,3,3,3,3,3,3,3,3,3,3,3,4),
(216.769893097827,216.852286645666,216.934613755932,217.016901737036,217.099171012457,
217.181440577583,217.263729425788,217.34610372829,217.428524911439,217.511068641655,
217.561039727435,217.644778439281,217.728413950648,217.811966394047,217.895455829898,
217.978909780512,218.062346274358,218.145783384114,218.229239179031,218.312783671761,
218.396372754702,218.48009602226,218.560775738155,218.644514450001,218.728149961368,
218.811702404767,218.895191840618,218.978645791232,219.062082285078,219.145519394833,
219.228975189751,219.31251968248,219.396108765421,219.479832032979,219.560511748875,
219.644250460721,219.727885972088,219.811438415487,219.894927851338,219.978381801952,
220.061818295798,220.145255405553,220.228711200471,220.312255693201,220.395844776142,
220.4795680437,220.560247759595,220.643986471441,220.727621982808,220.811174426207,
220.894663862058,220.978117812672,221.061554306518,221.144991416273,221.228447211191,
221.31199170392,221.395580786861,221.479304054419,221.559983770315,221.643722482161,
221.727357993528,221.810910436927,221.894399872779,221.977853823392,222.061290317239,
222.144727426994,222.228183221912,222.311727714642,222.395316797583,222.479040065141,
222.559719781035,222.648038057741,222.736156359061,222.802758717798),
 .UNSPECIFIED.);
#191=B_SPLINE_CURVE_WITH_KNOTS('',3,(#32923,#32924,#32925,#32926,#32927,
#32928,#32929,#32930,#32931,#32932,#32933,#32934,#32935,#32936,#32937,#32938,
#32939,#32940,#32941,#32942,#32943,#32944,#32945,#32946,#32947,#32948,#32949,
#32950,#32951,#32952,#32953,#32954,#32955,#32956,#32957,#32958,#32959,#32960,
#32961,#32962,#32963,#32964,#32965,#32966,#32967,#32968,#32969,#32970,#32971,
#32972,#32973,#32974,#32975,#32976,#32977,#32978,#32979,#32980,#32981,#32982,
#32983,#32984,#32985,#32986,#32987,#32988,#32989,#32990,#32991,#32992,#32993,
#32994,#32995,#32996,#32997,#32998,#32999,#33000,#33001,#33002,#33003,#33004,
#33005,#33006,#33007,#33008,#33009,#33010,#33011,#33012,#33013,#33014,#33015,
#33016,#33017,#33018,#33019,#33020,#33021,#33022,#33023,#33024,#33025,#33026,
#33027,#33028,#33029,#33030,#33031,#33032,#33033,#33034,#33035,#33036,#33037,
#33038,#33039,#33040,#33041,#33042,#33043,#33044,#33045,#33046,#33047,#33048,
#33049,#33050,#33051,#33052,#33053,#33054,#33055,#33056,#33057,#33058,#33059,
#33060,#33061,#33062,#33063,#33064,#33065,#33066,#33067,#33068,#33069,#33070,
#33071,#33072,#33073,#33074,#33075,#33076,#33077,#33078,#33079,#33080,#33081,
#33082,#33083,#33084,#33085,#33086,#33087,#33088,#33089,#33090,#33091,#33092,
#33093,#33094,#33095,#33096,#33097,#33098,#33099,#33100,#33101,#33102,#33103,
#33104,#33105,#33106,#33107,#33108,#33109,#33110,#33111,#33112,#33113,#33114,
#33115,#33116,#33117,#33118,#33119,#33120,#33121,#33122,#33123,#33124,#33125,
#33126,#33127,#33128,#33129,#33130,#33131,#33132,#33133,#33134,#33135,#33136,
#33137,#33138,#33139),.UNSPECIFIED.,.F.,.F.,(4,3,3,3,3,3,3,3,3,3,3,3,3,
3,3,3,3,3,3,3,3,3,3,3,3,3,3,3,3,3,3,3,3,3,3,3,3,3,3,3,3,3,3,3,3,3,3,3,3,
3,3,3,3,3,3,3,3,3,3,3,3,3,3,3,3,3,3,3,3,3,3,3,4),(223.053078404856,223.174503651388,
223.24916517204,223.332903883886,223.416539395254,223.500091838652,223.583581274503,
223.667035225117,223.750471718963,223.833908828718,223.917364623636,224.000909116366,
224.084498199307,224.168221466864,224.248901182761,224.332639894607,224.416275405974,
224.499827849373,224.583317285224,224.666771235838,224.750207729684,224.83364483944,
224.917100634357,225.000645127087,225.084234210028,225.167957477586,225.248637193481,
225.332375905327,225.416011416694,225.499563860093,225.583053295944,225.666507246557,
225.749943740404,225.833380850159,225.916836645077,226.000381137806,226.083970220747,
226.167693488305,226.248373204201,226.332111916047,226.415747427414,226.499299870813,
226.582789306664,226.666243257278,226.749679751124,226.833116860879,226.916572655797,
227.000117148527,227.083706231468,227.167429499025,227.248109214921,227.331847926767,
227.415483438134,227.499035881533,227.582525317384,227.665979267998,227.749415761844,
227.832852871599,227.916308666517,227.999853159247,228.083442242188,228.167165509745,
228.247845225641,228.331593655558,228.41523673525,228.498910144718,228.582396452253,
228.665844198643,228.749271473125,228.833109607593,228.916575884921,229.000599947959,
229.084624010996),.UNSPECIFIED.);
#192=B_SPLINE_CURVE_WITH_KNOTS('',3,(#33140,#33141,#33142,#33143,#33144,
#33145,#33146,#33147,#33148,#33149),.UNSPECIFIED.,.F.,.F.,(4,3,3,4),(222.801474927361,
222.883746023741,222.968412214243,223.053078404745),.UNSPECIFIED.);
#193=B_SPLINE_CURVE_WITH_KNOTS('',3,(#33151,#33152,#33153,#33154,#33155,
#33156,#33157,#33158,#33159,#33160),.UNSPECIFIED.,.F.,.F.,(4,3,3,4),(222.802758717798,
222.890615341441,222.978298362488,223.053078404664),.UNSPECIFIED.);
#194=B_SPLINE_CURVE_WITH_KNOTS('',3,(#33161,#33162,#33163,#33164,#33165,
#33166,#33167,#33168,#33169,#33170,#33171,#33172,#33173,#33174,#33175,#33176,
#33177,#33178,#33179,#33180,#33181,#33182,#33183,#33184,#33185,#33186,#33187,
#33188,#33189,#33190,#33191,#33192,#33193,#33194,#33195,#33196,#33197,#33198,
#33199,#33200,#33201,#33202,#33203,#33204,#33205,#33206,#33207,#33208,#33209,
#33210,#33211,#33212,#33213,#33214,#33215,#33216,#33217,#33218,#33219,#33220,
#33221,#33222,#33223,#33224,#33225,#33226,#33227,#33228,#33229,#33230,#33231,
#33232,#33233,#33234,#33235,#33236,#33237,#33238,#33239,#33240,#33241,#33242,
#33243,#33244,#33245,#33246,#33247,#33248,#33249,#33250,#33251,#33252,#33253,
#33254,#33255,#33256,#33257,#33258,#33259,#33260,#33261,#33262,#33263,#33264,
#33265,#33266,#33267,#33268,#33269,#33270,#33271,#33272,#33273,#33274,#33275,
#33276,#33277,#33278,#33279,#33280,#33281,#33282,#33283,#33284,#33285,#33286,
#33287,#33288,#33289,#33290,#33291,#33292,#33293,#33294,#33295,#33296,#33297,
#33298,#33299,#33300,#33301,#33302,#33303,#33304,#33305,#33306,#33307,#33308,
#33309,#33310,#33311,#33312,#33313,#33314,#33315,#33316,#33317,#33318,#33319,
#33320,#33321,#33322,#33323,#33324,#33325,#33326,#33327,#33328,#33329,#33330,
#33331,#33332,#33333,#33334,#33335,#33336,#33337,#33338,#33339,#33340,#33341,
#33342,#33343,#33344,#33345,#33346,#33347,#33348,#33349,#33350,#33351,#33352,
#33353,#33354,#33355,#33356,#33357,#33358,#33359,#33360,#33361,#33362,#33363,
#33364,#33365,#33366,#33367,#33368,#33369,#33370,#33371,#33372,#33373,#33374,
#33375,#33376,#33377,#33378,#33379,#33380),.UNSPECIFIED.,.F.,.F.,(4,3,3,
3,3,3,3,3,3,3,3,3,3,3,3,3,3,3,3,3,3,3,3,3,3,3,3,3,3,3,3,3,3,3,3,3,3,3,3,
3,3,3,3,3,3,3,3,3,3,3,3,3,3,3,3,3,3,3,3,3,3,3,3,3,3,3,3,3,3,3,3,3,3,4),
(223.05307840486,223.140250227663,223.227528653432,223.315005472342,223.402585880388,
223.490366020583,223.559455791755,223.643194503601,223.726830014968,223.810382458367,
223.893871894218,223.977325844832,224.060762338678,224.144199448433,224.227655243351,
224.31119973608,224.394788819021,224.478512086579,224.559191802476,224.642930514322,
224.726566025689,224.810118469088,224.893607904939,224.977061855553,225.060498349399,
225.143935459155,225.227391254073,225.310935746803,225.394524829744,225.478248097301,
225.558927813196,225.642666525042,225.726302036409,225.809854479808,225.893343915659,
225.976797866273,226.060234360119,226.143671469874,226.227127264792,226.310671757522,
226.394260840463,226.47798410802,226.558663823916,226.642402535762,226.726038047129,
226.809590490528,226.893079926379,226.976533876993,227.059970370839,227.143407480594,
227.226863275512,227.310407768241,227.393996851182,227.47772011874,227.558399834636,
227.642138546482,227.725774057849,227.809326501248,227.892815937099,227.976269887713,
228.059706381559,228.143143491315,228.226599286233,228.310143778962,228.393732861904,
228.477456129461,228.558135845356,228.640732576949,228.72323240933,228.805654493565,
228.888013899624,228.970337205032,229.052651179031,229.084767271361),
 .UNSPECIFIED.);
#195=B_SPLINE_CURVE_WITH_KNOTS('',3,(#33386,#33387,#33388,#33389,#33390,
#33391,#33392,#33393,#33394,#33395,#33396,#33397,#33398,#33399,#33400,#33401,
#33402,#33403,#33404,#33405,#33406,#33407,#33408,#33409,#33410,#33411,#33412,
#33413,#33414,#33415,#33416,#33417,#33418,#33419,#33420,#33421,#33422,#33423,
#33424,#33425,#33426,#33427,#33428,#33429,#33430,#33431,#33432,#33433,#33434,
#33435,#33436,#33437,#33438,#33439,#33440,#33441,#33442,#33443,#33444,#33445,
#33446,#33447,#33448,#33449,#33450,#33451,#33452,#33453,#33454,#33455,#33456,
#33457,#33458,#33459,#33460,#33461,#33462,#33463,#33464,#33465,#33466,#33467,
#33468,#33469,#33470,#33471,#33472,#33473,#33474,#33475,#33476,#33477,#33478,
#33479,#33480,#33481,#33482,#33483,#33484,#33485,#33486,#33487,#33488,#33489,
#33490,#33491,#33492,#33493,#33494,#33495,#33496,#33497,#33498,#33499,#33500,
#33501,#33502,#33503,#33504,#33505,#33506,#33507,#33508,#33509,#33510,#33511,
#33512,#33513,#33514,#33515,#33516,#33517,#33518,#33519,#33520,#33521,#33522,
#33523,#33524,#33525,#33526,#33527,#33528,#33529,#33530,#33531,#33532,#33533,
#33534,#33535,#33536,#33537,#33538,#33539,#33540,#33541,#33542,#33543,#33544,
#33545,#33546,#33547,#33548,#33549,#33550,#33551,#33552,#33553,#33554,#33555,
#33556,#33557,#33558,#33559,#33560,#33561,#33562,#33563,#33564,#33565,#33566,
#33567,#33568,#33569,#33570,#33571,#33572,#33573,#33574,#33575,#33576,#33577,
#33578,#33579,#33580,#33581,#33582,#33583,#33584,#33585,#33586,#33587,#33588,
#33589,#33590,#33591,#33592,#33593,#33594,#33595,#33596,#33597,#33598,#33599,
#33600,#33601,#33602,#33603,#33604,#33605),.UNSPECIFIED.,.F.,.F.,(4,3,3,
3,3,3,3,3,3,3,3,3,3,3,3,3,3,3,3,3,3,3,3,3,3,3,3,3,3,3,3,3,3,3,3,3,3,3,3,
3,3,3,3,3,3,3,3,3,3,3,3,3,3,3,3,3,3,3,3,3,3,3,3,3,3,3,3,3,3,3,3,3,3,4),
(229.33626371217,229.418986435348,229.501614551539,229.584169058513,229.667062582084,
229.749542783262,229.83201651903,229.914502649429,229.997706298842,230.080315805856,
230.163816526468,230.247317247081,230.331055958927,230.414691470294,230.498243913693,
230.581733349544,230.665187300158,230.748623794004,230.83206090376,230.915516698677,
230.999061191407,231.082650274348,231.166373541906,231.247053257801,231.330791969647,
231.414427481015,231.497979924413,231.581469360264,231.664923310878,231.748359804724,
231.83179691448,231.915252709397,231.998797202127,232.082386285068,232.166109552626,
232.246789268522,232.330527980368,232.414163491736,232.497715935134,232.581205370985,
232.664659321599,232.748095815445,232.831532925201,232.914988720119,232.998533212848,
233.082122295789,233.165845563347,233.246525279242,233.330263991088,233.413899502455,
233.497451945854,233.580941381706,233.664395332319,233.747831826166,233.831268935921,
233.914724730839,233.998269223568,234.081858306509,234.165581574067,234.246261289962,
234.330000001808,234.413635513175,234.497187956574,234.580677392425,234.664131343039,
234.747567836885,234.83100494664,234.914460741557,234.998005234287,235.081594317228,
235.165317584785,235.245997300682,235.341055752039,235.369001591755),
 .UNSPECIFIED.);
#196=B_SPLINE_CURVE_WITH_KNOTS('',3,(#33606,#33607,#33608,#33609,#33610,
#33611,#33612,#33613,#33614,#33615),.UNSPECIFIED.,.F.,.F.,(4,3,3,4),(229.084624010996,
229.168347766236,229.247581236361,229.336263712035),.UNSPECIFIED.);
#197=B_SPLINE_CURVE_WITH_KNOTS('',3,(#33617,#33618,#33619,#33620,#33621,
#33622,#33623,#33624,#33625,#33626),.UNSPECIFIED.,.F.,.F.,(4,3,3,4),(229.084767271361,
229.167110719834,229.251687215869,229.336263711905),.UNSPECIFIED.);
#198=B_SPLINE_CURVE_WITH_KNOTS('',3,(#33627,#33628,#33629,#33630,#33631,
#33632,#33633,#33634,#33635,#33636,#33637,#33638,#33639,#33640,#33641,#33642,
#33643,#33644,#33645,#33646,#33647,#33648,#33649,#33650,#33651,#33652,#33653,
#33654,#33655,#33656,#33657,#33658,#33659,#33660,#33661,#33662,#33663,#33664,
#33665,#33666,#33667,#33668,#33669,#33670,#33671,#33672,#33673,#33674,#33675,
#33676,#33677,#33678,#33679,#33680,#33681,#33682,#33683,#33684,#33685,#33686,
#33687,#33688,#33689,#33690,#33691,#33692,#33693,#33694,#33695,#33696,#33697,
#33698,#33699,#33700,#33701,#33702,#33703,#33704,#33705,#33706,#33707,#33708,
#33709,#33710,#33711,#33712,#33713,#33714,#33715,#33716,#33717,#33718,#33719,
#33720,#33721,#33722,#33723,#33724,#33725,#33726,#33727,#33728,#33729,#33730,
#33731,#33732,#33733,#33734,#33735,#33736,#33737,#33738,#33739,#33740,#33741,
#33742,#33743,#33744,#33745,#33746,#33747,#33748,#33749,#33750,#33751,#33752,
#33753,#33754,#33755,#33756,#33757,#33758,#33759,#33760,#33761,#33762,#33763,
#33764,#33765,#33766,#33767,#33768,#33769,#33770,#33771,#33772,#33773,#33774,
#33775,#33776,#33777,#33778,#33779,#33780,#33781,#33782,#33783,#33784,#33785,
#33786,#33787,#33788,#33789,#33790,#33791,#33792,#33793,#33794,#33795,#33796,
#33797,#33798,#33799,#33800,#33801,#33802,#33803,#33804,#33805,#33806,#33807,
#33808,#33809,#33810,#33811,#33812,#33813,#33814,#33815,#33816,#33817,#33818,
#33819,#33820,#33821,#33822,#33823,#33824,#33825,#33826,#33827,#33828,#33829,
#33830,#33831,#33832,#33833,#33834,#33835,#33836,#33837,#33838,#33839,#33840,
#33841,#33842,#33843),.UNSPECIFIED.,.F.,.F.,(4,3,3,3,3,3,3,3,3,3,3,3,3,
3,3,3,3,3,3,3,3,3,3,3,3,3,3,3,3,3,3,3,3,3,3,3,3,3,3,3,3,3,3,3,3,3,3,3,3,
3,3,3,3,3,3,3,3,3,3,3,3,3,3,3,3,3,3,3,3,3,3,3,4),(229.336263712039,229.450657371009,
229.557871856076,229.641610567922,229.725246079289,229.808798522688,229.892287958539,
229.975741909153,230.059178402999,230.142615512755,230.226071307672,230.309615800402,
230.393204883343,230.476928150901,230.557607866796,230.641346578642,230.72498209001,
230.808534533408,230.892023969259,230.975477919873,231.058914413719,231.142351523475,
231.225807318393,231.309351811122,231.392940894063,231.476664161621,231.557343877517,
231.641082589363,231.72471810073,231.808270544129,231.89175997998,231.975213930594,
232.05865042444,232.142087534196,232.225543329113,232.309087821843,232.392676904784,
232.476400172341,232.557079888237,232.640818600083,232.72445411145,232.808006554849,
232.8914959907,232.974949941314,233.05838643516,233.141823544915,233.225279339833,
233.308823832563,233.392412915504,233.476136183061,233.556815898957,233.640554610803,
233.72419012217,233.807742565569,233.89123200142,233.974685952034,234.05812244588,
234.141559555635,234.225015350553,234.308559843283,234.392148926224,234.475872193781,
234.556551909677,234.640301970269,234.723946343581,234.807489853318,234.890976176804,
234.97442343389,235.057849714245,235.141299036663,235.224759079097,235.308287375594,
235.367788403087),.UNSPECIFIED.);
#199=B_SPLINE_CURVE_WITH_KNOTS('',3,(#33849,#33850,#33851,#33852,#33853,
#33854,#33855,#33856,#33857,#33858,#33859,#33860,#33861,#33862,#33863,#33864,
#33865,#33866,#33867,#33868,#33869,#33870,#33871,#33872,#33873,#33874,#33875,
#33876,#33877,#33878,#33879,#33880,#33881,#33882,#33883,#33884,#33885,#33886,
#33887,#33888,#33889,#33890,#33891,#33892,#33893,#33894,#33895,#33896,#33897,
#33898,#33899,#33900,#33901,#33902,#33903,#33904,#33905,#33906,#33907,#33908,
#33909,#33910,#33911,#33912,#33913,#33914,#33915,#33916,#33917,#33918,#33919,
#33920,#33921,#33922,#33923,#33924,#33925,#33926,#33927,#33928,#33929,#33930,
#33931,#33932,#33933,#33934,#33935,#33936,#33937,#33938,#33939,#33940,#33941,
#33942,#33943,#33944,#33945,#33946,#33947,#33948,#33949,#33950,#33951,#33952,
#33953,#33954,#33955,#33956,#33957,#33958,#33959,#33960,#33961,#33962,#33963,
#33964,#33965,#33966,#33967,#33968,#33969,#33970,#33971,#33972,#33973,#33974,
#33975,#33976,#33977,#33978,#33979,#33980,#33981,#33982,#33983,#33984,#33985,
#33986,#33987,#33988,#33989,#33990,#33991,#33992,#33993,#33994,#33995,#33996,
#33997,#33998,#33999,#34000,#34001,#34002,#34003,#34004,#34005,#34006,#34007,
#34008,#34009,#34010,#34011,#34012,#34013,#34014,#34015,#34016,#34017,#34018,
#34019,#34020,#34021,#34022,#34023,#34024,#34025,#34026,#34027,#34028,#34029,
#34030,#34031,#34032,#34033,#34034,#34035,#34036,#34037,#34038,#34039,#34040,
#34041,#34042,#34043,#34044,#34045,#34046,#34047,#34048,#34049,#34050,#34051,
#34052,#34053,#34054,#34055,#34056,#34057,#34058,#34059,#34060,#34061,#34062,
#34063,#34064,#34065,#34066,#34067,#34068),.UNSPECIFIED.,.F.,.F.,(4,3,3,
3,3,3,3,3,3,3,3,3,3,3,3,3,3,3,3,3,3,3,3,3,3,3,3,3,3,3,3,3,3,3,3,3,3,3,3,
3,3,3,3,3,3,3,3,3,3,3,3,3,3,3,3,3,3,3,3,3,3,3,3,3,3,3,3,3,3,3,3,3,3,4),
(235.619449019215,235.703485100474,235.787527689251,235.871594004824,235.955701278211,
236.039918534502,236.124198449062,236.208612528274,236.245733311402,236.329472023248,
236.413107534615,236.496659978014,236.580149413865,236.663603364479,236.747039858325,
236.83047696808,236.913932762998,236.997477255727,237.081066338668,237.164789606226,
237.245469322122,237.329208033968,237.412843545335,237.496395988734,237.579885424585,
237.663339375198,237.746775869045,237.8302129788,237.913668773717,237.997213266447,
238.080802349388,238.164525616946,238.245205332842,238.328944044688,238.412579556055,
238.496131999454,238.579621435305,238.663075385919,238.746511879765,238.829948989521,
238.913404784439,238.996949277169,239.080538360109,239.164261627667,239.244941343562,
239.328680055408,239.412315566775,239.495868010174,239.579357446025,239.662811396639,
239.746247890485,239.829685000241,239.913140795158,239.996685287888,240.080274370829,
240.163997638387,240.244677354283,240.328416066129,240.412051577497,240.495604020896,
240.579093456746,240.66254740736,240.745983901207,240.829421010962,240.91287680588,
240.99642129861,241.08001038155,241.163733649108,241.244413365003,241.328257974956,
241.411966864006,241.495597678354,241.579158265343,241.651741637788),
 .UNSPECIFIED.);
#200=B_SPLINE_CURVE_WITH_KNOTS('',3,(#34069,#34070,#34071,#34072,#34073,
#34074,#34075,#34076,#34077,#34078),.UNSPECIFIED.,.F.,.F.,(4,3,3,4),(235.369001591755,
235.463534631651,235.557500007405,235.619449019017),.UNSPECIFIED.);
#201=B_SPLINE_CURVE_WITH_KNOTS('',3,(#34080,#34081,#34082,#34083,#34084,
#34085,#34086,#34087,#34088,#34089,#34090,#34091,#34092),.UNSPECIFIED.,
 .F.,.F.,(4,3,3,3,4),(235.367788403087,235.451419133571,235.535167426197,
235.556287920397,235.619449019219),.UNSPECIFIED.);
#202=B_SPLINE_CURVE_WITH_KNOTS('',3,(#34093,#34094,#34095,#34096,#34097,
#34098,#34099,#34100,#34101,#34102,#34103,#34104,#34105,#34106,#34107,#34108,
#34109,#34110,#34111,#34112,#34113,#34114,#34115,#34116,#34117,#34118,#34119,
#34120,#34121,#34122,#34123,#34124,#34125,#34126,#34127,#34128,#34129,#34130,
#34131,#34132,#34133,#34134,#34135,#34136,#34137,#34138,#34139,#34140,#34141,
#34142,#34143,#34144,#34145,#34146,#34147,#34148,#34149,#34150,#34151,#34152,
#34153,#34154,#34155,#34156,#34157,#34158,#34159,#34160,#34161,#34162,#34163,
#34164,#34165,#34166,#34167,#34168,#34169,#34170,#34171,#34172,#34173,#34174,
#34175,#34176,#34177,#34178,#34179,#34180,#34181,#34182,#34183,#34184,#34185,
#34186,#34187,#34188,#34189,#34190,#34191,#34192,#34193,#34194,#34195,#34196,
#34197,#34198,#34199,#34200,#34201,#34202,#34203,#34204,#34205,#34206,#34207,
#34208,#34209,#34210,#34211,#34212,#34213,#34214,#34215,#34216,#34217,#34218,
#34219,#34220,#34221,#34222,#34223,#34224,#34225,#34226,#34227,#34228,#34229,
#34230,#34231,#34232,#34233,#34234,#34235,#34236,#34237,#34238,#34239,#34240,
#34241,#34242,#34243,#34244,#34245,#34246,#34247,#34248,#34249,#34250,#34251,
#34252,#34253,#34254,#34255,#34256,#34257,#34258,#34259,#34260,#34261,#34262,
#34263,#34264,#34265,#34266,#34267,#34268,#34269,#34270,#34271,#34272,#34273,
#34274,#34275,#34276,#34277,#34278,#34279,#34280,#34281,#34282,#34283,#34284,
#34285,#34286,#34287,#34288,#34289,#34290,#34291,#34292,#34293,#34294,#34295,
#34296,#34297,#34298,#34299,#34300,#34301,#34302,#34303,#34304,#34305,#34306,
#34307,#34308,#34309,#34310,#34311,#34312),.UNSPECIFIED.,.F.,.F.,(4,3,3,
3,3,3,3,3,3,3,3,3,3,3,3,3,3,3,3,3,3,3,3,3,3,3,3,3,3,3,3,3,3,3,3,3,3,3,3,
3,3,3,3,3,3,3,3,3,3,3,3,3,3,3,3,3,3,3,3,3,3,3,3,3,3,3,3,3,3,3,3,3,3,4),
(235.619449019335,235.702396000431,235.785244541703,235.868015492367,235.95401654721,
236.036703039314,236.119379716895,236.202065298067,236.284778504414,236.367582433388,
236.450440219168,236.533414519597,236.556023931117,236.639762642963,236.72339815433,
236.806950597729,236.89044003358,236.973893984194,237.05733047804,237.140767587795,
237.224223382713,237.307767875443,237.391356958383,237.475080225941,237.555759941837,
237.639498653683,237.723134165051,237.806686608449,237.8901760443,237.973629994914,
238.05706648876,238.140503598516,238.223959393434,238.307503886163,238.391092969104,
238.474816236662,238.555495952557,238.639234664403,238.72287017577,238.806422619169,
238.88991205502,238.973366005633,239.05680249948,239.140239609235,239.223695404152,
239.307239896882,239.390828979823,239.474552247381,239.555231963278,239.638970675124,
239.722606186492,239.80615862989,239.889648065741,239.973102016355,240.056538510201,
240.139975619957,240.223431414875,240.306975907605,240.390564990546,240.474288258103,
240.554967973998,240.638706685844,240.722342197211,240.805894640609,240.88938407646,
240.972838027074,241.05627452092,241.139711630676,241.223167425593,241.306711918323,
241.390301001264,241.474024268822,241.554703984718,241.652092022884),
 .UNSPECIFIED.);
#203=B_SPLINE_CURVE_WITH_KNOTS('',3,(#34318,#34319,#34320,#34321,#34322,
#34323,#34324,#34325,#34326,#34327,#34328,#34329,#34330,#34331,#34332,#34333,
#34334,#34335,#34336,#34337,#34338,#34339,#34340,#34341,#34342,#34343,#34344,
#34345,#34346,#34347,#34348,#34349,#34350,#34351,#34352,#34353,#34354,#34355,
#34356,#34357,#34358,#34359,#34360,#34361,#34362,#34363,#34364,#34365,#34366,
#34367,#34368,#34369,#34370,#34371,#34372,#34373,#34374,#34375,#34376,#34377,
#34378,#34379,#34380,#34381,#34382,#34383,#34384,#34385,#34386,#34387,#34388,
#34389,#34390,#34391,#34392,#34393,#34394,#34395,#34396,#34397,#34398,#34399,
#34400,#34401,#34402,#34403,#34404,#34405,#34406,#34407,#34408,#34409,#34410,
#34411,#34412,#34413,#34414,#34415,#34416,#34417,#34418,#34419,#34420,#34421,
#34422,#34423,#34424,#34425,#34426,#34427,#34428,#34429,#34430,#34431,#34432,
#34433,#34434,#34435,#34436,#34437,#34438,#34439,#34440,#34441,#34442,#34443,
#34444,#34445,#34446,#34447,#34448,#34449,#34450,#34451,#34452,#34453,#34454,
#34455,#34456,#34457,#34458,#34459,#34460,#34461,#34462,#34463,#34464,#34465,
#34466,#34467,#34468,#34469,#34470,#34471,#34472,#34473,#34474,#34475,#34476,
#34477,#34478,#34479,#34480,#34481,#34482,#34483,#34484,#34485,#34486,#34487,
#34488,#34489,#34490,#34491,#34492,#34493,#34494,#34495,#34496,#34497,#34498,
#34499,#34500,#34501,#34502,#34503,#34504,#34505,#34506,#34507,#34508,#34509,
#34510,#34511,#34512,#34513,#34514,#34515,#34516,#34517,#34518,#34519,#34520,
#34521,#34522,#34523,#34524,#34525,#34526,#34527,#34528,#34529,#34530,#34531,
#34532,#34533,#34534,#34535,#34536,#34537),.UNSPECIFIED.,.F.,.F.,(4,3,3,
3,3,3,3,3,3,3,3,3,3,3,3,3,3,3,3,3,3,3,3,3,3,3,3,3,3,3,3,3,3,3,3,3,3,3,3,
3,3,3,3,3,3,3,3,3,3,3,3,3,3,3,3,3,3,3,3,3,3,3,3,3,3,3,3,3,3,3,3,3,3,4),
(241.902634326587,241.999158887911,242.096209234875,242.193901448682,242.244149375723,
242.327888087569,242.411523598936,242.495076042335,242.578565478186,242.6620194288,
242.745455922646,242.828893032401,242.912348827319,242.995893320048,243.079482402989,
243.163205670547,243.243885386443,243.327624098289,243.411259609656,243.494812053055,
243.578301488906,243.66175543952,243.745191933366,243.828629043121,243.912084838039,
243.995629330769,244.07921841371,244.162941681267,244.243621397163,244.327360109009,
244.410995620376,244.494548063775,244.578037499626,244.661491450239,244.744927944086,
244.828365053841,244.911820848759,244.995365341488,245.078954424429,245.162677691987,
245.243357407883,245.327096119729,245.410731631096,245.494284074495,245.577773510346,
245.66122746096,245.744663954806,245.828101064562,245.911556859479,245.995101352209,
246.07869043515,246.162413702708,246.243093418603,246.326832130449,246.410467641816,
246.494020085215,246.577509521066,246.66096347168,246.744399965526,246.827837075282,
246.911292870199,246.994837362929,247.07842644587,247.162149713428,247.242829429323,
247.329226206015,247.412137556038,247.494973941528,247.577754132961,247.660496854229,
247.743234853931,247.82597074059,247.908743988731,247.934003642858),
 .UNSPECIFIED.);
#204=B_SPLINE_CURVE_WITH_KNOTS('',3,(#34538,#34539,#34540,#34541,#34542,
#34543,#34544,#34545,#34546,#34547),.UNSPECIFIED.,.F.,.F.,(4,3,3,4),(241.651741637788,
241.735236595357,241.818935460876,241.902634326395),.UNSPECIFIED.);
#205=B_SPLINE_CURVE_WITH_KNOTS('',3,(#34549,#34550,#34551,#34552,#34553,
#34554,#34555,#34556,#34557,#34558),.UNSPECIFIED.,.F.,.F.,(4,3,3,4),(241.652092022884,
241.748746650711,241.844665469492,241.902634326203),.UNSPECIFIED.);
#206=B_SPLINE_CURVE_WITH_KNOTS('',3,(#34559,#34560,#34561,#34562,#34563,
#34564,#34565,#34566,#34567,#34568,#34569,#34570,#34571,#34572,#34573,#34574,
#34575,#34576,#34577,#34578,#34579,#34580,#34581,#34582,#34583,#34584,#34585,
#34586,#34587,#34588,#34589,#34590,#34591,#34592,#34593,#34594,#34595,#34596,
#34597,#34598,#34599,#34600,#34601,#34602,#34603,#34604,#34605,#34606,#34607,
#34608,#34609,#34610,#34611,#34612,#34613,#34614,#34615,#34616,#34617,#34618,
#34619,#34620,#34621,#34622,#34623,#34624,#34625,#34626,#34627,#34628,#34629,
#34630,#34631,#34632,#34633,#34634,#34635,#34636,#34637,#34638,#34639,#34640,
#34641,#34642,#34643,#34644,#34645,#34646,#34647,#34648,#34649,#34650,#34651,
#34652,#34653,#34654,#34655,#34656,#34657,#34658,#34659,#34660,#34661,#34662,
#34663,#34664,#34665,#34666,#34667,#34668,#34669,#34670,#34671,#34672,#34673,
#34674,#34675,#34676,#34677,#34678,#34679,#34680,#34681,#34682,#34683,#34684,
#34685,#34686,#34687,#34688,#34689,#34690,#34691,#34692,#34693,#34694,#34695,
#34696,#34697,#34698,#34699,#34700,#34701,#34702,#34703,#34704,#34705,#34706,
#34707,#34708,#34709,#34710,#34711,#34712,#34713,#34714,#34715,#34716,#34717,
#34718,#34719,#34720,#34721,#34722,#34723,#34724,#34725,#34726,#34727,#34728,
#34729,#34730,#34731,#34732,#34733,#34734,#34735,#34736,#34737,#34738,#34739,
#34740,#34741,#34742,#34743,#34744,#34745,#34746,#34747,#34748,#34749,#34750,
#34751,#34752,#34753,#34754,#34755,#34756,#34757,#34758,#34759,#34760,#34761,
#34762,#34763,#34764,#34765,#34766,#34767,#34768,#34769,#34770,#34771,#34772,
#34773,#34774,#34775,#34776,#34777,#34778),.UNSPECIFIED.,.F.,.F.,(4,3,3,
3,3,3,3,3,3,3,3,3,3,3,3,3,3,3,3,3,3,3,3,3,3,3,3,3,3,3,3,3,3,3,3,3,3,3,3,
3,3,3,3,3,3,3,3,3,3,3,3,3,3,3,3,3,3,3,3,3,3,3,3,3,3,3,3,3,3,3,3,3,3,4),
(241.902634326398,241.986237486797,242.069834027506,242.153441752423,242.237078468855,
242.320815591498,242.404605844241,242.488534263311,242.554439995438,242.638178707284,
242.721814218652,242.80536666205,242.888856097901,242.972310048515,243.055746542361,
243.139183652116,243.222639447034,243.306183939764,243.389773022705,243.473496290262,
243.554176006158,243.637914718004,243.721550229371,243.80510267277,243.888592108621,
243.972046059235,244.055482553081,244.138919662837,244.222375457754,244.305919950484,
244.389509033425,244.473232300982,244.553912016878,244.637650728724,244.721286240092,
244.80483868349,244.888328119341,244.971782069955,245.055218563801,245.138655673557,
245.222111468475,245.305655961205,245.389245044146,245.472968311703,245.553648027598,
245.637386739444,245.721022250812,245.80457469421,245.888064130061,245.971518080675,
246.054954574521,246.138391684277,246.221847479194,246.305391971924,246.388981054865,
246.472704322423,246.553384038319,246.637122750165,246.720758261533,246.804310704931,
246.887800140782,246.971254091396,247.054690585242,247.138127694997,247.221583489915,
247.305127982644,247.388717065586,247.472440333143,247.553120049039,247.637422699873,
247.721583874919,247.805663482454,247.889664215379,247.935052702017),
 .UNSPECIFIED.);
#207=B_SPLINE_CURVE_WITH_KNOTS('',3,(#34784,#34785,#34786,#34787,#34788,
#34789,#34790,#34791,#34792,#34793,#34794,#34795,#34796,#34797,#34798,#34799,
#34800,#34801,#34802,#34803,#34804,#34805,#34806,#34807,#34808,#34809,#34810,
#34811,#34812,#34813,#34814,#34815,#34816,#34817,#34818,#34819,#34820,#34821,
#34822,#34823,#34824,#34825,#34826,#34827,#34828,#34829,#34830,#34831,#34832,
#34833,#34834,#34835,#34836,#34837,#34838,#34839,#34840,#34841,#34842,#34843,
#34844,#34845,#34846,#34847,#34848,#34849,#34850,#34851,#34852,#34853,#34854,
#34855,#34856,#34857,#34858,#34859,#34860,#34861,#34862,#34863,#34864,#34865,
#34866,#34867,#34868,#34869,#34870,#34871,#34872,#34873,#34874,#34875,#34876,
#34877,#34878,#34879,#34880,#34881,#34882,#34883,#34884,#34885,#34886,#34887,
#34888,#34889,#34890,#34891,#34892,#34893,#34894,#34895,#34896,#34897,#34898,
#34899,#34900,#34901,#34902,#34903,#34904,#34905,#34906,#34907,#34908,#34909,
#34910,#34911,#34912,#34913,#34914,#34915,#34916,#34917,#34918,#34919,#34920,
#34921,#34922,#34923,#34924,#34925,#34926,#34927,#34928,#34929,#34930,#34931,
#34932,#34933,#34934,#34935,#34936,#34937,#34938,#34939,#34940,#34941,#34942,
#34943,#34944,#34945,#34946,#34947,#34948,#34949,#34950,#34951,#34952,#34953,
#34954,#34955,#34956,#34957,#34958,#34959,#34960,#34961,#34962,#34963,#34964,
#34965,#34966,#34967,#34968,#34969,#34970,#34971,#34972,#34973,#34974,#34975,
#34976,#34977,#34978,#34979,#34980,#34981,#34982,#34983,#34984,#34985,#34986,
#34987,#34988,#34989,#34990,#34991,#34992,#34993,#34994,#34995,#34996,#34997,
#34998,#34999,#35000,#35001,#35002,#35003),.UNSPECIFIED.,.F.,.F.,(4,3,3,
3,3,3,3,3,3,3,3,3,3,3,3,3,3,3,3,3,3,3,3,3,3,3,3,3,3,3,3,3,3,3,3,3,3,3,3,
3,3,3,3,3,3,3,3,3,3,3,3,3,3,3,3,3,3,3,3,3,3,3,3,3,3,3,3,3,3,3,3,3,3,4),
(248.185819633574,248.242565440044,248.32630415189,248.409939663257,248.493492106656,
248.576981542507,248.66043549312,248.743871986967,248.827309096722,248.91076489164,
248.994309384369,249.07789846731,249.161621734868,249.242301450764,249.32604016261,
249.409675673977,249.493228117376,249.576717553227,249.660171503841,249.743607997687,
249.827045107442,249.91050090236,249.99404539509,250.077634478031,250.161357745588,
250.242037461484,250.32577617333,250.409411684697,250.492964128096,250.576453563947,
250.65990751456,250.743344008406,250.826781118162,250.910236913079,250.993781405809,
251.07737048875,251.161093756307,251.241773472204,251.32551218405,251.409147695417,
251.492700138816,251.576189574667,251.659643525281,251.743080019127,251.826517128883,
251.9099729238,251.99351741653,252.077106499471,252.160829767029,252.241509482924,
252.32524819477,252.408883706137,252.492436149536,252.575925585387,252.659379536001,
252.742816029847,252.826253139602,252.90970893452,252.993253427249,253.07684251019,
253.160565777748,253.241245493644,253.324985515348,253.408622030889,253.492175174065,
253.575665006275,253.659117790273,253.742552685343,253.825987763872,253.909441094444,
253.992977143822,254.076557604818,254.160258240132,254.217804721095),
 .UNSPECIFIED.);
#208=B_SPLINE_CURVE_WITH_KNOTS('',3,(#35004,#35005,#35006,#35007,#35008,
#35009,#35010,#35011,#35012,#35013),.UNSPECIFIED.,.F.,.F.,(4,3,3,4),(247.934003642858,
248.016867615733,248.101343624599,248.185819633466),.UNSPECIFIED.);
#209=B_SPLINE_CURVE_WITH_KNOTS('',3,(#35015,#35016,#35017,#35018,#35019,
#35020,#35021,#35022,#35023,#35024),.UNSPECIFIED.,.F.,.F.,(4,3,3,4),(247.935052702017,
248.018983507691,248.102906829926,248.185819633578),.UNSPECIFIED.);
#210=B_SPLINE_CURVE_WITH_KNOTS('',3,(#35025,#35026,#35027,#35028,#35029,
#35030,#35031,#35032,#35033,#35034,#35035,#35036,#35037,#35038,#35039,#35040,
#35041,#35042,#35043,#35044,#35045,#35046,#35047,#35048,#35049,#35050,#35051,
#35052,#35053,#35054,#35055,#35056,#35057,#35058,#35059,#35060,#35061,#35062,
#35063,#35064,#35065,#35066,#35067,#35068,#35069,#35070,#35071,#35072,#35073,
#35074,#35075,#35076,#35077,#35078,#35079,#35080,#35081,#35082,#35083,#35084,
#35085,#35086,#35087,#35088,#35089,#35090,#35091,#35092,#35093,#35094,#35095,
#35096,#35097,#35098,#35099,#35100,#35101,#35102,#35103,#35104,#35105,#35106,
#35107,#35108,#35109,#35110,#35111,#35112,#35113,#35114,#35115,#35116,#35117,
#35118,#35119,#35120,#35121,#35122,#35123,#35124,#35125,#35126,#35127,#35128,
#35129,#35130,#35131,#35132,#35133,#35134,#35135,#35136,#35137,#35138,#35139,
#35140,#35141,#35142,#35143,#35144,#35145,#35146,#35147,#35148,#35149,#35150,
#35151,#35152,#35153,#35154,#35155,#35156,#35157,#35158,#35159,#35160,#35161,
#35162,#35163,#35164,#35165,#35166,#35167,#35168,#35169,#35170,#35171,#35172,
#35173,#35174,#35175,#35176,#35177,#35178,#35179,#35180,#35181,#35182,#35183,
#35184,#35185,#35186,#35187,#35188,#35189,#35190,#35191,#35192,#35193,#35194,
#35195,#35196,#35197,#35198,#35199,#35200,#35201,#35202,#35203,#35204,#35205,
#35206,#35207,#35208,#35209,#35210,#35211,#35212,#35213,#35214,#35215,#35216,
#35217,#35218,#35219,#35220,#35221,#35222,#35223,#35224,#35225,#35226,#35227,
#35228,#35229,#35230,#35231,#35232,#35233,#35234,#35235,#35236,#35237,#35238,
#35239,#35240,#35241),.UNSPECIFIED.,.F.,.F.,(4,3,3,3,3,3,3,3,3,3,3,3,3,
3,3,3,3,3,3,3,3,3,3,3,3,3,3,3,3,3,3,3,3,3,3,3,3,3,3,3,3,3,3,3,3,3,3,3,3,
3,3,3,3,3,3,3,3,3,3,3,3,3,3,3,3,3,3,3,3,3,3,3,4),(248.185819633777,248.280331492552,
248.375236871607,248.470685077426,248.552856059759,248.636594771605,248.720230282972,
248.803782726371,248.887272162222,248.970726112836,249.054162606682,249.137599716437,
249.221055511355,249.304600004085,249.388189087026,249.471912354583,249.552592070479,
249.636330782325,249.719966293692,249.803518737091,249.887008172942,249.970462123556,
250.053898617402,250.137335727157,250.220791522075,250.304336014805,250.387925097746,
250.471648365303,250.552328081199,250.636066793045,250.719702304412,250.803254747811,
250.886744183662,250.970198134275,251.053634628122,251.137071737877,251.220527532795,
251.304072025524,251.387661108465,251.471384376023,251.552064091919,251.635802803765,
251.719438315132,251.802990758531,251.886480194382,251.969934144996,252.053370638842,
252.136807748597,252.220263543515,252.303808036245,252.387397119186,252.471120386743,
252.551800102639,252.635538814485,252.719174325852,252.802726769251,252.886216205102,
252.969670155716,253.053106649562,253.136543759317,253.219999554235,253.303544046965,
253.387133129906,253.470856397463,253.551536113359,253.63474008064,253.717434336362,
253.800053146387,253.882615442224,253.966253544571,254.048771139043,254.132969495327,
254.217167851611),.UNSPECIFIED.);
#211=B_SPLINE_CURVE_WITH_KNOTS('',3,(#35247,#35248,#35249,#35250,#35251,
#35252,#35253,#35254,#35255,#35256,#35257,#35258,#35259,#35260,#35261,#35262,
#35263,#35264,#35265,#35266,#35267,#35268,#35269,#35270,#35271,#35272,#35273,
#35274,#35275,#35276,#35277,#35278,#35279,#35280,#35281,#35282,#35283,#35284,
#35285,#35286,#35287,#35288,#35289,#35290,#35291,#35292,#35293,#35294,#35295,
#35296,#35297,#35298,#35299,#35300,#35301,#35302,#35303,#35304,#35305,#35306,
#35307,#35308,#35309,#35310,#35311,#35312,#35313,#35314,#35315,#35316,#35317,
#35318,#35319,#35320,#35321,#35322,#35323,#35324,#35325,#35326,#35327,#35328,
#35329,#35330,#35331,#35332,#35333,#35334,#35335,#35336,#35337,#35338,#35339,
#35340,#35341,#35342,#35343,#35344,#35345,#35346,#35347,#35348,#35349,#35350,
#35351,#35352,#35353,#35354,#35355,#35356,#35357,#35358,#35359,#35360,#35361,
#35362,#35363,#35364,#35365,#35366,#35367,#35368,#35369,#35370,#35371,#35372,
#35373,#35374,#35375,#35376,#35377,#35378,#35379,#35380,#35381,#35382,#35383,
#35384,#35385,#35386,#35387,#35388,#35389,#35390,#35391,#35392,#35393,#35394,
#35395,#35396,#35397,#35398,#35399,#35400,#35401,#35402,#35403,#35404,#35405,
#35406,#35407,#35408,#35409,#35410,#35411,#35412,#35413,#35414,#35415,#35416,
#35417,#35418,#35419,#35420,#35421,#35422,#35423,#35424,#35425,#35426,#35427,
#35428,#35429,#35430,#35431,#35432,#35433,#35434,#35435,#35436,#35437,#35438,
#35439,#35440,#35441,#35442,#35443,#35444,#35445,#35446,#35447,#35448,#35449,
#35450,#35451,#35452,#35453,#35454,#35455,#35456,#35457,#35458,#35459,#35460,
#35461,#35462,#35463,#35464,#35465,#35466),.UNSPECIFIED.,.F.,.F.,(4,3,3,
3,3,3,3,3,3,3,3,3,3,3,3,3,3,3,3,3,3,3,3,3,3,3,3,3,3,3,3,3,3,3,3,3,3,3,3,
3,3,3,3,3,3,3,3,3,3,3,3,3,3,3,3,3,3,3,3,3,3,3,3,3,3,3,3,3,3,3,3,3,3,4),
(254.469004940866,254.551459079282,254.637616383758,254.719977767009,254.802326638354,
254.884681938213,254.967062609701,255.049532107573,255.132053855559,255.214692257449,
255.240717515084,255.32445622693,255.408091738297,255.491644181696,255.575133617547,
255.658587568161,255.742024062007,255.825461171763,255.90891696668,255.99246145941,
256.076050542351,256.159773809909,256.240453525805,256.324192237651,256.407827749019,
256.491380192417,256.574869628268,256.658323578882,256.741760072729,256.825197182484,
256.908652977402,256.992197470132,257.075786553073,257.15950982063,257.240189536525,
257.323928248371,257.407563759738,257.491116203137,257.574605638988,257.658059589601,
257.741496083448,257.824933193203,257.90838898812,257.99193348085,258.075522563791,
258.159245831348,258.239925547245,258.323664259091,258.407299770458,258.490852213857,
258.574341649707,258.657795600321,258.741232094167,258.824669203923,258.908124998841,
258.991669491571,259.075258574512,259.158981842069,259.239661557965,259.323400269811,
259.407035781179,259.490588224577,259.574077660428,259.657531611042,259.740968104888,
259.824405214644,259.907861009562,259.991405502292,260.074994585232,260.15871785279,
260.239397568685,260.326957592193,260.414399638384,260.501841684575),
 .UNSPECIFIED.);
#212=B_SPLINE_CURVE_WITH_KNOTS('',3,(#35467,#35468,#35469,#35470,#35471,
#35472,#35473,#35474,#35475,#35476),.UNSPECIFIED.,.F.,.F.,(4,3,3,4),(254.217804721095,
254.240981504364,254.354993222559,254.469004940754),.UNSPECIFIED.);
#213=B_SPLINE_CURVE_WITH_KNOTS('',3,(#35478,#35479,#35480,#35481,#35482,
#35483,#35484,#35485,#35486,#35487),.UNSPECIFIED.,.F.,.F.,(4,3,3,4),(254.217167851611,
254.29979899428,254.384401967453,254.469004940626),.UNSPECIFIED.);
#214=B_SPLINE_CURVE_WITH_KNOTS('',3,(#35488,#35489,#35490,#35491,#35492,
#35493,#35494,#35495,#35496,#35497,#35498,#35499,#35500,#35501,#35502,#35503,
#35504,#35505,#35506,#35507,#35508,#35509,#35510,#35511,#35512,#35513,#35514,
#35515,#35516,#35517,#35518,#35519,#35520,#35521,#35522,#35523,#35524,#35525,
#35526,#35527,#35528,#35529,#35530,#35531,#35532,#35533,#35534,#35535,#35536,
#35537,#35538,#35539,#35540,#35541,#35542,#35543,#35544,#35545,#35546,#35547,
#35548,#35549,#35550,#35551,#35552,#35553,#35554,#35555,#35556,#35557,#35558,
#35559,#35560,#35561,#35562,#35563,#35564,#35565,#35566,#35567,#35568,#35569,
#35570,#35571,#35572,#35573,#35574,#35575,#35576,#35577,#35578,#35579,#35580,
#35581,#35582,#35583,#35584,#35585,#35586,#35587,#35588,#35589,#35590,#35591,
#35592,#35593,#35594,#35595,#35596,#35597,#35598,#35599,#35600,#35601,#35602,
#35603,#35604,#35605,#35606,#35607,#35608,#35609,#35610,#35611,#35612,#35613,
#35614,#35615,#35616,#35617,#35618,#35619,#35620,#35621,#35622,#35623,#35624,
#35625,#35626,#35627,#35628,#35629,#35630,#35631,#35632,#35633,#35634,#35635,
#35636,#35637,#35638,#35639,#35640,#35641,#35642,#35643,#35644,#35645,#35646,
#35647,#35648,#35649,#35650,#35651,#35652,#35653,#35654,#35655,#35656,#35657,
#35658,#35659,#35660,#35661,#35662,#35663,#35664,#35665,#35666,#35667,#35668,
#35669,#35670,#35671,#35672,#35673,#35674,#35675,#35676,#35677,#35678,#35679,
#35680,#35681,#35682,#35683,#35684,#35685,#35686,#35687,#35688,#35689,#35690,
#35691,#35692,#35693,#35694,#35695,#35696,#35697,#35698,#35699,#35700,#35701,
#35702,#35703,#35704,#35705,#35706,#35707),.UNSPECIFIED.,.F.,.F.,(4,3,3,
3,3,3,3,3,3,3,3,3,3,3,3,3,3,3,3,3,3,3,3,3,3,3,3,3,3,3,3,3,3,3,3,3,3,3,3,
3,3,3,3,3,3,3,3,3,3,3,3,3,3,3,3,3,3,3,3,3,3,3,3,3,3,3,3,3,3,3,3,3,3,4),
(254.469004940758,254.55127212408,254.635010835926,254.718646347293,254.802198790692,
254.885688226543,254.969142177157,255.052578671003,255.136015780759,255.219471575676,
255.303016068406,255.386605151347,255.470328418905,255.5510081348,255.634746846646,
255.718382358013,255.801934801412,255.885424237263,255.968878187876,256.052314681723,
256.135751791478,256.219207586396,256.302752079125,256.386341162066,256.470064429624,
256.55074414552,256.634482857366,256.718118368733,256.801670812132,256.885160247983,
256.968614198597,257.052050692443,257.135487802199,257.218943597116,257.302488089846,
257.386077172787,257.469800440344,257.55048015624,257.634218868086,257.717854379453,
257.801406822852,257.884896258703,257.968350209317,258.051786703163,258.135223812918,
258.218679607836,258.302224100566,258.385813183507,258.469536451064,258.55021616696,
258.633954878806,258.717590390173,258.801142833572,258.884632269423,258.968086220037,
259.051522713883,259.134959823638,259.218415618556,259.301960111286,259.385549194227,
259.469272461784,259.54995217768,259.633693676875,259.7173313316,259.80088527709,
259.888382505455,259.971832815521,260.055265626256,260.138699009296,260.222151032625,
260.305679936236,260.389253833429,260.472932818464,260.50086310401),
 .UNSPECIFIED.);
#215=B_SPLINE_CURVE_WITH_KNOTS('',3,(#35713,#35714,#35715,#35716,#35717,
#35718,#35719,#35720,#35721,#35722,#35723,#35724,#35725,#35726,#35727,#35728,
#35729,#35730,#35731,#35732,#35733,#35734,#35735,#35736,#35737,#35738,#35739,
#35740,#35741,#35742,#35743,#35744,#35745,#35746,#35747,#35748,#35749,#35750,
#35751,#35752,#35753,#35754,#35755,#35756,#35757,#35758,#35759,#35760,#35761,
#35762,#35763,#35764,#35765,#35766,#35767,#35768,#35769,#35770,#35771,#35772,
#35773,#35774,#35775,#35776,#35777,#35778,#35779,#35780,#35781,#35782,#35783,
#35784,#35785,#35786,#35787,#35788,#35789,#35790,#35791,#35792,#35793,#35794,
#35795,#35796,#35797,#35798,#35799,#35800,#35801,#35802,#35803,#35804,#35805,
#35806,#35807,#35808,#35809,#35810,#35811,#35812,#35813,#35814,#35815,#35816,
#35817,#35818,#35819,#35820,#35821,#35822,#35823,#35824,#35825,#35826,#35827,
#35828,#35829,#35830,#35831,#35832,#35833,#35834,#35835,#35836,#35837,#35838,
#35839,#35840,#35841,#35842,#35843,#35844,#35845,#35846,#35847,#35848,#35849,
#35850,#35851,#35852,#35853,#35854,#35855,#35856,#35857,#35858,#35859,#35860,
#35861,#35862,#35863,#35864,#35865,#35866,#35867,#35868,#35869,#35870,#35871,
#35872,#35873,#35874,#35875,#35876,#35877,#35878,#35879,#35880,#35881,#35882,
#35883,#35884,#35885,#35886,#35887,#35888,#35889,#35890,#35891,#35892,#35893,
#35894,#35895,#35896,#35897,#35898,#35899,#35900,#35901,#35902,#35903,#35904,
#35905,#35906,#35907,#35908,#35909,#35910,#35911,#35912,#35913,#35914,#35915,
#35916,#35917,#35918,#35919,#35920,#35921,#35922,#35923,#35924,#35925,#35926,
#35927,#35928,#35929,#35930,#35931,#35932),.UNSPECIFIED.,.F.,.F.,(4,3,3,
3,3,3,3,3,3,3,3,3,3,3,3,3,3,3,3,3,3,3,3,3,3,3,3,3,3,3,3,3,3,3,3,3,3,3,3,
3,3,3,3,3,3,3,3,3,3,3,3,3,3,3,3,3,3,3,3,3,3,3,3,3,3,3,3,3,3,3,3,3,3,4),
(260.752190248039,260.840077818288,260.928098755491,261.016344437238,261.104711000688,
261.193282498438,261.239133579405,261.322872291251,261.406507802619,261.490060246017,
261.573549681868,261.657003632482,261.740440126328,261.823877236084,261.907333031002,
261.990877523732,262.074466606673,262.15818987423,262.238869590125,262.322608301971,
262.406243813339,262.489796256737,262.573285692588,262.656739643202,262.740176137048,
262.823613246804,262.907069041721,262.990613534451,263.074202617392,263.15792588495,
263.238605600846,263.322344312692,263.405979824059,263.489532267458,263.573021703309,
263.656475653923,263.739912147769,263.823349257524,263.906805052442,263.990349545172,
264.073938628113,264.15766189567,264.238341611566,264.322080323412,264.405715834779,
264.489268278178,264.572757714029,264.656211664643,264.739648158489,264.823085268244,
264.906541063162,264.990085555892,265.073674638833,265.15739790639,265.238077622286,
265.321816334132,265.405451845499,265.489004288898,265.572493724749,265.655947675363,
265.739384169209,265.822821278965,265.906277073882,265.989821566612,266.073410649553,
266.157133917111,266.237813633006,266.320335372003,266.402760918938,266.48510946943,
266.567397842967,266.649650649338,266.731899755698,266.783796292336),
 .UNSPECIFIED.);
#216=B_SPLINE_CURVE_WITH_KNOTS('',3,(#35933,#35934,#35935,#35936,#35937,
#35938,#35939,#35940,#35941,#35942),.UNSPECIFIED.,.F.,.F.,(4,3,3,4),(260.501841684575,
260.588962512034,260.675942991099,260.752190247933),.UNSPECIFIED.);
#217=B_SPLINE_CURVE_WITH_KNOTS('',3,(#35944,#35945,#35946,#35947,#35948,
#35949,#35950,#35951,#35952,#35953),.UNSPECIFIED.,.F.,.F.,(4,3,3,4),(260.50086310401,
260.5496881884,260.669135343435,260.752190247937),.UNSPECIFIED.);
#218=B_SPLINE_CURVE_WITH_KNOTS('',3,(#35954,#35955,#35956,#35957,#35958,
#35959,#35960,#35961,#35962,#35963,#35964,#35965,#35966,#35967,#35968,#35969,
#35970,#35971,#35972,#35973,#35974,#35975,#35976,#35977,#35978,#35979,#35980,
#35981,#35982,#35983,#35984,#35985,#35986,#35987,#35988,#35989,#35990,#35991,
#35992,#35993,#35994,#35995,#35996,#35997,#35998,#35999,#36000,#36001,#36002,
#36003,#36004,#36005,#36006,#36007,#36008,#36009,#36010,#36011,#36012,#36013,
#36014,#36015,#36016,#36017,#36018,#36019,#36020,#36021,#36022,#36023,#36024,
#36025,#36026,#36027,#36028,#36029,#36030,#36031,#36032,#36033,#36034,#36035,
#36036,#36037,#36038,#36039,#36040,#36041,#36042,#36043,#36044,#36045,#36046,
#36047,#36048,#36049,#36050,#36051,#36052,#36053,#36054,#36055,#36056,#36057,
#36058,#36059,#36060,#36061,#36062,#36063,#36064,#36065,#36066,#36067,#36068,
#36069,#36070,#36071,#36072,#36073,#36074,#36075,#36076,#36077,#36078,#36079,
#36080,#36081,#36082,#36083,#36084,#36085,#36086,#36087,#36088,#36089,#36090,
#36091,#36092,#36093,#36094,#36095,#36096,#36097,#36098,#36099,#36100,#36101,
#36102,#36103,#36104,#36105,#36106,#36107,#36108,#36109,#36110,#36111,#36112,
#36113,#36114,#36115,#36116,#36117,#36118,#36119,#36120,#36121,#36122,#36123,
#36124,#36125,#36126,#36127,#36128,#36129,#36130,#36131,#36132,#36133,#36134,
#36135,#36136,#36137,#36138,#36139,#36140,#36141,#36142,#36143,#36144,#36145,
#36146,#36147,#36148,#36149,#36150,#36151,#36152,#36153,#36154,#36155,#36156,
#36157,#36158,#36159,#36160,#36161,#36162,#36163,#36164,#36165,#36166,#36167,
#36168,#36169,#36170,#36171,#36172,#36173),.UNSPECIFIED.,.F.,.F.,(4,3,3,
3,3,3,3,3,3,3,3,3,3,3,3,3,3,3,3,3,3,3,3,3,3,3,3,3,3,3,3,3,3,3,3,3,3,3,3,
3,3,3,3,3,3,3,3,3,3,3,3,3,3,3,3,3,3,3,3,3,3,3,3,3,3,3,3,3,3,3,3,3,3,4),
(260.752190248121,260.834571493874,260.916884504121,260.999156020819,261.081407233152,
261.163657149231,261.245924773897,261.328276962325,261.410674639221,261.493196468606,
261.54942419912,261.633162910966,261.716798422334,261.800350865732,261.883840301583,
261.967294252197,262.050730746043,262.134167855798,262.217623650716,262.301168143446,
262.384757226387,262.468480493944,262.549160209841,262.632898921687,262.716534433055,
262.800086876454,262.883576312304,262.967030262918,263.050466756764,263.13390386652,
263.217359661438,263.300904154168,263.384493237109,263.468216504666,263.548896220561,
263.632634932407,263.716270443774,263.799822887173,263.883312323024,263.966766273637,
264.050202767484,264.133639877239,264.217095672156,264.300640164886,264.384229247827,
264.467952515385,264.548632231281,264.632370943127,264.716006454494,264.799558897893,
264.883048333744,264.966502284357,265.049938778204,265.133375887959,265.216831682877,
265.300376175607,265.383965258548,265.467688526105,265.548368242001,265.632106953847,
265.715742465215,265.799294908613,265.882784344464,265.966238295078,266.049674788924,
266.13311189868,266.216567693597,266.300112186327,266.383701269268,266.467424536826,
266.548104252721,266.636675884245,266.725043738978,266.785062210057),
 .UNSPECIFIED.);
#219=B_SPLINE_CURVE_WITH_KNOTS('',3,(#36179,#36180,#36181,#36182,#36183,
#36184,#36185,#36186,#36187,#36188,#36189,#36190,#36191,#36192,#36193,#36194,
#36195,#36196,#36197,#36198,#36199,#36200,#36201,#36202,#36203,#36204,#36205,
#36206,#36207,#36208,#36209,#36210,#36211,#36212,#36213,#36214,#36215,#36216,
#36217,#36218,#36219,#36220,#36221,#36222,#36223,#36224,#36225,#36226,#36227,
#36228,#36229,#36230,#36231,#36232,#36233,#36234,#36235,#36236,#36237,#36238,
#36239,#36240,#36241,#36242,#36243,#36244,#36245,#36246,#36247,#36248,#36249,
#36250,#36251,#36252,#36253,#36254,#36255,#36256,#36257,#36258,#36259,#36260,
#36261,#36262,#36263,#36264,#36265,#36266,#36267,#36268,#36269,#36270,#36271,
#36272,#36273,#36274,#36275,#36276,#36277,#36278,#36279,#36280,#36281,#36282,
#36283,#36284,#36285,#36286,#36287,#36288,#36289,#36290,#36291,#36292,#36293,
#36294,#36295,#36296,#36297,#36298,#36299,#36300,#36301,#36302,#36303,#36304,
#36305,#36306,#36307,#36308,#36309,#36310,#36311,#36312,#36313,#36314,#36315,
#36316,#36317,#36318,#36319,#36320,#36321,#36322,#36323,#36324,#36325,#36326,
#36327,#36328,#36329,#36330,#36331,#36332,#36333,#36334,#36335,#36336,#36337,
#36338,#36339,#36340,#36341,#36342,#36343,#36344,#36345,#36346,#36347,#36348,
#36349,#36350,#36351,#36352,#36353,#36354,#36355,#36356,#36357,#36358,#36359,
#36360,#36361,#36362,#36363,#36364,#36365,#36366,#36367,#36368,#36369,#36370,
#36371,#36372,#36373,#36374,#36375,#36376,#36377,#36378,#36379,#36380,#36381,
#36382,#36383,#36384,#36385,#36386,#36387,#36388,#36389,#36390,#36391,#36392,
#36393,#36394,#36395),.UNSPECIFIED.,.F.,.F.,(4,3,3,3,3,3,3,3,3,3,3,3,3,
3,3,3,3,3,3,3,3,3,3,3,3,3,3,3,3,3,3,3,3,3,3,3,3,3,3,3,3,3,3,3,3,3,3,3,3,
3,3,3,3,3,3,3,3,3,3,3,3,3,3,3,3,3,3,3,3,3,3,3,4),(267.035375555113,267.154919976287,
267.237549643726,267.321288355572,267.404923866939,267.488476310338,267.571965746189,
267.655419696803,267.738856190649,267.822293300404,267.905749095322,267.989293588052,
268.072882670993,268.156605938551,268.237285654446,268.321024366292,268.404659877659,
268.488212321058,268.571701756909,268.655155707522,268.738592201369,268.822029311124,
268.905485106042,268.989029598771,269.072618681712,269.15634194927,269.237021665166,
269.320760377012,269.404395888379,269.487948331778,269.571437767629,269.654891718243,
269.738328212089,269.821765321845,269.905221116762,269.988765609492,270.072354692433,
270.156077959991,270.236757675886,270.320496387732,270.4041318991,270.487684342498,
270.571173778349,270.654627728963,270.738064222809,270.821501332565,270.904957127483,
270.988501620212,271.072090703153,271.155813970711,271.236493686607,271.320232398453,
271.403867909821,271.487420353219,271.57090978907,271.654363739684,271.73780023353,
271.821237343286,271.904693138204,271.988237630933,272.071826713874,272.155549981432,
272.236229697327,272.319978513639,272.403621899315,272.487165079065,272.570651436406,
272.654099090554,272.737526130872,272.820979923044,272.904444581242,272.987986644754,
273.06691472068),.UNSPECIFIED.);
#220=B_SPLINE_CURVE_WITH_KNOTS('',3,(#36396,#36397,#36398,#36399,#36400,
#36401,#36402,#36403,#36404,#36405),.UNSPECIFIED.,.F.,.F.,(4,3,3,4),(266.783796292336,
266.866079451347,266.950727503137,267.035375554927),.UNSPECIFIED.);
#221=B_SPLINE_CURVE_WITH_KNOTS('',3,(#36407,#36408,#36409,#36410,#36411,
#36412,#36413,#36414,#36415,#36416),.UNSPECIFIED.,.F.,.F.,(4,3,3,4),(266.785062210057,
266.873164835651,266.961082385074,267.035375555014),.UNSPECIFIED.);
#222=B_SPLINE_CURVE_WITH_KNOTS('',3,(#36417,#36418,#36419,#36420,#36421,
#36422,#36423,#36424,#36425,#36426,#36427,#36428,#36429,#36430,#36431,#36432,
#36433,#36434,#36435,#36436,#36437,#36438,#36439,#36440,#36441,#36442,#36443,
#36444,#36445,#36446,#36447,#36448,#36449,#36450,#36451,#36452,#36453,#36454,
#36455,#36456,#36457,#36458,#36459,#36460,#36461,#36462,#36463,#36464,#36465,
#36466,#36467,#36468,#36469,#36470,#36471,#36472,#36473,#36474,#36475,#36476,
#36477,#36478,#36479,#36480,#36481,#36482,#36483,#36484,#36485,#36486,#36487,
#36488,#36489,#36490,#36491,#36492,#36493,#36494,#36495,#36496,#36497,#36498,
#36499,#36500,#36501,#36502,#36503,#36504,#36505,#36506,#36507,#36508,#36509,
#36510,#36511,#36512,#36513,#36514,#36515,#36516,#36517,#36518,#36519,#36520,
#36521,#36522,#36523,#36524,#36525,#36526,#36527,#36528,#36529,#36530,#36531,
#36532,#36533,#36534,#36535,#36536,#36537,#36538,#36539,#36540,#36541,#36542,
#36543,#36544,#36545,#36546,#36547,#36548,#36549,#36550,#36551,#36552,#36553,
#36554,#36555,#36556,#36557,#36558,#36559,#36560,#36561,#36562,#36563,#36564,
#36565,#36566,#36567,#36568,#36569,#36570,#36571,#36572,#36573,#36574,#36575,
#36576,#36577,#36578,#36579,#36580,#36581,#36582,#36583,#36584,#36585,#36586,
#36587,#36588,#36589,#36590,#36591,#36592,#36593,#36594,#36595,#36596,#36597,
#36598,#36599,#36600,#36601,#36602,#36603,#36604,#36605,#36606,#36607,#36608,
#36609,#36610,#36611,#36612,#36613,#36614,#36615,#36616,#36617,#36618,#36619,
#36620,#36621,#36622,#36623,#36624,#36625,#36626,#36627,#36628,#36629,#36630,
#36631,#36632,#36633,#36634,#36635,#36636),.UNSPECIFIED.,.F.,.F.,(4,3,3,
3,3,3,3,3,3,3,3,3,3,3,3,3,3,3,3,3,3,3,3,3,3,3,3,3,3,3,3,3,3,3,3,3,3,3,3,
3,3,3,3,3,3,3,3,3,3,3,3,3,3,3,3,3,3,3,3,3,3,3,3,3,3,3,3,3,3,3,3,3,3,4),
(267.035375555117,267.122336957127,267.209397452547,267.296648856939,267.383998872037,
267.47154721962,267.547840263441,267.631578975287,267.715214486655,267.798766930053,
267.882256365904,267.965710316518,268.049146810364,268.13258392012,268.216039715037,
268.299584207767,268.383173290708,268.466896558266,268.547576274161,268.631314986007,
268.714950497375,268.798502940773,268.881992376624,268.965446327238,269.048882821084,
269.13231993084,269.215775725758,269.299320218487,269.382909301429,269.466632568986,
269.547312284882,269.631050996728,269.714686508096,269.798238951494,269.881728387345,
269.965182337959,270.048618831805,270.132055941561,270.215511736478,270.299056229208,
270.382645312149,270.466368579707,270.547048295602,270.630787007448,270.714422518815,
270.797974962214,270.881464398065,270.964918348679,271.048354842525,271.13179195228,
271.215247747198,271.298792239928,271.382381322868,271.466104590426,271.546784306322,
271.630523018168,271.714158529536,271.797710972934,271.881200408785,271.964654359398,
272.048090853245,272.131527963,272.214983757918,272.298528250647,272.382117333588,
272.465840601146,272.546520317042,272.629147478544,272.71167748403,272.794129465717,
272.876517967464,272.958870159486,273.041211385537,273.067091906304),
 .UNSPECIFIED.);
#223=B_SPLINE_CURVE_WITH_KNOTS('',3,(#36642,#36643,#36644,#36645,#36646,
#36647,#36648,#36649,#36650,#36651,#36652,#36653,#36654,#36655,#36656,#36657,
#36658,#36659,#36660,#36661,#36662,#36663,#36664,#36665,#36666,#36667,#36668,
#36669,#36670,#36671,#36672,#36673,#36674,#36675,#36676,#36677,#36678,#36679,
#36680,#36681,#36682,#36683,#36684,#36685,#36686,#36687,#36688,#36689,#36690,
#36691,#36692,#36693,#36694,#36695,#36696,#36697,#36698,#36699,#36700,#36701,
#36702,#36703,#36704,#36705,#36706,#36707,#36708,#36709,#36710,#36711,#36712,
#36713,#36714,#36715,#36716,#36717,#36718,#36719,#36720,#36721,#36722,#36723,
#36724,#36725,#36726,#36727,#36728,#36729,#36730,#36731,#36732,#36733,#36734,
#36735,#36736,#36737,#36738,#36739,#36740,#36741,#36742,#36743,#36744,#36745,
#36746,#36747,#36748,#36749,#36750,#36751,#36752,#36753,#36754,#36755,#36756,
#36757,#36758,#36759,#36760,#36761,#36762,#36763,#36764,#36765,#36766,#36767,
#36768,#36769,#36770,#36771,#36772,#36773,#36774,#36775,#36776,#36777,#36778,
#36779,#36780,#36781,#36782,#36783,#36784,#36785,#36786,#36787,#36788,#36789,
#36790,#36791,#36792,#36793,#36794,#36795,#36796,#36797,#36798,#36799,#36800,
#36801,#36802,#36803,#36804,#36805,#36806,#36807,#36808,#36809,#36810,#36811,
#36812,#36813,#36814,#36815,#36816,#36817,#36818,#36819,#36820,#36821,#36822,
#36823,#36824,#36825,#36826,#36827,#36828,#36829,#36830,#36831,#36832,#36833,
#36834,#36835,#36836,#36837,#36838,#36839,#36840,#36841,#36842,#36843,#36844,
#36845,#36846,#36847,#36848,#36849,#36850,#36851,#36852,#36853,#36854,#36855,
#36856,#36857,#36858,#36859,#36860,#36861),.UNSPECIFIED.,.F.,.F.,(4,3,3,
3,3,3,3,3,3,3,3,3,3,3,3,3,3,3,3,3,3,3,3,3,3,3,3,3,3,3,3,3,3,3,3,3,3,3,3,
3,3,3,3,3,3,3,3,3,3,3,3,3,3,3,3,3,3,3,3,3,3,3,3,3,3,3,3,3,3,3,3,3,3,4),
(273.318560862424,273.401332140583,273.48400781649,273.566608858109,273.650245465692,
273.732769655677,273.815286530553,273.8978149211,273.982286620517,274.06493792759,
274.150319823179,274.235701718767,274.319440430613,274.403075941981,274.486628385379,
274.57011782123,274.653571771844,274.73700826569,274.820445375445,274.903901170363,
274.987445663092,275.071034746033,275.154758013591,275.235437729487,275.319176441333,
275.4028119527,275.486364396099,275.56985383195,275.653307782563,275.73674427641,
275.820181386165,275.903637181083,275.987181673812,276.070770756753,276.154494024311,
276.235173740207,276.318912452053,276.40254796342,276.486100406819,276.569589842671,
276.653043793284,276.736480287131,276.819917396886,276.903373191804,276.986917684533,
277.070506767474,277.154230035032,277.234909750927,277.318648462773,277.40228397414,
277.485836417539,277.56932585339,277.652779804003,277.73621629785,277.819653407605,
277.903109202523,277.986653695253,278.070242778194,278.153966045751,278.234645761647,
278.318384473493,278.402019984861,278.48557242826,278.569061864111,278.652515814725,
278.735952308571,278.819389418327,278.902845213245,278.986389705974,279.069978788915,
279.153702056473,279.234381772368,279.329926919196,279.351278122143),
 .UNSPECIFIED.);
#224=B_SPLINE_CURVE_WITH_KNOTS('',3,(#36862,#36863,#36864,#36865,#36866,
#36867,#36868,#36869,#36870,#36871),.UNSPECIFIED.,.F.,.F.,(4,3,3,4),(273.06691472068,
273.151440214363,273.235965708047,273.318560862292),.UNSPECIFIED.);
#225=B_SPLINE_CURVE_WITH_KNOTS('',3,(#36873,#36874,#36875,#36876,#36877,
#36878,#36879,#36880,#36881,#36882),.UNSPECIFIED.,.F.,.F.,(4,3,3,4),(273.067091906304,
273.149461125864,273.23401099402,273.318560862176),.UNSPECIFIED.);
#226=B_SPLINE_CURVE_WITH_KNOTS('',3,(#36883,#36884,#36885,#36886,#36887,
#36888,#36889,#36890,#36891,#36892,#36893,#36894,#36895,#36896,#36897,#36898,
#36899,#36900,#36901,#36902,#36903,#36904,#36905,#36906,#36907,#36908,#36909,
#36910,#36911,#36912,#36913,#36914,#36915,#36916,#36917,#36918,#36919,#36920,
#36921,#36922,#36923,#36924,#36925,#36926,#36927,#36928,#36929,#36930,#36931,
#36932,#36933,#36934,#36935,#36936,#36937,#36938,#36939,#36940,#36941,#36942,
#36943,#36944,#36945,#36946,#36947,#36948,#36949,#36950,#36951,#36952,#36953,
#36954,#36955,#36956,#36957,#36958,#36959,#36960,#36961,#36962,#36963,#36964,
#36965,#36966,#36967,#36968,#36969,#36970,#36971,#36972,#36973,#36974,#36975,
#36976,#36977,#36978,#36979,#36980,#36981,#36982,#36983,#36984,#36985,#36986,
#36987,#36988,#36989,#36990,#36991,#36992,#36993,#36994,#36995,#36996,#36997,
#36998,#36999,#37000,#37001,#37002,#37003,#37004,#37005,#37006,#37007,#37008,
#37009,#37010,#37011,#37012,#37013,#37014,#37015,#37016,#37017,#37018,#37019,
#37020,#37021,#37022,#37023,#37024,#37025,#37026,#37027,#37028,#37029,#37030,
#37031,#37032,#37033,#37034,#37035,#37036,#37037,#37038,#37039,#37040,#37041,
#37042,#37043,#37044,#37045,#37046,#37047,#37048,#37049,#37050,#37051,#37052,
#37053,#37054,#37055,#37056,#37057,#37058,#37059,#37060,#37061,#37062,#37063,
#37064,#37065,#37066,#37067,#37068,#37069,#37070,#37071,#37072,#37073,#37074,
#37075,#37076,#37077,#37078,#37079,#37080,#37081,#37082,#37083,#37084,#37085,
#37086,#37087,#37088,#37089,#37090,#37091,#37092,#37093,#37094,#37095,#37096,
#37097,#37098,#37099),.UNSPECIFIED.,.F.,.F.,(4,3,3,3,3,3,3,3,3,3,3,3,3,
3,3,3,3,3,3,3,3,3,3,3,3,3,3,3,3,3,3,3,3,3,3,3,3,3,3,3,3,3,3,3,3,3,3,3,3,
3,3,3,3,3,3,3,3,3,3,3,3,3,3,3,3,3,3,3,3,3,3,3,4),(273.318560862296,273.432408595029,
273.546256327762,273.629995039608,273.713630550976,273.797182994374,273.880672430225,
273.964126380839,274.047562874685,274.130999984441,274.214455779359,274.298000272089,
274.38158935503,274.465312622587,274.545992338482,274.629731050328,274.713366561695,
274.796919005094,274.880408440945,274.963862391558,275.047298885404,275.13073599516,
275.214191790077,275.297736282807,275.381325365748,275.465048633305,275.545728349202,
275.629467061048,275.713102572415,275.796655015814,275.880144451665,275.963598402279,
276.047034896125,276.130472005881,276.213927800798,276.297472293528,276.381061376469,
276.464784644027,276.545464359922,276.629203071768,276.712838583136,276.796391026534,
276.879880462385,276.963334412999,277.046770906845,277.130208016601,277.213663811519,
277.297208304248,277.380797387189,277.464520654747,277.545200370643,277.628939082489,
277.712574593856,277.796127037255,277.879616473106,277.96307042372,278.046506917566,
278.129944027322,278.213399822239,278.296944314969,278.38053339791,278.464256665468,
278.544936381363,278.628686835053,278.712331521095,278.795875148069,278.879361474852,
278.962808621501,279.046234677786,279.129682656208,279.213141308916,279.296665516618,
279.350082863217),.UNSPECIFIED.);
#227=B_SPLINE_CURVE_WITH_KNOTS('',3,(#37105,#37106,#37107,#37108,#37109,
#37110,#37111,#37112,#37113,#37114,#37115,#37116,#37117,#37118,#37119,#37120,
#37121,#37122,#37123,#37124,#37125,#37126,#37127,#37128,#37129,#37130,#37131,
#37132,#37133,#37134,#37135,#37136,#37137,#37138,#37139,#37140,#37141,#37142,
#37143,#37144,#37145,#37146,#37147,#37148,#37149,#37150,#37151,#37152,#37153,
#37154,#37155,#37156,#37157,#37158,#37159,#37160,#37161,#37162,#37163,#37164,
#37165,#37166,#37167,#37168,#37169,#37170,#37171,#37172,#37173,#37174,#37175,
#37176,#37177,#37178,#37179,#37180,#37181,#37182,#37183,#37184,#37185,#37186,
#37187,#37188,#37189,#37190,#37191,#37192,#37193,#37194,#37195,#37196,#37197,
#37198,#37199,#37200,#37201,#37202,#37203,#37204,#37205,#37206,#37207,#37208,
#37209,#37210,#37211,#37212,#37213,#37214,#37215,#37216,#37217,#37218,#37219,
#37220,#37221,#37222,#37223,#37224,#37225,#37226,#37227,#37228,#37229,#37230,
#37231,#37232,#37233,#37234,#37235,#37236,#37237,#37238,#37239,#37240,#37241,
#37242,#37243,#37244,#37245,#37246,#37247,#37248,#37249,#37250,#37251,#37252,
#37253,#37254,#37255,#37256,#37257,#37258,#37259,#37260,#37261,#37262,#37263,
#37264,#37265,#37266,#37267,#37268,#37269,#37270,#37271,#37272,#37273,#37274,
#37275,#37276,#37277,#37278,#37279,#37280,#37281,#37282,#37283,#37284,#37285,
#37286,#37287,#37288,#37289,#37290,#37291,#37292,#37293,#37294,#37295,#37296,
#37297,#37298,#37299,#37300,#37301,#37302,#37303,#37304,#37305,#37306,#37307,
#37308,#37309,#37310,#37311,#37312,#37313,#37314,#37315,#37316,#37317,#37318,
#37319,#37320,#37321,#37322,#37323,#37324),.UNSPECIFIED.,.F.,.F.,(4,3,3,
3,3,3,3,3,3,3,3,3,3,3,3,3,3,3,3,3,3,3,3,3,3,3,3,3,3,3,3,3,3,3,3,3,3,3,3,
3,3,3,3,3,3,3,3,3,3,3,3,3,3,3,3,3,3,3,3,3,3,3,3,3,3,3,3,3,3,3,3,3,3,4),
(279.601746169472,279.685672429252,279.769601901197,279.853551962208,279.937539998755,
280.021635635826,280.105791581247,280.190082572072,280.234117783088,280.317856494934,
280.401492006301,280.4850444497,280.568533885551,280.651987836165,280.735424330011,
280.818861439766,280.902317234684,280.985861727414,281.069450810355,281.153174077913,
281.233853793808,281.317592505654,281.401228017021,281.48478046042,281.568269896271,
281.651723846884,281.735160340731,281.818597450486,281.902053245403,281.985597738133,
282.069186821074,282.152910088631,282.233589804528,282.317328516374,282.400964027741,
282.48451647114,282.56800590699,282.651459857604,282.734896351451,282.818333461206,
282.901789256124,282.985333748854,283.068922831795,283.152646099352,283.233325815248,
283.317064527094,283.400700038461,283.48425248186,283.567741917711,283.651195868325,
283.734632362171,283.818069471927,283.901525266845,283.985069759574,284.068658842515,
284.152382110073,284.233061825968,284.316800537814,284.400436049181,284.48398849258,
284.567477928431,284.650931879045,284.734368372891,284.817805482646,284.901261277563,
284.984805770293,285.068394853234,285.152118120792,285.232797836688,285.316744966212,
285.400555054353,285.484286316186,285.56794519696,285.634069424409),
 .UNSPECIFIED.);
#228=B_SPLINE_CURVE_WITH_KNOTS('',3,(#37325,#37326,#37327,#37328,#37329,
#37330,#37331,#37332,#37333,#37334),.UNSPECIFIED.,.F.,.F.,(4,3,3,4),(279.351278122143,
279.446286643589,279.540691824518,279.601746169273),.UNSPECIFIED.);
#229=B_SPLINE_CURVE_WITH_KNOTS('',3,(#37336,#37337,#37338,#37339,#37340,
#37341,#37342,#37343,#37344,#37345,#37346,#37347,#37348),.UNSPECIFIED.,
 .F.,.F.,(4,3,3,3,4),(279.350082863217,279.433708952402,279.517454217818,
279.544672392083,279.601746169476),.UNSPECIFIED.);
#230=B_SPLINE_CURVE_WITH_KNOTS('',3,(#37349,#37350,#37351,#37352,#37353,
#37354,#37355,#37356,#37357,#37358,#37359,#37360,#37361,#37362,#37363,#37364,
#37365,#37366,#37367,#37368,#37369,#37370,#37371,#37372,#37373,#37374,#37375,
#37376,#37377,#37378,#37379,#37380,#37381,#37382,#37383,#37384,#37385,#37386,
#37387,#37388,#37389,#37390,#37391,#37392,#37393,#37394,#37395,#37396,#37397,
#37398,#37399,#37400,#37401,#37402,#37403,#37404,#37405,#37406,#37407,#37408,
#37409,#37410,#37411,#37412,#37413,#37414,#37415,#37416,#37417,#37418,#37419,
#37420,#37421,#37422,#37423,#37424,#37425,#37426,#37427,#37428,#37429,#37430,
#37431,#37432,#37433,#37434,#37435,#37436,#37437,#37438,#37439,#37440,#37441,
#37442,#37443,#37444,#37445,#37446,#37447,#37448,#37449,#37450,#37451,#37452,
#37453,#37454,#37455,#37456,#37457,#37458,#37459,#37460,#37461,#37462,#37463,
#37464,#37465,#37466,#37467,#37468,#37469,#37470,#37471,#37472,#37473,#37474,
#37475,#37476,#37477,#37478,#37479,#37480,#37481,#37482,#37483,#37484,#37485,
#37486,#37487,#37488,#37489,#37490,#37491,#37492,#37493,#37494,#37495,#37496,
#37497,#37498,#37499,#37500,#37501,#37502,#37503,#37504,#37505,#37506,#37507,
#37508,#37509,#37510,#37511,#37512,#37513,#37514,#37515,#37516,#37517,#37518,
#37519,#37520,#37521,#37522,#37523,#37524,#37525,#37526,#37527,#37528,#37529,
#37530,#37531,#37532,#37533,#37534,#37535,#37536,#37537,#37538,#37539,#37540,
#37541,#37542,#37543,#37544,#37545,#37546,#37547,#37548,#37549,#37550,#37551,
#37552,#37553,#37554,#37555,#37556,#37557,#37558,#37559,#37560,#37561,#37562,
#37563,#37564,#37565,#37566,#37567,#37568),.UNSPECIFIED.,.F.,.F.,(4,3,3,
3,3,3,3,3,3,3,3,3,3,3,3,3,3,3,3,3,3,3,3,3,3,3,3,3,3,3,3,3,3,3,3,3,3,3,3,
3,3,3,3,3,3,3,3,3,3,3,3,3,3,3,3,3,3,3,3,3,3,3,3,3,3,3,3,3,3,3,3,3,3,4),
(279.601746169585,279.684754693531,279.767664002698,279.850494901022,279.937234088745,
280.019978327433,280.102712039047,280.185453899734,280.268222588391,280.351081808708,
280.433994088779,280.517024272122,280.544408402803,280.628147114649,280.711782626016,
280.795335069415,280.878824505266,280.96227845588,281.045714949726,281.129152059481,
281.212607854399,281.296152347129,281.37974143007,281.463464697627,281.544144413523,
281.627883125369,281.711518636736,281.795071080135,281.878560515986,281.9620144666,
282.045450960446,282.128888070201,282.212343865119,282.295888357849,282.379477440789,
282.463200708347,282.543880424243,282.627619136089,282.711254647456,282.794807090855,
282.878296526706,282.96175047732,283.045186971166,283.128624080921,283.212079875839,
283.295624368568,283.379213451509,283.462936719067,283.543616434963,283.627355146809,
283.710990658177,283.794543101575,283.878032537427,283.96148648804,284.044922981887,
284.128360091642,284.21181588656,284.29536037929,284.378949462231,284.462672729788,
284.543352445683,284.627091157529,284.710726668896,284.794279112295,284.877768548146,
284.96122249876,285.044658992606,285.128096102361,285.211551897279,285.295096390009,
285.37868547295,285.462408740508,285.543088456404,285.63436337626),
 .UNSPECIFIED.);
#231=B_SPLINE_CURVE_WITH_KNOTS('',3,(#37574,#37575,#37576,#37577,#37578,
#37579,#37580,#37581,#37582,#37583,#37584,#37585,#37586,#37587,#37588,#37589,
#37590,#37591,#37592,#37593,#37594,#37595,#37596,#37597,#37598,#37599,#37600,
#37601,#37602,#37603,#37604,#37605,#37606,#37607,#37608,#37609,#37610,#37611,
#37612,#37613,#37614,#37615,#37616,#37617,#37618,#37619,#37620,#37621,#37622,
#37623,#37624,#37625,#37626,#37627,#37628,#37629,#37630,#37631,#37632,#37633,
#37634,#37635,#37636,#37637,#37638,#37639,#37640,#37641,#37642,#37643,#37644,
#37645,#37646,#37647,#37648,#37649,#37650,#37651,#37652,#37653,#37654,#37655,
#37656,#37657,#37658,#37659,#37660,#37661,#37662,#37663,#37664,#37665,#37666,
#37667,#37668,#37669,#37670,#37671,#37672,#37673,#37674,#37675,#37676,#37677,
#37678,#37679,#37680,#37681,#37682,#37683,#37684,#37685,#37686,#37687,#37688,
#37689,#37690,#37691,#37692,#37693,#37694,#37695,#37696,#37697,#37698,#37699,
#37700,#37701,#37702,#37703,#37704,#37705,#37706,#37707,#37708,#37709,#37710,
#37711,#37712,#37713,#37714,#37715,#37716,#37717,#37718,#37719,#37720,#37721,
#37722,#37723,#37724,#37725,#37726,#37727,#37728,#37729,#37730,#37731,#37732,
#37733,#37734,#37735,#37736,#37737,#37738,#37739,#37740,#37741,#37742,#37743,
#37744,#37745,#37746,#37747,#37748,#37749,#37750,#37751,#37752,#37753,#37754,
#37755,#37756,#37757,#37758,#37759,#37760,#37761,#37762,#37763,#37764,#37765,
#37766,#37767,#37768,#37769,#37770,#37771,#37772,#37773,#37774,#37775,#37776,
#37777,#37778,#37779,#37780,#37781,#37782,#37783,#37784,#37785,#37786,#37787,
#37788,#37789,#37790,#37791,#37792,#37793),.UNSPECIFIED.,.F.,.F.,(4,3,3,
3,3,3,3,3,3,3,3,3,3,3,3,3,3,3,3,3,3,3,3,3,3,3,3,3,3,3,3,3,3,3,3,3,3,3,3,
3,3,3,3,3,3,3,3,3,3,3,3,3,3,3,3,3,3,3,3,3,3,3,3,3,3,3,3,3,3,3,3,3,3,4),
(285.884931476846,285.98094828738,286.077455092432,286.174577660897,286.232533847408,
286.316272559254,286.399908070621,286.48346051402,286.566949949871,286.650403900485,
286.733840394331,286.817277504086,286.900733299004,286.984277791734,287.067866874675,
287.151590142232,287.232269858129,287.316008569975,287.399644081342,287.483196524741,
287.566685960592,287.650139911206,287.733576405052,287.817013514808,287.900469309725,
287.984013802455,288.067602885396,288.151326152954,288.232005868849,288.315744580695,
288.399380092062,288.482932535461,288.566421971312,288.649875921926,288.733312415772,
288.816749525527,288.900205320445,288.983749813175,289.067338896116,289.151062163673,
289.231741879569,289.315480591415,289.399116102782,289.482668546181,289.566157982032,
289.649611932645,289.733048426492,289.816485536247,289.899941331165,289.983485823894,
290.067074906835,290.150798174393,290.231477890289,290.315216602135,290.398852113502,
290.482404556901,290.565893992752,290.649347943366,290.732784437212,290.816221546968,
290.899677341886,290.983221834615,291.066810917556,291.150534185114,291.231213901009,
291.316848773597,291.39970298138,291.482482124273,291.565205016221,291.64789042395,
291.730570621983,291.813248806099,291.895962990363,291.916292881714),
 .UNSPECIFIED.);
#232=B_SPLINE_CURVE_WITH_KNOTS('',3,(#37794,#37795,#37796,#37797,#37798,
#37799,#37800,#37801,#37802,#37803),.UNSPECIFIED.,.F.,.F.,(4,3,3,4),(285.634069424409,
285.717661682716,285.801296579684,285.884931476652),.UNSPECIFIED.);
#233=B_SPLINE_CURVE_WITH_KNOTS('',3,(#37805,#37806,#37807,#37808,#37809,
#37810,#37811,#37812,#37813,#37814),.UNSPECIFIED.,.F.,.F.,(4,3,3,4),(285.63436337626,
285.731577997215,285.828008467893,285.884931476463),.UNSPECIFIED.);
#234=B_SPLINE_CURVE_WITH_KNOTS('',3,(#37815,#37816,#37817,#37818,#37819,
#37820,#37821,#37822,#37823,#37824,#37825,#37826,#37827,#37828,#37829,#37830,
#37831,#37832,#37833,#37834,#37835,#37836,#37837,#37838,#37839,#37840,#37841,
#37842,#37843,#37844,#37845,#37846,#37847,#37848,#37849,#37850,#37851,#37852,
#37853,#37854,#37855,#37856,#37857,#37858,#37859,#37860,#37861,#37862,#37863,
#37864,#37865,#37866,#37867,#37868,#37869,#37870,#37871,#37872,#37873,#37874,
#37875,#37876,#37877,#37878,#37879,#37880,#37881,#37882,#37883,#37884,#37885,
#37886,#37887,#37888,#37889,#37890,#37891,#37892,#37893,#37894,#37895,#37896,
#37897,#37898,#37899,#37900,#37901,#37902,#37903,#37904,#37905,#37906,#37907,
#37908,#37909,#37910,#37911,#37912,#37913,#37914,#37915,#37916,#37917,#37918,
#37919,#37920,#37921,#37922,#37923,#37924,#37925,#37926,#37927,#37928,#37929,
#37930,#37931,#37932,#37933,#37934,#37935,#37936,#37937,#37938,#37939,#37940,
#37941,#37942,#37943,#37944,#37945,#37946,#37947,#37948,#37949,#37950,#37951,
#37952,#37953,#37954,#37955,#37956,#37957,#37958,#37959,#37960,#37961,#37962,
#37963,#37964,#37965,#37966,#37967,#37968,#37969,#37970,#37971,#37972,#37973,
#37974,#37975,#37976,#37977,#37978,#37979,#37980,#37981,#37982,#37983,#37984,
#37985,#37986,#37987,#37988,#37989,#37990,#37991,#37992,#37993,#37994,#37995,
#37996,#37997,#37998,#37999,#38000,#38001,#38002,#38003,#38004,#38005,#38006,
#38007,#38008,#38009,#38010,#38011,#38012,#38013,#38014,#38015,#38016,#38017,
#38018,#38019,#38020,#38021,#38022,#38023,#38024,#38025,#38026,#38027,#38028,
#38029,#38030,#38031,#38032,#38033,#38034),.UNSPECIFIED.,.F.,.F.,(4,3,3,
3,3,3,3,3,3,3,3,3,3,3,3,3,3,3,3,3,3,3,3,3,3,3,3,3,3,3,3,3,3,3,3,3,3,3,3,
3,3,3,3,3,3,3,3,3,3,3,3,3,3,3,3,3,3,3,3,3,3,3,3,3,3,3,3,3,3,3,3,3,3,4),
(285.884931476655,285.968441827263,286.051942674745,286.135451936067,286.218987529848,
286.302621397412,286.386306242386,286.470130331817,286.542824467124,286.62656317897,
286.710198690337,286.793751133736,286.877240569587,286.9606945202,287.044131014047,
287.127568123802,287.21102391872,287.29456841145,287.378157494391,287.461880761948,
287.542560477844,287.62629918969,287.709934701057,287.793487144456,287.876976580307,
287.960430530921,288.043867024767,288.127304134522,288.21075992944,288.294304422169,
288.37789350511,288.461616772668,288.542296488564,288.62603520041,288.709670711777,
288.793223155176,288.876712591027,288.96016654164,289.043603035487,289.127040145242,
289.21049594016,289.29404043289,289.377629515831,289.461352783388,289.542032499284,
289.62577121113,289.709406722497,289.792959165896,289.876448601746,289.95990255236,
290.043339046206,290.126776155962,290.21023195088,290.29377644361,290.377365526551,
290.461088794108,290.541768510004,290.62550722185,290.709142733218,290.792695176616,
290.876184612467,290.95963856308,291.043075056927,291.126512166682,291.2099679616,
291.29351245433,291.37710153727,291.460824804828,291.541504520724,291.625927635,
291.710207808076,291.794405436709,291.878522273998,291.917378633395),
 .UNSPECIFIED.);
#235=B_SPLINE_CURVE_WITH_KNOTS('',3,(#38040,#38041,#38042,#38043,#38044,
#38045,#38046,#38047,#38048,#38049,#38050,#38051,#38052,#38053,#38054,#38055,
#38056,#38057,#38058,#38059,#38060,#38061,#38062,#38063,#38064,#38065,#38066,
#38067,#38068,#38069,#38070,#38071,#38072,#38073,#38074,#38075,#38076,#38077,
#38078,#38079,#38080,#38081,#38082,#38083,#38084,#38085,#38086,#38087,#38088,
#38089,#38090,#38091,#38092,#38093,#38094,#38095,#38096,#38097,#38098,#38099,
#38100,#38101,#38102,#38103,#38104,#38105,#38106,#38107,#38108,#38109,#38110,
#38111,#38112,#38113,#38114,#38115,#38116,#38117,#38118,#38119,#38120,#38121,
#38122,#38123,#38124,#38125,#38126,#38127,#38128,#38129,#38130,#38131,#38132,
#38133,#38134,#38135,#38136,#38137,#38138,#38139,#38140,#38141,#38142,#38143,
#38144,#38145,#38146,#38147,#38148,#38149,#38150,#38151,#38152,#38153,#38154,
#38155,#38156,#38157,#38158,#38159,#38160,#38161,#38162,#38163,#38164,#38165,
#38166,#38167,#38168,#38169,#38170,#38171,#38172,#38173,#38174,#38175,#38176,
#38177,#38178,#38179,#38180,#38181,#38182,#38183,#38184,#38185,#38186,#38187,
#38188,#38189,#38190,#38191,#38192,#38193,#38194,#38195,#38196,#38197,#38198,
#38199,#38200,#38201,#38202,#38203,#38204,#38205,#38206,#38207,#38208,#38209,
#38210,#38211,#38212,#38213,#38214,#38215,#38216,#38217,#38218,#38219,#38220,
#38221,#38222,#38223,#38224,#38225,#38226,#38227,#38228,#38229,#38230,#38231,
#38232,#38233,#38234,#38235,#38236,#38237,#38238,#38239,#38240,#38241,#38242,
#38243,#38244,#38245,#38246,#38247,#38248,#38249,#38250,#38251,#38252,#38253,
#38254,#38255,#38256,#38257,#38258,#38259),.UNSPECIFIED.,.F.,.F.,(4,3,3,
3,3,3,3,3,3,3,3,3,3,3,3,3,3,3,3,3,3,3,3,3,3,3,3,3,3,3,3,3,3,3,3,3,3,3,3,
3,3,3,3,3,3,3,3,3,3,3,3,3,3,3,3,3,3,3,3,3,3,3,3,3,3,3,3,3,3,3,3,3,3,4),
(292.168116783831,292.230949911729,292.314688623575,292.398324134942,292.481876578341,
292.565366014192,292.648819964806,292.732256458652,292.815693568407,292.899149363325,
292.982693856055,293.066282938996,293.150006206554,293.230685922449,293.314424634295,
293.398060145663,293.481612589061,293.565102024912,293.648555975526,293.731992469372,
293.815429579128,293.898885374045,293.982429866775,294.066018949716,294.149742217274,
294.23042193317,294.314160645016,294.397796156383,294.481348599782,294.564838035633,
294.648291986247,294.731728480093,294.815165589849,294.898621384766,294.982165877496,
295.065754960437,295.149478227995,295.23015794389,295.313896655736,295.397532167103,
295.481084610502,295.564574046353,295.648027996967,295.731464490813,295.814901600568,
295.898357395486,295.981901888216,296.065490971157,296.149214238714,296.22989395461,
296.313632666456,296.397268177823,296.480820621222,296.564310057073,296.647764007687,
296.731200501533,296.814637611289,296.898093406206,296.981637898936,297.065226981877,
297.148950249435,297.22962996533,297.313370336896,297.397007121582,297.480560453526,
297.564050394389,297.647502886383,297.730937375339,297.814371933571,297.897824629494,
297.981358513522,298.06493676202,298.148631676786,298.200069497888),
 .UNSPECIFIED.);
#236=B_SPLINE_CURVE_WITH_KNOTS('',3,(#38260,#38261,#38262,#38263,#38264,
#38265,#38266,#38267,#38268,#38269),.UNSPECIFIED.,.F.,.F.,(4,3,3,4),(291.916292881714,
291.999096197699,292.083606490707,292.168116783716),.UNSPECIFIED.);
#237=B_SPLINE_CURVE_WITH_KNOTS('',3,(#38271,#38272,#38273,#38274,#38275,
#38276,#38277,#38278,#38279,#38280),.UNSPECIFIED.,.F.,.F.,(4,3,3,4),(291.917378633395,
292.001424477781,292.085458033319,292.168116783835),.UNSPECIFIED.);
#238=B_SPLINE_CURVE_WITH_KNOTS('',3,(#38281,#38282,#38283,#38284,#38285,
#38286,#38287,#38288,#38289,#38290,#38291,#38292,#38293,#38294,#38295,#38296,
#38297,#38298,#38299,#38300,#38301,#38302,#38303,#38304,#38305,#38306,#38307,
#38308,#38309,#38310,#38311,#38312,#38313,#38314,#38315,#38316,#38317,#38318,
#38319,#38320,#38321,#38322,#38323,#38324,#38325,#38326,#38327,#38328,#38329,
#38330,#38331,#38332,#38333,#38334,#38335,#38336,#38337,#38338,#38339,#38340,
#38341,#38342,#38343,#38344,#38345,#38346,#38347,#38348,#38349,#38350,#38351,
#38352,#38353,#38354,#38355,#38356,#38357,#38358,#38359,#38360,#38361,#38362,
#38363,#38364,#38365,#38366,#38367,#38368,#38369,#38370,#38371,#38372,#38373,
#38374,#38375,#38376,#38377,#38378,#38379,#38380,#38381,#38382,#38383,#38384,
#38385,#38386,#38387,#38388,#38389,#38390,#38391,#38392,#38393,#38394,#38395,
#38396,#38397,#38398,#38399,#38400,#38401,#38402,#38403,#38404,#38405,#38406,
#38407,#38408,#38409,#38410,#38411,#38412,#38413,#38414,#38415,#38416,#38417,
#38418,#38419,#38420,#38421,#38422,#38423,#38424,#38425,#38426,#38427,#38428,
#38429,#38430,#38431,#38432,#38433,#38434,#38435,#38436,#38437,#38438,#38439,
#38440,#38441,#38442,#38443,#38444,#38445,#38446,#38447,#38448,#38449,#38450,
#38451,#38452,#38453,#38454,#38455,#38456,#38457,#38458,#38459,#38460,#38461,
#38462,#38463,#38464,#38465,#38466,#38467,#38468,#38469,#38470,#38471,#38472,
#38473,#38474,#38475,#38476,#38477,#38478,#38479,#38480,#38481,#38482,#38483,
#38484,#38485,#38486,#38487,#38488,#38489,#38490,#38491,#38492,#38493,#38494,
#38495,#38496,#38497),.UNSPECIFIED.,.F.,.F.,(4,3,3,3,3,3,3,3,3,3,3,3,3,
3,3,3,3,3,3,3,3,3,3,3,3,3,3,3,3,3,3,3,3,3,3,3,3,3,3,3,3,3,3,3,3,3,3,3,3,
3,3,3,3,3,3,3,3,3,3,3,3,3,3,3,3,3,3,3,3,3,3,3,4),(292.168116784033,292.262190609695,
292.356632402376,292.451597059885,292.541240531445,292.624979243291,292.708614754658,
292.792167198057,292.875656633908,292.959110584522,293.042547078368,293.125984188123,
293.209439983041,293.292984475771,293.376573558712,293.460296826269,293.540976542165,
293.624715254011,293.708350765378,293.791903208777,293.875392644628,293.958846595242,
294.042283089088,294.125720198843,294.209175993761,294.292720486491,294.376309569432,
294.460032836989,294.540712552885,294.624451264731,294.708086776098,294.791639219497,
294.875128655348,294.958582605961,295.042019099808,295.125456209563,295.208912004481,
295.29245649721,295.376045580151,295.459768847709,295.540448563605,295.624187275451,
295.707822786818,295.791375230217,295.874864666068,295.958318616682,296.041755110528,
296.125192220283,296.208648015201,296.292192507931,296.375781590872,296.459504858429,
296.540184574325,296.623923286171,296.707558797538,296.791111240937,296.874600676788,
296.958054627402,297.041491121248,297.124928231003,297.208384025921,297.291928518651,
297.375517601592,297.459240869149,297.539920585045,297.622665935703,297.70531674218,
297.787892033416,297.870410771497,297.952903044171,298.035376688061,298.117882955238,
298.199464534781),.UNSPECIFIED.);
#239=B_SPLINE_CURVE_WITH_KNOTS('',3,(#38503,#38504,#38505,#38506,#38507,
#38508,#38509,#38510,#38511,#38512,#38513,#38514,#38515,#38516,#38517,#38518,
#38519,#38520,#38521,#38522,#38523,#38524,#38525,#38526,#38527,#38528,#38529,
#38530,#38531,#38532,#38533,#38534,#38535,#38536,#38537,#38538,#38539,#38540,
#38541,#38542,#38543,#38544,#38545,#38546,#38547,#38548,#38549,#38550,#38551,
#38552,#38553,#38554,#38555,#38556,#38557,#38558,#38559,#38560,#38561,#38562,
#38563,#38564,#38565,#38566,#38567,#38568,#38569,#38570,#38571,#38572,#38573,
#38574,#38575,#38576,#38577,#38578,#38579,#38580,#38581,#38582,#38583,#38584,
#38585,#38586,#38587,#38588,#38589,#38590,#38591,#38592,#38593,#38594,#38595,
#38596,#38597,#38598,#38599,#38600,#38601,#38602,#38603,#38604,#38605,#38606,
#38607,#38608,#38609,#38610,#38611,#38612,#38613,#38614,#38615,#38616,#38617,
#38618,#38619,#38620,#38621,#38622,#38623,#38624,#38625,#38626,#38627,#38628,
#38629,#38630,#38631,#38632,#38633,#38634,#38635,#38636,#38637,#38638,#38639,
#38640,#38641,#38642,#38643,#38644,#38645,#38646,#38647,#38648,#38649,#38650,
#38651,#38652,#38653,#38654,#38655,#38656,#38657,#38658,#38659,#38660,#38661,
#38662,#38663,#38664,#38665,#38666,#38667,#38668,#38669,#38670,#38671,#38672,
#38673,#38674,#38675,#38676,#38677,#38678,#38679,#38680,#38681,#38682,#38683,
#38684,#38685,#38686,#38687,#38688,#38689,#38690,#38691,#38692,#38693,#38694,
#38695,#38696,#38697,#38698,#38699,#38700,#38701,#38702,#38703,#38704,#38705,
#38706,#38707,#38708,#38709,#38710,#38711,#38712,#38713,#38714,#38715,#38716,
#38717,#38718,#38719,#38720,#38721,#38722),.UNSPECIFIED.,.F.,.F.,(4,3,3,
3,3,3,3,3,3,3,3,3,3,3,3,3,3,3,3,3,3,3,3,3,3,3,3,3,3,3,3,3,3,3,3,3,3,3,3,
3,3,3,3,3,3,3,3,3,3,3,3,3,3,3,3,3,3,3,3,3,3,3,3,3,3,3,3,3,3,3,3,3,3,4),
(298.451302091141,298.533733738966,298.616103034285,298.698438526061,298.780758933961,
298.863083218192,298.945430339711,299.027864932082,299.110349533729,299.192953273766,
299.22910198677,299.312840698616,299.396476209983,299.480028653382,299.563518089232,
299.646972039846,299.730408533692,299.813845643448,299.897301438365,299.980845931095,
300.064435014036,300.148158281593,300.22883799749,300.312576709336,300.396212220703,
300.479764664102,300.563254099953,300.646708050567,300.730144544413,300.813581654168,
300.897037449086,300.980581941816,301.064171024757,301.147894292314,301.22857400821,
301.312312720056,301.395948231423,301.479500674822,301.562990110673,301.646444061287,
301.729880555133,301.813317664889,301.896773459806,301.980317952536,302.063907035477,
302.147630303035,302.228310018931,302.312048730777,302.395684242145,302.479236685543,
302.562726121394,302.646180072008,302.729616565854,302.81305367561,302.896509470527,
302.980053963257,303.063643046198,303.147366313756,303.228046029651,303.311784741497,
303.395420252864,303.478972696263,303.562462132114,303.645916082727,303.729352576573,
303.812789686329,303.896245481247,303.979789973976,304.063379056917,304.147102324475,
304.227782040371,304.315571556541,304.40316930023,304.48414926919),
 .UNSPECIFIED.);
#240=B_SPLINE_CURVE_WITH_KNOTS('',3,(#38723,#38724,#38725,#38726,#38727,
#38728,#38729,#38730,#38731,#38732),.UNSPECIFIED.,.F.,.F.,(4,3,3,4),(298.200069497888,
298.22936597605,298.343682204307,298.451302091011),.UNSPECIFIED.);
#241=B_SPLINE_CURVE_WITH_KNOTS('',3,(#38734,#38735,#38736,#38737,#38738,
#38739,#38740,#38741,#38742,#38743),.UNSPECIFIED.,.F.,.F.,(4,3,3,4),(298.199464534781,
298.28204843746,298.36667526417,298.45130209088),.UNSPECIFIED.);
#242=B_SPLINE_CURVE_WITH_KNOTS('',3,(#38744,#38745,#38746,#38747,#38748,
#38749,#38750,#38751,#38752,#38753,#38754,#38755,#38756,#38757,#38758,#38759,
#38760,#38761,#38762,#38763,#38764,#38765,#38766,#38767,#38768,#38769,#38770,
#38771,#38772,#38773,#38774,#38775,#38776,#38777,#38778,#38779,#38780,#38781,
#38782,#38783,#38784,#38785,#38786,#38787,#38788,#38789,#38790,#38791,#38792,
#38793,#38794,#38795,#38796,#38797,#38798,#38799,#38800,#38801,#38802,#38803,
#38804,#38805,#38806,#38807,#38808,#38809,#38810,#38811,#38812,#38813,#38814,
#38815,#38816,#38817,#38818,#38819,#38820,#38821,#38822,#38823,#38824,#38825,
#38826,#38827,#38828,#38829,#38830,#38831,#38832,#38833,#38834,#38835,#38836,
#38837,#38838,#38839,#38840,#38841,#38842,#38843,#38844,#38845,#38846,#38847,
#38848,#38849,#38850,#38851,#38852,#38853,#38854,#38855,#38856,#38857,#38858,
#38859,#38860,#38861,#38862,#38863,#38864,#38865,#38866,#38867,#38868,#38869,
#38870,#38871,#38872,#38873,#38874,#38875,#38876,#38877,#38878,#38879,#38880,
#38881,#38882,#38883,#38884,#38885,#38886,#38887,#38888,#38889,#38890,#38891,
#38892,#38893,#38894,#38895,#38896,#38897,#38898,#38899,#38900,#38901,#38902,
#38903,#38904,#38905,#38906,#38907,#38908,#38909,#38910,#38911,#38912,#38913,
#38914,#38915,#38916,#38917,#38918,#38919,#38920,#38921,#38922,#38923,#38924,
#38925,#38926,#38927,#38928,#38929,#38930,#38931,#38932,#38933,#38934,#38935,
#38936,#38937,#38938,#38939,#38940,#38941,#38942,#38943,#38944,#38945,#38946,
#38947,#38948,#38949,#38950,#38951,#38952,#38953,#38954,#38955,#38956,#38957,
#38958,#38959,#38960,#38961,#38962,#38963),.UNSPECIFIED.,.F.,.F.,(4,3,3,
3,3,3,3,3,3,3,3,3,3,3,3,3,3,3,3,3,3,3,3,3,3,3,3,3,3,3,3,3,3,3,3,3,3,3,3,
3,3,3,3,3,3,3,3,3,3,3,3,3,3,3,3,3,3,3,3,3,3,3,3,3,3,3,3,3,3,3,3,3,3,4),
(298.451302091015,298.539656595765,298.623395307611,298.707030818978,298.790583262377,
298.874072698228,298.957526648842,299.040963142688,299.124400252444,299.207856047361,
299.291400540091,299.374989623032,299.45871289059,299.539392606485,299.623131318331,
299.706766829699,299.790319273097,299.873808708948,299.957262659562,300.040699153408,
300.124136263164,300.207592058082,300.291136550811,300.374725633752,300.45844890131,
300.539128617206,300.622867329052,300.706502840419,300.790055283818,300.873544719669,
300.956998670283,301.040435164129,301.123872273884,301.207328068802,301.290872561532,
301.374461644473,301.458184912031,301.538864627926,301.622603339772,301.706238851139,
301.789791294538,301.873280730389,301.956734681003,302.040171174849,302.123608284604,
302.207064079522,302.290608572252,302.374197655193,302.45792092275,302.538600638646,
302.622339350492,302.70597486186,302.789527305258,302.873016741109,302.956470691723,
303.039907185569,303.123344295325,303.206800090242,303.290344582972,303.373933665913,
303.45765693347,303.538336649366,303.622078505112,303.705716435735,303.789270576816,
303.876003420953,303.959453706735,304.042886213594,304.12631901319,304.209770173324,
304.293296686938,304.376867998284,304.460541428353,304.483133329908),
 .UNSPECIFIED.);
#243=B_SPLINE_CURVE_WITH_KNOTS('',3,(#38969,#38970,#38971,#38972,#38973,
#38974,#38975,#38976,#38977,#38978,#38979,#38980,#38981,#38982,#38983,#38984,
#38985,#38986,#38987,#38988,#38989,#38990,#38991,#38992,#38993,#38994,#38995,
#38996,#38997,#38998,#38999,#39000,#39001,#39002,#39003,#39004,#39005,#39006,
#39007,#39008,#39009,#39010,#39011,#39012,#39013,#39014,#39015,#39016,#39017,
#39018,#39019,#39020,#39021,#39022,#39023,#39024,#39025,#39026,#39027,#39028,
#39029,#39030,#39031,#39032,#39033,#39034,#39035,#39036,#39037,#39038,#39039,
#39040,#39041,#39042,#39043,#39044,#39045,#39046,#39047,#39048,#39049,#39050,
#39051,#39052,#39053,#39054,#39055,#39056,#39057,#39058,#39059,#39060,#39061,
#39062,#39063,#39064,#39065,#39066,#39067,#39068,#39069,#39070,#39071,#39072,
#39073,#39074,#39075,#39076,#39077,#39078,#39079,#39080,#39081,#39082,#39083,
#39084,#39085,#39086,#39087,#39088,#39089,#39090,#39091,#39092,#39093,#39094,
#39095,#39096,#39097,#39098,#39099,#39100,#39101,#39102,#39103,#39104,#39105,
#39106,#39107,#39108,#39109,#39110,#39111,#39112,#39113,#39114,#39115,#39116,
#39117,#39118,#39119,#39120,#39121,#39122,#39123,#39124,#39125,#39126,#39127,
#39128,#39129,#39130,#39131,#39132,#39133,#39134,#39135,#39136,#39137,#39138,
#39139,#39140,#39141,#39142,#39143,#39144,#39145,#39146,#39147,#39148,#39149,
#39150,#39151,#39152,#39153,#39154,#39155,#39156,#39157,#39158,#39159,#39160,
#39161,#39162,#39163,#39164,#39165,#39166,#39167,#39168,#39169,#39170,#39171,
#39172,#39173,#39174,#39175,#39176,#39177,#39178,#39179,#39180,#39181,#39182,
#39183,#39184,#39185,#39186,#39187,#39188),.UNSPECIFIED.,.F.,.F.,(4,3,3,
3,3,3,3,3,3,3,3,3,3,3,3,3,3,3,3,3,3,3,3,3,3,3,3,3,3,3,3,3,3,3,3,3,3,3,3,
3,3,3,3,3,3,3,3,3,3,3,3,3,3,3,3,3,3,3,3,3,3,3,3,3,3,3,3,3,3,3,3,3,3,4),
(304.734487398294,304.822143358111,304.90992380932,304.997920322264,305.086032057283,
305.174346980483,305.227518051091,305.311256762937,305.394892274304,305.478444717703,
305.561934153554,305.645388104167,305.728824598013,305.812261707769,305.895717502687,
305.979261995416,306.062851078357,306.146574345915,306.227254061811,306.310992773657,
306.394628285024,306.478180728423,306.561670164274,306.645124114888,306.728560608734,
306.811997718489,306.895453513407,306.978998006137,307.062587089078,307.146310356635,
307.226990072531,307.310728784377,307.394364295744,307.477916739143,307.561406174994,
307.644860125607,307.728296619454,307.811733729209,307.895189524127,307.978734016856,
308.062323099797,308.146046367355,308.226726083251,308.310464795097,308.394100306465,
308.477652749863,308.561142185714,308.644596136328,308.728032630174,308.81146973993,
308.894925534847,308.978470027577,309.062059110518,309.145782378076,309.226462093971,
309.310200805817,309.393836317185,309.477388760583,309.560878196434,309.644332147048,
309.727768640895,309.81120575065,309.894661545568,309.978206038298,310.061795121239,
310.145518388796,310.226198104692,310.308739724589,310.391184948521,310.473552960617,
310.555860021654,310.638131369339,310.720397187219,310.766118518563),
 .UNSPECIFIED.);
#244=B_SPLINE_CURVE_WITH_KNOTS('',3,(#39189,#39190,#39191,#39192,#39193,
#39194,#39195,#39196,#39197,#39198),.UNSPECIFIED.,.F.,.F.,(4,3,3,4),(304.48414926919,
304.571492717686,304.658685916941,304.73448739819),.UNSPECIFIED.);
#245=B_SPLINE_CURVE_WITH_KNOTS('',3,(#39200,#39201,#39202,#39203,#39204,
#39205,#39206,#39207,#39208,#39209),.UNSPECIFIED.,.F.,.F.,(4,3,3,4),(304.483133329908,
304.538072660086,304.659392772604,304.734487398194),.UNSPECIFIED.);
#246=B_SPLINE_CURVE_WITH_KNOTS('',3,(#39210,#39211,#39212,#39213,#39214,
#39215,#39216,#39217,#39218,#39219,#39220,#39221,#39222,#39223,#39224,#39225,
#39226,#39227,#39228,#39229,#39230,#39231,#39232,#39233,#39234,#39235,#39236,
#39237,#39238,#39239,#39240,#39241,#39242,#39243,#39244,#39245,#39246,#39247,
#39248,#39249,#39250,#39251,#39252,#39253,#39254,#39255,#39256,#39257,#39258,
#39259,#39260,#39261,#39262,#39263,#39264,#39265,#39266,#39267,#39268,#39269,
#39270,#39271,#39272,#39273,#39274,#39275,#39276,#39277,#39278,#39279,#39280,
#39281,#39282,#39283,#39284,#39285,#39286,#39287,#39288,#39289,#39290,#39291,
#39292,#39293,#39294,#39295,#39296,#39297,#39298,#39299,#39300,#39301,#39302,
#39303,#39304,#39305,#39306,#39307,#39308,#39309,#39310,#39311,#39312,#39313,
#39314,#39315,#39316,#39317,#39318,#39319,#39320,#39321,#39322,#39323,#39324,
#39325,#39326,#39327,#39328,#39329,#39330,#39331,#39332,#39333,#39334,#39335,
#39336,#39337,#39338,#39339,#39340,#39341,#39342,#39343,#39344,#39345,#39346,
#39347,#39348,#39349,#39350,#39351,#39352,#39353,#39354,#39355,#39356,#39357,
#39358,#39359,#39360,#39361,#39362,#39363,#39364,#39365,#39366,#39367,#39368,
#39369,#39370,#39371,#39372,#39373,#39374,#39375,#39376,#39377,#39378,#39379,
#39380,#39381,#39382,#39383,#39384,#39385,#39386,#39387,#39388,#39389,#39390,
#39391,#39392,#39393,#39394,#39395,#39396,#39397,#39398,#39399,#39400,#39401,
#39402,#39403,#39404,#39405,#39406,#39407,#39408,#39409,#39410,#39411,#39412,
#39413,#39414,#39415,#39416,#39417,#39418,#39419,#39420,#39421,#39422,#39423,
#39424,#39425,#39426,#39427,#39428,#39429),.UNSPECIFIED.,.F.,.F.,(4,3,3,
3,3,3,3,3,3,3,3,3,3,3,3,3,3,3,3,3,3,3,3,3,3,3,3,3,3,3,3,3,3,3,3,3,3,3,3,
3,3,3,3,3,3,3,3,3,3,3,3,3,3,3,3,3,3,3,3,3,3,3,3,3,3,3,3,3,3,3,3,3,3,4),
(304.734487398304,304.816859499383,304.89916160694,304.98141989639,305.063656315399,
305.145889882814,305.228139612957,305.310473034548,305.392850573995,305.475353902802,
305.537808670806,305.621547382652,305.705182894019,305.788735337418,305.872224773269,
305.955678723882,306.039115217729,306.122552327484,306.206008122402,306.289552615131,
306.373141698072,306.45686496563,306.537544681526,306.621283393372,306.70491890474,
306.788471348138,306.871960783989,306.955414734603,307.038851228449,307.122288338205,
307.205744133122,307.289288625852,307.372877708793,307.45660097635,307.537280692246,
307.621019404092,307.70465491546,307.788207358858,307.871696794709,307.955150745323,
308.038587239169,308.122024348925,308.205480143842,308.289024636572,308.372613719513,
308.456336987071,308.537016702967,308.620755414813,308.70439092618,308.787943369579,
308.871432805429,308.954886756043,309.03832324989,309.121760359645,309.205216154563,
309.288760647293,309.372349730234,309.456072997791,309.536752713687,309.620491425533,
309.7041269369,309.787679380299,309.87116881615,309.954622766763,310.03805926061,
310.121496370365,310.204952165282,310.288496658012,310.372085740952,310.45580900851,
310.536488724407,310.625321699943,310.713947049508,310.767364380203),
 .UNSPECIFIED.);
#247=B_SPLINE_CURVE_WITH_KNOTS('',3,(#39435,#39436,#39437,#39438,#39439,
#39440,#39441,#39442,#39443,#39444,#39445,#39446,#39447,#39448,#39449,#39450,
#39451,#39452,#39453,#39454,#39455,#39456,#39457,#39458,#39459,#39460,#39461,
#39462,#39463,#39464,#39465,#39466,#39467,#39468,#39469,#39470,#39471,#39472,
#39473,#39474,#39475,#39476,#39477,#39478,#39479,#39480,#39481,#39482,#39483,
#39484,#39485,#39486,#39487,#39488,#39489,#39490,#39491,#39492,#39493,#39494,
#39495,#39496,#39497,#39498,#39499,#39500,#39501,#39502,#39503,#39504,#39505,
#39506,#39507,#39508,#39509,#39510,#39511,#39512,#39513,#39514,#39515,#39516,
#39517,#39518,#39519,#39520,#39521,#39522,#39523,#39524,#39525,#39526,#39527,
#39528,#39529,#39530,#39531,#39532,#39533,#39534,#39535,#39536,#39537,#39538,
#39539,#39540,#39541,#39542,#39543,#39544,#39545,#39546,#39547,#39548,#39549,
#39550,#39551,#39552,#39553,#39554,#39555,#39556,#39557,#39558,#39559,#39560,
#39561,#39562,#39563,#39564,#39565,#39566,#39567,#39568,#39569,#39570,#39571,
#39572,#39573,#39574,#39575,#39576,#39577,#39578,#39579,#39580,#39581,#39582,
#39583,#39584,#39585,#39586,#39587,#39588,#39589,#39590,#39591,#39592,#39593,
#39594,#39595,#39596,#39597,#39598,#39599,#39600,#39601,#39602,#39603,#39604,
#39605,#39606,#39607,#39608,#39609,#39610,#39611,#39612,#39613,#39614,#39615,
#39616,#39617,#39618,#39619,#39620,#39621,#39622,#39623,#39624,#39625,#39626,
#39627,#39628,#39629,#39630,#39631,#39632,#39633,#39634,#39635,#39636,#39637,
#39638,#39639,#39640,#39641,#39642,#39643,#39644,#39645,#39646,#39647,#39648,
#39649,#39650,#39651),.UNSPECIFIED.,.F.,.F.,(4,3,3,3,3,3,3,3,3,3,3,3,3,
3,3,3,3,3,3,3,3,3,3,3,3,3,3,3,3,3,3,3,3,3,3,3,3,3,3,3,3,3,3,3,3,3,3,3,3,
3,3,3,3,3,3,3,3,3,3,3,3,3,3,3,3,3,3,3,3,3,3,3,4),(311.01767270537,311.135474503209,
311.225934115412,311.309672827258,311.393308338626,311.476860782024,311.560350217875,
311.643804168489,311.727240662335,311.810677772091,311.894133567009,311.977678059738,
312.061267142679,312.144990410237,312.225670126132,312.309408837978,312.393044349345,
312.476596792744,312.560086228595,312.643540179209,312.726976673055,312.81041378281,
312.893869577728,312.977414070458,313.061003153399,313.144726420956,313.225406136852,
313.309144848698,313.392780360065,313.476332803464,313.559822239315,313.643276189928,
313.726712683775,313.81014979353,313.893605588448,313.977150081177,314.060739164118,
314.144462431676,314.225142147572,314.308880859418,314.392516370785,314.476068814184,
314.559558250035,314.643012200649,314.726448694495,314.809885804251,314.893341599168,
314.976886091898,315.060475174839,315.144198442397,315.224878158292,315.308616870138,
315.392252381505,315.475804824904,315.559294260755,315.642748211369,315.726184705215,
315.80962181497,315.893077609888,315.976622102618,316.060211185559,316.143934453116,
316.224614169012,316.308363373317,316.392007066586,316.475550342438,316.5590366819,
316.642484204386,316.725910999349,316.809363362124,316.892826545189,316.97636417955,
317.049206352649),.UNSPECIFIED.);
#248=B_SPLINE_CURVE_WITH_KNOTS('',3,(#39652,#39653,#39654,#39655,#39656,
#39657,#39658,#39659,#39660,#39661),.UNSPECIFIED.,.F.,.F.,(4,3,3,4),(310.766118518563,
310.848416982258,310.933044843739,311.017672705221),.UNSPECIFIED.);
#249=B_SPLINE_CURVE_WITH_KNOTS('',3,(#39663,#39664,#39665,#39666,#39667,
#39668,#39669,#39670,#39671,#39672),.UNSPECIFIED.,.F.,.F.,(4,3,3,4),(310.767364380203,
310.855720839339,310.943880183788,311.017672705217),.UNSPECIFIED.);
#250=B_SPLINE_CURVE_WITH_KNOTS('',3,(#39673,#39674,#39675,#39676,#39677,
#39678,#39679,#39680,#39681,#39682,#39683,#39684,#39685,#39686,#39687,#39688,
#39689,#39690,#39691,#39692,#39693,#39694,#39695,#39696,#39697,#39698,#39699,
#39700,#39701,#39702,#39703,#39704,#39705,#39706,#39707,#39708,#39709,#39710,
#39711,#39712,#39713,#39714,#39715,#39716,#39717,#39718,#39719,#39720,#39721,
#39722,#39723,#39724,#39725,#39726,#39727,#39728,#39729,#39730,#39731,#39732,
#39733,#39734,#39735,#39736,#39737,#39738,#39739,#39740,#39741,#39742,#39743,
#39744,#39745,#39746,#39747,#39748,#39749,#39750,#39751,#39752,#39753,#39754,
#39755,#39756,#39757,#39758,#39759,#39760,#39761,#39762,#39763,#39764,#39765,
#39766,#39767,#39768,#39769,#39770,#39771,#39772,#39773,#39774,#39775,#39776,
#39777,#39778,#39779,#39780,#39781,#39782,#39783,#39784,#39785,#39786,#39787,
#39788,#39789,#39790,#39791,#39792,#39793,#39794,#39795,#39796,#39797,#39798,
#39799,#39800,#39801,#39802,#39803,#39804,#39805,#39806,#39807,#39808,#39809,
#39810,#39811,#39812,#39813,#39814,#39815,#39816,#39817,#39818,#39819,#39820,
#39821,#39822,#39823,#39824,#39825,#39826,#39827,#39828,#39829,#39830,#39831,
#39832,#39833,#39834,#39835,#39836,#39837,#39838,#39839,#39840,#39841,#39842,
#39843,#39844,#39845,#39846,#39847,#39848,#39849,#39850,#39851,#39852,#39853,
#39854,#39855,#39856,#39857,#39858,#39859,#39860,#39861,#39862,#39863,#39864,
#39865,#39866,#39867,#39868,#39869,#39870,#39871,#39872,#39873,#39874,#39875,
#39876,#39877,#39878,#39879,#39880,#39881,#39882,#39883,#39884,#39885,#39886,
#39887,#39888,#39889,#39890,#39891,#39892),.UNSPECIFIED.,.F.,.F.,(4,3,3,
3,3,3,3,3,3,3,3,3,3,3,3,3,3,3,3,3,3,3,3,3,3,3,3,3,3,3,3,3,3,3,3,3,3,3,3,
3,3,3,3,3,3,3,3,3,3,3,3,3,3,3,3,3,3,3,3,3,3,3,3,3,3,3,3,3,3,3,3,3,3,4),
(311.017672705374,311.104429954621,311.191279156298,311.278312113916,311.365438893343,
311.452762719316,311.536224735127,311.619963446973,311.70359895834,311.787151401739,
311.87064083759,311.954094788204,312.03753128205,312.120968391805,312.204424186723,
312.287968679453,312.371557762394,312.455281029951,312.535960745847,312.619699457693,
312.70333496906,312.786887412459,312.870376848309,312.953830798923,313.037267292769,
313.120704402525,313.204160197442,313.287704690172,313.371293773113,313.45501704067,
313.535696756567,313.619435468413,313.703070979781,313.786623423179,313.87011285903,
313.953566809644,314.03700330349,314.120440413246,314.203896208163,314.287440700893,
314.371029783834,314.454753051392,314.535432767287,314.619171479133,314.702806990501,
314.786359433899,314.869848869751,314.953302820365,315.036739314211,315.120176423966,
315.203632218884,315.287176711614,315.370765794554,315.454489062112,315.535168778008,
315.618907489854,315.702543001222,315.78609544462,315.869584880471,315.953038831085,
316.036475324931,316.119912434686,316.203368229605,316.286912722334,316.370501805276,
316.454225072833,316.534904788728,316.617565724114,316.700129228481,316.782614412715,
316.865035306066,316.947419658952,317.029791475497,317.049417187792),
 .UNSPECIFIED.);
#251=B_SPLINE_CURVE_WITH_KNOTS('',3,(#39898,#39899,#39900,#39901,#39902,
#39903,#39904,#39905,#39906,#39907,#39908,#39909,#39910,#39911,#39912,#39913,
#39914,#39915,#39916,#39917,#39918,#39919,#39920,#39921,#39922,#39923,#39924,
#39925,#39926,#39927,#39928,#39929,#39930,#39931,#39932,#39933,#39934,#39935,
#39936,#39937,#39938,#39939,#39940,#39941,#39942,#39943,#39944,#39945,#39946,
#39947,#39948,#39949,#39950,#39951,#39952,#39953,#39954,#39955,#39956,#39957,
#39958,#39959,#39960,#39961,#39962,#39963,#39964,#39965,#39966,#39967,#39968,
#39969,#39970,#39971,#39972,#39973,#39974,#39975,#39976,#39977,#39978,#39979,
#39980,#39981,#39982,#39983,#39984,#39985,#39986,#39987,#39988,#39989,#39990,
#39991,#39992,#39993,#39994,#39995,#39996,#39997,#39998,#39999,#40000,#40001,
#40002,#40003,#40004,#40005,#40006,#40007,#40008,#40009,#40010,#40011,#40012,
#40013,#40014,#40015,#40016,#40017,#40018,#40019,#40020,#40021,#40022,#40023,
#40024,#40025,#40026,#40027,#40028,#40029,#40030,#40031,#40032,#40033,#40034,
#40035,#40036,#40037,#40038,#40039,#40040,#40041,#40042,#40043,#40044,#40045,
#40046,#40047,#40048,#40049,#40050,#40051,#40052,#40053,#40054,#40055,#40056,
#40057,#40058,#40059,#40060,#40061,#40062,#40063,#40064,#40065,#40066,#40067,
#40068,#40069,#40070,#40071,#40072,#40073,#40074,#40075,#40076,#40077,#40078,
#40079,#40080,#40081,#40082,#40083,#40084,#40085,#40086,#40087,#40088,#40089,
#40090,#40091,#40092,#40093,#40094,#40095,#40096,#40097,#40098,#40099,#40100,
#40101,#40102,#40103,#40104,#40105,#40106,#40107,#40108,#40109,#40110,#40111,
#40112,#40113,#40114,#40115,#40116,#40117,#40118,#40119,#40120),
 .UNSPECIFIED.,.F.,.F.,(4,3,3,3,3,3,3,3,3,3,3,3,3,3,3,3,3,3,3,3,3,3,3,3,
3,3,3,3,3,3,3,3,3,3,3,3,3,3,3,3,3,3,3,3,3,3,3,3,3,3,3,3,3,3,3,3,3,3,3,3,
3,3,3,3,3,3,3,3,3,3,3,3,3,3,4),(317.300858012677,317.383680932198,317.466407303603,
317.549058061659,317.633436577758,317.716008012657,317.798571313966,317.881145280446,
317.966880507947,318.049576946045,318.132329695274,318.215195165216,318.224086190453,
318.307824902299,318.391460413666,318.475012857065,318.558502292916,318.64195624353,
318.725392737376,318.808829847132,318.892285642049,318.975830134779,319.05941921772,
319.143142485278,319.223822201173,319.307560913019,319.391196424386,319.474748867785,
319.558238303635,319.641692254249,319.725128748095,319.808565857851,319.892021652768,
319.975566145498,320.059155228439,320.142878495996,320.223558211893,320.307296923739,
320.390932435106,320.474484878505,320.557974314356,320.64142826497,320.724864758816,
320.808301868572,320.891757663489,320.975302156219,321.05889123916,321.142614506718,
321.223294222613,321.307032934459,321.390668445827,321.474220889225,321.557710325076,
321.64116427569,321.724600769536,321.808037879292,321.89149367421,321.975038166939,
322.05862724988,322.142350517438,322.223030233333,322.306768945179,322.390404456546,
322.473956899945,322.557446335796,322.64090028641,322.724336780256,322.807773890012,
322.891229684929,322.974774177659,323.0583632606,323.142086528158,323.222766244053,
323.318816741582,323.333553374426),.UNSPECIFIED.);
#252=B_SPLINE_CURVE_WITH_KNOTS('',3,(#40121,#40122,#40123,#40124,#40125,
#40126,#40127,#40128,#40129,#40130),.UNSPECIFIED.,.F.,.F.,(4,3,3,4),(317.049206352649,
317.13677826619,317.224350179732,317.300858012549),.UNSPECIFIED.);
#253=B_SPLINE_CURVE_WITH_KNOTS('',3,(#40132,#40133,#40134,#40135,#40136,
#40137,#40138,#40139,#40140,#40141),.UNSPECIFIED.,.F.,.F.,(4,3,3,4),(317.049417187792,
317.131815498541,317.216336755547,317.300858012553),.UNSPECIFIED.);
#254=B_SPLINE_CURVE_WITH_KNOTS('',3,(#40142,#40143,#40144,#40145,#40146,
#40147,#40148,#40149,#40150,#40151,#40152,#40153,#40154,#40155,#40156,#40157,
#40158,#40159,#40160,#40161,#40162,#40163,#40164,#40165,#40166,#40167,#40168,
#40169,#40170,#40171,#40172,#40173,#40174,#40175,#40176,#40177,#40178,#40179,
#40180,#40181,#40182,#40183,#40184,#40185,#40186,#40187,#40188,#40189,#40190,
#40191,#40192,#40193,#40194,#40195,#40196,#40197,#40198,#40199,#40200,#40201,
#40202,#40203,#40204,#40205,#40206,#40207,#40208,#40209,#40210,#40211,#40212,
#40213,#40214,#40215,#40216,#40217,#40218,#40219,#40220,#40221,#40222,#40223,
#40224,#40225,#40226,#40227,#40228,#40229,#40230,#40231,#40232,#40233,#40234,
#40235,#40236,#40237,#40238,#40239,#40240,#40241,#40242,#40243,#40244,#40245,
#40246,#40247,#40248,#40249,#40250,#40251,#40252,#40253,#40254,#40255,#40256,
#40257,#40258,#40259,#40260,#40261,#40262,#40263,#40264,#40265,#40266,#40267,
#40268,#40269,#40270,#40271,#40272,#40273,#40274,#40275,#40276,#40277,#40278,
#40279,#40280,#40281,#40282,#40283,#40284,#40285,#40286,#40287,#40288,#40289,
#40290,#40291,#40292,#40293,#40294,#40295,#40296,#40297,#40298,#40299,#40300,
#40301,#40302,#40303,#40304,#40305,#40306,#40307,#40308,#40309,#40310,#40311,
#40312,#40313,#40314,#40315,#40316,#40317,#40318,#40319,#40320,#40321,#40322,
#40323,#40324,#40325,#40326,#40327,#40328,#40329,#40330,#40331,#40332,#40333,
#40334,#40335,#40336,#40337,#40338,#40339,#40340,#40341,#40342,#40343,#40344,
#40345,#40346,#40347,#40348,#40349,#40350,#40351,#40352,#40353,#40354,#40355,
#40356,#40357,#40358,#40359,#40360,#40361),.UNSPECIFIED.,.F.,.F.,(4,3,3,
3,3,3,3,3,3,3,3,3,3,3,3,3,3,3,3,3,3,3,3,3,3,3,3,3,3,3,3,3,3,3,3,3,3,3,3,
3,3,3,3,3,3,3,3,3,3,3,3,3,3,3,3,3,3,3,3,3,3,3,3,3,3,3,3,3,3,3,3,3,3,4),
(317.300858012747,317.410911531517,317.524033175183,317.534640799448,317.618379511294,
317.702015022661,317.78556746606,317.869056901911,317.952510852525,318.035947346371,
318.119384456126,318.202840251044,318.286384743774,318.369973826715,318.453697094272,
318.534376810168,318.618115522014,318.701751033381,318.78530347678,318.868792912631,
318.952246863245,319.035683357091,319.119120466846,319.202576261764,319.286120754493,
319.369709837434,319.453433104992,319.534112820888,319.617851532734,319.701487044101,
319.7850394875,319.868528923351,319.951982873965,320.035419367811,320.118856477566,
320.202312272484,320.285856765214,320.369445848155,320.453169115712,320.533848831608,
320.617587543454,320.701223054821,320.78477549822,320.868264934071,320.951718884684,
321.035155378531,321.118592488286,321.202048283204,321.285592775933,321.369181858874,
321.452905126432,321.533584842328,321.617323554174,321.700959065542,321.78451150894,
321.868000944791,321.951454895405,322.034891389251,322.118328499007,322.201784293925,
322.285328786654,322.368917869595,322.452641137153,322.533320853048,322.617071701435,
322.700716701817,322.784260452642,322.867746789349,322.951193832203,323.034619671076,
323.118066332219,323.201523621922,323.285043847328,323.332378172878),
 .UNSPECIFIED.);
#255=B_SPLINE_CURVE_WITH_KNOTS('',3,(#40367,#40368,#40369,#40370,#40371,
#40372,#40373,#40374,#40375,#40376,#40377,#40378,#40379,#40380,#40381,#40382,
#40383,#40384,#40385,#40386,#40387,#40388,#40389,#40390,#40391,#40392,#40393,
#40394,#40395,#40396,#40397,#40398,#40399,#40400,#40401,#40402,#40403,#40404,
#40405,#40406,#40407,#40408,#40409,#40410,#40411,#40412,#40413,#40414,#40415,
#40416,#40417,#40418,#40419,#40420,#40421,#40422,#40423,#40424,#40425,#40426,
#40427,#40428,#40429,#40430,#40431,#40432,#40433,#40434,#40435,#40436,#40437,
#40438,#40439,#40440,#40441,#40442,#40443,#40444,#40445,#40446,#40447,#40448,
#40449,#40450,#40451,#40452,#40453,#40454,#40455,#40456,#40457,#40458,#40459,
#40460,#40461,#40462,#40463,#40464,#40465,#40466,#40467,#40468,#40469,#40470,
#40471,#40472,#40473,#40474,#40475,#40476,#40477,#40478,#40479,#40480,#40481,
#40482,#40483,#40484,#40485,#40486,#40487,#40488,#40489,#40490,#40491,#40492,
#40493,#40494,#40495,#40496,#40497,#40498,#40499,#40500,#40501,#40502,#40503,
#40504,#40505,#40506,#40507,#40508,#40509,#40510,#40511,#40512,#40513,#40514,
#40515,#40516,#40517,#40518,#40519,#40520,#40521,#40522,#40523,#40524,#40525,
#40526,#40527,#40528,#40529,#40530,#40531,#40532,#40533,#40534,#40535,#40536,
#40537,#40538,#40539,#40540,#40541,#40542,#40543,#40544,#40545,#40546,#40547,
#40548,#40549,#40550,#40551,#40552,#40553,#40554,#40555,#40556,#40557,#40558,
#40559,#40560,#40561,#40562,#40563,#40564,#40565,#40566,#40567,#40568,#40569,
#40570,#40571,#40572,#40573,#40574,#40575,#40576,#40577,#40578,#40579,#40580,
#40581,#40582,#40583,#40584,#40585,#40586),.UNSPECIFIED.,.F.,.F.,(4,3,3,
3,3,3,3,3,3,3,3,3,3,3,3,3,3,3,3,3,3,3,3,3,3,3,3,3,3,3,3,3,3,3,3,3,3,3,3,
3,3,3,3,3,3,3,3,3,3,3,3,3,3,3,3,3,3,3,3,3,3,3,3,3,3,3,3,3,3,3,3,3,3,4),
(323.584043319729,323.66786391523,323.751684534608,323.835522700307,323.919395942302,
324.003374465569,324.087410996865,324.171583499636,324.222502254773,324.306240966619,
324.389876477986,324.473428921385,324.556918357236,324.64037230785,324.723808801696,
324.807245911452,324.890701706369,324.974246199099,325.05783528204,325.141558549598,
325.222238265494,325.30597697734,325.389612488707,325.473164932106,325.556654367957,
325.640108318571,325.723544812417,325.806981922173,325.89043771709,325.97398220982,
326.057571292761,326.141294560319,326.221974276214,326.30571298806,326.389348499427,
326.472900942826,326.556390378677,326.63984432929,326.723280823137,326.806717932892,
326.89017372781,326.97371822054,327.057307303481,327.141030571038,327.221710286934,
327.30544899878,327.389084510147,327.472636953546,327.556126389397,327.63958034001,
327.723016833856,327.806453943612,327.889909738529,327.973454231259,328.0570433142,
328.140766581757,328.221446297654,328.3051850095,328.388820520867,328.472372964266,
328.555862400117,328.63931635073,328.722752844577,328.806189954332,328.88964574925,
328.97319024198,329.056779324921,329.140502592479,329.221182308374,329.305236123548,
329.389151545692,329.472987341021,329.55674865914,329.616396844457),
 .UNSPECIFIED.);
#256=B_SPLINE_CURVE_WITH_KNOTS('',3,(#40587,#40588,#40589,#40590,#40591,
#40592,#40593,#40594,#40595,#40596),.UNSPECIFIED.,.F.,.F.,(4,3,3,4),(323.333553374426,
323.429055721388,323.523916465494,323.58404331953),.UNSPECIFIED.);
#257=B_SPLINE_CURVE_WITH_KNOTS('',3,(#40598,#40599,#40600,#40601,#40602,
#40603,#40604,#40605,#40606,#40607,#40608,#40609,#40610),.UNSPECIFIED.,
 .F.,.F.,(4,3,3,3,4),(323.332378172878,323.415999707598,323.499742052346,
323.533056863769,323.584043319733),.UNSPECIFIED.);
#258=B_SPLINE_CURVE_WITH_KNOTS('',3,(#40611,#40612,#40613,#40614,#40615,
#40616,#40617,#40618,#40619,#40620,#40621,#40622,#40623,#40624,#40625,#40626,
#40627,#40628,#40629,#40630,#40631,#40632,#40633,#40634,#40635,#40636,#40637,
#40638,#40639,#40640,#40641,#40642,#40643,#40644,#40645,#40646,#40647,#40648,
#40649,#40650,#40651,#40652,#40653,#40654,#40655,#40656,#40657,#40658,#40659,
#40660,#40661,#40662,#40663,#40664,#40665,#40666,#40667,#40668,#40669,#40670,
#40671,#40672,#40673,#40674,#40675,#40676,#40677,#40678,#40679,#40680,#40681,
#40682,#40683,#40684,#40685,#40686,#40687,#40688,#40689,#40690,#40691,#40692,
#40693,#40694,#40695,#40696,#40697,#40698,#40699,#40700,#40701,#40702,#40703,
#40704,#40705,#40706,#40707,#40708,#40709,#40710,#40711,#40712,#40713,#40714,
#40715,#40716,#40717,#40718,#40719,#40720,#40721,#40722,#40723,#40724,#40725,
#40726,#40727,#40728,#40729,#40730,#40731,#40732,#40733,#40734,#40735,#40736,
#40737,#40738,#40739,#40740,#40741,#40742,#40743,#40744,#40745,#40746,#40747,
#40748,#40749,#40750,#40751,#40752,#40753,#40754,#40755,#40756,#40757,#40758,
#40759,#40760,#40761,#40762,#40763,#40764,#40765,#40766,#40767,#40768,#40769,
#40770,#40771,#40772,#40773,#40774,#40775,#40776,#40777,#40778,#40779,#40780,
#40781,#40782,#40783,#40784,#40785,#40786,#40787,#40788,#40789,#40790,#40791,
#40792,#40793,#40794,#40795,#40796,#40797,#40798,#40799,#40800,#40801,#40802,
#40803,#40804,#40805,#40806,#40807,#40808,#40809,#40810,#40811,#40812,#40813,
#40814,#40815,#40816,#40817,#40818,#40819,#40820,#40821,#40822,#40823,#40824,
#40825,#40826,#40827,#40828,#40829,#40830),.UNSPECIFIED.,.F.,.F.,(4,3,3,
3,3,3,3,3,3,3,3,3,3,3,3,3,3,3,3,3,3,3,3,3,3,3,3,3,3,3,3,3,3,3,3,3,3,3,3,
3,3,3,3,3,3,3,3,3,3,3,3,3,3,3,3,3,3,3,3,3,3,3,3,3,3,3,3,3,3,3,3,3,3,4),
(323.584043319934,323.667116505993,323.75008976071,323.83298383851,323.91581941661,
323.99862590948,324.081420154102,324.164220781389,324.247046423578,324.32996194568,
324.412928810753,324.496016216833,324.532792874489,324.616531586335,324.700167097702,
324.783719541101,324.867208976952,324.950662927566,325.034099421412,325.117536531168,
325.200992326085,325.284536818815,325.368125901756,325.451849169314,325.532528885209,
325.616267597055,325.699903108422,325.783455551821,325.866944987672,325.950398938286,
326.033835432132,326.117272541887,326.200728336805,326.284272829535,326.367861912476,
326.451585180034,326.532264895929,326.616003607775,326.699639119142,326.783191562541,
326.866680998392,326.950134949006,327.033571442852,327.117008552607,327.200464347524,
327.284008840254,327.367597923195,327.451321190753,327.532000906649,327.615739618495,
327.699375129863,327.782927573261,327.866417009112,327.949870959726,328.033307453572,
328.116744563328,328.200200358245,328.283744850975,328.367333933916,328.451057201474,
328.531736917369,328.615475629215,328.699111140582,328.782663583981,328.866153019832,
328.949606970446,329.033043464292,329.116480574048,329.199936368965,329.283480861695,
329.367069944636,329.450793212194,329.531472928089,329.61663357438),
 .UNSPECIFIED.);
#259=B_SPLINE_CURVE_WITH_KNOTS('',3,(#40836,#40837,#40838,#40839,#40840,
#40841,#40842,#40843,#40844,#40845,#40846,#40847,#40848,#40849,#40850,#40851,
#40852,#40853,#40854,#40855,#40856,#40857,#40858,#40859,#40860,#40861,#40862,
#40863,#40864,#40865,#40866,#40867,#40868,#40869,#40870,#40871,#40872,#40873,
#40874,#40875,#40876,#40877,#40878,#40879,#40880,#40881,#40882,#40883,#40884,
#40885,#40886,#40887,#40888,#40889,#40890,#40891,#40892,#40893,#40894,#40895,
#40896,#40897,#40898,#40899,#40900,#40901,#40902,#40903,#40904,#40905,#40906,
#40907,#40908,#40909,#40910,#40911,#40912,#40913,#40914,#40915,#40916,#40917,
#40918,#40919,#40920,#40921,#40922,#40923,#40924,#40925,#40926,#40927,#40928,
#40929,#40930,#40931,#40932,#40933,#40934,#40935,#40936,#40937,#40938,#40939,
#40940,#40941,#40942,#40943,#40944,#40945,#40946,#40947,#40948,#40949,#40950,
#40951,#40952,#40953,#40954,#40955,#40956,#40957,#40958,#40959,#40960,#40961,
#40962,#40963,#40964,#40965,#40966,#40967,#40968,#40969,#40970,#40971,#40972,
#40973,#40974,#40975,#40976,#40977,#40978,#40979,#40980,#40981,#40982,#40983,
#40984,#40985,#40986,#40987,#40988,#40989,#40990,#40991,#40992,#40993,#40994,
#40995,#40996,#40997,#40998,#40999,#41000,#41001,#41002,#41003,#41004,#41005,
#41006,#41007,#41008,#41009,#41010,#41011,#41012,#41013,#41014,#41015,#41016,
#41017,#41018,#41019,#41020,#41021,#41022,#41023,#41024,#41025,#41026,#41027,
#41028,#41029,#41030,#41031,#41032,#41033,#41034,#41035,#41036,#41037,#41038,
#41039,#41040,#41041,#41042,#41043,#41044,#41045,#41046,#41047,#41048,#41049,
#41050,#41051,#41052,#41053,#41054,#41055),.UNSPECIFIED.,.F.,.F.,(4,3,3,
3,3,3,3,3,3,3,3,3,3,3,3,3,3,3,3,3,3,3,3,3,3,3,3,3,3,3,3,3,3,3,3,3,3,3,3,
3,3,3,3,3,3,3,3,3,3,3,3,3,3,3,3,3,3,3,3,3,3,3,3,3,3,3,3,3,3,3,3,3,3,4),
(329.867228627105,329.962755668786,330.058739773327,330.155315172663,330.220918319094,
330.30465703094,330.388292542307,330.471844985706,330.555334421557,330.63878837217,
330.722224866016,330.805661975772,330.889117770689,330.972662263419,331.05625134636,
331.139974613917,331.220654329814,331.30439304166,331.388028553027,331.471580996426,
331.555070432277,331.638524382891,331.721960876737,331.805397986493,331.88885378141,
331.97239827414,332.055987357081,332.139710624639,332.220390340534,332.30412905238,
332.387764563748,332.471317007146,332.554806442997,332.638260393611,332.721696887457,
332.805133997213,332.88858979213,332.97213428486,333.055723367801,333.139446635359,
333.220126351255,333.303865063101,333.387500574469,333.471053017867,333.554542453718,
333.637996404332,333.721432898178,333.804870007934,333.888325802852,333.971870295581,
334.055459378522,334.13918264608,334.219862361975,334.303601073821,334.387236585188,
334.470789028587,334.554278464438,334.637732415052,334.721168908898,334.804606018653,
334.888061813571,334.971606306301,335.055195389242,335.138918656799,335.219598372695,
335.30447156949,335.387272010219,335.469997276829,335.552666223432,335.639145654337,
335.721770900446,335.804394995688,335.88705363544,335.898583947052),
 .UNSPECIFIED.);
#260=B_SPLINE_CURVE_WITH_KNOTS('',3,(#41056,#41057,#41058,#41059,#41060,
#41061,#41062,#41063,#41064,#41065),.UNSPECIFIED.,.F.,.F.,(4,3,3,4),(329.616396844457,
329.700090524835,329.783786786313,329.867228626909),.UNSPECIFIED.);
#261=B_SPLINE_CURVE_WITH_KNOTS('',3,(#41067,#41068,#41069,#41070,#41071,
#41072,#41073,#41074,#41075,#41076),.UNSPECIFIED.,.F.,.F.,(4,3,3,4),(329.61663357438,
329.714431689665,329.811393456063,329.867228626724),.UNSPECIFIED.);
#262=B_SPLINE_CURVE_WITH_KNOTS('',3,(#41077,#41078,#41079,#41080,#41081,
#41082,#41083,#41084,#41085,#41086,#41087,#41088,#41089,#41090,#41091,#41092,
#41093,#41094,#41095,#41096,#41097,#41098,#41099,#41100,#41101,#41102,#41103,
#41104,#41105,#41106,#41107,#41108,#41109,#41110,#41111,#41112,#41113,#41114,
#41115,#41116,#41117,#41118,#41119,#41120,#41121,#41122,#41123,#41124,#41125,
#41126,#41127,#41128,#41129,#41130,#41131,#41132,#41133,#41134,#41135,#41136,
#41137,#41138,#41139,#41140,#41141,#41142,#41143,#41144,#41145,#41146,#41147,
#41148,#41149,#41150,#41151,#41152,#41153,#41154,#41155,#41156,#41157,#41158,
#41159,#41160,#41161,#41162,#41163,#41164,#41165,#41166,#41167,#41168,#41169,
#41170,#41171,#41172,#41173,#41174,#41175,#41176,#41177,#41178,#41179,#41180,
#41181,#41182,#41183,#41184,#41185,#41186,#41187,#41188,#41189,#41190,#41191,
#41192,#41193,#41194,#41195,#41196,#41197,#41198,#41199,#41200,#41201,#41202,
#41203,#41204,#41205,#41206,#41207,#41208,#41209,#41210,#41211,#41212,#41213,
#41214,#41215,#41216,#41217,#41218,#41219,#41220,#41221,#41222,#41223,#41224,
#41225,#41226,#41227,#41228,#41229,#41230,#41231,#41232,#41233,#41234,#41235,
#41236,#41237,#41238,#41239,#41240,#41241,#41242,#41243,#41244,#41245,#41246,
#41247,#41248,#41249,#41250,#41251,#41252,#41253,#41254,#41255,#41256,#41257,
#41258,#41259,#41260,#41261,#41262,#41263,#41264,#41265,#41266,#41267,#41268,
#41269,#41270,#41271,#41272,#41273,#41274,#41275,#41276,#41277,#41278,#41279,
#41280,#41281,#41282,#41283,#41284,#41285,#41286,#41287,#41288,#41289,#41290,
#41291,#41292,#41293,#41294,#41295,#41296),.UNSPECIFIED.,.F.,.F.,(4,3,3,
3,3,3,3,3,3,3,3,3,3,3,3,3,3,3,3,3,3,3,3,3,3,3,3,3,3,3,3,3,3,3,3,3,3,3,3,
3,3,3,3,3,3,3,3,3,3,3,3,3,3,3,3,3,3,3,3,3,3,3,3,3,3,3,3,3,3,3,3,3,3,4),
(329.867228626912,329.950650073194,330.034059218144,330.117474083261,330.200912690001,
330.284447492303,330.368031162443,330.451755204459,330.53120893881,330.614947650656,
330.698583162023,330.782135605422,330.865625041273,330.949078991886,331.032515485733,
331.115952595488,331.199408390406,331.282952883136,331.366541966077,331.450265233634,
331.53094494953,331.614683661376,331.698319172744,331.781871616142,331.865361051993,
331.948815002607,332.032251496453,332.115688606209,332.199144401126,332.282688893856,
332.366277976797,332.450001244354,332.53068096025,332.614419672096,332.698055183463,
332.781607626861,332.865097062713,332.948551013326,333.031987507172,333.115424616928,
333.198880411846,333.282424904576,333.366013987517,333.449737255074,333.53041697097,
333.614155682816,333.697791194183,333.781343637582,333.864833073433,333.948287024047,
334.031723517893,334.115160627648,334.198616422565,334.282160915295,334.365749998236,
334.449473265794,334.53015298169,334.613891693536,334.697527204904,334.781079648302,
334.864569084154,334.948023034767,335.031459528614,335.114896638369,335.198352433287,
335.281896926017,335.365486008958,335.449209276515,335.52988899241,335.61443704822,
335.698840656777,335.783160681546,335.867398052658,335.899704001206),
 .UNSPECIFIED.);
#263=B_SPLINE_CURVE_WITH_KNOTS('',3,(#41302,#41303,#41304,#41305,#41306,
#41307,#41308,#41309,#41310,#41311,#41312,#41313,#41314,#41315,#41316,#41317,
#41318,#41319,#41320,#41321,#41322,#41323,#41324,#41325,#41326,#41327,#41328,
#41329,#41330,#41331,#41332,#41333,#41334,#41335,#41336,#41337,#41338,#41339,
#41340,#41341,#41342,#41343,#41344,#41345,#41346,#41347,#41348,#41349,#41350,
#41351,#41352,#41353,#41354,#41355,#41356,#41357,#41358,#41359,#41360,#41361,
#41362,#41363,#41364,#41365,#41366,#41367,#41368,#41369,#41370,#41371,#41372,
#41373,#41374,#41375,#41376,#41377,#41378,#41379,#41380,#41381,#41382,#41383,
#41384,#41385,#41386,#41387,#41388,#41389,#41390,#41391,#41392,#41393,#41394,
#41395,#41396,#41397,#41398,#41399,#41400,#41401,#41402,#41403,#41404,#41405,
#41406,#41407,#41408,#41409,#41410,#41411,#41412,#41413,#41414,#41415,#41416,
#41417,#41418,#41419,#41420,#41421,#41422,#41423,#41424,#41425,#41426,#41427,
#41428,#41429,#41430,#41431,#41432,#41433,#41434,#41435,#41436,#41437,#41438,
#41439,#41440,#41441,#41442,#41443,#41444,#41445,#41446,#41447,#41448,#41449,
#41450,#41451,#41452,#41453,#41454,#41455,#41456,#41457,#41458,#41459,#41460,
#41461,#41462,#41463,#41464,#41465,#41466,#41467,#41468,#41469,#41470,#41471,
#41472,#41473,#41474,#41475,#41476,#41477,#41478,#41479,#41480,#41481,#41482,
#41483,#41484,#41485,#41486,#41487,#41488,#41489,#41490,#41491,#41492,#41493,
#41494,#41495,#41496,#41497,#41498,#41499,#41500,#41501,#41502,#41503,#41504,
#41505,#41506,#41507,#41508,#41509,#41510,#41511,#41512,#41513,#41514,#41515,
#41516,#41517,#41518,#41519,#41520,#41521),.UNSPECIFIED.,.F.,.F.,(4,3,3,
3,3,3,3,3,3,3,3,3,3,3,3,3,3,3,3,3,3,3,3,3,3,3,3,3,3,3,3,3,3,3,3,3,3,3,3,
3,3,3,3,3,3,3,3,3,3,3,3,3,3,3,3,3,3,3,3,3,3,3,3,3,3,3,3,3,3,3,3,3,3,4),
(336.150413934088,336.219334383415,336.303073095261,336.386708606628,336.470261050027,
336.553750485878,336.637204436491,336.720640930337,336.804078040093,336.88753383501,
336.97107832774,337.054667410681,337.138390678238,337.219070394135,337.302809105981,
337.386444617348,337.469997060747,337.553486496598,337.636940447212,337.720376941058,
337.803814050813,337.887269845731,337.970814338461,338.054403421402,338.138126688959,
338.218806404855,338.302545116701,338.386180628068,338.469733071467,338.553222507318,
338.636676457931,338.720112951778,338.803550061533,338.887005856451,338.97055034918,
339.054139432121,339.137862699679,339.218542415575,339.302281127421,339.385916638788,
339.469469082187,339.552958518038,339.636412468652,339.719848962498,339.803286072254,
339.886741867171,339.970286359901,340.053875442842,340.137598710399,340.218278426295,
340.302017138141,340.385652649509,340.469205092907,340.552694528758,340.636148479372,
340.719584973218,340.803022082974,340.886477877892,340.970022370621,341.053611453562,
341.13733472112,341.218014437016,341.30175516004,341.385392215482,341.468945737824,
341.552435788984,341.635887995735,341.71932208536,341.802756130105,341.88620819822,
341.969739944127,342.05331600737,342.137005309499,342.182335603278),
 .UNSPECIFIED.);
#264=B_SPLINE_CURVE_WITH_KNOTS('',3,(#41522,#41523,#41524,#41525,#41526,
#41527,#41528,#41529,#41530,#41531),.UNSPECIFIED.,.F.,.F.,(4,3,3,4),(335.898583947052,
335.981329823347,336.065871878657,336.150413933966),.UNSPECIFIED.);
#265=B_SPLINE_CURVE_WITH_KNOTS('',3,(#41533,#41534,#41535,#41536,#41537,
#41538,#41539,#41540,#41541,#41542),.UNSPECIFIED.,.F.,.F.,(4,3,3,4),(335.899704001206,
335.983869305751,336.06801737133,336.150413934092),.UNSPECIFIED.);
#266=B_SPLINE_CURVE_WITH_KNOTS('',3,(#41543,#41544,#41545,#41546,#41547,
#41548,#41549,#41550,#41551,#41552,#41553,#41554,#41555,#41556,#41557,#41558,
#41559,#41560,#41561,#41562,#41563,#41564,#41565,#41566,#41567,#41568,#41569,
#41570,#41571,#41572,#41573,#41574,#41575,#41576,#41577,#41578,#41579,#41580,
#41581,#41582,#41583,#41584,#41585,#41586,#41587,#41588,#41589,#41590,#41591,
#41592,#41593,#41594,#41595,#41596,#41597,#41598,#41599,#41600,#41601,#41602,
#41603,#41604,#41605,#41606,#41607,#41608,#41609,#41610,#41611,#41612,#41613,
#41614,#41615,#41616,#41617,#41618,#41619,#41620,#41621,#41622,#41623,#41624,
#41625,#41626,#41627,#41628,#41629,#41630,#41631,#41632,#41633,#41634,#41635,
#41636,#41637,#41638,#41639,#41640,#41641,#41642,#41643,#41644,#41645,#41646,
#41647,#41648,#41649,#41650,#41651,#41652,#41653,#41654,#41655,#41656,#41657,
#41658,#41659,#41660,#41661,#41662,#41663,#41664,#41665,#41666,#41667,#41668,
#41669,#41670,#41671,#41672,#41673,#41674,#41675,#41676,#41677,#41678,#41679,
#41680,#41681,#41682,#41683,#41684,#41685,#41686,#41687,#41688,#41689,#41690,
#41691,#41692,#41693,#41694,#41695,#41696,#41697,#41698,#41699,#41700,#41701,
#41702,#41703,#41704,#41705,#41706,#41707,#41708,#41709,#41710,#41711,#41712,
#41713,#41714,#41715,#41716,#41717,#41718,#41719,#41720,#41721,#41722,#41723,
#41724,#41725,#41726,#41727,#41728,#41729,#41730,#41731,#41732,#41733,#41734,
#41735,#41736,#41737,#41738,#41739,#41740,#41741,#41742,#41743,#41744,#41745,
#41746,#41747,#41748,#41749,#41750,#41751,#41752,#41753,#41754,#41755,#41756,
#41757,#41758,#41759),.UNSPECIFIED.,.F.,.F.,(4,3,3,3,3,3,3,3,3,3,3,3,3,
3,3,3,3,3,3,3,3,3,3,3,3,3,3,3,3,3,3,3,3,3,3,3,3,3,3,3,3,3,3,3,3,3,3,3,3,
3,3,3,3,3,3,3,3,3,3,3,3,3,3,3,3,3,3,3,3,3,3,3,4),(336.150413934288,336.245216701498,
336.339215446596,336.434420224863,336.52962500313,336.613363714976,336.696999226343,
336.780551669742,336.864041105593,336.947495056207,337.030931550053,337.114368659809,
337.197824454726,337.281368947456,337.364958030397,337.448681297955,337.52936101385,
337.613099725696,337.696735237064,337.780287680462,337.863777116313,337.947231066927,
338.030667560773,338.114104670529,338.197560465446,338.281104958176,338.364694041117,
338.448417308675,338.529097024571,338.612835736417,338.696471247784,338.780023691183,
338.863513127034,338.946967077648,339.030403571494,339.113840681249,339.197296476167,
339.280840968897,339.364430051838,339.448153319396,339.528833035291,339.612571747137,
339.696207258504,339.779759701903,339.863249137754,339.946703088367,340.030139582214,
340.113576691969,340.197032486887,340.280576979616,340.364166062557,340.447889330115,
340.528569046011,340.612307757857,340.695943269225,340.779495712623,340.862985148474,
340.946439099088,341.029875592934,341.11331270269,341.196768497607,341.280312990337,
341.363902073278,341.447625340836,341.528305056731,341.611009828143,341.693620044045,
341.776154761799,341.858632971129,341.941084209395,342.023516950066,342.105980397765,
342.181762906209),.UNSPECIFIED.);
#267=B_SPLINE_CURVE_WITH_KNOTS('',3,(#41765,#41766,#41767,#41768,#41769,
#41770,#41771,#41772,#41773,#41774,#41775,#41776,#41777,#41778,#41779,#41780,
#41781,#41782,#41783,#41784,#41785,#41786,#41787,#41788,#41789,#41790,#41791,
#41792,#41793,#41794,#41795,#41796,#41797,#41798,#41799,#41800,#41801,#41802,
#41803,#41804,#41805,#41806,#41807,#41808,#41809,#41810,#41811,#41812,#41813,
#41814,#41815,#41816,#41817,#41818,#41819,#41820,#41821,#41822,#41823,#41824,
#41825,#41826,#41827,#41828,#41829,#41830,#41831,#41832,#41833,#41834,#41835,
#41836,#41837,#41838,#41839,#41840,#41841,#41842,#41843,#41844,#41845,#41846,
#41847,#41848,#41849,#41850,#41851,#41852,#41853,#41854,#41855,#41856,#41857,
#41858,#41859,#41860,#41861,#41862,#41863,#41864,#41865,#41866,#41867,#41868,
#41869,#41870,#41871,#41872,#41873,#41874,#41875,#41876,#41877,#41878,#41879,
#41880,#41881,#41882,#41883,#41884,#41885,#41886,#41887,#41888,#41889,#41890,
#41891,#41892,#41893,#41894,#41895,#41896,#41897,#41898,#41899,#41900,#41901,
#41902,#41903,#41904,#41905,#41906,#41907,#41908,#41909,#41910,#41911,#41912,
#41913,#41914,#41915,#41916,#41917,#41918,#41919,#41920,#41921,#41922,#41923,
#41924,#41925,#41926,#41927,#41928,#41929,#41930,#41931,#41932,#41933,#41934,
#41935,#41936,#41937,#41938,#41939,#41940,#41941,#41942,#41943,#41944,#41945,
#41946,#41947,#41948,#41949,#41950,#41951,#41952,#41953,#41954,#41955,#41956,
#41957,#41958,#41959,#41960,#41961,#41962,#41963,#41964,#41965,#41966,#41967,
#41968,#41969,#41970,#41971,#41972,#41973,#41974,#41975,#41976,#41977,#41978,
#41979,#41980,#41981,#41982,#41983,#41984),.UNSPECIFIED.,.F.,.F.,(4,3,3,
3,3,3,3,3,3,3,3,3,3,3,3,3,3,3,3,3,3,3,3,3,3,3,3,3,3,3,3,3,3,3,3,3,3,3,3,
3,3,3,3,3,3,3,3,3,3,3,3,3,3,3,3,3,3,3,3,3,3,3,3,3,3,3,3,3,3,3,3,3,3,4),
(342.433599241371,342.516011609185,342.598359736635,342.680671607215,342.762966721928,
342.845264058301,342.927582593349,343.009987668582,343.092441313092,343.175015631616,
343.217486458456,343.301225170302,343.384860681669,343.468413125068,343.551902560919,
343.635356511532,343.718793005379,343.802230115134,343.885685910052,343.969230402782,
344.052819485723,344.13654275328,344.217222469176,344.300961181022,344.384596692389,
344.468149135788,344.551638571639,344.635092522253,344.718529016099,344.801966125855,
344.885421920772,344.968966413502,345.052555496443,345.136278764001,345.216958479896,
345.300697191742,345.384332703109,345.467885146508,345.551374582359,345.634828532972,
345.718265026819,345.801702136574,345.885157931492,345.968702424222,346.052291507163,
346.13601477472,346.216694490616,346.300433202462,346.384068713829,346.467621157228,
346.551110593079,346.634564543693,346.718001037539,346.801438147294,346.884893942212,
346.968438434941,347.052027517882,347.13575078544,347.216430501336,347.300169213182,
347.38380472455,347.467357167948,347.550846603799,347.634300554413,347.71773704826,
347.801174158015,347.884629952933,347.968174445662,348.051763528603,348.135486796161,
348.216166512056,348.304192741535,348.392023476754,348.466455594936),
 .UNSPECIFIED.);
#268=B_SPLINE_CURVE_WITH_KNOTS('',3,(#41985,#41986,#41987,#41988,#41989,
#41990,#41991,#41992,#41993,#41994),.UNSPECIFIED.,.F.,.F.,(4,3,3,4),(342.182335603278,
342.217750447736,342.333550962604,342.433599241268),.UNSPECIFIED.);
#269=B_SPLINE_CURVE_WITH_KNOTS('',3,(#41996,#41997,#41998,#41999,#42000,
#42001,#42002,#42003,#42004,#42005),.UNSPECIFIED.,.F.,.F.,(4,3,3,4),(342.181762906209,
342.26430274518,342.348950993158,342.433599241137),.UNSPECIFIED.);
#270=B_SPLINE_CURVE_WITH_KNOTS('',3,(#42006,#42007,#42008,#42009,#42010,
#42011,#42012,#42013,#42014,#42015,#42016,#42017,#42018,#42019,#42020,#42021,
#42022,#42023,#42024,#42025,#42026,#42027,#42028,#42029,#42030,#42031,#42032,
#42033,#42034,#42035,#42036,#42037,#42038,#42039,#42040,#42041,#42042,#42043,
#42044,#42045,#42046,#42047,#42048,#42049,#42050,#42051,#42052,#42053,#42054,
#42055,#42056,#42057,#42058,#42059,#42060,#42061,#42062,#42063,#42064,#42065,
#42066,#42067,#42068,#42069,#42070,#42071,#42072,#42073,#42074,#42075,#42076,
#42077,#42078,#42079,#42080,#42081,#42082,#42083,#42084,#42085,#42086,#42087,
#42088,#42089,#42090,#42091,#42092,#42093,#42094,#42095,#42096,#42097,#42098,
#42099,#42100,#42101,#42102,#42103,#42104,#42105,#42106,#42107,#42108,#42109,
#42110,#42111,#42112,#42113,#42114,#42115,#42116,#42117,#42118,#42119,#42120,
#42121,#42122,#42123,#42124,#42125,#42126,#42127,#42128,#42129,#42130,#42131,
#42132,#42133,#42134,#42135,#42136,#42137,#42138,#42139,#42140,#42141,#42142,
#42143,#42144,#42145,#42146,#42147,#42148,#42149,#42150,#42151,#42152,#42153,
#42154,#42155,#42156,#42157,#42158,#42159,#42160,#42161,#42162,#42163,#42164,
#42165,#42166,#42167,#42168,#42169,#42170,#42171,#42172,#42173,#42174,#42175,
#42176,#42177,#42178,#42179,#42180,#42181,#42182,#42183,#42184,#42185,#42186,
#42187,#42188,#42189,#42190,#42191,#42192,#42193,#42194,#42195,#42196,#42197,
#42198,#42199,#42200,#42201,#42202,#42203,#42204,#42205,#42206,#42207,#42208,
#42209,#42210,#42211,#42212,#42213,#42214,#42215,#42216,#42217,#42218,#42219,
#42220,#42221,#42222,#42223,#42224,#42225),.UNSPECIFIED.,.F.,.F.,(4,3,3,
3,3,3,3,3,3,3,3,3,3,3,3,3,3,3,3,3,3,3,3,3,3,3,3,3,3,3,3,3,3,3,3,3,3,3,3,
3,3,3,3,3,3,3,3,3,3,3,3,3,3,3,3,3,3,3,3,3,3,3,3,3,3,3,3,3,3,3,3,3,3,4),
(342.433599241272,342.528041067451,342.611779779297,342.695415290664,342.778967734063,
342.862457169914,342.945911120527,343.029347614374,343.112784724129,343.196240519047,
343.279785011776,343.363374094717,343.447097362275,343.527777078171,343.611515790017,
343.695151301384,343.778703744783,343.862193180634,343.945647131247,344.029083625094,
344.112520734849,344.195976529767,344.279521022497,344.363110105437,344.446833372995,
344.527513088891,344.611251800737,344.694887312104,344.778439755503,344.861929191354,
344.945383141968,345.028819635814,345.11225674557,345.195712540487,345.279257033217,
345.362846116158,345.446569383716,345.527249099611,345.610987811457,345.694623322825,
345.778175766223,345.861665202074,345.945119152688,346.028555646534,346.11199275629,
346.195448551207,346.278993043937,346.362582126878,346.446305394436,346.526985110332,
346.610723822178,346.694359333545,346.777911776944,346.861401212795,346.944855163409,
347.028291657255,347.111728767011,347.195184561928,347.278729054658,347.362318137599,
347.446041405157,347.526721121052,347.610463334944,347.694101543076,347.777655881374,
347.863624497286,347.94707476908,348.030506982412,348.113939208974,348.19738951639,
348.28091366941,348.364482424372,348.448150397174,348.465404808675),
 .UNSPECIFIED.);
#271=B_SPLINE_CURVE_WITH_KNOTS('',3,(#42231,#42232,#42233,#42234,#42235,
#42236,#42237,#42238,#42239,#42240,#42241,#42242,#42243,#42244,#42245,#42246,
#42247,#42248,#42249,#42250,#42251,#42252,#42253,#42254,#42255,#42256,#42257,
#42258,#42259,#42260,#42261,#42262,#42263,#42264,#42265,#42266,#42267,#42268,
#42269,#42270,#42271,#42272,#42273,#42274,#42275,#42276,#42277,#42278,#42279,
#42280,#42281,#42282,#42283,#42284,#42285,#42286,#42287,#42288,#42289,#42290,
#42291,#42292,#42293,#42294,#42295,#42296,#42297,#42298,#42299,#42300,#42301,
#42302,#42303,#42304,#42305,#42306,#42307,#42308,#42309,#42310,#42311,#42312,
#42313,#42314,#42315,#42316,#42317,#42318,#42319,#42320,#42321,#42322,#42323,
#42324,#42325,#42326,#42327,#42328,#42329,#42330,#42331,#42332,#42333,#42334,
#42335,#42336,#42337,#42338,#42339,#42340,#42341,#42342,#42343,#42344,#42345,
#42346,#42347,#42348,#42349,#42350,#42351,#42352,#42353,#42354,#42355,#42356,
#42357,#42358,#42359,#42360,#42361,#42362,#42363,#42364,#42365,#42366,#42367,
#42368,#42369,#42370,#42371,#42372,#42373,#42374,#42375,#42376,#42377,#42378,
#42379,#42380,#42381,#42382,#42383,#42384,#42385,#42386,#42387,#42388,#42389,
#42390,#42391,#42392,#42393,#42394,#42395,#42396,#42397,#42398,#42399,#42400,
#42401,#42402,#42403,#42404,#42405,#42406,#42407,#42408,#42409,#42410,#42411,
#42412,#42413,#42414,#42415,#42416,#42417,#42418,#42419,#42420,#42421,#42422,
#42423,#42424,#42425,#42426,#42427,#42428,#42429,#42430,#42431,#42432,#42433,
#42434,#42435,#42436,#42437,#42438,#42439,#42440,#42441,#42442,#42443,#42444,
#42445,#42446,#42447,#42448,#42449,#42450),.UNSPECIFIED.,.F.,.F.,(4,3,3,
3,3,3,3,3,3,3,3,3,3,3,3,3,3,3,3,3,3,3,3,3,3,3,3,3,3,3,3,3,3,3,3,3,3,3,3,
3,3,3,3,3,3,3,3,3,3,3,3,3,3,3,3,3,3,3,3,3,3,3,3,3,3,3,3,3,3,3,3,3,3,4),
(348.716784548596,348.804215738956,348.891763006794,348.979518053926,349.067382890157,
349.155449273507,349.215902522777,349.299641234623,349.38327674599,349.466829189389,
349.55031862524,349.633772575854,349.7172090697,349.800646179455,349.884101974373,
349.967646467103,350.051235550044,350.134958817601,350.215638533497,350.299377245343,
350.38301275671,350.466565200109,350.55005463596,350.633508586573,350.71694508042,
350.800382190175,350.883837985093,350.967382477822,351.050971560763,351.134694828321,
351.215374544217,351.299113256063,351.38274876743,351.466301210829,351.54979064668,
351.633244597294,351.71668109114,351.800118200895,351.883573995813,351.967118488543,
352.050707571484,352.134430839041,352.215110554937,352.298849266783,352.38248477815,
352.466037221549,352.5495266574,352.632980608014,352.71641710186,352.799854211615,
352.883310006533,352.966854499263,353.050443582204,353.134166849761,353.214846565657,
353.298585277503,353.382220788871,353.465773232269,353.54926266812,353.632716618734,
353.71615311258,353.799590222336,353.883046017254,353.966590509983,354.050179592924,
354.133902860482,354.214582576377,354.297147362669,354.379615533327,354.462006258773,
354.544335250586,354.626628364119,354.708914177518,354.748441555367),
 .UNSPECIFIED.);
#272=B_SPLINE_CURVE_WITH_KNOTS('',3,(#42451,#42452,#42453,#42454,#42455,
#42456,#42457,#42458,#42459,#42460),.UNSPECIFIED.,.F.,.F.,(4,3,3,4),(348.466455594936,
348.55402873825,348.641441273661,348.716784548447),.UNSPECIFIED.);
#273=B_SPLINE_CURVE_WITH_KNOTS('',3,(#42462,#42463,#42464,#42465,#42466,
#42467,#42468,#42469,#42470,#42471),.UNSPECIFIED.,.F.,.F.,(4,3,3,4),(348.465404808675,
348.526457131772,348.649804787013,348.716784548451),.UNSPECIFIED.);
#274=B_SPLINE_CURVE_WITH_KNOTS('',3,(#42472,#42473,#42474,#42475,#42476,
#42477,#42478,#42479,#42480,#42481,#42482,#42483,#42484,#42485,#42486,#42487,
#42488,#42489,#42490,#42491,#42492,#42493,#42494,#42495,#42496,#42497,#42498,
#42499,#42500,#42501,#42502,#42503,#42504,#42505,#42506,#42507,#42508,#42509,
#42510,#42511,#42512,#42513,#42514,#42515,#42516,#42517,#42518,#42519,#42520,
#42521,#42522,#42523,#42524,#42525,#42526,#42527,#42528,#42529,#42530,#42531,
#42532,#42533,#42534,#42535,#42536,#42537,#42538,#42539,#42540,#42541,#42542,
#42543,#42544,#42545,#42546,#42547,#42548,#42549,#42550,#42551,#42552,#42553,
#42554,#42555,#42556,#42557,#42558,#42559,#42560,#42561,#42562,#42563,#42564,
#42565,#42566,#42567,#42568,#42569,#42570,#42571,#42572,#42573,#42574,#42575,
#42576,#42577,#42578,#42579,#42580,#42581,#42582,#42583,#42584,#42585,#42586,
#42587,#42588,#42589,#42590,#42591,#42592,#42593,#42594,#42595,#42596,#42597,
#42598,#42599,#42600,#42601,#42602,#42603,#42604,#42605,#42606,#42607,#42608,
#42609,#42610,#42611,#42612,#42613,#42614,#42615,#42616,#42617,#42618,#42619,
#42620,#42621,#42622,#42623,#42624,#42625,#42626,#42627,#42628,#42629,#42630,
#42631,#42632,#42633,#42634,#42635,#42636,#42637,#42638,#42639,#42640,#42641,
#42642,#42643,#42644,#42645,#42646,#42647,#42648,#42649,#42650,#42651,#42652,
#42653,#42654,#42655,#42656,#42657,#42658,#42659,#42660,#42661,#42662,#42663,
#42664,#42665,#42666,#42667,#42668,#42669,#42670,#42671,#42672,#42673,#42674,
#42675,#42676,#42677,#42678,#42679,#42680,#42681,#42682,#42683,#42684,#42685,
#42686,#42687,#42688,#42689,#42690,#42691),.UNSPECIFIED.,.F.,.F.,(4,3,3,
3,3,3,3,3,3,3,3,3,3,3,3,3,3,3,3,3,3,3,3,3,3,3,3,3,3,3,3,3,3,3,3,3,3,3,3,
3,3,3,3,3,3,3,3,3,3,3,3,3,3,3,3,3,3,3,3,3,3,3,3,3,3,3,3,3,3,3,3,3,3,4),
(348.716784548578,348.799150648385,348.881445036037,348.963693320568,349.045918200772,
349.128138704293,349.210373853009,349.292691839066,349.375052593812,349.457540805916,
349.526193142492,349.609931854338,349.693567365705,349.777119809104,349.860609244955,
349.944063195568,350.027499689415,350.11093679917,350.194392594088,350.277937086818,
350.361526169759,350.445249437316,350.525929153212,350.609667865058,350.693303376425,
350.776855819824,350.860345255674,350.943799206288,351.027235700134,351.11067280989,
351.194128604807,351.277673097537,351.361262180478,351.444985448035,351.525665163932,
351.609403875778,351.693039387146,351.776591830545,351.860081266395,351.943535217009,
352.026971710855,352.11040882061,352.193864615528,352.277409108258,352.360998191199,
352.444721458757,352.525401174652,352.609139886498,352.692775397865,352.776327841264,
352.859817277115,352.943271227728,353.026707721574,353.11014483133,353.193600626247,
353.277145118977,353.360734201918,353.444457469476,353.525137185373,353.608875897219,
353.692511408586,353.776063851985,353.859553287836,353.94300723845,354.026443732296,
354.109880842052,354.193336636969,354.276881129699,354.36047021264,354.444193480197,
354.524873196093,354.613975775307,354.702866823617,354.749665211946),
 .UNSPECIFIED.);
#275=B_SPLINE_CURVE_WITH_KNOTS('',3,(#42697,#42698,#42699,#42700,#42701,
#42702,#42703,#42704,#42705,#42706,#42707,#42708,#42709,#42710,#42711,#42712,
#42713,#42714,#42715,#42716,#42717,#42718,#42719,#42720,#42721,#42722,#42723,
#42724,#42725,#42726,#42727,#42728,#42729,#42730,#42731,#42732,#42733,#42734,
#42735,#42736,#42737,#42738,#42739,#42740,#42741,#42742,#42743,#42744,#42745,
#42746,#42747,#42748,#42749,#42750,#42751,#42752,#42753,#42754,#42755,#42756,
#42757,#42758,#42759,#42760,#42761,#42762,#42763,#42764,#42765,#42766,#42767,
#42768,#42769,#42770,#42771,#42772,#42773,#42774,#42775,#42776,#42777,#42778,
#42779,#42780,#42781,#42782,#42783,#42784,#42785,#42786,#42787,#42788,#42789,
#42790,#42791,#42792,#42793,#42794,#42795,#42796,#42797,#42798,#42799,#42800,
#42801,#42802,#42803,#42804,#42805,#42806,#42807,#42808,#42809,#42810,#42811,
#42812,#42813,#42814,#42815,#42816,#42817,#42818,#42819,#42820,#42821,#42822,
#42823,#42824,#42825,#42826,#42827,#42828,#42829,#42830,#42831,#42832,#42833,
#42834,#42835,#42836,#42837,#42838,#42839,#42840,#42841,#42842,#42843,#42844,
#42845,#42846,#42847,#42848,#42849,#42850,#42851,#42852,#42853,#42854,#42855,
#42856,#42857,#42858,#42859,#42860,#42861,#42862,#42863,#42864,#42865,#42866,
#42867,#42868,#42869,#42870,#42871,#42872,#42873,#42874,#42875,#42876,#42877,
#42878,#42879,#42880,#42881,#42882,#42883,#42884,#42885,#42886,#42887,#42888,
#42889,#42890,#42891,#42892,#42893,#42894,#42895,#42896,#42897,#42898,#42899,
#42900,#42901,#42902,#42903,#42904,#42905,#42906,#42907,#42908,#42909,#42910,
#42911,#42912,#42913),.UNSPECIFIED.,.F.,.F.,(4,3,3,3,3,3,3,3,3,3,3,3,3,
3,3,3,3,3,3,3,3,3,3,3,3,3,3,3,3,3,3,3,3,3,3,3,3,3,3,3,3,3,3,3,3,3,3,3,3,
3,3,3,3,3,3,3,3,3,3,3,3,3,3,3,3,3,3,3,3,3,3,3,4),(354.999969855627,355.116152110623,
355.214318587097,355.298057298943,355.38169281031,355.465245253709,355.54873468956,
355.632188640174,355.71562513402,355.799062243776,355.882518038693,355.966062531423,
356.049651614364,356.133374881922,356.214054597817,356.297793309663,356.381428821031,
356.464981264429,356.54847070028,356.631924650894,356.71536114474,356.798798254496,
356.882254049414,356.965798542143,357.049387625084,357.133110892642,357.213790608538,
357.297529320384,357.381164831751,357.46471727515,357.548206711001,357.631660661615,
357.715097155461,357.798534265216,357.881990060134,357.965534552864,358.049123635805,
358.132846903362,358.213526619258,358.297265331104,358.380900842471,358.46445328587,
358.547942721721,358.631396672335,358.714833166181,358.798270275936,358.881726070854,
358.965270563584,359.048859646525,359.132582914082,359.213262629978,359.297001341824,
359.380636853192,359.46418929659,359.547678732441,359.631132683055,359.714569176901,
359.798006286657,359.881462081574,359.965006574304,360.048595657245,360.132318924803,
360.212998640698,360.296748234594,360.380392237065,360.463935615642,360.547421943862,
360.630869341337,360.714295897617,360.797746857763,360.881208592463,360.964741904342,
361.031498889511),.UNSPECIFIED.);
#276=B_SPLINE_CURVE_WITH_KNOTS('',3,(#42914,#42915,#42916,#42917,#42918,
#42919,#42920,#42921,#42922,#42923),.UNSPECIFIED.,.F.,.F.,(4,3,3,4),(354.748441555367,
354.830758582066,354.915364218791,354.999969855515),.UNSPECIFIED.);
#277=B_SPLINE_CURVE_WITH_KNOTS('',3,(#42925,#42926,#42927,#42928,#42929,
#42930,#42931,#42932,#42933,#42934),.UNSPECIFIED.,.F.,.F.,(4,3,3,4),(354.749665211946,
354.838283603898,354.926692238297,354.999969855526),.UNSPECIFIED.);
#278=B_SPLINE_CURVE_WITH_KNOTS('',3,(#42935,#42936,#42937,#42938,#42939,
#42940,#42941,#42942,#42943,#42944,#42945,#42946,#42947,#42948,#42949,#42950,
#42951,#42952,#42953,#42954,#42955,#42956,#42957,#42958,#42959,#42960,#42961,
#42962,#42963,#42964,#42965,#42966,#42967,#42968,#42969,#42970,#42971,#42972,
#42973,#42974,#42975,#42976,#42977,#42978,#42979,#42980,#42981,#42982,#42983,
#42984,#42985,#42986,#42987,#42988,#42989,#42990,#42991,#42992,#42993,#42994,
#42995,#42996,#42997,#42998,#42999,#43000,#43001,#43002,#43003,#43004,#43005,
#43006,#43007,#43008,#43009,#43010,#43011,#43012,#43013,#43014,#43015,#43016,
#43017,#43018,#43019,#43020,#43021,#43022,#43023,#43024,#43025,#43026,#43027,
#43028,#43029,#43030,#43031,#43032,#43033,#43034,#43035,#43036,#43037,#43038,
#43039,#43040,#43041,#43042,#43043,#43044,#43045,#43046,#43047,#43048,#43049,
#43050,#43051,#43052,#43053,#43054,#43055,#43056,#43057,#43058,#43059,#43060,
#43061,#43062,#43063,#43064,#43065,#43066,#43067,#43068,#43069,#43070,#43071,
#43072,#43073,#43074,#43075,#43076,#43077,#43078,#43079,#43080,#43081,#43082,
#43083,#43084,#43085,#43086,#43087,#43088,#43089,#43090,#43091,#43092,#43093,
#43094,#43095,#43096,#43097,#43098,#43099,#43100,#43101,#43102,#43103,#43104,
#43105,#43106,#43107,#43108,#43109,#43110,#43111,#43112,#43113,#43114,#43115,
#43116,#43117,#43118,#43119,#43120,#43121,#43122,#43123,#43124,#43125,#43126,
#43127,#43128,#43129,#43130,#43131,#43132,#43133,#43134,#43135,#43136,#43137,
#43138,#43139,#43140,#43141,#43142,#43143,#43144,#43145,#43146,#43147,#43148,
#43149,#43150,#43151,#43152,#43153,#43154),.UNSPECIFIED.,.F.,.F.,(4,3,3,
3,3,3,3,3,3,3,3,3,3,3,3,3,3,3,3,3,3,3,3,3,3,3,3,3,3,3,3,3,3,3,3,3,3,3,3,
3,3,3,3,3,3,3,3,3,3,3,3,3,3,3,3,3,3,3,3,3,3,3,3,3,3,3,3,3,3,3,3,3,3,4),
(354.999969855631,355.086529058888,355.173173417606,355.261032364908,355.347943982277,
355.436276594545,355.524609206813,355.608347918659,355.691983430026,355.775535873425,
355.859025309276,355.94247925989,356.025915753736,356.109352863491,356.192808658409,
356.276353151138,356.359942234079,356.443665501637,356.524345217533,356.608083929379,
356.691719440746,356.775271884145,356.858761319996,356.942215270609,357.025651764456,
357.109088874211,357.192544669129,357.276089161858,357.359678244799,357.443401512357,
357.524081228253,357.607819940099,357.691455451466,357.775007894865,357.858497330716,
357.94195128133,358.025387775176,358.108824884931,358.192280679848,358.275825172578,
358.359414255519,358.443137523077,358.523817238973,358.607555950819,358.691191462187,
358.774743905585,358.858233341436,358.94168729205,359.025123785896,359.108560895652,
359.192016690569,359.275561183299,359.35915026624,359.442873533798,359.523553249693,
359.607291961539,359.690927472906,359.774479916305,359.857969352156,359.94142330277,
360.024859796616,360.108296906372,360.19175270129,360.275297194019,360.358886276961,
360.442609544518,360.523289260413,360.605987335625,360.688587685776,360.774376530304,
360.856831350972,360.939250049255,361.021655093284,361.031743063889),
 .UNSPECIFIED.);
#279=B_SPLINE_CURVE_WITH_KNOTS('',3,(#43160,#43161,#43162,#43163,#43164,
#43165,#43166,#43167,#43168,#43169,#43170,#43171,#43172,#43173,#43174,#43175,
#43176,#43177,#43178,#43179,#43180,#43181,#43182,#43183,#43184,#43185,#43186,
#43187,#43188,#43189,#43190,#43191,#43192,#43193,#43194,#43195,#43196,#43197,
#43198,#43199,#43200,#43201,#43202,#43203,#43204,#43205,#43206,#43207,#43208,
#43209,#43210,#43211,#43212,#43213,#43214,#43215,#43216,#43217,#43218,#43219,
#43220,#43221,#43222,#43223,#43224,#43225,#43226,#43227,#43228,#43229,#43230,
#43231,#43232,#43233,#43234,#43235,#43236,#43237,#43238,#43239,#43240,#43241,
#43242,#43243,#43244,#43245,#43246,#43247,#43248,#43249,#43250,#43251,#43252,
#43253,#43254,#43255,#43256,#43257,#43258,#43259,#43260,#43261,#43262,#43263,
#43264,#43265,#43266,#43267,#43268,#43269,#43270,#43271,#43272,#43273,#43274,
#43275,#43276,#43277,#43278,#43279,#43280,#43281,#43282,#43283,#43284,#43285,
#43286,#43287,#43288,#43289,#43290,#43291,#43292,#43293,#43294,#43295,#43296,
#43297,#43298,#43299,#43300,#43301,#43302,#43303,#43304,#43305,#43306,#43307,
#43308,#43309,#43310,#43311,#43312,#43313,#43314,#43315,#43316,#43317,#43318,
#43319,#43320,#43321,#43322,#43323,#43324,#43325,#43326,#43327,#43328,#43329,
#43330,#43331,#43332,#43333,#43334,#43335,#43336,#43337,#43338,#43339,#43340,
#43341,#43342,#43343,#43344,#43345,#43346,#43347,#43348,#43349,#43350,#43351,
#43352,#43353,#43354,#43355,#43356,#43357,#43358,#43359,#43360,#43361,#43362,
#43363,#43364,#43365,#43366,#43367,#43368,#43369,#43370,#43371,#43372,#43373,
#43374,#43375,#43376,#43377,#43378,#43379,#43380,#43381,#43382),
 .UNSPECIFIED.,.F.,.F.,(4,3,3,3,3,3,3,3,3,3,3,3,3,3,3,3,3,3,3,3,3,3,3,3,
3,3,3,3,3,3,3,3,3,3,3,3,3,3,3,3,3,3,3,3,3,3,3,3,3,3,3,3,3,3,3,3,3,3,3,3,
3,3,3,3,3,3,3,3,3,3,3,3,3,3,4),(361.283155162929,361.366032816794,361.448813027917,
361.531516694294,361.616635940275,361.699257890964,361.781870921663,361.864493796201,
361.951488012686,362.034232931093,362.117033568309,362.199947972622,362.212470662138,
362.296209373984,362.379844885351,362.46339732875,362.546886764601,362.630340715215,
362.713777209061,362.797214318817,362.880670113734,362.964214606464,363.047803689405,
363.131526956963,363.212206672858,363.295945384704,363.379580896072,363.46313333947,
363.546622775321,363.630076725934,363.713513219781,363.796950329536,363.880406124454,
363.963950617184,364.047539700125,364.131262967682,364.211942683579,364.295681395425,
364.379316906793,364.462869350191,364.546358786043,364.629812736656,364.713249230503,
364.796686340258,364.880142135176,364.963686627905,365.047275710846,365.130998978404,
365.211678694299,365.295417406145,365.379052917512,365.462605360911,365.546094796762,
365.629548747375,365.712985241222,365.796422350977,365.879878145895,365.963422638625,
366.047011721566,366.130734989123,366.211414705019,366.295153416865,366.378788928233,
366.462341371631,366.545830807482,366.629284758095,366.712721251942,366.796158361697,
366.879614156615,366.963158649344,367.046747732285,367.130470999843,367.211150715739,
367.307726271185,367.315827373902),.UNSPECIFIED.);
#280=B_SPLINE_CURVE_WITH_KNOTS('',3,(#43383,#43384,#43385,#43386,#43387,
#43388,#43389,#43390,#43391,#43392,#43393,#43394,#43395),.UNSPECIFIED.,
 .F.,.F.,(4,3,3,3,4),(361.031498889511,361.115135268541,361.198887310602,
361.212734651418,361.283155162806),.UNSPECIFIED.);
#281=B_SPLINE_CURVE_WITH_KNOTS('',3,(#43397,#43398,#43399,#43400,#43401,
#43402,#43403,#43404,#43405,#43406),.UNSPECIFIED.,.F.,.F.,(4,3,3,4),(361.031743063889,
361.114173808488,361.198664485649,361.28315516281),.UNSPECIFIED.);
#282=B_SPLINE_CURVE_WITH_KNOTS('',3,(#43407,#43408,#43409,#43410,#43411,
#43412,#43413,#43414,#43415,#43416,#43417,#43418,#43419,#43420,#43421,#43422,
#43423,#43424,#43425,#43426,#43427,#43428,#43429,#43430,#43431,#43432,#43433,
#43434,#43435,#43436,#43437,#43438,#43439,#43440,#43441,#43442,#43443,#43444,
#43445,#43446,#43447,#43448,#43449,#43450,#43451,#43452,#43453,#43454,#43455,
#43456,#43457,#43458,#43459,#43460,#43461,#43462,#43463,#43464,#43465,#43466,
#43467,#43468,#43469,#43470,#43471,#43472,#43473,#43474,#43475,#43476,#43477,
#43478,#43479,#43480,#43481,#43482,#43483,#43484,#43485,#43486,#43487,#43488,
#43489,#43490,#43491,#43492,#43493,#43494,#43495,#43496,#43497,#43498,#43499,
#43500,#43501,#43502,#43503,#43504,#43505,#43506,#43507,#43508,#43509,#43510,
#43511,#43512,#43513,#43514,#43515,#43516,#43517,#43518,#43519,#43520,#43521,
#43522,#43523,#43524,#43525,#43526,#43527,#43528,#43529,#43530,#43531,#43532,
#43533,#43534,#43535,#43536,#43537,#43538,#43539,#43540,#43541,#43542,#43543,
#43544,#43545,#43546,#43547,#43548,#43549,#43550,#43551,#43552,#43553,#43554,
#43555,#43556,#43557,#43558,#43559,#43560,#43561,#43562,#43563,#43564,#43565,
#43566,#43567,#43568,#43569,#43570,#43571,#43572,#43573,#43574,#43575,#43576,
#43577,#43578,#43579,#43580,#43581,#43582,#43583,#43584,#43585,#43586,#43587,
#43588,#43589,#43590,#43591,#43592,#43593,#43594,#43595,#43596,#43597,#43598,
#43599,#43600,#43601,#43602,#43603,#43604,#43605,#43606,#43607,#43608,#43609,
#43610,#43611,#43612,#43613,#43614,#43615,#43616,#43617,#43618,#43619,#43620,
#43621,#43622,#43623,#43624,#43625,#43626),.UNSPECIFIED.,.F.,.F.,(4,3,3,
3,3,3,3,3,3,3,3,3,3,3,3,3,3,3,3,3,3,3,3,3,3,3,3,3,3,3,3,3,3,3,3,3,3,3,3,
3,3,3,3,3,3,3,3,3,3,3,3,3,3,3,3,3,3,3,3,3,3,3,3,3,3,3,3,3,3,3,3,3,3,4),
(361.283155162958,361.392106189189,361.503854892668,361.523025271134,361.60676398298,
361.690399494347,361.773951937746,361.857441373597,361.940895324211,362.024331818057,
362.107768927812,362.19122472273,362.27476921546,362.358358298401,362.442081565958,
362.522761281854,362.6064999937,362.690135505067,362.773687948466,362.857177384317,
362.94063133493,363.024067828777,363.107504938532,363.19096073345,363.274505226179,
363.35809430912,363.441817576678,363.522497292574,363.60623600442,363.689871515787,
363.773423959186,363.856913395037,363.940367345651,364.023803839497,364.107240949252,
364.19069674417,364.2742412369,364.357830319841,364.441553587398,364.522233303294,
364.60597201514,364.689607526507,364.773159969906,364.856649405757,364.940103356371,
365.023539850217,365.106976959972,365.19043275489,365.27397724762,365.357566330561,
365.441289598119,365.521969314014,365.60570802586,365.689343537227,365.772895980626,
365.856385416477,365.93983936709,366.023275860937,366.106712970692,366.19016876561,
366.27371325834,366.35730234128,366.441025608838,366.521705324734,366.605456569419,
366.689101885749,366.772645767038,366.856132120293,366.939579065989,367.023004694106,
367.106450064674,367.189906018076,367.273422367636,367.31467431478),
 .UNSPECIFIED.);
#283=B_SPLINE_CURVE_WITH_KNOTS('',3,(#43632,#43633,#43634,#43635,#43636,
#43637,#43638,#43639,#43640,#43641,#43642,#43643,#43644,#43645,#43646,#43647,
#43648,#43649,#43650,#43651,#43652,#43653,#43654,#43655,#43656,#43657,#43658,
#43659,#43660,#43661,#43662,#43663,#43664,#43665,#43666,#43667,#43668,#43669,
#43670,#43671,#43672,#43673,#43674,#43675,#43676,#43677,#43678,#43679,#43680,
#43681,#43682,#43683,#43684,#43685,#43686,#43687,#43688,#43689,#43690,#43691,
#43692,#43693,#43694,#43695,#43696,#43697,#43698,#43699,#43700,#43701,#43702,
#43703,#43704,#43705,#43706,#43707,#43708,#43709,#43710,#43711,#43712,#43713,
#43714,#43715,#43716,#43717,#43718,#43719,#43720,#43721,#43722,#43723,#43724,
#43725,#43726,#43727,#43728,#43729,#43730,#43731,#43732,#43733,#43734,#43735,
#43736,#43737,#43738,#43739,#43740,#43741,#43742,#43743,#43744,#43745,#43746,
#43747,#43748,#43749,#43750,#43751,#43752,#43753,#43754,#43755,#43756,#43757,
#43758,#43759,#43760,#43761,#43762,#43763,#43764,#43765,#43766,#43767,#43768,
#43769,#43770,#43771,#43772,#43773,#43774,#43775,#43776,#43777,#43778,#43779,
#43780,#43781,#43782,#43783,#43784,#43785,#43786,#43787,#43788,#43789,#43790,
#43791,#43792,#43793,#43794,#43795,#43796,#43797,#43798,#43799,#43800,#43801,
#43802,#43803,#43804,#43805,#43806,#43807,#43808,#43809,#43810,#43811,#43812,
#43813,#43814,#43815,#43816,#43817,#43818,#43819,#43820,#43821,#43822,#43823,
#43824,#43825,#43826,#43827,#43828,#43829,#43830,#43831,#43832,#43833,#43834,
#43835,#43836,#43837,#43838,#43839,#43840,#43841,#43842,#43843,#43844,#43845,
#43846,#43847,#43848,#43849,#43850,#43851),.UNSPECIFIED.,.F.,.F.,(4,3,3,
3,3,3,3,3,3,3,3,3,3,3,3,3,3,3,3,3,3,3,3,3,3,3,3,3,3,3,3,3,3,3,3,3,3,3,3,
3,3,3,3,3,3,3,3,3,3,3,3,3,3,3,3,3,3,3,3,3,3,3,3,3,3,3,3,3,3,3,3,3,3,4),
(367.566340469986,367.650059493962,367.733775454788,367.817506009342,367.9012688201,
367.985134653745,368.069056243052,368.153114776464,368.210886726459,368.294625438305,
368.378260949673,368.461813393071,368.545302828922,368.628756779536,368.712193273382,
368.795630383138,368.879086178055,368.962630670785,369.046219753726,369.129943021284,
369.210622737179,369.294361449025,369.377996960392,369.461549403791,369.545038839641,
369.628492790255,369.711929284101,369.795366393857,369.878822188774,369.962366681504,
370.045955764445,370.129679032002,370.210358747899,370.294097459745,370.377732971112,
370.461285414511,370.544774850362,370.628228800976,370.711665294822,370.795102404578,
370.878558199495,370.962102692225,371.045691775166,371.129415042724,371.210094758619,
371.293833470465,371.377468981833,371.461021425232,371.544510861083,371.627964811697,
371.711401305543,371.794838415299,371.878294210217,371.961838702947,372.045427785888,
372.129151053445,372.20983076934,372.293569481186,372.377204992554,372.460757435952,
372.544246871803,372.627700822417,372.711137316264,372.794574426019,372.878030220937,
372.961574713667,373.045163796608,373.128887064166,373.20956678006,373.293731515783,
373.377756473631,373.461700952373,373.545568914742,373.598723849892),
 .UNSPECIFIED.);
#284=B_SPLINE_CURVE_WITH_KNOTS('',3,(#43852,#43853,#43854,#43855,#43856,
#43857,#43858,#43859,#43860,#43861),.UNSPECIFIED.,.F.,.F.,(4,3,3,4),(367.315827373902,
367.411842954212,367.507175834098,367.566340469788),.UNSPECIFIED.);
#285=B_SPLINE_CURVE_WITH_KNOTS('',3,(#43863,#43864,#43865,#43866,#43867,
#43868,#43869,#43870,#43871,#43872,#43873,#43874,#43875),.UNSPECIFIED.,
 .F.,.F.,(4,3,3,3,4),(367.31467431478,367.398291381823,367.482030912403,
367.521441335454,367.56634046999),.UNSPECIFIED.);
#286=B_SPLINE_CURVE_WITH_KNOTS('',3,(#43876,#43877,#43878,#43879,#43880,
#43881,#43882,#43883,#43884,#43885,#43886,#43887,#43888,#43889,#43890,#43891,
#43892,#43893,#43894,#43895,#43896,#43897,#43898,#43899,#43900,#43901,#43902,
#43903,#43904,#43905,#43906,#43907,#43908,#43909,#43910,#43911,#43912,#43913,
#43914,#43915,#43916,#43917,#43918,#43919,#43920,#43921,#43922,#43923,#43924,
#43925,#43926,#43927,#43928,#43929,#43930,#43931,#43932,#43933,#43934,#43935,
#43936,#43937,#43938,#43939,#43940,#43941,#43942,#43943,#43944,#43945,#43946,
#43947,#43948,#43949,#43950,#43951,#43952,#43953,#43954,#43955,#43956,#43957,
#43958,#43959,#43960,#43961,#43962,#43963,#43964,#43965,#43966,#43967,#43968,
#43969,#43970,#43971,#43972,#43973,#43974,#43975,#43976,#43977,#43978,#43979,
#43980,#43981,#43982,#43983,#43984,#43985,#43986,#43987,#43988,#43989,#43990,
#43991,#43992,#43993,#43994,#43995,#43996,#43997,#43998,#43999,#44000,#44001,
#44002,#44003,#44004,#44005,#44006,#44007,#44008,#44009,#44010,#44011,#44012,
#44013,#44014,#44015,#44016,#44017,#44018,#44019,#44020,#44021,#44022,#44023,
#44024,#44025,#44026,#44027,#44028,#44029,#44030,#44031,#44032,#44033,#44034,
#44035,#44036,#44037,#44038,#44039,#44040,#44041,#44042,#44043,#44044,#44045,
#44046,#44047,#44048,#44049,#44050,#44051,#44052,#44053,#44054,#44055,#44056,
#44057,#44058,#44059,#44060,#44061,#44062,#44063,#44064,#44065,#44066,#44067,
#44068,#44069,#44070,#44071,#44072,#44073,#44074,#44075,#44076,#44077,#44078,
#44079,#44080,#44081,#44082,#44083,#44084,#44085,#44086,#44087,#44088,#44089,
#44090,#44091,#44092,#44093,#44094,#44095),.UNSPECIFIED.,.F.,.F.,(4,3,3,
3,3,3,3,3,3,3,3,3,3,3,3,3,3,3,3,3,3,3,3,3,3,3,3,3,3,3,3,3,3,3,3,3,3,3,3,
3,3,3,3,3,3,3,3,3,3,3,3,3,3,3,3,3,3,3,3,3,3,3,3,3,3,3,3,3,3,3,3,3,3,4),
(367.566340470175,367.649481447308,367.732521837641,367.815482341599,367.898383582848,
367.981254713856,368.064112809716,368.146976452127,368.229864223374,368.312841649614,
368.395869528455,368.479019551326,368.521177346175,368.604916058021,368.688551569388,
368.772104012787,368.855593448637,368.939047399251,369.022483893097,369.105921002853,
369.189376797771,369.2729212905,369.356510373441,369.440233640999,369.520913356895,
369.604652068741,369.688287580108,369.771840023507,369.855329459358,369.938783409972,
370.022219903818,370.105657013573,370.189112808491,370.272657301221,370.356246384162,
370.439969651719,370.520649367615,370.604388079461,370.688023590828,370.771576034227,
370.855065470078,370.938519420692,371.021955914538,371.105393024293,371.18884881921,
371.27239331194,371.355982394881,371.439705662439,371.520385378335,371.604124090181,
371.687759601548,371.771312044947,371.854801480797,371.938255431411,372.021691925257,
372.105129035013,372.188584829931,372.272129322661,372.355718405602,372.439441673159,
372.520121389055,372.603860100901,372.687495612268,372.771048055667,372.854537491519,
372.937991442132,373.021427935979,373.104865045735,373.188320840653,373.271865333382,
373.355454416323,373.439177683881,373.519857399775,373.598902653178),
 .UNSPECIFIED.);
#287=B_SPLINE_CURVE_WITH_KNOTS('',3,(#44101,#44102,#44103,#44104,#44105,
#44106,#44107,#44108,#44109,#44110,#44111,#44112,#44113,#44114,#44115,#44116,
#44117,#44118,#44119,#44120,#44121,#44122,#44123,#44124,#44125,#44126,#44127,
#44128,#44129,#44130,#44131,#44132,#44133,#44134,#44135,#44136,#44137,#44138,
#44139,#44140,#44141,#44142,#44143,#44144,#44145,#44146,#44147,#44148,#44149,
#44150,#44151,#44152,#44153,#44154,#44155,#44156,#44157,#44158,#44159,#44160,
#44161,#44162,#44163,#44164,#44165,#44166,#44167,#44168,#44169,#44170,#44171,
#44172,#44173,#44174,#44175,#44176,#44177,#44178,#44179,#44180,#44181,#44182,
#44183,#44184,#44185,#44186,#44187,#44188,#44189,#44190,#44191,#44192,#44193,
#44194,#44195,#44196,#44197,#44198,#44199,#44200,#44201,#44202,#44203,#44204,
#44205,#44206,#44207,#44208,#44209,#44210,#44211,#44212,#44213,#44214,#44215,
#44216,#44217,#44218,#44219,#44220,#44221,#44222,#44223,#44224,#44225,#44226,
#44227,#44228,#44229,#44230,#44231,#44232,#44233,#44234,#44235,#44236,#44237,
#44238,#44239,#44240,#44241,#44242,#44243,#44244,#44245,#44246,#44247,#44248,
#44249,#44250,#44251,#44252,#44253,#44254,#44255,#44256,#44257,#44258,#44259,
#44260,#44261,#44262,#44263,#44264,#44265,#44266,#44267,#44268,#44269,#44270,
#44271,#44272,#44273,#44274,#44275,#44276,#44277,#44278,#44279,#44280,#44281,
#44282,#44283,#44284,#44285,#44286,#44287,#44288,#44289,#44290,#44291,#44292,
#44293,#44294,#44295,#44296,#44297,#44298,#44299,#44300,#44301,#44302,#44303,
#44304,#44305,#44306,#44307,#44308,#44309,#44310,#44311,#44312,#44313,#44314,
#44315,#44316,#44317),.UNSPECIFIED.,.F.,.F.,(4,3,3,3,3,3,3,3,3,3,3,3,3,
3,3,3,3,3,3,3,3,3,3,3,3,3,3,3,3,3,3,3,3,3,3,3,3,3,3,3,3,3,3,3,3,3,3,3,3,
3,3,3,3,3,3,3,3,3,3,3,3,3,3,3,3,3,3,3,3,3,3,3,4),(373.849525777362,373.944580138424,
374.040061204896,374.136110618714,374.20930279078,374.293041502626,374.376677013994,
374.460229457392,374.543718893243,374.627172843857,374.710609337703,374.794046447459,
374.877502242376,374.961046735106,375.044635818047,375.128359085605,375.2090388015,
375.292777513346,375.376413024713,375.459965468112,375.543454903963,375.626908854576,
375.710345348423,375.793782458178,375.877238253096,375.960782745825,376.044371828766,
376.128095096324,376.20877481222,376.292513524066,376.376149035433,376.459701478832,
376.543190914683,376.626644865296,376.710081359143,376.793518468898,376.876974263816,
376.960518756545,377.044107839486,377.127831107044,377.20851082294,377.292249534786,
377.375885046153,377.459437489552,377.542926925403,377.626380876017,377.709817369863,
377.793254479618,377.876710274536,377.960254767266,378.043843850207,378.127567117764,
378.20824683366,378.291985545506,378.375621056873,378.459173500272,378.542662936123,
378.626116886737,378.709553380583,378.792990490338,378.876446285256,378.959990777986,
379.043579860927,379.127303128484,379.20798284438,379.292094589826,379.374844615425,
379.457519348592,379.540137680491,379.625322462356,379.707896657838,379.794386732894,
379.880876807951),.UNSPECIFIED.);
#288=B_SPLINE_CURVE_WITH_KNOTS('',3,(#44318,#44319,#44320,#44321,#44322,
#44323,#44324,#44325,#44326,#44327),.UNSPECIFIED.,.F.,.F.,(4,3,3,4),(373.598723849892,
373.682523139848,373.766320497947,373.849525777165),.UNSPECIFIED.);
#289=B_SPLINE_CURVE_WITH_KNOTS('',3,(#44329,#44330,#44331,#44332,#44333,
#44334,#44335,#44336,#44337,#44338),.UNSPECIFIED.,.F.,.F.,(4,3,3,4),(373.598902653178,
373.697309312522,373.794823155724,373.849525776986),.UNSPECIFIED.);
#290=B_SPLINE_CURVE_WITH_KNOTS('',3,(#44339,#44340,#44341,#44342,#44343,
#44344,#44345,#44346,#44347,#44348,#44349,#44350,#44351,#44352,#44353,#44354,
#44355,#44356,#44357,#44358,#44359,#44360,#44361,#44362,#44363,#44364,#44365,
#44366,#44367,#44368,#44369,#44370,#44371,#44372,#44373,#44374,#44375,#44376,
#44377,#44378,#44379,#44380,#44381,#44382,#44383,#44384,#44385,#44386,#44387,
#44388,#44389,#44390,#44391,#44392,#44393,#44394,#44395,#44396,#44397,#44398,
#44399,#44400,#44401,#44402,#44403,#44404,#44405,#44406,#44407,#44408,#44409,
#44410,#44411,#44412,#44413,#44414,#44415,#44416,#44417,#44418,#44419,#44420,
#44421,#44422,#44423,#44424,#44425,#44426,#44427,#44428,#44429,#44430,#44431,
#44432,#44433,#44434,#44435,#44436,#44437,#44438,#44439,#44440,#44441,#44442,
#44443,#44444,#44445,#44446,#44447,#44448,#44449,#44450,#44451,#44452,#44453,
#44454,#44455,#44456,#44457,#44458,#44459,#44460,#44461,#44462,#44463,#44464,
#44465,#44466,#44467,#44468,#44469,#44470,#44471,#44472,#44473,#44474,#44475,
#44476,#44477,#44478,#44479,#44480,#44481,#44482,#44483,#44484,#44485,#44486,
#44487,#44488,#44489,#44490,#44491,#44492,#44493,#44494,#44495,#44496,#44497,
#44498,#44499,#44500,#44501,#44502,#44503,#44504,#44505,#44506,#44507,#44508,
#44509,#44510,#44511,#44512,#44513,#44514,#44515,#44516,#44517,#44518,#44519,
#44520,#44521,#44522,#44523,#44524,#44525,#44526,#44527,#44528,#44529,#44530,
#44531,#44532,#44533,#44534,#44535,#44536,#44537,#44538,#44539,#44540,#44541,
#44542,#44543,#44544,#44545,#44546,#44547,#44548,#44549,#44550,#44551,#44552,
#44553,#44554,#44555,#44556,#44557,#44558),.UNSPECIFIED.,.F.,.F.,(4,3,3,
3,3,3,3,3,3,3,3,3,3,3,3,3,3,3,3,3,3,3,3,3,3,3,3,3,3,3,3,3,3,3,3,3,3,3,3,
3,3,3,3,3,3,3,3,3,3,3,3,3,3,3,3,3,3,3,3,3,3,3,3,3,3,3,3,3,3,3,3,3,3,4),
(373.849525777169,373.933284231335,374.016605576888,374.099930113727,374.183275958349,
374.267355321385,374.350842682452,374.435218046474,374.519593410495,374.603332122341,
374.686967633709,374.770520077107,374.854009512958,374.937463463572,375.020899957418,
375.104337067174,375.187792862091,375.271337354821,375.354926437762,375.43864970532,
375.519329421215,375.603068133061,375.686703644428,375.770256087827,375.853745523678,
375.937199474292,376.020635968138,376.104073077894,376.187528872811,376.271073365541,
376.354662448482,376.43838571604,376.519065431936,376.602804143782,376.686439655149,
376.769992098548,376.853481534399,376.936935485012,377.020371978859,377.103809088614,
377.187264883532,377.270809376262,377.354398459203,377.43812172676,377.518801442656,
377.602540154502,377.686175665869,377.769728109268,377.853217545119,377.936671495733,
378.020107989579,378.103545099334,378.187000894251,378.270545386981,378.354134469922,
378.437857737479,378.518537453376,378.602276165222,378.68591167659,378.769464119989,
378.85295355584,378.936407506454,379.0198440003,379.103281110055,379.186736904973,
379.270281397703,379.353870480644,379.437593748202,379.518273464096,379.602951023663,
379.687482586612,379.771929460174,379.856291871132,379.882028760327),
 .UNSPECIFIED.);
#291=B_SPLINE_CURVE_WITH_KNOTS('',3,(#44564,#44565,#44566,#44567,#44568,
#44569,#44570,#44571,#44572,#44573,#44574,#44575,#44576,#44577,#44578,#44579,
#44580,#44581,#44582,#44583,#44584,#44585,#44586,#44587,#44588,#44589,#44590,
#44591,#44592,#44593,#44594,#44595,#44596,#44597,#44598,#44599,#44600,#44601,
#44602,#44603,#44604,#44605,#44606,#44607,#44608,#44609,#44610,#44611,#44612,
#44613,#44614,#44615,#44616,#44617,#44618,#44619,#44620,#44621,#44622,#44623,
#44624,#44625,#44626,#44627,#44628,#44629,#44630,#44631,#44632,#44633,#44634,
#44635,#44636,#44637,#44638,#44639,#44640,#44641,#44642,#44643,#44644,#44645,
#44646,#44647,#44648,#44649,#44650,#44651,#44652,#44653,#44654,#44655,#44656,
#44657,#44658,#44659,#44660,#44661,#44662,#44663,#44664,#44665,#44666,#44667,
#44668,#44669,#44670,#44671,#44672,#44673,#44674,#44675,#44676,#44677,#44678,
#44679,#44680,#44681,#44682,#44683,#44684,#44685,#44686,#44687,#44688,#44689,
#44690,#44691,#44692,#44693,#44694,#44695,#44696,#44697,#44698,#44699,#44700,
#44701,#44702,#44703,#44704,#44705,#44706,#44707,#44708,#44709,#44710,#44711,
#44712,#44713,#44714,#44715,#44716,#44717,#44718,#44719,#44720,#44721,#44722,
#44723,#44724,#44725,#44726,#44727,#44728,#44729,#44730,#44731,#44732,#44733,
#44734,#44735,#44736,#44737,#44738,#44739,#44740,#44741,#44742,#44743,#44744,
#44745,#44746,#44747,#44748,#44749,#44750,#44751,#44752,#44753,#44754,#44755,
#44756,#44757,#44758,#44759,#44760,#44761,#44762,#44763,#44764,#44765,#44766,
#44767,#44768,#44769,#44770,#44771,#44772,#44773,#44774,#44775,#44776,#44777,
#44778,#44779,#44780,#44781,#44782,#44783),.UNSPECIFIED.,.F.,.F.,(4,3,3,
3,3,3,3,3,3,3,3,3,3,3,3,3,3,3,3,3,3,3,3,3,3,3,3,3,3,3,3,3,3,3,3,3,3,3,3,
3,3,3,3,3,3,3,3,3,3,3,3,3,3,3,3,3,3,3,3,3,3,3,3,3,3,3,3,3,3,3,3,3,3,4),
(380.132711084345,380.207718855101,380.291457566947,380.375093078314,380.458645521713,
380.542134957564,380.625588908178,380.709025402024,380.792462511779,380.875918306697,
380.959462799426,381.043051882367,381.126775149925,381.207454865821,381.291193577667,
381.374829089034,381.458381532433,381.541870968284,381.625324918898,381.708761412744,
381.792198522499,381.875654317417,381.959198810147,382.042787893087,382.126511160645,
382.207190876541,382.290929588387,382.374565099754,382.458117543153,382.541606979004,
382.625060929618,382.708497423464,382.791934533219,382.875390328137,382.958934820867,
383.042523903807,383.126247171365,383.206926887261,383.290665599107,383.374301110474,
383.457853553873,383.541342989724,383.624796940338,383.708233434184,383.791670543939,
383.875126338857,383.958670831587,384.042259914528,384.125983182085,384.206662897981,
384.290401609827,384.374037121194,384.457589564593,384.541079000444,384.624532951058,
384.707969444904,384.791406554659,384.874862349577,384.958406842306,385.041995925247,
385.125719192805,385.206398908701,385.290139984778,385.373777312587,385.457331026953,
385.540821190055,385.624273118317,385.707706815389,385.791140353452,385.874591800591,
385.958121435581,386.041695340788,386.125379138116,386.164603019142),
 .UNSPECIFIED.);
#292=B_SPLINE_CURVE_WITH_KNOTS('',3,(#44784,#44785,#44786,#44787,#44788,
#44789,#44790,#44791,#44792,#44793),.UNSPECIFIED.,.F.,.F.,(4,3,3,4),(379.880876807951,
379.963568450344,380.048139767281,380.132711084218),.UNSPECIFIED.);
#293=B_SPLINE_CURVE_WITH_KNOTS('',3,(#44795,#44796,#44797,#44798,#44799,
#44800,#44801,#44802,#44803,#44804),.UNSPECIFIED.,.F.,.F.,(4,3,3,4),(379.882028760327,
379.966318027482,380.050584953051,380.132711084349),.UNSPECIFIED.);
#294=B_SPLINE_CURVE_WITH_KNOTS('',3,(#44805,#44806,#44807,#44808,#44809,
#44810,#44811,#44812,#44813,#44814,#44815,#44816,#44817,#44818,#44819,#44820,
#44821,#44822,#44823,#44824,#44825,#44826,#44827,#44828,#44829,#44830,#44831,
#44832,#44833,#44834,#44835,#44836,#44837,#44838,#44839,#44840,#44841,#44842,
#44843,#44844,#44845,#44846,#44847,#44848,#44849,#44850,#44851,#44852,#44853,
#44854,#44855,#44856,#44857,#44858,#44859,#44860,#44861,#44862,#44863,#44864,
#44865,#44866,#44867,#44868,#44869,#44870,#44871,#44872,#44873,#44874,#44875,
#44876,#44877,#44878,#44879,#44880,#44881,#44882,#44883,#44884,#44885,#44886,
#44887,#44888,#44889,#44890,#44891,#44892,#44893,#44894,#44895,#44896,#44897,
#44898,#44899,#44900,#44901,#44902,#44903,#44904,#44905,#44906,#44907,#44908,
#44909,#44910,#44911,#44912,#44913,#44914,#44915,#44916,#44917,#44918,#44919,
#44920,#44921,#44922,#44923,#44924,#44925,#44926,#44927,#44928,#44929,#44930,
#44931,#44932,#44933,#44934,#44935,#44936,#44937,#44938,#44939,#44940,#44941,
#44942,#44943,#44944,#44945,#44946,#44947,#44948,#44949,#44950,#44951,#44952,
#44953,#44954,#44955,#44956,#44957,#44958,#44959,#44960,#44961,#44962,#44963,
#44964,#44965,#44966,#44967,#44968,#44969,#44970,#44971,#44972,#44973,#44974,
#44975,#44976,#44977,#44978,#44979,#44980,#44981,#44982,#44983,#44984,#44985,
#44986,#44987,#44988,#44989,#44990,#44991,#44992,#44993,#44994,#44995,#44996,
#44997,#44998,#44999,#45000,#45001,#45002,#45003,#45004,#45005,#45006,#45007,
#45008,#45009,#45010,#45011,#45012,#45013,#45014,#45015,#45016,#45017,#45018,
#45019,#45020,#45021),.UNSPECIFIED.,.F.,.F.,(4,3,3,3,3,3,3,3,3,3,3,3,3,
3,3,3,3,3,3,3,3,3,3,3,3,3,3,3,3,3,3,3,3,3,3,3,3,3,3,3,3,3,3,3,3,3,3,3,3,
3,3,3,3,3,3,3,3,3,3,3,3,3,3,3,3,3,3,3,3,3,3,3,4),(380.132711084541,380.22903568211,
380.322609168171,380.420309321493,380.518009474816,380.601748186662,380.685383698029,
380.768936141428,380.852425577279,380.935879527893,381.019316021739,381.102753131494,
381.186208926412,381.269753419141,381.353342502082,381.43706576964,381.517745485536,
381.601484197382,381.685119708749,381.768672152148,381.852161587999,381.935615538612,
382.019052032458,382.102489142214,382.185944937131,382.269489429861,382.353078512802,
382.43680178036,382.517481496256,382.601220208102,382.68485571947,382.768408162868,
382.851897598719,382.935351549333,383.018788043179,383.102225152935,383.185680947853,
383.269225440583,383.352814523524,383.436537791081,383.517217506976,383.600956218822,
383.684591730189,383.768144173588,383.851633609439,383.935087560053,384.018524053899,
384.101961163654,384.185416958572,384.268961451302,384.352550534243,384.4362738018,
384.516953517697,384.600692229543,384.684327740911,384.767880184309,384.85136962016,
384.934823570774,385.01826006462,385.101697174376,385.185152969293,385.268697462023,
385.352286544964,385.436009812522,385.516689528417,385.599356995582,385.681929889722,
385.764427294063,385.846868223446,385.929281659743,386.011676716368,386.094100583877,
386.16406292974),.UNSPECIFIED.);
#295=B_SPLINE_CURVE_WITH_KNOTS('',3,(#45027,#45028,#45029,#45030,#45031,
#45032,#45033,#45034,#45035,#45036,#45037,#45038,#45039,#45040,#45041,#45042,
#45043,#45044,#45045,#45046,#45047,#45048,#45049,#45050,#45051,#45052,#45053,
#45054,#45055,#45056,#45057,#45058,#45059,#45060,#45061,#45062,#45063,#45064,
#45065,#45066,#45067,#45068,#45069,#45070,#45071,#45072,#45073,#45074,#45075,
#45076,#45077,#45078,#45079,#45080,#45081,#45082,#45083,#45084,#45085,#45086,
#45087,#45088,#45089,#45090,#45091,#45092,#45093,#45094,#45095,#45096,#45097,
#45098,#45099,#45100,#45101,#45102,#45103,#45104,#45105,#45106,#45107,#45108,
#45109,#45110,#45111,#45112,#45113,#45114,#45115,#45116,#45117,#45118,#45119,
#45120,#45121,#45122,#45123,#45124,#45125,#45126,#45127,#45128,#45129,#45130,
#45131,#45132,#45133,#45134,#45135,#45136,#45137,#45138,#45139,#45140,#45141,
#45142,#45143,#45144,#45145,#45146,#45147,#45148,#45149,#45150,#45151,#45152,
#45153,#45154,#45155,#45156,#45157,#45158,#45159,#45160,#45161,#45162,#45163,
#45164,#45165,#45166,#45167,#45168,#45169,#45170,#45171,#45172,#45173,#45174,
#45175,#45176,#45177,#45178,#45179,#45180,#45181,#45182,#45183,#45184,#45185,
#45186,#45187,#45188,#45189,#45190,#45191,#45192,#45193,#45194,#45195,#45196,
#45197,#45198,#45199,#45200,#45201,#45202,#45203,#45204,#45205,#45206,#45207,
#45208,#45209,#45210,#45211,#45212,#45213,#45214,#45215,#45216,#45217,#45218,
#45219,#45220,#45221,#45222,#45223,#45224,#45225,#45226,#45227,#45228,#45229,
#45230,#45231,#45232,#45233,#45234,#45235,#45236,#45237,#45238,#45239,#45240,
#45241,#45242,#45243,#45244,#45245,#45246),.UNSPECIFIED.,.F.,.F.,(4,3,3,
3,3,3,3,3,3,3,3,3,3,3,3,3,3,3,3,3,3,3,3,3,3,3,3,3,3,3,3,3,3,3,3,3,3,3,3,
3,3,3,3,3,3,3,3,3,3,3,3,3,3,3,3,3,3,3,3,3,3,3,3,3,3,3,3,3,3,3,3,3,3,4),
(386.415896391665,386.498292671986,386.580622865556,386.662914389823,386.74518752001,
386.827461248823,386.909754567193,386.992133513426,387.074559610852,387.157107949862,
387.205870930141,387.289609641987,387.373245153355,387.456797596753,387.540287032604,
387.623740983218,387.707177477064,387.790614586819,387.874070381737,387.957614874467,
388.041203957408,388.124927224965,388.205606940862,388.289345652708,388.372981164076,
388.456533607474,388.540023043325,388.623476993939,388.706913487785,388.790350597541,
388.873806392459,388.957350885188,389.04093996813,389.124663235687,389.205342951582,
389.289081663428,389.372717174795,389.456269618194,389.539759054044,389.623213004658,
389.706649498504,389.790086608259,389.873542403177,389.957086895907,390.040675978848,
390.124399246405,390.205078962302,390.288817674148,390.372453185516,390.456005628914,
390.539495064766,390.622949015379,390.706385509225,390.789822618981,390.873278413898,
390.956822906628,391.040411989569,391.124135257126,391.204814973022,391.288553684868,
391.372189196236,391.455741639634,391.539231075485,391.622685026098,391.706121519945,
391.7895586297,391.873014424618,391.956558917348,392.040148000289,392.123871267847,
392.204550983742,392.292821373478,392.380892514915,392.448760640207),
 .UNSPECIFIED.);
#296=B_SPLINE_CURVE_WITH_KNOTS('',3,(#45247,#45248,#45249,#45250,#45251,
#45252,#45253,#45254,#45255,#45256),.UNSPECIFIED.,.F.,.F.,(4,3,3,4),(386.164603019142,
386.206134919421,386.323526732866,386.415896391525),.UNSPECIFIED.);
#297=B_SPLINE_CURVE_WITH_KNOTS('',3,(#45258,#45259,#45260,#45261,#45262,
#45263,#45264,#45265,#45266,#45267),.UNSPECIFIED.,.F.,.F.,(4,3,3,4),(386.16406292974,
386.246561874291,386.331229132842,386.415896391393),.UNSPECIFIED.);
#298=B_SPLINE_CURVE_WITH_KNOTS('',3,(#45268,#45269,#45270,#45271,#45272,
#45273,#45274,#45275,#45276,#45277,#45278,#45279,#45280,#45281,#45282,#45283,
#45284,#45285,#45286,#45287,#45288,#45289,#45290,#45291,#45292,#45293,#45294,
#45295,#45296,#45297,#45298,#45299,#45300,#45301,#45302,#45303,#45304,#45305,
#45306,#45307,#45308,#45309,#45310,#45311,#45312,#45313,#45314,#45315,#45316,
#45317,#45318,#45319,#45320,#45321,#45322,#45323,#45324,#45325,#45326,#45327,
#45328,#45329,#45330,#45331,#45332,#45333,#45334,#45335,#45336,#45337,#45338,
#45339,#45340,#45341,#45342,#45343,#45344,#45345,#45346,#45347,#45348,#45349,
#45350,#45351,#45352,#45353,#45354,#45355,#45356,#45357,#45358,#45359,#45360,
#45361,#45362,#45363,#45364,#45365,#45366,#45367,#45368,#45369,#45370,#45371,
#45372,#45373,#45374,#45375,#45376,#45377,#45378,#45379,#45380,#45381,#45382,
#45383,#45384,#45385,#45386,#45387,#45388,#45389,#45390,#45391,#45392,#45393,
#45394,#45395,#45396,#45397,#45398,#45399,#45400,#45401,#45402,#45403,#45404,
#45405,#45406,#45407,#45408,#45409,#45410,#45411,#45412,#45413,#45414,#45415,
#45416,#45417,#45418,#45419,#45420,#45421,#45422,#45423,#45424,#45425,#45426,
#45427,#45428,#45429,#45430,#45431,#45432,#45433,#45434,#45435,#45436,#45437,
#45438,#45439,#45440,#45441,#45442,#45443,#45444,#45445,#45446,#45447,#45448,
#45449,#45450,#45451,#45452,#45453,#45454,#45455,#45456,#45457,#45458,#45459,
#45460,#45461,#45462,#45463,#45464,#45465,#45466,#45467,#45468,#45469,#45470,
#45471,#45472,#45473,#45474,#45475,#45476,#45477,#45478,#45479,#45480,#45481,
#45482,#45483,#45484,#45485,#45486,#45487),.UNSPECIFIED.,.F.,.F.,(4,3,3,
3,3,3,3,3,3,3,3,3,3,3,3,3,3,3,3,3,3,3,3,3,3,3,3,3,3,3,3,3,3,3,3,3,3,3,3,
3,3,3,3,3,3,3,3,3,3,3,3,3,3,3,3,3,3,3,3,3,3,3,3,3,3,3,3,3,3,3,3,3,3,4),
(386.415896391529,386.516425539137,386.600164250983,386.68379976235,386.767352205749,
386.8508416416,386.934295592214,387.01773208606,387.101169195815,387.184624990733,
387.268169483463,387.351758566404,387.435481833961,387.516161549857,387.599900261703,
387.68353577307,387.767088216469,387.85057765232,387.934031602934,388.01746809678,
388.100905206535,388.184361001453,388.267905494183,388.351494577124,388.435217844681,
388.515897560577,388.599636272423,388.68327178379,388.766824227189,388.85031366304,
388.933767613654,389.0172041075,389.100641217255,389.184097012173,389.267641504903,
389.351230587844,389.434953855401,389.515633571297,389.599372283143,389.68300779451,
389.766560237909,389.85004967376,389.933503624373,390.01694011822,390.100377227975,
390.183833022893,390.267377515622,390.350966598563,390.434689866121,390.515369582017,
390.599108293863,390.682743805231,390.766296248629,390.84978568448,390.933239635094,
391.01667612894,391.100113238696,391.183569033614,391.267113526343,391.350702609284,
391.434425876842,391.515105592737,391.59884816637,391.682486653621,391.76604119076,
391.851245732208,391.934696000301,392.01812793045,392.101559594379,392.18808907637,
392.271612247594,392.355180424172,392.438844357499,392.447677522342),
 .UNSPECIFIED.);
#299=B_SPLINE_CURVE_WITH_KNOTS('',3,(#45493,#45494,#45495,#45496,#45497,
#45498,#45499,#45500,#45501,#45502,#45503,#45504,#45505,#45506,#45507,#45508,
#45509,#45510,#45511,#45512,#45513,#45514,#45515,#45516,#45517,#45518,#45519,
#45520,#45521,#45522,#45523,#45524,#45525,#45526,#45527,#45528,#45529,#45530,
#45531,#45532,#45533,#45534,#45535,#45536,#45537,#45538,#45539,#45540,#45541,
#45542,#45543,#45544,#45545,#45546,#45547,#45548,#45549,#45550,#45551,#45552,
#45553,#45554,#45555,#45556,#45557,#45558,#45559,#45560,#45561,#45562,#45563,
#45564,#45565,#45566,#45567,#45568,#45569,#45570,#45571,#45572,#45573,#45574,
#45575,#45576,#45577,#45578,#45579,#45580,#45581,#45582,#45583,#45584,#45585,
#45586,#45587,#45588,#45589,#45590,#45591,#45592,#45593,#45594,#45595,#45596,
#45597,#45598,#45599,#45600,#45601,#45602,#45603,#45604,#45605,#45606,#45607,
#45608,#45609,#45610,#45611,#45612,#45613,#45614,#45615,#45616,#45617,#45618,
#45619,#45620,#45621,#45622,#45623,#45624,#45625,#45626,#45627,#45628,#45629,
#45630,#45631,#45632,#45633,#45634,#45635,#45636,#45637,#45638,#45639,#45640,
#45641,#45642,#45643,#45644,#45645,#45646,#45647,#45648,#45649,#45650,#45651,
#45652,#45653,#45654,#45655,#45656,#45657,#45658,#45659,#45660,#45661,#45662,
#45663,#45664,#45665,#45666,#45667,#45668,#45669,#45670,#45671,#45672,#45673,
#45674,#45675,#45676,#45677,#45678,#45679,#45680,#45681,#45682,#45683,#45684,
#45685,#45686,#45687,#45688,#45689,#45690,#45691,#45692,#45693,#45694,#45695,
#45696,#45697,#45698,#45699,#45700,#45701,#45702,#45703,#45704,#45705,#45706,
#45707,#45708,#45709,#45710,#45711,#45712),.UNSPECIFIED.,.F.,.F.,(4,3,3,
3,3,3,3,3,3,3,3,3,3,3,3,3,3,3,3,3,3,3,3,3,3,3,3,3,3,3,3,3,3,3,3,3,3,3,3,
3,3,3,3,3,3,3,3,3,3,3,3,3,3,3,3,3,3,3,3,3,3,3,3,3,3,3,3,3,3,3,3,3,3,4),
(392.699081698704,392.786294770962,392.873615936636,392.961136976178,393.048762586095,
393.136588210556,393.204286994462,393.288025706308,393.371661217676,393.455213661074,
393.538703096925,393.622157047539,393.705593541386,393.789030651141,393.872486446059,
393.956030938789,394.03962002173,394.123343289288,394.204023005182,394.287761717028,
394.371397228395,394.454949671794,394.538439107645,394.621893058259,394.705329552105,
394.78876666186,394.872222456778,394.955766949508,395.039356032449,395.123079300006,
395.203759015903,395.287497727749,395.371133239117,395.454685682515,395.538175118366,
395.62162906898,395.705065562826,395.788502672582,395.871958467499,395.955502960229,
396.03909204317,396.122815310728,396.203495026623,396.287233738469,396.370869249836,
396.454421693235,396.537911129085,396.621365079699,396.704801573545,396.7882386833,
396.871694478217,396.955238970947,397.038828053888,397.122551321445,397.203231037343,
397.286969749189,397.370605260557,397.454157703955,397.537647139806,397.62110109042,
397.704537584266,397.787974694022,397.871430488939,397.954974981669,398.03856406461,
398.122287332168,398.202967048063,398.285558302687,398.368052705527,398.450469410997,
398.532823591639,398.615141709484,398.697450817903,398.730765351708),
 .UNSPECIFIED.);
#300=B_SPLINE_CURVE_WITH_KNOTS('',3,(#45713,#45714,#45715,#45716,#45717,
#45718,#45719,#45720,#45721,#45722),.UNSPECIFIED.,.F.,.F.,(4,3,3,4),(392.448760640207,
392.536570774805,392.624209454243,392.699081698589),.UNSPECIFIED.);
#301=B_SPLINE_CURVE_WITH_KNOTS('',3,(#45724,#45725,#45726,#45727,#45728,
#45729,#45730,#45731,#45732,#45733),.UNSPECIFIED.,.F.,.F.,(4,3,3,4),(392.447677522342,
392.514841603458,392.64039107027,392.699081698708),.UNSPECIFIED.);
#302=B_SPLINE_CURVE_WITH_KNOTS('',3,(#45734,#45735,#45736,#45737,#45738,
#45739,#45740,#45741,#45742,#45743,#45744,#45745,#45746,#45747,#45748,#45749,
#45750,#45751,#45752,#45753,#45754,#45755,#45756,#45757,#45758,#45759,#45760,
#45761,#45762,#45763,#45764,#45765,#45766,#45767,#45768,#45769,#45770,#45771,
#45772,#45773,#45774,#45775,#45776,#45777,#45778,#45779,#45780,#45781,#45782,
#45783,#45784,#45785,#45786,#45787,#45788,#45789,#45790,#45791,#45792,#45793,
#45794,#45795,#45796,#45797,#45798,#45799,#45800,#45801,#45802,#45803,#45804,
#45805,#45806,#45807,#45808,#45809,#45810,#45811,#45812,#45813,#45814,#45815,
#45816,#45817,#45818,#45819,#45820,#45821,#45822,#45823,#45824,#45825,#45826,
#45827,#45828,#45829,#45830,#45831,#45832,#45833,#45834,#45835,#45836,#45837,
#45838,#45839,#45840,#45841,#45842,#45843,#45844,#45845,#45846,#45847,#45848,
#45849,#45850,#45851,#45852,#45853,#45854,#45855,#45856,#45857,#45858,#45859,
#45860,#45861,#45862,#45863,#45864,#45865,#45866,#45867,#45868,#45869,#45870,
#45871,#45872,#45873,#45874,#45875,#45876,#45877,#45878,#45879,#45880,#45881,
#45882,#45883,#45884,#45885,#45886,#45887,#45888,#45889,#45890,#45891,#45892,
#45893,#45894,#45895,#45896,#45897,#45898,#45899,#45900,#45901,#45902,#45903,
#45904,#45905,#45906,#45907,#45908,#45909,#45910,#45911,#45912,#45913,#45914,
#45915,#45916,#45917,#45918,#45919,#45920,#45921,#45922,#45923,#45924,#45925,
#45926,#45927,#45928,#45929,#45930,#45931,#45932,#45933,#45934,#45935,#45936,
#45937,#45938,#45939,#45940,#45941,#45942,#45943,#45944,#45945,#45946,#45947,
#45948,#45949,#45950,#45951,#45952,#45953),.UNSPECIFIED.,.F.,.F.,(4,3,3,
3,3,3,3,3,3,3,3,3,3,3,3,3,3,3,3,3,3,3,3,3,3,3,3,3,3,3,3,3,3,3,3,3,3,3,3,
3,3,3,3,3,3,3,3,3,3,3,3,3,3,3,3,3,3,3,3,3,3,3,3,3,3,3,3,3,3,3,3,3,3,4),
(392.699081698853,392.781444927998,392.863734765316,392.945976253879,393.028192836073,
393.110403546445,393.192627412544,393.274933280105,393.357280588535,393.439757053061,
393.514577614178,393.598316326024,393.681951837391,393.76550428079,393.848993716641,
393.932447667255,394.015884161101,394.099321270857,394.182777065774,394.266321558504,
394.349910641445,394.433633909003,394.514313624898,394.598052336744,394.681687848111,
394.76524029151,394.848729727361,394.932183677975,395.015620171821,395.099057281577,
395.182513076495,395.266057569224,395.349646652165,395.433369919723,395.514049635618,
395.597788347464,395.681423858831,395.76497630223,395.84846573808,395.931919688694,
396.01535618254,396.098793292295,396.182249087213,396.265793579943,396.349382662884,
396.433105930441,396.513785646338,396.597524358184,396.681159869552,396.76471231295,
396.848201748802,396.931655699415,397.015092193261,397.098529303017,397.181985097934,
397.265529590664,397.349118673605,397.432841941162,397.513521657058,397.597260368904,
397.680895880271,397.76444832367,397.847937759521,397.931391710135,398.014828203981,
398.098265313736,398.181721108654,398.265265601384,398.348854684324,398.432577951882,
398.513257667778,398.602638396779,398.691803625613,398.731964690749),
 .UNSPECIFIED.);
#303=B_SPLINE_CURVE_WITH_KNOTS('',3,(#45959,#45960,#45961,#45962,#45963,
#45964,#45965,#45966,#45967,#45968,#45969,#45970,#45971,#45972,#45973,#45974,
#45975,#45976,#45977,#45978,#45979,#45980,#45981,#45982,#45983,#45984,#45985,
#45986,#45987,#45988,#45989,#45990,#45991,#45992,#45993,#45994,#45995,#45996,
#45997,#45998,#45999,#46000,#46001,#46002,#46003,#46004,#46005,#46006,#46007,
#46008,#46009,#46010,#46011,#46012,#46013,#46014,#46015,#46016,#46017,#46018,
#46019,#46020,#46021,#46022,#46023,#46024,#46025,#46026,#46027,#46028,#46029,
#46030,#46031,#46032,#46033,#46034,#46035,#46036,#46037,#46038,#46039,#46040,
#46041,#46042,#46043,#46044,#46045,#46046,#46047,#46048,#46049,#46050,#46051,
#46052,#46053,#46054,#46055,#46056,#46057,#46058,#46059,#46060,#46061,#46062,
#46063,#46064,#46065,#46066,#46067,#46068,#46069,#46070,#46071,#46072,#46073,
#46074,#46075,#46076,#46077,#46078,#46079,#46080,#46081,#46082,#46083,#46084,
#46085,#46086,#46087,#46088,#46089,#46090,#46091,#46092,#46093,#46094,#46095,
#46096,#46097,#46098,#46099,#46100,#46101,#46102,#46103,#46104,#46105,#46106,
#46107,#46108,#46109,#46110,#46111,#46112,#46113,#46114,#46115,#46116,#46117,
#46118,#46119,#46120,#46121,#46122,#46123,#46124,#46125,#46126,#46127,#46128,
#46129,#46130,#46131,#46132,#46133,#46134,#46135,#46136,#46137,#46138,#46139,
#46140,#46141,#46142,#46143,#46144,#46145,#46146,#46147,#46148,#46149,#46150,
#46151,#46152,#46153,#46154,#46155,#46156,#46157,#46158,#46159,#46160,#46161,
#46162,#46163,#46164,#46165,#46166,#46167,#46168,#46169,#46170,#46171,#46172,
#46173,#46174,#46175),.UNSPECIFIED.,.F.,.F.,(4,3,3,3,3,3,3,3,3,3,3,3,3,
3,3,3,3,3,3,3,3,3,3,3,3,3,3,3,3,3,3,3,3,3,3,3,3,3,3,3,3,3,3,3,3,3,3,3,3,
3,3,3,3,3,3,3,3,3,3,3,3,3,3,3,3,3,3,3,3,3,3,3,4),(398.982267005884,399.096939683955,
399.202703058783,399.286441770629,399.370077281996,399.453629725395,399.537119161246,
399.62057311186,399.704009605706,399.787446715462,399.870902510379,399.954447003109,
400.03803608605,400.121759353607,400.202439069503,400.286177781349,400.369813292716,
400.453365736115,400.536855171966,400.620309122579,400.703745616426,400.787182726181,
400.870638521099,400.954183013828,401.037772096769,401.121495364327,401.202175080223,
401.285913792069,401.369549303436,401.453101746835,401.536591182686,401.6200451333,
401.703481627146,401.786918736901,401.870374531819,401.953919024549,402.03750810749,
402.121231375048,402.201911090943,402.285649802789,402.369285314157,402.452837757555,
402.536327193406,402.61978114402,402.703217637866,402.786654747622,402.870110542539,
402.953655035269,403.03724411821,403.120967385768,403.201647101664,403.28538581351,
403.369021324878,403.452573768276,403.536063204127,403.619517154741,403.702953648587,
403.786390758343,403.869846553261,403.95339104599,404.036980128931,404.120703396489,
404.201383112384,404.285133097471,404.368777410752,404.452320898675,404.535807222286,
404.619254501399,404.702680825663,404.786130409931,404.86959072302,404.953119819031,
405.013792313897),.UNSPECIFIED.);
#304=B_SPLINE_CURVE_WITH_KNOTS('',3,(#46176,#46177,#46178,#46179,#46180,
#46181,#46182,#46183,#46184,#46185),.UNSPECIFIED.,.F.,.F.,(4,3,3,4),(398.730765351708,
398.813104217448,398.897685611592,398.982267005735),.UNSPECIFIED.);
#305=B_SPLINE_CURVE_WITH_KNOTS('',3,(#46187,#46188,#46189,#46190,#46191,
#46192,#46193,#46194,#46195,#46196),.UNSPECIFIED.,.F.,.F.,(4,3,3,4),(398.731964690749,
398.820853398844,398.909519059497,398.982267005757),.UNSPECIFIED.);
#306=B_SPLINE_CURVE_WITH_KNOTS('',3,(#46197,#46198,#46199,#46200,#46201,
#46202,#46203,#46204,#46205,#46206,#46207,#46208,#46209,#46210,#46211,#46212,
#46213,#46214,#46215,#46216,#46217,#46218,#46219,#46220,#46221,#46222,#46223,
#46224,#46225,#46226,#46227,#46228,#46229,#46230,#46231,#46232,#46233,#46234,
#46235,#46236,#46237,#46238,#46239,#46240,#46241,#46242,#46243,#46244,#46245,
#46246,#46247,#46248,#46249,#46250,#46251,#46252,#46253,#46254,#46255,#46256,
#46257,#46258,#46259,#46260,#46261,#46262,#46263,#46264,#46265,#46266,#46267,
#46268,#46269,#46270,#46271,#46272,#46273,#46274,#46275,#46276,#46277,#46278,
#46279,#46280,#46281,#46282,#46283,#46284,#46285,#46286,#46287,#46288,#46289,
#46290,#46291,#46292,#46293,#46294,#46295,#46296,#46297,#46298,#46299,#46300,
#46301,#46302,#46303,#46304,#46305,#46306,#46307,#46308,#46309,#46310,#46311,
#46312,#46313,#46314,#46315,#46316,#46317,#46318,#46319,#46320,#46321,#46322,
#46323,#46324,#46325,#46326,#46327,#46328,#46329,#46330,#46331,#46332,#46333,
#46334,#46335,#46336,#46337,#46338,#46339,#46340,#46341,#46342,#46343,#46344,
#46345,#46346,#46347,#46348,#46349,#46350,#46351,#46352,#46353,#46354,#46355,
#46356,#46357,#46358,#46359,#46360,#46361,#46362,#46363,#46364,#46365,#46366,
#46367,#46368,#46369,#46370,#46371,#46372,#46373,#46374,#46375,#46376,#46377,
#46378,#46379,#46380,#46381,#46382,#46383,#46384,#46385,#46386,#46387,#46388,
#46389,#46390,#46391,#46392,#46393,#46394,#46395,#46396,#46397,#46398,#46399,
#46400,#46401,#46402,#46403,#46404,#46405,#46406,#46407,#46408,#46409,#46410,
#46411,#46412,#46413),.UNSPECIFIED.,.F.,.F.,(4,3,3,3,3,3,3,3,3,3,3,3,3,
3,3,3,3,3,3,3,3,3,3,3,3,3,3,3,3,3,3,3,3,3,3,3,3,3,3,3,3,3,3,3,3,3,3,3,3,
3,3,3,3,3,3,3,3,3,3,3,3,3,3,3,3,3,3,3,3,3,3,3,4),(398.982267005888,399.068634116483,
399.15507990689,399.244558349792,399.331262275071,399.422127976785,399.512993678499,
399.596732390345,399.680367901713,399.763920345111,399.847409780962,399.930863731576,
400.014300225422,400.097737335178,400.181193130095,400.264737622825,400.348326705766,
400.432049973324,400.512729689219,400.596468401065,400.680103912432,400.763656355831,
400.847145791682,400.930599742295,401.014036236142,401.097473345897,401.180929140815,
401.264473633545,401.348062716486,401.431785984043,401.512465699939,401.596204411785,
401.679839923152,401.763392366551,401.846881802402,401.930335753016,402.013772246862,
402.097209356618,402.180665151535,402.264209644265,402.347798727206,402.431521994764,
402.512201710659,402.595940422505,402.679575933872,402.763128377271,402.846617813121,
402.930071763735,403.013508257581,403.096945367337,403.180401162255,403.263945654985,
403.347534737926,403.431258005483,403.511937721379,403.595676433225,403.679311944592,
403.762864387991,403.846353823842,403.929807774456,404.013244268302,404.096681378057,
404.180137172975,404.263681665705,404.347270748646,404.430994016203,404.511673732099,
404.594412336844,404.677052902557,404.761307047535,404.84380176223,404.92893562235,
405.014069482469),.UNSPECIFIED.);
#307=B_SPLINE_CURVE_WITH_KNOTS('',3,(#46419,#46420,#46421,#46422,#46423,
#46424,#46425,#46426,#46427,#46428,#46429,#46430,#46431,#46432,#46433,#46434,
#46435,#46436,#46437,#46438,#46439,#46440,#46441,#46442,#46443,#46444,#46445,
#46446,#46447,#46448,#46449,#46450,#46451,#46452,#46453,#46454,#46455,#46456,
#46457,#46458,#46459,#46460,#46461,#46462,#46463,#46464,#46465,#46466,#46467,
#46468,#46469,#46470,#46471,#46472,#46473,#46474,#46475,#46476,#46477,#46478,
#46479,#46480,#46481,#46482,#46483,#46484,#46485,#46486,#46487,#46488,#46489,
#46490,#46491,#46492,#46493,#46494,#46495,#46496,#46497,#46498,#46499,#46500,
#46501,#46502,#46503,#46504,#46505,#46506,#46507,#46508,#46509,#46510,#46511,
#46512,#46513,#46514,#46515,#46516,#46517,#46518,#46519,#46520,#46521,#46522,
#46523,#46524,#46525,#46526,#46527,#46528,#46529,#46530,#46531,#46532,#46533,
#46534,#46535,#46536,#46537,#46538,#46539,#46540,#46541,#46542,#46543,#46544,
#46545,#46546,#46547,#46548,#46549,#46550,#46551,#46552,#46553,#46554,#46555,
#46556,#46557,#46558,#46559,#46560,#46561,#46562,#46563,#46564,#46565,#46566,
#46567,#46568,#46569,#46570,#46571,#46572,#46573,#46574,#46575,#46576,#46577,
#46578,#46579,#46580,#46581,#46582,#46583,#46584,#46585,#46586,#46587,#46588,
#46589,#46590,#46591,#46592,#46593,#46594,#46595,#46596,#46597,#46598,#46599,
#46600,#46601,#46602,#46603,#46604,#46605,#46606,#46607,#46608,#46609,#46610,
#46611,#46612,#46613,#46614,#46615,#46616,#46617,#46618,#46619,#46620,#46621,
#46622,#46623,#46624,#46625,#46626,#46627,#46628,#46629,#46630,#46631,#46632,
#46633,#46634,#46635,#46636,#46637,#46638),.UNSPECIFIED.,.F.,.F.,(4,3,3,
3,3,3,3,3,3,3,3,3,3,3,3,3,3,3,3,3,3,3,3,3,3,3,3,3,3,3,3,3,3,3,3,3,3,3,3,
3,3,3,3,3,3,3,3,3,3,3,3,3,3,3,3,3,3,3,3,3,3,3,3,3,3,3,3,3,3,3,3,3,3,4),
(405.26545231318,405.348387801783,405.431225006267,405.513984784103,405.599843577818,
405.682519331484,405.765185411802,405.847860544578,405.930563459232,406.01335713532,
406.096204823849,406.179168760872,406.200855133824,406.28459384567,406.368229357037,
406.451781800436,406.535271236287,406.618725186901,406.702161680747,406.785598790502,
406.869054585419,406.952599078149,407.03618816109,407.119911428648,407.200591144544,
407.28432985639,407.367965367757,407.451517811156,407.535007247006,407.61846119762,
407.701897691466,407.785334801222,407.868790596139,407.952335088869,408.03592417181,
408.119647439367,408.200327155264,408.28406586711,408.367701378477,408.451253821876,
408.534743257727,408.61819720834,408.701633702187,408.785070811942,408.86852660686,
408.952071099589,409.03566018253,409.119383450088,409.200063165984,409.28380187783,
409.367437389197,409.450989832596,409.534479268446,409.61793321906,409.701369712907,
409.784806822662,409.86826261758,409.951807110309,410.03539619325,410.119119460808,
410.199799176704,410.28353788855,410.367173399917,410.450725843316,410.534215279167,
410.61766922978,410.701105723627,410.784542833382,410.867998628299,410.951543121029,
411.03513220397,411.118855471527,411.199535187425,411.298100148351),
 .UNSPECIFIED.);
#308=B_SPLINE_CURVE_WITH_KNOTS('',3,(#46639,#46640,#46641,#46642,#46643,
#46644,#46645,#46646,#46647,#46648,#46649,#46650,#46651),.UNSPECIFIED.,
 .F.,.F.,(4,3,3,3,4),(405.013792313897,405.097423948019,405.181172835758,
405.201119123104,405.265452313063),.UNSPECIFIED.);
#309=B_SPLINE_CURVE_WITH_KNOTS('',3,(#46653,#46654,#46655,#46656,#46657,
#46658,#46659,#46660,#46661,#46662),.UNSPECIFIED.,.F.,.F.,(4,3,3,4),(405.014069482469,
405.096536027737,405.180994170402,405.265452313067),.UNSPECIFIED.);
#310=B_SPLINE_CURVE_WITH_KNOTS('',3,(#46663,#46664,#46665,#46666,#46667,
#46668,#46669,#46670,#46671,#46672,#46673,#46674,#46675,#46676,#46677,#46678,
#46679,#46680,#46681,#46682,#46683,#46684,#46685,#46686,#46687,#46688,#46689,
#46690,#46691,#46692,#46693,#46694,#46695,#46696,#46697,#46698,#46699,#46700,
#46701,#46702,#46703,#46704,#46705,#46706,#46707,#46708,#46709,#46710,#46711,
#46712,#46713,#46714,#46715,#46716,#46717,#46718,#46719,#46720,#46721,#46722,
#46723,#46724,#46725,#46726,#46727,#46728,#46729,#46730,#46731,#46732,#46733,
#46734,#46735,#46736,#46737,#46738,#46739,#46740,#46741,#46742,#46743,#46744,
#46745,#46746,#46747,#46748,#46749,#46750,#46751,#46752,#46753,#46754,#46755,
#46756,#46757,#46758,#46759,#46760,#46761,#46762,#46763,#46764,#46765,#46766,
#46767,#46768,#46769,#46770,#46771,#46772,#46773,#46774,#46775,#46776,#46777,
#46778,#46779,#46780,#46781,#46782,#46783,#46784,#46785,#46786,#46787,#46788,
#46789,#46790,#46791,#46792,#46793,#46794,#46795,#46796,#46797,#46798,#46799,
#46800,#46801,#46802,#46803,#46804,#46805,#46806,#46807,#46808,#46809,#46810,
#46811,#46812,#46813,#46814,#46815,#46816,#46817,#46818,#46819,#46820,#46821,
#46822,#46823,#46824,#46825,#46826,#46827,#46828,#46829,#46830,#46831,#46832,
#46833,#46834,#46835,#46836,#46837,#46838,#46839,#46840,#46841,#46842,#46843,
#46844,#46845,#46846,#46847,#46848,#46849,#46850,#46851,#46852,#46853,#46854,
#46855,#46856,#46857,#46858,#46859,#46860,#46861,#46862,#46863,#46864,#46865,
#46866,#46867,#46868,#46869,#46870,#46871,#46872,#46873,#46874,#46875,#46876,
#46877,#46878,#46879,#46880,#46881,#46882),.UNSPECIFIED.,.F.,.F.,(4,3,3,
3,3,3,3,3,3,3,3,3,3,3,3,3,3,3,3,3,3,3,3,3,3,3,3,3,3,3,3,3,3,3,3,3,3,3,3,
3,3,3,3,3,3,3,3,3,3,3,3,3,3,3,3,3,3,3,3,3,3,3,3,3,3,3,3,3,3,3,3,3,3,4),
(405.265452313201,405.373358109382,405.483824806747,405.511409742819,405.595148454665,
405.678783966033,405.762336409431,405.845825845283,405.929279795896,406.012716289743,
406.096153399498,406.179609194416,406.263153687146,406.346742770087,406.430466037645,
406.511145753539,406.594884465385,406.678519976753,406.762072420151,406.845561856002,
406.929015806616,407.012452300462,407.095889410218,407.179345205135,407.262889697865,
407.346478780806,407.430202048364,407.51088176426,407.594620476106,407.678255987474,
407.761808430872,407.845297866723,407.928751817337,408.012188311183,408.095625420938,
408.179081215856,408.262625708586,408.346214791527,408.429938059084,408.51061777498,
408.594356486826,408.677991998193,408.761544441592,408.845033877443,408.928487828057,
409.011924321903,409.095361431658,409.178817226576,409.262361719306,409.345950802247,
409.429674069804,409.5103537857,409.594092497546,409.677728008913,409.761280452312,
409.844769888163,409.928223838776,410.011660332623,410.095097442378,410.178553237296,
410.262097730026,410.345686812966,410.429410080524,410.51008979642,410.593841439003,
410.681732668085,410.765273320821,410.848757253055,410.932202583627,411.015627401392,
411.099071652666,411.182527263906,411.266040390765,411.296971271658),
 .UNSPECIFIED.);
#311=B_SPLINE_CURVE_WITH_KNOTS('',3,(#46888,#46889,#46890,#46891,#46892,
#46893,#46894,#46895,#46896,#46897,#46898,#46899,#46900,#46901,#46902,#46903,
#46904,#46905,#46906,#46907,#46908,#46909,#46910,#46911,#46912,#46913,#46914,
#46915,#46916,#46917,#46918,#46919,#46920,#46921,#46922,#46923,#46924,#46925,
#46926,#46927,#46928,#46929,#46930,#46931,#46932,#46933,#46934,#46935,#46936,
#46937,#46938,#46939,#46940,#46941,#46942,#46943,#46944,#46945,#46946,#46947,
#46948,#46949,#46950,#46951,#46952,#46953,#46954,#46955,#46956,#46957,#46958,
#46959,#46960,#46961,#46962,#46963,#46964,#46965,#46966,#46967,#46968,#46969,
#46970,#46971,#46972,#46973,#46974,#46975,#46976,#46977,#46978,#46979,#46980,
#46981,#46982,#46983,#46984,#46985,#46986,#46987,#46988,#46989,#46990,#46991,
#46992,#46993,#46994,#46995,#46996,#46997,#46998,#46999,#47000,#47001,#47002,
#47003,#47004,#47005,#47006,#47007,#47008,#47009,#47010,#47011,#47012,#47013,
#47014,#47015,#47016,#47017,#47018,#47019,#47020,#47021,#47022,#47023,#47024,
#47025,#47026,#47027,#47028,#47029,#47030,#47031,#47032,#47033,#47034,#47035,
#47036,#47037,#47038,#47039,#47040,#47041,#47042,#47043,#47044,#47045,#47046,
#47047,#47048,#47049,#47050,#47051,#47052,#47053,#47054,#47055,#47056,#47057,
#47058,#47059,#47060,#47061,#47062,#47063,#47064,#47065,#47066,#47067,#47068,
#47069,#47070,#47071,#47072,#47073,#47074,#47075,#47076,#47077,#47078,#47079,
#47080,#47081,#47082,#47083,#47084,#47085,#47086,#47087,#47088,#47089,#47090,
#47091,#47092,#47093,#47094,#47095,#47096,#47097,#47098,#47099,#47100,#47101,
#47102,#47103,#47104,#47105,#47106,#47107),.UNSPECIFIED.,.F.,.F.,(4,3,3,
3,3,3,3,3,3,3,3,3,3,3,3,3,3,3,3,3,3,3,3,3,3,3,3,3,3,3,3,3,3,3,3,3,3,3,3,
3,3,3,3,3,3,3,3,3,3,3,3,3,3,3,3,3,3,3,3,3,3,3,3,3,3,3,3,3,3,3,3,3,3,4),
(411.548637620243,411.632259103847,411.715874533125,411.799501689164,411.883158356806,
411.966915847641,412.050726888138,412.134675892978,412.199271198145,412.283009909991,
412.366645421358,412.450197864757,412.533687300608,412.617141251222,412.700577745068,
412.784014854823,412.867470649741,412.95101514247,413.034604225411,413.118327492969,
413.199007208865,413.282745920711,413.366381432078,413.449933875477,413.533423311328,
413.616877261941,413.700313755788,413.783750865543,413.867206660461,413.95075115319,
414.034340236131,414.118063503689,414.198743219585,414.282481931431,414.366117442798,
414.449669886197,414.533159322048,414.616613272662,414.700049766508,414.783486876264,
414.866942671182,414.950487163911,415.034076246852,415.11779951441,415.198479230305,
415.282217942151,415.365853453518,415.449405896917,415.532895332768,415.616349283381,
415.699785777228,415.783222886983,415.866678681901,415.950223174631,416.033812257572,
416.117535525129,416.198215241025,416.281953952871,416.365589464238,416.449141907637,
416.532631343488,416.616085294102,416.699521787948,416.782958897703,416.866414692621,
416.94995918535,417.033548268291,417.117271535849,417.197951251745,417.282231215125,
417.366369980425,417.450427359457,417.534406239268,417.581050393302),
 .UNSPECIFIED.);
#312=B_SPLINE_CURVE_WITH_KNOTS('',3,(#47108,#47109,#47110,#47111,#47112,
#47113,#47114,#47115,#47116,#47117),.UNSPECIFIED.,.F.,.F.,(4,3,3,4),(411.298100148351,
411.394649529236,411.490471997343,411.548637620046),.UNSPECIFIED.);
#313=B_SPLINE_CURVE_WITH_KNOTS('',3,(#47119,#47120,#47121,#47122,#47123,
#47124,#47125,#47126,#47127,#47128,#47129,#47130,#47131),.UNSPECIFIED.,
 .F.,.F.,(4,3,3,3,4),(411.296971271658,411.380583957771,411.464320780643,
411.50982580714,411.548637620247),.UNSPECIFIED.);
#314=B_SPLINE_CURVE_WITH_KNOTS('',3,(#47132,#47133,#47134,#47135,#47136,
#47137,#47138,#47139,#47140,#47141,#47142,#47143,#47144,#47145,#47146,#47147,
#47148,#47149,#47150,#47151,#47152,#47153,#47154,#47155,#47156,#47157,#47158,
#47159,#47160,#47161,#47162,#47163,#47164,#47165,#47166,#47167,#47168,#47169,
#47170,#47171,#47172,#47173,#47174,#47175,#47176,#47177,#47178,#47179,#47180,
#47181,#47182,#47183,#47184,#47185,#47186,#47187,#47188,#47189,#47190,#47191,
#47192,#47193,#47194,#47195,#47196,#47197,#47198,#47199,#47200,#47201,#47202,
#47203,#47204,#47205,#47206,#47207,#47208,#47209,#47210,#47211,#47212,#47213,
#47214,#47215,#47216,#47217,#47218,#47219,#47220,#47221,#47222,#47223,#47224,
#47225,#47226,#47227,#47228,#47229,#47230,#47231,#47232,#47233,#47234,#47235,
#47236,#47237,#47238,#47239,#47240,#47241,#47242,#47243,#47244,#47245,#47246,
#47247,#47248,#47249,#47250,#47251,#47252,#47253,#47254,#47255,#47256,#47257,
#47258,#47259,#47260,#47261,#47262,#47263,#47264,#47265,#47266,#47267,#47268,
#47269,#47270,#47271,#47272,#47273,#47274,#47275,#47276,#47277,#47278,#47279,
#47280,#47281,#47282,#47283,#47284,#47285,#47286,#47287,#47288,#47289,#47290,
#47291,#47292,#47293,#47294,#47295,#47296,#47297,#47298,#47299,#47300,#47301,
#47302,#47303,#47304,#47305,#47306,#47307,#47308,#47309,#47310,#47311,#47312,
#47313,#47314,#47315,#47316,#47317,#47318,#47319,#47320,#47321,#47322,#47323,
#47324,#47325,#47326,#47327,#47328,#47329,#47330,#47331,#47332,#47333,#47334,
#47335,#47336,#47337,#47338,#47339,#47340,#47341,#47342,#47343,#47344,#47345,
#47346,#47347,#47348,#47349,#47350,#47351),.UNSPECIFIED.,.F.,.F.,(4,3,3,
3,3,3,3,3,3,3,3,3,3,3,3,3,3,3,3,3,3,3,3,3,3,3,3,3,3,3,3,3,3,3,3,3,3,3,3,
3,3,3,3,3,3,3,3,3,3,3,3,3,3,3,3,3,3,3,3,3,3,3,3,3,3,3,3,3,3,3,3,3,3,4),
(411.548637620412,411.631849527888,411.714960257177,411.797990449943,411.880960671604,
411.963899820013,412.04682518702,412.129755301074,412.212708690519,412.295751530242,
412.378843954004,412.462060135133,412.50956181786,412.593300529706,412.676936041073,
412.760488484472,412.843977920323,412.927431870936,413.010868364783,413.094305474538,
413.177761269456,413.261305762185,413.344894845126,413.428618112684,413.50929782858,
413.593036540426,413.676672051794,413.760224495192,413.843713931043,413.927167881657,
414.010604375504,414.094041485259,414.177497280177,414.261041772907,414.344630855848,
414.428354123405,414.509033839301,414.592772551147,414.676408062515,414.759960505913,
414.843449941764,414.926903892378,415.010340386224,415.09377749598,415.177233290898,
415.260777783627,415.344366866568,415.428090134126,415.508769850021,415.592508561867,
415.676144073234,415.759696516633,415.843185952484,415.926639903097,416.010076396944,
416.093513506699,416.176969301617,416.260513794347,416.344102877288,416.427826144845,
416.508505860741,416.592244572587,416.675880083955,416.759432527353,416.842921963204,
416.926375913817,417.009812407664,417.093249517419,417.176705312336,417.260249805066,
417.343838888007,417.427562155565,417.508241871461,417.581170651204),
 .UNSPECIFIED.);
#315=B_SPLINE_CURVE_WITH_KNOTS('',3,(#47357,#47358,#47359,#47360,#47361,
#47362,#47363,#47364,#47365,#47366,#47367,#47368,#47369,#47370,#47371,#47372,
#47373,#47374,#47375,#47376,#47377,#47378,#47379,#47380,#47381,#47382,#47383,
#47384,#47385,#47386,#47387,#47388,#47389,#47390,#47391,#47392,#47393,#47394,
#47395,#47396,#47397,#47398,#47399,#47400,#47401,#47402,#47403,#47404,#47405,
#47406,#47407,#47408,#47409,#47410,#47411,#47412,#47413,#47414,#47415,#47416,
#47417,#47418,#47419,#47420,#47421,#47422,#47423,#47424,#47425,#47426,#47427,
#47428,#47429,#47430,#47431,#47432,#47433,#47434,#47435,#47436,#47437,#47438,
#47439,#47440,#47441,#47442,#47443,#47444,#47445,#47446,#47447,#47448,#47449,
#47450,#47451,#47452,#47453,#47454,#47455,#47456,#47457,#47458,#47459,#47460,
#47461,#47462,#47463,#47464,#47465,#47466,#47467,#47468,#47469,#47470,#47471,
#47472,#47473,#47474,#47475,#47476,#47477,#47478,#47479,#47480,#47481,#47482,
#47483,#47484,#47485,#47486,#47487,#47488,#47489,#47490,#47491,#47492,#47493,
#47494,#47495,#47496,#47497,#47498,#47499,#47500,#47501,#47502,#47503,#47504,
#47505,#47506,#47507,#47508,#47509,#47510,#47511,#47512,#47513,#47514,#47515,
#47516,#47517,#47518,#47519,#47520,#47521,#47522,#47523,#47524,#47525,#47526,
#47527,#47528,#47529,#47530,#47531,#47532,#47533,#47534,#47535,#47536,#47537,
#47538,#47539,#47540,#47541,#47542,#47543,#47544,#47545,#47546,#47547,#47548,
#47549,#47550,#47551,#47552,#47553,#47554,#47555,#47556,#47557,#47558,#47559,
#47560,#47561,#47562,#47563,#47564,#47565,#47566,#47567,#47568,#47569,#47570,
#47571,#47572,#47573),.UNSPECIFIED.,.F.,.F.,(4,3,3,3,3,3,3,3,3,3,3,3,3,
3,3,3,3,3,3,3,3,3,3,3,3,3,3,3,3,3,3,3,3,3,3,3,3,3,3,3,3,3,3,3,3,3,3,3,3,
3,3,3,3,3,3,3,3,3,3,3,3,3,3,3,3,3,3,3,3,3,3,3,4),(417.831822927619,417.926420867418,
418.021417477909,418.116960905954,418.197687262465,418.281425974311,418.365061485678,
418.448613929077,418.532103364928,418.615557315542,418.698993809388,418.782430919143,
418.865886714061,418.949431206791,419.033020289732,419.116743557289,419.197423273186,
419.281161985032,419.364797496399,419.448349939798,419.531839375649,419.615293326263,
419.698729820109,419.782166929864,419.865622724782,419.949167217512,420.032756300453,
420.116479568011,420.197159283906,420.280897995752,420.364533507119,420.448085950518,
420.531575386369,420.615029336983,420.698465830829,420.781902940584,420.865358735502,
420.948903228232,421.032492311173,421.11621557873,421.196895294626,421.280634006472,
421.364269517839,421.447821961238,421.531311397089,421.614765347703,421.698201841549,
421.781638951304,421.865094746222,421.948639238952,422.032228321893,422.11595158945,
422.196631305346,422.280370017192,422.364005528559,422.447557971958,422.531047407809,
422.614501358423,422.697937852269,422.781374962024,422.864830756942,422.948375249672,
423.031964332613,423.11568760017,423.196367316066,423.27971783058,423.362420771565,
423.445048292511,423.527619318683,423.611507347057,423.694033766242,423.77860259921,
423.863171432179),.UNSPECIFIED.);
#316=B_SPLINE_CURVE_WITH_KNOTS('',3,(#47574,#47575,#47576,#47577,#47578,
#47579,#47580,#47581,#47582,#47583),.UNSPECIFIED.,.F.,.F.,(4,3,3,4),(417.581050393302,
417.664959549787,417.748862132102,417.831822927422),.UNSPECIFIED.);
#317=B_SPLINE_CURVE_WITH_KNOTS('',3,(#47585,#47586,#47587,#47588,#47589,
#47590,#47591,#47592,#47593,#47594),.UNSPECIFIED.,.F.,.F.,(4,3,3,4),(417.581170651204,
417.680212608396,417.778300546283,417.831822927248),.UNSPECIFIED.);
#318=B_SPLINE_CURVE_WITH_KNOTS('',3,(#47595,#47596,#47597,#47598,#47599,
#47600,#47601,#47602,#47603,#47604,#47605,#47606,#47607,#47608,#47609,#47610,
#47611,#47612,#47613,#47614,#47615,#47616,#47617,#47618,#47619,#47620,#47621,
#47622,#47623,#47624,#47625,#47626,#47627,#47628,#47629,#47630,#47631,#47632,
#47633,#47634,#47635,#47636,#47637,#47638,#47639,#47640,#47641,#47642,#47643,
#47644,#47645,#47646,#47647,#47648,#47649,#47650,#47651,#47652,#47653,#47654,
#47655,#47656,#47657,#47658,#47659,#47660,#47661,#47662,#47663,#47664,#47665,
#47666,#47667,#47668,#47669,#47670,#47671,#47672,#47673,#47674,#47675,#47676,
#47677,#47678,#47679,#47680,#47681,#47682,#47683,#47684,#47685,#47686,#47687,
#47688,#47689,#47690,#47691,#47692,#47693,#47694,#47695,#47696,#47697,#47698,
#47699,#47700,#47701,#47702,#47703,#47704,#47705,#47706,#47707,#47708,#47709,
#47710,#47711,#47712,#47713,#47714,#47715,#47716,#47717,#47718,#47719,#47720,
#47721,#47722,#47723,#47724,#47725,#47726,#47727,#47728,#47729,#47730,#47731,
#47732,#47733,#47734,#47735,#47736,#47737,#47738,#47739,#47740,#47741,#47742,
#47743,#47744,#47745,#47746,#47747,#47748,#47749,#47750,#47751,#47752,#47753,
#47754,#47755,#47756,#47757,#47758,#47759,#47760,#47761,#47762,#47763,#47764,
#47765,#47766,#47767,#47768,#47769,#47770,#47771,#47772,#47773,#47774,#47775,
#47776,#47777,#47778,#47779,#47780,#47781,#47782,#47783,#47784,#47785,#47786,
#47787,#47788,#47789,#47790,#47791,#47792,#47793,#47794,#47795,#47796,#47797,
#47798,#47799,#47800,#47801,#47802,#47803,#47804,#47805,#47806,#47807,#47808,
#47809,#47810,#47811,#47812,#47813,#47814),.UNSPECIFIED.,.F.,.F.,(4,3,3,
3,3,3,3,3,3,3,3,3,3,3,3,3,3,3,3,3,3,3,3,3,3,3,3,3,3,3,3,3,3,3,3,3,3,3,3,
3,3,3,3,3,3,3,3,3,3,3,3,3,3,3,3,3,3,3,3,3,3,3,3,3,3,3,3,3,3,3,3,3,3,4),
(417.831822927426,417.91634229677,417.999579653168,418.082817834537,418.166075045188,
418.251550754437,418.334946674687,418.421462278434,418.507977882181,418.591716594027,
418.675352105395,418.758904548793,418.842393984644,418.925847935258,419.009284429104,
419.09272153886,419.176177333777,419.259721826507,419.343310909448,419.427034177006,
419.507713892901,419.591452604747,419.675088116114,419.758640559513,419.842129995364,
419.925583945977,420.009020439824,420.092457549579,420.175913344497,420.259457837226,
420.343046920168,420.426770187725,420.507449903621,420.591188615467,420.674824126834,
420.758376570233,420.841866006084,420.925319956698,421.008756450544,421.092193560299,
421.175649355217,421.259193847946,421.342782930887,421.426506198445,421.507185914341,
421.590924626187,421.674560137555,421.758112580953,421.841602016804,421.925055967418,
422.008492461264,422.09192957102,422.175385365938,422.258929858667,422.342518941608,
422.426242209166,422.506921925062,422.590660636908,422.674296148276,422.757848591675,
422.841338027526,422.924791978139,423.008228471986,423.091665581741,423.175121376659,
423.258665869388,423.34225495233,423.425978219887,423.506657935782,423.591469649572,
423.676133771211,423.760712027502,423.845204064411,423.864352866444),
 .UNSPECIFIED.);
#319=B_SPLINE_CURVE_WITH_KNOTS('',3,(#47820,#47821,#47822,#47823,#47824,
#47825,#47826,#47827,#47828,#47829,#47830,#47831,#47832,#47833,#47834,#47835,
#47836,#47837,#47838,#47839,#47840,#47841,#47842,#47843,#47844,#47845,#47846,
#47847,#47848,#47849,#47850,#47851,#47852,#47853,#47854,#47855,#47856,#47857,
#47858,#47859,#47860,#47861,#47862,#47863,#47864,#47865,#47866,#47867,#47868,
#47869,#47870,#47871,#47872,#47873,#47874,#47875,#47876,#47877,#47878,#47879,
#47880,#47881,#47882,#47883,#47884,#47885,#47886,#47887,#47888,#47889,#47890,
#47891,#47892,#47893,#47894,#47895,#47896,#47897,#47898,#47899,#47900,#47901,
#47902,#47903,#47904,#47905,#47906,#47907,#47908,#47909,#47910,#47911,#47912,
#47913,#47914,#47915,#47916,#47917,#47918,#47919,#47920,#47921,#47922,#47923,
#47924,#47925,#47926,#47927,#47928,#47929,#47930,#47931,#47932,#47933,#47934,
#47935,#47936,#47937,#47938,#47939,#47940,#47941,#47942,#47943,#47944,#47945,
#47946,#47947,#47948,#47949,#47950,#47951,#47952,#47953,#47954,#47955,#47956,
#47957,#47958,#47959,#47960,#47961,#47962,#47963,#47964,#47965,#47966,#47967,
#47968,#47969,#47970,#47971,#47972,#47973,#47974,#47975,#47976,#47977,#47978,
#47979,#47980,#47981,#47982,#47983,#47984,#47985,#47986,#47987,#47988,#47989,
#47990,#47991,#47992,#47993,#47994,#47995,#47996,#47997,#47998,#47999,#48000,
#48001,#48002,#48003,#48004,#48005,#48006,#48007,#48008,#48009,#48010,#48011,
#48012,#48013,#48014,#48015,#48016,#48017,#48018,#48019,#48020,#48021,#48022,
#48023,#48024,#48025,#48026,#48027,#48028,#48029,#48030,#48031,#48032,#48033,
#48034,#48035,#48036,#48037,#48038,#48039),.UNSPECIFIED.,.F.,.F.,(4,3,3,
3,3,3,3,3,3,3,3,3,3,3,3,3,3,3,3,3,3,3,3,3,3,3,3,3,3,3,3,3,3,3,3,3,3,3,3,
3,3,3,3,3,3,3,3,3,3,3,3,3,3,3,3,3,3,3,3,3,3,3,3,3,3,3,3,3,3,3,3,3,3,4),
(424.115008234602,424.196103326786,424.279842038632,424.363477549999,424.447029993398,
424.530519429249,424.613973379863,424.697409873709,424.780846983465,424.864302778382,
424.947847271112,425.031436354053,425.115159621611,425.195839337506,425.279578049352,
425.363213560719,425.446766004118,425.530255439969,425.613709390583,425.697145884429,
425.780582994185,425.864038789102,425.947583281832,426.031172364773,426.114895632331,
426.195575348226,426.279314060072,426.36294957144,426.446502014838,426.529991450689,
426.613445401303,426.696881895149,426.780319004905,426.863774799822,426.947319292552,
427.030908375493,427.114631643051,427.195311358947,427.279050070793,427.36268558216,
427.446238025559,427.52972746141,427.613181412024,427.69661790587,427.780055015626,
427.863510810543,427.947055303273,428.030644386214,428.114367653771,428.195047369667,
428.278786081513,428.36242159288,428.445974036279,428.52946347213,428.612917422744,
428.69635391659,428.779791026345,428.863246821263,428.946791313993,429.030380396934,
429.114103664491,429.194783380387,429.278524811112,429.362162412899,429.445716320916,
429.533360746726,429.616811062651,429.700243933085,429.783677429661,429.867129620398,
429.950658987571,430.034233386045,430.11791345189,430.146871727396),
 .UNSPECIFIED.);
#320=B_SPLINE_CURVE_WITH_KNOTS('',3,(#48040,#48041,#48042,#48043,#48044,
#48045,#48046,#48047,#48048,#48049),.UNSPECIFIED.,.F.,.F.,(4,3,3,4),(423.863171432179,
423.945812036063,424.030410135267,424.115008234471),.UNSPECIFIED.);
#321=B_SPLINE_CURVE_WITH_KNOTS('',3,(#48051,#48052,#48053,#48054,#48055,
#48056,#48057,#48058,#48059,#48060),.UNSPECIFIED.,.F.,.F.,(4,3,3,4),(423.864352866444,
423.948770683666,424.033160895861,424.115008234606),.UNSPECIFIED.);
#322=B_SPLINE_CURVE_WITH_KNOTS('',3,(#48061,#48062,#48063,#48064,#48065,
#48066,#48067,#48068,#48069,#48070,#48071,#48072,#48073,#48074,#48075,#48076,
#48077,#48078,#48079,#48080,#48081,#48082,#48083,#48084,#48085,#48086,#48087,
#48088,#48089,#48090,#48091,#48092,#48093,#48094,#48095,#48096,#48097,#48098,
#48099,#48100,#48101,#48102,#48103,#48104,#48105,#48106,#48107,#48108,#48109,
#48110,#48111,#48112,#48113,#48114,#48115,#48116,#48117,#48118,#48119,#48120,
#48121,#48122,#48123,#48124,#48125,#48126,#48127,#48128,#48129,#48130,#48131,
#48132,#48133,#48134,#48135,#48136,#48137,#48138,#48139,#48140,#48141,#48142,
#48143,#48144,#48145,#48146,#48147,#48148,#48149,#48150,#48151,#48152,#48153,
#48154,#48155,#48156,#48157,#48158,#48159,#48160,#48161,#48162,#48163,#48164,
#48165,#48166,#48167,#48168,#48169,#48170,#48171,#48172,#48173,#48174,#48175,
#48176,#48177,#48178,#48179,#48180,#48181,#48182,#48183,#48184,#48185,#48186,
#48187,#48188,#48189,#48190,#48191,#48192,#48193,#48194,#48195,#48196,#48197,
#48198,#48199,#48200,#48201,#48202,#48203,#48204,#48205,#48206,#48207,#48208,
#48209,#48210,#48211,#48212,#48213,#48214,#48215,#48216,#48217,#48218,#48219,
#48220,#48221,#48222,#48223,#48224,#48225,#48226,#48227,#48228,#48229,#48230,
#48231,#48232,#48233,#48234,#48235,#48236,#48237,#48238,#48239,#48240,#48241,
#48242,#48243,#48244,#48245,#48246,#48247,#48248,#48249,#48250,#48251,#48252,
#48253,#48254,#48255,#48256,#48257,#48258,#48259,#48260,#48261,#48262,#48263,
#48264,#48265,#48266,#48267,#48268,#48269,#48270,#48271,#48272,#48273,#48274,
#48275,#48276,#48277,#48278,#48279,#48280),.UNSPECIFIED.,.F.,.F.,(4,3,3,
3,3,3,3,3,3,3,3,3,3,3,3,3,3,3,3,3,3,3,3,3,3,3,3,3,3,3,3,3,3,3,3,3,3,3,3,
3,3,3,3,3,3,3,3,3,3,3,3,3,3,3,3,3,3,3,3,3,3,3,3,3,3,3,3,3,3,3,3,3,3,4),
(424.115008234794,424.2076199709,424.300766079146,424.394189860388,424.487960336065,
424.506393946502,424.590132658348,424.673768169715,424.757320613114,424.840810048965,
424.924263999578,425.007700493424,425.09113760318,425.174593398097,425.258137890827,
425.341726973768,425.425450241325,425.506129957222,425.589868669068,425.673504180435,
425.757056623834,425.840546059685,425.924000010298,426.007436504145,426.0908736139,
426.174329408818,426.257873901547,426.341462984488,426.425186252046,426.505865967942,
426.589604679788,426.673240191155,426.756792634554,426.840282070405,426.923736021019,
427.007172514865,427.090609624621,427.174065419538,427.257609912268,427.341198995209,
427.424922262767,427.505601978662,427.589340690508,427.672976201875,427.756528645274,
427.840018081125,427.923472031739,428.006908525585,428.09034563534,428.173801430258,
428.257345922988,428.340935005929,428.424658273486,428.505337989382,428.589076701228,
428.672712212595,428.756264655994,428.839754091845,428.923208042459,429.006644536305,
429.090081646061,429.173537440978,429.257081933708,429.340671016649,429.424394284206,
429.505074000102,429.587707424315,429.670246251362,429.752709587891,429.835116471439,
429.917495324619,429.999855902794,430.082243419595,430.146364568078),
 .UNSPECIFIED.);
#323=B_SPLINE_CURVE_WITH_KNOTS('',3,(#48286,#48287,#48288,#48289,#48290,
#48291,#48292,#48293,#48294,#48295,#48296,#48297,#48298,#48299,#48300,#48301,
#48302,#48303,#48304,#48305,#48306,#48307,#48308,#48309,#48310,#48311,#48312,
#48313,#48314,#48315,#48316,#48317,#48318,#48319,#48320,#48321,#48322,#48323,
#48324,#48325,#48326,#48327,#48328,#48329,#48330,#48331,#48332,#48333,#48334,
#48335,#48336,#48337,#48338,#48339,#48340,#48341,#48342,#48343,#48344,#48345,
#48346,#48347,#48348,#48349,#48350,#48351,#48352,#48353,#48354,#48355,#48356,
#48357,#48358,#48359,#48360,#48361,#48362,#48363,#48364,#48365,#48366,#48367,
#48368,#48369,#48370,#48371,#48372,#48373,#48374,#48375,#48376,#48377,#48378,
#48379,#48380,#48381,#48382,#48383,#48384,#48385,#48386,#48387,#48388,#48389,
#48390,#48391,#48392,#48393,#48394,#48395,#48396,#48397,#48398,#48399,#48400,
#48401,#48402,#48403,#48404,#48405,#48406,#48407,#48408,#48409,#48410,#48411,
#48412,#48413,#48414,#48415,#48416,#48417,#48418,#48419,#48420,#48421,#48422,
#48423,#48424,#48425,#48426,#48427,#48428,#48429,#48430,#48431,#48432,#48433,
#48434,#48435,#48436,#48437,#48438,#48439,#48440,#48441,#48442,#48443,#48444,
#48445,#48446,#48447,#48448,#48449,#48450,#48451,#48452,#48453,#48454,#48455,
#48456,#48457,#48458,#48459,#48460,#48461,#48462,#48463,#48464,#48465,#48466,
#48467,#48468,#48469,#48470,#48471,#48472,#48473,#48474,#48475,#48476,#48477,
#48478,#48479,#48480,#48481,#48482,#48483,#48484,#48485,#48486,#48487,#48488,
#48489,#48490,#48491,#48492,#48493,#48494,#48495,#48496,#48497,#48498,#48499,
#48500,#48501,#48502,#48503,#48504,#48505),.UNSPECIFIED.,.F.,.F.,(4,3,3,
3,3,3,3,3,3,3,3,3,3,3,3,3,3,3,3,3,3,3,3,3,3,3,3,3,3,3,3,3,3,3,3,3,3,3,3,
3,3,3,3,3,3,3,3,3,3,3,3,3,3,3,3,3,3,3,3,3,3,3,3,3,3,3,3,3,3,3,3,3,3,4),
(430.398193541959,430.480576910534,430.562892386668,430.645166821398,430.727421257035,
430.809674699398,430.891946151272,430.97430233696,431.056704277496,431.139230058947,
431.194255401827,431.277994113673,431.36162962504,431.445182068439,431.52867150429,
431.612125454903,431.695561948749,431.778999058505,431.862454853423,431.945999346153,
432.029588429093,432.113311696651,432.193991412547,432.277730124393,432.361365635761,
432.444918079159,432.52840751501,432.611861465624,432.69529795947,432.778735069225,
432.862190864143,432.945735356873,433.029324439814,433.113047707372,433.193727423267,
433.277466135113,433.361101646481,433.444654089879,433.52814352573,433.611597476344,
433.69503397019,433.778471079946,433.861926874863,433.945471367593,434.029060450534,
434.112783718092,434.193463433988,434.277202145834,434.360837657202,434.4443901006,
434.527879536451,434.611333487065,434.694769980912,434.778207090667,434.861662885585,
434.945207378315,435.028796461256,435.112519728813,435.193199444708,435.276938156554,
435.360573667921,435.44412611132,435.527615547171,435.611069497785,435.694505991631,
435.777943101386,435.861398896304,435.944943389034,436.028532471975,436.112255739532,
436.192935455428,436.281457691473,436.369776886151,436.431064385021),
 .UNSPECIFIED.);
#324=B_SPLINE_CURVE_WITH_KNOTS('',3,(#48506,#48507,#48508,#48509,#48510,
#48511,#48512,#48513,#48514,#48515),.UNSPECIFIED.,.F.,.F.,(4,3,3,4),(430.146871727396,
430.194519391107,430.313622175814,430.398193541782),.UNSPECIFIED.);
#325=B_SPLINE_CURVE_WITH_KNOTS('',3,(#48517,#48518,#48519,#48520,#48521,
#48522,#48523,#48524,#48525,#48526),.UNSPECIFIED.,.F.,.F.,(4,3,3,4),(430.146364568078,
430.228825781605,430.313509661627,430.398193541649),.UNSPECIFIED.);
#326=B_SPLINE_CURVE_WITH_KNOTS('',3,(#48527,#48528,#48529,#48530,#48531,
#48532,#48533,#48534,#48535,#48536,#48537,#48538,#48539,#48540,#48541,#48542,
#48543,#48544,#48545,#48546,#48547,#48548,#48549,#48550,#48551,#48552,#48553,
#48554,#48555,#48556,#48557,#48558,#48559,#48560,#48561,#48562,#48563,#48564,
#48565,#48566,#48567,#48568,#48569,#48570,#48571,#48572,#48573,#48574,#48575,
#48576,#48577,#48578,#48579,#48580,#48581,#48582,#48583,#48584,#48585,#48586,
#48587,#48588,#48589,#48590,#48591,#48592,#48593,#48594,#48595,#48596,#48597,
#48598,#48599,#48600,#48601,#48602,#48603,#48604,#48605,#48606,#48607,#48608,
#48609,#48610,#48611,#48612,#48613,#48614,#48615,#48616,#48617,#48618,#48619,
#48620,#48621,#48622,#48623,#48624,#48625,#48626,#48627,#48628,#48629,#48630,
#48631,#48632,#48633,#48634,#48635,#48636,#48637,#48638,#48639,#48640,#48641,
#48642,#48643,#48644,#48645,#48646,#48647,#48648,#48649,#48650,#48651,#48652,
#48653,#48654,#48655,#48656,#48657,#48658,#48659,#48660,#48661,#48662,#48663,
#48664,#48665,#48666,#48667,#48668,#48669,#48670,#48671,#48672,#48673,#48674,
#48675,#48676,#48677,#48678,#48679,#48680,#48681,#48682,#48683,#48684,#48685,
#48686,#48687,#48688,#48689,#48690,#48691,#48692,#48693,#48694,#48695,#48696,
#48697,#48698,#48699,#48700,#48701,#48702,#48703,#48704,#48705,#48706,#48707,
#48708,#48709,#48710,#48711,#48712,#48713,#48714,#48715,#48716,#48717,#48718,
#48719,#48720,#48721,#48722,#48723,#48724,#48725,#48726,#48727,#48728,#48729,
#48730,#48731,#48732,#48733,#48734,#48735,#48736,#48737,#48738,#48739,#48740,
#48741,#48742,#48743),.UNSPECIFIED.,.F.,.F.,(4,3,3,3,3,3,3,3,3,3,3,3,3,
3,3,3,3,3,3,3,3,3,3,3,3,3,3,3,3,3,3,3,3,3,3,3,3,3,3,3,3,3,3,3,3,3,3,3,3,
3,3,3,3,3,3,3,3,3,3,3,3,3,3,3,3,3,3,3,3,3,3,3,4),(430.398193541785,430.504810010823,
430.588548722669,430.672184234036,430.755736677435,430.839226113286,430.922680063899,
431.006116557746,431.089553667501,431.173009462419,431.256553955148,431.340143038089,
431.423866305647,431.504546021543,431.588284733389,431.671920244756,431.755472688155,
431.838962124006,431.922416074619,432.005852568466,432.089289678221,432.172745473139,
432.256289965868,432.339879048809,432.423602316367,432.504282032263,432.588020744109,
432.671656255476,432.755208698875,432.838698134726,432.92215208534,433.005588579186,
433.089025688941,433.172481483859,433.256025976589,433.33961505953,433.423338327087,
433.504018042983,433.587756754829,433.671392266196,433.754944709595,433.838434145446,
433.92188809606,434.005324589906,434.088761699661,434.172217494579,434.255761987309,
434.33935107025,434.423074337807,434.503754053703,434.587492765549,434.671128276916,
434.754680720315,434.838170156166,434.92162410678,435.005060600626,435.088497710381,
435.171953505299,435.255497998029,435.33908708097,435.422810348527,435.503490064423,
435.587232999392,435.670871767371,435.754426504978,435.838867123478,435.922317398153,
436.005749055453,436.089180167143,436.174372988602,436.257893265946,436.343922359462,
436.429951452978),.UNSPECIFIED.);
#327=B_SPLINE_CURVE_WITH_KNOTS('',3,(#48749,#48750,#48751,#48752,#48753,
#48754,#48755,#48756,#48757,#48758,#48759,#48760,#48761,#48762,#48763,#48764,
#48765,#48766,#48767,#48768,#48769,#48770,#48771,#48772,#48773,#48774,#48775,
#48776,#48777,#48778,#48779,#48780,#48781,#48782,#48783,#48784,#48785,#48786,
#48787,#48788,#48789,#48790,#48791,#48792,#48793,#48794,#48795,#48796,#48797,
#48798,#48799,#48800,#48801,#48802,#48803,#48804,#48805,#48806,#48807,#48808,
#48809,#48810,#48811,#48812,#48813,#48814,#48815,#48816,#48817,#48818,#48819,
#48820,#48821,#48822,#48823,#48824,#48825,#48826,#48827,#48828,#48829,#48830,
#48831,#48832,#48833,#48834,#48835,#48836,#48837,#48838,#48839,#48840,#48841,
#48842,#48843,#48844,#48845,#48846,#48847,#48848,#48849,#48850,#48851,#48852,
#48853,#48854,#48855,#48856,#48857,#48858,#48859,#48860,#48861,#48862,#48863,
#48864,#48865,#48866,#48867,#48868,#48869,#48870,#48871,#48872,#48873,#48874,
#48875,#48876,#48877,#48878,#48879,#48880,#48881,#48882,#48883,#48884,#48885,
#48886,#48887,#48888,#48889,#48890,#48891,#48892,#48893,#48894,#48895,#48896,
#48897,#48898,#48899,#48900,#48901,#48902,#48903,#48904,#48905,#48906,#48907,
#48908,#48909,#48910,#48911,#48912,#48913,#48914,#48915,#48916,#48917,#48918,
#48919,#48920,#48921,#48922,#48923,#48924,#48925,#48926,#48927,#48928,#48929,
#48930,#48931,#48932,#48933,#48934,#48935,#48936,#48937,#48938,#48939,#48940,
#48941,#48942,#48943,#48944,#48945,#48946,#48947,#48948,#48949,#48950,#48951,
#48952,#48953,#48954,#48955,#48956,#48957,#48958,#48959,#48960,#48961,#48962,
#48963,#48964,#48965,#48966,#48967,#48968),.UNSPECIFIED.,.F.,.F.,(4,3,3,
3,3,3,3,3,3,3,3,3,3,3,3,3,3,3,3,3,3,3,3,3,3,3,3,3,3,3,3,3,3,3,3,3,3,3,3,
3,3,3,3,3,3,3,3,3,3,3,3,3,3,3,3,3,3,3,3,3,3,3,3,3,3,3,3,3,3,3,3,3,3,4),
(436.681378848961,436.76838027434,436.855482209621,436.942776468581,437.030170281766,
437.117762688149,437.192671466148,437.276410177994,437.360045689362,437.44359813276,
437.527087568611,437.610541519225,437.693978013071,437.777415122827,437.860870917744,
437.944415410474,438.028004493415,438.111727760972,438.192407476868,438.276146188714,
438.359781700081,438.44333414348,438.526823579331,438.610277529944,438.693714023791,
438.777151133546,438.860606928463,438.944151421193,439.027740504134,439.111463771692,
439.192143487588,439.275882199434,439.359517710801,439.4430701542,439.526559590051,
439.610013540665,439.693450034511,439.776887144266,439.860342939184,439.943887431914,
440.027476514855,440.111199782413,440.191879498308,440.275618210154,440.359253721522,
440.44280616492,440.526295600771,440.609749551385,440.693186045231,440.776623154987,
440.860078949904,440.943623442634,441.027212525575,441.110935793133,441.191615509028,
441.275354220874,441.358989732241,441.44254217564,441.526031611491,441.609485562105,
441.692922055951,441.776359165707,441.859814960624,441.943359453354,442.026948536295,
442.110671803853,442.191351519749,442.273972562786,442.356496500643,442.438942469356,
442.52132511321,442.603671489248,442.686007209095,442.713089856218),
 .UNSPECIFIED.);
#328=B_SPLINE_CURVE_WITH_KNOTS('',3,(#48969,#48970,#48971,#48972,#48973,
#48974,#48975,#48976,#48977,#48978),.UNSPECIFIED.,.F.,.F.,(4,3,3,4),(436.431064385021,
436.519119043064,436.606990876881,436.681378848849),.UNSPECIFIED.);
#329=B_SPLINE_CURVE_WITH_KNOTS('',3,(#48980,#48981,#48982,#48983,#48984,
#48985,#48986,#48987,#48988,#48989),.UNSPECIFIED.,.F.,.F.,(4,3,3,4),(436.429951452978,
436.503226075143,436.631173716165,436.681378848965),.UNSPECIFIED.);
#330=B_SPLINE_CURVE_WITH_KNOTS('',3,(#48990,#48991,#48992,#48993,#48994,
#48995,#48996,#48997,#48998,#48999,#49000,#49001,#49002,#49003,#49004,#49005,
#49006,#49007,#49008,#49009,#49010,#49011,#49012,#49013,#49014,#49015,#49016,
#49017,#49018,#49019,#49020,#49021,#49022,#49023,#49024,#49025,#49026,#49027,
#49028,#49029,#49030,#49031,#49032,#49033,#49034,#49035,#49036,#49037,#49038,
#49039,#49040,#49041,#49042,#49043,#49044,#49045,#49046,#49047,#49048,#49049,
#49050,#49051,#49052,#49053,#49054,#49055,#49056,#49057,#49058,#49059,#49060,
#49061,#49062,#49063,#49064,#49065,#49066,#49067,#49068,#49069,#49070,#49071,
#49072,#49073,#49074,#49075,#49076,#49077,#49078,#49079,#49080,#49081,#49082,
#49083,#49084,#49085,#49086,#49087,#49088,#49089,#49090,#49091,#49092,#49093,
#49094,#49095,#49096,#49097,#49098,#49099,#49100,#49101,#49102,#49103,#49104,
#49105,#49106,#49107,#49108,#49109,#49110,#49111,#49112,#49113,#49114,#49115,
#49116,#49117,#49118,#49119,#49120,#49121,#49122,#49123,#49124,#49125,#49126,
#49127,#49128,#49129,#49130,#49131,#49132,#49133,#49134,#49135,#49136,#49137,
#49138,#49139,#49140,#49141,#49142,#49143,#49144,#49145,#49146,#49147,#49148,
#49149,#49150,#49151,#49152,#49153,#49154,#49155,#49156,#49157,#49158,#49159,
#49160,#49161,#49162,#49163,#49164,#49165,#49166,#49167,#49168,#49169,#49170,
#49171,#49172,#49173,#49174,#49175,#49176,#49177,#49178,#49179,#49180,#49181,
#49182,#49183,#49184,#49185,#49186,#49187,#49188,#49189,#49190,#49191,#49192,
#49193,#49194,#49195,#49196,#49197,#49198,#49199,#49200,#49201,#49202,#49203,
#49204,#49205,#49206,#49207,#49208,#49209),.UNSPECIFIED.,.F.,.F.,(4,3,3,
3,3,3,3,3,3,3,3,3,3,3,3,3,3,3,3,3,3,3,3,3,3,3,3,3,3,3,3,3,3,3,3,3,3,3,3,
3,3,3,3,3,3,3,3,3,3,3,3,3,3,3,3,3,3,3,3,3,3,3,3,3,3,3,3,3,3,3,3,3,3,4),
(436.681378849126,436.763742326637,436.846030771284,436.928268660878,437.010480173638,
437.092684349144,437.174900218767,437.257197272248,437.339534460059,437.422002532994,
437.502962085864,437.58670079771,437.670336309077,437.753888752476,437.837378188327,
437.92083213894,438.004268632787,438.087705742542,438.17116153746,438.254706030189,
438.33829511313,438.422018380688,438.502698096584,438.58643680843,438.670072319797,
438.753624763196,438.837114199047,438.92056814966,439.004004643507,439.087441753262,
439.170897548179,439.254442040909,439.33803112385,439.421754391407,439.502434107304,
439.58617281915,439.669808330517,439.753360773916,439.836850209767,439.920304160381,
440.003740654227,440.087177763983,440.1706335589,440.25417805163,440.337767134571,
440.421490402129,440.502170118024,440.58590882987,440.669544341237,440.753096784636,
440.836586220487,440.920040171101,441.003476664947,441.086913774703,441.17036956962,
441.25391406235,441.337503145291,441.421226412849,441.501906128744,441.58564484059,
441.669280351958,441.752832795356,441.836322231208,441.919776181822,442.003212675668,
442.086649785423,442.170105580341,442.253650073071,442.337239156012,442.42096242357,
442.501642139464,442.591309868028,442.680758053547,442.714262803867),
 .UNSPECIFIED.);
#331=B_SPLINE_CURVE_WITH_KNOTS('',3,(#49215,#49216,#49217,#49218,#49219,
#49220,#49221,#49222,#49223,#49224,#49225,#49226,#49227,#49228,#49229,#49230,
#49231,#49232,#49233,#49234,#49235,#49236,#49237,#49238,#49239,#49240,#49241,
#49242,#49243,#49244,#49245,#49246,#49247,#49248,#49249,#49250,#49251,#49252,
#49253,#49254,#49255,#49256,#49257,#49258,#49259,#49260,#49261,#49262,#49263,
#49264,#49265,#49266,#49267,#49268,#49269,#49270,#49271,#49272,#49273,#49274,
#49275,#49276,#49277,#49278,#49279,#49280,#49281,#49282,#49283,#49284,#49285,
#49286,#49287,#49288,#49289,#49290,#49291,#49292,#49293,#49294,#49295,#49296,
#49297,#49298,#49299,#49300,#49301,#49302,#49303,#49304,#49305,#49306,#49307,
#49308,#49309,#49310,#49311,#49312,#49313,#49314,#49315,#49316,#49317,#49318,
#49319,#49320,#49321,#49322,#49323,#49324,#49325,#49326,#49327,#49328,#49329,
#49330,#49331,#49332,#49333,#49334,#49335,#49336,#49337,#49338,#49339,#49340,
#49341,#49342,#49343,#49344,#49345,#49346,#49347,#49348,#49349,#49350,#49351,
#49352,#49353,#49354,#49355,#49356,#49357,#49358,#49359,#49360,#49361,#49362,
#49363,#49364,#49365,#49366,#49367,#49368,#49369,#49370,#49371,#49372,#49373,
#49374,#49375,#49376,#49377,#49378,#49379,#49380,#49381,#49382,#49383,#49384,
#49385,#49386,#49387,#49388,#49389,#49390,#49391,#49392,#49393,#49394,#49395,
#49396,#49397,#49398,#49399,#49400,#49401,#49402,#49403,#49404,#49405,#49406,
#49407,#49408,#49409,#49410,#49411,#49412,#49413,#49414,#49415,#49416,#49417,
#49418,#49419,#49420,#49421,#49422,#49423,#49424,#49425,#49426,#49427,#49428,
#49429,#49430,#49431),.UNSPECIFIED.,.F.,.F.,(4,3,3,3,3,3,3,3,3,3,3,3,3,
3,3,3,3,3,3,3,3,3,3,3,3,3,3,3,3,3,3,3,3,3,3,3,3,3,3,3,3,3,3,3,3,3,3,3,3,
3,3,3,3,3,3,3,3,3,3,3,3,3,3,3,3,3,3,3,3,3,3,3,4),(442.964564156141,443.07782585304,
443.191087530469,443.274826242315,443.358461753682,443.442014197081,443.525503632932,
443.608957583545,443.692394077392,443.775831187147,443.859286982065,443.942831474795,
444.026420557736,444.110143825293,444.190823541189,444.274562253035,444.358197764402,
444.441750207801,444.525239643652,444.608693594266,444.692130088112,444.775567197867,
444.859022992785,444.942567485515,445.026156568456,445.109879836013,445.190559551909,
445.274298263755,445.357933775122,445.441486218521,445.524975654372,445.608429604986,
445.691866098832,445.775303208587,445.858759003505,445.942303496235,446.025892579176,
446.109615846733,446.190295562629,446.274034274475,446.357669785842,446.441222229241,
446.524711665092,446.608165615706,446.691602109552,446.775039219307,446.858495014225,
446.942039506955,447.025628589896,447.109351857453,447.190031573349,447.273770285195,
447.357405796562,447.440958239961,447.524447675812,447.607901626426,447.691338120272,
447.774775230027,447.858231024945,447.941775517675,448.025364600616,448.109087868173,
448.189767584069,448.273517961945,448.357162587647,448.440706191533,448.524192517166,
448.607639684563,448.691065783473,448.774514018599,448.857972936816,448.94149792352,
448.996086608465),.UNSPECIFIED.);
#332=B_SPLINE_CURVE_WITH_KNOTS('',3,(#49432,#49433,#49434,#49435,#49436,
#49437,#49438,#49439,#49440,#49441),.UNSPECIFIED.,.F.,.F.,(4,3,3,4),(442.713089856218,
442.795453856229,442.880009006111,442.964564155993),.UNSPECIFIED.);
#333=B_SPLINE_CURVE_WITH_KNOTS('',3,(#49443,#49444,#49445,#49446,#49447,
#49448,#49449,#49450,#49451,#49452),.UNSPECIFIED.,.F.,.F.,(4,3,3,4),(442.714262803867,
442.803430513116,442.892361191748,442.964564155987),.UNSPECIFIED.);
#334=B_SPLINE_CURVE_WITH_KNOTS('',3,(#49453,#49454,#49455,#49456,#49457,
#49458,#49459,#49460,#49461,#49462,#49463,#49464,#49465,#49466,#49467,#49468,
#49469,#49470,#49471,#49472,#49473,#49474,#49475,#49476,#49477,#49478,#49479,
#49480,#49481,#49482,#49483,#49484,#49485,#49486,#49487,#49488,#49489,#49490,
#49491,#49492,#49493,#49494,#49495,#49496,#49497,#49498,#49499,#49500,#49501,
#49502,#49503,#49504,#49505,#49506,#49507,#49508,#49509,#49510,#49511,#49512,
#49513,#49514,#49515,#49516,#49517,#49518,#49519,#49520,#49521,#49522,#49523,
#49524,#49525,#49526,#49527,#49528,#49529,#49530,#49531,#49532,#49533,#49534,
#49535,#49536,#49537,#49538,#49539,#49540,#49541,#49542,#49543,#49544,#49545,
#49546,#49547,#49548,#49549,#49550,#49551,#49552,#49553,#49554,#49555,#49556,
#49557,#49558,#49559,#49560,#49561,#49562,#49563,#49564,#49565,#49566,#49567,
#49568,#49569,#49570,#49571,#49572,#49573,#49574,#49575,#49576,#49577,#49578,
#49579,#49580,#49581,#49582,#49583,#49584,#49585,#49586,#49587,#49588,#49589,
#49590,#49591,#49592,#49593,#49594,#49595,#49596,#49597,#49598,#49599,#49600,
#49601,#49602,#49603,#49604,#49605,#49606,#49607,#49608,#49609,#49610,#49611,
#49612,#49613,#49614,#49615,#49616,#49617,#49618,#49619,#49620,#49621,#49622,
#49623,#49624,#49625,#49626,#49627,#49628,#49629,#49630,#49631,#49632,#49633,
#49634,#49635,#49636,#49637,#49638,#49639,#49640,#49641,#49642,#49643,#49644,
#49645,#49646,#49647,#49648,#49649,#49650,#49651,#49652,#49653,#49654,#49655,
#49656,#49657,#49658,#49659,#49660,#49661,#49662,#49663,#49664,#49665,#49666,
#49667,#49668,#49669,#49670,#49671,#49672),.UNSPECIFIED.,.F.,.F.,(4,3,3,
3,3,3,3,3,3,3,3,3,3,3,3,3,3,3,3,3,3,3,3,3,3,3,3,3,3,3,3,3,3,3,3,3,3,3,3,
3,3,3,3,3,3,3,3,3,3,3,3,3,3,3,3,3,3,3,3,3,3,3,3,3,3,3,3,3,3,3,3,3,3,4),
(442.964564156144,443.050744981324,443.136998310996,443.223336707115,443.309834552856,
443.396424672269,443.483172125001,443.501378150184,443.58511686203,443.668752373397,
443.752304816796,443.835794252647,443.91924820326,444.002684697107,444.086121806862,
444.16957760178,444.253122094509,444.33671117745,444.420434445008,444.501114160904,
444.58485287275,444.668488384117,444.752040827516,444.835530263367,444.918984213981,
445.002420707827,445.085857817583,445.169313612501,445.25285810523,445.336447188171,
445.420170455729,445.500850171625,445.584588883471,445.668224394839,445.751776838237,
445.835266274088,445.918720224702,446.002156718549,446.085593828304,446.169049623222,
446.252594115951,446.336183198893,446.41990646645,446.500586182345,446.584324894191,
446.667960405559,446.751512848957,446.835002284809,446.918456235422,447.001892729268,
447.085329839024,447.168785633942,447.252330126671,447.335919209612,447.41964247717,
447.500322193065,447.584060904911,447.667696416278,447.751248859677,447.834738295528,
447.918192246142,448.001628739988,448.085065849744,448.168521644661,448.252066137391,
448.335655220332,448.41937848789,448.500058203785,448.582840753366,448.665524929084,
448.748242794626,448.830780781812,448.913588586533,448.996396391254),
 .UNSPECIFIED.);
#335=B_SPLINE_CURVE_WITH_KNOTS('',3,(#49678,#49679,#49680,#49681,#49682,
#49683,#49684,#49685,#49686,#49687),.UNSPECIFIED.,.F.,.F.,(4,1,1,1,1,1,
1,4),(449.247756624963,450.18923960551,451.18897561623,452.18871162695,
453.18844763767,454.18818364839,455.18791965911,455.280414679422),
 .UNSPECIFIED.);
#336=B_SPLINE_CURVE_WITH_KNOTS('',3,(#49688,#49689,#49690,#49691,#49692,
#49693,#49694,#49695,#49696,#49697,#49698,#49699,#49700),.UNSPECIFIED.,
 .F.,.F.,(4,3,3,3,4),(448.996086608465,449.079713584564,449.163459424575,
449.189503594789,449.24774946332),.UNSPECIFIED.);
#337=B_SPLINE_CURVE_WITH_KNOTS('',3,(#49702,#49703,#49704,#49705,#49706,
#49707,#49708,#49709,#49710,#49711),.UNSPECIFIED.,.F.,.F.,(4,3,3,4),(448.996396391254,
449.078902129801,449.163325796563,449.247749463324),.UNSPECIFIED.);
#338=B_SPLINE_CURVE_WITH_KNOTS('',3,(#49712,#49713,#49714,#49715,#49716,
#49717,#49718,#49719,#49720,#49721,#49722,#49723,#49724,#49725,#49726,#49727,
#49728,#49729,#49730,#49731,#49732,#49733,#49734,#49735,#49736,#49737,#49738,
#49739,#49740,#49741,#49742,#49743,#49744,#49745,#49746,#49747,#49748,#49749,
#49750,#49751,#49752,#49753,#49754,#49755,#49756,#49757,#49758,#49759,#49760,
#49761,#49762,#49763,#49764,#49765,#49766,#49767,#49768,#49769,#49770,#49771,
#49772,#49773,#49774,#49775,#49776,#49777,#49778,#49779,#49780,#49781,#49782,
#49783,#49784,#49785,#49786,#49787,#49788,#49789,#49790,#49791,#49792,#49793,
#49794,#49795,#49796,#49797,#49798,#49799,#49800,#49801,#49802,#49803,#49804,
#49805,#49806,#49807,#49808,#49809,#49810,#49811,#49812,#49813,#49814,#49815,
#49816,#49817,#49818,#49819,#49820,#49821,#49822,#49823,#49824,#49825,#49826,
#49827,#49828,#49829,#49830,#49831,#49832,#49833,#49834,#49835,#49836,#49837,
#49838,#49839,#49840,#49841,#49842,#49843,#49844,#49845,#49846,#49847,#49848,
#49849,#49850,#49851,#49852,#49853,#49854,#49855,#49856,#49857,#49858,#49859,
#49860,#49861,#49862,#49863,#49864,#49865,#49866,#49867,#49868,#49869,#49870,
#49871,#49872,#49873,#49874,#49875,#49876,#49877,#49878,#49879,#49880,#49881,
#49882,#49883,#49884,#49885,#49886,#49887,#49888,#49889,#49890,#49891,#49892,
#49893,#49894,#49895,#49896,#49897,#49898,#49899,#49900,#49901,#49902,#49903,
#49904,#49905,#49906,#49907,#49908,#49909,#49910,#49911,#49912,#49913,#49914,
#49915,#49916,#49917,#49918,#49919,#49920,#49921,#49922,#49923,#49924,#49925,
#49926,#49927,#49928,#49929,#49930,#49931),.UNSPECIFIED.,.F.,.F.,(4,3,3,
3,3,3,3,3,3,3,3,3,3,3,3,3,3,3,3,3,3,3,3,3,3,3,3,3,3,3,3,3,3,3,3,3,3,3,3,
3,3,3,3,3,3,3,3,3,3,3,3,3,3,3,3,3,3,3,3,3,3,3,3,3,3,3,3,3,3,3,3,3,3,4),
(449.247749463518,449.354662883124,449.463928728413,449.499794214505,449.583532926351,
449.667168437718,449.750720881117,449.834210316968,449.917664267582,450.001100761428,
450.084537871183,450.167993666101,450.251538158831,450.335127241772,450.41885050933,
450.499530225225,450.583268937071,450.666904448438,450.750456891837,450.833946327688,
450.917400278301,451.000836772148,451.084273881903,451.16772967682,451.25127416955,
451.334863252491,451.418586520049,451.499266235945,451.583004947791,451.666640459158,
451.750192902557,451.833682338408,451.917136289022,452.000572782868,452.084009892624,
452.167465687541,452.251010180271,452.334599263212,452.41832253077,452.499002246665,
452.582740958511,452.666376469879,452.749928913277,452.833418349128,452.916872299742,
453.000308793588,453.083745903344,453.167201698261,453.250746190991,453.334335273932,
453.41805854149,453.498738257386,453.582476969232,453.666112480599,453.749664923998,
453.833154359849,453.916608310463,454.000044804309,454.083481914064,454.166937708982,
454.250482201712,454.334071284653,454.41779455221,454.498474268106,454.582226310188,
454.669356649698,454.752898041365,454.836382433444,454.919827945315,455.00325266616,
455.086695649327,455.170149799188,455.253659187583,455.279269026268),
 .UNSPECIFIED.);
#339=B_SPLINE_CURVE_WITH_KNOTS('',3,(#49937,#49938,#49939,#49940,#49941,
#49942,#49943,#49944,#49945,#49946),.UNSPECIFIED.,.F.,.F.,(4,1,1,1,1,1,
1,4),(455.5309347705,456.18765566983,457.18739168055,458.187127691271,459.186863701991,
460.186599712711,461.186335723431,461.563668011779),.UNSPECIFIED.);
#340=B_SPLINE_CURVE_WITH_KNOTS('',3,(#49947,#49948,#49949,#49950),
 .UNSPECIFIED.,.F.,.F.,(4,4),(455.280414679422,455.5309347705),
 .UNSPECIFIED.);
#341=B_SPLINE_CURVE_WITH_KNOTS('',3,(#49952,#49953,#49954,#49955,#49956,
#49957,#49958,#49959,#49960,#49961,#49962,#49963,#49964),.UNSPECIFIED.,
 .F.,.F.,(4,3,3,3,4),(455.279269026268,455.362877418155,455.44661163974,
455.498210278826,455.530934770504),.UNSPECIFIED.);
#342=B_SPLINE_CURVE_WITH_KNOTS('',3,(#49965,#49966,#49967,#49968,#49969,
#49970,#49971,#49972,#49973,#49974,#49975,#49976,#49977,#49978,#49979,#49980,
#49981,#49982,#49983,#49984,#49985,#49986,#49987,#49988,#49989,#49990,#49991,
#49992,#49993,#49994,#49995,#49996,#49997,#49998,#49999,#50000,#50001,#50002,
#50003,#50004,#50005,#50006,#50007,#50008,#50009,#50010,#50011,#50012,#50013,
#50014,#50015,#50016,#50017,#50018,#50019,#50020,#50021,#50022,#50023,#50024,
#50025,#50026,#50027,#50028,#50029,#50030,#50031,#50032,#50033,#50034,#50035,
#50036,#50037,#50038,#50039,#50040,#50041,#50042,#50043,#50044,#50045,#50046,
#50047,#50048,#50049,#50050,#50051,#50052,#50053,#50054,#50055,#50056,#50057,
#50058,#50059,#50060,#50061,#50062,#50063,#50064,#50065,#50066,#50067,#50068,
#50069,#50070,#50071,#50072,#50073,#50074,#50075,#50076,#50077,#50078,#50079,
#50080,#50081,#50082,#50083,#50084,#50085,#50086,#50087,#50088,#50089,#50090,
#50091,#50092,#50093,#50094,#50095,#50096,#50097,#50098,#50099,#50100,#50101,
#50102,#50103,#50104,#50105,#50106,#50107,#50108,#50109,#50110,#50111,#50112,
#50113,#50114,#50115,#50116,#50117,#50118,#50119,#50120,#50121,#50122,#50123,
#50124,#50125,#50126,#50127,#50128,#50129,#50130,#50131,#50132,#50133,#50134,
#50135,#50136,#50137,#50138,#50139,#50140,#50141,#50142,#50143,#50144,#50145,
#50146,#50147,#50148,#50149,#50150,#50151,#50152,#50153,#50154,#50155,#50156,
#50157,#50158,#50159,#50160,#50161,#50162,#50163,#50164,#50165,#50166,#50167,
#50168,#50169,#50170,#50171,#50172,#50173,#50174,#50175,#50176,#50177,#50178,
#50179,#50180,#50181,#50182,#50183,#50184),.UNSPECIFIED.,.F.,.F.,(4,3,3,
3,3,3,3,3,3,3,3,3,3,3,3,3,3,3,3,3,3,3,3,3,3,3,3,3,3,3,3,3,3,3,3,3,3,3,3,
3,3,3,3,3,3,3,3,3,3,3,3,3,3,3,3,3,3,3,3,3,3,3,3,3,3,3,3,3,3,3,3,3,3,4),
(455.530934770647,455.614220758589,455.697405044271,455.780508205535,455.863550744547,
455.94656131294,456.029557396033,456.112557464698,456.195579989061,456.278691780244,
456.361852309144,456.445138217639,456.497946289546,456.581685001392,456.665320512759,
456.748872956158,456.832362392009,456.915816342623,456.999252836469,457.082689946224,
457.166145741142,457.249690233872,457.333279316813,457.41700258437,457.497682300266,
457.581421012112,457.665056523479,457.748608966878,457.832098402729,457.915552353342,
457.998988847189,458.082425956944,458.165881751862,458.249426244592,458.333015327533,
458.41673859509,458.497418310986,458.581157022832,458.664792534199,458.748344977598,
458.831834413449,458.915288364063,458.99872485791,459.082161967665,459.165617762583,
459.249162255312,459.332751338254,459.416474605811,459.497154321706,459.580893033552,
459.66452854492,459.748080988318,459.83157042417,459.915024374783,459.99846086863,
460.081897978385,460.165353773303,460.248898266033,460.332487348974,460.416210616532,
460.496890332427,460.580629044273,460.66426455564,460.747816999039,460.83130643489,
460.914760385504,460.99819687935,461.081633989105,461.165089784023,461.248634276753,
461.332223359694,461.415946627251,461.496626343147,461.563437609655),
 .UNSPECIFIED.);
#343=B_SPLINE_CURVE_WITH_KNOTS('',3,(#50190,#50191,#50192,#50193,#50194,
#50195,#50196,#50197,#50198,#50199,#50200,#50201,#50202,#50203,#50204,#50205,
#50206,#50207,#50208,#50209,#50210,#50211,#50212,#50213,#50214,#50215,#50216,
#50217,#50218,#50219,#50220,#50221,#50222,#50223,#50224,#50225,#50226,#50227,
#50228,#50229,#50230,#50231,#50232,#50233,#50234,#50235,#50236,#50237,#50238,
#50239,#50240,#50241,#50242,#50243,#50244,#50245,#50246,#50247,#50248,#50249,
#50250,#50251,#50252,#50253,#50254,#50255,#50256,#50257,#50258,#50259,#50260,
#50261,#50262,#50263,#50264,#50265,#50266,#50267,#50268,#50269,#50270,#50271,
#50272,#50273,#50274,#50275,#50276,#50277,#50278,#50279,#50280,#50281,#50282,
#50283,#50284,#50285,#50286,#50287,#50288,#50289,#50290,#50291,#50292,#50293,
#50294,#50295,#50296,#50297,#50298,#50299,#50300,#50301,#50302,#50303,#50304,
#50305,#50306,#50307,#50308,#50309,#50310,#50311,#50312,#50313,#50314,#50315,
#50316,#50317,#50318,#50319,#50320,#50321,#50322,#50323,#50324,#50325,#50326,
#50327,#50328,#50329,#50330,#50331,#50332,#50333,#50334,#50335,#50336,#50337,
#50338,#50339,#50340,#50341,#50342,#50343,#50344,#50345,#50346,#50347,#50348,
#50349,#50350,#50351,#50352,#50353,#50354,#50355,#50356,#50357,#50358,#50359,
#50360,#50361,#50362,#50363,#50364,#50365,#50366,#50367,#50368,#50369,#50370,
#50371,#50372,#50373,#50374,#50375,#50376,#50377,#50378,#50379,#50380,#50381,
#50382,#50383,#50384,#50385,#50386,#50387,#50388,#50389,#50390,#50391,#50392,
#50393,#50394,#50395,#50396,#50397,#50398,#50399,#50400,#50401,#50402,#50403,
#50404,#50405,#50406),.UNSPECIFIED.,.F.,.F.,(4,3,3,3,3,3,3,3,3,3,3,3,3,
3,3,3,3,3,3,3,3,3,3,3,3,3,3,3,3,3,3,3,3,3,3,3,3,3,3,3,3,3,3,3,3,3,3,3,3,
3,3,3,3,3,3,3,3,3,3,3,3,3,3,3,3,3,3,3,3,3,3,3,4),(461.814120077679,461.908277085704,
462.002806830092,462.09786318546,462.186071734151,462.269810445997,462.353445957364,
462.436998400763,462.520487836614,462.603941787228,462.687378281074,462.77081539083,
462.854271185747,462.937815678477,463.021404761418,463.105128028975,463.185807744871,
463.269546456717,463.353181968084,463.436734411483,463.520223847334,463.603677797948,
463.687114291794,463.77055140155,463.854007196467,463.937551689197,464.021140772138,
464.104864039696,464.185543755591,464.269282467437,464.352917978804,464.436470422203,
464.519959858054,464.603413808668,464.686850302514,464.77028741227,464.853743207187,
464.937287699917,465.020876782858,465.104600050416,465.185279766312,465.269018478158,
465.352653989526,465.436206432924,465.519695868775,465.603149819389,465.686586313236,
465.770023422991,465.853479217909,465.937023710639,466.02061279358,466.104336061137,
466.185015777032,466.268754488878,466.352390000245,466.435942443644,466.519431879495,
466.602885830109,466.686322323955,466.76975943371,466.853215228628,466.936759721357,
467.020348804298,467.104072071856,467.184751787752,467.26750532906,467.350164327694,
467.432747806821,467.515274722903,467.597822988734,467.680304873322,467.762886329776,
467.845467786229),.UNSPECIFIED.);
#344=B_SPLINE_CURVE_WITH_KNOTS('',3,(#50407,#50408,#50409,#50410),
 .UNSPECIFIED.,.F.,.F.,(4,4),(461.563668011779,461.814120077679),
 .UNSPECIFIED.);
#345=B_SPLINE_CURVE_WITH_KNOTS('',3,(#50412,#50413,#50414,#50415,#50416,
#50417,#50418,#50419,#50420,#50421),.UNSPECIFIED.,.F.,.F.,(4,3,3,4),(461.563437609655,
461.663143498821,461.761828896827,461.814120077512),.UNSPECIFIED.);
#346=B_SPLINE_CURVE_WITH_KNOTS('',3,(#50422,#50423,#50424,#50425,#50426,
#50427,#50428,#50429,#50430,#50431,#50432,#50433,#50434,#50435,#50436,#50437,
#50438,#50439,#50440,#50441,#50442,#50443,#50444,#50445,#50446,#50447,#50448,
#50449,#50450,#50451,#50452,#50453,#50454,#50455,#50456,#50457,#50458,#50459,
#50460,#50461,#50462,#50463,#50464,#50465,#50466,#50467,#50468,#50469,#50470,
#50471,#50472,#50473,#50474,#50475,#50476,#50477,#50478,#50479,#50480,#50481,
#50482,#50483,#50484,#50485,#50486,#50487,#50488,#50489,#50490,#50491,#50492,
#50493,#50494,#50495,#50496,#50497,#50498,#50499,#50500,#50501,#50502,#50503,
#50504,#50505,#50506,#50507,#50508,#50509,#50510,#50511,#50512,#50513,#50514,
#50515,#50516,#50517,#50518,#50519,#50520,#50521,#50522,#50523,#50524,#50525,
#50526,#50527,#50528,#50529,#50530,#50531,#50532,#50533,#50534,#50535,#50536,
#50537,#50538,#50539,#50540,#50541,#50542,#50543,#50544,#50545,#50546,#50547,
#50548,#50549,#50550,#50551,#50552,#50553,#50554,#50555,#50556,#50557,#50558,
#50559,#50560,#50561,#50562,#50563,#50564,#50565,#50566,#50567,#50568,#50569,
#50570,#50571,#50572,#50573,#50574,#50575,#50576,#50577,#50578,#50579,#50580,
#50581,#50582,#50583,#50584,#50585,#50586,#50587,#50588,#50589,#50590,#50591,
#50592,#50593,#50594,#50595,#50596,#50597,#50598,#50599,#50600,#50601,#50602,
#50603,#50604,#50605,#50606,#50607,#50608,#50609,#50610,#50611,#50612,#50613,
#50614,#50615,#50616,#50617,#50618,#50619,#50620,#50621,#50622,#50623,#50624,
#50625,#50626,#50627,#50628,#50629,#50630,#50631,#50632,#50633,#50634,#50635,
#50636,#50637,#50638,#50639,#50640,#50641,#50642,#50643,#50644),
 .UNSPECIFIED.,.F.,.F.,(4,3,3,3,3,3,3,3,3,3,3,3,3,3,3,3,3,3,3,3,3,3,3,3,
3,3,3,3,3,3,3,3,3,3,3,3,3,3,3,3,3,3,3,3,3,3,3,3,3,3,3,3,3,3,3,3,3,3,3,3,
3,3,3,3,3,3,3,3,3,3,3,3,3,3,4),(461.814120077683,461.899400362206,461.982557506644,
462.065713177296,462.148885659595,462.235754833163,462.319063252884,462.402432042527,
462.485918963466,462.496362353867,462.580101065713,462.66373657708,462.747289020479,
462.83077845633,462.914232406944,462.99766890079,463.081106010546,463.164561805463,
463.248106298193,463.331695381134,463.415418648691,463.496098364587,463.579837076433,
463.6634725878,463.747025031199,463.830514467049,463.913968417663,463.997404911509,
464.080842021265,464.164297816183,464.247842308912,464.331431391853,464.415154659411,
464.495834375307,464.579573087153,464.66320859852,464.746761041919,464.83025047777,
464.913704428384,464.99714092223,465.080578031985,465.164033826903,465.247578319632,
465.331167402573,465.414890670131,465.495570386027,465.579309097873,465.66294460924,
465.746497052639,465.82998648849,465.913440439103,465.99687693295,466.080314042705,
466.163769837623,466.247314330353,466.330903413294,466.414626680851,466.495306396747,
466.579045108593,466.662680619961,466.746233063359,466.82972249921,466.913176449824,
466.99661294367,467.080050053425,467.163505848343,467.247050341073,467.330639424014,
467.414362691571,467.495042407467,467.582950874621,467.667748959495,467.752460450876,
467.837084945233,467.846676276085),.UNSPECIFIED.);
#347=B_SPLINE_CURVE_WITH_KNOTS('',3,(#50650,#50651,#50652,#50653,#50654,
#50655,#50656,#50657,#50658,#50659,#50660,#50661,#50662,#50663,#50664,#50665,
#50666,#50667,#50668,#50669,#50670,#50671,#50672,#50673,#50674,#50675,#50676,
#50677,#50678,#50679,#50680,#50681,#50682,#50683,#50684,#50685,#50686,#50687,
#50688,#50689,#50690,#50691,#50692,#50693,#50694,#50695,#50696,#50697,#50698,
#50699,#50700,#50701,#50702,#50703,#50704,#50705,#50706,#50707,#50708,#50709,
#50710,#50711,#50712,#50713,#50714,#50715,#50716,#50717,#50718,#50719,#50720,
#50721,#50722,#50723,#50724,#50725,#50726,#50727,#50728,#50729,#50730,#50731,
#50732,#50733,#50734,#50735,#50736,#50737,#50738,#50739,#50740,#50741,#50742,
#50743,#50744,#50745,#50746,#50747,#50748,#50749,#50750,#50751,#50752,#50753,
#50754,#50755,#50756,#50757,#50758,#50759,#50760,#50761,#50762,#50763,#50764,
#50765,#50766,#50767,#50768,#50769,#50770,#50771,#50772,#50773,#50774,#50775,
#50776,#50777,#50778,#50779,#50780,#50781,#50782,#50783,#50784,#50785,#50786,
#50787,#50788,#50789,#50790,#50791,#50792,#50793,#50794,#50795,#50796,#50797,
#50798,#50799,#50800,#50801,#50802,#50803,#50804,#50805,#50806,#50807,#50808,
#50809,#50810,#50811,#50812,#50813,#50814,#50815,#50816,#50817,#50818,#50819,
#50820,#50821,#50822,#50823,#50824,#50825,#50826,#50827,#50828,#50829,#50830,
#50831,#50832,#50833,#50834,#50835,#50836,#50837,#50838,#50839,#50840,#50841,
#50842,#50843,#50844,#50845,#50846,#50847,#50848,#50849,#50850,#50851,#50852,
#50853,#50854,#50855,#50856,#50857,#50858,#50859,#50860,#50861,#50862,#50863,
#50864,#50865,#50866,#50867,#50868,#50869),.UNSPECIFIED.,.F.,.F.,(4,3,3,
3,3,3,3,3,3,3,3,3,3,3,3,3,3,3,3,3,3,3,3,3,3,3,3,3,3,3,3,3,3,3,3,3,3,3,3,
3,3,3,3,3,3,3,3,3,3,3,3,3,3,3,3,3,3,3,3,3,3,3,3,3,3,3,3,3,3,3,3,3,3,4),
(468.097305384859,468.184487798472,468.268226510318,468.351862021685,468.435414465084,
468.518903900935,468.602357851549,468.685794345395,468.76923145515,468.852687250068,
468.936231742798,469.019820825739,469.103544093296,469.184223809192,469.267962521038,
469.351598032405,469.435150475804,469.518639911655,469.602093862269,469.685530356115,
469.76896746587,469.852423260788,469.935967753518,470.019556836459,470.103280104016,
470.183959819912,470.267698531758,470.351334043125,470.434886486524,470.518375922375,
470.601829872989,470.685266366835,470.76870347659,470.852159271508,470.935703764237,
471.019292847178,471.103016114736,471.183695830632,471.267434542478,471.351070053845,
471.434622497244,471.518111933095,471.601565883709,471.685002377555,471.768439487311,
471.851895282228,471.935439774958,472.019028857899,472.102752125457,472.183431841352,
472.267170553198,472.350806064566,472.434358507964,472.517847943815,472.601301894429,
472.684738388275,472.768175498031,472.851631292948,472.935175785678,473.018764868619,
473.102488136177,473.183167852073,473.266909639042,473.350547516417,473.434101619712,
473.520981630997,473.604431920655,473.68786448522,473.771297396346,473.854748721871,
473.938275693383,474.021847500333,474.105521992394,474.129141709994),
 .UNSPECIFIED.);
#348=B_SPLINE_CURVE_WITH_KNOTS('',3,(#50870,#50871,#50872,#50873,#50874,
#50875,#50876,#50877,#50878,#50879),.UNSPECIFIED.,.F.,.F.,(4,3,3,4),(467.845467786229,
467.928060537647,468.012682961186,468.097305384725),.UNSPECIFIED.);
#349=B_SPLINE_CURVE_WITH_KNOTS('',3,(#50881,#50882,#50883,#50884,#50885,
#50886,#50887,#50888,#50889,#50890),.UNSPECIFIED.,.F.,.F.,(4,3,3,4),(467.846676276085,
467.931227320063,468.015745325857,468.097305384863),.UNSPECIFIED.);
#350=B_SPLINE_CURVE_WITH_KNOTS('',3,(#50891,#50892,#50893,#50894,#50895,
#50896,#50897,#50898,#50899,#50900,#50901,#50902,#50903,#50904,#50905,#50906,
#50907,#50908,#50909,#50910,#50911,#50912,#50913,#50914,#50915,#50916,#50917,
#50918,#50919,#50920,#50921,#50922,#50923,#50924,#50925,#50926,#50927,#50928,
#50929,#50930,#50931,#50932,#50933,#50934,#50935,#50936,#50937,#50938,#50939,
#50940,#50941,#50942,#50943,#50944,#50945,#50946,#50947,#50948,#50949,#50950,
#50951,#50952,#50953,#50954,#50955,#50956,#50957,#50958,#50959,#50960,#50961,
#50962,#50963,#50964,#50965,#50966,#50967,#50968,#50969,#50970,#50971,#50972,
#50973,#50974,#50975,#50976,#50977,#50978,#50979,#50980,#50981,#50982,#50983,
#50984,#50985,#50986,#50987,#50988,#50989,#50990,#50991,#50992,#50993,#50994,
#50995,#50996,#50997,#50998,#50999,#51000,#51001,#51002,#51003,#51004,#51005,
#51006,#51007,#51008,#51009,#51010,#51011,#51012,#51013,#51014,#51015,#51016,
#51017,#51018,#51019,#51020,#51021,#51022,#51023,#51024,#51025,#51026,#51027,
#51028,#51029,#51030,#51031,#51032,#51033,#51034,#51035,#51036,#51037,#51038,
#51039,#51040,#51041,#51042,#51043,#51044,#51045,#51046,#51047,#51048,#51049,
#51050,#51051,#51052,#51053,#51054,#51055,#51056,#51057,#51058,#51059,#51060,
#51061,#51062,#51063,#51064,#51065,#51066,#51067,#51068,#51069,#51070,#51071,
#51072,#51073,#51074,#51075,#51076,#51077,#51078,#51079,#51080,#51081,#51082,
#51083,#51084,#51085,#51086,#51087,#51088,#51089,#51090,#51091,#51092,#51093,
#51094,#51095,#51096,#51097,#51098,#51099,#51100,#51101,#51102,#51103,#51104,
#51105,#51106,#51107,#51108,#51109,#51110),.UNSPECIFIED.,.F.,.F.,(4,3,3,
3,3,3,3,3,3,3,3,3,3,3,3,3,3,3,3,3,3,3,3,3,3,3,3,3,3,3,3,3,3,3,3,3,3,3,3,
3,3,3,3,3,3,3,3,3,3,3,3,3,3,3,3,3,3,3,3,3,3,3,3,3,3,3,3,3,3,3,3,3,3,4),
(468.097305385047,468.189543032656,468.282286929498,468.375293080407,468.468637906394,
468.494778418188,468.578517130034,468.662152641401,468.7457050848,468.829194520651,
468.912648471265,468.996084965111,469.079522074867,469.162977869784,469.246522362514,
469.330111445455,469.413834713013,469.494514428908,469.578253140754,469.661888652121,
469.74544109552,469.828930531371,469.912384481985,469.995820975831,470.079258085586,
470.162713880504,470.246258373234,470.329847456174,470.413570723732,470.494250439628,
470.577989151474,470.661624662841,470.74517710624,470.828666542091,470.912120492705,
470.995556986551,471.078994096307,471.162449891224,471.245994383954,471.329583466895,
471.413306734453,471.493986450348,471.577725162194,471.661360673561,471.74491311696,
471.828402552811,471.911856503425,471.995292997271,472.078730107026,472.162185901944,
472.245730394673,472.329319477614,472.413042745172,472.493722461068,472.577461172914,
472.661096684282,472.74464912768,472.828138563531,472.911592514145,472.995029007991,
473.078466117747,473.161921912664,473.245466405394,473.329055488335,473.412778755893,
473.493458471788,473.57606110231,473.658569104472,473.741001605987,473.823377664764,
473.905725141663,473.988054434924,474.070408822026,474.128667782826),
 .UNSPECIFIED.);
#351=B_SPLINE_CURVE_WITH_KNOTS('',3,(#51116,#51117,#51118,#51119,#51120,
#51121,#51122,#51123,#51124,#51125,#51126,#51127,#51128,#51129,#51130,#51131,
#51132,#51133,#51134,#51135,#51136,#51137,#51138,#51139,#51140,#51141,#51142,
#51143,#51144,#51145,#51146,#51147,#51148,#51149,#51150,#51151,#51152,#51153,
#51154,#51155,#51156,#51157,#51158,#51159,#51160,#51161,#51162,#51163,#51164,
#51165,#51166,#51167,#51168,#51169,#51170,#51171,#51172,#51173,#51174,#51175,
#51176,#51177,#51178,#51179,#51180,#51181,#51182,#51183,#51184,#51185,#51186,
#51187,#51188,#51189,#51190,#51191,#51192,#51193,#51194,#51195,#51196,#51197,
#51198,#51199,#51200,#51201,#51202,#51203,#51204,#51205,#51206,#51207,#51208,
#51209,#51210,#51211,#51212,#51213,#51214,#51215,#51216,#51217,#51218,#51219,
#51220,#51221,#51222,#51223,#51224,#51225,#51226,#51227,#51228,#51229,#51230,
#51231,#51232,#51233,#51234,#51235,#51236,#51237,#51238,#51239,#51240,#51241,
#51242,#51243,#51244,#51245,#51246,#51247,#51248,#51249,#51250,#51251,#51252,
#51253,#51254,#51255,#51256,#51257,#51258,#51259,#51260,#51261,#51262,#51263,
#51264,#51265,#51266,#51267,#51268,#51269,#51270,#51271,#51272,#51273,#51274,
#51275,#51276,#51277,#51278,#51279,#51280,#51281,#51282,#51283,#51284,#51285,
#51286,#51287,#51288,#51289,#51290,#51291,#51292,#51293,#51294,#51295,#51296,
#51297,#51298,#51299,#51300,#51301,#51302,#51303,#51304,#51305,#51306,#51307,
#51308,#51309,#51310,#51311,#51312,#51313,#51314,#51315,#51316,#51317,#51318,
#51319,#51320,#51321,#51322,#51323,#51324,#51325,#51326,#51327,#51328,#51329,
#51330,#51331,#51332,#51333,#51334,#51335),.UNSPECIFIED.,.F.,.F.,(4,3,3,
3,3,3,3,3,3,3,3,3,3,3,3,3,3,3,3,3,3,3,3,3,3,3,3,3,3,3,3,3,3,3,3,3,3,3,3,
3,3,3,3,3,3,3,3,3,3,3,3,3,3,3,3,3,3,3,3,3,3,3,3,3,3,3,3,3,3,3,3,3,3,4),
(474.380490692145,474.462864309227,474.545168268208,474.627428853586,474.709667867551,
474.791904327036,474.874157244687,474.95649402033,475.038875176067,475.121381803559,
475.182639873513,475.266378585359,475.350014096726,475.433566540125,475.517055975976,
475.60050992659,475.683946420436,475.767383530192,475.850839325109,475.934383817839,
476.01797290078,476.101696168337,476.182375884233,476.266114596079,476.349750107446,
476.433302550845,476.516791986696,476.60024593731,476.683682431156,476.767119540911,
476.850575335829,476.934119828559,477.0177089115,477.101432179057,477.182111894953,
477.265850606799,477.349486118166,477.433038561565,477.516527997415,477.599981948029,
477.683418441875,477.766855551631,477.850311346548,477.933855839278,478.017444922219,
478.101168189777,478.181847905673,478.265586617519,478.349222128886,478.432774572285,
478.516264008136,478.59971795875,478.683154452596,478.766591562351,478.850047357269,
478.933591849999,479.01718093294,479.100904200497,479.181583916393,479.265322628239,
479.348958139607,479.432510583006,479.516000018856,479.59945396947,479.682890463316,
479.766327573071,479.849783367989,479.933327860719,480.01691694366,480.100640211218,
480.181319927113,480.27010194833,480.358677088798,480.413366811053),
 .UNSPECIFIED.);
#352=B_SPLINE_CURVE_WITH_KNOTS('',3,(#51336,#51337,#51338,#51339,#51340,
#51341,#51342,#51343,#51344,#51345),.UNSPECIFIED.,.F.,.F.,(4,3,3,4),(474.129141709994,
474.182903862793,474.30385189376,474.380490692039),.UNSPECIFIED.);
#353=B_SPLINE_CURVE_WITH_KNOTS('',3,(#51347,#51348,#51349,#51350,#51351,
#51352,#51353,#51354,#51355,#51356),.UNSPECIFIED.,.F.,.F.,(4,3,3,4),(474.128667782826,
474.211094423954,474.29579255793,474.380490691907),.UNSPECIFIED.);
#354=B_SPLINE_CURVE_WITH_KNOTS('',3,(#51357,#51358,#51359,#51360,#51361,
#51362,#51363,#51364,#51365,#51366,#51367,#51368,#51369,#51370,#51371,#51372,
#51373,#51374,#51375,#51376,#51377,#51378,#51379,#51380,#51381,#51382,#51383,
#51384,#51385,#51386,#51387,#51388,#51389,#51390,#51391,#51392,#51393,#51394,
#51395,#51396,#51397,#51398,#51399,#51400,#51401,#51402,#51403,#51404,#51405,
#51406,#51407,#51408,#51409,#51410,#51411,#51412,#51413,#51414,#51415,#51416,
#51417,#51418,#51419,#51420,#51421,#51422,#51423,#51424,#51425,#51426,#51427,
#51428,#51429,#51430,#51431,#51432,#51433,#51434,#51435,#51436,#51437,#51438,
#51439,#51440,#51441,#51442,#51443,#51444,#51445,#51446,#51447,#51448,#51449,
#51450,#51451,#51452,#51453,#51454,#51455,#51456,#51457,#51458,#51459,#51460,
#51461,#51462,#51463,#51464,#51465,#51466,#51467,#51468,#51469,#51470,#51471,
#51472,#51473,#51474,#51475,#51476,#51477,#51478,#51479,#51480,#51481,#51482,
#51483,#51484,#51485,#51486,#51487,#51488,#51489,#51490,#51491,#51492,#51493,
#51494,#51495,#51496,#51497,#51498,#51499,#51500,#51501,#51502,#51503,#51504,
#51505,#51506,#51507,#51508,#51509,#51510,#51511,#51512,#51513,#51514,#51515,
#51516,#51517,#51518,#51519,#51520,#51521,#51522,#51523,#51524,#51525,#51526,
#51527,#51528,#51529,#51530,#51531,#51532,#51533,#51534,#51535,#51536,#51537,
#51538,#51539,#51540,#51541,#51542,#51543,#51544,#51545,#51546,#51547,#51548,
#51549,#51550,#51551,#51552,#51553,#51554,#51555,#51556,#51557,#51558,#51559,
#51560,#51561,#51562,#51563,#51564,#51565,#51566,#51567,#51568,#51569,#51570,
#51571,#51572,#51573),.UNSPECIFIED.,.F.,.F.,(4,3,3,3,3,3,3,3,3,3,3,3,3,
3,3,3,3,3,3,3,3,3,3,3,3,3,3,3,3,3,3,3,3,3,3,3,3,3,3,3,3,3,3,3,3,3,3,3,3,
3,3,3,3,3,3,3,3,3,3,3,3,3,3,3,3,3,3,3,3,3,3,3,4),(474.380490692042,474.493194482508,
474.576933194354,474.660568705722,474.74412114912,474.827610584971,474.911064535585,
474.994501029431,475.077938139187,475.161393934104,475.244938426834,475.328527509775,
475.412250777333,475.492930493229,475.576669205075,475.660304716442,475.743857159841,
475.827346595692,475.910800546306,475.994237040152,476.077674149907,476.161129944825,
476.244674437555,476.328263520496,476.411986788053,476.492666503949,476.576405215795,
476.660040727162,476.743593170561,476.827082606412,476.910536557026,476.993973050872,
477.077410160627,477.160865955545,477.244410448275,477.327999531216,477.411722798773,
477.492402514669,477.576141226515,477.659776737882,477.743329181281,477.826818617132,
477.910272567746,477.993709061592,478.077146171347,478.160601966265,478.244146458995,
478.327735541936,478.411458809493,478.492138525389,478.575877237235,478.659512748602,
478.743065192001,478.826554627852,478.910008578466,478.993445072312,479.076882182067,
479.160337976985,479.243882469715,479.327471552656,479.411194820213,479.491874536109,
479.57561783401,479.659256884327,479.742811824025,479.826488668858,479.909938960391,
479.99337035517,480.076800925009,480.160657339428,480.244174762693,480.328200672689,
480.412226582686),.UNSPECIFIED.);
#355=B_SPLINE_CURVE_WITH_KNOTS('',3,(#51579,#51580,#51581,#51582,#51583,
#51584,#51585,#51586,#51587,#51588,#51589,#51590,#51591,#51592,#51593,#51594,
#51595,#51596,#51597,#51598,#51599,#51600,#51601,#51602,#51603,#51604,#51605,
#51606,#51607,#51608,#51609,#51610,#51611,#51612,#51613,#51614,#51615,#51616,
#51617,#51618,#51619,#51620,#51621,#51622,#51623,#51624,#51625,#51626,#51627,
#51628,#51629,#51630,#51631,#51632,#51633,#51634,#51635,#51636,#51637,#51638,
#51639,#51640,#51641,#51642,#51643,#51644,#51645,#51646,#51647,#51648,#51649,
#51650,#51651,#51652,#51653,#51654,#51655,#51656,#51657,#51658,#51659,#51660,
#51661,#51662,#51663,#51664,#51665,#51666,#51667,#51668,#51669,#51670,#51671,
#51672,#51673,#51674,#51675,#51676,#51677,#51678,#51679,#51680,#51681,#51682,
#51683,#51684,#51685,#51686,#51687,#51688,#51689,#51690,#51691,#51692,#51693,
#51694,#51695,#51696,#51697,#51698,#51699,#51700,#51701,#51702,#51703,#51704,
#51705,#51706,#51707,#51708,#51709,#51710,#51711,#51712,#51713,#51714,#51715,
#51716,#51717,#51718,#51719,#51720,#51721,#51722,#51723,#51724,#51725,#51726,
#51727,#51728,#51729,#51730,#51731,#51732,#51733,#51734,#51735,#51736,#51737,
#51738,#51739,#51740,#51741,#51742,#51743,#51744,#51745,#51746,#51747,#51748,
#51749,#51750,#51751,#51752,#51753,#51754,#51755,#51756,#51757,#51758,#51759,
#51760,#51761,#51762,#51763,#51764,#51765,#51766,#51767,#51768,#51769,#51770,
#51771,#51772,#51773,#51774,#51775,#51776,#51777,#51778,#51779,#51780,#51781,
#51782,#51783,#51784,#51785,#51786,#51787,#51788,#51789,#51790,#51791,#51792,
#51793,#51794,#51795,#51796,#51797,#51798),.UNSPECIFIED.,.F.,.F.,(4,3,3,
3,3,3,3,3,3,3,3,3,3,3,3,3,3,3,3,3,3,3,3,3,3,3,3,3,3,3,3,3,3,3,3,3,3,3,3,
3,3,3,3,3,3,3,3,3,3,3,3,3,3,3,3,3,3,3,3,3,3,3,3,3,3,3,3,3,3,3,3,3,3,4),
(480.663675999218,480.750472077734,480.837361456173,480.924435942999,481.011605159472,
481.098971661175,481.181055937834,481.26479464968,481.348430161048,481.431982604446,
481.515472040297,481.598925990911,481.682362484757,481.765799594513,481.84925538943,
481.93279988216,482.016388965101,482.100112232659,482.180791948554,482.2645306604,
482.348166171767,482.431718615166,482.515208051016,482.59866200163,482.682098495476,
482.765535605232,482.848991400149,482.932535892879,483.01612497582,483.099848243377,
483.180527959274,483.26426667112,483.347902182487,483.431454625886,483.514944061737,
483.598398012351,483.681834506197,483.765271615952,483.84872741087,483.932271903599,
484.01586098654,484.099584254098,484.180263969994,484.26400268184,484.347638193207,
484.431190636606,484.514680072456,484.59813402307,484.681570516916,484.765007626672,
484.848463421589,484.932007914319,485.01559699726,485.099320264818,485.179999980714,
485.26373869256,485.347374203927,485.430926647326,485.514416083177,485.597870033791,
485.681306527637,485.764743637392,485.84819943231,485.93174392504,486.015333007981,
486.099056275539,486.179735991434,486.262390162833,486.344946957616,486.427425490976,
486.509839890327,486.592217795374,486.674583461396,486.695415017246),
 .UNSPECIFIED.);
#356=B_SPLINE_CURVE_WITH_KNOTS('',3,(#51799,#51800,#51801,#51802,#51803,
#51804,#51805,#51806,#51807,#51808),.UNSPECIFIED.,.F.,.F.,(4,3,3,4),(480.413366811053,
480.50167377437,480.589785986689,480.663675999053),.UNSPECIFIED.);
#357=B_SPLINE_CURVE_WITH_KNOTS('',3,(#51810,#51811,#51812,#51813,#51814,
#51815,#51816,#51817,#51818,#51819),.UNSPECIFIED.,.F.,.F.,(4,3,3,4),(480.412226582686,
480.491610546829,480.622176733975,480.663675999222),.UNSPECIFIED.);
#358=B_SPLINE_CURVE_WITH_KNOTS('',3,(#51820,#51821,#51822,#51823,#51824,
#51825,#51826,#51827,#51828,#51829,#51830,#51831,#51832,#51833,#51834,#51835,
#51836,#51837,#51838,#51839,#51840,#51841,#51842,#51843,#51844,#51845,#51846,
#51847,#51848,#51849,#51850,#51851,#51852,#51853,#51854,#51855,#51856,#51857,
#51858,#51859,#51860,#51861,#51862,#51863,#51864,#51865,#51866,#51867,#51868,
#51869,#51870,#51871,#51872,#51873,#51874,#51875,#51876,#51877,#51878,#51879,
#51880,#51881,#51882,#51883,#51884,#51885,#51886,#51887,#51888,#51889,#51890,
#51891,#51892,#51893,#51894,#51895,#51896,#51897,#51898,#51899,#51900,#51901,
#51902,#51903,#51904,#51905,#51906,#51907,#51908,#51909,#51910,#51911,#51912,
#51913,#51914,#51915,#51916,#51917,#51918,#51919,#51920,#51921,#51922,#51923,
#51924,#51925,#51926,#51927,#51928,#51929,#51930,#51931,#51932,#51933,#51934,
#51935,#51936,#51937,#51938,#51939,#51940,#51941,#51942,#51943,#51944,#51945,
#51946,#51947,#51948,#51949,#51950,#51951,#51952,#51953,#51954,#51955,#51956,
#51957,#51958,#51959,#51960,#51961,#51962,#51963,#51964,#51965,#51966,#51967,
#51968,#51969,#51970,#51971,#51972,#51973,#51974,#51975,#51976,#51977,#51978,
#51979,#51980,#51981,#51982,#51983,#51984,#51985,#51986,#51987,#51988,#51989,
#51990,#51991,#51992,#51993,#51994,#51995,#51996,#51997,#51998,#51999,#52000,
#52001,#52002,#52003,#52004,#52005,#52006,#52007,#52008,#52009,#52010,#52011,
#52012,#52013,#52014,#52015,#52016,#52017,#52018,#52019,#52020,#52021,#52022,
#52023,#52024,#52025,#52026,#52027,#52028,#52029,#52030,#52031,#52032,#52033,
#52034,#52035,#52036,#52037,#52038,#52039),.UNSPECIFIED.,.F.,.F.,(4,3,3,
3,3,3,3,3,3,3,3,3,3,3,3,3,3,3,3,3,3,3,3,3,3,3,3,3,3,3,3,3,3,3,3,3,3,3,3,
3,3,3,3,3,3,3,3,3,3,3,3,3,3,3,3,3,3,3,3,3,3,3,3,3,3,3,3,3,3,3,3,3,3,4),
(480.663675999399,480.746042833896,480.828333032913,480.911209723492,480.993419243018,
481.075620137376,481.15783143992,481.241210219328,481.323541599451,481.4074440785,
481.491346557549,481.575085269395,481.658720780763,481.742273224161,481.825762660012,
481.909216610626,481.992653104472,482.076090214228,482.159546009145,482.243090501875,
482.326679584816,482.410402852374,482.491082568269,482.574821280115,482.658456791482,
482.742009234881,482.825498670732,482.908952621346,482.992389115192,483.075826224948,
483.159282019866,483.242826512595,483.326415595536,483.410138863094,483.49081857899,
483.574557290836,483.658192802204,483.741745245602,483.825234681453,483.908688632067,
483.992125125913,484.075562235669,484.159018030587,484.242562523316,484.326151606257,
484.409874873815,484.49055458971,484.574293301556,484.657928812923,484.741481256322,
484.824970692172,484.908424642786,484.991861136632,485.075298246387,485.158754041305,
485.242298534034,485.325887616975,485.409610884532,485.49029060043,485.574029312276,
485.657664823644,485.741217267042,485.824706702892,485.908160653506,485.991597147352,
486.075034257108,486.158490052025,486.242034544755,486.325623627696,486.409346895254,
486.49002661115,486.579990511233,486.669730741741,486.696559540383),
 .UNSPECIFIED.);
#359=B_SPLINE_CURVE_WITH_KNOTS('',3,(#52045,#52046,#52047,#52048,#52049,
#52050,#52051,#52052,#52053,#52054,#52055,#52056,#52057,#52058,#52059,#52060,
#52061,#52062,#52063,#52064,#52065,#52066,#52067,#52068,#52069,#52070,#52071,
#52072,#52073,#52074,#52075,#52076,#52077,#52078,#52079,#52080,#52081,#52082,
#52083,#52084,#52085,#52086,#52087,#52088,#52089,#52090,#52091,#52092,#52093,
#52094,#52095,#52096,#52097,#52098,#52099,#52100,#52101,#52102,#52103,#52104,
#52105,#52106,#52107,#52108,#52109,#52110,#52111,#52112,#52113,#52114,#52115,
#52116,#52117,#52118,#52119,#52120,#52121,#52122,#52123,#52124,#52125,#52126,
#52127,#52128,#52129,#52130,#52131,#52132,#52133,#52134,#52135,#52136,#52137,
#52138,#52139,#52140,#52141,#52142,#52143,#52144,#52145,#52146,#52147,#52148,
#52149,#52150,#52151,#52152,#52153,#52154,#52155,#52156,#52157,#52158,#52159,
#52160,#52161,#52162,#52163,#52164,#52165,#52166,#52167,#52168,#52169,#52170,
#52171,#52172,#52173,#52174,#52175,#52176,#52177,#52178,#52179,#52180,#52181,
#52182,#52183,#52184,#52185,#52186,#52187,#52188,#52189,#52190,#52191,#52192,
#52193,#52194,#52195,#52196,#52197,#52198,#52199,#52200,#52201,#52202,#52203,
#52204,#52205,#52206,#52207,#52208,#52209,#52210,#52211,#52212,#52213,#52214,
#52215,#52216,#52217,#52218,#52219,#52220,#52221,#52222,#52223,#52224,#52225,
#52226,#52227,#52228,#52229,#52230,#52231,#52232,#52233,#52234,#52235,#52236,
#52237,#52238,#52239,#52240,#52241,#52242,#52243,#52244,#52245,#52246,#52247,
#52248,#52249,#52250,#52251,#52252,#52253,#52254,#52255,#52256,#52257,#52258,
#52259,#52260,#52261,#52262,#52263,#52264),.UNSPECIFIED.,.F.,.F.,(4,3,3,
3,3,3,3,3,3,3,3,3,3,3,3,3,3,3,3,3,3,3,3,3,3,3,3,3,3,3,3,3,3,3,3,3,3,3,3,
3,3,3,3,3,3,3,3,3,3,3,3,3,3,3,3,3,3,3,3,3,3,3,3,3,3,3,3,3,3,3,3,3,3,4),
(486.946861306398,487.057134081218,487.170531457197,487.179472002154,487.263210714,
487.346846225367,487.430398668766,487.513888104617,487.597342055231,487.680778549077,
487.764215658832,487.84767145375,487.93121594648,488.014805029421,488.098528296979,
488.179208012874,488.26294672472,488.346582236088,488.430134679486,488.513624115337,
488.597078065951,488.680514559797,488.763951669553,488.84740746447,488.9309519572,
489.014541040141,489.098264307699,489.178944023595,489.262682735441,489.346318246809,
489.429870690207,489.513360126058,489.596814076672,489.680250570518,489.763687680274,
489.847143475192,489.930687967921,490.014277050862,490.09800031842,490.178680034315,
490.262418746161,490.346054257528,490.429606700927,490.513096136778,490.596550087391,
490.679986581237,490.763423690993,490.846879485911,490.93042397864,491.014013061581,
491.097736329139,491.178416045035,491.262154756881,491.345790268248,491.429342711647,
491.512832147498,491.596286098112,491.679722591958,491.763159701714,491.846615496631,
491.930159989361,492.013749072302,492.09747233986,492.178152055755,492.26190282802,
492.345547767752,492.429091494216,492.512577828497,492.59602489082,492.679450771037,
492.762897683742,492.84635523381,492.929876217716,492.978381755897),
 .UNSPECIFIED.);
#360=B_SPLINE_CURVE_WITH_KNOTS('',3,(#52265,#52266,#52267,#52268,#52269,
#52270,#52271,#52272,#52273,#52274),.UNSPECIFIED.,.F.,.F.,(4,3,3,4),(486.695415017246,
486.777807467469,486.862334386933,486.946861306398),.UNSPECIFIED.);
#361=B_SPLINE_CURVE_WITH_KNOTS('',3,(#52276,#52277,#52278,#52279,#52280,
#52281,#52282,#52283,#52284,#52285),.UNSPECIFIED.,.F.,.F.,(4,3,3,4),(486.696559540383,
486.786015256491,486.875219215317,486.946861306221),.UNSPECIFIED.);
#362=B_SPLINE_CURVE_WITH_KNOTS('',3,(#52286,#52287,#52288,#52289,#52290,
#52291,#52292,#52293,#52294,#52295,#52296,#52297,#52298,#52299,#52300,#52301,
#52302,#52303,#52304,#52305,#52306,#52307,#52308,#52309,#52310,#52311,#52312,
#52313,#52314,#52315,#52316,#52317,#52318,#52319,#52320,#52321,#52322,#52323,
#52324,#52325,#52326,#52327,#52328,#52329,#52330,#52331,#52332,#52333,#52334,
#52335,#52336,#52337,#52338,#52339,#52340,#52341,#52342,#52343,#52344,#52345,
#52346,#52347,#52348,#52349,#52350,#52351,#52352,#52353,#52354,#52355,#52356,
#52357,#52358,#52359,#52360,#52361,#52362,#52363,#52364,#52365,#52366,#52367,
#52368,#52369,#52370,#52371,#52372,#52373,#52374,#52375,#52376,#52377,#52378,
#52379,#52380,#52381,#52382,#52383,#52384,#52385,#52386,#52387,#52388,#52389,
#52390,#52391,#52392,#52393,#52394,#52395,#52396,#52397,#52398,#52399,#52400,
#52401,#52402,#52403,#52404,#52405,#52406,#52407,#52408,#52409,#52410,#52411,
#52412,#52413,#52414,#52415,#52416,#52417,#52418,#52419,#52420,#52421,#52422,
#52423,#52424,#52425,#52426,#52427,#52428,#52429,#52430,#52431,#52432,#52433,
#52434,#52435,#52436,#52437,#52438,#52439,#52440,#52441,#52442,#52443,#52444,
#52445,#52446,#52447,#52448,#52449,#52450,#52451,#52452,#52453,#52454,#52455,
#52456,#52457,#52458,#52459,#52460,#52461,#52462,#52463,#52464,#52465,#52466,
#52467,#52468,#52469,#52470,#52471,#52472,#52473,#52474,#52475,#52476,#52477,
#52478,#52479,#52480,#52481,#52482,#52483,#52484,#52485,#52486,#52487,#52488,
#52489,#52490,#52491,#52492,#52493,#52494,#52495,#52496,#52497,#52498,#52499,
#52500,#52501,#52502,#52503,#52504,#52505),.UNSPECIFIED.,.F.,.F.,(4,3,3,
3,3,3,3,3,3,3,3,3,3,3,3,3,3,3,3,3,3,3,3,3,3,3,3,3,3,3,3,3,3,3,3,3,3,3,3,
3,3,3,3,3,3,3,3,3,3,3,3,3,3,3,3,3,3,3,3,3,3,3,3,3,3,3,3,3,3,3,3,3,3,4),
(486.946861306402,487.032861514281,487.118928332231,487.20507484832,487.291376054737,
487.377765824186,487.464312824274,487.48976262187,487.573501333716,487.657136845083,
487.740689288482,487.824178724332,487.907632674946,487.991069168792,488.074506278548,
488.157962073465,488.241506566195,488.325095649136,488.408818916693,488.48949863259,
488.573237344436,488.656872855803,488.740425299202,488.823914735053,488.907368685667,
488.990805179513,489.074242289269,489.157698084186,489.241242576916,489.324831659857,
489.408554927414,489.48923464331,489.572973355156,489.656608866524,489.740161309922,
489.823650745774,489.907104696387,489.990541190234,490.073978299989,490.157434094907,
490.240978587637,490.324567670578,490.408290938135,490.48897065403,490.572709365876,
490.656344877243,490.739897320642,490.823386756494,490.906840707107,490.990277200954,
491.073714310709,491.157170105627,491.240714598357,491.324303681298,491.408026948855,
491.488706664751,491.572445376597,491.656080887964,491.739633331363,491.823122767214,
491.906576717828,491.990013211674,492.07345032143,492.156906116347,492.240450609077,
492.324039692018,492.407762959576,492.488442675471,492.571272612664,492.654003819318,
492.736642260717,492.819226107672,492.901781529493,492.978723737855),
 .UNSPECIFIED.);
#363=B_SPLINE_CURVE_WITH_KNOTS('',3,(#52511,#52512,#52513,#52514,#52515,
#52516,#52517,#52518,#52519,#52520,#52521,#52522,#52523,#52524,#52525,#52526,
#52527,#52528,#52529,#52530,#52531,#52532,#52533,#52534,#52535,#52536,#52537,
#52538,#52539,#52540,#52541,#52542,#52543,#52544,#52545,#52546,#52547,#52548,
#52549,#52550,#52551,#52552,#52553,#52554,#52555,#52556,#52557,#52558,#52559,
#52560,#52561,#52562,#52563,#52564,#52565,#52566,#52567,#52568,#52569,#52570,
#52571,#52572,#52573,#52574,#52575,#52576,#52577,#52578,#52579,#52580,#52581,
#52582,#52583,#52584,#52585,#52586,#52587,#52588,#52589,#52590,#52591,#52592,
#52593,#52594,#52595,#52596,#52597,#52598,#52599,#52600,#52601,#52602,#52603,
#52604,#52605,#52606,#52607,#52608,#52609,#52610,#52611,#52612,#52613,#52614,
#52615,#52616,#52617,#52618,#52619,#52620,#52621,#52622,#52623,#52624,#52625,
#52626,#52627,#52628,#52629,#52630,#52631,#52632,#52633,#52634,#52635,#52636,
#52637,#52638,#52639,#52640,#52641,#52642,#52643,#52644,#52645,#52646,#52647,
#52648,#52649,#52650,#52651,#52652,#52653,#52654,#52655,#52656,#52657,#52658,
#52659,#52660,#52661,#52662,#52663,#52664,#52665,#52666,#52667,#52668,#52669,
#52670,#52671,#52672,#52673,#52674,#52675,#52676,#52677,#52678,#52679,#52680,
#52681,#52682,#52683,#52684,#52685,#52686,#52687,#52688,#52689,#52690,#52691,
#52692,#52693,#52694,#52695,#52696,#52697,#52698,#52699,#52700,#52701,#52702,
#52703,#52704,#52705,#52706,#52707,#52708,#52709,#52710,#52711,#52712,#52713,
#52714,#52715,#52716,#52717,#52718,#52719,#52720,#52721,#52722,#52723,#52724,
#52725,#52726,#52727,#52728,#52729,#52730),.UNSPECIFIED.,.F.,.F.,(4,3,3,
3,3,3,3,3,3,3,3,3,3,3,3,3,3,3,3,3,3,3,3,3,3,3,3,3,3,3,3,3,3,3,3,3,3,3,3,
3,3,3,3,3,3,3,3,3,3,3,3,3,3,3,3,3,3,3,3,3,3,3,3,3,3,3,3,3,3,3,3,3,3,4),
(493.230046613679,493.313107106364,493.396067801015,493.478949461932,493.561772776128,
493.644567209288,493.727349550249,493.810138438958,493.892952516834,493.975856520167,
494.058812040378,494.141887794238,494.177624077195,494.261362789041,494.344998300409,
494.428550743807,494.512040179658,494.595494130272,494.678930624118,494.762367733873,
494.845823528791,494.929368021521,495.012957104462,495.096680372019,495.177360087915,
495.261098799761,495.344734311128,495.428286754527,495.511776190378,495.595230140992,
495.678666634838,495.762103744594,495.845559539511,495.929104032241,496.012693115182,
496.09641638274,496.177096098636,496.260834810482,496.34447032185,496.428022765248,
496.511512201099,496.594966151713,496.678402645559,496.761839755315,496.845295550233,
496.928840042962,497.012429125903,497.096152393461,497.176832109356,497.260570821202,
497.344206332569,497.427758775968,497.511248211818,497.594702162432,497.678138656279,
497.761575766034,497.845031560952,497.928576053682,498.012165136622,498.09588840418,
498.176568120076,498.260306831922,498.343942343289,498.427494786688,498.510984222539,
498.594438173153,498.677874666999,498.761311776754,498.844767571672,498.928312064401,
499.011901147342,499.095624414899,499.176304130796,499.262642145922),
 .UNSPECIFIED.);
#364=B_SPLINE_CURVE_WITH_KNOTS('',3,(#52731,#52732,#52733,#52734,#52735,
#52736,#52737,#52738,#52739,#52740,#52741,#52742,#52743),.UNSPECIFIED.,
 .F.,.F.,(4,3,3,3,4),(492.978381755897,493.062004160814,493.145747059646,
493.177888066475,493.230046613577),.UNSPECIFIED.);
#365=B_SPLINE_CURVE_WITH_KNOTS('',3,(#52745,#52746,#52747,#52748,#52749,
#52750,#52751,#52752,#52753,#52754),.UNSPECIFIED.,.F.,.F.,(4,3,3,4),(492.978723737855,
493.061272089773,493.145659351677,493.230046613581),.UNSPECIFIED.);
#366=B_SPLINE_CURVE_WITH_KNOTS('',3,(#52755,#52756,#52757,#52758,#52759,
#52760,#52761,#52762,#52763,#52764,#52765,#52766,#52767,#52768,#52769,#52770,
#52771,#52772,#52773,#52774,#52775,#52776,#52777,#52778,#52779,#52780,#52781,
#52782,#52783,#52784,#52785,#52786,#52787,#52788,#52789,#52790,#52791,#52792,
#52793,#52794,#52795,#52796,#52797,#52798,#52799,#52800,#52801,#52802,#52803,
#52804,#52805,#52806,#52807,#52808,#52809,#52810,#52811,#52812,#52813,#52814,
#52815,#52816,#52817,#52818,#52819,#52820,#52821,#52822,#52823,#52824,#52825,
#52826,#52827,#52828,#52829,#52830,#52831,#52832,#52833,#52834,#52835,#52836,
#52837,#52838,#52839,#52840,#52841,#52842,#52843,#52844,#52845,#52846,#52847,
#52848,#52849,#52850,#52851,#52852,#52853,#52854,#52855,#52856,#52857,#52858,
#52859,#52860,#52861,#52862,#52863,#52864,#52865,#52866,#52867,#52868,#52869,
#52870,#52871,#52872,#52873,#52874,#52875,#52876,#52877,#52878,#52879,#52880,
#52881,#52882,#52883,#52884,#52885,#52886,#52887,#52888,#52889,#52890,#52891,
#52892,#52893,#52894,#52895,#52896,#52897,#52898,#52899,#52900,#52901,#52902,
#52903,#52904,#52905,#52906,#52907,#52908,#52909,#52910,#52911,#52912,#52913,
#52914,#52915,#52916,#52917,#52918,#52919,#52920,#52921,#52922,#52923,#52924,
#52925,#52926,#52927,#52928,#52929,#52930,#52931,#52932,#52933,#52934,#52935,
#52936,#52937,#52938,#52939,#52940,#52941,#52942,#52943,#52944,#52945,#52946,
#52947,#52948,#52949,#52950,#52951,#52952,#52953,#52954,#52955,#52956,#52957,
#52958,#52959,#52960,#52961,#52962,#52963,#52964,#52965,#52966,#52967,#52968,
#52969,#52970,#52971,#52972,#52973,#52974),.UNSPECIFIED.,.F.,.F.,(4,3,3,
3,3,3,3,3,3,3,3,3,3,3,3,3,3,3,3,3,3,3,3,3,3,3,3,3,3,3,3,3,3,3,3,3,3,3,3,
3,3,3,3,3,3,3,3,3,3,3,3,3,3,3,3,3,3,3,3,3,3,3,3,3,3,3,3,3,3,3,3,3,3,4),
(493.230046613707,493.336016526352,493.444154354458,493.488178686191,493.571917398037,
493.655552909404,493.739105352803,493.822594788654,493.906048739268,493.989485233114,
494.072922342869,494.156378137787,494.239922630517,494.323511713458,494.407234981015,
494.487914696911,494.571653408757,494.655288920124,494.738841363523,494.822330799374,
494.905784749988,494.989221243834,495.072658353589,495.156114148507,495.239658641237,
495.323247724178,495.406970991735,495.487650707631,495.571389419477,495.655024930844,
495.738577374243,495.822066810094,495.905520760707,495.988957254554,496.072394364309,
496.155850159227,496.239394651956,496.322983734897,496.406707002455,496.487386718351,
496.571125430197,496.654760941565,496.738313384963,496.821802820814,496.905256771428,
496.988693265274,497.07213037503,497.155586169947,497.239130662677,497.322719745618,
497.406443013176,497.487122729071,497.570861440917,497.654496952284,497.738049395683,
497.821538831534,497.904992782148,497.988429275994,498.07186638575,498.155322180667,
498.238866673397,498.322455756338,498.406179023896,498.486858739792,498.570611182974,
498.656980730276,498.740522870978,498.824007733033,498.907453436365,498.990878070489,
499.074319814382,499.157772531728,499.241278278077,499.261567561389),
 .UNSPECIFIED.);
#367=B_SPLINE_CURVE_WITH_KNOTS('',3,(#52980,#52981,#52982,#52983,#52984,
#52985,#52986,#52987,#52988,#52989,#52990,#52991,#52992,#52993,#52994,#52995,
#52996,#52997,#52998,#52999,#53000,#53001,#53002,#53003,#53004,#53005,#53006,
#53007,#53008,#53009,#53010,#53011,#53012,#53013,#53014,#53015,#53016,#53017,
#53018,#53019,#53020,#53021,#53022,#53023,#53024,#53025,#53026,#53027,#53028,
#53029,#53030,#53031,#53032,#53033,#53034,#53035,#53036,#53037,#53038,#53039,
#53040,#53041,#53042,#53043,#53044,#53045,#53046,#53047,#53048,#53049,#53050,
#53051,#53052,#53053,#53054,#53055,#53056,#53057,#53058,#53059,#53060,#53061,
#53062,#53063,#53064,#53065,#53066,#53067,#53068,#53069,#53070,#53071,#53072,
#53073,#53074,#53075,#53076,#53077,#53078,#53079,#53080,#53081,#53082,#53083,
#53084,#53085,#53086,#53087,#53088,#53089,#53090,#53091,#53092,#53093,#53094,
#53095,#53096,#53097,#53098,#53099,#53100,#53101,#53102,#53103,#53104,#53105,
#53106,#53107,#53108,#53109,#53110,#53111,#53112,#53113,#53114,#53115,#53116,
#53117,#53118,#53119,#53120,#53121,#53122,#53123,#53124,#53125,#53126,#53127,
#53128,#53129,#53130,#53131,#53132,#53133,#53134,#53135,#53136,#53137,#53138,
#53139,#53140,#53141,#53142,#53143,#53144,#53145,#53146,#53147,#53148,#53149,
#53150,#53151,#53152,#53153,#53154,#53155,#53156,#53157,#53158,#53159,#53160,
#53161,#53162,#53163,#53164,#53165,#53166,#53167,#53168,#53169,#53170,#53171,
#53172,#53173,#53174,#53175,#53176,#53177,#53178,#53179,#53180,#53181,#53182,
#53183,#53184,#53185,#53186,#53187,#53188,#53189,#53190,#53191,#53192,#53193,
#53194,#53195,#53196,#53197,#53198,#53199),.UNSPECIFIED.,.F.,.F.,(4,3,3,
3,3,3,3,3,3,3,3,3,3,3,3,3,3,3,3,3,3,3,3,3,3,3,3,3,3,3,3,3,3,3,3,3,3,3,3,
3,3,3,3,3,3,3,3,3,3,3,3,3,3,3,3,3,3,3,3,3,3,3,3,3,3,3,3,3,3,3,3,3,3,4),
(499.513231920757,499.596670184171,499.680096678619,499.763529406103,499.846986368907,
499.930539923303,500.014142748441,500.097885724517,500.176040141516,500.259778853362,
500.343414364729,500.426966808128,500.510456243979,500.593910194592,500.677346688439,
500.760783798194,500.844239593111,500.927784085841,501.011373168782,501.09509643634,
501.175776152236,501.259514864082,501.343150375449,501.426702818848,501.510192254698,
501.593646205312,501.677082699158,501.760519808914,501.843975603832,501.927520096562,
502.011109179503,502.09483244706,502.175512162956,502.259250874802,502.342886386169,
502.426438829568,502.509928265419,502.593382216033,502.676818709879,502.760255819634,
502.843711614552,502.927256107281,503.010845190222,503.09456845778,503.175248173676,
503.258986885522,503.342622396889,503.426174840288,503.509664276139,503.593118226753,
503.676554720599,503.759991830355,503.843447625273,503.926992118002,504.010581200943,
504.094304468501,504.174984184397,504.258722896243,504.342358407611,504.42591085101,
504.509400286861,504.592854237474,504.676290731321,504.759727841076,504.843183635994,
504.926728128724,505.010317211665,505.094040479223,505.174720195117,505.259243841905,
505.343623334706,505.427919448869,505.512133263776,505.545701907803),
 .UNSPECIFIED.);
#368=B_SPLINE_CURVE_WITH_KNOTS('',3,(#53200,#53201,#53202,#53203,#53204,
#53205,#53206,#53207,#53208,#53209),.UNSPECIFIED.,.F.,.F.,(4,3,3,4),(499.262642145922,
499.360326014176,499.457183902584,499.513231920567),.UNSPECIFIED.);
#369=B_SPLINE_CURVE_WITH_KNOTS('',3,(#53211,#53212,#53213,#53214,#53215,
#53216,#53217,#53218,#53219,#53220,#53221,#53222,#53223),.UNSPECIFIED.,
 .F.,.F.,(4,3,3,3,4),(499.261567561389,499.345171745714,499.428903472395,
499.486594750512,499.513231920761),.UNSPECIFIED.);
#370=B_SPLINE_CURVE_WITH_KNOTS('',3,(#53224,#53225,#53226,#53227,#53228,
#53229,#53230,#53231,#53232,#53233,#53234,#53235,#53236,#53237,#53238,#53239,
#53240,#53241,#53242,#53243,#53244,#53245,#53246,#53247,#53248,#53249,#53250,
#53251,#53252,#53253,#53254,#53255,#53256,#53257,#53258,#53259,#53260,#53261,
#53262,#53263,#53264,#53265,#53266,#53267,#53268,#53269,#53270,#53271,#53272,
#53273,#53274,#53275,#53276,#53277,#53278,#53279,#53280,#53281,#53282,#53283,
#53284,#53285,#53286,#53287,#53288,#53289,#53290,#53291,#53292,#53293,#53294,
#53295,#53296,#53297,#53298,#53299,#53300,#53301,#53302,#53303,#53304,#53305,
#53306,#53307,#53308,#53309,#53310,#53311,#53312,#53313,#53314,#53315,#53316,
#53317,#53318,#53319,#53320,#53321,#53322,#53323,#53324,#53325,#53326,#53327,
#53328,#53329,#53330,#53331,#53332,#53333,#53334,#53335,#53336,#53337,#53338,
#53339,#53340,#53341,#53342,#53343,#53344,#53345,#53346,#53347,#53348,#53349,
#53350,#53351,#53352,#53353,#53354,#53355,#53356,#53357,#53358,#53359,#53360,
#53361,#53362,#53363,#53364,#53365,#53366,#53367,#53368,#53369,#53370,#53371,
#53372,#53373,#53374,#53375,#53376,#53377,#53378,#53379,#53380,#53381,#53382,
#53383,#53384,#53385,#53386,#53387,#53388,#53389,#53390,#53391,#53392,#53393,
#53394,#53395,#53396,#53397,#53398,#53399,#53400,#53401,#53402,#53403,#53404,
#53405,#53406,#53407,#53408,#53409,#53410,#53411,#53412,#53413,#53414,#53415,
#53416,#53417,#53418,#53419,#53420,#53421,#53422,#53423,#53424,#53425,#53426,
#53427,#53428,#53429,#53430,#53431,#53432,#53433,#53434,#53435,#53436,#53437,
#53438,#53439,#53440,#53441,#53442,#53443),.UNSPECIFIED.,.F.,.F.,(4,3,3,
3,3,3,3,3,3,3,3,3,3,3,3,3,3,3,3,3,3,3,3,3,3,3,3,3,3,3,3,3,3,3,3,3,3,3,3,
3,3,3,3,3,3,3,3,3,3,3,3,3,3,3,3,3,3,3,3,3,3,3,3,3,3,3,3,3,3,3,3,3,3,4),
(499.513231920881,499.596595150741,499.679856225129,499.763035652673,499.84615386694,
499.92923928284,500.012309553756,500.095383088349,500.178478293937,500.261662605286,
500.344894830732,500.428254065379,500.486330761232,500.570069473078,500.653704984445,
500.737257427844,500.820746863695,500.904200814309,500.987637308155,501.07107441791,
501.154530212828,501.238074705558,501.321663788499,501.405387056056,501.486066771952,
501.569805483798,501.653440995165,501.736993438563,501.820482874414,501.903936825028,
501.987373318874,502.07081042863,502.154266223547,502.237810716277,502.321399799218,
502.405123066775,502.485802782672,502.569541494518,502.653177005886,502.736729449284,
502.820218885135,502.903672835749,502.987109329595,503.070546439351,503.154002234268,
503.237546726998,503.321135809939,503.404859077496,503.485538793392,503.569277505238,
503.652913016605,503.736465460004,503.819954895854,503.903408846468,503.986845340314,
504.07028245007,504.153738244987,504.237282737717,504.320871820658,504.404595088216,
504.485274804112,504.569013515958,504.652649027325,504.736201470724,504.819690906575,
504.903144857189,504.986581351035,505.070018460791,505.153474255708,505.237018748438,
505.320607831379,505.404331098937,505.485010814832,505.545703572404),
 .UNSPECIFIED.);
#371=B_SPLINE_CURVE_WITH_KNOTS('',3,(#53449,#53450,#53451,#53452,#53453,
#53454,#53455,#53456,#53457,#53458,#53459,#53460,#53461,#53462,#53463,#53464,
#53465,#53466,#53467,#53468,#53469,#53470,#53471,#53472,#53473,#53474,#53475,
#53476,#53477,#53478,#53479,#53480,#53481,#53482,#53483,#53484,#53485,#53486,
#53487,#53488,#53489,#53490,#53491,#53492,#53493,#53494,#53495,#53496,#53497,
#53498,#53499,#53500,#53501,#53502,#53503,#53504,#53505,#53506,#53507,#53508,
#53509,#53510,#53511,#53512,#53513,#53514,#53515,#53516,#53517,#53518,#53519,
#53520,#53521,#53522,#53523,#53524,#53525,#53526,#53527,#53528,#53529,#53530,
#53531,#53532,#53533,#53534,#53535,#53536,#53537,#53538,#53539,#53540,#53541,
#53542,#53543,#53544,#53545,#53546,#53547,#53548,#53549,#53550,#53551,#53552,
#53553,#53554,#53555,#53556,#53557,#53558,#53559,#53560,#53561,#53562,#53563,
#53564,#53565,#53566,#53567,#53568,#53569,#53570,#53571,#53572,#53573,#53574,
#53575,#53576,#53577,#53578,#53579,#53580,#53581,#53582,#53583,#53584,#53585,
#53586,#53587,#53588,#53589,#53590,#53591,#53592,#53593,#53594,#53595,#53596,
#53597,#53598,#53599,#53600,#53601,#53602,#53603,#53604,#53605,#53606,#53607,
#53608,#53609,#53610,#53611,#53612,#53613,#53614,#53615,#53616,#53617,#53618,
#53619,#53620,#53621,#53622,#53623,#53624,#53625,#53626,#53627,#53628,#53629,
#53630,#53631,#53632,#53633,#53634,#53635,#53636,#53637,#53638,#53639,#53640,
#53641,#53642,#53643,#53644,#53645,#53646,#53647,#53648,#53649,#53650,#53651,
#53652,#53653,#53654,#53655,#53656,#53657,#53658,#53659,#53660,#53661,#53662,
#53663,#53664,#53665),.UNSPECIFIED.,.F.,.F.,(4,3,3,3,3,3,3,3,3,3,3,3,3,
3,3,3,3,3,3,3,3,3,3,3,3,3,3,3,3,3,3,3,3,3,3,3,3,3,3,3,3,3,3,3,3,3,3,3,3,
3,3,3,3,3,3,3,3,3,3,3,3,3,3,3,3,3,3,3,3,3,3,3,4),(505.79641722813,505.890926972556,
505.985009282388,506.079732744112,506.174456205837,506.258194917683,506.34183042905,
506.425382872449,506.5088723083,506.592326258913,506.675762752759,506.759199862515,
506.842655657432,506.926200150162,507.009789233103,507.09351250066,507.174192216557,
507.257930928403,507.34156643977,507.425118883169,507.50860831902,507.592062269633,
507.67549876348,507.758935873235,507.842391668153,507.925936160882,508.009525243823,
508.093248511381,508.173928227277,508.257666939123,508.34130245049,508.424854893889,
508.50834432974,508.591798280354,508.6752347742,508.758671883955,508.842127678873,
508.925672171603,509.009261254544,509.092984522101,509.173664237997,509.257402949843,
509.34103846121,509.424590904609,509.50808034046,509.591534291074,509.67497078492,
509.758407894675,509.841863689593,509.925408182323,510.008997265264,510.092720532821,
510.173400248717,510.257138960563,510.34077447193,510.424326915329,510.50781635118,
510.591270301794,510.67470679564,510.758143905396,510.841599700313,510.925144193043,
511.008733275984,511.092456543541,511.173136259437,511.255848589194,511.338466366091,
511.421008642217,511.503494402176,511.585953289741,511.668393655483,511.750865095778,
511.827765835364),.UNSPECIFIED.);
#372=B_SPLINE_CURVE_WITH_KNOTS('',3,(#53666,#53667,#53668,#53669,#53670,
#53671,#53672,#53673,#53674,#53675),.UNSPECIFIED.,.F.,.F.,(4,3,3,4),(505.545701907803,
505.629843863293,505.713969544551,505.796417227936),.UNSPECIFIED.);
#373=B_SPLINE_CURVE_WITH_KNOTS('',3,(#53677,#53678,#53679,#53680,#53681,
#53682,#53683,#53684,#53685,#53686),.UNSPECIFIED.,.F.,.F.,(4,3,3,4),(505.545703572404,
505.646104108299,505.745411802745,505.796417227777),.UNSPECIFIED.);
#374=B_SPLINE_CURVE_WITH_KNOTS('',3,(#53687,#53688,#53689,#53690,#53691,
#53692,#53693,#53694,#53695,#53696,#53697,#53698,#53699,#53700,#53701,#53702,
#53703,#53704,#53705,#53706,#53707,#53708,#53709,#53710,#53711,#53712,#53713,
#53714,#53715,#53716,#53717,#53718,#53719,#53720,#53721,#53722,#53723,#53724,
#53725,#53726,#53727,#53728,#53729,#53730,#53731,#53732,#53733,#53734,#53735,
#53736,#53737,#53738,#53739,#53740,#53741,#53742,#53743,#53744,#53745,#53746,
#53747,#53748,#53749,#53750,#53751,#53752,#53753,#53754,#53755,#53756,#53757,
#53758,#53759,#53760,#53761,#53762,#53763,#53764,#53765,#53766,#53767,#53768,
#53769,#53770,#53771,#53772,#53773,#53774,#53775,#53776,#53777,#53778,#53779,
#53780,#53781,#53782,#53783,#53784,#53785,#53786,#53787,#53788,#53789,#53790,
#53791,#53792,#53793,#53794,#53795,#53796,#53797,#53798,#53799,#53800,#53801,
#53802,#53803,#53804,#53805,#53806,#53807,#53808,#53809,#53810,#53811,#53812,
#53813,#53814,#53815,#53816,#53817,#53818,#53819,#53820,#53821,#53822,#53823,
#53824,#53825,#53826,#53827,#53828,#53829,#53830,#53831,#53832,#53833,#53834,
#53835,#53836,#53837,#53838,#53839,#53840,#53841,#53842,#53843,#53844,#53845,
#53846,#53847,#53848,#53849,#53850,#53851,#53852,#53853,#53854,#53855,#53856,
#53857,#53858,#53859,#53860,#53861,#53862,#53863,#53864,#53865,#53866,#53867,
#53868,#53869,#53870,#53871,#53872,#53873,#53874,#53875,#53876,#53877,#53878,
#53879,#53880,#53881,#53882,#53883,#53884,#53885,#53886,#53887,#53888,#53889,
#53890,#53891,#53892,#53893,#53894,#53895,#53896,#53897,#53898,#53899,#53900,
#53901,#53902,#53903,#53904,#53905,#53906),.UNSPECIFIED.,.F.,.F.,(4,3,3,
3,3,3,3,3,3,3,3,3,3,3,3,3,3,3,3,3,3,3,3,3,3,3,3,3,3,3,3,3,3,3,3,3,3,3,3,
3,3,3,3,3,3,3,3,3,3,3,3,3,3,3,3,3,3,3,3,3,3,3,3,3,3,3,3,3,3,3,3,3,3,4),
(505.79641722794,505.882458427642,505.965539089651,506.048616043483,506.131707649494,
506.21483227441,506.298053982271,506.381333616868,506.464733332468,506.484746825553,
506.568485537399,506.652121048766,506.735673492165,506.819162928016,506.90261687863,
506.986053372476,507.069490482231,507.152946277149,507.236490769879,507.32007985282,
507.403803120377,507.484482836273,507.568221548119,507.651857059486,507.735409502885,
507.818898938736,507.90235288935,507.985789383196,508.069226492952,508.152682287869,
508.236226780599,508.31981586354,508.403539131097,508.484218846993,508.567957558839,
508.651593070206,508.735145513605,508.818634949455,508.902088900069,508.985525393915,
509.06896250367,509.152418298588,509.235962791318,509.319551874259,509.403275141816,
509.483954857713,509.567693569559,509.651329080926,509.734881524325,509.818370960176,
509.90182491079,509.985261404636,510.068698514392,510.152154309309,510.235698802039,
510.31928788498,510.403011152537,510.483690868433,510.567429580279,510.651065091646,
510.734617535045,510.818106970896,510.901560921509,510.984997415356,511.068434525111,
511.151890320029,511.235434812759,511.3190238957,511.402747163258,511.483426879153,
511.569819896032,511.654761847421,511.741880397046,511.82899894667),
 .UNSPECIFIED.);
#375=B_SPLINE_CURVE_WITH_KNOTS('',3,(#53912,#53913,#53914,#53915,#53916,
#53917,#53918,#53919,#53920,#53921,#53922,#53923,#53924,#53925,#53926,#53927,
#53928,#53929,#53930,#53931,#53932,#53933,#53934,#53935,#53936,#53937,#53938,
#53939,#53940,#53941,#53942,#53943,#53944,#53945,#53946,#53947,#53948,#53949,
#53950,#53951,#53952,#53953,#53954,#53955,#53956,#53957,#53958,#53959,#53960,
#53961,#53962,#53963,#53964,#53965,#53966,#53967,#53968,#53969,#53970,#53971,
#53972,#53973,#53974,#53975,#53976,#53977,#53978,#53979,#53980,#53981,#53982,
#53983,#53984,#53985,#53986,#53987,#53988,#53989,#53990,#53991,#53992,#53993,
#53994,#53995,#53996,#53997,#53998,#53999,#54000,#54001,#54002,#54003,#54004,
#54005,#54006,#54007,#54008,#54009,#54010,#54011,#54012,#54013,#54014,#54015,
#54016,#54017,#54018,#54019,#54020,#54021,#54022,#54023,#54024,#54025,#54026,
#54027,#54028,#54029,#54030,#54031,#54032,#54033,#54034,#54035,#54036,#54037,
#54038,#54039,#54040,#54041,#54042,#54043,#54044,#54045,#54046,#54047,#54048,
#54049,#54050,#54051,#54052,#54053,#54054,#54055,#54056,#54057,#54058,#54059,
#54060,#54061,#54062,#54063,#54064,#54065,#54066,#54067,#54068,#54069,#54070,
#54071,#54072,#54073,#54074,#54075,#54076,#54077,#54078,#54079,#54080,#54081,
#54082,#54083,#54084,#54085,#54086,#54087,#54088,#54089,#54090,#54091,#54092,
#54093,#54094,#54095,#54096,#54097,#54098,#54099,#54100,#54101,#54102,#54103,
#54104,#54105,#54106,#54107,#54108,#54109,#54110,#54111,#54112,#54113,#54114,
#54115,#54116,#54117,#54118,#54119,#54120,#54121,#54122,#54123,#54124,#54125,
#54126,#54127,#54128,#54129,#54130,#54131),.UNSPECIFIED.,.F.,.F.,(4,3,3,
3,3,3,3,3,3,3,3,3,3,3,3,3,3,3,3,3,3,3,3,3,3,3,3,3,3,3,3,3,3,3,3,3,3,3,3,
3,3,3,3,3,3,3,3,3,3,3,3,3,3,3,3,3,3,3,3,3,3,3,3,3,3,3,3,3,3,3,3,3,3,4),
(512.079602535116,512.172872270158,512.256610982004,512.340246493371,512.42379893677,
512.507288372621,512.590742323234,512.67417881708,512.757615926836,512.841071721753,
512.924616214483,513.008205297423,513.091928564981,513.172608280878,513.256346992724,
513.339982504091,513.42353494749,513.507024383341,513.590478333954,513.673914827801,
513.757351937556,513.840807732474,513.924352225203,514.007941308144,514.091664575702,
514.172344291598,514.256083003444,514.339718514812,514.42327095821,514.506760394061,
514.590214344675,514.673650838521,514.757087948277,514.840543743195,514.924088235924,
515.007677318865,515.091400586423,515.172080302318,515.255819014164,515.339454525531,
515.42300696893,515.506496404781,515.589950355395,515.673386849241,515.756823958996,
515.840279753914,515.923824246643,516.007413329584,516.091136597142,516.171816313038,
516.255555024884,516.339190536252,516.42274297965,516.506232415501,516.589686366115,
516.673122859961,516.756559969716,516.840015764634,516.923560257364,517.007149340305,
517.090872607862,517.171552323758,517.255294468566,517.338932623139,517.422486923337,
517.508602676535,517.592052950222,517.675485219268,517.758917555356,517.842368026146,
517.925892631405,518.0094618763,518.093130892287,518.111412948922),
 .UNSPECIFIED.);
#376=B_SPLINE_CURVE_WITH_KNOTS('',3,(#54132,#54133,#54134,#54135,#54136,
#54137,#54138,#54139,#54140,#54141),.UNSPECIFIED.,.F.,.F.,(4,3,3,4),(511.827765835364,
511.910313912069,511.994958223525,512.079602534982),.UNSPECIFIED.);
#377=B_SPLINE_CURVE_WITH_KNOTS('',3,(#54143,#54144,#54145,#54146,#54147,
#54148,#54149,#54150,#54151,#54152),.UNSPECIFIED.,.F.,.F.,(4,3,3,4),(511.82899894667,
511.913687987766,511.99833837829,512.07960253512),.UNSPECIFIED.);
#378=B_SPLINE_CURVE_WITH_KNOTS('',3,(#54153,#54154,#54155,#54156,#54157,
#54158,#54159,#54160,#54161,#54162,#54163,#54164,#54165,#54166,#54167,#54168,
#54169,#54170,#54171,#54172,#54173,#54174,#54175,#54176,#54177,#54178,#54179,
#54180,#54181,#54182,#54183,#54184,#54185,#54186,#54187,#54188,#54189,#54190,
#54191,#54192,#54193,#54194,#54195,#54196,#54197,#54198,#54199,#54200,#54201,
#54202,#54203,#54204,#54205,#54206,#54207,#54208,#54209,#54210,#54211,#54212,
#54213,#54214,#54215,#54216,#54217,#54218,#54219,#54220,#54221,#54222,#54223,
#54224,#54225,#54226,#54227,#54228,#54229,#54230,#54231,#54232,#54233,#54234,
#54235,#54236,#54237,#54238,#54239,#54240,#54241,#54242,#54243,#54244,#54245,
#54246,#54247,#54248,#54249,#54250,#54251,#54252,#54253,#54254,#54255,#54256,
#54257,#54258,#54259,#54260,#54261,#54262,#54263,#54264,#54265,#54266,#54267,
#54268,#54269,#54270,#54271,#54272,#54273,#54274,#54275,#54276,#54277,#54278,
#54279,#54280,#54281,#54282,#54283,#54284,#54285,#54286,#54287,#54288,#54289,
#54290,#54291,#54292,#54293,#54294,#54295,#54296,#54297,#54298,#54299,#54300,
#54301,#54302,#54303,#54304,#54305,#54306,#54307,#54308,#54309,#54310,#54311,
#54312,#54313,#54314,#54315,#54316,#54317,#54318,#54319,#54320,#54321,#54322,
#54323,#54324,#54325,#54326,#54327,#54328,#54329,#54330,#54331,#54332,#54333,
#54334,#54335,#54336,#54337,#54338,#54339,#54340,#54341,#54342,#54343,#54344,
#54345,#54346,#54347,#54348,#54349,#54350,#54351,#54352,#54353,#54354,#54355,
#54356,#54357,#54358,#54359,#54360,#54361,#54362,#54363,#54364,#54365,#54366,
#54367,#54368,#54369,#54370,#54371,#54372),.UNSPECIFIED.,.F.,.F.,(4,3,3,
3,3,3,3,3,3,3,3,3,3,3,3,3,3,3,3,3,3,3,3,3,3,3,3,3,3,3,3,3,3,3,3,3,3,3,3,
3,3,3,3,3,3,3,3,3,3,3,3,3,3,3,3,3,3,3,3,3,3,3,3,3,3,3,3,3,3,3,3,3,3,4),
(512.079602535298,512.171477821645,512.263833046544,512.356436043018,512.449370007146,
512.483162889873,512.566901601719,512.650537113087,512.734089556487,512.817578992338,
512.901032942952,512.984469436799,513.067906546555,513.151362341473,513.234906834204,
513.318495917145,513.402219184703,513.482898900594,513.56663761244,513.650273123808,
513.733825567206,513.817315003057,513.900768953671,513.984205447517,514.067642557272,
514.15109835219,514.23464284492,514.318231927861,514.401955195418,514.482634911314,
514.56637362316,514.650009134527,514.733561577925,514.817051013776,514.900504964389,
514.983941458236,515.067378567991,515.150834362908,515.234378855638,515.317967938579,
515.401691206136,515.482370922034,515.56610963388,515.649745145248,515.733297588646,
515.816787024497,515.900240975111,515.983677468958,516.067114578713,516.150570373631,
516.234114866361,516.317703949302,516.40142721686,516.482106932754,516.5658456446,
516.649481155967,516.733033599366,516.816523035217,516.89997698583,516.983413479677,
517.066850589432,517.15030638435,517.233850877079,517.31743996002,517.401163227578,
517.481842943474,517.564418019187,517.646898427861,517.729303315999,517.811651759644,
517.893971056624,517.976272247947,518.058596719203,518.110972534525),
 .UNSPECIFIED.);
#379=B_SPLINE_CURVE_WITH_KNOTS('',3,(#54378,#54379,#54380,#54381,#54382,
#54383,#54384,#54385,#54386,#54387,#54388,#54389,#54390,#54391,#54392,#54393,
#54394,#54395,#54396,#54397,#54398,#54399,#54400,#54401,#54402,#54403,#54404,
#54405,#54406,#54407,#54408,#54409,#54410,#54411,#54412,#54413,#54414,#54415,
#54416,#54417,#54418,#54419,#54420,#54421,#54422,#54423,#54424,#54425,#54426,
#54427,#54428,#54429,#54430,#54431,#54432,#54433,#54434,#54435,#54436,#54437,
#54438,#54439,#54440,#54441,#54442,#54443,#54444,#54445,#54446,#54447,#54448,
#54449,#54450,#54451,#54452,#54453,#54454,#54455,#54456,#54457,#54458,#54459,
#54460,#54461,#54462,#54463,#54464,#54465,#54466,#54467,#54468,#54469,#54470,
#54471,#54472,#54473,#54474,#54475,#54476,#54477,#54478,#54479,#54480,#54481,
#54482,#54483,#54484,#54485,#54486,#54487,#54488,#54489,#54490,#54491,#54492,
#54493,#54494,#54495,#54496,#54497,#54498,#54499,#54500,#54501,#54502,#54503,
#54504,#54505,#54506,#54507,#54508,#54509,#54510,#54511,#54512,#54513,#54514,
#54515,#54516,#54517,#54518,#54519,#54520,#54521,#54522,#54523,#54524,#54525,
#54526,#54527,#54528,#54529,#54530,#54531,#54532,#54533,#54534,#54535,#54536,
#54537,#54538,#54539,#54540,#54541,#54542,#54543,#54544,#54545,#54546,#54547,
#54548,#54549,#54550,#54551,#54552,#54553,#54554,#54555,#54556,#54557,#54558,
#54559,#54560,#54561,#54562,#54563,#54564,#54565,#54566,#54567,#54568,#54569,
#54570,#54571,#54572,#54573,#54574,#54575,#54576,#54577,#54578,#54579,#54580,
#54581,#54582,#54583,#54584,#54585,#54586,#54587,#54588,#54589,#54590,#54591,
#54592,#54593,#54594,#54595,#54596,#54597),.UNSPECIFIED.,.F.,.F.,(4,3,3,
3,3,3,3,3,3,3,3,3,3,3,3,3,3,3,3,3,3,3,3,3,3,3,3,3,3,3,3,3,3,3,3,3,3,3,3,
3,3,3,3,3,3,3,3,3,3,3,3,3,3,3,3,3,3,3,3,3,3,3,3,3,3,3,3,3,3,3,3,3,3,4),
(518.362787842419,518.445154854009,518.52745048132,518.609700442417,518.691927292045,
518.774150056304,518.856387755764,518.938708455605,519.021072182249,519.103563042683,
519.171024345199,519.254763057045,519.338398568412,519.421951011811,519.505440447662,
519.588894398276,519.672330892122,519.755768001877,519.839223796794,519.922768289524,
520.006357372465,520.090080640023,520.170760355919,520.254499067765,520.338134579132,
520.42168702253,520.505176458381,520.588630408995,520.672066902841,520.755504012596,
520.838959807513,520.922504300243,521.006093383184,521.089816650741,521.170496366639,
521.254235078485,521.337870589853,521.421423033251,521.504912469102,521.588366419715,
521.671802913562,521.755240023317,521.838695818235,521.922240310965,522.005829393906,
522.089552661463,522.170232377359,522.253971089205,522.337606600572,522.421159043971,
522.504648479823,522.588102430436,522.671538924282,522.754976034038,522.838431828956,
522.921976321685,523.005565404627,523.089288672184,523.169968388079,523.253707099925,
523.337342611292,523.42089505469,523.504384490541,523.587838441154,523.671274935001,
523.754712044756,523.838167839673,523.921712332403,524.005301415344,524.089024682901,
524.169704398799,524.25875441157,524.347593650043,524.395667901685),
 .UNSPECIFIED.);
#380=B_SPLINE_CURVE_WITH_KNOTS('',3,(#54598,#54599,#54600,#54601,#54602,
#54603,#54604,#54605,#54606,#54607),.UNSPECIFIED.,.F.,.F.,(4,3,3,4),(518.111412948922,
518.171288334478,518.294232689854,518.362787842295),.UNSPECIFIED.);
#381=B_SPLINE_CURVE_WITH_KNOTS('',3,(#54609,#54610,#54611,#54612,#54613,
#54614,#54615,#54616,#54617,#54618),.UNSPECIFIED.,.F.,.F.,(4,3,3,4),(518.110972534525,
518.193367758242,518.278077800204,518.362787842165),.UNSPECIFIED.);
#382=B_SPLINE_CURVE_WITH_KNOTS('',3,(#54619,#54620,#54621,#54622,#54623,
#54624,#54625,#54626,#54627,#54628,#54629,#54630,#54631,#54632,#54633,#54634,
#54635,#54636,#54637,#54638,#54639,#54640,#54641,#54642,#54643,#54644,#54645,
#54646,#54647,#54648,#54649,#54650,#54651,#54652,#54653,#54654,#54655,#54656,
#54657,#54658,#54659,#54660,#54661,#54662,#54663,#54664,#54665,#54666,#54667,
#54668,#54669,#54670,#54671,#54672,#54673,#54674,#54675,#54676,#54677,#54678,
#54679,#54680,#54681,#54682,#54683,#54684,#54685,#54686,#54687,#54688,#54689,
#54690,#54691,#54692,#54693,#54694,#54695,#54696,#54697,#54698,#54699,#54700,
#54701,#54702,#54703,#54704,#54705,#54706,#54707,#54708,#54709,#54710,#54711,
#54712,#54713,#54714,#54715,#54716,#54717,#54718,#54719,#54720,#54721,#54722,
#54723,#54724,#54725,#54726,#54727,#54728,#54729,#54730,#54731,#54732,#54733,
#54734,#54735,#54736,#54737,#54738,#54739,#54740,#54741,#54742,#54743,#54744,
#54745,#54746,#54747,#54748,#54749,#54750,#54751,#54752,#54753,#54754,#54755,
#54756,#54757,#54758,#54759,#54760,#54761,#54762,#54763,#54764,#54765,#54766,
#54767,#54768,#54769,#54770,#54771,#54772,#54773,#54774,#54775,#54776,#54777,
#54778,#54779,#54780,#54781,#54782,#54783,#54784,#54785,#54786,#54787,#54788,
#54789,#54790,#54791,#54792,#54793,#54794,#54795,#54796,#54797,#54798,#54799,
#54800,#54801,#54802,#54803,#54804,#54805,#54806,#54807,#54808,#54809,#54810,
#54811,#54812,#54813,#54814,#54815,#54816,#54817,#54818,#54819,#54820,#54821,
#54822,#54823,#54824,#54825,#54826,#54827,#54828,#54829,#54830,#54831,#54832,
#54833,#54834,#54835),.UNSPECIFIED.,.F.,.F.,(4,3,3,3,3,3,3,3,3,3,3,3,3,
3,3,3,3,3,3,3,3,3,3,3,3,3,3,3,3,3,3,3,3,3,3,3,3,3,3,3,3,3,3,3,3,3,3,3,3,
3,3,3,3,3,3,3,3,3,3,3,3,3,3,3,3,3,3,3,3,3,3,3,4),(518.362787842299,518.481578954194,
518.56531766604,518.648953177408,518.732505620807,518.815995056658,518.899449007272,
518.982885501119,519.066322610875,519.149778405793,519.233322898523,519.316911981464,
519.400635249022,519.481314964914,519.56505367676,519.648689188128,519.732241631526,
519.815731067378,519.899185017991,519.982621511838,520.066058621593,520.149514416511,
520.233058909241,520.316647992182,520.40037125974,520.481050975635,520.564789687481,
520.648425198848,520.731977642247,520.815467078098,520.898921028711,520.982357522557,
521.065794632313,521.14925042723,521.23279491996,521.3163840029,521.400107270458,
521.480786986355,521.564525698201,521.648161209569,521.731713652967,521.815203088818,
521.898657039432,521.982093533278,522.065530643034,522.148986437952,522.232530930681,
522.316120013622,522.39984328118,522.480522997075,522.564261708921,522.647897220288,
522.731449663687,522.814939099538,522.898393050152,522.981829543998,523.065266653753,
523.148722448671,523.232266941401,523.315856024342,523.399579291899,523.480259007795,
523.564002670223,523.647642004487,523.731197147901,523.814684413027,523.898134538052,
523.981565611332,524.064995704658,524.148483264892,524.231998532224,524.315618988745,
524.394502893603),.UNSPECIFIED.);
#383=B_SPLINE_CURVE_WITH_KNOTS('',3,(#54841,#54842,#54843,#54844,#54845,
#54846,#54847,#54848,#54849,#54850,#54851,#54852,#54853,#54854,#54855,#54856,
#54857,#54858,#54859,#54860,#54861,#54862,#54863,#54864,#54865,#54866,#54867,
#54868,#54869,#54870,#54871,#54872,#54873,#54874,#54875,#54876,#54877,#54878,
#54879,#54880,#54881,#54882,#54883,#54884,#54885,#54886,#54887,#54888,#54889,
#54890,#54891,#54892,#54893,#54894,#54895,#54896,#54897,#54898,#54899,#54900,
#54901,#54902,#54903,#54904,#54905,#54906,#54907,#54908,#54909,#54910,#54911,
#54912,#54913,#54914,#54915,#54916,#54917,#54918,#54919,#54920,#54921,#54922,
#54923,#54924,#54925,#54926,#54927,#54928,#54929,#54930,#54931,#54932,#54933,
#54934,#54935,#54936,#54937,#54938,#54939,#54940,#54941,#54942,#54943,#54944,
#54945,#54946,#54947,#54948,#54949,#54950,#54951,#54952,#54953,#54954,#54955,
#54956,#54957,#54958,#54959,#54960,#54961,#54962,#54963,#54964,#54965,#54966,
#54967,#54968,#54969,#54970,#54971,#54972,#54973,#54974,#54975,#54976,#54977,
#54978,#54979,#54980,#54981,#54982,#54983,#54984,#54985,#54986,#54987,#54988,
#54989,#54990,#54991,#54992,#54993,#54994,#54995,#54996,#54997,#54998,#54999,
#55000,#55001,#55002,#55003,#55004,#55005,#55006,#55007,#55008,#55009,#55010,
#55011,#55012,#55013,#55014,#55015,#55016,#55017,#55018,#55019,#55020,#55021,
#55022,#55023,#55024,#55025,#55026,#55027,#55028,#55029,#55030,#55031,#55032,
#55033,#55034,#55035,#55036,#55037,#55038,#55039,#55040,#55041,#55042,#55043,
#55044,#55045,#55046,#55047,#55048,#55049,#55050,#55051,#55052,#55053,#55054,
#55055,#55056,#55057,#55058,#55059,#55060),.UNSPECIFIED.,.F.,.F.,(4,3,3,
3,3,3,3,3,3,3,3,3,3,3,3,3,3,3,3,3,3,3,3,3,3,3,3,3,3,3,3,3,3,3,3,3,3,3,3,
3,3,3,3,3,3,3,3,3,3,3,3,3,3,3,3,3,3,3,3,3,3,3,3,3,3,3,3,3,3,3,3,3,3,4),
(524.645973149475,524.732570018328,524.819253325717,524.906800096668,524.993752452295,
525.081596430907,525.169440409519,525.253179121365,525.336814632732,525.420367076131,
525.503856511982,525.587310462595,525.670746956442,525.754184066197,525.837639861115,
525.921184353845,526.004773436786,526.088496704343,526.169176420239,526.252915132085,
526.336550643452,526.420103086851,526.503592522703,526.587046473316,526.670482967162,
526.753920076918,526.837375871836,526.920920364565,527.004509447506,527.088232715064,
527.168912430959,527.252651142805,527.336286654173,527.419839097571,527.503328533422,
527.586782484036,527.670218977882,527.753656087637,527.837111882555,527.920656375285,
528.004245458226,528.087968725783,528.16864844168,528.252387153526,528.336022664894,
528.419575108292,528.503064544143,528.586518494757,528.669954988603,528.753392098358,
528.836847893276,528.920392386006,529.003981468947,529.087704736504,529.1683844524,
529.252123164246,529.335758675613,529.419311119012,529.502800554863,529.586254505477,
529.669690999323,529.753128109078,529.836583903995,529.920128396725,530.003717479666,
530.087440747223,530.16812046312,530.250811124454,530.333404118865,530.419488284874,
530.501935809903,530.58434732562,530.666745501053,530.677740782901),
 .UNSPECIFIED.);
#384=B_SPLINE_CURVE_WITH_KNOTS('',3,(#55061,#55062,#55063,#55064,#55065,
#55066,#55067,#55068,#55069,#55070),.UNSPECIFIED.,.F.,.F.,(4,3,3,4),(524.395667901685,
524.484235216775,524.57259525758,524.645973149366),.UNSPECIFIED.);
#385=B_SPLINE_CURVE_WITH_KNOTS('',3,(#55072,#55073,#55074,#55075,#55076,
#55077,#55078,#55079,#55080,#55081),.UNSPECIFIED.,.F.,.F.,(4,3,3,4),(524.394502893603,
524.479995018515,524.613424523667,524.645973149479),.UNSPECIFIED.);
#386=B_SPLINE_CURVE_WITH_KNOTS('',3,(#55082,#55083,#55084,#55085,#55086,
#55087,#55088,#55089,#55090,#55091,#55092,#55093,#55094,#55095,#55096,#55097,
#55098,#55099,#55100,#55101,#55102,#55103,#55104,#55105,#55106,#55107,#55108,
#55109,#55110,#55111,#55112,#55113,#55114,#55115,#55116,#55117,#55118,#55119,
#55120,#55121,#55122,#55123,#55124,#55125,#55126,#55127,#55128,#55129,#55130,
#55131,#55132,#55133,#55134,#55135,#55136,#55137,#55138,#55139,#55140,#55141,
#55142,#55143,#55144,#55145,#55146,#55147,#55148,#55149,#55150,#55151,#55152,
#55153,#55154,#55155,#55156,#55157,#55158,#55159,#55160,#55161,#55162,#55163,
#55164,#55165,#55166,#55167,#55168,#55169,#55170,#55171,#55172,#55173,#55174,
#55175,#55176,#55177,#55178,#55179,#55180,#55181,#55182,#55183,#55184,#55185,
#55186,#55187,#55188,#55189,#55190,#55191,#55192,#55193,#55194,#55195,#55196,
#55197,#55198,#55199,#55200,#55201,#55202,#55203,#55204,#55205,#55206,#55207,
#55208,#55209,#55210,#55211,#55212,#55213,#55214,#55215,#55216,#55217,#55218,
#55219,#55220,#55221,#55222,#55223,#55224,#55225,#55226,#55227,#55228,#55229,
#55230,#55231,#55232,#55233,#55234,#55235,#55236,#55237,#55238,#55239,#55240,
#55241,#55242,#55243,#55244,#55245,#55246,#55247,#55248,#55249,#55250,#55251,
#55252,#55253,#55254,#55255,#55256,#55257,#55258,#55259,#55260,#55261,#55262,
#55263,#55264,#55265,#55266,#55267,#55268,#55269,#55270,#55271,#55272,#55273,
#55274,#55275,#55276,#55277,#55278,#55279,#55280,#55281,#55282,#55283,#55284,
#55285,#55286,#55287,#55288,#55289,#55290,#55291,#55292,#55293,#55294,#55295,
#55296,#55297,#55298,#55299,#55300,#55301),.UNSPECIFIED.,.F.,.F.,(4,3,3,
3,3,3,3,3,3,3,3,3,3,3,3,3,3,3,3,3,3,3,3,3,3,3,3,3,3,3,3,3,3,3,3,3,3,3,3,
3,3,3,3,3,3,3,3,3,3,3,3,3,3,3,3,3,3,3,3,3,3,3,3,3,3,3,3,3,3,3,3,3,3,4),
(524.645973149671,524.728346440534,524.810641531603,524.894277718807,524.97648840522,
525.058689235174,525.140899242172,525.225607188938,525.307936227225,525.39383362823,
525.479731029235,525.563469741081,525.647105252449,525.730657695847,525.814147131698,
525.897601082312,525.981037576158,526.064474685913,526.147930480831,526.23147497356,
526.315064056501,526.398787324059,526.479467039955,526.563205751801,526.646841263168,
526.730393706567,526.813883142418,526.897337093032,526.980773586878,527.064210696633,
527.147666491551,527.231210984281,527.314800067222,527.398523334779,527.479203050675,
527.562941762521,527.646577273889,527.730129717287,527.813619153138,527.897073103752,
527.980509597598,528.063946707353,528.147402502271,528.230946995001,528.314536077942,
528.3982593455,528.478939061396,528.562677773242,528.64631328461,528.729865728008,
528.813355163859,528.896809114473,528.980245608319,529.063682718075,529.147138512993,
529.230683005722,529.314272088664,529.397995356221,529.478675072116,529.562413783962,
529.646049295329,529.729601738727,529.813091174578,529.896545125192,529.979981619038,
530.063418728794,530.146874523711,530.230419016441,530.314008099382,530.397731366939,
530.478411082836,530.568680668526,530.6587223636,530.67885489125),
 .UNSPECIFIED.);
#387=B_SPLINE_CURVE_WITH_KNOTS('',3,(#55307,#55308,#55309,#55310,#55311,
#55312,#55313,#55314,#55315,#55316,#55317,#55318,#55319,#55320,#55321,#55322,
#55323,#55324,#55325,#55326,#55327,#55328,#55329,#55330,#55331,#55332,#55333,
#55334,#55335,#55336,#55337,#55338,#55339,#55340,#55341,#55342,#55343,#55344,
#55345,#55346,#55347,#55348,#55349,#55350,#55351,#55352,#55353,#55354,#55355,
#55356,#55357,#55358,#55359,#55360,#55361,#55362,#55363,#55364,#55365,#55366,
#55367,#55368,#55369,#55370,#55371,#55372,#55373,#55374,#55375,#55376,#55377,
#55378,#55379,#55380,#55381,#55382,#55383,#55384,#55385,#55386,#55387,#55388,
#55389,#55390,#55391,#55392,#55393,#55394,#55395,#55396,#55397,#55398,#55399,
#55400,#55401,#55402,#55403,#55404,#55405,#55406,#55407,#55408,#55409,#55410,
#55411,#55412,#55413,#55414,#55415,#55416,#55417,#55418,#55419,#55420,#55421,
#55422,#55423,#55424,#55425,#55426,#55427,#55428,#55429,#55430,#55431,#55432,
#55433,#55434,#55435,#55436,#55437,#55438,#55439,#55440,#55441,#55442,#55443,
#55444,#55445,#55446,#55447,#55448,#55449,#55450,#55451,#55452,#55453,#55454,
#55455,#55456,#55457,#55458,#55459,#55460,#55461,#55462,#55463,#55464,#55465,
#55466,#55467,#55468,#55469,#55470,#55471,#55472,#55473,#55474,#55475,#55476,
#55477,#55478,#55479,#55480,#55481,#55482,#55483,#55484,#55485,#55486,#55487,
#55488,#55489,#55490,#55491,#55492,#55493,#55494,#55495,#55496,#55497,#55498,
#55499,#55500,#55501,#55502,#55503,#55504,#55505,#55506,#55507,#55508,#55509,
#55510,#55511,#55512,#55513,#55514,#55515,#55516,#55517,#55518,#55519,#55520,
#55521,#55522,#55523,#55524,#55525,#55526),.UNSPECIFIED.,.F.,.F.,(4,3,3,
3,3,3,3,3,3,3,3,3,3,3,3,3,3,3,3,3,3,3,3,3,3,3,3,3,3,3,3,3,3,3,3,3,3,3,3,
3,3,3,3,3,3,3,3,3,3,3,3,3,3,3,3,3,3,3,3,3,3,3,3,3,3,3,3,3,3,3,3,3,3,4),
(530.929158456779,531.038317168575,531.150322827254,531.16785647384,531.251595185686,
531.335230697053,531.418783140452,531.502272576303,531.585726526917,531.669163020763,
531.752600130519,531.836055925437,531.919600418166,532.003189501107,532.086912768665,
532.16759248456,532.251331196406,532.334966707774,532.418519151172,532.502008587023,
532.585462537637,532.668899031483,532.752336141238,532.835791936156,532.919336428886,
533.002925511826,533.086648779384,533.16732849528,533.251067207126,533.334702718494,
533.418255161892,533.501744597743,533.585198548357,533.668635042203,533.752072151958,
533.835527946876,533.919072439606,534.002661522547,534.086384790104,534.167064506,
534.250803217846,534.334438729214,534.417991172612,534.501480608463,534.584934559077,
534.668371052923,534.751808162679,534.835263957596,534.918808450326,535.002397533267,
535.086120800825,535.166800516721,535.250539228567,535.334174739934,535.417727183333,
535.501216619184,535.584670569798,535.668107063644,535.7515441734,535.834999968318,
535.918544461047,536.002133543988,536.085856811546,536.166536527441,536.250287695696,
536.333932951066,536.41747680672,536.500963156274,536.584410120162,536.667835788342,
536.75128140533,536.834737613956,536.918254701524,536.960677738898),
 .UNSPECIFIED.);
#388=B_SPLINE_CURVE_WITH_KNOTS('',3,(#55527,#55528,#55529,#55530,#55531,
#55532,#55533,#55534,#55535,#55536),.UNSPECIFIED.,.F.,.F.,(4,3,3,4),(530.677740782901,
530.760165021528,530.844661739092,530.929158456655),.UNSPECIFIED.);
#389=B_SPLINE_CURVE_WITH_KNOTS('',3,(#55538,#55539,#55540,#55541,#55542,
#55543,#55544,#55545,#55546,#55547),.UNSPECIFIED.,.F.,.F.,(4,3,3,4),(530.67885489125,
530.768607961165,530.858093749068,530.929158456555),.UNSPECIFIED.);
#390=B_SPLINE_CURVE_WITH_KNOTS('',3,(#55548,#55549,#55550,#55551,#55552,
#55553,#55554,#55555,#55556,#55557,#55558,#55559,#55560,#55561,#55562,#55563,
#55564,#55565,#55566,#55567,#55568,#55569,#55570,#55571,#55572,#55573,#55574,
#55575,#55576,#55577,#55578,#55579,#55580,#55581,#55582,#55583,#55584,#55585,
#55586,#55587,#55588,#55589,#55590,#55591,#55592,#55593,#55594,#55595,#55596,
#55597,#55598,#55599,#55600,#55601,#55602,#55603,#55604,#55605,#55606,#55607,
#55608,#55609,#55610,#55611,#55612,#55613,#55614,#55615,#55616,#55617,#55618,
#55619,#55620,#55621,#55622,#55623,#55624,#55625,#55626,#55627,#55628,#55629,
#55630,#55631,#55632,#55633,#55634,#55635,#55636,#55637,#55638,#55639,#55640,
#55641,#55642,#55643,#55644,#55645,#55646,#55647,#55648,#55649,#55650,#55651,
#55652,#55653,#55654,#55655,#55656,#55657,#55658,#55659,#55660,#55661,#55662,
#55663,#55664,#55665,#55666,#55667,#55668,#55669,#55670,#55671,#55672,#55673,
#55674,#55675,#55676,#55677,#55678,#55679,#55680,#55681,#55682,#55683,#55684,
#55685,#55686,#55687,#55688,#55689,#55690,#55691,#55692,#55693,#55694,#55695,
#55696,#55697,#55698,#55699,#55700,#55701,#55702,#55703,#55704,#55705,#55706,
#55707,#55708,#55709,#55710,#55711,#55712,#55713,#55714,#55715,#55716,#55717,
#55718,#55719,#55720,#55721,#55722,#55723,#55724,#55725,#55726,#55727,#55728,
#55729,#55730,#55731,#55732,#55733,#55734,#55735,#55736,#55737,#55738,#55739,
#55740,#55741,#55742,#55743,#55744,#55745,#55746,#55747,#55748,#55749,#55750,
#55751,#55752,#55753,#55754,#55755,#55756,#55757,#55758,#55759,#55760,#55761,
#55762,#55763,#55764,#55765,#55766,#55767),.UNSPECIFIED.,.F.,.F.,(4,3,3,
3,3,3,3,3,3,3,3,3,3,3,3,3,3,3,3,3,3,3,3,3,3,3,3,3,3,3,3,3,3,3,3,3,3,3,3,
3,3,3,3,3,3,3,3,3,3,3,3,3,3,3,3,3,3,3,3,3,3,3,3,3,3,3,3,3,3,3,3,3,3,4),
(530.929158456658,531.014983582773,531.100869687444,531.186830342444,531.272941100469,
531.35913682173,531.445489719647,531.478147093556,531.561885805402,531.645521316769,
531.729073760168,531.812563196019,531.896017146633,531.979453640479,532.062890750234,
532.146346545152,532.229891037881,532.313480120822,532.39720338838,532.477883104276,
532.561621816122,532.64525732749,532.728809770888,532.812299206739,532.895753157353,
532.979189651199,533.062626760954,533.146082555872,533.229627048602,533.313216131543,
533.3969393991,533.477619114996,533.561357826842,533.644993338209,533.728545781608,
533.812035217459,533.895489168073,533.978925661919,534.062362771674,534.145818566592,
534.229363059321,534.312952142262,534.39667540982,534.477355125716,534.561093837562,
534.64472934893,534.728281792328,534.811771228179,534.895225178793,534.978661672639,
535.062098782395,535.145554577312,535.229099070042,535.312688152983,535.396411420541,
535.477091136436,535.560829848282,535.644465359649,535.728017803047,535.811507238898,
535.894961189512,535.978397683358,536.061834793114,536.145290588032,536.228835080762,
536.312424163703,536.39614743126,536.476827147157,536.559707944129,536.642489631007,
536.725177599064,536.807810647652,536.890413189107,536.96105146982),
 .UNSPECIFIED.);
#391=B_SPLINE_CURVE_WITH_KNOTS('',3,(#55773,#55774,#55775,#55776,#55777,
#55778,#55779,#55780,#55781,#55782,#55783,#55784,#55785,#55786,#55787,#55788,
#55789,#55790,#55791,#55792,#55793,#55794,#55795,#55796,#55797,#55798,#55799,
#55800,#55801,#55802,#55803,#55804,#55805,#55806,#55807,#55808,#55809,#55810,
#55811,#55812,#55813,#55814,#55815,#55816,#55817,#55818,#55819,#55820,#55821,
#55822,#55823,#55824,#55825,#55826,#55827,#55828,#55829,#55830,#55831,#55832,
#55833,#55834,#55835,#55836,#55837,#55838,#55839,#55840,#55841,#55842,#55843,
#55844,#55845,#55846,#55847,#55848,#55849,#55850,#55851,#55852,#55853,#55854,
#55855,#55856,#55857,#55858,#55859,#55860,#55861,#55862,#55863,#55864,#55865,
#55866,#55867,#55868,#55869,#55870,#55871,#55872,#55873,#55874,#55875,#55876,
#55877,#55878,#55879,#55880,#55881,#55882,#55883,#55884,#55885,#55886,#55887,
#55888,#55889,#55890,#55891,#55892,#55893,#55894,#55895,#55896,#55897,#55898,
#55899,#55900,#55901,#55902,#55903,#55904,#55905,#55906,#55907,#55908,#55909,
#55910,#55911,#55912,#55913,#55914,#55915,#55916,#55917,#55918,#55919,#55920,
#55921,#55922,#55923,#55924,#55925,#55926,#55927,#55928,#55929,#55930,#55931,
#55932,#55933,#55934,#55935,#55936,#55937,#55938,#55939,#55940,#55941,#55942,
#55943,#55944,#55945,#55946,#55947,#55948,#55949,#55950,#55951,#55952,#55953,
#55954,#55955,#55956,#55957,#55958,#55959,#55960,#55961,#55962,#55963,#55964,
#55965,#55966,#55967,#55968,#55969,#55970,#55971,#55972,#55973,#55974,#55975,
#55976,#55977,#55978,#55979,#55980,#55981,#55982,#55983,#55984,#55985,#55986,
#55987,#55988,#55989,#55990,#55991,#55992),.UNSPECIFIED.,.F.,.F.,(4,3,3,
3,3,3,3,3,3,3,3,3,3,3,3,3,3,3,3,3,3,3,3,3,3,3,3,3,3,3,3,3,3,3,3,3,3,3,3,
3,3,3,3,3,3,3,3,3,3,3,3,3,3,3,3,3,3,3,3,3,3,3,3,3,3,3,3,3,3,3,3,3,3,4),
(537.212343764021,537.295471444526,537.378498659553,537.461446120284,537.544334461052,
537.627192884229,537.710038420663,537.792889661834,537.875765199949,537.958730434824,
538.041746292055,538.124883983816,538.166008548881,538.249747260727,538.333382772094,
538.416935215493,538.500424651344,538.583878601958,538.667315095804,538.750752205559,
538.834208000477,538.917752493206,539.001341576147,539.085064843705,539.165744559601,
539.249483271447,539.333118782814,539.416671226213,539.500160662064,539.583614612678,
539.667051106524,539.750488216279,539.833944011197,539.917488503927,540.001077586868,
540.084800854425,540.165480570321,540.249219282167,540.332854793534,540.416407236933,
540.499896672783,540.583350623397,540.666787117243,540.750224226999,540.833680021917,
540.917224514646,541.000813597587,541.084536865145,541.165216581041,541.248955292887,
541.332590804255,541.416143247653,541.499632683504,541.583086634118,541.666523127965,
541.74996023772,541.833416032638,541.916960525368,542.000549608309,542.084272875866,
542.164952591761,542.248691303607,542.332326814974,542.415879258372,542.499368694223,
542.582822644836,542.666259138682,542.749696248438,542.833152043356,542.916696536085,
543.000285619026,543.084008886584,543.164688602482,543.244911437326),
 .UNSPECIFIED.);
#392=B_SPLINE_CURVE_WITH_KNOTS('',3,(#55993,#55994,#55995,#55996,#55997,
#55998,#55999,#56000,#56001,#56002,#56003,#56004,#56005),.UNSPECIFIED.,
 .F.,.F.,(4,3,3,3,4),(536.960677738898,537.044295659432,537.128035723592,
537.166272538161,537.212343763834),.UNSPECIFIED.);
#393=B_SPLINE_CURVE_WITH_KNOTS('',3,(#56007,#56008,#56009,#56010,#56011,
#56012,#56013,#56014,#56015,#56016),.UNSPECIFIED.,.F.,.F.,(4,3,3,4),(536.96105146982,
537.043645884405,537.127994824122,537.212343763838),.UNSPECIFIED.);
#394=B_SPLINE_CURVE_WITH_KNOTS('',3,(#56017,#56018,#56019,#56020,#56021,
#56022,#56023,#56024,#56025,#56026,#56027,#56028,#56029,#56030,#56031,#56032,
#56033,#56034,#56035,#56036,#56037,#56038,#56039,#56040,#56041,#56042,#56043,
#56044,#56045,#56046,#56047,#56048,#56049,#56050,#56051,#56052,#56053,#56054,
#56055,#56056,#56057,#56058,#56059,#56060,#56061,#56062,#56063,#56064,#56065,
#56066,#56067,#56068,#56069,#56070,#56071,#56072,#56073,#56074,#56075,#56076,
#56077,#56078,#56079,#56080,#56081,#56082,#56083,#56084,#56085,#56086,#56087,
#56088,#56089,#56090,#56091,#56092,#56093,#56094,#56095,#56096,#56097,#56098,
#56099,#56100,#56101,#56102,#56103,#56104,#56105,#56106,#56107,#56108,#56109,
#56110,#56111,#56112,#56113,#56114,#56115,#56116,#56117,#56118,#56119,#56120,
#56121,#56122,#56123,#56124,#56125,#56126,#56127,#56128,#56129,#56130,#56131,
#56132,#56133,#56134,#56135,#56136,#56137,#56138,#56139,#56140,#56141,#56142,
#56143,#56144,#56145,#56146,#56147,#56148,#56149,#56150,#56151,#56152,#56153,
#56154,#56155,#56156,#56157,#56158,#56159,#56160,#56161,#56162,#56163,#56164,
#56165,#56166,#56167,#56168,#56169,#56170,#56171,#56172,#56173,#56174,#56175,
#56176,#56177,#56178,#56179,#56180,#56181,#56182,#56183,#56184,#56185,#56186,
#56187,#56188,#56189,#56190,#56191,#56192,#56193,#56194,#56195,#56196,#56197,
#56198,#56199,#56200,#56201,#56202,#56203,#56204,#56205,#56206,#56207,#56208,
#56209,#56210,#56211,#56212,#56213,#56214,#56215,#56216,#56217,#56218,#56219,
#56220,#56221,#56222,#56223,#56224,#56225,#56226,#56227,#56228,#56229,#56230,
#56231,#56232,#56233,#56234,#56235,#56236),.UNSPECIFIED.,.F.,.F.,(4,3,3,
3,3,3,3,3,3,3,3,3,3,3,3,3,3,3,3,3,3,3,3,3,3,3,3,3,3,3,3,3,3,3,3,3,3,3,3,
3,3,3,3,3,3,3,3,3,3,3,3,3,3,3,3,3,3,3,3,3,3,3,3,3,3,3,3,3,3,3,3,3,3,4),
(537.212343763992,537.317415438732,537.424490953973,537.476563157877,537.560301869723,
537.64393738109,537.727489824489,537.81097926034,537.894433210954,537.9778697048,
538.061306814556,538.144762609473,538.228307102203,538.311896185144,538.395619452702,
538.476299168597,538.560037880443,538.643673391811,538.727225835209,538.81071527106,
538.894169221674,538.97760571552,539.061042825275,539.144498620193,539.228043112923,
539.311632195864,539.395355463421,539.476035179317,539.559773891163,539.64340940253,
539.726961845929,539.81045128178,539.893905232393,539.97734172624,540.060778835995,
540.144234630913,540.227779123642,540.311368206583,540.395091474141,540.475771190037,
540.559509901883,540.643145413251,540.726697856649,540.8101872925,540.893641243114,
540.97707773696,541.060514846715,541.143970641633,541.227515134363,541.311104217304,
541.394827484861,541.475507200757,541.559245912603,541.64288142397,541.726433867369,
541.80992330322,541.893377253834,541.97681374768,542.060250857435,542.143706652353,
542.227251145083,542.310840228024,542.394563495581,542.475243211477,542.558996057361,
542.644604907669,542.728147807509,542.811633149667,542.895079054618,542.982276005919,
543.06571667707,543.149168860928,543.232671653005,543.24386685982),
 .UNSPECIFIED.);
#395=B_SPLINE_CURVE_WITH_KNOTS('',3,(#56242,#56243,#56244,#56245,#56246,
#56247,#56248,#56249,#56250,#56251,#56252,#56253,#56254,#56255,#56256,#56257,
#56258,#56259,#56260,#56261,#56262,#56263,#56264,#56265,#56266,#56267,#56268,
#56269,#56270,#56271,#56272,#56273,#56274,#56275,#56276,#56277,#56278,#56279,
#56280,#56281,#56282,#56283,#56284,#56285,#56286,#56287,#56288,#56289,#56290,
#56291,#56292,#56293,#56294,#56295,#56296,#56297,#56298,#56299,#56300,#56301,
#56302,#56303,#56304,#56305,#56306,#56307,#56308,#56309,#56310,#56311,#56312,
#56313,#56314,#56315,#56316,#56317,#56318,#56319,#56320,#56321,#56322,#56323,
#56324,#56325,#56326,#56327,#56328,#56329,#56330,#56331,#56332,#56333,#56334,
#56335,#56336,#56337,#56338,#56339,#56340,#56341,#56342,#56343,#56344,#56345,
#56346,#56347,#56348,#56349,#56350,#56351,#56352,#56353,#56354,#56355,#56356,
#56357,#56358,#56359,#56360,#56361,#56362,#56363,#56364,#56365,#56366,#56367,
#56368,#56369,#56370,#56371,#56372,#56373,#56374,#56375,#56376,#56377,#56378,
#56379,#56380,#56381,#56382,#56383,#56384,#56385,#56386,#56387,#56388,#56389,
#56390,#56391,#56392,#56393,#56394,#56395,#56396,#56397,#56398,#56399,#56400,
#56401,#56402,#56403,#56404,#56405,#56406,#56407,#56408,#56409,#56410,#56411,
#56412,#56413,#56414,#56415,#56416,#56417,#56418,#56419,#56420,#56421,#56422,
#56423,#56424,#56425,#56426,#56427,#56428,#56429,#56430,#56431,#56432,#56433,
#56434,#56435,#56436,#56437,#56438,#56439,#56440,#56441,#56442,#56443,#56444,
#56445,#56446,#56447,#56448,#56449,#56450,#56451,#56452,#56453,#56454,#56455,
#56456,#56457,#56458,#56459,#56460,#56461),.UNSPECIFIED.,.F.,.F.,(4,3,3,
3,3,3,3,3,3,3,3,3,3,3,3,3,3,3,3,3,3,3,3,3,3,3,3,3,3,3,3,3,3,3,3,3,3,3,3,
3,3,3,3,3,3,3,3,3,3,3,3,3,3,3,3,3,3,3,3,3,3,3,3,3,3,3,3,3,3,3,3,3,3,4),
(543.495529071014,543.579141013787,543.662478968956,543.745820579077,543.829183942922,
543.912994110492,543.996499535333,544.080462074267,544.164424613202,544.248163325048,
544.331798836415,544.415351279814,544.498840715664,544.582294666278,544.665731160124,
544.749168269879,544.832624064797,544.916168557526,544.999757640467,545.083480908025,
545.164160623922,545.247899335768,545.331534847135,545.415087290534,545.498576726385,
545.582030676999,545.665467170845,545.7489042806,545.832360075518,545.915904568247,
545.999493651188,546.083216918746,546.163896634642,546.247635346488,546.331270857856,
546.414823301254,546.498312737105,546.581766687719,546.665203181565,546.748640291321,
546.832096086239,546.915640578968,546.99922966191,547.082952929467,547.163632645362,
547.247371357208,547.331006868575,547.414559311973,547.498048747824,547.581502698438,
547.664939192284,547.748376302039,547.831832096956,547.915376589686,547.998965672627,
548.082688940184,548.163368656082,548.247107367928,548.330742879295,548.414295322694,
548.497784758545,548.581238709159,548.664675203005,548.74811231276,548.831568107678,
548.915112600408,548.998701683349,549.082424950906,549.163104666802,549.247756932178,
549.332263502758,549.41668560217,549.50102358319,549.528026787596),
 .UNSPECIFIED.);
#396=B_SPLINE_CURVE_WITH_KNOTS('',3,(#56462,#56463,#56464,#56465,#56466,
#56467,#56468,#56469,#56470,#56471),.UNSPECIFIED.,.F.,.F.,(4,3,3,4),(543.244911437326,
543.343198899028,543.440604770004,543.495529070829),.UNSPECIFIED.);
#397=B_SPLINE_CURVE_WITH_KNOTS('',3,(#56473,#56474,#56475,#56476,#56477,
#56478,#56479,#56480,#56481,#56482,#56483,#56484,#56485),.UNSPECIFIED.,
 .F.,.F.,(4,3,3,3,4),(543.24386685982,543.327466923206,543.41119626133,
543.474979222197,543.495529071018),.UNSPECIFIED.);
#398=B_SPLINE_CURVE_WITH_KNOTS('',3,(#56486,#56487,#56488,#56489,#56490,
#56491,#56492,#56493,#56494,#56495,#56496,#56497,#56498,#56499,#56500,#56501,
#56502,#56503,#56504,#56505,#56506,#56507,#56508,#56509,#56510,#56511,#56512,
#56513,#56514,#56515,#56516,#56517,#56518,#56519,#56520,#56521,#56522,#56523,
#56524,#56525,#56526,#56527,#56528,#56529,#56530,#56531,#56532,#56533,#56534,
#56535,#56536,#56537,#56538,#56539,#56540,#56541,#56542,#56543,#56544,#56545,
#56546,#56547,#56548,#56549,#56550,#56551,#56552,#56553,#56554,#56555,#56556,
#56557,#56558,#56559,#56560,#56561,#56562,#56563,#56564,#56565,#56566,#56567,
#56568,#56569,#56570,#56571,#56572,#56573,#56574,#56575,#56576,#56577,#56578,
#56579,#56580,#56581,#56582,#56583,#56584,#56585,#56586,#56587,#56588,#56589,
#56590,#56591,#56592,#56593,#56594,#56595,#56596,#56597,#56598,#56599,#56600,
#56601,#56602,#56603,#56604,#56605,#56606,#56607,#56608,#56609,#56610,#56611,
#56612,#56613,#56614,#56615,#56616,#56617,#56618,#56619,#56620,#56621,#56622,
#56623,#56624,#56625,#56626,#56627,#56628,#56629,#56630,#56631,#56632,#56633,
#56634,#56635,#56636,#56637,#56638,#56639,#56640,#56641,#56642,#56643,#56644,
#56645,#56646,#56647,#56648,#56649,#56650,#56651,#56652,#56653,#56654,#56655,
#56656,#56657,#56658,#56659,#56660,#56661,#56662,#56663,#56664,#56665,#56666,
#56667,#56668,#56669,#56670,#56671,#56672,#56673,#56674,#56675,#56676,#56677,
#56678,#56679,#56680,#56681,#56682,#56683,#56684,#56685,#56686,#56687,#56688,
#56689,#56690,#56691,#56692,#56693,#56694,#56695,#56696,#56697,#56698,#56699,
#56700,#56701,#56702,#56703,#56704,#56705),.UNSPECIFIED.,.F.,.F.,(4,3,3,
3,3,3,3,3,3,3,3,3,3,3,3,3,3,3,3,3,3,3,3,3,3,3,3,3,3,3,3,3,3,3,3,3,3,3,3,
3,3,3,3,3,3,3,3,3,3,3,3,3,3,3,3,3,3,3,3,3,3,3,3,3,3,3,3,3,3,3,3,3,3,4),
(543.495529071208,543.578972716166,543.662313827173,543.745572837891,543.82877010757,
543.911933825072,543.995081784154,544.078232326288,544.161403791053,544.244664224159,
544.327971770939,544.411407962298,544.474715232918,544.558453944764,544.642089456131,
544.72564189953,544.809131335381,544.892585285995,544.976021779841,545.059458889596,
545.142914684514,545.226459177244,545.310048260185,545.393771527742,545.474451243638,
545.558189955484,545.641825466851,545.72537791025,545.808867346101,545.892321296714,
545.975757790561,546.059194900316,546.142650695233,546.226195187963,546.309784270904,
546.393507538462,546.474187254358,546.557925966204,546.641561477571,546.72511392097,
546.808603356822,546.892057307435,546.975493801281,547.058930911037,547.142386705955,
547.225931198684,547.309520281625,547.393243549183,547.473923265078,547.557661976924,
547.641297488292,547.72484993169,547.808339367541,547.891793318155,547.975229812001,
548.058666921756,548.142122716674,548.225667209403,548.309256292344,548.392979559902,
548.473659275798,548.557397987644,548.641033499012,548.72458594241,548.808075378261,
548.891529328875,548.974965822721,549.058402932477,549.141858727395,549.225403220124,
549.308992303066,549.392715570623,549.473395286518,549.52796858603),
 .UNSPECIFIED.);
#399=B_SPLINE_CURVE_WITH_KNOTS('',3,(#56711,#56712,#56713,#56714,#56715,
#56716,#56717,#56718,#56719,#56720,#56721,#56722,#56723,#56724,#56725,#56726,
#56727,#56728,#56729,#56730,#56731,#56732,#56733,#56734,#56735,#56736,#56737,
#56738,#56739,#56740,#56741,#56742,#56743,#56744,#56745,#56746,#56747,#56748,
#56749,#56750,#56751,#56752,#56753,#56754,#56755,#56756,#56757,#56758,#56759,
#56760,#56761,#56762,#56763,#56764,#56765,#56766,#56767,#56768,#56769,#56770,
#56771,#56772,#56773,#56774,#56775,#56776,#56777,#56778,#56779,#56780,#56781,
#56782,#56783,#56784,#56785,#56786,#56787,#56788,#56789,#56790,#56791,#56792,
#56793,#56794,#56795,#56796,#56797,#56798,#56799,#56800,#56801,#56802,#56803,
#56804,#56805,#56806,#56807,#56808,#56809,#56810,#56811,#56812,#56813,#56814,
#56815,#56816,#56817,#56818,#56819,#56820,#56821,#56822,#56823,#56824,#56825,
#56826,#56827,#56828,#56829,#56830,#56831,#56832,#56833,#56834,#56835,#56836,
#56837,#56838,#56839,#56840,#56841,#56842,#56843,#56844,#56845,#56846,#56847,
#56848,#56849,#56850,#56851,#56852,#56853,#56854,#56855,#56856,#56857,#56858,
#56859,#56860,#56861,#56862,#56863,#56864,#56865,#56866,#56867,#56868,#56869,
#56870,#56871,#56872,#56873,#56874,#56875,#56876,#56877,#56878,#56879,#56880,
#56881,#56882,#56883,#56884,#56885,#56886,#56887,#56888,#56889,#56890,#56891,
#56892,#56893,#56894,#56895,#56896,#56897,#56898,#56899,#56900,#56901,#56902,
#56903,#56904,#56905,#56906,#56907,#56908,#56909,#56910,#56911,#56912,#56913,
#56914,#56915,#56916,#56917,#56918,#56919,#56920,#56921,#56922,#56923,#56924,
#56925,#56926,#56927),.UNSPECIFIED.,.F.,.F.,(4,3,3,3,3,3,3,3,3,3,3,3,3,
3,3,3,3,3,3,3,3,3,3,3,3,3,3,3,3,3,3,3,3,3,3,3,3,3,3,3,3,3,3,3,3,3,3,3,3,
3,3,3,3,3,3,3,3,3,3,3,3,3,3,3,3,3,3,3,3,3,3,3,4),(549.778714378383,549.874745953168,
549.96840019969,550.065620438607,550.162840677523,550.246579389368,550.330214900735,
550.413767344133,550.497256779984,550.580710730597,550.664147224443,550.747584334197,
550.831040129114,550.914584621843,550.998173704784,551.081896972341,551.162576688243,
551.246315400089,551.329950911457,551.413503354855,551.496992790706,551.58044674132,
551.663883235166,551.747320344921,551.830776139839,551.914320632569,551.99790971551,
552.081632983067,552.162312698963,552.246051410809,552.329686922177,552.413239365575,
552.496728801426,552.58018275204,552.663619245886,552.747056355642,552.830512150559,
552.914056643289,552.99764572623,553.081368993788,553.162048709683,553.245787421529,
553.329422932896,553.412975376295,553.496464812146,553.579918762759,553.663355256606,
553.746792366361,553.830248161279,553.913792654008,553.997381736949,554.081105004507,
554.161784720403,554.245523432249,554.329158943616,554.412711387015,554.496200822866,
554.57965477348,554.663091267326,554.746528377081,554.829984171999,554.913528664729,
554.99711774767,555.080841015227,555.161520731123,555.244195127162,555.32677495405,
555.409279290226,555.491727145886,555.574147610193,555.656549673153,555.738980910349,
555.810065543653),.UNSPECIFIED.);
#400=B_SPLINE_CURVE_WITH_KNOTS('',3,(#56928,#56929,#56930,#56931,#56932,
#56933,#56934,#56935,#56936,#56937),.UNSPECIFIED.,.F.,.F.,(4,3,3,4),(549.528026787596,
549.612291832284,549.696535530113,549.778714378193),.UNSPECIFIED.);
#401=B_SPLINE_CURVE_WITH_KNOTS('',3,(#56939,#56940,#56941,#56942,#56943,
#56944,#56945,#56946,#56947,#56948),.UNSPECIFIED.,.F.,.F.,(4,3,3,4),(549.52796858603,
549.629096792747,549.729053228591,549.778714378042),.UNSPECIFIED.);
#402=B_SPLINE_CURVE_WITH_KNOTS('',3,(#56949,#56950,#56951,#56952,#56953,
#56954,#56955,#56956,#56957,#56958,#56959,#56960,#56961,#56962,#56963,#56964,
#56965,#56966,#56967,#56968,#56969,#56970,#56971,#56972,#56973,#56974,#56975,
#56976,#56977,#56978,#56979,#56980,#56981,#56982,#56983,#56984,#56985,#56986,
#56987,#56988,#56989,#56990,#56991,#56992,#56993,#56994,#56995,#56996,#56997,
#56998,#56999,#57000,#57001,#57002,#57003,#57004,#57005,#57006,#57007,#57008,
#57009,#57010,#57011,#57012,#57013,#57014,#57015,#57016,#57017,#57018,#57019,
#57020,#57021,#57022,#57023,#57024,#57025,#57026,#57027,#57028,#57029,#57030,
#57031,#57032,#57033,#57034,#57035,#57036,#57037,#57038,#57039,#57040,#57041,
#57042,#57043,#57044,#57045,#57046,#57047,#57048,#57049,#57050,#57051,#57052,
#57053,#57054,#57055,#57056,#57057,#57058,#57059,#57060,#57061,#57062,#57063,
#57064,#57065,#57066,#57067,#57068,#57069,#57070,#57071,#57072,#57073,#57074,
#57075,#57076,#57077,#57078,#57079,#57080,#57081,#57082,#57083,#57084,#57085,
#57086,#57087,#57088,#57089,#57090,#57091,#57092,#57093,#57094,#57095,#57096,
#57097,#57098,#57099,#57100,#57101,#57102,#57103,#57104,#57105,#57106,#57107,
#57108,#57109,#57110,#57111,#57112,#57113,#57114,#57115,#57116,#57117,#57118,
#57119,#57120,#57121,#57122,#57123,#57124,#57125,#57126,#57127,#57128,#57129,
#57130,#57131,#57132,#57133,#57134,#57135,#57136,#57137,#57138,#57139,#57140,
#57141,#57142,#57143,#57144,#57145,#57146,#57147,#57148,#57149,#57150,#57151,
#57152,#57153,#57154,#57155,#57156,#57157,#57158,#57159,#57160,#57161,#57162,
#57163,#57164,#57165,#57166,#57167,#57168),.UNSPECIFIED.,.F.,.F.,(4,3,3,
3,3,3,3,3,3,3,3,3,3,3,3,3,3,3,3,3,3,3,3,3,3,3,3,3,3,3,3,3,3,3,3,3,3,3,3,
3,3,3,3,3,3,3,3,3,3,3,3,3,3,3,3,3,3,3,3,3,3,3,3,3,3,3,3,3,3,3,3,3,3,4),
(549.778714378197,549.865516493077,549.948524356781,550.031526339296,550.114540870175,
550.197586384082,550.280727545981,550.363924948296,550.447243433877,550.473131297238,
550.556870009084,550.640505520451,550.724057963849,550.8075473997,550.891001350314,
550.97443784416,551.057874953916,551.141330748833,551.224875241563,551.308464324503,
551.392187592061,551.472867307958,551.556606019804,551.640241531172,551.723793974571,
551.807283410422,551.890737361036,551.974173854882,552.057610964638,552.141066759556,
552.224611252286,552.308200335227,552.391923602785,552.472603318679,552.556342030525,
552.639977541893,552.723529985291,552.807019421142,552.890473371756,552.973909865602,
553.057346975358,553.140802770276,553.224347263005,553.307936345947,553.391659613504,
553.472339329399,553.556078041245,553.639713552612,553.723265996011,553.806755431861,
553.890209382475,553.973645876321,554.057082986076,554.140538780993,554.224083273723,
554.307672356664,554.391395624221,554.472075340119,554.555814051965,554.639449563332,
554.723002006731,554.806491442581,554.889945393195,554.973381887041,555.056818996797,
555.140274791715,555.223819284444,555.307408367385,555.391131634943,555.471811350839,
555.557006243862,555.642096639219,555.727068916262,555.811320836548),
 .UNSPECIFIED.);
#403=B_SPLINE_CURVE_WITH_KNOTS('',3,(#57174,#57175,#57176,#57177,#57178,
#57179,#57180,#57181,#57182,#57183,#57184,#57185,#57186,#57187,#57188,#57189,
#57190,#57191,#57192,#57193,#57194,#57195,#57196,#57197,#57198,#57199,#57200,
#57201,#57202,#57203,#57204,#57205,#57206,#57207,#57208,#57209,#57210,#57211,
#57212,#57213,#57214,#57215,#57216,#57217,#57218,#57219,#57220,#57221,#57222,
#57223,#57224,#57225,#57226,#57227,#57228,#57229,#57230,#57231,#57232,#57233,
#57234,#57235,#57236,#57237,#57238,#57239,#57240,#57241,#57242,#57243,#57244,
#57245,#57246,#57247,#57248,#57249,#57250,#57251,#57252,#57253,#57254,#57255,
#57256,#57257,#57258,#57259,#57260,#57261,#57262,#57263,#57264,#57265,#57266,
#57267,#57268,#57269,#57270,#57271,#57272,#57273,#57274,#57275,#57276,#57277,
#57278,#57279,#57280,#57281,#57282,#57283,#57284,#57285,#57286,#57287,#57288,
#57289,#57290,#57291,#57292,#57293,#57294,#57295,#57296,#57297,#57298,#57299,
#57300,#57301,#57302,#57303,#57304,#57305,#57306,#57307,#57308,#57309,#57310,
#57311,#57312,#57313,#57314,#57315,#57316,#57317,#57318,#57319,#57320,#57321,
#57322,#57323,#57324,#57325,#57326,#57327,#57328,#57329,#57330,#57331,#57332,
#57333,#57334,#57335,#57336,#57337,#57338,#57339,#57340,#57341,#57342,#57343,
#57344,#57345,#57346,#57347,#57348,#57349,#57350,#57351,#57352,#57353,#57354,
#57355,#57356,#57357,#57358,#57359,#57360,#57361,#57362,#57363,#57364,#57365,
#57366,#57367,#57368,#57369,#57370,#57371,#57372,#57373,#57374,#57375,#57376,
#57377,#57378,#57379,#57380,#57381,#57382,#57383,#57384,#57385,#57386,#57387,
#57388,#57389,#57390,#57391,#57392,#57393),.UNSPECIFIED.,.F.,.F.,(4,3,3,
3,3,3,3,3,3,3,3,3,3,3,3,3,3,3,3,3,3,3,3,3,3,3,3,3,3,3,3,3,3,3,3,3,3,3,3,
3,3,3,3,3,3,3,3,3,3,3,3,3,3,3,3,3,3,3,3,3,3,3,3,3,3,3,3,3,3,3,3,3,3,4),
(556.061899685373,556.161256741843,556.244995453689,556.328630965056,556.412183408455,
556.495672844306,556.579126794919,556.662563288766,556.746000398521,556.829456193439,
556.913000686169,556.996589769109,557.080313036667,557.160992752563,557.244731464409,
557.328366975777,557.411919419175,557.495408855027,557.57886280564,557.662299299487,
557.745736409242,557.82919220416,557.91273669689,557.996325779831,558.080049047389,
558.160728763284,558.24446747513,558.328102986498,558.411655429896,558.495144865747,
558.578598816361,558.662035310207,558.745472419963,558.828928214881,558.91247270761,
558.996061790551,559.079785058109,559.160464774004,559.24420348585,559.327838997217,
559.411391440616,559.494880876467,559.57833482708,559.661771320926,559.745208430682,
559.828664225599,559.912208718329,559.99579780127,560.079521068827,560.160200784724,
560.24393949657,560.327575007937,560.411127451336,560.494616887187,560.578070837801,
560.661507331647,560.744944441402,560.82840023632,560.911944729049,560.99553381199,
561.079257079548,561.159936795444,561.243679299686,561.327317733069,561.410872231796,
561.496223881097,561.579674149104,561.663106132975,561.746537904429,561.833324784874,
561.916848517875,562.000417343959,562.084082409679,562.093685426209),
 .UNSPECIFIED.);
#404=B_SPLINE_CURVE_WITH_KNOTS('',3,(#57394,#57395,#57396,#57397,#57398,
#57399,#57400,#57401,#57402,#57403),.UNSPECIFIED.,.F.,.F.,(4,3,3,4),(555.810065543653,
555.892572116197,555.977235900717,556.061899685237),.UNSPECIFIED.);
#405=B_SPLINE_CURVE_WITH_KNOTS('',3,(#57405,#57406,#57407,#57408,#57409,
#57410,#57411,#57412,#57413,#57414),.UNSPECIFIED.,.F.,.F.,(4,3,3,4),(555.811320836548,
555.896152743485,555.980940198063,556.061899685377),.UNSPECIFIED.);
#406=B_SPLINE_CURVE_WITH_KNOTS('',3,(#57415,#57416,#57417,#57418,#57419,
#57420,#57421,#57422,#57423,#57424,#57425,#57426,#57427,#57428,#57429,#57430,
#57431,#57432,#57433,#57434,#57435,#57436,#57437,#57438,#57439,#57440,#57441,
#57442,#57443,#57444,#57445,#57446,#57447,#57448,#57449,#57450,#57451,#57452,
#57453,#57454,#57455,#57456,#57457,#57458,#57459,#57460,#57461,#57462,#57463,
#57464,#57465,#57466,#57467,#57468,#57469,#57470,#57471,#57472,#57473,#57474,
#57475,#57476,#57477,#57478,#57479,#57480,#57481,#57482,#57483,#57484,#57485,
#57486,#57487,#57488,#57489,#57490,#57491,#57492,#57493,#57494,#57495,#57496,
#57497,#57498,#57499,#57500,#57501,#57502,#57503,#57504,#57505,#57506,#57507,
#57508,#57509,#57510,#57511,#57512,#57513,#57514,#57515,#57516,#57517,#57518,
#57519,#57520,#57521,#57522,#57523,#57524,#57525,#57526,#57527,#57528,#57529,
#57530,#57531,#57532,#57533,#57534,#57535,#57536,#57537,#57538,#57539,#57540,
#57541,#57542,#57543,#57544,#57545,#57546,#57547,#57548,#57549,#57550,#57551,
#57552,#57553,#57554,#57555,#57556,#57557,#57558,#57559,#57560,#57561,#57562,
#57563,#57564,#57565,#57566,#57567,#57568,#57569,#57570,#57571,#57572,#57573,
#57574,#57575,#57576,#57577,#57578,#57579,#57580,#57581,#57582,#57583,#57584,
#57585,#57586,#57587,#57588,#57589,#57590,#57591,#57592,#57593,#57594,#57595,
#57596,#57597,#57598,#57599,#57600,#57601,#57602,#57603,#57604,#57605,#57606,
#57607,#57608,#57609,#57610,#57611,#57612,#57613,#57614,#57615,#57616,#57617,
#57618,#57619,#57620,#57621,#57622,#57623,#57624,#57625,#57626,#57627,#57628,
#57629,#57630,#57631,#57632,#57633,#57634),.UNSPECIFIED.,.F.,.F.,(4,3,3,
3,3,3,3,3,3,3,3,3,3,3,3,3,3,3,3,3,3,3,3,3,3,3,3,3,3,3,3,3,3,3,3,3,3,3,3,
3,3,3,3,3,3,3,3,3,3,3,3,3,3,3,3,3,3,3,3,3,3,3,3,3,3,3,3,3,3,3,3,3,3,4),
(556.061899685548,556.153423872283,556.245403354288,556.337616989708,556.430154199635,
556.471547361559,556.555286073405,556.638921584773,556.722474028172,556.805963464024,
556.889417414637,556.972853908484,557.05629101824,557.139746813158,557.223291305888,
557.306880388829,557.390603656387,557.471283372279,557.555022084125,557.638657595493,
557.722210038891,557.805699474743,557.889153425356,557.972589919203,558.056027028959,
558.139482823876,558.223027316606,558.306616399547,558.390339667105,558.471019383,
558.554758094846,558.638393606213,558.721946049612,558.805435485463,558.888889436077,
558.972325929923,559.055763039678,559.139218834596,559.222763327325,559.306352410266,
559.390075677824,559.47075539372,559.554494105566,559.638129616933,559.721682060332,
559.805171496183,559.888625446796,559.972061940643,560.055499050398,560.138954845316,
560.222499338045,560.306088420986,560.389811688544,560.47049140444,560.554230116286,
560.637865627654,560.721418071052,560.804907506903,560.888361457517,560.971797951363,
561.055235061119,561.138690856037,561.222235348767,561.305824431708,561.389547699265,
561.47022741516,561.552778166199,561.635234203606,561.717614690464,561.799938718783,
561.882233023257,561.96450928654,562.046807049963,562.093278782699),
 .UNSPECIFIED.);
#407=B_SPLINE_CURVE_WITH_KNOTS('',3,(#57640,#57641,#57642,#57643,#57644,
#57645,#57646,#57647,#57648,#57649,#57650,#57651,#57652,#57653,#57654,#57655,
#57656,#57657,#57658,#57659,#57660,#57661,#57662,#57663,#57664,#57665,#57666,
#57667,#57668,#57669,#57670,#57671,#57672,#57673,#57674,#57675,#57676,#57677,
#57678,#57679,#57680,#57681,#57682,#57683,#57684,#57685,#57686,#57687,#57688,
#57689,#57690,#57691,#57692,#57693,#57694,#57695,#57696,#57697,#57698,#57699,
#57700,#57701,#57702,#57703,#57704,#57705,#57706,#57707,#57708,#57709,#57710,
#57711,#57712,#57713,#57714,#57715,#57716,#57717,#57718,#57719,#57720,#57721,
#57722,#57723,#57724,#57725,#57726,#57727,#57728,#57729,#57730,#57731,#57732,
#57733,#57734,#57735,#57736,#57737,#57738,#57739,#57740,#57741,#57742,#57743,
#57744,#57745,#57746,#57747,#57748,#57749,#57750,#57751,#57752,#57753,#57754,
#57755,#57756,#57757,#57758,#57759,#57760,#57761,#57762,#57763,#57764,#57765,
#57766,#57767,#57768,#57769,#57770,#57771,#57772,#57773,#57774,#57775,#57776,
#57777,#57778,#57779,#57780,#57781,#57782,#57783,#57784,#57785,#57786,#57787,
#57788,#57789,#57790,#57791,#57792,#57793,#57794,#57795,#57796,#57797,#57798,
#57799,#57800,#57801,#57802,#57803,#57804,#57805,#57806,#57807,#57808,#57809,
#57810,#57811,#57812,#57813,#57814,#57815,#57816,#57817,#57818,#57819,#57820,
#57821,#57822,#57823,#57824,#57825,#57826,#57827,#57828,#57829,#57830,#57831,
#57832,#57833,#57834,#57835,#57836,#57837,#57838,#57839,#57840,#57841,#57842,
#57843,#57844,#57845,#57846,#57847,#57848,#57849,#57850,#57851,#57852,#57853,
#57854,#57855,#57856,#57857,#57858,#57859),.UNSPECIFIED.,.F.,.F.,(4,3,3,
3,3,3,3,3,3,3,3,3,3,3,3,3,3,3,3,3,3,3,3,3,3,3,3,3,3,3,3,3,3,3,3,3,3,3,3,
3,3,3,3,3,3,3,3,3,3,3,3,3,3,3,3,3,3,3,3,3,3,3,3,3,3,3,3,3,3,3,3,3,3,4),
(562.345084992693,562.427448531772,562.509738999425,562.591981547654,562.674199476266,
562.756411818623,562.838637601327,562.92094554502,563.003295183593,563.085773648807,
563.159408816884,563.24314752873,563.326783040097,563.410335483496,563.493824919347,
563.577278869961,563.660715363807,563.744152473562,563.82760826848,563.91115276121,
563.994741844151,564.078465111708,564.159144827604,564.24288353945,564.326519050818,
564.410071494216,564.493560930067,564.57701488068,564.660451374527,564.743888484282,
564.8273442792,564.91088877193,564.994477854871,565.078201122428,565.158880838324,
565.24261955017,565.326255061537,565.409807504936,565.493296940786,565.5767508914,
565.660187385246,565.743624495002,565.827080289919,565.910624782649,565.99421386559,
566.077937133148,566.158616849045,566.242355560891,566.325991072258,566.409543515657,
566.493032951509,566.576486902122,566.659923395969,566.743360505724,566.826816300642,
566.910360793372,566.993949876313,567.07767314387,567.158352859765,567.242091571611,
567.325727082978,567.409279526377,567.492768962228,567.576222912842,567.659659406688,
567.743096516444,567.826552311361,567.910096804091,567.993685887032,568.077409154589,
568.158088870485,568.247415364467,568.336527127973,568.37796764204),
 .UNSPECIFIED.);
#408=B_SPLINE_CURVE_WITH_KNOTS('',3,(#57860,#57861,#57862,#57863,#57864,
#57865,#57866,#57867,#57868,#57869),.UNSPECIFIED.,.F.,.F.,(4,3,3,4),(562.093685426209,
562.159672806164,562.284783772402,562.345084992552),.UNSPECIFIED.);
#409=B_SPLINE_CURVE_WITH_KNOTS('',3,(#57871,#57872,#57873,#57874,#57875,
#57876,#57877,#57878,#57879,#57880),.UNSPECIFIED.,.F.,.F.,(4,3,3,4),(562.093278782699,
562.175645741503,562.260365366964,562.345084992425),.UNSPECIFIED.);
#410=B_SPLINE_CURVE_WITH_KNOTS('',3,(#57881,#57882,#57883,#57884,#57885,
#57886,#57887,#57888,#57889,#57890,#57891,#57892,#57893,#57894,#57895,#57896,
#57897,#57898,#57899,#57900,#57901,#57902,#57903,#57904,#57905,#57906,#57907,
#57908,#57909,#57910,#57911,#57912,#57913,#57914,#57915,#57916,#57917,#57918,
#57919,#57920,#57921,#57922,#57923,#57924,#57925,#57926,#57927,#57928,#57929,
#57930,#57931,#57932,#57933,#57934,#57935,#57936,#57937,#57938,#57939,#57940,
#57941,#57942,#57943,#57944,#57945,#57946,#57947,#57948,#57949,#57950,#57951,
#57952,#57953,#57954,#57955,#57956,#57957,#57958,#57959,#57960,#57961,#57962,
#57963,#57964,#57965,#57966,#57967,#57968,#57969,#57970,#57971,#57972,#57973,
#57974,#57975,#57976,#57977,#57978,#57979,#57980,#57981,#57982,#57983,#57984,
#57985,#57986,#57987,#57988,#57989,#57990,#57991,#57992,#57993,#57994,#57995,
#57996,#57997,#57998,#57999,#58000,#58001,#58002,#58003,#58004,#58005,#58006,
#58007,#58008,#58009,#58010,#58011,#58012,#58013,#58014,#58015,#58016,#58017,
#58018,#58019,#58020,#58021,#58022,#58023,#58024,#58025,#58026,#58027,#58028,
#58029,#58030,#58031,#58032,#58033,#58034,#58035,#58036,#58037,#58038,#58039,
#58040,#58041,#58042,#58043,#58044,#58045,#58046,#58047,#58048,#58049,#58050,
#58051,#58052,#58053,#58054,#58055,#58056,#58057,#58058,#58059,#58060,#58061,
#58062,#58063,#58064,#58065,#58066,#58067,#58068,#58069,#58070,#58071,#58072,
#58073,#58074,#58075,#58076,#58077,#58078,#58079,#58080,#58081,#58082,#58083,
#58084,#58085,#58086,#58087,#58088,#58089,#58090,#58091,#58092,#58093,#58094,
#58095,#58096,#58097),.UNSPECIFIED.,.F.,.F.,(4,3,3,3,3,3,3,3,3,3,3,3,3,
3,3,3,3,3,3,3,3,3,3,3,3,3,3,3,3,3,3,3,3,3,3,3,3,3,3,3,3,3,3,3,3,3,3,3,3,
3,3,3,3,3,3,3,3,3,3,3,3,3,3,3,3,3,3,3,3,3,3,3,4),(562.345084992556,562.46996342588,
562.553702137726,562.637337649093,562.720890092492,562.804379528343,562.887833478956,
562.971269972802,563.054707082558,563.138162877476,563.221707370205,563.305296453146,
563.389019720704,563.4696994366,563.553438148446,563.637073659813,563.720626103212,
563.804115539063,563.887569489677,563.971005983523,564.054443093278,564.137898888196,
564.221443380925,564.305032463866,564.388755731424,564.46943544732,564.553174159166,
564.636809670533,564.720362113932,564.803851549783,564.887305500397,564.970741994243,
565.054179103998,565.137634898916,565.221179391645,565.304768474586,565.388491742144,
565.46917145804,565.552910169886,565.636545681254,565.720098124652,565.803587560503,
565.887041511117,565.970478004963,566.053915114719,566.137370909636,566.220915402366,
566.304504485307,566.388227752865,566.46890746876,566.552646180606,566.636281691974,
566.719834135372,566.803323571223,566.886777521837,566.970214015683,567.053651125439,
567.137106920357,567.220651413086,567.304240496028,567.387963763585,567.468643479481,
567.552387508031,567.636027127852,567.719582476606,567.803069632465,567.886519534233,
567.969950270323,568.053379912481,568.136865629516,568.220379007305,568.303994204407,
568.3767803679),.UNSPECIFIED.);
#411=B_SPLINE_CURVE_WITH_KNOTS('',3,(#58103,#58104,#58105,#58106,#58107,
#58108,#58109,#58110,#58111,#58112,#58113,#58114,#58115,#58116,#58117,#58118,
#58119,#58120,#58121,#58122,#58123,#58124,#58125,#58126,#58127,#58128,#58129,
#58130,#58131,#58132,#58133,#58134,#58135,#58136,#58137,#58138,#58139,#58140,
#58141,#58142,#58143,#58144,#58145,#58146,#58147,#58148,#58149,#58150,#58151,
#58152,#58153,#58154,#58155,#58156,#58157,#58158,#58159,#58160,#58161,#58162,
#58163,#58164,#58165,#58166,#58167,#58168,#58169,#58170,#58171,#58172,#58173,
#58174,#58175,#58176,#58177,#58178,#58179,#58180,#58181,#58182,#58183,#58184,
#58185,#58186,#58187,#58188,#58189,#58190,#58191,#58192,#58193,#58194,#58195,
#58196,#58197,#58198,#58199,#58200,#58201,#58202,#58203,#58204,#58205,#58206,
#58207,#58208,#58209,#58210,#58211,#58212,#58213,#58214,#58215,#58216,#58217,
#58218,#58219,#58220,#58221,#58222,#58223,#58224,#58225,#58226,#58227,#58228,
#58229,#58230,#58231,#58232,#58233,#58234,#58235,#58236,#58237,#58238,#58239,
#58240,#58241,#58242,#58243,#58244,#58245,#58246,#58247,#58248,#58249,#58250,
#58251,#58252,#58253,#58254,#58255,#58256,#58257,#58258,#58259,#58260,#58261,
#58262,#58263,#58264,#58265,#58266,#58267,#58268,#58269,#58270,#58271,#58272,
#58273,#58274,#58275,#58276,#58277,#58278,#58279,#58280,#58281,#58282,#58283,
#58284,#58285,#58286,#58287,#58288,#58289,#58290,#58291,#58292,#58293,#58294,
#58295,#58296,#58297,#58298,#58299,#58300,#58301,#58302,#58303,#58304,#58305,
#58306,#58307,#58308,#58309,#58310,#58311,#58312,#58313,#58314,#58315,#58316,
#58317,#58318,#58319),.UNSPECIFIED.,.F.,.F.,(4,3,3,3,3,3,3,3,3,3,3,3,3,
3,3,3,3,3,3,3,3,3,3,3,3,3,3,3,3,3,3,3,3,3,3,3,3,3,3,3,3,3,3,3,3,3,3,3,3,
3,3,3,3,3,3,3,3,3,3,3,3,3,3,3,3,3,3,3,3,3,3,3,4),(568.628270299732,568.714673941208,
568.801157485386,568.890324334341,568.977067748322,569.067446314764,569.157824881205,
569.241563593051,569.325199104419,569.408751547817,569.492240983668,569.575694934282,
569.659131428128,569.742568537883,569.826024332801,569.909568825531,569.993157908472,
570.07688117603,570.157560891925,570.241299603771,570.324935115138,570.408487558537,
570.491976994388,570.575430945002,570.658867438848,570.742304548603,570.825760343521,
570.90930483625,570.992893919191,571.076617186749,571.157296902645,571.241035614491,
571.324671125859,571.408223569257,571.491713005108,571.575166955722,571.658603449568,
571.742040559324,571.825496354241,571.909040846971,571.992629929912,572.07635319747,
572.157032913365,572.240771625211,572.324407136578,572.407959579977,572.491449015828,
572.574902966442,572.658339460288,572.741776570043,572.825232364961,572.908776857691,
572.992365940632,573.076089208189,573.156768924085,573.240507635931,573.324143147299,
573.407695590697,573.491185026548,573.574638977162,573.658075471008,573.741512580764,
573.824968375682,573.908512868411,573.992101951352,574.07582521891,574.156504934806,
574.239235471064,574.321868030338,574.406417798025,574.488904569422,574.574485835255,
574.660067101088),.UNSPECIFIED.);
#412=B_SPLINE_CURVE_WITH_KNOTS('',3,(#58320,#58321,#58322,#58323,#58324,
#58325,#58326,#58327,#58328,#58329),.UNSPECIFIED.,.F.,.F.,(4,3,3,4),(568.37796764204,
568.466803636206,568.555419194261,568.628270299597),.UNSPECIFIED.);
#413=B_SPLINE_CURVE_WITH_KNOTS('',3,(#58331,#58332,#58333,#58334,#58335,
#58336,#58337,#58338,#58339,#58340,#58341,#58342,#58343),.UNSPECIFIED.,
 .F.,.F.,(4,3,3,3,4),(568.3767803679,568.460535618476,568.468379490201,
568.604938226218,568.628270299736),.UNSPECIFIED.);
#414=B_SPLINE_CURVE_WITH_KNOTS('',3,(#58344,#58345,#58346,#58347,#58348,
#58349,#58350,#58351,#58352,#58353,#58354,#58355,#58356,#58357,#58358,#58359,
#58360,#58361,#58362,#58363,#58364,#58365,#58366,#58367,#58368,#58369,#58370,
#58371,#58372,#58373,#58374,#58375,#58376,#58377,#58378,#58379,#58380,#58381,
#58382,#58383,#58384,#58385,#58386,#58387,#58388,#58389,#58390,#58391,#58392,
#58393,#58394,#58395,#58396,#58397,#58398,#58399,#58400,#58401,#58402,#58403,
#58404,#58405,#58406,#58407,#58408,#58409,#58410,#58411,#58412,#58413,#58414,
#58415,#58416,#58417,#58418,#58419,#58420,#58421,#58422,#58423,#58424,#58425,
#58426,#58427,#58428,#58429,#58430,#58431,#58432,#58433,#58434,#58435,#58436,
#58437,#58438,#58439,#58440,#58441,#58442,#58443,#58444,#58445,#58446,#58447,
#58448,#58449,#58450,#58451,#58452,#58453,#58454,#58455,#58456,#58457,#58458,
#58459,#58460,#58461,#58462,#58463,#58464,#58465,#58466,#58467,#58468,#58469,
#58470,#58471,#58472,#58473,#58474,#58475,#58476,#58477,#58478,#58479,#58480,
#58481,#58482,#58483,#58484,#58485,#58486,#58487,#58488,#58489,#58490,#58491,
#58492,#58493,#58494,#58495,#58496,#58497,#58498,#58499,#58500,#58501,#58502,
#58503,#58504,#58505,#58506,#58507,#58508,#58509,#58510,#58511,#58512,#58513,
#58514,#58515,#58516,#58517,#58518,#58519,#58520,#58521,#58522,#58523,#58524,
#58525,#58526,#58527,#58528,#58529,#58530,#58531,#58532,#58533,#58534,#58535,
#58536,#58537,#58538,#58539,#58540,#58541,#58542,#58543,#58544,#58545,#58546,
#58547,#58548,#58549,#58550,#58551,#58552,#58553,#58554,#58555,#58556,#58557,
#58558,#58559,#58560,#58561,#58562,#58563,#58564,#58565,#58566),
 .UNSPECIFIED.,.F.,.F.,(4,3,3,3,3,3,3,3,3,3,3,3,3,3,3,3,3,3,3,3,3,3,3,3,
3,3,3,3,3,3,3,3,3,3,3,3,3,3,3,3,3,3,3,3,3,3,3,3,3,3,3,3,3,3,3,3,3,3,3,3,
3,3,3,3,3,3,3,3,3,3,3,3,3,3,4),(568.628270299839,568.710653138352,568.792956251044,
568.877351157279,568.959566188819,569.041770160988,569.12398210561,569.210015454438,
569.292345390399,569.374730026394,569.457226730502,569.468115500921,569.551854212767,
569.635489724134,569.719042167533,569.802531603384,569.885985553998,569.969422047844,
570.052859157599,570.136314952517,570.219859445246,570.303448528187,570.387171795745,
570.467851511641,570.551590223487,570.635225734855,570.718778178253,570.802267614104,
570.885721564718,570.969158058564,571.052595168319,571.136050963237,571.219595455967,
571.303184538908,571.386907806466,571.467587522361,571.551326234207,571.634961745575,
571.718514188973,571.802003624824,571.885457575438,571.968894069284,572.05233117904,
572.135786973957,572.219331466687,572.302920549628,572.386643817186,572.467323533081,
572.551062244927,572.634697756294,572.718250199692,572.801739635544,572.885193586158,
572.968630080004,573.05206718976,573.135522984677,573.219067477407,573.302656560348,
573.386379827905,573.467059543801,573.550798255647,573.634433767015,573.717986210413,
573.801475646264,573.884929596878,573.968366090724,574.05180320048,574.135258995397,
574.218803488127,574.302392571068,574.386115838625,574.466795554521,574.557380703572,
574.647733634699,574.661148849332),.UNSPECIFIED.);
#415=B_SPLINE_CURVE_WITH_KNOTS('',3,(#58572,#58573,#58574,#58575,#58576,
#58577,#58578,#58579,#58580,#58581,#58582,#58583,#58584,#58585,#58586,#58587,
#58588,#58589,#58590,#58591,#58592,#58593,#58594,#58595,#58596,#58597,#58598,
#58599,#58600,#58601,#58602,#58603,#58604,#58605,#58606,#58607,#58608,#58609,
#58610,#58611,#58612,#58613,#58614,#58615,#58616,#58617,#58618,#58619,#58620,
#58621,#58622,#58623,#58624,#58625,#58626,#58627,#58628,#58629,#58630,#58631,
#58632,#58633,#58634,#58635,#58636,#58637,#58638,#58639,#58640,#58641,#58642,
#58643,#58644,#58645,#58646,#58647,#58648,#58649,#58650,#58651,#58652,#58653,
#58654,#58655,#58656,#58657,#58658,#58659,#58660,#58661,#58662,#58663,#58664,
#58665,#58666,#58667,#58668,#58669,#58670,#58671,#58672,#58673,#58674,#58675,
#58676,#58677,#58678,#58679,#58680,#58681,#58682,#58683,#58684,#58685,#58686,
#58687,#58688,#58689,#58690,#58691,#58692,#58693,#58694,#58695,#58696,#58697,
#58698,#58699,#58700,#58701,#58702,#58703,#58704,#58705,#58706,#58707,#58708,
#58709,#58710,#58711,#58712,#58713,#58714,#58715,#58716,#58717,#58718,#58719,
#58720,#58721,#58722,#58723,#58724,#58725,#58726,#58727,#58728,#58729,#58730,
#58731,#58732,#58733,#58734,#58735,#58736,#58737,#58738,#58739,#58740,#58741,
#58742,#58743,#58744,#58745,#58746,#58747,#58748,#58749,#58750,#58751,#58752,
#58753,#58754,#58755,#58756,#58757,#58758,#58759,#58760,#58761,#58762,#58763,
#58764,#58765,#58766,#58767,#58768,#58769,#58770,#58771,#58772,#58773,#58774,
#58775,#58776,#58777,#58778,#58779,#58780,#58781,#58782,#58783,#58784,#58785,
#58786,#58787,#58788,#58789,#58790,#58791),.UNSPECIFIED.,.F.,.F.,(4,3,3,
3,3,3,3,3,3,3,3,3,3,3,3,3,3,3,3,3,3,3,3,3,3,3,3,3,3,3,3,3,3,3,3,3,3,3,3,
3,3,3,3,3,3,3,3,3,3,3,3,3,3,3,3,3,3,3,3,3,3,3,3,3,3,3,3,3,3,3,3,3,3,4),
(574.911455607035,575.019558419726,575.130265374109,575.156240945526,575.239979657372,
575.323615168739,575.407167612138,575.490657047989,575.574110998603,575.657547492449,
575.740984602205,575.824440397122,575.907984889852,575.991573972793,576.075297240351,
576.155976956246,576.239715668092,576.32335117946,576.406903622858,576.490393058709,
576.573847009323,576.657283503169,576.740720612924,576.824176407842,576.907720900572,
576.991309983512,577.07503325107,577.155712966966,577.239451678812,577.323087190179,
577.406639633578,577.490129069429,577.573583020042,577.657019513889,577.740456623644,
577.823912418562,577.907456911291,577.991045994232,578.07476926179,578.155448977686,
578.239187689532,578.3228232009,578.406375644298,578.489865080149,578.573319030763,
578.656755524609,578.740192634365,578.823648429282,578.907192922012,578.990782004953,
579.074505272511,579.155184988406,579.238923700252,579.322559211619,579.406111655018,
579.489601090869,579.573055041483,579.656491535329,579.739928645084,579.823384440002,
579.906928932732,579.990518015673,580.07424128323,580.154920999126,580.238672564971,
580.326710311874,580.410250823492,580.493734668348,580.577179965179,580.660604802776,
580.744049301531,580.82750519747,580.91101905523,580.942974540196),
 .UNSPECIFIED.);
#416=B_SPLINE_CURVE_WITH_KNOTS('',3,(#58792,#58793,#58794,#58795,#58796,
#58797,#58798,#58799,#58800,#58801),.UNSPECIFIED.,.F.,.F.,(4,3,3,4),(574.660067101088,
574.742526490161,574.826991048537,574.911455606912),.UNSPECIFIED.);
#417=B_SPLINE_CURVE_WITH_KNOTS('',3,(#58803,#58804,#58805,#58806,#58807,
#58808,#58809,#58810,#58811,#58812),.UNSPECIFIED.,.F.,.F.,(4,3,3,4),(574.661148849332,
574.751208983431,574.840985453372,574.911455606801),.UNSPECIFIED.);
#418=B_SPLINE_CURVE_WITH_KNOTS('',3,(#58813,#58814,#58815,#58816,#58817,
#58818,#58819,#58820,#58821,#58822,#58823,#58824,#58825,#58826,#58827,#58828,
#58829,#58830,#58831,#58832,#58833,#58834,#58835,#58836,#58837,#58838,#58839,
#58840,#58841,#58842,#58843,#58844,#58845,#58846,#58847,#58848,#58849,#58850,
#58851,#58852,#58853,#58854,#58855,#58856,#58857,#58858,#58859,#58860,#58861,
#58862,#58863,#58864,#58865,#58866,#58867,#58868,#58869,#58870,#58871,#58872,
#58873,#58874,#58875,#58876,#58877,#58878,#58879,#58880,#58881,#58882,#58883,
#58884,#58885,#58886,#58887,#58888,#58889,#58890,#58891,#58892,#58893,#58894,
#58895,#58896,#58897,#58898,#58899,#58900,#58901,#58902,#58903,#58904,#58905,
#58906,#58907,#58908,#58909,#58910,#58911,#58912,#58913,#58914,#58915,#58916,
#58917,#58918,#58919,#58920,#58921,#58922,#58923,#58924,#58925,#58926,#58927,
#58928,#58929,#58930,#58931,#58932,#58933,#58934,#58935,#58936,#58937,#58938,
#58939,#58940,#58941,#58942,#58943,#58944,#58945,#58946,#58947,#58948,#58949,
#58950,#58951,#58952,#58953,#58954,#58955,#58956,#58957,#58958,#58959,#58960,
#58961,#58962,#58963,#58964,#58965,#58966,#58967,#58968,#58969,#58970,#58971,
#58972,#58973,#58974,#58975,#58976,#58977,#58978,#58979,#58980,#58981,#58982,
#58983,#58984,#58985,#58986,#58987,#58988,#58989,#58990,#58991,#58992,#58993,
#58994,#58995,#58996,#58997,#58998,#58999,#59000,#59001,#59002,#59003,#59004,
#59005,#59006,#59007,#59008,#59009,#59010,#59011,#59012,#59013,#59014,#59015,
#59016,#59017,#59018,#59019,#59020,#59021,#59022,#59023,#59024,#59025,#59026,
#59027,#59028,#59029,#59030,#59031,#59032),.UNSPECIFIED.,.F.,.F.,(4,3,3,
3,3,3,3,3,3,3,3,3,3,3,3,3,3,3,3,3,3,3,3,3,3,3,3,3,3,3,3,3,3,3,3,3,3,3,3,
3,3,3,3,3,3,3,3,3,3,3,3,3,3,3,3,3,3,3,3,3,3,3,3,3,3,3,3,3,3,3,3,3,3,4),
(574.911455606915,574.997111060428,575.082822107205,575.168602763877,575.254529100318,
575.340536906395,575.426701887711,575.466531565242,575.550270277088,575.633905788455,
575.717458231854,575.800947667705,575.884401618319,575.967838112165,576.05127522192,
576.134731016837,576.218275509567,576.301864592508,576.385587860065,576.466267575962,
576.550006287808,576.633641799176,576.717194242574,576.800683678425,576.884137629039,
576.967574122885,577.051011232641,577.134467027558,577.218011520288,577.301600603229,
577.385323870787,577.466003586682,577.549742298528,577.633377809895,577.716930253294,
577.800419689145,577.883873639758,577.967310133604,578.05074724336,578.134203038277,
578.217747531007,578.301336613948,578.385059881506,578.465739597402,578.549478309248,
578.633113820615,578.716666264014,578.800155699865,578.883609650479,578.967046144325,
579.05048325408,579.133939048997,579.217483541727,579.301072624668,579.384795892226,
579.465475608122,579.549214319968,579.632849831336,579.716402274735,579.799891710585,
579.883345661199,579.966782155046,580.050219264801,580.133675059718,580.217219552448,
580.300808635389,580.384531902946,580.465211618842,580.548146779117,580.630982425771,
580.713723386536,580.796409076522,580.879062240394,580.943379534668),
 .UNSPECIFIED.);
#419=B_SPLINE_CURVE_WITH_KNOTS('',3,(#59038,#59039,#59040,#59041,#59042,
#59043,#59044,#59045,#59046,#59047,#59048,#59049,#59050,#59051,#59052,#59053,
#59054,#59055,#59056,#59057,#59058,#59059,#59060,#59061,#59062,#59063,#59064,
#59065,#59066,#59067,#59068,#59069,#59070,#59071,#59072,#59073,#59074,#59075,
#59076,#59077,#59078,#59079,#59080,#59081,#59082,#59083,#59084,#59085,#59086,
#59087,#59088,#59089,#59090,#59091,#59092,#59093,#59094,#59095,#59096,#59097,
#59098,#59099,#59100,#59101,#59102,#59103,#59104,#59105,#59106,#59107,#59108,
#59109,#59110,#59111,#59112,#59113,#59114,#59115,#59116,#59117,#59118,#59119,
#59120,#59121,#59122,#59123,#59124,#59125,#59126,#59127,#59128,#59129,#59130,
#59131,#59132,#59133,#59134,#59135,#59136,#59137,#59138,#59139,#59140,#59141,
#59142,#59143,#59144,#59145,#59146,#59147,#59148,#59149,#59150,#59151,#59152,
#59153,#59154,#59155,#59156,#59157,#59158,#59159,#59160,#59161,#59162,#59163,
#59164,#59165,#59166,#59167,#59168,#59169,#59170,#59171,#59172,#59173,#59174,
#59175,#59176,#59177,#59178,#59179,#59180,#59181,#59182,#59183,#59184,#59185,
#59186,#59187,#59188,#59189,#59190,#59191,#59192,#59193,#59194,#59195,#59196,
#59197,#59198,#59199,#59200,#59201,#59202,#59203,#59204,#59205,#59206,#59207,
#59208,#59209,#59210,#59211,#59212,#59213,#59214,#59215,#59216,#59217,#59218,
#59219,#59220,#59221,#59222,#59223,#59224,#59225,#59226,#59227,#59228,#59229,
#59230,#59231,#59232,#59233,#59234,#59235,#59236,#59237,#59238,#59239,#59240,
#59241,#59242,#59243,#59244,#59245,#59246,#59247,#59248,#59249,#59250,#59251,
#59252,#59253,#59254,#59255,#59256,#59257),.UNSPECIFIED.,.F.,.F.,(4,3,3,
3,3,3,3,3,3,3,3,3,3,3,3,3,3,3,3,3,3,3,3,3,3,3,3,3,3,3,3,3,3,3,3,3,3,3,3,
3,3,3,3,3,3,3,3,3,3,3,3,3,3,3,3,3,3,3,3,3,3,3,3,3,3,3,3,3,3,3,3,3,3,4),
(581.19464091426,581.277838919826,581.360935855946,581.443952375982,581.526909056947,
581.609834845097,581.692746992297,581.775664037574,581.858604519983,581.941634490468,
582.024714210515,582.107917376551,582.154393020567,582.238131732413,582.321767243781,
582.405319687179,582.48880912303,582.572263073644,582.65569956749,582.739136677245,
582.822592472162,582.906136964892,582.989726047833,583.073449315391,583.154129031287,
583.237867743133,583.3215032545,583.405055697899,583.48854513375,583.571999084363,
583.655435578209,583.738872687965,583.822328482882,583.905872975611,583.989462058552,
584.07318532611,584.153865042007,584.237603753853,584.321239265221,584.404791708619,
584.48828114447,584.571735095084,584.65517158893,584.738608698686,584.822064493604,
584.905608986333,584.989198069274,585.072921336832,585.153601052727,585.237339764573,
585.32097527594,585.404527719338,585.488017155189,585.571471105803,585.654907599649,
585.738344709405,585.821800504322,585.905344997052,585.988934079993,586.07265734755,
586.153337063447,586.237075775293,586.32071128666,586.404263730059,586.487753165909,
586.571207116523,586.654643610369,586.738080720125,586.821536515042,586.905081007772,
586.988670090713,587.07239335827,587.153073074167,587.227179640329),
 .UNSPECIFIED.);
#420=B_SPLINE_CURVE_WITH_KNOTS('',3,(#59258,#59259,#59260,#59261,#59262,
#59263,#59264,#59265,#59266,#59267,#59268,#59269,#59270),.UNSPECIFIED.,
 .F.,.F.,(4,3,3,3,4),(580.942974540196,581.0265880631,581.110325399057,
581.154657009846,581.194640914091),.UNSPECIFIED.);
#421=B_SPLINE_CURVE_WITH_KNOTS('',3,(#59272,#59273,#59274,#59275,#59276,
#59277,#59278,#59279,#59280,#59281),.UNSPECIFIED.,.F.,.F.,(4,3,3,4),(580.943379534668,
581.026023492215,581.110332203155,581.194640914095),.UNSPECIFIED.);
#422=B_SPLINE_CURVE_WITH_KNOTS('',3,(#59282,#59283,#59284,#59285,#59286,
#59287,#59288,#59289,#59290,#59291,#59292,#59293,#59294,#59295,#59296,#59297,
#59298,#59299,#59300,#59301,#59302,#59303,#59304,#59305,#59306,#59307,#59308,
#59309,#59310,#59311,#59312,#59313,#59314,#59315,#59316,#59317,#59318,#59319,
#59320,#59321,#59322,#59323,#59324,#59325,#59326,#59327,#59328,#59329,#59330,
#59331,#59332,#59333,#59334,#59335,#59336,#59337,#59338,#59339,#59340,#59341,
#59342,#59343,#59344,#59345,#59346,#59347,#59348,#59349,#59350,#59351,#59352,
#59353,#59354,#59355,#59356,#59357,#59358,#59359,#59360,#59361,#59362,#59363,
#59364,#59365,#59366,#59367,#59368,#59369,#59370,#59371,#59372,#59373,#59374,
#59375,#59376,#59377,#59378,#59379,#59380,#59381,#59382,#59383,#59384,#59385,
#59386,#59387,#59388,#59389,#59390,#59391,#59392,#59393,#59394,#59395,#59396,
#59397,#59398,#59399,#59400,#59401,#59402,#59403,#59404,#59405,#59406,#59407,
#59408,#59409,#59410,#59411,#59412,#59413,#59414,#59415,#59416,#59417,#59418,
#59419,#59420,#59421,#59422,#59423,#59424,#59425,#59426,#59427,#59428,#59429,
#59430,#59431,#59432,#59433,#59434,#59435,#59436,#59437,#59438,#59439,#59440,
#59441,#59442,#59443,#59444,#59445,#59446,#59447,#59448,#59449,#59450,#59451,
#59452,#59453,#59454,#59455,#59456,#59457,#59458,#59459,#59460,#59461,#59462,
#59463,#59464,#59465,#59466,#59467,#59468,#59469,#59470,#59471,#59472,#59473,
#59474,#59475,#59476,#59477,#59478,#59479,#59480,#59481,#59482,#59483,#59484,
#59485,#59486,#59487,#59488,#59489,#59490,#59491,#59492,#59493,#59494,#59495,
#59496,#59497,#59498),.UNSPECIFIED.,.F.,.F.,(4,3,3,3,3,3,3,3,3,3,3,3,3,
3,3,3,3,3,3,3,3,3,3,3,3,3,3,3,3,3,3,3,3,3,3,3,3,3,3,3,3,3,3,3,3,3,3,3,3,
3,3,3,3,3,3,3,3,3,3,3,3,3,3,3,3,3,3,3,3,3,3,3,4),(581.194640914276,581.298856363405,
581.404929115638,581.464947629562,581.548686341409,581.632321852777,581.715874296177,
581.799363732029,581.882817682644,581.966254176491,582.049691286248,582.133147081167,
582.216691573897,582.30028065684,582.384003924398,582.464683640283,582.548422352129,
582.632057863496,582.715610306895,582.799099742746,582.882553693359,582.965990187205,
583.04942729696,583.132883091878,583.216427584607,583.300016667548,583.383739935106,
583.464419651003,583.548158362849,583.631793874216,583.715346317615,583.798835753466,
583.882289704079,583.965726197925,584.04916330768,584.132619102598,584.216163595328,
584.299752678268,584.383475945826,584.464155661723,584.547894373569,584.631529884937,
584.715082328335,584.798571764186,584.8820257148,584.965462208646,585.048899318402,
585.13235511332,585.215899606049,585.29948868899,585.383211956548,585.463891672443,
585.547630384289,585.631265895656,585.714818339055,585.798307774906,585.88176172552,
585.965198219366,586.048635329122,586.13209112404,586.215635616769,586.29922469971,
586.382947967268,586.463627683163,586.547380933352,586.632229179731,586.71577284881,
586.799258681196,586.882704797921,586.968570324537,587.05200975601,587.139088330197,
587.226166904384),.UNSPECIFIED.);
#423=B_SPLINE_CURVE_WITH_KNOTS('',3,(#59504,#59505,#59506,#59507,#59508,
#59509,#59510,#59511,#59512,#59513,#59514,#59515,#59516,#59517,#59518,#59519,
#59520,#59521,#59522,#59523,#59524,#59525,#59526,#59527,#59528,#59529,#59530,
#59531,#59532,#59533,#59534,#59535,#59536,#59537,#59538,#59539,#59540,#59541,
#59542,#59543,#59544,#59545,#59546,#59547,#59548,#59549,#59550,#59551,#59552,
#59553,#59554,#59555,#59556,#59557,#59558,#59559,#59560,#59561,#59562,#59563,
#59564,#59565,#59566,#59567,#59568,#59569,#59570,#59571,#59572,#59573,#59574,
#59575,#59576,#59577,#59578,#59579,#59580,#59581,#59582,#59583,#59584,#59585,
#59586,#59587,#59588,#59589,#59590,#59591,#59592,#59593,#59594,#59595,#59596,
#59597,#59598,#59599,#59600,#59601,#59602,#59603,#59604,#59605,#59606,#59607,
#59608,#59609,#59610,#59611,#59612,#59613,#59614,#59615,#59616,#59617,#59618,
#59619,#59620,#59621,#59622,#59623,#59624,#59625,#59626,#59627,#59628,#59629,
#59630,#59631,#59632,#59633,#59634,#59635,#59636,#59637,#59638,#59639,#59640,
#59641,#59642,#59643,#59644,#59645,#59646,#59647,#59648,#59649,#59650,#59651,
#59652,#59653,#59654,#59655,#59656,#59657,#59658,#59659,#59660,#59661,#59662,
#59663,#59664,#59665,#59666,#59667,#59668,#59669,#59670,#59671,#59672,#59673,
#59674,#59675,#59676,#59677,#59678,#59679,#59680,#59681,#59682,#59683,#59684,
#59685,#59686,#59687,#59688,#59689,#59690,#59691,#59692,#59693,#59694,#59695,
#59696,#59697,#59698,#59699,#59700,#59701,#59702,#59703,#59704,#59705,#59706,
#59707,#59708,#59709,#59710,#59711,#59712,#59713,#59714,#59715,#59716,#59717,
#59718,#59719,#59720,#59721,#59722,#59723),.UNSPECIFIED.,.F.,.F.,(4,3,3,
3,3,3,3,3,3,3,3,3,3,3,3,3,3,3,3,3,3,3,3,3,3,3,3,3,3,3,3,3,3,3,3,3,3,3,3,
3,3,3,3,3,3,3,3,3,3,3,3,3,3,3,3,3,3,3,3,3,3,3,3,3,3,3,3,3,3,3,3,3,3,4),
(587.477826221271,587.562199079223,587.645452312285,587.728706820588,587.811980792074,
587.897187865277,587.98060108407,588.066705084478,588.152809084887,588.236547796733,
588.320183308101,588.403735751499,588.48722518735,588.570679137964,588.65411563181,
588.737552741565,588.821008536483,588.904553029213,588.988142112154,589.071865379711,
589.152545095607,589.236283807453,589.319919318821,589.40347176222,589.486961198071,
589.570415148684,589.653851642531,589.737288752287,589.820744547204,589.904289039934,
589.987878122875,590.071601390433,590.152281106328,590.236019818174,590.319655329541,
590.40320777294,590.486697208792,590.570151159405,590.653587653252,590.737024763007,
590.820480557925,590.904025050655,590.987614133596,591.071337401153,591.152017117048,
591.235755828894,591.319391340261,591.40294378366,591.48643321951,591.569887170124,
591.65332366397,591.736760773726,591.820216568643,591.903761061373,591.987350144314,
592.071073411871,592.151753127768,592.235491839614,592.319127350981,592.40267979438,
592.486169230231,592.569623180845,592.653059674691,592.736496784446,592.819952579364,
592.903497072094,592.987086155035,593.070809422592,593.151489138488,593.236274655599,
593.320912891502,593.405465494156,593.489932211694,593.510351022852),
 .UNSPECIFIED.);
#424=B_SPLINE_CURVE_WITH_KNOTS('',3,(#59724,#59725,#59726,#59727,#59728,
#59729,#59730,#59731,#59732,#59733),.UNSPECIFIED.,.F.,.F.,(4,3,3,4),(587.227179640329,
587.32609710812,587.424072733153,587.477826221091),.UNSPECIFIED.);
#425=B_SPLINE_CURVE_WITH_KNOTS('',3,(#59735,#59736,#59737,#59738,#59739,
#59740,#59741,#59742,#59743,#59744,#59745,#59746,#59747),.UNSPECIFIED.,
 .F.,.F.,(4,3,3,3,4),(587.226166904384,587.309762933416,587.393489989296,
587.463363693883,587.477826221275),.UNSPECIFIED.);
#426=B_SPLINE_CURVE_WITH_KNOTS('',3,(#59748,#59749,#59750,#59751,#59752,
#59753,#59754,#59755,#59756,#59757,#59758,#59759,#59760,#59761,#59762,#59763,
#59764,#59765,#59766,#59767,#59768,#59769,#59770,#59771,#59772,#59773,#59774,
#59775,#59776,#59777,#59778,#59779,#59780,#59781,#59782,#59783,#59784,#59785,
#59786,#59787,#59788,#59789,#59790,#59791,#59792,#59793,#59794,#59795,#59796,
#59797,#59798,#59799,#59800,#59801,#59802,#59803,#59804,#59805,#59806,#59807,
#59808,#59809,#59810,#59811,#59812,#59813,#59814,#59815,#59816,#59817,#59818,
#59819,#59820,#59821,#59822,#59823,#59824,#59825,#59826,#59827,#59828,#59829,
#59830,#59831,#59832,#59833,#59834,#59835,#59836,#59837,#59838,#59839,#59840,
#59841,#59842,#59843,#59844,#59845,#59846,#59847,#59848,#59849,#59850,#59851,
#59852,#59853,#59854,#59855,#59856,#59857,#59858,#59859,#59860,#59861,#59862,
#59863,#59864,#59865,#59866,#59867,#59868,#59869,#59870,#59871,#59872,#59873,
#59874,#59875,#59876,#59877,#59878,#59879,#59880,#59881,#59882,#59883,#59884,
#59885,#59886,#59887,#59888,#59889,#59890,#59891,#59892,#59893,#59894,#59895,
#59896,#59897,#59898,#59899,#59900,#59901,#59902,#59903,#59904,#59905,#59906,
#59907,#59908,#59909,#59910,#59911,#59912,#59913,#59914,#59915,#59916,#59917,
#59918,#59919,#59920,#59921,#59922,#59923,#59924,#59925,#59926,#59927,#59928,
#59929,#59930,#59931,#59932,#59933,#59934,#59935,#59936,#59937,#59938,#59939,
#59940,#59941,#59942,#59943,#59944,#59945,#59946,#59947,#59948,#59949,#59950,
#59951,#59952,#59953,#59954,#59955,#59956,#59957,#59958,#59959,#59960,#59961,
#59962,#59963,#59964,#59965,#59966,#59967),.UNSPECIFIED.,.F.,.F.,(4,3,3,
3,3,3,3,3,3,3,3,3,3,3,3,3,3,3,3,3,3,3,3,3,3,3,3,3,3,3,3,3,3,3,3,3,3,3,3,
3,3,3,3,3,3,3,3,3,3,3,3,3,3,3,3,3,3,3,3,3,3,3,3,3,3,3,3,3,3,3,3,3,3,4),
(587.477826221412,587.56135346668,587.644777878487,587.728119809374,587.81139953815,
587.894645039578,587.977874217614,588.061105341191,588.14435667684,588.227696868397,
588.311083396933,588.394600209494,588.463099704603,588.546838416449,588.630473927817,
588.714026371216,588.797515807067,588.880969757681,588.964406251527,589.047843361283,
589.131299156201,589.214843648931,589.298432731872,589.38215599943,589.462835715324,
589.54657442717,589.630209938538,589.713762381936,589.797251817787,589.880705768401,
589.964142262248,590.047579372003,590.131035166921,590.214579659651,590.298168742592,
590.38189201015,590.462571726044,590.54631043789,590.629945949257,590.713498392655,
590.796987828507,590.88044177912,590.963878272966,591.047315382721,591.130771177639,
591.214315670369,591.297904753309,591.381628020867,591.462307736764,591.54604644861,
591.629681959978,591.713234403376,591.796723839227,591.880177789841,591.963614283687,
592.047051393443,592.130507188361,592.21405168109,592.297640764032,592.381364031589,
592.462043747484,592.54578245933,592.629417970697,592.712970414096,592.796459849947,
592.879913800561,592.963350294408,593.046787404163,593.130243199081,593.21378769181,
593.297376774751,593.381100042309,593.461779758204,593.510232699841),
 .UNSPECIFIED.);
#427=B_SPLINE_CURVE_WITH_KNOTS('',3,(#59973,#59974,#59975,#59976,#59977,
#59978,#59979,#59980,#59981,#59982,#59983,#59984,#59985,#59986,#59987,#59988,
#59989,#59990,#59991,#59992,#59993,#59994,#59995,#59996,#59997,#59998,#59999,
#60000,#60001,#60002,#60003,#60004,#60005,#60006,#60007,#60008,#60009,#60010,
#60011,#60012,#60013,#60014,#60015,#60016,#60017,#60018,#60019,#60020,#60021,
#60022,#60023,#60024,#60025,#60026,#60027,#60028,#60029,#60030,#60031,#60032,
#60033,#60034,#60035,#60036,#60037,#60038,#60039,#60040,#60041,#60042,#60043,
#60044,#60045,#60046,#60047,#60048,#60049,#60050,#60051,#60052,#60053,#60054,
#60055,#60056,#60057,#60058,#60059,#60060,#60061,#60062,#60063,#60064,#60065,
#60066,#60067,#60068,#60069,#60070,#60071,#60072,#60073,#60074,#60075,#60076,
#60077,#60078,#60079,#60080,#60081,#60082,#60083,#60084,#60085,#60086,#60087,
#60088,#60089,#60090,#60091,#60092,#60093,#60094,#60095,#60096,#60097,#60098,
#60099,#60100,#60101,#60102,#60103,#60104,#60105,#60106,#60107,#60108,#60109,
#60110,#60111,#60112,#60113,#60114,#60115,#60116,#60117,#60118,#60119,#60120,
#60121,#60122,#60123,#60124,#60125,#60126,#60127,#60128,#60129,#60130,#60131,
#60132,#60133,#60134,#60135,#60136,#60137,#60138,#60139,#60140,#60141,#60142,
#60143,#60144,#60145,#60146,#60147,#60148,#60149,#60150,#60151,#60152,#60153,
#60154,#60155,#60156,#60157,#60158,#60159,#60160,#60161,#60162,#60163,#60164,
#60165,#60166,#60167,#60168,#60169,#60170,#60171,#60172,#60173,#60174,#60175,
#60176,#60177,#60178,#60179,#60180,#60181,#60182,#60183,#60184,#60185,#60186,
#60187,#60188,#60189,#60190,#60191,#60192),.UNSPECIFIED.,.F.,.F.,(4,3,3,
3,3,3,3,3,3,3,3,3,3,3,3,3,3,3,3,3,3,3,3,3,3,3,3,3,3,3,3,3,3,3,3,3,3,3,3,
3,3,3,3,3,3,3,3,3,3,3,3,3,3,3,3,3,3,3,3,3,3,3,3,3,3,3,3,3,3,3,3,3,3,4),
(593.761011528636,593.858564933779,593.951805410787,594.045325295478,594.139187343676,
594.151225149208,594.234963861054,594.318599372422,594.40215181582,594.485641251671,
594.569095202285,594.652531696131,594.735968805886,594.819424600804,594.902969093533,
594.986558176474,595.070281444032,595.150961159928,595.234699871774,595.318335383141,
595.40188782654,595.485377262391,595.568831213004,595.65226770685,595.735704816606,
595.819160611524,595.902705104253,595.986294187194,596.070017454752,596.150697170648,
596.234435882494,596.318071393861,596.40162383726,596.485113273111,596.568567223725,
596.652003717571,596.735440827327,596.818896622245,596.902441114974,596.986030197915,
597.069753465473,597.150433181368,597.234171893214,597.317807404581,597.40135984798,
597.484849283831,597.568303234445,597.651739728291,597.735176838047,597.818632632964,
597.902177125694,597.985766208635,598.069489476193,598.150169192089,598.233907903935,
598.317543415303,598.401095858701,598.484585294552,598.568039245166,598.651475739012,
598.734912848768,598.818368643686,598.901913136415,598.985502219356,599.069225486914,
599.149905202809,599.232544928932,599.315090063073,599.397559707556,599.479972895729,
599.562358158123,599.644725126391,599.727119391754,599.792366874018),
 .UNSPECIFIED.);
#428=B_SPLINE_CURVE_WITH_KNOTS('',3,(#60193,#60194,#60195,#60196,#60197,
#60198,#60199,#60200,#60201,#60202),.UNSPECIFIED.,.F.,.F.,(4,3,3,4),(593.510351022852,
593.594743727506,593.679109853501,593.76101152845),.UNSPECIFIED.);
#429=B_SPLINE_CURVE_WITH_KNOTS('',3,(#60204,#60205,#60206,#60207,#60208,
#60209,#60210,#60211,#60212,#60213),.UNSPECIFIED.,.F.,.F.,(4,3,3,4),(593.510232699841,
593.612124172686,593.712757557617,593.761011528308),.UNSPECIFIED.);
#430=B_SPLINE_CURVE_WITH_KNOTS('',3,(#60214,#60215,#60216,#60217,#60218,
#60219,#60220,#60221,#60222,#60223,#60224,#60225,#60226,#60227,#60228,#60229,
#60230,#60231,#60232,#60233,#60234,#60235,#60236,#60237,#60238,#60239,#60240,
#60241,#60242,#60243,#60244,#60245,#60246,#60247,#60248,#60249,#60250,#60251,
#60252,#60253,#60254,#60255,#60256,#60257,#60258,#60259,#60260,#60261,#60262,
#60263,#60264,#60265,#60266,#60267,#60268,#60269,#60270,#60271,#60272,#60273,
#60274,#60275,#60276,#60277,#60278,#60279,#60280,#60281,#60282,#60283,#60284,
#60285,#60286,#60287,#60288,#60289,#60290,#60291,#60292,#60293,#60294,#60295,
#60296,#60297,#60298,#60299,#60300,#60301,#60302,#60303,#60304,#60305,#60306,
#60307,#60308,#60309,#60310,#60311,#60312,#60313,#60314,#60315,#60316,#60317,
#60318,#60319,#60320,#60321,#60322,#60323,#60324,#60325,#60326,#60327,#60328,
#60329,#60330,#60331,#60332,#60333,#60334,#60335,#60336,#60337,#60338,#60339,
#60340,#60341,#60342,#60343,#60344,#60345,#60346,#60347,#60348,#60349,#60350,
#60351,#60352,#60353,#60354,#60355,#60356,#60357,#60358,#60359,#60360,#60361,
#60362,#60363,#60364,#60365,#60366,#60367,#60368,#60369,#60370,#60371,#60372,
#60373,#60374,#60375,#60376,#60377,#60378,#60379,#60380,#60381,#60382,#60383,
#60384,#60385,#60386,#60387,#60388,#60389,#60390,#60391,#60392,#60393,#60394,
#60395,#60396,#60397,#60398,#60399,#60400,#60401,#60402,#60403,#60404,#60405,
#60406,#60407,#60408,#60409,#60410,#60411,#60412,#60413,#60414,#60415,#60416,
#60417,#60418,#60419,#60420,#60421,#60422,#60423,#60424,#60425,#60426,#60427,
#60428,#60429,#60430,#60431,#60432,#60433),.UNSPECIFIED.,.F.,.F.,(4,3,3,
3,3,3,3,3,3,3,3,3,3,3,3,3,3,3,3,3,3,3,3,3,3,3,3,3,3,3,3,3,3,3,3,3,3,3,3,
3,3,3,3,3,3,3,3,3,3,3,3,3,3,3,3,3,3,3,3,3,3,3,3,3,3,3,3,3,3,3,3,3,3,4),
(593.761011528454,593.843975061803,593.926914752704,594.009845422425,594.09278556456,
594.175753675864,594.258815591675,594.341931170951,594.425170135204,594.461515768924,
594.54525448077,594.628889992137,594.712442435536,594.795931871387,594.879385822,
594.962822315846,595.046259425602,595.129715220519,595.213259713249,595.29684879619,
595.380572063748,595.461251779644,595.54499049149,595.628626002857,595.712178446256,
595.795667882107,595.879121832721,595.962558326567,596.045995436323,596.129451231241,
596.21299572397,596.296584806911,596.380308074469,596.460987790364,596.54472650221,
596.628362013578,596.711914456976,596.795403892827,596.878857843441,596.962294337287,
597.045731447042,597.12918724196,597.21273173469,597.296320817631,597.380044085189,
597.460723801085,597.544462512931,597.628098024298,597.711650467697,597.795139903548,
597.878593854162,597.962030348008,598.045467457764,598.128923252681,598.212467745411,
598.296056828352,598.37978009591,598.460459811805,598.544198523651,598.627834035018,
598.711386478417,598.794875914268,598.878329864882,598.961766358728,599.045203468484,
599.128659263401,599.212203756131,599.295792839072,599.379516106629,599.460195822525,
599.545543916236,599.630786228184,599.715907753929,599.793641905039),
 .UNSPECIFIED.);
#431=B_SPLINE_CURVE_WITH_KNOTS('',3,(#60439,#60440,#60441,#60442,#60443,
#60444,#60445,#60446,#60447,#60448,#60449,#60450,#60451,#60452,#60453,#60454,
#60455,#60456,#60457,#60458,#60459,#60460,#60461,#60462,#60463,#60464,#60465,
#60466,#60467,#60468,#60469,#60470,#60471,#60472,#60473,#60474,#60475,#60476,
#60477,#60478,#60479,#60480,#60481,#60482,#60483,#60484,#60485,#60486,#60487,
#60488,#60489,#60490,#60491,#60492,#60493,#60494,#60495,#60496,#60497,#60498,
#60499,#60500,#60501,#60502,#60503,#60504,#60505,#60506,#60507,#60508,#60509,
#60510,#60511,#60512,#60513,#60514,#60515,#60516,#60517,#60518,#60519,#60520,
#60521,#60522,#60523,#60524,#60525,#60526,#60527,#60528,#60529,#60530,#60531,
#60532,#60533,#60534,#60535,#60536,#60537,#60538,#60539,#60540,#60541,#60542,
#60543,#60544,#60545,#60546,#60547,#60548,#60549,#60550,#60551,#60552,#60553,
#60554,#60555,#60556,#60557,#60558,#60559,#60560,#60561,#60562,#60563,#60564,
#60565,#60566,#60567,#60568,#60569,#60570,#60571,#60572,#60573,#60574,#60575,
#60576,#60577,#60578,#60579,#60580,#60581,#60582,#60583,#60584,#60585,#60586,
#60587,#60588,#60589,#60590,#60591,#60592,#60593,#60594,#60595,#60596,#60597,
#60598,#60599,#60600,#60601,#60602,#60603,#60604,#60605,#60606,#60607,#60608,
#60609,#60610,#60611,#60612,#60613,#60614,#60615,#60616,#60617,#60618,#60619,
#60620,#60621,#60622,#60623,#60624,#60625,#60626,#60627,#60628,#60629,#60630,
#60631,#60632,#60633,#60634,#60635,#60636,#60637,#60638,#60639,#60640,#60641,
#60642,#60643,#60644,#60645,#60646,#60647,#60648,#60649,#60650,#60651,#60652,
#60653,#60654,#60655),.UNSPECIFIED.,.F.,.F.,(4,3,3,3,3,3,3,3,3,3,3,3,3,
3,3,3,3,3,3,3,3,3,3,3,3,3,3,3,3,3,3,3,3,3,3,3,3,3,3,3,3,3,3,3,3,3,3,3,3,
3,3,3,3,3,3,3,3,3,3,3,3,3,3,3,3,3,3,3,3,3,3,3,4),(600.04419683563,600.149641213529,
600.233379925375,600.317015436743,600.400567880141,600.484057315992,600.567511266605,
600.650947760452,600.734384870207,600.817840665125,600.901385157854,600.984974240795,
601.068697508353,601.149377224249,601.233115936095,601.316751447462,601.400303890861,
601.483793326712,601.567247277326,601.650683771172,601.734120880928,601.817576675845,
601.901121168575,601.984710251516,602.068433519073,602.149113234969,602.232851946815,
602.316487458182,602.400039901581,602.483529337432,602.566983288045,602.650419781892,
602.733856891647,602.817312686564,602.900857179294,602.984446262235,603.068169529793,
603.148849245689,603.232587957535,603.316223468903,603.399775912301,603.483265348152,
603.566719298766,603.650155792612,603.733592902368,603.817048697286,603.900593190015,
603.984182272956,604.067905540514,604.148585256409,604.232323968255,604.315959479622,
604.399511923021,604.483001358872,604.566455309486,604.649891803332,604.733328913088,
604.816784708005,604.900329200735,604.983918283676,605.067641551234,605.14832126713,
605.232064132401,605.315702846202,605.399257545084,605.483845242438,605.567295515047,
605.650727224079,605.734158441295,605.81960861195,605.903129443405,605.98954428366,
606.075959123915),.UNSPECIFIED.);
#432=B_SPLINE_CURVE_WITH_KNOTS('',3,(#60656,#60657,#60658,#60659,#60660,
#60661,#60662,#60663,#60664,#60665),.UNSPECIFIED.,.F.,.F.,(4,3,3,4),(599.792366874018,
599.874835106843,599.959515971168,600.044196835494),.UNSPECIFIED.);
#433=B_SPLINE_CURVE_WITH_KNOTS('',3,(#60667,#60668,#60669,#60670,#60671,
#60672,#60673,#60674,#60675,#60676),.UNSPECIFIED.,.F.,.F.,(4,3,3,4),(599.793641905039,
599.878621649841,599.963550940226,600.044196835634),.UNSPECIFIED.);
#434=B_SPLINE_CURVE_WITH_KNOTS('',3,(#60677,#60678,#60679,#60680,#60681,
#60682,#60683,#60684,#60685,#60686,#60687,#60688,#60689,#60690,#60691,#60692,
#60693,#60694,#60695,#60696,#60697,#60698,#60699,#60700,#60701,#60702,#60703,
#60704,#60705,#60706,#60707,#60708,#60709,#60710,#60711,#60712,#60713,#60714,
#60715,#60716,#60717,#60718,#60719,#60720,#60721,#60722,#60723,#60724,#60725,
#60726,#60727,#60728,#60729,#60730,#60731,#60732,#60733,#60734,#60735,#60736,
#60737,#60738,#60739,#60740,#60741,#60742,#60743,#60744,#60745,#60746,#60747,
#60748,#60749,#60750,#60751,#60752,#60753,#60754,#60755,#60756,#60757,#60758,
#60759,#60760,#60761,#60762,#60763,#60764,#60765,#60766,#60767,#60768,#60769,
#60770,#60771,#60772,#60773,#60774,#60775,#60776,#60777,#60778,#60779,#60780,
#60781,#60782,#60783,#60784,#60785,#60786,#60787,#60788,#60789,#60790,#60791,
#60792,#60793,#60794,#60795,#60796,#60797,#60798,#60799,#60800,#60801,#60802,
#60803,#60804,#60805,#60806,#60807,#60808,#60809,#60810,#60811,#60812,#60813,
#60814,#60815,#60816,#60817,#60818,#60819,#60820,#60821,#60822,#60823,#60824,
#60825,#60826,#60827,#60828,#60829,#60830,#60831,#60832,#60833,#60834,#60835,
#60836,#60837,#60838,#60839,#60840,#60841,#60842,#60843,#60844,#60845,#60846,
#60847,#60848,#60849,#60850,#60851,#60852,#60853,#60854,#60855,#60856,#60857,
#60858,#60859,#60860,#60861,#60862,#60863,#60864,#60865,#60866,#60867,#60868,
#60869,#60870,#60871,#60872,#60873,#60874,#60875,#60876,#60877,#60878,#60879,
#60880,#60881,#60882,#60883,#60884,#60885,#60886,#60887,#60888,#60889,#60890,
#60891,#60892,#60893,#60894,#60895,#60896),.UNSPECIFIED.,.F.,.F.,(4,3,3,
3,3,3,3,3,3,3,3,3,3,3,3,3,3,3,3,3,3,3,3,3,3,3,3,3,3,3,3,3,3,3,3,3,3,3,3,
3,3,3,3,3,3,3,3,3,3,3,3,3,3,3,3,3,3,3,3,3,3,3,3,3,3,3,3,3,3,3,3,3,3,4),
(600.044196835797,600.135380747604,600.226996847853,600.31883428202,600.410988212238,
600.459931833245,600.543670545091,600.627306056459,600.710858499857,600.794347935708,
600.877801886322,600.961238380168,601.044675489923,601.128131284841,601.211675777571,
601.295264860512,601.378988128069,601.459667843965,601.543406555811,601.627042067178,
601.710594510577,601.794083946428,601.877537897041,601.960974390888,602.044411500643,
602.127867295561,602.21141178829,602.295000871231,602.378724138789,602.459403854685,
602.543142566531,602.626778077898,602.710330521297,602.793819957148,602.877273907761,
602.960710401608,603.044147511363,603.127603306281,603.211147799011,603.294736881952,
603.378460149509,603.459139865405,603.542878577251,603.626514088618,603.710066532017,
603.793555967868,603.877009918482,603.960446412328,604.043883522084,604.127339317002,
604.210883809731,604.294472892672,604.37819616023,604.458875876125,604.542614587971,
604.626250099339,604.709802542737,604.793291978588,604.876745929202,604.960182423048,
605.043619532804,605.127075327721,605.210619820451,605.294208903392,605.37793217095,
605.458611886846,605.54114153622,605.623576417017,605.705935706753,605.788238511302,
605.870511003234,605.952765504759,606.03503976382,606.075586485893),
 .UNSPECIFIED.);
#435=B_SPLINE_CURVE_WITH_KNOTS('',3,(#60902,#60903,#60904,#60905,#60906,
#60907,#60908,#60909,#60910,#60911,#60912,#60913,#60914,#60915,#60916,#60917,
#60918,#60919,#60920,#60921,#60922,#60923,#60924,#60925,#60926,#60927,#60928,
#60929,#60930,#60931,#60932,#60933,#60934,#60935,#60936,#60937,#60938,#60939,
#60940,#60941,#60942,#60943,#60944,#60945,#60946,#60947,#60948,#60949,#60950,
#60951,#60952,#60953,#60954,#60955,#60956,#60957,#60958,#60959,#60960,#60961,
#60962,#60963,#60964,#60965,#60966,#60967,#60968,#60969,#60970,#60971,#60972,
#60973,#60974,#60975,#60976,#60977,#60978,#60979,#60980,#60981,#60982,#60983,
#60984,#60985,#60986,#60987,#60988,#60989,#60990,#60991,#60992,#60993,#60994,
#60995,#60996,#60997,#60998,#60999,#61000,#61001,#61002,#61003,#61004,#61005,
#61006,#61007,#61008,#61009,#61010,#61011,#61012,#61013,#61014,#61015,#61016,
#61017,#61018,#61019,#61020,#61021,#61022,#61023,#61024,#61025,#61026,#61027,
#61028,#61029,#61030,#61031,#61032,#61033,#61034,#61035,#61036,#61037,#61038,
#61039,#61040,#61041,#61042,#61043,#61044,#61045,#61046,#61047,#61048,#61049,
#61050,#61051,#61052,#61053,#61054,#61055,#61056,#61057,#61058,#61059,#61060,
#61061,#61062,#61063,#61064,#61065,#61066,#61067,#61068,#61069,#61070,#61071,
#61072,#61073,#61074,#61075,#61076,#61077,#61078,#61079,#61080,#61081,#61082,
#61083,#61084,#61085,#61086,#61087,#61088,#61089,#61090,#61091,#61092,#61093,
#61094,#61095,#61096,#61097,#61098,#61099,#61100,#61101,#61102,#61103,#61104,
#61105,#61106,#61107,#61108,#61109,#61110,#61111,#61112,#61113,#61114,#61115,
#61116,#61117,#61118,#61119,#61120,#61121),.UNSPECIFIED.,.F.,.F.,(4,3,3,
3,3,3,3,3,3,3,3,3,3,3,3,3,3,3,3,3,3,3,3,3,3,3,3,3,3,3,3,3,3,3,3,3,3,3,3,
3,3,3,3,3,3,3,3,3,3,3,3,3,3,3,3,3,3,3,3,3,3,3,3,3,3,3,3,3,3,3,3,3,3,4),
(606.327382142967,606.409745330699,606.49203379855,606.574272133103,606.65648437151,
606.738689552527,606.820906706931,606.903205201195,606.985544079707,607.068013508093,
607.14779328857,607.231532000416,607.315167511784,607.398719955182,607.482209391033,
607.565663341647,607.649099835493,607.732536945249,607.815992740166,607.899537232896,
607.983126315837,608.066849583395,608.14752929929,608.231268011136,608.314903522503,
608.398455965902,608.481945401753,608.565399352367,608.648835846213,608.732272955968,
608.815728750886,608.899273243616,608.982862326557,609.066585594114,609.14726531001,
609.231004021856,609.314639533223,609.398191976622,609.481681412473,609.565135363087,
609.648571856933,609.732008966689,609.815464761606,609.899009254336,609.982598337277,
610.066321604835,610.14700132073,610.230740032576,610.314375543943,610.397927987342,
610.481417423193,610.564871373807,610.648307867653,610.731744977409,610.815200772326,
610.898745265056,610.982334347997,611.066057615554,611.14673733145,611.230476043296,
611.314111554663,611.397663998062,611.481153433913,611.564607384527,611.648043878373,
611.731480988128,611.814936783046,611.898481275776,611.982070358717,612.065793626274,
612.14647334217,612.236085107274,612.325478113949,612.360266019021),
 .UNSPECIFIED.);
#436=B_SPLINE_CURVE_WITH_KNOTS('',3,(#61122,#61123,#61124,#61125,#61126,
#61127,#61128,#61129,#61130,#61131),.UNSPECIFIED.,.F.,.F.,(4,3,3,4),(606.075959123915,
606.14805727785,606.275526789432,606.327382142809),.UNSPECIFIED.);
#437=B_SPLINE_CURVE_WITH_KNOTS('',3,(#61133,#61134,#61135,#61136,#61137,
#61138,#61139,#61140,#61141,#61142),.UNSPECIFIED.,.F.,.F.,(4,3,3,4),(606.075586485893,
606.157928330959,606.242655236822,606.327382142685),.UNSPECIFIED.);
#438=B_SPLINE_CURVE_WITH_KNOTS('',3,(#61143,#61144,#61145,#61146,#61147,
#61148,#61149,#61150,#61151,#61152,#61153,#61154,#61155,#61156,#61157,#61158,
#61159,#61160,#61161,#61162,#61163,#61164,#61165,#61166,#61167,#61168,#61169,
#61170,#61171,#61172,#61173,#61174,#61175,#61176,#61177,#61178,#61179,#61180,
#61181,#61182,#61183,#61184,#61185,#61186,#61187,#61188,#61189,#61190,#61191,
#61192,#61193,#61194,#61195,#61196,#61197,#61198,#61199,#61200,#61201,#61202,
#61203,#61204,#61205,#61206,#61207,#61208,#61209,#61210,#61211,#61212,#61213,
#61214,#61215,#61216,#61217,#61218,#61219,#61220,#61221,#61222,#61223,#61224,
#61225,#61226,#61227,#61228,#61229,#61230,#61231,#61232,#61233,#61234,#61235,
#61236,#61237,#61238,#61239,#61240,#61241,#61242,#61243,#61244,#61245,#61246,
#61247,#61248,#61249,#61250,#61251,#61252,#61253,#61254,#61255,#61256,#61257,
#61258,#61259,#61260,#61261,#61262,#61263,#61264,#61265,#61266,#61267,#61268,
#61269,#61270,#61271,#61272,#61273,#61274,#61275,#61276,#61277,#61278,#61279,
#61280,#61281,#61282,#61283,#61284,#61285,#61286,#61287,#61288,#61289,#61290,
#61291,#61292,#61293,#61294,#61295,#61296,#61297,#61298,#61299,#61300,#61301,
#61302,#61303,#61304,#61305,#61306,#61307,#61308,#61309,#61310,#61311,#61312,
#61313,#61314,#61315,#61316,#61317,#61318,#61319,#61320,#61321,#61322,#61323,
#61324,#61325,#61326,#61327,#61328,#61329,#61330,#61331,#61332,#61333,#61334,
#61335,#61336,#61337,#61338,#61339,#61340,#61341,#61342,#61343,#61344,#61345,
#61346,#61347,#61348,#61349,#61350,#61351,#61352,#61353,#61354,#61355,#61356,
#61357,#61358,#61359),.UNSPECIFIED.,.F.,.F.,(4,3,3,3,3,3,3,3,3,3,3,3,3,
3,3,3,3,3,3,3,3,3,3,3,3,3,3,3,3,3,3,3,3,3,3,3,3,3,3,3,3,3,3,3,3,3,3,3,3,
3,3,3,3,3,3,3,3,3,3,3,3,3,3,3,3,3,3,3,3,3,3,3,4),(606.327382142813,606.458347897566,
606.542086609412,606.62572212078,606.709274564178,606.792764000029,606.876217950643,
606.959654444489,607.043091554244,607.126547349162,607.210091841892,607.293680924833,
607.37740419239,607.458083908286,607.541822620132,607.625458131499,607.709010574898,
607.792500010749,607.875953961362,607.959390455209,608.042827564964,608.126283359882,
608.209827852611,608.293416935552,608.37714020311,608.457819919006,608.541558630852,
608.62519414222,608.708746585618,608.792236021469,608.875689972083,608.959126465929,
609.042563575685,609.126019370602,609.209563863332,609.293152946273,609.376876213831,
609.457555929726,609.541294641572,609.624930152939,609.708482596338,609.791972032189,
609.875425982802,609.958862476649,610.042299586404,610.125755381321,610.209299874051,
610.292888956992,610.376612224549,610.457291940446,610.541030652292,610.62466616366,
610.708218607058,610.791708042909,610.875161993523,610.958598487369,611.042035597125,
611.125491392042,611.209035884772,611.292624967713,611.376348235271,611.457027951166,
611.540772347434,611.624412254421,611.707967810137,611.791454863418,611.874904548639,
611.958334954268,612.041764152013,612.125248052861,612.208759568125,612.292369613153,
612.359058987781),.UNSPECIFIED.);
#439=B_SPLINE_CURVE_WITH_KNOTS('',3,(#61365,#61366,#61367,#61368,#61369,
#61370,#61371,#61372,#61373,#61374,#61375,#61376,#61377,#61378,#61379,#61380,
#61381,#61382,#61383,#61384,#61385,#61386,#61387,#61388,#61389,#61390,#61391,
#61392,#61393,#61394,#61395,#61396,#61397,#61398,#61399,#61400,#61401,#61402,
#61403,#61404,#61405,#61406,#61407,#61408,#61409,#61410,#61411,#61412,#61413,
#61414,#61415,#61416,#61417,#61418,#61419,#61420,#61421,#61422,#61423,#61424,
#61425,#61426,#61427,#61428,#61429,#61430,#61431,#61432,#61433,#61434,#61435,
#61436,#61437,#61438,#61439,#61440,#61441,#61442,#61443,#61444,#61445,#61446,
#61447,#61448,#61449,#61450,#61451,#61452,#61453,#61454,#61455,#61456,#61457,
#61458,#61459,#61460,#61461,#61462,#61463,#61464,#61465,#61466,#61467,#61468,
#61469,#61470,#61471,#61472,#61473,#61474,#61475,#61476,#61477,#61478,#61479,
#61480,#61481,#61482,#61483,#61484,#61485,#61486,#61487,#61488,#61489,#61490,
#61491,#61492,#61493,#61494,#61495,#61496,#61497,#61498,#61499,#61500,#61501,
#61502,#61503,#61504,#61505,#61506,#61507,#61508,#61509,#61510,#61511,#61512,
#61513,#61514,#61515,#61516,#61517,#61518,#61519,#61520,#61521,#61522,#61523,
#61524,#61525,#61526,#61527,#61528,#61529,#61530,#61531,#61532,#61533,#61534,
#61535,#61536,#61537,#61538,#61539,#61540,#61541,#61542,#61543,#61544,#61545,
#61546,#61547,#61548,#61549,#61550,#61551,#61552,#61553,#61554,#61555,#61556,
#61557,#61558,#61559,#61560,#61561,#61562,#61563,#61564,#61565,#61566,#61567,
#61568,#61569,#61570,#61571,#61572,#61573,#61574,#61575,#61576,#61577,#61578,
#61579,#61580,#61581,#61582,#61583,#61584),.UNSPECIFIED.,.F.,.F.,(4,3,3,
3,3,3,3,3,3,3,3,3,3,3,3,3,3,3,3,3,3,3,3,3,3,3,3,3,3,3,3,3,3,3,3,3,3,3,3,
3,3,3,3,3,3,3,3,3,3,3,3,3,3,3,3,3,3,3,3,3,3,3,3,3,3,3,3,3,3,3,3,3,3,4),
(612.610567449989,612.696783698912,612.783073618945,612.873857552431,612.960398441322,
613.047032929598,613.133823015052,613.146209352891,613.229948064737,613.313583576104,
613.397136019502,613.480625455353,613.564079405967,613.647515899813,613.730953009568,
613.814408804486,613.897953297216,613.981542380156,614.065265647714,614.145945363611,
614.229684075457,614.313319586824,614.396872030223,614.480361466074,614.563815416687,
614.647251910534,614.730689020289,614.814144815207,614.897689307937,614.981278390877,
615.065001658435,615.145681374331,615.229420086177,615.313055597545,615.396608040944,
615.480097476794,615.563551427408,615.646987921254,615.73042503101,615.813880825928,
615.897425318657,615.981014401598,616.064737669156,616.145417385051,616.229156096897,
616.312791608264,616.396344051663,616.479833487514,616.563287438128,616.646723931974,
616.730161041729,616.813616836646,616.897161329376,616.980750412317,617.064473679875,
617.145153395771,617.228892107617,617.312527618985,617.396080062383,617.479569498234,
617.563023448848,617.646459942694,617.729897052449,617.813352847367,617.896897340096,
617.980486423037,618.064209690595,618.144889406491,618.227663227904,618.310338741592,
618.393352536083,618.475881927484,618.559137923519,618.642393919554),
 .UNSPECIFIED.);
#440=B_SPLINE_CURVE_WITH_KNOTS('',3,(#61585,#61586,#61587,#61588,#61589,
#61590,#61591,#61592,#61593,#61594),.UNSPECIFIED.,.F.,.F.,(4,3,3,4),(612.360266019021,
612.449379317751,612.538258334461,612.610567449828),.UNSPECIFIED.);
#441=B_SPLINE_CURVE_WITH_KNOTS('',3,(#61596,#61597,#61598,#61599,#61600,
#61601,#61602,#61603,#61604,#61605,#61606,#61607,#61608),.UNSPECIFIED.,
 .F.,.F.,(4,3,3,3,4),(612.359058987781,612.442810974301,612.456763961887,
612.596727833402,612.610567449993),.UNSPECIFIED.);
#442=B_SPLINE_CURVE_WITH_KNOTS('',3,(#61609,#61610,#61611,#61612,#61613,
#61614,#61615,#61616,#61617,#61618,#61619,#61620,#61621,#61622,#61623,#61624,
#61625,#61626,#61627,#61628,#61629,#61630,#61631,#61632,#61633,#61634,#61635,
#61636,#61637,#61638,#61639,#61640,#61641,#61642,#61643,#61644,#61645,#61646,
#61647,#61648,#61649,#61650,#61651,#61652,#61653,#61654,#61655,#61656,#61657,
#61658,#61659,#61660,#61661,#61662,#61663,#61664,#61665,#61666,#61667,#61668,
#61669,#61670,#61671,#61672,#61673,#61674,#61675,#61676,#61677,#61678,#61679,
#61680,#61681,#61682,#61683,#61684,#61685,#61686,#61687,#61688,#61689,#61690,
#61691,#61692,#61693,#61694,#61695,#61696,#61697,#61698,#61699,#61700,#61701,
#61702,#61703,#61704,#61705,#61706,#61707,#61708,#61709,#61710,#61711,#61712,
#61713,#61714,#61715,#61716,#61717,#61718,#61719,#61720,#61721,#61722,#61723,
#61724,#61725,#61726,#61727,#61728,#61729,#61730,#61731,#61732,#61733,#61734,
#61735,#61736,#61737,#61738,#61739,#61740,#61741,#61742,#61743,#61744,#61745,
#61746,#61747,#61748,#61749,#61750,#61751,#61752,#61753,#61754,#61755,#61756,
#61757,#61758,#61759,#61760,#61761,#61762,#61763,#61764,#61765,#61766,#61767,
#61768,#61769,#61770,#61771,#61772,#61773,#61774,#61775,#61776,#61777,#61778,
#61779,#61780,#61781,#61782,#61783,#61784,#61785,#61786,#61787,#61788,#61789,
#61790,#61791,#61792,#61793,#61794,#61795,#61796,#61797,#61798,#61799,#61800,
#61801,#61802,#61803,#61804,#61805,#61806,#61807,#61808,#61809,#61810,#61811,
#61812,#61813,#61814,#61815,#61816,#61817,#61818,#61819,#61820,#61821,#61822,
#61823,#61824,#61825,#61826,#61827,#61828),.UNSPECIFIED.,.F.,.F.,(4,3,3,
3,3,3,3,3,3,3,3,3,3,3,3,3,3,3,3,3,3,3,3,3,3,3,3,3,3,3,3,3,3,3,3,3,3,3,3,
3,3,3,3,3,3,3,3,3,3,3,3,3,3,3,3,3,3,3,3,3,3,3,3,3,3,3,3,3,3,3,3,3,3,4),
(612.610567450102,612.692962920578,612.775277177584,612.860430026961,612.942652576491,
613.024862892056,613.107080001966,613.189322938079,613.271654224329,613.354038348432,
613.436536843195,613.456499972607,613.540238684453,613.62387419582,613.707426639219,
613.79091607507,613.874370025683,613.95780651953,614.041243629285,614.124699424203,
614.208243916932,614.291832999873,614.375556267431,614.456235983327,614.539974695173,
614.623610206541,614.707162649939,614.79065208579,614.874106036404,614.95754253025,
615.040979640006,615.124435434923,615.207979927653,615.291569010594,615.375292278152,
615.455971994047,615.539710705893,615.62334621726,615.706898660659,615.79038809651,
615.873842047124,615.95727854097,616.040715650726,616.124171445643,616.207715938373,
616.291305021314,616.375028288872,616.455708004767,616.539446716613,616.62308222798,
616.706634671378,616.79012410723,616.873578057843,616.957014551689,617.040451661445,
617.123907456363,617.207451949092,617.291041032033,617.374764299591,617.455444015487,
617.539182727333,617.6228182387,617.706370682099,617.78986011795,617.873314068564,
617.95675056241,618.040187672165,618.123643467082,618.207187959812,618.290777042753,
618.37450031031,618.455180026207,618.549310717824,618.643441409442),
 .UNSPECIFIED.);
#443=B_SPLINE_CURVE_WITH_KNOTS('',3,(#61834,#61835,#61836,#61837,#61838,
#61839,#61840,#61841,#61842,#61843,#61844,#61845,#61846,#61847,#61848,#61849,
#61850,#61851,#61852,#61853,#61854,#61855,#61856,#61857,#61858,#61859,#61860,
#61861,#61862,#61863,#61864,#61865,#61866,#61867,#61868,#61869,#61870,#61871,
#61872,#61873,#61874,#61875,#61876,#61877,#61878,#61879,#61880,#61881,#61882,
#61883,#61884,#61885,#61886,#61887,#61888,#61889,#61890,#61891,#61892,#61893,
#61894,#61895,#61896,#61897,#61898,#61899,#61900,#61901,#61902,#61903,#61904,
#61905,#61906,#61907,#61908,#61909,#61910,#61911,#61912,#61913,#61914,#61915,
#61916,#61917,#61918,#61919,#61920,#61921,#61922,#61923,#61924,#61925,#61926,
#61927,#61928,#61929,#61930,#61931,#61932,#61933,#61934,#61935,#61936,#61937,
#61938,#61939,#61940,#61941,#61942,#61943,#61944,#61945,#61946,#61947,#61948,
#61949,#61950,#61951,#61952,#61953,#61954,#61955,#61956,#61957,#61958,#61959,
#61960,#61961,#61962,#61963,#61964,#61965,#61966,#61967,#61968,#61969,#61970,
#61971,#61972,#61973,#61974,#61975,#61976,#61977,#61978,#61979,#61980,#61981,
#61982,#61983,#61984,#61985,#61986,#61987,#61988,#61989,#61990,#61991,#61992,
#61993,#61994,#61995,#61996,#61997,#61998,#61999,#62000,#62001,#62002,#62003,
#62004,#62005,#62006,#62007,#62008,#62009,#62010,#62011,#62012,#62013,#62014,
#62015,#62016,#62017,#62018,#62019,#62020,#62021,#62022,#62023,#62024,#62025,
#62026,#62027,#62028,#62029,#62030,#62031,#62032,#62033,#62034,#62035,#62036,
#62037,#62038,#62039,#62040,#62041,#62042,#62043,#62044,#62045,#62046,#62047,
#62048,#62049,#62050,#62051,#62052,#62053),.UNSPECIFIED.,.F.,.F.,(4,3,3,
3,3,3,3,3,3,3,3,3,3,3,3,3,3,3,3,3,3,3,3,3,3,3,3,3,3,3,3,3,3,3,3,3,3,3,3,
3,3,3,3,3,3,3,3,3,3,3,3,3,3,3,3,3,3,3,3,3,3,3,3,3,3,3,3,3,3,3,3,3,3,4),
(618.893752757351,619.000853338961,619.110344502978,619.144625417211,619.228364129057,
619.311999640424,619.395552083822,619.479041519673,619.562495470287,619.645931964133,
619.729369073888,619.812824868806,619.896369361535,619.979958444476,620.063681712033,
620.144361427932,620.228100139778,620.311735651146,620.395288094544,620.478777530395,
620.562231481009,620.645667974855,620.729105084611,620.812560879528,620.896105372258,
620.979694455199,621.063417722757,621.144097438652,621.227836150498,621.311471661865,
621.395024105264,621.478513541115,621.561967491728,621.645403985574,621.72884109533,
621.812296890247,621.895841382977,621.979430465918,622.063153733475,622.143833449372,
622.227572161218,622.311207672586,622.394760115984,622.478249551835,622.561703502449,
622.645139996295,622.728577106051,622.812032900968,622.895577393698,622.979166476639,
623.062889744197,623.143569460092,623.227308171938,623.310943683305,623.394496126704,
623.477985562555,623.561439513169,623.644876007015,623.728313116771,623.811768911688,
623.895313404418,623.978902487359,624.062625754917,624.143305470812,624.227057435847,
624.314334274184,624.397875522788,624.481359825538,624.564805301711,624.648230040424,
624.731673265519,624.815127694519,624.898637795245,624.925272142545),
 .UNSPECIFIED.);
#444=B_SPLINE_CURVE_WITH_KNOTS('',3,(#62054,#62055,#62056,#62057,#62058,
#62059,#62060,#62061,#62062,#62063),.UNSPECIFIED.,.F.,.F.,(4,3,3,4),(618.642393919554,
618.72489184659,618.809322301879,618.893752757168),.UNSPECIFIED.);
#445=B_SPLINE_CURVE_WITH_KNOTS('',3,(#62065,#62066,#62067,#62068,#62069,
#62070,#62071,#62072,#62073,#62074),.UNSPECIFIED.,.F.,.F.,(4,3,3,4),(618.643441409442,
618.733818705617,618.823895033376,618.893752757047),.UNSPECIFIED.);
#446=B_SPLINE_CURVE_WITH_KNOTS('',3,(#62075,#62076,#62077,#62078,#62079,
#62080,#62081,#62082,#62083,#62084,#62085,#62086,#62087,#62088,#62089,#62090,
#62091,#62092,#62093,#62094,#62095,#62096,#62097,#62098,#62099,#62100,#62101,
#62102,#62103,#62104,#62105,#62106,#62107,#62108,#62109,#62110,#62111,#62112,
#62113,#62114,#62115,#62116,#62117,#62118,#62119,#62120,#62121,#62122,#62123,
#62124,#62125,#62126,#62127,#62128,#62129,#62130,#62131,#62132,#62133,#62134,
#62135,#62136,#62137,#62138,#62139,#62140,#62141,#62142,#62143,#62144,#62145,
#62146,#62147,#62148,#62149,#62150,#62151,#62152,#62153,#62154,#62155,#62156,
#62157,#62158,#62159,#62160,#62161,#62162,#62163,#62164,#62165,#62166,#62167,
#62168,#62169,#62170,#62171,#62172,#62173,#62174,#62175,#62176,#62177,#62178,
#62179,#62180,#62181,#62182,#62183,#62184,#62185,#62186,#62187,#62188,#62189,
#62190,#62191,#62192,#62193,#62194,#62195,#62196,#62197,#62198,#62199,#62200,
#62201,#62202,#62203,#62204,#62205,#62206,#62207,#62208,#62209,#62210,#62211,
#62212,#62213,#62214,#62215,#62216,#62217,#62218,#62219,#62220,#62221,#62222,
#62223,#62224,#62225,#62226,#62227,#62228,#62229,#62230,#62231,#62232,#62233,
#62234,#62235,#62236,#62237,#62238,#62239,#62240,#62241,#62242,#62243,#62244,
#62245,#62246,#62247,#62248,#62249,#62250,#62251,#62252,#62253,#62254,#62255,
#62256,#62257,#62258,#62259,#62260,#62261,#62262,#62263,#62264,#62265,#62266,
#62267,#62268,#62269,#62270,#62271,#62272,#62273,#62274,#62275,#62276,#62277,
#62278,#62279,#62280,#62281,#62282,#62283,#62284,#62285,#62286,#62287,#62288,
#62289,#62290,#62291,#62292,#62293,#62294),.UNSPECIFIED.,.F.,.F.,(4,3,3,
3,3,3,3,3,3,3,3,3,3,3,3,3,3,3,3,3,3,3,3,3,3,3,3,3,3,3,3,3,3,3,3,3,3,3,3,
3,3,3,3,3,3,3,3,3,3,3,3,3,3,3,3,3,3,3,3,3,3,3,3,3,3,3,3,3,3,3,3,3,3,4),
(618.893752757172,618.979243826729,619.064785335007,619.150391707895,619.236139493783,
619.321965357415,619.407948450812,619.454916036928,619.538654748774,619.622290260141,
619.70584270354,619.78933213939,619.872786090004,619.95622258385,620.039659693606,
620.123115488524,620.206659981253,620.290249064194,620.373972331751,620.454652047648,
620.538390759494,620.622026270862,620.70557871426,620.789068150111,620.872522100725,
620.955958594571,621.039395704327,621.122851499244,621.206395991974,621.289985074915,
621.373708342473,621.454388058368,621.538126770214,621.621762281581,621.70531472498,
621.788804160831,621.872258111445,621.955694605291,622.039131715046,622.122587509964,
622.206132002693,622.289721085634,622.373444353192,622.454124069088,622.537862780934,
622.621498292301,622.7050507357,622.788540171551,622.871994122165,622.955430616011,
623.038867725766,623.122323520684,623.205868013413,623.289457096354,623.373180363912,
623.453860079808,623.537598791654,623.621234303022,623.70478674642,623.788276182272,
623.871730132886,623.955166626732,624.038603736487,624.122059531405,624.205604024135,
624.289193107076,624.372916374633,624.453596090528,624.536589151006,624.619482269218,
624.702279720181,624.785021521373,624.867728841325,624.925707879934),
 .UNSPECIFIED.);
#447=B_SPLINE_CURVE_WITH_KNOTS('',3,(#62300,#62301,#62302,#62303,#62304,
#62305,#62306,#62307,#62308,#62309,#62310,#62311,#62312,#62313,#62314,#62315,
#62316,#62317,#62318,#62319,#62320,#62321,#62322,#62323,#62324,#62325,#62326,
#62327,#62328,#62329,#62330,#62331,#62332,#62333,#62334,#62335,#62336,#62337,
#62338,#62339,#62340,#62341,#62342,#62343,#62344,#62345,#62346,#62347,#62348,
#62349,#62350,#62351,#62352,#62353,#62354,#62355,#62356,#62357,#62358,#62359,
#62360,#62361,#62362,#62363,#62364,#62365,#62366,#62367,#62368,#62369,#62370,
#62371,#62372,#62373,#62374,#62375,#62376,#62377,#62378,#62379,#62380,#62381,
#62382,#62383,#62384,#62385,#62386,#62387,#62388,#62389,#62390,#62391,#62392,
#62393,#62394,#62395,#62396,#62397,#62398,#62399,#62400,#62401,#62402,#62403,
#62404,#62405,#62406,#62407,#62408,#62409,#62410,#62411,#62412,#62413,#62414,
#62415,#62416,#62417,#62418,#62419,#62420,#62421,#62422,#62423,#62424,#62425,
#62426,#62427,#62428,#62429,#62430,#62431,#62432,#62433,#62434,#62435,#62436,
#62437,#62438,#62439,#62440,#62441,#62442,#62443,#62444,#62445,#62446,#62447,
#62448,#62449,#62450,#62451,#62452,#62453,#62454,#62455,#62456,#62457,#62458,
#62459,#62460,#62461,#62462,#62463,#62464,#62465,#62466,#62467,#62468,#62469,
#62470,#62471,#62472,#62473,#62474,#62475,#62476,#62477,#62478,#62479,#62480,
#62481,#62482,#62483,#62484,#62485,#62486,#62487,#62488,#62489,#62490,#62491,
#62492,#62493,#62494,#62495,#62496,#62497,#62498,#62499,#62500,#62501,#62502,
#62503,#62504,#62505,#62506,#62507,#62508,#62509,#62510,#62511,#62512,#62513,
#62514,#62515,#62516,#62517,#62518,#62519),.UNSPECIFIED.,.F.,.F.,(4,3,3,
3,3,3,3,3,3,3,3,3,3,3,3,3,3,3,3,3,3,3,3,3,3,3,3,3,3,3,3,3,3,3,3,3,3,3,3,
3,3,3,3,3,3,3,3,3,3,3,3,3,3,3,3,3,3,3,3,3,3,3,3,3,3,3,3,3,3,3,3,3,3,4),
(625.176938064496,625.260209543116,625.34337941499,625.426468270658,625.509496624868,
625.59249317596,625.675475373907,625.758461701018,625.841470638977,625.924568877374,
626.007716014695,626.090988218634,626.142777492252,626.226516204098,626.310151715465,
626.393704158864,626.477193594715,626.560647545328,626.644084039175,626.72752114893,
626.810976943847,626.894521436577,626.978110519518,627.061833787075,627.142513502972,
627.226252214818,627.309887726185,627.393440169584,627.476929605435,627.560383556049,
627.643820049895,627.72725715965,627.810712954568,627.894257447297,627.977846530238,
628.061569797796,628.142249513692,628.225988225538,628.309623736906,628.393176180304,
628.476665616155,628.560119566769,628.643556060615,628.726993170371,628.810448965288,
628.893993458018,628.977582540959,629.061305808517,629.141985524413,629.225724236259,
629.309359747627,629.392912191025,629.476401626876,629.55985557749,629.643292071336,
629.726729181092,629.810184976009,629.893729468739,629.97731855168,630.061041819238,
630.141721535133,630.225460246979,630.309095758346,630.392648201745,630.476137637597,
630.55959158821,630.643028082057,630.726465191812,630.809920986729,630.893465479459,
630.9770545624,631.060777829957,631.141457545853,631.209446795619),
 .UNSPECIFIED.);
#448=B_SPLINE_CURVE_WITH_KNOTS('',3,(#62520,#62521,#62522,#62523,#62524,
#62525,#62526,#62527,#62528,#62529,#62530,#62531,#62532),.UNSPECIFIED.,
 .F.,.F.,(4,3,3,3,4),(624.925272142545,625.008881354531,625.092616068713,
625.143041481532,625.176938064348),.UNSPECIFIED.);
#449=B_SPLINE_CURVE_WITH_KNOTS('',3,(#62534,#62535,#62536,#62537,#62538,
#62539,#62540,#62541,#62542,#62543),.UNSPECIFIED.,.F.,.F.,(4,3,3,4),(624.925707879934,
625.008404893569,625.09267147896,625.176938064352),.UNSPECIFIED.);
#450=B_SPLINE_CURVE_WITH_KNOTS('',3,(#62544,#62545,#62546,#62547,#62548,
#62549,#62550,#62551,#62552,#62553,#62554,#62555,#62556,#62557,#62558,#62559,
#62560,#62561,#62562,#62563,#62564,#62565,#62566,#62567,#62568,#62569,#62570,
#62571,#62572,#62573,#62574,#62575,#62576,#62577,#62578,#62579,#62580,#62581,
#62582,#62583,#62584,#62585,#62586,#62587,#62588,#62589,#62590,#62591,#62592,
#62593,#62594,#62595,#62596,#62597,#62598,#62599,#62600,#62601,#62602,#62603,
#62604,#62605,#62606,#62607,#62608,#62609,#62610,#62611,#62612,#62613,#62614,
#62615,#62616,#62617,#62618,#62619,#62620,#62621,#62622,#62623,#62624,#62625,
#62626,#62627,#62628,#62629,#62630,#62631,#62632,#62633,#62634,#62635,#62636,
#62637,#62638,#62639,#62640,#62641,#62642,#62643,#62644,#62645,#62646,#62647,
#62648,#62649,#62650,#62651,#62652,#62653,#62654,#62655,#62656,#62657,#62658,
#62659,#62660,#62661,#62662,#62663,#62664,#62665,#62666,#62667,#62668,#62669,
#62670,#62671,#62672,#62673,#62674,#62675,#62676,#62677,#62678,#62679,#62680,
#62681,#62682,#62683,#62684,#62685,#62686,#62687,#62688,#62689,#62690,#62691,
#62692,#62693,#62694,#62695,#62696,#62697,#62698,#62699,#62700,#62701,#62702,
#62703,#62704,#62705,#62706,#62707,#62708,#62709,#62710,#62711,#62712,#62713,
#62714,#62715,#62716,#62717,#62718,#62719,#62720,#62721,#62722,#62723,#62724,
#62725,#62726,#62727,#62728,#62729,#62730,#62731,#62732,#62733,#62734,#62735,
#62736,#62737,#62738,#62739,#62740,#62741,#62742,#62743,#62744,#62745,#62746,
#62747,#62748,#62749,#62750,#62751,#62752,#62753,#62754,#62755,#62756,#62757,
#62758,#62759,#62760),.UNSPECIFIED.,.F.,.F.,(4,3,3,3,3,3,3,3,3,3,3,3,3,
3,3,3,3,3,3,3,3,3,3,3,3,3,3,3,3,3,3,3,3,3,3,3,3,3,3,3,3,3,3,3,3,3,3,3,3,
3,3,3,3,3,3,3,3,3,3,3,3,3,3,3,3,3,3,3,3,3,3,3,4),(625.176938064455,625.280336351129,
625.385460544446,625.453332101248,625.537070813094,625.620706324461,625.70425876786,
625.787748203711,625.871202154325,625.954638648171,626.038075757926,626.121531552844,
626.205076045573,626.288665128514,626.372388396072,626.453068111968,626.536806823814,
626.620442335182,626.70399477858,626.787484214431,626.870938165045,626.954374658891,
627.037811768647,627.121267563564,627.204812056294,627.288401139235,627.372124406793,
627.452804122688,627.536542834534,627.620178345902,627.7037307893,627.787220225151,
627.870674175765,627.954110669611,628.037547779367,628.121003574284,628.204548067014,
628.288137149955,628.371860417513,628.452540133409,628.536278845255,628.619914356623,
628.703466800021,628.786956235872,628.870410186486,628.953846680332,629.037283790087,
629.120739585005,629.204284077735,629.287873160676,629.371596428233,629.452276144129,
629.536014855975,629.619650367343,629.703202810741,629.786692246592,629.870146197206,
629.953582691052,630.037019800807,630.120475595725,630.204020088455,630.287609171396,
630.371332438953,630.452012154849,630.535765810946,630.619853544318,630.703397992737,
630.786884325473,630.870330664123,630.954864917574,631.038303148445,631.123385413185,
631.208467677925),.UNSPECIFIED.);
#451=B_SPLINE_CURVE_WITH_KNOTS('',3,(#62766,#62767,#62768,#62769,#62770,
#62771,#62772,#62773,#62774,#62775,#62776,#62777,#62778,#62779,#62780,#62781,
#62782,#62783,#62784,#62785,#62786,#62787,#62788,#62789,#62790,#62791,#62792,
#62793,#62794,#62795,#62796,#62797,#62798,#62799,#62800,#62801,#62802,#62803,
#62804,#62805,#62806,#62807,#62808,#62809,#62810,#62811,#62812,#62813,#62814,
#62815,#62816,#62817,#62818,#62819,#62820,#62821,#62822,#62823,#62824,#62825,
#62826,#62827,#62828,#62829,#62830,#62831,#62832,#62833,#62834,#62835,#62836,
#62837,#62838,#62839,#62840,#62841,#62842,#62843,#62844,#62845,#62846,#62847,
#62848,#62849,#62850,#62851,#62852,#62853,#62854,#62855,#62856,#62857,#62858,
#62859,#62860,#62861,#62862,#62863,#62864,#62865,#62866,#62867,#62868,#62869,
#62870,#62871,#62872,#62873,#62874,#62875,#62876,#62877,#62878,#62879,#62880,
#62881,#62882,#62883,#62884,#62885,#62886,#62887,#62888,#62889,#62890,#62891,
#62892,#62893,#62894,#62895,#62896,#62897,#62898,#62899,#62900,#62901,#62902,
#62903,#62904,#62905,#62906,#62907,#62908,#62909,#62910,#62911,#62912,#62913,
#62914,#62915,#62916,#62917,#62918,#62919,#62920,#62921,#62922,#62923,#62924,
#62925,#62926,#62927,#62928,#62929,#62930,#62931,#62932,#62933,#62934,#62935,
#62936,#62937,#62938,#62939,#62940,#62941,#62942,#62943,#62944,#62945,#62946,
#62947,#62948,#62949,#62950,#62951,#62952,#62953,#62954,#62955,#62956,#62957,
#62958,#62959,#62960,#62961,#62962,#62963,#62964,#62965,#62966,#62967,#62968,
#62969,#62970,#62971,#62972,#62973,#62974,#62975,#62976,#62977,#62978,#62979,
#62980,#62981,#62982,#62983,#62984,#62985,#62986,#62987,#62988),
 .UNSPECIFIED.,.F.,.F.,(4,3,3,3,3,3,3,3,3,3,3,3,3,3,3,3,3,3,3,3,3,3,3,3,
3,3,3,3,3,3,3,3,3,3,3,3,3,3,3,3,3,3,3,3,3,3,3,3,3,3,3,3,3,3,3,3,3,3,3,3,
3,3,3,3,3,3,3,3,3,3,3,3,3,3,4),(631.460123371528,631.545257144659,631.628429442251,
631.711600703576,631.794789198943,631.88139028835,631.964715252283,632.048100864044,
632.131604501457,632.141193556573,632.224932268419,632.308567779786,632.392120223185,
632.475609659036,632.55906360965,632.642500103496,632.725937213251,632.809393008169,
632.892937500899,632.97652658384,633.060249851397,633.140929567293,633.224668279139,
633.308303790506,633.391856233905,633.475345669756,633.55879962037,633.642236114216,
633.725673223971,633.809129018888,633.892673511618,633.976262594559,634.059985862116,
634.140665578013,634.224404289859,634.308039801227,634.391592244625,634.475081680476,
634.55853563109,634.641972124936,634.725409234691,634.808865029609,634.892409522339,
634.97599860528,635.059721872837,635.140401588733,635.224140300579,635.307775811946,
635.391328255345,635.474817691196,635.55827164181,635.641708135656,635.725145245412,
635.80860104033,635.892145533059,635.975734616,636.059457883558,636.140137599454,
636.2238763113,636.307511822667,636.391064266066,636.474553701917,636.55800765253,
636.641444146377,636.724881256132,636.80833705105,636.89188154378,636.975470626721,
637.059193894279,637.139873610174,637.228073850114,637.31284479252,637.397529446154,
637.482127520008,637.492674569935),.UNSPECIFIED.);
#452=B_SPLINE_CURVE_WITH_KNOTS('',3,(#62989,#62990,#62991,#62992,#62993,
#62994,#62995,#62996,#62997,#62998),.UNSPECIFIED.,.F.,.F.,(4,3,3,4),(631.209446795619,
631.309022526793,631.407591002671,631.460123371355),.UNSPECIFIED.);
#453=B_SPLINE_CURVE_WITH_KNOTS('',3,(#63000,#63001,#63002,#63003,#63004,
#63005,#63006,#63007,#63008,#63009,#63010,#63011,#63012),.UNSPECIFIED.,
 .F.,.F.,(4,3,3,3,4),(631.208467677925,631.292059759149,631.375784639063,
631.451748165569,631.460123371531),.UNSPECIFIED.);
#454=B_SPLINE_CURVE_WITH_KNOTS('',3,(#63013,#63014,#63015,#63016,#63017,
#63018,#63019,#63020,#63021,#63022,#63023,#63024,#63025,#63026,#63027,#63028,
#63029,#63030,#63031,#63032,#63033,#63034,#63035,#63036,#63037,#63038,#63039,
#63040,#63041,#63042,#63043,#63044,#63045,#63046,#63047,#63048,#63049,#63050,
#63051,#63052,#63053,#63054,#63055,#63056,#63057,#63058,#63059,#63060,#63061,
#63062,#63063,#63064,#63065,#63066,#63067,#63068,#63069,#63070,#63071,#63072,
#63073,#63074,#63075,#63076,#63077,#63078,#63079,#63080,#63081,#63082,#63083,
#63084,#63085,#63086,#63087,#63088,#63089,#63090,#63091,#63092,#63093,#63094,
#63095,#63096,#63097,#63098,#63099,#63100,#63101,#63102,#63103,#63104,#63105,
#63106,#63107,#63108,#63109,#63110,#63111,#63112,#63113,#63114,#63115,#63116,
#63117,#63118,#63119,#63120,#63121,#63122,#63123,#63124,#63125,#63126,#63127,
#63128,#63129,#63130,#63131,#63132,#63133,#63134,#63135,#63136,#63137,#63138,
#63139,#63140,#63141,#63142,#63143,#63144,#63145,#63146,#63147,#63148,#63149,
#63150,#63151,#63152,#63153,#63154,#63155,#63156,#63157,#63158,#63159,#63160,
#63161,#63162,#63163,#63164,#63165,#63166,#63167,#63168,#63169,#63170,#63171,
#63172,#63173,#63174,#63175,#63176,#63177,#63178,#63179,#63180,#63181,#63182,
#63183,#63184,#63185,#63186,#63187,#63188,#63189,#63190,#63191,#63192,#63193,
#63194,#63195,#63196,#63197,#63198,#63199,#63200,#63201,#63202,#63203,#63204,
#63205,#63206,#63207,#63208,#63209,#63210,#63211,#63212,#63213,#63214,#63215,
#63216,#63217,#63218,#63219,#63220,#63221,#63222,#63223,#63224,#63225,#63226,
#63227,#63228,#63229,#63230,#63231,#63232),.UNSPECIFIED.,.F.,.F.,(4,3,3,
3,3,3,3,3,3,3,3,3,3,3,3,3,3,3,3,3,3,3,3,3,3,3,3,3,3,3,3,3,3,3,3,3,3,3,3,
3,3,3,3,3,3,3,3,3,3,3,3,3,3,3,3,3,3,3,3,3,3,3,3,3,3,3,3,3,3,3,3,3,3,4),
(631.460123371693,631.54373741473,631.627248408381,631.710676617484,631.794042233833,
631.87737303142,631.96068699152,632.04400230477,632.127337158942,632.21076078304,
632.294229991713,632.377831126119,632.451484176289,632.535222888135,632.618858399503,
632.702410842901,632.785900278752,632.869354229366,632.952790723213,633.036227832968,
633.119683627886,633.203228120616,633.286817203557,633.370540471114,633.451220187009,
633.534958898855,633.618594410222,633.702146853621,633.785636289472,633.869090240085,
633.952526733931,634.035963843687,634.119419638604,634.202964131333,634.286553214274,
634.370276481832,634.450956197729,634.534694909575,634.618330420943,634.701882864341,
634.785372300192,634.868826250806,634.952262744652,635.035699854407,635.119155649325,
635.202700142055,635.286289224996,635.370012492554,635.450692208449,635.534430920295,
635.618066431662,635.701618875061,635.785108310911,635.868562261525,635.951998755371,
636.035435865127,636.118891660045,636.202436152775,636.286025235716,636.369748503273,
636.45042821917,636.534166931016,636.617802442384,636.701354885782,636.784844321633,
636.868298272247,636.951734766093,637.035171875849,637.118627670766,637.202172163496,
637.285761246437,637.369484513995,637.45016422989,637.492495965904),
 .UNSPECIFIED.);
#455=B_SPLINE_CURVE_WITH_KNOTS('',3,(#63238,#63239,#63240,#63241,#63242,
#63243,#63244,#63245,#63246,#63247,#63248,#63249,#63250,#63251,#63252,#63253,
#63254,#63255,#63256,#63257,#63258,#63259,#63260,#63261,#63262,#63263,#63264,
#63265,#63266,#63267,#63268,#63269,#63270,#63271,#63272,#63273,#63274,#63275,
#63276,#63277,#63278,#63279,#63280,#63281,#63282,#63283,#63284,#63285,#63286,
#63287,#63288,#63289,#63290,#63291,#63292,#63293,#63294,#63295,#63296,#63297,
#63298,#63299,#63300,#63301,#63302,#63303,#63304,#63305,#63306,#63307,#63308,
#63309,#63310,#63311,#63312,#63313,#63314,#63315,#63316,#63317,#63318,#63319,
#63320,#63321,#63322,#63323,#63324,#63325,#63326,#63327,#63328,#63329,#63330,
#63331,#63332,#63333,#63334,#63335,#63336,#63337,#63338,#63339,#63340,#63341,
#63342,#63343,#63344,#63345,#63346,#63347,#63348,#63349,#63350,#63351,#63352,
#63353,#63354,#63355,#63356,#63357,#63358,#63359,#63360,#63361,#63362,#63363,
#63364,#63365,#63366,#63367,#63368,#63369,#63370,#63371,#63372,#63373,#63374,
#63375,#63376,#63377,#63378,#63379,#63380,#63381,#63382,#63383,#63384,#63385,
#63386,#63387,#63388,#63389,#63390,#63391,#63392,#63393,#63394,#63395,#63396,
#63397,#63398,#63399,#63400,#63401,#63402,#63403,#63404,#63405,#63406,#63407,
#63408,#63409,#63410,#63411,#63412,#63413,#63414,#63415,#63416,#63417,#63418,
#63419,#63420,#63421,#63422,#63423,#63424,#63425,#63426,#63427,#63428,#63429,
#63430,#63431,#63432,#63433,#63434,#63435,#63436,#63437,#63438,#63439,#63440,
#63441,#63442,#63443,#63444,#63445,#63446,#63447,#63448,#63449,#63450,#63451,
#63452,#63453,#63454,#63455,#63456,#63457),.UNSPECIFIED.,.F.,.F.,(4,3,3,
3,3,3,3,3,3,3,3,3,3,3,3,3,3,3,3,3,3,3,3,3,3,3,3,3,3,3,3,3,3,3,3,3,3,3,3,
3,3,3,3,3,3,3,3,3,3,3,3,3,3,3,3,3,3,3,3,3,3,3,3,3,3,3,3,3,3,3,3,3,3,4),
(637.743308678889,637.835617429321,637.928437698344,638.02152311515,638.114948726993,
638.139609620894,638.22334833274,638.306983844108,638.390536287506,638.474025723357,
638.557479673971,638.640916167817,638.724353277572,638.80780907249,638.89135356522,
638.97494264816,639.058665915718,639.139345631614,639.22308434346,639.306719854827,
639.390272298226,639.473761734077,639.55721568469,639.640652178537,639.724089288292,
639.80754508321,639.891089575939,639.97467865888,640.058401926438,640.139081642334,
640.22282035418,640.306455865547,640.390008308946,640.473497744797,640.556951695411,
640.640388189257,640.723825299012,640.80728109393,640.89082558666,640.974414669601,
641.058137937158,641.138817653054,641.2225563649,641.306191876267,641.389744319666,
641.473233755517,641.55668770613,641.640124199977,641.723561309732,641.80701710465,
641.890561597379,641.97415068032,642.057873947878,642.138553663774,642.22229237562,
642.305927886988,642.389480330386,642.472969766237,642.556423716851,642.639860210697,
642.723297320453,642.80675311537,642.8902976081,642.973886691041,643.057609958599,
643.138289674494,643.220897982151,643.303411668023,643.385849855946,643.468231600083,
643.550584869593,643.63291993891,643.715280454977,643.774669788269),
 .UNSPECIFIED.);
#456=B_SPLINE_CURVE_WITH_KNOTS('',3,(#63458,#63459,#63460,#63461,#63462,
#63463,#63464,#63465,#63466,#63467),.UNSPECIFIED.,.F.,.F.,(4,3,3,4),(637.492674569935,
637.577199593725,637.661692639095,637.743308678707),.UNSPECIFIED.);
#457=B_SPLINE_CURVE_WITH_KNOTS('',3,(#63469,#63470,#63471,#63472,#63473,
#63474,#63475,#63476,#63477,#63478),.UNSPECIFIED.,.F.,.F.,(4,3,3,4),(637.492495965904,
637.595189172829,637.696529649985,637.743308678576),.UNSPECIFIED.);
#458=B_SPLINE_CURVE_WITH_KNOTS('',3,(#63479,#63480,#63481,#63482,#63483,
#63484,#63485,#63486,#63487,#63488,#63489,#63490,#63491,#63492,#63493,#63494,
#63495,#63496,#63497,#63498,#63499,#63500,#63501,#63502,#63503,#63504,#63505,
#63506,#63507,#63508,#63509,#63510,#63511,#63512,#63513,#63514,#63515,#63516,
#63517,#63518,#63519,#63520,#63521,#63522,#63523,#63524,#63525,#63526,#63527,
#63528,#63529,#63530,#63531,#63532,#63533,#63534,#63535,#63536,#63537,#63538,
#63539,#63540,#63541,#63542,#63543,#63544,#63545,#63546,#63547,#63548,#63549,
#63550,#63551,#63552,#63553,#63554,#63555,#63556,#63557,#63558,#63559,#63560,
#63561,#63562,#63563,#63564,#63565,#63566,#63567,#63568,#63569,#63570,#63571,
#63572,#63573,#63574,#63575,#63576,#63577,#63578,#63579,#63580,#63581,#63582,
#63583,#63584,#63585,#63586,#63587,#63588,#63589,#63590,#63591,#63592,#63593,
#63594,#63595,#63596,#63597,#63598,#63599,#63600,#63601,#63602,#63603,#63604,
#63605,#63606,#63607,#63608,#63609,#63610,#63611,#63612,#63613,#63614,#63615,
#63616,#63617,#63618,#63619,#63620,#63621,#63622,#63623,#63624,#63625,#63626,
#63627,#63628,#63629,#63630,#63631,#63632,#63633,#63634,#63635,#63636,#63637,
#63638,#63639,#63640,#63641,#63642,#63643,#63644,#63645,#63646,#63647,#63648,
#63649,#63650,#63651,#63652,#63653,#63654,#63655,#63656,#63657,#63658,#63659,
#63660,#63661,#63662,#63663,#63664,#63665,#63666,#63667,#63668,#63669,#63670,
#63671,#63672,#63673,#63674,#63675,#63676,#63677,#63678,#63679,#63680,#63681,
#63682,#63683,#63684,#63685,#63686,#63687,#63688,#63689,#63690,#63691,#63692,
#63693,#63694,#63695,#63696,#63697,#63698),.UNSPECIFIED.,.F.,.F.,(4,3,3,
3,3,3,3,3,3,3,3,3,3,3,3,3,3,3,3,3,3,3,3,3,3,3,3,3,3,3,3,3,3,3,3,3,3,3,3,
3,3,3,3,3,3,3,3,3,3,3,3,3,3,3,3,3,3,3,3,3,3,3,3,3,3,3,3,3,3,3,3,3,3,4),
(637.743308678711,637.826210344786,637.909084797821,637.991947982986,638.074818452954,
638.157714762192,638.240703416289,638.323743941136,638.406909159978,638.44990024061,
638.533638952456,638.617274463823,638.700826907222,638.784316343073,638.867770293687,
638.951206787533,639.034643897288,639.118099692206,639.201644184936,639.285233267877,
639.368956535434,639.44963625133,639.533374963176,639.617010474544,639.700562917942,
639.784052353793,639.867506304406,639.950942798253,640.034379908008,640.117835702925,
640.201380195655,640.284969278596,640.368692546154,640.44937226205,640.533110973896,
640.616746485263,640.700298928662,640.783788364513,640.867242315127,640.950678808973,
641.034115918728,641.117571713646,641.201116206376,641.284705289317,641.368428556874,
641.44910827277,641.532846984616,641.616482495984,641.700034939382,641.783524375233,
641.866978325847,641.950414819693,642.033851929448,642.117307724366,642.200852217096,
642.284441300037,642.368164567595,642.44884428349,642.532582995336,642.616218506703,
642.699770950101,642.783260385952,642.866714336566,642.950150830412,643.033587940168,
643.117043735085,643.200588227815,643.284177310756,643.367900578314,643.448580294211,
643.534086763533,643.619486089427,643.704761993063,643.775962112477),
 .UNSPECIFIED.);
#459=B_SPLINE_CURVE_WITH_KNOTS('',3,(#63704,#63705,#63706,#63707,#63708,
#63709,#63710,#63711,#63712,#63713,#63714,#63715,#63716,#63717,#63718,#63719,
#63720,#63721,#63722,#63723,#63724,#63725,#63726,#63727,#63728,#63729,#63730,
#63731,#63732,#63733,#63734,#63735,#63736,#63737,#63738,#63739,#63740,#63741,
#63742,#63743,#63744,#63745,#63746,#63747,#63748,#63749,#63750,#63751,#63752,
#63753,#63754,#63755,#63756,#63757,#63758,#63759,#63760,#63761,#63762,#63763,
#63764,#63765,#63766,#63767,#63768,#63769,#63770,#63771,#63772,#63773,#63774,
#63775,#63776,#63777,#63778,#63779,#63780,#63781,#63782,#63783,#63784,#63785,
#63786,#63787,#63788,#63789,#63790,#63791,#63792,#63793,#63794,#63795,#63796,
#63797,#63798,#63799,#63800,#63801,#63802,#63803,#63804,#63805,#63806,#63807,
#63808,#63809,#63810,#63811,#63812,#63813,#63814,#63815,#63816,#63817,#63818,
#63819,#63820,#63821,#63822,#63823,#63824,#63825,#63826,#63827,#63828,#63829,
#63830,#63831,#63832,#63833,#63834,#63835,#63836,#63837,#63838,#63839,#63840,
#63841,#63842,#63843,#63844,#63845,#63846,#63847,#63848,#63849,#63850,#63851,
#63852,#63853,#63854,#63855,#63856,#63857,#63858,#63859,#63860,#63861,#63862,
#63863,#63864,#63865,#63866,#63867,#63868,#63869,#63870,#63871,#63872,#63873,
#63874,#63875,#63876,#63877,#63878,#63879,#63880,#63881,#63882,#63883,#63884,
#63885,#63886,#63887,#63888,#63889,#63890,#63891,#63892,#63893,#63894,#63895,
#63896,#63897,#63898,#63899,#63900,#63901,#63902,#63903,#63904,#63905,#63906,
#63907,#63908,#63909,#63910,#63911,#63912,#63913,#63914,#63915,#63916,#63917,
#63918,#63919,#63920),.UNSPECIFIED.,.F.,.F.,(4,3,3,3,3,3,3,3,3,3,3,3,3,
3,3,3,3,3,3,3,3,3,3,3,3,3,3,3,3,3,3,3,3,3,3,3,3,3,3,3,3,3,3,3,3,3,3,3,3,
3,3,3,3,3,3,3,3,3,3,3,3,3,3,3,3,3,3,3,3,3,3,3,4),(644.026493985887,644.138025685215,
644.22176439706,644.305399908426,644.388952351823,644.472441787673,644.555895738286,
644.639332232131,644.722769341885,644.806225136801,644.88976962953,644.97335871247,
645.057081980026,645.137761695935,645.221500407781,645.305135919149,645.388688362548,
645.472177798399,645.555631749013,645.639068242859,645.722505352615,645.805961147533,
645.889505640263,645.973094723204,646.056817990762,646.137497706655,646.221236418501,
646.304871929869,646.388424373267,646.471913809118,646.555367759732,646.638804253578,
646.722241363334,646.805697158252,646.889241650981,646.972830733922,647.05655400148,
647.137233717375,647.220972429221,647.304607940588,647.388160383987,647.471649819838,
647.555103770451,647.638540264297,647.721977374053,647.80543316897,647.8889776617,
647.972566744641,648.056290012198,648.136969728095,648.220708439941,648.304343951309,
648.387896394707,648.471385830558,648.554839781172,648.638276275018,648.721713384774,
648.805169179691,648.888713672421,648.972302755362,649.05602602292,649.136705738815,
649.220448966711,649.30408796254,649.3876428632,649.471466758317,649.554917045806,
649.63834849033,649.721779163694,649.805892878804,649.889410848519,649.973822436327,
650.058234024135),.UNSPECIFIED.);
#460=B_SPLINE_CURVE_WITH_KNOTS('',3,(#63921,#63922,#63923,#63924,#63925,
#63926,#63927,#63928,#63929,#63930),.UNSPECIFIED.,.F.,.F.,(4,3,3,4),(643.774669788269,
643.857102840832,643.941798413292,644.026493985751),.UNSPECIFIED.);
#461=B_SPLINE_CURVE_WITH_KNOTS('',3,(#63932,#63933,#63934,#63935,#63936,
#63937,#63938,#63939,#63940,#63941),.UNSPECIFIED.,.F.,.F.,(4,3,3,4),(643.775962112477,
643.861094775698,643.946170770531,644.026493985891),.UNSPECIFIED.);
#462=B_SPLINE_CURVE_WITH_KNOTS('',3,(#63942,#63943,#63944,#63945,#63946,
#63947,#63948,#63949,#63950,#63951,#63952,#63953,#63954,#63955,#63956,#63957,
#63958,#63959,#63960,#63961,#63962,#63963,#63964,#63965,#63966,#63967,#63968,
#63969,#63970,#63971,#63972,#63973,#63974,#63975,#63976,#63977,#63978,#63979,
#63980,#63981,#63982,#63983,#63984,#63985,#63986,#63987,#63988,#63989,#63990,
#63991,#63992,#63993,#63994,#63995,#63996,#63997,#63998,#63999,#64000,#64001,
#64002,#64003,#64004,#64005,#64006,#64007,#64008,#64009,#64010,#64011,#64012,
#64013,#64014,#64015,#64016,#64017,#64018,#64019,#64020,#64021,#64022,#64023,
#64024,#64025,#64026,#64027,#64028,#64029,#64030,#64031,#64032,#64033,#64034,
#64035,#64036,#64037,#64038,#64039,#64040,#64041,#64042,#64043,#64044,#64045,
#64046,#64047,#64048,#64049,#64050,#64051,#64052,#64053,#64054,#64055,#64056,
#64057,#64058,#64059,#64060,#64061,#64062,#64063,#64064,#64065,#64066,#64067,
#64068,#64069,#64070,#64071,#64072,#64073,#64074,#64075,#64076,#64077,#64078,
#64079,#64080,#64081,#64082,#64083,#64084,#64085,#64086,#64087,#64088,#64089,
#64090,#64091,#64092,#64093,#64094,#64095,#64096,#64097,#64098,#64099,#64100,
#64101,#64102,#64103,#64104,#64105,#64106,#64107,#64108,#64109,#64110,#64111,
#64112,#64113,#64114,#64115,#64116,#64117,#64118,#64119,#64120,#64121,#64122,
#64123,#64124,#64125,#64126,#64127,#64128,#64129,#64130,#64131,#64132,#64133,
#64134,#64135,#64136,#64137,#64138,#64139,#64140,#64141,#64142,#64143,#64144,
#64145,#64146,#64147,#64148,#64149,#64150,#64151,#64152,#64153,#64154,#64155,
#64156,#64157,#64158,#64159,#64160,#64161),.UNSPECIFIED.,.F.,.F.,(4,3,3,
3,3,3,3,3,3,3,3,3,3,3,3,3,3,3,3,3,3,3,3,3,3,3,3,3,3,3,3,3,3,3,3,3,3,3,3,
3,3,3,3,3,3,3,3,3,3,3,3,3,3,3,3,3,3,3,3,3,3,3,3,3,3,3,3,3,3,3,3,3,3,4),
(644.026493986046,644.117348037072,644.208612587543,644.300086391216,644.391869926028,
644.448316304931,644.532055016777,644.615690528145,644.699242971544,644.782732407395,
644.866186358009,644.949622851855,645.033059961611,645.116515756529,645.200060249259,
645.2836493322,645.367372599758,645.448052315651,645.531791027497,645.615426538864,
645.698978982263,645.782468418114,645.865922368727,645.949358862573,646.032795972329,
646.116251767246,646.199796259976,646.283385342917,646.367108610474,646.447788326371,
646.531527038217,646.615162549584,646.698714992983,646.782204428834,646.865658379447,
646.949094873294,647.032531983049,647.115987777967,647.199532270696,647.283121353637,
647.366844621195,647.447524337091,647.531263048937,647.614898560304,647.698451003703,
647.781940439554,647.865394390168,647.948830884014,648.03226799377,648.115723788688,
648.199268281417,648.282857364358,648.366580631916,648.447260347811,648.530999059657,
648.614634571024,648.698187014423,648.781676450274,648.865130400887,648.948566894734,
649.032004004489,649.115459799406,649.199004292136,649.282593375077,649.366316642635,
649.446996358531,649.529508123726,649.611925056606,649.694266347022,649.776551112661,
649.858804966058,649.941040865934,650.023294820861,650.057895601715),
 .UNSPECIFIED.);
#463=B_SPLINE_CURVE_WITH_KNOTS('',3,(#64167,#64168,#64169,#64170,#64171,
#64172,#64173,#64174,#64175,#64176,#64177,#64178,#64179,#64180,#64181,#64182,
#64183,#64184,#64185,#64186,#64187,#64188,#64189,#64190,#64191,#64192,#64193,
#64194,#64195,#64196,#64197,#64198,#64199,#64200,#64201,#64202,#64203,#64204,
#64205,#64206,#64207,#64208,#64209,#64210,#64211,#64212,#64213,#64214,#64215,
#64216,#64217,#64218,#64219,#64220,#64221,#64222,#64223,#64224,#64225,#64226,
#64227,#64228,#64229,#64230,#64231,#64232,#64233,#64234,#64235,#64236,#64237,
#64238,#64239,#64240,#64241,#64242,#64243,#64244,#64245,#64246,#64247,#64248,
#64249,#64250,#64251,#64252,#64253,#64254,#64255,#64256,#64257,#64258,#64259,
#64260,#64261,#64262,#64263,#64264,#64265,#64266,#64267,#64268,#64269,#64270,
#64271,#64272,#64273,#64274,#64275,#64276,#64277,#64278,#64279,#64280,#64281,
#64282,#64283,#64284,#64285,#64286,#64287,#64288,#64289,#64290,#64291,#64292,
#64293,#64294,#64295,#64296,#64297,#64298,#64299,#64300,#64301,#64302,#64303,
#64304,#64305,#64306,#64307,#64308,#64309,#64310,#64311,#64312,#64313,#64314,
#64315,#64316,#64317,#64318,#64319,#64320,#64321,#64322,#64323,#64324,#64325,
#64326,#64327,#64328,#64329,#64330,#64331,#64332,#64333,#64334,#64335,#64336,
#64337,#64338,#64339,#64340,#64341,#64342,#64343,#64344,#64345,#64346,#64347,
#64348,#64349,#64350,#64351,#64352,#64353,#64354,#64355,#64356,#64357,#64358,
#64359,#64360,#64361,#64362,#64363,#64364,#64365,#64366,#64367,#64368,#64369,
#64370,#64371,#64372,#64373,#64374,#64375,#64376,#64377,#64378,#64379,#64380,
#64381,#64382,#64383,#64384,#64385,#64386),.UNSPECIFIED.,.F.,.F.,(4,3,3,
3,3,3,3,3,3,3,3,3,3,3,3,3,3,3,3,3,3,3,3,3,3,3,3,3,3,3,3,3,3,3,3,3,3,3,3,
3,3,3,3,3,3,3,3,3,3,3,3,3,3,3,3,3,3,3,3,3,3,3,3,3,3,3,3,3,3,3,3,3,3,4),
(650.30967929324,650.392045240159,650.474334857195,650.557065220078,650.639274880365,
650.721476155833,650.803688079595,650.88681049976,650.969142703203,651.052660231729,
651.136177760256,651.219916472102,651.303551983469,651.387104426868,651.470593862719,
651.554047813333,651.637484307179,651.720921416934,651.804377211852,651.887921704582,
651.971510787523,652.05523405508,652.135913770976,652.219652482822,652.303287994189,
652.386840437588,652.470329873438,652.553783824052,652.637220317898,652.720657427653,
652.804113222571,652.887657715301,652.971246798242,653.054970065799,653.135649781696,
653.219388493542,653.30302400491,653.386576448308,653.470065884159,653.553519834773,
653.636956328619,653.720393438375,653.803849233292,653.887393726022,653.970982808963,
654.054706076521,654.135385792416,654.219124504262,654.302760015629,654.386312459028,
654.469801894879,654.553255845492,654.636692339339,654.720129449094,654.803585244012,
654.887129736742,654.970718819683,655.05444208724,655.135121803136,655.218860514982,
655.30249602635,655.386048469748,655.469537905599,655.552991856213,655.636428350059,
655.719865459815,655.803321254733,655.886865747462,655.970454830404,656.054178097961,
656.134857813856,656.224763958492,656.314447235095,656.342563021358),
 .UNSPECIFIED.);
#464=B_SPLINE_CURVE_WITH_KNOTS('',3,(#64387,#64388,#64389,#64390,#64391,
#64392,#64393,#64394,#64395,#64396),.UNSPECIFIED.,.F.,.F.,(4,3,3,4),(650.058234024135,
650.136441749535,650.266485457141,650.309679293066),.UNSPECIFIED.);
#465=B_SPLINE_CURVE_WITH_KNOTS('',3,(#64398,#64399,#64400,#64401,#64402,
#64403,#64404,#64405,#64406,#64407),.UNSPECIFIED.,.F.,.F.,(4,3,3,4),(650.057895601715,
650.140215484069,650.224947388508,650.309679292946),.UNSPECIFIED.);
#466=B_SPLINE_CURVE_WITH_KNOTS('',3,(#64408,#64409,#64410,#64411,#64412,
#64413,#64414,#64415,#64416,#64417,#64418,#64419,#64420,#64421,#64422,#64423,
#64424,#64425,#64426,#64427,#64428,#64429,#64430,#64431,#64432,#64433,#64434,
#64435,#64436,#64437,#64438,#64439,#64440,#64441,#64442,#64443,#64444,#64445,
#64446,#64447,#64448,#64449,#64450,#64451,#64452,#64453,#64454,#64455,#64456,
#64457,#64458,#64459,#64460,#64461,#64462,#64463,#64464,#64465,#64466,#64467,
#64468,#64469,#64470,#64471,#64472,#64473,#64474,#64475,#64476,#64477,#64478,
#64479,#64480,#64481,#64482,#64483,#64484,#64485,#64486,#64487,#64488,#64489,
#64490,#64491,#64492,#64493,#64494,#64495,#64496,#64497,#64498,#64499,#64500,
#64501,#64502,#64503,#64504,#64505,#64506,#64507,#64508,#64509,#64510,#64511,
#64512,#64513,#64514,#64515,#64516,#64517,#64518,#64519,#64520,#64521,#64522,
#64523,#64524,#64525,#64526,#64527,#64528,#64529,#64530,#64531,#64532,#64533,
#64534,#64535,#64536,#64537,#64538,#64539,#64540,#64541,#64542,#64543,#64544,
#64545,#64546,#64547,#64548,#64549,#64550,#64551,#64552,#64553,#64554,#64555,
#64556,#64557,#64558,#64559,#64560,#64561,#64562,#64563,#64564,#64565,#64566,
#64567,#64568,#64569,#64570,#64571,#64572,#64573,#64574,#64575,#64576,#64577,
#64578,#64579,#64580,#64581,#64582,#64583,#64584,#64585,#64586,#64587,#64588,
#64589,#64590,#64591,#64592,#64593,#64594,#64595,#64596,#64597,#64598,#64599,
#64600,#64601,#64602,#64603,#64604,#64605,#64606,#64607,#64608,#64609,#64610,
#64611,#64612,#64613,#64614,#64615,#64616,#64617,#64618,#64619,#64620,#64621,
#64622,#64623,#64624),.UNSPECIFIED.,.F.,.F.,(4,3,3,3,3,3,3,3,3,3,3,3,3,
3,3,3,3,3,3,3,3,3,3,3,3,3,3,3,3,3,3,3,3,3,3,3,3,3,3,3,3,3,3,3,3,3,3,3,3,
3,3,3,3,3,3,3,3,3,3,3,3,3,3,3,3,3,3,3,3,3,3,3,4),(650.30967929307,650.446732369252,
650.530471081096,650.614106592462,650.697659035858,650.781148471707,650.864602422319,
650.948038916163,651.031476025916,651.114931820832,651.198476313559,651.282065396498,
651.365788664054,651.446468379972,651.530207091818,651.613842603186,651.697395046585,
651.780884482436,651.86433843305,651.947774926897,652.031212036653,652.114667831571,
652.198212324301,652.281801407242,652.3655246748,652.446204390692,652.529943102538,
652.613578613906,652.697131057305,652.780620493156,652.86407444377,652.947510937617,
653.030948047372,653.11440384229,653.19794833502,653.281537417961,653.365260685519,
653.445940401412,653.529679113258,653.613314624625,653.696867068023,653.780356503874,
653.863810454487,653.947246948333,654.030684058088,654.114139853006,654.197684345735,
654.281273428676,654.364996696233,654.445676412132,654.529415123978,654.613050635346,
654.696603078744,654.780092514595,654.863546465209,654.946982959055,655.030420068811,
655.113875863729,655.197420356458,655.281009439399,655.364732706957,655.445412422852,
655.529157188434,655.612797384195,655.696353148497,655.779840105885,655.863289581261,
655.946719663156,656.030148423237,656.113630534888,656.197140214626,656.280745214861,
656.341338735484),.UNSPECIFIED.);
#467=B_SPLINE_CURVE_WITH_KNOTS('',3,(#64630,#64631,#64632,#64633,#64634,
#64635,#64636,#64637,#64638,#64639,#64640,#64641,#64642,#64643,#64644,#64645,
#64646,#64647,#64648,#64649,#64650,#64651,#64652,#64653,#64654,#64655,#64656,
#64657,#64658,#64659,#64660,#64661,#64662,#64663,#64664,#64665,#64666,#64667,
#64668,#64669,#64670,#64671,#64672,#64673,#64674,#64675,#64676,#64677,#64678,
#64679,#64680,#64681,#64682,#64683,#64684,#64685,#64686,#64687,#64688,#64689,
#64690,#64691,#64692,#64693,#64694,#64695,#64696,#64697,#64698,#64699,#64700,
#64701,#64702,#64703,#64704,#64705,#64706,#64707,#64708,#64709,#64710,#64711,
#64712,#64713,#64714,#64715,#64716,#64717,#64718,#64719,#64720,#64721,#64722,
#64723,#64724,#64725,#64726,#64727,#64728,#64729,#64730,#64731,#64732,#64733,
#64734,#64735,#64736,#64737,#64738,#64739,#64740,#64741,#64742,#64743,#64744,
#64745,#64746,#64747,#64748,#64749,#64750,#64751,#64752,#64753,#64754,#64755,
#64756,#64757,#64758,#64759,#64760,#64761,#64762,#64763,#64764,#64765,#64766,
#64767,#64768,#64769,#64770,#64771,#64772,#64773,#64774,#64775,#64776,#64777,
#64778,#64779,#64780,#64781,#64782,#64783,#64784,#64785,#64786,#64787,#64788,
#64789,#64790,#64791,#64792,#64793,#64794,#64795,#64796,#64797,#64798,#64799,
#64800,#64801,#64802,#64803,#64804,#64805,#64806,#64807,#64808,#64809,#64810,
#64811,#64812,#64813,#64814,#64815,#64816,#64817,#64818,#64819,#64820,#64821,
#64822,#64823,#64824,#64825,#64826,#64827,#64828,#64829,#64830,#64831,#64832,
#64833,#64834,#64835,#64836,#64837,#64838,#64839,#64840,#64841,#64842,#64843,
#64844,#64845,#64846,#64847,#64848,#64849),.UNSPECIFIED.,.F.,.F.,(4,3,3,
3,3,3,3,3,3,3,3,3,3,3,3,3,3,3,3,3,3,3,3,3,3,3,3,3,3,3,3,3,3,3,3,3,3,3,3,
3,3,3,3,3,3,3,3,3,3,3,3,3,3,3,3,3,3,3,3,3,3,3,3,3,3,3,3,3,3,3,3,3,3,4),
(656.592864600246,656.678899150996,656.765001425791,656.85118441481,656.937522996922,
657.02395084777,657.110535945372,657.134593824576,657.218332536422,657.301968047789,
657.385520491188,657.469009927039,657.552463877653,657.635900371499,657.719337481254,
657.802793276172,657.886337768901,657.969926851842,658.0536501194,658.134329835296,
658.218068547142,658.301704058509,658.385256501908,658.468745937759,658.552199888373,
658.635636382219,658.719073491974,658.802529286892,658.886073779622,658.969662862563,
659.05338613012,659.134065846016,659.217804557862,659.301440069229,659.384992512628,
659.468481948479,659.551935899093,659.635372392939,659.718809502695,659.802265297612,
659.885809790342,659.969398873283,660.053122140841,660.133801856737,660.217540568583,
660.301176079951,660.384728523349,660.4682179592,660.551671909814,660.63510840366,
660.718545513416,660.802001308334,660.885545801063,660.969134884005,661.052858151562,
661.133537867457,661.217276579303,661.300912090671,661.384464534069,661.46795396992,
661.551407920534,661.63484441438,661.718281524136,661.801737319053,661.885281811783,
661.968870894724,662.052594162281,662.133273878177,662.216094422083,662.298816305874,
662.381445606525,662.464020372407,662.546567121197,662.624721185932),
 .UNSPECIFIED.);
#468=B_SPLINE_CURVE_WITH_KNOTS('',3,(#64850,#64851,#64852,#64853,#64854,
#64855,#64856,#64857,#64858,#64859),.UNSPECIFIED.,.F.,.F.,(4,3,3,4),(656.342563021358,
656.431962567064,656.52111325134,656.592864600061),.UNSPECIFIED.);
#469=B_SPLINE_CURVE_WITH_KNOTS('',3,(#64861,#64862,#64863,#64864,#64865,
#64866,#64867,#64868,#64869,#64870),.UNSPECIFIED.,.F.,.F.,(4,3,3,4),(656.341338735484,
656.425087564978,656.445148433572,656.59286460025),.UNSPECIFIED.);
#470=B_SPLINE_CURVE_WITH_KNOTS('',3,(#64871,#64872,#64873,#64874,#64875,
#64876,#64877,#64878,#64879,#64880,#64881,#64882,#64883,#64884,#64885,#64886,
#64887,#64888,#64889,#64890,#64891,#64892,#64893,#64894,#64895,#64896,#64897,
#64898,#64899,#64900,#64901,#64902,#64903,#64904,#64905,#64906,#64907,#64908,
#64909,#64910,#64911,#64912,#64913,#64914,#64915,#64916,#64917,#64918,#64919,
#64920,#64921,#64922,#64923,#64924,#64925,#64926,#64927,#64928,#64929,#64930,
#64931,#64932,#64933,#64934,#64935,#64936,#64937,#64938,#64939,#64940,#64941,
#64942,#64943,#64944,#64945,#64946,#64947,#64948,#64949,#64950,#64951,#64952,
#64953,#64954,#64955,#64956,#64957,#64958,#64959,#64960,#64961,#64962,#64963,
#64964,#64965,#64966,#64967,#64968,#64969,#64970,#64971,#64972,#64973,#64974,
#64975,#64976,#64977,#64978,#64979,#64980,#64981,#64982,#64983,#64984,#64985,
#64986,#64987,#64988,#64989,#64990,#64991,#64992,#64993,#64994,#64995,#64996,
#64997,#64998,#64999,#65000,#65001,#65002,#65003,#65004,#65005,#65006,#65007,
#65008,#65009,#65010,#65011,#65012,#65013,#65014,#65015,#65016,#65017,#65018,
#65019,#65020,#65021,#65022,#65023,#65024,#65025,#65026,#65027,#65028,#65029,
#65030,#65031,#65032,#65033,#65034,#65035,#65036,#65037,#65038,#65039,#65040,
#65041,#65042,#65043,#65044,#65045,#65046,#65047,#65048,#65049,#65050,#65051,
#65052,#65053,#65054,#65055,#65056,#65057,#65058,#65059,#65060,#65061,#65062,
#65063,#65064,#65065,#65066,#65067,#65068,#65069,#65070,#65071,#65072,#65073,
#65074,#65075,#65076,#65077,#65078,#65079,#65080,#65081,#65082,#65083,#65084,
#65085,#65086,#65087,#65088,#65089,#65090),.UNSPECIFIED.,.F.,.F.,(4,3,3,
3,3,3,3,3,3,3,3,3,3,3,3,3,3,3,3,3,3,3,3,3,3,3,3,3,3,3,3,3,3,3,3,3,3,3,3,
3,3,3,3,3,3,3,3,3,3,3,3,3,3,3,3,3,3,3,3,3,3,3,3,3,3,3,3,3,3,3,3,3,3,4),
(656.592864600365,656.675275781259,656.757604299598,656.843514317685,656.925747554104,
657.007967410282,657.090192909171,657.17244307627,657.254781085733,657.337170879931,
657.419676421055,657.444884444292,657.528623156138,657.612258667505,657.695811110904,
657.779300546755,657.862754497369,657.946190991215,658.02962810097,658.113083895888,
658.196628388618,658.280217471559,658.363940739116,658.444620455012,658.528359166858,
658.611994678226,658.695547121624,658.779036557476,658.862490508089,658.945927001936,
659.029364111691,659.112819906609,659.196364399339,659.27995348228,659.363676749838,
659.444356465733,659.528095177579,659.611730688947,659.695283132345,659.778772568196,
659.86222651881,659.945663012656,660.029100122411,660.112555917329,660.196100410059,
660.279689493,660.363412760557,660.444092476453,660.527831188299,660.611466699666,
660.695019143065,660.778508578915,660.861962529529,660.945399023375,661.02883613313,
661.112291928048,661.195836420778,661.279425503719,661.363148771276,661.443828487173,
661.527567199019,661.611202710387,661.694755153785,661.778244589636,661.86169854025,
661.945135034096,662.028572143852,662.112027938769,662.195572431499,662.27916151444,
662.362884781998,662.443564497893,662.534703199586,662.62573256838),
 .UNSPECIFIED.);
#471=B_SPLINE_CURVE_WITH_KNOTS('',3,(#65096,#65097,#65098,#65099,#65100,
#65101,#65102,#65103,#65104,#65105,#65106,#65107,#65108,#65109,#65110,#65111,
#65112,#65113,#65114,#65115,#65116,#65117,#65118,#65119,#65120,#65121,#65122,
#65123,#65124,#65125,#65126,#65127,#65128,#65129,#65130,#65131,#65132,#65133,
#65134,#65135,#65136,#65137,#65138,#65139,#65140,#65141,#65142,#65143,#65144,
#65145,#65146,#65147,#65148,#65149,#65150,#65151,#65152,#65153,#65154,#65155,
#65156,#65157,#65158,#65159,#65160,#65161,#65162,#65163,#65164,#65165,#65166,
#65167,#65168,#65169,#65170,#65171,#65172,#65173,#65174,#65175,#65176,#65177,
#65178,#65179,#65180,#65181,#65182,#65183,#65184,#65185,#65186,#65187,#65188,
#65189,#65190,#65191,#65192,#65193,#65194,#65195,#65196,#65197,#65198,#65199,
#65200,#65201,#65202,#65203,#65204,#65205,#65206,#65207,#65208,#65209,#65210,
#65211,#65212,#65213,#65214,#65215,#65216,#65217,#65218,#65219,#65220,#65221,
#65222,#65223,#65224,#65225,#65226,#65227,#65228,#65229,#65230,#65231,#65232,
#65233,#65234,#65235,#65236,#65237,#65238,#65239,#65240,#65241,#65242,#65243,
#65244,#65245,#65246,#65247,#65248,#65249,#65250,#65251,#65252,#65253,#65254,
#65255,#65256,#65257,#65258,#65259,#65260,#65261,#65262,#65263,#65264,#65265,
#65266,#65267,#65268,#65269,#65270,#65271,#65272,#65273,#65274,#65275,#65276,
#65277,#65278,#65279,#65280,#65281,#65282,#65283,#65284,#65285,#65286,#65287,
#65288,#65289,#65290,#65291,#65292,#65293,#65294,#65295,#65296,#65297,#65298,
#65299,#65300,#65301,#65302,#65303,#65304,#65305,#65306,#65307,#65308,#65309,
#65310,#65311,#65312,#65313,#65314,#65315),.UNSPECIFIED.,.F.,.F.,(4,3,3,
3,3,3,3,3,3,3,3,3,3,3,3,3,3,3,3,3,3,3,3,3,3,3,3,3,3,3,3,3,3,3,3,3,3,3,3,
3,3,3,3,3,3,3,3,3,3,3,3,3,3,3,3,3,3,3,3,3,3,3,3,3,3,3,3,3,3,3,3,3,3,4),
(662.876049907546,662.982197863683,663.09054757415,663.133009888897,663.216748600743,
663.30038411211,663.383936555509,663.46742599136,663.550879941973,663.63431643582,
663.717753545575,663.801209340493,663.884753833222,663.968342916163,664.052066183721,
664.132745899617,664.216484611463,664.30012012283,664.383672566229,664.46716200208,
664.550615952693,664.634052446539,664.717489556295,664.800945351212,664.884489843942,
664.968078926883,665.051802194441,665.132481910337,665.216220622183,665.299856133551,
665.383408576949,665.4668980128,665.550351963414,665.63378845726,665.717225567016,
665.800681361934,665.884225854663,665.967814937604,666.051538205162,666.132217921057,
666.215956632903,666.29959214427,666.383144587669,666.46663402352,666.550087974134,
666.63352446798,666.716961577735,666.800417372653,666.883961865383,666.967550948324,
667.051274215882,667.131953931778,667.215692643624,667.299328154991,667.38288059839,
667.466370034241,667.549823984855,667.633260478701,667.716697588457,667.800153383375,
667.883697876104,667.967286959046,668.051010226603,668.131689942498,668.215442308325,
668.301958335874,668.385500331567,668.468985102343,668.55243076802,668.635855418049,
668.719297398319,668.802750389247,668.886256829366,668.907570528719),
 .UNSPECIFIED.);
#472=B_SPLINE_CURVE_WITH_KNOTS('',3,(#65316,#65317,#65318,#65319,#65320,
#65321,#65322,#65323,#65324,#65325),.UNSPECIFIED.,.F.,.F.,(4,3,3,4),(662.624721185932,
662.707261065595,662.79165548651,662.876049907425),.UNSPECIFIED.);
#473=B_SPLINE_CURVE_WITH_KNOTS('',3,(#65327,#65328,#65329,#65330,#65331,
#65332,#65333,#65334,#65335,#65336),.UNSPECIFIED.,.F.,.F.,(4,3,3,4),(662.62573256838,
662.716437538103,662.806823242474,662.876049907294),.UNSPECIFIED.);
#474=B_SPLINE_CURVE_WITH_KNOTS('',3,(#65337,#65338,#65339,#65340,#65341,
#65342,#65343,#65344,#65345,#65346,#65347,#65348,#65349,#65350,#65351,#65352,
#65353,#65354,#65355,#65356,#65357,#65358,#65359,#65360,#65361,#65362,#65363,
#65364,#65365,#65366,#65367,#65368,#65369,#65370,#65371,#65372,#65373,#65374,
#65375,#65376,#65377,#65378,#65379,#65380,#65381,#65382,#65383,#65384,#65385,
#65386,#65387,#65388,#65389,#65390,#65391,#65392,#65393,#65394,#65395,#65396,
#65397,#65398,#65399,#65400,#65401,#65402,#65403,#65404,#65405,#65406,#65407,
#65408,#65409,#65410,#65411,#65412,#65413,#65414,#65415,#65416,#65417,#65418,
#65419,#65420,#65421,#65422,#65423,#65424,#65425,#65426,#65427,#65428,#65429,
#65430,#65431,#65432,#65433,#65434,#65435,#65436,#65437,#65438,#65439,#65440,
#65441,#65442,#65443,#65444,#65445,#65446,#65447,#65448,#65449,#65450,#65451,
#65452,#65453,#65454,#65455,#65456,#65457,#65458,#65459,#65460,#65461,#65462,
#65463,#65464,#65465,#65466,#65467,#65468,#65469,#65470,#65471,#65472,#65473,
#65474,#65475,#65476,#65477,#65478,#65479,#65480,#65481,#65482,#65483,#65484,
#65485,#65486,#65487,#65488,#65489,#65490,#65491,#65492,#65493,#65494,#65495,
#65496,#65497,#65498,#65499,#65500,#65501,#65502,#65503,#65504,#65505,#65506,
#65507,#65508,#65509,#65510,#65511,#65512,#65513,#65514,#65515,#65516,#65517,
#65518,#65519,#65520,#65521,#65522,#65523,#65524,#65525,#65526,#65527,#65528,
#65529,#65530,#65531,#65532,#65533,#65534,#65535,#65536,#65537,#65538,#65539,
#65540,#65541,#65542,#65543,#65544,#65545,#65546,#65547,#65548,#65549,#65550,
#65551,#65552,#65553,#65554,#65555,#65556),.UNSPECIFIED.,.F.,.F.,(4,3,3,
3,3,3,3,3,3,3,3,3,3,3,3,3,3,3,3,3,3,3,3,3,3,3,3,3,3,3,3,3,3,3,3,3,3,3,3,
3,3,3,3,3,3,3,3,3,3,3,3,3,3,3,3,3,3,3,3,3,3,3,3,3,3,3,3,3,3,3,3,3,3,4),
(662.876049907429,662.961381766709,663.046759126554,663.13219678947,663.217771747914,
663.303421489595,663.389228574437,663.443300508613,663.527039220459,663.610674731827,
663.694227175225,663.777716611076,663.86117056169,663.944607055536,664.028044165291,
664.111499960209,664.195044452939,664.27863353588,664.362356803438,664.443036519333,
664.526775231179,664.610410742546,664.693963185945,664.777452621796,664.860906572409,
664.944343066256,665.027780176011,665.111235970929,665.194780463659,665.2783695466,
665.362092814157,665.442772530053,665.526511241899,665.610146753267,665.693699196665,
665.777188632516,665.86064258313,665.944079076976,666.027516186732,666.11097198165,
666.194516474379,666.27810555732,666.361828824878,666.442508540774,666.52624725262,
666.609882763988,666.693435207386,666.776924643237,666.860378593851,666.943815087697,
667.027252197452,667.11070799237,667.1942524851,667.277841568041,667.361564835599,
667.442244551494,667.52598326334,667.609618774707,667.693171218105,667.776660653956,
667.86011460457,667.943551098416,668.026988208172,668.110444003089,668.193988495819,
668.27757757876,668.361300846318,668.441980562214,668.525035095247,668.607989231031,
668.690846703051,668.773648117135,668.856413159468,668.908036453214),
 .UNSPECIFIED.);
#475=B_SPLINE_CURVE_WITH_KNOTS('',3,(#65562,#65563,#65564,#65565,#65566,
#65567,#65568,#65569,#65570,#65571,#65572,#65573,#65574,#65575,#65576,#65577,
#65578,#65579,#65580,#65581,#65582,#65583,#65584,#65585,#65586,#65587,#65588,
#65589,#65590,#65591,#65592,#65593,#65594,#65595,#65596,#65597,#65598,#65599,
#65600,#65601,#65602,#65603,#65604,#65605,#65606,#65607,#65608,#65609,#65610,
#65611,#65612,#65613,#65614,#65615,#65616,#65617,#65618,#65619,#65620,#65621,
#65622,#65623,#65624,#65625,#65626,#65627,#65628,#65629,#65630,#65631,#65632,
#65633,#65634,#65635,#65636,#65637,#65638,#65639,#65640,#65641,#65642,#65643,
#65644,#65645,#65646,#65647,#65648,#65649,#65650,#65651,#65652,#65653,#65654,
#65655,#65656,#65657,#65658,#65659,#65660,#65661,#65662,#65663,#65664,#65665,
#65666,#65667,#65668,#65669,#65670,#65671,#65672,#65673,#65674,#65675,#65676,
#65677,#65678,#65679,#65680,#65681,#65682,#65683,#65684,#65685,#65686,#65687,
#65688,#65689,#65690,#65691,#65692,#65693,#65694,#65695,#65696,#65697,#65698,
#65699,#65700,#65701,#65702,#65703,#65704,#65705,#65706,#65707,#65708,#65709,
#65710,#65711,#65712,#65713,#65714,#65715,#65716,#65717,#65718,#65719,#65720,
#65721,#65722,#65723,#65724,#65725,#65726,#65727,#65728,#65729,#65730,#65731,
#65732,#65733,#65734,#65735,#65736,#65737,#65738,#65739,#65740,#65741,#65742,
#65743,#65744,#65745,#65746,#65747,#65748,#65749,#65750,#65751,#65752,#65753,
#65754,#65755,#65756,#65757,#65758,#65759,#65760,#65761,#65762,#65763,#65764,
#65765,#65766,#65767,#65768,#65769,#65770,#65771,#65772,#65773,#65774,#65775,
#65776,#65777,#65778,#65779,#65780,#65781),.UNSPECIFIED.,.F.,.F.,(4,3,3,
3,3,3,3,3,3,3,3,3,3,3,3,3,3,3,3,3,3,3,3,3,3,3,3,3,3,3,3,3,3,3,3,3,3,3,3,
3,3,3,3,3,3,3,3,3,3,3,3,3,3,3,3,3,3,3,3,3,3,3,3,3,3,3,3,3,3,3,3,3,3,4),
(669.15923521473,669.242583325641,669.325829362661,669.408993848178,669.492097229402,
669.575167966028,669.65822368116,669.741282795814,669.824363729774,669.907533798707,
669.990751938535,670.07409677329,670.131161963938,670.214900675784,670.298536187151,
670.38208863055,670.465578066401,670.549032017015,670.632468510861,670.715905620616,
670.799361415534,670.882905908263,670.966494991204,671.050218258762,671.130897974658,
671.214636686504,671.298272197871,671.38182464127,671.465314077121,671.548768027735,
671.632204521581,671.715641631337,671.799097426254,671.882641918984,671.966231001925,
672.049954269483,672.130633985378,672.214372697224,672.298008208592,672.38156065199,
672.465050087841,672.548504038455,672.631940532301,672.715377642056,672.798833436974,
672.882377929704,672.965967012645,673.049690280202,673.130369996098,673.214108707944,
673.297744219312,673.38129666271,673.464786098561,673.548240049175,673.631676543021,
673.715113652777,673.798569447694,673.882113940424,673.965703023365,674.049426290923,
674.130106006818,674.213844718664,674.297480230032,674.38103267343,674.464522109281,
674.547976059895,674.631412553741,674.714849663497,674.798305458415,674.881849951144,
674.965439034085,675.049162301643,675.129842017539,675.19171294655),
 .UNSPECIFIED.);
#476=B_SPLINE_CURVE_WITH_KNOTS('',3,(#65782,#65783,#65784,#65785,#65786,
#65787,#65788,#65789,#65790,#65791,#65792,#65793,#65794),.UNSPECIFIED.,
 .F.,.F.,(4,3,3,3,4),(668.907570528719,668.991175516459,669.074907715256,
669.131425953218,669.159235214605),.UNSPECIFIED.);
#477=B_SPLINE_CURVE_WITH_KNOTS('',3,(#65796,#65797,#65798,#65799,#65800,
#65801,#65802,#65803,#65804,#65805),.UNSPECIFIED.,.F.,.F.,(4,3,3,4),(668.908036453214,
668.990790070795,669.075012642702,669.159235214609),.UNSPECIFIED.);
#478=B_SPLINE_CURVE_WITH_KNOTS('',3,(#65806,#65807,#65808,#65809,#65810,
#65811,#65812,#65813,#65814,#65815,#65816,#65817,#65818,#65819,#65820,#65821,
#65822,#65823,#65824,#65825,#65826,#65827,#65828,#65829,#65830,#65831,#65832,
#65833,#65834,#65835,#65836,#65837,#65838,#65839,#65840,#65841,#65842,#65843,
#65844,#65845,#65846,#65847,#65848,#65849,#65850,#65851,#65852,#65853,#65854,
#65855,#65856,#65857,#65858,#65859,#65860,#65861,#65862,#65863,#65864,#65865,
#65866,#65867,#65868,#65869,#65870,#65871,#65872,#65873,#65874,#65875,#65876,
#65877,#65878,#65879,#65880,#65881,#65882,#65883,#65884,#65885,#65886,#65887,
#65888,#65889,#65890,#65891,#65892,#65893,#65894,#65895,#65896,#65897,#65898,
#65899,#65900,#65901,#65902,#65903,#65904,#65905,#65906,#65907,#65908,#65909,
#65910,#65911,#65912,#65913,#65914,#65915,#65916,#65917,#65918,#65919,#65920,
#65921,#65922,#65923,#65924,#65925,#65926,#65927,#65928,#65929,#65930,#65931,
#65932,#65933,#65934,#65935,#65936,#65937,#65938,#65939,#65940,#65941,#65942,
#65943,#65944,#65945,#65946,#65947,#65948,#65949,#65950,#65951,#65952,#65953,
#65954,#65955,#65956,#65957,#65958,#65959,#65960,#65961,#65962,#65963,#65964,
#65965,#65966,#65967,#65968,#65969,#65970,#65971,#65972,#65973,#65974,#65975,
#65976,#65977,#65978,#65979,#65980,#65981,#65982,#65983,#65984,#65985,#65986,
#65987,#65988,#65989,#65990,#65991,#65992,#65993,#65994,#65995,#65996,#65997,
#65998,#65999,#66000,#66001,#66002,#66003,#66004,#66005,#66006,#66007,#66008,
#66009,#66010,#66011,#66012,#66013,#66014,#66015,#66016,#66017,#66018,#66019,
#66020,#66021,#66022),.UNSPECIFIED.,.F.,.F.,(4,3,3,3,3,3,3,3,3,3,3,3,3,
3,3,3,3,3,3,3,3,3,3,3,3,3,3,3,3,3,3,3,3,3,3,3,3,3,3,3,3,3,3,3,3,3,3,3,3,
3,3,3,3,3,3,3,3,3,3,3,3,3,3,3,3,3,3,3,3,3,3,3,4),(669.159235214725,669.261852727765,
669.366077895762,669.441716572934,669.52545528478,669.609090796147,669.692643239546,
669.776132675397,669.85958662601,669.943023119857,670.026460229612,670.10991602453,
670.193460517259,670.2770496002,670.360772867758,670.441452583654,670.5251912955,
670.608826806867,670.692379250266,670.775868686117,670.85932263673,670.942759130577,
671.026196240332,671.10965203525,671.193196527979,671.27678561092,671.360508878478,
671.441188594374,671.52492730622,671.608562817588,671.692115260986,671.775604696837,
671.859058647451,671.942495141297,672.025932251052,672.10938804597,672.1929325387,
672.276521621641,672.360244889198,672.440924605094,672.52466331694,672.608298828308,
672.691851271706,672.775340707557,672.858794658171,672.942231152017,673.025668261773,
673.109124056691,673.19266854942,673.276257632361,673.359980899919,673.440660615815,
673.524399327661,673.608034839029,673.691587282427,673.775076718278,673.858530668892,
673.941967162738,674.025404272494,674.108860067412,674.192404560142,674.275993643083,
674.35971691064,674.440396626535,674.524150690143,674.60777218701,674.691317187497,
674.774803857193,674.858250318129,674.941693339784,675.025130422603,675.108618520543,
675.190769163306),.UNSPECIFIED.);
#479=B_SPLINE_CURVE_WITH_KNOTS('',3,(#66028,#66029,#66030,#66031,#66032,
#66033,#66034,#66035,#66036,#66037,#66038,#66039,#66040,#66041,#66042,#66043,
#66044,#66045,#66046,#66047,#66048,#66049,#66050,#66051,#66052,#66053,#66054,
#66055,#66056,#66057,#66058,#66059,#66060,#66061,#66062,#66063,#66064,#66065,
#66066,#66067,#66068,#66069,#66070,#66071,#66072,#66073,#66074,#66075,#66076,
#66077,#66078,#66079,#66080,#66081,#66082,#66083,#66084,#66085,#66086,#66087,
#66088,#66089,#66090,#66091,#66092,#66093,#66094,#66095,#66096,#66097,#66098,
#66099,#66100,#66101,#66102,#66103,#66104,#66105,#66106,#66107,#66108,#66109,
#66110,#66111,#66112,#66113,#66114,#66115,#66116,#66117,#66118,#66119,#66120,
#66121,#66122,#66123,#66124,#66125,#66126,#66127,#66128,#66129,#66130,#66131,
#66132,#66133,#66134,#66135,#66136,#66137,#66138,#66139,#66140,#66141,#66142,
#66143,#66144,#66145,#66146,#66147,#66148,#66149,#66150,#66151,#66152,#66153,
#66154,#66155,#66156,#66157,#66158,#66159,#66160,#66161,#66162,#66163,#66164,
#66165,#66166,#66167,#66168,#66169,#66170,#66171,#66172,#66173,#66174,#66175,
#66176,#66177,#66178,#66179,#66180,#66181,#66182,#66183,#66184,#66185,#66186,
#66187,#66188,#66189,#66190,#66191,#66192,#66193,#66194,#66195,#66196,#66197,
#66198,#66199,#66200,#66201,#66202,#66203,#66204,#66205,#66206,#66207,#66208,
#66209,#66210,#66211,#66212,#66213,#66214,#66215,#66216,#66217,#66218,#66219,
#66220,#66221,#66222,#66223,#66224,#66225,#66226,#66227,#66228,#66229,#66230,
#66231,#66232,#66233,#66234,#66235,#66236,#66237,#66238,#66239,#66240,#66241,
#66242,#66243,#66244,#66245,#66246,#66247),.UNSPECIFIED.,.F.,.F.,(4,3,3,
3,3,3,3,3,3,3,3,3,3,3,3,3,3,3,3,3,3,3,3,3,3,3,3,3,3,3,3,3,3,3,3,3,3,3,3,
3,3,3,3,3,3,3,3,3,3,3,3,3,3,3,3,3,3,3,3,3,3,3,3,3,3,3,3,3,3,3,3,3,3,4),
(675.442420521784,675.528315210093,675.611410310749,675.694502128589,675.777609010005,
675.860749307999,675.943986969613,676.027282886383,676.110698695133,676.129578028259,
676.213316740105,676.296952251472,676.380504694871,676.463994130722,676.547448081336,
676.630884575182,676.714321684938,676.797777479856,676.881321972585,676.964911055526,
677.048634323084,677.129314038979,677.213052750825,677.296688262192,677.380240705591,
677.463730141442,677.547184092056,677.630620585902,677.714057695657,677.797513490575,
677.881057983305,677.964647066246,678.048370333803,678.129050049699,678.212788761545,
678.296424272913,678.379976716311,678.463466152162,678.546920102776,678.630356596622,
678.713793706377,678.797249501295,678.880793994025,678.964383076966,679.048106344523,
679.128786060419,679.212524772265,679.296160283633,679.379712727031,679.463202162882,
679.546656113496,679.630092607342,679.713529717097,679.796985512015,679.880530004744,
679.964119087685,680.047842355243,680.128522071139,680.212260782985,680.295896294352,
680.379448737751,680.462938173603,680.546392124216,680.629828618062,680.713265727818,
680.796721522735,680.880266015465,680.963855098406,681.047578365964,681.128258081859,
681.214942907917,681.299856777557,681.387427081823,681.47499738609),
 .UNSPECIFIED.);
#480=B_SPLINE_CURVE_WITH_KNOTS('',3,(#66248,#66249,#66250,#66251,#66252,
#66253,#66254,#66255,#66256,#66257),.UNSPECIFIED.,.F.,.F.,(4,3,3,4),(675.19171294655,
675.291977238445,675.391163108053,675.442420521618),.UNSPECIFIED.);
#481=B_SPLINE_CURVE_WITH_KNOTS('',3,(#66259,#66260,#66261,#66262,#66263,
#66264,#66265,#66266,#66267,#66268,#66269,#66270,#66271),.UNSPECIFIED.,
 .F.,.F.,(4,3,3,3,4),(675.190769163306,675.274357383231,675.358080193425,
675.440132637255,675.442420521788),.UNSPECIFIED.);
#482=B_SPLINE_CURVE_WITH_KNOTS('',3,(#66272,#66273,#66274,#66275,#66276,
#66277,#66278,#66279,#66280,#66281,#66282,#66283,#66284,#66285,#66286,#66287,
#66288,#66289,#66290,#66291,#66292,#66293,#66294,#66295,#66296,#66297,#66298,
#66299,#66300,#66301,#66302,#66303,#66304,#66305,#66306,#66307,#66308,#66309,
#66310,#66311,#66312,#66313,#66314,#66315,#66316,#66317,#66318,#66319,#66320,
#66321,#66322,#66323,#66324,#66325,#66326,#66327,#66328,#66329,#66330,#66331,
#66332,#66333,#66334,#66335,#66336,#66337,#66338,#66339,#66340,#66341,#66342,
#66343,#66344,#66345,#66346,#66347,#66348,#66349,#66350,#66351,#66352,#66353,
#66354,#66355,#66356,#66357,#66358,#66359,#66360,#66361,#66362,#66363,#66364,
#66365,#66366,#66367,#66368,#66369,#66370,#66371,#66372,#66373,#66374,#66375,
#66376,#66377,#66378,#66379,#66380,#66381,#66382,#66383,#66384,#66385,#66386,
#66387,#66388,#66389,#66390,#66391,#66392,#66393,#66394,#66395,#66396,#66397,
#66398,#66399,#66400,#66401,#66402,#66403,#66404,#66405,#66406,#66407,#66408,
#66409,#66410,#66411,#66412,#66413,#66414,#66415,#66416,#66417,#66418,#66419,
#66420,#66421,#66422,#66423,#66424,#66425,#66426,#66427,#66428,#66429,#66430,
#66431,#66432,#66433,#66434,#66435,#66436,#66437,#66438,#66439,#66440,#66441,
#66442,#66443,#66444,#66445,#66446,#66447,#66448,#66449,#66450,#66451,#66452,
#66453,#66454,#66455,#66456,#66457,#66458,#66459,#66460,#66461,#66462,#66463,
#66464,#66465,#66466,#66467,#66468,#66469,#66470,#66471,#66472,#66473,#66474,
#66475,#66476,#66477,#66478,#66479,#66480,#66481,#66482,#66483,#66484,#66485,
#66486,#66487,#66488,#66489,#66490,#66491),.UNSPECIFIED.,.F.,.F.,(4,3,3,
3,3,3,3,3,3,3,3,3,3,3,3,3,3,3,3,3,3,3,3,3,3,3,3,3,3,3,3,3,3,3,3,3,3,3,3,
3,3,3,3,3,3,3,3,3,3,3,3,3,3,3,3,3,3,3,3,3,3,3,3,3,3,3,3,3,3,3,3,3,3,4),
(675.442420521969,675.526124572569,675.6097254465,675.693243313824,675.776698272257,
675.860117909839,675.943520249349,676.026923396924,676.110345455421,676.193856225904,
676.277411853459,676.361101048798,676.439868647975,676.523607359821,676.607242871188,
676.690795314587,676.774284750438,676.857738701052,676.941175194898,677.024612304653,
677.10806809957,677.1916125923,677.275201675241,677.358924942799,677.439604658695,
677.523343370541,677.606978881909,677.690531325307,677.774020761158,677.857474711772,
677.940911205618,678.024348315373,678.107804110291,678.191348603021,678.274937685962,
678.358660953519,678.439340669415,678.523079381261,678.606714892628,678.690267336027,
678.773756771878,678.857210722491,678.940647216338,679.024084326093,679.107540121011,
679.191084613741,679.274673696682,679.358396964239,679.439076680135,679.522815391981,
679.606450903349,679.690003346748,679.773492782599,679.856946733213,679.940383227059,
680.023820336815,680.107276131732,680.190820624462,680.274409707403,680.358132974961,
680.438812690855,680.522551402701,680.606186914068,680.689739357467,680.773228793319,
680.856682743933,680.940119237779,681.023556347535,681.107012142452,681.190556635182,
681.274145718123,681.357868985681,681.438548701576,681.474758439067),
 .UNSPECIFIED.);
#483=B_SPLINE_CURVE_WITH_KNOTS('',3,(#66497,#66498,#66499,#66500,#66501,
#66502,#66503,#66504,#66505,#66506,#66507,#66508,#66509,#66510,#66511,#66512,
#66513,#66514,#66515,#66516,#66517,#66518,#66519,#66520,#66521,#66522,#66523,
#66524,#66525,#66526,#66527,#66528,#66529,#66530,#66531,#66532,#66533,#66534,
#66535,#66536,#66537,#66538,#66539,#66540,#66541,#66542,#66543,#66544,#66545,
#66546,#66547,#66548,#66549,#66550,#66551,#66552,#66553,#66554,#66555,#66556,
#66557,#66558,#66559,#66560,#66561,#66562,#66563,#66564,#66565,#66566,#66567,
#66568,#66569,#66570,#66571,#66572,#66573,#66574,#66575,#66576,#66577,#66578,
#66579,#66580,#66581,#66582,#66583,#66584,#66585,#66586,#66587,#66588,#66589,
#66590,#66591,#66592,#66593,#66594,#66595,#66596,#66597,#66598,#66599,#66600,
#66601,#66602,#66603,#66604,#66605,#66606,#66607,#66608,#66609,#66610,#66611,
#66612,#66613,#66614,#66615,#66616,#66617,#66618,#66619,#66620,#66621,#66622,
#66623,#66624,#66625,#66626,#66627,#66628,#66629,#66630,#66631,#66632,#66633,
#66634,#66635,#66636,#66637,#66638,#66639,#66640,#66641,#66642,#66643,#66644,
#66645,#66646,#66647,#66648,#66649,#66650,#66651,#66652,#66653,#66654,#66655,
#66656,#66657,#66658,#66659,#66660,#66661,#66662,#66663,#66664,#66665,#66666,
#66667,#66668,#66669,#66670,#66671,#66672,#66673,#66674,#66675,#66676,#66677,
#66678,#66679,#66680,#66681,#66682,#66683,#66684,#66685,#66686,#66687,#66688,
#66689,#66690,#66691,#66692,#66693,#66694,#66695,#66696,#66697,#66698,#66699,
#66700,#66701,#66702,#66703,#66704,#66705,#66706,#66707,#66708,#66709,#66710,
#66711,#66712,#66713,#66714,#66715,#66716),.UNSPECIFIED.,.F.,.F.,(4,3,3,
3,3,3,3,3,3,3,3,3,3,3,3,3,3,3,3,3,3,3,3,3,3,3,3,3,3,3,3,3,3,3,3,3,3,3,3,
3,3,3,3,3,3,3,3,3,3,3,3,3,3,3,3,3,3,3,3,3,3,3,3,3,3,3,3,3,3,3,3,3,3,4),
(681.72560582914,681.817549997391,681.90997903633,682.00265856607,682.095670523113,
682.127994092579,682.211732804426,682.295368315794,682.378920759193,682.462410195044,
682.545864145659,682.629300639506,682.712737749262,682.79619354418,682.879738036911,
682.963327119852,683.04705038741,683.1277301033,683.211468815146,683.295104326513,
683.378656769912,683.462146205763,683.545600156376,683.629036650223,683.712473759978,
683.795929554896,683.879474047625,683.963063130566,684.046786398124,684.12746611402,
684.211204825866,684.294840337233,684.378392780632,684.461882216483,684.545336167096,
684.628772660942,684.712209770698,684.795665565615,684.879210058345,684.962799141285,
685.046522408843,685.12720212474,685.210940836586,685.294576347954,685.378128791352,
685.461618227203,685.545072177817,685.628508671663,685.711945781419,685.795401576337,
685.878946069066,685.962535152007,686.046258419565,686.12693813546,686.210676847306,
686.294312358673,686.377864802072,686.461354237923,686.544808188536,686.628244682383,
686.711681792138,686.795137587055,686.878682079785,686.962271162726,687.045994430283,
687.12667414618,687.209254276124,687.291739747078,687.374149702101,687.456503213914,
687.538827688801,687.621134044061,687.703464025962,687.75697424715),
 .UNSPECIFIED.);
#484=B_SPLINE_CURVE_WITH_KNOTS('',3,(#66717,#66718,#66719,#66720,#66721,
#66722,#66723,#66724,#66725,#66726),.UNSPECIFIED.,.F.,.F.,(4,3,3,4),(681.47499738609,
681.559659480984,681.64428402035,681.725605828964),.UNSPECIFIED.);
#485=B_SPLINE_CURVE_WITH_KNOTS('',3,(#66728,#66729,#66730,#66731,#66732,
#66733,#66734,#66735,#66736,#66737),.UNSPECIFIED.,.F.,.F.,(4,3,3,4),(681.474758439067,
681.578295068869,681.680374910821,681.725605828844),.UNSPECIFIED.);
#486=B_SPLINE_CURVE_WITH_KNOTS('',3,(#66738,#66739,#66740,#66741,#66742,
#66743,#66744,#66745,#66746,#66747,#66748,#66749,#66750,#66751,#66752,#66753,
#66754,#66755,#66756,#66757,#66758,#66759,#66760,#66761,#66762,#66763,#66764,
#66765,#66766,#66767,#66768,#66769,#66770,#66771,#66772,#66773,#66774,#66775,
#66776,#66777,#66778,#66779,#66780,#66781,#66782,#66783,#66784,#66785,#66786,
#66787,#66788,#66789,#66790,#66791,#66792,#66793,#66794,#66795,#66796,#66797,
#66798,#66799,#66800,#66801,#66802,#66803,#66804,#66805,#66806,#66807,#66808,
#66809,#66810,#66811,#66812,#66813,#66814,#66815,#66816,#66817,#66818,#66819,
#66820,#66821,#66822,#66823,#66824,#66825,#66826,#66827,#66828,#66829,#66830,
#66831,#66832,#66833,#66834,#66835,#66836,#66837,#66838,#66839,#66840,#66841,
#66842,#66843,#66844,#66845,#66846,#66847,#66848,#66849,#66850,#66851,#66852,
#66853,#66854,#66855,#66856,#66857,#66858,#66859,#66860,#66861,#66862,#66863,
#66864,#66865,#66866,#66867,#66868,#66869,#66870,#66871,#66872,#66873,#66874,
#66875,#66876,#66877,#66878,#66879,#66880,#66881,#66882,#66883,#66884,#66885,
#66886,#66887,#66888,#66889,#66890,#66891,#66892,#66893,#66894,#66895,#66896,
#66897,#66898,#66899,#66900,#66901,#66902,#66903,#66904,#66905,#66906,#66907,
#66908,#66909,#66910,#66911,#66912,#66913,#66914,#66915,#66916,#66917,#66918,
#66919,#66920,#66921,#66922,#66923,#66924,#66925,#66926,#66927,#66928,#66929,
#66930,#66931,#66932,#66933,#66934,#66935,#66936,#66937,#66938,#66939,#66940,
#66941,#66942,#66943,#66944,#66945,#66946,#66947,#66948,#66949,#66950,#66951,
#66952,#66953,#66954,#66955,#66956,#66957),.UNSPECIFIED.,.F.,.F.,(4,3,3,
3,3,3,3,3,3,3,3,3,3,3,3,3,3,3,3,3,3,3,3,3,3,3,3,3,3,3,3,3,3,3,3,3,3,3,3,
3,3,3,3,3,3,3,3,3,3,3,3,3,3,3,3,3,3,3,3,3,3,3,3,3,3,3,3,3,3,3,3,3,3,4),
(681.725605828968,681.808449156847,681.891261971294,681.974061324514,682.056865823715,
682.13969407653,682.22261324518,682.305582521765,682.388677839725,682.438284712296,
682.522023424142,682.605658935509,682.689211378908,682.772700814759,682.856154765373,
682.939591259219,683.023028368974,683.106484163892,683.190028656622,683.273617739562,
683.35734100712,683.438020723016,683.521759434862,683.605394946229,683.688947389627,
683.772436825478,683.855890776091,683.939327269938,684.022764379693,684.10622017461,
684.18976466734,684.273353750281,684.357077017838,684.437756733736,684.521495445582,
684.60513095695,684.688683400348,684.772172836199,684.855626786813,684.939063280659,
685.022500390415,685.105956185333,685.189500678062,685.273089761004,685.356813028562,
685.437492744456,685.521231456302,685.604866967669,685.688419411067,685.771908846918,
685.855362797532,685.938799291378,686.022236401133,686.10569219605,686.18923668878,
686.272825771721,686.356549039278,686.437228755176,686.520967467022,686.60460297839,
686.688155421788,686.771644857639,686.855098808253,686.938535302099,687.021972411854,
687.105428206772,687.188972699502,687.272561782443,687.35628505,687.436964765896,
687.52263490387,687.608196454512,687.693631976101,687.758281420251),
 .UNSPECIFIED.);
#487=B_SPLINE_CURVE_WITH_KNOTS('',3,(#66963,#66964,#66965,#66966,#66967,
#66968,#66969,#66970,#66971,#66972,#66973,#66974,#66975,#66976,#66977,#66978,
#66979,#66980,#66981,#66982,#66983,#66984,#66985,#66986,#66987,#66988,#66989,
#66990,#66991,#66992,#66993,#66994,#66995,#66996,#66997,#66998,#66999,#67000,
#67001,#67002,#67003,#67004,#67005,#67006,#67007,#67008,#67009,#67010,#67011,
#67012,#67013,#67014,#67015,#67016,#67017,#67018,#67019,#67020,#67021,#67022,
#67023,#67024,#67025,#67026,#67027,#67028,#67029,#67030,#67031,#67032,#67033,
#67034,#67035,#67036,#67037,#67038,#67039,#67040,#67041,#67042,#67043,#67044,
#67045,#67046,#67047,#67048,#67049,#67050,#67051,#67052,#67053,#67054,#67055,
#67056,#67057,#67058,#67059,#67060,#67061,#67062,#67063,#67064,#67065,#67066,
#67067,#67068,#67069,#67070,#67071,#67072,#67073,#67074,#67075,#67076,#67077,
#67078,#67079,#67080,#67081,#67082,#67083,#67084,#67085,#67086,#67087,#67088,
#67089,#67090,#67091,#67092,#67093,#67094,#67095,#67096,#67097,#67098,#67099,
#67100,#67101,#67102,#67103,#67104,#67105,#67106,#67107,#67108,#67109,#67110,
#67111,#67112,#67113,#67114,#67115,#67116,#67117,#67118,#67119,#67120,#67121,
#67122,#67123,#67124,#67125,#67126,#67127,#67128,#67129,#67130,#67131,#67132,
#67133,#67134,#67135,#67136,#67137,#67138,#67139,#67140,#67141,#67142,#67143,
#67144,#67145,#67146,#67147,#67148,#67149,#67150,#67151,#67152,#67153,#67154,
#67155,#67156,#67157,#67158,#67159,#67160,#67161,#67162,#67163,#67164,#67165,
#67166,#67167,#67168,#67169,#67170,#67171,#67172,#67173,#67174,#67175,#67176,
#67177,#67178,#67179),.UNSPECIFIED.,.F.,.F.,(4,3,3,3,3,3,3,3,3,3,3,3,3,
3,3,3,3,3,3,3,3,3,3,3,3,3,3,3,3,3,3,3,3,3,3,3,3,3,3,3,3,3,3,3,3,3,3,3,3,
3,3,3,3,3,3,3,3,3,3,3,3,3,3,3,3,3,3,3,3,3,3,3,4),(688.008791136144,688.1264101569,
688.210148868748,688.293784380117,688.377336823517,688.460826259369,688.544280209985,
688.627716703833,688.71115381359,688.794609608509,688.87815410124,688.961743184183,
689.045466451742,689.126146167621,689.209884879467,689.293520390834,689.377072834232,
689.460562270083,689.544016220696,689.627452714542,689.710889824298,689.794345619215,
689.877890111945,689.961479194885,690.045202462443,690.125882178341,690.209620890187,
690.293256401554,690.376808844952,690.460298280803,690.543752231416,690.627188725262,
690.710625835017,690.794081629935,690.877626122664,690.961215205605,691.044938473162,
691.125618189061,691.209356900907,691.292992412275,691.376544855673,691.460034291525,
691.543488242138,691.626924735985,691.710361845741,691.793817640658,691.877362133388,
691.960951216329,692.044674483887,692.125354199781,692.209092911627,692.292728422995,
692.376280866393,692.459770302244,692.543224252858,692.626660746704,692.71009785646,
692.793553651377,692.877098144107,692.960687227048,693.044410494605,693.125090210501,
693.208833802616,693.292473082083,693.376028186146,693.459515473079,693.542965641862,
693.62639678084,693.709826961812,693.79331488005,693.87683051431,693.960451995844,
694.040510109002),.UNSPECIFIED.);
#488=B_SPLINE_CURVE_WITH_KNOTS('',3,(#67180,#67181,#67182,#67183,#67184,
#67185,#67186,#67187,#67188,#67189),.UNSPECIFIED.,.F.,.F.,(4,3,3,4),(687.75697424715,
687.839375275049,687.92408320553,688.00879113601),.UNSPECIFIED.);
#489=B_SPLINE_CURVE_WITH_KNOTS('',3,(#67191,#67192,#67193,#67194,#67195,
#67196,#67197,#67198,#67199,#67200),.UNSPECIFIED.,.F.,.F.,(4,3,3,4),(687.758281420251,
687.843572196486,687.928799866004,688.008791136148),.UNSPECIFIED.);
#490=B_SPLINE_CURVE_WITH_KNOTS('',3,(#67201,#67202,#67203,#67204,#67205,
#67206,#67207,#67208,#67209,#67210,#67211,#67212,#67213,#67214,#67215,#67216,
#67217,#67218,#67219,#67220,#67221,#67222,#67223,#67224,#67225,#67226,#67227,
#67228,#67229,#67230,#67231,#67232,#67233,#67234,#67235,#67236,#67237,#67238,
#67239,#67240,#67241,#67242,#67243,#67244,#67245,#67246,#67247,#67248,#67249,
#67250,#67251,#67252,#67253,#67254,#67255,#67256,#67257,#67258,#67259,#67260,
#67261,#67262,#67263,#67264,#67265,#67266,#67267,#67268,#67269,#67270,#67271,
#67272,#67273,#67274,#67275,#67276,#67277,#67278,#67279,#67280,#67281,#67282,
#67283,#67284,#67285,#67286,#67287,#67288,#67289,#67290,#67291,#67292,#67293,
#67294,#67295,#67296,#67297,#67298,#67299,#67300,#67301,#67302,#67303,#67304,
#67305,#67306,#67307,#67308,#67309,#67310,#67311,#67312,#67313,#67314,#67315,
#67316,#67317,#67318,#67319,#67320,#67321,#67322,#67323,#67324,#67325,#67326,
#67327,#67328,#67329,#67330,#67331,#67332,#67333,#67334,#67335,#67336,#67337,
#67338,#67339,#67340,#67341,#67342,#67343,#67344,#67345,#67346,#67347,#67348,
#67349,#67350,#67351,#67352,#67353,#67354,#67355,#67356,#67357,#67358,#67359,
#67360,#67361,#67362,#67363,#67364,#67365,#67366,#67367,#67368,#67369,#67370,
#67371,#67372,#67373,#67374,#67375,#67376,#67377,#67378,#67379,#67380,#67381,
#67382,#67383,#67384,#67385,#67386,#67387,#67388,#67389,#67390,#67391,#67392,
#67393,#67394,#67395,#67396,#67397,#67398,#67399,#67400,#67401,#67402,#67403,
#67404,#67405,#67406,#67407,#67408,#67409,#67410,#67411,#67412,#67413,#67414,
#67415,#67416,#67417,#67418,#67419,#67420),.UNSPECIFIED.,.F.,.F.,(4,3,3,
3,3,3,3,3,3,3,3,3,3,3,3,3,3,3,3,3,3,3,3,3,3,3,3,3,3,3,3,3,3,3,3,3,3,3,3,
3,3,3,3,3,3,3,3,3,3,3,3,3,3,3,3,3,3,3,3,3,3,3,3,3,3,3,3,3,3,3,3,3,3,4),
(688.008791136294,688.099325354651,688.190249693613,688.281371889162,688.372797362083,
688.436700776617,688.520439488463,688.60407499983,688.687627443229,688.77111687908,
688.854570829693,688.93800732354,689.021444433295,689.104900228213,689.188444720942,
689.272033803883,689.355757071441,689.436436787337,689.520175499183,689.60381101055,
689.687363453949,689.7708528898,689.854306840413,689.937743334259,690.021180444015,
690.104636238933,690.188180731662,690.271769814603,690.355493082161,690.436172798057,
690.519911509903,690.603547021271,690.687099464669,690.77058890052,690.854042851134,
690.93747934498,691.020916454735,691.104372249653,691.187916742383,691.271505825324,
691.355229092881,691.435908808777,691.519647520623,691.60328303199,691.686835475389,
691.77032491124,691.853778861854,691.9372153557,692.020652465456,692.104108260373,
692.187652753103,692.271241836044,692.354965103602,692.435644819497,692.519383531343,
692.60301904271,692.686571486109,692.77006092196,692.853514872574,692.93695136642,
693.020388476175,693.103844271093,693.187388763822,693.270977846763,693.354701114321,
693.435380830217,693.517877924792,693.600280114073,693.682606598185,693.76487650462,
693.847114889009,693.929335342606,694.011572191676,694.04020608688),
 .UNSPECIFIED.);
#491=B_SPLINE_CURVE_WITH_KNOTS('',3,(#67426,#67427,#67428,#67429,#67430,
#67431,#67432,#67433,#67434,#67435,#67436,#67437,#67438,#67439,#67440,#67441,
#67442,#67443,#67444,#67445,#67446,#67447,#67448,#67449,#67450,#67451,#67452,
#67453,#67454,#67455,#67456,#67457,#67458,#67459,#67460,#67461,#67462,#67463,
#67464,#67465,#67466,#67467,#67468,#67469,#67470,#67471,#67472,#67473,#67474,
#67475,#67476,#67477,#67478,#67479,#67480,#67481,#67482,#67483,#67484,#67485,
#67486,#67487,#67488,#67489,#67490,#67491,#67492,#67493,#67494,#67495,#67496,
#67497,#67498,#67499,#67500,#67501,#67502,#67503,#67504,#67505,#67506,#67507,
#67508,#67509,#67510,#67511,#67512,#67513,#67514,#67515,#67516,#67517,#67518,
#67519,#67520,#67521,#67522,#67523,#67524,#67525,#67526,#67527,#67528,#67529,
#67530,#67531,#67532,#67533,#67534,#67535,#67536,#67537,#67538,#67539,#67540,
#67541,#67542,#67543,#67544,#67545,#67546,#67547,#67548,#67549,#67550,#67551,
#67552,#67553,#67554,#67555,#67556,#67557,#67558,#67559,#67560,#67561,#67562,
#67563,#67564,#67565,#67566,#67567,#67568,#67569,#67570,#67571,#67572,#67573,
#67574,#67575,#67576,#67577,#67578,#67579,#67580,#67581,#67582,#67583,#67584,
#67585,#67586,#67587,#67588,#67589,#67590,#67591,#67592,#67593,#67594,#67595,
#67596,#67597,#67598,#67599,#67600,#67601,#67602,#67603,#67604,#67605,#67606,
#67607,#67608,#67609,#67610,#67611,#67612,#67613,#67614,#67615,#67616,#67617,
#67618,#67619,#67620,#67621,#67622,#67623,#67624,#67625,#67626,#67627,#67628,
#67629,#67630,#67631,#67632,#67633,#67634,#67635,#67636,#67637,#67638,#67639,
#67640,#67641,#67642,#67643,#67644,#67645),.UNSPECIFIED.,.F.,.F.,(4,3,3,
3,3,3,3,3,3,3,3,3,3,3,3,3,3,3,3,3,3,3,3,3,3,3,3,3,3,3,3,3,3,3,3,3,3,3,3,
3,3,3,3,3,3,3,3,3,3,3,3,3,3,3,3,3,3,3,3,3,3,3,3,3,3,3,3,3,3,3,3,3,3,4),
(694.291976443512,694.374348250688,694.456642156296,694.540132165751,694.62234238023,
694.704542973122,694.786752978043,694.871205291518,694.953534528726,695.039048380334,
695.124562231941,695.208300943787,695.291936455154,695.375488898553,695.458978334404,
695.542432285018,695.625868778864,695.709305888619,695.792761683537,695.876306176267,
695.959895259208,696.043618526765,696.124298242661,696.208036954507,696.291672465874,
696.375224909273,696.458714345123,696.542168295737,696.625604789583,696.709041899339,
696.792497694256,696.876042186986,696.959631269927,697.043354537484,697.124034253381,
697.207772965227,697.291408476594,697.374960919993,697.458450355845,697.541904306458,
697.625340800304,697.70877791006,697.792233704978,697.875778197708,697.959367280649,
698.043090548206,698.123770264101,698.207508975947,698.291144487314,698.374696930713,
698.458186366563,698.541640317177,698.625076811023,698.708513920779,698.791969715697,
698.875514208427,698.959103291368,699.042826558925,699.123506274822,699.207244986668,
699.290880498036,699.374432941434,699.457922377285,699.541376327899,699.624812821745,
699.708249931501,699.791705726419,699.875250219148,699.958839302089,700.042562569647,
700.123242285542,700.213452256298,700.303435157064,700.324858639641),
 .UNSPECIFIED.);
#492=B_SPLINE_CURVE_WITH_KNOTS('',3,(#67646,#67647,#67648,#67649,#67650,
#67651,#67652,#67653,#67654,#67655),.UNSPECIFIED.,.F.,.F.,(4,3,3,4),(694.040510109002,
694.124826221221,694.257684296808,694.291976443323),.UNSPECIFIED.);
#493=B_SPLINE_CURVE_WITH_KNOTS('',3,(#67657,#67658,#67659,#67660,#67661,
#67662,#67663,#67664,#67665,#67666),.UNSPECIFIED.,.F.,.F.,(4,3,3,4),(694.04020608688,
694.122507158593,694.207241800901,694.291976443208),.UNSPECIFIED.);
#494=B_SPLINE_CURVE_WITH_KNOTS('',3,(#67667,#67668,#67669,#67670,#67671,
#67672,#67673,#67674,#67675,#67676,#67677,#67678,#67679,#67680,#67681,#67682,
#67683,#67684,#67685,#67686,#67687,#67688,#67689,#67690,#67691,#67692,#67693,
#67694,#67695,#67696,#67697,#67698,#67699,#67700,#67701,#67702,#67703,#67704,
#67705,#67706,#67707,#67708,#67709,#67710,#67711,#67712,#67713,#67714,#67715,
#67716,#67717,#67718,#67719,#67720,#67721,#67722,#67723,#67724,#67725,#67726,
#67727,#67728,#67729,#67730,#67731,#67732,#67733,#67734,#67735,#67736,#67737,
#67738,#67739,#67740,#67741,#67742,#67743,#67744,#67745,#67746,#67747,#67748,
#67749,#67750,#67751,#67752,#67753,#67754,#67755,#67756,#67757,#67758,#67759,
#67760,#67761,#67762,#67763,#67764,#67765,#67766,#67767,#67768,#67769,#67770,
#67771,#67772,#67773,#67774,#67775,#67776,#67777,#67778,#67779,#67780,#67781,
#67782,#67783,#67784,#67785,#67786,#67787,#67788,#67789,#67790,#67791,#67792,
#67793,#67794,#67795,#67796,#67797,#67798,#67799,#67800,#67801,#67802,#67803,
#67804,#67805,#67806,#67807,#67808,#67809,#67810,#67811,#67812,#67813,#67814,
#67815,#67816,#67817,#67818,#67819,#67820,#67821,#67822,#67823,#67824,#67825,
#67826,#67827,#67828,#67829,#67830,#67831,#67832,#67833,#67834,#67835,#67836,
#67837,#67838,#67839,#67840,#67841,#67842,#67843,#67844,#67845,#67846,#67847,
#67848,#67849,#67850,#67851,#67852,#67853,#67854,#67855,#67856,#67857,#67858,
#67859,#67860,#67861,#67862,#67863,#67864,#67865,#67866,#67867,#67868,#67869,
#67870,#67871,#67872,#67873,#67874,#67875,#67876,#67877,#67878,#67879,#67880,
#67881,#67882,#67883),.UNSPECIFIED.,.F.,.F.,(4,3,3,3,3,3,3,3,3,3,3,3,3,
3,3,3,3,3,3,3,3,3,3,3,3,3,3,3,3,3,3,3,3,3,3,3,3,3,3,3,3,3,3,3,3,3,3,3,3,
3,3,3,3,3,3,3,3,3,3,3,3,3,3,3,3,3,3,3,3,3,3,3,4),(694.291976443327,694.435116840937,
694.518855552783,694.602491064151,694.686043507549,694.7695329434,694.852986894013,
694.93642338786,695.019860497615,695.103316292533,695.186860785263,695.270449868204,
695.354173135761,695.434852851657,695.518591563503,695.60222707487,695.685779518269,
695.76926895412,695.852722904734,695.93615939858,696.019596508335,696.103052303253,
696.186596795983,696.270185878924,696.353909146481,696.434588862377,696.518327574223,
696.601963085591,696.685515528989,696.76900496484,696.852458915454,696.9358954093,
697.019332519056,697.102788313974,697.186332806703,697.269921889645,697.353645157202,
697.434324873098,697.518063584944,697.601699096312,697.68525153971,697.768740975561,
697.852194926175,697.935631420021,698.019068529777,698.102524324694,698.186068817424,
698.269657900365,698.353381167923,698.434060883818,698.517799595664,698.601435107031,
698.68498755043,698.768476986281,698.851930936895,698.935367430741,699.018804540496,
699.102260335414,699.185804828143,699.269393911084,699.353117178642,699.433796894538,
699.517542031029,699.601182517174,699.684738491684,699.768225359862,699.851674632092,
699.935104396973,700.018532726135,700.102013075559,700.18552094675,700.269121009406,
700.323619593279),.UNSPECIFIED.);
#495=B_SPLINE_CURVE_WITH_KNOTS('',3,(#67889,#67890,#67891,#67892,#67893,
#67894,#67895,#67896,#67897,#67898,#67899,#67900,#67901,#67902,#67903,#67904,
#67905,#67906,#67907,#67908,#67909,#67910,#67911,#67912,#67913,#67914,#67915,
#67916,#67917,#67918,#67919,#67920,#67921,#67922,#67923,#67924,#67925,#67926,
#67927,#67928,#67929,#67930,#67931,#67932,#67933,#67934,#67935,#67936,#67937,
#67938,#67939,#67940,#67941,#67942,#67943,#67944,#67945,#67946,#67947,#67948,
#67949,#67950,#67951,#67952,#67953,#67954,#67955,#67956,#67957,#67958,#67959,
#67960,#67961,#67962,#67963,#67964,#67965,#67966,#67967,#67968,#67969,#67970,
#67971,#67972,#67973,#67974,#67975,#67976,#67977,#67978,#67979,#67980,#67981,
#67982,#67983,#67984,#67985,#67986,#67987,#67988,#67989,#67990,#67991,#67992,
#67993,#67994,#67995,#67996,#67997,#67998,#67999,#68000,#68001,#68002,#68003,
#68004,#68005,#68006,#68007,#68008,#68009,#68010,#68011,#68012,#68013,#68014,
#68015,#68016,#68017,#68018,#68019,#68020,#68021,#68022,#68023,#68024,#68025,
#68026,#68027,#68028,#68029,#68030,#68031,#68032,#68033,#68034,#68035,#68036,
#68037,#68038,#68039,#68040,#68041,#68042,#68043,#68044,#68045,#68046,#68047,
#68048,#68049,#68050,#68051,#68052,#68053,#68054,#68055,#68056,#68057,#68058,
#68059,#68060,#68061,#68062,#68063,#68064,#68065,#68066,#68067,#68068,#68069,
#68070,#68071,#68072,#68073,#68074,#68075,#68076,#68077,#68078,#68079,#68080,
#68081,#68082,#68083,#68084,#68085,#68086,#68087,#68088,#68089,#68090,#68091,
#68092,#68093,#68094,#68095,#68096,#68097,#68098,#68099,#68100,#68101,#68102,
#68103,#68104,#68105,#68106,#68107,#68108),.UNSPECIFIED.,.F.,.F.,(4,3,3,
3,3,3,3,3,3,3,3,3,3,3,3,3,3,3,3,3,3,3,3,3,3,3,3,3,3,3,3,3,3,3,3,3,3,3,3,
3,3,3,3,3,3,3,3,3,3,3,3,3,3,3,3,3,3,3,3,3,3,3,3,3,3,3,3,3,3,3,3,3,3,4),
(700.575161750503,700.661020163653,700.746940620048,700.83293660145,700.919083556154,
701.005316158823,701.091705944569,701.122978296262,701.206717008108,701.290352519475,
701.373904962874,701.457394398725,701.540848349338,701.624284843185,701.70772195294,
701.791177747857,701.874722240587,701.958311323528,702.042034591086,702.122714306982,
702.206453018828,702.290088530195,702.373640973594,702.457130409445,702.540584360059,
702.624020853905,702.70745796366,702.790913758578,702.874458251308,702.958047334249,
703.041770601806,703.122450317702,703.206189029548,703.289824540915,703.373376984314,
703.456866420165,703.540320370779,703.623756864625,703.70719397438,703.790649769298,
703.874194262028,703.957783344969,704.041506612527,704.122186328422,704.205925040268,
704.289560551635,704.373112995034,704.456602430885,704.540056381499,704.623492875345,
704.706929985101,704.790385780018,704.873930272748,704.957519355689,705.041242623247,
705.121922339142,705.205661050988,705.289296562355,705.372849005754,705.456338441604,
705.539792392218,705.623228886064,705.70666599582,705.790121790737,705.873666283467,
705.957255366407,706.040978633965,706.121658349863,706.20452908262,706.287300780193,
706.369978943579,706.452602252079,706.535195449455,706.607048847776),
 .UNSPECIFIED.);
#496=B_SPLINE_CURVE_WITH_KNOTS('',3,(#68109,#68110,#68111,#68112,#68113,
#68114,#68115,#68116,#68117,#68118),.UNSPECIFIED.,.F.,.F.,(4,3,3,4),(700.324858639641,
700.414553711888,700.503984556103,700.575161750398),.UNSPECIFIED.);
#497=B_SPLINE_CURVE_WITH_KNOTS('',3,(#68120,#68121,#68122,#68123,#68124,
#68125,#68126,#68127,#68128,#68129),.UNSPECIFIED.,.F.,.F.,(4,3,3,4),(700.323619593279,
700.407365372727,700.433532905258,700.575161750507),.UNSPECIFIED.);
#498=B_SPLINE_CURVE_WITH_KNOTS('',3,(#68130,#68131,#68132,#68133,#68134,
#68135,#68136,#68137,#68138,#68139,#68140,#68141,#68142,#68143,#68144,#68145,
#68146,#68147,#68148,#68149,#68150,#68151,#68152,#68153,#68154,#68155,#68156,
#68157,#68158,#68159,#68160,#68161,#68162,#68163,#68164,#68165,#68166,#68167,
#68168,#68169,#68170,#68171,#68172,#68173,#68174,#68175,#68176,#68177,#68178,
#68179,#68180,#68181,#68182,#68183,#68184,#68185,#68186,#68187,#68188,#68189,
#68190,#68191,#68192,#68193,#68194,#68195,#68196,#68197,#68198,#68199,#68200,
#68201,#68202,#68203,#68204,#68205,#68206,#68207,#68208,#68209,#68210,#68211,
#68212,#68213,#68214,#68215,#68216,#68217,#68218,#68219,#68220,#68221,#68222,
#68223,#68224,#68225,#68226,#68227,#68228,#68229,#68230,#68231,#68232,#68233,
#68234,#68235,#68236,#68237,#68238,#68239,#68240,#68241,#68242,#68243,#68244,
#68245,#68246,#68247,#68248,#68249,#68250,#68251,#68252,#68253,#68254,#68255,
#68256,#68257,#68258,#68259,#68260,#68261,#68262,#68263,#68264,#68265,#68266,
#68267,#68268,#68269,#68270,#68271,#68272,#68273,#68274,#68275,#68276,#68277,
#68278,#68279,#68280,#68281,#68282,#68283,#68284,#68285,#68286,#68287,#68288,
#68289,#68290,#68291,#68292,#68293,#68294,#68295,#68296,#68297,#68298,#68299,
#68300,#68301,#68302,#68303,#68304,#68305,#68306,#68307,#68308,#68309,#68310,
#68311,#68312,#68313,#68314,#68315,#68316,#68317,#68318,#68319,#68320,#68321,
#68322,#68323,#68324,#68325,#68326,#68327,#68328,#68329,#68330,#68331,#68332,
#68333,#68334,#68335,#68336,#68337,#68338,#68339,#68340,#68341,#68342,#68343,
#68344,#68345,#68346,#68347,#68348,#68349),.UNSPECIFIED.,.F.,.F.,(4,3,3,
3,3,3,3,3,3,3,3,3,3,3,3,3,3,3,3,3,3,3,3,3,3,3,3,3,3,3,3,3,3,3,3,3,3,3,3,
3,3,3,3,3,3,3,3,3,3,3,3,3,3,3,3,3,3,3,3,3,3,3,3,3,3,3,3,3,3,3,3,3,3,4),
(700.575161750627,700.657591715628,700.739937607852,700.822220561261,700.904468957315,
700.986701841693,701.068938230475,701.151197140463,701.233542912853,701.315938523513,
701.398452425323,701.433268915978,701.517007627824,701.600643139191,701.68419558259,
701.767685018441,701.851138969054,701.9345754629,702.018012572656,702.101468367573,
702.185012860303,702.268601943244,702.352325210801,702.433004926698,702.516743638544,
702.600379149912,702.68393159331,702.767421029161,702.850874979775,702.934311473621,
703.017748583377,703.101204378294,703.184748871024,703.268337953965,703.352061221523,
703.432740937418,703.516479649264,703.600115160631,703.68366760403,703.76715703988,
703.850610990494,703.93404748434,704.017484594096,704.100940389013,704.184484881743,
704.268073964684,704.351797232242,704.432476948139,704.516215659985,704.599851171352,
704.683403614751,704.766893050603,704.850347001217,704.933783495063,705.017220604818,
705.100676399736,705.184220892466,705.267809975407,705.351533242964,705.432212958859,
705.515951670705,705.599587182072,705.683139625471,705.766629061321,705.850083011935,
705.933519505781,706.016956615537,706.100412410454,706.183956903184,706.267545986125,
706.351269253682,706.431948969579,706.523434315707,706.608022324974),
 .UNSPECIFIED.);
#499=B_SPLINE_CURVE_WITH_KNOTS('',3,(#68355,#68356,#68357,#68358,#68359,
#68360,#68361,#68362,#68363,#68364,#68365,#68366,#68367,#68368,#68369,#68370,
#68371,#68372,#68373,#68374,#68375,#68376,#68377,#68378,#68379,#68380,#68381,
#68382,#68383,#68384,#68385,#68386,#68387,#68388,#68389,#68390,#68391,#68392,
#68393,#68394,#68395,#68396,#68397,#68398,#68399,#68400,#68401,#68402,#68403,
#68404,#68405,#68406,#68407,#68408,#68409,#68410,#68411,#68412,#68413,#68414,
#68415,#68416,#68417,#68418,#68419,#68420,#68421,#68422,#68423,#68424,#68425,
#68426,#68427,#68428,#68429,#68430,#68431,#68432,#68433,#68434,#68435,#68436,
#68437,#68438,#68439,#68440,#68441,#68442,#68443,#68444,#68445,#68446,#68447,
#68448,#68449,#68450,#68451,#68452,#68453,#68454,#68455,#68456,#68457,#68458,
#68459,#68460,#68461,#68462,#68463,#68464,#68465,#68466,#68467,#68468,#68469,
#68470,#68471,#68472,#68473,#68474,#68475,#68476,#68477,#68478,#68479,#68480,
#68481,#68482,#68483,#68484,#68485,#68486,#68487,#68488,#68489,#68490,#68491,
#68492,#68493,#68494,#68495,#68496,#68497,#68498,#68499,#68500,#68501,#68502,
#68503,#68504,#68505,#68506,#68507,#68508,#68509,#68510,#68511,#68512,#68513,
#68514,#68515,#68516,#68517,#68518,#68519,#68520,#68521,#68522,#68523,#68524,
#68525,#68526,#68527,#68528,#68529,#68530,#68531,#68532,#68533,#68534,#68535,
#68536,#68537,#68538,#68539,#68540,#68541,#68542,#68543,#68544,#68545,#68546,
#68547,#68548,#68549,#68550,#68551,#68552,#68553,#68554,#68555,#68556,#68557,
#68558,#68559,#68560,#68561,#68562,#68563,#68564,#68565,#68566,#68567,#68568,
#68569,#68570,#68571,#68572,#68573,#68574),.UNSPECIFIED.,.F.,.F.,(4,3,3,
3,3,3,3,3,3,3,3,3,3,3,3,3,3,3,3,3,3,3,3,3,3,3,3,3,3,3,3,3,3,3,3,3,3,3,3,
3,3,3,3,3,3,3,3,3,3,3,3,3,3,3,3,3,3,3,3,3,3,3,3,3,3,3,3,3,3,3,3,3,3,4),
(706.858347057831,706.963588322933,707.070863575414,707.121394360583,707.205133072429,
707.288768583797,707.372321027195,707.455810463046,707.539264413659,707.622700907506,
707.706138017261,707.789593812179,707.873138304909,707.95672738785,708.040450655407,
708.121130371303,708.204869083149,708.288504594516,708.372057037915,708.455546473766,
708.539000424379,708.622436918226,708.705874027981,708.789329822899,708.872874315628,
708.956463398569,709.040186666127,709.120866382023,709.204605093869,709.288240605237,
709.371793048635,709.455282484486,709.5387364351,709.622172928946,709.705610038701,
709.789065833619,709.872610326349,709.95619940929,710.039922676847,710.120602392743,
710.204341104589,710.287976615956,710.371529059355,710.455018495206,710.53847244582,
710.621908939666,710.705346049421,710.788801844339,710.872346337069,710.955935420009,
711.039658687567,711.120338403463,711.204077115309,711.287712626676,711.371265070075,
711.454754505926,711.53820845654,711.621644950386,711.705082060141,711.788537855059,
711.872082347789,711.955671430729,712.039394698287,712.120074414183,712.203827182404,
712.289582494793,712.373125247679,712.456610496607,712.540056361948,712.62750969184,
712.710950606173,712.794403120195,712.877906624947,712.889869681513),
 .UNSPECIFIED.);
#500=B_SPLINE_CURVE_WITH_KNOTS('',3,(#68575,#68576,#68577,#68578,#68579,
#68580,#68581,#68582,#68583,#68584),.UNSPECIFIED.,.F.,.F.,(4,3,3,4),(706.607048847776,
706.689634123604,706.773990590643,706.858347057682),.UNSPECIFIED.);
#501=B_SPLINE_CURVE_WITH_KNOTS('',3,(#68586,#68587,#68588,#68589,#68590,
#68591,#68592,#68593,#68594,#68595),.UNSPECIFIED.,.F.,.F.,(4,3,3,4),(706.608022324974,
706.69906592166,706.789770886259,706.858347057541),.UNSPECIFIED.);
#502=B_SPLINE_CURVE_WITH_KNOTS('',3,(#68596,#68597,#68598,#68599,#68600,
#68601,#68602,#68603,#68604,#68605,#68606,#68607,#68608,#68609,#68610,#68611,
#68612,#68613,#68614,#68615,#68616,#68617,#68618,#68619,#68620,#68621,#68622,
#68623,#68624,#68625,#68626,#68627,#68628,#68629,#68630,#68631,#68632,#68633,
#68634,#68635,#68636,#68637,#68638,#68639,#68640,#68641,#68642,#68643,#68644,
#68645,#68646,#68647,#68648,#68649,#68650,#68651,#68652,#68653,#68654,#68655,
#68656,#68657,#68658,#68659,#68660,#68661,#68662,#68663,#68664,#68665,#68666,
#68667,#68668,#68669,#68670,#68671,#68672,#68673,#68674,#68675,#68676,#68677,
#68678,#68679,#68680,#68681,#68682,#68683,#68684,#68685,#68686,#68687,#68688,
#68689,#68690,#68691,#68692,#68693,#68694,#68695,#68696,#68697,#68698,#68699,
#68700,#68701,#68702,#68703,#68704,#68705,#68706,#68707,#68708,#68709,#68710,
#68711,#68712,#68713,#68714,#68715,#68716,#68717,#68718,#68719,#68720,#68721,
#68722,#68723,#68724,#68725,#68726,#68727,#68728,#68729,#68730,#68731,#68732,
#68733,#68734,#68735,#68736,#68737,#68738,#68739,#68740,#68741,#68742,#68743,
#68744,#68745,#68746,#68747,#68748,#68749,#68750,#68751,#68752,#68753,#68754,
#68755,#68756,#68757,#68758,#68759,#68760,#68761,#68762,#68763,#68764,#68765,
#68766,#68767,#68768,#68769,#68770,#68771,#68772,#68773,#68774,#68775,#68776,
#68777,#68778,#68779,#68780,#68781,#68782,#68783,#68784,#68785,#68786,#68787,
#68788,#68789,#68790,#68791,#68792,#68793,#68794,#68795,#68796,#68797,#68798,
#68799,#68800,#68801,#68802,#68803,#68804,#68805,#68806,#68807,#68808,#68809,
#68810,#68811,#68812,#68813,#68814,#68815),.UNSPECIFIED.,.F.,.F.,(4,3,3,
3,3,3,3,3,3,3,3,3,3,3,3,3,3,3,3,3,3,3,3,3,3,3,3,3,3,3,3,3,3,3,3,3,3,3,3,
3,3,3,3,3,3,3,3,3,3,3,3,3,3,3,3,3,3,3,3,3,3,3,3,3,3,3,3,3,3,3,3,3,3,4),
(706.858347057686,706.943524770658,707.028743249084,707.114017642153,707.199425355731,
707.284904651278,707.370541464767,707.431684980299,707.515423692145,707.599059203512,
707.682611646911,707.766101082762,707.849555033376,707.932991527222,708.016428636977,
708.099884431894,708.183428924624,708.267018007565,708.350741275123,708.431420991019,
708.515159702865,708.598795214232,708.682347657631,708.765837093482,708.849291044096,
708.932727537942,709.016164647697,709.099620442615,709.183164935344,709.266754018285,
709.350477285843,709.431157001739,709.514895713585,709.598531224952,709.682083668351,
709.765573104202,709.849027054816,709.932463548662,710.015900658418,710.099356453336,
710.182900946065,710.266490029006,710.350213296563,710.430893012459,710.514631724305,
710.598267235673,710.681819679071,710.765309114922,710.848763065536,710.932199559382,
711.015636669138,711.099092464055,711.182636956785,711.266226039726,711.349949307284,
711.430629023179,711.514367735025,711.598003246393,711.681555689791,711.765045125642,
711.848499076256,711.931935570102,712.015372679857,712.098828474775,712.182372967505,
712.265962050446,712.349685318003,712.4303650339,712.513484649423,712.596503385103,
712.67942444439,712.762289006816,712.845115372263,712.890365202201),
 .UNSPECIFIED.);
#503=B_SPLINE_CURVE_WITH_KNOTS('',3,(#68821,#68822,#68823,#68824,#68825,
#68826,#68827,#68828,#68829,#68830,#68831,#68832,#68833,#68834,#68835,#68836,
#68837,#68838,#68839,#68840,#68841,#68842,#68843,#68844,#68845,#68846,#68847,
#68848,#68849,#68850,#68851,#68852,#68853,#68854,#68855,#68856,#68857,#68858,
#68859,#68860,#68861,#68862,#68863,#68864,#68865,#68866,#68867,#68868,#68869,
#68870,#68871,#68872,#68873,#68874,#68875,#68876,#68877,#68878,#68879,#68880,
#68881,#68882,#68883,#68884,#68885,#68886,#68887,#68888,#68889,#68890,#68891,
#68892,#68893,#68894,#68895,#68896,#68897,#68898,#68899,#68900,#68901,#68902,
#68903,#68904,#68905,#68906,#68907,#68908,#68909,#68910,#68911,#68912,#68913,
#68914,#68915,#68916,#68917,#68918,#68919,#68920,#68921,#68922,#68923,#68924,
#68925,#68926,#68927,#68928,#68929,#68930,#68931,#68932,#68933,#68934,#68935,
#68936,#68937,#68938,#68939,#68940,#68941,#68942,#68943,#68944,#68945,#68946,
#68947,#68948,#68949,#68950,#68951,#68952,#68953,#68954,#68955,#68956,#68957,
#68958,#68959,#68960,#68961,#68962,#68963,#68964,#68965,#68966,#68967,#68968,
#68969,#68970,#68971,#68972,#68973,#68974,#68975,#68976,#68977,#68978,#68979,
#68980,#68981,#68982,#68983,#68984,#68985,#68986,#68987,#68988,#68989,#68990,
#68991,#68992,#68993,#68994,#68995,#68996,#68997,#68998,#68999,#69000,#69001,
#69002,#69003,#69004,#69005,#69006,#69007,#69008,#69009,#69010,#69011,#69012,
#69013,#69014,#69015,#69016,#69017,#69018,#69019,#69020,#69021,#69022,#69023,
#69024,#69025,#69026,#69027,#69028,#69029,#69030,#69031,#69032,#69033,#69034,
#69035,#69036,#69037,#69038,#69039,#69040),.UNSPECIFIED.,.F.,.F.,(4,3,3,
3,3,3,3,3,3,3,3,3,3,3,3,3,3,3,3,3,3,3,3,3,3,3,3,3,3,3,3,3,3,3,3,3,3,3,3,
3,3,3,3,3,3,3,3,3,3,3,3,3,3,3,3,3,3,3,3,3,3,3,3,3,3,3,3,3,3,3,3,3,3,4),
(713.141532365062,713.224960279161,713.308285726181,713.391529154684,713.474710938694,
713.557859309706,713.640992036717,713.724127474541,713.807283976197,713.890529470755,
713.973822231279,714.057243321125,714.119546435624,714.20328514747,714.286920658837,
714.370473102236,714.453962538087,714.5374164887,714.620852982547,714.704290092302,
714.787745887219,714.871290379949,714.95487946289,715.038602730447,715.119282446344,
715.20302115819,715.286656669557,715.370209112956,715.453698548807,715.537152499421,
715.620588993267,715.704026103022,715.78748189794,715.871026390669,715.95461547361,
716.038338741168,716.119018457064,716.20275716891,716.286392680278,716.369945123676,
716.453434559527,716.536888510141,716.620325003988,716.703762113743,716.78721790866,
716.87076240139,716.954351484331,717.038074751889,717.118754467784,717.20249317963,
717.286128690997,717.369681134396,717.453170570247,717.536624520861,717.620061014707,
717.703498124462,717.786953919379,717.870498412109,717.95408749505,718.037810762608,
718.118490478504,718.20222919035,718.285864701717,718.369417145116,718.452906580967,
718.536360531581,718.619797025427,718.703234135183,718.7866899301,718.87023442283,
718.953823505771,719.037546773328,719.118226489224,719.173978139178),
 .UNSPECIFIED.);
#504=B_SPLINE_CURVE_WITH_KNOTS('',3,(#69041,#69042,#69043,#69044,#69045,
#69046,#69047,#69048,#69049,#69050,#69051,#69052,#69053),.UNSPECIFIED.,
 .F.,.F.,(4,3,3,3,4),(712.889869681513,712.973470531639,713.057200321406,
713.119810424903,713.141532364862),.UNSPECIFIED.);
#505=B_SPLINE_CURVE_WITH_KNOTS('',3,(#69055,#69056,#69057,#69058,#69059,
#69060,#69061,#69062,#69063,#69064),.UNSPECIFIED.,.F.,.F.,(4,3,3,4),(712.890365202201,
712.973179008283,713.057355686575,713.141532364866),.UNSPECIFIED.);
#506=B_SPLINE_CURVE_WITH_KNOTS('',3,(#69065,#69066,#69067,#69068,#69069,
#69070,#69071,#69072,#69073,#69074,#69075,#69076,#69077,#69078,#69079,#69080,
#69081,#69082,#69083,#69084,#69085,#69086,#69087,#69088,#69089,#69090,#69091,
#69092,#69093,#69094,#69095,#69096,#69097,#69098,#69099,#69100,#69101,#69102,
#69103,#69104,#69105,#69106,#69107,#69108,#69109,#69110,#69111,#69112,#69113,
#69114,#69115,#69116,#69117,#69118,#69119,#69120,#69121,#69122,#69123,#69124,
#69125,#69126,#69127,#69128,#69129,#69130,#69131,#69132,#69133,#69134,#69135,
#69136,#69137,#69138,#69139,#69140,#69141,#69142,#69143,#69144,#69145,#69146,
#69147,#69148,#69149,#69150,#69151,#69152,#69153,#69154,#69155,#69156,#69157,
#69158,#69159,#69160,#69161,#69162,#69163,#69164,#69165,#69166,#69167,#69168,
#69169,#69170,#69171,#69172,#69173,#69174,#69175,#69176,#69177,#69178,#69179,
#69180,#69181,#69182,#69183,#69184,#69185,#69186,#69187,#69188,#69189,#69190,
#69191,#69192,#69193,#69194,#69195,#69196,#69197,#69198,#69199,#69200,#69201,
#69202,#69203,#69204,#69205,#69206,#69207,#69208,#69209,#69210,#69211,#69212,
#69213,#69214,#69215,#69216,#69217,#69218,#69219,#69220,#69221,#69222,#69223,
#69224,#69225,#69226,#69227,#69228,#69229,#69230,#69231,#69232,#69233,#69234,
#69235,#69236,#69237,#69238,#69239,#69240,#69241,#69242,#69243,#69244,#69245,
#69246,#69247,#69248,#69249,#69250,#69251,#69252,#69253,#69254,#69255,#69256,
#69257,#69258,#69259,#69260,#69261,#69262,#69263,#69264,#69265,#69266,#69267,
#69268,#69269,#69270,#69271,#69272,#69273,#69274,#69275,#69276,#69277,#69278,
#69279,#69280,#69281),.UNSPECIFIED.,.F.,.F.,(4,3,3,3,3,3,3,3,3,3,3,3,3,
3,3,3,3,3,3,3,3,3,3,3,3,3,3,3,3,3,3,3,3,3,3,3,3,3,3,3,3,3,3,3,3,3,3,3,3,
3,3,3,3,3,3,3,3,3,3,3,3,3,3,3,3,3,3,3,3,3,3,3,4),(713.141532364993,713.243403064375,
713.346774638295,713.43010104462,713.513839756466,713.597475267833,713.681027711231,
713.764517147082,713.847971097695,713.931407591541,714.014844701296,714.098300496213,
714.181844988943,714.265434071883,714.34915733944,714.42983705534,714.513575767186,
714.597211278553,714.680763721952,714.764253157803,714.847707108416,714.931143602263,
715.014580712018,715.098036506936,715.181580999665,715.265170082606,715.348893350164,
715.42957306606,715.513311777906,715.596947289274,715.680499732673,715.763989168524,
715.847443119138,715.930879612984,716.01431672274,716.097772517657,716.181317010387,
716.264906093328,716.348629360886,716.42930907678,716.513047788626,716.596683299993,
716.680235743392,716.763725179243,716.847179129856,716.930615623702,717.014052733458,
717.097508528375,717.181053021105,717.264642104046,717.348365371603,717.4290450875,
717.512783799346,717.596419310713,717.679971754112,717.763461189963,717.846915140576,
717.930351634423,718.013788744178,718.097244539096,718.180789031825,718.264378114766,
718.348101382324,718.42878109822,718.512478123154,718.596042648195,718.679530701119,
718.762960502754,718.8463502302,718.929736147028,719.013116380725,719.096545899213,
719.173051552182),.UNSPECIFIED.);
#507=B_SPLINE_CURVE_WITH_KNOTS('',3,(#69287,#69288,#69289,#69290,#69291,
#69292,#69293,#69294,#69295,#69296,#69297,#69298,#69299,#69300,#69301,#69302,
#69303,#69304,#69305,#69306,#69307,#69308,#69309,#69310,#69311,#69312,#69313,
#69314,#69315,#69316,#69317,#69318,#69319,#69320,#69321,#69322,#69323,#69324,
#69325,#69326,#69327,#69328,#69329,#69330,#69331,#69332,#69333,#69334,#69335,
#69336,#69337,#69338,#69339,#69340,#69341,#69342,#69343,#69344,#69345,#69346,
#69347,#69348,#69349,#69350,#69351,#69352,#69353,#69354,#69355,#69356,#69357,
#69358,#69359,#69360,#69361,#69362,#69363,#69364,#69365,#69366,#69367,#69368,
#69369,#69370,#69371,#69372,#69373,#69374,#69375,#69376,#69377,#69378,#69379,
#69380,#69381,#69382,#69383,#69384,#69385,#69386,#69387,#69388,#69389,#69390,
#69391,#69392,#69393,#69394,#69395,#69396,#69397,#69398,#69399,#69400,#69401,
#69402,#69403,#69404,#69405,#69406,#69407,#69408,#69409,#69410,#69411,#69412,
#69413,#69414,#69415,#69416,#69417,#69418,#69419,#69420,#69421,#69422,#69423,
#69424,#69425,#69426,#69427,#69428,#69429,#69430,#69431,#69432,#69433,#69434,
#69435,#69436,#69437,#69438,#69439,#69440,#69441,#69442,#69443,#69444,#69445,
#69446,#69447,#69448,#69449,#69450,#69451,#69452,#69453,#69454,#69455,#69456,
#69457,#69458,#69459,#69460,#69461,#69462,#69463,#69464,#69465,#69466,#69467,
#69468,#69469,#69470,#69471,#69472,#69473,#69474,#69475,#69476,#69477,#69478,
#69479,#69480,#69481,#69482,#69483,#69484,#69485,#69486,#69487,#69488,#69489,
#69490,#69491,#69492,#69493,#69494,#69495,#69496,#69497,#69498,#69499,#69500,
#69501,#69502,#69503,#69504,#69505,#69506),.UNSPECIFIED.,.F.,.F.,(4,3,3,
3,3,3,3,3,3,3,3,3,3,3,3,3,3,3,3,3,3,3,3,3,3,3,3,3,3,3,3,3,3,3,3,3,3,3,3,
3,3,3,3,3,3,3,3,3,3,3,3,3,3,3,3,3,3,3,3,3,3,3,3,3,3,3,3,3,3,3,3,3,3,4),
(719.424717672042,719.51137327553,719.594394871942,719.677411000932,719.760440079154,
719.843500528614,719.926656899427,720.009869832851,720.093203653868,720.117962499944,
720.20170121179,720.285336723158,720.368889166556,720.452378602407,720.535832553021,
720.619269046867,720.702706156623,720.78616195154,720.86970644427,720.953295527211,
721.037018794769,721.117698510664,721.20143722251,721.285072733878,721.368625177277,
721.452114613128,721.535568563742,721.619005057588,721.702442167344,721.785897962262,
721.869442454991,721.953031537933,722.036754805491,722.117434521385,722.201173233231,
722.284808744598,722.368361187997,722.451850623848,722.535304574462,722.618741068308,
722.702178178063,722.785633972981,722.869178465711,722.952767548652,723.036490816209,
723.117170532105,723.200909243951,723.284544755318,723.368097198717,723.451586634568,
723.535040585181,723.618477079027,723.701914188783,723.785369983701,723.86891447643,
723.952503559371,724.036226826929,724.116906542825,724.200645254671,724.284280766038,
724.367833209437,724.451322645288,724.534776595901,724.618213089748,724.701650199503,
724.785105994421,724.868650487151,724.952239570092,725.03596283765,725.116642553545,
725.201811772529,725.286873489287,725.372096459385,725.457319429483),
 .UNSPECIFIED.);
#508=B_SPLINE_CURVE_WITH_KNOTS('',3,(#69507,#69508,#69509,#69510,#69511,
#69512,#69513,#69514,#69515,#69516),.UNSPECIFIED.,.F.,.F.,(4,3,3,4),(719.173978139178,
719.274963551938,719.37479293904,719.424717671885),.UNSPECIFIED.);
#509=B_SPLINE_CURVE_WITH_KNOTS('',3,(#69518,#69519,#69520,#69521,#69522,
#69523,#69524,#69525,#69526,#69527),.UNSPECIFIED.,.F.,.F.,(4,3,3,4),(719.173051552182,
719.256580922333,719.340649297114,719.424717671895),.UNSPECIFIED.);
#510=B_SPLINE_CURVE_WITH_KNOTS('',3,(#69528,#69529,#69530,#69531,#69532,
#69533,#69534,#69535,#69536,#69537,#69538,#69539,#69540,#69541,#69542,#69543,
#69544,#69545,#69546,#69547,#69548,#69549,#69550,#69551,#69552,#69553,#69554,
#69555,#69556,#69557,#69558,#69559,#69560,#69561,#69562,#69563,#69564,#69565,
#69566,#69567,#69568,#69569,#69570,#69571,#69572,#69573,#69574,#69575,#69576,
#69577,#69578,#69579,#69580,#69581,#69582,#69583,#69584,#69585,#69586,#69587,
#69588,#69589,#69590,#69591,#69592,#69593,#69594,#69595,#69596,#69597,#69598,
#69599,#69600,#69601,#69602,#69603,#69604,#69605,#69606,#69607,#69608,#69609,
#69610,#69611,#69612,#69613,#69614,#69615,#69616,#69617,#69618,#69619,#69620,
#69621,#69622,#69623,#69624,#69625,#69626,#69627,#69628,#69629,#69630,#69631,
#69632,#69633,#69634,#69635,#69636,#69637,#69638,#69639,#69640,#69641,#69642,
#69643,#69644,#69645,#69646,#69647,#69648,#69649,#69650,#69651,#69652,#69653,
#69654,#69655,#69656,#69657,#69658,#69659,#69660,#69661,#69662,#69663,#69664,
#69665,#69666,#69667,#69668,#69669,#69670,#69671,#69672,#69673,#69674,#69675,
#69676,#69677,#69678,#69679,#69680,#69681,#69682,#69683,#69684,#69685,#69686,
#69687,#69688,#69689,#69690,#69691,#69692,#69693,#69694,#69695,#69696,#69697,
#69698,#69699,#69700,#69701,#69702,#69703,#69704,#69705,#69706,#69707,#69708,
#69709,#69710,#69711,#69712,#69713,#69714,#69715,#69716,#69717,#69718,#69719,
#69720,#69721,#69722,#69723,#69724,#69725,#69726,#69727,#69728,#69729,#69730,
#69731,#69732,#69733,#69734,#69735,#69736,#69737,#69738,#69739,#69740,#69741,
#69742,#69743,#69744,#69745,#69746,#69747,#69748,#69749,#69750),
 .UNSPECIFIED.,.F.,.F.,(4,3,3,3,3,3,3,3,3,3,3,3,3,3,3,3,3,3,3,3,3,3,3,3,
3,3,3,3,3,3,3,3,3,3,3,3,3,3,3,3,3,3,3,3,3,3,3,3,3,3,3,3,3,3,3,3,3,3,3,3,
3,3,3,3,3,3,3,3,3,3,3,3,3,3,4),(719.424717672045,719.428517108941,719.512255820787,
719.595891332154,719.679443775553,719.762933211404,719.846387162017,719.929823655863,
720.013260765619,720.096716560536,720.180261053266,720.263850136207,720.347573403764,
720.428253119661,720.511991831507,720.595627342874,720.679179786273,720.762669222124,
720.846123172737,720.929559666584,721.012996776339,721.096452571257,721.179997063986,
721.263586146927,721.347309414485,721.427989130381,721.511727842227,721.595363353595,
721.678915796993,721.762405232844,721.845859183458,721.929295677304,722.01273278706,
722.096188581977,722.179733074707,722.263322157648,722.347045425206,722.427725141101,
722.511463852947,722.595099364314,722.678651807713,722.762141243564,722.845595194177,
722.929031688023,723.012468797779,723.095924592697,723.179469085426,723.263058168367,
723.346781435925,723.427461151821,723.511199863667,723.594835375035,723.678387818433,
723.761877254284,723.845331204898,723.928767698744,724.0122048085,724.095660603417,
724.179205096147,724.262794179088,724.346517446646,724.427197162541,724.510935874387,
724.594571385754,724.678123829153,724.761613265004,724.845067215618,724.928503709464,
725.011940819219,725.095396614137,725.178941106867,725.262530189808,725.346253457365,
725.426933173261,725.457020176983),.UNSPECIFIED.);
#511=B_SPLINE_CURVE_WITH_KNOTS('',3,(#69756,#69757,#69758,#69759,#69760,
#69761,#69762,#69763,#69764,#69765,#69766,#69767,#69768,#69769,#69770,#69771,
#69772,#69773,#69774,#69775,#69776,#69777,#69778,#69779,#69780,#69781,#69782,
#69783,#69784,#69785,#69786,#69787,#69788,#69789,#69790,#69791,#69792,#69793,
#69794,#69795,#69796,#69797,#69798,#69799,#69800,#69801,#69802,#69803,#69804,
#69805,#69806,#69807,#69808,#69809,#69810,#69811,#69812,#69813,#69814,#69815,
#69816,#69817,#69818,#69819,#69820,#69821,#69822,#69823,#69824,#69825,#69826,
#69827,#69828,#69829,#69830,#69831,#69832,#69833,#69834,#69835,#69836,#69837,
#69838,#69839,#69840,#69841,#69842,#69843,#69844,#69845,#69846,#69847,#69848,
#69849,#69850,#69851,#69852,#69853,#69854,#69855,#69856,#69857,#69858,#69859,
#69860,#69861,#69862,#69863,#69864,#69865,#69866,#69867,#69868,#69869,#69870,
#69871,#69872,#69873,#69874,#69875,#69876,#69877,#69878,#69879,#69880,#69881,
#69882,#69883,#69884,#69885,#69886,#69887,#69888,#69889,#69890,#69891,#69892,
#69893,#69894,#69895,#69896,#69897,#69898,#69899,#69900,#69901,#69902,#69903,
#69904,#69905,#69906,#69907,#69908,#69909,#69910,#69911,#69912,#69913,#69914,
#69915,#69916,#69917,#69918,#69919,#69920,#69921,#69922,#69923,#69924,#69925,
#69926,#69927,#69928,#69929,#69930,#69931,#69932,#69933,#69934,#69935,#69936,
#69937,#69938,#69939,#69940,#69941,#69942,#69943,#69944,#69945,#69946,#69947,
#69948,#69949,#69950,#69951,#69952,#69953,#69954,#69955,#69956,#69957,#69958,
#69959,#69960,#69961,#69962,#69963,#69964,#69965,#69966,#69967,#69968,#69969,
#69970,#69971,#69972,#69973,#69974,#69975),.UNSPECIFIED.,.F.,.F.,(4,3,3,
3,3,3,3,3,3,3,3,3,3,3,3,3,3,3,3,3,3,3,3,3,3,3,3,3,3,3,3,3,3,3,3,3,3,3,3,
3,3,3,3,3,3,3,3,3,3,3,3,3,3,3,3,3,3,3,3,3,3,3,3,3,3,3,3,3,3,3,3,3,3,4),
(725.70790297939,725.799493914464,725.891544766478,725.983832330002,726.076444867083,
726.116378564265,726.200117276111,726.283752787479,726.367305230877,726.450794666728,
726.534248617342,726.617685111188,726.701122220943,726.784578015861,726.868122508591,
726.951711591532,727.035434859089,727.116114574985,727.199853286831,727.283488798198,
727.367041241597,727.450530677448,727.533984628061,727.617421121908,727.700858231663,
727.784314026581,727.867858519311,727.951447602252,728.035170869809,728.115850585705,
728.199589297551,728.283224808918,728.366777252317,728.450266688168,728.533720638782,
728.617157132628,728.700594242383,728.784050037301,728.867594530031,728.951183612972,
729.034906880529,729.115586596425,729.199325308271,729.282960819639,729.366513263037,
729.450002698888,729.533456649502,729.616893143348,729.700330253104,729.783786048022,
729.867330540751,729.950919623692,730.03464289125,730.115322607146,730.199061318992,
730.28269683036,730.366249273758,730.449738709609,730.533192660223,730.616629154069,
730.700066263825,730.783522058743,730.867066551472,730.950655634413,731.034378901971,
731.115058617866,731.197613801789,731.280074281687,731.362459217619,731.444787698686,
731.527086567966,731.609367384702,731.691670041471,731.739280210377),
 .UNSPECIFIED.);
#512=B_SPLINE_CURVE_WITH_KNOTS('',3,(#69976,#69977,#69978,#69979,#69980,
#69981,#69982,#69983,#69984,#69985),.UNSPECIFIED.,.F.,.F.,(4,3,3,4),(725.457319429483,
725.54212344489,725.626884140274,725.707902979221),.UNSPECIFIED.);
#513=B_SPLINE_CURVE_WITH_KNOTS('',3,(#69987,#69988,#69989,#69990,#69991,
#69992,#69993,#69994,#69995,#69996),.UNSPECIFIED.,.F.,.F.,(4,3,3,4),(725.457020176983,
725.561445543817,725.664299370825,725.707902979112),.UNSPECIFIED.);
#514=B_SPLINE_CURVE_WITH_KNOTS('',3,(#69997,#69998,#69999,#70000,#70001,
#70002,#70003,#70004,#70005,#70006,#70007,#70008,#70009,#70010,#70011,#70012,
#70013,#70014,#70015,#70016,#70017,#70018,#70019,#70020,#70021,#70022,#70023,
#70024,#70025,#70026,#70027,#70028,#70029,#70030,#70031,#70032,#70033,#70034,
#70035,#70036,#70037,#70038,#70039,#70040,#70041,#70042,#70043,#70044,#70045,
#70046,#70047,#70048,#70049,#70050,#70051,#70052,#70053,#70054,#70055,#70056,
#70057,#70058,#70059,#70060,#70061,#70062,#70063,#70064,#70065,#70066,#70067,
#70068,#70069,#70070,#70071,#70072,#70073,#70074,#70075,#70076,#70077,#70078,
#70079,#70080,#70081,#70082,#70083,#70084,#70085,#70086,#70087,#70088,#70089,
#70090,#70091,#70092,#70093,#70094,#70095,#70096,#70097,#70098,#70099,#70100,
#70101,#70102,#70103,#70104,#70105,#70106,#70107,#70108,#70109,#70110,#70111,
#70112,#70113,#70114,#70115,#70116,#70117,#70118,#70119,#70120,#70121,#70122,
#70123,#70124,#70125,#70126,#70127,#70128,#70129,#70130,#70131,#70132,#70133,
#70134,#70135,#70136,#70137,#70138,#70139,#70140,#70141,#70142,#70143,#70144,
#70145,#70146,#70147,#70148,#70149,#70150,#70151,#70152,#70153,#70154,#70155,
#70156,#70157,#70158,#70159,#70160,#70161,#70162,#70163,#70164,#70165,#70166,
#70167,#70168,#70169,#70170,#70171,#70172,#70173,#70174,#70175,#70176,#70177,
#70178,#70179,#70180,#70181,#70182,#70183,#70184,#70185,#70186,#70187,#70188,
#70189,#70190,#70191,#70192,#70193,#70194,#70195,#70196,#70197,#70198,#70199,
#70200,#70201,#70202,#70203,#70204,#70205,#70206,#70207,#70208,#70209,#70210,
#70211,#70212,#70213,#70214,#70215,#70216),.UNSPECIFIED.,.F.,.F.,(4,3,3,
3,3,3,3,3,3,3,3,3,3,3,3,3,3,3,3,3,3,3,3,3,3,3,3,3,3,3,3,3,3,3,3,3,3,3,3,
3,3,3,3,3,3,3,3,3,3,3,3,3,3,3,3,3,3,3,3,3,3,3,3,3,3,3,3,3,3,3,3,3,3,4),
(725.707902979225,725.790691462221,725.873446198533,725.956185331489,726.038927518606,
726.121691416454,726.204544830995,726.287446619887,726.370475836275,726.426669183981,
726.510407895827,726.594043407194,726.677595850593,726.761085286444,726.844539237058,
726.927975730904,727.01141284066,727.094868635577,727.178413128307,727.262002211248,
727.345725478806,727.426405194702,727.510143906548,727.593779417915,727.677331861314,
727.760821297165,727.844275247779,727.927711741625,728.011148851381,728.094604646298,
728.178149139028,728.261738221969,728.345461489527,728.426141205422,728.509879917268,
728.593515428635,728.677067872034,728.760557307885,728.844011258499,728.927447752345,
729.0108848621,729.094340657017,729.177885149747,729.261474232688,729.345197500245,
729.425877216142,729.509615927988,729.593251439356,729.676803882754,729.760293318605,
729.843747269219,729.927183763065,730.01062087282,730.094076667738,730.177621160468,
730.261210243409,730.344933510966,730.425613226862,730.509351938708,730.592987450075,
730.676539893474,730.760029329326,730.84348327994,730.926919773786,731.010356883541,
731.093812678459,731.177357171189,731.26094625413,731.344669521687,731.425349237582,
731.511188461276,731.596917566492,731.682518062319,731.740599790848),
 .UNSPECIFIED.);
#515=B_SPLINE_CURVE_WITH_KNOTS('',3,(#70222,#70223,#70224,#70225,#70226,
#70227,#70228,#70229,#70230,#70231,#70232,#70233,#70234,#70235,#70236,#70237,
#70238,#70239,#70240,#70241,#70242,#70243,#70244,#70245,#70246,#70247,#70248,
#70249,#70250,#70251,#70252,#70253,#70254,#70255,#70256,#70257,#70258,#70259,
#70260,#70261,#70262,#70263,#70264,#70265,#70266,#70267,#70268,#70269,#70270,
#70271,#70272,#70273,#70274,#70275,#70276,#70277,#70278,#70279,#70280,#70281,
#70282,#70283,#70284,#70285,#70286,#70287,#70288,#70289,#70290,#70291,#70292,
#70293,#70294,#70295,#70296,#70297,#70298,#70299,#70300,#70301,#70302,#70303,
#70304,#70305,#70306,#70307,#70308,#70309,#70310,#70311,#70312,#70313,#70314,
#70315,#70316,#70317,#70318,#70319,#70320,#70321,#70322,#70323,#70324,#70325,
#70326,#70327,#70328,#70329,#70330,#70331,#70332,#70333,#70334,#70335,#70336,
#70337,#70338,#70339,#70340,#70341,#70342,#70343,#70344,#70345,#70346,#70347,
#70348,#70349,#70350,#70351,#70352,#70353,#70354,#70355,#70356,#70357,#70358,
#70359,#70360,#70361,#70362,#70363,#70364,#70365,#70366,#70367,#70368,#70369,
#70370,#70371,#70372,#70373,#70374,#70375,#70376,#70377,#70378,#70379,#70380,
#70381,#70382,#70383,#70384,#70385,#70386,#70387,#70388,#70389,#70390,#70391,
#70392,#70393,#70394,#70395,#70396,#70397,#70398,#70399,#70400,#70401,#70402,
#70403,#70404,#70405,#70406,#70407,#70408,#70409,#70410,#70411,#70412,#70413,
#70414,#70415,#70416,#70417,#70418,#70419,#70420,#70421,#70422,#70423,#70424,
#70425,#70426,#70427,#70428,#70429,#70430,#70431,#70432,#70433,#70434,#70435,
#70436,#70437,#70438),.UNSPECIFIED.,.F.,.F.,(4,3,3,3,3,3,3,3,3,3,3,3,3,
3,3,3,3,3,3,3,3,3,3,3,3,3,3,3,3,3,3,3,3,3,3,3,3,3,3,3,3,3,3,3,3,3,3,3,3,
3,3,3,3,3,3,3,3,3,3,3,3,3,3,3,3,3,3,3,3,3,3,3,4),(731.991088286401,732.114794628586,
732.198533340432,732.282168851799,732.365721295198,732.449210731049,732.532664681662,
732.616101175508,732.699538285264,732.782994080181,732.866538572911,732.950127655852,
733.033850923409,733.114530639306,733.198269351152,733.28190486252,733.365457305918,
733.448946741769,733.532400692383,733.615837186229,733.699274295985,733.782730090902,
733.866274583632,733.949863666573,734.033586934131,734.114266650026,734.198005361872,
734.281640873239,734.365193316638,734.448682752489,734.532136703102,734.615573196949,
734.699010306704,734.782466101621,734.866010594351,734.949599677292,735.033322944849,
735.114002660746,735.197741372592,735.28137688396,735.364929327358,735.448418763209,
735.531872713823,735.615309207669,735.698746317425,735.782202112342,735.865746605072,
735.949335688013,736.033058955571,736.113738671466,736.197477383312,736.28111289468,
736.364665338078,736.448154773929,736.531608724543,736.615045218389,736.698482328145,
736.781938123063,736.865482615792,736.949071698733,737.032794966291,737.113474682187,
737.197218640118,737.280858204831,737.364413513921,737.447900690298,737.531350634533,
737.614781435024,737.698211163527,737.781697233363,737.865210972875,737.948827174312,
738.022787360679),.UNSPECIFIED.);
#516=B_SPLINE_CURVE_WITH_KNOTS('',3,(#70439,#70440,#70441,#70442,#70443,
#70444,#70445,#70446,#70447,#70448),.UNSPECIFIED.,.F.,.F.,(4,3,3,4),(731.739280210377,
731.8216523665,731.906370326385,731.991088286269),.UNSPECIFIED.);
#517=B_SPLINE_CURVE_WITH_KNOTS('',3,(#70450,#70451,#70452,#70453,#70454,
#70455,#70456,#70457,#70458,#70459),.UNSPECIFIED.,.F.,.F.,(4,3,3,4),(731.740599790848,
731.826053994574,731.911438415576,731.991088286405),.UNSPECIFIED.);
#518=B_SPLINE_CURVE_WITH_KNOTS('',3,(#70460,#70461,#70462,#70463,#70464,
#70465,#70466,#70467,#70468,#70469,#70470,#70471,#70472,#70473,#70474,#70475,
#70476,#70477,#70478,#70479,#70480,#70481,#70482,#70483,#70484,#70485,#70486,
#70487,#70488,#70489,#70490,#70491,#70492,#70493,#70494,#70495,#70496,#70497,
#70498,#70499,#70500,#70501,#70502,#70503,#70504,#70505,#70506,#70507,#70508,
#70509,#70510,#70511,#70512,#70513,#70514,#70515,#70516,#70517,#70518,#70519,
#70520,#70521,#70522,#70523,#70524,#70525,#70526,#70527,#70528,#70529,#70530,
#70531,#70532,#70533,#70534,#70535,#70536,#70537,#70538,#70539,#70540,#70541,
#70542,#70543,#70544,#70545,#70546,#70547,#70548,#70549,#70550,#70551,#70552,
#70553,#70554,#70555,#70556,#70557,#70558,#70559,#70560,#70561,#70562,#70563,
#70564,#70565,#70566,#70567,#70568,#70569,#70570,#70571,#70572,#70573,#70574,
#70575,#70576,#70577,#70578,#70579,#70580,#70581,#70582,#70583,#70584,#70585,
#70586,#70587,#70588,#70589,#70590,#70591,#70592,#70593,#70594,#70595,#70596,
#70597,#70598,#70599,#70600,#70601,#70602,#70603,#70604,#70605,#70606,#70607,
#70608,#70609,#70610,#70611,#70612,#70613,#70614,#70615,#70616,#70617,#70618,
#70619,#70620,#70621,#70622,#70623,#70624,#70625,#70626,#70627,#70628,#70629,
#70630,#70631,#70632,#70633,#70634,#70635,#70636,#70637,#70638,#70639,#70640,
#70641,#70642,#70643,#70644,#70645,#70646,#70647,#70648,#70649,#70650,#70651,
#70652,#70653,#70654,#70655,#70656,#70657,#70658,#70659,#70660,#70661,#70662,
#70663,#70664,#70665,#70666,#70667,#70668,#70669,#70670,#70671,#70672,#70673,
#70674,#70675,#70676,#70677,#70678,#70679),.UNSPECIFIED.,.F.,.F.,(4,3,3,
3,3,3,3,3,3,3,3,3,3,3,3,3,3,3,3,3,3,3,3,3,3,3,3,3,3,3,3,3,3,3,3,3,3,3,3,
3,3,3,3,3,3,3,3,3,3,3,3,3,3,3,3,3,3,3,3,3,3,3,3,3,3,3,3,3,3,3,3,3,3,4),
(731.991088286542,732.081312336988,732.17190734144,732.262689439977,732.35376866986,
732.425085248302,732.508823960148,732.592459471515,732.676011914914,732.759501350765,
732.842955301379,732.926391795225,733.00982890498,733.093284699898,733.176829192628,
733.260418275569,733.344141543127,733.424821259022,733.508559970868,733.592195482236,
733.675747925634,733.759237361485,733.842691312099,733.926127805945,734.0095649157,
734.093020710618,734.176565203348,734.260154286289,734.343877553846,734.424557269742,
734.508295981588,734.591931492955,734.675483936354,734.758973372205,734.842427322819,
734.925863816665,735.009300926421,735.092756721338,735.176301214068,735.259890297009,
735.343613564567,735.424293280463,735.508031992309,735.591667503676,735.675219947075,
735.758709382926,735.84216333354,735.925599827386,736.009036937142,736.09249273206,
736.176037224789,736.25962630773,736.343349575288,736.424029291183,736.507768003029,
736.591403514396,736.674955957795,736.758445393646,736.84189934426,736.925335838106,
737.008772947861,737.092228742779,737.175773235508,737.259362318449,737.343085586007,
737.423765301903,737.506250937077,737.588641584275,737.670956451871,737.753214675185,
737.835440757069,737.91764891644,737.999871857261,738.022517897246),
 .UNSPECIFIED.);
#519=B_SPLINE_CURVE_WITH_KNOTS('',3,(#70685,#70686,#70687,#70688,#70689,
#70690,#70691,#70692,#70693,#70694,#70695,#70696,#70697,#70698,#70699,#70700,
#70701,#70702,#70703,#70704,#70705,#70706,#70707,#70708,#70709,#70710,#70711,
#70712,#70713,#70714,#70715,#70716,#70717,#70718,#70719,#70720,#70721,#70722,
#70723,#70724,#70725,#70726,#70727,#70728,#70729,#70730,#70731,#70732,#70733,
#70734,#70735,#70736,#70737,#70738,#70739,#70740,#70741,#70742,#70743,#70744,
#70745,#70746,#70747,#70748,#70749,#70750,#70751,#70752,#70753,#70754,#70755,
#70756,#70757,#70758,#70759,#70760,#70761,#70762,#70763,#70764,#70765,#70766,
#70767,#70768,#70769,#70770,#70771,#70772,#70773,#70774,#70775,#70776,#70777,
#70778,#70779,#70780,#70781,#70782,#70783,#70784,#70785,#70786,#70787,#70788,
#70789,#70790,#70791,#70792,#70793,#70794,#70795,#70796,#70797,#70798,#70799,
#70800,#70801,#70802,#70803,#70804,#70805,#70806,#70807,#70808,#70809,#70810,
#70811,#70812,#70813,#70814,#70815,#70816,#70817,#70818,#70819,#70820,#70821,
#70822,#70823,#70824,#70825,#70826,#70827,#70828,#70829,#70830,#70831,#70832,
#70833,#70834,#70835,#70836,#70837,#70838,#70839,#70840,#70841,#70842,#70843,
#70844,#70845,#70846,#70847,#70848,#70849,#70850,#70851,#70852,#70853,#70854,
#70855,#70856,#70857,#70858,#70859,#70860,#70861,#70862,#70863,#70864,#70865,
#70866,#70867,#70868,#70869,#70870,#70871,#70872,#70873,#70874,#70875,#70876,
#70877,#70878,#70879,#70880,#70881,#70882,#70883,#70884,#70885,#70886,#70887,
#70888,#70889,#70890,#70891,#70892,#70893,#70894,#70895,#70896,#70897,#70898,
#70899,#70900,#70901,#70902,#70903,#70904,#70905,#70906,#70907),
 .UNSPECIFIED.,.F.,.F.,(4,3,3,3,3,3,3,3,3,3,3,3,3,3,3,3,3,3,3,3,3,3,3,3,
3,3,3,3,3,3,3,3,3,3,3,3,3,3,3,3,3,3,3,3,3,3,3,3,3,3,3,3,3,3,3,3,3,3,3,3,
3,3,3,3,3,3,3,3,3,3,3,3,3,3,4),(738.274273593783,738.356654353969,738.438955679186,
738.523204557241,738.605418505351,738.687621623504,738.769832943989,738.855611383899,
738.937940895418,739.020325262459,739.102821504759,739.112946703627,739.196685415473,
739.280320926841,739.363873370239,739.44736280609,739.530816756704,739.61425325055,
739.697690360305,739.781146155223,739.864690647952,739.948279730893,740.032002998451,
740.112682714347,740.196421426193,740.28005693756,740.363609380959,740.44709881681,
740.530552767424,740.61398926127,740.697426371025,740.780882165943,740.864426658672,
740.948015741613,741.031739009171,741.112418725067,741.196157436913,741.27979294828,
741.363345391679,741.44683482753,741.530288778144,741.61372527199,741.697162381746,
741.780618176663,741.864162669393,741.947751752334,742.031475019892,742.112154735787,
742.195893447633,742.279528959001,742.363081402399,742.44657083825,742.530024788864,
742.61346128271,742.696898392465,742.780354187382,742.863898680112,742.947487763053,
743.031211030611,743.111890746507,743.195629458353,743.279264969721,743.362817413119,
743.44630684897,743.529760799584,743.61319729343,743.696634403185,743.780090198102,
743.863634690832,743.947223773773,744.030947041331,744.111626757227,744.20215036008,
744.292442587059,744.307152866363),.UNSPECIFIED.);
#520=B_SPLINE_CURVE_WITH_KNOTS('',3,(#70908,#70909,#70910,#70911,#70912,
#70913,#70914,#70915,#70916,#70917,#70918,#70919,#70920),.UNSPECIFIED.,
 .F.,.F.,(4,3,3,3,4),(738.022787360679,738.106543252029,738.113210692907,
738.249145518636,738.27427359358),.UNSPECIFIED.);
#521=B_SPLINE_CURVE_WITH_KNOTS('',3,(#70922,#70923,#70924,#70925,#70926,
#70927,#70928,#70929,#70930,#70931),.UNSPECIFIED.,.F.,.F.,(4,3,3,4),(738.022517897246,
738.104803312639,738.189538453055,738.27427359347),.UNSPECIFIED.);
#522=B_SPLINE_CURVE_WITH_KNOTS('',3,(#70932,#70933,#70934,#70935,#70936,
#70937,#70938,#70939,#70940,#70941,#70942,#70943,#70944,#70945,#70946,#70947,
#70948,#70949,#70950,#70951,#70952,#70953,#70954,#70955,#70956,#70957,#70958,
#70959,#70960,#70961,#70962,#70963,#70964,#70965,#70966,#70967,#70968,#70969,
#70970,#70971,#70972,#70973,#70974,#70975,#70976,#70977,#70978,#70979,#70980,
#70981,#70982,#70983,#70984,#70985,#70986,#70987,#70988,#70989,#70990,#70991,
#70992,#70993,#70994,#70995,#70996,#70997,#70998,#70999,#71000,#71001,#71002,
#71003,#71004,#71005,#71006,#71007,#71008,#71009,#71010,#71011,#71012,#71013,
#71014,#71015,#71016,#71017,#71018,#71019,#71020,#71021,#71022,#71023,#71024,
#71025,#71026,#71027,#71028,#71029,#71030,#71031,#71032,#71033,#71034,#71035,
#71036,#71037,#71038,#71039,#71040,#71041,#71042,#71043,#71044,#71045,#71046,
#71047,#71048,#71049,#71050,#71051,#71052,#71053,#71054,#71055,#71056,#71057,
#71058,#71059,#71060,#71061,#71062,#71063,#71064,#71065,#71066,#71067,#71068,
#71069,#71070,#71071,#71072,#71073,#71074,#71075,#71076,#71077,#71078,#71079,
#71080,#71081,#71082,#71083,#71084,#71085,#71086,#71087,#71088,#71089,#71090,
#71091,#71092,#71093,#71094,#71095,#71096,#71097,#71098,#71099,#71100,#71101,
#71102,#71103,#71104,#71105,#71106,#71107,#71108,#71109,#71110,#71111,#71112,
#71113,#71114,#71115,#71116,#71117,#71118,#71119,#71120,#71121,#71122,#71123,
#71124,#71125,#71126,#71127,#71128,#71129,#71130,#71131,#71132,#71133,#71134,
#71135,#71136,#71137,#71138,#71139,#71140,#71141,#71142,#71143,#71144,#71145,
#71146,#71147,#71148),.UNSPECIFIED.,.F.,.F.,(4,3,3,3,3,3,3,3,3,3,3,3,3,
3,3,3,3,3,3,3,3,3,3,3,3,3,3,3,3,3,3,3,3,3,3,3,3,3,3,3,3,3,3,3,3,3,3,3,3,
3,3,3,3,3,3,3,3,3,3,3,3,3,3,3,3,3,3,3,3,3,3,3,4),(738.274273593584,738.423501312623,
738.507240024469,738.590875535836,738.674427979235,738.757917415086,738.841371365699,
738.924807859546,739.008244969301,739.091700764219,739.175245256948,739.258834339889,
739.342557607447,739.423237323343,739.506976035189,739.590611546556,739.674163989955,
739.757653425806,739.84110737642,739.924543870266,740.007980980021,740.091436774939,
740.174981267669,740.25857035061,740.342293618167,740.422973334063,740.506712045909,
740.590347557276,740.673900000675,740.757389436526,740.840843387139,740.924279880986,
741.007716990741,741.091172785659,741.174717278388,741.258306361329,741.342029628887,
741.422709344783,741.506448056629,741.590083567997,741.673636011395,741.757125447246,
741.84057939786,741.924015891707,742.007453001462,742.09090879638,742.17445328911,
742.258042372051,742.341765639608,742.422445355504,742.50618406735,742.589819578718,
742.673372022116,742.756861457967,742.840315408581,742.923751902427,743.007189012183,
743.0906448071,743.17418929983,743.257778382771,743.341501650329,743.422181366224,
743.50592687522,743.589567653357,743.673123839699,743.756610625342,743.840059701123,
743.923489155705,744.006917060688,744.090395674837,744.173901764441,744.257496996667,
744.305901543465),.UNSPECIFIED.);
#523=B_SPLINE_CURVE_WITH_KNOTS('',3,(#71154,#71155,#71156,#71157,#71158,
#71159,#71160,#71161,#71162,#71163,#71164,#71165,#71166,#71167,#71168,#71169,
#71170,#71171,#71172,#71173,#71174,#71175,#71176,#71177,#71178,#71179,#71180,
#71181,#71182,#71183,#71184,#71185,#71186,#71187,#71188,#71189,#71190,#71191,
#71192,#71193,#71194,#71195,#71196,#71197,#71198,#71199,#71200,#71201,#71202,
#71203,#71204,#71205,#71206,#71207,#71208,#71209,#71210,#71211,#71212,#71213,
#71214,#71215,#71216,#71217,#71218,#71219,#71220,#71221,#71222,#71223,#71224,
#71225,#71226,#71227,#71228,#71229,#71230,#71231,#71232,#71233,#71234,#71235,
#71236,#71237,#71238,#71239,#71240,#71241,#71242,#71243,#71244,#71245,#71246,
#71247,#71248,#71249,#71250,#71251,#71252,#71253,#71254,#71255,#71256,#71257,
#71258,#71259,#71260,#71261,#71262,#71263,#71264,#71265,#71266,#71267,#71268,
#71269,#71270,#71271,#71272,#71273,#71274,#71275,#71276,#71277,#71278,#71279,
#71280,#71281,#71282,#71283,#71284,#71285,#71286,#71287,#71288,#71289,#71290,
#71291,#71292,#71293,#71294,#71295,#71296,#71297,#71298,#71299,#71300,#71301,
#71302,#71303,#71304,#71305,#71306,#71307,#71308,#71309,#71310,#71311,#71312,
#71313,#71314,#71315,#71316,#71317,#71318,#71319,#71320,#71321,#71322,#71323,
#71324,#71325,#71326,#71327,#71328,#71329,#71330,#71331,#71332,#71333,#71334,
#71335,#71336,#71337,#71338,#71339,#71340,#71341,#71342,#71343,#71344,#71345,
#71346,#71347,#71348,#71349,#71350,#71351,#71352,#71353,#71354,#71355,#71356,
#71357,#71358,#71359,#71360,#71361,#71362,#71363,#71364,#71365,#71366,#71367,
#71368,#71369,#71370,#71371,#71372,#71373),.UNSPECIFIED.,.F.,.F.,(4,3,3,
3,3,3,3,3,3,3,3,3,3,3,3,3,3,3,3,3,3,3,3,3,3,3,3,3,3,3,3,3,3,3,3,3,3,3,3,
3,3,3,3,3,3,3,3,3,3,3,3,3,3,3,3,3,3,3,3,3,3,3,3,3,3,3,3,3,3,3,3,3,3,4),
(744.55745890076,744.643146609339,744.7288909297,744.814705795683,744.900667180722,
744.986710700036,745.072911390609,745.111362767948,745.195101479794,745.278736991162,
745.36228943456,745.445778870411,745.529232821025,745.612669314871,745.696106424627,
745.779562219544,745.863106712274,745.946695795215,746.030419062773,746.111098778668,
746.194837490514,746.278473001881,746.36202544528,746.445514881131,746.528968831744,
746.612405325591,746.695842435346,746.779298230264,746.862842722994,746.946431805935,
747.030155073492,747.110834789388,747.194573501234,747.278209012601,747.361761456,
747.445250891851,747.528704842465,747.612141336311,747.695578446066,747.779034240983,
747.862578733713,747.946167816654,748.029891084211,748.110570800108,748.194309511954,
748.277945023322,748.36149746672,748.444986902571,748.528440853185,748.611877347031,
748.695314456787,748.778770251704,748.862314744434,748.945903827375,749.029627094933,
749.110306810828,749.194045522674,749.277681034042,749.36123347744,749.444722913291,
749.528176863904,749.61161335775,749.695050467506,749.778506262423,749.862050755153,
749.945639838094,750.029363105652,750.110042821548,750.192967240485,750.275792225416,
750.358522711749,750.441197997053,750.523841140051,750.589376852607),
 .UNSPECIFIED.);
#524=B_SPLINE_CURVE_WITH_KNOTS('',3,(#71374,#71375,#71376,#71377,#71378,
#71379,#71380,#71381,#71382,#71383),.UNSPECIFIED.,.F.,.F.,(4,3,3,4),(744.307152866363,
744.397153103746,744.486872900899,744.557458900644),.UNSPECIFIED.);
#525=B_SPLINE_CURVE_WITH_KNOTS('',3,(#71385,#71386,#71387,#71388,#71389,
#71390,#71391,#71392,#71393,#71394),.UNSPECIFIED.,.F.,.F.,(4,3,3,4),(744.305901543465,
744.389644379796,744.421917376944,744.557458900764),.UNSPECIFIED.);
#526=B_SPLINE_CURVE_WITH_KNOTS('',3,(#71395,#71396,#71397,#71398,#71399,
#71400,#71401,#71402,#71403,#71404,#71405,#71406,#71407,#71408,#71409,#71410,
#71411,#71412,#71413,#71414,#71415,#71416,#71417,#71418,#71419,#71420,#71421,
#71422,#71423,#71424,#71425,#71426,#71427,#71428,#71429,#71430,#71431,#71432,
#71433,#71434,#71435,#71436,#71437,#71438,#71439,#71440,#71441,#71442,#71443,
#71444,#71445,#71446,#71447,#71448,#71449,#71450,#71451,#71452,#71453,#71454,
#71455,#71456,#71457,#71458,#71459,#71460,#71461,#71462,#71463,#71464,#71465,
#71466,#71467,#71468,#71469,#71470,#71471,#71472,#71473,#71474,#71475,#71476,
#71477,#71478,#71479,#71480,#71481,#71482,#71483,#71484,#71485,#71486,#71487,
#71488,#71489,#71490,#71491,#71492,#71493,#71494,#71495,#71496,#71497,#71498,
#71499,#71500,#71501,#71502,#71503,#71504,#71505,#71506,#71507,#71508,#71509,
#71510,#71511,#71512,#71513,#71514,#71515,#71516,#71517,#71518,#71519,#71520,
#71521,#71522,#71523,#71524,#71525,#71526,#71527,#71528,#71529,#71530,#71531,
#71532,#71533,#71534,#71535,#71536,#71537,#71538,#71539,#71540,#71541,#71542,
#71543,#71544,#71545,#71546,#71547,#71548,#71549,#71550,#71551,#71552,#71553,
#71554,#71555,#71556,#71557,#71558,#71559,#71560,#71561,#71562,#71563,#71564,
#71565,#71566,#71567,#71568,#71569,#71570,#71571,#71572,#71573,#71574,#71575,
#71576,#71577,#71578,#71579,#71580,#71581,#71582,#71583,#71584,#71585,#71586,
#71587,#71588,#71589,#71590,#71591,#71592,#71593,#71594,#71595,#71596,#71597,
#71598,#71599,#71600,#71601,#71602,#71603,#71604,#71605,#71606,#71607,#71608,
#71609,#71610,#71611,#71612,#71613,#71614),.UNSPECIFIED.,.F.,.F.,(4,3,3,
3,3,3,3,3,3,3,3,3,3,3,3,3,3,3,3,3,3,3,3,3,3,3,3,3,3,3,3,3,3,3,3,3,3,3,3,
3,3,3,3,3,3,3,3,3,3,3,3,3,3,3,3,3,3,3,3,3,3,3,3,3,3,3,3,3,3,3,3,3,3,4),
(744.557458900889,744.639910719997,744.722277095366,744.804579155342,744.886844861793,
744.969093797692,745.0513449701,745.133617385711,745.215976099959,745.298383484231,
745.380910787678,745.421653387664,745.50539209951,745.589027610877,745.672580054276,
745.756069490127,745.839523440741,745.922959934587,746.006397044343,746.08985283926,
746.17339733199,746.256986414931,746.340709682489,746.421389398384,746.50512811023,
746.588763621597,746.672316064996,746.755805500847,746.839259451461,746.922695945307,
747.006133055062,747.08958884998,747.173133342709,747.25672242565,747.340445693208,
747.421125409104,747.50486412095,747.588499632317,747.672052075716,747.755541511567,
747.83899546218,747.922431956027,748.005869065782,748.0893248607,748.172869353429,
748.25645843637,748.340181703928,748.420861419824,748.50460013167,748.588235643037,
748.671788086436,748.755277522287,748.8387314729,748.922167966747,749.005605076502,
749.08906087142,749.17260536415,749.256194447091,749.339917714648,749.420597430544,
749.50433614239,749.587971653758,749.671524097157,749.755013533008,749.838467483622,
749.921903977468,750.005341087224,750.088796882142,750.172341374872,750.255930457813,
750.339653725371,750.420333441265,750.51217718284,750.590310680117),
 .UNSPECIFIED.);
#527=B_SPLINE_CURVE_WITH_KNOTS('',3,(#71620,#71621,#71622,#71623,#71624,
#71625,#71626,#71627,#71628,#71629,#71630,#71631,#71632,#71633,#71634,#71635,
#71636,#71637,#71638,#71639,#71640,#71641,#71642,#71643,#71644,#71645,#71646,
#71647,#71648,#71649,#71650,#71651,#71652,#71653,#71654,#71655,#71656,#71657,
#71658,#71659,#71660,#71661,#71662,#71663,#71664,#71665,#71666,#71667,#71668,
#71669,#71670,#71671,#71672,#71673,#71674,#71675,#71676,#71677,#71678,#71679,
#71680,#71681,#71682,#71683,#71684,#71685,#71686,#71687,#71688,#71689,#71690,
#71691,#71692,#71693,#71694,#71695,#71696,#71697,#71698,#71699,#71700,#71701,
#71702,#71703,#71704,#71705,#71706,#71707,#71708,#71709,#71710,#71711,#71712,
#71713,#71714,#71715,#71716,#71717,#71718,#71719,#71720,#71721,#71722,#71723,
#71724,#71725,#71726,#71727,#71728,#71729,#71730,#71731,#71732,#71733,#71734,
#71735,#71736,#71737,#71738,#71739,#71740,#71741,#71742,#71743,#71744,#71745,
#71746,#71747,#71748,#71749,#71750,#71751,#71752,#71753,#71754,#71755,#71756,
#71757,#71758,#71759,#71760,#71761,#71762,#71763,#71764,#71765,#71766,#71767,
#71768,#71769,#71770,#71771,#71772,#71773,#71774,#71775,#71776,#71777,#71778,
#71779,#71780,#71781,#71782,#71783,#71784,#71785,#71786,#71787,#71788,#71789,
#71790,#71791,#71792,#71793,#71794,#71795,#71796,#71797,#71798,#71799,#71800,
#71801,#71802,#71803,#71804,#71805,#71806,#71807,#71808,#71809,#71810,#71811,
#71812,#71813,#71814,#71815,#71816,#71817,#71818,#71819,#71820,#71821,#71822,
#71823,#71824,#71825,#71826,#71827,#71828,#71829,#71830,#71831,#71832,#71833,
#71834,#71835,#71836),.UNSPECIFIED.,.F.,.F.,(4,3,3,3,3,3,3,3,3,3,3,3,3,
3,3,3,3,3,3,3,3,3,3,3,3,3,3,3,3,3,3,3,3,3,3,3,3,3,3,3,3,3,3,3,3,3,3,3,3,
3,3,3,3,3,3,3,3,3,3,3,3,3,3,3,3,3,3,3,3,3,3,3,4),(750.840644208115,750.945021396592,
751.051282858485,751.109778832268,751.193517544114,751.277153055482,751.360705498881,
751.444194934733,751.527648885347,751.611085379193,751.694522488949,751.777978283867,
751.861522776597,751.945111859538,752.028835127096,752.109514842989,752.193253554835,
752.276889066202,752.360441509601,752.443930945452,752.527384896065,752.610821389912,
752.694258499667,752.777714294585,752.861258787314,752.944847870255,753.028571137813,
753.109250853709,753.192989565555,753.276625076922,753.360177520321,753.443666956172,
753.527120906785,753.610557400631,753.693994510387,753.777450305304,753.860994798034,
753.944583880975,754.028307148532,754.108986864429,754.192725576275,754.276361087642,
754.359913531041,754.443402966892,754.526856917506,754.610293411352,754.693730521108,
754.777186316025,754.860730808755,754.944319891696,755.028043159254,755.108722875149,
755.192461586995,755.276097098363,755.359649541761,755.443138977612,755.526592928226,
755.610029422072,755.693466531828,755.776922326745,755.860466819475,755.944055902416,
756.027779169974,756.108458885869,756.192212058086,756.277206748794,756.360750268974,
756.444236006182,756.527682081341,756.613803956943,756.697243624074,756.784706603911,
756.872169583747),.UNSPECIFIED.);
#528=B_SPLINE_CURVE_WITH_KNOTS('',3,(#71837,#71838,#71839,#71840,#71841,
#71842,#71843,#71844,#71845,#71846),.UNSPECIFIED.,.F.,.F.,(4,3,3,4),(750.589376852607,
750.672010998785,750.756327603362,750.840644207939),.UNSPECIFIED.);
#529=B_SPLINE_CURVE_WITH_KNOTS('',3,(#71848,#71849,#71850,#71851,#71852,
#71853,#71854,#71855,#71856,#71857),.UNSPECIFIED.,.F.,.F.,(4,3,3,4),(750.590310680117,
750.681704329962,750.772738826785,750.840644207789),.UNSPECIFIED.);
#530=B_SPLINE_CURVE_WITH_KNOTS('',3,(#71858,#71859,#71860,#71861,#71862,
#71863,#71864,#71865,#71866,#71867,#71868,#71869,#71870,#71871,#71872,#71873,
#71874,#71875,#71876,#71877,#71878,#71879,#71880,#71881,#71882,#71883,#71884,
#71885,#71886,#71887,#71888,#71889,#71890,#71891,#71892,#71893,#71894,#71895,
#71896,#71897,#71898,#71899,#71900,#71901,#71902,#71903,#71904,#71905,#71906,
#71907,#71908,#71909,#71910,#71911,#71912,#71913,#71914,#71915,#71916,#71917,
#71918,#71919,#71920,#71921,#71922,#71923,#71924,#71925,#71926,#71927,#71928,
#71929,#71930,#71931,#71932,#71933,#71934,#71935,#71936,#71937,#71938,#71939,
#71940,#71941,#71942,#71943,#71944,#71945,#71946,#71947,#71948,#71949,#71950,
#71951,#71952,#71953,#71954,#71955,#71956,#71957,#71958,#71959,#71960,#71961,
#71962,#71963,#71964,#71965,#71966,#71967,#71968,#71969,#71970,#71971,#71972,
#71973,#71974,#71975,#71976,#71977,#71978,#71979,#71980,#71981,#71982,#71983,
#71984,#71985,#71986,#71987,#71988,#71989,#71990,#71991,#71992,#71993,#71994,
#71995,#71996,#71997,#71998,#71999,#72000,#72001,#72002,#72003,#72004,#72005,
#72006,#72007,#72008,#72009,#72010,#72011,#72012,#72013,#72014,#72015,#72016,
#72017,#72018,#72019,#72020,#72021,#72022,#72023,#72024,#72025,#72026,#72027,
#72028,#72029,#72030,#72031,#72032,#72033,#72034,#72035,#72036,#72037,#72038,
#72039,#72040,#72041,#72042,#72043,#72044,#72045,#72046,#72047,#72048,#72049,
#72050,#72051,#72052,#72053,#72054,#72055,#72056,#72057,#72058,#72059,#72060,
#72061,#72062,#72063,#72064,#72065,#72066,#72067,#72068,#72069,#72070,#72071,
#72072,#72073,#72074,#72075,#72076,#72077),.UNSPECIFIED.,.F.,.F.,(4,3,3,
3,3,3,3,3,3,3,3,3,3,3,3,3,3,3,3,3,3,3,3,3,3,3,3,3,3,3,3,3,3,3,3,3,3,3,3,
3,3,3,3,3,3,3,3,3,3,3,3,3,3,3,3,3,3,3,3,3,3,3,3,3,3,3,3,3,3,3,3,3,3,4),
(750.840644207943,750.925672733848,751.010737480744,751.095853917042,751.181099834772,
751.266414222463,751.351886366408,751.420069451985,751.503808163831,751.587443675199,
751.670996118597,751.754485554448,751.837939505062,751.921375998908,752.004813108663,
752.088268903581,752.17181339631,752.255402479251,752.339125746809,752.419805462705,
752.503544174551,752.587179685918,752.670732129317,752.754221565168,752.837675515782,
752.921112009628,753.004549119384,753.088004914302,753.171549407032,753.255138489973,
753.33886175753,753.419541473425,753.503280185271,753.586915696638,753.670468140037,
753.753957575888,753.837411526502,753.920848020348,754.004285130103,754.087740925021,
754.17128541775,754.254874500691,754.338597768249,754.419277484145,754.503016195991,
754.586651707358,754.670204150757,754.753693586608,754.837147537222,754.920584031068,
755.004021140824,755.087476935742,755.171021428471,755.254610511412,755.33833377897,
755.419013494865,755.502752206711,755.586387718078,755.669940161476,755.753429597327,
755.836883547941,755.920320041787,756.003757151542,756.087212946459,756.170757439189,
756.25434652213,756.338069789687,756.418749505585,756.501937853318,756.585024809647,
756.668013059796,756.750944341703,756.833835667285,756.872694074728),
 .UNSPECIFIED.);
#531=B_SPLINE_CURVE_WITH_KNOTS('',3,(#72083,#72084,#72085,#72086,#72087,
#72088,#72089,#72090,#72091,#72092,#72093,#72094,#72095,#72096,#72097,#72098,
#72099,#72100,#72101,#72102,#72103,#72104,#72105,#72106,#72107,#72108,#72109,
#72110,#72111,#72112,#72113,#72114,#72115,#72116,#72117,#72118,#72119,#72120,
#72121,#72122,#72123,#72124,#72125,#72126,#72127,#72128,#72129,#72130,#72131,
#72132,#72133,#72134,#72135,#72136,#72137,#72138,#72139,#72140,#72141,#72142,
#72143,#72144,#72145,#72146,#72147,#72148,#72149,#72150,#72151,#72152,#72153,
#72154,#72155,#72156,#72157,#72158,#72159,#72160,#72161,#72162,#72163,#72164,
#72165,#72166,#72167,#72168,#72169,#72170,#72171,#72172,#72173,#72174,#72175,
#72176,#72177,#72178,#72179,#72180,#72181,#72182,#72183,#72184,#72185,#72186,
#72187,#72188,#72189,#72190,#72191,#72192,#72193,#72194,#72195,#72196,#72197,
#72198,#72199,#72200,#72201,#72202,#72203,#72204,#72205,#72206,#72207,#72208,
#72209,#72210,#72211,#72212,#72213,#72214,#72215,#72216,#72217,#72218,#72219,
#72220,#72221,#72222,#72223,#72224,#72225,#72226,#72227,#72228,#72229,#72230,
#72231,#72232,#72233,#72234,#72235,#72236,#72237,#72238,#72239,#72240,#72241,
#72242,#72243,#72244,#72245,#72246,#72247,#72248,#72249,#72250,#72251,#72252,
#72253,#72254,#72255,#72256,#72257,#72258,#72259,#72260,#72261,#72262,#72263,
#72264,#72265,#72266,#72267,#72268,#72269,#72270,#72271,#72272,#72273,#72274,
#72275,#72276,#72277,#72278,#72279,#72280,#72281,#72282,#72283,#72284,#72285,
#72286,#72287,#72288,#72289,#72290,#72291,#72292,#72293,#72294,#72295,#72296,
#72297,#72298,#72299,#72300,#72301,#72302),.UNSPECIFIED.,.F.,.F.,(4,3,3,
3,3,3,3,3,3,3,3,3,3,3,3,3,3,3,3,3,3,3,3,3,3,3,3,3,3,3,3,3,3,3,3,3,3,3,3,
3,3,3,3,3,3,3,3,3,3,3,3,3,3,3,3,3,3,3,3,3,3,3,3,3,3,3,3,3,3,3,3,3,3,4),
(757.123829515267,757.207340415428,757.290748533449,757.374074237987,757.457337823838,
757.540567305995,757.623780569666,757.706995898186,757.790231572581,757.873556122523,
757.956927157123,758.040428159847,758.107930907309,758.191669619155,758.275305130522,
758.35885757392,758.442347009771,758.525800960385,758.609237454231,758.692674563986,
758.776130358904,758.859674851634,758.943263934574,759.026987202132,759.107666918029,
759.191405629875,759.275041141243,759.358593584642,759.442083020493,759.525536971107,
759.608973464954,759.69241057471,759.775866369628,759.859410862358,759.942999945299,
760.026723212857,760.10740292875,760.191141640596,760.274777151963,760.358329595362,
760.441819031212,760.525272981826,760.608709475672,760.692146585428,760.775602380345,
760.859146873075,760.942735956016,761.026459223573,761.10713893947,761.190877651316,
761.274513162684,761.358065606082,761.441555041933,761.525008992547,761.608445486393,
761.691882596149,761.775338391067,761.858882883796,761.942471966738,762.026195234295,
762.10687495019,762.190613662036,762.274249173404,762.357801616802,762.441291052653,
762.524745003267,762.608181497114,762.691618606869,762.775074401788,762.858618894518,
762.942207977459,763.025931245016,763.10661096091,763.156242422283),
 .UNSPECIFIED.);
#532=B_SPLINE_CURVE_WITH_KNOTS('',3,(#72303,#72304,#72305,#72306,#72307,
#72308,#72309,#72310,#72311,#72312,#72313,#72314,#72315),.UNSPECIFIED.,
 .F.,.F.,(4,3,3,3,4),(756.872169583747,756.95576638285,757.039493869905,
757.108194896589,757.123829515119),.UNSPECIFIED.);
#533=B_SPLINE_CURVE_WITH_KNOTS('',3,(#72317,#72318,#72319,#72320,#72321,
#72322,#72323,#72324,#72325,#72326),.UNSPECIFIED.,.F.,.F.,(4,3,3,4),(756.872694074728,
756.955571692592,757.039700603857,757.123829515123),.UNSPECIFIED.);
#534=B_SPLINE_CURVE_WITH_KNOTS('',3,(#72327,#72328,#72329,#72330,#72331,
#72332,#72333,#72334,#72335,#72336,#72337,#72338,#72339,#72340,#72341,#72342,
#72343,#72344,#72345,#72346,#72347,#72348,#72349,#72350,#72351,#72352,#72353,
#72354,#72355,#72356,#72357,#72358,#72359,#72360,#72361,#72362,#72363,#72364,
#72365,#72366,#72367,#72368,#72369,#72370,#72371,#72372,#72373,#72374,#72375,
#72376,#72377,#72378,#72379,#72380,#72381,#72382,#72383,#72384,#72385,#72386,
#72387,#72388,#72389,#72390,#72391,#72392,#72393,#72394,#72395,#72396,#72397,
#72398,#72399,#72400,#72401,#72402,#72403,#72404,#72405,#72406,#72407,#72408,
#72409,#72410,#72411,#72412,#72413,#72414,#72415,#72416,#72417,#72418,#72419,
#72420,#72421,#72422,#72423,#72424,#72425,#72426,#72427,#72428,#72429,#72430,
#72431,#72432,#72433,#72434,#72435,#72436,#72437,#72438,#72439,#72440,#72441,
#72442,#72443,#72444,#72445,#72446,#72447,#72448,#72449,#72450,#72451,#72452,
#72453,#72454,#72455,#72456,#72457,#72458,#72459,#72460,#72461,#72462,#72463,
#72464,#72465,#72466,#72467,#72468,#72469,#72470,#72471,#72472,#72473,#72474,
#72475,#72476,#72477,#72478,#72479,#72480,#72481,#72482,#72483,#72484,#72485,
#72486,#72487,#72488,#72489,#72490,#72491,#72492,#72493,#72494,#72495,#72496,
#72497,#72498,#72499,#72500,#72501,#72502,#72503,#72504,#72505,#72506,#72507,
#72508,#72509,#72510,#72511,#72512,#72513,#72514,#72515,#72516,#72517,#72518,
#72519,#72520,#72521,#72522,#72523,#72524,#72525,#72526,#72527,#72528,#72529,
#72530,#72531,#72532,#72533,#72534,#72535,#72536,#72537,#72538,#72539,#72540,
#72541,#72542,#72543),.UNSPECIFIED.,.F.,.F.,(4,3,3,3,3,3,3,3,3,3,3,3,3,
3,3,3,3,3,3,3,3,3,3,3,3,3,3,3,3,3,3,3,3,3,3,3,3,3,3,3,3,3,3,3,3,3,3,3,3,
3,3,3,3,3,3,3,3,3,3,3,3,3,3,3,3,3,3,3,3,3,3,3,4),(757.123829515261,757.224985151375,
757.327544941235,757.418485516306,757.502224228152,757.585859739519,757.669412182918,
757.752901618769,757.836355569382,757.919792063228,758.003229172984,758.086684967901,
758.170229460631,758.253818543572,758.337541811129,758.418221527026,758.501960238872,
758.585595750239,758.669148193638,758.752637629489,758.836091580102,758.919528073949,
759.002965183704,759.086420978622,759.169965471351,759.253554554292,759.33727782185,
759.417957537746,759.501696249592,759.58533176096,759.668884204358,759.752373640209,
759.835827590823,759.919264084669,760.002701194424,760.086156989342,760.169701482072,
760.253290565013,760.33701383257,760.417693548466,760.501432260312,760.585067771679,
760.668620215078,760.752109650929,760.835563601543,760.919000095389,761.002437205144,
761.085893000062,761.169437492791,761.253026575732,761.33674984329,761.417429559186,
761.501168271032,761.584803782399,761.668356225798,761.751845661649,761.835299612263,
761.918736106109,762.002173215865,762.085629010782,762.169173503512,762.252762586453,
762.336485854011,762.417165569906,762.500773963721,762.5842500345,762.667649737885,
762.750991377849,762.834293214392,762.917591204417,763.000883927774,763.084224691449,
763.155323815868),.UNSPECIFIED.);
#535=B_SPLINE_CURVE_WITH_KNOTS('',3,(#72549,#72550,#72551,#72552,#72553,
#72554,#72555,#72556,#72557,#72558,#72559,#72560,#72561,#72562,#72563,#72564,
#72565,#72566,#72567,#72568,#72569,#72570,#72571,#72572,#72573,#72574,#72575,
#72576,#72577,#72578,#72579,#72580,#72581,#72582,#72583,#72584,#72585,#72586,
#72587,#72588,#72589,#72590,#72591,#72592,#72593,#72594,#72595,#72596,#72597,
#72598,#72599,#72600,#72601,#72602,#72603,#72604,#72605,#72606,#72607,#72608,
#72609,#72610,#72611,#72612,#72613,#72614,#72615,#72616,#72617,#72618,#72619,
#72620,#72621,#72622,#72623,#72624,#72625,#72626,#72627,#72628,#72629,#72630,
#72631,#72632,#72633,#72634,#72635,#72636,#72637,#72638,#72639,#72640,#72641,
#72642,#72643,#72644,#72645,#72646,#72647,#72648,#72649,#72650,#72651,#72652,
#72653,#72654,#72655,#72656,#72657,#72658,#72659,#72660,#72661,#72662,#72663,
#72664,#72665,#72666,#72667,#72668,#72669,#72670,#72671,#72672,#72673,#72674,
#72675,#72676,#72677,#72678,#72679,#72680,#72681,#72682,#72683,#72684,#72685,
#72686,#72687,#72688,#72689,#72690,#72691,#72692,#72693,#72694,#72695,#72696,
#72697,#72698,#72699,#72700,#72701,#72702,#72703,#72704,#72705,#72706,#72707,
#72708,#72709,#72710,#72711,#72712,#72713,#72714,#72715,#72716,#72717,#72718,
#72719,#72720,#72721,#72722,#72723,#72724,#72725,#72726,#72727,#72728,#72729,
#72730,#72731,#72732,#72733,#72734,#72735,#72736,#72737,#72738,#72739,#72740,
#72741,#72742,#72743,#72744,#72745,#72746,#72747,#72748,#72749,#72750,#72751,
#72752,#72753,#72754,#72755,#72756,#72757,#72758,#72759,#72760,#72761,#72762,
#72763,#72764,#72765,#72766,#72767,#72768),.UNSPECIFIED.,.F.,.F.,(4,3,3,
3,3,3,3,3,3,3,3,3,3,3,3,3,3,3,3,3,3,3,3,3,3,3,3,3,3,3,3,3,3,3,3,3,3,3,3,
3,3,3,3,3,3,3,3,3,3,3,3,3,3,3,3,3,3,3,3,3,3,3,3,3,3,3,3,3,3,3,3,3,3,4),
(763.407014822298,763.489990676255,763.572943345094,763.655887431654,763.738841417603,
763.821823788036,763.904900247605,763.988030719312,764.071284328313,764.10634697163,
764.190085683476,764.273721194844,764.357273638242,764.440763074093,764.524217024707,
764.607653518553,764.691090628309,764.774546423226,764.858090915956,764.941679998897,
765.025403266455,765.10608298235,765.189821694196,765.273457205564,765.357009648962,
765.440499084813,765.523953035426,765.607389529273,765.690826639028,765.774282433945,
765.857826926675,765.941416009616,766.025139277173,766.10581899307,766.189557704916,
766.273193216284,766.356745659682,766.440235095533,766.523689046147,766.607125539993,
766.690562649748,766.774018444666,766.857562937396,766.941152020337,767.024875287894,
767.10555500379,767.189293715636,767.272929227004,767.356481670402,767.439971106254,
767.523425056867,767.606861550714,767.690298660469,767.773754455387,767.857298948116,
767.940888031058,768.024611298615,768.10529101451,768.189029726356,768.272665237723,
768.356217681122,768.439707116974,768.523161067587,768.606597561434,768.690034671189,
768.773490466107,768.857034958837,768.940624041778,769.024347309336,769.105027025231,
769.190345221994,769.275557890134,769.36065028321,769.439640659244),
 .UNSPECIFIED.);
#536=B_SPLINE_CURVE_WITH_KNOTS('',3,(#72769,#72770,#72771,#72772,#72773,
#72774,#72775,#72776,#72777,#72778),.UNSPECIFIED.,.F.,.F.,(4,3,3,4),(763.156242422283,
763.257984034045,763.358484794115,763.40701482215),.UNSPECIFIED.);
#537=B_SPLINE_CURVE_WITH_KNOTS('',3,(#72780,#72781,#72782,#72783,#72784,
#72785,#72786,#72787,#72788,#72789),.UNSPECIFIED.,.F.,.F.,(4,3,3,4),(763.155323815868,
763.238763926004,763.322889374058,763.407014822111),.UNSPECIFIED.);
#538=B_SPLINE_CURVE_WITH_KNOTS('',3,(#72790,#72791,#72792,#72793,#72794,
#72795,#72796,#72797,#72798,#72799,#72800,#72801,#72802,#72803,#72804,#72805,
#72806,#72807,#72808,#72809,#72810,#72811,#72812,#72813,#72814,#72815,#72816,
#72817,#72818,#72819,#72820,#72821,#72822,#72823,#72824,#72825,#72826,#72827,
#72828,#72829,#72830,#72831,#72832,#72833,#72834,#72835,#72836,#72837,#72838,
#72839,#72840,#72841,#72842,#72843,#72844,#72845,#72846,#72847,#72848,#72849,
#72850,#72851,#72852,#72853,#72854,#72855,#72856,#72857,#72858,#72859,#72860,
#72861,#72862,#72863,#72864,#72865,#72866,#72867,#72868,#72869,#72870,#72871,
#72872,#72873,#72874,#72875,#72876,#72877,#72878,#72879,#72880,#72881,#72882,
#72883,#72884,#72885,#72886,#72887,#72888,#72889,#72890,#72891,#72892,#72893,
#72894,#72895,#72896,#72897,#72898,#72899,#72900,#72901,#72902,#72903,#72904,
#72905,#72906,#72907,#72908,#72909,#72910,#72911,#72912,#72913,#72914,#72915,
#72916,#72917,#72918,#72919,#72920,#72921,#72922,#72923,#72924,#72925,#72926,
#72927,#72928,#72929,#72930,#72931,#72932,#72933,#72934,#72935,#72936,#72937,
#72938,#72939,#72940,#72941,#72942,#72943,#72944,#72945,#72946,#72947,#72948,
#72949,#72950,#72951,#72952,#72953,#72954,#72955,#72956,#72957,#72958,#72959,
#72960,#72961,#72962,#72963,#72964,#72965,#72966,#72967,#72968,#72969,#72970,
#72971,#72972,#72973,#72974,#72975,#72976,#72977,#72978,#72979,#72980,#72981,
#72982,#72983,#72984,#72985,#72986,#72987,#72988,#72989,#72990,#72991,#72992,
#72993,#72994,#72995,#72996,#72997,#72998,#72999,#73000,#73001,#73002,#73003,
#73004,#73005,#73006,#73007,#73008,#73009,#73010,#73011,#73012),
 .UNSPECIFIED.,.F.,.F.,(4,3,3,3,3,3,3,3,3,3,3,3,3,3,3,3,3,3,3,3,3,3,3,3,
3,3,3,3,3,3,3,3,3,3,3,3,3,3,3,3,3,3,3,3,3,3,3,3,3,3,3,3,3,3,3,3,3,3,3,3,
3,3,3,3,3,3,3,3,3,3,3,3,3,3,4),(763.407014822302,763.416901580626,763.500640292472,
763.58427580384,763.667828247238,763.751317683089,763.834771633703,763.918208127549,
764.001645237305,764.085101032222,764.168645524952,764.252234607893,764.335957875451,
764.416637591346,764.500376303192,764.58401181456,764.667564257958,764.751053693809,
764.834507644423,764.917944138269,765.001381248025,765.084837042942,765.168381535672,
765.251970618613,765.335693886171,765.416373602067,765.500112313913,765.583747825281,
765.667300268679,765.75078970453,765.834243655144,765.91768014899,766.001117258746,
766.084573053663,766.168117546393,766.251706629334,766.335429896892,766.416109612787,
766.499848324633,766.583483836,766.667036279399,766.75052571525,766.833979665864,
766.91741615971,767.000853269465,767.084309064383,767.167853557113,767.251442640054,
767.335165907611,767.415845623507,767.499584335353,767.58321984672,767.666772290119,
767.75026172597,767.833715676584,767.91715217043,768.000589280185,768.084045075103,
768.167589567832,768.251178650773,768.334901918331,768.415581634227,768.499320346073,
768.582955857441,768.666508300839,768.74999773669,768.833451687304,768.91688818115,
769.000325290906,769.083781085823,769.167325578553,769.250914661494,769.334637929052,
769.415317644947,769.43928124014),.UNSPECIFIED.);
#539=B_SPLINE_CURVE_WITH_KNOTS('',3,(#73018,#73019,#73020,#73021,#73022,
#73023,#73024,#73025,#73026,#73027,#73028,#73029,#73030,#73031,#73032,#73033,
#73034,#73035,#73036,#73037,#73038,#73039,#73040,#73041,#73042,#73043,#73044,
#73045,#73046,#73047,#73048,#73049,#73050,#73051,#73052,#73053,#73054,#73055,
#73056,#73057,#73058,#73059,#73060,#73061,#73062,#73063,#73064,#73065,#73066,
#73067,#73068,#73069,#73070,#73071,#73072,#73073,#73074,#73075,#73076,#73077,
#73078,#73079,#73080,#73081,#73082,#73083,#73084,#73085,#73086,#73087,#73088,
#73089,#73090,#73091,#73092,#73093,#73094,#73095,#73096,#73097,#73098,#73099,
#73100,#73101,#73102,#73103,#73104,#73105,#73106,#73107,#73108,#73109,#73110,
#73111,#73112,#73113,#73114,#73115,#73116,#73117,#73118,#73119,#73120,#73121,
#73122,#73123,#73124,#73125,#73126,#73127,#73128,#73129,#73130,#73131,#73132,
#73133,#73134,#73135,#73136,#73137,#73138,#73139,#73140,#73141,#73142,#73143,
#73144,#73145,#73146,#73147,#73148,#73149,#73150,#73151,#73152,#73153,#73154,
#73155,#73156,#73157,#73158,#73159,#73160,#73161,#73162,#73163,#73164,#73165,
#73166,#73167,#73168,#73169,#73170,#73171,#73172,#73173,#73174,#73175,#73176,
#73177,#73178,#73179,#73180,#73181,#73182,#73183,#73184,#73185,#73186,#73187,
#73188,#73189,#73190,#73191,#73192,#73193,#73194,#73195,#73196,#73197,#73198,
#73199,#73200,#73201,#73202,#73203,#73204,#73205,#73206,#73207,#73208,#73209,
#73210,#73211,#73212,#73213,#73214,#73215,#73216,#73217,#73218,#73219,#73220,
#73221,#73222,#73223,#73224,#73225,#73226,#73227,#73228,#73229,#73230,#73231,
#73232,#73233,#73234,#73235,#73236,#73237),.UNSPECIFIED.,.F.,.F.,(4,3,3,
3,3,3,3,3,3,3,3,3,3,3,3,3,3,3,3,3,3,3,3,3,3,3,3,3,3,3,3,3,3,3,3,3,3,3,3,
3,3,3,3,3,3,3,3,3,3,3,3,3,3,3,3,3,3,3,3,3,3,3,3,3,3,3,3,3,3,3,3,3,3,4),
(769.690200129639,769.781448738232,769.87313387068,769.965042746187,770.057269456248,
770.104763035951,770.188501747797,770.272137259165,770.355689702563,770.439179138414,
770.522633089028,770.606069582874,770.68950669263,770.772962487548,770.856506980277,
770.940096063218,771.023819330776,771.104499046671,771.188237758517,771.271873269884,
771.355425713283,771.438915149134,771.522369099747,771.605805593594,771.689242703349,
771.772698498267,771.856242990997,771.939832073938,772.023555341495,772.104235057391,
772.187973769237,772.271609280604,772.355161724003,772.438651159854,772.522105110468,
772.605541604314,772.688978714069,772.772434508987,772.855979001717,772.939568084657,
773.023291352215,773.103971068111,773.187709779957,773.271345291324,773.354897734723,
773.438387170574,773.521841121187,773.605277615034,773.688714724789,773.772170519706,
773.855715012436,773.939304095377,774.023027362935,774.103707078831,774.187445790677,
774.271081302045,774.354633745443,774.438123181294,774.521577131908,774.605013625754,
774.68845073551,774.771906530427,774.855451023157,774.939040106098,775.022763373656,
775.103443089551,775.185976551709,775.268415256539,775.350778378943,775.433085022286,
775.515361467243,775.597619913088,775.679898448971,775.721587636679),
 .UNSPECIFIED.);
#540=B_SPLINE_CURVE_WITH_KNOTS('',3,(#73238,#73239,#73240,#73241,#73242,
#73243,#73244,#73245,#73246,#73247),.UNSPECIFIED.,.F.,.F.,(4,3,3,4),(769.439640659244,
769.524591546901,769.609493151917,769.690200129478),.UNSPECIFIED.);
#541=B_SPLINE_CURVE_WITH_KNOTS('',3,(#73249,#73250,#73251,#73252,#73253,
#73254,#73255,#73256,#73257,#73258),.UNSPECIFIED.,.F.,.F.,(4,3,3,4),(769.43928124014,
769.544644755484,769.648309781464,769.690200129282),.UNSPECIFIED.);
#542=B_SPLINE_CURVE_WITH_KNOTS('',3,(#73259,#73260,#73261,#73262,#73263,
#73264,#73265,#73266,#73267,#73268,#73269,#73270,#73271,#73272,#73273,#73274,
#73275,#73276,#73277,#73278,#73279,#73280,#73281,#73282,#73283,#73284,#73285,
#73286,#73287,#73288,#73289,#73290,#73291,#73292,#73293,#73294,#73295,#73296,
#73297,#73298,#73299,#73300,#73301,#73302,#73303,#73304,#73305,#73306,#73307,
#73308,#73309,#73310,#73311,#73312,#73313,#73314,#73315,#73316,#73317,#73318,
#73319,#73320,#73321,#73322,#73323,#73324,#73325,#73326,#73327,#73328,#73329,
#73330,#73331,#73332,#73333,#73334,#73335,#73336,#73337,#73338,#73339,#73340,
#73341,#73342,#73343,#73344,#73345,#73346,#73347,#73348,#73349,#73350,#73351,
#73352,#73353,#73354,#73355,#73356,#73357,#73358,#73359,#73360,#73361,#73362,
#73363,#73364,#73365,#73366,#73367,#73368,#73369,#73370,#73371,#73372,#73373,
#73374,#73375,#73376,#73377,#73378,#73379,#73380,#73381,#73382,#73383,#73384,
#73385,#73386,#73387,#73388,#73389,#73390,#73391,#73392,#73393,#73394,#73395,
#73396,#73397,#73398,#73399,#73400,#73401,#73402,#73403,#73404,#73405,#73406,
#73407,#73408,#73409,#73410,#73411,#73412,#73413,#73414,#73415,#73416,#73417,
#73418,#73419,#73420,#73421,#73422,#73423,#73424,#73425,#73426,#73427,#73428,
#73429,#73430,#73431,#73432,#73433,#73434,#73435,#73436,#73437,#73438,#73439,
#73440,#73441,#73442,#73443,#73444,#73445,#73446,#73447,#73448,#73449,#73450,
#73451,#73452,#73453,#73454,#73455,#73456,#73457,#73458,#73459,#73460,#73461,
#73462,#73463,#73464,#73465,#73466,#73467,#73468,#73469,#73470,#73471,#73472,
#73473,#73474,#73475,#73476,#73477,#73478),.UNSPECIFIED.,.F.,.F.,(4,3,3,
3,3,3,3,3,3,3,3,3,3,3,3,3,3,3,3,3,3,3,3,3,3,3,3,3,3,3,3,3,3,3,3,3,3,3,3,
3,3,3,3,3,3,3,3,3,3,3,3,3,3,3,3,3,3,3,3,3,3,3,3,3,3,3,3,3,3,3,3,3,3,4),
(769.690200129482,769.77293722689,769.855637408681,769.938319894256,770.021003387505,
770.103706590002,770.186497939218,770.269335957804,770.352302829011,770.415053655667,
770.498792367513,770.58242787888,770.665980322279,770.74946975813,770.832923708743,
770.91636020259,770.999797312345,771.083253107263,771.166797599992,771.250386682933,
771.334109950491,771.414789666387,771.498528378233,771.582163889601,771.665716332999,
771.74920576885,771.832659719464,771.916096213311,771.999533323066,772.082989117984,
772.166533610713,772.250122693655,772.333845961212,772.414525677107,772.498264388953,
772.58189990032,772.665452343718,772.748941779569,772.832395730183,772.915832224029,
772.999269333785,773.082725128702,773.166269621432,773.249858704373,773.333581971931,
773.414261687828,773.498000399674,773.581635911042,773.66518835444,773.748677790291,
773.832131740905,773.915568234752,773.999005344507,774.082461139425,774.166005632155,
774.249594715096,774.333317982653,774.413997698548,774.497736410394,774.581371921762,
774.66492436516,774.748413801012,774.831867751625,774.915304245472,774.998741355227,
775.082197150145,775.165741642875,775.249330725816,775.333053993373,775.413733709268,
775.499747566005,775.585649680523,775.671420628738,775.722917187892),
 .UNSPECIFIED.);
#543=B_SPLINE_CURVE_WITH_KNOTS('',3,(#73484,#73485,#73486,#73487,#73488,
#73489,#73490,#73491,#73492,#73493,#73494,#73495,#73496,#73497,#73498,#73499,
#73500,#73501,#73502,#73503,#73504,#73505,#73506,#73507,#73508,#73509,#73510,
#73511,#73512,#73513,#73514,#73515,#73516,#73517,#73518,#73519,#73520,#73521,
#73522,#73523,#73524,#73525,#73526,#73527,#73528,#73529,#73530,#73531,#73532,
#73533,#73534,#73535,#73536,#73537,#73538,#73539,#73540,#73541,#73542,#73543,
#73544,#73545,#73546,#73547,#73548,#73549,#73550,#73551,#73552,#73553,#73554,
#73555,#73556,#73557,#73558,#73559,#73560,#73561,#73562,#73563,#73564,#73565,
#73566,#73567,#73568,#73569,#73570,#73571,#73572,#73573,#73574,#73575,#73576,
#73577,#73578,#73579,#73580,#73581,#73582,#73583,#73584,#73585,#73586,#73587,
#73588,#73589,#73590,#73591,#73592,#73593,#73594,#73595,#73596,#73597,#73598,
#73599,#73600,#73601,#73602,#73603,#73604,#73605,#73606,#73607,#73608,#73609,
#73610,#73611,#73612,#73613,#73614,#73615,#73616,#73617,#73618,#73619,#73620,
#73621,#73622,#73623,#73624,#73625,#73626,#73627,#73628,#73629,#73630,#73631,
#73632,#73633,#73634,#73635,#73636,#73637,#73638,#73639,#73640,#73641,#73642,
#73643,#73644,#73645,#73646,#73647,#73648,#73649,#73650,#73651,#73652,#73653,
#73654,#73655,#73656,#73657,#73658,#73659,#73660,#73661,#73662,#73663,#73664,
#73665,#73666,#73667,#73668,#73669,#73670,#73671,#73672,#73673,#73674,#73675,
#73676,#73677,#73678,#73679,#73680,#73681,#73682,#73683,#73684,#73685,#73686,
#73687,#73688,#73689,#73690,#73691,#73692,#73693,#73694,#73695,#73696,#73697,
#73698,#73699,#73700),.UNSPECIFIED.,.F.,.F.,(4,3,3,3,3,3,3,3,3,3,3,3,3,
3,3,3,3,3,3,3,3,3,3,3,3,3,3,3,3,3,3,3,3,3,3,3,3,3,3,3,3,3,3,3,3,3,3,3,3,
3,3,3,3,3,3,3,3,3,3,3,3,3,3,3,3,3,3,3,3,3,3,3,4),(775.973385436658,776.103179100272,
776.186917812118,776.270553323486,776.354105766885,776.437595202736,776.52104915335,
776.604485647197,776.687922756953,776.77137855187,776.8549230446,776.938512127542,
777.0222353951,777.102915110992,777.186653822838,777.270289334205,777.353841777604,
777.437331213455,777.520785164068,777.604221657914,777.68765876767,777.771114562588,
777.854659055317,777.938248138258,778.021971405816,778.102651121712,778.186389833558,
778.270025344926,778.353577788324,778.437067224175,778.520521174789,778.603957668635,
778.687394778391,778.770850573309,778.854395066038,778.937984148979,779.021707416537,
779.102387132432,779.186125844278,779.269761355645,779.353313799044,779.436803234895,
779.520257185508,779.603693679355,779.68713078911,779.770586584028,779.854131076757,
779.937720159698,780.021443427256,780.102123143152,780.185861854998,780.269497366365,
780.353049809764,780.436539245615,780.519993196228,780.603429690075,780.68686679983,
780.770322594748,780.853867087477,780.937456170418,781.021179437976,781.101859153872,
781.185603479214,781.269243330783,781.352798846523,781.436285919035,781.51973564543,
781.603166114165,781.686595396955,781.770079645405,781.853591517192,781.937202545892,
782.005065761364),.UNSPECIFIED.);
#544=B_SPLINE_CURVE_WITH_KNOTS('',3,(#73701,#73702,#73703,#73704,#73705,
#73706,#73707,#73708,#73709,#73710),.UNSPECIFIED.,.F.,.F.,(4,3,3,4),(775.721587636679,
775.803934072365,775.888659754447,775.973385436529),.UNSPECIFIED.);
#545=B_SPLINE_CURVE_WITH_KNOTS('',3,(#73712,#73713,#73714,#73715,#73716,
#73717,#73718,#73719,#73720,#73721),.UNSPECIFIED.,.F.,.F.,(4,3,3,4),(775.722917187892,
775.808540259658,775.894086620738,775.973385436661),.UNSPECIFIED.);
#546=B_SPLINE_CURVE_WITH_KNOTS('',3,(#73722,#73723,#73724,#73725,#73726,
#73727,#73728,#73729,#73730,#73731,#73732,#73733,#73734,#73735,#73736,#73737,
#73738,#73739,#73740,#73741,#73742,#73743,#73744,#73745,#73746,#73747,#73748,
#73749,#73750,#73751,#73752,#73753,#73754,#73755,#73756,#73757,#73758,#73759,
#73760,#73761,#73762,#73763,#73764,#73765,#73766,#73767,#73768,#73769,#73770,
#73771,#73772,#73773,#73774,#73775,#73776,#73777,#73778,#73779,#73780,#73781,
#73782,#73783,#73784,#73785,#73786,#73787,#73788,#73789,#73790,#73791,#73792,
#73793,#73794,#73795,#73796,#73797,#73798,#73799,#73800,#73801,#73802,#73803,
#73804,#73805,#73806,#73807,#73808,#73809,#73810,#73811,#73812,#73813,#73814,
#73815,#73816,#73817,#73818,#73819,#73820,#73821,#73822,#73823,#73824,#73825,
#73826,#73827,#73828,#73829,#73830,#73831,#73832,#73833,#73834,#73835,#73836,
#73837,#73838,#73839,#73840,#73841,#73842,#73843,#73844,#73845,#73846,#73847,
#73848,#73849,#73850,#73851,#73852,#73853,#73854,#73855,#73856,#73857,#73858,
#73859,#73860,#73861,#73862,#73863,#73864,#73865,#73866,#73867,#73868,#73869,
#73870,#73871,#73872,#73873,#73874,#73875,#73876,#73877,#73878,#73879,#73880,
#73881,#73882,#73883,#73884,#73885,#73886,#73887,#73888,#73889,#73890,#73891,
#73892,#73893,#73894,#73895,#73896,#73897,#73898,#73899,#73900,#73901,#73902,
#73903,#73904,#73905,#73906,#73907,#73908,#73909,#73910,#73911,#73912,#73913,
#73914,#73915,#73916,#73917,#73918,#73919,#73920,#73921,#73922,#73923,#73924,
#73925,#73926,#73927,#73928,#73929,#73930,#73931,#73932,#73933,#73934,#73935,
#73936,#73937,#73938,#73939,#73940,#73941),.UNSPECIFIED.,.F.,.F.,(4,3,3,
3,3,3,3,3,3,3,3,3,3,3,3,3,3,3,3,3,3,3,3,3,3,3,3,3,3,3,3,3,3,3,3,3,3,3,3,
3,3,3,3,3,3,3,3,3,3,3,3,3,3,3,3,3,3,3,3,3,3,3,3,3,3,3,3,3,3,3,3,3,3,4),
(775.973385436787,776.06330864179,776.15358475724,776.244037792623,776.334782116871,
776.413469719988,776.497208431834,776.580843943202,776.6643963866,776.747885822451,
776.831339773064,776.914776266911,776.998213376666,777.081669171584,777.165213664314,
777.248802747254,777.332526014812,777.413205730708,777.496944442554,777.580579953921,
777.664132397319,777.74762183317,777.831075783784,777.91451227763,777.997949387385,
778.081405182303,778.164949675032,778.248538757973,778.33226202553,778.412941741428,
778.496680453274,778.580315964642,778.663868408041,778.747357843892,778.830811794506,
778.914248288352,778.997685398108,779.081141193026,779.164685685756,779.248274768697,
779.331998036255,779.412677752149,779.496416463995,779.580051975362,779.663604418761,
779.747093854612,779.830547805226,779.913984299072,779.997421408828,780.080877203746,
780.164421696475,780.248010779416,780.331734046974,780.412413762869,780.496152474715,
780.579787986082,780.663340429481,780.746829865331,780.830283815945,780.913720309791,
780.997157419546,781.080613214464,781.164157707193,781.247746790134,781.331470057691,
781.412149773589,781.494627159821,781.577009465221,781.659315904408,781.745694675271,
781.827910312565,781.910108877223,781.992320812228,782.004830987862),
 .UNSPECIFIED.);
#547=B_SPLINE_CURVE_WITH_KNOTS('',3,(#73947,#73948,#73949,#73950,#73951,
#73952,#73953,#73954,#73955,#73956,#73957,#73958,#73959,#73960,#73961,#73962,
#73963,#73964,#73965,#73966,#73967,#73968,#73969,#73970,#73971,#73972,#73973,
#73974,#73975,#73976,#73977,#73978,#73979,#73980,#73981,#73982,#73983,#73984,
#73985,#73986,#73987,#73988,#73989,#73990,#73991,#73992,#73993,#73994,#73995,
#73996,#73997,#73998,#73999,#74000,#74001,#74002,#74003,#74004,#74005,#74006,
#74007,#74008,#74009,#74010,#74011,#74012,#74013,#74014,#74015,#74016,#74017,
#74018,#74019,#74020,#74021,#74022,#74023,#74024,#74025,#74026,#74027,#74028,
#74029,#74030,#74031,#74032,#74033,#74034,#74035,#74036,#74037,#74038,#74039,
#74040,#74041,#74042,#74043,#74044,#74045,#74046,#74047,#74048,#74049,#74050,
#74051,#74052,#74053,#74054,#74055,#74056,#74057,#74058,#74059,#74060,#74061,
#74062,#74063,#74064,#74065,#74066,#74067,#74068,#74069,#74070,#74071,#74072,
#74073,#74074,#74075,#74076,#74077,#74078,#74079,#74080,#74081,#74082,#74083,
#74084,#74085,#74086,#74087,#74088,#74089,#74090,#74091,#74092,#74093,#74094,
#74095,#74096,#74097,#74098,#74099,#74100,#74101,#74102,#74103,#74104,#74105,
#74106,#74107,#74108,#74109,#74110,#74111,#74112,#74113,#74114,#74115,#74116,
#74117,#74118,#74119,#74120,#74121,#74122,#74123,#74124,#74125,#74126,#74127,
#74128,#74129,#74130,#74131,#74132,#74133,#74134,#74135,#74136,#74137,#74138,
#74139,#74140,#74141,#74142,#74143,#74144,#74145,#74146,#74147,#74148,#74149,
#74150,#74151,#74152,#74153,#74154,#74155,#74156,#74157,#74158,#74159,#74160,
#74161,#74162,#74163,#74164,#74165,#74166),.UNSPECIFIED.,.F.,.F.,(4,3,3,
3,3,3,3,3,3,3,3,3,3,3,3,3,3,3,3,3,3,3,3,3,3,3,3,3,3,3,3,3,3,3,3,3,3,3,3,
3,3,3,3,3,3,3,3,3,3,3,3,3,3,3,3,3,3,3,3,3,3,3,3,3,3,3,3,3,3,3,3,3,3,4),
(782.256570743945,782.338963542711,782.421275411456,782.506282381938,782.588503237466,
782.670712082992,782.752927947646,782.835169864301,782.917500230731,782.999883639915,
783.082381157245,783.101331175313,783.185069887159,783.268705398526,783.352257841925,
783.435747277776,783.519201228389,783.602637722236,783.686074831991,783.769530626909,
783.853075119638,783.936664202579,784.020387470136,784.101067186033,784.184805897879,
784.268441409246,784.351993852645,784.435483288496,784.51893723911,784.602373732956,
784.685810842711,784.769266637628,784.852811130358,784.936400213299,785.020123480856,
785.100803196753,785.184541908599,785.268177419966,785.351729863365,785.435219299217,
785.51867324983,785.602109743676,785.685546853432,785.76900264835,785.852547141079,
785.93613622402,786.019859491578,786.100539207473,786.184277919319,786.267913430686,
786.351465874085,786.434955309936,786.51840926055,786.601845754396,786.685282864151,
786.768738659069,786.852283151799,786.93587223474,787.019595502297,787.100275218193,
787.184013930039,787.267649441406,787.351201884805,787.434691320656,787.51814527127,
787.601581765116,787.685018874872,787.768474669789,787.852019162519,787.93560824546,
788.019331513017,788.100011228913,788.194728462435,788.289445695958),
 .UNSPECIFIED.);
#548=B_SPLINE_CURVE_WITH_KNOTS('',3,(#74167,#74168,#74169,#74170,#74171,
#74172,#74173,#74174,#74175,#74176,#74177,#74178,#74179),.UNSPECIFIED.,
 .F.,.F.,(4,3,3,3,4),(782.005065761364,782.088818368043,782.101595164592,
782.240882181406,782.256570743837),.UNSPECIFIED.);
#549=B_SPLINE_CURVE_WITH_KNOTS('',3,(#74181,#74182,#74183,#74184,#74185,
#74186,#74187,#74188,#74189,#74190),.UNSPECIFIED.,.F.,.F.,(4,3,3,4),(782.004830987862,
782.087103904726,782.17183732423,782.256570743733),.UNSPECIFIED.);
#550=B_SPLINE_CURVE_WITH_KNOTS('',3,(#74191,#74192,#74193,#74194,#74195,
#74196,#74197,#74198,#74199,#74200,#74201,#74202,#74203,#74204,#74205,#74206,
#74207,#74208,#74209,#74210,#74211,#74212,#74213,#74214,#74215,#74216,#74217,
#74218,#74219,#74220,#74221,#74222,#74223,#74224,#74225,#74226,#74227,#74228,
#74229,#74230,#74231,#74232,#74233,#74234,#74235,#74236,#74237,#74238,#74239,
#74240,#74241,#74242,#74243,#74244,#74245,#74246,#74247,#74248,#74249,#74250,
#74251,#74252,#74253,#74254,#74255,#74256,#74257,#74258,#74259,#74260,#74261,
#74262,#74263,#74264,#74265,#74266,#74267,#74268,#74269,#74270,#74271,#74272,
#74273,#74274,#74275,#74276,#74277,#74278,#74279,#74280,#74281,#74282,#74283,
#74284,#74285,#74286,#74287,#74288,#74289,#74290,#74291,#74292,#74293,#74294,
#74295,#74296,#74297,#74298,#74299,#74300,#74301,#74302,#74303,#74304,#74305,
#74306,#74307,#74308,#74309,#74310,#74311,#74312,#74313,#74314,#74315,#74316,
#74317,#74318,#74319,#74320,#74321,#74322,#74323,#74324,#74325,#74326,#74327,
#74328,#74329,#74330,#74331,#74332,#74333,#74334,#74335,#74336,#74337,#74338,
#74339,#74340,#74341,#74342,#74343,#74344,#74345,#74346,#74347,#74348,#74349,
#74350,#74351,#74352,#74353,#74354,#74355,#74356,#74357,#74358,#74359,#74360,
#74361,#74362,#74363,#74364,#74365,#74366,#74367,#74368,#74369,#74370,#74371,
#74372,#74373,#74374,#74375,#74376,#74377,#74378,#74379,#74380,#74381,#74382,
#74383,#74384,#74385,#74386,#74387,#74388,#74389,#74390,#74391,#74392,#74393,
#74394,#74395,#74396,#74397,#74398,#74399,#74400,#74401,#74402,#74403,#74404,
#74405,#74406,#74407,#74408,#74409,#74410),.UNSPECIFIED.,.F.,.F.,(4,3,3,
3,3,3,3,3,3,3,3,3,3,3,3,3,3,3,3,3,3,3,3,3,3,3,3,3,3,3,3,3,3,3,3,3,3,3,3,
3,3,3,3,3,3,3,3,3,3,3,3,3,3,3,3,3,3,3,3,3,3,3,3,3,3,3,3,3,3,3,3,3,3,4),
(782.256570743841,782.395663585156,782.411885784309,782.495624496155,782.579260007523,
782.662812450921,782.746301886772,782.829755837386,782.913192331232,782.996629440987,
783.080085235905,783.163629728635,783.247218811576,783.330942079133,783.411621795029,
783.495360506875,783.578996018242,783.662548461641,783.746037897492,783.829491848105,
783.912928341952,783.996365451707,784.079821246625,784.163365739354,784.246954822295,
784.330678089853,784.411357805749,784.495096517595,784.578732028962,784.662284472361,
784.745773908211,784.829227858825,784.912664352671,784.996101462426,785.079557257344,
785.163101750073,785.246690833014,785.330414100572,785.411093816469,785.494832528315,
785.578468039683,785.662020483082,785.745509918933,785.828963869547,785.912400363393,
785.995837473149,786.079293268067,786.162837760797,786.246426843738,786.330150111296,
786.41082982719,786.494568539036,786.578204050404,786.661756493802,786.745245929653,
786.828699880267,786.912136374113,786.995573483869,787.079029278786,787.162573771516,
787.246162854457,787.329886122015,787.41056583791,787.494311721008,787.577952792745,
787.661509192539,787.744995902321,787.828444788344,787.91187393934,787.995301426878,
788.078778332683,788.16228266764,788.245873176523,788.288184568376),
 .UNSPECIFIED.);
#551=B_SPLINE_CURVE_WITH_KNOTS('',3,(#74416,#74417,#74418,#74419,#74420,
#74421,#74422,#74423,#74424,#74425,#74426,#74427,#74428,#74429,#74430,#74431,
#74432,#74433,#74434,#74435,#74436,#74437,#74438,#74439,#74440,#74441,#74442,
#74443,#74444,#74445,#74446,#74447,#74448,#74449,#74450,#74451,#74452,#74453,
#74454,#74455,#74456,#74457,#74458,#74459,#74460,#74461,#74462,#74463,#74464,
#74465,#74466,#74467,#74468,#74469,#74470,#74471,#74472,#74473,#74474,#74475,
#74476,#74477,#74478,#74479,#74480,#74481,#74482,#74483,#74484,#74485,#74486,
#74487,#74488,#74489,#74490,#74491,#74492,#74493,#74494,#74495,#74496,#74497,
#74498,#74499,#74500,#74501,#74502,#74503,#74504,#74505,#74506,#74507,#74508,
#74509,#74510,#74511,#74512,#74513,#74514,#74515,#74516,#74517,#74518,#74519,
#74520,#74521,#74522,#74523,#74524,#74525,#74526,#74527,#74528,#74529,#74530,
#74531,#74532,#74533,#74534,#74535,#74536,#74537,#74538,#74539,#74540,#74541,
#74542,#74543,#74544,#74545,#74546,#74547,#74548,#74549,#74550,#74551,#74552,
#74553,#74554,#74555,#74556,#74557,#74558,#74559,#74560,#74561,#74562,#74563,
#74564,#74565,#74566,#74567,#74568,#74569,#74570,#74571,#74572,#74573,#74574,
#74575,#74576,#74577,#74578,#74579,#74580,#74581,#74582,#74583,#74584,#74585,
#74586,#74587,#74588,#74589,#74590,#74591,#74592,#74593,#74594,#74595,#74596,
#74597,#74598,#74599,#74600,#74601,#74602,#74603,#74604,#74605,#74606,#74607,
#74608,#74609,#74610,#74611,#74612,#74613,#74614,#74615,#74616,#74617,#74618,
#74619,#74620,#74621,#74622,#74623,#74624,#74625,#74626,#74627,#74628,#74629,
#74630,#74631,#74632,#74633,#74634,#74635),.UNSPECIFIED.,.F.,.F.,(4,3,3,
3,3,3,3,3,3,3,3,3,3,3,3,3,3,3,3,3,3,3,3,3,3,3,3,3,3,3,3,3,3,3,3,3,3,3,3,
3,3,3,3,3,3,3,3,3,3,3,3,3,3,3,3,3,3,3,3,3,3,3,3,3,3,3,3,3,3,3,3,3,3,4),
(788.539756051017,788.625278366436,788.710852095813,788.796491588863,788.88227330464,
788.968133743556,789.054151397246,789.099747239633,789.183485951479,789.267121462846,
789.350673906245,789.434163342096,789.51761729271,789.601053786556,789.684490896311,
789.767946691229,789.851491183959,789.9350802669,790.018803534458,790.099483250353,
790.183221962199,790.266857473567,790.350409916965,790.433899352816,790.51735330343,
790.600789797276,790.684226907031,790.767682701949,790.851227194678,790.934816277619,
791.018539545177,791.099219261073,791.182957972919,791.266593484287,791.350145927685,
791.433635363536,791.51708931415,791.600525807996,791.683962917752,791.76741871267,
791.8509632054,791.934552288341,792.018275555898,792.098955271794,792.18269398364,
792.266329495008,792.349881938406,792.433371374257,792.516825324871,792.600261818717,
792.683698928473,792.76715472339,792.85069921612,792.934288299061,793.018011566619,
793.098691282514,793.18242999436,793.266065505728,793.349617949126,793.433107384977,
793.516561335591,793.599997829437,793.683434939193,793.766890734111,793.85043522684,
793.934024309781,794.017747577339,794.098427293234,794.181408928667,794.264290706377,
794.347077006945,794.429807732937,794.51250434914,794.571705147957),
 .UNSPECIFIED.);
#552=B_SPLINE_CURVE_WITH_KNOTS('',3,(#74636,#74637,#74638,#74639,#74640,
#74641,#74642,#74643,#74644,#74645),.UNSPECIFIED.,.F.,.F.,(4,3,3,4),(788.289445695958,
788.379761119791,788.46977898198,788.53975605089),.UNSPECIFIED.);
#553=B_SPLINE_CURVE_WITH_KNOTS('',3,(#74647,#74648,#74649,#74650,#74651,
#74652,#74653,#74654,#74655,#74656),.UNSPECIFIED.,.F.,.F.,(4,3,3,4),(788.288184568376,
788.371924568467,788.41030184863,788.539756051021),.UNSPECIFIED.);
#554=B_SPLINE_CURVE_WITH_KNOTS('',3,(#74657,#74658,#74659,#74660,#74661,
#74662,#74663,#74664,#74665,#74666,#74667,#74668,#74669,#74670,#74671,#74672,
#74673,#74674,#74675,#74676,#74677,#74678,#74679,#74680,#74681,#74682,#74683,
#74684,#74685,#74686,#74687,#74688,#74689,#74690,#74691,#74692,#74693,#74694,
#74695,#74696,#74697,#74698,#74699,#74700,#74701,#74702,#74703,#74704,#74705,
#74706,#74707,#74708,#74709,#74710,#74711,#74712,#74713,#74714,#74715,#74716,
#74717,#74718,#74719,#74720,#74721,#74722,#74723,#74724,#74725,#74726,#74727,
#74728,#74729,#74730,#74731,#74732,#74733,#74734,#74735,#74736,#74737,#74738,
#74739,#74740,#74741,#74742,#74743,#74744,#74745,#74746,#74747,#74748,#74749,
#74750,#74751,#74752,#74753,#74754,#74755,#74756,#74757,#74758,#74759,#74760,
#74761,#74762,#74763,#74764,#74765,#74766,#74767,#74768,#74769,#74770,#74771,
#74772,#74773,#74774,#74775,#74776,#74777,#74778,#74779,#74780,#74781,#74782,
#74783,#74784,#74785,#74786,#74787,#74788,#74789,#74790,#74791,#74792,#74793,
#74794,#74795,#74796,#74797,#74798,#74799,#74800,#74801,#74802,#74803,#74804,
#74805,#74806,#74807,#74808,#74809,#74810,#74811,#74812,#74813,#74814,#74815,
#74816,#74817,#74818,#74819,#74820,#74821,#74822,#74823,#74824,#74825,#74826,
#74827,#74828,#74829,#74830,#74831,#74832,#74833,#74834,#74835,#74836,#74837,
#74838,#74839,#74840,#74841,#74842,#74843,#74844,#74845,#74846,#74847,#74848,
#74849,#74850,#74851,#74852,#74853,#74854,#74855,#74856,#74857,#74858,#74859,
#74860,#74861,#74862,#74863,#74864,#74865,#74866,#74867,#74868,#74869,#74870,
#74871,#74872,#74873,#74874,#74875,#74876),.UNSPECIFIED.,.F.,.F.,(4,3,3,
3,3,3,3,3,3,3,3,3,3,3,3,3,3,3,3,3,3,3,3,3,3,3,3,3,3,3,3,3,3,3,3,3,3,3,3,
3,3,3,3,3,3,3,3,3,3,3,3,3,3,3,3,3,3,3,3,3,3,3,3,3,3,3,3,3,3,3,3,3,3,4),
(788.53975605115,788.622232791737,788.70462275739,788.786947068423,788.869233268008,
788.951501468204,789.033770665122,789.116059853442,789.198434792231,789.280857252709,
789.363401284496,789.41003785935,789.493776571196,789.577412082563,789.660964525962,
789.744453961813,789.827907912427,789.911344406273,789.994781516028,790.078237310946,
790.161781803676,790.245370886617,790.329094154174,790.40977387007,790.493512581916,
790.577148093283,790.660700536682,790.744189972533,790.827643923146,790.911080416993,
790.994517526748,791.077973321666,791.161517814395,791.245106897336,791.328830164894,
791.40950988079,791.493248592636,791.576884104004,791.660436547402,791.743925983253,
791.827379933867,791.910816427713,791.994253537469,792.077709332387,792.161253825117,
792.244842908058,792.328566175615,792.40924589151,792.492984603356,792.576620114723,
792.660172558122,792.743661993973,792.827115944587,792.910552438433,792.993989548189,
793.077445343106,793.160989835836,793.244578918777,793.328302186335,793.40898190223,
793.492720614076,793.576356125443,793.659908568842,793.743398004692,793.826851955306,
793.910288449152,793.993725558907,794.077181353825,794.160725846555,794.244314929496,
794.328038197053,794.40871791295,794.500932310921,794.572597636804),
 .UNSPECIFIED.);
#555=B_SPLINE_CURVE_WITH_KNOTS('',3,(#74882,#74883,#74884,#74885,#74886,
#74887,#74888,#74889,#74890,#74891,#74892,#74893,#74894,#74895,#74896,#74897,
#74898,#74899,#74900,#74901,#74902,#74903,#74904,#74905,#74906,#74907,#74908,
#74909,#74910,#74911,#74912,#74913,#74914,#74915,#74916,#74917,#74918,#74919,
#74920,#74921,#74922,#74923,#74924,#74925,#74926,#74927,#74928,#74929,#74930,
#74931,#74932,#74933,#74934,#74935,#74936,#74937,#74938,#74939,#74940,#74941,
#74942,#74943,#74944,#74945,#74946,#74947,#74948,#74949,#74950,#74951,#74952,
#74953,#74954,#74955,#74956,#74957,#74958,#74959,#74960,#74961,#74962,#74963,
#74964,#74965,#74966,#74967,#74968,#74969,#74970,#74971,#74972,#74973,#74974,
#74975,#74976,#74977,#74978,#74979,#74980,#74981,#74982,#74983,#74984,#74985,
#74986,#74987,#74988,#74989,#74990,#74991,#74992,#74993,#74994,#74995,#74996,
#74997,#74998,#74999,#75000,#75001,#75002,#75003,#75004,#75005,#75006,#75007,
#75008,#75009,#75010,#75011,#75012,#75013,#75014,#75015,#75016,#75017,#75018,
#75019,#75020,#75021,#75022,#75023,#75024,#75025,#75026,#75027,#75028,#75029,
#75030,#75031,#75032,#75033,#75034,#75035,#75036,#75037,#75038,#75039,#75040,
#75041,#75042,#75043,#75044,#75045,#75046,#75047,#75048,#75049,#75050,#75051,
#75052,#75053,#75054,#75055,#75056,#75057,#75058,#75059,#75060,#75061,#75062,
#75063,#75064,#75065,#75066,#75067,#75068,#75069,#75070,#75071,#75072,#75073,
#75074,#75075,#75076,#75077,#75078,#75079,#75080,#75081,#75082,#75083,#75084,
#75085,#75086,#75087,#75088,#75089,#75090,#75091,#75092,#75093,#75094,#75095,
#75096,#75097,#75098),.UNSPECIFIED.,.F.,.F.,(4,3,3,3,3,3,3,3,3,3,3,3,3,
3,3,3,3,3,3,3,3,3,3,3,3,3,3,3,3,3,3,3,3,3,3,3,3,3,3,3,3,3,3,3,3,3,3,3,3,
3,3,3,3,3,3,3,3,3,3,3,3,3,3,3,3,3,3,3,3,3,3,3,4),(794.822941358398,794.926494078898,
795.031796927361,795.098163303954,795.1819020158,795.265537527167,795.349089970566,
795.432579406417,795.516033357031,795.599469850877,795.682906960633,795.76636275555,
795.84990724828,795.933496331221,796.017219598778,796.097899314674,796.18163802652,
796.265273537887,796.348825981286,796.432315417137,796.515769367751,796.599205861597,
796.682642971352,796.76609876627,796.849643258999,796.93323234194,797.016955609498,
797.097635325394,797.18137403724,797.265009548607,797.348561992006,797.432051427857,
797.51550537847,797.598941872317,797.682378982072,797.76583477699,797.849379269719,
797.93296835266,798.016691620218,798.097371336114,798.18111004796,798.264745559327,
798.348298002726,798.431787438577,798.515241389191,798.598677883037,798.682114992793,
798.765570787711,798.84911528044,798.932704363382,799.016427630939,799.097107346834,
799.18084605868,799.264481570047,799.348034013446,799.431523449297,799.514977399911,
799.598413893757,799.681851003513,799.765306798431,799.84885129116,799.932440374101,
800.016163641659,800.096843357555,800.180596935371,800.264831095732,800.348375393307,
800.431861628916,800.515307924047,800.6000984976,800.683536956606,800.769003587433,
800.85447021826),.UNSPECIFIED.);
#556=B_SPLINE_CURVE_WITH_KNOTS('',3,(#75099,#75100,#75101,#75102,#75103,
#75104,#75105,#75106,#75107,#75108),.UNSPECIFIED.,.F.,.F.,(4,3,3,4),(794.571705147957,
794.654391671142,794.738666514669,794.822941358196),.UNSPECIFIED.);
#557=B_SPLINE_CURVE_WITH_KNOTS('',3,(#75110,#75111,#75112,#75113,#75114,
#75115,#75116,#75117,#75118,#75119),.UNSPECIFIED.,.F.,.F.,(4,3,3,4),(794.572597636804,
794.664353272392,794.755727987324,794.822941358038),.UNSPECIFIED.);
#558=B_SPLINE_CURVE_WITH_KNOTS('',3,(#75120,#75121,#75122,#75123,#75124,
#75125,#75126,#75127,#75128,#75129,#75130,#75131,#75132,#75133,#75134,#75135,
#75136,#75137,#75138,#75139,#75140,#75141,#75142,#75143,#75144,#75145,#75146,
#75147,#75148,#75149,#75150,#75151,#75152,#75153,#75154,#75155,#75156,#75157,
#75158,#75159,#75160,#75161,#75162,#75163,#75164,#75165,#75166,#75167,#75168,
#75169,#75170,#75171,#75172,#75173,#75174,#75175,#75176,#75177,#75178,#75179,
#75180,#75181,#75182,#75183,#75184,#75185,#75186,#75187,#75188,#75189,#75190,
#75191,#75192,#75193,#75194,#75195,#75196,#75197,#75198,#75199,#75200,#75201,
#75202,#75203,#75204,#75205,#75206,#75207,#75208,#75209,#75210,#75211,#75212,
#75213,#75214,#75215,#75216,#75217,#75218,#75219,#75220,#75221,#75222,#75223,
#75224,#75225,#75226,#75227,#75228,#75229,#75230,#75231,#75232,#75233,#75234,
#75235,#75236,#75237,#75238,#75239,#75240,#75241,#75242,#75243,#75244,#75245,
#75246,#75247,#75248,#75249,#75250,#75251,#75252,#75253,#75254,#75255,#75256,
#75257,#75258,#75259,#75260,#75261,#75262,#75263,#75264,#75265,#75266,#75267,
#75268,#75269,#75270,#75271,#75272,#75273,#75274,#75275,#75276,#75277,#75278,
#75279,#75280,#75281,#75282,#75283,#75284,#75285,#75286,#75287,#75288,#75289,
#75290,#75291,#75292,#75293,#75294,#75295,#75296,#75297,#75298,#75299,#75300,
#75301,#75302,#75303,#75304,#75305,#75306,#75307,#75308,#75309,#75310,#75311,
#75312,#75313,#75314,#75315,#75316,#75317,#75318,#75319,#75320,#75321,#75322,
#75323,#75324,#75325,#75326,#75327,#75328,#75329,#75330,#75331,#75332,#75333,
#75334,#75335,#75336,#75337,#75338,#75339),.UNSPECIFIED.,.F.,.F.,(4,3,3,
3,3,3,3,3,3,3,3,3,3,3,3,3,3,3,3,3,3,3,3,3,3,3,3,3,3,3,3,3,3,3,3,3,3,3,3,
3,3,3,3,3,3,3,3,3,3,3,3,3,3,3,3,3,3,3,3,3,3,3,3,3,3,3,3,3,3,3,3,3,3,4),
(794.8229413582,794.90782555628,794.992741610013,795.077705281825,795.162794725737,
795.247949613061,795.333262560284,795.40845392367,795.492192635516,795.575828146884,
795.659380590282,795.742870026133,795.826323976747,795.909760470593,795.993197580348,
796.076653375266,796.160197867996,796.243786950937,796.327510218494,796.408189934391,
796.491928646237,796.575564157605,796.659116601003,796.742606036854,796.826059987468,
796.909496481314,796.992933591069,797.076389385987,797.159933878717,797.243522961658,
797.327246229216,797.407925945111,797.491664656957,797.575300168324,797.658852611723,
797.742342047574,797.825795998188,797.909232492034,797.992669601789,798.076125396707,
798.159669889436,798.243258972377,798.326982239935,798.407661955831,798.491400667677,
798.575036179045,798.658588622443,798.742078058294,798.825532008908,798.908968502754,
798.992405612509,799.075861407427,799.159405900156,799.242994983097,799.326718250655,
799.407397966551,799.491136678397,799.574772189765,799.658324633163,799.741814069014,
799.825268019628,799.908704513474,799.992141623229,800.075597418147,800.159141910877,
800.242730993818,800.326454261375,800.407133977271,800.490394748986,800.573553587345,
800.656612671435,800.739614281639,800.822574242566,800.855023018815),
 .UNSPECIFIED.);
#559=B_SPLINE_CURVE_WITH_KNOTS('',3,(#75345,#75346,#75347,#75348,#75349,
#75350,#75351,#75352,#75353,#75354,#75355,#75356,#75357,#75358,#75359,#75360,
#75361,#75362,#75363,#75364,#75365,#75366,#75367,#75368,#75369,#75370,#75371,
#75372,#75373,#75374,#75375,#75376,#75377,#75378,#75379,#75380,#75381,#75382,
#75383,#75384,#75385,#75386,#75387,#75388,#75389,#75390,#75391,#75392,#75393,
#75394,#75395,#75396,#75397,#75398,#75399,#75400,#75401,#75402,#75403,#75404,
#75405,#75406,#75407,#75408,#75409,#75410,#75411,#75412,#75413,#75414,#75415,
#75416,#75417,#75418,#75419,#75420,#75421,#75422,#75423,#75424,#75425,#75426,
#75427,#75428,#75429,#75430,#75431,#75432,#75433,#75434,#75435,#75436,#75437,
#75438,#75439,#75440,#75441,#75442,#75443,#75444,#75445,#75446,#75447,#75448,
#75449,#75450,#75451,#75452,#75453,#75454,#75455,#75456,#75457,#75458,#75459,
#75460,#75461,#75462,#75463,#75464,#75465,#75466,#75467,#75468,#75469,#75470,
#75471,#75472,#75473,#75474,#75475,#75476,#75477,#75478,#75479,#75480,#75481,
#75482,#75483,#75484,#75485,#75486,#75487,#75488,#75489,#75490,#75491,#75492,
#75493,#75494,#75495,#75496,#75497,#75498,#75499,#75500,#75501,#75502,#75503,
#75504,#75505,#75506,#75507,#75508,#75509,#75510,#75511,#75512,#75513,#75514,
#75515,#75516,#75517,#75518,#75519,#75520,#75521,#75522,#75523,#75524,#75525,
#75526,#75527,#75528,#75529,#75530,#75531,#75532,#75533,#75534,#75535,#75536,
#75537,#75538,#75539,#75540,#75541,#75542,#75543,#75544,#75545,#75546,#75547,
#75548,#75549,#75550,#75551,#75552,#75553,#75554,#75555,#75556,#75557,#75558,
#75559,#75560,#75561,#75562,#75563,#75564),.UNSPECIFIED.,.F.,.F.,(4,3,3,
3,3,3,3,3,3,3,3,3,3,3,3,3,3,3,3,3,3,3,3,3,3,3,3,3,3,3,3,3,3,3,3,3,3,3,3,
3,3,3,3,3,3,3,3,3,3,3,3,3,3,3,3,3,3,3,3,3,3,3,3,3,3,3,3,3,3,3,3,3,3,4),
(801.106126665561,801.189723746874,801.273217813649,801.356629148145,801.439977959442,
801.523292059086,801.606589416156,801.689888236832,801.773206724513,801.856613996548,
801.940066996113,802.023651605219,802.096315378995,802.180054090841,802.263689602208,
802.347242045607,802.430731481458,802.514185432072,802.597621925918,802.681059035674,
802.764514830591,802.848059323321,802.931648406262,803.015371673819,803.096051389715,
803.179790101561,803.263425612928,803.346978056327,803.430467492178,803.513921442791,
803.597357936638,803.680795046393,803.764250841311,803.847795334041,803.931384416982,
804.015107684539,804.095787400435,804.179526112281,804.263161623648,804.346714067047,
804.430203502898,804.513657453512,804.597093947358,804.680531057113,804.76398685203,
804.84753134476,804.931120427701,805.014843695259,805.095523411155,805.179262123001,
805.262897634369,805.346450077767,805.429939513618,805.513393464232,805.596829958078,
805.680267067833,805.763722862751,805.847267355481,805.930856438422,806.014579705979,
806.095259421875,806.178998133721,806.262633645088,806.346186088487,806.429675524338,
806.513129474951,806.596565968798,806.680003078553,806.76345887347,806.8470033662,
806.930592449141,807.014315716699,807.094995432596,807.1385058474),
 .UNSPECIFIED.);
#560=B_SPLINE_CURVE_WITH_KNOTS('',3,(#75565,#75566,#75567,#75568,#75569,
#75570,#75571,#75572,#75573,#75574,#75575,#75576,#75577),.UNSPECIFIED.,
 .F.,.F.,(4,3,3,3,4),(800.85447021826,800.938063052894,801.021788343522,
801.096579368275,801.106126665376),.UNSPECIFIED.);
#561=B_SPLINE_CURVE_WITH_KNOTS('',3,(#75579,#75580,#75581,#75582,#75583,
#75584,#75585,#75586,#75587,#75588),.UNSPECIFIED.,.F.,.F.,(4,3,3,4),(800.855023018815,
800.937968112572,801.022047388976,801.10612666538),.UNSPECIFIED.);
#562=B_SPLINE_CURVE_WITH_KNOTS('',3,(#75589,#75590,#75591,#75592,#75593,
#75594,#75595,#75596,#75597,#75598,#75599,#75600,#75601,#75602,#75603,#75604,
#75605,#75606,#75607,#75608,#75609,#75610,#75611,#75612,#75613,#75614,#75615,
#75616,#75617,#75618,#75619,#75620,#75621,#75622,#75623,#75624,#75625,#75626,
#75627,#75628,#75629,#75630,#75631,#75632,#75633,#75634,#75635,#75636,#75637,
#75638,#75639,#75640,#75641,#75642,#75643,#75644,#75645,#75646,#75647,#75648,
#75649,#75650,#75651,#75652,#75653,#75654,#75655,#75656,#75657,#75658,#75659,
#75660,#75661,#75662,#75663,#75664,#75665,#75666,#75667,#75668,#75669,#75670,
#75671,#75672,#75673,#75674,#75675,#75676,#75677,#75678,#75679,#75680,#75681,
#75682,#75683,#75684,#75685,#75686,#75687,#75688,#75689,#75690,#75691,#75692,
#75693,#75694,#75695,#75696,#75697,#75698,#75699,#75700,#75701,#75702,#75703,
#75704,#75705,#75706,#75707,#75708,#75709,#75710,#75711,#75712,#75713,#75714,
#75715,#75716,#75717,#75718,#75719,#75720,#75721,#75722,#75723,#75724,#75725,
#75726,#75727,#75728,#75729,#75730,#75731,#75732,#75733,#75734,#75735,#75736,
#75737,#75738,#75739,#75740,#75741,#75742,#75743,#75744,#75745,#75746,#75747,
#75748,#75749,#75750,#75751,#75752,#75753,#75754,#75755,#75756,#75757,#75758,
#75759,#75760,#75761,#75762,#75763,#75764,#75765,#75766,#75767,#75768,#75769,
#75770,#75771,#75772,#75773,#75774,#75775,#75776,#75777,#75778,#75779,#75780,
#75781,#75782,#75783,#75784,#75785,#75786,#75787,#75788,#75789,#75790,#75791,
#75792,#75793,#75794,#75795,#75796,#75797,#75798,#75799,#75800,#75801,#75802,
#75803,#75804,#75805),.UNSPECIFIED.,.F.,.F.,(4,3,3,3,3,3,3,3,3,3,3,3,3,
3,3,3,3,3,3,3,3,3,3,3,3,3,3,3,3,3,3,3,3,3,3,3,3,3,3,3,3,3,3,3,3,3,3,3,3,
3,3,3,3,3,3,3,3,3,3,3,3,3,3,3,3,3,3,3,3,3,3,3,4),(801.106126665528,801.206596975234,
801.308383579925,801.406869987991,801.490608699837,801.574244211204,801.657796654603,
801.741286090454,801.824740041068,801.908176534914,801.99161364467,802.075069439587,
802.158613932317,802.242203015258,802.325926282816,802.406605998711,802.490344710557,
802.573980221925,802.657532665323,802.741022101174,802.824476051788,802.907912545634,
802.99134965539,803.074805450308,803.158349943037,803.241939025978,803.325662293536,
803.406342009432,803.490080721278,803.573716232646,803.657268676044,803.740758111895,
803.824212062509,803.907648556355,803.991085666111,804.074541461028,804.158085953758,
804.241675036699,804.325398304257,804.406078020152,804.489816731998,804.573452243366,
804.657004686764,804.740494122615,804.823948073229,804.907384567075,804.99082167683,
805.074277471748,805.157821964478,805.241411047419,805.325134314976,805.405814030872,
805.489552742718,805.573188254085,805.656740697484,805.740230133335,805.823684083949,
805.907120577795,805.99055768755,806.074013482468,806.157557975198,806.241147058139,
806.324870325696,806.405550041592,806.489073461701,806.572464736515,806.655779744683,
806.739036867379,806.822254441502,806.905468087397,806.988676858978,807.071932381418,
807.137598113524),.UNSPECIFIED.);
#563=B_SPLINE_CURVE_WITH_KNOTS('',3,(#75811,#75812,#75813,#75814,#75815,
#75816,#75817,#75818,#75819,#75820,#75821,#75822,#75823,#75824,#75825,#75826,
#75827,#75828,#75829,#75830,#75831,#75832,#75833,#75834,#75835,#75836,#75837,
#75838,#75839,#75840,#75841,#75842,#75843,#75844,#75845,#75846,#75847,#75848,
#75849,#75850,#75851,#75852,#75853,#75854,#75855,#75856,#75857,#75858,#75859,
#75860,#75861,#75862,#75863,#75864,#75865,#75866,#75867,#75868,#75869,#75870,
#75871,#75872,#75873,#75874,#75875,#75876,#75877,#75878,#75879,#75880,#75881,
#75882,#75883,#75884,#75885,#75886,#75887,#75888,#75889,#75890,#75891,#75892,
#75893,#75894,#75895,#75896,#75897,#75898,#75899,#75900,#75901,#75902,#75903,
#75904,#75905,#75906,#75907,#75908,#75909,#75910,#75911,#75912,#75913,#75914,
#75915,#75916,#75917,#75918,#75919,#75920,#75921,#75922,#75923,#75924,#75925,
#75926,#75927,#75928,#75929,#75930,#75931,#75932,#75933,#75934,#75935,#75936,
#75937,#75938,#75939,#75940,#75941,#75942,#75943,#75944,#75945,#75946,#75947,
#75948,#75949,#75950,#75951,#75952,#75953,#75954,#75955,#75956,#75957,#75958,
#75959,#75960,#75961,#75962,#75963,#75964,#75965,#75966,#75967,#75968,#75969,
#75970,#75971,#75972,#75973,#75974,#75975,#75976,#75977,#75978,#75979,#75980,
#75981,#75982,#75983,#75984,#75985,#75986,#75987,#75988,#75989,#75990,#75991,
#75992,#75993,#75994,#75995,#75996,#75997,#75998,#75999,#76000,#76001,#76002,
#76003,#76004,#76005,#76006,#76007,#76008,#76009,#76010,#76011,#76012,#76013,
#76014,#76015,#76016,#76017,#76018,#76019,#76020,#76021,#76022,#76023,#76024,
#76025,#76026,#76027,#76028,#76029,#76030),.UNSPECIFIED.,.F.,.F.,(4,3,3,
3,3,3,3,3,3,3,3,3,3,3,3,3,3,3,3,3,3,3,3,3,3,3,3,3,3,3,3,3,3,3,3,3,3,3,3,
3,3,3,3,3,3,3,3,3,3,3,3,3,3,3,3,3,3,3,3,3,3,3,3,3,3,3,3,3,3,3,3,3,3,4),
(807.389311972555,807.472225275472,807.555112008788,807.637987902611,807.720871498604,
807.803781340485,807.886783805871,807.969838484841,808.053017602792,808.094731443316,
808.178470155162,808.26210566653,808.345658109928,808.429147545779,808.512601496393,
808.596037990239,808.679475099994,808.762930894912,808.846475387642,808.930064470583,
809.01378773814,809.094467454036,809.178206165882,809.261841677249,809.345394120648,
809.428883556499,809.512337507112,809.595774000959,809.679211110714,809.762666905631,
809.846211398361,809.929800481302,810.013523748859,810.094203464756,810.177942176602,
810.26157768797,810.345130131368,810.428619567219,810.512073517833,810.595510011679,
810.678947121434,810.762402916351,810.845947409081,810.929536492022,811.01325975958,
811.093939475476,811.177678187322,811.261313698689,811.344866142088,811.428355577939,
811.511809528552,811.595246022398,811.678683132154,811.762138927072,811.845683419801,
811.929272502743,812.0129957703,812.093675486196,812.177414198042,812.261049709409,
812.344602152808,812.428091588659,812.511545539273,812.594982033119,812.678419142875,
812.761874937793,812.845419430522,812.929008513464,813.012731781021,813.093411496916,
813.178887063871,813.264255755827,813.34950153073,813.421961035509),
 .UNSPECIFIED.);
#564=B_SPLINE_CURVE_WITH_KNOTS('',3,(#76031,#76032,#76033,#76034,#76035,
#76036,#76037,#76038,#76039,#76040),.UNSPECIFIED.,.F.,.F.,(4,3,3,4),(807.1385058474,
807.241041547493,807.342243436622,807.389311972417),.UNSPECIFIED.);
#565=B_SPLINE_CURVE_WITH_KNOTS('',3,(#76042,#76043,#76044,#76045,#76046,
#76047,#76048,#76049,#76050,#76051),.UNSPECIFIED.,.F.,.F.,(4,3,3,4),(807.137598113524,
807.220952318012,807.30513214521,807.389311972408),.UNSPECIFIED.);
#566=B_SPLINE_CURVE_WITH_KNOTS('',3,(#76052,#76053,#76054,#76055,#76056,
#76057,#76058,#76059,#76060,#76061,#76062,#76063,#76064,#76065,#76066,#76067,
#76068,#76069,#76070,#76071,#76072,#76073,#76074,#76075,#76076,#76077,#76078,
#76079,#76080,#76081,#76082,#76083,#76084,#76085,#76086,#76087,#76088,#76089,
#76090,#76091,#76092,#76093,#76094,#76095,#76096,#76097,#76098,#76099,#76100,
#76101,#76102,#76103,#76104,#76105,#76106,#76107,#76108,#76109,#76110,#76111,
#76112,#76113,#76114,#76115,#76116,#76117,#76118,#76119,#76120,#76121,#76122,
#76123,#76124,#76125,#76126,#76127,#76128,#76129,#76130,#76131,#76132,#76133,
#76134,#76135,#76136,#76137,#76138,#76139,#76140,#76141,#76142,#76143,#76144,
#76145,#76146,#76147,#76148,#76149,#76150,#76151,#76152,#76153,#76154,#76155,
#76156,#76157,#76158,#76159,#76160,#76161,#76162,#76163,#76164,#76165,#76166,
#76167,#76168,#76169,#76170,#76171,#76172,#76173,#76174,#76175,#76176,#76177,
#76178,#76179,#76180,#76181,#76182,#76183,#76184,#76185,#76186,#76187,#76188,
#76189,#76190,#76191,#76192,#76193,#76194,#76195,#76196,#76197,#76198,#76199,
#76200,#76201,#76202,#76203,#76204,#76205,#76206,#76207,#76208,#76209,#76210,
#76211,#76212,#76213,#76214,#76215,#76216,#76217,#76218,#76219,#76220,#76221,
#76222,#76223,#76224,#76225,#76226,#76227,#76228,#76229,#76230,#76231,#76232,
#76233,#76234,#76235,#76236,#76237,#76238,#76239,#76240,#76241,#76242,#76243,
#76244,#76245,#76246,#76247,#76248,#76249,#76250,#76251,#76252,#76253,#76254,
#76255,#76256,#76257,#76258,#76259,#76260,#76261,#76262,#76263,#76264,#76265,
#76266,#76267,#76268,#76269,#76270,#76271,#76272,#76273,#76274),
 .UNSPECIFIED.,.F.,.F.,(4,3,3,3,3,3,3,3,3,3,3,3,3,3,3,3,3,3,3,3,3,3,3,3,
3,3,3,3,3,3,3,3,3,3,3,3,3,3,3,3,3,3,3,3,3,3,3,3,3,3,3,3,3,3,3,3,3,3,3,3,
3,3,3,3,3,3,3,3,3,3,3,3,3,3,4),(807.389311972559,807.405286052312,807.489024764158,
807.572660275525,807.656212718924,807.739702154775,807.823156105389,807.906592599235,
807.99002970899,808.073485503908,808.157029996638,808.240619079579,808.324342347136,
808.405022063032,808.488760774878,808.572396286245,808.655948729644,808.739438165495,
808.822892116108,808.906328609955,808.98976571971,809.073221514628,809.156766007357,
809.240355090298,809.324078357856,809.404758073752,809.488496785598,809.572132296965,
809.655684740364,809.739174176215,809.822628126829,809.906064620675,809.989501730431,
810.072957525348,810.156502018078,810.240091101019,810.323814368577,810.404494084472,
810.488232796318,810.571868307686,810.655420751084,810.738910186935,810.822364137549,
810.905800631395,810.989237741151,811.072693536069,811.156238028798,811.239827111739,
811.323550379297,811.404230095193,811.487968807039,811.571604318407,811.655156761805,
811.738646197656,811.82210014827,811.905536642116,811.988973751872,812.07242954679,
812.155974039519,812.23956312246,812.323286390018,812.403966105913,812.487704817759,
812.571340329126,812.654892772525,812.738382208375,812.821836158989,812.905272652835,
812.988709762591,813.072165557508,813.155710050238,813.239299133179,813.323022400736,
813.403702116633,813.421541691872),.UNSPECIFIED.);
#567=B_SPLINE_CURVE_WITH_KNOTS('',3,(#76280,#76281,#76282,#76283,#76284,
#76285,#76286,#76287,#76288,#76289,#76290,#76291,#76292,#76293,#76294,#76295,
#76296,#76297,#76298,#76299,#76300,#76301,#76302,#76303,#76304,#76305,#76306,
#76307,#76308,#76309,#76310,#76311,#76312,#76313,#76314,#76315,#76316,#76317,
#76318,#76319,#76320,#76321,#76322,#76323,#76324,#76325,#76326,#76327,#76328,
#76329,#76330,#76331,#76332,#76333,#76334,#76335,#76336,#76337,#76338,#76339,
#76340,#76341,#76342,#76343,#76344,#76345,#76346,#76347,#76348,#76349,#76350,
#76351,#76352,#76353,#76354,#76355,#76356,#76357,#76358,#76359,#76360,#76361,
#76362,#76363,#76364,#76365,#76366,#76367,#76368,#76369,#76370,#76371,#76372,
#76373,#76374,#76375,#76376,#76377,#76378,#76379,#76380,#76381,#76382,#76383,
#76384,#76385,#76386,#76387,#76388,#76389,#76390,#76391,#76392,#76393,#76394,
#76395,#76396,#76397,#76398,#76399,#76400,#76401,#76402,#76403,#76404,#76405,
#76406,#76407,#76408,#76409,#76410,#76411,#76412,#76413,#76414,#76415,#76416,
#76417,#76418,#76419,#76420,#76421,#76422,#76423,#76424,#76425,#76426,#76427,
#76428,#76429,#76430,#76431,#76432,#76433,#76434,#76435,#76436,#76437,#76438,
#76439,#76440,#76441,#76442,#76443,#76444,#76445,#76446,#76447,#76448,#76449,
#76450,#76451,#76452,#76453,#76454,#76455,#76456,#76457,#76458,#76459,#76460,
#76461,#76462,#76463,#76464,#76465,#76466,#76467,#76468,#76469,#76470,#76471,
#76472,#76473,#76474,#76475,#76476,#76477,#76478,#76479,#76480,#76481,#76482,
#76483,#76484,#76485,#76486,#76487,#76488,#76489,#76490,#76491,#76492,#76493,
#76494,#76495,#76496,#76497,#76498,#76499),.UNSPECIFIED.,.F.,.F.,(4,3,3,
3,3,3,3,3,3,3,3,3,3,3,3,3,3,3,3,3,3,3,3,3,3,3,3,3,3,3,3,3,3,3,3,3,3,3,3,
3,3,3,3,3,3,3,3,3,3,3,3,3,3,3,3,3,3,3,3,3,3,3,3,3,3,3,3,3,3,3,3,3,3,4),
(813.672497279888,813.763414053234,813.854745397129,813.946288265523,814.038142143338,
814.093147507636,814.176886219482,814.26052173085,814.344074174249,814.427563610101,
814.511017560715,814.594454054562,814.677891164318,814.761346959237,814.844891451967,
814.928480534908,815.012203802467,815.092883518357,815.176622230203,815.26025774157,
815.343810184968,815.427299620819,815.510753571433,815.594190065279,815.677627175034,
815.761082969952,815.844627462681,815.928216545622,816.011939813179,816.092619529077,
816.176358240923,816.25999375229,816.343546195689,816.42703563154,816.510489582153,
816.593926076,816.677363185755,816.760818980673,816.844363473402,816.927952556343,
817.011675823901,817.092355539797,817.176094251643,817.259729763011,817.343282206409,
817.42677164226,817.510225592874,817.59366208672,817.677099196476,817.760554991394,
817.844099484123,817.927688567064,818.011411834622,818.092091550517,818.175830262363,
818.25946577373,818.343018217128,818.426507652979,818.509961603593,818.593398097439,
818.676835207194,818.760291002111,818.843835494841,818.927424577782,819.011147845339,
819.091827561237,819.174342520055,819.256762659536,819.339107167316,819.421395158965,
819.503652354638,819.58589159078,819.668149206529,819.703896483842),
 .UNSPECIFIED.);
#568=B_SPLINE_CURVE_WITH_KNOTS('',3,(#76500,#76501,#76502,#76503,#76504,
#76505,#76506,#76507,#76508,#76509),.UNSPECIFIED.,.F.,.F.,(4,3,3,4),(813.421961035509,
813.507063854652,813.592111218928,813.672497279735),.UNSPECIFIED.);
#569=B_SPLINE_CURVE_WITH_KNOTS('',3,(#76511,#76512,#76513,#76514,#76515,
#76516,#76517,#76518,#76519,#76520),.UNSPECIFIED.,.F.,.F.,(4,3,3,4),(813.421541691872,
813.527897418378,813.632413728413,813.672497279565),.UNSPECIFIED.);
#570=B_SPLINE_CURVE_WITH_KNOTS('',3,(#76521,#76522,#76523,#76524,#76525,
#76526,#76527,#76528,#76529,#76530,#76531,#76532,#76533,#76534,#76535,#76536,
#76537,#76538,#76539,#76540,#76541,#76542,#76543,#76544,#76545,#76546,#76547,
#76548,#76549,#76550,#76551,#76552,#76553,#76554,#76555,#76556,#76557,#76558,
#76559,#76560,#76561,#76562,#76563,#76564,#76565,#76566,#76567,#76568,#76569,
#76570,#76571,#76572,#76573,#76574,#76575,#76576,#76577,#76578,#76579,#76580,
#76581,#76582,#76583,#76584,#76585,#76586,#76587,#76588,#76589,#76590,#76591,
#76592,#76593,#76594,#76595,#76596,#76597,#76598,#76599,#76600,#76601,#76602,
#76603,#76604,#76605,#76606,#76607,#76608,#76609,#76610,#76611,#76612,#76613,
#76614,#76615,#76616,#76617,#76618,#76619,#76620,#76621,#76622,#76623,#76624,
#76625,#76626,#76627,#76628,#76629,#76630,#76631,#76632,#76633,#76634,#76635,
#76636,#76637,#76638,#76639,#76640,#76641,#76642,#76643,#76644,#76645,#76646,
#76647,#76648,#76649,#76650,#76651,#76652,#76653,#76654,#76655,#76656,#76657,
#76658,#76659,#76660,#76661,#76662,#76663,#76664,#76665,#76666,#76667,#76668,
#76669,#76670,#76671,#76672,#76673,#76674,#76675,#76676,#76677,#76678,#76679,
#76680,#76681,#76682,#76683,#76684,#76685,#76686,#76687,#76688,#76689,#76690,
#76691,#76692,#76693,#76694,#76695,#76696,#76697,#76698,#76699,#76700,#76701,
#76702,#76703,#76704,#76705,#76706,#76707,#76708,#76709,#76710,#76711,#76712,
#76713,#76714,#76715,#76716,#76717,#76718,#76719,#76720,#76721,#76722,#76723,
#76724,#76725,#76726,#76727,#76728,#76729,#76730,#76731,#76732,#76733,#76734,
#76735,#76736,#76737,#76738,#76739,#76740),.UNSPECIFIED.,.F.,.F.,(4,3,3,
3,3,3,3,3,3,3,3,3,3,3,3,3,3,3,3,3,3,3,3,3,3,3,3,3,3,3,3,3,3,3,3,3,3,3,3,
3,3,3,3,3,3,3,3,3,3,3,3,3,3,3,3,3,3,3,3,3,3,3,3,3,3,3,3,3,3,3,3,3,3,4),
(813.672497279739,813.75518641853,813.837835534489,813.920464908825,814.00309328813,
814.085739415308,814.168472347732,814.251250272538,814.334158514269,814.403438127353,
814.487176839199,814.570812350566,814.654364793965,814.737854229817,814.82130818043,
814.904744674277,814.988181784032,815.07163757895,815.15518207168,815.238771154621,
815.322494422179,815.403174138073,815.486912849919,815.570548361287,815.654100804685,
815.737590240536,815.82104419115,815.904480684996,815.987917794751,816.071373589669,
816.154918082398,816.238507165339,816.322230432897,816.402910148793,816.486648860639,
816.570284372006,816.653836815404,816.737326251255,816.820780201869,816.904216695715,
816.98765380547,817.071109600387,817.154654093117,817.238243176058,817.321966443615,
817.402646159513,817.486384871359,817.570020382727,817.653572826126,817.737062261977,
817.820516212591,817.903952706438,817.987389816194,818.070845611112,818.154390103841,
818.237979186783,818.321702454341,818.402382170234,818.48612088208,818.569756393448,
818.653308836846,818.736798272697,818.820252223311,818.903688717158,818.987125826914,
819.070581621832,819.154126114561,819.237715197503,819.321438465061,819.402118180954,
819.488312354914,819.574393064568,819.660340071141,819.705233576188),
 .UNSPECIFIED.);
#571=B_SPLINE_CURVE_WITH_KNOTS('',3,(#76746,#76747,#76748,#76749,#76750,
#76751,#76752,#76753,#76754,#76755,#76756,#76757,#76758,#76759,#76760,#76761,
#76762,#76763,#76764,#76765,#76766,#76767,#76768,#76769,#76770,#76771,#76772,
#76773,#76774,#76775,#76776,#76777,#76778,#76779,#76780,#76781,#76782,#76783,
#76784,#76785,#76786,#76787,#76788,#76789,#76790,#76791,#76792,#76793,#76794,
#76795,#76796,#76797,#76798,#76799,#76800,#76801,#76802,#76803,#76804,#76805,
#76806,#76807,#76808,#76809,#76810,#76811,#76812,#76813,#76814,#76815,#76816,
#76817,#76818,#76819,#76820,#76821,#76822,#76823,#76824,#76825,#76826,#76827,
#76828,#76829,#76830,#76831,#76832,#76833,#76834,#76835,#76836,#76837,#76838,
#76839,#76840,#76841,#76842,#76843,#76844,#76845,#76846,#76847,#76848,#76849,
#76850,#76851,#76852,#76853,#76854,#76855,#76856,#76857,#76858,#76859,#76860,
#76861,#76862,#76863,#76864,#76865,#76866,#76867,#76868,#76869,#76870,#76871,
#76872,#76873,#76874,#76875,#76876,#76877,#76878,#76879,#76880,#76881,#76882,
#76883,#76884,#76885,#76886,#76887,#76888,#76889,#76890,#76891,#76892,#76893,
#76894,#76895,#76896,#76897,#76898,#76899,#76900,#76901,#76902,#76903,#76904,
#76905,#76906,#76907,#76908,#76909,#76910,#76911,#76912,#76913,#76914,#76915,
#76916,#76917,#76918,#76919,#76920,#76921,#76922,#76923,#76924,#76925,#76926,
#76927,#76928,#76929,#76930,#76931,#76932,#76933,#76934,#76935,#76936,#76937,
#76938,#76939,#76940,#76941,#76942,#76943,#76944,#76945,#76946,#76947,#76948,
#76949,#76950,#76951,#76952,#76953,#76954,#76955,#76956,#76957,#76958,#76959,
#76960,#76961,#76962),.UNSPECIFIED.,.F.,.F.,(4,3,3,3,3,3,3,3,3,3,3,3,3,
3,3,3,3,3,3,3,3,3,3,3,3,3,3,3,3,3,3,3,3,3,3,3,3,3,3,3,3,3,3,3,3,3,3,3,3,
3,3,3,3,3,3,3,3,3,3,3,3,3,3,3,3,3,3,3,3,3,3,3,4),(819.955682586915,820.091563571957,
820.175302283805,820.258937795175,820.342490238576,820.425979674429,820.509433625045,
820.592870118894,820.676307228652,820.759763023573,820.843307516305,820.926896599248,
821.010619866809,821.091299582677,821.175038294523,821.25867380589,821.342226249288,
821.425715685139,821.509169635753,821.592606129598,821.676043239354,821.759499034271,
821.843043527001,821.926632609941,822.010355877499,822.091035593398,822.174774305244,
822.258409816611,822.341962260009,822.42545169586,822.508905646474,822.59234214032,
822.675779250075,822.759235044992,822.842779537722,822.926368620662,823.01009188822,
823.090771604118,823.174510315964,823.258145827332,823.34169827073,823.425187706581,
823.508641657195,823.592078151041,823.675515260797,823.758971055714,823.842515548444,
823.926104631385,824.009827898943,824.090507614838,824.174246326684,824.257881838051,
824.34143428145,824.424923717301,824.508377667914,824.591814161761,824.675251271516,
824.758707066434,824.842251559163,824.925840642104,825.009563909662,825.090243625558,
825.173988319906,825.25762845994,825.341184183953,825.424671159286,825.508120674546,
825.591550818252,825.67497966208,825.758462116136,825.8419721472,825.925578110456,
825.987345293289),.UNSPECIFIED.);
#572=B_SPLINE_CURVE_WITH_KNOTS('',3,(#76963,#76964,#76965,#76966,#76967,
#76968,#76969,#76970,#76971,#76972),.UNSPECIFIED.,.F.,.F.,(4,3,3,4),(819.703896483842,
819.786220350054,819.870951468422,819.95568258679),.UNSPECIFIED.);
#573=B_SPLINE_CURVE_WITH_KNOTS('',3,(#76974,#76975,#76976,#76977,#76978,
#76979,#76980,#76981,#76982,#76983),.UNSPECIFIED.,.F.,.F.,(4,3,3,4),(819.705233576188,
819.79103108917,819.876744696265,819.955682586918),.UNSPECIFIED.);
#574=B_SPLINE_CURVE_WITH_KNOTS('',3,(#76984,#76985,#76986,#76987,#76988,
#76989,#76990,#76991,#76992,#76993,#76994,#76995,#76996,#76997,#76998,#76999,
#77000,#77001,#77002,#77003,#77004,#77005,#77006,#77007,#77008,#77009,#77010,
#77011,#77012,#77013,#77014,#77015,#77016,#77017,#77018,#77019,#77020,#77021,
#77022,#77023,#77024,#77025,#77026,#77027,#77028,#77029,#77030,#77031,#77032,
#77033,#77034,#77035,#77036,#77037,#77038,#77039,#77040,#77041,#77042,#77043,
#77044,#77045,#77046,#77047,#77048,#77049,#77050,#77051,#77052,#77053,#77054,
#77055,#77056,#77057,#77058,#77059,#77060,#77061,#77062,#77063,#77064,#77065,
#77066,#77067,#77068,#77069,#77070,#77071,#77072,#77073,#77074,#77075,#77076,
#77077,#77078,#77079,#77080,#77081,#77082,#77083,#77084,#77085,#77086,#77087,
#77088,#77089,#77090,#77091,#77092,#77093,#77094,#77095,#77096,#77097,#77098,
#77099,#77100,#77101,#77102,#77103,#77104,#77105,#77106,#77107,#77108,#77109,
#77110,#77111,#77112,#77113,#77114,#77115,#77116,#77117,#77118,#77119,#77120,
#77121,#77122,#77123,#77124,#77125,#77126,#77127,#77128,#77129,#77130,#77131,
#77132,#77133,#77134,#77135,#77136,#77137,#77138,#77139,#77140,#77141,#77142,
#77143,#77144,#77145,#77146,#77147,#77148,#77149,#77150,#77151,#77152,#77153,
#77154,#77155,#77156,#77157,#77158,#77159,#77160,#77161,#77162,#77163,#77164,
#77165,#77166,#77167,#77168,#77169,#77170,#77171,#77172,#77173,#77174,#77175,
#77176,#77177,#77178,#77179,#77180,#77181,#77182,#77183,#77184,#77185,#77186,
#77187,#77188,#77189,#77190,#77191,#77192,#77193,#77194,#77195,#77196,#77197,
#77198,#77199,#77200),.UNSPECIFIED.,.F.,.F.,(4,3,3,3,3,3,3,3,3,3,3,3,3,
3,3,3,3,3,3,3,3,3,3,3,3,3,3,3,3,3,3,3,3,3,3,3,3,3,3,3,3,3,3,3,3,3,3,3,3,
3,3,3,3,3,3,3,3,3,3,3,3,3,3,3,3,3,3,3,3,3,3,3,4),(819.955682587033,820.045313946329,
820.135281214152,820.225415774172,820.315836079296,820.401854191674,820.485592903519,
820.569228414886,820.652780858284,820.736270294135,820.819724244748,820.903160738594,
820.986597848349,821.070053643266,821.153598135995,821.237187218935,821.320910486492,
821.401590202394,821.48532891424,821.568964425608,821.652516869006,821.736006304857,
821.819460255471,821.902896749317,821.986333859072,822.06978965399,822.15333414672,
822.236923229661,822.320646497218,822.401326213114,822.48506492496,822.568700436328,
822.652252879726,822.735742315577,822.819196266191,822.902632760037,822.986069869792,
823.06952566471,823.15307015744,823.236659240381,823.320382507938,823.401062223834,
823.48480093568,823.568436447047,823.651988890446,823.735478326297,823.818932276911,
823.902368770757,823.985805880512,824.06926167543,824.15280616816,824.236395251101,
824.320118518658,824.400798234554,824.4845369464,824.568172457768,824.651724901166,
824.735214337017,824.818668287631,824.902104781477,824.985541891233,825.068997686151,
825.15254217888,825.236131261821,825.319854529379,825.400534245274,825.48300659384,
825.565383758059,825.647684956802,825.732550045853,825.814760182079,825.900952747541,
825.987145313003),.UNSPECIFIED.);
#575=B_SPLINE_CURVE_WITH_KNOTS('',3,(#77206,#77207,#77208,#77209,#77210,
#77211,#77212,#77213,#77214,#77215,#77216,#77217,#77218,#77219,#77220,#77221,
#77222,#77223,#77224,#77225,#77226,#77227,#77228,#77229,#77230,#77231,#77232,
#77233,#77234,#77235,#77236,#77237,#77238,#77239,#77240,#77241,#77242,#77243,
#77244,#77245,#77246,#77247,#77248,#77249,#77250,#77251,#77252,#77253,#77254,
#77255,#77256,#77257,#77258,#77259,#77260,#77261,#77262,#77263,#77264,#77265,
#77266,#77267,#77268,#77269,#77270,#77271,#77272,#77273,#77274,#77275,#77276,
#77277,#77278,#77279,#77280,#77281,#77282,#77283,#77284,#77285,#77286,#77287,
#77288,#77289,#77290,#77291,#77292,#77293,#77294,#77295,#77296,#77297,#77298,
#77299,#77300,#77301,#77302,#77303,#77304,#77305,#77306,#77307,#77308,#77309,
#77310,#77311,#77312,#77313,#77314,#77315,#77316,#77317,#77318,#77319,#77320,
#77321,#77322,#77323,#77324,#77325,#77326,#77327,#77328,#77329,#77330,#77331,
#77332,#77333,#77334,#77335,#77336,#77337,#77338,#77339,#77340,#77341,#77342,
#77343,#77344,#77345,#77346,#77347,#77348,#77349,#77350,#77351,#77352,#77353,
#77354,#77355,#77356,#77357,#77358,#77359,#77360,#77361,#77362,#77363,#77364,
#77365,#77366,#77367,#77368,#77369,#77370,#77371,#77372,#77373,#77374,#77375,
#77376,#77377,#77378,#77379,#77380,#77381,#77382,#77383,#77384,#77385,#77386,
#77387,#77388,#77389,#77390,#77391,#77392,#77393,#77394,#77395,#77396,#77397,
#77398,#77399,#77400,#77401,#77402,#77403,#77404,#77405,#77406,#77407,#77408,
#77409,#77410,#77411,#77412,#77413,#77414,#77415,#77416,#77417,#77418,#77419,
#77420,#77421,#77422,#77423,#77424,#77425),.UNSPECIFIED.,.F.,.F.,(4,3,3,
3,3,3,3,3,3,3,3,3,3,3,3,3,3,3,3,3,3,3,3,3,3,3,3,3,3,3,3,3,3,3,3,3,3,3,3,
3,3,3,3,3,3,3,3,3,3,3,3,3,3,3,3,3,3,3,3,3,3,3,3,3,3,3,3,3,3,3,3,3,3,4),
(826.238867894208,826.32127581105,826.403601341344,826.489365629551,826.57159656205,
826.653814332816,826.736037965977,826.818286488398,826.900622949684,826.983011397038,
827.065515324656,827.089715646998,827.173454358844,827.257089870211,827.34064231361,
827.424131749461,827.507585700075,827.591022193921,827.674459303676,827.757915098594,
827.841459591324,827.925048674265,828.008771941822,828.089451657718,828.173190369564,
828.256825880931,828.340378324329,828.42386776018,828.507321710794,828.59075820464,
828.674195314395,828.757651109313,828.841195602043,828.924784684984,829.008507952541,
829.089187668438,829.172926380284,829.256561891651,829.34011433505,829.423603770901,
829.507057721515,829.590494215361,829.673931325117,829.757387120035,829.840931612764,
829.924520695706,830.008243963263,830.088923679158,830.172662391004,830.256297902372,
830.33985034577,830.423339781621,830.506793732235,830.590230226081,830.673667335836,
830.757123130754,830.840667623484,830.924256706425,831.007979973982,831.088659689879,
831.172398401725,831.256033913093,831.339586356492,831.423075792343,831.506529742956,
831.589966236803,831.673403346558,831.756859141476,831.840403634205,831.923992717146,
832.007715984704,832.088395700599,832.18006641272,832.271737124841),
 .UNSPECIFIED.);
#576=B_SPLINE_CURVE_WITH_KNOTS('',3,(#77426,#77427,#77428,#77429,#77430,
#77431,#77432,#77433,#77434,#77435),.UNSPECIFIED.,.F.,.F.,(4,3,3,4),(825.987345293289,
826.071094722339,826.089979636278,826.238867894094),.UNSPECIFIED.);
#577=B_SPLINE_CURVE_WITH_KNOTS('',3,(#77437,#77438,#77439,#77440,#77441,
#77442,#77443,#77444,#77445,#77446),.UNSPECIFIED.,.F.,.F.,(4,3,3,4),(825.987145313003,
826.069408893835,826.154138393866,826.238867893896),.UNSPECIFIED.);
#578=B_SPLINE_CURVE_WITH_KNOTS('',3,(#77447,#77448,#77449,#77450,#77451,
#77452,#77453,#77454,#77455,#77456,#77457,#77458,#77459,#77460,#77461,#77462,
#77463,#77464,#77465,#77466,#77467,#77468,#77469,#77470,#77471,#77472,#77473,
#77474,#77475,#77476,#77477,#77478,#77479,#77480,#77481,#77482,#77483,#77484,
#77485,#77486,#77487,#77488,#77489,#77490,#77491,#77492,#77493,#77494,#77495,
#77496,#77497,#77498,#77499,#77500,#77501,#77502,#77503,#77504,#77505,#77506,
#77507,#77508,#77509,#77510,#77511,#77512,#77513,#77514,#77515,#77516,#77517,
#77518,#77519,#77520,#77521,#77522,#77523,#77524,#77525,#77526,#77527,#77528,
#77529,#77530,#77531,#77532,#77533,#77534,#77535,#77536,#77537,#77538,#77539,
#77540,#77541,#77542,#77543,#77544,#77545,#77546,#77547,#77548,#77549,#77550,
#77551,#77552,#77553,#77554,#77555,#77556,#77557,#77558,#77559,#77560,#77561,
#77562,#77563,#77564,#77565,#77566,#77567,#77568,#77569,#77570,#77571,#77572,
#77573,#77574,#77575,#77576,#77577,#77578,#77579,#77580,#77581,#77582,#77583,
#77584,#77585,#77586,#77587,#77588,#77589,#77590,#77591,#77592,#77593,#77594,
#77595,#77596,#77597,#77598,#77599,#77600,#77601,#77602,#77603,#77604,#77605,
#77606,#77607,#77608,#77609,#77610,#77611,#77612,#77613,#77614,#77615,#77616,
#77617,#77618,#77619,#77620,#77621,#77622,#77623,#77624,#77625,#77626,#77627,
#77628,#77629,#77630,#77631,#77632,#77633,#77634,#77635,#77636,#77637,#77638,
#77639,#77640,#77641,#77642,#77643,#77644,#77645,#77646,#77647,#77648,#77649,
#77650,#77651,#77652,#77653,#77654,#77655,#77656,#77657,#77658,#77659,#77660,
#77661,#77662,#77663,#77664,#77665,#77666),.UNSPECIFIED.,.F.,.F.,(4,3,3,
3,3,3,3,3,3,3,3,3,3,3,3,3,3,3,3,3,3,3,3,3,3,3,3,3,3,3,3,3,3,3,3,3,3,3,3,
3,3,3,3,3,3,3,3,3,3,3,3,3,3,3,3,3,3,3,3,3,3,3,3,3,3,3,3,3,3,3,3,3,3,4),
(826.238867894098,826.374623943545,826.400270255995,826.484008967841,826.567644479209,
826.651196922607,826.734686358458,826.818140309072,826.901576802918,826.985013912674,
827.068469707591,827.152014200321,827.235603283262,827.319326550819,827.400006266715,
827.483744978561,827.567380489928,827.650932933327,827.734422369178,827.817876319791,
827.901312813638,827.984749923393,828.068205718311,828.15175021104,828.235339293981,
828.319062561539,828.399742277435,828.483480989281,828.567116500649,828.650668944047,
828.734158379898,828.817612330512,828.901048824358,828.984485934113,829.067941729031,
829.151486221761,829.235075304702,829.318798572259,829.399478288155,829.483217000001,
829.566852511369,829.650404954767,829.733894390618,829.817348341232,829.900784835078,
829.984221944833,830.067677739751,830.151222232481,830.234811315422,830.318534582979,
830.399214298875,830.482953010721,830.566588522088,830.650140965487,830.733630401338,
830.817084351952,830.900520845798,830.983957955553,831.067413750471,831.150958243201,
831.234547326142,831.318270593699,831.398950309595,831.48269656839,831.566337935338,
831.649894550206,831.733381190797,831.816829893747,831.900258747863,831.983685824687,
832.067161049063,832.150663656295,832.23424954886,832.270468650374),
 .UNSPECIFIED.);
#579=B_SPLINE_CURVE_WITH_KNOTS('',3,(#77672,#77673,#77674,#77675,#77676,
#77677,#77678,#77679,#77680,#77681,#77682,#77683,#77684,#77685,#77686,#77687,
#77688,#77689,#77690,#77691,#77692,#77693,#77694,#77695,#77696,#77697,#77698,
#77699,#77700,#77701,#77702,#77703,#77704,#77705,#77706,#77707,#77708,#77709,
#77710,#77711,#77712,#77713,#77714,#77715,#77716,#77717,#77718,#77719,#77720,
#77721,#77722,#77723,#77724,#77725,#77726,#77727,#77728,#77729,#77730,#77731,
#77732,#77733,#77734,#77735,#77736,#77737,#77738,#77739,#77740,#77741,#77742,
#77743,#77744,#77745,#77746,#77747,#77748,#77749,#77750,#77751,#77752,#77753,
#77754,#77755,#77756,#77757,#77758,#77759,#77760,#77761,#77762,#77763,#77764,
#77765,#77766,#77767,#77768,#77769,#77770,#77771,#77772,#77773,#77774,#77775,
#77776,#77777,#77778,#77779,#77780,#77781,#77782,#77783,#77784,#77785,#77786,
#77787,#77788,#77789,#77790,#77791,#77792,#77793,#77794,#77795,#77796,#77797,
#77798,#77799,#77800,#77801,#77802,#77803,#77804,#77805,#77806,#77807,#77808,
#77809,#77810,#77811,#77812,#77813,#77814,#77815,#77816,#77817,#77818,#77819,
#77820,#77821,#77822,#77823,#77824,#77825,#77826,#77827,#77828,#77829,#77830,
#77831,#77832,#77833,#77834,#77835,#77836,#77837,#77838,#77839,#77840,#77841,
#77842,#77843,#77844,#77845,#77846,#77847,#77848,#77849,#77850,#77851,#77852,
#77853,#77854,#77855,#77856,#77857,#77858,#77859,#77860,#77861,#77862,#77863,
#77864,#77865,#77866,#77867,#77868,#77869,#77870,#77871,#77872,#77873,#77874,
#77875,#77876,#77877,#77878,#77879,#77880,#77881,#77882,#77883,#77884,#77885,
#77886,#77887,#77888,#77889,#77890,#77891),.UNSPECIFIED.,.F.,.F.,(4,3,3,
3,3,3,3,3,3,3,3,3,3,3,3,3,3,3,3,3,3,3,3,3,3,3,3,3,3,3,3,3,3,3,3,3,3,3,3,
3,3,3,3,3,3,3,3,3,3,3,3,3,3,3,3,3,3,3,3,3,3,3,3,3,3,3,3,3,3,3,3,3,3,4),
(832.522053201274,832.60741531893,832.692823871791,832.778293592255,832.863901389771,
832.949584597495,833.035425121847,833.088131711319,833.171870423165,833.255505934532,
833.339058377931,833.422547813782,833.506001764395,833.589438258241,833.672875367997,
833.756331162914,833.839875655643,833.923464738584,834.007188006142,834.087867722039,
834.171606433885,834.255241945253,834.338794388651,834.422283824502,834.505737775116,
834.589174268962,834.672611378717,834.756067173635,834.839611666365,834.923200749306,
835.006924016863,835.087603732759,835.171342444605,835.254977955973,835.338530399371,
835.422019835222,835.505473785836,835.588910279682,835.672347389438,835.755803184355,
835.839347677085,835.922936760026,836.006660027584,836.087339743479,836.171078455325,
836.254713966693,836.338266410091,836.421755845942,836.505209796556,836.588646290402,
836.672083400158,836.755539195075,836.839083687805,836.922672770746,837.006396038303,
837.087075754199,837.170814466045,837.254449977413,837.338002420811,837.421491856662,
837.504945807275,837.588382301122,837.671819410877,837.755275205794,837.838819698524,
837.922408781465,838.006132049023,838.08681176492,838.16985418221,838.252796291963,
838.335641931048,838.41843159313,838.501185242415,838.554033681403),
 .UNSPECIFIED.);
#580=B_SPLINE_CURVE_WITH_KNOTS('',3,(#77892,#77893,#77894,#77895,#77896,
#77897,#77898,#77899,#77900,#77901),.UNSPECIFIED.,.F.,.F.,(4,3,3,4),(832.271737124841,
832.362378164833,832.452703543163,832.522053201137),.UNSPECIFIED.);
#581=B_SPLINE_CURVE_WITH_KNOTS('',3,(#77903,#77904,#77905,#77906,#77907,
#77908,#77909,#77910,#77911,#77912),.UNSPECIFIED.,.F.,.F.,(4,3,3,4),(832.270468650374,
832.354205921054,832.398686320315,832.522053201278),.UNSPECIFIED.);
#582=B_SPLINE_CURVE_WITH_KNOTS('',3,(#77913,#77914,#77915,#77916,#77917,
#77918,#77919,#77920,#77921,#77922,#77923,#77924,#77925,#77926,#77927,#77928,
#77929,#77930,#77931,#77932,#77933,#77934,#77935,#77936,#77937,#77938,#77939,
#77940,#77941,#77942,#77943,#77944,#77945,#77946,#77947,#77948,#77949,#77950,
#77951,#77952,#77953,#77954,#77955,#77956,#77957,#77958,#77959,#77960,#77961,
#77962,#77963,#77964,#77965,#77966,#77967,#77968,#77969,#77970,#77971,#77972,
#77973,#77974,#77975,#77976,#77977,#77978,#77979,#77980,#77981,#77982,#77983,
#77984,#77985,#77986,#77987,#77988,#77989,#77990,#77991,#77992,#77993,#77994,
#77995,#77996,#77997,#77998,#77999,#78000,#78001,#78002,#78003,#78004,#78005,
#78006,#78007,#78008,#78009,#78010,#78011,#78012,#78013,#78014,#78015,#78016,
#78017,#78018,#78019,#78020,#78021,#78022,#78023,#78024,#78025,#78026,#78027,
#78028,#78029,#78030,#78031,#78032,#78033,#78034,#78035,#78036,#78037,#78038,
#78039,#78040,#78041,#78042,#78043,#78044,#78045,#78046,#78047,#78048,#78049,
#78050,#78051,#78052,#78053,#78054,#78055,#78056,#78057,#78058,#78059,#78060,
#78061,#78062,#78063,#78064,#78065,#78066,#78067,#78068,#78069,#78070,#78071,
#78072,#78073,#78074,#78075,#78076,#78077,#78078,#78079,#78080,#78081,#78082,
#78083,#78084,#78085,#78086,#78087,#78088,#78089,#78090,#78091,#78092,#78093,
#78094,#78095,#78096,#78097,#78098,#78099,#78100,#78101,#78102,#78103,#78104,
#78105,#78106,#78107,#78108,#78109,#78110,#78111,#78112,#78113,#78114,#78115,
#78116,#78117,#78118,#78119,#78120,#78121,#78122,#78123,#78124,#78125,#78126,
#78127,#78128,#78129,#78130,#78131,#78132),.UNSPECIFIED.,.F.,.F.,(4,3,3,
3,3,3,3,3,3,3,3,3,3,3,3,3,3,3,3,3,3,3,3,3,3,3,3,3,3,3,3,3,3,3,3,3,3,3,3,
3,3,3,3,3,3,3,3,3,3,3,3,3,3,3,3,3,3,3,3,3,3,3,3,3,3,3,3,3,3,3,3,3,3,4),
(832.52205320141,832.604557929264,832.686974591374,832.76932429753,832.851634173575,
832.933924851774,833.016215315304,833.098524544869,833.180918992729,833.26335983401,
833.345923922194,833.398422331035,833.482161042881,833.565796554248,833.649348997647,
833.732838433498,833.816292384111,833.899728877957,833.983165987713,834.06662178263,
834.15016627536,834.233755358301,834.317478625858,834.398158341756,834.481897053602,
834.56553256497,834.649085008368,834.732574444219,834.816028394833,834.899464888679,
834.982901998434,835.066357793352,835.149902286082,835.233491369023,835.317214636581,
835.397894352476,835.481633064322,835.565268575689,835.648821019088,835.732310454939,
835.815764405553,835.899200899399,835.982638009155,836.066093804072,836.149638296802,
836.233227379743,836.316950647301,836.397630363196,836.481369075042,836.565004586409,
836.648557029808,836.732046465659,836.815500416273,836.898936910119,836.982374019874,
837.065829814792,837.149374307522,837.232963390463,837.31668665802,837.397366373916,
837.481105085762,837.56474059713,837.648293040528,837.731782476379,837.815236426993,
837.898672920839,837.982110030595,838.065565825513,838.149110318242,838.232699401183,
838.316422668741,838.397102384636,838.489700245904,838.554883200175),
 .UNSPECIFIED.);
#583=B_SPLINE_CURVE_WITH_KNOTS('',3,(#78138,#78139,#78140,#78141,#78142,
#78143,#78144,#78145,#78146,#78147,#78148,#78149,#78150,#78151,#78152,#78153,
#78154,#78155,#78156,#78157,#78158,#78159,#78160,#78161,#78162,#78163,#78164,
#78165,#78166,#78167,#78168,#78169,#78170,#78171,#78172,#78173,#78174,#78175,
#78176,#78177,#78178,#78179,#78180,#78181,#78182,#78183,#78184,#78185,#78186,
#78187,#78188,#78189,#78190,#78191,#78192,#78193,#78194,#78195,#78196,#78197,
#78198,#78199,#78200,#78201,#78202,#78203,#78204,#78205,#78206,#78207,#78208,
#78209,#78210,#78211,#78212,#78213,#78214,#78215,#78216,#78217,#78218,#78219,
#78220,#78221,#78222,#78223,#78224,#78225,#78226,#78227,#78228,#78229,#78230,
#78231,#78232,#78233,#78234,#78235,#78236,#78237,#78238,#78239,#78240,#78241,
#78242,#78243,#78244,#78245,#78246,#78247,#78248,#78249,#78250,#78251,#78252,
#78253,#78254,#78255,#78256,#78257,#78258,#78259,#78260,#78261,#78262,#78263,
#78264,#78265,#78266,#78267,#78268,#78269,#78270,#78271,#78272,#78273,#78274,
#78275,#78276,#78277,#78278,#78279,#78280,#78281,#78282,#78283,#78284,#78285,
#78286,#78287,#78288,#78289,#78290,#78291,#78292,#78293,#78294,#78295,#78296,
#78297,#78298,#78299,#78300,#78301,#78302,#78303,#78304,#78305,#78306,#78307,
#78308,#78309,#78310,#78311,#78312,#78313,#78314,#78315,#78316,#78317,#78318,
#78319,#78320,#78321,#78322,#78323,#78324,#78325,#78326,#78327,#78328,#78329,
#78330,#78331,#78332,#78333,#78334,#78335,#78336,#78337,#78338,#78339,#78340,
#78341,#78342,#78343,#78344,#78345,#78346,#78347,#78348,#78349,#78350,#78351,
#78352,#78353,#78354),.UNSPECIFIED.,.F.,.F.,(4,3,3,3,3,3,3,3,3,3,3,3,3,
3,3,3,3,3,3,3,3,3,3,3,3,3,3,3,3,3,3,3,3,3,3,3,3,3,3,3,3,3,3,3,3,3,3,3,3,
3,3,3,3,3,3,3,3,3,3,3,3,3,3,3,3,3,3,3,3,3,3,3,4),(838.805238508566,838.908003644901,
839.012398265655,839.08654777564,839.170286487486,839.253921998854,839.337474442252,
839.420963878103,839.504417828717,839.587854322563,839.671291432319,839.754747227237,
839.838291719966,839.921880802907,840.005604070465,840.08628378636,840.170022498206,
840.253658009573,840.337210452972,840.420699888823,840.504153839436,840.587590333282,
840.671027443038,840.754483237955,840.838027730685,840.921616813626,841.005340081183,
841.08601979708,841.169758508926,841.253394020294,841.336946463692,841.420435899543,
841.503889850157,841.587326344003,841.670763453758,841.754219248676,841.837763741406,
841.921352824347,842.005076091904,842.0857558078,842.169494519646,842.253130031013,
842.336682474412,842.420171910263,842.503625860877,842.587062354723,842.670499464479,
842.753955259396,842.837499752126,842.921088835067,843.004812102625,843.08549181852,
843.169230530366,843.252866041734,843.336418485132,843.419907920983,843.503361871597,
843.586798365443,843.670235475198,843.753691270116,843.837235762846,843.920824845787,
844.004548113344,844.08522782924,844.168981814258,844.252603254596,844.336148220539,
844.419634877612,844.5030813478,844.586524571239,844.669961864576,844.753450679487,
844.836771567909),.UNSPECIFIED.);
#584=B_SPLINE_CURVE_WITH_KNOTS('',3,(#78355,#78356,#78357,#78358,#78359,
#78360,#78361,#78362,#78363,#78364),.UNSPECIFIED.,.F.,.F.,(4,3,3,4),(838.554033681403,
838.636776122618,838.721007315535,838.805238508453),.UNSPECIFIED.);
#585=B_SPLINE_CURVE_WITH_KNOTS('',3,(#78366,#78367,#78368,#78369,#78370,
#78371,#78372,#78373,#78374,#78375),.UNSPECIFIED.,.F.,.F.,(4,3,3,4),(838.554883200175,
838.647013297185,838.738739357629,838.805238508288),.UNSPECIFIED.);
#586=B_SPLINE_CURVE_WITH_KNOTS('',3,(#78376,#78377,#78378,#78379,#78380,
#78381,#78382,#78383,#78384,#78385,#78386,#78387,#78388,#78389,#78390,#78391,
#78392,#78393,#78394,#78395,#78396,#78397,#78398,#78399,#78400,#78401,#78402,
#78403,#78404,#78405,#78406,#78407,#78408,#78409,#78410,#78411,#78412,#78413,
#78414,#78415,#78416,#78417,#78418,#78419,#78420,#78421,#78422,#78423,#78424,
#78425,#78426,#78427,#78428,#78429,#78430,#78431,#78432,#78433,#78434,#78435,
#78436,#78437,#78438,#78439,#78440,#78441,#78442,#78443,#78444,#78445,#78446,
#78447,#78448,#78449,#78450,#78451,#78452,#78453,#78454,#78455,#78456,#78457,
#78458,#78459,#78460,#78461,#78462,#78463,#78464,#78465,#78466,#78467,#78468,
#78469,#78470,#78471,#78472,#78473,#78474,#78475,#78476,#78477,#78478,#78479,
#78480,#78481,#78482,#78483,#78484,#78485,#78486,#78487,#78488,#78489,#78490,
#78491,#78492,#78493,#78494,#78495,#78496,#78497,#78498,#78499,#78500,#78501,
#78502,#78503,#78504,#78505,#78506,#78507,#78508,#78509,#78510,#78511,#78512,
#78513,#78514,#78515,#78516,#78517,#78518,#78519,#78520,#78521,#78522,#78523,
#78524,#78525,#78526,#78527,#78528,#78529,#78530,#78531,#78532,#78533,#78534,
#78535,#78536,#78537,#78538,#78539,#78540,#78541,#78542,#78543,#78544,#78545,
#78546,#78547,#78548,#78549,#78550,#78551,#78552,#78553,#78554,#78555,#78556,
#78557,#78558,#78559,#78560,#78561,#78562,#78563,#78564,#78565,#78566,#78567,
#78568,#78569,#78570,#78571,#78572,#78573,#78574,#78575,#78576,#78577,#78578,
#78579,#78580,#78581,#78582,#78583,#78584,#78585,#78586,#78587,#78588,#78589,
#78590,#78591,#78592,#78593,#78594,#78595),.UNSPECIFIED.,.F.,.F.,(4,3,3,
3,3,3,3,3,3,3,3,3,3,3,3,3,3,3,3,3,3,3,3,3,3,3,3,3,3,3,3,3,3,3,3,3,3,3,3,
3,3,3,3,3,3,3,3,3,3,3,3,3,3,3,3,3,3,3,3,3,3,3,3,3,3,3,3,3,3,3,3,3,3,4),
(838.805238508457,838.889983142447,838.974755435149,839.059571419872,839.144509591216,
839.229510261239,839.314669361647,839.396838395356,839.480577107202,839.564212618569,
839.647765061968,839.731254497819,839.814708448432,839.898144942279,839.981582052034,
840.065037846951,840.148582339681,840.232171422622,840.315894690179,840.396574406076,
840.480313117922,840.56394862929,840.647501072688,840.73099050854,840.814444459153,
840.897880953,840.981318062755,841.064773857673,841.148318350403,841.231907433344,
841.315630700901,841.396310416796,841.480049128642,841.563684640009,841.647237083408,
841.730726519259,841.814180469873,841.897616963719,841.981054073475,842.064509868392,
842.148054361122,842.231643444063,842.315366711621,842.396046427517,842.479785139363,
842.563420650731,842.646973094129,842.73046252998,842.813916480594,842.89735297444,
842.980790084196,843.064245879113,843.147790371843,843.231379454784,843.315102722342,
843.395782438237,843.479521150083,843.56315666145,843.646709104849,843.7301985407,
843.813652491314,843.89708898516,843.980526094916,844.063981889833,844.147526382563,
844.231115465504,844.314838733061,844.395518448957,844.478855380823,844.562089805476,
844.645223408232,844.728298995265,844.811331306897,844.837351982703),
 .UNSPECIFIED.);
#587=B_SPLINE_CURVE_WITH_KNOTS('',3,(#78601,#78602,#78603,#78604,#78605,
#78606,#78607,#78608,#78609,#78610,#78611,#78612,#78613,#78614,#78615,#78616,
#78617,#78618,#78619,#78620,#78621,#78622,#78623,#78624,#78625,#78626,#78627,
#78628,#78629,#78630,#78631,#78632,#78633,#78634,#78635,#78636,#78637,#78638,
#78639,#78640,#78641,#78642,#78643,#78644,#78645,#78646,#78647,#78648,#78649,
#78650,#78651,#78652,#78653,#78654,#78655,#78656,#78657,#78658,#78659,#78660,
#78661,#78662,#78663,#78664,#78665,#78666,#78667,#78668,#78669,#78670,#78671,
#78672,#78673,#78674,#78675,#78676,#78677,#78678,#78679,#78680,#78681,#78682,
#78683,#78684,#78685,#78686,#78687,#78688,#78689,#78690,#78691,#78692,#78693,
#78694,#78695,#78696,#78697,#78698,#78699,#78700,#78701,#78702,#78703,#78704,
#78705,#78706,#78707,#78708,#78709,#78710,#78711,#78712,#78713,#78714,#78715,
#78716,#78717,#78718,#78719,#78720,#78721,#78722,#78723,#78724,#78725,#78726,
#78727,#78728,#78729,#78730,#78731,#78732,#78733,#78734,#78735,#78736,#78737,
#78738,#78739,#78740,#78741,#78742,#78743,#78744,#78745,#78746,#78747,#78748,
#78749,#78750,#78751,#78752,#78753,#78754,#78755,#78756,#78757,#78758,#78759,
#78760,#78761,#78762,#78763,#78764,#78765,#78766,#78767,#78768,#78769,#78770,
#78771,#78772,#78773,#78774,#78775,#78776,#78777,#78778,#78779,#78780,#78781,
#78782,#78783,#78784,#78785,#78786,#78787,#78788,#78789,#78790,#78791,#78792,
#78793,#78794,#78795,#78796,#78797,#78798,#78799,#78800,#78801,#78802,#78803,
#78804,#78805,#78806,#78807,#78808,#78809,#78810,#78811,#78812,#78813,#78814,
#78815,#78816,#78817,#78818,#78819,#78820),.UNSPECIFIED.,.F.,.F.,(4,3,3,
3,3,3,3,3,3,3,3,3,3,3,3,3,3,3,3,3,3,3,3,3,3,3,3,3,3,3,3,3,3,3,3,3,3,3,3,
3,3,3,3,3,3,3,3,3,3,3,3,3,3,3,3,3,3,3,3,3,3,3,3,3,3,3,3,3,3,3,3,3,3,4),
(845.088423815769,845.172110285652,845.255693596232,845.339193936393,845.42263142254,
845.50603367729,845.589418718362,845.672804668667,845.756209647912,845.839703348041,
845.923242043354,846.006913990348,846.084699850681,846.168438562527,846.252074073895,
846.335626517293,846.419115953144,846.502569903758,846.586006397604,846.66944350736,
846.752899302277,846.836443795007,846.920032877948,847.003756145506,847.084435861401,
847.168174573247,847.251810084614,847.335362528013,847.418851963864,847.502305914478,
847.585742408324,847.66917951808,847.752635312998,847.836179805727,847.919768888668,
848.003492156226,848.084171872121,848.167910583967,848.251546095335,848.335098538733,
848.418587974584,848.502041925198,848.585478419044,848.6689155288,848.752371323718,
848.835915816447,848.919504899388,849.003228166946,849.083907882841,849.167646594687,
849.251282106054,849.334834549453,849.418323985304,849.501777935918,849.585214429764,
849.668651539519,849.752107334437,849.835651827166,849.919240910107,850.002964177665,
850.083643893561,850.167382605407,850.251018116774,850.334570560173,850.418059996024,
850.501513946638,850.584950440484,850.66838755024,850.751843345158,850.835387837888,
850.918976920829,851.002700188386,851.083379904281,851.120768468837),
 .UNSPECIFIED.);
#588=B_SPLINE_CURVE_WITH_KNOTS('',3,(#78821,#78822,#78823,#78824,#78825,
#78826,#78827,#78828,#78829,#78830,#78831,#78832,#78833),.UNSPECIFIED.,
 .F.,.F.,(4,3,3,3,4),(844.836771567909,844.92036052459,845.004083725043,
845.08496383996,845.088423815633),.UNSPECIFIED.);
#589=B_SPLINE_CURVE_WITH_KNOTS('',3,(#78835,#78836,#78837,#78838,#78839,
#78840,#78841,#78842,#78843,#78844),.UNSPECIFIED.,.F.,.F.,(4,3,3,4),(844.837351982703,
844.920368259476,845.004396037556,845.088423815637),.UNSPECIFIED.);
#590=B_SPLINE_CURVE_WITH_KNOTS('',3,(#78845,#78846,#78847,#78848,#78849,
#78850,#78851,#78852,#78853,#78854,#78855,#78856,#78857,#78858,#78859,#78860,
#78861,#78862,#78863,#78864,#78865,#78866,#78867,#78868,#78869,#78870,#78871,
#78872,#78873,#78874,#78875,#78876,#78877,#78878,#78879,#78880,#78881,#78882,
#78883,#78884,#78885,#78886,#78887,#78888,#78889,#78890,#78891,#78892,#78893,
#78894,#78895,#78896,#78897,#78898,#78899,#78900,#78901,#78902,#78903,#78904,
#78905,#78906,#78907,#78908,#78909,#78910,#78911,#78912,#78913,#78914,#78915,
#78916,#78917,#78918,#78919,#78920,#78921,#78922,#78923,#78924,#78925,#78926,
#78927,#78928,#78929,#78930,#78931,#78932,#78933,#78934,#78935,#78936,#78937,
#78938,#78939,#78940,#78941,#78942,#78943,#78944,#78945,#78946,#78947,#78948,
#78949,#78950,#78951,#78952,#78953,#78954,#78955,#78956,#78957,#78958,#78959,
#78960,#78961,#78962,#78963,#78964,#78965,#78966,#78967,#78968,#78969,#78970,
#78971,#78972,#78973,#78974,#78975,#78976,#78977,#78978,#78979,#78980,#78981,
#78982,#78983,#78984,#78985,#78986,#78987,#78988,#78989,#78990,#78991,#78992,
#78993,#78994,#78995,#78996,#78997,#78998,#78999,#79000,#79001,#79002,#79003,
#79004,#79005,#79006,#79007,#79008,#79009,#79010,#79011,#79012,#79013,#79014,
#79015,#79016,#79017,#79018,#79019,#79020,#79021,#79022,#79023,#79024,#79025,
#79026,#79027,#79028,#79029,#79030,#79031,#79032,#79033,#79034,#79035,#79036,
#79037,#79038,#79039,#79040,#79041,#79042,#79043,#79044,#79045,#79046,#79047,
#79048,#79049,#79050,#79051,#79052,#79053,#79054,#79055,#79056,#79057,#79058,
#79059,#79060,#79061),.UNSPECIFIED.,.F.,.F.,(4,3,3,3,3,3,3,3,3,3,3,3,3,
3,3,3,3,3,3,3,3,3,3,3,3,3,3,3,3,3,3,3,3,3,3,3,3,3,3,3,3,3,3,3,3,3,3,3,3,
3,3,3,3,3,3,3,3,3,3,3,3,3,3,3,3,3,3,3,3,3,3,3,4),(845.088423815795,845.188236697791,
845.291745578734,845.395254459677,845.478993171523,845.562628682891,845.64618112629,
845.729670562141,845.813124512755,845.896561006601,845.979998116357,846.063453911274,
846.146998404004,846.230587486945,846.314310754503,846.394990470397,846.478729182243,
846.56236469361,846.645917137009,846.72940657286,846.812860523473,846.896297017319,
846.979734127075,847.063189921992,847.146734414722,847.230323497663,847.31404676522,
847.394726481117,847.478465192963,847.562100704331,847.645653147729,847.729142583581,
847.812596534194,847.896033028041,847.979470137797,848.062925932714,848.146470425444,
848.230059508385,848.313782775943,848.394462491838,848.478201203684,848.561836715052,
848.64538915845,848.728878594301,848.812332544915,848.895769038761,848.979206148517,
849.062661943435,849.146206436164,849.229795519105,849.313518786663,849.394198502558,
849.477937214404,849.561572725771,849.64512516917,849.728614605021,849.812068555634,
849.89550504948,849.978942159236,850.062397954153,850.145942446883,850.229531529824,
850.313254797381,850.393934513278,850.477376576719,850.560686672338,850.643920597657,
850.727096805523,850.810233704164,850.893366550294,850.976494891575,851.059668657128,
851.119874427346),.UNSPECIFIED.);
#591=B_SPLINE_CURVE_WITH_KNOTS('',3,(#79067,#79068,#79069,#79070,#79071,
#79072,#79073,#79074,#79075,#79076,#79077,#79078,#79079,#79080,#79081,#79082,
#79083,#79084,#79085,#79086,#79087,#79088,#79089,#79090,#79091,#79092,#79093,
#79094,#79095,#79096,#79097,#79098,#79099,#79100,#79101,#79102,#79103,#79104,
#79105,#79106,#79107,#79108,#79109,#79110,#79111,#79112,#79113,#79114,#79115,
#79116,#79117,#79118,#79119,#79120,#79121,#79122,#79123,#79124,#79125,#79126,
#79127,#79128,#79129,#79130,#79131,#79132,#79133,#79134,#79135,#79136,#79137,
#79138,#79139,#79140,#79141,#79142,#79143,#79144,#79145,#79146,#79147,#79148,
#79149,#79150,#79151,#79152,#79153,#79154,#79155,#79156,#79157,#79158,#79159,
#79160,#79161,#79162,#79163,#79164,#79165,#79166,#79167,#79168,#79169,#79170,
#79171,#79172,#79173,#79174,#79175,#79176,#79177,#79178,#79179,#79180,#79181,
#79182,#79183,#79184,#79185,#79186,#79187,#79188,#79189,#79190,#79191,#79192,
#79193,#79194,#79195,#79196,#79197,#79198,#79199,#79200,#79201,#79202,#79203,
#79204,#79205,#79206,#79207,#79208,#79209,#79210,#79211,#79212,#79213,#79214,
#79215,#79216,#79217,#79218,#79219,#79220,#79221,#79222,#79223,#79224,#79225,
#79226,#79227,#79228,#79229,#79230,#79231,#79232,#79233,#79234,#79235,#79236,
#79237,#79238,#79239,#79240,#79241,#79242,#79243,#79244,#79245,#79246,#79247,
#79248,#79249,#79250,#79251,#79252,#79253,#79254,#79255,#79256,#79257,#79258,
#79259,#79260,#79261,#79262,#79263,#79264,#79265,#79266,#79267,#79268,#79269,
#79270,#79271,#79272,#79273,#79274,#79275,#79276,#79277,#79278,#79279,#79280,
#79281,#79282,#79283,#79284,#79285,#79286),.UNSPECIFIED.,.F.,.F.,(4,3,3,
3,3,3,3,3,3,3,3,3,3,3,3,3,3,3,3,3,3,3,3,3,3,3,3,3,3,3,3,3,3,3,3,3,3,3,3,
3,3,3,3,3,3,3,3,3,3,3,3,3,3,3,3,3,3,3,3,3,3,3,3,3,3,3,3,3,3,3,3,3,3,4),
(851.371609122812,851.454463410857,851.537287815637,851.620099177469,851.702916093396,
851.785757161153,851.868689417554,851.95167211902,852.034780599427,852.083115915001,
852.166854626847,852.250490138214,852.334042581613,852.417532017464,852.500985968077,
852.584422461924,852.667859571679,852.751315366596,852.834859859326,852.918448942267,
853.002172209824,853.082851925721,853.166590637567,853.250226148935,853.333778592334,
853.417268028185,853.500721978799,853.584158472646,853.667595582401,853.751051377319,
853.834595870049,853.91818495299,854.001908220548,854.082587936442,854.166326648288,
854.249962159655,854.333514603054,854.417004038905,854.500457989519,854.583894483365,
854.66733159312,854.750787388038,854.834331880767,854.917920963708,855.001644231265,
855.082323947162,855.166062659008,855.249698170375,855.333250613773,855.416740049625,
855.500194000238,855.583630494085,855.66706760384,855.750523398758,855.834067891488,
855.917656974429,856.001380241986,856.082059957882,856.165798669728,856.249434181096,
856.332986624494,856.416476060346,856.499930010959,856.583366504806,856.666803614561,
856.750259409479,856.833803902209,856.91739298515,857.001116252707,857.081795968602,
857.1674341756,857.252964079907,857.338368454942,857.404280519461),
 .UNSPECIFIED.);
#592=B_SPLINE_CURVE_WITH_KNOTS('',3,(#79287,#79288,#79289,#79290,#79291,
#79292,#79293,#79294,#79295,#79296),.UNSPECIFIED.,.F.,.F.,(4,3,3,4),(851.120768468837,
851.224139296325,851.326074160885,851.371609122685),.UNSPECIFIED.);
#593=B_SPLINE_CURVE_WITH_KNOTS('',3,(#79298,#79299,#79300,#79301,#79302,
#79303,#79304,#79305,#79306,#79307),.UNSPECIFIED.,.F.,.F.,(4,3,3,4),(851.119874427346,
851.203146061834,851.287377592223,851.371609122613),.UNSPECIFIED.);
#594=B_SPLINE_CURVE_WITH_KNOTS('',3,(#79308,#79309,#79310,#79311,#79312,
#79313,#79314,#79315,#79316,#79317,#79318,#79319,#79320,#79321,#79322,#79323,
#79324,#79325,#79326,#79327,#79328,#79329,#79330,#79331,#79332,#79333,#79334,
#79335,#79336,#79337,#79338,#79339,#79340,#79341,#79342,#79343,#79344,#79345,
#79346,#79347,#79348,#79349,#79350,#79351,#79352,#79353,#79354,#79355,#79356,
#79357,#79358,#79359,#79360,#79361,#79362,#79363,#79364,#79365,#79366,#79367,
#79368,#79369,#79370,#79371,#79372,#79373,#79374,#79375,#79376,#79377,#79378,
#79379,#79380,#79381,#79382,#79383,#79384,#79385,#79386,#79387,#79388,#79389,
#79390,#79391,#79392,#79393,#79394,#79395,#79396,#79397,#79398,#79399,#79400,
#79401,#79402,#79403,#79404,#79405,#79406,#79407,#79408,#79409,#79410,#79411,
#79412,#79413,#79414,#79415,#79416,#79417,#79418,#79419,#79420,#79421,#79422,
#79423,#79424,#79425,#79426,#79427,#79428,#79429,#79430,#79431,#79432,#79433,
#79434,#79435,#79436,#79437,#79438,#79439,#79440,#79441,#79442,#79443,#79444,
#79445,#79446,#79447,#79448,#79449,#79450,#79451,#79452,#79453,#79454,#79455,
#79456,#79457,#79458,#79459,#79460,#79461,#79462,#79463,#79464,#79465,#79466,
#79467,#79468,#79469,#79470,#79471,#79472,#79473,#79474,#79475,#79476,#79477,
#79478,#79479,#79480,#79481,#79482,#79483,#79484,#79485,#79486,#79487,#79488,
#79489,#79490,#79491,#79492,#79493,#79494,#79495,#79496,#79497,#79498,#79499,
#79500,#79501,#79502,#79503,#79504,#79505,#79506,#79507,#79508,#79509,#79510,
#79511,#79512,#79513,#79514,#79515,#79516,#79517,#79518,#79519,#79520,#79521,
#79522,#79523,#79524,#79525,#79526,#79527,#79528,#79529,#79530),
 .UNSPECIFIED.,.F.,.F.,(4,3,3,3,3,3,3,3,3,3,3,3,3,3,3,3,3,3,3,3,3,3,3,3,
3,3,3,3,3,3,3,3,3,3,3,3,3,3,3,3,3,3,3,3,3,3,3,3,3,3,3,3,3,3,3,3,3,3,3,3,
3,3,3,3,3,3,3,3,3,3,3,3,3,3,4),(851.371609122816,851.393670523998,851.477409235844,
851.561044747211,851.64459719061,851.728086626461,851.811540577074,851.89497707092,
851.978414180676,852.061869975593,852.145414468323,852.229003551263,852.312726818821,
852.393406534718,852.477145246564,852.560780757931,852.64433320133,852.727822637181,
852.811276587794,852.894713081641,852.978150191396,853.061605986314,853.145150479043,
853.228739561984,853.312462829542,853.393142545438,853.476881257284,853.560516768651,
853.64406921205,853.727558647901,853.811012598515,853.894449092361,853.977886202116,
854.061341997034,854.144886489764,854.228475572705,854.312198840262,854.392878556158,
854.476617268004,854.560252779371,854.64380522277,854.727294658621,854.810748609235,
854.894185103081,854.977622212836,855.061078007754,855.144622500483,855.228211583424,
855.311934850982,855.392614566878,855.476353278724,855.559988790091,855.64354123349,
855.727030669341,855.810484619954,855.893921113801,855.977358223556,856.060814018473,
856.144358511203,856.227947594144,856.311670861701,856.392350577598,856.476089289444,
856.559724800812,856.64327724421,856.726766680061,856.810220630675,856.893657124522,
856.977094234277,857.060550029195,857.144094521925,857.227683604866,857.311406872424,
857.392086588319,857.403801598388),.UNSPECIFIED.);
#595=B_SPLINE_CURVE_WITH_KNOTS('',3,(#79536,#79537,#79538,#79539,#79540,
#79541,#79542,#79543,#79544,#79545,#79546,#79547,#79548,#79549,#79550,#79551,
#79552,#79553,#79554,#79555,#79556,#79557,#79558,#79559,#79560,#79561,#79562,
#79563,#79564,#79565,#79566,#79567,#79568,#79569,#79570,#79571,#79572,#79573,
#79574,#79575,#79576,#79577,#79578,#79579,#79580,#79581,#79582,#79583,#79584,
#79585,#79586,#79587,#79588,#79589,#79590,#79591,#79592,#79593,#79594,#79595,
#79596,#79597,#79598,#79599,#79600,#79601,#79602,#79603,#79604,#79605,#79606,
#79607,#79608,#79609,#79610,#79611,#79612,#79613,#79614,#79615,#79616,#79617,
#79618,#79619,#79620,#79621,#79622,#79623,#79624,#79625,#79626,#79627,#79628,
#79629,#79630,#79631,#79632,#79633,#79634,#79635,#79636,#79637,#79638,#79639,
#79640,#79641,#79642,#79643,#79644,#79645,#79646,#79647,#79648,#79649,#79650,
#79651,#79652,#79653,#79654,#79655,#79656,#79657,#79658,#79659,#79660,#79661,
#79662,#79663,#79664,#79665,#79666,#79667,#79668,#79669,#79670,#79671,#79672,
#79673,#79674,#79675,#79676,#79677,#79678,#79679,#79680,#79681,#79682,#79683,
#79684,#79685,#79686,#79687,#79688,#79689,#79690,#79691,#79692,#79693,#79694,
#79695,#79696,#79697,#79698,#79699,#79700,#79701,#79702,#79703,#79704,#79705,
#79706,#79707,#79708,#79709,#79710,#79711,#79712,#79713,#79714,#79715,#79716,
#79717,#79718,#79719,#79720,#79721,#79722,#79723,#79724,#79725,#79726,#79727,
#79728,#79729,#79730,#79731,#79732,#79733,#79734,#79735,#79736,#79737,#79738,
#79739,#79740,#79741,#79742,#79743,#79744,#79745,#79746,#79747,#79748,#79749,
#79750,#79751,#79752,#79753,#79754,#79755),.UNSPECIFIED.,.F.,.F.,(4,3,3,
3,3,3,3,3,3,3,3,3,3,3,3,3,3,3,3,3,3,3,3,3,3,3,3,3,3,3,3,3,3,3,3,3,3,3,3,
3,3,3,3,3,3,3,3,3,3,3,3,3,3,3,3,3,3,3,3,3,3,3,3,3,3,3,3,3,3,3,3,3,3,4),
(857.654794430136,857.74538946886,857.836378454926,857.927567441179,858.019060923412,
858.081531979322,858.165270691168,858.248906202536,858.332458645934,858.415948081785,
858.499402032399,858.582838526245,858.666275636001,858.749731430919,858.833275923648,
858.916865006589,859.000588274147,859.081267990042,859.165006701888,859.248642213255,
859.332194656654,859.415684092505,859.499138043118,859.582574536965,859.66601164672,
859.749467441638,859.833011934367,859.916601017308,860.000324284866,860.081004000762,
860.164742712608,860.248378223976,860.331930667374,860.415420103225,860.498874053839,
860.582310547685,860.665747657441,860.749203452359,860.832747945088,860.916337028029,
861.000060295587,861.080740011482,861.164478723328,861.248114234695,861.331666678094,
861.415156113945,861.498610064559,861.582046558405,861.665483668161,861.748939463078,
861.832483955808,861.916073038749,861.999796306307,862.080476022203,862.164214734049,
862.247850245417,862.331402688815,862.414892124666,862.49834607528,862.581782569126,
862.665219678882,862.7486754738,862.832219966529,862.91580904947,862.999532317028,
863.080212032923,863.162711702593,863.245116481761,863.327445568733,863.409718089265,
863.491959205929,863.574182388538,863.656422282705,863.68620670875),
 .UNSPECIFIED.);
#596=B_SPLINE_CURVE_WITH_KNOTS('',3,(#79756,#79757,#79758,#79759,#79760,
#79761,#79762,#79763,#79764,#79765),.UNSPECIFIED.,.F.,.F.,(4,3,3,4),(857.404280519461,
857.489540442283,857.574738516118,857.654794429992),.UNSPECIFIED.);
#597=B_SPLINE_CURVE_WITH_KNOTS('',3,(#79767,#79768,#79769,#79770,#79771,
#79772,#79773,#79774,#79775,#79776),.UNSPECIFIED.,.F.,.F.,(4,3,3,4),(857.403801598388,
857.511208903319,857.616619766979,857.654794429849),.UNSPECIFIED.);
#598=B_SPLINE_CURVE_WITH_KNOTS('',3,(#79777,#79778,#79779,#79780,#79781,
#79782,#79783,#79784,#79785,#79786,#79787,#79788,#79789,#79790,#79791,#79792,
#79793,#79794,#79795,#79796,#79797,#79798,#79799,#79800,#79801,#79802,#79803,
#79804,#79805,#79806,#79807,#79808,#79809,#79810,#79811,#79812,#79813,#79814,
#79815,#79816,#79817,#79818,#79819,#79820,#79821,#79822,#79823,#79824,#79825,
#79826,#79827,#79828,#79829,#79830,#79831,#79832,#79833,#79834,#79835,#79836,
#79837,#79838,#79839,#79840,#79841,#79842,#79843,#79844,#79845,#79846,#79847,
#79848,#79849,#79850,#79851,#79852,#79853,#79854,#79855,#79856,#79857,#79858,
#79859,#79860,#79861,#79862,#79863,#79864,#79865,#79866,#79867,#79868,#79869,
#79870,#79871,#79872,#79873,#79874,#79875,#79876,#79877,#79878,#79879,#79880,
#79881,#79882,#79883,#79884,#79885,#79886,#79887,#79888,#79889,#79890,#79891,
#79892,#79893,#79894,#79895,#79896,#79897,#79898,#79899,#79900,#79901,#79902,
#79903,#79904,#79905,#79906,#79907,#79908,#79909,#79910,#79911,#79912,#79913,
#79914,#79915,#79916,#79917,#79918,#79919,#79920,#79921,#79922,#79923,#79924,
#79925,#79926,#79927,#79928,#79929,#79930,#79931,#79932,#79933,#79934,#79935,
#79936,#79937,#79938,#79939,#79940,#79941,#79942,#79943,#79944,#79945,#79946,
#79947,#79948,#79949,#79950,#79951,#79952,#79953,#79954,#79955,#79956,#79957,
#79958,#79959,#79960,#79961,#79962,#79963,#79964,#79965,#79966,#79967,#79968,
#79969,#79970,#79971,#79972,#79973,#79974,#79975,#79976,#79977,#79978,#79979,
#79980,#79981,#79982,#79983,#79984,#79985,#79986,#79987,#79988,#79989,#79990,
#79991,#79992,#79993,#79994,#79995,#79996),.UNSPECIFIED.,.F.,.F.,(4,3,3,
3,3,3,3,3,3,3,3,3,3,3,3,3,3,3,3,3,3,3,3,3,3,3,3,3,3,3,3,3,3,3,3,3,3,3,3,
3,3,3,3,3,3,3,3,3,3,3,3,3,3,3,3,3,3,3,3,3,3,3,3,3,3,3,3,3,3,3,3,3,3,4),
(857.654794429996,857.737439006459,857.820040512216,857.902620276709,857.985197085807,
858.067789720308,858.150467846438,858.233189315394,858.31604260483,858.391822599039,
858.475561310885,858.559196822252,858.642749265651,858.726238701502,858.809692652115,
858.893129145961,858.976566255717,859.060022050635,859.143566543364,859.227155626305,
859.310878893863,859.391558609759,859.475297321605,859.558932832972,859.642485276371,
859.725974712222,859.809428662836,859.892865156682,859.976302266437,860.059758061355,
860.143302554085,860.226891637026,860.310614904583,860.391294620479,860.475033332325,
860.558668843692,860.642221287091,860.725710722942,860.809164673556,860.892601167402,
860.976038277157,861.059494072074,861.143038564804,861.226627647745,861.310350915303,
861.391030631199,861.474769343045,861.558404854412,861.641957297811,861.725446733662,
861.808900684276,861.892337178122,861.975774287878,862.059230082796,862.142774575525,
862.226363658466,862.310086926024,862.390766641919,862.474505353765,862.558140865132,
862.64169330853,862.725182744381,862.808636694995,862.892073188841,862.975510298596,
863.058966093514,863.142510586243,863.226099669184,863.309822936742,863.390502652639,
863.476882971832,863.563148000132,863.649276805144,863.687548921762),
 .UNSPECIFIED.);
#599=B_SPLINE_CURVE_WITH_KNOTS('',3,(#80002,#80003,#80004,#80005,#80006,
#80007,#80008,#80009,#80010,#80011,#80012,#80013,#80014,#80015,#80016,#80017,
#80018,#80019,#80020,#80021,#80022,#80023,#80024,#80025,#80026,#80027,#80028,
#80029,#80030,#80031,#80032,#80033,#80034,#80035,#80036,#80037,#80038,#80039,
#80040,#80041,#80042,#80043,#80044,#80045,#80046,#80047,#80048,#80049,#80050,
#80051,#80052,#80053,#80054,#80055,#80056,#80057,#80058,#80059,#80060,#80061,
#80062,#80063,#80064,#80065,#80066,#80067,#80068,#80069,#80070,#80071,#80072,
#80073,#80074,#80075,#80076,#80077,#80078,#80079,#80080,#80081,#80082,#80083,
#80084,#80085,#80086,#80087,#80088,#80089,#80090,#80091,#80092,#80093,#80094,
#80095,#80096,#80097,#80098,#80099,#80100,#80101,#80102,#80103,#80104,#80105,
#80106,#80107,#80108,#80109,#80110,#80111,#80112,#80113,#80114,#80115,#80116,
#80117,#80118,#80119,#80120,#80121,#80122,#80123,#80124,#80125,#80126,#80127,
#80128,#80129,#80130,#80131,#80132,#80133,#80134,#80135,#80136,#80137,#80138,
#80139,#80140,#80141,#80142,#80143,#80144,#80145,#80146,#80147,#80148,#80149,
#80150,#80151,#80152,#80153,#80154,#80155,#80156,#80157,#80158,#80159,#80160,
#80161,#80162,#80163,#80164,#80165,#80166,#80167,#80168,#80169,#80170,#80171,
#80172,#80173,#80174,#80175,#80176,#80177,#80178,#80179,#80180,#80181,#80182,
#80183,#80184,#80185,#80186,#80187,#80188,#80189,#80190,#80191,#80192,#80193,
#80194,#80195,#80196,#80197,#80198,#80199,#80200,#80201,#80202,#80203,#80204,
#80205,#80206,#80207,#80208,#80209,#80210,#80211,#80212,#80213,#80214,#80215,
#80216,#80217,#80218),.UNSPECIFIED.,.F.,.F.,(4,3,3,3,3,3,3,3,3,3,3,3,3,
3,3,3,3,3,3,3,3,3,3,3,3,3,3,3,3,3,3,3,3,3,3,3,3,3,3,3,3,3,3,3,3,3,3,3,3,
3,3,3,3,3,3,3,3,3,3,3,3,3,3,3,3,3,3,3,3,3,3,3,4),(863.937979737172,864.079948043643,
864.163686755489,864.247322266856,864.330874710255,864.414364146106,864.49781809672,
864.581254590566,864.664691700322,864.748147495239,864.831691987969,864.91528107091,
864.999004338468,865.079684054363,865.163422766209,865.247058277577,865.330610720975,
865.414100156826,865.49755410744,865.580990601286,865.664427711041,865.747883505959,
865.831427998689,865.91501708163,865.998740349187,866.079420065083,866.163158776929,
866.246794288297,866.330346731695,866.413836167546,866.49729011816,866.580726612006,
866.664163721761,866.747619516679,866.831164009409,866.91475309235,866.998476359907,
867.079156075803,867.162894787649,867.246530299016,867.330082742415,867.413572178266,
867.497026128879,867.580462622726,867.663899732481,867.747355527399,867.830900020128,
867.914489103069,867.998212370627,868.078892086523,868.162630798369,868.246266309736,
868.329818753135,868.413308188986,868.4967621396,868.580198633446,868.663635743202,
868.74709153812,868.830636030849,868.91422511379,868.997948381348,869.078628097243,
869.162373162193,869.2460135923,869.32956952621,869.413056411045,869.49650572187,
869.579935547268,869.663363958879,869.746844645517,869.830352862841,869.913953867878,
869.969625938716),.UNSPECIFIED.);
#600=B_SPLINE_CURVE_WITH_KNOTS('',3,(#80219,#80220,#80221,#80222,#80223,
#80224,#80225,#80226,#80227,#80228),.UNSPECIFIED.,.F.,.F.,(4,3,3,4),(863.68620670875,
863.768511157265,863.853245447158,863.937979737052),.UNSPECIFIED.);
#601=B_SPLINE_CURVE_WITH_KNOTS('',3,(#80230,#80231,#80232,#80233,#80234,
#80235,#80236,#80237,#80238,#80239),.UNSPECIFIED.,.F.,.F.,(4,3,3,4),(863.687548921762,
863.773526588714,863.859412870955,863.937979737175),.UNSPECIFIED.);
#602=B_SPLINE_CURVE_WITH_KNOTS('',3,(#80240,#80241,#80242,#80243,#80244,
#80245,#80246,#80247,#80248,#80249,#80250,#80251,#80252,#80253,#80254,#80255,
#80256,#80257,#80258,#80259,#80260,#80261,#80262,#80263,#80264,#80265,#80266,
#80267,#80268,#80269,#80270,#80271,#80272,#80273,#80274,#80275,#80276,#80277,
#80278,#80279,#80280,#80281,#80282,#80283,#80284,#80285,#80286,#80287,#80288,
#80289,#80290,#80291,#80292,#80293,#80294,#80295,#80296,#80297,#80298,#80299,
#80300,#80301,#80302,#80303,#80304,#80305,#80306,#80307,#80308,#80309,#80310,
#80311,#80312,#80313,#80314,#80315,#80316,#80317,#80318,#80319,#80320,#80321,
#80322,#80323,#80324,#80325,#80326,#80327,#80328,#80329,#80330,#80331,#80332,
#80333,#80334,#80335,#80336,#80337,#80338,#80339,#80340,#80341,#80342,#80343,
#80344,#80345,#80346,#80347,#80348,#80349,#80350,#80351,#80352,#80353,#80354,
#80355,#80356,#80357,#80358,#80359,#80360,#80361,#80362,#80363,#80364,#80365,
#80366,#80367,#80368,#80369,#80370,#80371,#80372,#80373,#80374,#80375,#80376,
#80377,#80378,#80379,#80380,#80381,#80382,#80383,#80384,#80385,#80386,#80387,
#80388,#80389,#80390,#80391,#80392,#80393,#80394,#80395,#80396,#80397,#80398,
#80399,#80400,#80401,#80402,#80403,#80404,#80405,#80406,#80407,#80408,#80409,
#80410,#80411,#80412,#80413,#80414,#80415,#80416,#80417,#80418,#80419,#80420,
#80421,#80422,#80423,#80424,#80425,#80426,#80427,#80428,#80429,#80430,#80431,
#80432,#80433,#80434,#80435,#80436,#80437,#80438,#80439,#80440,#80441,#80442,
#80443,#80444,#80445,#80446,#80447,#80448,#80449,#80450,#80451,#80452,#80453,
#80454,#80455,#80456),.UNSPECIFIED.,.F.,.F.,(4,3,3,3,3,3,3,3,3,3,3,3,3,
3,3,3,3,3,3,3,3,3,3,3,3,3,3,3,3,3,3,3,3,3,3,3,3,3,3,3,3,3,3,3,3,3,3,3,3,
3,3,3,3,3,3,3,3,3,3,3,3,3,3,3,3,3,3,3,3,3,3,3,4),(863.937979737279,864.027327946061,
864.118055625386,864.207883747777,864.299061205568,864.390238663359,864.473977375205,
864.557612886573,864.641165329971,864.724654765822,864.808108716436,864.891545210282,
864.974982320037,865.058438114955,865.141982607685,865.225571690626,865.309294958184,
865.38997467408,865.473713385926,865.557348897294,865.640901340692,865.724390776543,
865.807844727157,865.891281221003,865.974718330758,866.058174125676,866.141718618406,
866.225307701347,866.309030968904,866.3897106848,866.473449396646,866.557084908013,
866.640637351412,866.724126787263,866.807580737876,866.891017231723,866.974454341478,
867.057910136396,867.141454629125,867.225043712066,867.308766979624,867.38944669552,
867.473185407366,867.556820918733,867.640373362132,867.723862797983,867.807316748596,
867.890753242443,867.974190352198,868.057646147116,868.141190639845,868.224779722786,
868.308502990344,868.38918270624,868.472921418086,868.556556929454,868.640109372852,
868.723598808703,868.807052759317,868.890489253163,868.973926362918,869.057382157836,
869.140926650566,869.224515733507,869.308239001065,869.38891871696,869.471389241532,
869.553764467079,869.636063614742,869.719412917611,869.801620727064,869.885540776641,
869.969460826219),.UNSPECIFIED.);
#603=B_SPLINE_CURVE_WITH_KNOTS('',3,(#80462,#80463,#80464,#80465,#80466,
#80467,#80468,#80469,#80470,#80471,#80472,#80473,#80474,#80475,#80476,#80477,
#80478,#80479,#80480,#80481,#80482,#80483,#80484,#80485,#80486,#80487,#80488,
#80489,#80490,#80491,#80492,#80493,#80494,#80495,#80496,#80497,#80498,#80499,
#80500,#80501,#80502,#80503,#80504,#80505,#80506,#80507,#80508,#80509,#80510,
#80511,#80512,#80513,#80514,#80515,#80516,#80517,#80518,#80519,#80520,#80521,
#80522,#80523,#80524,#80525,#80526,#80527,#80528,#80529,#80530,#80531,#80532,
#80533,#80534,#80535,#80536,#80537,#80538,#80539,#80540,#80541,#80542,#80543,
#80544,#80545,#80546,#80547,#80548,#80549,#80550,#80551,#80552,#80553,#80554,
#80555,#80556,#80557,#80558,#80559,#80560,#80561,#80562,#80563,#80564,#80565,
#80566,#80567,#80568,#80569,#80570,#80571,#80572,#80573,#80574,#80575,#80576,
#80577,#80578,#80579,#80580,#80581,#80582,#80583,#80584,#80585,#80586,#80587,
#80588,#80589,#80590,#80591,#80592,#80593,#80594,#80595,#80596,#80597,#80598,
#80599,#80600,#80601,#80602,#80603,#80604,#80605,#80606,#80607,#80608,#80609,
#80610,#80611,#80612,#80613,#80614,#80615,#80616,#80617,#80618,#80619,#80620,
#80621,#80622,#80623,#80624,#80625,#80626,#80627,#80628,#80629,#80630,#80631,
#80632,#80633,#80634,#80635,#80636,#80637,#80638,#80639,#80640,#80641,#80642,
#80643,#80644,#80645,#80646,#80647,#80648,#80649,#80650,#80651,#80652,#80653,
#80654,#80655,#80656,#80657,#80658,#80659,#80660,#80661,#80662,#80663,#80664,
#80665,#80666,#80667,#80668,#80669,#80670,#80671,#80672,#80673,#80674,#80675,
#80676,#80677,#80678,#80679,#80680,#80681),.UNSPECIFIED.,.F.,.F.,(4,3,3,
3,3,3,3,3,3,3,3,3,3,3,3,3,3,3,3,3,3,3,3,3,3,3,3,3,3,3,3,3,3,3,3,3,3,3,3,
3,3,3,3,3,3,3,3,3,3,3,3,3,3,3,3,3,3,3,3,3,3,3,3,3,3,3,3,3,3,3,3,3,3,4),
(870.22116504447,870.303591153912,870.385933459072,870.472454291523,870.554698467721,
870.636928358824,870.719162982089,870.80142135653,870.883767175294,870.966163941988,
871.048677582414,871.078100118684,871.16183883053,871.245474341898,871.329026785296,
871.412516221147,871.495970171761,871.579406665607,871.662843775362,871.74629957028,
871.82984406301,871.913433145951,871.997156413508,872.077836129404,872.16157484125,
872.245210352618,872.328762796016,872.412252231867,872.495706182481,872.579142676327,
872.662579786082,872.746035581,872.82958007373,872.913169156671,872.996892424228,
873.077572140124,873.16131085197,873.244946363337,873.328498806736,873.411988242587,
873.495442193201,873.578878687047,873.662315796802,873.74577159172,873.82931608445,
873.912905167391,873.996628434948,874.077308150844,874.16104686269,874.244682374057,
874.328234817456,874.411724253307,874.495178203921,874.578614697767,874.662051807522,
874.74550760244,874.829052095169,874.91264117811,874.996364445668,875.077044161564,
875.16078287341,875.244418384777,875.327970828176,875.411460264028,875.494914214641,
875.578350708488,875.661787818243,875.745243613161,875.828788105891,875.912377188832,
875.996100456389,876.076780172284,876.168197875014,876.254027151446),
 .UNSPECIFIED.);
#604=B_SPLINE_CURVE_WITH_KNOTS('',3,(#80682,#80683,#80684,#80685,#80686,
#80687,#80688,#80689,#80690,#80691),.UNSPECIFIED.,.F.,.F.,(4,3,3,4),(869.969625938716,
870.053372297126,870.078364107964,870.221165044351),.UNSPECIFIED.);
#605=B_SPLINE_CURVE_WITH_KNOTS('',3,(#80693,#80694,#80695,#80696,#80697,
#80698,#80699,#80700,#80701,#80702),.UNSPECIFIED.,.F.,.F.,(4,3,3,4),(869.969460826219,
870.051718239475,870.136441641821,870.221165044167),.UNSPECIFIED.);
#606=B_SPLINE_CURVE_WITH_KNOTS('',3,(#80703,#80704,#80705,#80706,#80707,
#80708,#80709,#80710,#80711,#80712,#80713,#80714,#80715,#80716,#80717,#80718,
#80719,#80720,#80721,#80722,#80723,#80724,#80725,#80726,#80727,#80728,#80729,
#80730,#80731,#80732,#80733,#80734,#80735,#80736,#80737,#80738,#80739,#80740,
#80741,#80742,#80743,#80744,#80745,#80746,#80747,#80748,#80749,#80750,#80751,
#80752,#80753,#80754,#80755,#80756,#80757,#80758,#80759,#80760,#80761,#80762,
#80763,#80764,#80765,#80766,#80767,#80768,#80769,#80770,#80771,#80772,#80773,
#80774,#80775,#80776,#80777,#80778,#80779,#80780,#80781,#80782,#80783,#80784,
#80785,#80786,#80787,#80788,#80789,#80790,#80791,#80792,#80793,#80794,#80795,
#80796,#80797,#80798,#80799,#80800,#80801,#80802,#80803,#80804,#80805,#80806,
#80807,#80808,#80809,#80810,#80811,#80812,#80813,#80814,#80815,#80816,#80817,
#80818,#80819,#80820,#80821,#80822,#80823,#80824,#80825,#80826,#80827,#80828,
#80829,#80830,#80831,#80832,#80833,#80834,#80835,#80836,#80837,#80838,#80839,
#80840,#80841,#80842,#80843,#80844,#80845,#80846,#80847,#80848,#80849,#80850,
#80851,#80852,#80853,#80854,#80855,#80856,#80857,#80858,#80859,#80860,#80861,
#80862,#80863,#80864,#80865,#80866,#80867,#80868,#80869,#80870,#80871,#80872,
#80873,#80874,#80875,#80876,#80877,#80878,#80879,#80880,#80881,#80882,#80883,
#80884,#80885,#80886,#80887,#80888,#80889,#80890,#80891,#80892,#80893,#80894,
#80895,#80896,#80897,#80898,#80899,#80900,#80901,#80902,#80903,#80904,#80905,
#80906,#80907,#80908,#80909,#80910,#80911,#80912,#80913,#80914,#80915,#80916,
#80917,#80918,#80919,#80920,#80921,#80922),.UNSPECIFIED.,.F.,.F.,(4,3,3,
3,3,3,3,3,3,3,3,3,3,3,3,3,3,3,3,3,3,3,3,3,3,3,3,3,3,3,3,3,3,3,3,3,3,3,3,
3,3,3,3,3,3,3,3,3,3,3,3,3,3,3,3,3,3,3,3,3,3,3,3,3,3,3,3,3,3,3,3,3,3,4),
(870.221165044355,870.353859449894,870.38865472768,870.472393439526,870.556028950894,
870.639581394292,870.723070830144,870.806524780757,870.889961274604,870.973398384359,
871.056854179277,871.140398672007,871.223987754948,871.307711022506,871.3883907384,
871.472129450246,871.555764961613,871.639317405012,871.722806840863,871.806260791477,
871.889697285323,871.973134395079,872.056590189996,872.140134682726,872.223723765667,
872.307447033224,872.388126749121,872.471865460967,872.555500972335,872.639053415733,
872.722542851584,872.805996802198,872.889433296044,872.9728704058,873.056326200718,
873.139870693447,873.223459776388,873.307183043946,873.387862759841,873.471601471687,
873.555236983054,873.638789426453,873.722278862304,873.805732812917,873.889169306764,
873.972606416519,874.056062211436,874.139606704166,874.223195787107,874.306919054664,
874.387598770561,874.471337482407,874.554972993774,874.638525437173,874.722014873024,
874.805468823638,874.888905317484,874.972342427239,875.055798222157,875.139342714887,
875.222931797828,875.306655065385,875.387334781281,875.47108141737,875.554723081136,
875.641976917475,875.725461427968,875.808908688283,875.892336786282,875.975763792985,
876.059238229605,876.142740720485,876.226323097985,876.252753771852),
 .UNSPECIFIED.);
#607=B_SPLINE_CURVE_WITH_KNOTS('',3,(#80928,#80929,#80930,#80931,#80932,
#80933,#80934,#80935,#80936,#80937,#80938,#80939,#80940,#80941,#80942,#80943,
#80944,#80945,#80946,#80947,#80948,#80949,#80950,#80951,#80952,#80953,#80954,
#80955,#80956,#80957,#80958,#80959,#80960,#80961,#80962,#80963,#80964,#80965,
#80966,#80967,#80968,#80969,#80970,#80971,#80972,#80973,#80974,#80975,#80976,
#80977,#80978,#80979,#80980,#80981,#80982,#80983,#80984,#80985,#80986,#80987,
#80988,#80989,#80990,#80991,#80992,#80993,#80994,#80995,#80996,#80997,#80998,
#80999,#81000,#81001,#81002,#81003,#81004,#81005,#81006,#81007,#81008,#81009,
#81010,#81011,#81012,#81013,#81014,#81015,#81016,#81017,#81018,#81019,#81020,
#81021,#81022,#81023,#81024,#81025,#81026,#81027,#81028,#81029,#81030,#81031,
#81032,#81033,#81034,#81035,#81036,#81037,#81038,#81039,#81040,#81041,#81042,
#81043,#81044,#81045,#81046,#81047,#81048,#81049,#81050,#81051,#81052,#81053,
#81054,#81055,#81056,#81057,#81058,#81059,#81060,#81061,#81062,#81063,#81064,
#81065,#81066,#81067,#81068,#81069,#81070,#81071,#81072,#81073,#81074,#81075,
#81076,#81077,#81078,#81079,#81080,#81081,#81082,#81083,#81084,#81085,#81086,
#81087,#81088,#81089,#81090,#81091,#81092,#81093,#81094,#81095,#81096,#81097,
#81098,#81099,#81100,#81101,#81102,#81103,#81104,#81105,#81106,#81107,#81108,
#81109,#81110,#81111,#81112,#81113,#81114,#81115,#81116,#81117,#81118,#81119,
#81120,#81121,#81122,#81123,#81124,#81125,#81126,#81127,#81128,#81129,#81130,
#81131,#81132,#81133,#81134,#81135,#81136,#81137,#81138,#81139,#81140,#81141,
#81142,#81143,#81144,#81145,#81146,#81147),.UNSPECIFIED.,.F.,.F.,(4,3,3,
3,3,3,3,3,3,3,3,3,3,3,3,3,3,3,3,3,3,3,3,3,3,3,3,3,3,3,3,3,3,3,3,3,3,3,3,
3,3,3,3,3,3,3,3,3,3,3,3,3,3,3,3,3,3,3,3,3,3,3,3,3,3,3,3,3,3,3,3,3,3,4),
(876.504350351531,876.589557356121,876.674806022702,876.760111435919,876.845550924257,
876.931062603895,877.016731762945,877.076516183005,877.160254894851,877.243890406219,
877.327442849617,877.410932285469,877.494386236082,877.577822729929,877.661259839684,
877.744715634602,877.828260127332,877.911849210273,877.99557247783,878.076252193725,
878.159990905571,878.243626416938,878.327178860337,878.410668296188,878.494122246802,
878.577558740648,878.660995850403,878.744451645321,878.82799613805,878.911585220991,
878.995308488549,879.075988204445,879.159726916291,879.243362427658,879.326914871057,
879.410404306908,879.493858257522,879.577294751368,879.660731861123,879.74418765604,
879.82773214877,879.911321231711,879.995044499269,880.075724215165,880.159462927011,
880.243098438379,880.326650881777,880.410140317628,880.493594268242,880.577030762088,
880.660467871844,880.743923666761,880.827468159491,880.911057242432,880.994780509989,
881.075460225885,881.159198937731,881.242834449098,881.326386892496,881.409876328348,
881.493330278961,881.576766772807,881.660203882563,881.743659677481,881.827204170211,
881.910793253152,881.99451652071,882.075196236605,882.158303038281,882.241309055246,
882.324217592094,882.407069719065,882.489883995394,882.536362400618),
 .UNSPECIFIED.);
#608=B_SPLINE_CURVE_WITH_KNOTS('',3,(#81148,#81149,#81150,#81151,#81152,
#81153,#81154,#81155,#81156,#81157),.UNSPECIFIED.,.F.,.F.,(4,3,3,4),(876.254027151446,
876.345004673597,876.435647379661,876.504350351384),.UNSPECIFIED.);
#609=B_SPLINE_CURVE_WITH_KNOTS('',3,(#81159,#81160,#81161,#81162,#81163,
#81164,#81165,#81166,#81167,#81168),.UNSPECIFIED.,.F.,.F.,(4,3,3,4),(876.252753771852,
876.336488419904,876.387070792001,876.504350351535),.UNSPECIFIED.);
#610=B_SPLINE_CURVE_WITH_KNOTS('',3,(#81169,#81170,#81171,#81172,#81173,
#81174,#81175,#81176,#81177,#81178,#81179,#81180,#81181,#81182,#81183,#81184,
#81185,#81186,#81187,#81188,#81189,#81190,#81191,#81192,#81193,#81194,#81195,
#81196,#81197,#81198,#81199,#81200,#81201,#81202,#81203,#81204,#81205,#81206,
#81207,#81208,#81209,#81210,#81211,#81212,#81213,#81214,#81215,#81216,#81217,
#81218,#81219,#81220,#81221,#81222,#81223,#81224,#81225,#81226,#81227,#81228,
#81229,#81230,#81231,#81232,#81233,#81234,#81235,#81236,#81237,#81238,#81239,
#81240,#81241,#81242,#81243,#81244,#81245,#81246,#81247,#81248,#81249,#81250,
#81251,#81252,#81253,#81254,#81255,#81256,#81257,#81258,#81259,#81260,#81261,
#81262,#81263,#81264,#81265,#81266,#81267,#81268,#81269,#81270,#81271,#81272,
#81273,#81274,#81275,#81276,#81277,#81278,#81279,#81280,#81281,#81282,#81283,
#81284,#81285,#81286,#81287,#81288,#81289,#81290,#81291,#81292,#81293,#81294,
#81295,#81296,#81297,#81298,#81299,#81300,#81301,#81302,#81303,#81304,#81305,
#81306,#81307,#81308,#81309,#81310,#81311,#81312,#81313,#81314,#81315,#81316,
#81317,#81318,#81319,#81320,#81321,#81322,#81323,#81324,#81325,#81326,#81327,
#81328,#81329,#81330,#81331,#81332,#81333,#81334,#81335,#81336,#81337,#81338,
#81339,#81340,#81341,#81342,#81343,#81344,#81345,#81346,#81347,#81348,#81349,
#81350,#81351,#81352,#81353,#81354,#81355,#81356,#81357,#81358,#81359,#81360,
#81361,#81362,#81363,#81364,#81365,#81366,#81367,#81368,#81369,#81370,#81371,
#81372,#81373,#81374,#81375,#81376,#81377,#81378,#81379,#81380,#81381,#81382,
#81383,#81384,#81385,#81386,#81387,#81388),.UNSPECIFIED.,.F.,.F.,(4,3,3,
3,3,3,3,3,3,3,3,3,3,3,3,3,3,3,3,3,3,3,3,3,3,3,3,3,3,3,3,3,3,3,3,3,3,3,3,
3,3,3,3,3,3,3,3,3,3,3,3,3,3,3,3,3,3,3,3,3,3,3,3,3,3,3,3,3,3,3,3,3,3,4),
(876.504350351669,876.586886132016,876.669332596924,876.751710843094,876.83404758089,
876.916363953182,876.998678928157,877.081011470526,877.163428715444,877.245891245748,
877.328478721327,877.386806802721,877.470545514567,877.554181025935,877.637733469333,
877.721222905184,877.804676855798,877.888113349644,877.9715504594,878.055006254318,
878.138550747047,878.222139829988,878.305863097546,878.386542813441,878.470281525287,
878.553917036655,878.637469480054,878.720958915905,878.804412866519,878.887849360365,
878.971286470121,879.054742265039,879.138286757769,879.22187584071,879.305599108268,
879.386278824162,879.470017536008,879.553653047375,879.637205490774,879.720694926625,
879.804148877238,879.887585371085,879.97102248084,880.054478275757,880.138022768487,
880.221611851428,880.305335118986,880.386014834882,880.469753546728,880.553389058095,
880.636941501493,880.720430937344,880.803884887958,880.887321381804,880.970758491559,
881.054214286477,881.137758779206,881.221347862147,881.305071129705,881.385750845602,
881.469489557448,881.553125068816,881.636677512215,881.720166948066,881.80362089868,
881.887057392526,881.970494502282,882.053950297199,882.137494789929,882.22108387287,
882.304807140428,882.385486856322,882.478481573058,882.537167377545),
 .UNSPECIFIED.);
#611=B_SPLINE_CURVE_WITH_KNOTS('',3,(#81394,#81395,#81396,#81397,#81398,
#81399,#81400,#81401,#81402,#81403,#81404,#81405,#81406,#81407,#81408,#81409,
#81410,#81411,#81412,#81413,#81414,#81415,#81416,#81417,#81418,#81419,#81420,
#81421,#81422,#81423,#81424,#81425,#81426,#81427,#81428,#81429,#81430,#81431,
#81432,#81433,#81434,#81435,#81436,#81437,#81438,#81439,#81440,#81441,#81442,
#81443,#81444,#81445,#81446,#81447,#81448,#81449,#81450,#81451,#81452,#81453,
#81454,#81455,#81456,#81457,#81458,#81459,#81460,#81461,#81462,#81463,#81464,
#81465,#81466,#81467,#81468,#81469,#81470,#81471,#81472,#81473,#81474,#81475,
#81476,#81477,#81478,#81479,#81480,#81481,#81482,#81483,#81484,#81485,#81486,
#81487,#81488,#81489,#81490,#81491,#81492,#81493,#81494,#81495,#81496,#81497,
#81498,#81499,#81500,#81501,#81502,#81503,#81504,#81505,#81506,#81507,#81508,
#81509,#81510,#81511,#81512,#81513,#81514,#81515,#81516,#81517,#81518,#81519,
#81520,#81521,#81522,#81523,#81524,#81525,#81526,#81527,#81528,#81529,#81530,
#81531,#81532,#81533,#81534,#81535,#81536,#81537,#81538,#81539,#81540,#81541,
#81542,#81543,#81544,#81545,#81546,#81547,#81548,#81549,#81550,#81551,#81552,
#81553,#81554,#81555,#81556,#81557,#81558,#81559,#81560,#81561,#81562,#81563,
#81564,#81565,#81566,#81567,#81568,#81569,#81570,#81571,#81572,#81573,#81574,
#81575,#81576,#81577,#81578,#81579,#81580,#81581,#81582,#81583,#81584,#81585,
#81586,#81587,#81588,#81589,#81590,#81591,#81592,#81593,#81594,#81595,#81596,
#81597,#81598,#81599,#81600,#81601,#81602,#81603,#81604,#81605,#81606,#81607,
#81608,#81609,#81610),.UNSPECIFIED.,.F.,.F.,(4,3,3,3,3,3,3,3,3,3,3,3,3,
3,3,3,3,3,3,3,3,3,3,3,3,3,3,3,3,3,3,3,3,3,3,3,3,3,3,3,3,3,3,3,3,3,3,3,3,
3,3,3,3,3,3,3,3,3,3,3,3,3,3,3,3,3,3,3,3,3,3,3,4),(882.787535658835,882.889547620838,
882.993080195182,883.074932247325,883.158670959172,883.24230647054,883.325858913939,
883.409348349791,883.492802300405,883.576238794252,883.659675904008,883.743131698927,
883.826676191657,883.910265274599,883.993988542157,884.074668258046,884.158406969892,
884.242042481259,884.325594924658,884.409084360509,884.492538311123,884.575974804969,
884.659411914724,884.742867709642,884.826412202372,884.910001285312,884.99372455287,
885.074404268766,885.158142980612,885.241778491979,885.325330935377,885.408820371228,
885.492274321841,885.575710815687,885.659147925442,885.74260372036,885.826148213089,
885.90973729603,885.993460563587,886.074140279486,886.157878991332,886.2415145027,
886.325066946098,886.40855638195,886.492010332563,886.57544682641,886.658883936165,
886.742339731083,886.825884223813,886.909473306754,886.993196574312,887.073876290206,
887.157615002052,887.241250513419,887.324802956818,887.408292392669,887.491746343283,
887.575182837129,887.658619946884,887.742075741802,887.825620234531,887.909209317472,
887.99293258503,888.073612300926,888.157326814901,888.240908795136,888.324414282672,
888.407861481606,888.491268552351,888.574671813844,888.658069309137,888.74151632298,
888.81905987275),.UNSPECIFIED.);
#612=B_SPLINE_CURVE_WITH_KNOTS('',3,(#81611,#81612,#81613,#81614,#81615,
#81616,#81617,#81618,#81619,#81620),.UNSPECIFIED.,.F.,.F.,(4,3,3,4),(882.536362400618,
882.619164337193,882.703349997951,882.78753565871),.UNSPECIFIED.);
#613=B_SPLINE_CURVE_WITH_KNOTS('',3,(#81622,#81623,#81624,#81625,#81626,
#81627,#81628,#81629,#81630,#81631),.UNSPECIFIED.,.F.,.F.,(4,3,3,4),(882.537167377545,
882.629684994883,882.721773999743,882.787535658538),.UNSPECIFIED.);
#614=B_SPLINE_CURVE_WITH_KNOTS('',3,(#81632,#81633,#81634,#81635,#81636,
#81637,#81638,#81639,#81640,#81641,#81642,#81643,#81644,#81645,#81646,#81647,
#81648,#81649,#81650,#81651,#81652,#81653,#81654,#81655,#81656,#81657,#81658,
#81659,#81660,#81661,#81662,#81663,#81664,#81665,#81666,#81667,#81668,#81669,
#81670,#81671,#81672,#81673,#81674,#81675,#81676,#81677,#81678,#81679,#81680,
#81681,#81682,#81683,#81684,#81685,#81686,#81687,#81688,#81689,#81690,#81691,
#81692,#81693,#81694,#81695,#81696,#81697,#81698,#81699,#81700,#81701,#81702,
#81703,#81704,#81705,#81706,#81707,#81708,#81709,#81710,#81711,#81712,#81713,
#81714,#81715,#81716,#81717,#81718,#81719,#81720,#81721,#81722,#81723,#81724,
#81725,#81726,#81727,#81728,#81729,#81730,#81731,#81732,#81733,#81734,#81735,
#81736,#81737,#81738,#81739,#81740,#81741,#81742,#81743,#81744,#81745,#81746,
#81747,#81748,#81749,#81750,#81751,#81752,#81753,#81754,#81755,#81756,#81757,
#81758,#81759,#81760,#81761,#81762,#81763,#81764,#81765,#81766,#81767,#81768,
#81769,#81770,#81771,#81772,#81773,#81774,#81775,#81776,#81777,#81778,#81779,
#81780,#81781,#81782,#81783,#81784,#81785,#81786,#81787,#81788,#81789,#81790,
#81791,#81792,#81793,#81794,#81795,#81796,#81797,#81798,#81799,#81800,#81801,
#81802,#81803,#81804,#81805,#81806,#81807,#81808,#81809,#81810,#81811,#81812,
#81813,#81814,#81815,#81816,#81817,#81818,#81819,#81820,#81821,#81822,#81823,
#81824,#81825,#81826,#81827,#81828,#81829,#81830,#81831,#81832,#81833,#81834,
#81835,#81836,#81837,#81838,#81839,#81840,#81841,#81842,#81843,#81844,#81845,
#81846,#81847,#81848,#81849,#81850,#81851),.UNSPECIFIED.,.F.,.F.,(4,3,3,
3,3,3,3,3,3,3,3,3,3,3,3,3,3,3,3,3,3,3,3,3,3,3,3,3,3,3,3,3,3,3,3,3,3,3,3,
3,3,3,3,3,3,3,3,3,3,3,3,3,3,3,3,3,3,3,3,3,3,3,3,3,3,3,3,3,3,3,3,3,3,4),
(882.787535658714,882.872145401109,882.956778763697,883.041452029423,883.127394738828,
883.212247266875,883.298735066959,883.385222867042,883.468961578888,883.552597090256,
883.636149533654,883.719638969505,883.803092920119,883.886529413965,883.96996652372,
884.053422318637,884.136966811367,884.220555894308,884.304279161866,884.384958877762,
884.468697589608,884.552333100975,884.635885544374,884.719374980225,884.802828930838,
884.886265424684,884.96970253444,885.053158329357,885.136702822086,885.220291905027,
885.304015172585,885.384694888482,885.468433600328,885.552069111695,885.635621555094,
885.719110990945,885.802564941559,885.886001435405,885.96943854516,886.052894340078,
886.136438832807,886.220027915748,886.303751183306,886.384430899202,886.468169611048,
886.551805122416,886.635357565815,886.718847001666,886.80230095228,886.885737446126,
886.969174555882,887.0526303508,887.13617484353,887.219763926471,887.303487194029,
887.384166909923,887.467905621769,887.551541133137,887.635093576535,887.718583012385,
887.802036962999,887.885473456846,887.968910566601,888.052366361519,888.135910854248,
888.219499937189,888.303223204747,888.383902920643,888.467319795645,888.550633556085,
888.633845406105,888.716998660311,888.800107080176,888.819680914903),
 .UNSPECIFIED.);
#615=B_SPLINE_CURVE_WITH_KNOTS('',3,(#81857,#81858,#81859,#81860,#81861,
#81862,#81863,#81864,#81865,#81866,#81867,#81868,#81869,#81870,#81871,#81872,
#81873,#81874,#81875,#81876,#81877,#81878,#81879,#81880,#81881,#81882,#81883,
#81884,#81885,#81886,#81887,#81888,#81889,#81890,#81891,#81892,#81893,#81894,
#81895,#81896,#81897,#81898,#81899,#81900,#81901,#81902,#81903,#81904,#81905,
#81906,#81907,#81908,#81909,#81910,#81911,#81912,#81913,#81914,#81915,#81916,
#81917,#81918,#81919,#81920,#81921,#81922,#81923,#81924,#81925,#81926,#81927,
#81928,#81929,#81930,#81931,#81932,#81933,#81934,#81935,#81936,#81937,#81938,
#81939,#81940,#81941,#81942,#81943,#81944,#81945,#81946,#81947,#81948,#81949,
#81950,#81951,#81952,#81953,#81954,#81955,#81956,#81957,#81958,#81959,#81960,
#81961,#81962,#81963,#81964,#81965,#81966,#81967,#81968,#81969,#81970,#81971,
#81972,#81973,#81974,#81975,#81976,#81977,#81978,#81979,#81980,#81981,#81982,
#81983,#81984,#81985,#81986,#81987,#81988,#81989,#81990,#81991,#81992,#81993,
#81994,#81995,#81996,#81997,#81998,#81999,#82000,#82001,#82002,#82003,#82004,
#82005,#82006,#82007,#82008,#82009,#82010,#82011,#82012,#82013,#82014,#82015,
#82016,#82017,#82018,#82019,#82020,#82021,#82022,#82023,#82024,#82025,#82026,
#82027,#82028,#82029,#82030,#82031,#82032,#82033,#82034,#82035,#82036,#82037,
#82038,#82039,#82040,#82041,#82042,#82043,#82044,#82045,#82046,#82047,#82048,
#82049,#82050,#82051,#82052,#82053,#82054,#82055,#82056,#82057,#82058,#82059,
#82060,#82061,#82062,#82063,#82064,#82065,#82066,#82067,#82068,#82069,#82070,
#82071,#82072,#82073,#82074,#82075,#82076,#82077,#82078,#82079),
 .UNSPECIFIED.,.F.,.F.,(4,3,3,3,3,3,3,3,3,3,3,3,3,3,3,3,3,3,3,3,3,3,3,3,
3,3,3,3,3,3,3,3,3,3,3,3,3,3,3,3,3,3,3,3,3,3,3,3,3,3,3,3,3,3,3,3,3,3,3,3,
3,3,3,3,3,3,3,3,3,3,3,3,3,3,4),(889.07072096589,889.073348311646,889.157087023492,
889.24072253486,889.324274978258,889.407764414109,889.491218364723,889.574654858569,
889.658091968324,889.741547763242,889.825092255972,889.908681338913,889.99240460647,
890.073084322366,890.156823034212,890.240458545579,890.324010988978,890.407500424829,
890.490954375443,890.574390869289,890.657827979044,890.741283773962,890.824828266692,
890.908417349633,890.99214061719,891.072820333086,891.156559044932,891.240194556299,
891.323746999698,891.407236435548,891.490690386162,891.574126880008,891.657563989763,
891.741019784681,891.82456427741,891.908153360351,891.991876627909,892.072556343806,
892.156295055652,892.23993056702,892.323483010418,892.406972446269,892.490426396883,
892.57386289073,892.657300000485,892.740755795403,892.824300288133,892.907889371074,
892.991612638632,893.072292354527,893.156031066373,893.239666577741,893.323219021139,
893.40670845699,893.490162407604,893.573598901451,893.657036011206,893.740491806124,
893.824036298854,893.907625381795,893.991348649352,894.072028365247,894.155767077093,
894.23940258846,894.322955031859,894.40644446771,894.489898418323,894.573334912169,
894.656772021925,894.740227816842,894.823772309572,894.907361392512,894.99108466007,
895.071764375967,895.103030343709),.UNSPECIFIED.);
#616=B_SPLINE_CURVE_WITH_KNOTS('',3,(#82080,#82081,#82082,#82083,#82084,
#82085,#82086,#82087,#82088,#82089),.UNSPECIFIED.,.F.,.F.,(4,3,3,4),(888.81905987275,
888.902606816309,888.986663891048,889.070720965786),.UNSPECIFIED.);
#617=B_SPLINE_CURVE_WITH_KNOTS('',3,(#82091,#82092,#82093,#82094,#82095,
#82096,#82097,#82098,#82099,#82100),.UNSPECIFIED.,.F.,.F.,(4,3,3,4),(888.819680914903,
888.90277212709,888.986746546492,889.070720965894),.UNSPECIFIED.);
#618=B_SPLINE_CURVE_WITH_KNOTS('',3,(#82101,#82102,#82103,#82104,#82105,
#82106,#82107,#82108,#82109,#82110),.UNSPECIFIED.,.F.,.F.,(4,1,1,1,1,1,
1,4),(889.070727437116,889.383638931363,890.383374942083,891.383110952803,
892.382846963523,893.382582974243,894.382318984963,895.101947493761),
 .UNSPECIFIED.);
#619=B_SPLINE_CURVE_WITH_KNOTS('',3,(#82116,#82117,#82118,#82119,#82120,
#82121,#82122,#82123,#82124,#82125,#82126,#82127,#82128,#82129,#82130,#82131,
#82132,#82133,#82134,#82135,#82136,#82137,#82138,#82139,#82140,#82141,#82142,
#82143,#82144,#82145,#82146,#82147,#82148,#82149,#82150,#82151,#82152,#82153,
#82154,#82155,#82156,#82157,#82158,#82159,#82160,#82161,#82162,#82163,#82164,
#82165,#82166,#82167,#82168,#82169,#82170,#82171,#82172,#82173,#82174,#82175,
#82176,#82177,#82178,#82179,#82180,#82181,#82182,#82183,#82184,#82185,#82186,
#82187,#82188,#82189,#82190,#82191,#82192,#82193,#82194,#82195,#82196,#82197,
#82198,#82199,#82200,#82201,#82202,#82203,#82204,#82205,#82206,#82207,#82208,
#82209,#82210,#82211,#82212,#82213,#82214,#82215,#82216,#82217,#82218,#82219,
#82220,#82221,#82222,#82223,#82224,#82225,#82226,#82227,#82228,#82229,#82230,
#82231,#82232,#82233,#82234,#82235,#82236,#82237,#82238,#82239,#82240,#82241,
#82242,#82243,#82244,#82245,#82246,#82247,#82248,#82249,#82250,#82251,#82252,
#82253,#82254,#82255,#82256,#82257,#82258,#82259,#82260,#82261,#82262,#82263,
#82264,#82265,#82266,#82267,#82268,#82269,#82270,#82271,#82272,#82273,#82274,
#82275,#82276,#82277,#82278,#82279,#82280,#82281,#82282,#82283,#82284,#82285,
#82286,#82287,#82288,#82289,#82290,#82291,#82292,#82293,#82294,#82295,#82296,
#82297,#82298,#82299,#82300,#82301,#82302,#82303,#82304,#82305,#82306,#82307,
#82308,#82309,#82310,#82311,#82312,#82313,#82314,#82315,#82316,#82317,#82318,
#82319,#82320,#82321,#82322,#82323,#82324,#82325,#82326,#82327,#82328,#82329,
#82330,#82331,#82332,#82333,#82334,#82335),.UNSPECIFIED.,.F.,.F.,(4,3,3,
3,3,3,3,3,3,3,3,3,3,3,3,3,3,3,3,3,3,3,3,3,3,3,3,3,3,3,3,3,3,3,3,3,3,3,3,
3,3,3,3,3,3,3,3,3,3,3,3,3,3,3,3,3,3,3,3,3,3,3,3,3,3,3,3,3,3,3,3,3,3,4),
(895.353906273069,895.436705046304,895.519470690322,895.602221139555,895.684975042146,
895.767751045559,895.850616832775,895.933531325895,896.016572976593,896.071500386687,
896.155239098533,896.238874609901,896.322427053299,896.40591648915,896.489370439764,
896.57280693361,896.656244043365,896.739699838282,896.823244331012,896.906833413953,
896.99055668151,897.071236397407,897.154975109253,897.238610620621,897.322163064019,
897.40565249987,897.489106450484,897.57254294433,897.655980054085,897.739435849002,
897.822980341732,897.906569424673,897.99029269223,898.070972408127,898.154711119973,
898.23834663134,898.321899074739,898.40538851059,898.488842461203,898.57227895505,
898.655716064805,898.739171859722,898.822716352452,898.906305435393,898.990028702951,
899.070708418847,899.154447130693,899.23808264206,899.321635085459,899.40512452131,
899.488578471924,899.57201496577,899.655452075525,899.738907870443,899.822452363173,
899.906041446114,899.989764713671,900.070444429567,900.154183141413,900.237818652781,
900.321371096179,900.40486053203,900.488314482643,900.57175097649,900.655188086245,
900.738643881162,900.822188373892,900.905777456833,900.989500724391,901.070180440288,
901.155986680042,901.241683103162,901.327251411809,901.386599073372),
 .UNSPECIFIED.);
#620=B_SPLINE_CURVE_WITH_KNOTS('',3,(#82336,#82337,#82338,#82339,#82340,
#82341,#82342,#82343,#82344,#82345),.UNSPECIFIED.,.F.,.F.,(4,3,3,4),(895.103030343709,
895.207280880286,895.309982870308,895.353906272954),.UNSPECIFIED.);
#621=B_SPLINE_CURVE_WITH_KNOTS('',3,(#82347,#82348,#82349,#82350),
 .UNSPECIFIED.,.F.,.F.,(4,4),(895.101947493761,895.353906273073),
 .UNSPECIFIED.);
#622=B_SPLINE_CURVE_WITH_KNOTS('',3,(#82351,#82352,#82353,#82354,#82355,
#82356,#82357,#82358,#82359,#82360,#82361),.UNSPECIFIED.,.F.,.F.,(4,1,1,
1,1,1,1,1,4),(895.353906273073,895.382054995684,896.381791006404,897.381527017124,
898.381263027844,899.380999038564,900.380735049284,901.380471060004,901.386062069609),
 .UNSPECIFIED.);
#623=B_SPLINE_CURVE_WITH_KNOTS('',3,(#82367,#82368,#82369,#82370,#82371,
#82372,#82373,#82374,#82375,#82376,#82377,#82378,#82379,#82380,#82381,#82382,
#82383,#82384,#82385,#82386,#82387,#82388,#82389,#82390,#82391,#82392,#82393,
#82394,#82395,#82396,#82397,#82398,#82399,#82400,#82401,#82402,#82403,#82404,
#82405,#82406,#82407,#82408,#82409,#82410,#82411,#82412,#82413,#82414,#82415,
#82416,#82417,#82418,#82419,#82420,#82421,#82422,#82423,#82424,#82425,#82426,
#82427,#82428,#82429,#82430,#82431,#82432,#82433,#82434,#82435,#82436,#82437,
#82438,#82439,#82440,#82441,#82442,#82443,#82444,#82445,#82446,#82447,#82448,
#82449,#82450,#82451,#82452,#82453,#82454,#82455,#82456,#82457,#82458,#82459,
#82460,#82461,#82462,#82463,#82464,#82465,#82466,#82467,#82468,#82469,#82470,
#82471,#82472,#82473,#82474,#82475,#82476,#82477,#82478,#82479,#82480,#82481,
#82482,#82483,#82484,#82485,#82486,#82487,#82488,#82489,#82490,#82491,#82492,
#82493,#82494,#82495,#82496,#82497,#82498,#82499,#82500,#82501,#82502,#82503,
#82504,#82505,#82506,#82507,#82508,#82509,#82510,#82511,#82512,#82513,#82514,
#82515,#82516,#82517,#82518,#82519,#82520,#82521,#82522,#82523,#82524,#82525,
#82526,#82527,#82528,#82529,#82530,#82531,#82532,#82533,#82534,#82535,#82536,
#82537,#82538,#82539,#82540,#82541,#82542,#82543,#82544,#82545,#82546,#82547,
#82548,#82549,#82550,#82551,#82552,#82553,#82554,#82555,#82556,#82557,#82558,
#82559,#82560,#82561,#82562,#82563,#82564,#82565,#82566,#82567,#82568,#82569,
#82570,#82571,#82572,#82573,#82574,#82575,#82576,#82577,#82578,#82579,#82580,
#82581,#82582,#82583,#82584,#82585,#82586),.UNSPECIFIED.,.F.,.F.,(4,3,3,
3,3,3,3,3,3,3,3,3,3,3,3,3,3,3,3,3,3,3,3,3,3,3,3,3,3,3,3,3,3,3,3,3,3,3,3,
3,3,3,3,3,3,3,3,3,3,3,3,3,3,3,3,3,3,3,3,3,3,3,3,3,3,3,3,3,3,3,3,3,3,4),
(901.637091580384,901.727374617521,901.818032209178,901.908878920106,902.000023922038,
902.069916451008,902.153655162854,902.237290674222,902.32084311762,902.404332553471,
902.487786504085,902.571222997931,902.654660107686,902.738115902604,902.821660395334,
902.905249478275,902.988972745832,903.069652461728,903.153391173574,903.237026684941,
903.32057912834,903.404068564191,903.487522514805,903.570959008651,903.654396118406,
903.737851913324,903.821396406054,903.904985488995,903.988708756552,904.069388472448,
904.153127184294,904.236762695661,904.32031513906,904.403804574911,904.487258525524,
904.570695019371,904.654132129126,904.737587924044,904.821132416773,904.904721499714,
904.988444767272,905.069124483168,905.152863195014,905.236498706382,905.32005114978,
905.403540585631,905.486994536245,905.570431030091,905.653868139847,905.737323934764,
905.820868427494,905.904457510435,905.988180777993,906.068860493888,906.152599205734,
906.236234717101,906.3197871605,906.403276596351,906.486730546965,906.570167040811,
906.653604150566,906.737059945484,906.820604438213,906.904193521154,906.987916788712,
907.068596504608,907.151084096677,907.233476717466,907.315793573918,907.398053799997,
907.480282004625,907.562492286284,907.644717656506,907.668518267423),
 .UNSPECIFIED.);
#624=B_SPLINE_CURVE_WITH_KNOTS('',3,(#82587,#82588,#82589,#82590,#82591,
#82592,#82593,#82594,#82595,#82596),.UNSPECIFIED.,.F.,.F.,(4,3,3,4),(901.386599073372,
901.4720213908,901.557375230074,901.637091580249),.UNSPECIFIED.);
#625=B_SPLINE_CURVE_WITH_KNOTS('',3,(#82598,#82599,#82600,#82601),
 .UNSPECIFIED.,.F.,.F.,(4,4),(901.386062069609,901.637089254157),
 .UNSPECIFIED.);
#626=B_SPLINE_CURVE_WITH_KNOTS('',3,(#82602,#82603,#82604,#82605,#82606,
#82607,#82608,#82609,#82610,#82611,#82612,#82613,#82614,#82615,#82616,#82617,
#82618,#82619,#82620,#82621,#82622,#82623,#82624,#82625,#82626,#82627,#82628,
#82629,#82630,#82631,#82632,#82633,#82634,#82635,#82636,#82637,#82638,#82639,
#82640,#82641,#82642,#82643,#82644,#82645,#82646,#82647,#82648,#82649,#82650,
#82651,#82652,#82653,#82654,#82655,#82656,#82657,#82658,#82659,#82660,#82661,
#82662,#82663,#82664,#82665,#82666,#82667,#82668,#82669,#82670,#82671,#82672,
#82673,#82674,#82675,#82676,#82677,#82678,#82679,#82680,#82681,#82682,#82683,
#82684,#82685,#82686,#82687,#82688,#82689,#82690,#82691,#82692,#82693,#82694,
#82695,#82696,#82697,#82698,#82699,#82700,#82701,#82702,#82703,#82704,#82705,
#82706,#82707,#82708,#82709,#82710,#82711,#82712,#82713,#82714,#82715,#82716,
#82717,#82718,#82719,#82720,#82721,#82722,#82723,#82724,#82725,#82726,#82727,
#82728,#82729,#82730,#82731,#82732,#82733,#82734,#82735,#82736,#82737,#82738,
#82739,#82740,#82741,#82742,#82743,#82744,#82745,#82746,#82747,#82748,#82749,
#82750,#82751,#82752,#82753,#82754,#82755,#82756,#82757,#82758,#82759,#82760,
#82761,#82762,#82763,#82764,#82765,#82766,#82767,#82768,#82769,#82770,#82771,
#82772,#82773,#82774,#82775,#82776,#82777,#82778,#82779,#82780,#82781,#82782,
#82783,#82784,#82785,#82786,#82787,#82788,#82789,#82790,#82791,#82792,#82793,
#82794,#82795,#82796,#82797,#82798,#82799,#82800,#82801,#82802,#82803,#82804,
#82805,#82806,#82807,#82808,#82809,#82810,#82811,#82812,#82813,#82814,#82815,
#82816,#82817,#82818,#82819,#82820,#82821),.UNSPECIFIED.,.F.,.F.,(4,3,3,
3,3,3,3,3,3,3,3,3,3,3,3,3,3,3,3,3,3,3,3,3,3,3,3,3,3,3,3,3,3,3,3,3,3,3,3,
3,3,3,3,3,3,3,3,3,3,3,3,3,3,3,3,3,3,3,3,3,3,3,3,3,3,3,3,3,3,3,3,3,3,4),
(901.637091580253,901.719694961594,901.802258975235,901.884792597306,901.967321346146,
902.049864037226,902.132490934378,902.215159553066,902.297961533055,902.380207070725,
902.463945782571,902.547581293938,902.631133737337,902.714623173188,902.798077123801,
902.881513617648,902.964950727403,903.048406522321,903.131951015051,903.215540097991,
903.299263365549,903.379943081445,903.463681793291,903.547317304658,903.630869748057,
903.714359183908,903.797813134521,903.881249628368,903.964686738123,904.04814253304,
904.13168702577,904.215276108711,904.298999376268,904.379679092165,904.463417804011,
904.547053315379,904.630605758777,904.714095194628,904.797549145242,904.880985639088,
904.964422748844,905.047878543761,905.131423036491,905.215012119432,905.29873538699,
905.379415102885,905.463153814731,905.546789326099,905.630341769497,905.713831205348,
905.797285155962,905.880721649808,905.964158759564,906.047614554481,906.131159047211,
906.214748130152,906.298471397709,906.379151113605,906.462889825451,906.546525336818,
906.630077780216,906.713567216068,906.797021166681,906.880457660527,906.963894770283,
907.047350565201,907.130895057931,907.214484140871,907.298207408429,907.378887124325,
907.465459567995,907.551914783059,907.638231267352,907.669863191904),
 .UNSPECIFIED.);
#627=B_SPLINE_CURVE_WITH_KNOTS('',3,(#82827,#82828,#82829,#82830,#82831,
#82832,#82833,#82834,#82835,#82836,#82837,#82838,#82839,#82840,#82841,#82842,
#82843,#82844,#82845,#82846,#82847,#82848,#82849,#82850,#82851,#82852,#82853,
#82854,#82855,#82856,#82857,#82858,#82859,#82860,#82861,#82862,#82863,#82864,
#82865,#82866,#82867,#82868,#82869,#82870,#82871,#82872,#82873,#82874,#82875,
#82876,#82877,#82878,#82879,#82880,#82881,#82882,#82883,#82884,#82885,#82886,
#82887,#82888,#82889,#82890,#82891,#82892,#82893,#82894,#82895,#82896,#82897,
#82898,#82899,#82900,#82901,#82902,#82903,#82904,#82905,#82906,#82907,#82908,
#82909,#82910,#82911,#82912,#82913,#82914,#82915,#82916,#82917,#82918,#82919,
#82920,#82921,#82922,#82923,#82924,#82925,#82926,#82927,#82928,#82929,#82930,
#82931,#82932,#82933,#82934,#82935,#82936,#82937,#82938,#82939,#82940,#82941,
#82942,#82943,#82944,#82945,#82946,#82947,#82948,#82949,#82950,#82951,#82952,
#82953,#82954,#82955,#82956,#82957,#82958,#82959,#82960,#82961,#82962,#82963,
#82964,#82965,#82966,#82967,#82968,#82969,#82970,#82971,#82972,#82973,#82974,
#82975,#82976,#82977,#82978,#82979,#82980,#82981,#82982,#82983,#82984,#82985,
#82986,#82987,#82988,#82989,#82990,#82991,#82992,#82993,#82994,#82995,#82996,
#82997,#82998,#82999,#83000,#83001,#83002,#83003,#83004,#83005,#83006,#83007,
#83008,#83009,#83010,#83011,#83012,#83013,#83014,#83015,#83016,#83017,#83018,
#83019,#83020,#83021,#83022,#83023,#83024,#83025,#83026,#83027,#83028,#83029,
#83030,#83031,#83032,#83033,#83034,#83035,#83036,#83037,#83038,#83039,#83040,
#83041,#83042,#83043),.UNSPECIFIED.,.F.,.F.,(4,3,3,3,3,3,3,3,3,3,3,3,3,
3,3,3,3,3,3,3,3,3,3,3,3,3,3,3,3,3,3,3,3,3,3,3,3,3,3,3,3,3,3,3,3,3,3,3,3,
3,3,3,3,3,3,3,3,3,3,3,3,3,3,3,3,3,3,3,3,3,3,3,4),(907.920276887428,908.068332515329,
908.152071227175,908.235706738542,908.319259181941,908.402748617792,908.486202568405,
908.569639062252,908.653076172007,908.736531966925,908.820076459654,908.903665542595,
908.987388810152,909.068068526049,909.151807237895,909.235442749263,909.318995192661,
909.402484628512,909.485938579126,909.569375072972,909.652812182727,909.736267977645,
909.819812470374,909.903401553315,909.987124820873,910.067804536769,910.151543248615,
910.235178759982,910.318731203381,910.402220639232,910.485674589845,910.569111083692,
910.652548193447,910.736003988365,910.819548481094,910.903137564035,910.986860831593,
911.067540547489,911.151279259335,911.234914770703,911.318467214101,911.401956649952,
911.485410600566,911.568847094412,911.652284204167,911.735739999085,911.819284491815,
911.902873574756,911.986596842313,912.067276558209,912.151015270055,912.234650781422,
912.318203224821,912.401692660672,912.485146611285,912.568583105132,912.652020214887,
912.735476009805,912.819020502534,912.902609585475,912.986332853033,913.067012568929,
913.150758006077,913.234398727867,913.317954873295,913.401441674311,913.484890787398,
913.568320301205,913.651748287339,913.735227233515,913.818733664062,913.902329818043,
913.951907679941),.UNSPECIFIED.);
#628=B_SPLINE_CURVE_WITH_KNOTS('',3,(#83044,#83045,#83046,#83047,#83048,
#83049,#83050,#83051,#83052,#83053),.UNSPECIFIED.,.F.,.F.,(4,3,3,4),(907.668518267423,
907.750806452033,907.835541669673,907.920276887313),.UNSPECIFIED.);
#629=B_SPLINE_CURVE_WITH_KNOTS('',3,(#83055,#83056,#83057,#83058,#83059,
#83060,#83061,#83062,#83063,#83064),.UNSPECIFIED.,.F.,.F.,(4,3,3,4),(907.669863191904,
907.756026872551,907.842091388467,907.920276887432),.UNSPECIFIED.);
#630=B_SPLINE_CURVE_WITH_KNOTS('',3,(#83065,#83066,#83067,#83068,#83069,
#83070,#83071,#83072,#83073,#83074,#83075,#83076,#83077,#83078,#83079,#83080,
#83081,#83082,#83083,#83084,#83085,#83086,#83087,#83088,#83089,#83090,#83091,
#83092,#83093,#83094,#83095,#83096,#83097,#83098,#83099,#83100,#83101,#83102,
#83103,#83104,#83105,#83106,#83107,#83108,#83109,#83110,#83111,#83112,#83113,
#83114,#83115,#83116,#83117,#83118,#83119,#83120,#83121,#83122,#83123,#83124,
#83125,#83126,#83127,#83128,#83129,#83130,#83131,#83132,#83133,#83134,#83135,
#83136,#83137,#83138,#83139,#83140,#83141,#83142,#83143,#83144,#83145,#83146,
#83147,#83148,#83149,#83150,#83151,#83152,#83153,#83154,#83155,#83156,#83157,
#83158,#83159,#83160,#83161,#83162,#83163,#83164,#83165,#83166,#83167,#83168,
#83169,#83170,#83171,#83172,#83173,#83174,#83175,#83176,#83177,#83178,#83179,
#83180,#83181,#83182,#83183,#83184,#83185,#83186,#83187,#83188,#83189,#83190,
#83191,#83192,#83193,#83194,#83195,#83196,#83197,#83198,#83199,#83200,#83201,
#83202,#83203,#83204,#83205,#83206,#83207,#83208,#83209,#83210,#83211,#83212,
#83213,#83214,#83215,#83216,#83217,#83218,#83219,#83220,#83221,#83222,#83223,
#83224,#83225,#83226,#83227,#83228,#83229,#83230,#83231,#83232,#83233,#83234,
#83235,#83236,#83237,#83238,#83239,#83240,#83241,#83242,#83243,#83244,#83245,
#83246,#83247,#83248,#83249,#83250,#83251,#83252,#83253,#83254,#83255,#83256,
#83257,#83258,#83259,#83260,#83261,#83262,#83263,#83264,#83265,#83266,#83267,
#83268,#83269,#83270,#83271,#83272,#83273,#83274,#83275,#83276,#83277,#83278,
#83279,#83280,#83281),.UNSPECIFIED.,.F.,.F.,(4,3,3,3,3,3,3,3,3,3,3,3,3,
3,3,3,3,3,3,3,3,3,3,3,3,3,3,3,3,3,3,3,3,3,3,3,3,3,3,3,3,3,3,3,3,3,3,3,3,
3,3,3,3,3,3,3,3,3,3,3,3,3,3,3,3,3,3,3,3,3,3,3,4),(907.920276887616,908.009350353477,
908.101668548869,908.191201216186,908.284912175615,908.378623135045,908.462361846891,
908.545997358259,908.629549801657,908.713039237508,908.796493188122,908.879929681968,
908.963366791724,909.046822586642,909.130367079371,909.213956162312,909.29767942987,
909.378359145765,909.462097857611,909.545733368978,909.629285812377,909.712775248228,
909.796229198842,909.879665692688,909.963102802443,910.046558597361,910.130103090091,
910.213692173032,910.297415440589,910.378095156486,910.461833868332,910.5454693797,
910.629021823098,910.712511258949,910.795965209563,910.879401703409,910.962838813165,
911.046294608083,911.129839100812,911.213428183753,911.297151451311,911.377831167206,
911.461569879052,911.545205390419,911.628757833818,911.712247269669,911.795701220282,
911.879137714129,911.962574823884,912.046030618802,912.129575111531,912.213164194472,
912.29688746203,912.377567177926,912.461305889772,912.54494140114,912.628493844538,
912.711983280389,912.795437231003,912.878873724849,912.962310834605,913.045766629522,
913.129311122252,913.212900205193,913.296623472751,913.377303188646,913.459775106865,
913.542151599702,913.624451888579,913.706695524716,913.788904051849,913.871118218614,
913.951777480369),.UNSPECIFIED.);
#631=B_SPLINE_CURVE_WITH_KNOTS('',3,(#83287,#83288,#83289,#83290,#83291,
#83292,#83293,#83294,#83295,#83296,#83297,#83298,#83299,#83300,#83301,#83302,
#83303,#83304,#83305,#83306,#83307,#83308,#83309,#83310,#83311,#83312,#83313,
#83314,#83315,#83316,#83317,#83318,#83319,#83320,#83321,#83322,#83323,#83324,
#83325,#83326,#83327,#83328,#83329,#83330,#83331,#83332,#83333,#83334,#83335,
#83336,#83337,#83338,#83339,#83340,#83341,#83342,#83343,#83344,#83345,#83346,
#83347,#83348,#83349,#83350,#83351,#83352,#83353,#83354,#83355,#83356,#83357,
#83358,#83359,#83360,#83361,#83362,#83363,#83364,#83365,#83366,#83367,#83368,
#83369,#83370,#83371,#83372,#83373,#83374,#83375,#83376,#83377,#83378,#83379,
#83380,#83381,#83382,#83383,#83384,#83385,#83386,#83387,#83388,#83389,#83390,
#83391,#83392,#83393,#83394,#83395,#83396,#83397,#83398,#83399,#83400,#83401,
#83402,#83403,#83404,#83405,#83406,#83407,#83408,#83409,#83410,#83411,#83412,
#83413,#83414,#83415,#83416,#83417,#83418,#83419,#83420,#83421,#83422,#83423,
#83424,#83425,#83426,#83427,#83428,#83429,#83430,#83431,#83432,#83433,#83434,
#83435,#83436,#83437,#83438,#83439,#83440,#83441,#83442,#83443,#83444,#83445,
#83446,#83447,#83448,#83449,#83450,#83451,#83452,#83453,#83454,#83455,#83456,
#83457,#83458,#83459,#83460,#83461,#83462,#83463,#83464,#83465,#83466,#83467,
#83468,#83469,#83470,#83471,#83472,#83473,#83474,#83475,#83476,#83477,#83478,
#83479,#83480,#83481,#83482,#83483,#83484,#83485,#83486,#83487,#83488,#83489,
#83490,#83491,#83492,#83493,#83494,#83495,#83496,#83497,#83498,#83499,#83500,
#83501,#83502,#83503,#83504,#83505,#83506),.UNSPECIFIED.,.F.,.F.,(4,3,3,
3,3,3,3,3,3,3,3,3,3,3,3,3,3,3,3,3,3,3,3,3,3,3,3,3,3,3,3,3,3,3,3,3,3,3,3,
3,3,3,3,3,3,3,3,3,3,3,3,3,3,3,3,3,3,3,3,3,3,3,3,3,3,3,3,3,3,3,3,3,3,4),
(914.203462194732,914.2859095674,914.368271757229,914.450569893832,914.532832019811,
914.615077615304,914.697325689258,914.779595250459,914.861951217647,914.944356078256,
915.026880542678,915.066484590369,915.150223302215,915.233858813583,915.317411256982,
915.400900692834,915.484354643448,915.567791137294,915.65122824705,915.734684041968,
915.818228534698,915.901817617639,915.985540885197,916.06622060109,916.149959312936,
916.233594824304,916.317147267702,916.400636703553,916.484090654167,916.567527148013,
916.650964257769,916.734420052686,916.817964545416,916.901553628357,916.985276895914,
917.06595661181,917.149695323656,917.233330835023,917.316883278422,917.400372714273,
917.483826664886,917.567263158732,917.650700268488,917.734156063405,917.817700556135,
917.901289639076,917.985012906633,918.06569262253,918.149431334376,918.233066845744,
918.316619289142,918.400108724993,918.483562675607,918.566999169453,918.650436279208,
918.733892074126,918.817436566856,918.901025649797,918.984748917355,919.06542863325,
919.149167345096,919.232802856463,919.316355299862,919.399844735712,919.483298686326,
919.566735180172,919.650172289927,919.733628084845,919.817172577575,919.900761660516,
919.984484928073,920.06516464397,920.156938440952,920.236315776265),
 .UNSPECIFIED.);
#632=B_SPLINE_CURVE_WITH_KNOTS('',3,(#83507,#83508,#83509,#83510,#83511,
#83512,#83513,#83514,#83515,#83516),.UNSPECIFIED.,.F.,.F.,(4,3,3,4),(913.951907679941,
914.035651074648,914.066748579649,914.203462194608),.UNSPECIFIED.);
#633=B_SPLINE_CURVE_WITH_KNOTS('',3,(#83518,#83519,#83520,#83521,#83522,
#83523,#83524,#83525,#83526,#83527),.UNSPECIFIED.,.F.,.F.,(4,3,3,4),(913.951777480369,
914.034031901732,914.118747048086,914.203462194439),.UNSPECIFIED.);
#634=B_SPLINE_CURVE_WITH_KNOTS('',3,(#83528,#83529,#83530,#83531,#83532,
#83533,#83534,#83535,#83536,#83537,#83538,#83539,#83540,#83541,#83542,#83543,
#83544,#83545,#83546,#83547,#83548,#83549,#83550,#83551,#83552,#83553,#83554,
#83555,#83556,#83557,#83558,#83559,#83560,#83561,#83562,#83563,#83564,#83565,
#83566,#83567,#83568,#83569,#83570,#83571,#83572,#83573,#83574,#83575,#83576,
#83577,#83578,#83579,#83580,#83581,#83582,#83583,#83584,#83585,#83586,#83587,
#83588,#83589,#83590,#83591,#83592,#83593,#83594,#83595,#83596,#83597,#83598,
#83599,#83600,#83601,#83602,#83603,#83604,#83605,#83606,#83607,#83608,#83609,
#83610,#83611,#83612,#83613,#83614,#83615,#83616,#83617,#83618,#83619,#83620,
#83621,#83622,#83623,#83624,#83625,#83626,#83627,#83628,#83629,#83630,#83631,
#83632,#83633,#83634,#83635,#83636,#83637,#83638,#83639,#83640,#83641,#83642,
#83643,#83644,#83645,#83646,#83647,#83648,#83649,#83650,#83651,#83652,#83653,
#83654,#83655,#83656,#83657,#83658,#83659,#83660,#83661,#83662,#83663,#83664,
#83665,#83666,#83667,#83668,#83669,#83670,#83671,#83672,#83673,#83674,#83675,
#83676,#83677,#83678,#83679,#83680,#83681,#83682,#83683,#83684,#83685,#83686,
#83687,#83688,#83689,#83690,#83691,#83692,#83693,#83694,#83695,#83696,#83697,
#83698,#83699,#83700,#83701,#83702,#83703,#83704,#83705,#83706,#83707,#83708,
#83709,#83710,#83711,#83712,#83713,#83714,#83715,#83716,#83717,#83718,#83719,
#83720,#83721,#83722,#83723,#83724,#83725,#83726,#83727,#83728,#83729,#83730,
#83731,#83732,#83733,#83734,#83735,#83736,#83737,#83738,#83739,#83740,#83741,
#83742,#83743,#83744,#83745,#83746,#83747),.UNSPECIFIED.,.F.,.F.,(4,3,3,
3,3,3,3,3,3,3,3,3,3,3,3,3,3,3,3,3,3,3,3,3,3,3,3,3,3,3,3,3,3,3,3,3,3,3,3,
3,3,3,3,3,3,3,3,3,3,3,3,3,3,3,3,3,3,3,3,3,3,3,3,3,3,3,3,3,3,3,3,3,3,4),
(914.203462194612,914.333356253278,914.377039199366,914.460777911212,914.54441342258,
914.627965865979,914.71145530183,914.794909252444,914.87834574629,914.961782856046,
915.045238650964,915.128783143694,915.212372226635,915.296095494193,915.376775210086,
915.460513921932,915.544149433299,915.627701876698,915.711191312549,915.794645263162,
915.878081757009,915.961518866764,916.044974661682,916.128519154411,916.212108237352,
916.29583150491,916.376511220806,916.460249932652,916.543885444019,916.627437887418,
916.710927323269,916.794381273882,916.877817767729,916.961254877484,917.044710672402,
917.128255165131,917.211844248072,917.29556751563,917.376247231526,917.459985943372,
917.54362145474,917.627173898138,917.71066333399,917.794117284604,917.87755377845,
917.960990888206,918.044446683124,918.127991175853,918.211580258794,918.295303526352,
918.375983242247,918.459721954093,918.543357465461,918.626909908859,918.71039934471,
918.793853295324,918.87728978917,918.960726898926,919.044182693843,919.127727186573,
919.211316269514,919.295039537072,919.375719252967,919.459466267946,919.543108230139,
919.629599690776,919.713084564985,919.796531909885,919.879959813621,919.963386347286,
920.04685897325,920.130359459133,920.21393724819,920.235039915232),
 .UNSPECIFIED.);
#635=B_SPLINE_CURVE_WITH_KNOTS('',3,(#83753,#83754,#83755,#83756,#83757,
#83758,#83759,#83760,#83761,#83762,#83763,#83764,#83765,#83766,#83767,#83768,
#83769,#83770,#83771,#83772,#83773,#83774,#83775,#83776,#83777,#83778,#83779,
#83780,#83781,#83782,#83783,#83784,#83785,#83786,#83787,#83788,#83789,#83790,
#83791,#83792,#83793,#83794,#83795,#83796,#83797,#83798,#83799,#83800,#83801,
#83802,#83803,#83804,#83805,#83806,#83807,#83808,#83809,#83810,#83811,#83812,
#83813,#83814,#83815,#83816,#83817,#83818,#83819,#83820,#83821,#83822,#83823,
#83824,#83825,#83826,#83827,#83828,#83829,#83830,#83831,#83832,#83833,#83834,
#83835,#83836,#83837,#83838,#83839,#83840,#83841,#83842,#83843,#83844,#83845,
#83846,#83847,#83848,#83849,#83850,#83851,#83852,#83853,#83854,#83855,#83856,
#83857,#83858,#83859,#83860,#83861,#83862,#83863,#83864,#83865,#83866,#83867,
#83868,#83869,#83870,#83871,#83872,#83873,#83874,#83875,#83876,#83877,#83878,
#83879,#83880,#83881,#83882,#83883,#83884,#83885,#83886,#83887,#83888,#83889,
#83890,#83891,#83892,#83893,#83894,#83895,#83896,#83897,#83898,#83899,#83900,
#83901,#83902,#83903,#83904,#83905,#83906,#83907,#83908,#83909,#83910,#83911,
#83912,#83913,#83914,#83915,#83916,#83917,#83918,#83919,#83920,#83921,#83922,
#83923,#83924,#83925,#83926,#83927,#83928,#83929,#83930,#83931,#83932,#83933,
#83934,#83935,#83936,#83937,#83938,#83939,#83940,#83941,#83942,#83943,#83944,
#83945,#83946,#83947,#83948,#83949,#83950,#83951,#83952,#83953,#83954,#83955,
#83956,#83957,#83958,#83959,#83960,#83961,#83962,#83963,#83964,#83965,#83966,
#83967,#83968,#83969,#83970,#83971,#83972),.UNSPECIFIED.,.F.,.F.,(4,3,3,
3,3,3,3,3,3,3,3,3,3,3,3,3,3,3,3,3,3,3,3,3,3,3,3,3,3,3,3,3,3,3,3,3,3,3,3,
3,3,3,3,3,3,3,3,3,3,3,3,3,3,3,3,3,3,3,3,3,3,3,3,3,3,3,3,3,3,3,3,3,3,4),
(920.486647501788,920.571704372344,920.656798324641,920.741944767653,920.827221421023,
920.912567136802,920.998070557921,921.06490065469,921.148639366536,921.232274877904,
921.315827321302,921.399316757153,921.482770707767,921.566207201614,921.649644311369,
921.733100106287,921.816644599017,921.900233681958,921.983956949516,922.06463666541,
922.148375377256,922.232010888624,922.315563332023,922.399052767874,922.482506718488,
922.565943212334,922.64938032209,922.732836117008,922.816380609738,922.899969692679,
922.983692960237,923.064372676131,923.148111387977,923.231746899345,923.315299342743,
923.398788778594,923.482242729208,923.565679223054,923.649116332809,923.732572127726,
923.816116620456,923.899705703397,923.983428970955,924.064108686851,924.147847398697,
924.231482910064,924.315035353463,924.398524789314,924.481978739928,924.565415233774,
924.648852343529,924.732308138447,924.815852631176,924.899441714117,924.983164981675,
925.063844697571,925.147583409417,925.231218920785,925.314771364184,925.398260800035,
925.481714750648,925.565151244495,925.64858835425,925.732044149168,925.815588641898,
925.899177724839,925.982900992397,926.063580708291,926.14675553624,926.229829073602,
926.31280410445,926.395722260427,926.478600793687,926.518691253405),
 .UNSPECIFIED.);
#636=B_SPLINE_CURVE_WITH_KNOTS('',3,(#83973,#83974,#83975,#83976,#83977,
#83978,#83979,#83980,#83981,#83982),.UNSPECIFIED.,.F.,.F.,(4,3,3,4),(920.236315776265,
920.327641113218,920.418611342316,920.486647501632),.UNSPECIFIED.);
#637=B_SPLINE_CURVE_WITH_KNOTS('',3,(#83984,#83985,#83986,#83987,#83988,
#83989,#83990,#83991,#83992,#83993),.UNSPECIFIED.,.F.,.F.,(4,3,3,4),(920.235039915232,
920.318772047392,920.375455263687,920.486647501791),.UNSPECIFIED.);
#638=B_SPLINE_CURVE_WITH_KNOTS('',3,(#83994,#83995,#83996,#83997,#83998,
#83999,#84000,#84001,#84002,#84003,#84004,#84005,#84006,#84007,#84008,#84009,
#84010,#84011,#84012,#84013,#84014,#84015,#84016,#84017,#84018,#84019,#84020,
#84021,#84022,#84023,#84024,#84025,#84026,#84027,#84028,#84029,#84030,#84031,
#84032,#84033,#84034,#84035,#84036,#84037,#84038,#84039,#84040,#84041,#84042,
#84043,#84044,#84045,#84046,#84047,#84048,#84049,#84050,#84051,#84052,#84053,
#84054,#84055,#84056,#84057,#84058,#84059,#84060,#84061,#84062,#84063,#84064,
#84065,#84066,#84067,#84068,#84069,#84070,#84071,#84072,#84073,#84074,#84075,
#84076,#84077,#84078,#84079,#84080,#84081,#84082,#84083,#84084,#84085,#84086,
#84087,#84088,#84089,#84090,#84091,#84092,#84093,#84094,#84095,#84096,#84097,
#84098,#84099,#84100,#84101,#84102,#84103,#84104,#84105,#84106,#84107,#84108,
#84109,#84110,#84111,#84112,#84113,#84114,#84115,#84116,#84117,#84118,#84119,
#84120,#84121,#84122,#84123,#84124,#84125,#84126,#84127,#84128,#84129,#84130,
#84131,#84132,#84133,#84134,#84135,#84136,#84137,#84138,#84139,#84140,#84141,
#84142,#84143,#84144,#84145,#84146,#84147,#84148,#84149,#84150,#84151,#84152,
#84153,#84154,#84155,#84156,#84157,#84158,#84159,#84160,#84161,#84162,#84163,
#84164,#84165,#84166,#84167,#84168,#84169,#84170,#84171,#84172,#84173,#84174,
#84175,#84176,#84177,#84178,#84179,#84180,#84181,#84182,#84183,#84184,#84185,
#84186,#84187,#84188,#84189,#84190,#84191,#84192,#84193,#84194,#84195,#84196,
#84197,#84198,#84199,#84200,#84201,#84202,#84203,#84204,#84205,#84206,#84207,
#84208,#84209,#84210,#84211,#84212,#84213),.UNSPECIFIED.,.F.,.F.,(4,3,3,
3,3,3,3,3,3,3,3,3,3,3,3,3,3,3,3,3,3,3,3,3,3,3,3,3,3,3,3,3,3,3,3,3,3,3,3,
3,3,3,3,3,3,3,3,3,3,3,3,3,3,3,3,3,3,3,3,3,3,3,3,3,3,3,3,3,3,3,3,3,3,4),
(920.486647501927,920.569217400438,920.651696775787,920.73410670892,920.816473497108,
920.89881878342,920.981161518928,921.063520650256,921.145963985295,921.228451518121,
921.311065716616,921.375191274407,921.458929986253,921.54256549762,921.626117941019,
921.70960737687,921.793061327484,921.87649782133,921.959934931086,922.043390726003,
922.126935218733,922.210524301674,922.294247569232,922.374927285127,922.458665996973,
922.542301508341,922.625853951739,922.70934338759,922.792797338203,922.87623383205,
922.959670941805,923.043126736722,923.126671229452,923.210260312393,923.293983579951,
923.374663295847,923.458402007693,923.54203751906,923.625589962459,923.70907939831,
923.792533348923,923.875969842769,923.959406952524,924.042862747442,924.126407240172,
924.209996323113,924.29371959067,924.374399306567,924.458138018413,924.541773529781,
924.62532597318,924.708815409031,924.792269359644,924.875705853491,924.959142963247,
925.042598758165,925.126143250895,925.209732333836,925.293455601394,925.374135317288,
925.457874029134,925.541509540502,925.6250619839,925.708551419751,925.792005370365,
925.875441864211,925.958878973966,926.042334768884,926.125879261614,926.209468344555,
926.293191612113,926.373871328008,926.467276920671,926.519450178445),
 .UNSPECIFIED.);
#639=B_SPLINE_CURVE_WITH_KNOTS('',3,(#84219,#84220,#84221,#84222,#84223,
#84224,#84225,#84226,#84227,#84228,#84229,#84230,#84231,#84232,#84233,#84234,
#84235,#84236,#84237,#84238,#84239,#84240,#84241,#84242,#84243,#84244,#84245,
#84246,#84247,#84248,#84249,#84250,#84251,#84252,#84253,#84254,#84255,#84256,
#84257,#84258,#84259,#84260,#84261,#84262,#84263,#84264,#84265,#84266,#84267,
#84268,#84269,#84270,#84271,#84272,#84273,#84274,#84275,#84276,#84277,#84278,
#84279,#84280,#84281,#84282,#84283,#84284,#84285,#84286,#84287,#84288,#84289,
#84290,#84291,#84292,#84293,#84294,#84295,#84296,#84297,#84298,#84299,#84300,
#84301,#84302,#84303,#84304,#84305,#84306,#84307,#84308,#84309,#84310,#84311,
#84312,#84313,#84314,#84315,#84316,#84317,#84318,#84319,#84320,#84321,#84322,
#84323,#84324,#84325,#84326,#84327,#84328,#84329,#84330,#84331,#84332,#84333,
#84334,#84335,#84336,#84337,#84338,#84339,#84340,#84341,#84342,#84343,#84344,
#84345,#84346,#84347,#84348,#84349,#84350,#84351,#84352,#84353,#84354,#84355,
#84356,#84357,#84358,#84359,#84360,#84361,#84362,#84363,#84364,#84365,#84366,
#84367,#84368,#84369,#84370,#84371,#84372,#84373,#84374,#84375,#84376,#84377,
#84378,#84379,#84380,#84381,#84382,#84383,#84384,#84385,#84386,#84387,#84388,
#84389,#84390,#84391,#84392,#84393,#84394,#84395,#84396,#84397,#84398,#84399,
#84400,#84401,#84402,#84403,#84404,#84405,#84406,#84407,#84408,#84409,#84410,
#84411,#84412,#84413,#84414,#84415,#84416,#84417,#84418,#84419,#84420,#84421,
#84422,#84423,#84424,#84425,#84426,#84427,#84428,#84429,#84430,#84431,#84432,
#84433,#84434,#84435),.UNSPECIFIED.,.F.,.F.,(4,3,3,3,3,3,3,3,3,3,3,3,3,
3,3,3,3,3,3,3,3,3,3,3,3,3,3,3,3,3,3,3,3,3,3,3,3,3,3,3,3,3,3,3,3,3,3,3,3,
3,3,3,3,3,3,3,3,3,3,3,3,3,3,3,3,3,3,3,3,3,3,3,4),(926.769832809103,926.871123756702,
926.973836758034,927.063316719011,927.147055430857,927.230690942225,927.314243385623,
927.397732821475,927.481186772088,927.564623265935,927.64806037569,927.731516170608,
927.815060663338,927.898649746279,927.982373013837,928.063052729731,928.146791441577,
928.230426952944,928.313979396343,928.397468832194,928.480922782807,928.564359276653,
928.647796386409,928.731252181327,928.814796674056,928.898385756997,928.982109024555,
929.062788740451,929.146527452297,929.230162963664,929.313715407063,929.397204842914,
929.480658793528,929.564095287374,929.647532397129,929.730988192047,929.814532684777,
929.898121767718,929.981845035275,930.062524751171,930.146263463017,930.229898974385,
930.313451417783,930.396940853634,930.480394804248,930.563831298094,930.647268407849,
930.730724202767,930.814268695497,930.897857778438,930.981581045995,931.062260761891,
931.145999473737,931.229634985105,931.313187428503,931.396676864354,931.480130814968,
931.563567308814,931.64700441857,931.730460213488,931.814004706217,931.897593789159,
931.981317056716,932.061996772612,932.145621946421,932.229114763035,932.312531192385,
932.395889522913,932.479207999135,932.562522639417,932.645831934757,932.729189513781,
932.8013317429),.UNSPECIFIED.);
#640=B_SPLINE_CURVE_WITH_KNOTS('',3,(#84436,#84437,#84438,#84439,#84440,
#84441,#84442,#84443,#84444,#84445),.UNSPECIFIED.,.F.,.F.,(4,3,3,4),(926.518691253405,
926.601556301005,926.685694554986,926.769832808967),.UNSPECIFIED.);
#641=B_SPLINE_CURVE_WITH_KNOTS('',3,(#84447,#84448,#84449,#84450,#84451,
#84452,#84453,#84454,#84455,#84456),.UNSPECIFIED.,.F.,.F.,(4,3,3,4),(926.519450178445,
926.612369002246,926.704833054526,926.769832808789),.UNSPECIFIED.);
#642=B_SPLINE_CURVE_WITH_KNOTS('',3,(#84457,#84458,#84459,#84460,#84461,
#84462,#84463,#84464,#84465,#84466,#84467,#84468,#84469,#84470,#84471,#84472,
#84473,#84474,#84475,#84476,#84477,#84478,#84479,#84480,#84481,#84482,#84483,
#84484,#84485,#84486,#84487,#84488,#84489,#84490,#84491,#84492,#84493,#84494,
#84495,#84496,#84497,#84498,#84499,#84500,#84501,#84502,#84503,#84504,#84505,
#84506,#84507,#84508,#84509,#84510,#84511,#84512,#84513,#84514,#84515,#84516,
#84517,#84518,#84519,#84520,#84521,#84522,#84523,#84524,#84525,#84526,#84527,
#84528,#84529,#84530,#84531,#84532,#84533,#84534,#84535,#84536,#84537,#84538,
#84539,#84540,#84541,#84542,#84543,#84544,#84545,#84546,#84547,#84548,#84549,
#84550,#84551,#84552,#84553,#84554,#84555,#84556,#84557,#84558,#84559,#84560,
#84561,#84562,#84563,#84564,#84565,#84566,#84567,#84568,#84569,#84570,#84571,
#84572,#84573,#84574,#84575,#84576,#84577,#84578,#84579,#84580,#84581,#84582,
#84583,#84584,#84585,#84586,#84587,#84588,#84589,#84590,#84591,#84592,#84593,
#84594,#84595,#84596,#84597,#84598,#84599,#84600,#84601,#84602,#84603,#84604,
#84605,#84606,#84607,#84608,#84609,#84610,#84611,#84612,#84613,#84614,#84615,
#84616,#84617,#84618,#84619,#84620,#84621,#84622,#84623,#84624,#84625,#84626,
#84627,#84628,#84629,#84630,#84631,#84632,#84633,#84634,#84635,#84636,#84637,
#84638,#84639,#84640,#84641,#84642,#84643,#84644,#84645,#84646,#84647,#84648,
#84649,#84650,#84651,#84652,#84653,#84654,#84655,#84656,#84657,#84658,#84659,
#84660,#84661,#84662,#84663,#84664,#84665,#84666,#84667,#84668,#84669,#84670,
#84671,#84672,#84673,#84674,#84675,#84676),.UNSPECIFIED.,.F.,.F.,(4,3,3,
3,3,3,3,3,3,3,3,3,3,3,3,3,3,3,3,3,3,3,3,3,3,3,3,3,3,3,3,3,3,3,3,3,3,3,3,
3,3,3,3,3,3,3,3,3,3,3,3,3,3,3,3,3,3,3,3,3,3,3,3,3,3,3,3,3,3,3,3,3,3,4),
(926.769832808971,926.854312245086,926.938811412004,927.023346822792,927.110911951776,
927.195621791297,927.284614565012,927.373607338728,927.457346050574,927.540981561942,
927.62453400534,927.708023441191,927.791477391805,927.874913885651,927.958350995407,
928.041806790324,928.125351283054,928.208940365995,928.292663633553,928.373343349448,
928.457082061294,928.540717572661,928.62427001606,928.707759451911,928.791213402524,
928.874649896371,928.958087006126,929.041542801044,929.125087293774,929.208676376715,
929.292399644272,929.373079360168,929.456818072014,929.540453583382,929.62400602678,
929.707495462631,929.790949413245,929.874385907091,929.957823016847,930.041278811764,
930.124823304494,930.208412387435,930.292135654993,930.372815370888,930.456554082734,
930.540189594101,930.6237420375,930.707231473351,930.790685423965,930.874121917811,
930.957559027566,931.041014822483,931.124559315213,931.208148398154,931.291871665712,
931.372551381608,931.456290093454,931.539925604822,931.62347804822,931.706967484071,
931.790421434685,931.873857928531,931.957295038286,932.040750833203,932.124295325933,
932.207884408874,932.291607676431,932.372287392328,932.455788042781,932.542343473143,
932.625634800808,932.708867535087,932.79205460146,932.802009764231),
 .UNSPECIFIED.);
#643=B_SPLINE_CURVE_WITH_KNOTS('',3,(#84682,#84683,#84684,#84685,#84686,
#84687,#84688,#84689,#84690,#84691,#84692,#84693,#84694,#84695,#84696,#84697,
#84698,#84699,#84700,#84701,#84702,#84703,#84704,#84705,#84706,#84707,#84708,
#84709,#84710,#84711,#84712,#84713,#84714,#84715,#84716,#84717,#84718,#84719,
#84720,#84721,#84722,#84723,#84724,#84725,#84726,#84727,#84728,#84729,#84730,
#84731,#84732,#84733,#84734,#84735,#84736,#84737,#84738,#84739,#84740,#84741,
#84742,#84743,#84744,#84745,#84746,#84747,#84748,#84749,#84750,#84751,#84752,
#84753,#84754,#84755,#84756,#84757,#84758,#84759,#84760,#84761,#84762,#84763,
#84764,#84765,#84766,#84767,#84768,#84769,#84770,#84771,#84772,#84773,#84774,
#84775,#84776,#84777,#84778,#84779,#84780,#84781,#84782,#84783,#84784,#84785,
#84786,#84787,#84788,#84789,#84790,#84791,#84792,#84793,#84794,#84795,#84796,
#84797,#84798,#84799,#84800,#84801,#84802,#84803,#84804,#84805,#84806,#84807,
#84808,#84809,#84810,#84811,#84812,#84813,#84814,#84815,#84816,#84817,#84818,
#84819,#84820,#84821,#84822,#84823,#84824,#84825,#84826,#84827,#84828,#84829,
#84830,#84831,#84832,#84833,#84834,#84835,#84836,#84837,#84838,#84839,#84840,
#84841,#84842,#84843,#84844,#84845,#84846,#84847,#84848,#84849,#84850,#84851,
#84852,#84853,#84854,#84855,#84856,#84857,#84858,#84859,#84860,#84861,#84862,
#84863,#84864,#84865,#84866,#84867,#84868,#84869,#84870,#84871,#84872,#84873,
#84874,#84875,#84876,#84877,#84878,#84879,#84880,#84881,#84882,#84883,#84884,
#84885,#84886,#84887,#84888,#84889,#84890,#84891,#84892,#84893,#84894,#84895,
#84896,#84897,#84898,#84899,#84900,#84901,#84902,#84903,#84904),
 .UNSPECIFIED.,.F.,.F.,(4,3,3,3,3,3,3,3,3,3,3,3,3,3,3,3,3,3,3,3,3,3,3,3,
3,3,3,3,3,3,3,3,3,3,3,3,3,3,3,3,3,3,3,3,3,3,3,3,3,3,3,3,3,3,3,3,3,3,3,3,
3,3,3,3,3,3,3,3,3,3,3,3,3,3,4),(933.053018116147,933.061732783332,933.145471495178,
933.229107006546,933.312659449944,933.396148885795,933.479602836409,933.563039330255,
933.64647644001,933.729932234928,933.813476727658,933.897065810599,933.980789078156,
934.061468794052,934.145207505898,934.228843017265,934.312395460664,934.395884896515,
934.479338847128,934.562775340975,934.64621245073,934.729668245648,934.813212738378,
934.896801821318,934.980525088876,935.061204804772,935.144943516618,935.228579027986,
935.312131471384,935.395620907235,935.479074857849,935.562511351695,935.645948461451,
935.729404256368,935.812948749098,935.896537832039,935.980261099597,936.060940815492,
936.144679527338,936.228315038705,936.311867482104,936.395356917955,936.478810868568,
936.562247362415,936.64568447217,936.729140267087,936.812684759817,936.896273842758,
936.979997110315,937.060676826212,937.144415538058,937.228051049426,937.311603492824,
937.395092928675,937.478546879289,937.561983373135,937.64542048289,937.728876277808,
937.812420770538,937.896009853479,937.979733121036,938.060412836932,938.144151548778,
938.227787060145,938.311339503544,938.394828939395,938.478282890009,938.561719383855,
938.64515649361,938.728612288528,938.812156781258,938.895745864199,938.979469131756,
939.060148847652,939.085291531953),.UNSPECIFIED.);
#644=B_SPLINE_CURVE_WITH_KNOTS('',3,(#84905,#84906,#84907,#84908,#84909,
#84910,#84911,#84912,#84913,#84914),.UNSPECIFIED.,.F.,.F.,(4,3,3,4),(932.8013317429,
932.884788778377,932.968903447177,933.053018115978),.UNSPECIFIED.);
#645=B_SPLINE_CURVE_WITH_KNOTS('',3,(#84916,#84917,#84918,#84919,#84920,
#84921,#84922,#84923,#84924,#84925),.UNSPECIFIED.,.F.,.F.,(4,3,3,4),(932.802009764231,
932.88517971186,932.969098914005,933.053018116151),.UNSPECIFIED.);
#646=B_SPLINE_CURVE_WITH_KNOTS('',3,(#84926,#84927,#84928,#84929,#84930,
#84931,#84932,#84933,#84934,#84935,#84936,#84937,#84938,#84939,#84940,#84941,
#84942,#84943,#84944,#84945,#84946,#84947,#84948,#84949,#84950,#84951,#84952,
#84953,#84954,#84955,#84956,#84957,#84958,#84959,#84960,#84961,#84962,#84963,
#84964,#84965,#84966,#84967,#84968,#84969,#84970,#84971,#84972,#84973,#84974,
#84975,#84976,#84977,#84978,#84979,#84980,#84981,#84982,#84983,#84984,#84985,
#84986,#84987,#84988,#84989,#84990,#84991,#84992,#84993,#84994,#84995,#84996,
#84997,#84998,#84999,#85000,#85001,#85002,#85003,#85004,#85005,#85006,#85007,
#85008,#85009,#85010,#85011,#85012,#85013,#85014,#85015,#85016,#85017,#85018,
#85019,#85020,#85021,#85022,#85023,#85024,#85025,#85026,#85027,#85028,#85029,
#85030,#85031,#85032,#85033,#85034,#85035,#85036,#85037,#85038,#85039,#85040,
#85041,#85042,#85043,#85044,#85045,#85046,#85047,#85048,#85049,#85050,#85051,
#85052,#85053,#85054,#85055,#85056,#85057,#85058,#85059,#85060,#85061,#85062,
#85063,#85064,#85065,#85066,#85067,#85068,#85069,#85070,#85071,#85072,#85073,
#85074,#85075,#85076,#85077,#85078,#85079,#85080,#85081,#85082,#85083,#85084,
#85085,#85086,#85087,#85088,#85089,#85090,#85091,#85092,#85093,#85094,#85095,
#85096,#85097,#85098,#85099,#85100,#85101,#85102,#85103,#85104,#85105,#85106,
#85107,#85108,#85109,#85110,#85111,#85112,#85113,#85114,#85115,#85116,#85117,
#85118,#85119,#85120,#85121,#85122,#85123,#85124,#85125,#85126,#85127,#85128,
#85129,#85130,#85131,#85132,#85133,#85134,#85135,#85136,#85137,#85138,#85139,
#85140,#85141,#85142,#85143,#85144,#85145),.UNSPECIFIED.,.F.,.F.,(4,3,3,
3,3,3,3,3,3,3,3,3,3,3,3,3,3,3,3,3,3,3,3,3,3,3,3,3,3,3,3,3,3,3,3,3,3,3,3,
3,3,3,3,3,3,3,3,3,3,3,3,3,3,3,3,3,3,3,3,3,3,3,3,3,3,3,3,3,3,3,3,3,3,4),
(933.053018116324,933.151593256213,933.250857262522,933.350876069408,933.372023403049,
933.455762114895,933.539397626262,933.622950069661,933.706439505512,933.789893456126,
933.873329949972,933.956767059727,934.040222854645,934.123767347375,934.207356430316,
934.291079697873,934.371759413769,934.455498125615,934.539133636983,934.622686080381,
934.706175516232,934.789629466846,934.873065960692,934.956503070447,935.039958865365,
935.123503358095,935.207092441036,935.290815708593,935.371495424489,935.455234136335,
935.538869647702,935.622422091101,935.705911526952,935.789365477565,935.872801971412,
935.956239081167,936.039694876085,936.123239368814,936.206828451755,936.290551719313,
936.371231435209,936.454970147055,936.538605658423,936.622158101821,936.705647537672,
936.789101488286,936.872537982132,936.955975091888,937.039430886805,937.122975379535,
937.206564462476,937.290287730034,937.370967445929,937.454706157775,937.538341669142,
937.621894112541,937.705383548392,937.788837499006,937.872273992852,937.955711102608,
938.039166897525,938.122711390255,938.206300473196,938.290023740754,938.370703456649,
938.453993507398,938.537151940436,938.62023438107,938.703259410404,938.786245564127,
938.86922730096,938.95220520749,939.035225802725,939.084433024015),
 .UNSPECIFIED.);
#647=B_SPLINE_CURVE_WITH_KNOTS('',3,(#85151,#85152,#85153,#85154,#85155,
#85156,#85157,#85158,#85159,#85160,#85161,#85162,#85163,#85164,#85165,#85166,
#85167,#85168,#85169,#85170,#85171,#85172,#85173,#85174,#85175,#85176,#85177,
#85178,#85179,#85180,#85181,#85182,#85183,#85184,#85185,#85186,#85187,#85188,
#85189,#85190,#85191,#85192,#85193,#85194,#85195,#85196,#85197,#85198,#85199,
#85200,#85201,#85202,#85203,#85204,#85205,#85206,#85207,#85208,#85209,#85210,
#85211,#85212,#85213,#85214,#85215,#85216,#85217,#85218,#85219,#85220,#85221,
#85222,#85223,#85224,#85225,#85226,#85227,#85228,#85229,#85230,#85231,#85232,
#85233,#85234,#85235,#85236,#85237,#85238,#85239,#85240,#85241,#85242,#85243,
#85244,#85245,#85246,#85247,#85248,#85249,#85250,#85251,#85252,#85253,#85254,
#85255,#85256,#85257,#85258,#85259,#85260,#85261,#85262,#85263,#85264,#85265,
#85266,#85267,#85268,#85269,#85270,#85271,#85272,#85273,#85274,#85275,#85276,
#85277,#85278,#85279,#85280,#85281,#85282,#85283,#85284,#85285,#85286,#85287,
#85288,#85289,#85290,#85291,#85292,#85293,#85294,#85295,#85296,#85297,#85298,
#85299,#85300,#85301,#85302,#85303,#85304,#85305,#85306,#85307,#85308,#85309,
#85310,#85311,#85312,#85313,#85314,#85315,#85316,#85317,#85318,#85319,#85320,
#85321,#85322,#85323,#85324,#85325,#85326,#85327,#85328,#85329,#85330,#85331,
#85332,#85333,#85334,#85335,#85336,#85337,#85338,#85339,#85340,#85341,#85342,
#85343,#85344,#85345,#85346,#85347,#85348,#85349,#85350,#85351,#85352,#85353,
#85354,#85355,#85356,#85357,#85358,#85359,#85360,#85361,#85362,#85363,#85364,
#85365,#85366,#85367,#85368,#85369,#85370),.UNSPECIFIED.,.F.,.F.,(4,3,3,
3,3,3,3,3,3,3,3,3,3,3,3,3,3,3,3,3,3,3,3,3,3,3,3,3,3,3,3,3,3,3,3,3,3,3,3,
3,3,3,3,3,3,3,3,3,3,3,3,3,3,3,3,3,3,3,3,3,3,3,3,3,3,3,3,3,3,3,3,3,3,4),
(939.336203423326,939.418950147463,939.501660561274,939.584353678099,939.667048193191,
939.749762799753,939.832565814582,939.915415824873,939.998394410342,940.059884858373,
940.143623570219,940.227259081587,940.310811524985,940.394300960836,940.47775491145,
940.561191405296,940.644628515052,940.728084309969,940.811628802699,940.89521788564,
940.978941153198,941.059620869093,941.143359580939,941.226995092306,941.310547535705,
941.394036971556,941.47749092217,941.560927416016,941.644364525771,941.727820320688,
941.811364813418,941.894953896359,941.978677163916,942.059356879813,942.143095591659,
942.226731103027,942.310283546425,942.393772982276,942.477226932889,942.560663426736,
942.644100536491,942.727556331409,942.811100824139,942.89468990708,942.978413174637,
943.059092890533,943.142831602379,943.226467113746,943.310019557145,943.393508992996,
943.47696294361,943.560399437456,943.643836547211,943.727292342129,943.810836834859,
943.8944259178,943.978149185357,944.058828901253,944.142567613099,944.226203124467,
944.309755567865,944.393245003716,944.47669895433,944.560135448176,944.643572557932,
944.727028352849,944.810572845579,944.89416192852,944.977885196078,945.058564911973,
945.144544706224,945.230413078362,945.316150774852,945.368916660643),
 .UNSPECIFIED.);
#648=B_SPLINE_CURVE_WITH_KNOTS('',3,(#85371,#85372,#85373,#85374,#85375,
#85376,#85377,#85378,#85379,#85380),.UNSPECIFIED.,.F.,.F.,(4,3,3,4),(939.085291531953,
939.190470359852,939.293976169291,939.336203423223),.UNSPECIFIED.);
#649=B_SPLINE_CURVE_WITH_KNOTS('',3,(#85382,#85383,#85384,#85385,#85386,
#85387,#85388,#85389,#85390,#85391),.UNSPECIFIED.,.F.,.F.,(4,3,3,4),(939.084433024015,
939.167549453827,939.251876438504,939.336203423181),.UNSPECIFIED.);
#650=B_SPLINE_CURVE_WITH_KNOTS('',3,(#85392,#85393,#85394,#85395,#85396,
#85397,#85398,#85399,#85400,#85401,#85402,#85403,#85404,#85405,#85406,#85407,
#85408,#85409,#85410,#85411,#85412,#85413,#85414,#85415,#85416,#85417,#85418,
#85419,#85420,#85421,#85422,#85423,#85424,#85425,#85426,#85427,#85428,#85429,
#85430,#85431,#85432,#85433,#85434,#85435,#85436,#85437,#85438,#85439,#85440,
#85441,#85442,#85443,#85444,#85445,#85446,#85447,#85448,#85449,#85450,#85451,
#85452,#85453,#85454,#85455,#85456,#85457,#85458,#85459,#85460,#85461,#85462,
#85463,#85464,#85465,#85466,#85467,#85468,#85469,#85470,#85471,#85472,#85473,
#85474,#85475,#85476,#85477,#85478,#85479,#85480,#85481,#85482,#85483,#85484,
#85485,#85486,#85487,#85488,#85489,#85490,#85491,#85492,#85493,#85494,#85495,
#85496,#85497,#85498,#85499,#85500,#85501,#85502,#85503,#85504,#85505,#85506,
#85507,#85508,#85509,#85510,#85511,#85512,#85513,#85514,#85515,#85516,#85517,
#85518,#85519,#85520,#85521,#85522,#85523,#85524,#85525,#85526,#85527,#85528,
#85529,#85530,#85531,#85532,#85533,#85534,#85535,#85536,#85537,#85538,#85539,
#85540,#85541,#85542,#85543,#85544,#85545,#85546,#85547,#85548,#85549,#85550,
#85551,#85552,#85553,#85554,#85555,#85556,#85557,#85558,#85559,#85560,#85561,
#85562,#85563,#85564,#85565,#85566,#85567,#85568,#85569,#85570,#85571,#85572,
#85573,#85574,#85575,#85576,#85577,#85578,#85579,#85580,#85581,#85582,#85583,
#85584,#85585,#85586,#85587,#85588,#85589,#85590,#85591,#85592,#85593,#85594,
#85595,#85596,#85597,#85598,#85599,#85600,#85601,#85602,#85603,#85604,#85605,
#85606,#85607,#85608,#85609,#85610,#85611),.UNSPECIFIED.,.F.,.F.,(4,3,3,
3,3,3,3,3,3,3,3,3,3,3,3,3,3,3,3,3,3,3,3,3,3,3,3,3,3,3,3,3,3,3,3,3,3,3,3,
3,3,3,3,3,3,3,3,3,3,3,3,3,3,3,3,3,3,3,3,3,3,3,3,3,3,3,3,3,3,3,3,3,3,4),
(939.33620342333,939.370439467369,939.454178179215,939.537813690583,939.621366133981,
939.704855569833,939.788309520447,939.871746014293,939.955183124049,940.038638918967,
940.122183411696,940.205772494638,940.289495762195,940.370175478089,940.453914189935,
940.537549701303,940.621102144701,940.704591580552,940.788045531166,940.871482025012,
940.954919134767,941.038374929685,941.121919422415,941.205508505356,941.289231772913,
941.36991148881,941.453650200656,941.537285712024,941.620838155422,941.704327591273,
941.787781541887,941.871218035733,941.954655145489,942.038110940406,942.121655433136,
942.205244516077,942.288967783635,942.36964749953,942.453386211376,942.537021722743,
942.620574166142,942.704063601993,942.787517552607,942.870954046453,942.954391156208,
943.037846951126,943.121391443855,943.204980526796,943.288703794354,943.36938351025,
943.453122222096,943.536757733464,943.620310176862,943.703799612713,943.787253563327,
943.870690057173,943.954127166928,944.037582961846,944.121127454576,944.204716537517,
944.288439805074,944.36911952097,944.452858262808,944.536493797105,944.620046256401,
944.703535701139,944.786989623716,944.87042607954,944.953863141282,945.037318878179,
945.120863171504,945.204452050913,945.288174778316,945.36832006177),
 .UNSPECIFIED.);
#651=B_SPLINE_CURVE_WITH_KNOTS('',3,(#85617,#85618,#85619,#85620,#85621,
#85622,#85623,#85624,#85625,#85626,#85627,#85628,#85629,#85630,#85631,#85632,
#85633,#85634,#85635,#85636,#85637,#85638,#85639,#85640,#85641,#85642,#85643,
#85644,#85645,#85646,#85647,#85648,#85649,#85650,#85651,#85652,#85653,#85654,
#85655,#85656,#85657,#85658,#85659,#85660,#85661,#85662,#85663,#85664,#85665,
#85666,#85667,#85668,#85669,#85670,#85671,#85672,#85673,#85674,#85675,#85676,
#85677,#85678,#85679,#85680,#85681,#85682,#85683,#85684,#85685,#85686,#85687,
#85688,#85689,#85690,#85691,#85692,#85693,#85694,#85695,#85696,#85697,#85698,
#85699,#85700,#85701,#85702,#85703,#85704,#85705,#85706,#85707,#85708,#85709,
#85710,#85711,#85712,#85713,#85714,#85715,#85716,#85717,#85718,#85719,#85720,
#85721,#85722,#85723,#85724,#85725,#85726,#85727,#85728,#85729,#85730,#85731,
#85732,#85733,#85734,#85735,#85736,#85737,#85738,#85739,#85740,#85741,#85742,
#85743,#85744,#85745,#85746,#85747,#85748,#85749,#85750,#85751,#85752,#85753,
#85754,#85755,#85756,#85757,#85758,#85759,#85760,#85761,#85762,#85763,#85764,
#85765,#85766,#85767,#85768,#85769,#85770,#85771,#85772,#85773,#85774,#85775,
#85776,#85777,#85778,#85779,#85780,#85781,#85782,#85783,#85784,#85785,#85786,
#85787,#85788,#85789,#85790,#85791,#85792,#85793,#85794,#85795,#85796,#85797,
#85798,#85799,#85800,#85801,#85802,#85803,#85804,#85805,#85806,#85807,#85808,
#85809,#85810,#85811,#85812,#85813,#85814,#85815,#85816,#85817,#85818,#85819,
#85820,#85821,#85822,#85823,#85824,#85825,#85826,#85827,#85828,#85829,#85830,
#85831,#85832,#85833,#85834,#85835,#85836),.UNSPECIFIED.,.F.,.F.,(4,3,3,
3,3,3,3,3,3,3,3,3,3,3,3,3,3,3,3,3,3,3,3,3,3,3,3,3,3,3,3,3,3,3,3,3,3,3,3,
3,3,3,3,3,3,3,3,3,3,3,3,3,3,3,3,3,3,3,3,3,3,3,3,3,3,3,3,3,3,3,3,3,3,4),
(945.61938873063,945.70936915299,945.799705876632,945.890221435482,945.981029384766,
946.058300922693,946.142039634539,946.225675145907,946.309227589306,946.392717025158,
946.476170975772,946.559607469619,946.643044579375,946.726500374293,946.810044867023,
946.893633949964,946.977357217522,947.058036933414,947.14177564526,947.225411156627,
947.308963600026,947.392453035876,947.47590698649,947.559343480336,947.642780590091,
947.726236385009,947.809780877738,947.893369960679,947.977093228237,948.057772944134,
948.14151165598,948.225147167347,948.308699610746,948.392189046597,948.47564299721,
948.559079491057,948.642516600812,948.72597239573,948.809516888459,948.8931059714,
948.976829238958,949.057508954854,949.1412476667,949.224883178068,949.308435621466,
949.391925057317,949.475379007931,949.558815501777,949.642252611533,949.725708406451,
949.809252899181,949.892841982122,949.976565249679,950.057244965574,950.14098367742,
950.224619188787,950.308171632186,950.391661068037,950.475115018651,950.558551512497,
950.641988622252,950.72544441717,950.808988909899,950.89257799284,950.976301260398,
951.056980976294,951.139459701244,951.221843364055,951.304151178297,951.386402284189,
951.468620741908,951.550821273017,951.633035317302,951.650831115062),
 .UNSPECIFIED.);
#652=B_SPLINE_CURVE_WITH_KNOTS('',3,(#85837,#85838,#85839,#85840,#85841,
#85842,#85843,#85844,#85845,#85846),.UNSPECIFIED.,.F.,.F.,(4,3,3,4),(945.368916660643,
945.454506788451,945.540021559813,945.619388730506),.UNSPECIFIED.);
#653=B_SPLINE_CURVE_WITH_KNOTS('',3,(#85848,#85849,#85850,#85851,#85852,
#85853,#85854,#85855,#85856,#85857,#85858,#85859,#85860),.UNSPECIFIED.,
 .F.,.F.,(4,3,3,3,4),(945.36832006177,945.36885553169,945.478563499207,
945.585901681379,945.61938873033),.UNSPECIFIED.);
#654=B_SPLINE_CURVE_WITH_KNOTS('',3,(#85861,#85862,#85863,#85864,#85865,
#85866,#85867,#85868,#85869,#85870,#85871,#85872,#85873,#85874,#85875,#85876,
#85877,#85878,#85879,#85880,#85881,#85882,#85883,#85884,#85885,#85886,#85887,
#85888,#85889,#85890,#85891,#85892,#85893,#85894,#85895,#85896,#85897,#85898,
#85899,#85900,#85901,#85902,#85903,#85904,#85905,#85906,#85907,#85908,#85909,
#85910,#85911,#85912,#85913,#85914,#85915,#85916,#85917,#85918,#85919,#85920,
#85921,#85922,#85923,#85924,#85925,#85926,#85927,#85928,#85929,#85930,#85931,
#85932,#85933,#85934,#85935,#85936,#85937,#85938,#85939,#85940,#85941,#85942,
#85943,#85944,#85945,#85946,#85947,#85948,#85949,#85950,#85951,#85952,#85953,
#85954,#85955,#85956,#85957,#85958,#85959,#85960,#85961,#85962,#85963,#85964,
#85965,#85966,#85967,#85968,#85969,#85970,#85971,#85972,#85973,#85974,#85975,
#85976,#85977,#85978,#85979,#85980,#85981,#85982,#85983,#85984,#85985,#85986,
#85987,#85988,#85989,#85990,#85991,#85992,#85993,#85994,#85995,#85996,#85997,
#85998,#85999,#86000,#86001,#86002,#86003,#86004,#86005,#86006,#86007,#86008,
#86009,#86010,#86011,#86012,#86013,#86014,#86015,#86016,#86017,#86018,#86019,
#86020,#86021,#86022,#86023,#86024,#86025,#86026,#86027,#86028,#86029,#86030,
#86031,#86032,#86033,#86034,#86035,#86036,#86037,#86038,#86039,#86040,#86041,
#86042,#86043,#86044,#86045,#86046,#86047,#86048,#86049,#86050,#86051,#86052,
#86053,#86054,#86055,#86056,#86057,#86058,#86059,#86060,#86061,#86062,#86063,
#86064,#86065,#86066,#86067,#86068,#86069,#86070,#86071,#86072,#86073,#86074,
#86075,#86076,#86077,#86078,#86079,#86080),.UNSPECIFIED.,.F.,.F.,(4,3,3,
3,3,3,3,3,3,3,3,3,3,3,3,3,3,3,3,3,3,3,3,3,3,3,3,3,3,3,3,3,3,3,3,3,3,3,3,
3,3,3,3,3,3,3,3,3,3,3,3,3,3,3,3,3,3,3,3,3,3,3,3,3,3,3,3,3,3,3,3,3,3,4),
(945.61938873051,945.701954256402,945.785283917153,945.867774678202,945.950258870669,
946.032755341671,946.116714391856,946.199335015738,946.283963279074,946.36859154241,
946.452330254256,946.535965765623,946.619518209021,946.703007644873,946.786461595486,
946.869898089332,946.953335199088,947.036790994005,947.120335486734,947.203924569675,
947.287647837233,947.36832755313,947.452066264976,947.535701776344,947.619254219743,
947.702743655595,947.786197606209,947.869634100055,947.953071209811,948.036527004729,
948.120071497459,948.203660580401,948.287383847958,948.368063563851,948.451802275697,
948.535437787064,948.618990230463,948.702479666314,948.785933616928,948.869370110774,
948.952807220529,949.036263015446,949.119807508176,949.203396591117,949.287119858675,
949.367799574571,949.451538286417,949.535173797784,949.618726241183,949.702215677034,
949.785669627648,949.869106121494,949.952543231249,950.035999026167,950.119543518896,
950.203132601837,950.286855869395,950.367535585291,950.451274297137,950.534909808505,
950.618462251903,950.701951687755,950.785405638368,950.868842132215,950.95227924197,
951.035735036888,951.119279529618,951.202868612559,951.286591880117,951.367271596011,
951.454042302477,951.540693724387,951.627203916606,951.652176355207),
 .UNSPECIFIED.);
#655=B_SPLINE_CURVE_WITH_KNOTS('',3,(#86086,#86087,#86088,#86089,#86090,
#86091,#86092,#86093,#86094,#86095,#86096,#86097,#86098,#86099,#86100,#86101,
#86102,#86103,#86104,#86105,#86106,#86107,#86108,#86109,#86110,#86111,#86112,
#86113,#86114,#86115,#86116,#86117,#86118,#86119,#86120,#86121,#86122,#86123,
#86124,#86125,#86126,#86127,#86128,#86129,#86130,#86131,#86132,#86133,#86134,
#86135,#86136,#86137,#86138,#86139,#86140,#86141,#86142,#86143,#86144,#86145,
#86146,#86147,#86148,#86149,#86150,#86151,#86152,#86153,#86154,#86155,#86156,
#86157,#86158,#86159,#86160,#86161,#86162,#86163,#86164,#86165,#86166,#86167,
#86168,#86169,#86170,#86171,#86172,#86173,#86174,#86175,#86176,#86177,#86178,
#86179,#86180,#86181,#86182,#86183,#86184,#86185,#86186,#86187,#86188,#86189,
#86190,#86191,#86192,#86193,#86194,#86195,#86196,#86197,#86198,#86199,#86200,
#86201,#86202,#86203,#86204,#86205,#86206,#86207,#86208,#86209,#86210,#86211,
#86212,#86213,#86214,#86215,#86216,#86217,#86218,#86219,#86220,#86221,#86222,
#86223,#86224,#86225,#86226,#86227,#86228,#86229,#86230,#86231,#86232,#86233,
#86234,#86235,#86236,#86237,#86238,#86239,#86240,#86241,#86242,#86243,#86244,
#86245,#86246,#86247,#86248,#86249,#86250,#86251,#86252,#86253,#86254,#86255,
#86256,#86257,#86258,#86259,#86260,#86261,#86262,#86263,#86264,#86265,#86266,
#86267,#86268,#86269,#86270,#86271,#86272,#86273,#86274,#86275,#86276,#86277,
#86278,#86279,#86280,#86281,#86282,#86283,#86284,#86285,#86286,#86287,#86288,
#86289,#86290,#86291,#86292,#86293,#86294,#86295,#86296,#86297,#86298,#86299,
#86300,#86301,#86302,#86303,#86304,#86305),.UNSPECIFIED.,.F.,.F.,(4,3,3,
3,3,3,3,3,3,3,3,3,3,3,3,3,3,3,3,3,3,3,3,3,3,3,3,3,3,3,3,3,3,3,3,3,3,3,3,
3,3,3,3,3,3,3,3,3,3,3,3,3,3,3,3,3,3,3,3,3,3,3,3,3,3,3,3,3,3,3,3,3,3,4),
(951.902574037685,952.042340863672,952.056716987014,952.14045569886,952.224091210227,
952.307643653625,952.391133089475,952.474587040089,952.558023533934,952.641460643689,
952.724916438606,952.808460931336,952.892050014276,952.975773281834,953.056452997734,
953.14019170958,953.223827220948,953.307379664347,953.390869100198,953.474323050812,
953.557759544658,953.641196654414,953.724652449332,953.808196942062,953.891786025003,
953.97550929256,954.056189008455,954.139927720301,954.223563231669,954.307115675067,
954.390605110918,954.474059061532,954.557495555378,954.640932665134,954.724388460052,
954.807932952781,954.891522035722,954.97524530328,955.055925019175,955.139663731021,
955.223299242388,955.306851685786,955.390341121637,955.473795072251,955.557231566097,
955.640668675852,955.72412447077,955.807668963499,955.89125804644,955.974981313997,
956.055661029895,956.139399741741,956.223035253109,956.306587696507,956.390077132359,
956.473531082972,956.556967576819,956.640404686574,956.723860481492,956.807404974222,
956.890994057163,956.974717324721,957.055397040615,957.139142851557,957.222783866638,
957.306340225206,957.389826949076,957.473275871116,957.556705080045,957.640132647437,
957.723609880086,957.8071145508,957.890705960823,957.934190499289),
 .UNSPECIFIED.);
#656=B_SPLINE_CURVE_WITH_KNOTS('',3,(#86306,#86307,#86308,#86309,#86310,
#86311,#86312,#86313,#86314,#86315),.UNSPECIFIED.,.F.,.F.,(4,3,3,4),(951.650831115062,
951.733106192795,951.817840115185,951.902574037576),.UNSPECIFIED.);
#657=B_SPLINE_CURVE_WITH_KNOTS('',3,(#86317,#86318,#86319,#86320,#86321,
#86322,#86323,#86324,#86325,#86326),.UNSPECIFIED.,.F.,.F.,(4,3,3,4),(951.652176355207,
951.738532064097,951.824780508187,951.902574037689),.UNSPECIFIED.);
#658=B_SPLINE_CURVE_WITH_KNOTS('',3,(#86327,#86328,#86329,#86330,#86331,
#86332,#86333,#86334,#86335,#86336,#86337,#86338,#86339,#86340,#86341,#86342,
#86343,#86344,#86345,#86346,#86347,#86348,#86349,#86350,#86351,#86352,#86353,
#86354,#86355,#86356,#86357,#86358,#86359,#86360,#86361,#86362,#86363,#86364,
#86365,#86366,#86367,#86368,#86369,#86370,#86371,#86372,#86373,#86374,#86375,
#86376,#86377,#86378,#86379,#86380,#86381,#86382,#86383,#86384,#86385,#86386,
#86387,#86388,#86389,#86390,#86391,#86392,#86393,#86394,#86395,#86396,#86397,
#86398,#86399,#86400,#86401,#86402,#86403,#86404,#86405,#86406,#86407,#86408,
#86409,#86410,#86411,#86412,#86413,#86414,#86415,#86416,#86417,#86418,#86419,
#86420,#86421,#86422,#86423,#86424,#86425,#86426,#86427,#86428,#86429,#86430,
#86431,#86432,#86433,#86434,#86435,#86436,#86437,#86438,#86439,#86440,#86441,
#86442,#86443,#86444,#86445,#86446,#86447,#86448,#86449,#86450,#86451,#86452,
#86453,#86454,#86455,#86456,#86457,#86458,#86459,#86460,#86461,#86462,#86463,
#86464,#86465,#86466,#86467,#86468,#86469,#86470,#86471,#86472,#86473,#86474,
#86475,#86476,#86477,#86478,#86479,#86480,#86481,#86482,#86483,#86484,#86485,
#86486,#86487,#86488,#86489,#86490,#86491,#86492,#86493,#86494,#86495,#86496,
#86497,#86498,#86499,#86500,#86501,#86502,#86503,#86504,#86505,#86506,#86507,
#86508,#86509,#86510,#86511,#86512,#86513,#86514,#86515,#86516,#86517,#86518,
#86519,#86520,#86521,#86522,#86523,#86524,#86525,#86526,#86527,#86528,#86529,
#86530,#86531,#86532,#86533,#86534,#86535,#86536,#86537,#86538,#86539,#86540,
#86541,#86542,#86543,#86544,#86545,#86546),.UNSPECIFIED.,.F.,.F.,(4,3,3,
3,3,3,3,3,3,3,3,3,3,3,3,3,3,3,3,3,3,3,3,3,3,3,3,3,3,3,3,3,3,3,3,3,3,3,3,
3,3,3,3,3,3,3,3,3,3,3,3,3,3,3,3,3,3,3,3,3,3,3,3,3,3,3,3,3,3,3,3,3,3,4),
(951.902574037848,951.991380896566,952.080358557091,952.169596981776,952.258979410966,
952.348574064124,952.367007606731,952.450746318577,952.534381829944,952.617934273341,
952.701423709192,952.784877659805,952.868314153651,952.951751263406,953.035207058323,
953.118751551052,953.202340633993,953.28606390155,953.366743617451,953.450482329297,
953.534117840664,953.617670284063,953.701159719914,953.784613670527,953.868050164373,
953.951487274128,954.034943069046,954.118487561775,954.202076644716,954.285799912274,
954.366479628171,954.450218340017,954.533853851385,954.617406294784,954.700895730636,
954.78434968125,954.867786175096,954.951223284852,955.03467907977,955.1182235725,
955.201812655442,955.285535923,955.366215638892,955.449954350738,955.533589862105,
955.617142305504,955.700631741355,955.784085691969,955.867522185815,955.95095929557,
956.034415090488,956.117959583218,956.201548666159,956.285271933716,956.365951649612,
956.449690361458,956.533325872825,956.616878316224,956.700367752074,956.783821702688,
956.867258196534,956.950695306289,957.034151101207,957.117695593936,957.201284676877,
957.285007944435,957.365687660332,957.448164195396,957.530545166499,957.612849793349,
957.695097032956,957.777309095665,957.859524712643,957.934095227666),
 .UNSPECIFIED.);
#659=B_SPLINE_CURVE_WITH_KNOTS('',3,(#86552,#86553,#86554,#86555,#86556,
#86557,#86558,#86559,#86560,#86561,#86562,#86563,#86564,#86565,#86566,#86567,
#86568,#86569,#86570,#86571,#86572,#86573,#86574,#86575,#86576,#86577,#86578,
#86579,#86580,#86581,#86582,#86583,#86584,#86585,#86586,#86587,#86588,#86589,
#86590,#86591,#86592,#86593,#86594,#86595,#86596,#86597,#86598,#86599,#86600,
#86601,#86602,#86603,#86604,#86605,#86606,#86607,#86608,#86609,#86610,#86611,
#86612,#86613,#86614,#86615,#86616,#86617,#86618,#86619,#86620,#86621,#86622,
#86623,#86624,#86625,#86626,#86627,#86628,#86629,#86630,#86631,#86632,#86633,
#86634,#86635,#86636,#86637,#86638,#86639,#86640,#86641,#86642,#86643,#86644,
#86645,#86646,#86647,#86648,#86649,#86650,#86651,#86652,#86653,#86654,#86655,
#86656,#86657,#86658,#86659,#86660,#86661,#86662,#86663,#86664,#86665,#86666,
#86667,#86668,#86669,#86670,#86671,#86672,#86673,#86674,#86675,#86676,#86677,
#86678,#86679,#86680,#86681,#86682,#86683,#86684,#86685,#86686,#86687,#86688,
#86689,#86690,#86691,#86692,#86693,#86694,#86695,#86696,#86697,#86698,#86699,
#86700,#86701,#86702,#86703,#86704,#86705,#86706,#86707,#86708,#86709,#86710,
#86711,#86712,#86713,#86714,#86715,#86716,#86717,#86718,#86719,#86720,#86721,
#86722,#86723,#86724,#86725,#86726,#86727,#86728,#86729,#86730,#86731,#86732,
#86733,#86734,#86735,#86736,#86737,#86738,#86739,#86740,#86741,#86742,#86743,
#86744,#86745,#86746,#86747,#86748,#86749,#86750,#86751,#86752,#86753,#86754,
#86755,#86756,#86757,#86758,#86759,#86760,#86761,#86762,#86763,#86764,#86765,
#86766,#86767,#86768,#86769,#86770,#86771),.UNSPECIFIED.,.F.,.F.,(4,3,3,
3,3,3,3,3,3,3,3,3,3,3,3,3,3,3,3,3,3,3,3,3,3,3,3,3,3,3,3,3,3,3,3,3,3,3,3,
3,3,3,3,3,3,3,3,3,3,3,3,3,3,3,3,3,3,3,3,3,3,3,3,3,3,3,3,3,3,3,3,3,3,4),
(958.185759344993,958.268231048685,958.350616230641,958.432936012912,958.515218019199,
958.597482260353,958.67974773475,958.76203343953,958.844404999096,958.926824299906,
959.009364852066,959.054869062055,959.138607773901,959.222243285268,959.305795728667,
959.389285164518,959.472739115132,959.556175608978,959.639612718734,959.723068513651,
959.806613006381,959.890202089322,959.973925356879,960.054605072775,960.138343784621,
960.221979295989,960.305531739388,960.389021175239,960.472475125853,960.5559116197,
960.639348729455,960.722804524373,960.806349017103,960.889938100044,960.973661367602,
961.054341083496,961.138079795342,961.221715306709,961.305267750108,961.388757185959,
961.472211136572,961.555647630418,961.639084740174,961.722540535091,961.806085027821,
961.889674110762,961.973397378319,962.054077094216,962.137815806062,962.22145131743,
962.305003760828,962.388493196679,962.471947147293,962.555383641139,962.638820750894,
962.722276545811,962.805821038541,962.889410121482,962.973133389039,963.053813104936,
963.137551816782,963.22118732815,963.304739771548,963.388229207399,963.471683158013,
963.555119651859,963.638556761615,963.722012556532,963.805557049262,963.889146132203,
963.97286939976,964.053549115656,964.145691166955,964.218603001888),
 .UNSPECIFIED.);
#660=B_SPLINE_CURVE_WITH_KNOTS('',3,(#86772,#86773,#86774,#86775,#86776,
#86777,#86778,#86779,#86780,#86781),.UNSPECIFIED.,.F.,.F.,(4,3,3,4),(957.934190499289,
958.017931037181,958.055133051335,958.185759344865),.UNSPECIFIED.);
#661=B_SPLINE_CURVE_WITH_KNOTS('',3,(#86783,#86784,#86785,#86786,#86787,
#86788,#86789,#86790,#86791,#86792),.UNSPECIFIED.,.F.,.F.,(4,3,3,4),(957.934095227666,
958.016349841335,958.101054593024,958.185759344712),.UNSPECIFIED.);
#662=B_SPLINE_CURVE_WITH_KNOTS('',3,(#86793,#86794,#86795,#86796,#86797,
#86798,#86799,#86800,#86801,#86802,#86803,#86804,#86805,#86806,#86807,#86808,
#86809,#86810,#86811,#86812,#86813,#86814,#86815,#86816,#86817,#86818,#86819,
#86820,#86821,#86822,#86823,#86824,#86825,#86826,#86827,#86828,#86829,#86830,
#86831,#86832,#86833,#86834,#86835,#86836,#86837,#86838,#86839,#86840,#86841,
#86842,#86843,#86844,#86845,#86846,#86847,#86848,#86849,#86850,#86851,#86852,
#86853,#86854,#86855,#86856,#86857,#86858,#86859,#86860,#86861,#86862,#86863,
#86864,#86865,#86866,#86867,#86868,#86869,#86870,#86871,#86872,#86873,#86874,
#86875,#86876,#86877,#86878,#86879,#86880,#86881,#86882,#86883,#86884,#86885,
#86886,#86887,#86888,#86889,#86890,#86891,#86892,#86893,#86894,#86895,#86896,
#86897,#86898,#86899,#86900,#86901,#86902,#86903,#86904,#86905,#86906,#86907,
#86908,#86909,#86910,#86911,#86912,#86913,#86914,#86915,#86916,#86917,#86918,
#86919,#86920,#86921,#86922,#86923,#86924,#86925,#86926,#86927,#86928,#86929,
#86930,#86931,#86932,#86933,#86934,#86935,#86936,#86937,#86938,#86939,#86940,
#86941,#86942,#86943,#86944,#86945,#86946,#86947,#86948,#86949,#86950,#86951,
#86952,#86953,#86954,#86955,#86956,#86957,#86958,#86959,#86960,#86961,#86962,
#86963,#86964,#86965,#86966,#86967,#86968,#86969,#86970,#86971,#86972,#86973,
#86974,#86975,#86976,#86977,#86978,#86979,#86980,#86981,#86982,#86983,#86984,
#86985,#86986,#86987,#86988,#86989,#86990,#86991,#86992,#86993,#86994,#86995,
#86996,#86997,#86998,#86999,#87000,#87001,#87002,#87003,#87004,#87005,#87006,
#87007,#87008,#87009,#87010,#87011,#87012),.UNSPECIFIED.,.F.,.F.,(4,3,3,
3,3,3,3,3,3,3,3,3,3,3,3,3,3,3,3,3,3,3,3,3,3,3,3,3,3,3,3,3,3,3,3,3,3,3,3,
3,3,3,3,3,3,3,3,3,3,3,3,3,3,3,3,3,3,3,3,3,3,3,3,3,3,3,3,3,3,3,3,3,3,4),
(958.185759344869,958.31309188077,958.365423671052,958.449162382898,958.532797894266,
958.616350337665,958.699839773516,958.78329372413,958.866730217977,958.950167327733,
959.033623122651,959.117167615381,959.200756698322,959.28447996588,959.365159681772,
959.448898393618,959.532533904985,959.616086348384,959.699575784235,959.783029734848,
959.866466228695,959.94990333845,960.033359133368,960.116903626097,960.200492709038,
960.284215976596,960.364895692492,960.448634404338,960.532269915705,960.615822359104,
960.699311794955,960.782765745568,960.866202239414,960.94963934917,961.033095144087,
961.116639636817,961.200228719758,961.283951987315,961.364631703212,961.448370415058,
961.532005926425,961.615558369824,961.699047805675,961.782501756288,961.865938250135,
961.94937535989,962.032831154807,962.116375647537,962.199964730478,962.283687998035,
962.364367713932,962.448106425778,962.531741937146,962.615294380545,962.698783816396,
962.78223776701,962.865674260857,962.949111370613,963.032567165531,963.11611165826,
963.199700741202,963.28342400876,963.364103724653,963.44785112012,963.531493382349,
963.617222592426,963.700707840529,963.784155280232,963.867582999968,963.955019015717,
964.038490818479,964.121991065998,964.205565530793,964.217327062966),
 .UNSPECIFIED.);
#663=B_SPLINE_CURVE_WITH_KNOTS('',3,(#87018,#87019,#87020,#87021,#87022,
#87023,#87024,#87025,#87026,#87027,#87028,#87029,#87030,#87031,#87032,#87033,
#87034,#87035,#87036,#87037,#87038,#87039,#87040,#87041,#87042,#87043,#87044,
#87045,#87046,#87047,#87048,#87049,#87050,#87051,#87052,#87053,#87054,#87055,
#87056,#87057,#87058,#87059,#87060,#87061,#87062,#87063,#87064,#87065,#87066,
#87067,#87068,#87069,#87070,#87071,#87072,#87073,#87074,#87075,#87076,#87077,
#87078,#87079,#87080,#87081,#87082,#87083,#87084,#87085,#87086,#87087,#87088,
#87089,#87090,#87091,#87092,#87093,#87094,#87095,#87096,#87097,#87098,#87099,
#87100,#87101,#87102,#87103,#87104,#87105,#87106,#87107,#87108,#87109,#87110,
#87111,#87112,#87113,#87114,#87115,#87116,#87117,#87118,#87119,#87120,#87121,
#87122,#87123,#87124,#87125,#87126,#87127,#87128,#87129,#87130,#87131,#87132,
#87133,#87134,#87135,#87136,#87137,#87138,#87139,#87140,#87141,#87142,#87143,
#87144,#87145,#87146,#87147,#87148,#87149,#87150,#87151,#87152,#87153,#87154,
#87155,#87156,#87157,#87158,#87159,#87160,#87161,#87162,#87163,#87164,#87165,
#87166,#87167,#87168,#87169,#87170,#87171,#87172,#87173,#87174,#87175,#87176,
#87177,#87178,#87179,#87180,#87181,#87182,#87183,#87184,#87185,#87186,#87187,
#87188,#87189,#87190,#87191,#87192,#87193,#87194,#87195,#87196,#87197,#87198,
#87199,#87200,#87201,#87202,#87203,#87204,#87205,#87206,#87207,#87208,#87209,
#87210,#87211,#87212,#87213,#87214,#87215,#87216,#87217,#87218,#87219,#87220,
#87221,#87222,#87223,#87224,#87225,#87226,#87227,#87228,#87229,#87230,#87231,
#87232,#87233,#87234,#87235,#87236,#87237),.UNSPECIFIED.,.F.,.F.,(4,3,3,
3,3,3,3,3,3,3,3,3,3,3,3,3,3,3,3,3,3,3,3,3,3,3,3,3,3,3,3,3,3,3,3,3,3,3,3,
3,3,3,3,3,3,3,3,3,3,3,3,3,3,3,3,3,3,3,3,3,3,3,3,3,3,3,3,3,3,3,3,3,3,4),
(964.468944652045,964.553856266707,964.63880056414,964.723793252019,964.80891241641,
964.894097600493,964.979440780856,965.053285126376,965.137023838222,965.220659349589,
965.304211792988,965.387701228839,965.471155179452,965.554591673298,965.638028783054,
965.721484577971,965.805029070701,965.888618153642,965.972341421199,966.053021137096,
966.136759848942,966.22039536031,966.303947803708,966.387437239559,966.470891190173,
966.554327684019,966.637764793774,966.721220588692,966.804765081422,966.888354164363,
966.972077431921,967.052757147816,967.136495859662,967.220131371029,967.303683814428,
967.387173250279,967.470627200893,967.554063694739,967.637500804495,967.720956599413,
967.804501092142,967.888090175083,967.971813442641,968.052493158536,968.136231870382,
968.219867381749,968.303419825148,968.386909260999,968.470363211613,968.553799705459,
968.637236815214,968.720692610132,968.804237102861,968.887826185802,968.97154945336,
969.052229169256,969.135967881102,969.219603392469,969.303155835867,969.386645271719,
969.470099222332,969.553535716179,969.636972825934,969.720428620852,969.803973113582,
969.887562196523,969.97128546408,970.051965179976,970.135211717693,970.218356428836,
970.301401588995,970.38438937538,970.467335833278,970.501020187744),
 .UNSPECIFIED.);
#664=B_SPLINE_CURVE_WITH_KNOTS('',3,(#87238,#87239,#87240,#87241,#87242,
#87243,#87244,#87245,#87246,#87247),.UNSPECIFIED.,.F.,.F.,(4,3,3,4),(964.218603001888,
964.31028798597,964.401596342216,964.468944651881),.UNSPECIFIED.);
#665=B_SPLINE_CURVE_WITH_KNOTS('',3,(#87249,#87250,#87251,#87252,#87253,
#87254,#87255,#87256,#87257,#87258),.UNSPECIFIED.,.F.,.F.,(4,3,3,4),(964.217327062966,
964.301056785927,964.363839735373,964.468944652048),.UNSPECIFIED.);
#666=B_SPLINE_CURVE_WITH_KNOTS('',3,(#87259,#87260,#87261,#87262,#87263,
#87264,#87265,#87266,#87267,#87268,#87269,#87270,#87271,#87272,#87273,#87274,
#87275,#87276,#87277,#87278,#87279,#87280,#87281,#87282,#87283,#87284,#87285,
#87286,#87287,#87288,#87289,#87290,#87291,#87292,#87293,#87294,#87295,#87296,
#87297,#87298,#87299,#87300,#87301,#87302,#87303,#87304,#87305,#87306,#87307,
#87308,#87309,#87310,#87311,#87312,#87313,#87314,#87315,#87316,#87317,#87318,
#87319,#87320,#87321,#87322,#87323,#87324,#87325,#87326,#87327,#87328,#87329,
#87330,#87331,#87332,#87333,#87334,#87335,#87336,#87337,#87338,#87339,#87340,
#87341,#87342,#87343,#87344,#87345,#87346,#87347,#87348,#87349,#87350,#87351,
#87352,#87353,#87354,#87355,#87356,#87357,#87358,#87359,#87360,#87361,#87362,
#87363,#87364,#87365,#87366,#87367,#87368,#87369,#87370,#87371,#87372,#87373,
#87374,#87375,#87376,#87377,#87378,#87379,#87380,#87381,#87382,#87383,#87384,
#87385,#87386,#87387,#87388,#87389,#87390,#87391,#87392,#87393,#87394,#87395,
#87396,#87397,#87398,#87399,#87400,#87401,#87402,#87403,#87404,#87405,#87406,
#87407,#87408,#87409,#87410,#87411,#87412,#87413,#87414,#87415,#87416,#87417,
#87418,#87419,#87420,#87421,#87422,#87423,#87424,#87425,#87426,#87427,#87428,
#87429,#87430,#87431,#87432,#87433,#87434,#87435,#87436,#87437,#87438,#87439,
#87440,#87441,#87442,#87443,#87444,#87445,#87446,#87447,#87448,#87449,#87450,
#87451,#87452,#87453,#87454,#87455,#87456,#87457,#87458,#87459,#87460,#87461,
#87462,#87463,#87464,#87465,#87466,#87467,#87468,#87469,#87470,#87471,#87472,
#87473,#87474,#87475,#87476,#87477,#87478),.UNSPECIFIED.,.F.,.F.,(4,3,3,
3,3,3,3,3,3,3,3,3,3,3,3,3,3,3,3,3,3,3,3,3,3,3,3,3,3,3,3,3,3,3,3,3,3,3,3,
3,3,3,3,3,3,3,3,3,3,3,3,3,3,3,3,3,3,3,3,3,3,3,3,3,3,3,3,3,3,3,3,3,3,4),
(964.468944652184,964.551551735966,964.634067131806,964.716511902131,964.798911934073,
964.881289359624,964.963663110529,965.046052113148,965.128524838076,965.211040693846,
965.293684956907,965.363575746093,965.447314457939,965.530949969307,965.614502412705,
965.697991848556,965.78144579917,965.864882293016,965.948319402772,966.031775197689,
966.115319690419,966.19890877336,966.282632040918,966.363311756813,966.447050468659,
966.530685980026,966.614238423425,966.697727859276,966.78118180989,966.864618303736,
966.948055413491,967.031511208409,967.115055701138,967.198644784079,967.282368051637,
967.363047767533,967.446786479379,967.530421990746,967.613974434145,967.697463869996,
967.780917820609,967.864354314456,967.947791424211,968.031247219128,968.114791711858,
968.198380794799,968.282104062356,968.362783778253,968.446522490099,968.530158001466,
968.613710444865,968.697199880717,968.78065383133,968.864090325176,968.947527434932,
969.03098322985,969.114527722579,969.19811680552,969.281840073078,969.362519788973,
969.446258500819,969.529894012187,969.613446455585,969.696935891436,969.78038984205,
969.863826335896,969.947263445651,970.030719240569,970.114263733299,970.19785281624,
970.281576083798,970.362255799693,970.45608696417,970.501731614662),
 .UNSPECIFIED.);
#667=B_SPLINE_CURVE_WITH_KNOTS('',3,(#87484,#87485,#87486,#87487,#87488,
#87489,#87490,#87491,#87492,#87493,#87494,#87495,#87496,#87497,#87498,#87499,
#87500,#87501,#87502,#87503,#87504,#87505,#87506,#87507,#87508,#87509,#87510,
#87511,#87512,#87513,#87514,#87515,#87516,#87517,#87518,#87519,#87520,#87521,
#87522,#87523,#87524,#87525,#87526,#87527,#87528,#87529,#87530,#87531,#87532,
#87533,#87534,#87535,#87536,#87537,#87538,#87539,#87540,#87541,#87542,#87543,
#87544,#87545,#87546,#87547,#87548,#87549,#87550,#87551,#87552,#87553,#87554,
#87555,#87556,#87557,#87558,#87559,#87560,#87561,#87562,#87563,#87564,#87565,
#87566,#87567,#87568,#87569,#87570,#87571,#87572,#87573,#87574,#87575,#87576,
#87577,#87578,#87579,#87580,#87581,#87582,#87583,#87584,#87585,#87586,#87587,
#87588,#87589,#87590,#87591,#87592,#87593,#87594,#87595,#87596,#87597,#87598,
#87599,#87600,#87601,#87602,#87603,#87604,#87605,#87606,#87607,#87608,#87609,
#87610,#87611,#87612,#87613,#87614,#87615,#87616,#87617,#87618,#87619,#87620,
#87621,#87622,#87623,#87624,#87625,#87626,#87627,#87628,#87629,#87630,#87631,
#87632,#87633,#87634,#87635,#87636,#87637,#87638,#87639,#87640,#87641,#87642,
#87643,#87644,#87645,#87646,#87647,#87648,#87649,#87650,#87651,#87652,#87653,
#87654,#87655,#87656,#87657,#87658,#87659,#87660,#87661,#87662,#87663,#87664,
#87665,#87666,#87667,#87668,#87669,#87670,#87671,#87672,#87673,#87674,#87675,
#87676,#87677,#87678,#87679,#87680,#87681,#87682,#87683,#87684,#87685,#87686,
#87687,#87688,#87689,#87690,#87691,#87692,#87693,#87694,#87695,#87696,#87697,
#87698,#87699,#87700),.UNSPECIFIED.,.F.,.F.,(4,3,3,3,3,3,3,3,3,3,3,3,3,
3,3,3,3,3,3,3,3,3,3,3,3,3,3,3,3,3,3,3,3,3,3,3,3,3,3,3,3,3,3,3,3,3,3,3,3,
3,3,3,3,3,3,3,3,3,3,3,3,3,3,3,3,3,3,3,3,3,3,3,4),(970.75212995937,970.852730002883,
970.954662619401,971.051701190697,971.135439902543,971.219075413911,971.302627857309,
971.38611729316,971.469571243774,971.55300773762,971.636444847375,971.719900642293,
971.803445135023,971.887034217964,971.970757485521,972.051437201417,972.135175913263,
972.21881142463,972.302363868029,972.38585330388,972.469307254493,972.552743748339,
972.636180858095,972.719636653013,972.803181145742,972.886770228683,972.970493496241,
973.051173212137,973.134911923983,973.218547435351,973.302099878749,973.3855893146,
973.469043265214,973.55247975906,973.635916868816,973.719372663734,973.802917156463,
973.886506239404,973.970229506962,974.050909222857,974.134647934703,974.21828344607,
974.301835889469,974.38532532532,974.468779275933,974.55221576978,974.635652879535,
974.719108674453,974.802653167182,974.886242250123,974.969965517681,975.050645233577,
975.134383945423,975.218019456791,975.301571900189,975.38506133604,975.468515286654,
975.5519517805,975.635388890256,975.718844685174,975.802389177903,975.885978260844,
975.969701528402,976.050381244297,976.133920743387,976.217328062945,976.300659096788,
976.383932211667,976.467165730121,976.550395339485,976.633620000805,976.716891664386,
976.783605650254),.UNSPECIFIED.);
#668=B_SPLINE_CURVE_WITH_KNOTS('',3,(#87701,#87702,#87703,#87704,#87705,
#87706,#87707,#87708,#87709,#87710),.UNSPECIFIED.,.F.,.F.,(4,3,3,4),(970.501020187744,
970.583952002451,970.668040980838,970.752129959224),.UNSPECIFIED.);
#669=B_SPLINE_CURVE_WITH_KNOTS('',3,(#87712,#87713,#87714,#87715,#87716,
#87717,#87718,#87719,#87720,#87721),.UNSPECIFIED.,.F.,.F.,(4,3,3,4),(970.501731614662,
970.595066006553,970.687917748817,970.752129959041),.UNSPECIFIED.);
#670=B_SPLINE_CURVE_WITH_KNOTS('',3,(#87722,#87723,#87724,#87725,#87726,
#87727,#87728,#87729,#87730,#87731,#87732,#87733,#87734,#87735,#87736,#87737,
#87738,#87739,#87740,#87741,#87742,#87743,#87744,#87745,#87746,#87747,#87748,
#87749,#87750,#87751,#87752,#87753,#87754,#87755,#87756,#87757,#87758,#87759,
#87760,#87761,#87762,#87763,#87764,#87765,#87766,#87767,#87768,#87769,#87770,
#87771,#87772,#87773,#87774,#87775,#87776,#87777,#87778,#87779,#87780,#87781,
#87782,#87783,#87784,#87785,#87786,#87787,#87788,#87789,#87790,#87791,#87792,
#87793,#87794,#87795,#87796,#87797,#87798,#87799,#87800,#87801,#87802,#87803,
#87804,#87805,#87806,#87807,#87808,#87809,#87810,#87811,#87812,#87813,#87814,
#87815,#87816,#87817,#87818,#87819,#87820,#87821,#87822,#87823,#87824,#87825,
#87826,#87827,#87828,#87829,#87830,#87831,#87832,#87833,#87834,#87835,#87836,
#87837,#87838,#87839,#87840,#87841,#87842,#87843,#87844,#87845,#87846,#87847,
#87848,#87849,#87850,#87851,#87852,#87853,#87854,#87855,#87856,#87857,#87858,
#87859,#87860,#87861,#87862,#87863,#87864,#87865,#87866,#87867,#87868,#87869,
#87870,#87871,#87872,#87873,#87874,#87875,#87876,#87877,#87878,#87879,#87880,
#87881,#87882,#87883,#87884,#87885,#87886,#87887,#87888,#87889,#87890,#87891,
#87892,#87893,#87894,#87895,#87896,#87897,#87898,#87899,#87900,#87901,#87902,
#87903,#87904,#87905,#87906,#87907,#87908,#87909,#87910,#87911,#87912,#87913,
#87914,#87915,#87916,#87917,#87918,#87919,#87920,#87921,#87922,#87923,#87924,
#87925,#87926,#87927,#87928,#87929,#87930,#87931,#87932,#87933,#87934,#87935,
#87936,#87937,#87938,#87939,#87940,#87941),.UNSPECIFIED.,.F.,.F.,(4,3,3,
3,3,3,3,3,3,3,3,3,3,3,3,3,3,3,3,3,3,3,3,3,3,3,3,3,3,3,3,3,3,3,3,3,3,3,3,
3,3,3,3,3,3,3,3,3,3,3,3,3,3,3,3,3,3,3,3,3,3,3,3,3,3,3,3,3,3,3,3,3,3,4),
(970.752129959228,970.836483591065,970.920853204787,971.005255525662,971.089707297296,
971.174275812516,971.258913586583,971.343683363136,971.361991810414,971.44573052226,
971.529366033628,971.612918477026,971.696407912877,971.779861863491,971.863298357337,
971.946735467092,972.03019126201,972.11373575474,972.197324837681,972.281048105238,
972.361727821134,972.44546653298,972.529102044347,972.612654487746,972.696143923597,
972.779597874211,972.863034368057,972.946471477812,973.02992727273,973.11347176546,
973.197060848401,973.280784115958,973.361463831854,973.4452025437,973.528838055067,
973.612390498466,973.695879934317,973.779333884931,973.862770378777,973.946207488532,
974.02966328345,974.113207776179,974.19679685912,974.280520126678,974.361199842574,
974.44493855442,974.528574065787,974.612126509186,974.695615945037,974.779069895651,
974.862506389497,974.945943499252,975.02939929417,975.112943786899,975.19653286984,
975.280256137398,975.360935853294,975.44467456514,975.528310076508,975.611862519906,
975.695351955757,975.778805906371,975.862242400217,975.945679509972,976.02913530489,
976.11267979762,976.196268880561,976.279992148118,976.360671864014,976.444260174154,
976.52927975058,976.612658217677,976.698498348767,976.784338479856),
 .UNSPECIFIED.);
#671=B_SPLINE_CURVE_WITH_KNOTS('',3,(#87947,#87948,#87949,#87950,#87951,
#87952,#87953,#87954,#87955,#87956,#87957,#87958,#87959,#87960,#87961,#87962,
#87963,#87964,#87965,#87966,#87967,#87968,#87969,#87970,#87971,#87972,#87973,
#87974,#87975,#87976,#87977,#87978,#87979,#87980,#87981,#87982,#87983,#87984,
#87985,#87986,#87987,#87988,#87989,#87990,#87991,#87992,#87993,#87994,#87995,
#87996,#87997,#87998,#87999,#88000,#88001,#88002,#88003,#88004,#88005,#88006,
#88007,#88008,#88009,#88010,#88011,#88012,#88013,#88014,#88015,#88016,#88017,
#88018,#88019,#88020,#88021,#88022,#88023,#88024,#88025,#88026,#88027,#88028,
#88029,#88030,#88031,#88032,#88033,#88034,#88035,#88036,#88037,#88038,#88039,
#88040,#88041,#88042,#88043,#88044,#88045,#88046,#88047,#88048,#88049,#88050,
#88051,#88052,#88053,#88054,#88055,#88056,#88057,#88058,#88059,#88060,#88061,
#88062,#88063,#88064,#88065,#88066,#88067,#88068,#88069,#88070,#88071,#88072,
#88073,#88074,#88075,#88076,#88077,#88078,#88079,#88080,#88081,#88082,#88083,
#88084,#88085,#88086,#88087,#88088,#88089,#88090,#88091,#88092,#88093,#88094,
#88095,#88096,#88097,#88098,#88099,#88100,#88101,#88102,#88103,#88104,#88105,
#88106,#88107,#88108,#88109,#88110,#88111,#88112,#88113,#88114,#88115,#88116,
#88117,#88118,#88119,#88120,#88121,#88122,#88123,#88124,#88125,#88126,#88127,
#88128,#88129,#88130,#88131,#88132,#88133,#88134,#88135,#88136,#88137,#88138,
#88139,#88140,#88141,#88142,#88143,#88144,#88145,#88146,#88147,#88148,#88149,
#88150,#88151,#88152,#88153,#88154,#88155,#88156,#88157,#88158,#88159,#88160,
#88161,#88162,#88163,#88164,#88165,#88166,#88167,#88168,#88169),
 .UNSPECIFIED.,.F.,.F.,(4,3,3,3,3,3,3,3,3,3,3,3,3,3,3,3,3,3,3,3,3,3,3,3,
3,3,3,3,3,3,3,3,3,3,3,3,3,3,3,3,3,3,3,3,3,3,3,3,3,3,3,3,3,3,3,3,3,3,3,3,
3,3,3,3,3,3,3,3,3,3,3,3,3,3,4),(977.035315266404,977.050117255017,977.133855966863,
977.217491478231,977.30104392163,977.384533357481,977.467987308095,977.551423801942,
977.634860911698,977.718316706616,977.801861199346,977.885450282287,977.969173549845,
978.049853265738,978.133591977584,978.217227488951,978.30077993235,978.384269368201,
978.467723318814,978.55115981266,978.634596922416,978.718052717333,978.801597210063,
978.885186293004,978.968909560561,979.049589276458,979.133327988304,979.216963499671,
979.30051594307,979.384005378921,979.467459329534,979.55089582338,979.634332933136,
979.717788728053,979.801333220783,979.884922303724,979.968645571281,980.049325287178,
980.133063999024,980.216699510392,980.30025195379,980.383741389641,980.467195340255,
980.550631834101,980.634068943857,980.717524738775,980.801069231504,980.884658314445,
980.968381582003,981.049061297898,981.132800009744,981.216435521112,981.29998796451,
981.383477400361,981.466931350975,981.550367844821,981.633804954576,981.717260749494,
981.800805242224,981.884394325165,981.968117592722,982.048797308618,982.132536020464,
982.216171531831,982.29972397523,982.383213411081,982.466667361694,982.550103855541,
982.633540965296,982.716996760214,982.800541252943,982.884130335884,982.967853603442,
983.048533319338,983.067552096354),.UNSPECIFIED.);
#672=B_SPLINE_CURVE_WITH_KNOTS('',3,(#88170,#88171,#88172,#88173,#88174,
#88175,#88176,#88177,#88178,#88179),.UNSPECIFIED.,.F.,.F.,(4,3,3,4),(976.783605650254,
976.866976135685,976.951145700975,977.035315266264),.UNSPECIFIED.);
#673=B_SPLINE_CURVE_WITH_KNOTS('',3,(#88181,#88182,#88183,#88184,#88185,
#88186,#88187,#88188,#88189,#88190),.UNSPECIFIED.,.F.,.F.,(4,3,3,4),(976.784338479856,
976.867591013031,976.95145313972,977.035315266408),.UNSPECIFIED.);
#674=B_SPLINE_CURVE_WITH_KNOTS('',3,(#88191,#88192,#88193,#88194,#88195,
#88196,#88197,#88198,#88199,#88200,#88201,#88202,#88203,#88204,#88205,#88206,
#88207,#88208,#88209,#88210,#88211,#88212,#88213,#88214,#88215,#88216,#88217,
#88218,#88219,#88220,#88221,#88222,#88223,#88224,#88225,#88226,#88227,#88228,
#88229,#88230,#88231,#88232,#88233,#88234,#88235,#88236,#88237,#88238,#88239,
#88240,#88241,#88242,#88243,#88244,#88245,#88246,#88247,#88248,#88249,#88250,
#88251,#88252,#88253,#88254,#88255,#88256,#88257,#88258,#88259,#88260,#88261,
#88262,#88263,#88264,#88265,#88266,#88267,#88268,#88269,#88270,#88271,#88272,
#88273,#88274,#88275,#88276,#88277,#88278,#88279,#88280,#88281,#88282,#88283,
#88284,#88285,#88286,#88287,#88288,#88289,#88290,#88291,#88292,#88293,#88294,
#88295,#88296,#88297,#88298,#88299,#88300,#88301,#88302,#88303,#88304,#88305,
#88306,#88307,#88308,#88309,#88310,#88311,#88312,#88313,#88314,#88315,#88316,
#88317,#88318,#88319,#88320,#88321,#88322,#88323,#88324,#88325,#88326,#88327,
#88328,#88329,#88330,#88331,#88332,#88333,#88334,#88335,#88336,#88337,#88338,
#88339,#88340,#88341,#88342,#88343,#88344,#88345,#88346,#88347,#88348,#88349,
#88350,#88351,#88352,#88353,#88354,#88355,#88356,#88357,#88358,#88359,#88360,
#88361,#88362,#88363,#88364,#88365,#88366,#88367,#88368,#88369,#88370,#88371,
#88372,#88373,#88374,#88375,#88376,#88377,#88378,#88379,#88380,#88381,#88382,
#88383,#88384,#88385,#88386,#88387,#88388,#88389,#88390,#88391,#88392,#88393,
#88394,#88395,#88396,#88397,#88398,#88399,#88400,#88401,#88402,#88403,#88404,
#88405,#88406,#88407,#88408,#88409,#88410),.UNSPECIFIED.,.F.,.F.,(4,3,3,
3,3,3,3,3,3,3,3,3,3,3,3,3,3,3,3,3,3,3,3,3,3,3,3,3,3,3,3,3,3,3,3,3,3,3,3,
3,3,3,3,3,3,3,3,3,3,3,3,3,3,3,3,3,3,3,3,3,3,3,3,3,3,3,3,3,3,3,3,3,3,4),
(977.035315266588,977.133307139005,977.231938308519,977.331290940343,977.360407874734,
977.444146586581,977.527782097949,977.611334541349,977.694823977201,977.778277927815,
977.861714421662,977.945151531419,978.028607326338,978.112151819068,978.19574090201,
978.279464169569,978.360143885455,978.443882597301,978.527518108668,978.611070552067,
978.694559987918,978.778013938531,978.861450432378,978.944887542133,979.028343337051,
979.11188782978,979.195476912721,979.279200180279,979.359879896175,979.443618608021,
979.527254119388,979.610806562786,979.694295998637,979.777749949251,979.861186443097,
979.944623552852,980.028079347769,980.111623840499,980.19521292344,980.278936190997,
980.359615906895,980.443354618741,980.526990130109,980.610542573507,980.694032009358,
980.777485959972,980.860922453818,980.944359563574,981.027815358491,981.111359851221,
981.194948934162,981.27867220172,981.359351917615,981.443090629461,981.526726140828,
981.610278584227,981.693768020078,981.777221970692,981.860658464538,981.944095574294,
982.027551369211,982.111095861941,982.194684944882,982.27840821244,982.359087928335,
982.442307253171,982.525395131154,982.60840709754,982.691361790686,982.774277803087,
982.857189163963,982.940097001489,983.023046132135,983.06671526311),
 .UNSPECIFIED.);
#675=B_SPLINE_CURVE_WITH_KNOTS('',3,(#88416,#88417,#88418,#88419,#88420,
#88421,#88422,#88423,#88424,#88425,#88426,#88427,#88428,#88429,#88430,#88431,
#88432,#88433,#88434,#88435,#88436,#88437,#88438,#88439,#88440,#88441,#88442,
#88443,#88444,#88445,#88446,#88447,#88448,#88449,#88450,#88451,#88452,#88453,
#88454,#88455,#88456,#88457,#88458,#88459,#88460,#88461,#88462,#88463,#88464,
#88465,#88466,#88467,#88468,#88469,#88470,#88471,#88472,#88473,#88474,#88475,
#88476,#88477,#88478,#88479,#88480,#88481,#88482,#88483,#88484,#88485,#88486,
#88487,#88488,#88489,#88490,#88491,#88492,#88493,#88494,#88495,#88496,#88497,
#88498,#88499,#88500,#88501,#88502,#88503,#88504,#88505,#88506,#88507,#88508,
#88509,#88510,#88511,#88512,#88513,#88514,#88515,#88516,#88517,#88518,#88519,
#88520,#88521,#88522,#88523,#88524,#88525,#88526,#88527,#88528,#88529,#88530,
#88531,#88532,#88533,#88534,#88535,#88536,#88537,#88538,#88539,#88540,#88541,
#88542,#88543,#88544,#88545,#88546,#88547,#88548,#88549,#88550,#88551,#88552,
#88553,#88554,#88555,#88556,#88557,#88558,#88559,#88560,#88561,#88562,#88563,
#88564,#88565,#88566,#88567,#88568,#88569,#88570,#88571,#88572,#88573,#88574,
#88575,#88576,#88577,#88578,#88579,#88580,#88581,#88582,#88583,#88584,#88585,
#88586,#88587,#88588,#88589,#88590,#88591,#88592,#88593,#88594,#88595,#88596,
#88597,#88598,#88599,#88600,#88601,#88602,#88603,#88604,#88605,#88606,#88607,
#88608,#88609,#88610,#88611,#88612,#88613,#88614,#88615,#88616,#88617,#88618,
#88619,#88620,#88621,#88622,#88623,#88624,#88625,#88626,#88627,#88628,#88629,
#88630,#88631,#88632,#88633,#88634,#88635),.UNSPECIFIED.,.F.,.F.,(4,3,3,
3,3,3,3,3,3,3,3,3,3,3,3,3,3,3,3,3,3,3,3,3,3,3,3,3,3,3,3,3,3,3,3,3,3,3,3,
3,3,3,3,3,3,3,3,3,3,3,3,3,3,3,3,3,3,3,3,3,3,3,3,3,3,3,3,3,3,3,3,3,3,4),
(983.318500573583,983.401198681688,983.48385736056,983.566496688037,983.649135402762,
983.731792239955,983.814536138504,983.897325350184,983.980244593793,984.048269330058,
984.132008041904,984.215643553272,984.299195996671,984.382685432522,984.466139383136,
984.549575876982,984.633012986738,984.716468781656,984.800013274386,984.883602357327,
984.967325624885,985.048005340779,985.131744052625,985.215379563992,985.298932007391,
985.382421443242,985.465875393856,985.549311887702,985.632748997458,985.716204792375,
985.799749285105,985.883338368046,985.967061635603,986.047741351499,986.131480063345,
986.215115574712,986.298668018111,986.382157453962,986.465611404576,986.549047898422,
986.632485008177,986.715940803095,986.799485295824,986.883074378765,986.966797646323,
987.047477362219,987.131216074065,987.214851585432,987.298404028831,987.381893464682,
987.465347415296,987.548783909142,987.632221018897,987.715676813815,987.799221306545,
987.882810389486,987.966533657043,988.047213372939,988.130952084785,988.214587596152,
988.298140039551,988.381629475402,988.465083426015,988.548519919862,988.631957029617,
988.715412824534,988.798957317263,988.882546400204,988.966269667762,989.046949383659,
989.133108389705,989.219154270956,989.305066936171,989.351233245849),
 .UNSPECIFIED.);
#676=B_SPLINE_CURVE_WITH_KNOTS('',3,(#88636,#88637,#88638,#88639,#88640,
#88641,#88642,#88643,#88644,#88645),.UNSPECIFIED.,.F.,.F.,(4,3,3,4),(983.067552096354,
983.173712335231,983.278061473153,983.318500573403),.UNSPECIFIED.);
#677=B_SPLINE_CURVE_WITH_KNOTS('',3,(#88647,#88648,#88649,#88650,#88651,
#88652,#88653,#88654,#88655,#88656),.UNSPECIFIED.,.F.,.F.,(4,3,3,4),(983.06671526311,
983.14975902426,983.234129798838,983.318500573417),.UNSPECIFIED.);
#678=B_SPLINE_CURVE_WITH_KNOTS('',3,(#88657,#88658,#88659,#88660,#88661,
#88662,#88663,#88664,#88665,#88666,#88667,#88668,#88669,#88670,#88671,#88672,
#88673,#88674,#88675,#88676,#88677,#88678,#88679,#88680,#88681,#88682,#88683,
#88684,#88685,#88686,#88687,#88688,#88689,#88690,#88691,#88692,#88693,#88694,
#88695,#88696,#88697,#88698,#88699,#88700,#88701,#88702,#88703,#88704,#88705,
#88706,#88707,#88708,#88709,#88710,#88711,#88712,#88713,#88714,#88715,#88716,
#88717,#88718,#88719,#88720,#88721,#88722,#88723,#88724,#88725,#88726,#88727,
#88728,#88729,#88730,#88731,#88732,#88733,#88734,#88735,#88736,#88737,#88738,
#88739,#88740,#88741,#88742,#88743,#88744,#88745,#88746,#88747,#88748,#88749,
#88750,#88751,#88752,#88753,#88754,#88755,#88756,#88757,#88758,#88759,#88760,
#88761,#88762,#88763,#88764,#88765,#88766,#88767,#88768,#88769,#88770,#88771,
#88772,#88773,#88774,#88775,#88776,#88777,#88778,#88779,#88780,#88781,#88782,
#88783,#88784,#88785,#88786,#88787,#88788,#88789,#88790,#88791,#88792,#88793,
#88794,#88795,#88796,#88797,#88798,#88799,#88800,#88801,#88802,#88803,#88804,
#88805,#88806,#88807,#88808,#88809,#88810,#88811,#88812,#88813,#88814,#88815,
#88816,#88817,#88818,#88819,#88820,#88821,#88822,#88823,#88824,#88825,#88826,
#88827,#88828,#88829,#88830,#88831,#88832,#88833,#88834,#88835,#88836,#88837,
#88838,#88839,#88840,#88841,#88842,#88843,#88844,#88845,#88846,#88847,#88848,
#88849,#88850,#88851,#88852,#88853,#88854,#88855,#88856,#88857,#88858,#88859,
#88860,#88861,#88862,#88863,#88864,#88865,#88866,#88867,#88868,#88869,#88870,
#88871,#88872,#88873,#88874,#88875,#88876),.UNSPECIFIED.,.F.,.F.,(4,3,3,
3,3,3,3,3,3,3,3,3,3,3,3,3,3,3,3,3,3,3,3,3,3,3,3,3,3,3,3,3,3,3,3,3,3,3,3,
3,3,3,3,3,3,3,3,3,3,3,3,3,3,3,3,3,3,3,3,3,3,3,3,3,3,3,3,3,3,3,3,3,3,4),
(983.318500573587,983.358823939055,983.442562650901,983.526198162268,983.609750605667,
983.693240041518,983.776693992131,983.860130485977,983.943567595733,984.027023390651,
984.11056788338,984.194156966321,984.277880233879,984.358559949775,984.442298661621,
984.525934172989,984.609486616387,984.692976052239,984.776430002853,984.859866496699,
984.943303606454,985.026759401372,985.110303894102,985.193892977043,985.277616244601,
985.358295960496,985.442034672342,985.525670183709,985.609222627108,985.692712062959,
985.776166013572,985.859602507418,985.943039617174,986.026495412092,986.110039904821,
986.193628987762,986.27735225532,986.358031971216,986.441770683062,986.525406194429,
986.608958637828,986.692448073679,986.775902024293,986.859338518139,986.942775627895,
987.026231422812,987.109775915542,987.193364998483,987.277088266041,987.357767981936,
987.441506693782,987.52514220515,987.608694648548,987.692184084399,987.775638035013,
987.859074528859,987.942511638614,988.025967433532,988.109511926262,988.193101009202,
988.27682427676,988.357503992656,988.441243078456,988.524878875936,988.608431517975,
988.691921065274,988.775374670802,988.858810695376,988.942247211585,989.025702288485,
989.109244315567,989.192830881534,989.276547488672,989.35057976761),
 .UNSPECIFIED.);
#679=B_SPLINE_CURVE_WITH_KNOTS('',3,(#88882,#88883,#88884,#88885,#88886,
#88887,#88888,#88889,#88890,#88891,#88892,#88893,#88894,#88895,#88896,#88897,
#88898,#88899,#88900,#88901,#88902,#88903,#88904,#88905,#88906,#88907,#88908,
#88909,#88910,#88911,#88912,#88913,#88914,#88915,#88916,#88917,#88918,#88919,
#88920,#88921,#88922,#88923,#88924,#88925,#88926,#88927,#88928,#88929,#88930,
#88931,#88932,#88933,#88934,#88935,#88936,#88937,#88938,#88939,#88940,#88941,
#88942,#88943,#88944,#88945,#88946,#88947,#88948,#88949,#88950,#88951,#88952,
#88953,#88954,#88955,#88956,#88957,#88958,#88959,#88960,#88961,#88962,#88963,
#88964,#88965,#88966,#88967,#88968,#88969,#88970,#88971,#88972,#88973,#88974,
#88975,#88976,#88977,#88978,#88979,#88980,#88981,#88982,#88983,#88984,#88985,
#88986,#88987,#88988,#88989,#88990,#88991,#88992,#88993,#88994,#88995,#88996,
#88997,#88998,#88999,#89000,#89001,#89002,#89003,#89004,#89005,#89006,#89007,
#89008,#89009,#89010,#89011,#89012,#89013,#89014,#89015,#89016,#89017,#89018,
#89019,#89020,#89021,#89022,#89023,#89024,#89025,#89026,#89027,#89028,#89029,
#89030,#89031,#89032,#89033,#89034,#89035,#89036,#89037,#89038,#89039,#89040,
#89041,#89042,#89043,#89044,#89045,#89046,#89047,#89048,#89049,#89050,#89051,
#89052,#89053,#89054,#89055,#89056,#89057,#89058,#89059,#89060,#89061,#89062,
#89063,#89064,#89065,#89066,#89067,#89068,#89069,#89070,#89071,#89072,#89073,
#89074,#89075,#89076,#89077,#89078,#89079,#89080,#89081,#89082,#89083,#89084,
#89085,#89086,#89087,#89088,#89089,#89090,#89091,#89092,#89093,#89094,#89095,
#89096,#89097,#89098,#89099,#89100,#89101),.UNSPECIFIED.,.F.,.F.,(4,3,3,
3,3,3,3,3,3,3,3,3,3,3,3,3,3,3,3,3,3,3,3,3,3,3,3,3,3,3,3,3,3,3,3,3,3,3,3,
3,3,3,3,3,3,3,3,3,3,3,3,3,3,3,3,3,3,3,3,3,3,3,3,3,3,3,3,3,3,3,3,3,3,4),
(989.601685880876,989.691372748879,989.781398721669,989.871593799813,989.962075667513,
990.046685394379,990.130424106225,990.214059617593,990.297612060992,990.381101496843,
990.464555447457,990.547991941303,990.631429051059,990.714884845977,990.798429338707,
990.882018421648,990.965741689206,991.046421405099,991.130160116945,991.213795628312,
991.297348071711,991.380837507562,991.464291458175,991.547727952021,991.631165061777,
991.714620856694,991.798165349424,991.881754432365,991.965477699922,992.046157415819,
992.129896127665,992.213531639033,992.297084082431,992.380573518283,992.464027468896,
992.547463962743,992.630901072498,992.714356867416,992.797901360146,992.881490443087,
992.965213710645,993.04589342654,993.129632138386,993.213267649754,993.296820093152,
993.380309529003,993.463763479617,993.547199973463,993.630637083219,993.714092878137,
993.797637370866,993.881226453807,993.964949721365,994.04562943726,994.129368149106,
994.213003660473,994.296556103872,994.380045539723,994.463499490336,994.546935984183,
994.630373093938,994.713828888855,994.797373381585,994.880962464526,994.964685732083,
995.04536544798,995.127838516808,995.210216422072,995.292518381979,995.377675088007,
995.459886036772,995.542079644179,995.624285367826,995.63314520609),
 .UNSPECIFIED.);
#680=B_SPLINE_CURVE_WITH_KNOTS('',3,(#89102,#89103,#89104,#89105,#89106,
#89107,#89108,#89109,#89110,#89111),.UNSPECIFIED.,.F.,.F.,(4,3,3,4),(989.351233245849,
989.436996731148,989.522677717496,989.601685880763),.UNSPECIFIED.);
#681=B_SPLINE_CURVE_WITH_KNOTS('',3,(#89113,#89114,#89115,#89116,#89117,
#89118,#89119,#89120,#89121,#89122,#89123,#89124,#89125),.UNSPECIFIED.,
 .F.,.F.,(4,3,3,3,4),(989.35057976761,989.357240003376,989.468145220993,
989.576452495159,989.601685880647),.UNSPECIFIED.);
#682=B_SPLINE_CURVE_WITH_KNOTS('',3,(#89126,#89127,#89128,#89129,#89130,
#89131,#89132,#89133,#89134,#89135,#89136,#89137,#89138,#89139,#89140,#89141,
#89142,#89143,#89144,#89145,#89146,#89147,#89148,#89149,#89150,#89151,#89152,
#89153,#89154,#89155,#89156,#89157,#89158,#89159,#89160,#89161,#89162,#89163,
#89164,#89165,#89166,#89167,#89168,#89169,#89170,#89171,#89172,#89173,#89174,
#89175,#89176,#89177,#89178,#89179,#89180,#89181,#89182,#89183,#89184,#89185,
#89186,#89187,#89188,#89189,#89190,#89191,#89192,#89193,#89194,#89195,#89196,
#89197,#89198,#89199,#89200,#89201,#89202,#89203,#89204,#89205,#89206,#89207,
#89208,#89209,#89210,#89211,#89212,#89213,#89214,#89215,#89216,#89217,#89218,
#89219,#89220,#89221,#89222,#89223,#89224,#89225,#89226,#89227,#89228,#89229,
#89230,#89231,#89232,#89233,#89234,#89235,#89236,#89237,#89238,#89239,#89240,
#89241,#89242,#89243,#89244,#89245,#89246,#89247,#89248,#89249,#89250,#89251,
#89252,#89253,#89254,#89255,#89256,#89257,#89258,#89259,#89260,#89261,#89262,
#89263,#89264,#89265,#89266,#89267,#89268,#89269,#89270,#89271,#89272,#89273,
#89274,#89275,#89276,#89277,#89278,#89279,#89280,#89281,#89282,#89283,#89284,
#89285,#89286,#89287,#89288,#89289,#89290,#89291,#89292,#89293,#89294,#89295,
#89296,#89297,#89298,#89299,#89300,#89301,#89302,#89303,#89304,#89305,#89306,
#89307,#89308,#89309,#89310,#89311,#89312,#89313,#89314,#89315,#89316,#89317,
#89318,#89319,#89320,#89321,#89322,#89323,#89324,#89325,#89326,#89327,#89328,
#89329,#89330,#89331,#89332,#89333,#89334,#89335,#89336,#89337,#89338,#89339,
#89340,#89341,#89342,#89343,#89344,#89345),.UNSPECIFIED.,.F.,.F.,(4,3,3,
3,3,3,3,3,3,3,3,3,3,3,3,3,3,3,3,3,3,3,3,3,3,3,3,3,3,3,3,3,3,3,3,3,3,3,3,
3,3,3,3,3,3,3,3,3,3,3,3,3,3,3,3,3,3,3,3,3,3,3,3,3,3,3,3,3,3,3,3,3,3,4),
(989.601685880767,989.684216864866,989.768311758519,989.850763033228,989.933206082506,
990.015659782248,990.10098884021,990.183564952774,990.270270483435,990.356976014096,
990.440714725942,990.524350237309,990.607902680708,990.691392116559,990.774846067173,
990.858282561019,990.941719670774,991.025175465692,991.108719958422,991.192309041363,
991.27603230892,991.356712024816,991.440450736662,991.52408624803,991.607638691428,
991.691128127279,991.774582077893,991.858018571739,991.941455681495,992.024911476413,
992.108455969142,992.192045052083,992.275768319641,992.356448035536,992.440186747382,
992.523822258749,992.607374702147,992.690864137998,992.774318088612,992.857754582458,
992.941191692213,993.02464748713,993.10819197986,993.191781062801,993.275504330358,
993.356184046256,993.439922758102,993.52355826947,993.607110712868,993.690600148719,
993.774054099333,993.857490593179,993.940927702935,994.024383497852,994.107927990582,
994.191517073524,994.275240341081,994.355920056977,994.439658768823,994.52329428019,
994.606846723589,994.690336159441,994.773790110055,994.857226603901,994.940663713658,
995.024119508576,995.107664001306,995.191253084247,995.274976351805,995.355656067697,
995.442631342696,995.529485151282,995.616195235346,995.634488381611),
 .UNSPECIFIED.);
#683=B_SPLINE_CURVE_WITH_KNOTS('',3,(#89351,#89352,#89353,#89354,#89355,
#89356,#89357,#89358,#89359,#89360,#89361,#89362,#89363,#89364,#89365,#89366,
#89367,#89368,#89369,#89370,#89371,#89372,#89373,#89374,#89375,#89376,#89377,
#89378,#89379,#89380,#89381,#89382,#89383,#89384,#89385,#89386,#89387,#89388,
#89389,#89390,#89391,#89392,#89393,#89394,#89395,#89396,#89397,#89398,#89399,
#89400,#89401,#89402,#89403,#89404,#89405,#89406,#89407,#89408,#89409,#89410,
#89411,#89412,#89413,#89414,#89415,#89416,#89417,#89418,#89419,#89420,#89421,
#89422,#89423,#89424,#89425,#89426,#89427,#89428,#89429,#89430,#89431,#89432,
#89433,#89434,#89435,#89436,#89437,#89438,#89439,#89440,#89441,#89442,#89443,
#89444,#89445,#89446,#89447,#89448,#89449,#89450,#89451,#89452,#89453,#89454,
#89455,#89456,#89457,#89458,#89459,#89460,#89461,#89462,#89463,#89464,#89465,
#89466,#89467,#89468,#89469,#89470,#89471,#89472,#89473,#89474,#89475,#89476,
#89477,#89478,#89479,#89480,#89481,#89482,#89483,#89484,#89485,#89486,#89487,
#89488,#89489,#89490,#89491,#89492,#89493,#89494,#89495,#89496,#89497,#89498,
#89499,#89500,#89501,#89502,#89503,#89504,#89505,#89506,#89507,#89508,#89509,
#89510,#89511,#89512,#89513,#89514,#89515,#89516,#89517,#89518,#89519,#89520,
#89521,#89522,#89523,#89524,#89525,#89526,#89527,#89528,#89529,#89530,#89531,
#89532,#89533,#89534,#89535,#89536,#89537,#89538,#89539,#89540,#89541,#89542,
#89543,#89544,#89545,#89546,#89547,#89548,#89549,#89550,#89551,#89552,#89553,
#89554,#89555,#89556,#89557,#89558,#89559,#89560,#89561,#89562,#89563,#89564,
#89565,#89566,#89567,#89568,#89569,#89570),.UNSPECIFIED.,.F.,.F.,(4,3,3,
3,3,3,3,3,3,3,3,3,3,3,3,3,3,3,3,3,3,3,3,3,3,3,3,3,3,3,3,3,3,3,3,3,3,3,3,
3,3,3,3,3,3,3,3,3,3,3,3,3,3,3,3,3,3,3,3,3,3,3,3,3,3,3,3,3,3,3,3,3,3,4),
(995.884871187942,996.021248167525,996.0451014587,996.128840170546,996.212475681913,
996.296028125312,996.379517561163,996.462971511777,996.546408005623,996.629845115378,
996.713300910296,996.796845403025,996.880434485966,996.964157753524,997.04483746942,
997.128576181266,997.212211692633,997.295764136032,997.379253571883,997.462707522496,
997.546144016343,997.629581126098,997.713036921016,997.796581413745,997.880170496686,
997.963893764244,998.04457348014,998.128312191986,998.211947703354,998.295500146752,
998.378989582603,998.462443533217,998.545880027063,998.629317136818,998.712772931736,
998.796317424466,998.879906507407,998.963629774964,999.04430949086,999.128048202706,
999.211683714074,999.295236157472,999.378725593323,999.462179543937,999.545616037783,
999.629053147538,999.712508942456,999.796053435186,999.879642518127,999.963365785684,
1000.04404550158,1000.12778421343,1000.21141972479,1000.29497216819,1000.37846160404,
1000.46191555466,1000.5453520485,1000.62878915826,1000.71224495318,1000.79578944591,
1000.87937852885,1000.96310179641,1001.0437815123,1001.12752769863,1001.21116900861,
1001.29472558194,1001.37821223534,1001.46166097302,1001.54508988378,1001.62851703916,
1001.7119925852,1001.79549552301,1001.87908229611,1001.91647437912),
 .UNSPECIFIED.);
#684=B_SPLINE_CURVE_WITH_KNOTS('',3,(#89571,#89572,#89573,#89574,#89575,
#89576,#89577,#89578,#89579,#89580),.UNSPECIFIED.,.F.,.F.,(4,3,3,4),(995.63314520609,
995.715410338439,995.800140763139,995.88487118784),.UNSPECIFIED.);
#685=B_SPLINE_CURVE_WITH_KNOTS('',3,(#89582,#89583,#89584,#89585,#89586,
#89587,#89588,#89589,#89590,#89591),.UNSPECIFIED.,.F.,.F.,(4,3,3,4),(995.634488381611,
995.721042296476,995.807480506179,995.884871187946),.UNSPECIFIED.);
#686=B_SPLINE_CURVE_WITH_KNOTS('',3,(#89592,#89593,#89594,#89595,#89596,
#89597,#89598,#89599,#89600,#89601,#89602,#89603,#89604,#89605,#89606,#89607,
#89608,#89609,#89610,#89611,#89612,#89613,#89614,#89615,#89616,#89617,#89618,
#89619,#89620,#89621,#89622,#89623,#89624,#89625,#89626,#89627,#89628,#89629,
#89630,#89631,#89632,#89633,#89634,#89635,#89636,#89637,#89638,#89639,#89640,
#89641,#89642,#89643,#89644,#89645,#89646,#89647,#89648,#89649,#89650,#89651,
#89652,#89653,#89654,#89655,#89656,#89657,#89658,#89659,#89660,#89661,#89662,
#89663,#89664,#89665,#89666,#89667,#89668,#89669,#89670,#89671,#89672,#89673,
#89674,#89675,#89676,#89677,#89678,#89679,#89680,#89681,#89682,#89683,#89684,
#89685,#89686,#89687,#89688,#89689,#89690,#89691,#89692,#89693,#89694,#89695,
#89696,#89697,#89698,#89699,#89700,#89701,#89702,#89703,#89704,#89705,#89706,
#89707,#89708,#89709,#89710,#89711,#89712,#89713,#89714,#89715,#89716,#89717,
#89718,#89719,#89720,#89721,#89722,#89723,#89724,#89725,#89726,#89727,#89728,
#89729,#89730,#89731,#89732,#89733,#89734,#89735,#89736,#89737,#89738,#89739,
#89740,#89741,#89742,#89743,#89744,#89745,#89746,#89747,#89748,#89749,#89750,
#89751,#89752,#89753,#89754,#89755,#89756,#89757,#89758,#89759,#89760,#89761,
#89762,#89763,#89764,#89765,#89766,#89767,#89768,#89769,#89770,#89771,#89772,
#89773,#89774,#89775,#89776,#89777,#89778,#89779,#89780,#89781,#89782,#89783,
#89784,#89785,#89786,#89787,#89788,#89789,#89790,#89791,#89792,#89793,#89794,
#89795,#89796,#89797,#89798,#89799,#89800,#89801,#89802,#89803,#89804,#89805,
#89806,#89807,#89808,#89809,#89810,#89811),.UNSPECIFIED.,.F.,.F.,(4,3,3,
3,3,3,3,3,3,3,3,3,3,3,3,3,3,3,3,3,3,3,3,3,3,3,3,3,3,3,3,3,3,3,3,3,3,3,3,
3,3,3,3,3,3,3,3,3,3,3,3,3,3,3,3,3,3,3,3,3,3,3,3,3,3,3,3,3,3,3,3,3,3,4),
(995.88487118808,995.973419318332,996.062127342903,996.151085735606,996.240181514523,
996.329487426633,996.355392078417,996.439130790263,996.52276630163,996.606318745029,
996.68980818088,996.773262131493,996.85669862534,996.940135735095,997.023591530013,
997.107136022742,997.190725105683,997.274448373241,997.355128089137,997.438866800983,
997.52250231235,997.606054755749,997.6895441916,997.772998142213,997.856434636059,
997.939871745815,998.023327540733,998.106872033462,998.190461116403,998.274184383961,
998.354864099857,998.438602811703,998.52223832307,998.605790766468,998.689280202319,
998.772734152932,998.856170646778,998.939607756534,999.023063551451,999.106608044181,
999.190197127122,999.273920394679,999.354600110577,999.438338822424,999.521974333792,
999.605526777191,999.689016213043,999.772470163657,999.855906657504,999.93934376726,
1000.02279956218,1000.10634405491,1000.18993313785,1000.27365640541,1000.3543361213,
1000.43807483315,1000.52171034451,1000.60526278791,1000.68875222376,1000.77220617438,
1000.85564266822,1000.93907977798,1001.0225355729,1001.10608006563,1001.18966914857,
1001.27339241612,1001.35407213202,1001.43655651427,1001.51894518119,1001.60125734878,
1001.68351138604,1001.76573016305,1001.8479504598,1001.91641401972),
 .UNSPECIFIED.);
#687=B_SPLINE_CURVE_WITH_KNOTS('',3,(#89817,#89818,#89819,#89820,#89821,
#89822,#89823,#89824,#89825,#89826,#89827,#89828,#89829,#89830,#89831,#89832,
#89833,#89834,#89835,#89836,#89837,#89838,#89839,#89840,#89841,#89842,#89843,
#89844,#89845,#89846,#89847,#89848,#89849,#89850,#89851,#89852,#89853,#89854,
#89855,#89856,#89857,#89858,#89859,#89860,#89861,#89862,#89863,#89864,#89865,
#89866,#89867,#89868,#89869,#89870,#89871,#89872,#89873,#89874,#89875,#89876,
#89877,#89878,#89879,#89880,#89881,#89882,#89883,#89884,#89885,#89886,#89887,
#89888,#89889,#89890,#89891,#89892,#89893,#89894,#89895,#89896,#89897,#89898,
#89899,#89900,#89901,#89902,#89903,#89904,#89905,#89906,#89907,#89908,#89909,
#89910,#89911,#89912,#89913,#89914,#89915,#89916,#89917,#89918,#89919,#89920,
#89921,#89922,#89923,#89924,#89925,#89926,#89927,#89928,#89929,#89930,#89931,
#89932,#89933,#89934,#89935,#89936,#89937,#89938,#89939,#89940,#89941,#89942,
#89943,#89944,#89945,#89946,#89947,#89948,#89949,#89950,#89951,#89952,#89953,
#89954,#89955,#89956,#89957,#89958,#89959,#89960,#89961,#89962,#89963,#89964,
#89965,#89966,#89967,#89968,#89969,#89970,#89971,#89972,#89973,#89974,#89975,
#89976,#89977,#89978,#89979,#89980,#89981,#89982,#89983,#89984,#89985,#89986,
#89987,#89988,#89989,#89990,#89991,#89992,#89993,#89994,#89995,#89996,#89997,
#89998,#89999,#90000,#90001,#90002,#90003,#90004,#90005,#90006,#90007,#90008,
#90009,#90010,#90011,#90012,#90013,#90014,#90015,#90016,#90017,#90018,#90019,
#90020,#90021,#90022,#90023,#90024,#90025,#90026,#90027,#90028,#90029,#90030,
#90031,#90032,#90033,#90034,#90035,#90036),.UNSPECIFIED.,.F.,.F.,(4,3,3,
3,3,3,3,3,3,3,3,3,3,3,3,3,3,3,3,3,3,3,3,3,3,3,3,3,3,3,3,3,3,3,3,3,3,3,3,
3,3,3,3,3,3,3,3,3,3,3,3,3,3,3,3,3,3,3,3,3,3,3,3,3,3,3,3,3,3,3,3,3,3,4),
(1002.16805649525,1002.25055559598,1002.33296687633,1002.41531144832,1002.49761651802,
1002.57990261825,1002.66218873484,1002.74449385133,1002.82688428733,1002.90932133242,
1002.99188129999,1003.04325353374,1003.12699224559,1003.21062775695,1003.29418020035,
1003.3776696362,1003.46112358682,1003.54456008066,1003.62799719042,1003.71145298534,
1003.79499747807,1003.87858656101,1003.96230982856,1004.04298954446,1004.12672825631,
1004.21036376767,1004.29391621107,1004.37740564692,1004.46085959754,1004.54429609138,
1004.62773320114,1004.71118899606,1004.79473348879,1004.87832257173,1004.96204583928,
1005.04272555518,1005.12646426703,1005.21009977839,1005.29365222179,1005.37714165764,
1005.46059560826,1005.5440321021,1005.62746921186,1005.71092500678,1005.79446949951,
1005.87805858245,1005.96178185,1006.0424615659,1006.12620027775,1006.20983578911,
1006.29338823251,1006.37687766836,1006.46033161898,1006.54376811282,1006.62720522258,
1006.7106610175,1006.79420551023,1006.87779459317,1006.96151786072,1007.04219757662,
1007.12593628847,1007.20957179983,1007.29312424323,1007.37661367908,1007.4600676297,
1007.54350412354,1007.6269412333,1007.71039702821,1007.79394152094,1007.87753060389,
1007.96125387144,1008.04193358734,1008.13445659178,1008.20088883303),
 .UNSPECIFIED.);
#688=B_SPLINE_CURVE_WITH_KNOTS('',3,(#90037,#90038,#90039,#90040,#90041,
#90042,#90043,#90044,#90045,#90046),.UNSPECIFIED.,.F.,.F.,(4,3,3,4),(1001.91647437912,
1002.00021216703,1002.04351752302,1002.16805649512),.UNSPECIFIED.);
#689=B_SPLINE_CURVE_WITH_KNOTS('',3,(#90048,#90049,#90050,#90051,#90052,
#90053,#90054,#90055,#90056,#90057),.UNSPECIFIED.,.F.,.F.,(4,3,3,4),(1001.91641401972,
1001.99867201972,1002.08336425735,1002.16805649499),.UNSPECIFIED.);
#690=B_SPLINE_CURVE_WITH_KNOTS('',3,(#90058,#90059,#90060,#90061,#90062,
#90063,#90064,#90065,#90066,#90067,#90068,#90069,#90070,#90071,#90072,#90073,
#90074,#90075,#90076,#90077,#90078,#90079,#90080,#90081,#90082,#90083,#90084,
#90085,#90086,#90087,#90088,#90089,#90090,#90091,#90092,#90093,#90094,#90095,
#90096,#90097,#90098,#90099,#90100,#90101,#90102,#90103,#90104,#90105,#90106,
#90107,#90108,#90109,#90110,#90111,#90112,#90113,#90114,#90115,#90116,#90117,
#90118,#90119,#90120,#90121,#90122,#90123,#90124,#90125,#90126,#90127,#90128,
#90129,#90130,#90131,#90132,#90133,#90134,#90135,#90136,#90137,#90138,#90139,
#90140,#90141,#90142,#90143,#90144,#90145,#90146,#90147,#90148,#90149,#90150,
#90151,#90152,#90153,#90154,#90155,#90156,#90157,#90158,#90159,#90160,#90161,
#90162,#90163,#90164,#90165,#90166,#90167,#90168,#90169,#90170,#90171,#90172,
#90173,#90174,#90175,#90176,#90177,#90178,#90179,#90180,#90181,#90182,#90183,
#90184,#90185,#90186,#90187,#90188,#90189,#90190,#90191,#90192,#90193,#90194,
#90195,#90196,#90197,#90198,#90199,#90200,#90201,#90202,#90203,#90204,#90205,
#90206,#90207,#90208,#90209,#90210,#90211,#90212,#90213,#90214,#90215,#90216,
#90217,#90218,#90219,#90220,#90221,#90222,#90223,#90224,#90225,#90226,#90227,
#90228,#90229,#90230,#90231,#90232,#90233,#90234,#90235,#90236,#90237,#90238,
#90239,#90240,#90241,#90242,#90243,#90244,#90245,#90246,#90247,#90248,#90249,
#90250,#90251,#90252,#90253,#90254,#90255,#90256,#90257,#90258,#90259,#90260,
#90261,#90262,#90263,#90264,#90265,#90266,#90267,#90268,#90269,#90270,#90271,
#90272,#90273,#90274),.UNSPECIFIED.,.F.,.F.,(4,3,3,3,3,3,3,3,3,3,3,3,3,
3,3,3,3,3,3,3,3,3,3,3,3,3,3,3,3,3,3,3,3,3,3,3,3,3,3,3,3,3,3,3,3,3,3,3,3,
3,3,3,3,3,3,3,3,3,3,3,3,3,3,3,3,3,3,3,3,3,3,3,4),(1002.16805649513,1002.29304179767,
1002.35380814274,1002.43754685459,1002.52118236595,1002.60473480935,1002.6882242452,
1002.77167819582,1002.85511468966,1002.93855179942,1003.02200759434,1003.10555208707,
1003.18914117001,1003.27286443756,1003.35354415346,1003.43728286531,1003.52091837667,
1003.60447082007,1003.68796025592,1003.77141420654,1003.85485070038,1003.93828781014,
1004.02174360506,1004.10528809779,1004.18887718073,1004.27260044828,1004.35328016418,
1004.43701887603,1004.52065438739,1004.60420683079,1004.68769626664,1004.77115021726,
1004.8545867111,1004.93802382086,1005.02147961578,1005.10502410851,1005.18861319145,
1005.272336459,1005.3530161749,1005.43675488675,1005.52039039811,1005.60394284151,
1005.68743227736,1005.77088622798,1005.85432272182,1005.93775983158,1006.0212156265,
1006.10476011923,1006.18834920217,1006.27207246972,1006.35275218562,1006.43649089747,
1006.52012640883,1006.60367885223,1006.68716828808,1006.7706222387,1006.85405873254,
1006.9374958423,1007.02095163722,1007.10449612994,1007.18808521289,1007.27180848044,
1007.35248819634,1007.43623597389,1007.51987853776,1007.60484562024,1007.68833125241,
1007.77177879713,1007.85520634312,1007.94130855672,1008.02477827793,1008.11219673773,
1008.19961519754),.UNSPECIFIED.);
#691=B_SPLINE_CURVE_WITH_KNOTS('',3,(#90280,#90281,#90282,#90283,#90284,
#90285,#90286,#90287,#90288,#90289,#90290,#90291,#90292,#90293,#90294,#90295,
#90296,#90297,#90298,#90299,#90300,#90301,#90302,#90303,#90304,#90305,#90306,
#90307,#90308,#90309,#90310,#90311,#90312,#90313,#90314,#90315,#90316,#90317,
#90318,#90319,#90320,#90321,#90322,#90323,#90324,#90325,#90326,#90327,#90328,
#90329,#90330,#90331,#90332,#90333,#90334,#90335,#90336,#90337,#90338,#90339,
#90340,#90341,#90342,#90343,#90344,#90345,#90346,#90347,#90348,#90349,#90350,
#90351,#90352,#90353,#90354,#90355,#90356,#90357,#90358,#90359,#90360,#90361,
#90362,#90363,#90364,#90365,#90366,#90367,#90368,#90369,#90370,#90371,#90372,
#90373,#90374,#90375,#90376,#90377,#90378,#90379,#90380,#90381,#90382,#90383,
#90384,#90385,#90386,#90387,#90388,#90389,#90390,#90391,#90392,#90393,#90394,
#90395,#90396,#90397,#90398,#90399,#90400,#90401,#90402,#90403,#90404,#90405,
#90406,#90407,#90408,#90409,#90410,#90411,#90412,#90413,#90414,#90415,#90416,
#90417,#90418,#90419,#90420,#90421,#90422,#90423,#90424,#90425,#90426,#90427,
#90428,#90429,#90430,#90431,#90432,#90433,#90434,#90435,#90436,#90437,#90438,
#90439,#90440,#90441,#90442,#90443,#90444,#90445,#90446,#90447,#90448,#90449,
#90450,#90451,#90452,#90453,#90454,#90455,#90456,#90457,#90458,#90459,#90460,
#90461,#90462,#90463,#90464,#90465,#90466,#90467,#90468,#90469,#90470,#90471,
#90472,#90473,#90474,#90475,#90476,#90477,#90478,#90479,#90480,#90481,#90482,
#90483,#90484,#90485,#90486,#90487,#90488,#90489,#90490,#90491,#90492,#90493,
#90494,#90495,#90496,#90497,#90498,#90499),.UNSPECIFIED.,.F.,.F.,(4,3,3,
3,3,3,3,3,3,3,3,3,3,3,3,3,3,3,3,3,3,3,3,3,3,3,3,3,3,3,3,3,3,3,3,3,3,3,3,
3,3,3,3,3,3,3,3,3,3,3,3,3,3,3,3,3,3,3,3,3,3,3,3,3,3,3,3,3,3,3,3,3,3,4),
(1008.4512418023,1008.53601294285,1008.62081253761,1008.70565656944,1008.79062346889,
1008.87565342782,1008.96084174054,1009.04166959806,1009.12540830991,1009.20904382127,
1009.29259626467,1009.37608570052,1009.45953965114,1009.54297614498,1009.62641325474,
1009.70986904966,1009.79341354239,1009.87700262533,1009.96072589288,1010.04140560878,
1010.12514432063,1010.20877983199,1010.29233227539,1010.37582171124,1010.45927566186,
1010.5427121557,1010.62614926546,1010.70960506037,1010.7931495531,1010.87673863604,
1010.9604619036,1011.0411416195,1011.12488033135,1011.20851584271,1011.29206828611,
1011.37555772196,1011.45901167258,1011.54244816642,1011.62588527618,1011.7093410711,
1011.79288556383,1011.87647464677,1011.96019791433,1012.04087763022,1012.12461634207,
1012.20825185343,1012.29180429683,1012.37529373268,1012.4587476833,1012.54218417714,
1012.6256212869,1012.70907708182,1012.79262157455,1012.87621065749,1012.95993392504,
1013.04061364094,1013.12435235279,1013.20798786415,1013.29154030755,1013.3750297434,
1013.45848369402,1013.54192018786,1013.62535729762,1013.70881309253,1013.79235758526,
1013.8759466682,1013.95966993576,1014.04034965166,1014.12367162658,1014.20689120733,
1014.29001017334,1014.37307123086,1014.45608932087,1014.48334915183),
 .UNSPECIFIED.);
#692=B_SPLINE_CURVE_WITH_KNOTS('',3,(#90500,#90501,#90502,#90503,#90504,
#90505,#90506,#90507,#90508,#90509),.UNSPECIFIED.,.F.,.F.,(4,3,3,4),(1008.20088883303,
1008.29294583235,1008.38460335587,1008.45124180213),.UNSPECIFIED.);
#693=B_SPLINE_CURVE_WITH_KNOTS('',3,(#90511,#90512,#90513,#90514,#90515,
#90516,#90517,#90518,#90519,#90520),.UNSPECIFIED.,.F.,.F.,(4,3,3,4),(1008.19961519754,
1008.28334261795,1008.35222420706,1008.45124180231),.UNSPECIFIED.);
#694=B_SPLINE_CURVE_WITH_KNOTS('',3,(#90521,#90522,#90523,#90524,#90525,
#90526,#90527,#90528,#90529,#90530,#90531,#90532,#90533,#90534,#90535,#90536,
#90537,#90538,#90539,#90540,#90541,#90542,#90543,#90544,#90545,#90546,#90547,
#90548,#90549,#90550,#90551,#90552,#90553,#90554,#90555,#90556,#90557,#90558,
#90559,#90560,#90561,#90562,#90563,#90564,#90565,#90566,#90567,#90568,#90569,
#90570,#90571,#90572,#90573,#90574,#90575,#90576,#90577,#90578,#90579,#90580,
#90581,#90582,#90583,#90584,#90585,#90586,#90587,#90588,#90589,#90590,#90591,
#90592,#90593,#90594,#90595,#90596,#90597,#90598,#90599,#90600,#90601,#90602,
#90603,#90604,#90605,#90606,#90607,#90608,#90609,#90610,#90611,#90612,#90613,
#90614,#90615,#90616,#90617,#90618,#90619,#90620,#90621,#90622,#90623,#90624,
#90625,#90626,#90627,#90628,#90629,#90630,#90631,#90632,#90633,#90634,#90635,
#90636,#90637,#90638,#90639,#90640,#90641,#90642,#90643,#90644,#90645,#90646,
#90647,#90648,#90649,#90650,#90651,#90652,#90653,#90654,#90655,#90656,#90657,
#90658,#90659,#90660,#90661,#90662,#90663,#90664,#90665,#90666,#90667,#90668,
#90669,#90670,#90671,#90672,#90673,#90674,#90675,#90676,#90677,#90678,#90679,
#90680,#90681,#90682,#90683,#90684,#90685,#90686,#90687,#90688,#90689,#90690,
#90691,#90692,#90693,#90694,#90695,#90696,#90697,#90698,#90699,#90700,#90701,
#90702,#90703,#90704,#90705,#90706,#90707,#90708,#90709,#90710,#90711,#90712,
#90713,#90714,#90715,#90716,#90717,#90718,#90719,#90720,#90721,#90722,#90723,
#90724,#90725,#90726,#90727,#90728,#90729,#90730,#90731,#90732,#90733,#90734,
#90735,#90736,#90737,#90738,#90739,#90740),.UNSPECIFIED.,.F.,.F.,(4,3,3,
3,3,3,3,3,3,3,3,3,3,3,3,3,3,3,3,3,3,3,3,3,3,3,3,3,3,3,3,3,3,3,3,3,3,3,3,
3,3,3,3,3,3,3,3,3,3,3,3,3,3,3,3,3,3,3,3,3,3,3,3,3,3,3,3,3,3,3,3,3,3,4),
(1008.45124180245,1008.533889141,1008.61644367089,1008.69892643314,1008.78136290829,
1008.86377570506,1008.94618373353,1009.02860589755,1009.11111132048,1009.19365882821,
1009.27633650523,1009.35196021778,1009.43569892963,1009.51933444099,1009.60288688439,
1009.68637632024,1009.76983027086,1009.8532667647,1009.93670387446,1010.02015966938,
1010.10370416211,1010.18729324505,1010.27101651261,1010.3516962285,1010.43543494035,
1010.51907045171,1010.60262289511,1010.68611233096,1010.76956628158,1010.85300277543,
1010.93643988518,1011.0198956801,1011.10344017283,1011.18702925577,1011.27075252333,
1011.35143223922,1011.43517095107,1011.51880646243,1011.60235890583,1011.68584834168,
1011.7693022923,1011.85273878614,1011.9361758959,1012.01963169081,1012.10317618354,
1012.18676526648,1012.27048853404,1012.35116824994,1012.43490696179,1012.51854247315,
1012.60209491655,1012.6855843524,1012.76903830302,1012.85247479686,1012.93591190662,
1013.01936770154,1013.10291219427,1013.18650127721,1013.27022454476,1013.35090426066,
1013.43464297251,1013.51827848388,1013.60183092728,1013.68532036313,1013.76877431374,
1013.85221080759,1013.93564791735,1014.01910371226,1014.102648205,1014.18623728794,
1014.2699605555,1014.35064027138,1014.44491243077,1014.48401170027),
 .UNSPECIFIED.);
#695=B_SPLINE_CURVE_WITH_KNOTS('',3,(#90746,#90747,#90748,#90749,#90750,
#90751,#90752,#90753,#90754,#90755,#90756,#90757,#90758,#90759,#90760,#90761,
#90762,#90763,#90764,#90765,#90766,#90767,#90768,#90769,#90770,#90771,#90772,
#90773,#90774,#90775,#90776,#90777,#90778,#90779,#90780,#90781,#90782,#90783,
#90784,#90785,#90786,#90787,#90788,#90789,#90790,#90791,#90792,#90793,#90794,
#90795,#90796,#90797,#90798,#90799,#90800,#90801,#90802,#90803,#90804,#90805,
#90806,#90807,#90808,#90809,#90810,#90811,#90812,#90813,#90814,#90815,#90816,
#90817,#90818,#90819,#90820,#90821,#90822,#90823,#90824,#90825,#90826,#90827,
#90828,#90829,#90830,#90831,#90832,#90833,#90834,#90835,#90836,#90837,#90838,
#90839,#90840,#90841,#90842,#90843,#90844,#90845,#90846,#90847,#90848,#90849,
#90850,#90851,#90852,#90853,#90854,#90855,#90856,#90857,#90858,#90859,#90860,
#90861,#90862,#90863,#90864,#90865,#90866,#90867,#90868,#90869,#90870,#90871,
#90872,#90873,#90874,#90875,#90876,#90877,#90878,#90879,#90880,#90881,#90882,
#90883,#90884,#90885,#90886,#90887,#90888,#90889,#90890,#90891,#90892,#90893,
#90894,#90895,#90896,#90897,#90898,#90899,#90900,#90901,#90902,#90903,#90904,
#90905,#90906,#90907,#90908,#90909,#90910,#90911,#90912,#90913,#90914,#90915,
#90916,#90917,#90918,#90919,#90920,#90921,#90922,#90923,#90924,#90925,#90926,
#90927,#90928,#90929,#90930,#90931,#90932,#90933,#90934,#90935,#90936,#90937,
#90938,#90939,#90940,#90941,#90942,#90943,#90944,#90945,#90946,#90947,#90948,
#90949,#90950,#90951,#90952,#90953,#90954,#90955,#90956,#90957,#90958,#90959,
#90960,#90961,#90962),.UNSPECIFIED.,.F.,.F.,(4,3,3,3,3,3,3,3,3,3,3,3,3,
3,3,3,3,3,3,3,3,3,3,3,3,3,3,3,3,3,3,3,3,3,3,3,3,3,3,3,3,3,3,3,3,3,3,3,3,
3,3,3,3,3,3,3,3,3,3,3,3,3,3,3,3,3,3,3,3,3,3,3,4),(1014.73442710964,1014.83436448893,
1014.93722507566,1015.04008566238,1015.12382437423,1015.2074598856,1015.291012329,
1015.37450176485,1015.45795571546,1015.54139220931,1015.62482931907,1015.70828511399,
1015.79182960672,1015.87541868966,1015.95914195722,1016.0398216731,1016.12356038495,
1016.20719589631,1016.29074833971,1016.37423777556,1016.45769172618,1016.54112822002,
1016.62456532978,1016.7080211247,1016.79156561743,1016.87515470037,1016.95887796792,
1017.03955768382,1017.12329639567,1017.20693190703,1017.29048435043,1017.37397378628,
1017.4574277369,1017.54086423074,1017.6243013405,1017.70775713541,1017.79130162814,
1017.87489071108,1017.95861397864,1018.03929369454,1018.12303240639,1018.20666791775,
1018.29022036115,1018.373709797,1018.45716374762,1018.54060024146,1018.62403735122,
1018.70749314614,1018.79103763887,1018.87462672181,1018.95834998937,1019.03902970526,
1019.12276841711,1019.20640392847,1019.28995637187,1019.37344580772,1019.45689975834,
1019.54033625218,1019.62377336194,1019.70722915685,1019.79077364958,1019.87436273252,
1019.95808600008,1020.03876571598,1020.12222316499,1020.20554861207,1020.28879787067,
1020.37198938023,1020.45514153568,1020.5382896657,1020.62143322146,1020.70462245946,
1020.76588157733),.UNSPECIFIED.);
#696=B_SPLINE_CURVE_WITH_KNOTS('',3,(#90963,#90964,#90965,#90966,#90967,
#90968,#90969,#90970,#90971,#90972),.UNSPECIFIED.,.F.,.F.,(4,3,3,4),(1014.48334915183,
1014.56635143231,1014.6503892709,1014.73442710948),.UNSPECIFIED.);
#697=B_SPLINE_CURVE_WITH_KNOTS('',3,(#90974,#90975,#90976,#90977,#90978,
#90979,#90980,#90981,#90982,#90983),.UNSPECIFIED.,.F.,.F.,(4,3,3,4),(1014.48401170027,
1014.57777675051,1014.67102940355,1014.73442710929),.UNSPECIFIED.);
#698=B_SPLINE_CURVE_WITH_KNOTS('',3,(#90984,#90985,#90986,#90987,#90988,
#90989,#90990,#90991,#90992,#90993,#90994,#90995,#90996,#90997,#90998,#90999,
#91000,#91001,#91002,#91003,#91004,#91005,#91006,#91007,#91008,#91009,#91010,
#91011,#91012,#91013,#91014,#91015,#91016,#91017,#91018,#91019,#91020,#91021,
#91022,#91023,#91024,#91025,#91026,#91027,#91028,#91029,#91030,#91031,#91032,
#91033,#91034,#91035,#91036,#91037,#91038,#91039,#91040,#91041,#91042,#91043,
#91044,#91045,#91046,#91047,#91048,#91049,#91050,#91051,#91052,#91053,#91054,
#91055,#91056,#91057,#91058,#91059,#91060,#91061,#91062,#91063,#91064,#91065,
#91066,#91067,#91068,#91069,#91070,#91071,#91072,#91073,#91074,#91075,#91076,
#91077,#91078,#91079,#91080,#91081,#91082,#91083,#91084,#91085,#91086,#91087,
#91088,#91089,#91090,#91091,#91092,#91093,#91094,#91095,#91096,#91097,#91098,
#91099,#91100,#91101,#91102,#91103,#91104,#91105,#91106,#91107,#91108,#91109,
#91110,#91111,#91112,#91113,#91114,#91115,#91116,#91117,#91118,#91119,#91120,
#91121,#91122,#91123,#91124,#91125,#91126,#91127,#91128,#91129,#91130,#91131,
#91132,#91133,#91134,#91135,#91136,#91137,#91138,#91139,#91140,#91141,#91142,
#91143,#91144,#91145,#91146,#91147,#91148,#91149,#91150,#91151,#91152,#91153,
#91154,#91155,#91156,#91157,#91158,#91159,#91160,#91161,#91162,#91163,#91164,
#91165,#91166,#91167,#91168,#91169,#91170,#91171,#91172,#91173,#91174,#91175,
#91176,#91177,#91178,#91179,#91180,#91181,#91182,#91183,#91184,#91185,#91186,
#91187,#91188,#91189,#91190,#91191,#91192,#91193,#91194,#91195,#91196,#91197,
#91198,#91199,#91200,#91201,#91202,#91203),.UNSPECIFIED.,.F.,.F.,(4,3,3,
3,3,3,3,3,3,3,3,3,3,3,3,3,3,3,3,3,3,3,3,3,3,3,3,3,3,3,3,3,3,3,3,3,3,3,3,
3,3,3,3,3,3,3,3,3,3,3,3,3,3,3,3,3,3,3,3,3,3,3,3,3,3,3,3,3,3,3,3,3,3,4),
(1014.73442710948,1014.81865935941,1014.90290397472,1014.98717787641,1015.07149800121,
1015.15593230497,1015.24043337517,1015.32506721425,1015.3503762821,1015.43411499394,
1015.51775050531,1015.60130294871,1015.68479238456,1015.76824633517,1015.85168282902,
1015.93511993877,1016.01857573369,1016.10212022642,1016.18570930935,1016.26943257691,
1016.35011229282,1016.43385100467,1016.51748651603,1016.60103895943,1016.68452839528,
1016.76798234589,1016.85141883974,1016.93485594949,1017.01831174441,1017.10185623714,
1017.18544532008,1017.26916858764,1017.34984830354,1017.43358701539,1017.51722252675,
1017.60077497015,1017.68426440601,1017.76771835662,1017.85115485047,1017.93459196022,
1018.01804775514,1018.10159224787,1018.18518133081,1018.26890459837,1018.34958431426,
1018.43332302611,1018.51695853747,1018.60051098087,1018.68400041672,1018.76745436734,
1018.85089086118,1018.93432797094,1019.01778376585,1019.10132825858,1019.18491734152,
1019.26864060908,1019.34932032498,1019.43305903683,1019.51669454819,1019.60024699159,
1019.68373642744,1019.76719037806,1019.85062687191,1019.93406398166,1020.01751977658,
1020.10106426931,1020.18465335225,1020.26837661981,1020.3490563357,1020.43273624439,
1020.51628260801,1020.59975206856,1020.68320953995,1020.76666701133),
 .UNSPECIFIED.);
#699=B_SPLINE_CURVE_WITH_KNOTS('',3,(#91209,#91210,#91211,#91212,#91213,
#91214,#91215,#91216,#91217,#91218,#91219,#91220,#91221,#91222,#91223,#91224,
#91225,#91226,#91227,#91228,#91229,#91230,#91231,#91232,#91233,#91234,#91235,
#91236,#91237,#91238,#91239,#91240,#91241,#91242,#91243,#91244,#91245,#91246,
#91247,#91248,#91249,#91250,#91251,#91252,#91253,#91254,#91255,#91256,#91257,
#91258,#91259,#91260,#91261,#91262,#91263,#91264,#91265,#91266,#91267,#91268,
#91269,#91270,#91271,#91272,#91273,#91274,#91275,#91276,#91277,#91278,#91279,
#91280,#91281,#91282,#91283,#91284,#91285,#91286,#91287,#91288,#91289,#91290,
#91291,#91292,#91293,#91294,#91295,#91296,#91297,#91298,#91299,#91300,#91301,
#91302,#91303,#91304,#91305,#91306,#91307,#91308,#91309,#91310,#91311,#91312,
#91313,#91314,#91315,#91316,#91317,#91318,#91319,#91320,#91321,#91322,#91323,
#91324,#91325,#91326,#91327,#91328,#91329,#91330,#91331,#91332,#91333,#91334,
#91335,#91336,#91337,#91338,#91339,#91340,#91341,#91342,#91343,#91344,#91345,
#91346,#91347,#91348,#91349,#91350,#91351,#91352,#91353,#91354,#91355,#91356,
#91357,#91358,#91359,#91360,#91361,#91362,#91363,#91364,#91365,#91366,#91367,
#91368,#91369,#91370,#91371,#91372,#91373,#91374,#91375,#91376,#91377,#91378,
#91379,#91380,#91381,#91382,#91383,#91384,#91385,#91386,#91387,#91388,#91389,
#91390,#91391,#91392,#91393,#91394,#91395,#91396,#91397,#91398,#91399,#91400,
#91401,#91402,#91403,#91404,#91405,#91406,#91407,#91408,#91409,#91410,#91411,
#91412,#91413,#91414,#91415,#91416,#91417,#91418,#91419,#91420,#91421,#91422,
#91423,#91424,#91425,#91426,#91427,#91428,#91429,#91430,#91431),
 .UNSPECIFIED.,.F.,.F.,(4,3,3,3,3,3,3,3,3,3,3,3,3,3,3,3,3,3,3,3,3,3,3,3,
3,3,3,3,3,3,3,3,3,3,3,3,3,3,3,3,3,3,3,3,3,3,3,3,3,3,3,3,3,3,3,3,3,3,3,3,
3,3,3,3,3,3,3,3,3,3,3,3,3,3,4),(1021.01761241666,1021.0385017267,1021.12224043855,
1021.20587594991,1021.28942839331,1021.37291782916,1021.45637177978,1021.53980827363,
1021.62324538338,1021.7067011783,1021.79024567103,1021.87383475397,1021.95755802153,
1022.03823773742,1022.12197644927,1022.20561196063,1022.28916440403,1022.37265383988,
1022.4561077905,1022.53954428434,1022.6229813941,1022.70643718902,1022.78998168175,
1022.87357076469,1022.95729403224,1023.03797374814,1023.12171245999,1023.20534797135,
1023.28890041475,1023.3723898506,1023.45584380122,1023.53928029506,1023.62271740482,
1023.70617319974,1023.78971769246,1023.87330677541,1023.95703004296,1024.03770975886,
1024.12144847071,1024.20508398207,1024.28863642547,1024.37212586132,1024.45557981194,
1024.53901630578,1024.62245341554,1024.70590921046,1024.78945370319,1024.87304278613,
1024.95676605368,1025.03744576958,1025.12118448143,1025.20481999279,1025.28837243619,
1025.37186187204,1025.45531582266,1025.5387523165,1025.62218942626,1025.70564522118,
1025.78918971391,1025.87277879685,1025.9565020644,1026.0371817803,1026.12092049215,
1026.20455600351,1026.28810844691,1026.37159788276,1026.45505183337,1026.53848832722,
1026.62192543697,1026.70538123189,1026.78892572462,1026.87251480756,1026.95623807512,
1027.03691779102,1027.04981210257),.UNSPECIFIED.);
#700=B_SPLINE_CURVE_WITH_KNOTS('',3,(#91432,#91433,#91434,#91435,#91436,
#91437,#91438,#91439,#91440,#91441),.UNSPECIFIED.,.F.,.F.,(4,3,3,4),(1020.76588157733,
1020.84916885192,1020.9333906342,1021.01761241647),.UNSPECIFIED.);
#701=B_SPLINE_CURVE_WITH_KNOTS('',3,(#91443,#91444,#91445,#91446,#91447,
#91448,#91449,#91450,#91451,#91452),.UNSPECIFIED.,.F.,.F.,(4,3,3,4),(1020.76666701133,
1020.85000603278,1020.93380922472,1021.01761241666),.UNSPECIFIED.);
#702=B_SPLINE_CURVE_WITH_KNOTS('',3,(#91453,#91454,#91455,#91456,#91457,
#91458,#91459,#91460,#91461,#91462,#91463,#91464,#91465,#91466,#91467,#91468,
#91469,#91470,#91471,#91472,#91473,#91474,#91475,#91476,#91477,#91478,#91479,
#91480,#91481,#91482,#91483,#91484,#91485,#91486,#91487,#91488,#91489,#91490,
#91491,#91492,#91493,#91494,#91495,#91496,#91497,#91498,#91499,#91500,#91501,
#91502,#91503,#91504,#91505,#91506,#91507,#91508,#91509,#91510,#91511,#91512,
#91513,#91514,#91515,#91516,#91517,#91518,#91519,#91520,#91521,#91522,#91523,
#91524,#91525,#91526,#91527,#91528,#91529,#91530,#91531,#91532,#91533,#91534,
#91535,#91536,#91537,#91538,#91539,#91540,#91541,#91542,#91543,#91544,#91545,
#91546,#91547,#91548,#91549,#91550,#91551,#91552,#91553,#91554,#91555,#91556,
#91557,#91558,#91559,#91560,#91561,#91562,#91563,#91564,#91565,#91566,#91567,
#91568,#91569,#91570,#91571,#91572,#91573,#91574,#91575,#91576,#91577,#91578,
#91579,#91580,#91581,#91582,#91583,#91584,#91585,#91586,#91587,#91588,#91589,
#91590,#91591,#91592,#91593,#91594,#91595,#91596,#91597,#91598,#91599,#91600,
#91601,#91602,#91603,#91604,#91605,#91606,#91607,#91608,#91609,#91610,#91611,
#91612,#91613,#91614,#91615,#91616,#91617,#91618,#91619,#91620,#91621,#91622,
#91623,#91624,#91625,#91626,#91627,#91628,#91629,#91630,#91631,#91632,#91633,
#91634,#91635,#91636,#91637,#91638,#91639,#91640,#91641,#91642,#91643,#91644,
#91645,#91646,#91647,#91648,#91649,#91650,#91651,#91652,#91653,#91654,#91655,
#91656,#91657,#91658,#91659,#91660,#91661,#91662,#91663,#91664,#91665,#91666,
#91667,#91668,#91669,#91670,#91671,#91672),.UNSPECIFIED.,.F.,.F.,(4,3,3,
3,3,3,3,3,3,3,3,3,3,3,3,3,3,3,3,3,3,3,3,3,3,3,3,3,3,3,3,3,3,3,3,3,3,3,3,
3,3,3,3,3,3,3,3,3,3,3,3,3,3,3,3,3,3,3,3,3,3,3,3,3,3,3,3,3,3,3,3,3,3,4),
(1021.01761241685,1021.11504298746,1021.21306759752,1021.31178249612,1021.34879234642,
1021.43253105826,1021.51616656963,1021.59971901302,1021.68320844887,1021.76666239948,
1021.85009889332,1021.93353600308,1022.01699179799,1022.10053629072,1022.18412537365,
1022.26784864121,1022.34852835714,1022.43226706899,1022.51590258035,1022.59945502375,
1022.6829444596,1022.76639841022,1022.84983490406,1022.93327201382,1023.01672780874,
1023.10027230147,1023.18386138441,1023.26758465196,1023.34826436786,1023.43200307971,
1023.51563859107,1023.59919103447,1023.68268047032,1023.76613442094,1023.84957091479,
1023.93300802454,1024.01646381946,1024.10000831219,1024.18359739513,1024.26732066269,
1024.34800037858,1024.43173909043,1024.51537460179,1024.59892704519,1024.68241648104,
1024.76587043166,1024.8493069255,1024.93274403526,1025.01619983017,1025.0997443229,
1025.18333340584,1025.2670566734,1025.3477363893,1025.43147510115,1025.51511061251,
1025.59866305591,1025.68215249176,1025.76560644238,1025.84904293623,1025.93248004598,
1026.0159358409,1026.09948033363,1026.18306941657,1026.26679268413,1026.34747240002,
1026.43062447609,1026.51364527232,1026.59659023187,1026.67947804615,1026.76232736026,
1026.84517175658,1026.92801291739,1027.01089396545,1027.04899943094),
 .UNSPECIFIED.);
#703=B_SPLINE_CURVE_WITH_KNOTS('',3,(#91678,#91679,#91680,#91681,#91682,
#91683,#91684,#91685,#91686,#91687,#91688,#91689,#91690,#91691,#91692,#91693,
#91694,#91695,#91696,#91697,#91698,#91699,#91700,#91701,#91702,#91703,#91704,
#91705,#91706,#91707,#91708,#91709,#91710,#91711,#91712,#91713,#91714,#91715,
#91716,#91717,#91718,#91719,#91720,#91721,#91722,#91723,#91724,#91725,#91726,
#91727,#91728,#91729,#91730,#91731,#91732,#91733,#91734,#91735,#91736,#91737,
#91738,#91739,#91740,#91741,#91742,#91743,#91744,#91745,#91746,#91747,#91748,
#91749,#91750,#91751,#91752,#91753,#91754,#91755,#91756,#91757,#91758,#91759,
#91760,#91761,#91762,#91763,#91764,#91765,#91766,#91767,#91768,#91769,#91770,
#91771,#91772,#91773,#91774,#91775,#91776,#91777,#91778,#91779,#91780,#91781,
#91782,#91783,#91784,#91785,#91786,#91787,#91788,#91789,#91790,#91791,#91792,
#91793,#91794,#91795,#91796,#91797,#91798,#91799,#91800,#91801,#91802,#91803,
#91804,#91805,#91806,#91807,#91808,#91809,#91810,#91811,#91812,#91813,#91814,
#91815,#91816,#91817,#91818,#91819,#91820,#91821,#91822,#91823,#91824,#91825,
#91826,#91827,#91828,#91829,#91830,#91831,#91832,#91833,#91834,#91835,#91836,
#91837,#91838,#91839,#91840,#91841,#91842,#91843,#91844,#91845,#91846,#91847,
#91848,#91849,#91850,#91851,#91852,#91853,#91854,#91855,#91856,#91857,#91858,
#91859,#91860,#91861,#91862,#91863,#91864,#91865,#91866,#91867,#91868,#91869,
#91870,#91871,#91872,#91873,#91874,#91875,#91876,#91877,#91878,#91879,#91880,
#91881,#91882,#91883,#91884,#91885,#91886,#91887,#91888,#91889,#91890,#91891,
#91892,#91893,#91894,#91895,#91896,#91897),.UNSPECIFIED.,.F.,.F.,(4,3,3,
3,3,3,3,3,3,3,3,3,3,3,3,3,3,3,3,3,3,3,3,3,3,3,3,3,3,3,3,3,3,3,3,3,3,3,3,
3,3,3,3,3,3,3,3,3,3,3,3,3,3,3,3,3,3,3,3,3,3,3,3,3,3,3,3,3,3,3,3,3,3,4),
(1027.30079772384,1027.38345061798,1027.46606102377,1027.54865006983,1027.63123653473,
1027.71383919223,1027.79652759215,1027.8792596504,1027.96212323658,1028.03665380174,
1028.12039251359,1028.20402802495,1028.28758046835,1028.3710699042,1028.45452385482,
1028.53796034866,1028.62139745842,1028.70485325334,1028.78839774607,1028.87198682901,
1028.95571009657,1029.03638981246,1029.12012852431,1029.20376403567,1029.28731647907,
1029.37080591492,1029.45425986554,1029.53769635938,1029.62113346914,1029.70458926406,
1029.78813375679,1029.87172283973,1029.95544610729,1030.03612582318,1030.11986453503,
1030.20350004639,1030.28705248979,1030.37054192564,1030.45399587626,1030.5374323701,
1030.62086947986,1030.70432527478,1030.7878697675,1030.87145885045,1030.955182118,
1031.0358618339,1031.11960054575,1031.20323605711,1031.28678850051,1031.37027793636,
1031.45373188697,1031.53716838082,1031.62060549057,1031.70406128549,1031.78760577822,
1031.87119486116,1031.95491812871,1032.03559784462,1032.11933655647,1032.20297206784,
1032.28652451124,1032.37001394709,1032.45346789771,1032.53690439156,1032.62034150132,
1032.70379729624,1032.78734178897,1032.87093087191,1032.95465413947,1033.03533385535,
1033.12167787295,1033.20790695979,1033.29400030748,1033.33354879478),
 .UNSPECIFIED.);
#704=B_SPLINE_CURVE_WITH_KNOTS('',3,(#91898,#91899,#91900,#91901,#91902,
#91903,#91904,#91905,#91906,#91907),.UNSPECIFIED.,.F.,.F.,(4,3,3,4),(1027.04981210257,
1027.15701204208,1027.26224713867,1027.30079772369),.UNSPECIFIED.);
#705=B_SPLINE_CURVE_WITH_KNOTS('',3,(#91909,#91910,#91911,#91912,#91913,
#91914,#91915,#91916,#91917,#91918),.UNSPECIFIED.,.F.,.F.,(4,3,3,4),(1027.04899943094,
1027.13197379122,1027.21638575744,1027.30079772365),.UNSPECIFIED.);
#706=B_SPLINE_CURVE_WITH_KNOTS('',3,(#91919,#91920,#91921,#91922,#91923,
#91924,#91925,#91926,#91927,#91928,#91929,#91930,#91931,#91932,#91933,#91934,
#91935,#91936,#91937,#91938,#91939,#91940,#91941,#91942,#91943,#91944,#91945,
#91946,#91947,#91948,#91949,#91950,#91951,#91952,#91953,#91954,#91955,#91956,
#91957,#91958,#91959,#91960,#91961,#91962,#91963,#91964,#91965,#91966,#91967,
#91968,#91969,#91970,#91971,#91972,#91973,#91974,#91975,#91976,#91977,#91978,
#91979,#91980,#91981,#91982,#91983,#91984,#91985,#91986,#91987,#91988,#91989,
#91990,#91991,#91992,#91993,#91994,#91995,#91996,#91997,#91998,#91999,#92000,
#92001,#92002,#92003,#92004,#92005,#92006,#92007,#92008,#92009,#92010,#92011,
#92012,#92013,#92014,#92015,#92016,#92017,#92018,#92019,#92020,#92021,#92022,
#92023,#92024,#92025,#92026,#92027,#92028,#92029,#92030,#92031,#92032,#92033,
#92034,#92035,#92036,#92037,#92038,#92039,#92040,#92041,#92042,#92043,#92044,
#92045,#92046,#92047,#92048,#92049,#92050,#92051,#92052,#92053,#92054,#92055,
#92056,#92057,#92058,#92059,#92060,#92061,#92062,#92063,#92064,#92065,#92066,
#92067,#92068,#92069,#92070,#92071,#92072,#92073,#92074,#92075,#92076,#92077,
#92078,#92079,#92080,#92081,#92082,#92083,#92084,#92085,#92086,#92087,#92088,
#92089,#92090,#92091,#92092,#92093,#92094,#92095,#92096,#92097,#92098,#92099,
#92100,#92101,#92102,#92103,#92104,#92105,#92106,#92107,#92108,#92109,#92110,
#92111,#92112,#92113,#92114,#92115,#92116,#92117,#92118,#92119,#92120,#92121,
#92122,#92123,#92124,#92125,#92126,#92127,#92128,#92129,#92130,#92131,#92132,
#92133,#92134,#92135,#92136,#92137,#92138),.UNSPECIFIED.,.F.,.F.,(4,3,3,
3,3,3,3,3,3,3,3,3,3,3,3,3,3,3,3,3,3,3,3,3,3,3,3,3,3,3,3,3,3,3,3,3,3,3,3,
3,3,3,3,3,3,3,3,3,3,3,3,3,3,3,3,3,3,3,3,3,3,3,3,3,3,3,3,3,3,3,3,3,3,4),
(1027.30079772384,1027.34720841074,1027.43094712259,1027.51458263395,1027.59813507735,
1027.6816245132,1027.76507846381,1027.84851495766,1027.93195206742,1028.01540786233,
1028.09895235506,1028.182541438,1028.26626470556,1028.34694442146,1028.43068313331,
1028.51431864467,1028.59787108807,1028.68136052392,1028.76481447454,1028.84825096838,
1028.93168807814,1029.01514387306,1029.09868836579,1029.18227744873,1029.26600071628,
1029.34668043218,1029.43041914403,1029.51405465539,1029.59760709879,1029.68109653464,
1029.76455048526,1029.8479869791,1029.93142408886,1030.01487988377,1030.0984243765,
1030.18201345944,1030.265736727,1030.3464164429,1030.43015515475,1030.51379066611,
1030.59734310951,1030.68083254536,1030.76428649598,1030.84772298982,1030.93116009958,
1031.0146158945,1031.09816038723,1031.18174947017,1031.26547273773,1031.34615245362,
1031.42989116547,1031.51352667683,1031.59707912023,1031.68056855608,1031.7640225067,
1031.84745900054,1031.9308961103,1032.01435190522,1032.09789639795,1032.18148548089,
1032.26520874844,1032.34588846434,1032.4296278957,1032.51326395797,1032.59681678439,
1032.6803064359,1032.76375973116,1032.84719533129,1032.9306313088,1033.01408573256,
1033.09762552072,1033.18120980058,1033.26492039566,1033.3328408694),
 .UNSPECIFIED.);
#707=B_SPLINE_CURVE_WITH_KNOTS('',3,(#92144,#92145,#92146,#92147,#92148,
#92149,#92150,#92151,#92152,#92153,#92154,#92155,#92156,#92157,#92158,#92159,
#92160,#92161,#92162,#92163,#92164,#92165,#92166,#92167,#92168,#92169,#92170,
#92171,#92172,#92173,#92174,#92175,#92176,#92177,#92178,#92179,#92180,#92181,
#92182,#92183,#92184,#92185,#92186,#92187,#92188,#92189,#92190,#92191,#92192,
#92193,#92194,#92195,#92196,#92197,#92198,#92199,#92200,#92201,#92202,#92203,
#92204,#92205,#92206,#92207,#92208,#92209,#92210,#92211,#92212,#92213,#92214,
#92215,#92216,#92217,#92218,#92219,#92220,#92221,#92222,#92223,#92224,#92225,
#92226,#92227,#92228,#92229,#92230,#92231,#92232,#92233,#92234,#92235,#92236,
#92237,#92238,#92239,#92240,#92241,#92242,#92243,#92244,#92245,#92246,#92247,
#92248,#92249,#92250,#92251,#92252,#92253,#92254,#92255,#92256,#92257,#92258,
#92259,#92260,#92261,#92262,#92263,#92264,#92265,#92266,#92267,#92268,#92269,
#92270,#92271,#92272,#92273,#92274,#92275,#92276,#92277,#92278,#92279,#92280,
#92281,#92282,#92283,#92284,#92285,#92286,#92287,#92288,#92289,#92290,#92291,
#92292,#92293,#92294,#92295,#92296,#92297,#92298,#92299,#92300,#92301,#92302,
#92303,#92304,#92305,#92306,#92307,#92308,#92309,#92310,#92311,#92312,#92313,
#92314,#92315,#92316,#92317,#92318,#92319,#92320,#92321,#92322,#92323,#92324,
#92325,#92326,#92327,#92328,#92329,#92330,#92331,#92332,#92333,#92334,#92335,
#92336,#92337,#92338,#92339,#92340,#92341,#92342,#92343,#92344,#92345,#92346,
#92347,#92348,#92349,#92350,#92351,#92352,#92353,#92354,#92355,#92356,#92357,
#92358,#92359,#92360),.UNSPECIFIED.,.F.,.F.,(4,3,3,3,3,3,3,3,3,3,3,3,3,
3,3,3,3,3,3,3,3,3,3,3,3,3,3,3,3,3,3,3,3,3,3,3,3,3,3,3,3,3,3,3,3,3,3,3,3,
3,3,3,3,3,3,3,3,3,3,3,3,3,3,3,3,3,3,3,3,3,3,3,4),(1033.58398303112,1033.67338509724,
1033.76380628944,1033.85369237392,1033.94438111999,1034.03506986606,1034.11880857791,
1034.20244408928,1034.28599653269,1034.36948596854,1034.45293991916,1034.53637641301,
1034.61981352278,1034.7032693177,1034.78681381043,1034.87040289338,1034.95412616094,
1035.03480587679,1035.11854458864,1035.2021801,1035.2857325434,1035.36922197925,
1035.45267592987,1035.53611242371,1035.61954953347,1035.70300532839,1035.78654982112,
1035.87013890406,1035.95386217161,1036.03454188751,1036.11828059935,1036.20191611072,
1036.28546855412,1036.36895798997,1036.45241194058,1036.53584843442,1036.61928554418,
1036.70274133909,1036.78628583182,1036.86987491476,1036.95359818232,1037.03427789823,
1037.11801661008,1037.20165212144,1037.28520456484,1037.3686940007,1037.45214795131,
1037.53558444516,1037.61902155491,1037.70247734983,1037.78602184256,1037.8696109255,
1037.95333419306,1038.03401390895,1038.1177526208,1038.20138813216,1038.28494057556,
1038.36843001142,1038.45188396203,1038.53532045588,1038.61875756563,1038.70221336055,
1038.78575785328,1038.86934693622,1038.95307020378,1039.03374991967,1039.11622054546,
1039.1985958952,1039.28089518975,1039.36453651586,1039.44674452642,1039.5311025103,
1039.61546049419),.UNSPECIFIED.);
#708=B_SPLINE_CURVE_WITH_KNOTS('',3,(#92361,#92362,#92363,#92364,#92365,
#92366,#92367,#92368,#92369,#92370),.UNSPECIFIED.,.F.,.F.,(4,3,3,4),(1033.33354879478,
1033.41949132289,1033.50534392917,1033.58398303102),.UNSPECIFIED.);
#709=B_SPLINE_CURVE_WITH_KNOTS('',3,(#92372,#92373,#92374,#92375,#92376,
#92377,#92378,#92379,#92380,#92381,#92382,#92383,#92384),.UNSPECIFIED.,
 .F.,.F.,(4,3,3,3,4),(1033.3328408694,1033.34562447506,1033.45780467658,
1033.56712465127,1033.5839830309),.UNSPECIFIED.);
#710=B_SPLINE_CURVE_WITH_KNOTS('',3,(#92385,#92386,#92387,#92388,#92389,
#92390,#92391,#92392,#92393,#92394,#92395,#92396,#92397,#92398,#92399,#92400,
#92401,#92402,#92403,#92404,#92405,#92406,#92407,#92408,#92409,#92410,#92411,
#92412,#92413,#92414,#92415,#92416,#92417,#92418,#92419,#92420,#92421,#92422,
#92423,#92424,#92425,#92426,#92427,#92428,#92429,#92430,#92431,#92432,#92433,
#92434,#92435,#92436,#92437,#92438,#92439,#92440,#92441,#92442,#92443,#92444,
#92445,#92446,#92447,#92448,#92449,#92450,#92451,#92452,#92453,#92454,#92455,
#92456,#92457,#92458,#92459,#92460,#92461,#92462,#92463,#92464,#92465,#92466,
#92467,#92468,#92469,#92470,#92471,#92472,#92473,#92474,#92475,#92476,#92477,
#92478,#92479,#92480,#92481,#92482,#92483,#92484,#92485,#92486,#92487,#92488,
#92489,#92490,#92491,#92492,#92493,#92494,#92495,#92496,#92497,#92498,#92499,
#92500,#92501,#92502,#92503,#92504,#92505,#92506,#92507,#92508,#92509,#92510,
#92511,#92512,#92513,#92514,#92515,#92516,#92517,#92518,#92519,#92520,#92521,
#92522,#92523,#92524,#92525,#92526,#92527,#92528,#92529,#92530,#92531,#92532,
#92533,#92534,#92535,#92536,#92537,#92538,#92539,#92540,#92541,#92542,#92543,
#92544,#92545,#92546,#92547,#92548,#92549,#92550,#92551,#92552,#92553,#92554,
#92555,#92556,#92557,#92558,#92559,#92560,#92561,#92562,#92563,#92564,#92565,
#92566,#92567,#92568,#92569,#92570,#92571,#92572,#92573,#92574,#92575,#92576,
#92577,#92578,#92579,#92580,#92581,#92582,#92583,#92584,#92585,#92586,#92587,
#92588,#92589,#92590,#92591,#92592,#92593,#92594,#92595,#92596,#92597,#92598,
#92599,#92600,#92601,#92602,#92603,#92604,#92605,#92606,#92607),
 .UNSPECIFIED.,.F.,.F.,(4,3,3,3,3,3,3,3,3,3,3,3,3,3,3,3,3,3,3,3,3,3,3,3,
3,3,3,3,3,3,3,3,3,3,3,3,3,3,3,3,3,3,3,3,3,3,3,3,3,3,3,3,3,3,3,3,3,3,3,3,
3,3,3,3,3,3,3,3,3,3,3,3,3,3,4),(1033.58398303102,1033.66648276244,1033.75134247786,
1033.83375761489,1033.916162907,1033.99857725614,1034.08527306355,1034.1678080953,
1034.25039850859,1034.33310237985,1034.34536048578,1034.42909919763,1034.51273470899,
1034.59628715239,1034.67977658824,1034.76323053885,1034.8466670327,1034.93010414246,
1035.01355993737,1035.0971044301,1035.18069351304,1035.2644167806,1035.3450964965,
1035.42883520835,1035.51247071971,1035.59602316311,1035.67951259896,1035.76296654958,
1035.84640304342,1035.92984015318,1036.0132959481,1036.09684044082,1036.18042952377,
1036.26415279132,1036.34483250722,1036.42857121907,1036.51220673043,1036.59575917383,
1036.67924860968,1036.7627025603,1036.84613905414,1036.9295761639,1037.01303195882,
1037.09657645155,1037.18016553449,1037.26388880205,1037.34456851794,1037.42830722979,
1037.51194274115,1037.59549518455,1037.6789846204,1037.76243857102,1037.84587506486,
1037.92931217462,1038.01276796954,1038.09631246226,1038.17990154521,1038.26362481276,
1038.34430452866,1038.42804324051,1038.51167875187,1038.59523119527,1038.67872063112,
1038.76217458174,1038.84561107558,1038.92904818534,1039.01250398026,1039.09604847299,
1039.17963755593,1039.26336082349,1039.34404053938,1039.43122686491,1039.51828940803,
1039.60520573103,1039.61679924244),.UNSPECIFIED.);
#711=B_SPLINE_CURVE_WITH_KNOTS('',3,(#92613,#92614,#92615,#92616,#92617,
#92618,#92619,#92620,#92621,#92622,#92623,#92624,#92625,#92626,#92627,#92628,
#92629,#92630,#92631,#92632,#92633,#92634,#92635,#92636,#92637,#92638,#92639,
#92640,#92641,#92642,#92643,#92644,#92645,#92646,#92647,#92648,#92649,#92650,
#92651,#92652,#92653,#92654,#92655,#92656,#92657,#92658,#92659,#92660,#92661,
#92662,#92663,#92664,#92665,#92666,#92667,#92668,#92669,#92670,#92671,#92672,
#92673,#92674,#92675,#92676,#92677,#92678,#92679,#92680,#92681,#92682,#92683,
#92684,#92685,#92686,#92687,#92688,#92689,#92690,#92691,#92692,#92693,#92694,
#92695,#92696,#92697,#92698,#92699,#92700,#92701,#92702,#92703,#92704,#92705,
#92706,#92707,#92708,#92709,#92710,#92711,#92712,#92713,#92714,#92715,#92716,
#92717,#92718,#92719,#92720,#92721,#92722,#92723,#92724,#92725,#92726,#92727,
#92728,#92729,#92730,#92731,#92732,#92733,#92734,#92735,#92736,#92737,#92738,
#92739,#92740,#92741,#92742,#92743,#92744,#92745,#92746,#92747,#92748,#92749,
#92750,#92751,#92752,#92753,#92754,#92755,#92756,#92757,#92758,#92759,#92760,
#92761,#92762,#92763,#92764,#92765,#92766,#92767,#92768,#92769,#92770,#92771,
#92772,#92773,#92774,#92775,#92776,#92777,#92778,#92779,#92780,#92781,#92782,
#92783,#92784,#92785,#92786,#92787,#92788,#92789,#92790,#92791,#92792,#92793,
#92794,#92795,#92796,#92797,#92798,#92799,#92800,#92801,#92802,#92803,#92804,
#92805,#92806,#92807,#92808,#92809,#92810,#92811,#92812,#92813,#92814,#92815,
#92816,#92817,#92818,#92819,#92820,#92821,#92822,#92823,#92824,#92825,#92826,
#92827,#92828,#92829,#92830,#92831,#92832),.UNSPECIFIED.,.F.,.F.,(4,3,3,
3,3,3,3,3,3,3,3,3,3,3,3,3,3,3,3,3,3,3,3,3,3,3,3,3,3,3,3,3,3,3,3,3,3,3,3,
3,3,3,3,3,3,3,3,3,3,3,3,3,3,3,3,3,3,3,3,3,3,3,3,3,3,3,3,3,3,3,3,3,3,4),
(1039.8671683382,1040.00043133528,1040.03348593039,1040.11722464224,1040.2008601536,
1040.284412597,1040.36790203285,1040.45135598347,1040.53479247731,1040.61822958707,
1040.70168538198,1040.78522987471,1040.86881895765,1040.95254222521,1041.03322194111,
1041.11696065296,1041.20059616432,1041.28414860772,1041.36763804357,1041.45109199419,
1041.53452848803,1041.61796559779,1041.70142139271,1041.78496588544,1041.86855496838,
1041.95227823593,1042.03295795183,1042.11669666368,1042.20033217504,1042.28388461844,
1042.36737405429,1042.45082800491,1042.53426449875,1042.61770160851,1042.70115740343,
1042.78470189616,1042.8682909791,1042.95201424665,1043.03269396255,1043.1164326744,
1043.20006818576,1043.28362062916,1043.36711006501,1043.45056401563,1043.53400050947,
1043.61743761923,1043.70089341415,1043.78443790688,1043.86802698982,1043.95175025737,
1044.03242997327,1044.11616868512,1044.19980419648,1044.28335663988,1044.36684607573,
1044.45030002635,1044.53373652019,1044.61717362995,1044.70062942487,1044.7841739176,
1044.86776300054,1044.95148626809,1045.03216598399,1045.11591254731,1045.1995541538,
1045.2869547973,1045.37043923893,1045.45388648413,1045.53731462072,1045.62074171969,
1045.70421650828,1045.78771938856,1045.87130266069,1045.89875930182),
 .UNSPECIFIED.);
#712=B_SPLINE_CURVE_WITH_KNOTS('',3,(#92833,#92834,#92835,#92836,#92837,
#92838,#92839,#92840,#92841,#92842),.UNSPECIFIED.,.F.,.F.,(4,3,3,4),(1039.61546049419,
1039.69771884837,1039.78244359319,1039.86716833801),.UNSPECIFIED.);
#713=B_SPLINE_CURVE_WITH_KNOTS('',3,(#92844,#92845,#92846,#92847,#92848,
#92849,#92850,#92851,#92852,#92853),.UNSPECIFIED.,.F.,.F.,(4,3,3,4),(1039.61679924244,
1039.70355771309,1039.79019167618,1039.8671683382),.UNSPECIFIED.);
#714=B_SPLINE_CURVE_WITH_KNOTS('',3,(#92854,#92855,#92856,#92857,#92858,
#92859,#92860,#92861,#92862,#92863,#92864,#92865,#92866,#92867,#92868,#92869,
#92870,#92871,#92872,#92873,#92874,#92875,#92876,#92877,#92878,#92879,#92880,
#92881,#92882,#92883,#92884,#92885,#92886,#92887,#92888,#92889,#92890,#92891,
#92892,#92893,#92894,#92895,#92896,#92897,#92898,#92899,#92900,#92901,#92902,
#92903,#92904,#92905,#92906,#92907,#92908,#92909,#92910,#92911,#92912,#92913,
#92914,#92915,#92916,#92917,#92918,#92919,#92920,#92921,#92922,#92923,#92924,
#92925,#92926,#92927,#92928,#92929,#92930,#92931,#92932,#92933,#92934,#92935,
#92936,#92937,#92938,#92939,#92940,#92941,#92942,#92943,#92944,#92945,#92946,
#92947,#92948,#92949,#92950,#92951,#92952,#92953,#92954,#92955,#92956,#92957,
#92958,#92959,#92960,#92961,#92962,#92963,#92964,#92965,#92966,#92967,#92968,
#92969,#92970,#92971,#92972,#92973,#92974,#92975,#92976,#92977,#92978,#92979,
#92980,#92981,#92982,#92983,#92984,#92985,#92986,#92987,#92988,#92989,#92990,
#92991,#92992,#92993,#92994,#92995,#92996,#92997,#92998,#92999,#93000,#93001,
#93002,#93003,#93004,#93005,#93006,#93007,#93008,#93009,#93010,#93011,#93012,
#93013,#93014,#93015,#93016,#93017,#93018,#93019,#93020,#93021,#93022,#93023,
#93024,#93025,#93026,#93027,#93028,#93029,#93030,#93031,#93032,#93033,#93034,
#93035,#93036,#93037,#93038,#93039,#93040,#93041,#93042,#93043,#93044,#93045,
#93046,#93047,#93048,#93049,#93050,#93051,#93052,#93053,#93054,#93055,#93056,
#93057,#93058,#93059,#93060,#93061,#93062,#93063,#93064,#93065,#93066,#93067,
#93068,#93069,#93070,#93071,#93072,#93073),.UNSPECIFIED.,.F.,.F.,(4,3,3,
3,3,3,3,3,3,3,3,3,3,3,3,3,3,3,3,3,3,3,3,3,3,3,3,3,3,3,3,3,3,3,3,3,3,3,3,
3,3,3,3,3,3,3,3,3,3,3,3,3,3,3,3,3,3,3,3,3,3,3,3,3,3,3,3,3,3,3,3,3,3,4),
(1039.86716833831,1039.95546537544,1040.04391200484,1040.13259910912,1040.22141726067,
1040.31044353939,1040.3437765501,1040.42751526195,1040.51115077331,1040.59470321671,
1040.67819265256,1040.76164660318,1040.84508309702,1040.92852020678,1041.01197600169,
1041.09552049442,1041.17910957736,1041.26283284492,1041.34351256082,1041.42725127267,
1041.51088678403,1041.59443922743,1041.67792866328,1041.7613826139,1041.84481910774,
1041.9282562175,1042.01171201242,1042.09525650515,1042.17884558809,1042.26256885564,
1042.34324857154,1042.42698728339,1042.51062279475,1042.59417523815,1042.677664674,
1042.76111862462,1042.84455511846,1042.92799222822,1043.01144802314,1043.09499251587,
1043.17858159881,1043.26230486636,1043.34298458226,1043.42672329411,1043.51035880547,
1043.59391124887,1043.67740068472,1043.76085463534,1043.84429112918,1043.92772823894,
1044.01118403386,1044.09472852659,1044.17831760953,1044.26204087708,1044.34272059298,
1044.42645930483,1044.51009481619,1044.59364725959,1044.67713669544,1044.76059064606,
1044.8440271399,1044.92746424966,1045.01092004458,1045.09446453731,1045.17805362025,
1045.2617768878,1045.3424566037,1045.42495207221,1045.50735166068,1045.5896745793,
1045.67193861608,1045.75416729317,1045.83639550835,1045.89873380757),
 .UNSPECIFIED.);
#715=B_SPLINE_CURVE_WITH_KNOTS('',3,(#93079,#93080,#93081,#93082,#93083,
#93084,#93085,#93086,#93087,#93088,#93089,#93090,#93091,#93092,#93093,#93094,
#93095,#93096,#93097,#93098,#93099,#93100,#93101,#93102,#93103,#93104,#93105,
#93106,#93107,#93108,#93109,#93110,#93111,#93112,#93113,#93114,#93115,#93116,
#93117,#93118,#93119,#93120,#93121,#93122,#93123,#93124,#93125,#93126,#93127,
#93128,#93129,#93130,#93131,#93132,#93133,#93134,#93135,#93136,#93137,#93138,
#93139,#93140,#93141,#93142,#93143,#93144,#93145,#93146,#93147,#93148,#93149,
#93150,#93151,#93152,#93153,#93154,#93155,#93156,#93157,#93158,#93159,#93160,
#93161,#93162,#93163,#93164,#93165,#93166,#93167,#93168,#93169,#93170,#93171,
#93172,#93173,#93174,#93175,#93176,#93177,#93178,#93179,#93180,#93181,#93182,
#93183,#93184,#93185,#93186,#93187,#93188,#93189,#93190,#93191,#93192,#93193,
#93194,#93195,#93196,#93197,#93198,#93199,#93200,#93201,#93202,#93203,#93204,
#93205,#93206,#93207,#93208,#93209,#93210,#93211,#93212,#93213,#93214,#93215,
#93216,#93217,#93218,#93219,#93220,#93221,#93222,#93223,#93224,#93225,#93226,
#93227,#93228,#93229,#93230,#93231,#93232,#93233,#93234,#93235,#93236,#93237,
#93238,#93239,#93240,#93241,#93242,#93243,#93244,#93245,#93246,#93247,#93248,
#93249,#93250,#93251,#93252,#93253,#93254,#93255,#93256,#93257,#93258,#93259,
#93260,#93261,#93262,#93263,#93264,#93265,#93266,#93267,#93268,#93269,#93270,
#93271,#93272,#93273,#93274,#93275,#93276,#93277,#93278,#93279,#93280,#93281,
#93282,#93283,#93284,#93285,#93286,#93287,#93288,#93289,#93290,#93291,#93292,
#93293,#93294,#93295,#93296,#93297,#93298),.UNSPECIFIED.,.F.,.F.,(4,3,3,
3,3,3,3,3,3,3,3,3,3,3,3,3,3,3,3,3,3,3,3,3,3,3,3,3,3,3,3,3,3,3,3,3,3,3,3,
3,3,3,3,3,3,3,3,3,3,3,3,3,3,3,3,3,3,3,3,3,3,3,3,3,3,3,3,3,3,3,3,3,3,4),
(1046.15035364551,1046.23288320853,1046.3153236935,1046.39769619985,1046.48002751776,
1046.56233869259,1046.64464869556,1046.72697649462,1046.80938909424,1046.89184719101,
1046.9744299043,1047.03163800543,1047.11537671728,1047.19901222864,1047.28256467204,
1047.36605410789,1047.44950805851,1047.53294455235,1047.61638166211,1047.69983745703,
1047.78338194976,1047.8669710327,1047.95069430026,1048.03137401615,1048.115112728,
1048.19874823936,1048.28230068276,1048.36579011861,1048.44924406923,1048.53268056307,
1048.61611767283,1048.69957346774,1048.78311796047,1048.86670704341,1048.95043031097,
1049.03111002687,1049.11484873872,1049.19848425008,1049.28203669348,1049.36552612933,
1049.44898007995,1049.53241657379,1049.61585368355,1049.69930947847,1049.7828539712,
1049.86644305414,1049.95016632169,1050.03084603759,1050.11458474944,1050.1982202608,
1050.2817727042,1050.36526214005,1050.44871609067,1050.53215258451,1050.61558969427,
1050.69904548919,1050.78258998192,1050.86617906486,1050.94990233242,1051.03058204831,
1051.11432076016,1051.19795627152,1051.28150871492,1051.36499815077,1051.44845210139,
1051.53188859523,1051.61532570499,1051.69878149991,1051.78232599264,1051.86591507558,
1051.94963834313,1052.03031805903,1052.12323529288,1052.1831732766),
 .UNSPECIFIED.);
#716=B_SPLINE_CURVE_WITH_KNOTS('',3,(#93299,#93300,#93301,#93302,#93303,
#93304,#93305,#93306,#93307,#93308),.UNSPECIFIED.,.F.,.F.,(4,3,3,4),(1045.89875930182,
1045.98249444655,1046.03190199471,1046.15035364538),.UNSPECIFIED.);
#717=B_SPLINE_CURVE_WITH_KNOTS('',3,(#93310,#93311,#93312,#93313,#93314,
#93315,#93316,#93317,#93318,#93319),.UNSPECIFIED.,.F.,.F.,(4,3,3,4),(1045.89873380757,
1045.98099839907,1046.06567602216,1046.15035364526),.UNSPECIFIED.);
#718=B_SPLINE_CURVE_WITH_KNOTS('',3,(#93320,#93321,#93322,#93323,#93324,
#93325,#93326,#93327,#93328,#93329,#93330,#93331,#93332,#93333,#93334,#93335,
#93336,#93337,#93338,#93339,#93340,#93341,#93342,#93343,#93344,#93345,#93346,
#93347,#93348,#93349,#93350,#93351,#93352,#93353,#93354,#93355,#93356,#93357,
#93358,#93359,#93360,#93361,#93362,#93363,#93364,#93365,#93366,#93367,#93368,
#93369,#93370,#93371,#93372,#93373,#93374,#93375,#93376,#93377,#93378,#93379,
#93380,#93381,#93382,#93383,#93384,#93385,#93386,#93387,#93388,#93389,#93390,
#93391,#93392,#93393,#93394,#93395,#93396,#93397,#93398,#93399,#93400,#93401,
#93402,#93403,#93404,#93405,#93406,#93407,#93408,#93409,#93410,#93411,#93412,
#93413,#93414,#93415,#93416,#93417,#93418,#93419,#93420,#93421,#93422,#93423,
#93424,#93425,#93426,#93427,#93428,#93429,#93430,#93431,#93432,#93433,#93434,
#93435,#93436,#93437,#93438,#93439,#93440,#93441,#93442,#93443,#93444,#93445,
#93446,#93447,#93448,#93449,#93450,#93451,#93452,#93453,#93454,#93455,#93456,
#93457,#93458,#93459,#93460,#93461,#93462,#93463,#93464,#93465,#93466,#93467,
#93468,#93469,#93470,#93471,#93472,#93473,#93474,#93475,#93476,#93477,#93478,
#93479,#93480,#93481,#93482,#93483,#93484,#93485,#93486,#93487,#93488,#93489,
#93490,#93491,#93492,#93493,#93494,#93495,#93496,#93497,#93498,#93499,#93500,
#93501,#93502,#93503,#93504,#93505,#93506,#93507,#93508,#93509,#93510,#93511,
#93512,#93513,#93514,#93515,#93516,#93517,#93518,#93519,#93520,#93521,#93522,
#93523,#93524,#93525,#93526,#93527,#93528,#93529,#93530,#93531,#93532,#93533,
#93534,#93535,#93536),.UNSPECIFIED.,.F.,.F.,(4,3,3,3,3,3,3,3,3,3,3,3,3,
3,3,3,3,3,3,3,3,3,3,3,3,3,3,3,3,3,3,3,3,3,3,3,3,3,3,3,3,3,3,3,3,3,3,3,3,
3,3,3,3,3,3,3,3,3,3,3,3,3,3,3,3,3,3,3,3,3,3,3,4),(1046.15035364538,1046.27318238103,
1046.34219261442,1046.42593132627,1046.50956683763,1046.59311928103,1046.67660871688,
1046.7600626675,1046.84349916134,1046.9269362711,1047.01039206602,1047.09393655875,
1047.17752564169,1047.26124890924,1047.34192862514,1047.42566733699,1047.50930284835,
1047.59285529175,1047.6763447276,1047.75979867822,1047.84323517206,1047.92667228182,
1048.01012807674,1048.09367256947,1048.17726165241,1048.26098491996,1048.34166463586,
1048.42540334771,1048.50903885907,1048.59259130247,1048.67608073832,1048.75953468894,
1048.84297118278,1048.92640829254,1049.00986408746,1049.09340858019,1049.17699766313,
1049.26072093069,1049.34140064658,1049.42513935843,1049.50877486979,1049.59232731319,
1049.67581674904,1049.75927069966,1049.8427071935,1049.92614430326,1050.00960009818,
1050.09314459091,1050.17673367385,1050.2604569414,1050.3411366573,1050.42487536915,
1050.50851088051,1050.59206332391,1050.67555275976,1050.75900671038,1050.84244320422,
1050.92588031398,1051.0093361089,1051.09288060163,1051.17646968457,1051.26019295212,
1051.34087266802,1051.42462082925,1051.50826369638,1051.59246877201,1051.67595479842,
1051.75940245836,1051.84282984086,1051.92759845601,1052.01106613505,1052.09648521824,
1052.18190430144),.UNSPECIFIED.);
#719=B_SPLINE_CURVE_WITH_KNOTS('',3,(#93542,#93543,#93544,#93545,#93546,
#93547,#93548,#93549,#93550,#93551,#93552,#93553,#93554,#93555,#93556,#93557,
#93558,#93559,#93560,#93561,#93562,#93563,#93564,#93565,#93566,#93567,#93568,
#93569,#93570,#93571,#93572,#93573,#93574,#93575,#93576,#93577,#93578,#93579,
#93580,#93581,#93582,#93583,#93584,#93585,#93586,#93587,#93588,#93589,#93590,
#93591,#93592,#93593,#93594,#93595,#93596,#93597,#93598,#93599,#93600,#93601,
#93602,#93603,#93604,#93605,#93606,#93607,#93608,#93609,#93610,#93611,#93612,
#93613,#93614,#93615,#93616,#93617,#93618,#93619,#93620,#93621,#93622,#93623,
#93624,#93625,#93626,#93627,#93628,#93629,#93630,#93631,#93632,#93633,#93634,
#93635,#93636,#93637,#93638,#93639,#93640,#93641,#93642,#93643,#93644,#93645,
#93646,#93647,#93648,#93649,#93650,#93651,#93652,#93653,#93654,#93655,#93656,
#93657,#93658,#93659,#93660,#93661,#93662,#93663,#93664,#93665,#93666,#93667,
#93668,#93669,#93670,#93671,#93672,#93673,#93674,#93675,#93676,#93677,#93678,
#93679,#93680,#93681,#93682,#93683,#93684,#93685,#93686,#93687,#93688,#93689,
#93690,#93691,#93692,#93693,#93694,#93695,#93696,#93697,#93698,#93699,#93700,
#93701,#93702,#93703,#93704,#93705,#93706,#93707,#93708,#93709,#93710,#93711,
#93712,#93713,#93714,#93715,#93716,#93717,#93718,#93719,#93720,#93721,#93722,
#93723,#93724,#93725,#93726,#93727,#93728,#93729,#93730,#93731,#93732,#93733,
#93734,#93735,#93736,#93737,#93738,#93739,#93740,#93741,#93742,#93743,#93744,
#93745,#93746,#93747,#93748,#93749,#93750,#93751,#93752,#93753,#93754,#93755,
#93756,#93757,#93758,#93759,#93760,#93761),.UNSPECIFIED.,.F.,.F.,(4,3,3,
3,3,3,3,3,3,3,3,3,3,3,3,3,3,3,3,3,3,3,3,3,3,3,3,3,3,3,3,3,3,3,3,3,3,3,3,
3,3,3,3,3,3,3,3,3,3,3,3,3,3,3,3,3,3,3,3,3,3,3,3,3,3,3,3,3,3,3,3,3,3,4),
(1052.43353895256,1052.51817430875,1052.60283405086,1052.68753441534,1052.77316432894,
1052.85804489543,1052.94404948259,1053.03005406975,1053.1137927816,1053.19742829296,
1053.28098073636,1053.36447017221,1053.44792412283,1053.53136061667,1053.61479772643,
1053.69825352135,1053.78179801408,1053.86538709702,1053.94911036457,1054.02979008047,
1054.11352879232,1054.19716430368,1054.28071674708,1054.36420618293,1054.44766013355,
1054.53109662739,1054.61453373715,1054.69798953207,1054.78153402479,1054.86512310774,
1054.94884637529,1055.02952609119,1055.11326480304,1055.1969003144,1055.2804527578,
1055.36394219365,1055.44739614427,1055.53083263811,1055.61426974787,1055.69772554279,
1055.78127003552,1055.86485911846,1055.94858238601,1056.02926210191,1056.11300081376,
1056.19663632512,1056.28018876852,1056.36367820437,1056.44713215499,1056.53056864883,
1056.61400575859,1056.69746155351,1056.78100604624,1056.86459512918,1056.94831839673,
1057.02899811263,1057.11273682448,1057.19637233584,1057.27992477924,1057.36341421509,
1057.44686816571,1057.53030465955,1057.61374176931,1057.69719756423,1057.78074205696,
1057.8643311399,1057.94805440745,1058.02873412335,1058.11213530925,1058.19543350021,
1058.27862999203,1058.36176800281,1058.44486147418,1058.46567809412),
 .UNSPECIFIED.);
#720=B_SPLINE_CURVE_WITH_KNOTS('',3,(#93762,#93763,#93764,#93765,#93766,
#93767,#93768,#93769,#93770,#93771),.UNSPECIFIED.,.F.,.F.,(4,3,3,4),(1052.1831732766,
1052.27561523447,1052.36763343095,1052.43353895238),.UNSPECIFIED.);
#721=B_SPLINE_CURVE_WITH_KNOTS('',3,(#93773,#93774,#93775,#93776,#93777,
#93778,#93779,#93780,#93781,#93782),.UNSPECIFIED.,.F.,.F.,(4,3,3,4),(1052.18190430144,
1052.2656295259,1052.34060867874,1052.43353895256),.UNSPECIFIED.);
#722=B_SPLINE_CURVE_WITH_KNOTS('',3,(#93783,#93784,#93785,#93786,#93787,
#93788,#93789,#93790,#93791,#93792,#93793,#93794,#93795,#93796,#93797,#93798,
#93799,#93800,#93801,#93802,#93803,#93804,#93805,#93806,#93807,#93808,#93809,
#93810,#93811,#93812,#93813,#93814,#93815,#93816,#93817,#93818,#93819,#93820,
#93821,#93822,#93823,#93824,#93825,#93826,#93827,#93828,#93829,#93830,#93831,
#93832,#93833,#93834,#93835,#93836,#93837,#93838,#93839,#93840,#93841,#93842,
#93843,#93844,#93845,#93846,#93847,#93848,#93849,#93850,#93851,#93852,#93853,
#93854,#93855,#93856,#93857,#93858,#93859,#93860,#93861,#93862,#93863,#93864,
#93865,#93866,#93867,#93868,#93869,#93870,#93871,#93872,#93873,#93874,#93875,
#93876,#93877,#93878,#93879,#93880,#93881,#93882,#93883,#93884,#93885,#93886,
#93887,#93888,#93889,#93890,#93891,#93892,#93893,#93894,#93895,#93896,#93897,
#93898,#93899,#93900,#93901,#93902,#93903,#93904,#93905,#93906,#93907,#93908,
#93909,#93910,#93911,#93912,#93913,#93914,#93915,#93916,#93917,#93918,#93919,
#93920,#93921,#93922,#93923,#93924,#93925,#93926,#93927,#93928,#93929,#93930,
#93931,#93932,#93933,#93934,#93935,#93936,#93937,#93938,#93939,#93940,#93941,
#93942,#93943,#93944,#93945,#93946,#93947,#93948,#93949,#93950,#93951,#93952,
#93953,#93954,#93955,#93956,#93957,#93958,#93959,#93960,#93961,#93962,#93963,
#93964,#93965,#93966,#93967,#93968,#93969,#93970,#93971,#93972,#93973,#93974,
#93975,#93976,#93977,#93978,#93979,#93980,#93981,#93982,#93983,#93984,#93985,
#93986,#93987,#93988,#93989,#93990,#93991,#93992,#93993,#93994,#93995,#93996,
#93997,#93998,#93999,#94000,#94001,#94002),.UNSPECIFIED.,.F.,.F.,(4,3,3,
3,3,3,3,3,3,3,3,3,3,3,3,3,3,3,3,3,3,3,3,3,3,3,3,3,3,3,3,3,3,3,3,3,3,3,3,
3,3,3,3,3,3,3,3,3,3,3,3,3,3,3,3,3,3,3,3,3,3,3,3,3,3,3,3,3,3,3,3,3,3,4),
(1052.43353895269,1052.51622961888,1052.59882640096,1052.68135031557,1052.76382644087,
1052.84627784904,1052.92872342611,1053.011182051,1053.09372349006,1053.17630598907,
1053.25902043882,1053.34034468946,1053.42408340131,1053.50771891267,1053.59127135607,
1053.67476079192,1053.75821474254,1053.84165123638,1053.92508834614,1054.00854414106,
1054.09208863378,1054.17567771673,1054.25940098428,1054.34008070018,1054.42381941203,
1054.50745492339,1054.59100736679,1054.67449680264,1054.75795075326,1054.8413872471,
1054.92482435686,1055.00828015178,1055.09182464451,1055.17541372745,1055.259136995,
1055.3398167109,1055.42355542275,1055.50719093411,1055.59074337751,1055.67423281336,
1055.75768676398,1055.84112325782,1055.92456036758,1056.00801616249,1056.09156065522,
1056.17514973816,1056.25887300572,1056.33955272162,1056.42329143347,1056.50692694483,
1056.59047938823,1056.67396882409,1056.7574227747,1056.84085926855,1056.9242963783,
1057.00775217322,1057.09129666595,1057.17488574889,1057.25860901645,1057.33928873234,
1057.42302744419,1057.50666295555,1057.59021539895,1057.6737048348,1057.75715878542,
1057.84059527926,1057.92403238902,1058.00748818394,1058.09103267667,1058.17462175961,
1058.25834502717,1058.33902474307,1058.43375410464,1058.46629045166),
 .UNSPECIFIED.);
#723=B_SPLINE_CURVE_WITH_KNOTS('',3,(#94008,#94009,#94010,#94011,#94012,
#94013,#94014,#94015,#94016,#94017,#94018,#94019,#94020,#94021,#94022,#94023,
#94024,#94025,#94026,#94027,#94028,#94029,#94030,#94031,#94032,#94033,#94034,
#94035,#94036,#94037,#94038,#94039,#94040,#94041,#94042,#94043,#94044,#94045,
#94046,#94047,#94048,#94049,#94050,#94051,#94052,#94053,#94054,#94055,#94056,
#94057,#94058,#94059,#94060,#94061,#94062,#94063,#94064,#94065,#94066,#94067,
#94068,#94069,#94070,#94071,#94072,#94073,#94074,#94075,#94076,#94077,#94078,
#94079,#94080,#94081,#94082,#94083,#94084,#94085,#94086,#94087,#94088,#94089,
#94090,#94091,#94092,#94093,#94094,#94095,#94096,#94097,#94098,#94099,#94100,
#94101,#94102,#94103,#94104,#94105,#94106,#94107,#94108,#94109,#94110,#94111,
#94112,#94113,#94114,#94115,#94116,#94117,#94118,#94119,#94120,#94121,#94122,
#94123,#94124,#94125,#94126,#94127,#94128,#94129,#94130,#94131,#94132,#94133,
#94134,#94135,#94136,#94137,#94138,#94139,#94140,#94141,#94142,#94143,#94144,
#94145,#94146,#94147,#94148,#94149,#94150,#94151,#94152,#94153,#94154,#94155,
#94156,#94157,#94158,#94159,#94160,#94161,#94162,#94163,#94164,#94165,#94166,
#94167,#94168,#94169,#94170,#94171,#94172,#94173,#94174,#94175,#94176,#94177,
#94178,#94179,#94180,#94181,#94182,#94183,#94184,#94185,#94186,#94187,#94188,
#94189,#94190,#94191,#94192,#94193,#94194,#94195,#94196,#94197,#94198,#94199,
#94200,#94201,#94202,#94203,#94204,#94205,#94206,#94207,#94208,#94209,#94210,
#94211,#94212,#94213,#94214,#94215,#94216,#94217,#94218,#94219,#94220,#94221,
#94222,#94223,#94224,#94225,#94226,#94227),.UNSPECIFIED.,.F.,.F.,(4,3,3,
3,3,3,3,3,3,3,3,3,3,3,3,3,3,3,3,3,3,3,3,3,3,3,3,3,3,3,3,3,3,3,3,3,3,3,3,
3,3,3,3,3,3,3,3,3,3,3,3,3,3,3,3,3,3,3,3,3,3,3,3,3,3,3,3,3,3,3,3,3,3,4),
(1058.7167242599,1058.81602550497,1058.9160811218,1059.01693437788,1059.02847013407,
1059.11220884592,1059.19584435728,1059.27939680068,1059.36288623653,1059.44634018715,
1059.52977668099,1059.61321379075,1059.69666958567,1059.7802140784,1059.86380316134,
1059.94752642889,1060.02820614479,1060.11194485664,1060.195580368,1060.2791328114,
1060.36262224725,1060.44607619787,1060.52951269171,1060.61294980147,1060.69640559639,
1060.77995008912,1060.86353917206,1060.94726243961,1061.02794215551,1061.11168086736,
1061.19531637872,1061.27886882212,1061.36235825797,1061.44581220859,1061.52924870243,
1061.61268581219,1061.69614160711,1061.77968609984,1061.86327518278,1061.94699845033,
1062.02767816623,1062.11141687808,1062.19505238944,1062.27860483284,1062.36209426869,
1062.44554821931,1062.52898471315,1062.61242182291,1062.69587761783,1062.77942211056,
1062.8630111935,1062.94673446106,1063.02741417695,1063.1111528888,1063.19478840016,
1063.27834084356,1063.36183027941,1063.44528423003,1063.52872072387,1063.61215783363,
1063.69561362855,1063.77915812128,1063.86274720422,1063.94647047177,1064.02715018767,
1064.11052917265,1064.19377633222,1064.27694739578,1064.3600608703,1064.4431352178,
1064.52620538345,1064.60927132662,1064.69238160085,1064.74815950499),
 .UNSPECIFIED.);
#724=B_SPLINE_CURVE_WITH_KNOTS('',3,(#94228,#94229,#94230,#94231,#94232,
#94233,#94234,#94235,#94236,#94237),.UNSPECIFIED.,.F.,.F.,(4,3,3,4),(1058.46567809412,
1058.54875458388,1058.63273942181,1058.71672425974),.UNSPECIFIED.);
#725=B_SPLINE_CURVE_WITH_KNOTS('',3,(#94239,#94240,#94241,#94242,#94243,
#94244,#94245,#94246,#94247,#94248),.UNSPECIFIED.,.F.,.F.,(4,3,3,4),(1058.46629045166,
1058.56050203772,1058.6541694428,1058.71672425955),.UNSPECIFIED.);
#726=B_SPLINE_CURVE_WITH_KNOTS('',3,(#94249,#94250,#94251,#94252,#94253,
#94254,#94255,#94256,#94257,#94258,#94259,#94260,#94261,#94262,#94263,#94264,
#94265,#94266,#94267,#94268,#94269,#94270,#94271,#94272,#94273,#94274,#94275,
#94276,#94277,#94278,#94279,#94280,#94281,#94282,#94283,#94284,#94285,#94286,
#94287,#94288,#94289,#94290,#94291,#94292,#94293,#94294,#94295,#94296,#94297,
#94298,#94299,#94300,#94301,#94302,#94303,#94304,#94305,#94306,#94307,#94308,
#94309,#94310,#94311,#94312,#94313,#94314,#94315,#94316,#94317,#94318,#94319,
#94320,#94321,#94322,#94323,#94324,#94325,#94326,#94327,#94328,#94329,#94330,
#94331,#94332,#94333,#94334,#94335,#94336,#94337,#94338,#94339,#94340,#94341,
#94342,#94343,#94344,#94345,#94346,#94347,#94348,#94349,#94350,#94351,#94352,
#94353,#94354,#94355,#94356,#94357,#94358,#94359,#94360,#94361,#94362,#94363,
#94364,#94365,#94366,#94367,#94368,#94369,#94370,#94371,#94372,#94373,#94374,
#94375,#94376,#94377,#94378,#94379,#94380,#94381,#94382,#94383,#94384,#94385,
#94386,#94387,#94388,#94389,#94390,#94391,#94392,#94393,#94394,#94395,#94396,
#94397,#94398,#94399,#94400,#94401,#94402,#94403,#94404,#94405,#94406,#94407,
#94408,#94409,#94410,#94411,#94412,#94413,#94414,#94415,#94416,#94417,#94418,
#94419,#94420,#94421,#94422,#94423,#94424,#94425,#94426,#94427,#94428,#94429,
#94430,#94431,#94432,#94433,#94434,#94435,#94436,#94437,#94438,#94439,#94440,
#94441,#94442,#94443,#94444,#94445,#94446,#94447,#94448,#94449,#94450,#94451,
#94452,#94453,#94454,#94455,#94456,#94457,#94458,#94459,#94460,#94461,#94462,
#94463,#94464,#94465,#94466,#94467,#94468),.UNSPECIFIED.,.F.,.F.,(4,3,3,
3,3,3,3,3,3,3,3,3,3,3,3,3,3,3,3,3,3,3,3,3,3,3,3,3,3,3,3,3,3,3,3,3,3,3,3,
3,3,3,3,3,3,3,3,3,3,3,3,3,3,3,3,3,3,3,3,3,3,3,3,3,3,3,3,3,3,3,3,3,3,4),
(1058.71672425974,1058.80083947402,1058.88496356206,1058.96911362546,1059.0533067791,
1059.13761161675,1059.22198078275,1059.30648352489,1059.33876075378,1059.42249946563,
1059.50613497699,1059.58968742039,1059.67317685624,1059.75663080686,1059.84006730071,
1059.92350441046,1060.00696020538,1060.09050469811,1060.17409378105,1060.25781704861,
1060.33849676451,1060.42223547636,1060.50587098772,1060.58942343112,1060.67291286697,
1060.75636681759,1060.83980331143,1060.92324042119,1061.00669621611,1061.09024070884,
1061.17382979178,1061.25755305934,1061.33823277523,1061.42197148708,1061.50560699844,
1061.58915944184,1061.67264887769,1061.75610282831,1061.83953932215,1061.92297643191,
1062.00643222682,1062.08997671955,1062.17356580249,1062.25728907005,1062.33796878595,
1062.4217074978,1062.50534300916,1062.58889545256,1062.67238488841,1062.75583883903,
1062.83927533287,1062.92271244263,1063.00616823755,1063.08971273028,1063.17330181322,
1063.25702508078,1063.33770479667,1063.42144350852,1063.50507901988,1063.58863146328,
1063.67212089913,1063.75557484975,1063.83901134359,1063.92244845335,1064.00590424827,
1064.08944874099,1064.17303782394,1064.25676109149,1064.33744080739,1064.42121631092,
1064.50485699754,1064.58842010642,1064.67191452514,1064.74899530866),
 .UNSPECIFIED.);
#727=B_SPLINE_CURVE_WITH_KNOTS('',3,(#94474,#94475,#94476,#94477,#94478,
#94479,#94480,#94481,#94482,#94483,#94484,#94485,#94486,#94487,#94488,#94489,
#94490,#94491,#94492,#94493,#94494,#94495,#94496,#94497,#94498,#94499,#94500,
#94501,#94502,#94503,#94504,#94505,#94506,#94507,#94508,#94509,#94510,#94511,
#94512,#94513,#94514,#94515,#94516,#94517,#94518,#94519,#94520,#94521,#94522,
#94523,#94524,#94525,#94526,#94527,#94528,#94529,#94530,#94531,#94532,#94533,
#94534,#94535,#94536,#94537,#94538,#94539,#94540,#94541,#94542,#94543,#94544,
#94545,#94546,#94547,#94548,#94549,#94550,#94551,#94552,#94553,#94554,#94555,
#94556,#94557,#94558,#94559,#94560,#94561,#94562,#94563,#94564,#94565,#94566,
#94567,#94568,#94569,#94570,#94571,#94572,#94573,#94574,#94575,#94576,#94577,
#94578,#94579,#94580,#94581,#94582,#94583,#94584,#94585,#94586,#94587,#94588,
#94589,#94590,#94591,#94592,#94593,#94594,#94595,#94596,#94597,#94598,#94599,
#94600,#94601,#94602,#94603,#94604,#94605,#94606,#94607,#94608,#94609,#94610,
#94611,#94612,#94613,#94614,#94615,#94616,#94617,#94618,#94619,#94620,#94621,
#94622,#94623,#94624,#94625,#94626,#94627,#94628,#94629,#94630,#94631,#94632,
#94633,#94634,#94635,#94636,#94637,#94638,#94639,#94640,#94641,#94642,#94643,
#94644,#94645,#94646,#94647,#94648,#94649,#94650,#94651,#94652,#94653,#94654,
#94655,#94656,#94657,#94658,#94659,#94660,#94661,#94662,#94663,#94664,#94665,
#94666,#94667,#94668,#94669,#94670,#94671,#94672,#94673,#94674,#94675,#94676,
#94677,#94678,#94679,#94680,#94681,#94682,#94683,#94684,#94685,#94686,#94687,
#94688,#94689,#94690,#94691,#94692,#94693,#94694,#94695,#94696),
 .UNSPECIFIED.,.F.,.F.,(4,3,3,3,3,3,3,3,3,3,3,3,3,3,3,3,3,3,3,3,3,3,3,3,
3,3,3,3,3,3,3,3,3,3,3,3,3,3,3,3,3,3,3,3,3,3,3,3,3,3,3,3,3,3,3,3,3,3,3,3,
3,3,3,3,3,3,3,3,3,3,3,3,3,3,4),(1064.99990956692,1065.02688619839,1065.11062491024,
1065.1942604216,1065.277812865,1065.36130230085,1065.44475625147,1065.52819274531,
1065.61162985507,1065.69508564999,1065.77863014272,1065.86221922566,1065.94594249321,
1066.02662220911,1066.11036092096,1066.19399643232,1066.27754887572,1066.36103831157,
1066.44449226219,1066.52792875603,1066.61136586579,1066.69482166071,1066.77836615343,
1066.86195523638,1066.94567850393,1067.02635821983,1067.11009693168,1067.19373244304,
1067.27728488644,1067.36077432229,1067.44422827291,1067.52766476675,1067.61110187651,
1067.69455767143,1067.77810216416,1067.8616912471,1067.94541451465,1068.02609423055,
1068.1098329424,1068.19346845376,1068.27702089716,1068.36051033301,1068.44396428363,
1068.52740077747,1068.61083788723,1068.69429368215,1068.77783817487,1068.86142725782,
1068.94515052537,1069.02583024127,1069.10956895312,1069.19320446448,1069.27675690788,
1069.36024634373,1069.44370029435,1069.52713678819,1069.61057389795,1069.69402969287,
1069.7775741856,1069.86116326854,1069.94488653609,1070.02556625199,1070.10930496384,
1070.1929404752,1070.2764929186,1070.35998235445,1070.44343630507,1070.52687279891,
1070.61030990867,1070.69376570359,1070.77731019632,1070.86089927926,1070.94462254681,
1071.02530226271,1071.03207161914),.UNSPECIFIED.);
#728=B_SPLINE_CURVE_WITH_KNOTS('',3,(#94697,#94698,#94699,#94700,#94701,
#94702,#94703,#94704,#94705,#94706),.UNSPECIFIED.,.F.,.F.,(4,3,3,4),(1064.74815950499,
1064.83136688974,1064.91563822827,1064.9999095668),.UNSPECIFIED.);
#729=B_SPLINE_CURVE_WITH_KNOTS('',3,(#94708,#94709,#94710,#94711,#94712,
#94713,#94714,#94715,#94716,#94717),.UNSPECIFIED.,.F.,.F.,(4,3,3,4),(1064.74899530866,
1064.8324247764,1064.91616717166,1064.99990956692),.UNSPECIFIED.);
#730=B_SPLINE_CURVE_WITH_KNOTS('',3,(#94718,#94719,#94720,#94721,#94722,
#94723,#94724,#94725,#94726,#94727,#94728,#94729,#94730,#94731,#94732,#94733,
#94734,#94735,#94736,#94737,#94738,#94739,#94740,#94741,#94742,#94743,#94744,
#94745,#94746,#94747,#94748,#94749,#94750,#94751,#94752,#94753,#94754,#94755,
#94756,#94757,#94758,#94759,#94760,#94761,#94762,#94763,#94764,#94765,#94766,
#94767,#94768,#94769,#94770,#94771,#94772,#94773,#94774,#94775,#94776,#94777,
#94778,#94779,#94780,#94781,#94782,#94783,#94784,#94785,#94786,#94787,#94788,
#94789,#94790,#94791,#94792,#94793,#94794,#94795,#94796,#94797,#94798,#94799,
#94800,#94801,#94802,#94803,#94804,#94805,#94806,#94807,#94808,#94809,#94810,
#94811,#94812,#94813,#94814,#94815,#94816,#94817,#94818,#94819,#94820,#94821,
#94822,#94823,#94824,#94825,#94826,#94827,#94828,#94829,#94830,#94831,#94832,
#94833,#94834,#94835,#94836,#94837,#94838,#94839,#94840,#94841,#94842,#94843,
#94844,#94845,#94846,#94847,#94848,#94849,#94850,#94851,#94852,#94853,#94854,
#94855,#94856,#94857,#94858,#94859,#94860,#94861,#94862,#94863,#94864,#94865,
#94866,#94867,#94868,#94869,#94870,#94871,#94872,#94873,#94874,#94875,#94876,
#94877,#94878,#94879,#94880,#94881,#94882,#94883,#94884,#94885,#94886,#94887,
#94888,#94889,#94890,#94891,#94892,#94893,#94894,#94895,#94896,#94897,#94898,
#94899,#94900,#94901,#94902,#94903,#94904,#94905,#94906,#94907,#94908,#94909,
#94910,#94911,#94912,#94913,#94914,#94915,#94916,#94917,#94918,#94919,#94920,
#94921,#94922,#94923,#94924,#94925,#94926,#94927,#94928,#94929,#94930,#94931,
#94932,#94933,#94934,#94935,#94936,#94937),.UNSPECIFIED.,.F.,.F.,(4,3,3,
3,3,3,3,3,3,3,3,3,3,3,3,3,3,3,3,3,3,3,3,3,3,3,3,3,3,3,3,3,3,3,3,3,3,3,3,
3,3,3,3,3,3,3,3,3,3,3,3,3,3,3,3,3,3,3,3,3,3,3,3,3,3,3,3,3,3,3,3,3,3,4),
(1064.99990956711,1065.09679960539,1065.19424226973,1065.29234605066,1065.33717681811,
1065.42091552996,1065.50455104132,1065.58810348472,1065.67159292057,1065.75504687119,
1065.83848336503,1065.92192047479,1066.00537626971,1066.08892076244,1066.17250984538,
1066.25623311294,1066.33691282883,1066.42065154068,1066.50428705204,1066.58783949544,
1066.67132893129,1066.75478288191,1066.83821937575,1066.92165648551,1067.00511228042,
1067.08865677315,1067.17224585609,1067.25596912365,1067.33664883955,1067.4203875514,
1067.50402306276,1067.58757550616,1067.67106494201,1067.75451889263,1067.83795538647,
1067.92139249623,1068.00484829115,1068.08839278387,1068.17198186682,1068.25570513437,
1068.33638485027,1068.42012356212,1068.50375907348,1068.58731151688,1068.67080095273,
1068.75425490335,1068.83769139719,1068.92112850695,1069.00458430187,1069.0881287946,
1069.17171787754,1069.2554411451,1069.33612086099,1069.41985957284,1069.5034950842,
1069.5870475276,1069.67053696345,1069.75399091407,1069.83742740791,1069.92086451767,
1070.00432031259,1070.08786480531,1070.17145388826,1070.25517715581,1070.33585687171,
1070.42278545047,1070.50573868767,1070.58861702522,1070.67143920119,1070.75422390752,
1070.83700421657,1070.91978233213,1071.00259875718,1071.03128550181),
 .UNSPECIFIED.);
#731=B_SPLINE_CURVE_WITH_KNOTS('',3,(#94943,#94944,#94945,#94946,#94947,
#94948,#94949,#94950,#94951,#94952,#94953,#94954,#94955,#94956,#94957,#94958,
#94959,#94960,#94961,#94962,#94963,#94964,#94965,#94966,#94967,#94968,#94969,
#94970,#94971,#94972,#94973,#94974,#94975,#94976,#94977,#94978,#94979,#94980,
#94981,#94982,#94983,#94984,#94985,#94986,#94987,#94988,#94989,#94990,#94991,
#94992,#94993,#94994,#94995,#94996,#94997,#94998,#94999,#95000,#95001,#95002,
#95003,#95004,#95005,#95006,#95007,#95008,#95009,#95010,#95011,#95012,#95013,
#95014,#95015,#95016,#95017,#95018,#95019,#95020,#95021,#95022,#95023,#95024,
#95025,#95026,#95027,#95028,#95029,#95030,#95031,#95032,#95033,#95034,#95035,
#95036,#95037,#95038,#95039,#95040,#95041,#95042,#95043,#95044,#95045,#95046,
#95047,#95048,#95049,#95050,#95051,#95052,#95053,#95054,#95055,#95056,#95057,
#95058,#95059,#95060,#95061,#95062,#95063,#95064,#95065,#95066,#95067,#95068,
#95069,#95070,#95071,#95072,#95073,#95074,#95075,#95076,#95077,#95078,#95079,
#95080,#95081,#95082,#95083,#95084,#95085,#95086,#95087,#95088,#95089,#95090,
#95091,#95092,#95093,#95094,#95095,#95096,#95097,#95098,#95099,#95100,#95101,
#95102,#95103,#95104,#95105,#95106,#95107,#95108,#95109,#95110,#95111,#95112,
#95113,#95114,#95115,#95116,#95117,#95118,#95119,#95120,#95121,#95122,#95123,
#95124,#95125,#95126,#95127,#95128,#95129,#95130,#95131,#95132,#95133,#95134,
#95135,#95136,#95137,#95138,#95139,#95140,#95141,#95142,#95143,#95144,#95145,
#95146,#95147,#95148,#95149,#95150,#95151,#95152,#95153,#95154,#95155,#95156,
#95157,#95158,#95159,#95160,#95161,#95162),.UNSPECIFIED.,.F.,.F.,(4,3,3,
3,3,3,3,3,3,3,3,3,3,3,3,3,3,3,3,3,3,3,3,3,3,3,3,3,3,3,3,3,3,3,3,3,3,3,3,
3,3,3,3,3,3,3,3,3,3,3,3,3,3,3,3,3,3,3,3,3,3,3,3,3,3,3,3,3,3,3,3,3,3,4),
(1071.2830948741,1071.36570592697,1071.44827148991,1071.53081372931,1071.61335146039,
1071.69590349219,1071.77853997485,1071.86121848805,1071.9440300644,1072.02503827343,
1072.10877698528,1072.19241249664,1072.27596494004,1072.35945437589,1072.44290832651,
1072.52634482035,1072.60978193011,1072.69323772503,1072.77678221776,1072.8603713007,
1072.94409456825,1073.02477428415,1073.108512996,1073.19214850736,1073.27570095076,
1073.35919038661,1073.44264433723,1073.52608083107,1073.60951794083,1073.69297373575,
1073.77651822848,1073.86010731142,1073.94383057897,1074.02451029487,1074.10824900672,
1074.19188451808,1074.27543696148,1074.35892639733,1074.44238034795,1074.52581684179,
1074.60925395155,1074.69270974647,1074.7762542392,1074.85984332214,1074.94356658969,
1075.02424630559,1075.10798501744,1075.1916205288,1075.2751729722,1075.35866240805,
1075.44211635867,1075.52555285251,1075.60898996227,1075.69244575718,1075.77599024991,
1075.85957933286,1075.94330260041,1076.02398231631,1076.10772102816,1076.19135653952,
1076.27490898292,1076.35839841877,1076.44185236939,1076.52528886323,1076.60872597299,
1076.69218176791,1076.77572626064,1076.85931534358,1076.94303861114,1077.02371832703,
1077.1102533057,1077.19667143783,1077.2829513212,1077.31586327447),
 .UNSPECIFIED.);
#732=B_SPLINE_CURVE_WITH_KNOTS('',3,(#95163,#95164,#95165,#95166,#95167,
#95168,#95169,#95170,#95171,#95172),.UNSPECIFIED.,.F.,.F.,(4,3,3,4),(1071.03207161914,
1071.14037546939,1071.24654262183,1071.28309487398),.UNSPECIFIED.);
#733=B_SPLINE_CURVE_WITH_KNOTS('',3,(#95174,#95175,#95176,#95177,#95178,
#95179,#95180,#95181,#95182,#95183),.UNSPECIFIED.,.F.,.F.,(4,3,3,4),(1071.03128550181,
1071.11419371407,1071.19864429404,1071.283094874),.UNSPECIFIED.);
#734=B_SPLINE_CURVE_WITH_KNOTS('',3,(#95184,#95185,#95186,#95187,#95188,
#95189,#95190,#95191,#95192,#95193,#95194,#95195,#95196,#95197,#95198,#95199,
#95200,#95201,#95202,#95203,#95204,#95205,#95206,#95207,#95208,#95209,#95210,
#95211,#95212,#95213,#95214,#95215,#95216,#95217,#95218,#95219,#95220,#95221,
#95222,#95223,#95224,#95225,#95226,#95227,#95228,#95229,#95230,#95231,#95232,
#95233,#95234,#95235,#95236,#95237,#95238,#95239,#95240,#95241,#95242,#95243,
#95244,#95245,#95246,#95247,#95248,#95249,#95250,#95251,#95252,#95253,#95254,
#95255,#95256,#95257,#95258,#95259,#95260,#95261,#95262,#95263,#95264,#95265,
#95266,#95267,#95268,#95269,#95270,#95271,#95272,#95273,#95274,#95275,#95276,
#95277,#95278,#95279,#95280,#95281,#95282,#95283,#95284,#95285,#95286,#95287,
#95288,#95289,#95290,#95291,#95292,#95293,#95294,#95295,#95296,#95297,#95298,
#95299,#95300,#95301,#95302,#95303,#95304,#95305,#95306,#95307,#95308,#95309,
#95310,#95311,#95312,#95313,#95314,#95315,#95316,#95317,#95318,#95319,#95320,
#95321,#95322,#95323,#95324,#95325,#95326,#95327,#95328,#95329,#95330,#95331,
#95332,#95333,#95334,#95335,#95336,#95337,#95338,#95339,#95340,#95341,#95342,
#95343,#95344,#95345,#95346,#95347,#95348,#95349,#95350,#95351,#95352,#95353,
#95354,#95355,#95356,#95357,#95358,#95359,#95360,#95361,#95362,#95363,#95364,
#95365,#95366,#95367,#95368,#95369,#95370,#95371,#95372,#95373,#95374,#95375,
#95376,#95377,#95378,#95379,#95380,#95381,#95382,#95383,#95384,#95385,#95386,
#95387,#95388,#95389,#95390,#95391,#95392,#95393,#95394,#95395,#95396,#95397,
#95398,#95399,#95400,#95401,#95402,#95403),.UNSPECIFIED.,.F.,.F.,(4,3,3,
3,3,3,3,3,3,3,3,3,3,3,3,3,3,3,3,3,3,3,3,3,3,3,3,3,3,3,3,3,3,3,3,3,3,3,3,
3,3,3,3,3,3,3,3,3,3,3,3,3,3,3,3,3,3,3,3,3,3,3,3,3,3,3,3,3,3,3,3,3,3,4),
(1071.2830948741,1071.33559288243,1071.41933159428,1071.50296710564,1071.58651954904,
1071.67000898489,1071.75346293551,1071.83689942935,1071.92033653911,1072.00379233403,
1072.08733682676,1072.1709259097,1072.25464917725,1072.33532889315,1072.419067605,
1072.50270311636,1072.58625555976,1072.66974499561,1072.75319894623,1072.83663544007,
1072.92007254983,1073.00352834474,1073.08707283747,1073.17066192041,1073.25438518797,
1073.33506490387,1073.41880361572,1073.50243912708,1073.58599157048,1073.66948100633,
1073.75293495695,1073.83637145079,1073.91980856055,1074.00326435547,1074.0868088482,
1074.17039793114,1074.25412119869,1074.33480091459,1074.41853962644,1074.5021751378,
1074.5857275812,1074.66921701705,1074.75267096767,1074.83610746151,1074.91954457127,
1075.00300036619,1075.08654485892,1075.17013394186,1075.25385720941,1075.33453692531,
1075.41827563716,1075.50191114852,1075.58546359192,1075.66895302777,1075.75240697839,
1075.83584347223,1075.91928058199,1076.00273637691,1076.08628086964,1076.16986995258,
1076.25359322014,1076.33427293603,1076.41801271454,1076.50164904323,1076.58520205564,
1076.66869181301,1076.75214480477,1076.83557998726,1076.91901543289,1077.00246921039,
1077.08600678691,1077.16958880796,1077.2532934991,1077.31510334887),
 .UNSPECIFIED.);
#735=B_SPLINE_CURVE_WITH_KNOTS('',3,(#95409,#95410,#95411,#95412,#95413,
#95414,#95415,#95416,#95417,#95418,#95419,#95420,#95421,#95422,#95423,#95424,
#95425,#95426,#95427,#95428,#95429,#95430,#95431,#95432,#95433,#95434,#95435,
#95436,#95437,#95438,#95439,#95440,#95441,#95442,#95443,#95444,#95445,#95446,
#95447,#95448,#95449,#95450,#95451,#95452,#95453,#95454,#95455,#95456,#95457,
#95458,#95459,#95460,#95461,#95462,#95463,#95464,#95465,#95466,#95467,#95468,
#95469,#95470,#95471,#95472,#95473,#95474,#95475,#95476,#95477,#95478,#95479,
#95480,#95481,#95482,#95483,#95484,#95485,#95486,#95487,#95488,#95489,#95490,
#95491,#95492,#95493,#95494,#95495,#95496,#95497,#95498,#95499,#95500,#95501,
#95502,#95503,#95504,#95505,#95506,#95507,#95508,#95509,#95510,#95511,#95512,
#95513,#95514,#95515,#95516,#95517,#95518,#95519,#95520,#95521,#95522,#95523,
#95524,#95525,#95526,#95527,#95528,#95529,#95530,#95531,#95532,#95533,#95534,
#95535,#95536,#95537,#95538,#95539,#95540,#95541,#95542,#95543,#95544,#95545,
#95546,#95547,#95548,#95549,#95550,#95551,#95552,#95553,#95554,#95555,#95556,
#95557,#95558,#95559,#95560,#95561,#95562,#95563,#95564,#95565,#95566,#95567,
#95568,#95569,#95570,#95571,#95572,#95573,#95574,#95575,#95576,#95577,#95578,
#95579,#95580,#95581,#95582,#95583,#95584,#95585,#95586,#95587,#95588,#95589,
#95590,#95591,#95592,#95593,#95594,#95595,#95596,#95597,#95598,#95599,#95600,
#95601,#95602,#95603,#95604,#95605,#95606,#95607,#95608,#95609,#95610,#95611,
#95612,#95613,#95614,#95615,#95616,#95617,#95618,#95619,#95620,#95621,#95622,
#95623,#95624,#95625),.UNSPECIFIED.,.F.,.F.,(4,3,3,3,3,3,3,3,3,3,3,3,3,
3,3,3,3,3,3,3,3,3,3,3,3,3,3,3,3,3,3,3,3,3,3,3,3,3,3,3,3,3,3,3,3,3,3,3,3,
3,3,3,3,3,3,3,3,3,3,3,3,3,3,3,3,3,3,3,3,3,3,3,4),(1077.56628018146,1077.65540590742,
1077.747418015,1077.83700685327,1077.93023059551,1078.02345433775,1078.1071930496,
1078.19082856096,1078.27438100436,1078.35787044021,1078.44132439083,1078.52476088467,
1078.60819799443,1078.69165378935,1078.77519828208,1078.85878736502,1078.94251063257,
1079.02319034847,1079.10692906032,1079.19056457168,1079.27411701508,1079.35760645093,
1079.44106040155,1079.52449689539,1079.60793400515,1079.69138980007,1079.7749342928,
1079.85852337574,1079.94224664329,1080.02292635919,1080.10666507104,1080.1903005824,
1080.2738530258,1080.35734246165,1080.44079641227,1080.52423290611,1080.60767001587,
1080.69112581079,1080.77467030352,1080.85825938646,1080.94198265401,1081.02266236991,
1081.10640108176,1081.19003659312,1081.27358903652,1081.35707847237,1081.44053242299,
1081.52396891683,1081.60740602659,1081.69086182151,1081.77440631423,1081.85799539718,
1081.94171866473,1082.02239838063,1082.10613709248,1082.18977260384,1082.27332504724,
1082.35681448309,1082.44026843371,1082.52370492755,1082.60714203731,1082.69059783223,
1082.77414232496,1082.8577314079,1082.94145467546,1083.02213439135,1083.10460579086,
1083.18698179026,1083.26928161105,1083.35152491953,1083.43373313036,1083.515947388,
1083.59777693235),.UNSPECIFIED.);
#736=B_SPLINE_CURVE_WITH_KNOTS('',3,(#95626,#95627,#95628,#95629,#95630,
#95631,#95632,#95633,#95634,#95635),.UNSPECIFIED.,.F.,.F.,(4,3,3,4),(1077.31586327447,
1077.40199067622,1077.48802043553,1077.56628018128),.UNSPECIFIED.);
#737=B_SPLINE_CURVE_WITH_KNOTS('',3,(#95637,#95638,#95639,#95640,#95641,
#95642,#95643,#95644,#95645,#95646),.UNSPECIFIED.,.F.,.F.,(4,3,3,4),(1077.31510334887,
1077.33400894675,1077.45014456401,1077.56628018128),.UNSPECIFIED.);
#738=B_SPLINE_CURVE_WITH_KNOTS('',3,(#95647,#95648,#95649,#95650,#95651,
#95652,#95653,#95654,#95655,#95656,#95657,#95658,#95659,#95660,#95661,#95662,
#95663,#95664,#95665,#95666,#95667,#95668,#95669,#95670,#95671,#95672,#95673,
#95674,#95675,#95676,#95677,#95678,#95679,#95680,#95681,#95682,#95683,#95684,
#95685,#95686,#95687,#95688,#95689,#95690,#95691,#95692,#95693,#95694,#95695,
#95696,#95697,#95698,#95699,#95700,#95701,#95702,#95703,#95704,#95705,#95706,
#95707,#95708,#95709,#95710,#95711,#95712,#95713,#95714,#95715,#95716,#95717,
#95718,#95719,#95720,#95721,#95722,#95723,#95724,#95725,#95726,#95727,#95728,
#95729,#95730,#95731,#95732,#95733,#95734,#95735,#95736,#95737,#95738,#95739,
#95740,#95741,#95742,#95743,#95744,#95745,#95746,#95747,#95748,#95749,#95750,
#95751,#95752,#95753,#95754,#95755,#95756,#95757,#95758,#95759,#95760,#95761,
#95762,#95763,#95764,#95765,#95766,#95767,#95768,#95769,#95770,#95771,#95772,
#95773,#95774,#95775,#95776,#95777,#95778,#95779,#95780,#95781,#95782,#95783,
#95784,#95785,#95786,#95787,#95788,#95789,#95790,#95791,#95792,#95793,#95794,
#95795,#95796,#95797,#95798,#95799,#95800,#95801,#95802,#95803,#95804,#95805,
#95806,#95807,#95808,#95809,#95810,#95811,#95812,#95813,#95814,#95815,#95816,
#95817,#95818,#95819,#95820,#95821,#95822,#95823,#95824,#95825,#95826,#95827,
#95828,#95829,#95830,#95831,#95832,#95833,#95834,#95835,#95836,#95837,#95838,
#95839,#95840,#95841,#95842,#95843,#95844,#95845,#95846,#95847,#95848,#95849,
#95850,#95851,#95852,#95853,#95854,#95855,#95856,#95857,#95858,#95859,#95860,
#95861,#95862,#95863,#95864,#95865,#95866),.UNSPECIFIED.,.F.,.F.,(4,3,3,
3,3,3,3,3,3,3,3,3,3,3,3,3,3,3,3,3,3,3,3,3,3,3,3,3,3,3,3,3,3,3,3,3,3,3,3,
3,3,3,3,3,3,3,3,3,3,3,3,3,3,3,3,3,3,3,3,3,3,3,3,3,3,3,3,3,3,3,3,3,3,4),
(1077.5662801814,1077.64875192614,1077.73437605505,1077.81675837873,1077.89912927429,
1077.98150766719,1078.06391248638,1078.14640674046,1078.22895416328,1078.31161736021,
1078.33374495747,1078.41748366932,1078.50111918068,1078.58467162408,1078.66816105993,
1078.75161501055,1078.83505150439,1078.91848861415,1079.00194440907,1079.0854889018,
1079.16907798474,1079.2528012523,1079.33348096819,1079.41721968004,1079.5008551914,
1079.5844076348,1079.66789707065,1079.75135102127,1079.83478751511,1079.91822462487,
1080.00168041978,1080.08522491251,1080.16881399545,1080.25253726301,1080.33321697891,
1080.41695569076,1080.50059120212,1080.58414364552,1080.66763308137,1080.75108703199,
1080.83452352583,1080.91796063559,1081.00141643051,1081.08496092323,1081.16855000618,
1081.25227327373,1081.33295298963,1081.41669170148,1081.50032721284,1081.58387965624,
1081.66736909209,1081.75082304271,1081.83425953655,1081.91769664631,1082.00115244123,
1082.08469693396,1082.1682860169,1082.25200928446,1082.33268900035,1082.4164277122,
1082.50006322356,1082.58361566696,1082.66710510281,1082.75055905343,1082.83399554727,
1082.91743265703,1083.00088845195,1083.08443294467,1083.16802202762,1083.25174529517,
1083.33242501107,1083.41982905484,1083.50946898265,1083.59910891046),
 .UNSPECIFIED.);
#739=B_SPLINE_CURVE_WITH_KNOTS('',3,(#95872,#95873,#95874,#95875,#95876,
#95877,#95878,#95879,#95880,#95881,#95882,#95883,#95884,#95885,#95886,#95887,
#95888,#95889,#95890,#95891,#95892,#95893,#95894,#95895,#95896,#95897,#95898,
#95899,#95900,#95901,#95902,#95903,#95904,#95905,#95906,#95907,#95908,#95909,
#95910,#95911,#95912,#95913,#95914,#95915,#95916,#95917,#95918,#95919,#95920,
#95921,#95922,#95923,#95924,#95925,#95926,#95927,#95928,#95929,#95930,#95931,
#95932,#95933,#95934,#95935,#95936,#95937,#95938,#95939,#95940,#95941,#95942,
#95943,#95944,#95945,#95946,#95947,#95948,#95949,#95950,#95951,#95952,#95953,
#95954,#95955,#95956,#95957,#95958,#95959,#95960,#95961,#95962,#95963,#95964,
#95965,#95966,#95967,#95968,#95969,#95970,#95971,#95972,#95973,#95974,#95975,
#95976,#95977,#95978,#95979,#95980,#95981,#95982,#95983,#95984,#95985,#95986,
#95987,#95988,#95989,#95990,#95991,#95992,#95993,#95994,#95995,#95996,#95997,
#95998,#95999,#96000,#96001,#96002,#96003,#96004,#96005,#96006,#96007,#96008,
#96009,#96010,#96011,#96012,#96013,#96014,#96015,#96016,#96017,#96018,#96019,
#96020,#96021,#96022,#96023,#96024,#96025,#96026,#96027,#96028,#96029,#96030,
#96031,#96032,#96033,#96034,#96035,#96036,#96037,#96038,#96039,#96040,#96041,
#96042,#96043,#96044,#96045,#96046,#96047,#96048,#96049,#96050,#96051,#96052,
#96053,#96054,#96055,#96056,#96057,#96058,#96059,#96060,#96061,#96062,#96063,
#96064,#96065,#96066,#96067,#96068,#96069,#96070,#96071,#96072,#96073,#96074,
#96075,#96076,#96077,#96078,#96079,#96080,#96081,#96082,#96083,#96084,#96085,
#96086,#96087,#96088,#96089,#96090,#96091),.UNSPECIFIED.,.F.,.F.,(4,3,3,
3,3,3,3,3,3,3,3,3,3,3,3,3,3,3,3,3,3,3,3,3,3,3,3,3,3,3,3,3,3,3,3,3,3,3,3,
3,3,3,3,3,3,3,3,3,3,3,3,3,3,3,3,3,3,3,3,3,3,3,3,3,3,3,3,3,3,3,3,3,3,4),
(1083.84946548846,1083.97987942881,1084.02187040207,1084.10560911392,1084.18924462528,
1084.27279706868,1084.35628650453,1084.43974045515,1084.52317694899,1084.60661405875,
1084.69006985367,1084.77361434639,1084.85720342934,1084.94092669689,1085.02160641279,
1085.10534512464,1085.188980636,1085.2725330794,1085.35602251525,1085.43947646587,
1085.52291295971,1085.60635006947,1085.68980586439,1085.77335035712,1085.85693944006,
1085.94066270762,1086.02134242351,1086.10508113536,1086.18871664672,1086.27226909012,
1086.35575852597,1086.43921247659,1086.52264897043,1086.60608608019,1086.68954187511,
1086.77308636784,1086.85667545078,1086.94039871833,1087.02107843423,1087.10481714608,
1087.18845265744,1087.27200510084,1087.35549453669,1087.43894848731,1087.52238498115,
1087.60582209091,1087.68927788583,1087.77282237856,1087.8564114615,1087.94013472905,
1088.02081444495,1088.1045531568,1088.18818866816,1088.27174111156,1088.35523054741,
1088.43868449803,1088.52212099187,1088.60555810163,1088.68901389654,1088.77255838927,
1088.85614747221,1088.93987073977,1089.02055045567,1089.10429739757,1089.18793930218,
1089.27457754563,1089.35806234902,1089.44150967684,1089.52493761718,1089.60836424112,
1089.69183721346,1089.77533808313,1089.85891674814,1089.8810452498),
 .UNSPECIFIED.);
#740=B_SPLINE_CURVE_WITH_KNOTS('',3,(#96092,#96093,#96094,#96095,#96096,
#96097,#96098,#96099,#96100,#96101),.UNSPECIFIED.,.F.,.F.,(4,3,3,4),(1083.59777693235,
1083.68003168255,1083.76474858542,1083.84946548828),.UNSPECIFIED.);
#741=B_SPLINE_CURVE_WITH_KNOTS('',3,(#96103,#96104,#96105,#96106,#96107,
#96108,#96109,#96110,#96111,#96112),.UNSPECIFIED.,.F.,.F.,(4,3,3,4),(1083.59910891046,
1083.68607846829,1083.77291433074,1083.84946548846),.UNSPECIFIED.);
#742=B_SPLINE_CURVE_WITH_KNOTS('',3,(#96113,#96114,#96115,#96116,#96117,
#96118,#96119,#96120,#96121,#96122,#96123,#96124,#96125,#96126,#96127,#96128,
#96129,#96130,#96131,#96132,#96133,#96134,#96135,#96136,#96137,#96138,#96139,
#96140,#96141,#96142,#96143,#96144,#96145,#96146,#96147,#96148,#96149,#96150,
#96151,#96152,#96153,#96154,#96155,#96156,#96157,#96158,#96159,#96160,#96161,
#96162,#96163,#96164,#96165,#96166,#96167,#96168,#96169,#96170,#96171,#96172,
#96173,#96174,#96175,#96176,#96177,#96178,#96179,#96180,#96181,#96182,#96183,
#96184,#96185,#96186,#96187,#96188,#96189,#96190,#96191,#96192,#96193,#96194,
#96195,#96196,#96197,#96198,#96199,#96200,#96201,#96202,#96203,#96204,#96205,
#96206,#96207,#96208,#96209,#96210,#96211,#96212,#96213,#96214,#96215,#96216,
#96217,#96218,#96219,#96220,#96221,#96222,#96223,#96224,#96225,#96226,#96227,
#96228,#96229,#96230,#96231,#96232,#96233,#96234,#96235,#96236,#96237,#96238,
#96239,#96240,#96241,#96242,#96243,#96244,#96245,#96246,#96247,#96248,#96249,
#96250,#96251,#96252,#96253,#96254,#96255,#96256,#96257,#96258,#96259,#96260,
#96261,#96262,#96263,#96264,#96265,#96266,#96267,#96268,#96269,#96270,#96271,
#96272,#96273,#96274,#96275,#96276,#96277,#96278,#96279,#96280,#96281,#96282,
#96283,#96284,#96285,#96286,#96287,#96288,#96289,#96290,#96291,#96292,#96293,
#96294,#96295,#96296,#96297,#96298,#96299,#96300,#96301,#96302,#96303,#96304,
#96305,#96306,#96307,#96308,#96309,#96310,#96311,#96312,#96313,#96314,#96315,
#96316,#96317,#96318,#96319,#96320,#96321,#96322,#96323,#96324,#96325,#96326,
#96327,#96328,#96329,#96330,#96331,#96332),.UNSPECIFIED.,.F.,.F.,(4,3,3,
3,3,3,3,3,3,3,3,3,3,3,3,3,3,3,3,3,3,3,3,3,3,3,3,3,3,3,3,3,3,3,3,3,3,3,3,
3,3,3,3,3,3,3,3,3,3,3,3,3,3,3,3,3,3,3,3,3,3,3,3,3,3,3,3,3,3,3,3,3,3,4),
(1083.84946548862,1083.93751883751,1084.02571203857,1084.11413629358,1084.20268552087,
1084.29144096095,1084.33216102179,1084.41589973364,1084.499535245,1084.5830876884,
1084.66657712425,1084.75003107487,1084.83346756871,1084.91690467847,1085.00036047339,
1085.08390496612,1085.16749404906,1085.25121731662,1085.33189703251,1085.41563574436,
1085.49927125572,1085.58282369912,1085.66631313497,1085.74976708559,1085.83320357943,
1085.91664068919,1086.0000964841,1086.08364097683,1086.16723005978,1086.25095332733,
1086.33163304323,1086.41537175508,1086.49900726644,1086.58255970984,1086.66604914569,
1086.74950309631,1086.83293959015,1086.91637669991,1086.99983249483,1087.08337698756,
1087.1669660705,1087.25068933805,1087.33136905395,1087.4151077658,1087.49874327716,
1087.58229572056,1087.66578515641,1087.74923910703,1087.83267560087,1087.91611271063,
1087.99956850555,1088.08311299828,1088.16670208122,1088.25042534878,1088.33110506467,
1088.41484377652,1088.49847928788,1088.58203173128,1088.66552116713,1088.74897511775,
1088.83241161159,1088.91584872135,1088.99930451627,1089.082849009,1089.16643809194,
1089.25016135949,1089.33084107539,1089.41335087959,1089.49576462505,1089.57810151412,
1089.66037876144,1089.74262053293,1089.82485991559,1089.88105454176),
 .UNSPECIFIED.);
#743=B_SPLINE_CURVE_WITH_KNOTS('',3,(#96338,#96339,#96340,#96341,#96342,
#96343,#96344,#96345,#96346,#96347,#96348,#96349,#96350,#96351,#96352,#96353,
#96354,#96355,#96356,#96357,#96358,#96359,#96360,#96361,#96362,#96363,#96364,
#96365,#96366,#96367,#96368,#96369,#96370,#96371,#96372,#96373,#96374,#96375,
#96376,#96377,#96378,#96379,#96380,#96381,#96382,#96383,#96384,#96385,#96386,
#96387,#96388,#96389,#96390,#96391,#96392,#96393,#96394,#96395,#96396,#96397,
#96398,#96399,#96400,#96401,#96402,#96403,#96404,#96405,#96406,#96407,#96408,
#96409,#96410,#96411,#96412,#96413,#96414,#96415,#96416,#96417,#96418,#96419,
#96420,#96421,#96422,#96423,#96424,#96425,#96426,#96427,#96428,#96429,#96430,
#96431,#96432,#96433,#96434,#96435,#96436,#96437,#96438,#96439,#96440,#96441,
#96442,#96443,#96444,#96445,#96446,#96447,#96448,#96449,#96450,#96451,#96452,
#96453,#96454,#96455,#96456,#96457,#96458,#96459,#96460,#96461,#96462,#96463,
#96464,#96465,#96466,#96467,#96468,#96469,#96470,#96471,#96472,#96473,#96474,
#96475,#96476,#96477,#96478,#96479,#96480,#96481,#96482,#96483,#96484,#96485,
#96486,#96487,#96488,#96489,#96490,#96491,#96492,#96493,#96494,#96495,#96496,
#96497,#96498,#96499,#96500,#96501,#96502,#96503,#96504,#96505,#96506,#96507,
#96508,#96509,#96510,#96511,#96512,#96513,#96514,#96515,#96516,#96517,#96518,
#96519,#96520,#96521,#96522,#96523,#96524,#96525,#96526,#96527,#96528,#96529,
#96530,#96531,#96532,#96533,#96534,#96535,#96536,#96537,#96538,#96539,#96540,
#96541,#96542,#96543,#96544,#96545,#96546,#96547,#96548,#96549,#96550,#96551,
#96552,#96553,#96554,#96555,#96556,#96557),.UNSPECIFIED.,.F.,.F.,(4,3,3,
3,3,3,3,3,3,3,3,3,3,3,3,3,3,3,3,3,3,3,3,3,3,3,3,3,3,3,3,3,3,3,3,3,3,3,3,
3,3,3,3,3,3,3,3,3,3,3,3,3,3,3,3,3,3,3,3,3,3,3,3,3,3,3,3,3,3,3,3,3,3,4),
(1090.13265079578,1090.21521388659,1090.29768668348,1090.38009027064,1090.46245102466,
1090.54479049315,1090.62712763065,1090.70948138743,1090.79191944263,1090.87440190344,
1090.95701069698,1091.02002247711,1091.10376118896,1091.18739670032,1091.27094914372,
1091.35443857957,1091.43789253019,1091.52132902403,1091.60476613379,1091.68822192871,
1091.77176642144,1091.85535550438,1091.93907877194,1092.01975848783,1092.10349719968,
1092.18713271104,1092.27068515444,1092.35417459029,1092.43762854091,1092.52106503476,
1092.60450214451,1092.68795793943,1092.77150243216,1092.8550915151,1092.93881478266,
1093.01949449855,1093.1032332104,1093.18686872176,1093.27042116516,1093.35391060101,
1093.43736455163,1093.52080104547,1093.60423815523,1093.68769395014,1093.77123844287,
1093.85482752581,1093.93855079337,1094.01923050927,1094.10296922112,1094.18660473248,
1094.27015717588,1094.35364661173,1094.43710056235,1094.52053705619,1094.60397416595,
1094.68742996087,1094.7709744536,1094.85456353654,1094.93828680409,1095.01896651999,
1095.10270523184,1095.1863407432,1095.2698931866,1095.35338262245,1095.43683657306,
1095.52027306691,1095.60371017666,1095.68716597158,1095.77071046431,1095.85429954725,
1095.93802281481,1096.01870253071,1096.1120278899,1096.16545634169),
 .UNSPECIFIED.);
#744=B_SPLINE_CURVE_WITH_KNOTS('',3,(#96558,#96559,#96560,#96561,#96562,
#96563,#96564,#96565,#96566,#96567),.UNSPECIFIED.,.F.,.F.,(4,3,3,4),(1089.8810452498,
1089.96477785809,1090.02028646639,1090.13265079564),.UNSPECIFIED.);
#745=B_SPLINE_CURVE_WITH_KNOTS('',3,(#96569,#96570,#96571,#96572,#96573,
#96574,#96575,#96576,#96577,#96578),.UNSPECIFIED.,.F.,.F.,(4,3,3,4),(1089.88105454176,
1089.96332894242,1090.04798986898,1090.13265079553),.UNSPECIFIED.);
#746=B_SPLINE_CURVE_WITH_KNOTS('',3,(#96579,#96580,#96581,#96582,#96583,
#96584,#96585,#96586,#96587,#96588,#96589,#96590,#96591,#96592,#96593,#96594,
#96595,#96596,#96597,#96598,#96599,#96600,#96601,#96602,#96603,#96604,#96605,
#96606,#96607,#96608,#96609,#96610,#96611,#96612,#96613,#96614,#96615,#96616,
#96617,#96618,#96619,#96620,#96621,#96622,#96623,#96624,#96625,#96626,#96627,
#96628,#96629,#96630,#96631,#96632,#96633,#96634,#96635,#96636,#96637,#96638,
#96639,#96640,#96641,#96642,#96643,#96644,#96645,#96646,#96647,#96648,#96649,
#96650,#96651,#96652,#96653,#96654,#96655,#96656,#96657,#96658,#96659,#96660,
#96661,#96662,#96663,#96664,#96665,#96666,#96667,#96668,#96669,#96670,#96671,
#96672,#96673,#96674,#96675,#96676,#96677,#96678,#96679,#96680,#96681,#96682,
#96683,#96684,#96685,#96686,#96687,#96688,#96689,#96690,#96691,#96692,#96693,
#96694,#96695,#96696,#96697,#96698,#96699,#96700,#96701,#96702,#96703,#96704,
#96705,#96706,#96707,#96708,#96709,#96710,#96711,#96712,#96713,#96714,#96715,
#96716,#96717,#96718,#96719,#96720,#96721,#96722,#96723,#96724,#96725,#96726,
#96727,#96728,#96729,#96730,#96731,#96732,#96733,#96734,#96735,#96736,#96737,
#96738,#96739,#96740,#96741,#96742,#96743,#96744,#96745,#96746,#96747,#96748,
#96749,#96750,#96751,#96752,#96753,#96754,#96755,#96756,#96757,#96758,#96759,
#96760,#96761,#96762,#96763,#96764,#96765,#96766,#96767,#96768,#96769,#96770,
#96771,#96772,#96773,#96774,#96775,#96776,#96777,#96778,#96779,#96780,#96781,
#96782,#96783,#96784,#96785,#96786,#96787,#96788,#96789,#96790,#96791,#96792,
#96793,#96794,#96795),.UNSPECIFIED.,.F.,.F.,(4,3,3,3,3,3,3,3,3,3,3,3,3,
3,3,3,3,3,3,3,3,3,3,3,3,3,3,3,3,3,3,3,3,3,3,3,3,3,3,3,3,3,3,3,3,3,3,3,3,
3,3,3,3,3,3,3,3,3,3,3,3,3,3,3,3,3,3,3,3,3,3,3,4),(1090.13265079564,1090.2534921149,
1090.33057708611,1090.41431579796,1090.49795130932,1090.58150375272,1090.66499318857,
1090.74844713919,1090.83188363303,1090.91532074279,1090.9987765377,1091.08232103043,
1091.16591011337,1091.24963338093,1091.33031309683,1091.41405180868,1091.49768732004,
1091.58123976344,1091.66472919929,1091.74818314991,1091.83161964375,1091.91505675351,
1091.99851254843,1092.08205704116,1092.1656461241,1092.24936939165,1092.33004910755,
1092.4137878194,1092.49742333076,1092.58097577416,1092.66446521001,1092.74791916063,
1092.83135565447,1092.91479276423,1092.99824855915,1093.08179305188,1093.16538213482,
1093.24910540237,1093.32978511827,1093.41352383012,1093.49715934148,1093.58071178488,
1093.66420122073,1093.74765517135,1093.83109166519,1093.91452877495,1093.99798456987,
1094.0815290626,1094.16511814554,1094.24884141309,1094.32952112899,1094.41325984084,
1094.4968953522,1094.5804477956,1094.66393723145,1094.74739118207,1094.83082767591,
1094.91426478567,1094.99772058059,1095.08126507332,1095.16485415626,1095.24857742381,
1095.32925713971,1095.41300568622,1095.49664885821,1095.58019197483,1095.66367834858,
1095.74712609854,1095.83055331403,1095.91400811951,1095.99747382294,1096.08101904038,
1096.16419435723),.UNSPECIFIED.);
#747=B_SPLINE_CURVE_WITH_KNOTS('',3,(#96801,#96802,#96803,#96804,#96805,
#96806,#96807,#96808,#96809,#96810,#96811,#96812,#96813,#96814,#96815,#96816,
#96817,#96818,#96819,#96820,#96821,#96822,#96823,#96824,#96825,#96826,#96827,
#96828,#96829,#96830,#96831,#96832,#96833,#96834,#96835,#96836,#96837,#96838,
#96839,#96840,#96841,#96842,#96843,#96844,#96845,#96846,#96847,#96848,#96849,
#96850,#96851,#96852,#96853,#96854,#96855,#96856,#96857,#96858,#96859,#96860,
#96861,#96862,#96863,#96864,#96865,#96866,#96867,#96868,#96869,#96870,#96871,
#96872,#96873,#96874,#96875,#96876,#96877,#96878,#96879,#96880,#96881,#96882,
#96883,#96884,#96885,#96886,#96887,#96888,#96889,#96890,#96891,#96892,#96893,
#96894,#96895,#96896,#96897,#96898,#96899,#96900,#96901,#96902,#96903,#96904,
#96905,#96906,#96907,#96908,#96909,#96910,#96911,#96912,#96913,#96914,#96915,
#96916,#96917,#96918,#96919,#96920,#96921,#96922,#96923,#96924,#96925,#96926,
#96927,#96928,#96929,#96930,#96931,#96932,#96933,#96934,#96935,#96936,#96937,
#96938,#96939,#96940,#96941,#96942,#96943,#96944,#96945,#96946,#96947,#96948,
#96949,#96950,#96951,#96952,#96953,#96954,#96955,#96956,#96957,#96958,#96959,
#96960,#96961,#96962,#96963,#96964,#96965,#96966,#96967,#96968,#96969,#96970,
#96971,#96972,#96973,#96974,#96975,#96976,#96977,#96978,#96979,#96980,#96981,
#96982,#96983,#96984,#96985,#96986,#96987,#96988,#96989,#96990,#96991,#96992,
#96993,#96994,#96995,#96996,#96997,#96998,#96999,#97000,#97001,#97002,#97003,
#97004,#97005,#97006,#97007,#97008,#97009,#97010,#97011,#97012,#97013,#97014,
#97015,#97016,#97017,#97018,#97019,#97020),.UNSPECIFIED.,.F.,.F.,(4,3,3,
3,3,3,3,3,3,3,3,3,3,3,3,3,3,3,3,3,3,3,3,3,3,3,3,3,3,3,3,3,3,3,3,3,3,3,3,
3,3,3,3,3,3,3,3,3,3,3,3,3,3,3,3,3,3,3,3,3,3,3,3,3,3,3,3,3,3,3,3,3,3,4),
(1096.41583610282,1096.50034027643,1096.58486491856,1096.66942649939,1096.7566795099,
1096.84141644417,1096.9299274928,1097.01843854143,1097.10217725328,1097.18581276465,
1097.26936520804,1097.3528546439,1097.43630859451,1097.51974508836,1097.60318219812,
1097.68663799303,1097.77018248577,1097.85377156871,1097.93749483627,1098.01817455215,
1098.101913264,1098.18554877536,1098.26910121876,1098.35259065461,1098.43604460523,
1098.51948109908,1098.60291820883,1098.68637400375,1098.76991849648,1098.85350757942,
1098.93723084698,1099.01791056287,1099.10164927472,1099.18528478608,1099.26883722948,
1099.35232666533,1099.43578061594,1099.51921710979,1099.60265421955,1099.68611001446,
1099.76965450719,1099.85324359013,1099.93696685769,1100.01764657359,1100.10138528544,
1100.1850207968,1100.2685732402,1100.35206267605,1100.43551662667,1100.51895312051,
1100.60239023027,1100.68584602519,1100.76939051792,1100.85297960086,1100.93670286842,
1101.01738258431,1101.10112129616,1101.18475680752,1101.26830925092,1101.35179868677,
1101.43525263738,1101.51868913123,1101.60212624098,1101.6855820359,1101.76912652863,
1101.85271561157,1101.93643887913,1102.01711859503,1102.10060281453,1102.18745385174,
1102.27072884502,1102.35394542984,1102.43711668659,1102.44800696337),
 .UNSPECIFIED.);
#748=B_SPLINE_CURVE_WITH_KNOTS('',3,(#97021,#97022,#97023,#97024,#97025,
#97026,#97027,#97028,#97029,#97030),.UNSPECIFIED.,.F.,.F.,(4,3,3,4),(1096.16545634169,
1096.25829681984,1096.35068769254,1096.41583610264),.UNSPECIFIED.);
#749=B_SPLINE_CURVE_WITH_KNOTS('',3,(#97032,#97033,#97034,#97035,#97036,
#97037,#97038,#97039,#97040,#97041),.UNSPECIFIED.,.F.,.F.,(4,3,3,4),(1096.16419435723,
1096.24791749231,1096.32899315043,1096.41583610282),.UNSPECIFIED.);
#750=B_SPLINE_CURVE_WITH_KNOTS('',3,(#97042,#97043,#97044,#97045,#97046,
#97047,#97048,#97049,#97050,#97051,#97052,#97053,#97054,#97055,#97056,#97057,
#97058,#97059,#97060,#97061,#97062,#97063,#97064,#97065,#97066,#97067,#97068,
#97069,#97070,#97071,#97072,#97073,#97074,#97075,#97076,#97077,#97078,#97079,
#97080,#97081,#97082,#97083,#97084,#97085,#97086,#97087,#97088,#97089,#97090,
#97091,#97092,#97093,#97094,#97095,#97096,#97097,#97098,#97099,#97100,#97101,
#97102,#97103,#97104,#97105,#97106,#97107,#97108,#97109,#97110,#97111,#97112,
#97113,#97114,#97115,#97116,#97117,#97118,#97119,#97120,#97121,#97122,#97123,
#97124,#97125,#97126,#97127,#97128,#97129,#97130,#97131,#97132,#97133,#97134,
#97135,#97136,#97137,#97138,#97139,#97140,#97141,#97142,#97143,#97144,#97145,
#97146,#97147,#97148,#97149,#97150,#97151,#97152,#97153,#97154,#97155,#97156,
#97157,#97158,#97159,#97160,#97161,#97162,#97163,#97164,#97165,#97166,#97167,
#97168,#97169,#97170,#97171,#97172,#97173,#97174,#97175,#97176,#97177,#97178,
#97179,#97180,#97181,#97182,#97183,#97184,#97185,#97186,#97187,#97188,#97189,
#97190,#97191,#97192,#97193,#97194,#97195,#97196,#97197,#97198,#97199,#97200,
#97201,#97202,#97203,#97204,#97205,#97206,#97207,#97208,#97209,#97210,#97211,
#97212,#97213,#97214,#97215,#97216,#97217,#97218,#97219,#97220,#97221,#97222,
#97223,#97224,#97225,#97226,#97227,#97228,#97229,#97230,#97231,#97232,#97233,
#97234,#97235,#97236,#97237,#97238,#97239,#97240,#97241,#97242,#97243,#97244,
#97245,#97246,#97247,#97248,#97249,#97250,#97251,#97252,#97253,#97254,#97255,
#97256,#97257,#97258,#97259,#97260,#97261),.UNSPECIFIED.,.F.,.F.,(4,3,3,
3,3,3,3,3,3,3,3,3,3,3,3,3,3,3,3,3,3,3,3,3,3,3,3,3,3,3,3,3,3,3,3,3,3,3,3,
3,3,3,3,3,3,3,3,3,3,3,3,3,3,3,3,3,3,3,3,3,3,3,3,3,3,3,3,3,3,3,3,3,3,4),
(1096.41583610295,1096.49857317387,1096.58121533194,1096.66378356627,1096.74690176563,
1096.82939491726,1096.91188134348,1096.99437989575,1097.0779672121,1097.16058900046,
1097.2446590808,1097.32872916115,1097.412467873,1097.49610338436,1097.57965582776,
1097.66314526361,1097.74659921423,1097.83003570807,1097.91347281783,1097.99692861274,
1098.08047310547,1098.16406218841,1098.24778545597,1098.32846517187,1098.41220388372,
1098.49583939508,1098.57939183848,1098.66288127433,1098.74633522495,1098.82977171879,
1098.91320882855,1098.99666462346,1099.08020911619,1099.16379819913,1099.24752146669,
1099.32820118259,1099.41193989444,1099.4955754058,1099.5791278492,1099.66261728505,
1099.74607123567,1099.82950772951,1099.91294483927,1099.99640063419,1100.07994512692,
1100.16353420986,1100.24725747742,1100.32793719331,1100.41167590516,1100.49531141652,
1100.57886385992,1100.66235329577,1100.74580724639,1100.82924374023,1100.91268084999,
1100.99613664491,1101.07968113763,1101.16327022058,1101.24699348813,1101.32767320403,
1101.41141191588,1101.49504742724,1101.57859987064,1101.66208930649,1101.74554325711,
1101.82897975095,1101.91241686071,1101.99587265563,1102.07941714836,1102.1630062313,
1102.24672949886,1102.32740921475,1102.4226128327,1102.4485678876),
 .UNSPECIFIED.);
#751=B_SPLINE_CURVE_WITH_KNOTS('',3,(#97267,#97268,#97269,#97270,#97271,
#97272,#97273,#97274,#97275,#97276,#97277,#97278,#97279,#97280,#97281,#97282,
#97283,#97284,#97285,#97286,#97287,#97288,#97289,#97290,#97291,#97292,#97293,
#97294,#97295,#97296,#97297,#97298,#97299,#97300,#97301,#97302,#97303,#97304,
#97305,#97306,#97307,#97308,#97309,#97310,#97311,#97312,#97313,#97314,#97315,
#97316,#97317,#97318,#97319,#97320,#97321,#97322,#97323,#97324,#97325,#97326,
#97327,#97328,#97329,#97330,#97331,#97332,#97333,#97334,#97335,#97336,#97337,
#97338,#97339,#97340,#97341,#97342,#97343,#97344,#97345,#97346,#97347,#97348,
#97349,#97350,#97351,#97352,#97353,#97354,#97355,#97356,#97357,#97358,#97359,
#97360,#97361,#97362,#97363,#97364,#97365,#97366,#97367,#97368,#97369,#97370,
#97371,#97372,#97373,#97374,#97375,#97376,#97377,#97378,#97379,#97380,#97381,
#97382,#97383,#97384,#97385,#97386,#97387,#97388,#97389,#97390,#97391,#97392,
#97393,#97394,#97395,#97396,#97397,#97398,#97399,#97400,#97401,#97402,#97403,
#97404,#97405,#97406,#97407,#97408,#97409,#97410,#97411,#97412,#97413,#97414,
#97415,#97416,#97417,#97418,#97419,#97420,#97421,#97422,#97423,#97424,#97425,
#97426,#97427,#97428,#97429,#97430,#97431,#97432,#97433,#97434,#97435,#97436,
#97437,#97438,#97439,#97440,#97441,#97442,#97443,#97444,#97445,#97446,#97447,
#97448,#97449,#97450,#97451,#97452,#97453,#97454,#97455,#97456,#97457,#97458,
#97459,#97460,#97461,#97462,#97463,#97464,#97465,#97466,#97467,#97468,#97469,
#97470,#97471,#97472,#97473,#97474,#97475,#97476,#97477,#97478,#97479,#97480,
#97481,#97482,#97483,#97484,#97485,#97486),.UNSPECIFIED.,.F.,.F.,(4,3,3,
3,3,3,3,3,3,3,3,3,3,3,3,3,3,3,3,3,3,3,3,3,3,3,3,3,3,3,3,3,3,3,3,3,3,3,3,
3,3,3,3,3,3,3,3,3,3,3,3,3,3,3,3,3,3,3,3,3,3,3,3,3,3,3,3,3,3,3,3,3,3,4),
(1102.69902141017,1102.79771148504,1102.89710050959,1102.99725101716,1103.01685460575,
1103.1005933176,1103.18422882897,1103.26778127237,1103.35127070823,1103.43472465885,
1103.5181611527,1103.60159826246,1103.68505405738,1103.76859855011,1103.85218763306,
1103.93591090062,1104.01659061647,1104.10032932832,1104.18396483968,1104.26751728308,
1104.35100671893,1104.43446066955,1104.51789716339,1104.60133427315,1104.68479006807,
1104.7683345608,1104.85192364374,1104.93564691129,1105.01632662719,1105.10006533904,
1105.1837008504,1105.2672532938,1105.35074272965,1105.43419668026,1105.51763317411,
1105.60107028386,1105.68452607878,1105.76807057151,1105.85165965445,1105.93538292201,
1106.01606263791,1106.09980134976,1106.18343686112,1106.26698930452,1106.35047874037,
1106.43393269099,1106.51736918484,1106.60080629459,1106.68426208951,1106.76780658224,
1106.85139566518,1106.93511893274,1107.01579864863,1107.09953736047,1107.18317287184,
1107.26672531524,1107.35021475109,1107.4336687017,1107.51710519555,1107.6005423053,
1107.68399810022,1107.76754259295,1107.85113167589,1107.93485494345,1108.01553465935,
1108.09883872996,1108.18201114958,1108.2651075606,1108.34814653257,1108.43114658976,
1108.5141422714,1108.59713406137,1108.68016880708,1108.73043941245),
 .UNSPECIFIED.);
#752=B_SPLINE_CURVE_WITH_KNOTS('',3,(#97487,#97488,#97489,#97490,#97491,
#97492,#97493,#97494,#97495,#97496),.UNSPECIFIED.,.F.,.F.,(4,3,3,4),(1102.44800696337,
1102.53116145307,1102.61509143154,1102.69902141),.UNSPECIFIED.);
#753=B_SPLINE_CURVE_WITH_KNOTS('',3,(#97498,#97499,#97500,#97501,#97502,
#97503,#97504,#97505,#97506,#97507),.UNSPECIFIED.,.F.,.F.,(4,3,3,4),(1102.4485678876,
1102.54324273876,1102.63733940364,1102.6990214098),.UNSPECIFIED.);
#754=B_SPLINE_CURVE_WITH_KNOTS('',3,(#97508,#97509,#97510,#97511,#97512,
#97513,#97514,#97515,#97516,#97517,#97518,#97519,#97520,#97521,#97522,#97523,
#97524,#97525,#97526,#97527,#97528,#97529,#97530,#97531,#97532,#97533,#97534,
#97535,#97536,#97537,#97538,#97539,#97540,#97541,#97542,#97543,#97544,#97545,
#97546,#97547,#97548,#97549,#97550,#97551,#97552,#97553,#97554,#97555,#97556,
#97557,#97558,#97559,#97560,#97561,#97562,#97563,#97564,#97565,#97566,#97567,
#97568,#97569,#97570,#97571,#97572,#97573,#97574,#97575,#97576,#97577,#97578,
#97579,#97580,#97581,#97582,#97583,#97584,#97585,#97586,#97587,#97588,#97589,
#97590,#97591,#97592,#97593,#97594,#97595,#97596,#97597,#97598,#97599,#97600,
#97601,#97602,#97603,#97604,#97605,#97606,#97607,#97608,#97609,#97610,#97611,
#97612,#97613,#97614,#97615,#97616,#97617,#97618,#97619,#97620,#97621,#97622,
#97623,#97624,#97625,#97626,#97627,#97628,#97629,#97630,#97631,#97632,#97633,
#97634,#97635,#97636,#97637,#97638,#97639,#97640,#97641,#97642,#97643,#97644,
#97645,#97646,#97647,#97648,#97649,#97650,#97651,#97652,#97653,#97654,#97655,
#97656,#97657,#97658,#97659,#97660,#97661,#97662,#97663,#97664,#97665,#97666,
#97667,#97668,#97669,#97670,#97671,#97672,#97673,#97674,#97675,#97676,#97677,
#97678,#97679,#97680,#97681,#97682,#97683,#97684,#97685,#97686,#97687,#97688,
#97689,#97690,#97691,#97692,#97693,#97694,#97695,#97696,#97697,#97698,#97699,
#97700,#97701,#97702,#97703,#97704,#97705,#97706,#97707,#97708,#97709,#97710,
#97711,#97712,#97713,#97714,#97715,#97716,#97717,#97718,#97719,#97720,#97721,
#97722,#97723,#97724,#97725,#97726,#97727),.UNSPECIFIED.,.F.,.F.,(4,3,3,
3,3,3,3,3,3,3,3,3,3,3,3,3,3,3,3,3,3,3,3,3,3,3,3,3,3,3,3,3,3,3,3,3,3,3,3,
3,3,3,3,3,3,3,3,3,3,3,3,3,3,3,3,3,3,3,3,3,3,3,3,3,3,3,3,3,3,3,3,3,3,4),
(1102.69902141,1102.78302386211,1102.86703181426,1102.9510625347,1103.03513330275,
1103.11931332698,1103.20355529402,1103.28793168718,1103.32714522547,1103.41088393732,
1103.49451944868,1103.57807189208,1103.66156132793,1103.74501527855,1103.82845177239,
1103.91188888215,1103.99534467707,1104.0788891698,1104.16247825274,1104.24620152029,
1104.32688123619,1104.41061994804,1104.4942554594,1104.5778079028,1104.66129733865,
1104.74475128927,1104.82818778311,1104.91162489287,1104.99508068779,1105.07862518051,
1105.16221426346,1105.24593753101,1105.32661724691,1105.41035595876,1105.49399147012,
1105.57754391352,1105.66103334937,1105.74448729999,1105.82792379383,1105.91136090359,
1105.99481669851,1106.07836119124,1106.16195027418,1106.24567354173,1106.32635325763,
1106.41009196948,1106.49372748084,1106.57727992424,1106.66076936009,1106.74422331071,
1106.82765980455,1106.91109691431,1106.99455270923,1107.07809720196,1107.1616862849,
1107.24540955245,1107.32608926835,1107.4098279802,1107.49346349156,1107.57701593496,
1107.66050537081,1107.74395932143,1107.82739581527,1107.91083292503,1107.99428871995,
1108.07783321268,1108.16142229562,1108.24514556317,1108.32582527907,1108.40970043406,
1108.49343947228,1108.57710021367,1108.66069007077,1108.73132332231),
 .UNSPECIFIED.);
#755=B_SPLINE_CURVE_WITH_KNOTS('',3,(#97733,#97734,#97735,#97736,#97737,
#97738,#97739,#97740,#97741,#97742,#97743,#97744,#97745,#97746,#97747,#97748,
#97749,#97750,#97751,#97752,#97753,#97754,#97755,#97756,#97757,#97758,#97759,
#97760,#97761,#97762,#97763,#97764,#97765,#97766,#97767,#97768,#97769,#97770,
#97771,#97772,#97773,#97774,#97775,#97776,#97777,#97778,#97779,#97780,#97781,
#97782,#97783,#97784,#97785,#97786,#97787,#97788,#97789,#97790,#97791,#97792,
#97793,#97794,#97795,#97796,#97797,#97798,#97799,#97800,#97801,#97802,#97803,
#97804,#97805,#97806,#97807,#97808,#97809,#97810,#97811,#97812,#97813,#97814,
#97815,#97816,#97817,#97818,#97819,#97820,#97821,#97822,#97823,#97824,#97825,
#97826,#97827,#97828,#97829,#97830,#97831,#97832,#97833,#97834,#97835,#97836,
#97837,#97838,#97839,#97840,#97841,#97842,#97843,#97844,#97845,#97846,#97847,
#97848,#97849,#97850,#97851,#97852,#97853,#97854,#97855,#97856,#97857,#97858,
#97859,#97860,#97861,#97862,#97863,#97864,#97865,#97866,#97867,#97868,#97869,
#97870,#97871,#97872,#97873,#97874,#97875,#97876,#97877,#97878,#97879,#97880,
#97881,#97882,#97883,#97884,#97885,#97886,#97887,#97888,#97889,#97890,#97891,
#97892,#97893,#97894,#97895,#97896,#97897,#97898,#97899,#97900,#97901,#97902,
#97903,#97904,#97905,#97906,#97907,#97908,#97909,#97910,#97911,#97912,#97913,
#97914,#97915,#97916,#97917,#97918,#97919,#97920,#97921,#97922,#97923,#97924,
#97925,#97926,#97927,#97928,#97929,#97930,#97931,#97932,#97933,#97934,#97935,
#97936,#97937,#97938,#97939,#97940,#97941,#97942,#97943,#97944,#97945,#97946,
#97947,#97948,#97949,#97950,#97951,#97952,#97953,#97954,#97955),
 .UNSPECIFIED.,.F.,.F.,(4,3,3,3,3,3,3,3,3,3,3,3,3,3,3,3,3,3,3,3,3,3,3,3,
3,3,3,3,3,3,3,3,3,3,3,3,3,3,3,3,3,3,3,3,3,3,3,3,3,3,3,3,3,3,3,3,3,3,3,3,
3,3,3,3,3,3,3,3,3,3,3,3,3,3,4),(1108.98220671718,1109.01527067007,1109.09900938192,
1109.18264489328,1109.26619733668,1109.34968677253,1109.43314072315,1109.51657721699,
1109.60001432675,1109.68347012166,1109.76701461439,1109.85060369733,1109.93432696489,
1110.01500668079,1110.09874539264,1110.18238090401,1110.26593334741,1110.34942278327,
1110.43287673388,1110.51631322773,1110.59975033749,1110.68320613241,1110.76675062514,
1110.85033970809,1110.93406297565,1111.01474269152,1111.09848140336,1111.18211691473,
1111.26566935812,1111.34915879397,1111.43261274458,1111.51604923843,1111.59948634818,
1111.6829421431,1111.76648663582,1111.85007571876,1111.93379898632,1112.01447870223,
1112.09821741408,1112.18185292544,1112.26540536884,1112.34889480469,1112.43234875531,
1112.51578524916,1112.59922235891,1112.68267815383,1112.76622264656,1112.8498117295,
1112.93353499706,1113.01421471296,1113.09795342481,1113.18158893618,1113.26514137958,
1113.34863081543,1113.43208476605,1113.51552125989,1113.59895836965,1113.68241416457,
1113.7659586573,1113.84954774025,1113.93327100781,1114.01395072368,1114.09768943552,
1114.18132494689,1114.26487739029,1114.34836682614,1114.43182077675,1114.5152572706,
1114.59869438035,1114.68215017527,1114.76569466799,1114.84928375093,1114.93300701849,
1115.0136867344,1115.01433071751),.UNSPECIFIED.);
#756=B_SPLINE_CURVE_WITH_KNOTS('',3,(#97956,#97957,#97958,#97959,#97960,
#97961,#97962,#97963,#97964,#97965),.UNSPECIFIED.,.F.,.F.,(4,3,3,4),(1108.73043941245,
1108.81357021083,1108.89788846393,1108.98220671704),.UNSPECIFIED.);
#757=B_SPLINE_CURVE_WITH_KNOTS('',3,(#97967,#97968,#97969,#97970,#97971,
#97972,#97973,#97974,#97975,#97976),.UNSPECIFIED.,.F.,.F.,(4,3,3,4),(1108.73132332231,
1108.8148472524,1108.89852698479,1108.98220671718),.UNSPECIFIED.);
#758=B_SPLINE_CURVE_WITH_KNOTS('',3,(#97977,#97978,#97979,#97980,#97981,
#97982,#97983,#97984,#97985,#97986),.UNSPECIFIED.,.F.,.F.,(4,1,1,1,1,1,
1,4),(1108.98221426278,1109.32556128979,1110.32529730051,1111.32503331123,
1112.32476932195,1113.32450533267,1114.32424134339,1115.01349131436),
 .UNSPECIFIED.);
#759=B_SPLINE_CURVE_WITH_KNOTS('',3,(#97992,#97993,#97994,#97995,#97996,
#97997,#97998,#97999,#98000,#98001,#98002,#98003,#98004,#98005,#98006,#98007,
#98008,#98009,#98010,#98011,#98012,#98013,#98014,#98015,#98016,#98017,#98018,
#98019,#98020,#98021,#98022,#98023,#98024,#98025,#98026,#98027,#98028,#98029,
#98030,#98031,#98032,#98033,#98034,#98035,#98036,#98037,#98038,#98039,#98040,
#98041,#98042,#98043,#98044,#98045,#98046,#98047,#98048,#98049,#98050,#98051,
#98052,#98053,#98054,#98055,#98056,#98057,#98058,#98059,#98060,#98061,#98062,
#98063,#98064,#98065,#98066,#98067,#98068,#98069,#98070,#98071,#98072,#98073,
#98074,#98075,#98076,#98077,#98078,#98079,#98080,#98081,#98082,#98083,#98084,
#98085,#98086,#98087,#98088,#98089,#98090,#98091,#98092,#98093,#98094,#98095,
#98096,#98097,#98098,#98099,#98100,#98101,#98102,#98103,#98104,#98105,#98106,
#98107,#98108,#98109,#98110,#98111,#98112,#98113,#98114,#98115,#98116,#98117,
#98118,#98119,#98120,#98121,#98122,#98123,#98124,#98125,#98126,#98127,#98128,
#98129,#98130,#98131,#98132,#98133,#98134,#98135,#98136,#98137,#98138,#98139,
#98140,#98141,#98142,#98143,#98144,#98145,#98146,#98147,#98148,#98149,#98150,
#98151,#98152,#98153,#98154,#98155,#98156,#98157,#98158,#98159,#98160,#98161,
#98162,#98163,#98164,#98165,#98166,#98167,#98168,#98169,#98170,#98171,#98172,
#98173,#98174,#98175,#98176,#98177,#98178,#98179,#98180,#98181,#98182,#98183,
#98184,#98185,#98186,#98187,#98188,#98189,#98190,#98191,#98192,#98193,#98194,
#98195,#98196,#98197,#98198,#98199,#98200,#98201,#98202,#98203,#98204,#98205,
#98206,#98207,#98208,#98209,#98210,#98211),.UNSPECIFIED.,.F.,.F.,(4,3,3,
3,3,3,3,3,3,3,3,3,3,3,3,3,3,3,3,3,3,3,3,3,3,3,3,3,3,3,3,3,3,3,3,3,3,3,3,
3,3,3,3,3,3,3,3,3,3,3,3,3,3,3,3,3,3,3,3,3,3,3,3,3,3,3,3,3,3,3,3,3,3,4),
(1115.26539202436,1115.3479645808,1115.43114685134,1115.51364560196,1115.59613810739,
1115.6786432089,1115.76233809295,1115.8449676835,1115.92919521431,1116.01342274512,
1116.09716145697,1116.18079696833,1116.26434941173,1116.34783884758,1116.4312927982,
1116.51472929204,1116.5981664018,1116.68162219672,1116.76516668945,1116.84875577239,
1116.93247903994,1117.01315875584,1117.09689746769,1117.18053297905,1117.26408542245,
1117.3475748583,1117.43102880892,1117.51446530276,1117.59790241252,1117.68135820744,
1117.76490270017,1117.84849178311,1117.93221505066,1118.01289476656,1118.09663347841,
1118.18026898977,1118.26382143317,1118.34731086902,1118.43076481964,1118.51420131348,
1118.59763842324,1118.68109421816,1118.76463871089,1118.84822779383,1118.93195106138,
1119.01263077728,1119.09636948913,1119.18000500049,1119.26355744389,1119.34704687974,
1119.43050083036,1119.5139373242,1119.59737443396,1119.68083022888,1119.76437472161,
1119.84796380455,1119.9316870721,1120.012366788,1120.09610549985,1120.17974101121,
1120.26329345461,1120.34678289046,1120.43023684108,1120.51367333492,1120.59711044468,
1120.6805662396,1120.76411073233,1120.84769981527,1120.93142308282,1121.01210279872,
1121.09883484553,1121.18544801319,1121.27192043186,1121.29817665327),
 .UNSPECIFIED.);
#760=B_SPLINE_CURVE_WITH_KNOTS('',3,(#98212,#98213,#98214,#98215,#98216,
#98217,#98218,#98219,#98220,#98221),.UNSPECIFIED.,.F.,.F.,(4,3,3,4),(1115.01433071751,
1115.12380950414,1115.23095866677,1115.26539202417),.UNSPECIFIED.);
#761=B_SPLINE_CURVE_WITH_KNOTS('',3,(#98223,#98224,#98225,#98226),
 .UNSPECIFIED.,.F.,.F.,(4,4),(1115.01349131436,1115.26538483617),
 .UNSPECIFIED.);
#762=B_SPLINE_CURVE_WITH_KNOTS('',3,(#98227,#98228,#98229,#98230,#98231,
#98232,#98233,#98234,#98235,#98236,#98237,#98238,#98239,#98240,#98241,#98242,
#98243,#98244,#98245,#98246,#98247,#98248,#98249,#98250,#98251,#98252,#98253,
#98254,#98255,#98256,#98257,#98258,#98259,#98260,#98261,#98262,#98263,#98264,
#98265,#98266,#98267,#98268,#98269,#98270,#98271,#98272,#98273,#98274,#98275,
#98276,#98277,#98278,#98279,#98280,#98281,#98282,#98283,#98284,#98285,#98286,
#98287,#98288,#98289,#98290,#98291,#98292,#98293,#98294,#98295,#98296,#98297,
#98298,#98299,#98300,#98301,#98302,#98303,#98304,#98305,#98306,#98307,#98308,
#98309,#98310,#98311,#98312,#98313,#98314,#98315,#98316,#98317,#98318,#98319,
#98320,#98321,#98322,#98323,#98324,#98325,#98326,#98327,#98328,#98329,#98330,
#98331,#98332,#98333,#98334,#98335,#98336,#98337,#98338,#98339,#98340,#98341,
#98342,#98343,#98344,#98345,#98346,#98347,#98348,#98349,#98350,#98351,#98352,
#98353,#98354,#98355,#98356,#98357,#98358,#98359,#98360,#98361,#98362,#98363,
#98364,#98365,#98366,#98367,#98368,#98369,#98370,#98371,#98372,#98373,#98374,
#98375,#98376,#98377,#98378,#98379,#98380,#98381,#98382,#98383,#98384,#98385,
#98386,#98387,#98388,#98389,#98390,#98391,#98392,#98393,#98394,#98395,#98396,
#98397,#98398,#98399,#98400,#98401,#98402,#98403,#98404,#98405,#98406,#98407,
#98408,#98409,#98410,#98411,#98412,#98413,#98414,#98415,#98416,#98417,#98418,
#98419,#98420,#98421,#98422,#98423,#98424,#98425,#98426,#98427,#98428,#98429,
#98430,#98431,#98432,#98433,#98434,#98435,#98436,#98437,#98438,#98439,#98440,
#98441,#98442,#98443,#98444,#98445,#98446),.UNSPECIFIED.,.F.,.F.,(4,3,3,
3,3,3,3,3,3,3,3,3,3,3,3,3,3,3,3,3,3,3,3,3,3,3,3,3,3,3,3,3,3,3,3,3,3,3,3,
3,3,3,3,3,3,3,3,3,3,3,3,3,3,3,3,3,3,3,3,3,3,3,3,3,3,3,3,3,3,3,3,3,3,4),
(1115.26539202436,1115.32397735411,1115.40771606596,1115.49135157732,1115.57490402072,
1115.65839345657,1115.74184740719,1115.82528390103,1115.90872101079,1115.99217680571,
1116.07572129843,1116.15931038138,1116.24303364893,1116.32371336483,1116.40745207668,
1116.49108758804,1116.57464003144,1116.65812946729,1116.74158341791,1116.82501991175,
1116.90845702151,1116.99191281643,1117.07545730916,1117.1590463921,1117.24276965966,
1117.32344937555,1117.4071880874,1117.49082359876,1117.57437604216,1117.65786547801,
1117.74131942863,1117.82475592247,1117.90819303223,1117.99164882715,1118.07519331987,
1118.15878240282,1118.24250567037,1118.32318538627,1118.40692409812,1118.49055960948,
1118.57411205288,1118.65760148873,1118.74105543935,1118.82449193319,1118.90792904295,
1118.99138483787,1119.0749293306,1119.15851841354,1119.24224168109,1119.32292139699,
1119.40666010884,1119.4902956202,1119.5738480636,1119.65733749945,1119.74079145007,
1119.82422794391,1119.90766505367,1119.99112084859,1120.07466534132,1120.15825442426,
1120.24197769181,1120.32265740771,1120.40639753497,1120.49003413167,1120.57358733172,
1120.65707719659,1120.74052989164,1120.82396466327,1120.90739958385,1120.99085272192,
1121.07438811408,1121.15796790361,1121.24166679885,1121.2973671878),
 .UNSPECIFIED.);
#763=B_SPLINE_CURVE_WITH_KNOTS('',3,(#98452,#98453,#98454,#98455,#98456,
#98457,#98458,#98459,#98460,#98461,#98462,#98463,#98464,#98465,#98466,#98467,
#98468,#98469,#98470,#98471,#98472,#98473,#98474,#98475,#98476,#98477,#98478,
#98479,#98480,#98481,#98482,#98483,#98484,#98485,#98486,#98487,#98488,#98489,
#98490,#98491,#98492,#98493,#98494,#98495,#98496,#98497,#98498,#98499,#98500,
#98501,#98502,#98503,#98504,#98505,#98506,#98507,#98508,#98509,#98510,#98511,
#98512,#98513,#98514,#98515,#98516,#98517,#98518,#98519,#98520,#98521,#98522,
#98523,#98524,#98525,#98526,#98527,#98528,#98529,#98530,#98531,#98532,#98533,
#98534,#98535,#98536,#98537,#98538,#98539,#98540,#98541,#98542,#98543,#98544,
#98545,#98546,#98547,#98548,#98549,#98550,#98551,#98552,#98553,#98554,#98555,
#98556,#98557,#98558,#98559,#98560,#98561,#98562,#98563,#98564,#98565,#98566,
#98567,#98568,#98569,#98570,#98571,#98572,#98573,#98574,#98575,#98576,#98577,
#98578,#98579,#98580,#98581,#98582,#98583,#98584,#98585,#98586,#98587,#98588,
#98589,#98590,#98591,#98592,#98593,#98594,#98595,#98596,#98597,#98598,#98599,
#98600,#98601,#98602,#98603,#98604,#98605,#98606,#98607,#98608,#98609,#98610,
#98611,#98612,#98613,#98614,#98615,#98616,#98617,#98618,#98619,#98620,#98621,
#98622,#98623,#98624,#98625,#98626,#98627,#98628,#98629,#98630,#98631,#98632,
#98633,#98634,#98635,#98636,#98637,#98638,#98639,#98640,#98641,#98642,#98643,
#98644,#98645,#98646,#98647,#98648,#98649,#98650,#98651,#98652,#98653,#98654,
#98655,#98656,#98657,#98658,#98659,#98660,#98661,#98662,#98663,#98664,#98665,
#98666,#98667,#98668,#98669,#98670,#98671),.UNSPECIFIED.,.F.,.F.,(4,3,3,
3,3,3,3,3,3,3,3,3,3,3,3,3,3,3,3,3,3,3,3,3,3,3,3,3,3,3,3,3,3,3,3,3,3,3,3,
3,3,3,3,3,3,3,3,3,3,3,3,3,3,3,3,3,3,3,3,3,3,3,3,3,3,3,3,3,3,3,3,3,3,4),
(1121.5485773317,1121.63743490442,1121.73103588068,1121.82033663901,1121.90978283507,
1121.99943881037,1122.01183880944,1122.09557752129,1122.17921303265,1122.26276547605,
1122.3462549119,1122.42970886252,1122.51314535636,1122.59658246612,1122.68003826104,
1122.76358275377,1122.84717183671,1122.93089510426,1123.01157482016,1123.09531353201,
1123.17894904337,1123.26250148677,1123.34599092262,1123.42944487324,1123.51288136708,
1123.59631847684,1123.67977427176,1123.76331876449,1123.84690784743,1123.93063111498,
1124.01131083088,1124.09504954273,1124.17868505409,1124.26223749749,1124.34572693334,
1124.42918088396,1124.5126173778,1124.59605448756,1124.67951028248,1124.76305477521,
1124.84664385815,1124.9303671257,1125.0110468416,1125.09478555345,1125.17842106481,
1125.26197350821,1125.34546294406,1125.42891689468,1125.51235338852,1125.59579049828,
1125.6792462932,1125.76279078593,1125.84637986887,1125.93010313642,1126.01078285232,
1126.09452156417,1126.17815707553,1126.26170951893,1126.34519895478,1126.4286529054,
1126.51208939924,1126.595526509,1126.67898230392,1126.76252679665,1126.84611587959,
1126.92983914714,1127.01051886304,1127.09299425828,1127.17537411721,1127.25767766004,
1127.33992395772,1127.42213509276,1127.50435017971,1127.58009447292),
 .UNSPECIFIED.);
#764=B_SPLINE_CURVE_WITH_KNOTS('',3,(#98672,#98673,#98674,#98675,#98676,
#98677,#98678,#98679,#98680,#98681),.UNSPECIFIED.,.F.,.F.,(4,3,3,4),(1121.29817665327,
1121.38449491277,1121.47070749291,1121.54857733154),.UNSPECIFIED.);
#765=B_SPLINE_CURVE_WITH_KNOTS('',3,(#98683,#98684,#98685,#98686,#98687,
#98688,#98689,#98690,#98691,#98692),.UNSPECIFIED.,.F.,.F.,(4,3,3,4),(1121.2973671878,
1121.32239341843,1121.43573137779,1121.54857733154),.UNSPECIFIED.);
#766=B_SPLINE_CURVE_WITH_KNOTS('',3,(#98693,#98694,#98695,#98696,#98697,
#98698,#98699,#98700,#98701,#98702,#98703,#98704,#98705,#98706,#98707,#98708,
#98709,#98710,#98711,#98712,#98713,#98714,#98715,#98716,#98717,#98718,#98719,
#98720,#98721,#98722,#98723,#98724,#98725,#98726,#98727,#98728,#98729,#98730,
#98731,#98732,#98733,#98734,#98735,#98736,#98737,#98738,#98739,#98740,#98741,
#98742,#98743,#98744,#98745,#98746,#98747,#98748,#98749,#98750,#98751,#98752,
#98753,#98754,#98755,#98756,#98757,#98758,#98759,#98760,#98761,#98762,#98763,
#98764,#98765,#98766,#98767,#98768,#98769,#98770,#98771,#98772,#98773,#98774,
#98775,#98776,#98777,#98778,#98779,#98780,#98781,#98782,#98783,#98784,#98785,
#98786,#98787,#98788,#98789,#98790,#98791,#98792,#98793,#98794,#98795,#98796,
#98797,#98798,#98799,#98800,#98801,#98802,#98803,#98804,#98805,#98806,#98807,
#98808,#98809,#98810,#98811,#98812,#98813,#98814,#98815,#98816,#98817,#98818,
#98819,#98820,#98821,#98822,#98823,#98824,#98825,#98826,#98827,#98828,#98829,
#98830,#98831,#98832,#98833,#98834,#98835,#98836,#98837,#98838,#98839,#98840,
#98841,#98842,#98843,#98844,#98845,#98846,#98847,#98848,#98849,#98850,#98851,
#98852,#98853,#98854,#98855,#98856,#98857,#98858,#98859,#98860,#98861,#98862,
#98863,#98864,#98865,#98866,#98867,#98868,#98869,#98870,#98871,#98872,#98873,
#98874,#98875,#98876,#98877,#98878,#98879,#98880,#98881,#98882,#98883,#98884,
#98885,#98886,#98887,#98888,#98889,#98890,#98891,#98892,#98893,#98894,#98895,
#98896,#98897,#98898,#98899,#98900,#98901,#98902,#98903,#98904,#98905,#98906,
#98907,#98908,#98909,#98910,#98911,#98912),.UNSPECIFIED.,.F.,.F.,(4,3,3,
3,3,3,3,3,3,3,3,3,3,3,3,3,3,3,3,3,3,3,3,3,3,3,3,3,3,3,3,3,3,3,3,3,3,3,3,
3,3,3,3,3,3,3,3,3,3,3,3,3,3,3,3,3,3,3,3,3,3,3,3,3,3,3,3,3,3,3,3,3,3,4),
(1121.5485773317,1121.63102433406,1121.71741247094,1121.79976528288,1121.88210511884,
1121.96445092535,1122.04682165131,1122.12928094339,1122.21179209108,1122.29442027794,
1122.32212942915,1122.405868141,1122.48950365236,1122.57305609576,1122.65654553161,
1122.73999948223,1122.82343597607,1122.90687308583,1122.99032888075,1123.07387337347,
1123.15746245642,1123.24118572397,1123.32186543987,1123.40560415172,1123.48923966308,
1123.57279210648,1123.65628154233,1123.73973549295,1123.82317198679,1123.90660909655,
1123.99006489147,1124.0736093842,1124.15719846714,1124.24092173469,1124.32160145059,
1124.40534016244,1124.4889756738,1124.5725281172,1124.65601755305,1124.73947150367,
1124.82290799751,1124.90634510727,1124.98980090219,1125.07334539491,1125.15693447786,
1125.24065774541,1125.32133746131,1125.40507617316,1125.48871168452,1125.57226412792,
1125.65575356377,1125.73920751439,1125.82264400823,1125.90608111799,1125.98953691291,
1126.07308140564,1126.15667048858,1126.24039375613,1126.32107347203,1126.40481218388,
1126.48844769524,1126.57200013864,1126.65548957449,1126.73894352511,1126.82238001895,
1126.90581712871,1126.98927292363,1127.07281741636,1127.1564064993,1127.24012976685,
1127.32080948275,1127.40843810818,1127.49587754248,1127.58141735988),
 .UNSPECIFIED.);
#767=B_SPLINE_CURVE_WITH_KNOTS('',3,(#98918,#98919,#98920,#98921,#98922,
#98923,#98924,#98925,#98926,#98927,#98928,#98929,#98930,#98931,#98932,#98933,
#98934,#98935,#98936,#98937,#98938,#98939,#98940,#98941,#98942,#98943,#98944,
#98945,#98946,#98947,#98948,#98949,#98950,#98951,#98952,#98953,#98954,#98955,
#98956,#98957,#98958,#98959,#98960,#98961,#98962,#98963,#98964,#98965,#98966,
#98967,#98968,#98969,#98970,#98971,#98972,#98973,#98974,#98975,#98976,#98977,
#98978,#98979,#98980,#98981,#98982,#98983,#98984,#98985,#98986,#98987,#98988,
#98989,#98990,#98991,#98992,#98993,#98994,#98995,#98996,#98997,#98998,#98999,
#99000,#99001,#99002,#99003,#99004,#99005,#99006,#99007,#99008,#99009,#99010,
#99011,#99012,#99013,#99014,#99015,#99016,#99017,#99018,#99019,#99020,#99021,
#99022,#99023,#99024,#99025,#99026,#99027,#99028,#99029,#99030,#99031,#99032,
#99033,#99034,#99035,#99036,#99037,#99038,#99039,#99040,#99041,#99042,#99043,
#99044,#99045,#99046,#99047,#99048,#99049,#99050,#99051,#99052,#99053,#99054,
#99055,#99056,#99057,#99058,#99059,#99060,#99061,#99062,#99063,#99064,#99065,
#99066,#99067,#99068,#99069,#99070,#99071,#99072,#99073,#99074,#99075,#99076,
#99077,#99078,#99079,#99080,#99081,#99082,#99083,#99084,#99085,#99086,#99087,
#99088,#99089,#99090,#99091,#99092,#99093,#99094,#99095,#99096,#99097,#99098,
#99099,#99100,#99101,#99102,#99103,#99104,#99105,#99106,#99107,#99108,#99109,
#99110,#99111,#99112,#99113,#99114,#99115,#99116,#99117,#99118,#99119,#99120,
#99121,#99122,#99123,#99124,#99125,#99126,#99127,#99128,#99129,#99130,#99131,
#99132,#99133,#99134,#99135,#99136,#99137),.UNSPECIFIED.,.F.,.F.,(4,3,3,
3,3,3,3,3,3,3,3,3,3,3,3,3,3,3,3,3,3,3,3,3,3,3,3,3,3,3,3,3,3,3,3,3,3,3,3,
3,3,3,3,3,3,3,3,3,3,3,3,3,3,3,3,3,3,3,3,3,3,3,3,3,3,3,3,3,3,3,3,3,3,4),
(1127.83176263872,1127.95957097145,1128.01025487376,1128.09399358561,1128.17762909697,
1128.26118154037,1128.34467097622,1128.42812492684,1128.51156142068,1128.59499853044,
1128.67845432536,1128.76199881809,1128.84558790103,1128.92931116858,1129.00999088448,
1129.09372959633,1129.17736510769,1129.26091755109,1129.34440698694,1129.42786093756,
1129.5112974314,1129.59473454116,1129.67819033608,1129.7617348288,1129.84532391175,
1129.9290471793,1130.0097268952,1130.09346560705,1130.17710111841,1130.26065356181,
1130.34414299766,1130.42759694828,1130.51103344212,1130.59447055188,1130.6779263468,
1130.76147083953,1130.84505992247,1130.92878319002,1131.00946290592,1131.09320161777,
1131.17683712913,1131.26038957253,1131.34387900838,1131.427332959,1131.51076945284,
1131.5942065626,1131.67766235752,1131.76120685025,1131.84479593319,1131.92851920074,
1132.00919891664,1132.09293762849,1132.17657313985,1132.26012558325,1132.3436150191,
1132.42706896972,1132.51050546356,1132.59394257332,1132.67739836824,1132.76094286097,
1132.84453194391,1132.92825521146,1133.00893492736,1133.09268224944,1133.17632445377,
1133.26220042274,1133.34568559806,1133.42913301872,1133.51256077308,1133.60025363119,
1133.68372583927,1133.76722657941,1133.85080197334,1133.86333220551),
 .UNSPECIFIED.);
#768=B_SPLINE_CURVE_WITH_KNOTS('',3,(#99138,#99139,#99140,#99141,#99142,
#99143,#99144,#99145,#99146,#99147),.UNSPECIFIED.,.F.,.F.,(4,3,3,4),(1127.58009447292,
1127.66234880159,1127.74705572007,1127.83176263856),.UNSPECIFIED.);
#769=B_SPLINE_CURVE_WITH_KNOTS('',3,(#99149,#99150,#99151,#99152,#99153,
#99154,#99155,#99156,#99157,#99158),.UNSPECIFIED.,.F.,.F.,(4,3,3,4),(1127.58141735988,
1127.668604728,1127.75564880231,1127.83176263872),.UNSPECIFIED.);
#770=B_SPLINE_CURVE_WITH_KNOTS('',3,(#99159,#99160,#99161,#99162,#99163,
#99164,#99165,#99166,#99167,#99168,#99169,#99170,#99171,#99172,#99173,#99174,
#99175,#99176,#99177,#99178,#99179,#99180,#99181,#99182,#99183,#99184,#99185,
#99186,#99187,#99188,#99189,#99190,#99191,#99192,#99193,#99194,#99195,#99196,
#99197,#99198,#99199,#99200,#99201,#99202,#99203,#99204,#99205,#99206,#99207,
#99208,#99209,#99210,#99211,#99212,#99213,#99214,#99215,#99216,#99217,#99218,
#99219,#99220,#99221,#99222,#99223,#99224,#99225,#99226,#99227,#99228,#99229,
#99230,#99231,#99232,#99233,#99234,#99235,#99236,#99237,#99238,#99239,#99240,
#99241,#99242,#99243,#99244,#99245,#99246,#99247,#99248,#99249,#99250,#99251,
#99252,#99253,#99254,#99255,#99256,#99257,#99258,#99259,#99260,#99261,#99262,
#99263,#99264,#99265,#99266,#99267,#99268,#99269,#99270,#99271,#99272,#99273,
#99274,#99275,#99276,#99277,#99278,#99279,#99280,#99281,#99282,#99283,#99284,
#99285,#99286,#99287,#99288,#99289,#99290,#99291,#99292,#99293,#99294,#99295,
#99296,#99297,#99298,#99299,#99300,#99301,#99302,#99303,#99304,#99305,#99306,
#99307,#99308,#99309,#99310,#99311,#99312,#99313,#99314,#99315,#99316,#99317,
#99318,#99319,#99320,#99321,#99322,#99323,#99324,#99325,#99326,#99327,#99328,
#99329,#99330,#99331,#99332,#99333,#99334,#99335,#99336,#99337,#99338,#99339,
#99340,#99341,#99342,#99343,#99344,#99345,#99346,#99347,#99348,#99349,#99350,
#99351,#99352,#99353,#99354,#99355,#99356,#99357,#99358,#99359,#99360,#99361,
#99362,#99363,#99364,#99365,#99366,#99367,#99368,#99369,#99370,#99371,#99372,
#99373,#99374,#99375,#99376,#99377,#99378),.UNSPECIFIED.,.F.,.F.,(4,3,3,
3,3,3,3,3,3,3,3,3,3,3,3,3,3,3,3,3,3,3,3,3,3,3,3,3,3,3,3,3,3,3,3,3,3,3,3,
3,3,3,3,3,3,3,3,3,3,3,3,3,3,3,3,3,3,3,3,3,3,3,3,3,3,3,3,3,3,3,3,3,3,4),
(1127.83176263883,1127.91957948589,1128.00752696713,1128.09569652539,1128.18398523041,
1128.27247833123,1128.32054549347,1128.40428420532,1128.48791971668,1128.57147216008,
1128.65496159593,1128.73841554655,1128.82185204039,1128.90528915015,1128.98874494507,
1129.0722894378,1129.15587852074,1129.23960178829,1129.32028150419,1129.40402021604,
1129.4876557274,1129.5712081708,1129.65469760665,1129.73815155727,1129.82158805111,
1129.90502516087,1129.98848095579,1130.07202544852,1130.15561453146,1130.23933779902,
1130.32001751491,1130.40375622676,1130.48739173812,1130.57094418152,1130.65443361737,
1130.73788756799,1130.82132406183,1130.90476117159,1130.98821696651,1131.07176145923,
1131.15535054218,1131.23907380973,1131.31975352563,1131.40349223748,1131.48712774884,
1131.57068019224,1131.65416962809,1131.73762357871,1131.82106007255,1131.90449718231,
1131.98795297723,1132.07149746995,1132.1550865529,1132.23880982045,1132.31948953635,
1132.4032282482,1132.48686375956,1132.57041620296,1132.65390563881,1132.73735958943,
1132.82079608327,1132.90423319303,1132.98768898795,1133.07123348068,1133.15482256362,
1133.23854583118,1133.31922554707,1133.40175294837,1133.48418409761,1133.56653818716,
1133.64883186673,1133.73108993687,1133.8133437479,1133.86337617231),
 .UNSPECIFIED.);
#771=B_SPLINE_CURVE_WITH_KNOTS('',3,(#99384,#99385,#99386,#99387,#99388,
#99389,#99390,#99391,#99392,#99393,#99394,#99395,#99396,#99397,#99398,#99399,
#99400,#99401,#99402,#99403,#99404,#99405,#99406,#99407,#99408,#99409,#99410,
#99411,#99412,#99413,#99414,#99415,#99416,#99417,#99418,#99419,#99420,#99421,
#99422,#99423,#99424,#99425,#99426,#99427,#99428,#99429,#99430,#99431,#99432,
#99433,#99434,#99435,#99436,#99437,#99438,#99439,#99440,#99441,#99442,#99443,
#99444,#99445,#99446,#99447,#99448,#99449,#99450,#99451,#99452,#99453,#99454,
#99455,#99456,#99457,#99458,#99459,#99460,#99461,#99462,#99463,#99464,#99465,
#99466,#99467,#99468,#99469,#99470,#99471,#99472,#99473,#99474,#99475,#99476,
#99477,#99478,#99479,#99480,#99481,#99482,#99483,#99484,#99485,#99486,#99487,
#99488,#99489,#99490,#99491,#99492,#99493,#99494,#99495,#99496,#99497,#99498,
#99499,#99500,#99501,#99502,#99503,#99504,#99505,#99506,#99507,#99508,#99509,
#99510,#99511,#99512,#99513,#99514,#99515,#99516,#99517,#99518,#99519,#99520,
#99521,#99522,#99523,#99524,#99525,#99526,#99527,#99528,#99529,#99530,#99531,
#99532,#99533,#99534,#99535,#99536,#99537,#99538,#99539,#99540,#99541,#99542,
#99543,#99544,#99545,#99546,#99547,#99548,#99549,#99550,#99551,#99552,#99553,
#99554,#99555,#99556,#99557,#99558,#99559,#99560,#99561,#99562,#99563,#99564,
#99565,#99566,#99567,#99568,#99569,#99570,#99571,#99572,#99573,#99574,#99575,
#99576,#99577,#99578,#99579,#99580,#99581,#99582,#99583,#99584,#99585,#99586,
#99587,#99588,#99589,#99590,#99591,#99592,#99593,#99594,#99595,#99596,#99597,
#99598,#99599,#99600,#99601,#99602,#99603),.UNSPECIFIED.,.F.,.F.,(4,3,3,
3,3,3,3,3,3,3,3,3,3,3,3,3,3,3,3,3,3,3,3,3,3,3,3,3,3,3,3,3,3,3,3,3,3,3,3,
3,3,3,3,3,3,3,3,3,3,3,3,3,3,3,3,3,3,3,3,3,3,3,3,3,3,3,3,3,3,3,3,3,3,4),
(1134.11494794604,1134.19754763141,1134.28005584972,1134.3624936672,1134.44488704967,
1134.52725803592,1134.60962556158,1134.6920085571,1134.77447536623,1134.85698551003,
1134.93962372416,1135.0084069488,1135.09214566065,1135.17578117201,1135.25933361541,
1135.34282305126,1135.42627700188,1135.50971349572,1135.59315060548,1135.6766064004,
1135.76015089313,1135.84373997607,1135.92746324362,1136.00814295952,1136.09188167137,
1136.17551718273,1136.25906962613,1136.34255906198,1136.4260130126,1136.50944950644,
1136.5928866162,1136.67634241112,1136.75988690385,1136.84347598679,1136.92719925434,
1137.00787897024,1137.09161768209,1137.17525319345,1137.25880563685,1137.3422950727,
1137.42574902332,1137.50918551716,1137.59262262692,1137.67607842184,1137.75962291457,
1137.84321199751,1137.92693526506,1138.00761498096,1138.09135369281,1138.17498920417,
1138.25854164757,1138.34203108342,1138.42548503404,1138.50892152788,1138.59235863764,
1138.67581443255,1138.75935892528,1138.84294800823,1138.92667127578,1139.00735099168,
1139.09108970353,1139.17472521489,1139.25827765829,1139.34176709414,1139.42522104476,
1139.5086575386,1139.59209464836,1139.67555044328,1139.75909493601,1139.84268401895,
1139.9264072865,1140.0070870024,1140.1008350489,1140.14773803965),
 .UNSPECIFIED.);
#772=B_SPLINE_CURVE_WITH_KNOTS('',3,(#99604,#99605,#99606,#99607,#99608,
#99609,#99610,#99611,#99612,#99613),.UNSPECIFIED.,.F.,.F.,(4,3,3,4),(1133.86333220551,
1133.94706238406,1134.00867093808,1134.1149479459),.UNSPECIFIED.);
#773=B_SPLINE_CURVE_WITH_KNOTS('',3,(#99615,#99616,#99617,#99618,#99619,
#99620,#99621,#99622,#99623,#99624),.UNSPECIFIED.,.F.,.F.,(4,3,3,4),(1133.86337617231,
1133.94566361369,1134.03030577971,1134.11494794573),.UNSPECIFIED.);
#774=B_SPLINE_CURVE_WITH_KNOTS('',3,(#99625,#99626,#99627,#99628,#99629,
#99630,#99631,#99632,#99633,#99634,#99635,#99636,#99637,#99638,#99639,#99640,
#99641,#99642,#99643,#99644,#99645,#99646,#99647,#99648,#99649,#99650,#99651,
#99652,#99653,#99654,#99655,#99656,#99657,#99658,#99659,#99660,#99661,#99662,
#99663,#99664,#99665,#99666,#99667,#99668,#99669,#99670,#99671,#99672,#99673,
#99674,#99675,#99676,#99677,#99678,#99679,#99680,#99681,#99682,#99683,#99684,
#99685,#99686,#99687,#99688,#99689,#99690,#99691,#99692,#99693,#99694,#99695,
#99696,#99697,#99698,#99699,#99700,#99701,#99702,#99703,#99704,#99705,#99706,
#99707,#99708,#99709,#99710,#99711,#99712,#99713,#99714,#99715,#99716,#99717,
#99718,#99719,#99720,#99721,#99722,#99723,#99724,#99725,#99726,#99727,#99728,
#99729,#99730,#99731,#99732,#99733,#99734,#99735,#99736,#99737,#99738,#99739,
#99740,#99741,#99742,#99743,#99744,#99745,#99746,#99747,#99748,#99749,#99750,
#99751,#99752,#99753,#99754,#99755,#99756,#99757,#99758,#99759,#99760,#99761,
#99762,#99763,#99764,#99765,#99766,#99767,#99768,#99769,#99770,#99771,#99772,
#99773,#99774,#99775,#99776,#99777,#99778,#99779,#99780,#99781,#99782,#99783,
#99784,#99785,#99786,#99787,#99788,#99789,#99790,#99791,#99792,#99793,#99794,
#99795,#99796,#99797,#99798,#99799,#99800,#99801,#99802,#99803,#99804,#99805,
#99806,#99807,#99808,#99809,#99810,#99811,#99812,#99813,#99814,#99815,#99816,
#99817,#99818,#99819,#99820,#99821,#99822,#99823,#99824,#99825,#99826,#99827,
#99828,#99829,#99830,#99831,#99832,#99833,#99834,#99835,#99836,#99837,#99838,
#99839,#99840,#99841),.UNSPECIFIED.,.F.,.F.,(4,3,3,3,3,3,3,3,3,3,3,3,3,
3,3,3,3,3,3,3,3,3,3,3,3,3,3,3,3,3,3,3,3,3,3,3,3,3,3,3,3,3,3,3,3,3,3,3,3,
3,3,3,3,3,3,3,3,3,3,3,3,3,3,3,3,3,3,3,3,3,3,3,4),(1134.1149479459,1134.23395192778,
1134.31896155779,1134.40270026964,1134.486335781,1134.5698882244,1134.65337766025,
1134.73683161087,1134.82026810471,1134.90370521447,1134.98716100939,1135.07070550212,
1135.15429458506,1135.23801785262,1135.31869756852,1135.40243628037,1135.48607179173,
1135.56962423513,1135.65311367099,1135.7365676216,1135.82000411545,1135.9034412252,
1135.98689702012,1136.07044151285,1136.15403059579,1136.23775386335,1136.31843357924,
1136.40217229109,1136.48580780245,1136.56936024585,1136.6528496817,1136.73630363232,
1136.81974012616,1136.90317723592,1136.98663303083,1137.07017752356,1137.1537666065,
1137.23748987406,1137.31816958996,1137.40190830181,1137.48554381317,1137.56909625657,
1137.65258569242,1137.73603964304,1137.81947613688,1137.90291324664,1137.98636904156,
1138.06991353429,1138.15350261723,1138.23722588478,1138.31790560068,1138.40164431253,
1138.48527982389,1138.56883226729,1138.65232170314,1138.73577565376,1138.8192121476,
1138.90264925736,1138.98610505228,1139.06964954501,1139.15323862795,1139.23696189551,
1139.3176416114,1139.40139054479,1139.48503402325,1139.56857723134,1139.65206358258,
1139.73551119624,1139.81893816171,1139.90239151911,1139.98585572871,1140.06939644253,
1140.14648534745),.UNSPECIFIED.);
#775=B_SPLINE_CURVE_WITH_KNOTS('',3,(#99847,#99848,#99849,#99850,#99851,
#99852,#99853,#99854,#99855,#99856,#99857,#99858,#99859,#99860,#99861,#99862,
#99863,#99864,#99865,#99866,#99867,#99868,#99869,#99870,#99871,#99872,#99873,
#99874,#99875,#99876,#99877,#99878,#99879,#99880,#99881,#99882,#99883,#99884,
#99885,#99886,#99887,#99888,#99889,#99890,#99891,#99892,#99893,#99894,#99895,
#99896,#99897,#99898,#99899,#99900,#99901,#99902,#99903,#99904,#99905,#99906,
#99907,#99908,#99909,#99910,#99911,#99912,#99913,#99914,#99915,#99916,#99917,
#99918,#99919,#99920,#99921,#99922,#99923,#99924,#99925,#99926,#99927,#99928,
#99929,#99930,#99931,#99932,#99933,#99934,#99935,#99936,#99937,#99938,#99939,
#99940,#99941,#99942,#99943,#99944,#99945,#99946,#99947,#99948,#99949,#99950,
#99951,#99952,#99953,#99954,#99955,#99956,#99957,#99958,#99959,#99960,#99961,
#99962,#99963,#99964,#99965,#99966,#99967,#99968,#99969,#99970,#99971,#99972,
#99973,#99974,#99975,#99976,#99977,#99978,#99979,#99980,#99981,#99982,#99983,
#99984,#99985,#99986,#99987,#99988,#99989,#99990,#99991,#99992,#99993,#99994,
#99995,#99996,#99997,#99998,#99999,#100000,#100001,#100002,#100003,#100004,
#100005,#100006,#100007,#100008,#100009,#100010,#100011,#100012,#100013,
#100014,#100015,#100016,#100017,#100018,#100019,#100020,#100021,#100022,
#100023,#100024,#100025,#100026,#100027,#100028,#100029,#100030,#100031,
#100032,#100033,#100034,#100035,#100036,#100037,#100038,#100039,#100040,
#100041,#100042,#100043,#100044,#100045,#100046,#100047,#100048,#100049,
#100050,#100051,#100052,#100053,#100054,#100055,#100056,#100057,#100058,
#100059,#100060,#100061,#100062,#100063,#100064,#100065,#100066),
 .UNSPECIFIED.,.F.,.F.,(4,3,3,3,3,3,3,3,3,3,3,3,3,3,3,3,3,3,3,3,3,3,3,3,
3,3,3,3,3,3,3,3,3,3,3,3,3,3,3,3,3,3,3,3,3,3,3,3,3,3,3,3,3,3,3,3,3,3,3,3,
3,3,3,3,3,3,3,3,3,3,3,3,3,4),(1140.39813325308,1140.48251076188,1140.56690496386,
1140.65133254477,1140.74020516186,1140.8248033239,1140.90947201762,1140.99427121713,
1141.00682301312,1141.09056172497,1141.17419723633,1141.25774967973,1141.34123911558,
1141.4246930662,1141.50812956004,1141.5915666698,1141.67502246472,1141.75856695744,
1141.84215604039,1141.92587930794,1142.00655902384,1142.09029773569,1142.17393324705,
1142.25748569045,1142.3409751263,1142.42442907692,1142.50786557076,1142.59130268052,
1142.67475847544,1142.75830296817,1142.84189205111,1142.92561531866,1143.00629503456,
1143.09003374641,1143.17366925777,1143.25722170117,1143.34071113702,1143.42416508764,
1143.50760158148,1143.59103869124,1143.67449448616,1143.75803897888,1143.84162806183,
1143.92535132938,1144.00603104528,1144.08976975713,1144.17340526849,1144.25695771189,
1144.34044714774,1144.42390109836,1144.5073375922,1144.59077470196,1144.67423049688,
1144.75777498961,1144.84136407255,1144.9250873401,1145.005767056,1145.08950576785,
1145.17314127921,1145.25669372261,1145.34018315846,1145.42363710908,1145.50707360292,
1145.59051071268,1145.6739665076,1145.75751100033,1145.84110008327,1145.92482335083,
1146.00550306672,1146.08907419385,1146.17438957255,1146.25775095929,1146.34404333398,
1146.43033570868),.UNSPECIFIED.);
#776=B_SPLINE_CURVE_WITH_KNOTS('',3,(#100067,#100068,#100069,#100070,#100071,
#100072,#100073,#100074,#100075,#100076),.UNSPECIFIED.,.F.,.F.,(4,3,3,4),
(1140.14773803965,1140.24099126569,1140.33376735038,1140.39813325289),
 .UNSPECIFIED.);
#777=B_SPLINE_CURVE_WITH_KNOTS('',3,(#100078,#100079,#100080,#100081,#100082,
#100083,#100084,#100085,#100086,#100087),.UNSPECIFIED.,.F.,.F.,(4,3,3,4),
(1140.14648534745,1140.23193148479,1140.31737762212,1140.39813325308),
 .UNSPECIFIED.);
#778=B_SPLINE_CURVE_WITH_KNOTS('',3,(#100088,#100089,#100090,#100091,#100092,
#100093,#100094,#100095,#100096,#100097,#100098,#100099,#100100,#100101,
#100102,#100103,#100104,#100105,#100106,#100107,#100108,#100109,#100110,
#100111,#100112,#100113,#100114,#100115,#100116,#100117,#100118,#100119,
#100120,#100121,#100122,#100123,#100124,#100125,#100126,#100127,#100128,
#100129,#100130,#100131,#100132,#100133,#100134,#100135,#100136,#100137,
#100138,#100139,#100140,#100141,#100142,#100143,#100144,#100145,#100146,
#100147,#100148,#100149,#100150,#100151,#100152,#100153,#100154,#100155,
#100156,#100157,#100158,#100159,#100160,#100161,#100162,#100163,#100164,
#100165,#100166,#100167,#100168,#100169,#100170,#100171,#100172,#100173,
#100174,#100175,#100176,#100177,#100178,#100179,#100180,#100181,#100182,
#100183,#100184,#100185,#100186,#100187,#100188,#100189,#100190,#100191,
#100192,#100193,#100194,#100195,#100196,#100197,#100198,#100199,#100200,
#100201,#100202,#100203,#100204,#100205,#100206,#100207,#100208,#100209,
#100210,#100211,#100212,#100213,#100214,#100215,#100216,#100217,#100218,
#100219,#100220,#100221,#100222,#100223,#100224,#100225,#100226,#100227,
#100228,#100229,#100230,#100231,#100232,#100233,#100234,#100235,#100236,
#100237,#100238,#100239,#100240,#100241,#100242,#100243,#100244,#100245,
#100246,#100247,#100248,#100249,#100250,#100251,#100252,#100253,#100254,
#100255,#100256,#100257,#100258,#100259,#100260,#100261,#100262,#100263,
#100264,#100265,#100266,#100267,#100268,#100269,#100270,#100271,#100272,
#100273,#100274,#100275,#100276,#100277,#100278,#100279,#100280,#100281,
#100282,#100283,#100284,#100285,#100286,#100287,#100288,#100289,#100290,
#100291,#100292,#100293,#100294,#100295,#100296,#100297,#100298,#100299,
#100300,#100301,#100302,#100303,#100304,#100305,#100306,#100307),
 .UNSPECIFIED.,.F.,.F.,(4,3,3,3,3,3,3,3,3,3,3,3,3,3,3,3,3,3,3,3,3,3,3,3,
3,3,3,3,3,3,3,3,3,3,3,3,3,3,3,3,3,3,3,3,3,3,3,3,3,3,3,3,3,3,3,3,3,3,3,3,
3,3,3,3,3,3,3,3,3,3,3,3,3,4),(1140.39813325321,1140.48091981114,1140.56361047569,
1140.64622620517,1140.73008713363,1140.81262525657,1140.89515581373,1140.97769762652,
1141.0625516281,1141.14521622128,1141.23116492706,1141.31711363284,1141.40085234469,
1141.48448785605,1141.56804029945,1141.6515297353,1141.73498368592,1141.81842017976,
1141.90185728952,1141.98531308444,1142.06885757717,1142.15244666011,1142.23616992767,
1142.31684964356,1142.40058835541,1142.48422386677,1142.56777631017,1142.65126574602,
1142.73471969664,1142.81815619048,1142.90159330024,1142.98504909516,1143.06859358789,
1143.15218267083,1143.23590593838,1143.31658565428,1143.40032436613,1143.48395987749,
1143.56751232089,1143.65100175674,1143.73445570736,1143.8178922012,1143.90132931096,
1143.98478510588,1144.06832959861,1144.15191868155,1144.2356419491,1144.316321665,
1144.40006037685,1144.48369588821,1144.56724833161,1144.65073776746,1144.73419171808,
1144.81762821192,1144.90106532168,1144.9845211166,1145.06806560933,1145.15165469227,
1145.23537795982,1145.31605767572,1145.39979638757,1145.48343189893,1145.56698434233,
1145.65047377818,1145.7339277288,1145.81736422264,1145.9008013324,1145.98425712732,
1146.06780162004,1146.15139070299,1146.23511397054,1146.31579368644,1146.41148953146,
1146.43084402924),.UNSPECIFIED.);
#779=B_SPLINE_CURVE_WITH_KNOTS('',3,(#100313,#100314,#100315,#100316,#100317,
#100318,#100319,#100320,#100321,#100322,#100323,#100324,#100325,#100326,
#100327,#100328,#100329,#100330,#100331,#100332,#100333,#100334,#100335,
#100336,#100337,#100338,#100339,#100340,#100341,#100342,#100343,#100344,
#100345,#100346,#100347,#100348,#100349,#100350,#100351,#100352,#100353,
#100354,#100355,#100356,#100357,#100358,#100359,#100360,#100361,#100362,
#100363,#100364,#100365,#100366,#100367,#100368,#100369,#100370,#100371,
#100372,#100373,#100374,#100375,#100376,#100377,#100378,#100379,#100380,
#100381,#100382,#100383,#100384,#100385,#100386,#100387,#100388,#100389,
#100390,#100391,#100392,#100393,#100394,#100395,#100396,#100397,#100398,
#100399,#100400,#100401,#100402,#100403,#100404,#100405,#100406,#100407,
#100408,#100409,#100410,#100411,#100412,#100413,#100414,#100415,#100416,
#100417,#100418,#100419,#100420,#100421,#100422,#100423,#100424,#100425,
#100426,#100427,#100428,#100429,#100430,#100431,#100432,#100433,#100434,
#100435,#100436,#100437,#100438,#100439,#100440,#100441,#100442,#100443,
#100444,#100445,#100446,#100447,#100448,#100449,#100450,#100451,#100452,
#100453,#100454,#100455,#100456,#100457,#100458,#100459,#100460,#100461,
#100462,#100463,#100464,#100465,#100466,#100467,#100468,#100469,#100470,
#100471,#100472,#100473,#100474,#100475,#100476,#100477,#100478,#100479,
#100480,#100481,#100482,#100483,#100484,#100485,#100486,#100487,#100488,
#100489,#100490,#100491,#100492,#100493,#100494,#100495,#100496,#100497,
#100498,#100499,#100500,#100501,#100502,#100503,#100504,#100505,#100506,
#100507,#100508,#100509,#100510,#100511,#100512,#100513,#100514,#100515,
#100516,#100517,#100518,#100519,#100520,#100521,#100522,#100523,#100524,
#100525,#100526,#100527,#100528,#100529,#100530,#100531,#100532),
 .UNSPECIFIED.,.F.,.F.,(4,3,3,3,3,3,3,3,3,3,3,3,3,3,3,3,3,3,3,3,3,3,3,3,
3,3,3,3,3,3,3,3,3,3,3,3,3,3,3,3,3,3,3,3,3,3,3,3,3,3,3,3,3,3,3,3,3,3,3,3,
3,3,3,3,3,3,3,3,3,3,3,3,3,4),(1146.68131856044,1146.7794209927,1146.87817191571,
1146.97765054662,1147.00523907744,1147.08897778929,1147.17261330065,1147.25616574405,
1147.3396551799,1147.42310913052,1147.50654562436,1147.58998273412,1147.67343852904,
1147.75698302176,1147.84057210471,1147.92429537226,1148.00497508816,1148.08871380001,
1148.17234931137,1148.25590175477,1148.33939119062,1148.42284514124,1148.50628163508,
1148.58971874484,1148.67317453976,1148.75671903249,1148.84030811543,1148.92403138299,
1149.00471109888,1149.08844981073,1149.17208532209,1149.25563776549,1149.33912720134,
1149.42258115196,1149.5060176458,1149.58945475556,1149.67291055048,1149.75645504321,
1149.84004412615,1149.9237673937,1150.0044471096,1150.08818582145,1150.17182133281,
1150.25537377621,1150.33886321206,1150.42231716268,1150.50575365652,1150.58919076628,
1150.67264656119,1150.75619105392,1150.83978013687,1150.92350340442,1151.00418312032,
1151.08792183217,1151.17155734353,1151.25510978693,1151.33859922278,1151.4220531734,
1151.50548966724,1151.588926777,1151.67238257192,1151.75592706465,1151.83951614759,
1151.92323941515,1152.00391913104,1152.08715180263,1152.17025299475,1152.25327826016,
1152.33624622653,1152.41917547575,1152.50210012115,1152.58502118562,1152.6679838129,
1152.71272127735),.UNSPECIFIED.);
#780=B_SPLINE_CURVE_WITH_KNOTS('',3,(#100533,#100534,#100535,#100536,#100537,
#100538,#100539,#100540,#100541,#100542),.UNSPECIFIED.,.F.,.F.,(4,3,3,4),
(1146.43033570868,1146.51357203859,1146.59744529942,1146.68131856026),
 .UNSPECIFIED.);
#781=B_SPLINE_CURVE_WITH_KNOTS('',3,(#100544,#100545,#100546,#100547,#100548,
#100549,#100550,#100551,#100552,#100553),.UNSPECIFIED.,.F.,.F.,(4,3,3,4),
(1146.43084402924,1146.52599979843,1146.62054094815,1146.68131856006),
 .UNSPECIFIED.);
#782=B_SPLINE_CURVE_WITH_KNOTS('',3,(#100554,#100555,#100556,#100557,#100558,
#100559,#100560,#100561,#100562,#100563,#100564,#100565,#100566,#100567,
#100568,#100569,#100570,#100571,#100572,#100573,#100574,#100575,#100576,
#100577,#100578,#100579,#100580,#100581,#100582,#100583,#100584,#100585,
#100586,#100587,#100588,#100589,#100590,#100591,#100592,#100593,#100594,
#100595,#100596,#100597,#100598,#100599,#100600,#100601,#100602,#100603,
#100604,#100605,#100606,#100607,#100608,#100609,#100610,#100611,#100612,
#100613,#100614,#100615,#100616,#100617,#100618,#100619,#100620,#100621,
#100622,#100623,#100624,#100625,#100626,#100627,#100628,#100629,#100630,
#100631,#100632,#100633,#100634,#100635,#100636,#100637,#100638,#100639,
#100640,#100641,#100642,#100643,#100644,#100645,#100646,#100647,#100648,
#100649,#100650,#100651,#100652,#100653,#100654,#100655,#100656,#100657,
#100658,#100659,#100660,#100661,#100662,#100663,#100664,#100665,#100666,
#100667,#100668,#100669,#100670,#100671,#100672,#100673,#100674,#100675,
#100676,#100677,#100678,#100679,#100680,#100681,#100682,#100683,#100684,
#100685,#100686,#100687,#100688,#100689,#100690,#100691,#100692,#100693,
#100694,#100695,#100696,#100697,#100698,#100699,#100700,#100701,#100702,
#100703,#100704,#100705,#100706,#100707,#100708,#100709,#100710,#100711,
#100712,#100713,#100714,#100715,#100716,#100717,#100718,#100719,#100720,
#100721,#100722,#100723,#100724,#100725,#100726,#100727,#100728,#100729,
#100730,#100731,#100732,#100733,#100734,#100735,#100736,#100737,#100738,
#100739,#100740,#100741,#100742,#100743,#100744,#100745,#100746,#100747,
#100748,#100749,#100750,#100751,#100752,#100753,#100754,#100755,#100756,
#100757,#100758,#100759,#100760,#100761,#100762,#100763,#100764,#100765,
#100766,#100767,#100768,#100769,#100770,#100771,#100772,#100773),
 .UNSPECIFIED.,.F.,.F.,(4,3,3,3,3,3,3,3,3,3,3,3,3,3,3,3,3,3,3,3,3,3,3,3,
3,3,3,3,3,3,3,3,3,3,3,3,3,3,3,3,3,3,3,3,3,3,3,3,3,3,3,3,3,3,3,3,3,3,3,3,
3,3,3,3,3,3,3,3,3,3,3,3,3,4),(1146.68131856026,1146.76521245412,1146.84910858566,
1146.93302437699,1147.01697725917,1147.10103703447,1147.18515641783,1147.2694111216,
1147.31552969716,1147.39926840901,1147.48290392037,1147.56645636377,1147.64994579962,
1147.73339975024,1147.81683624408,1147.90027335384,1147.98372914876,1148.06727364149,
1148.15086272443,1148.23458599198,1148.31526570788,1148.39900441973,1148.48263993109,
1148.56619237449,1148.64968181034,1148.73313576096,1148.8165722548,1148.90000936456,
1148.98346515948,1149.0670096522,1149.15059873515,1149.2343220027,1149.3150017186,
1149.39874043045,1149.48237594181,1149.56592838521,1149.64941782106,1149.73287177168,
1149.81630826552,1149.89974537528,1149.9832011702,1150.06674566293,1150.15033474587,
1150.23405801342,1150.31473772932,1150.39847644117,1150.48211195253,1150.56566439593,
1150.64915383178,1150.7326077824,1150.81604427624,1150.899481386,1150.98293718092,
1151.06648167365,1151.15007075659,1151.23379402415,1151.31447374004,1151.39821245189,
1151.48184796325,1151.56540040665,1151.6488898425,1151.73234379312,1151.81578028696,
1151.89921739672,1151.98267319164,1152.06621768437,1152.14980676731,1152.23353003486,
1152.31420975076,1152.39818867721,1152.48203015719,1152.56579257425,1152.64948197077,
1152.71365100326),.UNSPECIFIED.);
#783=B_SPLINE_CURVE_WITH_KNOTS('',3,(#100779,#100780,#100781,#100782,#100783,
#100784,#100785,#100786,#100787,#100788,#100789,#100790,#100791,#100792,
#100793,#100794,#100795,#100796,#100797,#100798,#100799,#100800,#100801,
#100802,#100803,#100804,#100805,#100806,#100807,#100808,#100809,#100810,
#100811,#100812,#100813,#100814,#100815,#100816,#100817,#100818,#100819,
#100820,#100821,#100822,#100823,#100824,#100825,#100826,#100827,#100828,
#100829,#100830,#100831,#100832,#100833,#100834,#100835,#100836,#100837,
#100838,#100839,#100840,#100841,#100842,#100843,#100844,#100845,#100846,
#100847,#100848,#100849,#100850,#100851,#100852,#100853,#100854,#100855,
#100856,#100857,#100858,#100859,#100860,#100861,#100862,#100863,#100864,
#100865,#100866,#100867,#100868,#100869,#100870,#100871,#100872,#100873,
#100874,#100875,#100876,#100877,#100878,#100879,#100880,#100881,#100882,
#100883,#100884,#100885,#100886,#100887,#100888,#100889,#100890,#100891,
#100892,#100893,#100894,#100895,#100896,#100897,#100898,#100899,#100900,
#100901,#100902,#100903,#100904,#100905,#100906,#100907,#100908,#100909,
#100910,#100911,#100912,#100913,#100914,#100915,#100916,#100917,#100918,
#100919,#100920,#100921,#100922,#100923,#100924,#100925,#100926,#100927,
#100928,#100929,#100930,#100931,#100932,#100933,#100934,#100935,#100936,
#100937,#100938,#100939,#100940,#100941,#100942,#100943,#100944,#100945,
#100946,#100947,#100948,#100949,#100950,#100951,#100952,#100953,#100954,
#100955,#100956,#100957,#100958,#100959,#100960,#100961,#100962,#100963,
#100964,#100965,#100966,#100967,#100968,#100969,#100970,#100971,#100972,
#100973,#100974,#100975,#100976,#100977,#100978,#100979,#100980,#100981,
#100982,#100983,#100984,#100985,#100986,#100987,#100988,#100989,#100990,
#100991,#100992,#100993,#100994,#100995,#100996,#100997,#100998),
 .UNSPECIFIED.,.F.,.F.,(4,3,3,3,3,3,3,3,3,3,3,3,3,3,3,3,3,3,3,3,3,3,3,3,
3,3,3,3,3,3,3,3,3,3,3,3,3,3,3,3,3,3,3,3,3,3,3,3,3,3,3,3,3,3,3,3,3,3,3,3,
3,3,3,3,3,3,3,3,3,3,3,3,3,4),(1152.96450386744,1153.00365514176,1153.08739385361,
1153.17102936497,1153.25458180837,1153.33807124422,1153.42152519484,1153.50496168868,
1153.58839879844,1153.67185459336,1153.75539908609,1153.83898816903,1153.92271143658,
1154.00339115248,1154.08712986433,1154.17076537569,1154.25431781909,1154.33780725494,
1154.42126120556,1154.5046976994,1154.58813480916,1154.67159060408,1154.75513509681,
1154.83872417975,1154.92244744731,1155.0031271632,1155.08686587505,1155.17050138641,
1155.25405382981,1155.33754326566,1155.42099721628,1155.50443371012,1155.58787081988,
1155.6713266148,1155.75487110753,1155.83846019047,1155.92218345802,1156.00286317392,
1156.08660188577,1156.17023739713,1156.25378984053,1156.33727927638,1156.420733227,
1156.50416972084,1156.5876068306,1156.67106262552,1156.75460711825,1156.83819620119,
1156.92191946874,1157.00259918464,1157.08633789649,1157.16997340785,1157.25352585125,
1157.3370152871,1157.42046923772,1157.50390573156,1157.58734284132,1157.67079863623,
1157.75434312896,1157.8379322119,1157.92165547946,1158.00233519536,1158.08607421481,
1158.16970996149,1158.25326256821,1158.33675209564,1158.42020576168,1158.50364186877,
1158.58707848948,1158.67053369293,1158.75407615424,1158.83766316353,1158.92138094069,
1158.99659016216),.UNSPECIFIED.);
#784=B_SPLINE_CURVE_WITH_KNOTS('',3,(#100999,#101000,#101001,#101002,#101003,
#101004,#101005,#101006,#101007,#101008),.UNSPECIFIED.,.F.,.F.,(4,3,3,4),
(1152.71272127735,1152.79577877608,1152.88014132168,1152.96450386727),
 .UNSPECIFIED.);
#785=B_SPLINE_CURVE_WITH_KNOTS('',3,(#101010,#101011,#101012,#101013,#101014,
#101015,#101016,#101017,#101018,#101019),.UNSPECIFIED.,.F.,.F.,(4,3,3,4),
(1152.71365100326,1152.79727347273,1152.88090159923,1152.96450386744),
 .UNSPECIFIED.);
#786=B_SPLINE_CURVE_WITH_KNOTS('',3,(#101020,#101021,#101022,#101023,#101024,
#101025,#101026,#101027,#101028,#101029,#101030,#101031,#101032,#101033,
#101034,#101035,#101036,#101037,#101038,#101039,#101040,#101041,#101042,
#101043,#101044,#101045,#101046,#101047,#101048,#101049,#101050,#101051,
#101052,#101053,#101054,#101055,#101056,#101057,#101058,#101059,#101060,
#101061,#101062,#101063,#101064,#101065,#101066,#101067,#101068,#101069,
#101070,#101071,#101072,#101073,#101074,#101075,#101076,#101077,#101078,
#101079,#101080,#101081,#101082,#101083,#101084,#101085,#101086,#101087,
#101088,#101089,#101090,#101091,#101092,#101093,#101094,#101095,#101096,
#101097,#101098,#101099,#101100,#101101,#101102,#101103,#101104,#101105,
#101106,#101107,#101108,#101109,#101110,#101111,#101112,#101113,#101114,
#101115,#101116,#101117,#101118,#101119,#101120,#101121,#101122,#101123,
#101124,#101125,#101126,#101127,#101128,#101129,#101130,#101131,#101132,
#101133,#101134,#101135,#101136,#101137,#101138,#101139,#101140,#101141,
#101142,#101143,#101144,#101145,#101146,#101147,#101148,#101149,#101150,
#101151,#101152,#101153,#101154,#101155,#101156,#101157,#101158,#101159,
#101160,#101161,#101162,#101163,#101164,#101165,#101166,#101167,#101168,
#101169,#101170,#101171,#101172,#101173,#101174,#101175,#101176,#101177,
#101178,#101179,#101180,#101181,#101182,#101183,#101184,#101185,#101186,
#101187,#101188,#101189,#101190,#101191,#101192,#101193,#101194,#101195,
#101196,#101197,#101198,#101199,#101200,#101201,#101202,#101203,#101204,
#101205,#101206,#101207,#101208,#101209,#101210,#101211,#101212,#101213,
#101214,#101215,#101216,#101217,#101218,#101219,#101220,#101221,#101222,
#101223,#101224,#101225,#101226,#101227,#101228,#101229,#101230,#101231,
#101232,#101233,#101234,#101235,#101236,#101237,#101238,#101239),
 .UNSPECIFIED.,.F.,.F.,(4,3,3,3,3,3,3,3,3,3,3,3,3,3,3,3,3,3,3,3,3,3,3,3,
3,3,3,3,3,3,3,3,3,3,3,3,3,3,3,3,3,3,3,3,3,3,3,3,3,3,3,3,3,3,3,3,3,3,3,3,
3,3,3,3,3,3,3,3,3,3,3,3,3,4),(1152.96450386764,1153.06037082155,1153.15671753066,
1153.25367244208,1153.31394576148,1153.39768447333,1153.48131998469,1153.56487242809,
1153.64836186394,1153.73181581456,1153.8152523084,1153.89868941816,1153.98214521308,
1154.06568970581,1154.14927878875,1154.2330020563,1154.3136817722,1154.39742048405,
1154.48105599541,1154.56460843881,1154.64809787466,1154.73155182528,1154.81498831912,
1154.89842542888,1154.9818812238,1155.06542571653,1155.14901479947,1155.23273806702,
1155.31341778292,1155.39715649477,1155.48079200613,1155.56434444953,1155.64783388538,
1155.731287836,1155.81472432984,1155.8981614396,1155.98161723452,1156.06516172725,
1156.14875081019,1156.23247407774,1156.31315379364,1156.39689250549,1156.48052801685,
1156.56408046025,1156.6475698961,1156.73102384672,1156.81446034056,1156.89789745032,
1156.98135324524,1157.06489773797,1157.14848682091,1157.23221008847,1157.31288980436,
1157.39662851621,1157.48026402757,1157.56381647097,1157.64730590682,1157.73075985744,
1157.81419635128,1157.89763346104,1157.98108925596,1158.06463374869,1158.14822283163,
1158.23194609918,1158.31262581508,1158.39803049351,1158.4808680987,1158.56363060694,
1158.64633684465,1158.72900559084,1158.81166897465,1158.89433037083,1158.97702735572,
1158.99586324251),.UNSPECIFIED.);
#787=B_SPLINE_CURVE_WITH_KNOTS('',3,(#101245,#101246,#101247,#101248,#101249,
#101250,#101251,#101252,#101253,#101254,#101255,#101256,#101257,#101258,
#101259,#101260,#101261,#101262,#101263,#101264,#101265,#101266,#101267,
#101268,#101269,#101270,#101271,#101272,#101273,#101274,#101275,#101276,
#101277,#101278,#101279,#101280,#101281,#101282,#101283,#101284,#101285,
#101286,#101287,#101288,#101289,#101290,#101291,#101292,#101293,#101294,
#101295,#101296,#101297,#101298,#101299,#101300,#101301,#101302,#101303,
#101304,#101305,#101306,#101307,#101308,#101309,#101310,#101311,#101312,
#101313,#101314,#101315,#101316,#101317,#101318,#101319,#101320,#101321,
#101322,#101323,#101324,#101325,#101326,#101327,#101328,#101329,#101330,
#101331,#101332,#101333,#101334,#101335,#101336,#101337,#101338,#101339,
#101340,#101341,#101342,#101343,#101344,#101345,#101346,#101347,#101348,
#101349,#101350,#101351,#101352,#101353,#101354,#101355,#101356,#101357,
#101358,#101359,#101360,#101361,#101362,#101363,#101364,#101365,#101366,
#101367,#101368,#101369,#101370,#101371,#101372,#101373,#101374,#101375,
#101376,#101377,#101378,#101379,#101380,#101381,#101382,#101383,#101384,
#101385,#101386,#101387,#101388,#101389,#101390,#101391,#101392,#101393,
#101394,#101395,#101396,#101397,#101398,#101399,#101400,#101401,#101402,
#101403,#101404,#101405,#101406,#101407,#101408,#101409,#101410,#101411,
#101412,#101413,#101414,#101415,#101416,#101417,#101418,#101419,#101420,
#101421,#101422,#101423,#101424,#101425,#101426,#101427,#101428,#101429,
#101430,#101431,#101432,#101433,#101434,#101435,#101436,#101437,#101438,
#101439,#101440,#101441,#101442,#101443,#101444,#101445,#101446,#101447,
#101448,#101449,#101450,#101451,#101452,#101453,#101454,#101455,#101456,
#101457,#101458,#101459,#101460,#101461,#101462,#101463,#101464),
 .UNSPECIFIED.,.F.,.F.,(4,3,3,3,3,3,3,3,3,3,3,3,3,3,3,3,3,3,3,3,3,3,3,3,
3,3,3,3,3,3,3,3,3,3,3,3,3,3,3,3,3,3,3,3,3,3,3,3,3,3,3,3,3,3,3,3,3,3,3,3,
3,3,3,3,3,3,3,3,3,3,3,3,3,4),(1159.24768917462,1159.33022655319,1159.41417413614,
1159.49663275271,1159.57908345992,1159.66154512836,1159.74661065047,1159.82919506601,
1159.9155011414,1160.0018072168,1160.08554592865,1160.16918144001,1160.25273388341,
1160.33622331926,1160.41967726988,1160.50311376373,1160.58655087348,1160.6700066684,
1160.75355116113,1160.83714024407,1160.92086351163,1161.00154322752,1161.08528193937,
1161.16891745073,1161.25246989413,1161.33595932998,1161.4194132806,1161.50284977445,
1161.5862868842,1161.66974267912,1161.75328717185,1161.83687625479,1161.92059952235,
1162.00127923824,1162.08501795009,1162.16865346145,1162.25220590485,1162.3356953407,
1162.41914929132,1162.50258578516,1162.58602289492,1162.66947868983,1162.75302318256,
1162.8366122655,1162.92033553306,1163.00101524896,1163.08475396081,1163.16838947217,
1163.25194191557,1163.33543135142,1163.41888530204,1163.50232179588,1163.58575890564,
1163.66921470056,1163.75275919329,1163.83634827623,1163.92007154378,1164.00075125968,
1164.08448997153,1164.16812548289,1164.25167792629,1164.33516736214,1164.41862131275,
1164.5020578066,1164.58549491635,1164.66895071127,1164.752495204,1164.83608428694,
1164.9198075545,1165.0004872704,1165.08742265818,1165.17423700981,1165.2609081172,
1165.28048890086),.UNSPECIFIED.);
#788=B_SPLINE_CURVE_WITH_KNOTS('',3,(#101465,#101466,#101467,#101468,#101469,
#101470,#101471,#101472,#101473,#101474,#101475,#101476,#101477),
 .UNSPECIFIED.,.F.,.F.,(4,3,3,3,4),(1158.99659016216,1159.00207120608,1159.11274010456,
1159.22085745498,1159.24768917449),.UNSPECIFIED.);
#789=B_SPLINE_CURVE_WITH_KNOTS('',3,(#101479,#101480,#101481,#101482,#101483,
#101484,#101485,#101486,#101487,#101488),.UNSPECIFIED.,.F.,.F.,(4,3,3,4),
(1158.99586324251,1159.07864886217,1159.16316901834,1159.2476891745),
 .UNSPECIFIED.);
#790=B_SPLINE_CURVE_WITH_KNOTS('',3,(#101489,#101490,#101491,#101492,#101493,
#101494,#101495,#101496,#101497,#101498,#101499,#101500,#101501,#101502,
#101503,#101504,#101505,#101506,#101507,#101508,#101509,#101510,#101511,
#101512,#101513,#101514,#101515,#101516,#101517,#101518,#101519,#101520,
#101521,#101522,#101523,#101524,#101525,#101526,#101527,#101528,#101529,
#101530,#101531,#101532,#101533,#101534,#101535,#101536,#101537,#101538,
#101539,#101540,#101541,#101542,#101543,#101544,#101545,#101546,#101547,
#101548,#101549,#101550,#101551,#101552,#101553,#101554,#101555,#101556,
#101557,#101558,#101559,#101560,#101561,#101562,#101563,#101564,#101565,
#101566,#101567,#101568,#101569,#101570,#101571,#101572,#101573,#101574,
#101575,#101576,#101577,#101578,#101579,#101580,#101581,#101582,#101583,
#101584,#101585,#101586,#101587,#101588,#101589,#101590,#101591,#101592,
#101593,#101594,#101595,#101596,#101597,#101598,#101599,#101600,#101601,
#101602,#101603,#101604,#101605,#101606,#101607,#101608,#101609,#101610,
#101611,#101612,#101613,#101614,#101615,#101616,#101617,#101618,#101619,
#101620,#101621,#101622,#101623,#101624,#101625,#101626,#101627,#101628,
#101629,#101630,#101631,#101632,#101633,#101634,#101635,#101636,#101637,
#101638,#101639,#101640,#101641,#101642,#101643,#101644,#101645,#101646,
#101647,#101648,#101649,#101650,#101651,#101652,#101653,#101654,#101655,
#101656,#101657,#101658,#101659,#101660,#101661,#101662,#101663,#101664,
#101665,#101666,#101667,#101668,#101669,#101670,#101671,#101672,#101673,
#101674,#101675,#101676,#101677,#101678,#101679,#101680,#101681,#101682,
#101683,#101684,#101685,#101686,#101687,#101688,#101689,#101690,#101691,
#101692,#101693,#101694,#101695,#101696,#101697,#101698,#101699,#101700,
#101701,#101702,#101703,#101704,#101705,#101706,#101707,#101708),
 .UNSPECIFIED.,.F.,.F.,(4,3,3,3,3,3,3,3,3,3,3,3,3,3,3,3,3,3,3,3,3,3,3,3,
3,3,3,3,3,3,3,3,3,3,3,3,3,3,3,3,3,3,3,3,3,3,3,3,3,3,3,3,3,3,3,3,3,3,3,3,
3,3,3,3,3,3,3,3,3,3,3,3,3,4),(1159.24768917462,1159.3123618258,1159.39610053765,
1159.47973604901,1159.56328849241,1159.64677792826,1159.73023187888,1159.81366837272,
1159.89710548248,1159.9805612774,1160.06410577012,1160.14769485307,1160.23141812062,
1160.31209783652,1160.39583654837,1160.47947205973,1160.56302450313,1160.64651393898,
1160.7299678896,1160.81340438344,1160.8968414932,1160.98029728812,1161.06384178085,
1161.14743086379,1161.23115413134,1161.31183384724,1161.39557255909,1161.47920807045,
1161.56276051385,1161.6462499497,1161.72970390032,1161.81314039416,1161.89657750392,
1161.98003329884,1162.06357779156,1162.14716687451,1162.23089014206,1162.31156985796,
1162.39530856981,1162.47894408117,1162.56249652457,1162.64598596042,1162.72943991104,
1162.81287640488,1162.89631351464,1162.97976930956,1163.06331380229,1163.14690288523,
1163.23062615278,1163.31130586868,1163.39504458053,1163.47868009189,1163.56223253529,
1163.64572197114,1163.72917592176,1163.8126124156,1163.89604952536,1163.97950532028,
1164.06304981301,1164.14663889595,1164.2303621635,1164.3110418794,1164.394782357,
1164.47841922334,1164.56197261265,1164.64546258667,1164.72891499175,1164.81234935932,
1164.89578376167,1164.97923626715,1165.06276950219,1165.14634708746,1165.23004029477,
1165.27963236799),.UNSPECIFIED.);
#791=B_SPLINE_CURVE_WITH_KNOTS('',3,(#101714,#101715,#101716,#101717,#101718,
#101719,#101720,#101721,#101722,#101723,#101724,#101725,#101726,#101727,
#101728,#101729,#101730,#101731,#101732,#101733,#101734,#101735,#101736,
#101737,#101738,#101739,#101740,#101741,#101742,#101743,#101744,#101745,
#101746,#101747,#101748,#101749,#101750,#101751,#101752,#101753,#101754,
#101755,#101756,#101757,#101758,#101759,#101760,#101761,#101762,#101763,
#101764,#101765,#101766,#101767,#101768,#101769,#101770,#101771,#101772,
#101773,#101774,#101775,#101776,#101777,#101778,#101779,#101780,#101781,
#101782,#101783,#101784,#101785,#101786,#101787,#101788,#101789,#101790,
#101791,#101792,#101793,#101794,#101795,#101796,#101797,#101798,#101799,
#101800,#101801,#101802,#101803,#101804,#101805,#101806,#101807,#101808,
#101809,#101810,#101811,#101812,#101813,#101814,#101815,#101816,#101817,
#101818,#101819,#101820,#101821,#101822,#101823,#101824,#101825,#101826,
#101827,#101828,#101829,#101830,#101831,#101832,#101833,#101834,#101835,
#101836,#101837,#101838,#101839,#101840,#101841,#101842,#101843,#101844,
#101845,#101846,#101847,#101848,#101849,#101850,#101851,#101852,#101853,
#101854,#101855,#101856,#101857,#101858,#101859,#101860,#101861,#101862,
#101863,#101864,#101865,#101866,#101867,#101868,#101869,#101870,#101871,
#101872,#101873,#101874,#101875,#101876,#101877,#101878,#101879,#101880,
#101881,#101882,#101883,#101884,#101885,#101886,#101887,#101888,#101889,
#101890,#101891,#101892,#101893,#101894,#101895,#101896,#101897,#101898,
#101899,#101900,#101901,#101902,#101903,#101904,#101905,#101906,#101907,
#101908,#101909,#101910,#101911,#101912,#101913,#101914,#101915,#101916,
#101917,#101918,#101919,#101920,#101921,#101922,#101923,#101924,#101925,
#101926,#101927,#101928,#101929,#101930,#101931,#101932,#101933),
 .UNSPECIFIED.,.F.,.F.,(4,3,3,3,3,3,3,3,3,3,3,3,3,3,3,3,3,3,3,3,3,3,3,3,
3,3,3,3,3,3,3,3,3,3,3,3,3,3,3,3,3,3,3,3,3,3,3,3,3,3,3,3,3,3,3,3,3,3,3,3,
3,3,3,3,3,3,3,3,3,3,3,3,3,4),(1165.53087448193,1165.6194718285,1165.70823112112,
1165.79724274353,1165.88639300426,1165.97575379441,1166.00022328112,1166.08396199297,
1166.16759750434,1166.25114994774,1166.33463938359,1166.41809333421,1166.50152982806,
1166.58496693782,1166.66842273274,1166.75196722547,1166.83555630841,1166.91927957597,
1166.99995929184,1167.08369800369,1167.16733351505,1167.25088595845,1167.3343753943,
1167.41782934492,1167.50126583876,1167.58470294852,1167.66815874344,1167.75170323617,
1167.83529231911,1167.91901558667,1167.99969530256,1168.08343401441,1168.16706952577,
1168.25062196917,1168.33411140502,1168.41756535563,1168.50100184948,1168.58443895923,
1168.66789475415,1168.75143924688,1168.83502832982,1168.91875159738,1168.99943131328,
1169.08317002513,1169.16680553649,1169.25035797989,1169.33384741574,1169.41730136636,
1169.5007378602,1169.58417496996,1169.66763076488,1169.75117525761,1169.83476434055,
1169.91848760811,1169.999167324,1170.08290603585,1170.16654154721,1170.25009399061,
1170.33358342646,1170.41703737707,1170.50047387092,1170.58391098067,1170.66736677559,
1170.75091126832,1170.83450035126,1170.91822361882,1170.99890333472,1171.08138595452,
1171.16377288917,1171.24608335551,1171.32833583527,1171.41055307205,1171.49277221627,
1171.56241306759),.UNSPECIFIED.);
#792=B_SPLINE_CURVE_WITH_KNOTS('',3,(#101934,#101935,#101936,#101937,#101938,
#101939,#101940,#101941,#101942,#101943),.UNSPECIFIED.,.F.,.F.,(4,3,3,4),
(1165.28048890086,1165.36700416373,1165.45340537406,1165.5308744818),
 .UNSPECIFIED.);
#793=B_SPLINE_CURVE_WITH_KNOTS('',3,(#101945,#101946,#101947,#101948,#101949,
#101950,#101951,#101952,#101953,#101954),.UNSPECIFIED.,.F.,.F.,(4,3,3,4),
(1165.27963236799,1165.31077789012,1165.4255320562,1165.5308744818),
 .UNSPECIFIED.);
#794=B_SPLINE_CURVE_WITH_KNOTS('',3,(#101955,#101956,#101957,#101958,#101959,
#101960,#101961,#101962,#101963,#101964,#101965,#101966,#101967,#101968,
#101969,#101970,#101971,#101972,#101973,#101974,#101975,#101976,#101977,
#101978,#101979,#101980,#101981,#101982,#101983,#101984,#101985,#101986,
#101987,#101988,#101989,#101990,#101991,#101992,#101993,#101994,#101995,
#101996,#101997,#101998,#101999,#102000,#102001,#102002,#102003,#102004,
#102005,#102006,#102007,#102008,#102009,#102010,#102011,#102012,#102013,
#102014,#102015,#102016,#102017,#102018,#102019,#102020,#102021,#102022,
#102023,#102024,#102025,#102026,#102027,#102028,#102029,#102030,#102031,
#102032,#102033,#102034,#102035,#102036,#102037,#102038,#102039,#102040,
#102041,#102042,#102043,#102044,#102045,#102046,#102047,#102048,#102049,
#102050,#102051,#102052,#102053,#102054,#102055,#102056,#102057,#102058,
#102059,#102060,#102061,#102062,#102063,#102064,#102065,#102066,#102067,
#102068,#102069,#102070,#102071,#102072,#102073,#102074,#102075,#102076,
#102077,#102078,#102079,#102080,#102081,#102082,#102083,#102084,#102085,
#102086,#102087,#102088,#102089,#102090,#102091,#102092,#102093,#102094,
#102095,#102096,#102097,#102098,#102099,#102100,#102101,#102102,#102103,
#102104,#102105,#102106,#102107,#102108,#102109,#102110,#102111,#102112,
#102113,#102114,#102115,#102116,#102117,#102118,#102119,#102120,#102121,
#102122,#102123,#102124,#102125,#102126,#102127,#102128,#102129,#102130,
#102131,#102132,#102133,#102134,#102135,#102136,#102137,#102138,#102139,
#102140,#102141,#102142,#102143,#102144,#102145,#102146,#102147,#102148,
#102149,#102150,#102151,#102152,#102153,#102154,#102155,#102156,#102157,
#102158,#102159,#102160,#102161,#102162,#102163,#102164,#102165,#102166,
#102167,#102168,#102169,#102170,#102171,#102172,#102173,#102174),
 .UNSPECIFIED.,.F.,.F.,(4,3,3,3,3,3,3,3,3,3,3,3,3,3,3,3,3,3,3,3,3,3,3,3,
3,3,3,3,3,3,3,3,3,3,3,3,3,3,3,3,3,3,3,3,3,3,3,3,3,3,3,3,3,3,3,3,3,3,3,3,
3,3,3,3,3,3,3,3,3,3,3,3,3,4),(1165.53087448195,1165.61329996591,1165.69566252244,
1165.77799052972,1165.86030294426,1165.94261873174,1166.02495685819,1166.10738217233,
1166.18985705826,1166.27245154326,1166.31051390084,1166.39425261269,1166.47788812405,
1166.56144056745,1166.6449300033,1166.72838395392,1166.81182044776,1166.89525755752,
1166.97871335244,1167.06225784517,1167.14584692811,1167.22957019567,1167.31024991156,
1167.39398862341,1167.47762413477,1167.56117657817,1167.64466601402,1167.72811996464,
1167.81155645848,1167.89499356824,1167.97844936316,1168.06199385589,1168.14558293883,
1168.22930620638,1168.30998592228,1168.39372463413,1168.47736014549,1168.56091258889,
1168.64440202474,1168.72785597536,1168.8112924692,1168.89472957896,1168.97818537388,
1169.0617298666,1169.14531894955,1169.2290422171,1169.309721933,1169.39346064485,
1169.47709615621,1169.56064859961,1169.64413803546,1169.72759198608,1169.81102847992,
1169.89446558968,1169.9779213846,1170.06146587733,1170.14505496027,1170.22877822782,
1170.30945794372,1170.39319665557,1170.47683216693,1170.56038461033,1170.64387404618,
1170.7273279968,1170.81076449064,1170.8942016004,1170.97765739531,1171.06120188804,
1171.14479097098,1171.22851423854,1171.30919395444,1171.3970542314,1171.48472161422,
1171.56372456646),.UNSPECIFIED.);
#795=B_SPLINE_CURVE_WITH_KNOTS('',3,(#102180,#102181,#102182,#102183,#102184,
#102185,#102186,#102187,#102188,#102189,#102190,#102191,#102192,#102193,
#102194,#102195,#102196,#102197,#102198,#102199,#102200,#102201,#102202,
#102203,#102204,#102205,#102206,#102207,#102208,#102209,#102210,#102211,
#102212,#102213,#102214,#102215,#102216,#102217,#102218,#102219,#102220,
#102221,#102222,#102223,#102224,#102225,#102226,#102227,#102228,#102229,
#102230,#102231,#102232,#102233,#102234,#102235,#102236,#102237,#102238,
#102239,#102240,#102241,#102242,#102243,#102244,#102245,#102246,#102247,
#102248,#102249,#102250,#102251,#102252,#102253,#102254,#102255,#102256,
#102257,#102258,#102259,#102260,#102261,#102262,#102263,#102264,#102265,
#102266,#102267,#102268,#102269,#102270,#102271,#102272,#102273,#102274,
#102275,#102276,#102277,#102278,#102279,#102280,#102281,#102282,#102283,
#102284,#102285,#102286,#102287,#102288,#102289,#102290,#102291,#102292,
#102293,#102294,#102295,#102296,#102297,#102298,#102299,#102300,#102301,
#102302,#102303,#102304,#102305,#102306,#102307,#102308,#102309,#102310,
#102311,#102312,#102313,#102314,#102315,#102316,#102317,#102318,#102319,
#102320,#102321,#102322,#102323,#102324,#102325,#102326,#102327,#102328,
#102329,#102330,#102331,#102332,#102333,#102334,#102335,#102336,#102337,
#102338,#102339,#102340,#102341,#102342,#102343,#102344,#102345,#102346,
#102347,#102348,#102349,#102350,#102351,#102352,#102353,#102354,#102355,
#102356,#102357,#102358,#102359,#102360,#102361,#102362,#102363,#102364,
#102365,#102366,#102367,#102368,#102369,#102370,#102371,#102372,#102373,
#102374,#102375,#102376,#102377,#102378,#102379,#102380,#102381,#102382,
#102383,#102384,#102385,#102386,#102387,#102388,#102389,#102390,#102391,
#102392,#102393,#102394,#102395,#102396),.UNSPECIFIED.,.F.,.F.,(4,3,3,3,
3,3,3,3,3,3,3,3,3,3,3,3,3,3,3,3,3,3,3,3,3,3,3,3,3,3,3,3,3,3,3,3,3,3,3,3,
3,3,3,3,3,3,3,3,3,3,3,3,3,3,3,3,3,3,3,3,3,3,3,3,3,3,3,3,3,3,3,3,4),(1171.81405978898,
1171.93948151509,1171.99863934544,1172.08237805729,1172.16601356865,1172.24956601205,
1172.33305544791,1172.41650939852,1172.49994589237,1172.58338300212,1172.66683879704,
1172.75038328977,1172.83397237271,1172.91769564027,1172.99837535616,1173.08211406801,
1173.16574957937,1173.24930202277,1173.33279145862,1173.41624540924,1173.49968190308,
1173.58311901284,1173.66657480776,1173.75011930049,1173.83370838343,1173.91743165098,
1173.99811136688,1174.08185007873,1174.16548559009,1174.24903803349,1174.33252746934,
1174.41598141996,1174.4994179138,1174.58285502356,1174.66631081848,1174.74985531121,
1174.83344439415,1174.9171676617,1174.9978473776,1175.08158608945,1175.16522160081,
1175.24877404421,1175.33226348006,1175.41571743068,1175.49915392452,1175.58259103428,
1175.6660468292,1175.74959132193,1175.83318040487,1175.91690367242,1175.99758338832,
1176.08132210017,1176.16495761153,1176.24851005493,1176.33199949078,1176.4154534414,
1176.49888993524,1176.582327045,1176.66578283992,1176.74932733265,1176.83291641559,
1176.91663968314,1176.99731939904,1177.0810671029,1177.16470960856,1177.24982342642,
1177.33330898385,1177.41675650755,1177.5001840862,1177.5865431025,1177.67001322144,
1177.75781668643,1177.84562015143),.UNSPECIFIED.);
#796=B_SPLINE_CURVE_WITH_KNOTS('',3,(#102397,#102398,#102399,#102400,#102401,
#102402,#102403,#102404,#102405,#102406),.UNSPECIFIED.,.F.,.F.,(4,3,3,4),
(1171.56241306759,1171.64467016677,1171.7293649778,1171.81405978884),
 .UNSPECIFIED.);
#797=B_SPLINE_CURVE_WITH_KNOTS('',3,(#102408,#102409,#102410,#102411,#102412,
#102413,#102414,#102415,#102416,#102417),.UNSPECIFIED.,.F.,.F.,(4,3,3,4),
(1171.56372456646,1171.65113667049,1171.73839544464,1171.81405978898),
 .UNSPECIFIED.);
#798=B_SPLINE_CURVE_WITH_KNOTS('',3,(#102418,#102419,#102420,#102421,#102422,
#102423,#102424,#102425,#102426,#102427,#102428,#102429,#102430,#102431,
#102432,#102433,#102434,#102435,#102436,#102437,#102438,#102439,#102440,
#102441,#102442,#102443,#102444,#102445,#102446,#102447,#102448,#102449,
#102450,#102451,#102452,#102453,#102454,#102455,#102456,#102457,#102458,
#102459,#102460,#102461,#102462,#102463,#102464,#102465,#102466,#102467,
#102468,#102469,#102470,#102471,#102472,#102473,#102474,#102475,#102476,
#102477,#102478,#102479,#102480,#102481,#102482,#102483,#102484,#102485,
#102486,#102487,#102488,#102489,#102490,#102491,#102492,#102493,#102494,
#102495,#102496,#102497,#102498,#102499,#102500,#102501,#102502,#102503,
#102504,#102505,#102506,#102507,#102508,#102509,#102510,#102511,#102512,
#102513,#102514,#102515,#102516,#102517,#102518,#102519,#102520,#102521,
#102522,#102523,#102524,#102525,#102526,#102527,#102528,#102529,#102530,
#102531,#102532,#102533,#102534,#102535,#102536,#102537,#102538,#102539,
#102540,#102541,#102542,#102543,#102544,#102545,#102546,#102547,#102548,
#102549,#102550,#102551,#102552,#102553,#102554,#102555,#102556,#102557,
#102558,#102559,#102560,#102561,#102562,#102563,#102564,#102565,#102566,
#102567,#102568,#102569,#102570,#102571,#102572,#102573,#102574,#102575,
#102576,#102577,#102578,#102579,#102580,#102581,#102582,#102583,#102584,
#102585,#102586,#102587,#102588,#102589,#102590,#102591,#102592,#102593,
#102594,#102595,#102596,#102597,#102598,#102599,#102600,#102601,#102602,
#102603,#102604,#102605,#102606,#102607,#102608,#102609,#102610,#102611,
#102612,#102613,#102614,#102615,#102616,#102617,#102618,#102619,#102620,
#102621,#102622,#102623,#102624,#102625,#102626,#102627,#102628,#102629,
#102630,#102631,#102632,#102633,#102634,#102635,#102636,#102637),
 .UNSPECIFIED.,.F.,.F.,(4,3,3,3,3,3,3,3,3,3,3,3,3,3,3,3,3,3,3,3,3,3,3,3,
3,3,3,3,3,3,3,3,3,3,3,3,3,3,3,3,3,3,3,3,3,3,3,3,3,3,3,3,3,3,3,3,3,3,3,3,
3,3,3,3,3,3,3,3,3,3,3,3,3,4),(1171.81405978909,1171.90164711357,1171.98935633969,
1172.07727908356,1172.1653153844,1172.25355436627,1172.30892996516,1172.39266867701,
1172.47630418837,1172.55985663177,1172.64334606762,1172.72680001824,1172.81023651208,
1172.89367362184,1172.97712941676,1173.06067390949,1173.14426299243,1173.22798625999,
1173.30866597588,1173.39240468773,1173.47604019909,1173.55959264249,1173.64308207834,
1173.72653602896,1173.8099725228,1173.89340963256,1173.97686542748,1174.06040992021,
1174.14399900315,1174.22772227071,1174.3084019866,1174.39214069845,1174.47577620981,
1174.55932865321,1174.64281808906,1174.72627203968,1174.80970853352,1174.89314564328,
1174.97660143819,1175.06014593092,1175.14373501386,1175.22745828142,1175.30813799732,
1175.39187670917,1175.47551222053,1175.55906466393,1175.64255409978,1175.7260080504,
1175.80944454424,1175.892881654,1175.97633744892,1176.05988194165,1176.14347102459,
1176.22719429215,1176.30787400804,1176.39161271989,1176.47524823125,1176.55880067465,
1176.6422901105,1176.72574406112,1176.80918055496,1176.89261766472,1176.97607345964,
1177.05961795236,1177.14320703531,1177.22693030286,1177.30761001876,1177.39015829217,
1177.47261010492,1177.55498463725,1177.63729798293,1177.71957556743,1177.80184708081,
1177.84569864885),.UNSPECIFIED.);
#799=B_SPLINE_CURVE_WITH_KNOTS('',3,(#102643,#102644,#102645,#102646,#102647,
#102648,#102649,#102650,#102651,#102652,#102653,#102654,#102655,#102656,
#102657,#102658,#102659,#102660,#102661,#102662,#102663,#102664,#102665,
#102666,#102667,#102668,#102669,#102670,#102671,#102672,#102673,#102674,
#102675,#102676,#102677,#102678,#102679,#102680,#102681,#102682,#102683,
#102684,#102685,#102686,#102687,#102688,#102689,#102690,#102691,#102692,
#102693,#102694,#102695,#102696,#102697,#102698,#102699,#102700,#102701,
#102702,#102703,#102704,#102705,#102706,#102707,#102708,#102709,#102710,
#102711,#102712,#102713,#102714,#102715,#102716,#102717,#102718,#102719,
#102720,#102721,#102722,#102723,#102724,#102725,#102726,#102727,#102728,
#102729,#102730,#102731,#102732,#102733,#102734,#102735,#102736,#102737,
#102738,#102739,#102740,#102741,#102742,#102743,#102744,#102745,#102746,
#102747,#102748,#102749,#102750,#102751,#102752,#102753,#102754,#102755,
#102756,#102757,#102758,#102759,#102760,#102761,#102762,#102763,#102764,
#102765,#102766,#102767,#102768,#102769,#102770,#102771,#102772,#102773,
#102774,#102775,#102776,#102777,#102778,#102779,#102780,#102781,#102782,
#102783,#102784,#102785,#102786,#102787,#102788,#102789,#102790,#102791,
#102792,#102793,#102794,#102795,#102796,#102797,#102798,#102799,#102800,
#102801,#102802,#102803,#102804,#102805,#102806,#102807,#102808,#102809,
#102810,#102811,#102812,#102813,#102814,#102815,#102816,#102817,#102818,
#102819,#102820,#102821,#102822,#102823,#102824,#102825,#102826,#102827,
#102828,#102829,#102830,#102831,#102832,#102833,#102834,#102835,#102836,
#102837,#102838,#102839,#102840,#102841,#102842,#102843,#102844,#102845,
#102846,#102847,#102848,#102849,#102850,#102851,#102852,#102853,#102854,
#102855,#102856,#102857,#102858,#102859,#102860,#102861,#102862),
 .UNSPECIFIED.,.F.,.F.,(4,3,3,3,3,3,3,3,3,3,3,3,3,3,3,3,3,3,3,3,3,3,3,3,
3,3,3,3,3,3,3,3,3,3,3,3,3,3,3,3,3,3,3,3,3,3,3,3,3,3,3,3,3,3,3,3,3,3,3,3,
3,3,3,3,3,3,3,3,3,3,3,3,3,4),(1178.0972450963,1178.17988444519,1178.26243119773,
1178.34490639929,1178.42733560839,1178.50974134295,1178.59214251743,1178.67455804016,
1178.75705690961,1178.83959806364,1178.92226904614,1178.99679142048,1179.08053013233,
1179.16416564369,1179.24771808709,1179.33120752294,1179.41466147356,1179.4980979674,
1179.58153507716,1179.66499087207,1179.7485353648,1179.83212444774,1179.9158477153,
1179.9965274312,1180.08026614305,1180.16390165441,1180.24745409781,1180.33094353366,
1180.41439748428,1180.49783397812,1180.58127108788,1180.6647268828,1180.74827137553,
1180.83186045847,1180.91558372603,1180.99626344192,1181.08000215377,1181.16363766513,
1181.24719010853,1181.33067954438,1181.414133495,1181.49756998884,1181.5810070986,
1181.66446289352,1181.74800738625,1181.83159646919,1181.91531973674,1181.99599945264,
1182.07973816449,1182.16337367585,1182.24692611925,1182.3304155551,1182.41386950571,
1182.49730599956,1182.58074310932,1182.66419890423,1182.74774339696,1182.8313324799,
1182.91505574746,1182.99573546336,1183.07947417521,1183.16310968657,1183.24666212997,
1183.33015156582,1183.41360551644,1183.49704201028,1183.58047912004,1183.66393491496,
1183.74747940769,1183.83106849063,1183.91479175819,1183.99547147408,1184.08965748669,
1184.13001838411),.UNSPECIFIED.);
#800=B_SPLINE_CURVE_WITH_KNOTS('',3,(#102863,#102864,#102865,#102866,#102867,
#102868,#102869,#102870,#102871,#102872),.UNSPECIFIED.,.F.,.F.,(4,3,3,4),
(1177.84562015143,1177.92934800689,1177.99705540976,1178.09724509616),
 .UNSPECIFIED.);
#801=B_SPLINE_CURVE_WITH_KNOTS('',3,(#102874,#102875,#102876,#102877,#102878,
#102879,#102880,#102881,#102882,#102883),.UNSPECIFIED.,.F.,.F.,(4,3,3,4),
(1177.84569864885,1177.92800237776,1178.01262373689,1178.09724509602),
 .UNSPECIFIED.);
#802=B_SPLINE_CURVE_WITH_KNOTS('',3,(#102884,#102885,#102886,#102887,#102888,
#102889,#102890,#102891,#102892,#102893,#102894,#102895,#102896,#102897,
#102898,#102899,#102900,#102901,#102902,#102903,#102904,#102905,#102906,
#102907,#102908,#102909,#102910,#102911,#102912,#102913,#102914,#102915,
#102916,#102917,#102918,#102919,#102920,#102921,#102922,#102923,#102924,
#102925,#102926,#102927,#102928,#102929,#102930,#102931,#102932,#102933,
#102934,#102935,#102936,#102937,#102938,#102939,#102940,#102941,#102942,
#102943,#102944,#102945,#102946,#102947,#102948,#102949,#102950,#102951,
#102952,#102953,#102954,#102955,#102956,#102957,#102958,#102959,#102960,
#102961,#102962,#102963,#102964,#102965,#102966,#102967,#102968,#102969,
#102970,#102971,#102972,#102973,#102974,#102975,#102976,#102977,#102978,
#102979,#102980,#102981,#102982,#102983,#102984,#102985,#102986,#102987,
#102988,#102989,#102990,#102991,#102992,#102993,#102994,#102995,#102996,
#102997,#102998,#102999,#103000,#103001,#103002,#103003,#103004,#103005,
#103006,#103007,#103008,#103009,#103010,#103011,#103012,#103013,#103014,
#103015,#103016,#103017,#103018,#103019,#103020,#103021,#103022,#103023,
#103024,#103025,#103026,#103027,#103028,#103029,#103030,#103031,#103032,
#103033,#103034,#103035,#103036,#103037,#103038,#103039,#103040,#103041,
#103042,#103043,#103044,#103045,#103046,#103047,#103048,#103049,#103050,
#103051,#103052,#103053,#103054,#103055,#103056,#103057,#103058,#103059,
#103060,#103061,#103062,#103063,#103064,#103065,#103066,#103067,#103068,
#103069,#103070,#103071,#103072,#103073,#103074,#103075,#103076,#103077,
#103078,#103079,#103080,#103081,#103082,#103083,#103084,#103085,#103086,
#103087,#103088,#103089,#103090,#103091,#103092,#103093,#103094,#103095,
#103096,#103097,#103098,#103099,#103100),.UNSPECIFIED.,.F.,.F.,(4,3,3,3,
3,3,3,3,3,3,3,3,3,3,3,3,3,3,3,3,3,3,3,3,3,3,3,3,3,3,3,3,3,3,3,3,3,3,3,3,
3,3,3,3,3,3,3,3,3,3,3,3,3,3,3,3,3,3,3,3,3,3,3,3,3,3,3,3,3,3,3,3,4),(1178.09724509616,
1178.2145451453,1178.30734602948,1178.39108474133,1178.47472025269,1178.55827269609,
1178.64176213194,1178.72521608256,1178.8086525764,1178.89208968616,1178.97554548108,
1179.0590899738,1179.14267905675,1179.2264023243,1179.3070820402,1179.39082075205,
1179.47445626341,1179.55800870681,1179.64149814266,1179.72495209328,1179.80838858712,
1179.89182569688,1179.9752814918,1180.05882598453,1180.14241506747,1180.22613833502,
1180.30681805092,1180.39055676277,1180.47419227413,1180.55774471753,1180.64123415338,
1180.724688104,1180.80812459784,1180.8915617076,1180.97501750252,1181.05856199525,
1181.14215107819,1181.22587434574,1181.30655406164,1181.39029277349,1181.47392828485,
1181.55748072825,1181.6409701641,1181.72442411472,1181.80786060856,1181.89129771832,
1181.97475351324,1182.05829800597,1182.14188708891,1182.22561035646,1182.30629007236,
1182.39002878421,1182.47366429557,1182.55721673897,1182.64070617482,1182.72416012544,
1182.80759661928,1182.89103372904,1182.97448952396,1183.05803401669,1183.14162309963,
1183.22534636718,1183.30602608308,1183.38977540495,1183.47341919148,1183.55696249768,
1183.64044883304,1183.72389631705,1183.80732303918,1183.89077497528,1183.97423771784,
1184.05777403475,1184.1287772547),.UNSPECIFIED.);
#803=B_SPLINE_CURVE_WITH_KNOTS('',3,(#103106,#103107,#103108,#103109,#103110,
#103111,#103112,#103113,#103114,#103115,#103116,#103117,#103118,#103119,
#103120,#103121,#103122,#103123,#103124,#103125,#103126,#103127,#103128,
#103129,#103130,#103131,#103132,#103133,#103134,#103135,#103136,#103137,
#103138,#103139,#103140,#103141,#103142,#103143,#103144,#103145,#103146,
#103147,#103148,#103149,#103150,#103151,#103152,#103153,#103154,#103155,
#103156,#103157,#103158,#103159,#103160,#103161,#103162,#103163,#103164,
#103165,#103166,#103167,#103168,#103169,#103170,#103171,#103172,#103173,
#103174,#103175,#103176,#103177,#103178,#103179,#103180,#103181,#103182,
#103183,#103184,#103185,#103186,#103187,#103188,#103189,#103190,#103191,
#103192,#103193,#103194,#103195,#103196,#103197,#103198,#103199,#103200,
#103201,#103202,#103203,#103204,#103205,#103206,#103207,#103208,#103209,
#103210,#103211,#103212,#103213,#103214,#103215,#103216,#103217,#103218,
#103219,#103220,#103221,#103222,#103223,#103224,#103225,#103226,#103227,
#103228,#103229,#103230,#103231,#103232,#103233,#103234,#103235,#103236,
#103237,#103238,#103239,#103240,#103241,#103242,#103243,#103244,#103245,
#103246,#103247,#103248,#103249,#103250,#103251,#103252,#103253,#103254,
#103255,#103256,#103257,#103258,#103259,#103260,#103261,#103262,#103263,
#103264,#103265,#103266,#103267,#103268,#103269,#103270,#103271,#103272,
#103273,#103274,#103275,#103276,#103277,#103278,#103279,#103280,#103281,
#103282,#103283,#103284,#103285,#103286,#103287,#103288,#103289,#103290,
#103291,#103292,#103293,#103294,#103295,#103296,#103297,#103298,#103299,
#103300,#103301,#103302,#103303,#103304,#103305,#103306,#103307,#103308,
#103309,#103310,#103311,#103312,#103313,#103314,#103315,#103316,#103317,
#103318,#103319,#103320,#103321,#103322,#103323,#103324,#103325),
 .UNSPECIFIED.,.F.,.F.,(4,3,3,3,3,3,3,3,3,3,3,3,3,3,3,3,3,3,3,3,3,3,3,3,
3,3,3,3,3,3,3,3,3,3,3,3,3,3,3,3,3,3,3,3,3,3,3,3,3,3,3,3,3,3,3,3,3,3,3,3,
3,3,3,3,3,3,3,3,3,3,3,3,3,4),(1184.38043040334,1184.46468568474,1184.54895401794,
1184.63325228744,1184.71759739402,1184.80205716788,1184.8865841838,1184.97124381791,
1184.9952074848,1185.07894619665,1185.16258170801,1185.24613415141,1185.32962358726,
1185.41307753788,1185.49651403172,1185.57995114148,1185.66340693639,1185.74695142912,
1185.83054051206,1185.91426377962,1185.99494349552,1186.07868220737,1186.16231771873,
1186.24587016213,1186.32935959798,1186.4128135486,1186.49625004244,1186.5796871522,
1186.66314294712,1186.74668743985,1186.83027652279,1186.91399979035,1186.99467950624,
1187.07841821809,1187.16205372945,1187.24560617285,1187.3290956087,1187.41254955932,
1187.49598605316,1187.57942316292,1187.66287895783,1187.74642345056,1187.8300125335,
1187.91373580106,1187.99441551696,1188.07815422881,1188.16178974018,1188.24534218357,
1188.32883161943,1188.41228557004,1188.49572206389,1188.57915917364,1188.66261496856,
1188.74615946129,1188.82974854423,1188.91347181179,1188.99415152768,1189.07789023953,
1189.16152575089,1189.24507819429,1189.32856763014,1189.41202158076,1189.4954580746,
1189.57889518436,1189.66235097928,1189.74589547201,1189.82948455495,1189.91320782251,
1189.99388753841,1190.0775495013,1190.16132819585,1190.24477987203,1190.32872207577,
1190.41266427951),.UNSPECIFIED.);
#804=B_SPLINE_CURVE_WITH_KNOTS('',3,(#103326,#103327,#103328,#103329,#103330,
#103331,#103332,#103333,#103334,#103335),.UNSPECIFIED.,.F.,.F.,(4,3,3,4),
(1184.13001838411,1184.22369930359,1184.31687370656,1184.38043040315),
 .UNSPECIFIED.);
#805=B_SPLINE_CURVE_WITH_KNOTS('',3,(#103337,#103338,#103339,#103340,#103341,
#103342,#103343,#103344,#103345,#103346,#103347,#103348,#103349),
 .UNSPECIFIED.,.F.,.F.,(4,3,3,3,4),(1184.1287772547,1184.21241699627,1184.29617130262,
1184.3057620938,1184.38043040334),.UNSPECIFIED.);
#806=B_SPLINE_CURVE_WITH_KNOTS('',3,(#103350,#103351,#103352,#103353,#103354,
#103355,#103356,#103357,#103358,#103359,#103360,#103361,#103362,#103363,
#103364,#103365,#103366,#103367,#103368,#103369,#103370,#103371,#103372,
#103373,#103374,#103375,#103376,#103377,#103378,#103379,#103380,#103381,
#103382,#103383,#103384,#103385,#103386,#103387,#103388,#103389,#103390,
#103391,#103392,#103393,#103394,#103395,#103396,#103397,#103398,#103399,
#103400,#103401,#103402,#103403,#103404,#103405,#103406,#103407,#103408,
#103409,#103410,#103411,#103412,#103413,#103414,#103415,#103416,#103417,
#103418,#103419,#103420,#103421,#103422,#103423,#103424,#103425,#103426,
#103427,#103428,#103429,#103430,#103431,#103432,#103433,#103434,#103435,
#103436,#103437,#103438,#103439,#103440,#103441,#103442,#103443,#103444,
#103445,#103446,#103447,#103448,#103449,#103450,#103451,#103452,#103453,
#103454,#103455,#103456,#103457,#103458,#103459,#103460,#103461,#103462,
#103463,#103464,#103465,#103466,#103467,#103468,#103469,#103470,#103471,
#103472,#103473,#103474,#103475,#103476,#103477,#103478,#103479,#103480,
#103481,#103482,#103483,#103484,#103485,#103486,#103487,#103488,#103489,
#103490,#103491,#103492,#103493,#103494,#103495,#103496,#103497,#103498,
#103499,#103500,#103501,#103502,#103503,#103504,#103505,#103506,#103507,
#103508,#103509,#103510,#103511,#103512,#103513,#103514,#103515,#103516,
#103517,#103518,#103519,#103520,#103521,#103522,#103523,#103524,#103525,
#103526,#103527,#103528,#103529,#103530,#103531,#103532,#103533,#103534,
#103535,#103536,#103537,#103538,#103539,#103540,#103541,#103542,#103543,
#103544,#103545,#103546,#103547,#103548,#103549,#103550,#103551,#103552,
#103553,#103554,#103555,#103556,#103557,#103558,#103559,#103560,#103561,
#103562,#103563,#103564,#103565,#103566,#103567,#103568,#103569,#103570,
#103571,#103572),.UNSPECIFIED.,.F.,.F.,(4,3,3,3,3,3,3,3,3,3,3,3,3,3,3,3,
3,3,3,3,3,3,3,3,3,3,3,3,3,3,3,3,3,3,3,3,3,3,3,3,3,3,3,3,3,3,3,3,3,3,3,3,
3,3,3,3,3,3,3,3,3,3,3,3,3,3,3,3,3,3,3,3,3,3,4),(1184.38043040347,1184.46326953669,
1184.54601184595,1184.6286782553,1184.71328073646,1184.7958670911,1184.87844507109,
1184.96103346495,1185.04714962484,1185.12986035915,1185.21262722398,1185.29550712489,
1185.30549810452,1185.38923681637,1185.47287232773,1185.55642477113,1185.63991420698,
1185.7233681576,1185.80680465144,1185.8902417612,1185.97369755612,1186.05724204884,
1186.14083113179,1186.22455439934,1186.30523411524,1186.38897282709,1186.47260833845,
1186.55616078185,1186.6396502177,1186.72310416832,1186.80654066216,1186.88997777192,
1186.97343356684,1187.05697805957,1187.14056714251,1187.22429041006,1187.30497012596,
1187.38870883781,1187.47234434917,1187.55589679257,1187.63938622842,1187.72284017904,
1187.80627667288,1187.88971378264,1187.97316957756,1188.05671407029,1188.14030315323,
1188.22402642078,1188.30470613668,1188.38844484853,1188.47208035989,1188.55563280329,
1188.63912223914,1188.72257618976,1188.8060126836,1188.88944979336,1188.97290558827,
1189.056450081,1189.14003916395,1189.2237624315,1189.3044421474,1189.38818085925,
1189.47181637061,1189.55536881401,1189.63885824986,1189.72231220048,1189.80574869432,
1189.88918580408,1189.97264159899,1190.05618609172,1190.13977517467,1190.22349844222,
1190.30417815812,1190.40038519419,1190.41311890016),.UNSPECIFIED.);
#807=B_SPLINE_CURVE_WITH_KNOTS('',3,(#103578,#103579,#103580,#103581,#103582,
#103583,#103584,#103585,#103586,#103587,#103588,#103589,#103590,#103591,
#103592,#103593,#103594,#103595,#103596,#103597,#103598,#103599,#103600,
#103601,#103602,#103603,#103604,#103605,#103606,#103607,#103608,#103609,
#103610,#103611,#103612,#103613,#103614,#103615,#103616,#103617,#103618,
#103619,#103620,#103621,#103622,#103623,#103624,#103625,#103626,#103627,
#103628,#103629,#103630,#103631,#103632,#103633,#103634,#103635,#103636,
#103637,#103638,#103639,#103640,#103641,#103642,#103643,#103644,#103645,
#103646,#103647,#103648,#103649,#103650,#103651,#103652,#103653,#103654,
#103655,#103656,#103657,#103658,#103659,#103660,#103661,#103662,#103663,
#103664,#103665,#103666,#103667,#103668,#103669,#103670,#103671,#103672,
#103673,#103674,#103675,#103676,#103677,#103678,#103679,#103680,#103681,
#103682,#103683,#103684,#103685,#103686,#103687,#103688,#103689,#103690,
#103691,#103692,#103693,#103694,#103695,#103696,#103697,#103698,#103699,
#103700,#103701,#103702,#103703,#103704,#103705,#103706,#103707,#103708,
#103709,#103710,#103711,#103712,#103713,#103714,#103715,#103716,#103717,
#103718,#103719,#103720,#103721,#103722,#103723,#103724,#103725,#103726,
#103727,#103728,#103729,#103730,#103731,#103732,#103733,#103734,#103735,
#103736,#103737,#103738,#103739,#103740,#103741,#103742,#103743,#103744,
#103745,#103746,#103747,#103748,#103749,#103750,#103751,#103752,#103753,
#103754,#103755,#103756,#103757,#103758,#103759,#103760,#103761,#103762,
#103763,#103764,#103765,#103766,#103767,#103768,#103769,#103770,#103771,
#103772,#103773,#103774,#103775,#103776,#103777,#103778,#103779,#103780,
#103781,#103782,#103783,#103784,#103785,#103786,#103787,#103788,#103789,
#103790,#103791,#103792,#103793,#103794,#103795,#103796,#103797),
 .UNSPECIFIED.,.F.,.F.,(4,3,3,3,3,3,3,3,3,3,3,3,3,3,3,3,3,3,3,3,3,3,3,3,
3,3,3,3,3,3,3,3,3,3,3,3,3,3,3,3,3,3,3,3,3,3,3,3,3,3,3,3,3,3,3,3,3,3,3,3,
3,3,3,3,3,3,3,3,3,3,3,3,3,4),(1190.66361571069,1190.76115270768,1190.85929214592,
1190.95812771467,1190.99362354913,1191.07736226098,1191.16099777234,1191.24455021574,
1191.32803965159,1191.41149360221,1191.49493009605,1191.57836720581,1191.66182300073,
1191.74536749346,1191.8289565764,1191.91267984396,1191.99335955985,1192.0770982717,
1192.16073378306,1192.24428622646,1192.32777566231,1192.41122961292,1192.49466610677,
1192.57810321653,1192.66155901144,1192.74510350417,1192.82869258711,1192.91241585467,
1192.99309557057,1193.07683428242,1193.16046979378,1193.24402223718,1193.32751167303,
1193.41096562365,1193.49440211749,1193.57783922725,1193.66129502217,1193.7448395149,
1193.82842859784,1193.91215186539,1193.99283158129,1194.07657029314,1194.1602058045,
1194.2437582479,1194.32724768375,1194.41070163437,1194.49413812821,1194.57757523797,
1194.66103103289,1194.74457552562,1194.82816460856,1194.91188787612,1194.99256759201,
1195.07630630386,1195.15994181522,1195.24349425862,1195.32698369447,1195.41043764509,
1195.49387413893,1195.57731124869,1195.6607670436,1195.74431153633,1195.82790061927,
1195.91162388683,1195.99230360273,1196.07546835843,1196.15850180246,1196.24145939585,
1196.32435982013,1196.40722171057,1196.49007873684,1196.57293247362,1196.65582636887,
1196.69500507576),.UNSPECIFIED.);
#808=B_SPLINE_CURVE_WITH_KNOTS('',3,(#103798,#103799,#103800,#103801,#103802,
#103803,#103804,#103805,#103806,#103807),.UNSPECIFIED.,.F.,.F.,(4,3,3,4),
(1190.41266427951,1190.49598634203,1190.57980102627,1190.66361571051),
 .UNSPECIFIED.);
#809=B_SPLINE_CURVE_WITH_KNOTS('',3,(#103809,#103810,#103811,#103812,#103813,
#103814,#103815,#103816,#103817,#103818),.UNSPECIFIED.,.F.,.F.,(4,3,3,4),
(1190.41311890016,1190.50877424335,1190.60377587554,1190.66361571032),
 .UNSPECIFIED.);
#810=B_SPLINE_CURVE_WITH_KNOTS('',3,(#103819,#103820,#103821,#103822,#103823,
#103824,#103825,#103826,#103827,#103828,#103829,#103830,#103831,#103832,
#103833,#103834,#103835,#103836,#103837,#103838,#103839,#103840,#103841,
#103842,#103843,#103844,#103845,#103846,#103847,#103848,#103849,#103850,
#103851,#103852,#103853,#103854,#103855,#103856,#103857,#103858,#103859,
#103860,#103861,#103862,#103863,#103864,#103865,#103866,#103867,#103868,
#103869,#103870,#103871,#103872,#103873,#103874,#103875,#103876,#103877,
#103878,#103879,#103880,#103881,#103882,#103883,#103884,#103885,#103886,
#103887,#103888,#103889,#103890,#103891,#103892,#103893,#103894,#103895,
#103896,#103897,#103898,#103899,#103900,#103901,#103902,#103903,#103904,
#103905,#103906,#103907,#103908,#103909,#103910,#103911,#103912,#103913,
#103914,#103915,#103916,#103917,#103918,#103919,#103920,#103921,#103922,
#103923,#103924,#103925,#103926,#103927,#103928,#103929,#103930,#103931,
#103932,#103933,#103934,#103935,#103936,#103937,#103938,#103939,#103940,
#103941,#103942,#103943,#103944,#103945,#103946,#103947,#103948,#103949,
#103950,#103951,#103952,#103953,#103954,#103955,#103956,#103957,#103958,
#103959,#103960,#103961,#103962,#103963,#103964,#103965,#103966,#103967,
#103968,#103969,#103970,#103971,#103972,#103973,#103974,#103975,#103976,
#103977,#103978,#103979,#103980,#103981,#103982,#103983,#103984,#103985,
#103986,#103987,#103988,#103989,#103990,#103991,#103992,#103993,#103994,
#103995,#103996,#103997,#103998,#103999,#104000,#104001,#104002,#104003,
#104004,#104005,#104006,#104007,#104008,#104009,#104010,#104011,#104012,
#104013,#104014,#104015,#104016,#104017,#104018,#104019,#104020,#104021,
#104022,#104023,#104024,#104025,#104026,#104027,#104028,#104029,#104030,
#104031,#104032,#104033,#104034,#104035,#104036,#104037,#104038),
 .UNSPECIFIED.,.F.,.F.,(4,3,3,3,3,3,3,3,3,3,3,3,3,3,3,3,3,3,3,3,3,3,3,3,
3,3,3,3,3,3,3,3,3,3,3,3,3,3,3,3,3,3,3,3,3,3,3,3,3,3,3,3,3,3,3,3,3,3,3,3,
3,3,3,3,3,3,3,3,3,3,3,3,3,4),(1190.66361571052,1190.74740518355,1190.83119373716,
1190.91499893557,1190.99883834989,1191.08278235671,1191.16678368594,1191.2509212756,
1191.30391416884,1191.38765288069,1191.47128839205,1191.55484083545,1191.6383302713,
1191.72178422192,1191.80522071576,1191.88865782552,1191.97211362043,1192.05565811316,
1192.1392471961,1192.22297046366,1192.30365017956,1192.38738889141,1192.47102440277,
1192.55457684617,1192.63806628202,1192.72152023264,1192.80495672648,1192.88839383624,
1192.97184963116,1193.05539412389,1193.13898320683,1193.22270647438,1193.30338619028,
1193.38712490213,1193.47076041349,1193.55431285689,1193.63780229274,1193.72125624336,
1193.8046927372,1193.88812984696,1193.97158564188,1194.05513013461,1194.13871921755,
1194.2224424851,1194.303122201,1194.38686091285,1194.47049642421,1194.55404886761,
1194.63753830346,1194.72099225408,1194.80442874792,1194.88786585768,1194.97132165259,
1195.05486614532,1195.13845522826,1195.22217849582,1195.30285821172,1195.38659692357,
1195.47023243493,1195.55378487833,1195.63727431418,1195.7207282648,1195.80416475864,
1195.8876018684,1195.97105766332,1196.05460215605,1196.13819123899,1196.22191450655,
1196.30259422244,1196.38668110687,1196.47062918338,1196.55449738112,1196.63829047945,
1196.69597830305),.UNSPECIFIED.);
#811=B_SPLINE_CURVE_WITH_KNOTS('',3,(#104044,#104045,#104046,#104047,#104048,
#104049,#104050,#104051,#104052,#104053,#104054,#104055,#104056,#104057,
#104058,#104059,#104060,#104061,#104062,#104063,#104064,#104065,#104066,
#104067,#104068,#104069,#104070,#104071,#104072,#104073,#104074,#104075,
#104076,#104077,#104078,#104079,#104080,#104081,#104082,#104083,#104084,
#104085,#104086,#104087,#104088,#104089,#104090,#104091,#104092,#104093,
#104094,#104095,#104096,#104097,#104098,#104099,#104100,#104101,#104102,
#104103,#104104,#104105,#104106,#104107,#104108,#104109,#104110,#104111,
#104112,#104113,#104114,#104115,#104116,#104117,#104118,#104119,#104120,
#104121,#104122,#104123,#104124,#104125,#104126,#104127,#104128,#104129,
#104130,#104131,#104132,#104133,#104134,#104135,#104136,#104137,#104138,
#104139,#104140,#104141,#104142,#104143,#104144,#104145,#104146,#104147,
#104148,#104149,#104150,#104151,#104152,#104153,#104154,#104155,#104156,
#104157,#104158,#104159,#104160,#104161,#104162,#104163,#104164,#104165,
#104166,#104167,#104168,#104169,#104170,#104171,#104172,#104173,#104174,
#104175,#104176,#104177,#104178,#104179,#104180,#104181,#104182,#104183,
#104184,#104185,#104186,#104187,#104188,#104189,#104190,#104191,#104192,
#104193,#104194,#104195,#104196,#104197,#104198,#104199,#104200,#104201,
#104202,#104203,#104204,#104205,#104206,#104207,#104208,#104209,#104210,
#104211,#104212,#104213,#104214,#104215,#104216,#104217,#104218,#104219,
#104220,#104221,#104222,#104223,#104224,#104225,#104226,#104227,#104228,
#104229,#104230,#104231,#104232,#104233,#104234,#104235,#104236,#104237,
#104238,#104239,#104240,#104241,#104242,#104243,#104244,#104245,#104246,
#104247,#104248,#104249,#104250,#104251,#104252,#104253,#104254,#104255,
#104256,#104257,#104258,#104259,#104260,#104261,#104262,#104263),
 .UNSPECIFIED.,.F.,.F.,(4,3,3,3,3,3,3,3,3,3,3,3,3,3,3,3,3,3,3,3,3,3,3,3,
3,3,3,3,3,3,3,3,3,3,3,3,3,3,3,3,3,3,3,3,3,3,3,3,3,3,3,3,3,3,3,3,3,3,3,3,
3,3,3,3,3,3,3,3,3,3,3,3,3,4),(1196.94680101769,1196.99203961345,1197.0757783253,
1197.15941383666,1197.24296628006,1197.32645571591,1197.40990966653,1197.49334616037,
1197.57678327013,1197.66023906505,1197.74378355778,1197.82737264072,1197.91109590827,
1197.99177562417,1198.07551433602,1198.15914984738,1198.24270229078,1198.32619172663,
1198.40964567724,1198.49308217109,1198.57651928085,1198.65997507576,1198.74351956849,
1198.82710865143,1198.91083191899,1198.99151163489,1199.07525034674,1199.1588858581,
1199.2424383015,1199.32592773735,1199.40938168797,1199.49281818181,1199.57625529157,
1199.65971108649,1199.74325557922,1199.82684466216,1199.91056792971,1199.99124764561,
1200.07498635746,1200.15862186882,1200.24217431222,1200.32566374807,1200.40911769869,
1200.49255419253,1200.57599130229,1200.65944709721,1200.74299158994,1200.82658067288,
1200.91030394043,1200.99098365633,1201.07472236818,1201.15835787954,1201.24191032294,
1201.32539975879,1201.40885370941,1201.49229020326,1201.57572731301,1201.65918310793,
1201.74272760066,1201.8263166836,1201.91003995116,1201.99071966705,1202.07445903175,
1202.15809504291,1202.2416478337,1202.32513746501,1202.40859081949,1202.49202650081,
1202.57546258152,1202.65891713051,1202.74245734764,1202.82604206555,1202.90975380982,
1202.97885099659),.UNSPECIFIED.);
#812=B_SPLINE_CURVE_WITH_KNOTS('',3,(#104264,#104265,#104266,#104267,#104268,
#104269,#104270,#104271,#104272,#104273),.UNSPECIFIED.,.F.,.F.,(4,3,3,4),
(1196.69500507576,1196.7779925456,1196.86239678155,1196.9468010175),
 .UNSPECIFIED.);
#813=B_SPLINE_CURVE_WITH_KNOTS('',3,(#104275,#104276,#104277,#104278,#104279,
#104280,#104281,#104282,#104283,#104284),.UNSPECIFIED.,.F.,.F.,(4,3,3,4),
(1196.69597830305,1196.77970345289,1196.86342983331,1196.9468010177),
 .UNSPECIFIED.);
#814=B_SPLINE_CURVE_WITH_KNOTS('',3,(#104285,#104286,#104287,#104288,#104289,
#104290,#104291,#104292,#104293,#104294,#104295,#104296,#104297,#104298,
#104299,#104300,#104301,#104302,#104303,#104304,#104305,#104306,#104307,
#104308,#104309,#104310,#104311,#104312,#104313,#104314,#104315,#104316,
#104317,#104318,#104319,#104320,#104321,#104322,#104323,#104324,#104325,
#104326,#104327,#104328,#104329,#104330,#104331,#104332,#104333,#104334,
#104335,#104336,#104337,#104338,#104339,#104340,#104341,#104342,#104343,
#104344,#104345,#104346,#104347,#104348,#104349,#104350,#104351,#104352,
#104353,#104354,#104355,#104356,#104357,#104358,#104359,#104360,#104361,
#104362,#104363,#104364,#104365,#104366,#104367,#104368,#104369,#104370,
#104371,#104372,#104373,#104374,#104375,#104376,#104377,#104378,#104379,
#104380,#104381,#104382,#104383,#104384,#104385,#104386,#104387,#104388,
#104389,#104390,#104391,#104392,#104393,#104394,#104395,#104396,#104397,
#104398,#104399,#104400,#104401,#104402,#104403,#104404,#104405,#104406,
#104407,#104408,#104409,#104410,#104411,#104412,#104413,#104414,#104415,
#104416,#104417,#104418,#104419,#104420,#104421,#104422,#104423,#104424,
#104425,#104426,#104427,#104428,#104429,#104430,#104431,#104432,#104433,
#104434,#104435,#104436,#104437,#104438,#104439,#104440,#104441,#104442,
#104443,#104444,#104445,#104446,#104447,#104448,#104449,#104450,#104451,
#104452,#104453,#104454,#104455,#104456,#104457,#104458,#104459,#104460,
#104461,#104462,#104463,#104464,#104465,#104466,#104467,#104468,#104469,
#104470,#104471,#104472,#104473,#104474,#104475,#104476,#104477,#104478,
#104479,#104480,#104481,#104482,#104483,#104484,#104485,#104486,#104487,
#104488,#104489,#104490,#104491,#104492,#104493,#104494,#104495,#104496,
#104497,#104498,#104499,#104500,#104501,#104502,#104503,#104504),
 .UNSPECIFIED.,.F.,.F.,(4,3,3,3,3,3,3,3,3,3,3,3,3,3,3,3,3,3,3,3,3,3,3,3,
3,3,3,3,3,3,3,3,3,3,3,3,3,3,3,3,3,3,3,3,3,3,3,3,3,3,3,3,3,3,3,3,3,3,3,3,
3,3,3,3,3,3,3,3,3,3,3,3,3,4),(1196.9468010179,1197.04218345801,1197.13801352799,
1197.23442780283,1197.30233023316,1197.38606894501,1197.46970445637,1197.55325689977,
1197.63674633562,1197.72020028624,1197.80363678008,1197.88707388984,1197.97052968476,
1198.05407417749,1198.13766326043,1198.22138652798,1198.30206624388,1198.38580495573,
1198.46944046709,1198.55299291049,1198.63648234634,1198.71993629696,1198.8033727908,
1198.88680990056,1198.97026569548,1199.05381018821,1199.13739927115,1199.22112253871,
1199.3018022546,1199.38554096645,1199.46917647781,1199.55272892121,1199.63621835706,
1199.71967230768,1199.80310880152,1199.88654591128,1199.9700017062,1200.05354619893,
1200.13713528187,1200.22085854942,1200.30153826532,1200.38527697717,1200.46891248853,
1200.55246493193,1200.63595436778,1200.7194083184,1200.80284481224,1200.886281922,
1200.96973771691,1201.05328220964,1201.13687129258,1201.22059456014,1201.30127427604,
1201.38501298789,1201.46864849925,1201.55220094265,1201.6356903785,1201.71914432912,
1201.80258082296,1201.88601793272,1201.96947372764,1202.05301822037,1202.13660730331,
1202.22033057087,1202.30101028676,1202.38565335764,1202.46843821106,1202.55114785557,
1202.63380115682,1202.71988958105,1202.80249905388,1202.88510732086,1202.96774973769,
1202.97815485377),.UNSPECIFIED.);
#815=B_SPLINE_CURVE_WITH_KNOTS('',3,(#104510,#104511,#104512,#104513,#104514,
#104515,#104516,#104517,#104518,#104519,#104520,#104521,#104522,#104523,
#104524,#104525,#104526,#104527,#104528,#104529,#104530,#104531,#104532,
#104533,#104534,#104535,#104536,#104537,#104538,#104539,#104540,#104541,
#104542,#104543,#104544,#104545,#104546,#104547,#104548,#104549,#104550,
#104551,#104552,#104553,#104554,#104555,#104556,#104557,#104558,#104559,
#104560,#104561,#104562,#104563,#104564,#104565,#104566,#104567,#104568,
#104569,#104570,#104571,#104572,#104573,#104574,#104575,#104576,#104577,
#104578,#104579,#104580,#104581,#104582,#104583,#104584,#104585,#104586,
#104587,#104588,#104589,#104590,#104591,#104592,#104593,#104594,#104595,
#104596,#104597,#104598,#104599,#104600,#104601,#104602,#104603,#104604,
#104605,#104606,#104607,#104608,#104609,#104610,#104611,#104612,#104613,
#104614,#104615,#104616,#104617,#104618,#104619,#104620,#104621,#104622,
#104623,#104624,#104625,#104626,#104627,#104628,#104629,#104630,#104631,
#104632,#104633,#104634,#104635,#104636,#104637,#104638,#104639,#104640,
#104641,#104642,#104643,#104644,#104645,#104646,#104647,#104648,#104649,
#104650,#104651,#104652,#104653,#104654,#104655,#104656,#104657,#104658,
#104659,#104660,#104661,#104662,#104663,#104664,#104665,#104666,#104667,
#104668,#104669,#104670,#104671,#104672,#104673,#104674,#104675,#104676,
#104677,#104678,#104679,#104680,#104681,#104682,#104683,#104684,#104685,
#104686,#104687,#104688,#104689,#104690,#104691,#104692,#104693,#104694,
#104695,#104696,#104697,#104698,#104699,#104700,#104701,#104702,#104703,
#104704,#104705,#104706,#104707,#104708,#104709,#104710,#104711,#104712,
#104713,#104714,#104715,#104716,#104717,#104718,#104719,#104720,#104721,
#104722,#104723,#104724,#104725,#104726,#104727,#104728,#104729,#104730,
#104731,#104732),.UNSPECIFIED.,.F.,.F.,(4,3,3,3,3,3,3,3,3,3,3,3,3,3,3,3,
3,3,3,3,3,3,3,3,3,3,3,3,3,3,3,3,3,3,3,3,3,3,3,3,3,3,3,3,3,3,3,3,3,3,3,3,
3,3,3,3,3,3,3,3,3,3,3,3,3,3,3,3,3,3,3,3,3,3,4),(1203.22998632487,1203.31249181929,
1203.39720430294,1203.479626139,1203.56203843911,1203.64446010042,1203.73089299743,
1203.81343567372,1203.8960339351,1203.9787454899,1203.99019168849,1204.07393040034,
1204.1575659117,1204.2411183551,1204.32460779095,1204.40806174157,1204.49149823541,
1204.57493534517,1204.65839114009,1204.74193563282,1204.82552471576,1204.90924798332,
1204.98992769921,1205.07366641106,1205.15730192242,1205.24085436582,1205.32434380167,
1205.40779775229,1205.49123424613,1205.57467135589,1205.6581271508,1205.74167164353,
1205.82526072647,1205.90898399403,1205.98966370993,1206.07340242178,1206.15703793314,
1206.24059037654,1206.32407981239,1206.40753376301,1206.49097025685,1206.57440736661,
1206.65786316153,1206.74140765426,1206.8249967372,1206.90872000475,1206.98939972065,
1207.0731384325,1207.15677394386,1207.24032638726,1207.32381582311,1207.40726977373,
1207.49070626757,1207.57414337733,1207.65759917225,1207.74114366498,1207.82473274792,
1207.90845601548,1207.98913573137,1208.07287444322,1208.15650995458,1208.24006239798,
1208.32355183383,1208.40700578445,1208.49044227829,1208.57387938805,1208.65733518297,
1208.74087967569,1208.82446875864,1208.90819202619,1208.98887174209,1209.07601691819,
1209.16303876864,1209.24991487978,1209.26279998827),.UNSPECIFIED.);
#816=B_SPLINE_CURVE_WITH_KNOTS('',3,(#104733,#104734,#104735,#104736,#104737,
#104738,#104739,#104740,#104741,#104742,#104743,#104744,#104745),
 .UNSPECIFIED.,.F.,.F.,(4,3,3,3,4),(1202.97885099659,1202.99045567777,1203.10238395014,
1203.21150545175,1203.22998632473),.UNSPECIFIED.);
#817=B_SPLINE_CURVE_WITH_KNOTS('',3,(#104747,#104748,#104749,#104750,#104751,
#104752,#104753,#104754,#104755,#104756),.UNSPECIFIED.,.F.,.F.,(4,3,3,4),
(1202.97815485377,1203.06088400365,1203.14543516421,1203.22998632476),
 .UNSPECIFIED.);
#818=B_SPLINE_CURVE_WITH_KNOTS('',3,(#104757,#104758,#104759,#104760,#104761,
#104762,#104763,#104764,#104765,#104766,#104767,#104768,#104769,#104770,
#104771,#104772,#104773,#104774,#104775,#104776,#104777,#104778,#104779,
#104780,#104781,#104782,#104783,#104784,#104785,#104786,#104787,#104788,
#104789,#104790,#104791,#104792,#104793,#104794,#104795,#104796,#104797,
#104798,#104799,#104800,#104801,#104802,#104803,#104804,#104805,#104806,
#104807,#104808,#104809,#104810,#104811,#104812,#104813,#104814,#104815,
#104816,#104817,#104818,#104819,#104820,#104821,#104822,#104823,#104824,
#104825,#104826,#104827,#104828,#104829,#104830,#104831,#104832,#104833,
#104834,#104835,#104836,#104837,#104838,#104839,#104840,#104841,#104842,
#104843,#104844,#104845,#104846,#104847,#104848,#104849,#104850,#104851,
#104852,#104853,#104854,#104855,#104856,#104857,#104858,#104859,#104860,
#104861,#104862,#104863,#104864,#104865,#104866,#104867,#104868,#104869,
#104870,#104871,#104872,#104873,#104874,#104875,#104876,#104877,#104878,
#104879,#104880,#104881,#104882,#104883,#104884,#104885,#104886,#104887,
#104888,#104889,#104890,#104891,#104892,#104893,#104894,#104895,#104896,
#104897,#104898,#104899,#104900,#104901,#104902,#104903,#104904,#104905,
#104906,#104907,#104908,#104909,#104910,#104911,#104912,#104913,#104914,
#104915,#104916,#104917,#104918,#104919,#104920,#104921,#104922,#104923,
#104924,#104925,#104926,#104927,#104928,#104929,#104930,#104931,#104932,
#104933,#104934,#104935,#104936,#104937,#104938,#104939,#104940,#104941,
#104942,#104943,#104944,#104945,#104946,#104947,#104948,#104949,#104950,
#104951,#104952,#104953,#104954,#104955,#104956,#104957,#104958,#104959,
#104960,#104961,#104962,#104963,#104964,#104965,#104966,#104967,#104968,
#104969,#104970,#104971,#104972,#104973,#104974,#104975,#104976),
 .UNSPECIFIED.,.F.,.F.,(4,3,3,3,3,3,3,3,3,3,3,3,3,3,3,3,3,3,3,3,3,3,3,3,
3,3,3,3,3,3,3,3,3,3,3,3,3,3,3,3,3,3,3,3,3,3,3,3,3,3,3,3,3,3,3,3,3,3,3,3,
3,3,3,3,3,3,3,3,3,3,3,3,3,4),(1203.22998632488,1203.30074629748,1203.38448500933,
1203.46812052069,1203.55167296409,1203.63516239994,1203.71861635056,1203.8020528444,
1203.88548995416,1203.96894574908,1204.05249024181,1204.13607932475,1204.2198025923,
1204.3004823082,1204.38422102005,1204.46785653141,1204.55140897481,1204.63489841066,
1204.71835236128,1204.80178885512,1204.88522596488,1204.9686817598,1205.05222625253,
1205.13581533547,1205.21953860303,1205.30021831892,1205.38395703077,1205.46759254213,
1205.55114498553,1205.63463442138,1205.718088372,1205.80152486584,1205.8849619756,
1205.96841777052,1206.05196226325,1206.13555134619,1206.21927461374,1206.29995432964,
1206.38369304149,1206.46732855285,1206.55088099625,1206.6343704321,1206.71782438272,
1206.80126087656,1206.88469798632,1206.96815378124,1207.05169827397,1207.13528735691,
1207.21901062446,1207.29969034036,1207.38342905221,1207.46706456357,1207.55061700697,
1207.63410644282,1207.71756039344,1207.80099688728,1207.88443399704,1207.96788979195,
1208.05143428468,1208.13502336762,1208.21874663518,1208.29942635108,1208.38316718062,
1208.4668043182,1208.5503578984,1208.63384798321,1208.7173001051,1208.80073407538,
1208.8841679663,1208.96761984604,1209.05115095118,1209.13472635942,1209.21841398669,
1209.2618988713),.UNSPECIFIED.);
#819=B_SPLINE_CURVE_WITH_KNOTS('',3,(#104982,#104983,#104984,#104985,#104986,
#104987,#104988,#104989,#104990,#104991,#104992,#104993,#104994,#104995,
#104996,#104997,#104998,#104999,#105000,#105001,#105002,#105003,#105004,
#105005,#105006,#105007,#105008,#105009,#105010,#105011,#105012,#105013,
#105014,#105015,#105016,#105017,#105018,#105019,#105020,#105021,#105022,
#105023,#105024,#105025,#105026,#105027,#105028,#105029,#105030,#105031,
#105032,#105033,#105034,#105035,#105036,#105037,#105038,#105039,#105040,
#105041,#105042,#105043,#105044,#105045,#105046,#105047,#105048,#105049,
#105050,#105051,#105052,#105053,#105054,#105055,#105056,#105057,#105058,
#105059,#105060,#105061,#105062,#105063,#105064,#105065,#105066,#105067,
#105068,#105069,#105070,#105071,#105072,#105073,#105074,#105075,#105076,
#105077,#105078,#105079,#105080,#105081,#105082,#105083,#105084,#105085,
#105086,#105087,#105088,#105089,#105090,#105091,#105092,#105093,#105094,
#105095,#105096,#105097,#105098,#105099,#105100,#105101,#105102,#105103,
#105104,#105105,#105106,#105107,#105108,#105109,#105110,#105111,#105112,
#105113,#105114,#105115,#105116,#105117,#105118,#105119,#105120,#105121,
#105122,#105123,#105124,#105125,#105126,#105127,#105128,#105129,#105130,
#105131,#105132,#105133,#105134,#105135,#105136,#105137,#105138,#105139,
#105140,#105141,#105142,#105143,#105144,#105145,#105146,#105147,#105148,
#105149,#105150,#105151,#105152,#105153,#105154,#105155,#105156,#105157,
#105158,#105159,#105160,#105161,#105162,#105163,#105164,#105165,#105166,
#105167,#105168,#105169,#105170,#105171,#105172,#105173,#105174,#105175,
#105176,#105177,#105178,#105179,#105180,#105181,#105182,#105183,#105184,
#105185,#105186,#105187,#105188,#105189,#105190,#105191,#105192,#105193,
#105194,#105195,#105196,#105197,#105198,#105199,#105200,#105201),
 .UNSPECIFIED.,.F.,.F.,(4,3,3,3,3,3,3,3,3,3,3,3,3,3,3,3,3,3,3,3,3,3,3,3,
3,3,3,3,3,3,3,3,3,3,3,3,3,3,3,3,3,3,3,3,3,3,3,3,3,3,3,3,3,3,3,3,3,3,3,3,
3,3,3,3,3,3,3,3,3,3,3,3,3,4),(1209.51317163215,1209.60151643376,1209.69001276627,
1209.77875144095,1209.86762236245,1209.95670179045,1209.98860775281,1210.07234646466,
1210.15598197602,1210.23953441942,1210.32302385527,1210.40647780589,1210.48991429973,
1210.57335140949,1210.65680720441,1210.74035169714,1210.82394078008,1210.90766404764,
1210.98834376353,1211.07208247538,1211.15571798674,1211.23927043014,1211.32275986599,
1211.40621381661,1211.48965031045,1211.57308742021,1211.65654321512,1211.74008770785,
1211.82367679079,1211.90740005835,1211.98807977425,1212.0718184861,1212.15545399746,
1212.23900644086,1212.32249587671,1212.40594982733,1212.48938632117,1212.57282343093,
1212.65627922585,1212.73982371858,1212.82341280152,1212.90713606907,1212.98781578497,
1213.07155449682,1213.15519000818,1213.23874245158,1213.32223188743,1213.40568583805,
1213.48912233189,1213.57255944165,1213.65601523657,1213.7395597293,1213.82314881224,
1213.9068720798,1213.98755179569,1214.07129050754,1214.1549260189,1214.2384784623,
1214.32196789815,1214.40542184877,1214.48885834261,1214.57229545237,1214.65575124728,
1214.73929574001,1214.82288482295,1214.90660809051,1214.98728780641,1215.06978088805,
1215.15217812242,1215.23449872101,1215.31676058311,1215.39898710595,1215.48121354423,
1215.54473266754),.UNSPECIFIED.);
#820=B_SPLINE_CURVE_WITH_KNOTS('',3,(#105202,#105203,#105204,#105205,#105206,
#105207,#105208,#105209,#105210,#105211),.UNSPECIFIED.,.F.,.F.,(4,3,3,4),
(1209.26279998827,1209.34951857049,1209.43611436924,1209.51317163205),
 .UNSPECIFIED.);
#821=B_SPLINE_CURVE_WITH_KNOTS('',3,(#105213,#105214,#105215,#105216,#105217,
#105218,#105219,#105220,#105221,#105222),.UNSPECIFIED.,.F.,.F.,(4,3,3,4),
(1209.2618988713,1209.2991623618,1209.41543192236,1209.51317163206),
 .UNSPECIFIED.);
#822=B_SPLINE_CURVE_WITH_KNOTS('',3,(#105223,#105224,#105225,#105226,#105227,
#105228,#105229,#105230,#105231,#105232,#105233,#105234,#105235,#105236,
#105237,#105238,#105239,#105240,#105241,#105242,#105243,#105244,#105245,
#105246,#105247,#105248,#105249,#105250,#105251,#105252,#105253,#105254,
#105255,#105256,#105257,#105258,#105259,#105260,#105261,#105262,#105263,
#105264,#105265,#105266,#105267,#105268,#105269,#105270,#105271,#105272,
#105273,#105274,#105275,#105276,#105277,#105278,#105279,#105280,#105281,
#105282,#105283,#105284,#105285,#105286,#105287,#105288,#105289,#105290,
#105291,#105292,#105293,#105294,#105295,#105296,#105297,#105298,#105299,
#105300,#105301,#105302,#105303,#105304,#105305,#105306,#105307,#105308,
#105309,#105310,#105311,#105312,#105313,#105314,#105315,#105316,#105317,
#105318,#105319,#105320,#105321,#105322,#105323,#105324,#105325,#105326,
#105327,#105328,#105329,#105330,#105331,#105332,#105333,#105334,#105335,
#105336,#105337,#105338,#105339,#105340,#105341,#105342,#105343,#105344,
#105345,#105346,#105347,#105348,#105349,#105350,#105351,#105352,#105353,
#105354,#105355,#105356,#105357,#105358,#105359,#105360,#105361,#105362,
#105363,#105364,#105365,#105366,#105367,#105368,#105369,#105370,#105371,
#105372,#105373,#105374,#105375,#105376,#105377,#105378,#105379,#105380,
#105381,#105382,#105383,#105384,#105385,#105386,#105387,#105388,#105389,
#105390,#105391,#105392,#105393,#105394,#105395,#105396,#105397,#105398,
#105399,#105400,#105401,#105402,#105403,#105404,#105405,#105406,#105407,
#105408,#105409,#105410,#105411,#105412,#105413,#105414,#105415,#105416,
#105417,#105418,#105419,#105420,#105421,#105422,#105423,#105424,#105425,
#105426,#105427,#105428,#105429,#105430,#105431,#105432,#105433,#105434,
#105435,#105436,#105437,#105438,#105439,#105440,#105441,#105442),
 .UNSPECIFIED.,.F.,.F.,(4,3,3,3,3,3,3,3,3,3,3,3,3,3,3,3,3,3,3,3,3,3,3,3,
3,3,3,3,3,3,3,3,3,3,3,3,3,3,3,3,3,3,3,3,3,3,3,3,3,3,3,3,3,3,3,3,3,3,3,3,
3,3,3,3,3,3,3,3,3,3,3,3,3,4),(1209.51317163217,1209.59557880271,1209.67792117058,
1209.7602265483,1209.84251467156,1209.9248045227,1210.00711508318,1210.08951190621,
1210.17195686769,1210.25452297352,1210.29889837252,1210.38263708437,1210.46627259573,
1210.54982503913,1210.63331447498,1210.7167684256,1210.80020491944,1210.8836420292,
1210.96709782412,1211.05064231685,1211.13423139979,1211.21795466735,1211.29863438324,
1211.38237309509,1211.46600860645,1211.54956104985,1211.63305048571,1211.71650443632,
1211.79994093017,1211.88337803992,1211.96683383484,1212.05037832757,1212.13396741051,
1212.21769067807,1212.29837039397,1212.38210910582,1212.46574461718,1212.54929706058,
1212.63278649643,1212.71624044705,1212.79967694089,1212.88311405065,1212.96656984557,
1213.0501143383,1213.13370342124,1213.2174266888,1213.29810640469,1213.38184511654,
1213.4654806279,1213.5490330713,1213.63252250715,1213.71597645777,1213.79941295161,
1213.88285006137,1213.96630585628,1214.04985034901,1214.13343943195,1214.21716269951,
1214.29784241541,1214.38158112726,1214.46521663862,1214.54876908202,1214.63225851787,
1214.71571246849,1214.79914896233,1214.88258607209,1214.96604186701,1215.04958635974,
1215.13317544268,1215.21689871023,1215.29757842613,1215.38567764236,1215.47358023361,
1215.54603050746),.UNSPECIFIED.);
#823=B_SPLINE_CURVE_WITH_KNOTS('',3,(#105448,#105449,#105450,#105451,#105452,
#105453,#105454,#105455,#105456,#105457,#105458,#105459,#105460,#105461,
#105462,#105463,#105464,#105465,#105466,#105467,#105468,#105469,#105470,
#105471,#105472,#105473,#105474,#105475,#105476,#105477,#105478,#105479,
#105480,#105481,#105482,#105483,#105484,#105485,#105486,#105487,#105488,
#105489,#105490,#105491,#105492,#105493,#105494,#105495,#105496,#105497,
#105498,#105499,#105500,#105501,#105502,#105503,#105504,#105505,#105506,
#105507,#105508,#105509,#105510,#105511,#105512,#105513,#105514,#105515,
#105516,#105517,#105518,#105519,#105520,#105521,#105522,#105523,#105524,
#105525,#105526,#105527,#105528,#105529,#105530,#105531,#105532,#105533,
#105534,#105535,#105536,#105537,#105538,#105539,#105540,#105541,#105542,
#105543,#105544,#105545,#105546,#105547,#105548,#105549,#105550,#105551,
#105552,#105553,#105554,#105555,#105556,#105557,#105558,#105559,#105560,
#105561,#105562,#105563,#105564,#105565,#105566,#105567,#105568,#105569,
#105570,#105571,#105572,#105573,#105574,#105575,#105576,#105577,#105578,
#105579,#105580,#105581,#105582,#105583,#105584,#105585,#105586,#105587,
#105588,#105589,#105590,#105591,#105592,#105593,#105594,#105595,#105596,
#105597,#105598,#105599,#105600,#105601,#105602,#105603,#105604,#105605,
#105606,#105607,#105608,#105609,#105610,#105611,#105612,#105613,#105614,
#105615,#105616,#105617,#105618,#105619,#105620,#105621,#105622,#105623,
#105624,#105625,#105626,#105627,#105628,#105629,#105630,#105631,#105632,
#105633,#105634,#105635,#105636,#105637,#105638,#105639,#105640,#105641,
#105642,#105643,#105644,#105645,#105646,#105647,#105648,#105649,#105650,
#105651,#105652,#105653,#105654,#105655,#105656,#105657,#105658,#105659,
#105660,#105661,#105662,#105663,#105664),.UNSPECIFIED.,.F.,.F.,(4,3,3,3,
3,3,3,3,3,3,3,3,3,3,3,3,3,3,3,3,3,3,3,3,3,3,3,3,3,3,3,3,3,3,3,3,3,3,3,3,
3,3,3,3,3,3,3,3,3,3,3,3,3,3,3,3,3,3,3,3,3,3,3,3,3,3,3,3,3,3,3,3,4),(1215.79635693923,
1215.91958713295,1215.98702381713,1216.07076252898,1216.15439804034,1216.23795048374,
1216.32143991959,1216.40489387021,1216.48833036405,1216.57176747381,1216.65522326873,
1216.73876776146,1216.8223568444,1216.90608011196,1216.98675982785,1217.0704985397,
1217.15413405106,1217.23768649446,1217.32117593031,1217.40462988093,1217.48806637477,
1217.57150348453,1217.65495927944,1217.73850377217,1217.82209285511,1217.90581612267,
1217.98649583857,1218.07023455042,1218.15387006178,1218.23742250518,1218.32091194103,
1218.40436589165,1218.48780238549,1218.57123949525,1218.65469529017,1218.7382397829,
1218.82182886584,1218.90555213339,1218.98623184929,1219.06997056114,1219.1536060725,
1219.2371585159,1219.32064795175,1219.40410190237,1219.48753839621,1219.57097550597,
1219.65443130089,1219.73797579362,1219.82156487656,1219.90528814411,1219.98596786001,
1220.06970657186,1220.15334208322,1220.23689452662,1220.32038396247,1220.40383791309,
1220.48727440693,1220.57071151669,1220.65416731161,1220.73771180434,1220.82130088728,
1220.90502415484,1220.98570387073,1221.06945195796,1221.15309476657,1221.23744655451,
1221.32093250422,1221.40438014118,1221.48780755436,1221.57283293328,1221.65630100248,
1221.74210503626,1221.82790907005),.UNSPECIFIED.);
#824=B_SPLINE_CURVE_WITH_KNOTS('',3,(#105665,#105666,#105667,#105668,#105669,
#105670,#105671,#105672,#105673,#105674),.UNSPECIFIED.,.F.,.F.,(4,3,3,4),
(1215.54473266754,1215.62699574014,1215.71167633962,1215.7963569391),
 .UNSPECIFIED.);
#825=B_SPLINE_CURVE_WITH_KNOTS('',3,(#105676,#105677,#105678,#105679,#105680,
#105681,#105682,#105683,#105684,#105685),.UNSPECIFIED.,.F.,.F.,(4,3,3,4),
(1215.54603050746,1215.63367448717,1215.72115463404,1215.796356939),
 .UNSPECIFIED.);
#826=B_SPLINE_CURVE_WITH_KNOTS('',3,(#105686,#105687,#105688,#105689,#105690,
#105691,#105692,#105693,#105694,#105695,#105696,#105697,#105698,#105699,
#105700,#105701,#105702,#105703,#105704,#105705,#105706,#105707,#105708,
#105709,#105710,#105711,#105712,#105713,#105714,#105715,#105716,#105717,
#105718,#105719,#105720,#105721,#105722,#105723,#105724,#105725,#105726,
#105727,#105728,#105729,#105730,#105731,#105732,#105733,#105734,#105735,
#105736,#105737,#105738,#105739,#105740,#105741,#105742,#105743,#105744,
#105745,#105746,#105747,#105748,#105749,#105750,#105751,#105752,#105753,
#105754,#105755,#105756,#105757,#105758,#105759,#105760,#105761,#105762,
#105763,#105764,#105765,#105766,#105767,#105768,#105769,#105770,#105771,
#105772,#105773,#105774,#105775,#105776,#105777,#105778,#105779,#105780,
#105781,#105782,#105783,#105784,#105785,#105786,#105787,#105788,#105789,
#105790,#105791,#105792,#105793,#105794,#105795,#105796,#105797,#105798,
#105799,#105800,#105801,#105802,#105803,#105804,#105805,#105806,#105807,
#105808,#105809,#105810,#105811,#105812,#105813,#105814,#105815,#105816,
#105817,#105818,#105819,#105820,#105821,#105822,#105823,#105824,#105825,
#105826,#105827,#105828,#105829,#105830,#105831,#105832,#105833,#105834,
#105835,#105836,#105837,#105838,#105839,#105840,#105841,#105842,#105843,
#105844,#105845,#105846,#105847,#105848,#105849,#105850,#105851,#105852,
#105853,#105854,#105855,#105856,#105857,#105858,#105859,#105860,#105861,
#105862,#105863,#105864,#105865,#105866,#105867,#105868,#105869,#105870,
#105871,#105872,#105873,#105874,#105875,#105876,#105877,#105878,#105879,
#105880,#105881,#105882,#105883,#105884,#105885,#105886,#105887,#105888,
#105889,#105890,#105891,#105892,#105893,#105894,#105895,#105896,#105897,
#105898,#105899,#105900,#105901,#105902,#105903,#105904,#105905),
 .UNSPECIFIED.,.F.,.F.,(4,3,3,3,3,3,3,3,3,3,3,3,3,3,3,3,3,3,3,3,3,3,3,3,
3,3,3,3,3,3,3,3,3,3,3,3,3,3,3,3,3,3,3,3,3,3,3,3,3,3,3,3,3,3,3,3,3,3,3,3,
3,3,3,3,3,3,3,3,3,3,3,3,3,4),(1215.79635693924,1215.88372152378,1215.97119972917,
1216.05888328619,1216.14667503323,1216.23466785268,1216.29731443685,1216.3810531487,
1216.46468866006,1216.54824110346,1216.63173053931,1216.71518448993,1216.79862098377,
1216.88205809353,1216.96551388845,1217.04905838118,1217.13264746412,1217.21637073167,
1217.29705044757,1217.38078915942,1217.46442467078,1217.54797711418,1217.63146655003,
1217.71492050065,1217.79835699449,1217.88179410425,1217.96524989917,1218.04879439189,
1218.13238347484,1218.21610674239,1218.29678645829,1218.38052517014,1218.4641606815,
1218.5477131249,1218.63120256075,1218.71465651137,1218.79809300521,1218.88153011497,
1218.96498590989,1219.04853040262,1219.13211948556,1219.21584275312,1219.29652246901,
1219.38026118086,1219.46389669222,1219.54744913562,1219.63093857147,1219.71439252209,
1219.79782901593,1219.88126612569,1219.96472192061,1220.04826641334,1220.13185549628,
1220.21557876383,1220.29625847973,1220.37999719158,1220.46363270294,1220.54718514634,
1220.63067458219,1220.71412853281,1220.79756502665,1220.88100213641,1220.96445793133,
1221.04800242406,1221.131591507,1221.21531477455,1221.29599449045,1221.37856692625,
1221.46104267683,1221.54344090801,1221.62577716739,1221.70807749483,1221.7903699991,
1221.82802192058),.UNSPECIFIED.);
#827=B_SPLINE_CURVE_WITH_KNOTS('',3,(#105911,#105912,#105913,#105914,#105915,
#105916,#105917,#105918,#105919,#105920,#105921,#105922,#105923,#105924,
#105925,#105926,#105927,#105928,#105929,#105930,#105931,#105932,#105933,
#105934,#105935,#105936,#105937,#105938,#105939,#105940,#105941,#105942,
#105943,#105944,#105945,#105946,#105947,#105948,#105949,#105950,#105951,
#105952,#105953,#105954,#105955,#105956,#105957,#105958,#105959,#105960,
#105961,#105962,#105963,#105964,#105965,#105966,#105967,#105968,#105969,
#105970,#105971,#105972,#105973,#105974,#105975,#105976,#105977,#105978,
#105979,#105980,#105981,#105982,#105983,#105984,#105985,#105986,#105987,
#105988,#105989,#105990,#105991,#105992,#105993,#105994,#105995,#105996,
#105997,#105998,#105999,#106000,#106001,#106002,#106003,#106004,#106005,
#106006,#106007,#106008,#106009,#106010,#106011,#106012,#106013,#106014,
#106015,#106016,#106017,#106018,#106019,#106020,#106021,#106022,#106023,
#106024,#106025,#106026,#106027,#106028,#106029,#106030,#106031,#106032,
#106033,#106034,#106035,#106036,#106037,#106038,#106039,#106040,#106041,
#106042,#106043,#106044,#106045,#106046,#106047,#106048,#106049,#106050,
#106051,#106052,#106053,#106054,#106055,#106056,#106057,#106058,#106059,
#106060,#106061,#106062,#106063,#106064,#106065,#106066,#106067,#106068,
#106069,#106070,#106071,#106072,#106073,#106074,#106075,#106076,#106077,
#106078,#106079,#106080,#106081,#106082,#106083,#106084,#106085,#106086,
#106087,#106088,#106089,#106090,#106091,#106092,#106093,#106094,#106095,
#106096,#106097,#106098,#106099,#106100,#106101,#106102,#106103,#106104,
#106105,#106106,#106107,#106108,#106109,#106110,#106111,#106112,#106113,
#106114,#106115,#106116,#106117,#106118,#106119,#106120,#106121,#106122,
#106123,#106124,#106125,#106126,#106127,#106128,#106129,#106130),
 .UNSPECIFIED.,.F.,.F.,(4,3,3,3,3,3,3,3,3,3,3,3,3,3,3,3,3,3,3,3,3,3,3,3,
3,3,3,3,3,3,3,3,3,3,3,3,3,3,3,3,3,3,3,3,3,3,3,3,3,3,3,3,3,3,3,3,3,3,3,3,
3,3,3,3,3,3,3,3,3,3,3,3,3,4),(1222.07954224654,1222.1622243311,1222.24481273503,
1222.32732847992,1222.40979672105,1222.49224044242,1222.5746785349,1222.6571298824,
1222.73966412823,1222.82223962968,1222.90494673739,1222.98517589217,1223.06891460402,
1223.15255011538,1223.23610255878,1223.31959199463,1223.40304594525,1223.48648243909,
1223.56991954885,1223.65337534377,1223.7369198365,1223.82050891944,1223.904232187,
1223.98491190289,1224.06865061474,1224.1522861261,1224.2358385695,1224.31932800535,
1224.40278195597,1224.48621844981,1224.56965555957,1224.65311135448,1224.73665584721,
1224.82024493015,1224.90396819771,1224.98464791361,1225.06838662546,1225.15202213682,
1225.23557458022,1225.31906401607,1225.40251796669,1225.48595446053,1225.56939157029,
1225.65284736521,1225.73639185794,1225.81998094088,1225.90370420844,1225.98438392433,
1226.06812263618,1226.15175814754,1226.23531059094,1226.31880002679,1226.40225397741,
1226.48569047125,1226.56912758101,1226.65258337593,1226.73612786866,1226.8197169516,
1226.90344021916,1226.98411993505,1227.0678586469,1227.15149415826,1227.23504660166,
1227.31853603751,1227.40198998813,1227.48542648197,1227.56886359173,1227.65231938665,
1227.73586387938,1227.81945296232,1227.90317622987,1227.98385594577,1228.07849597611,
1228.11229739101),.UNSPECIFIED.);
#828=B_SPLINE_CURVE_WITH_KNOTS('',3,(#106131,#106132,#106133,#106134,#106135,
#106136,#106137,#106138,#106139,#106140),.UNSPECIFIED.,.F.,.F.,(4,3,3,4),
(1221.82790907005,1221.91163470905,1221.98543988145,1222.07954224641),
 .UNSPECIFIED.);
#829=B_SPLINE_CURVE_WITH_KNOTS('',3,(#106142,#106143,#106144,#106145,#106146,
#106147,#106148,#106149,#106150,#106151),.UNSPECIFIED.,.F.,.F.,(4,3,3,4),
(1221.82802192058,1221.91034520054,1221.99494372338,1222.07954224622),
 .UNSPECIFIED.);
#830=B_SPLINE_CURVE_WITH_KNOTS('',3,(#106152,#106153,#106154,#106155,#106156,
#106157,#106158,#106159,#106160,#106161,#106162,#106163,#106164,#106165,
#106166,#106167,#106168,#106169,#106170,#106171,#106172,#106173,#106174,
#106175,#106176,#106177,#106178,#106179,#106180,#106181,#106182,#106183,
#106184,#106185,#106186,#106187,#106188,#106189,#106190,#106191,#106192,
#106193,#106194,#106195,#106196,#106197,#106198,#106199,#106200,#106201,
#106202,#106203,#106204,#106205,#106206,#106207,#106208,#106209,#106210,
#106211,#106212,#106213,#106214,#106215,#106216,#106217,#106218,#106219,
#106220,#106221,#106222,#106223,#106224,#106225,#106226,#106227,#106228,
#106229,#106230,#106231,#106232,#106233,#106234,#106235,#106236,#106237,
#106238,#106239,#106240,#106241,#106242,#106243,#106244,#106245,#106246,
#106247,#106248,#106249,#106250,#106251,#106252,#106253,#106254,#106255,
#106256,#106257,#106258,#106259,#106260,#106261,#106262,#106263,#106264,
#106265,#106266,#106267,#106268,#106269,#106270,#106271,#106272,#106273,
#106274,#106275,#106276,#106277,#106278,#106279,#106280,#106281,#106282,
#106283,#106284,#106285,#106286,#106287,#106288,#106289,#106290,#106291,
#106292,#106293,#106294,#106295,#106296,#106297,#106298,#106299,#106300,
#106301,#106302,#106303,#106304,#106305,#106306,#106307,#106308,#106309,
#106310,#106311,#106312,#106313,#106314,#106315,#106316,#106317,#106318,
#106319,#106320,#106321,#106322,#106323,#106324,#106325,#106326,#106327,
#106328,#106329,#106330,#106331,#106332,#106333,#106334,#106335,#106336,
#106337,#106338,#106339,#106340,#106341,#106342,#106343,#106344,#106345,
#106346,#106347,#106348,#106349,#106350,#106351,#106352,#106353,#106354,
#106355,#106356,#106357,#106358,#106359,#106360,#106361,#106362,#106363,
#106364,#106365,#106366,#106367,#106368),.UNSPECIFIED.,.F.,.F.,(4,3,3,3,
3,3,3,3,3,3,3,3,3,3,3,3,3,3,3,3,3,3,3,3,3,3,3,3,3,3,3,3,3,3,3,3,3,3,3,3,
3,3,3,3,3,3,3,3,3,3,3,3,3,3,3,3,3,3,3,3,3,3,3,3,3,3,3,3,3,3,3,3,4),(1222.07954224642,
1222.19525728097,1222.29573050117,1222.37946921302,1222.46310472438,1222.54665716778,
1222.63014660363,1222.71360055425,1222.79703704809,1222.88047415785,1222.96392995277,
1223.0474744455,1223.13106352844,1223.21478679599,1223.29546651189,1223.37920522374,
1223.4628407351,1223.5463931785,1223.62988261435,1223.71333656497,1223.79677305881,
1223.88021016857,1223.96366596349,1224.04721045621,1224.13079953916,1224.21452280671,
1224.29520252261,1224.37894123446,1224.46257674582,1224.54612918922,1224.62961862507,
1224.71307257569,1224.79650906953,1224.87994617929,1224.96340197421,1225.04694646694,
1225.13053554988,1225.21425881743,1225.29493853333,1225.37867724518,1225.46231275654,
1225.54586519994,1225.62935463579,1225.71280858641,1225.79624508025,1225.87968219001,
1225.96313798493,1226.04668247766,1226.1302715606,1226.21399482815,1226.29467454405,
1226.3784132559,1226.46204876726,1226.54560121066,1226.62909064651,1226.71254459713,
1226.79598109097,1226.87941820073,1226.96287399565,1227.04641848838,1227.13000757132,
1227.21373083887,1227.29441055477,1227.37816026671,1227.46180436294,1227.54534777386,
1227.62883409999,1227.71228146099,1227.79570794646,1227.87915848801,1227.96261979029,
1228.04615181694,1228.1110700616),.UNSPECIFIED.);
#831=B_SPLINE_CURVE_WITH_KNOTS('',3,(#106374,#106375,#106376,#106377,#106378,
#106379,#106380,#106381,#106382,#106383,#106384,#106385,#106386,#106387,
#106388,#106389,#106390,#106391,#106392,#106393,#106394,#106395,#106396,
#106397,#106398,#106399,#106400,#106401,#106402,#106403,#106404,#106405,
#106406,#106407,#106408,#106409,#106410,#106411,#106412,#106413,#106414,
#106415,#106416,#106417,#106418,#106419,#106420,#106421,#106422,#106423,
#106424,#106425,#106426,#106427,#106428,#106429,#106430,#106431,#106432,
#106433,#106434,#106435,#106436,#106437,#106438,#106439,#106440,#106441,
#106442,#106443,#106444,#106445,#106446,#106447,#106448,#106449,#106450,
#106451,#106452,#106453,#106454,#106455,#106456,#106457,#106458,#106459,
#106460,#106461,#106462,#106463,#106464,#106465,#106466,#106467,#106468,
#106469,#106470,#106471,#106472,#106473,#106474,#106475,#106476,#106477,
#106478,#106479,#106480,#106481,#106482,#106483,#106484,#106485,#106486,
#106487,#106488,#106489,#106490,#106491,#106492,#106493,#106494,#106495,
#106496,#106497,#106498,#106499,#106500,#106501,#106502,#106503,#106504,
#106505,#106506,#106507,#106508,#106509,#106510,#106511,#106512,#106513,
#106514,#106515,#106516,#106517,#106518,#106519,#106520,#106521,#106522,
#106523,#106524,#106525,#106526,#106527,#106528,#106529,#106530,#106531,
#106532,#106533,#106534,#106535,#106536,#106537,#106538,#106539,#106540,
#106541,#106542,#106543,#106544,#106545,#106546,#106547,#106548,#106549,
#106550,#106551,#106552,#106553,#106554,#106555,#106556,#106557,#106558,
#106559,#106560,#106561,#106562,#106563,#106564,#106565,#106566,#106567,
#106568,#106569,#106570,#106571,#106572,#106573,#106574,#106575,#106576,
#106577,#106578,#106579,#106580,#106581,#106582,#106583,#106584,#106585,
#106586,#106587,#106588,#106589,#106590,#106591,#106592,#106593),
 .UNSPECIFIED.,.F.,.F.,(4,3,3,3,3,3,3,3,3,3,3,3,3,3,3,3,3,3,3,3,3,3,3,3,
3,3,3,3,3,3,3,3,3,3,3,3,3,3,3,3,3,3,3,3,3,3,3,3,3,3,3,3,3,3,3,3,3,3,3,3,
3,3,3,3,3,3,3,3,3,3,3,3,3,4),(1228.36272755359,1228.44686496824,1228.53101191958,
1228.61518547554,1228.69940271783,1228.78373211921,1228.86812631425,1228.95265392673,
1228.98359195649,1229.06733066834,1229.1509661797,1229.2345186231,1229.31800805895,
1229.40146200956,1229.48489850341,1229.56833561316,1229.65179140808,1229.73533590081,
1229.81892498375,1229.90264825131,1229.98332796721,1230.06706667906,1230.15070219042,
1230.23425463382,1230.31774406967,1230.40119802029,1230.48463451413,1230.56807162389,
1230.6515274188,1230.73507191153,1230.81866099447,1230.90238426203,1230.98306397793,
1231.06680268978,1231.15043820114,1231.23399064454,1231.31748008039,1231.40093403101,
1231.48437052485,1231.56780763461,1231.65126342953,1231.73480792226,1231.8183970052,
1231.90212027276,1231.98279998865,1232.0665387005,1232.15017421186,1232.23372665526,
1232.31721609111,1232.40067004173,1232.48410653557,1232.56754364533,1232.65099944025,
1232.73454393298,1232.81813301592,1232.90185628347,1232.98253599937,1233.06627471122,
1233.14991022258,1233.23346266598,1233.31695210183,1233.40040605245,1233.48384254629,
1233.56727965605,1233.65073545097,1233.7342799437,1233.81786902664,1233.9015922942,
1233.98227201009,1234.06602879375,1234.14965100751,1234.23319577681,1234.3166722851,
1234.39499262579),.UNSPECIFIED.);
#832=B_SPLINE_CURVE_WITH_KNOTS('',3,(#106594,#106595,#106596,#106597,#106598,
#106599,#106600,#106601,#106602,#106603),.UNSPECIFIED.,.F.,.F.,(4,3,3,4),
(1228.11229739101,1228.20642172505,1228.30000816463,1228.36272755339),
 .UNSPECIFIED.);
#833=B_SPLINE_CURVE_WITH_KNOTS('',3,(#106605,#106606,#106607,#106608,#106609,
#106610,#106611,#106612,#106613,#106614,#106615,#106616,#106617),
 .UNSPECIFIED.,.F.,.F.,(4,3,3,3,4),(1228.1110700616,1228.1947049976,1228.27845607522,
1228.29414656549,1228.3627275536),.UNSPECIFIED.);
#834=B_SPLINE_CURVE_WITH_KNOTS('',3,(#106618,#106619,#106620,#106621,#106622,
#106623,#106624,#106625,#106626,#106627,#106628,#106629,#106630,#106631,
#106632,#106633,#106634,#106635,#106636,#106637,#106638,#106639,#106640,
#106641,#106642,#106643,#106644,#106645,#106646,#106647,#106648,#106649,
#106650,#106651,#106652,#106653,#106654,#106655,#106656,#106657,#106658,
#106659,#106660,#106661,#106662,#106663,#106664,#106665,#106666,#106667,
#106668,#106669,#106670,#106671,#106672,#106673,#106674,#106675,#106676,
#106677,#106678,#106679,#106680,#106681,#106682,#106683,#106684,#106685,
#106686,#106687,#106688,#106689,#106690,#106691,#106692,#106693,#106694,
#106695,#106696,#106697,#106698,#106699,#106700,#106701,#106702,#106703,
#106704,#106705,#106706,#106707,#106708,#106709,#106710,#106711,#106712,
#106713,#106714,#106715,#106716,#106717,#106718,#106719,#106720,#106721,
#106722,#106723,#106724,#106725,#106726,#106727,#106728,#106729,#106730,
#106731,#106732,#106733,#106734,#106735,#106736,#106737,#106738,#106739,
#106740,#106741,#106742,#106743,#106744,#106745,#106746,#106747,#106748,
#106749,#106750,#106751,#106752,#106753,#106754,#106755,#106756,#106757,
#106758,#106759,#106760,#106761,#106762,#106763,#106764,#106765,#106766,
#106767,#106768,#106769,#106770,#106771,#106772,#106773,#106774,#106775,
#106776,#106777,#106778,#106779,#106780,#106781,#106782,#106783,#106784,
#106785,#106786,#106787,#106788,#106789,#106790,#106791,#106792,#106793,
#106794,#106795,#106796,#106797,#106798,#106799,#106800,#106801,#106802,
#106803,#106804,#106805,#106806,#106807,#106808,#106809,#106810,#106811,
#106812,#106813,#106814,#106815,#106816,#106817,#106818,#106819,#106820,
#106821,#106822,#106823,#106824,#106825,#106826,#106827,#106828,#106829,
#106830,#106831,#106832,#106833,#106834,#106835,#106836,#106837,#106838,
#106839,#106840),.UNSPECIFIED.,.F.,.F.,(4,3,3,3,3,3,3,3,3,3,3,3,3,3,3,3,
3,3,3,3,3,3,3,3,3,3,3,3,3,3,3,3,3,3,3,3,3,3,3,3,3,3,3,3,3,3,3,3,3,3,3,3,
3,3,3,3,3,3,3,3,3,3,3,3,3,3,3,3,3,3,3,3,3,3,4),(1228.36272755372,1228.44562235737,
1228.52841945832,1228.6111397427,1228.69648259689,1228.77912045889,1228.86174916971,
1228.94438748203,1229.02705415266,1229.10981173076,1229.19262389116,1229.27555133896,
1229.29388257621,1229.37762128806,1229.46125679942,1229.54480924282,1229.62829867867,
1229.71175262929,1229.79518912313,1229.87862623289,1229.96208202781,1230.04562652054,
1230.12921560348,1230.21293887103,1230.29361858693,1230.37735729878,1230.46099281014,
1230.54454525354,1230.62803468939,1230.71148864001,1230.79492513385,1230.87836224361,
1230.96181803853,1231.04536253126,1231.1289516142,1231.21267488175,1231.29335459765,
1231.3770933095,1231.46072882086,1231.54428126426,1231.62777070011,1231.71122465073,
1231.79466114457,1231.87809825433,1231.96155404925,1232.04509854198,1232.12868762492,
1232.21241089247,1232.29309060837,1232.37682932022,1232.46046483158,1232.54401727498,
1232.62750671083,1232.71096066145,1232.79439715529,1232.87783426505,1232.96129005997,
1233.0448345527,1233.12842363564,1233.21214690319,1233.29282661909,1233.37656533094,
1233.4602008423,1233.5437532857,1233.62724272155,1233.71069667216,1233.79413316601,
1233.87757027577,1233.96102607068,1234.04457056341,1234.12815964635,1234.21188291391,
1234.29256262981,1234.38930089973,1234.3953925264),.UNSPECIFIED.);
#835=B_SPLINE_CURVE_WITH_KNOTS('',3,(#106846,#106847,#106848,#106849,#106850,
#106851,#106852,#106853,#106854,#106855,#106856,#106857,#106858,#106859,
#106860,#106861,#106862,#106863,#106864,#106865,#106866,#106867,#106868,
#106869,#106870,#106871,#106872,#106873,#106874,#106875,#106876,#106877,
#106878,#106879,#106880,#106881,#106882,#106883,#106884,#106885,#106886,
#106887,#106888,#106889,#106890,#106891,#106892,#106893,#106894,#106895,
#106896,#106897,#106898,#106899,#106900,#106901,#106902,#106903,#106904,
#106905,#106906,#106907,#106908,#106909,#106910,#106911,#106912,#106913,
#106914,#106915,#106916,#106917,#106918,#106919,#106920,#106921,#106922,
#106923,#106924,#106925,#106926,#106927,#106928,#106929,#106930,#106931,
#106932,#106933,#106934,#106935,#106936,#106937,#106938,#106939,#106940,
#106941,#106942,#106943,#106944,#106945,#106946,#106947,#106948,#106949,
#106950,#106951,#106952,#106953,#106954,#106955,#106956,#106957,#106958,
#106959,#106960,#106961,#106962,#106963,#106964,#106965,#106966,#106967,
#106968,#106969,#106970,#106971,#106972,#106973,#106974,#106975,#106976,
#106977,#106978,#106979,#106980,#106981,#106982,#106983,#106984,#106985,
#106986,#106987,#106988,#106989,#106990,#106991,#106992,#106993,#106994,
#106995,#106996,#106997,#106998,#106999,#107000,#107001,#107002,#107003,
#107004,#107005,#107006,#107007,#107008,#107009,#107010,#107011,#107012,
#107013,#107014,#107015,#107016,#107017,#107018,#107019,#107020,#107021,
#107022,#107023,#107024,#107025,#107026,#107027,#107028,#107029,#107030,
#107031,#107032,#107033,#107034,#107035,#107036,#107037,#107038,#107039,
#107040,#107041,#107042,#107043,#107044,#107045,#107046,#107047,#107048,
#107049,#107050,#107051,#107052,#107053,#107054,#107055,#107056,#107057,
#107058,#107059,#107060,#107061,#107062,#107063,#107064,#107065),
 .UNSPECIFIED.,.F.,.F.,(4,3,3,3,3,3,3,3,3,3,3,3,3,3,3,3,3,3,3,3,3,3,3,3,
3,3,3,3,3,3,3,3,3,3,3,3,3,3,3,3,3,3,3,3,3,3,3,3,3,3,3,3,3,3,3,3,3,3,3,3,
3,3,3,3,3,3,3,3,3,3,3,3,3,4),(1234.64591286096,1234.74290541511,1234.84045829031,
1234.93867775055,1234.98200802081,1235.06574673265,1235.14938224402,1235.23293468742,
1235.31642412327,1235.39987807388,1235.48331456772,1235.56675167748,1235.65020747239,
1235.73375196512,1235.81734104806,1235.90106431562,1235.98174403153,1236.06548274338,
1236.14911825474,1236.23267069814,1236.31616013399,1236.39961408461,1236.48305057845,
1236.56648768821,1236.64994348313,1236.73348797586,1236.8170770588,1236.90080032635,
1236.98148004225,1237.0652187541,1237.14885426546,1237.23240670886,1237.31589614471,
1237.39935009533,1237.48278658917,1237.56622369893,1237.64967949385,1237.73322398658,
1237.81681306952,1237.90053633708,1237.98121605297,1238.06495476482,1238.14859027618,
1238.23214271958,1238.31563215543,1238.39908610605,1238.48252259989,1238.56595970965,
1238.64941550456,1238.73295999729,1238.81654908023,1238.90027234779,1238.98095206369,
1239.06469077554,1239.1483262869,1239.2318787303,1239.31536816615,1239.39882211677,
1239.48225861061,1239.56569572037,1239.64915151529,1239.73269600802,1239.81628509096,
1239.90000835852,1239.98068807441,1240.06776341289,1240.15072850065,1240.23361870592,
1240.31645275755,1240.39924933831,1240.4820416088,1240.56483166194,1240.64766028562,
1240.67729078227),.UNSPECIFIED.);
#836=B_SPLINE_CURVE_WITH_KNOTS('',3,(#107066,#107067,#107068,#107069,#107070,
#107071,#107072,#107073,#107074,#107075),.UNSPECIFIED.,.F.,.F.,(4,3,3,4),
(1234.39499262579,1234.47840436807,1234.56215861442,1234.64591286077),
 .UNSPECIFIED.);
#837=B_SPLINE_CURVE_WITH_KNOTS('',3,(#107077,#107078,#107079,#107080,#107081,
#107082,#107083,#107084,#107085,#107086),.UNSPECIFIED.,.F.,.F.,(4,3,3,4),
(1234.3953925264,1234.49156719124,1234.58704613723,1234.64591286058),
 .UNSPECIFIED.);
#838=B_SPLINE_CURVE_WITH_KNOTS('',3,(#107087,#107088,#107089,#107090,#107091,
#107092,#107093,#107094,#107095,#107096,#107097,#107098,#107099,#107100,
#107101,#107102,#107103,#107104,#107105,#107106,#107107,#107108,#107109,
#107110,#107111,#107112,#107113,#107114,#107115,#107116,#107117,#107118,
#107119,#107120,#107121,#107122,#107123,#107124,#107125,#107126,#107127,
#107128,#107129,#107130,#107131,#107132,#107133,#107134,#107135,#107136,
#107137,#107138,#107139,#107140,#107141,#107142,#107143,#107144,#107145,
#107146,#107147,#107148,#107149,#107150,#107151,#107152,#107153,#107154,
#107155,#107156,#107157,#107158,#107159,#107160,#107161,#107162,#107163,
#107164,#107165,#107166,#107167,#107168,#107169,#107170,#107171,#107172,
#107173,#107174,#107175,#107176,#107177,#107178,#107179,#107180,#107181,
#107182,#107183,#107184,#107185,#107186,#107187,#107188,#107189,#107190,
#107191,#107192,#107193,#107194,#107195,#107196,#107197,#107198,#107199,
#107200,#107201,#107202,#107203,#107204,#107205,#107206,#107207,#107208,
#107209,#107210,#107211,#107212,#107213,#107214,#107215,#107216,#107217,
#107218,#107219,#107220,#107221,#107222,#107223,#107224,#107225,#107226,
#107227,#107228,#107229,#107230,#107231,#107232,#107233,#107234,#107235,
#107236,#107237,#107238,#107239,#107240,#107241,#107242,#107243,#107244,
#107245,#107246,#107247,#107248,#107249,#107250,#107251,#107252,#107253,
#107254,#107255,#107256,#107257,#107258,#107259,#107260,#107261,#107262,
#107263,#107264,#107265,#107266,#107267,#107268,#107269,#107270,#107271,
#107272,#107273,#107274,#107275,#107276,#107277,#107278,#107279,#107280,
#107281,#107282,#107283,#107284,#107285,#107286,#107287,#107288,#107289,
#107290,#107291,#107292,#107293,#107294,#107295,#107296,#107297,#107298,
#107299,#107300,#107301,#107302,#107303,#107304,#107305,#107306),
 .UNSPECIFIED.,.F.,.F.,(4,3,3,3,3,3,3,3,3,3,3,3,3,3,3,3,3,3,3,3,3,3,3,3,
3,3,3,3,3,3,3,3,3,3,3,3,3,3,3,3,3,3,3,3,3,3,3,3,3,3,3,3,3,3,3,3,3,3,3,3,
3,3,3,3,3,3,3,3,3,3,3,3,3,4),(1234.64591286078,1234.72960198682,1234.81328713594,
1234.8969860036,1234.98071629027,1235.06454892901,1235.14843665197,1235.23246162227,
1235.29229864053,1235.37603735238,1235.45967286374,1235.54322530714,1235.62671474299,
1235.71016869361,1235.79360518745,1235.87704229721,1235.96049809213,1236.04404258486,
1236.1276316678,1236.21135493536,1236.29203465125,1236.3757733631,1236.45940887446,
1236.54296131786,1236.62645075371,1236.70990470433,1236.79334119817,1236.87677830793,
1236.96023410285,1237.04377859558,1237.12736767852,1237.21109094607,1237.29177066197,
1237.37550937382,1237.45914488518,1237.54269732858,1237.62618676443,1237.70964071505,
1237.79307720889,1237.87651431865,1237.95997011357,1238.0435146063,1238.12710368924,
1238.2108269568,1238.29150667269,1238.37524538454,1238.4588808959,1238.5424333393,
1238.62592277515,1238.70937672577,1238.79281321961,1238.87625032937,1238.95970612429,
1239.04325061702,1239.12683969996,1239.21056296751,1239.29124268341,1239.37498139526,
1239.45861690662,1239.54216935002,1239.62565878587,1239.70911273649,1239.79254923033,
1239.87598634009,1239.959442135,1240.04298662773,1240.12657571067,1240.21029897823,
1240.29097869413,1240.3751777929,1240.45923668845,1240.54321483669,1240.62711586346,
1240.67830517384),.UNSPECIFIED.);
#839=B_SPLINE_CURVE_WITH_KNOTS('',3,(#107312,#107313,#107314,#107315,#107316,
#107317,#107318,#107319,#107320,#107321,#107322,#107323,#107324,#107325,
#107326,#107327,#107328,#107329,#107330,#107331,#107332,#107333,#107334,
#107335,#107336,#107337,#107338,#107339,#107340,#107341,#107342,#107343,
#107344,#107345,#107346,#107347,#107348,#107349,#107350,#107351,#107352,
#107353,#107354,#107355,#107356,#107357,#107358,#107359,#107360,#107361,
#107362,#107363,#107364,#107365,#107366,#107367,#107368,#107369,#107370,
#107371,#107372,#107373,#107374,#107375,#107376,#107377,#107378,#107379,
#107380,#107381,#107382,#107383,#107384,#107385,#107386,#107387,#107388,
#107389,#107390,#107391,#107392,#107393,#107394,#107395,#107396,#107397,
#107398,#107399,#107400,#107401,#107402,#107403,#107404,#107405,#107406,
#107407,#107408,#107409,#107410,#107411,#107412,#107413,#107414,#107415,
#107416,#107417,#107418,#107419,#107420,#107421,#107422,#107423,#107424,
#107425,#107426,#107427,#107428,#107429,#107430,#107431,#107432,#107433,
#107434,#107435,#107436,#107437,#107438,#107439,#107440,#107441,#107442,
#107443,#107444,#107445,#107446,#107447,#107448,#107449,#107450,#107451,
#107452,#107453,#107454,#107455,#107456,#107457,#107458,#107459,#107460,
#107461,#107462,#107463,#107464,#107465,#107466,#107467,#107468,#107469,
#107470,#107471,#107472,#107473,#107474,#107475,#107476,#107477,#107478,
#107479,#107480,#107481,#107482,#107483,#107484,#107485,#107486,#107487,
#107488,#107489,#107490,#107491,#107492,#107493,#107494,#107495,#107496,
#107497,#107498,#107499,#107500,#107501,#107502,#107503,#107504,#107505,
#107506,#107507,#107508,#107509,#107510,#107511,#107512,#107513,#107514,
#107515,#107516,#107517,#107518,#107519,#107520,#107521,#107522,#107523,
#107524,#107525,#107526,#107527,#107528,#107529,#107530,#107531),
 .UNSPECIFIED.,.F.,.F.,(4,3,3,3,3,3,3,3,3,3,3,3,3,3,3,3,3,3,3,3,3,3,3,3,
3,3,3,3,3,3,3,3,3,3,3,3,3,3,3,3,3,3,3,3,3,3,3,3,3,3,3,3,3,3,3,3,3,3,3,3,
3,3,3,3,3,3,3,3,3,3,3,3,3,4),(1240.92909816795,1240.98042408513,1241.06416279698,
1241.14779830834,1241.23135075174,1241.31484018759,1241.39829413821,1241.48173063205,
1241.56516774181,1241.64862353672,1241.73216802945,1241.8157571124,1241.89948037995,
1241.98016009585,1242.0638988077,1242.14753431906,1242.23108676246,1242.31457619831,
1242.39803014893,1242.48146664277,1242.56490375253,1242.64835954745,1242.73190404018,
1242.81549312312,1242.89921639068,1242.97989610657,1243.06363481842,1243.14727032978,
1243.23082277318,1243.31431220903,1243.39776615965,1243.48120265349,1243.56463976325,
1243.64809555817,1243.7316400509,1243.81522913384,1243.89895240139,1243.97963211729,
1244.06337082914,1244.1470063405,1244.2305587839,1244.31404821975,1244.39750217037,
1244.48093866421,1244.56437577397,1244.64783156889,1244.73137606162,1244.81496514456,
1244.89868841211,1244.97936812801,1245.06310683986,1245.14674235122,1245.23029479462,
1245.31378423047,1245.39723818109,1245.48067467493,1245.56411178469,1245.64756757961,
1245.73111207234,1245.81470115528,1245.89842442283,1245.97910413873,1246.06284385027,
1246.14648012754,1246.23003310401,1246.31352284087,1246.39697589055,1246.48041115292,
1246.56384670043,1246.64730060183,1246.73083860208,1246.81442105593,1246.89812687545,
1246.96111321221),.UNSPECIFIED.);
#840=B_SPLINE_CURVE_WITH_KNOTS('',3,(#107532,#107533,#107534,#107535,#107536,
#107537,#107538,#107539,#107540,#107541),.UNSPECIFIED.,.F.,.F.,(4,3,3,4),
(1240.67729078227,1240.76021147889,1240.84465482332,1240.92909816775),
 .UNSPECIFIED.);
#841=B_SPLINE_CURVE_WITH_KNOTS('',3,(#107543,#107544,#107545,#107546,#107547,
#107548,#107549,#107550,#107551,#107552),.UNSPECIFIED.,.F.,.F.,(4,3,3,4),
(1240.67830517384,1240.76213721218,1240.84596592975,1240.92909816796),
 .UNSPECIFIED.);
#842=B_SPLINE_CURVE_WITH_KNOTS('',3,(#107553,#107554,#107555,#107556,#107557,
#107558,#107559,#107560,#107561,#107562,#107563,#107564,#107565,#107566,
#107567,#107568,#107569,#107570,#107571,#107572,#107573,#107574,#107575,
#107576,#107577,#107578,#107579,#107580,#107581,#107582,#107583,#107584,
#107585,#107586,#107587,#107588,#107589,#107590,#107591,#107592,#107593,
#107594,#107595,#107596,#107597,#107598,#107599,#107600,#107601,#107602,
#107603,#107604,#107605,#107606,#107607,#107608,#107609,#107610,#107611,
#107612,#107613,#107614,#107615,#107616,#107617,#107618,#107619,#107620,
#107621,#107622,#107623,#107624,#107625,#107626,#107627,#107628,#107629,
#107630,#107631,#107632,#107633,#107634,#107635,#107636,#107637,#107638,
#107639,#107640,#107641,#107642,#107643,#107644,#107645,#107646,#107647,
#107648,#107649,#107650,#107651,#107652,#107653,#107654,#107655,#107656,
#107657,#107658,#107659,#107660,#107661,#107662,#107663,#107664,#107665,
#107666,#107667,#107668,#107669,#107670,#107671,#107672,#107673,#107674,
#107675,#107676,#107677,#107678,#107679,#107680,#107681,#107682,#107683,
#107684,#107685,#107686,#107687,#107688,#107689,#107690,#107691,#107692,
#107693,#107694,#107695,#107696,#107697,#107698,#107699,#107700,#107701,
#107702,#107703,#107704,#107705,#107706,#107707,#107708,#107709,#107710,
#107711,#107712,#107713,#107714,#107715,#107716,#107717,#107718,#107719,
#107720,#107721,#107722,#107723,#107724,#107725,#107726,#107727,#107728,
#107729,#107730,#107731,#107732,#107733,#107734,#107735,#107736,#107737,
#107738,#107739,#107740,#107741,#107742,#107743,#107744,#107745,#107746,
#107747,#107748,#107749,#107750,#107751,#107752,#107753,#107754,#107755,
#107756,#107757,#107758,#107759,#107760,#107761,#107762,#107763,#107764,
#107765,#107766,#107767,#107768,#107769),.UNSPECIFIED.,.F.,.F.,(4,3,3,3,
3,3,3,3,3,3,3,3,3,3,3,3,3,3,3,3,3,3,3,3,3,3,3,3,3,3,3,3,3,3,3,3,3,3,3,3,
3,3,3,3,3,3,3,3,3,3,3,3,3,3,3,3,3,3,3,3,3,3,3,3,3,3,3,3,3,3,3,3,4),(1240.92909816816,
1241.02401292562,1241.11934568251,1241.21524013569,1241.29071470485,1241.3744534167,
1241.45808892806,1241.54164137146,1241.62513080732,1241.70858475793,1241.79202125178,
1241.87545836153,1241.95891415645,1242.04245864918,1242.12604773212,1242.20977099968,
1242.29045071557,1242.37418942742,1242.45782493878,1242.54137738218,1242.62486681803,
1242.70832076865,1242.79175726249,1242.87519437225,1242.95865016717,1243.0421946599,
1243.12578374284,1243.2095070104,1243.29018672629,1243.37392543814,1243.4575609495,
1243.5411133929,1243.62460282875,1243.70805677937,1243.79149327321,1243.87493038297,
1243.95838617788,1244.04193067061,1244.12551975356,1244.20924302111,1244.28992273701,
1244.37366144886,1244.45729696022,1244.54084940362,1244.62433883947,1244.70779279009,
1244.79122928393,1244.87466639369,1244.95812218861,1245.04166668134,1245.12525576428,
1245.20897903183,1245.28965874773,1245.37339745958,1245.45703297094,1245.54058541434,
1245.62407485019,1245.70752880081,1245.79096529465,1245.87440240441,1245.95785819932,
1246.04140269205,1246.12499177499,1246.20871504255,1246.28939475845,1246.37327644502,
1246.45601189193,1246.53867200883,1246.62127569751,1246.70606883588,1246.78862824948,
1246.87453825023,1246.96044825099),.UNSPECIFIED.);
#843=B_SPLINE_CURVE_WITH_KNOTS('',3,(#107775,#107776,#107777,#107778,#107779,
#107780,#107781,#107782,#107783,#107784,#107785,#107786,#107787,#107788,
#107789,#107790,#107791,#107792,#107793,#107794,#107795,#107796,#107797,
#107798,#107799,#107800,#107801,#107802,#107803,#107804,#107805,#107806,
#107807,#107808,#107809,#107810,#107811,#107812,#107813,#107814,#107815,
#107816,#107817,#107818,#107819,#107820,#107821,#107822,#107823,#107824,
#107825,#107826,#107827,#107828,#107829,#107830,#107831,#107832,#107833,
#107834,#107835,#107836,#107837,#107838,#107839,#107840,#107841,#107842,
#107843,#107844,#107845,#107846,#107847,#107848,#107849,#107850,#107851,
#107852,#107853,#107854,#107855,#107856,#107857,#107858,#107859,#107860,
#107861,#107862,#107863,#107864,#107865,#107866,#107867,#107868,#107869,
#107870,#107871,#107872,#107873,#107874,#107875,#107876,#107877,#107878,
#107879,#107880,#107881,#107882,#107883,#107884,#107885,#107886,#107887,
#107888,#107889,#107890,#107891,#107892,#107893,#107894,#107895,#107896,
#107897,#107898,#107899,#107900,#107901,#107902,#107903,#107904,#107905,
#107906,#107907,#107908,#107909,#107910,#107911,#107912,#107913,#107914,
#107915,#107916,#107917,#107918,#107919,#107920,#107921,#107922,#107923,
#107924,#107925,#107926,#107927,#107928,#107929,#107930,#107931,#107932,
#107933,#107934,#107935,#107936,#107937,#107938,#107939,#107940,#107941,
#107942,#107943,#107944,#107945,#107946,#107947,#107948,#107949,#107950,
#107951,#107952,#107953,#107954,#107955,#107956,#107957,#107958,#107959,
#107960,#107961,#107962,#107963,#107964,#107965,#107966,#107967,#107968,
#107969,#107970,#107971,#107972,#107973,#107974,#107975,#107976,#107977,
#107978,#107979,#107980,#107981,#107982,#107983,#107984,#107985,#107986,
#107987,#107988,#107989,#107990,#107991,#107992,#107993,#107994),
 .UNSPECIFIED.,.F.,.F.,(4,3,3,3,3,3,3,3,3,3,3,3,3,3,3,3,3,3,3,3,3,3,3,3,
3,3,3,3,3,3,3,3,3,3,3,3,3,3,3,3,3,3,3,3,3,3,3,3,3,3,3,3,3,3,3,3,3,3,3,3,
3,3,3,3,3,3,3,3,3,3,3,3,3,4),(1247.21228347513,1247.29476035575,1247.3802373313,
1247.46262571574,1247.54500297411,1247.62738802756,1247.70979980091,1247.79230117892,
1247.87485598102,1247.9575263169,1247.97857616017,1248.06231487202,1248.14595038338,
1248.22950282678,1248.31299226263,1248.39644621325,1248.47988270709,1248.56331981685,
1248.64677561177,1248.7303201045,1248.81390918744,1248.89763245499,1248.97831217089,
1249.06205088274,1249.1456863941,1249.2292388375,1249.31272827335,1249.39618222397,
1249.47961871781,1249.56305582757,1249.64651162249,1249.73005611522,1249.81364519816,
1249.89736846571,1249.97804818161,1250.06178689346,1250.14542240482,1250.22897484822,
1250.31246428407,1250.39591823469,1250.47935472853,1250.56279183829,1250.64624763321,
1250.72979212594,1250.81338120888,1250.89710447643,1250.97778419233,1251.06152290418,
1251.14515841554,1251.22871085894,1251.31220029479,1251.39565424541,1251.47909073925,
1251.56252784901,1251.64598364393,1251.72952813666,1251.8131172196,1251.89684048716,
1251.97752020305,1252.0612589149,1252.14489442626,1252.22844686966,1252.31193630551,
1252.39539025613,1252.47882674997,1252.56226385973,1252.64571965465,1252.72926414738,
1252.81285323032,1252.89657649787,1252.97725621377,1253.06461780936,1253.15486384868,
1253.24510988801),.UNSPECIFIED.);
#844=B_SPLINE_CURVE_WITH_KNOTS('',3,(#107995,#107996,#107997,#107998,#107999,
#108000,#108001,#108002,#108003,#108004,#108005,#108006,#108007),
 .UNSPECIFIED.,.F.,.F.,(4,3,3,3,4),(1246.96111321221,1246.97884014945,1247.09556181222,
1247.20567859351,1247.21228347499),.UNSPECIFIED.);
#845=B_SPLINE_CURVE_WITH_KNOTS('',3,(#108009,#108010,#108011,#108012,#108013,
#108014,#108015,#108016,#108017,#108018),.UNSPECIFIED.,.F.,.F.,(4,3,3,4),
(1246.96044825099,1247.04312413363,1247.12770380432,1247.21228347501),
 .UNSPECIFIED.);
#846=B_SPLINE_CURVE_WITH_KNOTS('',3,(#108019,#108020,#108021,#108022,#108023,
#108024,#108025,#108026,#108027,#108028,#108029,#108030,#108031,#108032,
#108033,#108034,#108035,#108036,#108037,#108038,#108039,#108040,#108041,
#108042,#108043,#108044,#108045,#108046,#108047,#108048,#108049,#108050,
#108051,#108052,#108053,#108054,#108055,#108056,#108057,#108058,#108059,
#108060,#108061,#108062,#108063,#108064,#108065,#108066,#108067,#108068,
#108069,#108070,#108071,#108072,#108073,#108074,#108075,#108076,#108077,
#108078,#108079,#108080,#108081,#108082,#108083,#108084,#108085,#108086,
#108087,#108088,#108089,#108090,#108091,#108092,#108093,#108094,#108095,
#108096,#108097,#108098,#108099,#108100,#108101,#108102,#108103,#108104,
#108105,#108106,#108107,#108108,#108109,#108110,#108111,#108112,#108113,
#108114,#108115,#108116,#108117,#108118,#108119,#108120,#108121,#108122,
#108123,#108124,#108125,#108126,#108127,#108128,#108129,#108130,#108131,
#108132,#108133,#108134,#108135,#108136,#108137,#108138,#108139,#108140,
#108141,#108142,#108143,#108144,#108145,#108146,#108147,#108148,#108149,
#108150,#108151,#108152,#108153,#108154,#108155,#108156,#108157,#108158,
#108159,#108160,#108161,#108162,#108163,#108164,#108165,#108166,#108167,
#108168,#108169,#108170,#108171,#108172,#108173,#108174,#108175,#108176,
#108177,#108178,#108179,#108180,#108181,#108182,#108183,#108184,#108185,
#108186,#108187,#108188,#108189,#108190,#108191,#108192,#108193,#108194,
#108195,#108196,#108197,#108198,#108199,#108200,#108201,#108202,#108203,
#108204,#108205,#108206,#108207,#108208,#108209,#108210,#108211,#108212,
#108213,#108214,#108215,#108216,#108217,#108218,#108219,#108220,#108221,
#108222,#108223,#108224,#108225,#108226,#108227,#108228,#108229,#108230,
#108231,#108232,#108233,#108234,#108235,#108236,#108237,#108238),
 .UNSPECIFIED.,.F.,.F.,(4,3,3,3,3,3,3,3,3,3,3,3,3,3,3,3,3,3,3,3,3,3,3,3,
3,3,3,3,3,3,3,3,3,3,3,3,3,3,3,3,3,3,3,3,3,3,3,3,3,3,3,3,3,3,3,3,3,3,3,3,
3,3,3,3,3,3,3,3,3,3,3,3,3,4),(1247.21228347514,1247.28913076917,1247.37286948102,
1247.45650499238,1247.54005743578,1247.62354687163,1247.70700082225,1247.79043731609,
1247.87387442585,1247.95733022077,1248.0408747135,1248.12446379644,1248.20818706399,
1248.28886677989,1248.37260549174,1248.4562410031,1248.5397934465,1248.62328288235,
1248.70673683297,1248.79017332681,1248.87361043657,1248.95706623149,1249.04061072422,
1249.12419980716,1249.20792307471,1249.28860279061,1249.37234150246,1249.45597701382,
1249.53952945722,1249.62301889307,1249.70647284369,1249.78990933753,1249.87334644729,
1249.95680224221,1250.04034673494,1250.12393581788,1250.20765908543,1250.28833880133,
1250.37207751318,1250.45571302454,1250.53926546794,1250.62275490379,1250.70620885441,
1250.78964534825,1250.87308245801,1250.95653825293,1251.04008274566,1251.1236718286,
1251.20739509615,1251.28807481205,1251.3718135239,1251.45544903526,1251.53900147866,
1251.62249091451,1251.70594486513,1251.78938135897,1251.87281846873,1251.95627426365,
1252.03981875637,1252.12340783932,1252.20713110687,1252.28781082277,1252.37155200585,
1252.45518941628,1252.538743189,1252.62223338625,1252.70568523168,1252.78911881146,
1252.87255219775,1252.95600345858,1253.03953246102,1253.12310571945,1253.20678787449,
1253.24416667962),.UNSPECIFIED.);
#847=B_SPLINE_CURVE_WITH_KNOTS('',3,(#108244,#108245,#108246,#108247,#108248,
#108249,#108250,#108251,#108252,#108253,#108254,#108255,#108256,#108257,
#108258,#108259,#108260,#108261,#108262,#108263,#108264,#108265,#108266,
#108267,#108268,#108269,#108270,#108271,#108272,#108273,#108274,#108275,
#108276,#108277,#108278,#108279,#108280,#108281,#108282,#108283,#108284,
#108285,#108286,#108287,#108288,#108289,#108290,#108291,#108292,#108293,
#108294,#108295,#108296,#108297,#108298,#108299,#108300,#108301,#108302,
#108303,#108304,#108305,#108306,#108307,#108308,#108309,#108310,#108311,
#108312,#108313,#108314,#108315,#108316,#108317,#108318,#108319,#108320,
#108321,#108322,#108323,#108324,#108325,#108326,#108327,#108328,#108329,
#108330,#108331,#108332,#108333,#108334,#108335,#108336,#108337,#108338,
#108339,#108340,#108341,#108342,#108343,#108344,#108345,#108346,#108347,
#108348,#108349,#108350,#108351,#108352,#108353,#108354,#108355,#108356,
#108357,#108358,#108359,#108360,#108361,#108362,#108363,#108364,#108365,
#108366,#108367,#108368,#108369,#108370,#108371,#108372,#108373,#108374,
#108375,#108376,#108377,#108378,#108379,#108380,#108381,#108382,#108383,
#108384,#108385,#108386,#108387,#108388,#108389,#108390,#108391,#108392,
#108393,#108394,#108395,#108396,#108397,#108398,#108399,#108400,#108401,
#108402,#108403,#108404,#108405,#108406,#108407,#108408,#108409,#108410,
#108411,#108412,#108413,#108414,#108415,#108416,#108417,#108418,#108419,
#108420,#108421,#108422,#108423,#108424,#108425,#108426,#108427,#108428,
#108429,#108430,#108431,#108432,#108433,#108434,#108435,#108436,#108437,
#108438,#108439,#108440,#108441,#108442,#108443,#108444,#108445,#108446,
#108447,#108448,#108449,#108450,#108451,#108452,#108453,#108454,#108455,
#108456,#108457,#108458,#108459,#108460,#108461,#108462,#108463),
 .UNSPECIFIED.,.F.,.F.,(4,3,3,3,3,3,3,3,3,3,3,3,3,3,3,3,3,3,3,3,3,3,3,3,
3,3,3,3,3,3,3,3,3,3,3,3,3,3,3,3,3,3,3,3,3,3,3,3,3,3,3,3,3,3,3,3,3,3,3,3,
3,3,3,3,3,3,3,3,3,3,3,3,3,4),(1253.49546878246,1253.58356848739,1253.67180987813,
1253.76028410143,1253.8488844469,1253.93769136636,1253.97699222449,1254.06073093634,
1254.1443664477,1254.2279188911,1254.31140832695,1254.39486227757,1254.47829877141,
1254.56173588117,1254.64519167609,1254.72873616882,1254.81232525176,1254.89604851931,
1254.97672823521,1255.06046694706,1255.14410245842,1255.22765490182,1255.31114433767,
1255.39459828829,1255.47803478213,1255.56147189189,1255.64492768681,1255.72847217954,
1255.81206126248,1255.89578453003,1255.97646424593,1256.06020295778,1256.14383846914,
1256.22739091254,1256.31088034839,1256.39433429901,1256.47777079285,1256.56120790261,
1256.64466369753,1256.72820819026,1256.8117972732,1256.89552054075,1256.97620025665,
1257.0599389685,1257.14357447986,1257.22712692326,1257.31061635911,1257.39407030973,
1257.47750680357,1257.56094391333,1257.64439970825,1257.72794420098,1257.81153328392,
1257.89525655147,1257.97593626737,1258.05967497922,1258.14331049058,1258.22686293398,
1258.31035236983,1258.39380632045,1258.47724281429,1258.56067992405,1258.64413571897,
1258.7276802117,1258.81126929464,1258.89499256219,1258.97567227809,1259.05817906887,
1259.14058983644,1259.2229237848,1259.30519823839,1259.38743723984,1259.46967421915,
1259.52705322338),.UNSPECIFIED.);
#848=B_SPLINE_CURVE_WITH_KNOTS('',3,(#108464,#108465,#108466,#108467,#108468,
#108469,#108470,#108471,#108472,#108473),.UNSPECIFIED.,.F.,.F.,(4,3,3,4),
(1253.24510988801,1253.33203828523,1253.41883478726,1253.49546878231),
 .UNSPECIFIED.);
#849=B_SPLINE_CURVE_WITH_KNOTS('',3,(#108475,#108476,#108477,#108478,#108479,
#108480,#108481,#108482,#108483,#108484),.UNSPECIFIED.,.F.,.F.,(4,3,3,4),
(1253.24416667962,1253.28754683349,1253.40544243805,1253.49546878232),
 .UNSPECIFIED.);
#850=B_SPLINE_CURVE_WITH_KNOTS('',3,(#108485,#108486,#108487,#108488,#108489,
#108490,#108491,#108492,#108493,#108494,#108495,#108496,#108497,#108498,
#108499,#108500,#108501,#108502,#108503,#108504,#108505,#108506,#108507,
#108508,#108509,#108510,#108511,#108512,#108513,#108514,#108515,#108516,
#108517,#108518,#108519,#108520,#108521,#108522,#108523,#108524,#108525,
#108526,#108527,#108528,#108529,#108530,#108531,#108532,#108533,#108534,
#108535,#108536,#108537,#108538,#108539,#108540,#108541,#108542,#108543,
#108544,#108545,#108546,#108547,#108548,#108549,#108550,#108551,#108552,
#108553,#108554,#108555,#108556,#108557,#108558,#108559,#108560,#108561,
#108562,#108563,#108564,#108565,#108566,#108567,#108568,#108569,#108570,
#108571,#108572,#108573,#108574,#108575,#108576,#108577,#108578,#108579,
#108580,#108581,#108582,#108583,#108584,#108585,#108586,#108587,#108588,
#108589,#108590,#108591,#108592,#108593,#108594,#108595,#108596,#108597,
#108598,#108599,#108600,#108601,#108602,#108603,#108604,#108605,#108606,
#108607,#108608,#108609,#108610,#108611,#108612,#108613,#108614,#108615,
#108616,#108617,#108618,#108619,#108620,#108621,#108622,#108623,#108624,
#108625,#108626,#108627,#108628,#108629,#108630,#108631,#108632,#108633,
#108634,#108635,#108636,#108637,#108638,#108639,#108640,#108641,#108642,
#108643,#108644,#108645,#108646,#108647,#108648,#108649,#108650,#108651,
#108652,#108653,#108654,#108655,#108656,#108657,#108658,#108659,#108660,
#108661,#108662,#108663,#108664,#108665,#108666,#108667,#108668,#108669,
#108670,#108671,#108672,#108673,#108674,#108675,#108676,#108677,#108678,
#108679,#108680,#108681,#108682,#108683,#108684,#108685,#108686,#108687,
#108688,#108689,#108690,#108691,#108692,#108693,#108694,#108695,#108696,
#108697,#108698,#108699,#108700,#108701,#108702,#108703,#108704),
 .UNSPECIFIED.,.F.,.F.,(4,3,3,3,3,3,3,3,3,3,3,3,3,3,3,3,3,3,3,3,3,3,3,3,
3,3,3,3,3,3,3,3,3,3,3,3,3,3,3,3,3,3,3,3,3,3,3,3,3,3,3,3,3,3,3,3,3,3,3,3,
3,3,3,3,3,3,3,3,3,3,3,3,3,4),(1253.49546878247,1253.5778608269,1253.66018623466,
1253.74247225206,1253.82473938688,1253.90700663602,1253.9892929942,1254.07166470814,
1254.15408314902,1254.23662431146,1254.28728284421,1254.37102155606,1254.45465706742,
1254.53820951082,1254.62169894667,1254.70515289729,1254.78858939113,1254.87202650089,
1254.95548229581,1255.03902678854,1255.12261587148,1255.20633913903,1255.28701885493,
1255.37075756678,1255.45439307814,1255.53794552154,1255.62143495739,1255.70488890801,
1255.78832540185,1255.87176251161,1255.95521830653,1256.03876279926,1256.1223518822,
1256.20607514976,1256.28675486565,1256.3704935775,1256.45412908886,1256.53768153226,
1256.62117096811,1256.70462491873,1256.78806141257,1256.87149852233,1256.95495431725,
1257.03849880997,1257.12208789292,1257.20581116047,1257.28649087637,1257.37022958822,
1257.45386509958,1257.53741754298,1257.62090697883,1257.70436092945,1257.78779742329,
1257.87123453305,1257.95469032796,1258.03823482069,1258.12182390363,1258.20554717119,
1258.28622688709,1258.36996559894,1258.4536011103,1258.5371535537,1258.62064298955,
1258.70409694017,1258.78753343401,1258.87097054377,1258.95442633869,1259.03797083142,
1259.12155991436,1259.20528318192,1259.28596289781,1259.37430857112,1259.46245385434,
1259.52833516178),.UNSPECIFIED.);
#851=B_SPLINE_CURVE_WITH_KNOTS('',3,(#108710,#108711,#108712,#108713,#108714,
#108715,#108716,#108717,#108718,#108719,#108720,#108721,#108722,#108723,
#108724,#108725,#108726,#108727,#108728,#108729,#108730,#108731,#108732,
#108733,#108734,#108735,#108736,#108737,#108738,#108739,#108740,#108741,
#108742,#108743,#108744,#108745,#108746,#108747,#108748,#108749,#108750,
#108751,#108752,#108753,#108754,#108755,#108756,#108757,#108758,#108759,
#108760,#108761,#108762,#108763,#108764,#108765,#108766,#108767,#108768,
#108769,#108770,#108771,#108772,#108773,#108774,#108775,#108776,#108777,
#108778,#108779,#108780,#108781,#108782,#108783,#108784,#108785,#108786,
#108787,#108788,#108789,#108790,#108791,#108792,#108793,#108794,#108795,
#108796,#108797,#108798,#108799,#108800,#108801,#108802,#108803,#108804,
#108805,#108806,#108807,#108808,#108809,#108810,#108811,#108812,#108813,
#108814,#108815,#108816,#108817,#108818,#108819,#108820,#108821,#108822,
#108823,#108824,#108825,#108826,#108827,#108828,#108829,#108830,#108831,
#108832,#108833,#108834,#108835,#108836,#108837,#108838,#108839,#108840,
#108841,#108842,#108843,#108844,#108845,#108846,#108847,#108848,#108849,
#108850,#108851,#108852,#108853,#108854,#108855,#108856,#108857,#108858,
#108859,#108860,#108861,#108862,#108863,#108864,#108865,#108866,#108867,
#108868,#108869,#108870,#108871,#108872,#108873,#108874,#108875,#108876,
#108877,#108878,#108879,#108880,#108881,#108882,#108883,#108884,#108885,
#108886,#108887,#108888,#108889,#108890,#108891,#108892,#108893,#108894,
#108895,#108896,#108897,#108898,#108899,#108900,#108901,#108902,#108903,
#108904,#108905,#108906,#108907,#108908,#108909,#108910,#108911,#108912,
#108913,#108914,#108915,#108916,#108917,#108918,#108919,#108920,#108921,
#108922,#108923,#108924,#108925,#108926),.UNSPECIFIED.,.F.,.F.,(4,3,3,3,
3,3,3,3,3,3,3,3,3,3,3,3,3,3,3,3,3,3,3,3,3,3,3,3,3,3,3,3,3,3,3,3,3,3,3,3,
3,3,3,3,3,3,3,3,3,3,3,3,3,3,3,3,3,3,3,3,3,3,3,3,3,3,3,3,3,3,3,3,4),(1259.77865408949,
1259.89986585675,1259.97540828881,1260.05914700066,1260.14278251202,1260.22633495542,
1260.30982439127,1260.39327834189,1260.47671483573,1260.56015194549,1260.64360774041,
1260.72715223314,1260.81074131608,1260.89446458363,1260.97514429953,1261.05888301138,
1261.14251852274,1261.22607096614,1261.30956040199,1261.39301435261,1261.47645084645,
1261.55988795621,1261.64334375113,1261.72688824386,1261.8104773268,1261.89420059435,
1261.97488031025,1262.0586190221,1262.14225453346,1262.22580697686,1262.30929641271,
1262.39275036333,1262.47618685717,1262.55962396693,1262.64307976185,1262.72662425458,
1262.81021333752,1262.89393660507,1262.97461632097,1263.05835503282,1263.14199054418,
1263.22554298758,1263.30903242343,1263.39248637405,1263.47592286789,1263.55935997765,
1263.64281577257,1263.7263602653,1263.80994934824,1263.89367261579,1263.97435233169,
1264.05809104354,1264.1417265549,1264.2252789983,1264.30876843415,1264.39222238477,
1264.47565887861,1264.55909598837,1264.64255178329,1264.72609627602,1264.80968535896,
1264.89340862651,1264.97408834241,1265.05783681461,1265.14147992778,1265.22506980479,
1265.30855615695,1265.39200391737,1265.47543117534,1265.55912311748,1265.64258917631,
1265.72639406011,1265.81019894391),.UNSPECIFIED.);
#852=B_SPLINE_CURVE_WITH_KNOTS('',3,(#108927,#108928,#108929,#108930,#108931,
#108932,#108933,#108934,#108935,#108936),.UNSPECIFIED.,.F.,.F.,(4,3,3,4),
(1259.52705322338,1259.60932548456,1259.69398978697,1259.77865408938),
 .UNSPECIFIED.);
#853=B_SPLINE_CURVE_WITH_KNOTS('',3,(#108938,#108939,#108940,#108941,#108942,
#108943,#108944,#108945,#108946,#108947),.UNSPECIFIED.,.F.,.F.,(4,3,3,4),
(1259.52833516178,1259.61621838343,1259.70392677093,1259.77865408939),
 .UNSPECIFIED.);
#854=B_SPLINE_CURVE_WITH_KNOTS('',3,(#108948,#108949,#108950,#108951,#108952,
#108953,#108954,#108955,#108956,#108957,#108958,#108959,#108960,#108961,
#108962,#108963,#108964,#108965,#108966,#108967,#108968,#108969,#108970,
#108971,#108972,#108973,#108974,#108975,#108976,#108977,#108978,#108979,
#108980,#108981,#108982,#108983,#108984,#108985,#108986,#108987,#108988,
#108989,#108990,#108991,#108992,#108993,#108994,#108995,#108996,#108997,
#108998,#108999,#109000,#109001,#109002,#109003,#109004,#109005,#109006,
#109007,#109008,#109009,#109010,#109011,#109012,#109013,#109014,#109015,
#109016,#109017,#109018,#109019,#109020,#109021,#109022,#109023,#109024,
#109025,#109026,#109027,#109028,#109029,#109030,#109031,#109032,#109033,
#109034,#109035,#109036,#109037,#109038,#109039,#109040,#109041,#109042,
#109043,#109044,#109045,#109046,#109047,#109048,#109049,#109050,#109051,
#109052,#109053,#109054,#109055,#109056,#109057,#109058,#109059,#109060,
#109061,#109062,#109063,#109064,#109065,#109066,#109067,#109068,#109069,
#109070,#109071,#109072,#109073,#109074,#109075,#109076,#109077,#109078,
#109079,#109080,#109081,#109082,#109083,#109084,#109085,#109086,#109087,
#109088,#109089,#109090,#109091,#109092,#109093,#109094,#109095,#109096,
#109097,#109098,#109099,#109100,#109101,#109102,#109103,#109104,#109105,
#109106,#109107,#109108,#109109,#109110,#109111,#109112,#109113,#109114,
#109115,#109116,#109117,#109118,#109119,#109120,#109121,#109122,#109123,
#109124,#109125,#109126,#109127,#109128,#109129,#109130,#109131,#109132,
#109133,#109134,#109135,#109136,#109137,#109138,#109139,#109140,#109141,
#109142,#109143,#109144,#109145,#109146,#109147,#109148,#109149,#109150,
#109151,#109152,#109153,#109154,#109155,#109156,#109157,#109158,#109159,
#109160,#109161,#109162,#109163,#109164,#109165,#109166,#109167),
 .UNSPECIFIED.,.F.,.F.,(4,3,3,3,3,3,3,3,3,3,3,3,3,3,3,3,3,3,3,3,3,3,3,3,
3,3,3,3,3,3,3,3,3,3,3,3,3,3,3,3,3,3,3,3,3,3,3,3,3,3,3,3,3,3,3,3,3,3,3,3,
3,3,3,3,3,3,3,3,3,3,3,3,3,4),(1259.7786540895,1259.86580253005,1259.95305673141,
1260.04050848855,1260.1280632794,1260.21581764344,1260.28569890853,1260.36943762038,
1260.45307313174,1260.53662557514,1260.62011501099,1260.70356896161,1260.78700545545,
1260.87044256521,1260.95389836013,1261.03744285286,1261.1210319358,1261.20475520335,
1261.28543491925,1261.3691736311,1261.45280914246,1261.53636158586,1261.61985102171,
1261.70330497233,1261.78674146617,1261.87017857593,1261.95363437085,1262.03717886358,
1262.12076794652,1262.20449121408,1262.28517092997,1262.36890964182,1262.45254515318,
1262.53609759658,1262.61958703243,1262.70304098305,1262.78647747689,1262.86991458665,
1262.95337038157,1263.0369148743,1263.12050395724,1263.20422722479,1263.28490694069,
1263.36864565254,1263.4522811639,1263.5358336073,1263.61932304315,1263.70277699377,
1263.78621348761,1263.86965059737,1263.95310639228,1264.03665088501,1264.12023996795,
1264.20396323551,1264.28464295141,1264.36838166326,1264.45201717462,1264.53556961802,
1264.61905905387,1264.70251300449,1264.78594949833,1264.86938660809,1264.95284240301,
1265.03638689574,1265.11997597868,1265.20369924624,1265.28437896213,1265.36697886756,
1265.44948184649,1265.53190704803,1265.61426948393,1265.69659579727,1265.7789125969,
1265.81034593635),.UNSPECIFIED.);
#855=B_SPLINE_CURVE_WITH_KNOTS('',3,(#109173,#109174,#109175,#109176,#109177,
#109178,#109179,#109180,#109181,#109182,#109183,#109184,#109185,#109186,
#109187,#109188,#109189,#109190,#109191,#109192,#109193,#109194,#109195,
#109196,#109197,#109198,#109199,#109200,#109201,#109202,#109203,#109204,
#109205,#109206,#109207,#109208,#109209,#109210,#109211,#109212,#109213,
#109214,#109215,#109216,#109217,#109218,#109219,#109220,#109221,#109222,
#109223,#109224,#109225,#109226,#109227,#109228,#109229,#109230,#109231,
#109232,#109233,#109234,#109235,#109236,#109237,#109238,#109239,#109240,
#109241,#109242,#109243,#109244,#109245,#109246,#109247,#109248,#109249,
#109250,#109251,#109252,#109253,#109254,#109255,#109256,#109257,#109258,
#109259,#109260,#109261,#109262,#109263,#109264,#109265,#109266,#109267,
#109268,#109269,#109270,#109271,#109272,#109273,#109274,#109275,#109276,
#109277,#109278,#109279,#109280,#109281,#109282,#109283,#109284,#109285,
#109286,#109287,#109288,#109289,#109290,#109291,#109292,#109293,#109294,
#109295,#109296,#109297,#109298,#109299,#109300,#109301,#109302,#109303,
#109304,#109305,#109306,#109307,#109308,#109309,#109310,#109311,#109312,
#109313,#109314,#109315,#109316,#109317,#109318,#109319,#109320,#109321,
#109322,#109323,#109324,#109325,#109326,#109327,#109328,#109329,#109330,
#109331,#109332,#109333,#109334,#109335,#109336,#109337,#109338,#109339,
#109340,#109341,#109342,#109343,#109344,#109345,#109346,#109347,#109348,
#109349,#109350,#109351,#109352,#109353,#109354,#109355,#109356,#109357,
#109358,#109359,#109360,#109361,#109362,#109363,#109364,#109365,#109366,
#109367,#109368,#109369,#109370,#109371,#109372,#109373,#109374,#109375,
#109376,#109377,#109378,#109379,#109380,#109381,#109382,#109383,#109384,
#109385,#109386,#109387,#109388,#109389,#109390,#109391,#109392),
 .UNSPECIFIED.,.F.,.F.,(4,3,3,3,3,3,3,3,3,3,3,3,3,3,3,3,3,3,3,3,3,3,3,3,
3,3,3,3,3,3,3,3,3,3,3,3,3,3,3,3,3,3,3,3,3,3,3,3,3,3,3,3,3,3,3,3,3,3,3,3,
3,3,3,3,3,3,3,3,3,3,3,3,3,4),(1266.0618393968,1266.14456729323,1266.22720047119,
1266.30975992534,1266.39273498016,1266.47521984589,1266.55769815155,1266.6401887541,
1266.72353165653,1266.80614558457,1266.88985297421,1266.97356036385,1267.0572990757,
1267.14093458706,1267.22448703046,1267.30797646631,1267.39143041693,1267.47486691078,
1267.55830402053,1267.64175981545,1267.72530430818,1267.80889339112,1267.89261665868,
1267.97329637458,1268.05703508643,1268.14067059779,1268.22422304119,1268.30771247704,
1268.39116642766,1268.47460292151,1268.55804003126,1268.64149582618,1268.72504031891,
1268.80862940185,1268.89235266941,1268.9730323853,1269.05677109715,1269.14040660851,
1269.22395905191,1269.30744848776,1269.39090243838,1269.47433893222,1269.55777604198,
1269.64123183689,1269.72477632962,1269.80836541256,1269.89208868012,1269.97276839602,
1270.05650710787,1270.14014261923,1270.22369506263,1270.30718449848,1270.3906384491,
1270.47407494294,1270.5575120527,1270.64096784762,1270.72451234035,1270.80810142329,
1270.89182469085,1270.97250440674,1271.05624311859,1271.13987862995,1271.22343107335,
1271.3069205092,1271.39037445982,1271.47381095366,1271.55724806342,1271.64070385833,
1271.72424835106,1271.80783743401,1271.89156070156,1271.97224041746,1272.06735135149,
1272.09457507867),.UNSPECIFIED.);
#856=B_SPLINE_CURVE_WITH_KNOTS('',3,(#109393,#109394,#109395,#109396,#109397,
#109398,#109399,#109400,#109401,#109402),.UNSPECIFIED.,.F.,.F.,(4,3,3,4),
(1265.81019894391,1265.89392247301,1265.97382435313,1266.06183939667),
 .UNSPECIFIED.);
#857=B_SPLINE_CURVE_WITH_KNOTS('',3,(#109404,#109405,#109406,#109407,#109408,
#109409,#109410,#109411,#109412,#109413),.UNSPECIFIED.,.F.,.F.,(4,3,3,4),
(1265.81034593635,1265.89269204904,1265.9772657228,1266.06183939655),
 .UNSPECIFIED.);
#858=B_SPLINE_CURVE_WITH_KNOTS('',3,(#109414,#109415,#109416,#109417,#109418,
#109419,#109420,#109421,#109422,#109423,#109424,#109425,#109426,#109427,
#109428,#109429,#109430,#109431,#109432,#109433,#109434,#109435,#109436,
#109437,#109438,#109439,#109440,#109441,#109442,#109443,#109444,#109445,
#109446,#109447,#109448,#109449,#109450,#109451,#109452,#109453,#109454,
#109455,#109456,#109457,#109458,#109459,#109460,#109461,#109462,#109463,
#109464,#109465,#109466,#109467,#109468,#109469,#109470,#109471,#109472,
#109473,#109474,#109475,#109476,#109477,#109478,#109479,#109480,#109481,
#109482,#109483,#109484,#109485,#109486,#109487,#109488,#109489,#109490,
#109491,#109492,#109493,#109494,#109495,#109496,#109497,#109498,#109499,
#109500,#109501,#109502,#109503,#109504,#109505,#109506,#109507,#109508,
#109509,#109510,#109511,#109512,#109513,#109514,#109515,#109516,#109517,
#109518,#109519,#109520,#109521,#109522,#109523,#109524,#109525,#109526,
#109527,#109528,#109529,#109530,#109531,#109532,#109533,#109534,#109535,
#109536,#109537,#109538,#109539,#109540,#109541,#109542,#109543,#109544,
#109545,#109546,#109547,#109548,#109549,#109550,#109551,#109552,#109553,
#109554,#109555,#109556,#109557,#109558,#109559,#109560,#109561,#109562,
#109563,#109564,#109565,#109566,#109567,#109568,#109569,#109570,#109571,
#109572,#109573,#109574,#109575,#109576,#109577,#109578,#109579,#109580,
#109581,#109582,#109583,#109584,#109585,#109586,#109587,#109588,#109589,
#109590,#109591,#109592,#109593,#109594,#109595,#109596,#109597,#109598,
#109599,#109600,#109601,#109602,#109603,#109604,#109605,#109606,#109607,
#109608,#109609,#109610,#109611,#109612,#109613,#109614,#109615,#109616,
#109617,#109618,#109619,#109620,#109621,#109622,#109623,#109624,#109625,
#109626,#109627,#109628,#109629,#109630),.UNSPECIFIED.,.F.,.F.,(4,3,3,3,
3,3,3,3,3,3,3,3,3,3,3,3,3,3,3,3,3,3,3,3,3,3,3,3,3,3,3,3,3,3,3,3,3,3,3,3,
3,3,3,3,3,3,3,3,3,3,3,3,3,3,3,3,3,3,3,3,3,3,3,3,3,3,3,3,3,3,3,3,4),(1266.06183939668,
1266.17607577489,1266.28411497285,1266.3678536847,1266.45148919606,1266.53504163946,
1266.61853107531,1266.70198502593,1266.78542151977,1266.86885862953,1266.95231442445,
1267.03585891718,1267.11944800012,1267.20317126767,1267.28385098357,1267.36758969542,
1267.45122520678,1267.53477765018,1267.61826708603,1267.70172103665,1267.78515753049,
1267.86859464025,1267.95205043517,1268.0355949279,1268.11918401084,1268.2029072784,
1268.28358699429,1268.36732570614,1268.4509612175,1268.5345136609,1268.61800309675,
1268.70145704737,1268.78489354121,1268.86833065097,1268.95178644589,1269.03533093862,
1269.11892002156,1269.20264328912,1269.28332300501,1269.36706171686,1269.45069722822,
1269.53424967162,1269.61773910747,1269.70119305809,1269.78462955193,1269.86806666169,
1269.95152245661,1270.03506694934,1270.11865603228,1270.20237929983,1270.28305901573,
1270.36679772758,1270.45043323894,1270.53398568234,1270.61747511819,1270.70092906881,
1270.78436556265,1270.86780267241,1270.95125846732,1271.03480296005,1271.11839204299,
1271.20211531055,1271.28279502645,1271.36654513006,1271.45018953759,1271.53373305985,
1271.61721938338,1271.70066662803,1271.78409288349,1271.86754205725,1271.951001946,
1272.03452978899,1272.09336375077),.UNSPECIFIED.);
#859=B_SPLINE_CURVE_WITH_KNOTS('',3,(#109636,#109637,#109638,#109639,#109640,
#109641,#109642,#109643,#109644,#109645),.UNSPECIFIED.,.F.,.F.,(4,1,1,1,
1,1,1,4),(1272.34502470385,1272.97197642818,1273.9717124389,1274.97144844962,
1275.97118446034,1276.97092047106,1277.97065648178,1278.37762693477),
 .UNSPECIFIED.);
#860=B_SPLINE_CURVE_WITH_KNOTS('',3,(#109646,#109647,#109648,#109649,#109650,
#109651,#109652,#109653,#109654,#109655),.UNSPECIFIED.,.F.,.F.,(4,3,3,4),
(1272.09457507867,1272.1891593872,1272.28317223907,1272.34502470385),
 .UNSPECIFIED.);
#861=B_SPLINE_CURVE_WITH_KNOTS('',3,(#109657,#109658,#109659,#109660,#109661,
#109662,#109663,#109664,#109665,#109666,#109667,#109668,#109669),
 .UNSPECIFIED.,.F.,.F.,(4,3,3,3,4),(1272.09336375077,1272.17699396813,1272.26074192364,
1272.28253103717,1272.34502470386),.UNSPECIFIED.);
#862=B_SPLINE_CURVE_WITH_KNOTS('',3,(#109670,#109671,#109672,#109673,#109674,
#109675,#109676,#109677,#109678,#109679,#109680,#109681,#109682,#109683,
#109684,#109685,#109686,#109687,#109688,#109689,#109690,#109691,#109692,
#109693,#109694,#109695,#109696,#109697,#109698,#109699,#109700,#109701,
#109702,#109703,#109704,#109705,#109706,#109707,#109708,#109709,#109710,
#109711,#109712,#109713,#109714,#109715,#109716,#109717,#109718,#109719,
#109720,#109721,#109722,#109723,#109724,#109725,#109726,#109727,#109728,
#109729,#109730,#109731,#109732,#109733,#109734,#109735,#109736,#109737,
#109738,#109739,#109740,#109741,#109742,#109743,#109744,#109745,#109746,
#109747,#109748,#109749,#109750,#109751,#109752,#109753,#109754,#109755,
#109756,#109757,#109758,#109759,#109760,#109761,#109762,#109763,#109764,
#109765,#109766,#109767,#109768,#109769,#109770,#109771,#109772,#109773,
#109774,#109775,#109776,#109777,#109778,#109779,#109780,#109781,#109782,
#109783,#109784,#109785,#109786,#109787,#109788,#109789,#109790,#109791,
#109792,#109793,#109794,#109795,#109796,#109797,#109798,#109799,#109800,
#109801,#109802,#109803,#109804,#109805,#109806,#109807,#109808,#109809,
#109810,#109811,#109812,#109813,#109814,#109815,#109816,#109817,#109818,
#109819,#109820,#109821,#109822,#109823,#109824,#109825,#109826,#109827,
#109828,#109829,#109830,#109831,#109832,#109833,#109834,#109835,#109836,
#109837,#109838,#109839,#109840,#109841,#109842,#109843,#109844,#109845,
#109846,#109847,#109848,#109849,#109850,#109851,#109852,#109853,#109854,
#109855,#109856,#109857,#109858,#109859,#109860,#109861,#109862,#109863,
#109864,#109865,#109866,#109867,#109868,#109869,#109870,#109871,#109872,
#109873,#109874,#109875,#109876,#109877,#109878,#109879,#109880,#109881,
#109882,#109883,#109884,#109885,#109886,#109887,#109888,#109889),
 .UNSPECIFIED.,.F.,.F.,(4,3,3,3,3,3,3,3,3,3,3,3,3,3,3,3,3,3,3,3,3,3,3,3,
3,3,3,3,3,3,3,3,3,3,3,3,3,3,3,3,3,3,3,3,3,3,3,3,3,3,3,3,3,3,3,3,3,3,3,3,
3,3,3,3,3,3,3,3,3,3,3,3,3,4),(1272.34502470398,1272.42797828084,1272.51083333015,
1272.59361069634,1272.67969274028,1272.76238540205,1272.84506816948,1272.92775975624,
1273.0104788794,1273.09328870338,1273.17615229585,1273.25913255471,1273.28226704789,
1273.36600575974,1273.4496412711,1273.5331937145,1273.61668315035,1273.70013710097,
1273.78357359481,1273.86701070457,1273.95046649948,1274.03401099221,1274.11760007515,
1274.20132334271,1274.28200305861,1274.36574177046,1274.44937728182,1274.53292972522,
1274.61641916107,1274.69987311169,1274.78330960553,1274.86674671529,1274.95020251021,
1275.03374700294,1275.11733608588,1275.20105935344,1275.28173906933,1275.36547778118,
1275.44911329254,1275.53266573594,1275.61615517179,1275.69960912241,1275.78304561625,
1275.86648272601,1275.94993852093,1276.03348301366,1276.1170720966,1276.20079536415,
1276.28147508005,1276.3652137919,1276.44884930326,1276.53240174666,1276.61589118251,
1276.69934513313,1276.78278162697,1276.86621873673,1276.94967453164,1277.03321902437,
1277.11680810731,1277.20053137487,1277.28121109077,1277.36494980262,1277.44858531398,
1277.53213775738,1277.61562719323,1277.69908114385,1277.78251763769,1277.86595474745,
1277.94941054237,1278.0329550351,1278.11654411804,1278.2002673856,1278.28094710149,
1278.37766493651),.UNSPECIFIED.);
#863=B_SPLINE_CURVE_WITH_KNOTS('',3,(#109895,#109896,#109897,#109898,#109899,
#109900,#109901,#109902,#109903,#109904,#109905,#109906,#109907,#109908,
#109909,#109910,#109911,#109912,#109913,#109914,#109915,#109916,#109917,
#109918,#109919,#109920,#109921,#109922,#109923,#109924,#109925,#109926,
#109927,#109928,#109929,#109930,#109931,#109932,#109933,#109934,#109935,
#109936,#109937,#109938,#109939,#109940,#109941,#109942,#109943,#109944,
#109945,#109946,#109947,#109948,#109949,#109950,#109951,#109952,#109953,
#109954,#109955,#109956,#109957,#109958,#109959,#109960,#109961,#109962,
#109963,#109964,#109965,#109966,#109967,#109968,#109969,#109970,#109971,
#109972,#109973,#109974,#109975,#109976,#109977,#109978,#109979,#109980,
#109981,#109982,#109983,#109984,#109985,#109986,#109987,#109988,#109989,
#109990,#109991,#109992,#109993,#109994,#109995,#109996,#109997,#109998,
#109999,#110000,#110001,#110002,#110003,#110004,#110005,#110006,#110007,
#110008,#110009,#110010,#110011,#110012,#110013,#110014,#110015,#110016,
#110017,#110018,#110019,#110020,#110021,#110022,#110023,#110024,#110025,
#110026,#110027,#110028,#110029,#110030,#110031,#110032,#110033,#110034,
#110035,#110036,#110037,#110038,#110039,#110040,#110041,#110042,#110043,
#110044,#110045,#110046,#110047,#110048,#110049,#110050,#110051,#110052,
#110053,#110054,#110055,#110056,#110057,#110058,#110059,#110060,#110061,
#110062,#110063,#110064,#110065,#110066,#110067,#110068,#110069,#110070,
#110071,#110072,#110073,#110074,#110075,#110076,#110077,#110078,#110079,
#110080,#110081,#110082,#110083,#110084,#110085,#110086,#110087,#110088,
#110089,#110090,#110091,#110092,#110093,#110094,#110095,#110096,#110097,
#110098,#110099,#110100,#110101,#110102,#110103,#110104,#110105,#110106,
#110107,#110108,#110109,#110110,#110111,#110112,#110113,#110114),
 .UNSPECIFIED.,.F.,.F.,(4,3,3,3,3,3,3,3,3,3,3,3,3,3,3,3,3,3,3,3,3,3,3,3,
3,3,3,3,3,3,3,3,3,3,3,3,3,3,3,3,3,3,3,3,3,3,3,3,3,3,3,3,3,3,3,3,3,3,3,3,
3,3,3,3,3,3,3,3,3,3,3,3,3,4),(1278.62821001103,1278.72467799427,1278.82166768971,
1278.91929630639,1278.9703924925,1279.05413120435,1279.13776671571,1279.22131915911,
1279.30480859496,1279.38826254558,1279.47169903942,1279.55513614918,1279.6385919441,
1279.72213643683,1279.80572551977,1279.88944878732,1279.97012850322,1280.05386721507,
1280.13750272643,1280.22105516983,1280.30454460568,1280.3879985563,1280.47143505014,
1280.5548721599,1280.63832795481,1280.72187244754,1280.80546153048,1280.88918479804,
1280.96986451394,1281.05360322579,1281.13723873715,1281.22079118055,1281.3042806164,
1281.38773456702,1281.47117106086,1281.55460817062,1281.63806396554,1281.72160845827,
1281.80519754121,1281.88892080876,1281.96960052466,1282.05333923651,1282.13697474787,
1282.22052719127,1282.30401662712,1282.38747057774,1282.47090707158,1282.55434418134,
1282.63779997626,1282.72134446899,1282.80493355193,1282.88865681949,1282.96933653538,
1283.05307524723,1283.13671075859,1283.22026320199,1283.30375263784,1283.38720658846,
1283.4706430823,1283.55408019206,1283.63753598698,1283.7210804797,1283.80466956265,
1283.8883928302,1283.9690725461,1284.05538577409,1284.13829069336,1284.22112063752,
1284.30389438199,1284.38663065551,1284.46936215526,1284.55209155376,1284.63485816459,
1284.65957836999),.UNSPECIFIED.);
#864=B_SPLINE_CURVE_WITH_KNOTS('',3,(#110115,#110116,#110117,#110118),
 .UNSPECIFIED.,.F.,.F.,(4,4),(1278.37762693477,1278.62821001103),
 .UNSPECIFIED.);
#865=B_SPLINE_CURVE_WITH_KNOTS('',3,(#110120,#110121,#110122,#110123,#110124,
#110125,#110126,#110127,#110128,#110129),.UNSPECIFIED.,.F.,.F.,(4,3,3,4),
(1278.37766493651,1278.47437986099,1278.5703538529,1278.62821001085),
 .UNSPECIFIED.);
#866=B_SPLINE_CURVE_WITH_KNOTS('',3,(#110130,#110131,#110132,#110133,#110134,
#110135,#110136,#110137,#110138,#110139,#110140,#110141,#110142,#110143,
#110144,#110145,#110146,#110147,#110148,#110149,#110150,#110151,#110152,
#110153,#110154,#110155,#110156,#110157,#110158,#110159,#110160,#110161,
#110162,#110163,#110164,#110165,#110166,#110167,#110168,#110169,#110170,
#110171,#110172,#110173,#110174,#110175,#110176,#110177,#110178,#110179,
#110180,#110181,#110182,#110183,#110184,#110185,#110186,#110187,#110188,
#110189,#110190,#110191,#110192,#110193,#110194,#110195,#110196,#110197,
#110198,#110199,#110200,#110201,#110202,#110203,#110204,#110205,#110206,
#110207,#110208,#110209,#110210,#110211,#110212,#110213,#110214,#110215,
#110216,#110217,#110218,#110219,#110220,#110221,#110222,#110223,#110224,
#110225,#110226,#110227,#110228,#110229,#110230,#110231,#110232,#110233,
#110234,#110235,#110236,#110237,#110238,#110239,#110240,#110241,#110242,
#110243,#110244,#110245,#110246,#110247,#110248,#110249,#110250,#110251,
#110252,#110253,#110254,#110255,#110256,#110257,#110258,#110259,#110260,
#110261,#110262,#110263,#110264,#110265,#110266,#110267,#110268,#110269,
#110270,#110271,#110272,#110273,#110274,#110275,#110276,#110277,#110278,
#110279,#110280,#110281,#110282,#110283,#110284,#110285,#110286,#110287,
#110288,#110289,#110290,#110291,#110292,#110293,#110294,#110295,#110296,
#110297,#110298,#110299,#110300,#110301,#110302,#110303,#110304,#110305,
#110306,#110307,#110308,#110309,#110310,#110311,#110312,#110313,#110314,
#110315,#110316,#110317,#110318,#110319,#110320,#110321,#110322,#110323,
#110324,#110325,#110326,#110327,#110328,#110329,#110330,#110331,#110332,
#110333,#110334,#110335,#110336,#110337,#110338,#110339,#110340,#110341,
#110342,#110343,#110344,#110345,#110346,#110347,#110348,#110349),
 .UNSPECIFIED.,.F.,.F.,(4,3,3,3,3,3,3,3,3,3,3,3,3,3,3,3,3,3,3,3,3,3,3,3,
3,3,3,3,3,3,3,3,3,3,3,3,3,3,3,3,3,3,3,3,3,3,3,3,3,3,3,3,3,3,3,3,3,3,3,3,
3,3,3,3,3,3,3,3,3,3,3,3,3,4),(1278.62821001104,1278.71180280317,1278.79538865517,
1278.87898538376,1278.96261080889,1279.04633640373,1279.13011489048,1279.21403165939,
1279.28068311221,1279.36442182406,1279.44805733542,1279.53160977882,1279.61509921467,
1279.69855316529,1279.78198965913,1279.86542676889,1279.9488825638,1280.03242705653,
1280.11601613947,1280.19973940703,1280.28041912293,1280.36415783478,1280.44779334614,
1280.53134578954,1280.61483522539,1280.69828917601,1280.78172566985,1280.86516277961,
1280.94861857453,1281.03216306726,1281.1157521502,1281.19947541776,1281.28015513365,
1281.3638938455,1281.44752935686,1281.53108180026,1281.61457123611,1281.69802518673,
1281.78146168057,1281.86489879033,1281.94835458525,1282.03189907798,1282.11548816092,
1282.19921142847,1282.27989114437,1282.36362985622,1282.44726536758,1282.53081781098,
1282.61430724683,1282.69776119744,1282.78119769129,1282.86463480105,1282.94809059596,
1283.03163508869,1283.11522417163,1283.19894743919,1283.27962715509,1283.36336586694,
1283.4470013783,1283.5305538217,1283.61404325755,1283.69749720817,1283.78093370202,
1283.86437081177,1283.94782660669,1284.03137109942,1284.11496018236,1284.19868344992,
1284.27936316581,1284.36367880853,1284.44785281671,1284.53194515319,1284.61595840221,
1284.6606315684),.UNSPECIFIED.);
#867=B_SPLINE_CURVE_WITH_KNOTS('',3,(#110355,#110356,#110357,#110358,#110359,
#110360,#110361,#110362,#110363,#110364,#110365,#110366,#110367,#110368,
#110369,#110370,#110371,#110372,#110373,#110374,#110375,#110376,#110377,
#110378,#110379,#110380,#110381,#110382,#110383,#110384,#110385,#110386,
#110387,#110388,#110389,#110390,#110391,#110392,#110393,#110394,#110395,
#110396,#110397,#110398,#110399,#110400,#110401,#110402,#110403,#110404,
#110405,#110406,#110407,#110408,#110409,#110410,#110411,#110412,#110413,
#110414,#110415,#110416,#110417,#110418,#110419,#110420,#110421,#110422,
#110423,#110424,#110425,#110426,#110427,#110428,#110429,#110430,#110431,
#110432,#110433,#110434,#110435,#110436,#110437,#110438,#110439,#110440,
#110441,#110442,#110443,#110444,#110445,#110446,#110447,#110448,#110449,
#110450,#110451,#110452,#110453,#110454,#110455,#110456,#110457,#110458,
#110459,#110460,#110461,#110462,#110463,#110464,#110465,#110466,#110467,
#110468,#110469,#110470,#110471,#110472,#110473,#110474,#110475,#110476,
#110477,#110478,#110479,#110480,#110481,#110482,#110483,#110484,#110485,
#110486,#110487,#110488,#110489,#110490,#110491,#110492,#110493,#110494,
#110495,#110496,#110497,#110498,#110499,#110500,#110501,#110502,#110503,
#110504,#110505,#110506,#110507,#110508,#110509,#110510,#110511,#110512,
#110513,#110514,#110515,#110516,#110517,#110518,#110519,#110520,#110521,
#110522,#110523,#110524,#110525,#110526,#110527,#110528,#110529,#110530,
#110531,#110532,#110533,#110534,#110535,#110536,#110537,#110538,#110539,
#110540,#110541,#110542,#110543,#110544,#110545,#110546,#110547,#110548,
#110549,#110550,#110551,#110552,#110553,#110554,#110555,#110556,#110557,
#110558,#110559,#110560,#110561,#110562,#110563,#110564,#110565,#110566,
#110567,#110568,#110569,#110570,#110571,#110572,#110573,#110574),
 .UNSPECIFIED.,.F.,.F.,(4,3,3,3,3,3,3,3,3,3,3,3,3,3,3,3,3,3,3,3,3,3,3,3,
3,3,3,3,3,3,3,3,3,3,3,3,3,3,3,3,3,3,3,3,3,3,3,3,3,3,3,3,3,3,3,3,3,3,3,3,
3,3,3,3,3,3,3,3,3,3,3,3,3,4),(1284.91139531821,1284.96880855682,1285.05254726867,
1285.13618278003,1285.21973522343,1285.30322465928,1285.3866786099,1285.47011510374,
1285.5535522135,1285.63700800842,1285.72055250115,1285.80414158409,1285.88786485164,
1285.96854456754,1286.05228327939,1286.13591879075,1286.21947123415,1286.30296067,
1286.38641462062,1286.46985111446,1286.55328822422,1286.63674401913,1286.72028851186,
1286.8038775948,1286.88760086236,1286.96828057826,1287.05201929011,1287.13565480147,
1287.21920724487,1287.30269668072,1287.38615063134,1287.46958712518,1287.55302423494,
1287.63648002986,1287.72002452259,1287.80361360553,1287.88733687308,1287.96801658898,
1288.05175530083,1288.13539081219,1288.21894325559,1288.30243269144,1288.38588664206,
1288.4693231359,1288.55276024566,1288.63621604058,1288.71976053331,1288.80334961625,
1288.8870728838,1288.9677525997,1289.05149131155,1289.13512682291,1289.21867926631,
1289.30216870216,1289.38562265278,1289.46905914662,1289.55249625638,1289.6359520513,
1289.71949654403,1289.80308562697,1289.88680889453,1289.96748861042,1290.05122867041,
1290.13486521538,1290.21841837917,1290.30190822321,1290.38536097487,1290.46879582508,
1290.55223084623,1290.63568410688,1290.71921991751,1290.80280013459,1290.88650013742,
1290.9433767908),.UNSPECIFIED.);
#868=B_SPLINE_CURVE_WITH_KNOTS('',3,(#110575,#110576,#110577,#110578,#110579,
#110580,#110581,#110582,#110583,#110584),.UNSPECIFIED.,.F.,.F.,(4,3,3,4),
(1284.65957836999,1284.74243553485,1284.82691542648,1284.9113953181),
 .UNSPECIFIED.);
#869=B_SPLINE_CURVE_WITH_KNOTS('',3,(#110586,#110587,#110588,#110589,#110590,
#110591,#110592,#110593,#110594,#110595),.UNSPECIFIED.,.F.,.F.,(4,3,3,4),
(1284.6606315684,1284.74457477385,1284.82850997582,1284.91139531822),
 .UNSPECIFIED.);
#870=B_SPLINE_CURVE_WITH_KNOTS('',3,(#110596,#110597,#110598,#110599,#110600,
#110601,#110602,#110603,#110604,#110605,#110606,#110607,#110608,#110609,
#110610,#110611,#110612,#110613,#110614,#110615,#110616,#110617,#110618,
#110619,#110620,#110621,#110622,#110623,#110624,#110625,#110626,#110627,
#110628,#110629,#110630,#110631,#110632,#110633,#110634,#110635,#110636,
#110637,#110638,#110639,#110640,#110641,#110642,#110643,#110644,#110645,
#110646,#110647,#110648,#110649,#110650,#110651,#110652,#110653,#110654,
#110655,#110656,#110657,#110658,#110659,#110660,#110661,#110662,#110663,
#110664,#110665,#110666,#110667,#110668,#110669,#110670,#110671,#110672,
#110673,#110674,#110675,#110676,#110677,#110678,#110679,#110680,#110681,
#110682,#110683,#110684,#110685,#110686,#110687,#110688,#110689,#110690,
#110691,#110692,#110693,#110694,#110695,#110696,#110697,#110698,#110699,
#110700,#110701,#110702,#110703,#110704,#110705,#110706,#110707,#110708,
#110709,#110710,#110711,#110712,#110713,#110714,#110715,#110716,#110717,
#110718,#110719,#110720,#110721,#110722,#110723,#110724,#110725,#110726,
#110727,#110728,#110729,#110730,#110731,#110732,#110733,#110734,#110735,
#110736,#110737,#110738,#110739,#110740,#110741,#110742,#110743,#110744,
#110745,#110746,#110747,#110748,#110749,#110750,#110751,#110752,#110753,
#110754,#110755,#110756,#110757,#110758,#110759,#110760,#110761,#110762,
#110763,#110764,#110765,#110766,#110767,#110768,#110769,#110770,#110771,
#110772,#110773,#110774,#110775,#110776,#110777,#110778,#110779,#110780,
#110781,#110782,#110783,#110784,#110785,#110786,#110787,#110788,#110789,
#110790,#110791,#110792,#110793,#110794,#110795,#110796,#110797,#110798,
#110799,#110800,#110801,#110802,#110803,#110804,#110805,#110806,#110807,
#110808,#110809,#110810,#110811,#110812),.UNSPECIFIED.,.F.,.F.,(4,3,3,3,
3,3,3,3,3,3,3,3,3,3,3,3,3,3,3,3,3,3,3,3,3,3,3,3,3,3,3,3,3,3,3,3,3,3,3,3,
3,3,3,3,3,3,3,3,3,3,3,3,3,3,3,3,3,3,3,3,3,3,3,3,3,3,3,3,3,3,3,3,4),(1284.91139531842,
1285.00585841401,1285.10071213125,1285.19610642442,1285.27909917653,1285.36283788838,
1285.44647339974,1285.53002584314,1285.61351527899,1285.6969692296,1285.78040572345,
1285.86384283321,1285.94729862812,1286.03084312085,1286.11443220379,1286.19815547135,
1286.27883518725,1286.3625738991,1286.44620941046,1286.52976185386,1286.61325128972,
1286.69670524033,1286.78014173418,1286.86357884393,1286.94703463885,1287.03057913158,
1287.11416821452,1287.19789148208,1287.27857119797,1287.36230990982,1287.44594542118,
1287.52949786458,1287.61298730044,1287.69644125105,1287.7798777449,1287.86331485465,
1287.94677064957,1288.0303151423,1288.11390422524,1288.1976274928,1288.2783072087,
1288.36204592055,1288.44568143191,1288.52923387531,1288.61272331116,1288.69617726178,
1288.77961375563,1288.86305086538,1288.9465066603,1289.03005115303,1289.11364023597,
1289.19736350353,1289.27804321942,1289.36178193127,1289.44541744263,1289.52896988603,
1289.61245932188,1289.6959132725,1289.77934976634,1289.8627868761,1289.94624267101,
1290.02978716374,1290.11337624668,1290.19709951424,1290.27777923014,1290.36089975157,
1290.44358911637,1290.52620302072,1290.60876039961,1290.69225615009,1290.77476877336,
1290.85875608745,1290.94274340154),.UNSPECIFIED.);
#871=B_SPLINE_CURVE_WITH_KNOTS('',3,(#110818,#110819,#110820,#110821,#110822,
#110823,#110824,#110825,#110826,#110827,#110828,#110829,#110830,#110831,
#110832,#110833,#110834,#110835,#110836,#110837,#110838,#110839,#110840,
#110841,#110842,#110843,#110844,#110845,#110846,#110847,#110848,#110849,
#110850,#110851,#110852,#110853,#110854,#110855,#110856,#110857,#110858,
#110859,#110860,#110861,#110862,#110863,#110864,#110865,#110866,#110867,
#110868,#110869,#110870,#110871,#110872,#110873,#110874,#110875,#110876,
#110877,#110878,#110879,#110880,#110881,#110882,#110883,#110884,#110885,
#110886,#110887,#110888,#110889,#110890,#110891,#110892,#110893,#110894,
#110895,#110896,#110897,#110898,#110899,#110900,#110901,#110902,#110903,
#110904,#110905,#110906,#110907,#110908,#110909,#110910,#110911,#110912,
#110913,#110914,#110915,#110916,#110917,#110918,#110919,#110920,#110921,
#110922,#110923,#110924,#110925,#110926,#110927,#110928,#110929,#110930,
#110931,#110932,#110933,#110934,#110935,#110936,#110937,#110938,#110939,
#110940,#110941,#110942,#110943,#110944,#110945,#110946,#110947,#110948,
#110949,#110950,#110951,#110952,#110953,#110954,#110955,#110956,#110957,
#110958,#110959,#110960,#110961,#110962,#110963,#110964,#110965,#110966,
#110967,#110968,#110969,#110970,#110971,#110972,#110973,#110974,#110975,
#110976,#110977,#110978,#110979,#110980,#110981,#110982,#110983,#110984,
#110985,#110986,#110987,#110988,#110989,#110990,#110991,#110992,#110993,
#110994,#110995,#110996,#110997,#110998,#110999,#111000,#111001,#111002,
#111003,#111004,#111005,#111006,#111007,#111008,#111009,#111010,#111011,
#111012,#111013,#111014,#111015,#111016,#111017,#111018,#111019,#111020,
#111021,#111022,#111023,#111024,#111025,#111026,#111027,#111028,#111029,
#111030,#111031,#111032,#111033,#111034,#111035,#111036,#111037),
 .UNSPECIFIED.,.F.,.F.,(4,3,3,3,3,3,3,3,3,3,3,3,3,3,3,3,3,3,3,3,3,3,3,3,
3,3,3,3,3,3,3,3,3,3,3,3,3,3,3,3,3,3,3,3,3,3,3,3,3,3,3,3,3,3,3,3,3,3,3,3,
3,3,3,3,3,3,3,3,3,3,3,3,3,4),(1291.19458062552,1291.2770321407,1291.3632732021,
1291.44563144077,1291.52797699879,1291.61032881882,1291.6927058461,1291.77517160511,
1291.85768947086,1291.94032413001,1291.96696063186,1292.05069934371,1292.13433485507,
1292.21788729847,1292.30137673432,1292.38483068493,1292.46826717878,1292.55170428853,
1292.63516008345,1292.71870457618,1292.80229365912,1292.88601692668,1292.96669664258,
1293.05043535443,1293.13407086579,1293.21762330919,1293.30111274504,1293.38456669566,
1293.4680031895,1293.55144029926,1293.63489609417,1293.7184405869,1293.80202966984,
1293.8857529374,1293.9664326533,1294.05017136515,1294.13380687651,1294.21735931991,
1294.30084875576,1294.38430270638,1294.46773920022,1294.55117630998,1294.6346321049,
1294.71817659763,1294.80176568057,1294.88548894813,1294.96616866402,1295.04990737587,
1295.13354288723,1295.21709533063,1295.30058476648,1295.3840387171,1295.46747521094,
1295.5509123207,1295.63436811562,1295.71791260834,1295.80150169129,1295.88522495884,
1295.96590467474,1296.04964338659,1296.13327889795,1296.21683134135,1296.3003207772,
1296.38377472782,1296.46721122166,1296.55064833142,1296.63410412634,1296.71764861907,
1296.80123770201,1296.88496096957,1296.96564068546,1297.05322552547,1297.14062188468,
1297.22741857401),.UNSPECIFIED.);
#872=B_SPLINE_CURVE_WITH_KNOTS('',3,(#111038,#111039,#111040,#111041,#111042,
#111043,#111044,#111045,#111046,#111047),.UNSPECIFIED.,.F.,.F.,(4,3,3,4),
(1290.9433767908,1290.96722462114,1291.08090262327,1291.19458062539),
 .UNSPECIFIED.);
#873=B_SPLINE_CURVE_WITH_KNOTS('',3,(#111049,#111050,#111051,#111052,#111053,
#111054,#111055,#111056,#111057,#111058),.UNSPECIFIED.,.F.,.F.,(4,3,3,4),
(1290.94274340154,1291.0253692094,1291.10997491734,1291.19458062527),
 .UNSPECIFIED.);
#874=B_SPLINE_CURVE_WITH_KNOTS('',3,(#111059,#111060,#111061,#111062,#111063,
#111064,#111065,#111066,#111067,#111068,#111069,#111070,#111071,#111072,
#111073,#111074,#111075,#111076,#111077,#111078,#111079,#111080,#111081,
#111082,#111083,#111084,#111085,#111086,#111087,#111088,#111089,#111090,
#111091,#111092,#111093,#111094,#111095,#111096,#111097,#111098,#111099,
#111100,#111101,#111102,#111103,#111104,#111105,#111106,#111107,#111108,
#111109,#111110,#111111,#111112,#111113,#111114,#111115,#111116,#111117,
#111118,#111119,#111120,#111121,#111122,#111123,#111124,#111125,#111126,
#111127,#111128,#111129,#111130,#111131,#111132,#111133,#111134,#111135,
#111136,#111137,#111138,#111139,#111140,#111141,#111142,#111143,#111144,
#111145,#111146,#111147,#111148,#111149,#111150,#111151,#111152,#111153,
#111154,#111155,#111156,#111157,#111158,#111159,#111160,#111161,#111162,
#111163,#111164,#111165,#111166,#111167,#111168,#111169,#111170,#111171,
#111172,#111173,#111174,#111175,#111176,#111177,#111178,#111179,#111180,
#111181,#111182,#111183,#111184,#111185,#111186,#111187,#111188,#111189,
#111190,#111191,#111192,#111193,#111194,#111195,#111196,#111197,#111198,
#111199,#111200,#111201,#111202,#111203,#111204,#111205,#111206,#111207,
#111208,#111209,#111210,#111211,#111212,#111213,#111214,#111215,#111216,
#111217,#111218,#111219,#111220,#111221,#111222,#111223,#111224,#111225,
#111226,#111227,#111228,#111229,#111230,#111231,#111232,#111233,#111234,
#111235,#111236,#111237,#111238,#111239,#111240,#111241,#111242,#111243,
#111244,#111245,#111246,#111247,#111248,#111249,#111250,#111251,#111252,
#111253,#111254,#111255,#111256,#111257,#111258,#111259,#111260,#111261,
#111262,#111263,#111264,#111265,#111266,#111267,#111268,#111269,#111270,
#111271,#111272,#111273,#111274,#111275,#111276,#111277,#111278),
 .UNSPECIFIED.,.F.,.F.,(4,3,3,3,3,3,3,3,3,3,3,3,3,3,3,3,3,3,3,3,3,3,3,3,
3,3,3,3,3,3,3,3,3,3,3,3,3,3,3,3,3,3,3,3,3,3,3,3,3,3,3,3,3,3,3,3,3,3,3,3,
3,3,3,3,3,3,3,3,3,3,3,3,3,4),(1291.1945806254,1291.27751524086,1291.36125395271,
1291.44488946407,1291.52844190747,1291.61193134332,1291.69538529394,1291.77882178778,
1291.86225889754,1291.94571469246,1292.02925918519,1292.11284826813,1292.19657153568,
1292.27725125158,1292.36098996343,1292.44462547479,1292.52817791819,1292.61166735404,
1292.69512130466,1292.7785577985,1292.86199490826,1292.94545070318,1293.02899519591,
1293.11258427885,1293.1963075464,1293.2769872623,1293.36072597415,1293.44436148551,
1293.52791392891,1293.61140336476,1293.69485731538,1293.77829380922,1293.86173091898,
1293.94518671389,1294.02873120662,1294.11232028956,1294.19604355712,1294.27672327302,
1294.36046198487,1294.44409749623,1294.52764993963,1294.61113937548,1294.6945933261,
1294.77802981994,1294.8614669297,1294.94492272462,1295.02846721735,1295.11205630029,
1295.19577956785,1295.27645928374,1295.36019799559,1295.44383350695,1295.52738595035,
1295.6108753862,1295.69432933682,1295.77776583066,1295.86120294042,1295.94465873534,
1296.02820322807,1296.11179231101,1296.19551557856,1296.27619529446,1296.35993683267,
1296.44357451757,1296.52712848442,1296.61454189573,1296.69799220263,1296.78142497954,
1296.8648582981,1296.94831022628,1297.0318388664,1297.11541247864,1297.19909084984,
1297.22643577487),.UNSPECIFIED.);
#875=B_SPLINE_CURVE_WITH_KNOTS('',3,(#111284,#111285,#111286,#111287,#111288,
#111289,#111290,#111291,#111292,#111293,#111294,#111295,#111296,#111297,
#111298,#111299,#111300,#111301,#111302,#111303,#111304,#111305,#111306,
#111307,#111308,#111309,#111310,#111311,#111312,#111313,#111314,#111315,
#111316,#111317,#111318,#111319,#111320,#111321,#111322,#111323,#111324,
#111325,#111326,#111327,#111328,#111329,#111330,#111331,#111332,#111333,
#111334,#111335,#111336,#111337,#111338,#111339,#111340,#111341,#111342,
#111343,#111344,#111345,#111346,#111347,#111348,#111349,#111350,#111351,
#111352,#111353,#111354,#111355,#111356,#111357,#111358,#111359,#111360,
#111361,#111362,#111363,#111364,#111365,#111366,#111367,#111368,#111369,
#111370,#111371,#111372,#111373,#111374,#111375,#111376,#111377,#111378,
#111379,#111380,#111381,#111382,#111383,#111384,#111385,#111386,#111387,
#111388,#111389,#111390,#111391,#111392,#111393,#111394,#111395,#111396,
#111397,#111398,#111399,#111400,#111401,#111402,#111403,#111404,#111405,
#111406,#111407,#111408,#111409,#111410,#111411,#111412,#111413,#111414,
#111415,#111416,#111417,#111418,#111419,#111420,#111421,#111422,#111423,
#111424,#111425,#111426,#111427,#111428,#111429,#111430,#111431,#111432,
#111433,#111434,#111435,#111436,#111437,#111438,#111439,#111440,#111441,
#111442,#111443,#111444,#111445,#111446,#111447,#111448,#111449,#111450,
#111451,#111452,#111453,#111454,#111455,#111456,#111457,#111458,#111459,
#111460,#111461,#111462,#111463,#111464,#111465,#111466,#111467,#111468,
#111469,#111470,#111471,#111472,#111473,#111474,#111475,#111476,#111477,
#111478,#111479,#111480,#111481,#111482,#111483,#111484,#111485,#111486,
#111487,#111488,#111489,#111490,#111491,#111492,#111493,#111494,#111495,
#111496,#111497,#111498,#111499,#111500,#111501,#111502,#111503),
 .UNSPECIFIED.,.F.,.F.,(4,3,3,3,3,3,3,3,3,3,3,3,3,3,3,3,3,3,3,3,3,3,3,3,
3,3,3,3,3,3,3,3,3,3,3,3,3,3,3,3,3,3,3,3,3,3,3,3,3,3,3,3,3,3,3,3,3,3,3,3,
3,3,3,3,3,3,3,3,3,3,3,3,3,4),(1297.47776593277,1297.5656277686,1297.65362197466,
1297.74183995296,1297.83017818097,1297.91872114682,1297.96537669618,1298.04911540803,
1298.13275091939,1298.21630336279,1298.29979279864,1298.38324674925,1298.4666832431,
1298.55012035285,1298.63357614777,1298.7171206405,1298.80070972344,1298.884432991,
1298.9651127069,1299.04885141875,1299.13248693011,1299.21603937351,1299.29952880936,
1299.38298275998,1299.46641925382,1299.54985636358,1299.6333121585,1299.71685665122,
1299.80044573417,1299.88416900172,1299.96484871762,1300.04858742947,1300.13222294083,
1300.21577538423,1300.29926482008,1300.3827187707,1300.46615526454,1300.5495923743,
1300.63304816922,1300.71659266195,1300.80018174489,1300.88390501245,1300.96458472834,
1301.04832344019,1301.13195895155,1301.21551139495,1301.2990008308,1301.38245478142,
1301.46589127526,1301.54932838502,1301.63278417994,1301.71632867267,1301.79991775561,
1301.88364102316,1301.96432073906,1302.04805945091,1302.13169496227,1302.21524740567,
1302.29873684152,1302.38219079214,1302.46562728598,1302.54906439574,1302.63252019066,
1302.71606468339,1302.79965376633,1302.88337703389,1302.96405674978,1303.04658050868,
1303.12900805391,1303.21135857993,1303.29364884454,1303.37590352684,1303.45815430565,
1303.50937468525),.UNSPECIFIED.);
#876=B_SPLINE_CURVE_WITH_KNOTS('',3,(#111504,#111505,#111506,#111507,#111508,
#111509,#111510,#111511,#111512,#111513),.UNSPECIFIED.,.F.,.F.,(4,3,3,4),
(1297.22741857401,1297.3145634716,1297.4015669567,1297.47776593257),
 .UNSPECIFIED.);
#877=B_SPLINE_CURVE_WITH_KNOTS('',3,(#111515,#111516,#111517,#111518,#111519,
#111520,#111521,#111522,#111523,#111524),.UNSPECIFIED.,.F.,.F.,(4,3,3,4),
(1297.22643577487,1297.27593130518,1297.39557682204,1297.47776593258),
 .UNSPECIFIED.);
#878=B_SPLINE_CURVE_WITH_KNOTS('',3,(#111525,#111526,#111527,#111528,#111529,
#111530,#111531,#111532,#111533,#111534,#111535,#111536,#111537,#111538,
#111539,#111540,#111541,#111542,#111543,#111544,#111545,#111546,#111547,
#111548,#111549,#111550,#111551,#111552,#111553,#111554,#111555,#111556,
#111557,#111558,#111559,#111560,#111561,#111562,#111563,#111564,#111565,
#111566,#111567,#111568,#111569,#111570,#111571,#111572,#111573,#111574,
#111575,#111576,#111577,#111578,#111579,#111580,#111581,#111582,#111583,
#111584,#111585,#111586,#111587,#111588,#111589,#111590,#111591,#111592,
#111593,#111594,#111595,#111596,#111597,#111598,#111599,#111600,#111601,
#111602,#111603,#111604,#111605,#111606,#111607,#111608,#111609,#111610,
#111611,#111612,#111613,#111614,#111615,#111616,#111617,#111618,#111619,
#111620,#111621,#111622,#111623,#111624,#111625,#111626,#111627,#111628,
#111629,#111630,#111631,#111632,#111633,#111634,#111635,#111636,#111637,
#111638,#111639,#111640,#111641,#111642,#111643,#111644,#111645,#111646,
#111647,#111648,#111649,#111650,#111651,#111652,#111653,#111654,#111655,
#111656,#111657,#111658,#111659,#111660,#111661,#111662,#111663,#111664,
#111665,#111666,#111667,#111668,#111669,#111670,#111671,#111672,#111673,
#111674,#111675,#111676,#111677,#111678,#111679,#111680,#111681,#111682,
#111683,#111684,#111685,#111686,#111687,#111688,#111689,#111690,#111691,
#111692,#111693,#111694,#111695,#111696,#111697,#111698,#111699,#111700,
#111701,#111702,#111703,#111704,#111705,#111706,#111707,#111708,#111709,
#111710,#111711,#111712,#111713,#111714,#111715,#111716,#111717,#111718,
#111719,#111720,#111721,#111722,#111723,#111724,#111725,#111726,#111727,
#111728,#111729,#111730,#111731,#111732,#111733,#111734,#111735,#111736,
#111737,#111738,#111739,#111740,#111741,#111742,#111743,#111744),
 .UNSPECIFIED.,.F.,.F.,(4,3,3,3,3,3,3,3,3,3,3,3,3,3,3,3,3,3,3,3,3,3,3,3,
3,3,3,3,3,3,3,3,3,3,3,3,3,3,3,3,3,3,3,3,3,3,3,3,3,3,3,3,3,3,3,3,3,3,3,3,
3,3,3,3,3,3,3,3,3,3,3,3,3,4),(1297.47776593277,1297.56014602202,1297.64245768107,
1297.72472758977,1297.8069770208,1297.88922498357,1297.97149048404,1298.05384045173,
1298.13623575657,1298.21875539183,1298.2756673159,1298.35940602775,1298.44304153911,
1298.52659398251,1298.61008341836,1298.69353736898,1298.77697386282,1298.86041097258,
1298.9438667675,1299.02741126023,1299.11100034317,1299.19472361073,1299.27540332662,
1299.35914203847,1299.44277754983,1299.52632999323,1299.60981942908,1299.6932733797,
1299.77670987354,1299.8601469833,1299.94360277822,1300.02714727095,1300.11073635389,
1300.19445962144,1300.27513933734,1300.35887804919,1300.44251356055,1300.52606600395,
1300.6095554398,1300.69300939042,1300.77644588426,1300.85988299402,1300.94333878894,
1301.02688328167,1301.11047236461,1301.19419563217,1301.27487534806,1301.35861405991,
1301.44224957127,1301.52580201467,1301.60929145052,1301.69274540114,1301.77618189498,
1301.85961900474,1301.94307479966,1302.02661929239,1302.11020837533,1302.19393164289,
1302.27461135878,1302.35835007063,1302.44198558199,1302.52553802539,1302.60902746124,
1302.69248141185,1302.7759179057,1302.85935501546,1302.94281081037,1303.0263553031,
1303.10994438604,1303.1936676536,1303.2743473695,1303.36294726085,1303.45134295585,
1303.51063850993),.UNSPECIFIED.);
#879=B_SPLINE_CURVE_WITH_KNOTS('',3,(#111750,#111751,#111752,#111753,#111754,
#111755,#111756,#111757,#111758,#111759,#111760,#111761,#111762,#111763,
#111764,#111765,#111766,#111767,#111768,#111769,#111770,#111771,#111772,
#111773,#111774,#111775,#111776,#111777,#111778,#111779,#111780,#111781,
#111782,#111783,#111784,#111785,#111786,#111787,#111788,#111789,#111790,
#111791,#111792,#111793,#111794,#111795,#111796,#111797,#111798,#111799,
#111800,#111801,#111802,#111803,#111804,#111805,#111806,#111807,#111808,
#111809,#111810,#111811,#111812,#111813,#111814,#111815,#111816,#111817,
#111818,#111819,#111820,#111821,#111822,#111823,#111824,#111825,#111826,
#111827,#111828,#111829,#111830,#111831,#111832,#111833,#111834,#111835,
#111836,#111837,#111838,#111839,#111840,#111841,#111842,#111843,#111844,
#111845,#111846,#111847,#111848,#111849,#111850,#111851,#111852,#111853,
#111854,#111855,#111856,#111857,#111858,#111859,#111860,#111861,#111862,
#111863,#111864,#111865,#111866,#111867,#111868,#111869,#111870,#111871,
#111872,#111873,#111874,#111875,#111876,#111877,#111878,#111879,#111880,
#111881,#111882,#111883,#111884,#111885,#111886,#111887,#111888,#111889,
#111890,#111891,#111892,#111893,#111894,#111895,#111896,#111897,#111898,
#111899,#111900,#111901,#111902,#111903,#111904,#111905,#111906,#111907,
#111908,#111909,#111910,#111911,#111912,#111913,#111914,#111915,#111916,
#111917,#111918,#111919,#111920,#111921,#111922,#111923,#111924,#111925,
#111926,#111927,#111928,#111929,#111930,#111931,#111932,#111933,#111934,
#111935,#111936,#111937,#111938,#111939,#111940,#111941,#111942,#111943,
#111944,#111945,#111946,#111947,#111948,#111949,#111950,#111951,#111952,
#111953,#111954,#111955,#111956,#111957,#111958,#111959,#111960,#111961,
#111962,#111963,#111964,#111965,#111966),.UNSPECIFIED.,.F.,.F.,(4,3,3,3,
3,3,3,3,3,3,3,3,3,3,3,3,3,3,3,3,3,3,3,3,3,3,3,3,3,3,3,3,3,3,3,3,3,3,3,3,
3,3,3,3,3,3,3,3,3,3,3,3,3,3,3,3,3,3,3,3,3,3,3,3,3,3,3,3,3,3,3,3,4),(1303.76095123975,
1303.88029814022,1303.9637927605,1304.04753147234,1304.13116698371,1304.21471942711,
1304.29820886296,1304.38166281357,1304.46509930742,1304.54853641717,1304.63199221209,
1304.71553670481,1304.79912578775,1304.88284905531,1304.96352877122,1305.04726748307,
1305.13090299443,1305.21445543783,1305.29794487368,1305.3813988243,1305.46483531814,
1305.5482724279,1305.63172822282,1305.71527271555,1305.79886179849,1305.88258506605,
1305.96326478194,1306.04700349379,1306.13063900515,1306.21419144855,1306.2976808844,
1306.38113483502,1306.46457132886,1306.54800843862,1306.63146423354,1306.71500872627,
1306.79859780921,1306.88232107676,1306.96300079266,1307.04673950451,1307.13037501587,
1307.21392745927,1307.29741689512,1307.38087084574,1307.46430733958,1307.54774444934,
1307.63120024426,1307.71474473699,1307.79833381993,1307.88205708748,1307.96273680338,
1308.04647551523,1308.13011102659,1308.21366346999,1308.29715290584,1308.38060685646,
1308.4640433503,1308.54748046006,1308.63093625498,1308.71448074771,1308.79806983065,
1308.8817930982,1308.9624728141,1309.04622167287,1309.1298650922,1309.21340828216,
1309.29689463722,1309.3803422766,1309.4637692897,1309.54722292384,1309.63068741899,
1309.71422899167,1309.79248975557),.UNSPECIFIED.);
#880=B_SPLINE_CURVE_WITH_KNOTS('',3,(#111967,#111968,#111969,#111970,#111971,
#111972,#111973,#111974,#111975,#111976),.UNSPECIFIED.,.F.,.F.,(4,3,3,4),
(1303.50937468525,1303.59165936378,1303.67630530167,1303.76095123957),
 .UNSPECIFIED.);
#881=B_SPLINE_CURVE_WITH_KNOTS('',3,(#111978,#111979,#111980,#111981,#111982,
#111983,#111984,#111985,#111986,#111987),.UNSPECIFIED.,.F.,.F.,(4,3,3,4),
(1303.51063850993,1303.59876857963,1303.68671228148,1303.76095123965),
 .UNSPECIFIED.);
#882=B_SPLINE_CURVE_WITH_KNOTS('',3,(#111988,#111989,#111990,#111991,#111992,
#111993,#111994,#111995,#111996,#111997,#111998,#111999,#112000,#112001,
#112002,#112003,#112004,#112005,#112006,#112007,#112008,#112009,#112010,
#112011,#112012,#112013,#112014,#112015,#112016,#112017,#112018,#112019,
#112020,#112021,#112022,#112023,#112024,#112025,#112026,#112027,#112028,
#112029,#112030,#112031,#112032,#112033,#112034,#112035,#112036,#112037,
#112038,#112039,#112040,#112041,#112042,#112043,#112044,#112045,#112046,
#112047,#112048,#112049,#112050,#112051,#112052,#112053,#112054,#112055,
#112056,#112057,#112058,#112059,#112060,#112061,#112062,#112063,#112064,
#112065,#112066,#112067,#112068,#112069,#112070,#112071,#112072,#112073,
#112074,#112075,#112076,#112077,#112078,#112079,#112080,#112081,#112082,
#112083,#112084,#112085,#112086,#112087,#112088,#112089,#112090,#112091,
#112092,#112093,#112094,#112095,#112096,#112097,#112098,#112099,#112100,
#112101,#112102,#112103,#112104,#112105,#112106,#112107,#112108,#112109,
#112110,#112111,#112112,#112113,#112114,#112115,#112116,#112117,#112118,
#112119,#112120,#112121,#112122,#112123,#112124,#112125,#112126,#112127,
#112128,#112129,#112130,#112131,#112132,#112133,#112134,#112135,#112136,
#112137,#112138,#112139,#112140,#112141,#112142,#112143,#112144,#112145,
#112146,#112147,#112148,#112149,#112150,#112151,#112152,#112153,#112154,
#112155,#112156,#112157,#112158,#112159,#112160,#112161,#112162,#112163,
#112164,#112165,#112166,#112167,#112168,#112169,#112170,#112171,#112172,
#112173,#112174,#112175,#112176,#112177,#112178,#112179,#112180,#112181,
#112182,#112183,#112184,#112185,#112186,#112187,#112188,#112189,#112190,
#112191,#112192,#112193,#112194,#112195,#112196,#112197,#112198,#112199,
#112200,#112201,#112202,#112203,#112204,#112205,#112206,#112207),
 .UNSPECIFIED.,.F.,.F.,(4,3,3,3,3,3,3,3,3,3,3,3,3,3,3,3,3,3,3,3,3,3,3,3,
3,3,3,3,3,3,3,3,3,3,3,3,3,3,3,3,3,3,3,3,3,3,3,3,3,3,3,3,3,3,3,3,3,3,3,3,
3,3,3,3,3,3,3,3,3,3,3,3,3,4),(1303.76095123976,1303.84788995488,1303.93492696292,
1304.02215407985,1304.10947927334,1304.19700265275,1304.27408338022,1304.35782209207,
1304.44145760344,1304.52501004683,1304.60849948269,1304.6919534333,1304.77538992715,
1304.8588270369,1304.94228283182,1305.02582732455,1305.10941640749,1305.19313967505,
1305.27381939094,1305.35755810279,1305.44119361415,1305.52474605755,1305.6082354934,
1305.69168944402,1305.77512593786,1305.85856304762,1305.94201884254,1306.02556333527,
1306.10915241821,1306.19287568576,1306.27355540166,1306.35729411351,1306.44092962487,
1306.52448206827,1306.60797150412,1306.69142545474,1306.77486194858,1306.85829905834,
1306.94175485325,1307.02529934598,1307.10888842892,1307.19261169648,1307.27329141238,
1307.35703012423,1307.44066563559,1307.52421807899,1307.60770751484,1307.69116146546,
1307.7745979593,1307.85803506906,1307.94149086398,1308.02503535671,1308.10862443965,
1308.19234770721,1308.2730274231,1308.35676613495,1308.44040164632,1308.52395408972,
1308.60744352557,1308.69089747618,1308.77433397003,1308.85777107978,1308.9412268747,
1309.02477136743,1309.10836045037,1309.19208371793,1309.27276343382,1309.35539413479,
1309.43792765049,1309.52038311093,1309.60277500297,1309.68513056106,1309.76747497784,
1309.7926706447),.UNSPECIFIED.);
#883=B_SPLINE_CURVE_WITH_KNOTS('',3,(#112213,#112214,#112215,#112216,#112217,
#112218,#112219,#112220,#112221,#112222,#112223,#112224,#112225,#112226,
#112227,#112228,#112229,#112230,#112231,#112232,#112233,#112234,#112235,
#112236,#112237,#112238,#112239,#112240,#112241,#112242,#112243,#112244,
#112245,#112246,#112247,#112248,#112249,#112250,#112251,#112252,#112253,
#112254,#112255,#112256,#112257,#112258,#112259,#112260,#112261,#112262,
#112263,#112264,#112265,#112266,#112267,#112268,#112269,#112270,#112271,
#112272,#112273,#112274,#112275,#112276,#112277,#112278,#112279,#112280,
#112281,#112282,#112283,#112284,#112285,#112286,#112287,#112288,#112289,
#112290,#112291,#112292,#112293,#112294,#112295,#112296,#112297,#112298,
#112299,#112300,#112301,#112302,#112303,#112304,#112305,#112306,#112307,
#112308,#112309,#112310,#112311,#112312,#112313,#112314,#112315,#112316,
#112317,#112318,#112319,#112320,#112321,#112322,#112323,#112324,#112325,
#112326,#112327,#112328,#112329,#112330,#112331,#112332,#112333,#112334,
#112335,#112336,#112337,#112338,#112339,#112340,#112341,#112342,#112343,
#112344,#112345,#112346,#112347,#112348,#112349,#112350,#112351,#112352,
#112353,#112354,#112355,#112356,#112357,#112358,#112359,#112360,#112361,
#112362,#112363,#112364,#112365,#112366,#112367,#112368,#112369,#112370,
#112371,#112372,#112373,#112374,#112375,#112376,#112377,#112378,#112379,
#112380,#112381,#112382,#112383,#112384,#112385,#112386,#112387,#112388,
#112389,#112390,#112391,#112392,#112393,#112394,#112395,#112396,#112397,
#112398,#112399,#112400,#112401,#112402,#112403,#112404,#112405,#112406,
#112407,#112408,#112409,#112410,#112411,#112412,#112413,#112414,#112415,
#112416,#112417,#112418,#112419,#112420,#112421,#112422,#112423,#112424,
#112425,#112426,#112427,#112428,#112429,#112430,#112431,#112432),
 .UNSPECIFIED.,.F.,.F.,(4,3,3,3,3,3,3,3,3,3,3,3,3,3,3,3,3,3,3,3,3,3,3,3,
3,3,3,3,3,3,3,3,3,3,3,3,3,3,3,3,3,3,3,3,3,3,3,3,3,3,3,3,3,3,3,3,3,3,3,3,
3,3,3,3,3,3,3,3,3,3,3,3,3,4),(1310.04413654706,1310.12691333657,1310.20959441768,
1310.29220075488,1310.37591876497,1310.45844797584,1310.54096978032,1310.62350300583,
1310.70811346325,1310.79076955573,1310.87635719563,1310.96194483554,1311.04568354739,
1311.12931905875,1311.21287150215,1311.296360938,1311.37981488862,1311.46325138246,
1311.54668849222,1311.63014428714,1311.71368877987,1311.79727786281,1311.88100113036,
1311.96168084626,1312.04541955811,1312.12905506947,1312.21260751287,1312.29609694872,
1312.37955089934,1312.46298739318,1312.54642450294,1312.62988029785,1312.71342479058,
1312.79701387353,1312.88073714108,1312.96141685698,1313.04515556883,1313.12879108019,
1313.21234352359,1313.29583295944,1313.37928691006,1313.4627234039,1313.54616051366,
1313.62961630858,1313.71316080131,1313.79674988425,1313.8804731518,1313.9611528677,
1314.04489157955,1314.12852709091,1314.21207953431,1314.29556897016,1314.37902292078,
1314.46245941462,1314.54589652438,1314.6293523193,1314.71289681203,1314.79648589497,
1314.88020916253,1314.96088887842,1315.04462759027,1315.12826310163,1315.21181554503,
1315.29530498088,1315.3787589315,1315.46219542534,1315.5456325351,1315.62908833002,
1315.71263282275,1315.79622190569,1315.87994517324,1315.96062488914,1316.0562245153,
1316.07685146776),.UNSPECIFIED.);
#884=B_SPLINE_CURVE_WITH_KNOTS('',3,(#112433,#112434,#112435,#112436,#112437,
#112438,#112439,#112440,#112441,#112442),.UNSPECIFIED.,.F.,.F.,(4,3,3,4),
(1309.79248975557,1309.87734929019,1309.96220882482,1310.04413654693),
 .UNSPECIFIED.);
#885=B_SPLINE_CURVE_WITH_KNOTS('',3,(#112444,#112445,#112446,#112447,#112448,
#112449,#112450,#112451,#112452,#112453),.UNSPECIFIED.,.F.,.F.,(4,3,3,4),
(1309.7926706447,1309.87504289146,1309.95958971914,1310.04413654683),
 .UNSPECIFIED.);
#886=B_SPLINE_CURVE_WITH_KNOTS('',3,(#112454,#112455,#112456,#112457,#112458,
#112459,#112460,#112461,#112462,#112463,#112464,#112465,#112466,#112467,
#112468,#112469,#112470,#112471,#112472,#112473,#112474,#112475,#112476,
#112477,#112478,#112479,#112480,#112481,#112482,#112483,#112484,#112485,
#112486,#112487,#112488,#112489,#112490,#112491,#112492,#112493,#112494,
#112495,#112496,#112497,#112498,#112499,#112500,#112501,#112502,#112503,
#112504,#112505,#112506,#112507,#112508,#112509,#112510,#112511,#112512,
#112513,#112514,#112515,#112516,#112517,#112518,#112519,#112520,#112521,
#112522,#112523,#112524,#112525,#112526,#112527,#112528,#112529,#112530,
#112531,#112532,#112533,#112534,#112535,#112536,#112537,#112538,#112539,
#112540,#112541,#112542,#112543,#112544,#112545,#112546,#112547,#112548,
#112549,#112550,#112551,#112552,#112553,#112554,#112555,#112556,#112557,
#112558,#112559,#112560,#112561,#112562,#112563,#112564,#112565,#112566,
#112567,#112568,#112569,#112570,#112571,#112572,#112573,#112574,#112575,
#112576,#112577,#112578,#112579,#112580,#112581,#112582,#112583,#112584,
#112585,#112586,#112587,#112588,#112589,#112590,#112591,#112592,#112593,
#112594,#112595,#112596,#112597,#112598,#112599,#112600,#112601,#112602,
#112603,#112604,#112605,#112606,#112607,#112608,#112609,#112610,#112611,
#112612,#112613,#112614,#112615,#112616,#112617,#112618,#112619,#112620,
#112621,#112622,#112623,#112624,#112625,#112626,#112627,#112628,#112629,
#112630,#112631,#112632,#112633,#112634,#112635,#112636,#112637,#112638,
#112639,#112640,#112641,#112642,#112643,#112644,#112645,#112646,#112647,
#112648,#112649,#112650,#112651,#112652,#112653,#112654,#112655,#112656,
#112657,#112658,#112659,#112660,#112661,#112662,#112663,#112664,#112665,
#112666,#112667,#112668,#112669,#112670),.UNSPECIFIED.,.F.,.F.,(4,3,3,3,
3,3,3,3,3,3,3,3,3,3,3,3,3,3,3,3,3,3,3,3,3,3,3,3,3,3,3,3,3,3,3,3,3,3,3,3,
3,3,3,3,3,3,3,3,3,3,3,3,3,3,3,3,3,3,3,3,3,3,3,3,3,3,3,3,3,3,3,3,4),(1310.04413654693,
1310.15831799574,1310.27249944454,1310.35623815639,1310.43987366775,1310.52342611115,
1310.606915547,1310.69036949762,1310.77380599146,1310.85724310122,1310.94069889614,
1311.02424338887,1311.10783247181,1311.19155573937,1311.27223545526,1311.35597416711,
1311.43960967847,1311.52316212187,1311.60665155772,1311.69010550834,1311.77354200218,
1311.85697911194,1311.94043490685,1312.02397939958,1312.10756848252,1312.19129175008,
1312.27197146598,1312.35571017783,1312.43934568919,1312.52289813259,1312.60638756844,
1312.68984151906,1312.7732780129,1312.85671512266,1312.94017091758,1313.02371541031,
1313.10730449325,1313.1910277608,1313.2717074767,1313.35544618855,1313.43908169991,
1313.52263414331,1313.60612357916,1313.68957752978,1313.77301402362,1313.85645113338,
1313.9399069283,1314.02345142103,1314.10704050397,1314.19076377152,1314.27144348742,
1314.35518219927,1314.43881771063,1314.52237015403,1314.60585958988,1314.6893135405,
1314.77275003434,1314.8561871441,1314.93964293902,1315.02318743175,1315.10677651469,
1315.19049978225,1315.27117949814,1315.35492999503,1315.43857471546,1315.52211835569,
1315.60560468323,1315.68905181818,1315.7724778503,1315.85592568299,1315.93938418495,
1316.02290795082,1316.07565830488),.UNSPECIFIED.);
#887=B_SPLINE_CURVE_WITH_KNOTS('',3,(#112676,#112677,#112678,#112679,#112680,
#112681,#112682,#112683,#112684,#112685,#112686,#112687,#112688,#112689,
#112690,#112691,#112692,#112693,#112694,#112695,#112696,#112697,#112698,
#112699,#112700,#112701,#112702,#112703,#112704,#112705,#112706,#112707,
#112708,#112709,#112710,#112711,#112712,#112713,#112714,#112715,#112716,
#112717,#112718,#112719,#112720,#112721,#112722,#112723,#112724,#112725,
#112726,#112727,#112728,#112729,#112730,#112731,#112732,#112733,#112734,
#112735,#112736,#112737,#112738,#112739,#112740,#112741,#112742,#112743,
#112744,#112745,#112746,#112747,#112748,#112749,#112750,#112751,#112752,
#112753,#112754,#112755,#112756,#112757,#112758,#112759,#112760,#112761,
#112762,#112763,#112764,#112765,#112766,#112767,#112768,#112769,#112770,
#112771,#112772,#112773,#112774,#112775,#112776,#112777,#112778,#112779,
#112780,#112781,#112782,#112783,#112784,#112785,#112786,#112787,#112788,
#112789,#112790,#112791,#112792,#112793,#112794,#112795,#112796,#112797,
#112798,#112799,#112800,#112801,#112802,#112803,#112804,#112805,#112806,
#112807,#112808,#112809,#112810,#112811,#112812,#112813,#112814,#112815,
#112816,#112817,#112818,#112819,#112820,#112821,#112822,#112823,#112824,
#112825,#112826,#112827,#112828,#112829,#112830,#112831,#112832,#112833,
#112834,#112835,#112836,#112837,#112838,#112839,#112840,#112841,#112842,
#112843,#112844,#112845,#112846,#112847,#112848,#112849,#112850,#112851,
#112852,#112853,#112854,#112855,#112856,#112857,#112858,#112859,#112860,
#112861,#112862,#112863,#112864,#112865,#112866,#112867,#112868,#112869,
#112870,#112871,#112872,#112873,#112874,#112875,#112876,#112877,#112878,
#112879,#112880,#112881,#112882,#112883,#112884,#112885,#112886,#112887,
#112888,#112889,#112890,#112891,#112892,#112893,#112894,#112895),
 .UNSPECIFIED.,.F.,.F.,(4,3,3,3,3,3,3,3,3,3,3,3,3,3,3,3,3,3,3,3,3,3,3,3,
3,3,3,3,3,3,3,3,3,3,3,3,3,3,3,3,3,3,3,3,3,3,3,3,3,3,3,3,3,3,3,3,3,3,3,3,
3,3,3,3,3,3,3,3,3,3,3,3,3,4),(1316.32732185411,1316.41123632682,1316.49515365699,
1316.57909123808,1316.66306647283,1316.74714905078,1316.83129168248,1316.91556945888,
1316.96036089986,1317.04409961171,1317.12773512307,1317.21128756647,1317.29477700232,
1317.37823095294,1317.46166744678,1317.54510455654,1317.62856035146,1317.71210484419,
1317.79569392713,1317.87941719468,1317.96009691058,1318.04383562243,1318.12747113379,
1318.21102357719,1318.29451301304,1318.37796696366,1318.4614034575,1318.54484056726,
1318.62829636218,1318.71184085491,1318.79542993785,1318.8791532054,1318.9598329213,
1319.04357163315,1319.12720714451,1319.21075958791,1319.29424902376,1319.37770297438,
1319.46113946822,1319.54457657798,1319.6280323729,1319.71157686563,1319.79516594857,
1319.87888921612,1319.95956893202,1320.04330764387,1320.12694315523,1320.21049559863,
1320.29398503448,1320.3774389851,1320.46087547894,1320.5443125887,1320.62776838362,
1320.71131287635,1320.79490195929,1320.87862522685,1320.95930494274,1321.04304365459,
1321.12667916595,1321.21023160935,1321.2937210452,1321.37717499582,1321.46061148966,
1321.54404859942,1321.62750439434,1321.71104888707,1321.79463797001,1321.87836123756,
1321.95904095346,1322.04299957575,1322.12682101002,1322.21056353265,1322.29423344159,
1322.35964844668),.UNSPECIFIED.);
#888=B_SPLINE_CURVE_WITH_KNOTS('',3,(#112896,#112897,#112898,#112899,#112900,
#112901,#112902,#112903,#112904,#112905),.UNSPECIFIED.,.F.,.F.,(4,3,3,4),
(1316.07685146776,1316.17191321989,1316.26636756679,1316.32732185391),
 .UNSPECIFIED.);
#889=B_SPLINE_CURVE_WITH_KNOTS('',3,(#112907,#112908,#112909,#112910,#112911,
#112912,#112913,#112914,#112915,#112916,#112917,#112918,#112919),
 .UNSPECIFIED.,.F.,.F.,(4,3,3,3,4),(1316.07565830488,1316.15928389047,1316.24302883045,
1316.27091550886,1316.32732185411),.UNSPECIFIED.);
#890=B_SPLINE_CURVE_WITH_KNOTS('',3,(#112920,#112921,#112922,#112923,#112924,
#112925,#112926,#112927,#112928,#112929,#112930,#112931,#112932,#112933,
#112934,#112935,#112936,#112937,#112938,#112939,#112940,#112941,#112942,
#112943,#112944,#112945,#112946,#112947,#112948,#112949,#112950,#112951,
#112952,#112953,#112954,#112955,#112956,#112957,#112958,#112959,#112960,
#112961,#112962,#112963,#112964,#112965,#112966,#112967,#112968,#112969,
#112970,#112971,#112972,#112973,#112974,#112975,#112976,#112977,#112978,
#112979,#112980,#112981,#112982,#112983,#112984,#112985,#112986,#112987,
#112988,#112989,#112990,#112991,#112992,#112993,#112994,#112995,#112996,
#112997,#112998,#112999,#113000,#113001,#113002,#113003,#113004,#113005,
#113006,#113007,#113008,#113009,#113010,#113011,#113012,#113013,#113014,
#113015,#113016,#113017,#113018,#113019,#113020,#113021,#113022,#113023,
#113024,#113025,#113026,#113027,#113028,#113029,#113030,#113031,#113032,
#113033,#113034,#113035,#113036,#113037,#113038,#113039,#113040,#113041,
#113042,#113043,#113044,#113045,#113046,#113047,#113048,#113049,#113050,
#113051,#113052,#113053,#113054,#113055,#113056,#113057,#113058,#113059,
#113060,#113061,#113062,#113063,#113064,#113065,#113066,#113067,#113068,
#113069,#113070,#113071,#113072,#113073,#113074,#113075,#113076,#113077,
#113078,#113079,#113080,#113081,#113082,#113083,#113084,#113085,#113086,
#113087,#113088,#113089,#113090,#113091,#113092,#113093,#113094,#113095,
#113096,#113097,#113098,#113099,#113100,#113101,#113102,#113103,#113104,
#113105,#113106,#113107,#113108,#113109,#113110,#113111,#113112,#113113,
#113114,#113115,#113116,#113117,#113118,#113119,#113120,#113121,#113122,
#113123,#113124,#113125,#113126,#113127,#113128,#113129,#113130,#113131,
#113132,#113133,#113134,#113135,#113136,#113137,#113138,#113139),
 .UNSPECIFIED.,.F.,.F.,(4,3,3,3,3,3,3,3,3,3,3,3,3,3,3,3,3,3,3,3,3,3,3,3,
3,3,3,3,3,3,3,3,3,3,3,3,3,3,3,3,3,3,3,3,3,3,3,3,3,3,3,3,3,3,3,3,3,3,3,3,
3,3,3,3,3,3,3,3,3,3,3,3,3,4),(1316.32732185422,1316.41033731549,1316.49325348052,
1316.57609114802,1316.66291119447,1316.74566196677,1316.82840213601,1316.91115037352,
1316.9939253533,1317.07679084491,1317.15970931004,1317.2427458313,1317.27065151958,
1317.35439023143,1317.43802574279,1317.52157818619,1317.60506762204,1317.68852157266,
1317.7719580665,1317.85539517626,1317.93885097118,1318.02239546391,1318.10598454685,
1318.18970781441,1318.2703875303,1318.35412624215,1318.43776175351,1318.52131419691,
1318.60480363276,1318.68825758338,1318.77169407722,1318.85513118698,1318.9385869819,
1319.02213147462,1319.10572055757,1319.18944382512,1319.27012354102,1319.35386225287,
1319.43749776423,1319.52105020763,1319.60453964348,1319.6879935941,1319.77143008794,
1319.8548671977,1319.93832299262,1320.02186748535,1320.10545656829,1320.18917983584,
1320.26985955174,1320.35359826359,1320.43723377495,1320.52078621835,1320.6042756542,
1320.68772960482,1320.77116609866,1320.85460320842,1320.93805900334,1321.02160349607,
1321.10519257901,1321.18891584657,1321.26959556246,1321.35333427431,1321.43696978567,
1321.52052222907,1321.60401166492,1321.68746561554,1321.77090210938,1321.85433921914,
1321.93779501405,1322.02133950678,1322.10492858972,1322.18865185728,1322.26933157318,
1322.35993616154),.UNSPECIFIED.);
#891=B_SPLINE_CURVE_WITH_KNOTS('',3,(#113145,#113146,#113147,#113148,#113149,
#113150,#113151,#113152,#113153,#113154,#113155,#113156,#113157,#113158,
#113159,#113160,#113161,#113162,#113163,#113164,#113165,#113166,#113167,
#113168,#113169,#113170,#113171,#113172,#113173,#113174,#113175,#113176,
#113177,#113178,#113179,#113180,#113181,#113182,#113183,#113184,#113185,
#113186,#113187,#113188,#113189,#113190,#113191,#113192,#113193,#113194,
#113195,#113196,#113197,#113198,#113199,#113200,#113201,#113202,#113203,
#113204,#113205,#113206,#113207,#113208,#113209,#113210,#113211,#113212,
#113213,#113214,#113215,#113216,#113217,#113218,#113219,#113220,#113221,
#113222,#113223,#113224,#113225,#113226,#113227,#113228,#113229,#113230,
#113231,#113232,#113233,#113234,#113235,#113236,#113237,#113238,#113239,
#113240,#113241,#113242,#113243,#113244,#113245,#113246,#113247,#113248,
#113249,#113250,#113251,#113252,#113253,#113254,#113255,#113256,#113257,
#113258,#113259,#113260,#113261,#113262,#113263,#113264,#113265,#113266,
#113267,#113268,#113269,#113270,#113271,#113272,#113273,#113274,#113275,
#113276,#113277,#113278,#113279,#113280,#113281,#113282,#113283,#113284,
#113285,#113286,#113287,#113288,#113289,#113290,#113291,#113292,#113293,
#113294,#113295,#113296,#113297,#113298,#113299,#113300,#113301,#113302,
#113303,#113304,#113305,#113306,#113307,#113308,#113309,#113310,#113311,
#113312,#113313,#113314,#113315,#113316,#113317,#113318,#113319,#113320,
#113321,#113322,#113323,#113324,#113325,#113326,#113327,#113328,#113329,
#113330,#113331,#113332,#113333,#113334,#113335,#113336,#113337,#113338,
#113339,#113340,#113341,#113342,#113343,#113344,#113345,#113346,#113347,
#113348,#113349,#113350,#113351,#113352,#113353,#113354,#113355,#113356,
#113357,#113358,#113359,#113360,#113361,#113362,#113363,#113364),
 .UNSPECIFIED.,.F.,.F.,(4,3,3,3,3,3,3,3,3,3,3,3,3,3,3,3,3,3,3,3,3,3,3,3,
3,3,3,3,3,3,3,3,3,3,3,3,3,3,3,3,3,3,3,3,3,3,3,3,3,3,3,3,3,3,3,3,3,3,3,3,
3,3,3,3,3,3,3,3,3,3,3,3,3,4),(1322.61050716148,1322.7064694113,1322.8029179108,
1322.89997941325,1322.95877696418,1323.04251567603,1323.12615118739,1323.20970363079,
1323.29319306664,1323.37664701726,1323.4600835111,1323.54352062086,1323.62697641578,
1323.7105209085,1323.79410999145,1323.877833259,1323.9585129749,1324.04225168675,
1324.12588719811,1324.20943964151,1324.29292907736,1324.37638302798,1324.45981952182,
1324.54325663158,1324.6267124265,1324.71025691923,1324.79384600217,1324.87756926972,
1324.95824898562,1325.04198769747,1325.12562320883,1325.20917565223,1325.29266508808,
1325.3761190387,1325.45955553254,1325.5429926423,1325.62644843722,1325.70999292995,
1325.79358201289,1325.87730528044,1325.95798499634,1326.04172370819,1326.12535921955,
1326.20891166295,1326.2924010988,1326.37585504942,1326.45929154326,1326.54272865302,
1326.62618444794,1326.70972894067,1326.79331802361,1326.87704129116,1326.95772100706,
1327.04145971891,1327.12509523027,1327.20864767367,1327.29213710952,1327.37559106014,
1327.45902755398,1327.54246466374,1327.62592045866,1327.70946495139,1327.79305403433,
1327.87677730188,1327.95745701778,1328.04300836688,1328.12585651517,1328.20862958704,
1328.29134640098,1328.37402572821,1328.45669979063,1328.53937184885,1328.62207975794,
1328.64186781057),.UNSPECIFIED.);
#892=B_SPLINE_CURVE_WITH_KNOTS('',3,(#113365,#113366,#113367,#113368,#113369,
#113370,#113371,#113372,#113373,#113374),.UNSPECIFIED.,.F.,.F.,(4,3,3,4),
(1322.35964844668,1322.44325162287,1322.52687939208,1322.61050716129),
 .UNSPECIFIED.);
#893=B_SPLINE_CURVE_WITH_KNOTS('',3,(#113376,#113377,#113378,#113379,#113380,
#113381,#113382,#113383,#113384,#113385),.UNSPECIFIED.,.F.,.F.,(4,3,3,4),
(1322.35993616154,1322.45721358474,1322.55370132972,1322.6105071611),
 .UNSPECIFIED.);
#894=B_SPLINE_CURVE_WITH_KNOTS('',3,(#113386,#113387,#113388,#113389,#113390,
#113391,#113392,#113393,#113394,#113395,#113396,#113397,#113398,#113399,
#113400,#113401,#113402,#113403,#113404,#113405,#113406,#113407,#113408,
#113409,#113410,#113411,#113412,#113413,#113414,#113415,#113416,#113417,
#113418,#113419,#113420,#113421,#113422,#113423,#113424,#113425,#113426,
#113427,#113428,#113429,#113430,#113431,#113432,#113433,#113434,#113435,
#113436,#113437,#113438,#113439,#113440,#113441,#113442,#113443,#113444,
#113445,#113446,#113447,#113448,#113449,#113450,#113451,#113452,#113453,
#113454,#113455,#113456,#113457,#113458,#113459,#113460,#113461,#113462,
#113463,#113464,#113465,#113466,#113467,#113468,#113469,#113470,#113471,
#113472,#113473,#113474,#113475,#113476,#113477,#113478,#113479,#113480,
#113481,#113482,#113483,#113484,#113485,#113486,#113487,#113488,#113489,
#113490,#113491,#113492,#113493,#113494,#113495,#113496,#113497,#113498,
#113499,#113500,#113501,#113502,#113503,#113504,#113505,#113506,#113507,
#113508,#113509,#113510,#113511,#113512,#113513,#113514,#113515,#113516,
#113517,#113518,#113519,#113520,#113521,#113522,#113523,#113524,#113525,
#113526,#113527,#113528,#113529,#113530,#113531,#113532,#113533,#113534,
#113535,#113536,#113537,#113538,#113539,#113540,#113541,#113542,#113543,
#113544,#113545,#113546,#113547,#113548,#113549,#113550,#113551,#113552,
#113553,#113554,#113555,#113556,#113557,#113558,#113559,#113560,#113561,
#113562,#113563,#113564,#113565,#113566,#113567,#113568,#113569,#113570,
#113571,#113572,#113573,#113574,#113575,#113576,#113577,#113578,#113579,
#113580,#113581,#113582,#113583,#113584,#113585,#113586,#113587,#113588,
#113589,#113590,#113591,#113592,#113593,#113594,#113595,#113596,#113597,
#113598,#113599,#113600,#113601,#113602,#113603,#113604,#113605),
 .UNSPECIFIED.,.F.,.F.,(4,3,3,3,3,3,3,3,3,3,3,3,3,3,3,3,3,3,3,3,3,3,3,3,
3,3,3,3,3,3,3,3,3,3,3,3,3,3,3,3,3,3,3,3,3,3,3,3,3,3,3,3,3,3,3,3,3,3,3,3,
3,3,3,3,3,3,3,3,3,3,3,3,3,4),(1322.61050716129,1322.69400757452,1322.77749817373,
1322.86099688777,1322.94452164693,1323.02814444939,1323.11181799589,1323.19563090804,
1323.2690675839,1323.35280629575,1323.43644180711,1323.51999425051,1323.60348368636,
1323.68693763698,1323.77037413082,1323.85381124058,1323.9372670355,1324.02081152823,
1324.10440061117,1324.18812387873,1324.26880359462,1324.35254230647,1324.43617781783,
1324.51973026123,1324.60321969708,1324.6866736477,1324.77011014154,1324.8535472513,
1324.93700304621,1325.02054753894,1325.10413662188,1325.18785988944,1325.26853960534,
1325.35227831719,1325.43591382855,1325.51946627195,1325.6029557078,1325.68640965842,
1325.76984615226,1325.85328326202,1325.93673905694,1326.02028354967,1326.10387263261,
1326.18759590016,1326.26827561606,1326.35201432791,1326.43564983927,1326.51920228267,
1326.60269171852,1326.68614566914,1326.76958216298,1326.85301927274,1326.93647506766,
1327.02001956039,1327.10360864333,1327.18733191089,1327.26801162678,1327.35175033863,
1327.43538584999,1327.51893829339,1327.60242772924,1327.68588167986,1327.7693181737,
1327.85275528346,1327.93621107838,1328.01975557111,1328.10334465405,1328.1870679216,
1328.2677476375,1328.35218423068,1328.43647771956,1328.52068855315,1328.60481838857,
1328.64295744021),.UNSPECIFIED.);
#895=B_SPLINE_CURVE_WITH_KNOTS('',3,(#113611,#113612,#113613,#113614,#113615,
#113616,#113617,#113618,#113619,#113620,#113621,#113622,#113623,#113624,
#113625,#113626,#113627,#113628,#113629,#113630,#113631,#113632,#113633,
#113634,#113635,#113636,#113637,#113638,#113639,#113640,#113641,#113642,
#113643,#113644,#113645,#113646,#113647,#113648,#113649,#113650,#113651,
#113652,#113653,#113654,#113655,#113656,#113657,#113658,#113659,#113660,
#113661,#113662,#113663,#113664,#113665,#113666,#113667,#113668,#113669,
#113670,#113671,#113672,#113673,#113674,#113675,#113676,#113677,#113678,
#113679,#113680,#113681,#113682,#113683,#113684,#113685,#113686,#113687,
#113688,#113689,#113690,#113691,#113692,#113693,#113694,#113695,#113696,
#113697,#113698,#113699,#113700,#113701,#113702,#113703,#113704,#113705,
#113706,#113707,#113708,#113709,#113710,#113711,#113712,#113713,#113714,
#113715,#113716,#113717,#113718,#113719,#113720,#113721,#113722,#113723,
#113724,#113725,#113726,#113727,#113728,#113729,#113730,#113731,#113732,
#113733,#113734,#113735,#113736,#113737,#113738,#113739,#113740,#113741,
#113742,#113743,#113744,#113745,#113746,#113747,#113748,#113749,#113750,
#113751,#113752,#113753,#113754,#113755,#113756,#113757,#113758,#113759,
#113760,#113761,#113762,#113763,#113764,#113765,#113766,#113767,#113768,
#113769,#113770,#113771,#113772,#113773,#113774,#113775,#113776,#113777,
#113778,#113779,#113780,#113781,#113782,#113783,#113784,#113785,#113786,
#113787,#113788,#113789,#113790,#113791,#113792,#113793,#113794,#113795,
#113796,#113797,#113798,#113799,#113800,#113801,#113802,#113803,#113804,
#113805,#113806,#113807,#113808,#113809,#113810,#113811,#113812,#113813,
#113814,#113815,#113816,#113817,#113818,#113819,#113820,#113821,#113822,
#113823,#113824,#113825,#113826,#113827,#113828,#113829,#113830),
 .UNSPECIFIED.,.F.,.F.,(4,3,3,3,3,3,3,3,3,3,3,3,3,3,3,3,3,3,3,3,3,3,3,3,
3,3,3,3,3,3,3,3,3,3,3,3,3,3,3,3,3,3,3,3,3,3,3,3,3,3,3,3,3,3,3,3,3,3,3,3,
3,3,3,3,3,3,3,3,3,3,3,3,3,4),(1328.89369246847,1328.9571930285,1329.04093174035,
1329.12456725171,1329.20811969511,1329.29160913096,1329.37506308158,1329.45849957542,
1329.54193668518,1329.6253924801,1329.70893697283,1329.79252605577,1329.87624932332,
1329.95692903922,1330.04066775107,1330.12430326243,1330.20785570583,1330.29134514168,
1330.3747990923,1330.45823558614,1330.5416726959,1330.62512849082,1330.70867298355,
1330.79226206649,1330.87598533405,1330.95666504994,1331.04040376179,1331.12403927315,
1331.20759171655,1331.2910811524,1331.37453510302,1331.45797159686,1331.54140870662,
1331.62486450154,1331.70840899427,1331.79199807721,1331.87572134476,1331.95640106066,
1332.04013977251,1332.12377528387,1332.20732772727,1332.29081716312,1332.37427111374,
1332.45770760758,1332.54114471734,1332.62460051226,1332.70814500499,1332.79173408793,
1332.87545735548,1332.95613707138,1333.03987578323,1333.12351129459,1333.20706373799,
1333.29055317384,1333.37400712446,1333.4574436183,1333.54088072806,1333.62433652297,
1333.7078810157,1333.79147009865,1333.8751933662,1333.9558730821,1334.03961349212,
1334.12325030642,1334.20680365916,1334.29029361203,1334.37374607242,1334.45718051726,
1334.54061501886,1334.62406764562,1334.70760129389,1334.79117930146,1334.87487359557,
1334.92564171414),.UNSPECIFIED.);
#896=B_SPLINE_CURVE_WITH_KNOTS('',3,(#113831,#113832,#113833,#113834,#113835,
#113836,#113837,#113838,#113839,#113840),.UNSPECIFIED.,.F.,.F.,(4,3,3,4),
(1328.64186781057,1328.72466467188,1328.80917857012,1328.89369246835),
 .UNSPECIFIED.);
#897=B_SPLINE_CURVE_WITH_KNOTS('',3,(#113842,#113843,#113844,#113845,#113846,
#113847,#113848,#113849,#113850,#113851),.UNSPECIFIED.,.F.,.F.,(4,3,3,4),
(1328.64295744021,1328.72701616532,1328.81106206604,1328.89369246847),
 .UNSPECIFIED.);
#898=B_SPLINE_CURVE_WITH_KNOTS('',3,(#113852,#113853,#113854,#113855,#113856,
#113857,#113858,#113859,#113860,#113861,#113862,#113863,#113864,#113865,
#113866,#113867,#113868,#113869,#113870,#113871,#113872,#113873,#113874,
#113875,#113876,#113877,#113878,#113879,#113880,#113881,#113882,#113883,
#113884,#113885,#113886,#113887,#113888,#113889,#113890,#113891,#113892,
#113893,#113894,#113895,#113896,#113897,#113898,#113899,#113900,#113901,
#113902,#113903,#113904,#113905,#113906,#113907,#113908,#113909,#113910,
#113911,#113912,#113913,#113914,#113915,#113916,#113917,#113918,#113919,
#113920,#113921,#113922,#113923,#113924,#113925,#113926,#113927,#113928,
#113929,#113930,#113931,#113932,#113933,#113934,#113935,#113936,#113937,
#113938,#113939,#113940,#113941,#113942,#113943,#113944,#113945,#113946,
#113947,#113948,#113949,#113950,#113951,#113952,#113953,#113954,#113955,
#113956,#113957,#113958,#113959,#113960,#113961,#113962,#113963,#113964,
#113965,#113966,#113967,#113968,#113969,#113970,#113971,#113972,#113973,
#113974,#113975,#113976,#113977,#113978,#113979,#113980,#113981,#113982,
#113983,#113984,#113985,#113986,#113987,#113988,#113989,#113990,#113991,
#113992,#113993,#113994,#113995,#113996,#113997,#113998,#113999,#114000,
#114001,#114002,#114003,#114004,#114005,#114006,#114007,#114008,#114009,
#114010,#114011,#114012,#114013,#114014,#114015,#114016,#114017,#114018,
#114019,#114020,#114021,#114022,#114023,#114024,#114025,#114026,#114027,
#114028,#114029,#114030,#114031,#114032,#114033,#114034,#114035,#114036,
#114037,#114038,#114039,#114040,#114041,#114042,#114043,#114044,#114045,
#114046,#114047,#114048,#114049,#114050,#114051,#114052,#114053,#114054,
#114055,#114056,#114057,#114058,#114059,#114060,#114061,#114062,#114063,
#114064,#114065,#114066,#114067,#114068),.UNSPECIFIED.,.F.,.F.,(4,3,3,3,
3,3,3,3,3,3,3,3,3,3,3,3,3,3,3,3,3,3,3,3,3,3,3,3,3,3,3,3,3,3,3,3,3,3,3,3,
3,3,3,3,3,3,3,3,3,3,3,3,3,3,3,3,3,3,3,3,3,3,3,3,3,3,3,3,3,3,3,3,4),(1328.89369246867,
1328.98771917001,1329.08211115352,1329.17702388892,1329.26748364822,1329.35122236007,
1329.43485787143,1329.51841031483,1329.60189975068,1329.6853537013,1329.76879019514,
1329.8522273049,1329.93568309982,1330.01922759255,1330.10281667549,1330.18653994305,
1330.26721965894,1330.35095837079,1330.43459388215,1330.51814632555,1330.6016357614,
1330.68508971202,1330.76852620586,1330.85196331562,1330.93541911054,1331.01896360326,
1331.10255268621,1331.18627595376,1331.26695566966,1331.35069438151,1331.43432989287,
1331.51788233627,1331.60137177212,1331.68482572274,1331.76826221658,1331.85169932634,
1331.93515512126,1332.01869961399,1332.10228869693,1332.18601196448,1332.26669168038,
1332.35043039223,1332.43406590359,1332.51761834699,1332.60110778284,1332.68456173346,
1332.7679982273,1332.85143533706,1332.93489113198,1333.01843562471,1333.10202470765,
1333.18574797521,1333.2664276911,1333.35016640295,1333.43380191431,1333.51735435771,
1333.60084379356,1333.68429774418,1333.76773423802,1333.85117134778,1333.9346271427,
1334.01817163543,1334.10176071837,1334.18548398592,1334.26616370182,1334.34890444293,
1334.43155063891,1334.51412132194,1334.59663545726,1334.67912307257,1334.76159207413,
1334.84409348801,1334.92504027154),.UNSPECIFIED.);
#899=B_SPLINE_CURVE_WITH_KNOTS('',3,(#114074,#114075,#114076,#114077,#114078,
#114079,#114080,#114081,#114082,#114083,#114084,#114085,#114086,#114087,
#114088,#114089,#114090,#114091,#114092,#114093,#114094,#114095,#114096,
#114097,#114098,#114099,#114100,#114101,#114102,#114103,#114104,#114105,
#114106,#114107,#114108,#114109,#114110,#114111,#114112,#114113,#114114,
#114115,#114116,#114117,#114118,#114119,#114120,#114121,#114122,#114123,
#114124,#114125,#114126,#114127,#114128,#114129,#114130,#114131,#114132,
#114133,#114134,#114135,#114136,#114137,#114138,#114139,#114140,#114141,
#114142,#114143,#114144,#114145,#114146,#114147,#114148,#114149,#114150,
#114151,#114152,#114153,#114154,#114155,#114156,#114157,#114158,#114159,
#114160,#114161,#114162,#114163,#114164,#114165,#114166,#114167,#114168,
#114169,#114170,#114171,#114172,#114173,#114174,#114175,#114176,#114177,
#114178,#114179,#114180,#114181,#114182,#114183,#114184,#114185,#114186,
#114187,#114188,#114189,#114190,#114191,#114192,#114193,#114194,#114195,
#114196,#114197,#114198,#114199,#114200,#114201,#114202,#114203,#114204,
#114205,#114206,#114207,#114208,#114209,#114210,#114211,#114212,#114213,
#114214,#114215,#114216,#114217,#114218,#114219,#114220,#114221,#114222,
#114223,#114224,#114225,#114226,#114227,#114228,#114229,#114230,#114231,
#114232,#114233,#114234,#114235,#114236,#114237,#114238,#114239,#114240,
#114241,#114242,#114243,#114244,#114245,#114246,#114247,#114248,#114249,
#114250,#114251,#114252,#114253,#114254,#114255,#114256,#114257,#114258,
#114259,#114260,#114261,#114262,#114263,#114264,#114265,#114266,#114267,
#114268,#114269,#114270,#114271,#114272,#114273,#114274,#114275,#114276,
#114277,#114278,#114279,#114280,#114281,#114282,#114283,#114284,#114285,
#114286,#114287,#114288,#114289,#114290,#114291,#114292,#114293),
 .UNSPECIFIED.,.F.,.F.,(4,3,3,3,3,3,3,3,3,3,3,3,3,3,3,3,3,3,3,3,3,3,3,3,
3,3,3,3,3,3,3,3,3,3,3,3,3,3,3,3,3,3,3,3,3,3,3,3,3,3,3,3,3,3,3,3,3,3,3,3,
3,3,3,3,3,3,3,3,3,3,3,3,3,4),(1335.17687777579,1335.25930715332,1335.34167396931,
1335.42400671075,1335.50632418332,1335.58864534924,1335.67098917132,1335.75342036133,
1335.83590140164,1335.91850174716,1335.95534510354,1336.03908381539,1336.12271932675,
1336.20627177015,1336.289761206,1336.37321515662,1336.45665165046,1336.54008876022,
1336.62354455513,1336.70708904786,1336.7906781308,1336.87440139836,1336.95508111426,
1337.03881982611,1337.12245533747,1337.20600778087,1337.28949721672,1337.37295116734,
1337.45638766118,1337.53982477094,1337.62328056586,1337.70682505859,1337.79041414153,
1337.87413740909,1337.95481712498,1338.03855583683,1338.12219134819,1338.20574379159,
1338.28923322744,1338.37268717806,1338.4561236719,1338.53956078166,1338.62301657658,
1338.70656106931,1338.79015015225,1338.8738734198,1338.9545531357,1339.03829184755,
1339.12192735891,1339.20547980231,1339.28896923816,1339.37242318878,1339.45585968262,
1339.53929679238,1339.6227525873,1339.70629708003,1339.78988616297,1339.87360943052,
1339.95428914642,1340.03802785827,1340.12166336963,1340.20521581303,1340.28870524888,
1340.3721591995,1340.45559569334,1340.5390328031,1340.62248859802,1340.70603309075,
1340.78962217369,1340.87334544125,1340.95402515714,1341.04184027084,1341.12946320536,
1341.2097260217),.UNSPECIFIED.);
#900=B_SPLINE_CURVE_WITH_KNOTS('',3,(#114294,#114295,#114296,#114297,#114298,
#114299,#114300,#114301,#114302,#114303),.UNSPECIFIED.,.F.,.F.,(4,3,3,4),
(1334.92564171414,1334.95560909282,1335.07008319006,1335.17687777565),
 .UNSPECIFIED.);
#901=B_SPLINE_CURVE_WITH_KNOTS('',3,(#114305,#114306,#114307,#114308,#114309,
#114310,#114311,#114312,#114313,#114314),.UNSPECIFIED.,.F.,.F.,(4,3,3,4),
(1334.92504027154,1335.00761918804,1335.09224848178,1335.17687777552),
 .UNSPECIFIED.);
#902=B_SPLINE_CURVE_WITH_KNOTS('',3,(#114315,#114316,#114317,#114318,#114319,
#114320,#114321,#114322,#114323,#114324,#114325,#114326,#114327,#114328,
#114329,#114330,#114331,#114332,#114333,#114334,#114335,#114336,#114337,
#114338,#114339,#114340,#114341,#114342,#114343,#114344,#114345,#114346,
#114347,#114348,#114349,#114350,#114351,#114352,#114353,#114354,#114355,
#114356,#114357,#114358,#114359,#114360,#114361,#114362,#114363,#114364,
#114365,#114366,#114367,#114368,#114369,#114370,#114371,#114372,#114373,
#114374,#114375,#114376,#114377,#114378,#114379,#114380,#114381,#114382,
#114383,#114384,#114385,#114386,#114387,#114388,#114389,#114390,#114391,
#114392,#114393,#114394,#114395,#114396,#114397,#114398,#114399,#114400,
#114401,#114402,#114403,#114404,#114405,#114406,#114407,#114408,#114409,
#114410,#114411,#114412,#114413,#114414,#114415,#114416,#114417,#114418,
#114419,#114420,#114421,#114422,#114423,#114424,#114425,#114426,#114427,
#114428,#114429,#114430,#114431,#114432,#114433,#114434,#114435,#114436,
#114437,#114438,#114439,#114440,#114441,#114442,#114443,#114444,#114445,
#114446,#114447,#114448,#114449,#114450,#114451,#114452,#114453,#114454,
#114455,#114456,#114457,#114458,#114459,#114460,#114461,#114462,#114463,
#114464,#114465,#114466,#114467,#114468,#114469,#114470,#114471,#114472,
#114473,#114474,#114475,#114476,#114477,#114478,#114479,#114480,#114481,
#114482,#114483,#114484,#114485,#114486,#114487,#114488,#114489,#114490,
#114491,#114492,#114493,#114494,#114495,#114496,#114497,#114498,#114499,
#114500,#114501,#114502,#114503,#114504,#114505,#114506,#114507,#114508,
#114509,#114510,#114511,#114512,#114513,#114514,#114515,#114516,#114517,
#114518,#114519,#114520,#114521,#114522,#114523,#114524,#114525,#114526,
#114527,#114528,#114529,#114530,#114531,#114532,#114533,#114534),
 .UNSPECIFIED.,.F.,.F.,(4,3,3,3,3,3,3,3,3,3,3,3,3,3,3,3,3,3,3,3,3,3,3,3,
3,3,3,3,3,3,3,3,3,3,3,3,3,3,3,3,3,3,3,3,3,3,3,3,3,3,3,3,3,3,3,3,3,3,3,3,
3,3,3,3,3,3,3,3,3,3,3,3,3,4),(1335.17687777565,1335.26589971254,1335.34963842439,
1335.43327393575,1335.51682637915,1335.600315815,1335.68376976562,1335.76720625946,
1335.85064336922,1335.93409916414,1336.01764365687,1336.10123273981,1336.18495600736,
1336.26563572326,1336.34937443511,1336.43300994647,1336.51656238987,1336.60005182572,
1336.68350577634,1336.76694227018,1336.85037937994,1336.93383517486,1337.01737966758,
1337.10096875053,1337.18469201808,1337.26537173398,1337.34911044583,1337.43274595719,
1337.51629840059,1337.59978783644,1337.68324178706,1337.7666782809,1337.85011539066,
1337.93357118558,1338.01711567831,1338.10070476125,1338.1844280288,1338.2651077447,
1338.34884645655,1338.43248196791,1338.51603441131,1338.59952384716,1338.68297779778,
1338.76641429162,1338.84985140138,1338.9333071963,1339.01685168903,1339.10044077197,
1339.18416403952,1339.26484375542,1339.34858246727,1339.43221797863,1339.51577042203,
1339.59925985788,1339.6827138085,1339.76615030234,1339.8495874121,1339.93304320702,
1340.01658769975,1340.10017678269,1340.18390005025,1340.26457976614,1340.34832166108,
1340.43195962205,1340.51551378467,1340.60216282896,1340.68561311271,1340.76904558688,
1340.85247832314,1340.93592938927,1341.01945564263,1341.10302667224,1341.18669949919,
1341.20870613901),.UNSPECIFIED.);
#903=B_SPLINE_CURVE_WITH_KNOTS('',3,(#114540,#114541,#114542,#114543,#114544,
#114545,#114546,#114547,#114548,#114549,#114550,#114551,#114552,#114553,
#114554,#114555,#114556,#114557,#114558,#114559,#114560,#114561,#114562,
#114563,#114564,#114565,#114566,#114567,#114568,#114569,#114570,#114571,
#114572,#114573,#114574,#114575,#114576,#114577,#114578,#114579,#114580,
#114581,#114582,#114583,#114584,#114585,#114586,#114587,#114588,#114589,
#114590,#114591,#114592,#114593,#114594,#114595,#114596,#114597,#114598,
#114599,#114600,#114601,#114602,#114603,#114604,#114605,#114606,#114607,
#114608,#114609,#114610,#114611,#114612,#114613,#114614,#114615,#114616,
#114617,#114618,#114619,#114620,#114621,#114622,#114623,#114624,#114625,
#114626,#114627,#114628,#114629,#114630,#114631,#114632,#114633,#114634,
#114635,#114636,#114637,#114638,#114639,#114640,#114641,#114642,#114643,
#114644,#114645,#114646,#114647,#114648,#114649,#114650,#114651,#114652,
#114653,#114654,#114655,#114656,#114657,#114658,#114659,#114660,#114661,
#114662,#114663,#114664,#114665,#114666,#114667,#114668,#114669,#114670,
#114671,#114672,#114673,#114674,#114675,#114676,#114677,#114678,#114679,
#114680,#114681,#114682,#114683,#114684,#114685,#114686,#114687,#114688,
#114689,#114690,#114691,#114692,#114693,#114694,#114695,#114696,#114697,
#114698,#114699,#114700,#114701,#114702,#114703,#114704,#114705,#114706,
#114707,#114708,#114709,#114710,#114711,#114712,#114713,#114714,#114715,
#114716,#114717,#114718,#114719,#114720,#114721,#114722,#114723,#114724,
#114725,#114726,#114727,#114728,#114729,#114730,#114731,#114732,#114733,
#114734,#114735,#114736,#114737,#114738,#114739,#114740,#114741,#114742,
#114743,#114744,#114745,#114746,#114747,#114748,#114749,#114750,#114751,
#114752,#114753,#114754,#114755,#114756,#114757,#114758,#114759),
 .UNSPECIFIED.,.F.,.F.,(4,3,3,3,3,3,3,3,3,3,3,3,3,3,3,3,3,3,3,3,3,3,3,3,
3,3,3,3,3,3,3,3,3,3,3,3,3,3,3,3,3,3,3,3,3,3,3,3,3,3,3,3,3,3,3,3,3,3,3,3,
3,3,3,3,3,3,3,3,3,3,3,3,3,4),(1341.46006308301,1341.54769406803,1341.63544859998,
1341.72341826644,1341.81150254846,1341.89978983354,1341.95376116786,1342.03749987971,
1342.12113539107,1342.20468783447,1342.28817727032,1342.37163122094,1342.45506771478,
1342.53850482454,1342.62196061946,1342.70550511219,1342.78909419513,1342.87281746268,
1342.95349717858,1343.03723589043,1343.12087140179,1343.20442384519,1343.28791328104,
1343.37136723166,1343.4548037255,1343.53824083526,1343.62169663017,1343.7052411229,
1343.78883020584,1343.8725534734,1343.9532331893,1344.03697190115,1344.12060741251,
1344.20415985591,1344.28764929176,1344.37110324238,1344.45453973623,1344.53797684598,
1344.6214326409,1344.70497713363,1344.78856621657,1344.87228948413,1344.95296920002,
1345.03670791187,1345.12034342323,1345.20389586663,1345.28738530249,1345.3708392531,
1345.45427574695,1345.5377128567,1345.62116865162,1345.70471314435,1345.78830222729,
1345.87202549485,1345.95270521075,1346.0364439226,1346.12007943396,1346.20363187736,
1346.28712131322,1346.37057526383,1346.45401175768,1346.53744886743,1346.62090466235,
1346.70444915508,1346.78803823802,1346.87176150558,1346.95244122147,1347.03498522075,
1347.11743280076,1347.19980314424,1347.28211245127,1347.3643860278,1347.44665387749,
1347.49169700283),.UNSPECIFIED.);
#904=B_SPLINE_CURVE_WITH_KNOTS('',3,(#114760,#114761,#114762,#114763,#114764,
#114765,#114766,#114767,#114768,#114769),.UNSPECIFIED.,.F.,.F.,(4,3,3,4),
(1341.2097260217,1341.29709430543,1341.38431122704,1341.46006308283),
 .UNSPECIFIED.);
#905=B_SPLINE_CURVE_WITH_KNOTS('',3,(#114771,#114772,#114773,#114774,#114775,
#114776,#114777,#114778,#114779,#114780),.UNSPECIFIED.,.F.,.F.,(4,3,3,4),
(1341.20870613901,1341.26431577686,1341.3858503157,1341.46006308283),
 .UNSPECIFIED.);
#906=B_SPLINE_CURVE_WITH_KNOTS('',3,(#114781,#114782,#114783,#114784,#114785,
#114786,#114787,#114788,#114789,#114790,#114791,#114792,#114793,#114794,
#114795,#114796,#114797,#114798,#114799,#114800,#114801,#114802,#114803,
#114804,#114805,#114806,#114807,#114808,#114809,#114810,#114811,#114812,
#114813,#114814,#114815,#114816,#114817,#114818,#114819,#114820,#114821,
#114822,#114823,#114824,#114825,#114826,#114827,#114828,#114829,#114830,
#114831,#114832,#114833,#114834,#114835,#114836,#114837,#114838,#114839,
#114840,#114841,#114842,#114843,#114844,#114845,#114846,#114847,#114848,
#114849,#114850,#114851,#114852,#114853,#114854,#114855,#114856,#114857,
#114858,#114859,#114860,#114861,#114862,#114863,#114864,#114865,#114866,
#114867,#114868,#114869,#114870,#114871,#114872,#114873,#114874,#114875,
#114876,#114877,#114878,#114879,#114880,#114881,#114882,#114883,#114884,
#114885,#114886,#114887,#114888,#114889,#114890,#114891,#114892,#114893,
#114894,#114895,#114896,#114897,#114898,#114899,#114900,#114901,#114902,
#114903,#114904,#114905,#114906,#114907,#114908,#114909,#114910,#114911,
#114912,#114913,#114914,#114915,#114916,#114917,#114918,#114919,#114920,
#114921,#114922,#114923,#114924,#114925,#114926,#114927,#114928,#114929,
#114930,#114931,#114932,#114933,#114934,#114935,#114936,#114937,#114938,
#114939,#114940,#114941,#114942,#114943,#114944,#114945,#114946,#114947,
#114948,#114949,#114950,#114951,#114952,#114953,#114954,#114955,#114956,
#114957,#114958,#114959,#114960,#114961,#114962,#114963,#114964,#114965,
#114966,#114967,#114968,#114969,#114970,#114971,#114972,#114973,#114974,
#114975,#114976,#114977,#114978,#114979,#114980,#114981,#114982,#114983,
#114984,#114985,#114986,#114987,#114988,#114989,#114990,#114991,#114992,
#114993,#114994,#114995,#114996,#114997,#114998,#114999,#115000),
 .UNSPECIFIED.,.F.,.F.,(4,3,3,3,3,3,3,3,3,3,3,3,3,3,3,3,3,3,3,3,3,3,3,3,
3,3,3,3,3,3,3,3,3,3,3,3,3,3,3,3,3,3,3,3,3,3,3,3,3,3,3,3,3,3,3,3,3,3,3,3,
3,3,3,3,3,3,3,3,3,3,3,3,3,4),(1341.46006308294,1341.54243437283,1341.62473547885,
1341.7069925143,1341.78922750957,1341.87145948455,1341.9537074545,1342.03603902136,
1342.11841455711,1342.20091606359,1342.26405178758,1342.34779049943,1342.43142601079,
1342.51497845419,1342.59846789004,1342.68192184066,1342.7653583345,1342.84879544426,
1342.93225123918,1343.01579573191,1343.09938481485,1343.1831080824,1343.2637877983,
1343.34752651015,1343.43116202151,1343.51471446491,1343.59820390076,1343.68165785138,
1343.76509434522,1343.84853145498,1343.9319872499,1344.01553174262,1344.09912082557,
1344.18284409312,1344.26352380902,1344.34726252087,1344.43089803223,1344.51445047563,
1344.59793991148,1344.6813938621,1344.76483035594,1344.8482674657,1344.93172326062,
1345.01526775335,1345.09885683629,1345.18258010384,1345.26325981974,1345.34699853159,
1345.43063404295,1345.51418648635,1345.5976759222,1345.68112987282,1345.76456636666,
1345.84800347642,1345.93145927134,1346.01500376407,1346.09859284701,1346.18231611456,
1346.26299583046,1346.34673454231,1346.43037005367,1346.51392249707,1346.59741193292,
1346.68086588354,1346.76430237738,1346.84773948714,1346.93119528206,1347.01473977479,
1347.09832885773,1347.18205212529,1347.26273184118,1347.35159396868,1347.44024804493,
1347.49294053409),.UNSPECIFIED.);
#907=B_SPLINE_CURVE_WITH_KNOTS('',3,(#115006,#115007,#115008,#115009,#115010,
#115011,#115012,#115013,#115014,#115015,#115016,#115017,#115018,#115019,
#115020,#115021,#115022,#115023,#115024,#115025,#115026,#115027,#115028,
#115029,#115030,#115031,#115032,#115033,#115034,#115035,#115036,#115037,
#115038,#115039,#115040,#115041,#115042,#115043,#115044,#115045,#115046,
#115047,#115048,#115049,#115050,#115051,#115052,#115053,#115054,#115055,
#115056,#115057,#115058,#115059,#115060,#115061,#115062,#115063,#115064,
#115065,#115066,#115067,#115068,#115069,#115070,#115071,#115072,#115073,
#115074,#115075,#115076,#115077,#115078,#115079,#115080,#115081,#115082,
#115083,#115084,#115085,#115086,#115087,#115088,#115089,#115090,#115091,
#115092,#115093,#115094,#115095,#115096,#115097,#115098,#115099,#115100,
#115101,#115102,#115103,#115104,#115105,#115106,#115107,#115108,#115109,
#115110,#115111,#115112,#115113,#115114,#115115,#115116,#115117,#115118,
#115119,#115120,#115121,#115122,#115123,#115124,#115125,#115126,#115127,
#115128,#115129,#115130,#115131,#115132,#115133,#115134,#115135,#115136,
#115137,#115138,#115139,#115140,#115141,#115142,#115143,#115144,#115145,
#115146,#115147,#115148,#115149,#115150,#115151,#115152,#115153,#115154,
#115155,#115156,#115157,#115158,#115159,#115160,#115161,#115162,#115163,
#115164,#115165,#115166,#115167,#115168,#115169,#115170,#115171,#115172,
#115173,#115174,#115175,#115176,#115177,#115178,#115179,#115180,#115181,
#115182,#115183,#115184,#115185,#115186,#115187,#115188,#115189,#115190,
#115191,#115192,#115193,#115194,#115195,#115196,#115197,#115198,#115199,
#115200,#115201,#115202,#115203,#115204,#115205,#115206,#115207,#115208,
#115209,#115210,#115211,#115212,#115213,#115214,#115215,#115216,#115217,
#115218,#115219,#115220,#115221,#115222),.UNSPECIFIED.,.F.,.F.,(4,3,3,3,
3,3,3,3,3,3,3,3,3,3,3,3,3,3,3,3,3,3,3,3,3,3,3,3,3,3,3,3,3,3,3,3,3,3,3,3,
3,3,3,3,3,3,3,3,3,3,3,3,3,3,3,3,3,3,3,3,3,3,3,3,3,3,3,3,3,3,3,3,4),(1347.74324839001,
1347.86086686141,1347.95217723219,1348.03591594404,1348.1195514554,1348.2031038988,
1348.28659333465,1348.37004728527,1348.45348377911,1348.53692088887,1348.62037668379,
1348.70392117652,1348.78751025946,1348.87123352702,1348.95191324291,1349.03565195476,
1349.11928746612,1349.20283990952,1349.28632934537,1349.36978329599,1349.45321978983,
1349.53665689959,1349.6201126945,1349.70365718723,1349.78724627017,1349.87096953773,
1349.95164925363,1350.03538796548,1350.11902347684,1350.20257592024,1350.28606535609,
1350.36951930671,1350.45295580055,1350.53639291031,1350.61984870523,1350.70339319796,
1350.7869822809,1350.87070554845,1350.95138526435,1351.0351239762,1351.11875948756,
1351.20231193096,1351.28580136681,1351.36925531743,1351.45269181127,1351.53612892103,
1351.61958471595,1351.70312920868,1351.78671829162,1351.87044155917,1351.95112127507,
1352.03485998692,1352.11849549828,1352.20204794168,1352.28553737753,1352.36899132815,
1352.45242782199,1352.53586493175,1352.61932072667,1352.7028652194,1352.78645430234,
1352.8701775699,1352.95085728579,1353.03460653273,1353.11825025982,1353.20179354662,
1353.28527988452,1353.36872739298,1353.45215416144,1353.53560636913,1353.61906939208,
1353.70260654731,1353.7747814876),.UNSPECIFIED.);
#908=B_SPLINE_CURVE_WITH_KNOTS('',3,(#115223,#115224,#115225,#115226,#115227,
#115228,#115229,#115230,#115231,#115232),.UNSPECIFIED.,.F.,.F.,(4,3,3,4),
(1347.49169700283,1347.57399734248,1347.65862286617,1347.74324838987),
 .UNSPECIFIED.);
#909=B_SPLINE_CURVE_WITH_KNOTS('',3,(#115234,#115235,#115236,#115237,#115238,
#115239,#115240,#115241,#115242,#115243),.UNSPECIFIED.,.F.,.F.,(4,3,3,4),
(1347.49294053409,1347.581325312,1347.66951161927,1347.74324838985),
 .UNSPECIFIED.);
#910=B_SPLINE_CURVE_WITH_KNOTS('',3,(#115244,#115245,#115246,#115247,#115248,
#115249,#115250,#115251,#115252,#115253,#115254,#115255,#115256,#115257,
#115258,#115259,#115260,#115261,#115262,#115263,#115264,#115265,#115266,
#115267,#115268,#115269,#115270,#115271,#115272,#115273,#115274,#115275,
#115276,#115277,#115278,#115279,#115280,#115281,#115282,#115283,#115284,
#115285,#115286,#115287,#115288,#115289,#115290,#115291,#115292,#115293,
#115294,#115295,#115296,#115297,#115298,#115299,#115300,#115301,#115302,
#115303,#115304,#115305,#115306,#115307,#115308,#115309,#115310,#115311,
#115312,#115313,#115314,#115315,#115316,#115317,#115318,#115319,#115320,
#115321,#115322,#115323,#115324,#115325,#115326,#115327,#115328,#115329,
#115330,#115331,#115332,#115333,#115334,#115335,#115336,#115337,#115338,
#115339,#115340,#115341,#115342,#115343,#115344,#115345,#115346,#115347,
#115348,#115349,#115350,#115351,#115352,#115353,#115354,#115355,#115356,
#115357,#115358,#115359,#115360,#115361,#115362,#115363,#115364,#115365,
#115366,#115367,#115368,#115369,#115370,#115371,#115372,#115373,#115374,
#115375,#115376,#115377,#115378,#115379,#115380,#115381,#115382,#115383,
#115384,#115385,#115386,#115387,#115388,#115389,#115390,#115391,#115392,
#115393,#115394,#115395,#115396,#115397,#115398,#115399,#115400,#115401,
#115402,#115403,#115404,#115405,#115406,#115407,#115408,#115409,#115410,
#115411,#115412,#115413,#115414,#115415,#115416,#115417,#115418,#115419,
#115420,#115421,#115422,#115423,#115424,#115425,#115426,#115427,#115428,
#115429,#115430,#115431,#115432,#115433,#115434,#115435,#115436,#115437,
#115438,#115439,#115440,#115441,#115442,#115443,#115444,#115445,#115446,
#115447,#115448,#115449,#115450,#115451,#115452,#115453,#115454,#115455,
#115456,#115457,#115458,#115459,#115460,#115461,#115462,#115463),
 .UNSPECIFIED.,.F.,.F.,(4,3,3,3,3,3,3,3,3,3,3,3,3,3,3,3,3,3,3,3,3,3,3,3,
3,3,3,3,3,3,3,3,3,3,3,3,3,3,3,3,3,3,3,3,3,3,3,3,3,3,3,3,3,3,3,3,3,3,3,3,
3,3,3,3,3,3,3,3,3,3,3,3,3,4),(1347.74324839001,1347.82998362966,1347.91681006014,
1348.0038194816,1348.0909222109,1348.17822185273,1348.2624678519,1348.34620656375,
1348.42984207511,1348.51339451851,1348.59688395436,1348.68033790498,1348.76377439882,
1348.84721150858,1348.9306673035,1349.01421179623,1349.09780087917,1349.18152414672,
1349.26220386262,1349.34594257447,1349.42957808583,1349.51313052923,1349.59661996508,
1349.6800739157,1349.76351040954,1349.8469475193,1349.93040331422,1350.01394780694,
1350.09753688989,1350.18126015744,1350.26193987334,1350.34567858519,1350.42931409655,
1350.51286653995,1350.5963559758,1350.67980992642,1350.76324642026,1350.84668353002,
1350.93013932494,1351.01368381766,1351.09727290061,1351.18099616816,1351.26167588406,
1351.34541459591,1351.42905010727,1351.51260255067,1351.59609198652,1351.67954593714,
1351.76298243098,1351.84641954074,1351.92987533566,1352.01341982838,1352.09700891133,
1352.18073217888,1352.26141189478,1352.34515060663,1352.42878611799,1352.51233856139,
1352.59582799724,1352.67928194786,1352.7627184417,1352.84615555146,1352.92961134638,
1353.01315583911,1353.09674492205,1353.1804681896,1353.2611479055,1353.3438127483,
1353.42638012879,1353.50886915535,1353.59129380154,1353.67368188061,1353.75605725512,
1353.77499599392),.UNSPECIFIED.);
#911=B_SPLINE_CURVE_WITH_KNOTS('',3,(#115469,#115470,#115471,#115472,#115473,
#115474,#115475,#115476,#115477,#115478,#115479,#115480,#115481,#115482,
#115483,#115484,#115485,#115486,#115487,#115488,#115489,#115490,#115491,
#115492,#115493,#115494,#115495,#115496,#115497,#115498,#115499,#115500,
#115501,#115502,#115503,#115504,#115505,#115506,#115507,#115508,#115509,
#115510,#115511,#115512,#115513,#115514,#115515,#115516,#115517,#115518,
#115519,#115520,#115521,#115522,#115523,#115524,#115525,#115526,#115527,
#115528,#115529,#115530,#115531,#115532,#115533,#115534,#115535,#115536,
#115537,#115538,#115539,#115540,#115541,#115542,#115543,#115544,#115545,
#115546,#115547,#115548,#115549,#115550,#115551,#115552,#115553,#115554,
#115555,#115556,#115557,#115558,#115559,#115560,#115561,#115562,#115563,
#115564,#115565,#115566,#115567,#115568,#115569,#115570,#115571,#115572,
#115573,#115574,#115575,#115576,#115577,#115578,#115579,#115580,#115581,
#115582,#115583,#115584,#115585,#115586,#115587,#115588,#115589,#115590,
#115591,#115592,#115593,#115594,#115595,#115596,#115597,#115598,#115599,
#115600,#115601,#115602,#115603,#115604,#115605,#115606,#115607,#115608,
#115609,#115610,#115611,#115612,#115613,#115614,#115615,#115616,#115617,
#115618,#115619,#115620,#115621,#115622,#115623,#115624,#115625,#115626,
#115627,#115628,#115629,#115630,#115631,#115632,#115633,#115634,#115635,
#115636,#115637,#115638,#115639,#115640,#115641,#115642,#115643,#115644,
#115645,#115646,#115647,#115648,#115649,#115650,#115651,#115652,#115653,
#115654,#115655,#115656,#115657,#115658,#115659,#115660,#115661,#115662,
#115663,#115664,#115665,#115666,#115667,#115668,#115669,#115670,#115671,
#115672,#115673,#115674,#115675,#115676,#115677,#115678,#115679,#115680,
#115681,#115682,#115683,#115684,#115685,#115686,#115687,#115688,#115689,
#115690,#115691),.UNSPECIFIED.,.F.,.F.,(4,3,3,3,3,3,3,3,3,3,3,3,3,3,3,3,
3,3,3,3,3,3,3,3,3,3,3,3,3,3,3,3,3,3,3,3,3,3,3,3,3,3,3,3,3,3,3,3,3,3,3,3,
3,3,3,3,3,3,3,3,3,3,3,3,3,3,3,3,3,3,3,3,3,3,4),(1354.02643369732,1354.10926246698,
1354.1919945879,1354.27465099099,1354.35911078052,1354.44168759419,1354.52425618646,
1354.60683535241,1354.69270884111,1354.77541043091,1354.85816826614,1354.94103893643,
1354.95032930723,1355.03406801908,1355.11770353044,1355.20125597384,1355.28474540969,
1355.36819936031,1355.45163585415,1355.53507296391,1355.61852875883,1355.70207325156,
1355.7856623345,1355.86938560205,1355.95006531795,1356.0338040298,1356.11743954116,
1356.20099198456,1356.28448142041,1356.36793537103,1356.45137186487,1356.53480897463,
1356.61826476954,1356.70180926227,1356.78539834522,1356.86912161277,1356.94980132867,
1357.03354004052,1357.11717555188,1357.20072799528,1357.28421743113,1357.36767138175,
1357.45110787559,1357.53454498535,1357.61800078027,1357.701545273,1357.78513435594,
1357.86885762349,1357.94953733939,1358.03327605124,1358.1169115626,1358.200464006,
1358.28395344185,1358.36740739247,1358.45084388631,1358.53428099607,1358.61773679099,
1358.70128128372,1358.78487036666,1358.86859363421,1358.94927335011,1359.03301206196,
1359.11664757332,1359.20020001672,1359.28368945257,1359.36714340319,1359.45057989703,
1359.53401700679,1359.6174728017,1359.70101729443,1359.78460637737,1359.86832964493,
1359.94900936083,1360.04511644553,1360.05912658141),.UNSPECIFIED.);
#912=B_SPLINE_CURVE_WITH_KNOTS('',3,(#115692,#115693,#115694,#115695,#115696,
#115697,#115698,#115699,#115700,#115701),.UNSPECIFIED.,.F.,.F.,(4,3,3,4),
(1353.7747814876,1353.86268739206,1353.95059329651,1354.02643369719),
 .UNSPECIFIED.);
#913=B_SPLINE_CURVE_WITH_KNOTS('',3,(#115703,#115704,#115705,#115706,#115707,
#115708,#115709,#115710,#115711,#115712),.UNSPECIFIED.,.F.,.F.,(4,3,3,4),
(1353.77499599392,1353.85739769724,1353.94191569721,1354.02643369719),
 .UNSPECIFIED.);
#914=B_SPLINE_CURVE_WITH_KNOTS('',3,(#115713,#115714,#115715,#115716,#115717,
#115718,#115719,#115720,#115721,#115722,#115723,#115724,#115725,#115726,
#115727,#115728,#115729,#115730,#115731,#115732,#115733,#115734,#115735,
#115736,#115737,#115738,#115739,#115740,#115741,#115742,#115743,#115744,
#115745,#115746,#115747,#115748,#115749,#115750,#115751,#115752,#115753,
#115754,#115755,#115756,#115757,#115758,#115759,#115760,#115761,#115762,
#115763,#115764,#115765,#115766,#115767,#115768,#115769,#115770,#115771,
#115772,#115773,#115774,#115775,#115776,#115777,#115778,#115779,#115780,
#115781,#115782,#115783,#115784,#115785,#115786,#115787,#115788,#115789,
#115790,#115791,#115792,#115793,#115794,#115795,#115796,#115797,#115798,
#115799,#115800,#115801,#115802,#115803,#115804,#115805,#115806,#115807,
#115808,#115809,#115810,#115811,#115812,#115813,#115814,#115815,#115816,
#115817,#115818,#115819,#115820,#115821,#115822,#115823,#115824,#115825,
#115826,#115827,#115828,#115829,#115830,#115831,#115832,#115833,#115834,
#115835,#115836,#115837,#115838,#115839,#115840,#115841,#115842,#115843,
#115844,#115845,#115846,#115847,#115848,#115849,#115850,#115851,#115852,
#115853,#115854,#115855,#115856,#115857,#115858,#115859,#115860,#115861,
#115862,#115863,#115864,#115865,#115866,#115867,#115868,#115869,#115870,
#115871,#115872,#115873,#115874,#115875,#115876,#115877,#115878,#115879,
#115880,#115881,#115882,#115883,#115884,#115885,#115886,#115887,#115888,
#115889,#115890,#115891,#115892,#115893,#115894,#115895,#115896,#115897,
#115898,#115899,#115900,#115901,#115902,#115903,#115904,#115905,#115906,
#115907,#115908,#115909,#115910,#115911,#115912,#115913,#115914,#115915,
#115916,#115917,#115918,#115919,#115920,#115921,#115922,#115923,#115924,
#115925,#115926,#115927,#115928,#115929,#115930,#115931,#115932),
 .UNSPECIFIED.,.F.,.F.,(4,3,3,3,3,3,3,3,3,3,3,3,3,3,3,3,3,3,3,3,3,3,3,3,
3,3,3,3,3,3,3,3,3,3,3,3,3,3,3,3,3,3,3,3,3,3,3,3,3,3,3,3,3,3,3,3,3,3,3,3,
3,3,3,3,3,3,3,3,3,3,3,3,3,4),(1354.02643369734,1354.13636339471,1354.24932972749,
1354.26088391622,1354.34462262807,1354.42825813943,1354.51181058283,1354.59530001868,
1354.6787539693,1354.76219046314,1354.8456275729,1354.92908336782,1355.01262786055,
1355.09621694349,1355.17994021105,1355.26061992694,1355.34435863879,1355.42799415015,
1355.51154659355,1355.5950360294,1355.67848998002,1355.76192647386,1355.84536358362,
1355.92881937854,1356.01236387127,1356.09595295421,1356.17967622176,1356.26035593766,
1356.34409464951,1356.42773016087,1356.51128260427,1356.59477204012,1356.67822599074,
1356.76166248458,1356.84509959434,1356.92855538926,1357.01209988199,1357.09568896493,
1357.17941223248,1357.26009194838,1357.34383066023,1357.42746617159,1357.51101861499,
1357.59450805084,1357.67796200146,1357.7613984953,1357.84483560506,1357.92829139998,
1358.01183589271,1358.09542497565,1358.1791482432,1358.2598279591,1358.34356667095,
1358.42720218231,1358.51075462571,1358.59424406156,1358.67769801218,1358.76113450602,
1358.84457161578,1358.9280274107,1359.01157190343,1359.09516098637,1359.17888425392,
1359.25956396982,1359.34331486158,1359.42695989653,1359.51050366133,1359.59398999953,
1359.67743703141,1359.76086284685,1359.84430936519,1359.92776650707,1360.01128630232,
1360.05795370664),.UNSPECIFIED.);
#915=B_SPLINE_CURVE_WITH_KNOTS('',3,(#115938,#115939,#115940,#115941,#115942,
#115943,#115944,#115945,#115946,#115947,#115948,#115949,#115950,#115951,
#115952,#115953,#115954,#115955,#115956,#115957,#115958,#115959,#115960,
#115961,#115962,#115963,#115964,#115965,#115966,#115967,#115968,#115969,
#115970,#115971,#115972,#115973,#115974,#115975,#115976,#115977,#115978,
#115979,#115980,#115981,#115982,#115983,#115984,#115985,#115986,#115987,
#115988,#115989,#115990,#115991,#115992,#115993,#115994,#115995,#115996,
#115997,#115998,#115999,#116000,#116001,#116002,#116003,#116004,#116005,
#116006,#116007,#116008,#116009,#116010,#116011,#116012,#116013,#116014,
#116015,#116016,#116017,#116018,#116019,#116020,#116021,#116022,#116023,
#116024,#116025,#116026,#116027,#116028,#116029,#116030,#116031,#116032,
#116033,#116034,#116035,#116036,#116037,#116038,#116039,#116040,#116041,
#116042,#116043,#116044,#116045,#116046,#116047,#116048,#116049,#116050,
#116051,#116052,#116053,#116054,#116055,#116056,#116057,#116058,#116059,
#116060,#116061,#116062,#116063,#116064,#116065,#116066,#116067,#116068,
#116069,#116070,#116071,#116072,#116073,#116074,#116075,#116076,#116077,
#116078,#116079,#116080,#116081,#116082,#116083,#116084,#116085,#116086,
#116087,#116088,#116089,#116090,#116091,#116092,#116093,#116094,#116095,
#116096,#116097,#116098,#116099,#116100,#116101,#116102,#116103,#116104,
#116105,#116106,#116107,#116108,#116109,#116110,#116111,#116112,#116113,
#116114,#116115,#116116,#116117,#116118,#116119,#116120,#116121,#116122,
#116123,#116124,#116125,#116126,#116127,#116128,#116129,#116130,#116131,
#116132,#116133,#116134,#116135,#116136,#116137,#116138,#116139,#116140,
#116141,#116142,#116143,#116144,#116145,#116146,#116147,#116148,#116149,
#116150,#116151,#116152,#116153,#116154,#116155,#116156,#116157),
 .UNSPECIFIED.,.F.,.F.,(4,3,3,3,3,3,3,3,3,3,3,3,3,3,3,3,3,3,3,3,3,3,3,3,
3,3,3,3,3,3,3,3,3,3,3,3,3,3,3,3,3,3,3,3,3,3,3,3,3,3,3,3,3,3,3,3,3,3,3,3,
3,3,3,3,3,3,3,3,3,3,3,3,3,4),(1360.30961900437,1360.39342826463,1360.47723720546,
1360.56106336456,1360.64492428695,1360.72889024008,1360.81291395196,1360.89707373967,
1360.94874537155,1361.0324840834,1361.11611959476,1361.19967203816,1361.28316147401,
1361.36661542463,1361.45005191847,1361.53348902823,1361.61694482314,1361.70048931587,
1361.78407839881,1361.86780166637,1361.94848138227,1362.03222009412,1362.11585560548,
1362.19940804888,1362.28289748473,1362.36635143535,1362.44978792919,1362.53322503895,
1362.61668083387,1362.7002253266,1362.78381440954,1362.86753767709,1362.94821739299,
1363.03195610484,1363.1155916162,1363.1991440596,1363.28263349545,1363.36608744607,
1363.44952393991,1363.53296104967,1363.61641684459,1363.69996133732,1363.78355042026,
1363.86727368782,1363.94795340371,1364.03169211556,1364.11532762692,1364.19888007032,
1364.28236950617,1364.36582345679,1364.44925995063,1364.53269706039,1364.61615285531,
1364.69969734804,1364.78328643098,1364.86700969853,1364.94768941443,1365.03142812628,
1365.11506363764,1365.19861608104,1365.28210551689,1365.36555946751,1365.44899596135,
1365.53243307111,1365.61588886603,1365.69943335876,1365.7830224417,1365.86674570925,
1365.94742542515,1366.031491194,1366.11541841964,1366.19926592761,1366.28303873201,
1366.3419758236),.UNSPECIFIED.);
#916=B_SPLINE_CURVE_WITH_KNOTS('',3,(#116158,#116159,#116160,#116161,#116162,
#116163,#116164,#116165,#116166,#116167),.UNSPECIFIED.,.F.,.F.,(4,3,3,4),
(1360.05912658141,1360.15468423343,1360.2495959197,1360.30961900417),
 .UNSPECIFIED.);
#917=B_SPLINE_CURVE_WITH_KNOTS('',3,(#116169,#116170,#116171,#116172,#116173,
#116174,#116175,#116176,#116177,#116178,#116179,#116180,#116181),
 .UNSPECIFIED.,.F.,.F.,(4,3,3,3,4),(1360.05795370664,1360.14157474727,1360.22531677827,
1360.25929998054,1360.30961900437),.UNSPECIFIED.);
#918=B_SPLINE_CURVE_WITH_KNOTS('',3,(#116182,#116183,#116184,#116185,#116186,
#116187,#116188,#116189,#116190,#116191,#116192,#116193,#116194,#116195,
#116196,#116197,#116198,#116199,#116200,#116201,#116202,#116203,#116204,
#116205,#116206,#116207,#116208,#116209,#116210,#116211,#116212,#116213,
#116214,#116215,#116216,#116217,#116218,#116219,#116220,#116221,#116222,
#116223,#116224,#116225,#116226,#116227,#116228,#116229,#116230,#116231,
#116232,#116233,#116234,#116235,#116236,#116237,#116238,#116239,#116240,
#116241,#116242,#116243,#116244,#116245,#116246,#116247,#116248,#116249,
#116250,#116251,#116252,#116253,#116254,#116255,#116256,#116257,#116258,
#116259,#116260,#116261,#116262,#116263,#116264,#116265,#116266,#116267,
#116268,#116269,#116270,#116271,#116272,#116273,#116274,#116275,#116276,
#116277,#116278,#116279,#116280,#116281,#116282,#116283,#116284,#116285,
#116286,#116287,#116288,#116289,#116290,#116291,#116292,#116293,#116294,
#116295,#116296,#116297,#116298,#116299,#116300,#116301,#116302,#116303,
#116304,#116305,#116306,#116307,#116308,#116309,#116310,#116311,#116312,
#116313,#116314,#116315,#116316,#116317,#116318,#116319,#116320,#116321,
#116322,#116323,#116324,#116325,#116326,#116327,#116328,#116329,#116330,
#116331,#116332,#116333,#116334,#116335,#116336,#116337,#116338,#116339,
#116340,#116341,#116342,#116343,#116344,#116345,#116346,#116347,#116348,
#116349,#116350,#116351,#116352,#116353,#116354,#116355,#116356,#116357,
#116358,#116359,#116360,#116361,#116362,#116363,#116364,#116365,#116366,
#116367,#116368,#116369,#116370,#116371,#116372,#116373,#116374,#116375,
#116376,#116377,#116378,#116379,#116380,#116381,#116382,#116383,#116384,
#116385,#116386,#116387,#116388,#116389,#116390,#116391,#116392,#116393,
#116394,#116395,#116396,#116397,#116398,#116399,#116400,#116401),
 .UNSPECIFIED.,.F.,.F.,(4,3,3,3,3,3,3,3,3,3,3,3,3,3,3,3,3,3,3,3,3,3,3,3,
3,3,3,3,3,3,3,3,3,3,3,3,3,3,3,3,3,3,3,3,3,3,3,3,3,3,3,3,3,3,3,3,3,3,3,3,
3,3,3,3,3,3,3,3,3,3,3,3,3,4),(1360.30961900457,1360.39269947054,1360.47567993026,
1360.55858113247,1360.64142374873,1360.72423716446,1360.80703824373,1360.88984561224,
1360.97267789694,1361.05560003594,1361.13857341923,1361.22166751875,1361.25903599126,
1361.3427747031,1361.42641021447,1361.50996265787,1361.59345209372,1361.67690604433,
1361.76034253818,1361.84377964793,1361.92723544285,1362.01077993558,1362.09436901852,
1362.17809228608,1362.25877200198,1362.34251071383,1362.4261462252,1362.5096986686,
1362.59318810445,1362.67664205507,1362.76007854892,1362.84351565867,1362.92697145359,
1363.01051594633,1363.09410502927,1363.17782829683,1363.25850801271,1363.34224672456,
1363.42588223592,1363.50943467932,1363.59292411518,1363.67637806579,1363.75981455964,
1363.84325166939,1363.92670746431,1364.01025195704,1364.09384103998,1364.17756430754,
1364.25824402343,1364.34198273527,1364.42561824664,1364.50917069004,1364.59266012589,
1364.6761140765,1364.75955057035,1364.8429876801,1364.92644347502,1365.00998796774,
1365.09357705068,1365.17730031824,1365.25798003415,1365.341718746,1365.42535425737,
1365.50890670077,1365.59239613662,1365.67585008724,1365.75928658108,1365.84272369084,
1365.92617948576,1366.00972397849,1366.09331306143,1366.17703632899,1366.25771604487,
1366.34220623514),.UNSPECIFIED.);
#919=B_SPLINE_CURVE_WITH_KNOTS('',3,(#116407,#116408,#116409,#116410,#116411,
#116412,#116413,#116414,#116415,#116416,#116417,#116418,#116419,#116420,
#116421,#116422,#116423,#116424,#116425,#116426,#116427,#116428,#116429,
#116430,#116431,#116432,#116433,#116434,#116435,#116436,#116437,#116438,
#116439,#116440,#116441,#116442,#116443,#116444,#116445,#116446,#116447,
#116448,#116449,#116450,#116451,#116452,#116453,#116454,#116455,#116456,
#116457,#116458,#116459,#116460,#116461,#116462,#116463,#116464,#116465,
#116466,#116467,#116468,#116469,#116470,#116471,#116472,#116473,#116474,
#116475,#116476,#116477,#116478,#116479,#116480,#116481,#116482,#116483,
#116484,#116485,#116486,#116487,#116488,#116489,#116490,#116491,#116492,
#116493,#116494,#116495,#116496,#116497,#116498,#116499,#116500,#116501,
#116502,#116503,#116504,#116505,#116506,#116507,#116508,#116509,#116510,
#116511,#116512,#116513,#116514,#116515,#116516,#116517,#116518,#116519,
#116520,#116521,#116522,#116523,#116524,#116525,#116526,#116527,#116528,
#116529,#116530,#116531,#116532,#116533,#116534,#116535,#116536,#116537,
#116538,#116539,#116540,#116541,#116542,#116543,#116544,#116545,#116546,
#116547,#116548,#116549,#116550,#116551,#116552,#116553,#116554,#116555,
#116556,#116557,#116558,#116559,#116560,#116561,#116562,#116563,#116564,
#116565,#116566,#116567,#116568,#116569,#116570,#116571,#116572,#116573,
#116574,#116575,#116576,#116577,#116578,#116579,#116580,#116581,#116582,
#116583,#116584,#116585,#116586,#116587,#116588,#116589,#116590,#116591,
#116592,#116593,#116594,#116595,#116596,#116597,#116598,#116599,#116600,
#116601,#116602,#116603,#116604,#116605,#116606,#116607,#116608,#116609,
#116610,#116611,#116612,#116613,#116614,#116615,#116616,#116617,#116618,
#116619,#116620,#116621,#116622,#116623,#116624,#116625,#116626),
 .UNSPECIFIED.,.F.,.F.,(4,3,3,3,3,3,3,3,3,3,3,3,3,3,3,3,3,3,3,3,3,3,3,3,
3,3,3,3,3,3,3,3,3,3,3,3,3,3,3,3,3,3,3,3,3,3,3,3,3,3,3,3,3,3,3,3,3,3,3,3,
3,3,3,3,3,3,3,3,3,3,3,3,3,4),(1366.59280431175,1366.68827870871,1366.78420671922,
1366.8807234362,1366.94716143587,1367.03090014772,1367.11453565908,1367.19808810248,
1367.28157753833,1367.36503148894,1367.44846798279,1367.53190509255,1367.61536088746,
1367.69890538019,1367.78249446313,1367.86621773069,1367.94689744659,1368.03063615844,
1368.1142716698,1368.1978241132,1368.28131354905,1368.36476749967,1368.44820399351,
1368.53164110327,1368.61509689819,1368.69864139092,1368.78223047386,1368.86595374141,
1368.94663345731,1369.03037216916,1369.11400768052,1369.19756012392,1369.28104955977,
1369.36450351039,1369.44794000423,1369.53137711399,1369.61483290891,1369.69837740164,
1369.78196648458,1369.86568975213,1369.94636946803,1370.03010817988,1370.11374369124,
1370.19729613464,1370.28078557049,1370.36423952111,1370.44767601495,1370.53111312471,
1370.61456891963,1370.69811341236,1370.7817024953,1370.86542576285,1370.94610547875,
1371.0298441906,1371.11347970196,1371.19703214536,1371.28052158121,1371.36397553183,
1371.44741202567,1371.53084913543,1371.61430493035,1371.69784942308,1371.78143850602,
1371.86516177357,1371.94584148947,1372.03063118758,1372.11342593743,1372.19614550064,
1372.27880873553,1372.36514632023,1372.4477658086,1372.53038412638,1372.61303684556,
1372.62415907432),.UNSPECIFIED.);
#920=B_SPLINE_CURVE_WITH_KNOTS('',3,(#116627,#116628,#116629,#116630,#116631,
#116632,#116633,#116634,#116635,#116636),.UNSPECIFIED.,.F.,.F.,(4,3,3,4),
(1366.3419758236,1366.42568087771,1366.50938802422,1366.59280431155),
 .UNSPECIFIED.);
#921=B_SPLINE_CURVE_WITH_KNOTS('',3,(#116638,#116639,#116640,#116641,#116642,
#116643,#116644,#116645,#116646,#116647),.UNSPECIFIED.,.F.,.F.,(4,3,3,4),
(1366.34220623514,1366.44006982097,1366.53709108296,1366.59280431136),
 .UNSPECIFIED.);
#922=B_SPLINE_CURVE_WITH_KNOTS('',3,(#116648,#116649,#116650,#116651,#116652,
#116653,#116654,#116655,#116656,#116657,#116658,#116659,#116660,#116661,
#116662,#116663,#116664,#116665,#116666,#116667,#116668,#116669,#116670,
#116671,#116672,#116673,#116674,#116675,#116676,#116677,#116678,#116679,
#116680,#116681,#116682,#116683,#116684,#116685,#116686,#116687,#116688,
#116689,#116690,#116691,#116692,#116693,#116694,#116695,#116696,#116697,
#116698,#116699,#116700,#116701,#116702,#116703,#116704,#116705,#116706,
#116707,#116708,#116709,#116710,#116711,#116712,#116713,#116714,#116715,
#116716,#116717,#116718,#116719,#116720,#116721,#116722,#116723,#116724,
#116725,#116726,#116727,#116728,#116729,#116730,#116731,#116732,#116733,
#116734,#116735,#116736,#116737,#116738,#116739,#116740,#116741,#116742,
#116743,#116744,#116745,#116746,#116747,#116748,#116749,#116750,#116751,
#116752,#116753,#116754,#116755,#116756,#116757,#116758,#116759,#116760,
#116761,#116762,#116763,#116764,#116765,#116766,#116767,#116768,#116769,
#116770,#116771,#116772,#116773,#116774,#116775,#116776,#116777,#116778,
#116779,#116780,#116781,#116782,#116783,#116784,#116785,#116786,#116787,
#116788,#116789,#116790,#116791,#116792,#116793,#116794,#116795,#116796,
#116797,#116798,#116799,#116800,#116801,#116802,#116803,#116804,#116805,
#116806,#116807,#116808,#116809,#116810,#116811,#116812,#116813,#116814,
#116815,#116816,#116817,#116818,#116819,#116820,#116821,#116822,#116823,
#116824,#116825,#116826,#116827,#116828,#116829,#116830,#116831,#116832,
#116833,#116834,#116835,#116836,#116837,#116838,#116839,#116840,#116841,
#116842,#116843,#116844,#116845,#116846,#116847,#116848,#116849,#116850,
#116851,#116852,#116853,#116854,#116855,#116856,#116857,#116858,#116859,
#116860,#116861,#116862,#116863,#116864,#116865,#116866,#116867),
 .UNSPECIFIED.,.F.,.F.,(4,3,3,3,3,3,3,3,3,3,3,3,3,3,3,3,3,3,3,3,3,3,3,3,
3,3,3,3,3,3,3,3,3,3,3,3,3,3,3,3,3,3,3,3,3,3,3,3,3,3,3,3,3,3,3,3,3,3,3,3,
3,3,3,3,3,3,3,3,3,3,3,3,3,4),(1366.59280431155,1366.67621624537,1366.75961557606,
1366.84302033608,1366.92644855767,1367.00997275018,1367.09354558179,1367.17725891191,
1367.25745205559,1367.34119076743,1367.4248262788,1367.5083787222,1367.59186815805,
1367.67532210866,1367.7587586025,1367.84219571226,1367.92565150718,1368.0091959999,
1368.09278508284,1368.1765083504,1368.25718806631,1368.34092677816,1368.42456228952,
1368.50811473292,1368.59160416877,1368.67505811938,1368.75849461323,1368.84193172298,
1368.9253875179,1369.00893201063,1369.09252109357,1369.17624436113,1369.25692407703,
1369.34066278888,1369.42429830024,1369.50785074364,1369.5913401795,1369.67479413011,
1369.75823062396,1369.84166773371,1369.92512352863,1370.00866802136,1370.0922571043,
1370.17598037186,1370.25666008775,1370.3403987996,1370.42403431096,1370.50758675436,
1370.59107619021,1370.67453014083,1370.75796663467,1370.84140374443,1370.92485953934,
1371.00840403207,1371.09199311501,1371.17571638257,1371.25639609847,1371.34013481032,
1371.42377032168,1371.50732276508,1371.59081220094,1371.67426615155,1371.7577026454,
1371.84113975515,1371.92459555007,1372.0081400428,1372.09172912574,1372.1754523933,
1372.25613210919,1372.34069413994,1372.42511155572,1372.5094452698,1372.59369612929,
1372.62528274347),.UNSPECIFIED.);
#923=B_SPLINE_CURVE_WITH_KNOTS('',3,(#116873,#116874,#116875,#116876,#116877,
#116878,#116879,#116880,#116881,#116882,#116883,#116884,#116885,#116886,
#116887,#116888,#116889,#116890,#116891,#116892,#116893,#116894,#116895,
#116896,#116897,#116898,#116899,#116900,#116901,#116902,#116903,#116904,
#116905,#116906,#116907,#116908,#116909,#116910,#116911,#116912,#116913,
#116914,#116915,#116916,#116917,#116918,#116919,#116920,#116921,#116922,
#116923,#116924,#116925,#116926,#116927,#116928,#116929,#116930,#116931,
#116932,#116933,#116934,#116935,#116936,#116937,#116938,#116939,#116940,
#116941,#116942,#116943,#116944,#116945,#116946,#116947,#116948,#116949,
#116950,#116951,#116952,#116953,#116954,#116955,#116956,#116957,#116958,
#116959,#116960,#116961,#116962,#116963,#116964,#116965,#116966,#116967,
#116968,#116969,#116970,#116971,#116972,#116973,#116974,#116975,#116976,
#116977,#116978,#116979,#116980,#116981,#116982,#116983,#116984,#116985,
#116986,#116987,#116988,#116989,#116990,#116991,#116992,#116993,#116994,
#116995,#116996,#116997,#116998,#116999,#117000,#117001,#117002,#117003,
#117004,#117005,#117006,#117007,#117008,#117009,#117010,#117011,#117012,
#117013,#117014,#117015,#117016,#117017,#117018,#117019,#117020,#117021,
#117022,#117023,#117024,#117025,#117026,#117027,#117028,#117029,#117030,
#117031,#117032,#117033,#117034,#117035,#117036,#117037,#117038,#117039,
#117040,#117041,#117042,#117043,#117044,#117045,#117046,#117047,#117048,
#117049,#117050,#117051,#117052,#117053,#117054,#117055,#117056,#117057,
#117058,#117059,#117060,#117061,#117062,#117063,#117064,#117065,#117066,
#117067,#117068,#117069,#117070,#117071,#117072,#117073,#117074,#117075,
#117076,#117077,#117078,#117079,#117080,#117081,#117082,#117083,#117084,
#117085,#117086,#117087,#117088,#117089,#117090,#117091,#117092),
 .UNSPECIFIED.,.F.,.F.,(4,3,3,3,3,3,3,3,3,3,3,3,3,3,3,3,3,3,3,3,3,3,3,3,
3,3,3,3,3,3,3,3,3,3,3,3,3,3,3,3,3,3,3,3,3,3,3,3,3,3,3,3,3,3,3,3,3,3,3,3,
3,3,3,3,3,3,3,3,3,3,3,3,3,4),(1372.87598961873,1372.94557750019,1373.02931621204,
1373.1129517234,1373.1965041668,1373.27999360265,1373.36344755327,1373.44688404711,
1373.53032115687,1373.61377695179,1373.69732144452,1373.78091052746,1373.86463379502,
1373.94531351091,1374.02905222276,1374.11268773412,1374.19624017752,1374.27972961337,
1374.36318356399,1374.44662005783,1374.53005716759,1374.6135129625,1374.69705745523,
1374.78064653818,1374.86436980573,1374.94504952163,1375.02878823348,1375.11242374484,
1375.19597618824,1375.27946562409,1375.36291957471,1375.44635606855,1375.52979317831,
1375.61324897323,1375.69679346596,1375.7803825489,1375.86410581645,1375.94478553235,
1376.0285242442,1376.11215975556,1376.19571219896,1376.27920163481,1376.36265558543,
1376.44609207927,1376.52952918903,1376.61298498395,1376.69652947668,1376.78011855962,
1376.86384182718,1376.94452154307,1377.02826025492,1377.11189576628,1377.19544820968,
1377.27893764553,1377.36239159615,1377.44582808999,1377.52926519975,1377.61272099467,
1377.6962654874,1377.77985457034,1377.86357783789,1377.94425755379,1378.02799831545,
1378.11163540067,1378.19518894399,1378.27867900734,1378.36213118323,1378.44556522948,
1378.52899921834,1378.61245121803,1378.69598273117,1378.77955855647,1378.86324724977,
1378.9079079641),.UNSPECIFIED.);
#924=B_SPLINE_CURVE_WITH_KNOTS('',3,(#117093,#117094,#117095,#117096,#117097,
#117098,#117099,#117100,#117101,#117102),.UNSPECIFIED.,.F.,.F.,(4,3,3,4),
(1372.62415907432,1372.70689884796,1372.79144423329,1372.87598961861),
 .UNSPECIFIED.);
#925=B_SPLINE_CURVE_WITH_KNOTS('',3,(#117104,#117105,#117106,#117107,#117108,
#117109,#117110,#117111,#117112,#117113),.UNSPECIFIED.,.F.,.F.,(4,3,3,4),
(1372.62528274347,1372.70946141838,1372.79362230245,1372.87598961873),
 .UNSPECIFIED.);
#926=B_SPLINE_CURVE_WITH_KNOTS('',3,(#117114,#117115,#117116,#117117,#117118,
#117119,#117120,#117121,#117122,#117123,#117124,#117125,#117126,#117127,
#117128,#117129,#117130,#117131,#117132,#117133,#117134,#117135,#117136,
#117137,#117138,#117139,#117140,#117141,#117142,#117143,#117144,#117145,
#117146,#117147,#117148,#117149,#117150,#117151,#117152,#117153,#117154,
#117155,#117156,#117157,#117158,#117159,#117160,#117161,#117162,#117163,
#117164,#117165,#117166,#117167,#117168,#117169,#117170,#117171,#117172,
#117173,#117174,#117175,#117176,#117177,#117178,#117179,#117180,#117181,
#117182,#117183,#117184,#117185,#117186,#117187,#117188,#117189,#117190,
#117191,#117192,#117193,#117194,#117195,#117196,#117197,#117198,#117199,
#117200,#117201,#117202,#117203,#117204,#117205,#117206,#117207,#117208,
#117209,#117210,#117211,#117212,#117213,#117214,#117215,#117216,#117217,
#117218,#117219,#117220,#117221,#117222,#117223,#117224,#117225,#117226,
#117227,#117228,#117229,#117230,#117231,#117232,#117233,#117234,#117235,
#117236,#117237,#117238,#117239,#117240,#117241,#117242,#117243,#117244,
#117245,#117246,#117247,#117248,#117249,#117250,#117251,#117252,#117253,
#117254,#117255,#117256,#117257,#117258,#117259,#117260,#117261,#117262,
#117263,#117264,#117265,#117266,#117267,#117268,#117269,#117270,#117271,
#117272,#117273,#117274,#117275,#117276,#117277,#117278,#117279,#117280,
#117281,#117282,#117283,#117284,#117285,#117286,#117287,#117288,#117289,
#117290,#117291,#117292,#117293,#117294,#117295,#117296,#117297,#117298,
#117299,#117300,#117301,#117302,#117303,#117304,#117305,#117306,#117307,
#117308,#117309,#117310,#117311,#117312,#117313,#117314,#117315,#117316,
#117317,#117318,#117319,#117320,#117321,#117322,#117323,#117324,#117325,
#117326,#117327,#117328,#117329,#117330),.UNSPECIFIED.,.F.,.F.,(4,3,3,3,
3,3,3,3,3,3,3,3,3,3,3,3,3,3,3,3,3,3,3,3,3,3,3,3,3,3,3,3,3,3,3,3,3,3,3,3,
3,3,3,3,3,3,3,3,3,3,3,3,3,3,3,3,3,3,3,3,3,3,3,3,3,3,3,3,3,3,3,3,4),(1372.87598961893,
1372.97095924417,1373.06491065064,1373.16038938527,1373.25586811991,1373.33960683175,
1373.42324234312,1373.50679478651,1373.59028422236,1373.67373817297,1373.75717466681,
1373.84061177656,1373.92406757148,1374.0076120642,1374.09120114714,1374.17492441469,
1374.25560413063,1374.33934284248,1374.42297835384,1374.50653079724,1374.59002023309,
1374.67347418371,1374.75691067755,1374.84034778731,1374.92380358223,1375.00734807496,
1375.0909371579,1375.17466042545,1375.25534014135,1375.3390788532,1375.42271436456,
1375.50626680796,1375.58975624382,1375.67321019443,1375.75664668828,1375.84008379803,
1375.92353959295,1376.00708408568,1376.09067316862,1376.17439643618,1376.25507615207,
1376.33881486392,1376.42245037528,1376.50600281868,1376.58949225453,1376.67294620514,
1376.75638269899,1376.83981980874,1376.92327560366,1377.00682009639,1377.09040917933,
1377.17413244689,1377.25481216279,1377.33855087464,1377.422186386,1377.5057388294,
1377.58922826526,1377.67268221587,1377.75611870972,1377.83955581947,1377.92301161439,
1378.00655610712,1378.09014519006,1378.17386845762,1378.25454817351,1378.33724869518,
1378.41985465973,1378.50238512748,1378.58485909102,1378.66730602705,1378.74973447906,
1378.83219342914,1378.9073388259),.UNSPECIFIED.);
#927=B_SPLINE_CURVE_WITH_KNOTS('',3,(#117336,#117337,#117338,#117339,#117340,
#117341,#117342,#117343,#117344,#117345,#117346,#117347,#117348,#117349,
#117350,#117351,#117352,#117353,#117354,#117355,#117356,#117357,#117358,
#117359,#117360,#117361,#117362,#117363,#117364,#117365,#117366,#117367,
#117368,#117369,#117370,#117371,#117372,#117373,#117374,#117375,#117376,
#117377,#117378,#117379,#117380,#117381,#117382,#117383,#117384,#117385,
#117386,#117387,#117388,#117389,#117390,#117391,#117392,#117393,#117394,
#117395,#117396,#117397,#117398,#117399,#117400,#117401,#117402,#117403,
#117404,#117405,#117406,#117407,#117408,#117409,#117410,#117411,#117412,
#117413,#117414,#117415,#117416,#117417,#117418,#117419,#117420,#117421,
#117422,#117423,#117424,#117425,#117426,#117427,#117428,#117429,#117430,
#117431,#117432,#117433,#117434,#117435,#117436,#117437,#117438,#117439,
#117440,#117441,#117442,#117443,#117444,#117445,#117446,#117447,#117448,
#117449,#117450,#117451,#117452,#117453,#117454,#117455,#117456,#117457,
#117458,#117459,#117460,#117461,#117462,#117463,#117464,#117465,#117466,
#117467,#117468,#117469,#117470,#117471,#117472,#117473,#117474,#117475,
#117476,#117477,#117478,#117479,#117480,#117481,#117482,#117483,#117484,
#117485,#117486,#117487,#117488,#117489,#117490,#117491,#117492,#117493,
#117494,#117495,#117496,#117497,#117498,#117499,#117500,#117501,#117502,
#117503,#117504,#117505,#117506,#117507,#117508,#117509,#117510,#117511,
#117512,#117513,#117514,#117515,#117516,#117517,#117518,#117519,#117520,
#117521,#117522,#117523,#117524,#117525,#117526,#117527,#117528,#117529,
#117530,#117531,#117532,#117533,#117534,#117535,#117536,#117537,#117538,
#117539,#117540,#117541,#117542,#117543,#117544,#117545,#117546,#117547,
#117548,#117549,#117550,#117551,#117552,#117553,#117554,#117555),
 .UNSPECIFIED.,.F.,.F.,(4,3,3,3,3,3,3,3,3,3,3,3,3,3,3,3,3,3,3,3,3,3,3,3,
3,3,3,3,3,3,3,3,3,3,3,3,3,3,3,3,3,3,3,3,3,3,3,3,3,3,3,3,3,3,3,3,3,3,3,3,
3,3,3,3,3,3,3,3,3,3,3,3,3,4),(1379.15917492602,1379.24158537443,1379.32393137804,
1379.40624085828,1379.48853340139,1379.57082798668,1379.65314359278,1379.73554563815,
1379.81799609624,1379.90056739866,1379.94372957523,1380.02746828708,1380.11110379844,
1380.19465624184,1380.27814567769,1380.36159962831,1380.44503612215,1380.52847323191,
1380.61192902683,1380.69547351956,1380.7790626025,1380.86278587005,1380.94346558595,
1381.0272042978,1381.11083980916,1381.19439225256,1381.27788168841,1381.36133563903,
1381.44477213287,1381.52820924263,1381.61166503755,1381.69520953028,1381.77879861322,
1381.86252188077,1381.94320159667,1382.02694030852,1382.11057581988,1382.19412826328,
1382.27761769913,1382.36107164975,1382.44450814359,1382.52794525335,1382.61140104827,
1382.694945541,1382.77853462394,1382.86225789149,1382.94293760739,1383.02667631924,
1383.1103118306,1383.193864274,1383.27735370985,1383.36080766047,1383.44424415431,
1383.52768126407,1383.61113705899,1383.69468155172,1383.77827063466,1383.86199390221,
1383.94267361811,1384.02641232996,1384.11004784132,1384.19360028472,1384.27708972057,
1384.36054367119,1384.44398016503,1384.52741727479,1384.61087306971,1384.69441756244,
1384.77800664538,1384.86172991294,1384.94240962883,1385.03046226107,1385.11831898915,
1385.19203220808),.UNSPECIFIED.);
#928=B_SPLINE_CURVE_WITH_KNOTS('',3,(#117556,#117557,#117558,#117559,#117560,
#117561,#117562,#117563,#117564,#117565),.UNSPECIFIED.,.F.,.F.,(4,3,3,4),
(1378.9079079641,1378.94399356451,1379.05996311743,1379.15917492591),
 .UNSPECIFIED.);
#929=B_SPLINE_CURVE_WITH_KNOTS('',3,(#117567,#117568,#117569,#117570,#117571,
#117572,#117573,#117574,#117575,#117576),.UNSPECIFIED.,.F.,.F.,(4,3,3,4),
(1378.9073388259,1378.9898740265,1379.07452447614,1379.15917492578),
 .UNSPECIFIED.);
#930=B_SPLINE_CURVE_WITH_KNOTS('',3,(#117577,#117578,#117579,#117580,#117581,
#117582,#117583,#117584,#117585,#117586,#117587,#117588,#117589,#117590,
#117591,#117592,#117593,#117594,#117595,#117596,#117597,#117598,#117599,
#117600,#117601,#117602,#117603,#117604,#117605,#117606,#117607,#117608,
#117609,#117610,#117611,#117612,#117613,#117614,#117615,#117616,#117617,
#117618,#117619,#117620,#117621,#117622,#117623,#117624,#117625,#117626,
#117627,#117628,#117629,#117630,#117631,#117632,#117633,#117634,#117635,
#117636,#117637,#117638,#117639,#117640,#117641,#117642,#117643,#117644,
#117645,#117646,#117647,#117648,#117649,#117650,#117651,#117652,#117653,
#117654,#117655,#117656,#117657,#117658,#117659,#117660,#117661,#117662,
#117663,#117664,#117665,#117666,#117667,#117668,#117669,#117670,#117671,
#117672,#117673,#117674,#117675,#117676,#117677,#117678,#117679,#117680,
#117681,#117682,#117683,#117684,#117685,#117686,#117687,#117688,#117689,
#117690,#117691,#117692,#117693,#117694,#117695,#117696,#117697,#117698,
#117699,#117700,#117701,#117702,#117703,#117704,#117705,#117706,#117707,
#117708,#117709,#117710,#117711,#117712,#117713,#117714,#117715,#117716,
#117717,#117718,#117719,#117720,#117721,#117722,#117723,#117724,#117725,
#117726,#117727,#117728,#117729,#117730,#117731,#117732,#117733,#117734,
#117735,#117736,#117737,#117738,#117739,#117740,#117741,#117742,#117743,
#117744,#117745,#117746,#117747,#117748,#117749,#117750,#117751,#117752,
#117753,#117754,#117755,#117756,#117757,#117758,#117759,#117760,#117761,
#117762,#117763,#117764,#117765,#117766,#117767,#117768,#117769,#117770,
#117771,#117772,#117773,#117774,#117775,#117776,#117777,#117778,#117779,
#117780,#117781,#117782,#117783,#117784,#117785,#117786,#117787,#117788,
#117789,#117790,#117791,#117792,#117793,#117794,#117795,#117796),
 .UNSPECIFIED.,.F.,.F.,(4,3,3,3,3,3,3,3,3,3,3,3,3,3,3,3,3,3,3,3,3,3,3,3,
3,3,3,3,3,3,3,3,3,3,3,3,3,3,3,3,3,3,3,3,3,3,3,3,3,3,3,3,3,3,3,3,3,3,3,3,
3,3,3,3,3,3,3,3,3,3,3,3,3,4),(1379.15917492591,1379.25428418423,1379.33802289608,
1379.42165840744,1379.50521085084,1379.58870028669,1379.67215423731,1379.75559073115,
1379.83902784091,1379.92248363583,1380.00602812856,1380.0896172115,1380.17334047906,
1380.25402019495,1380.3377589068,1380.42139441816,1380.50494686156,1380.58843629741,
1380.67189024803,1380.75532674187,1380.83876385163,1380.92221964654,1381.00576413927,
1381.08935322221,1381.17307648977,1381.25375620567,1381.33749491752,1381.42113042888,
1381.50468287228,1381.58817230813,1381.67162625875,1381.75506275259,1381.83849986235,
1381.92195565727,1382.00550015,1382.08908923294,1382.17281250049,1382.25349221639,
1382.33723092824,1382.4208664396,1382.504418883,1382.58790831885,1382.67136226947,
1382.75479876331,1382.83823587307,1382.92169166799,1383.00523616072,1383.08882524366,
1383.17254851121,1383.25322822711,1383.33696693896,1383.42060245032,1383.50415489372,
1383.58764432957,1383.67109828019,1383.75453477403,1383.83797188379,1383.92142767871,
1384.00497217144,1384.08856125438,1384.17228452194,1384.25296423783,1384.33670649109,
1384.42034472974,1384.50389908976,1384.5897839228,1384.67323419369,1384.75666637546,
1384.84009853983,1384.92781834339,1385.01134412471,1385.0949153171,1385.17858451418,
1385.19097775405),.UNSPECIFIED.);
#931=B_SPLINE_CURVE_WITH_KNOTS('',3,(#117802,#117803,#117804,#117805,#117806,
#117807,#117808,#117809,#117810,#117811,#117812,#117813,#117814,#117815,
#117816,#117817,#117818,#117819,#117820,#117821,#117822,#117823,#117824,
#117825,#117826,#117827,#117828,#117829,#117830,#117831,#117832,#117833,
#117834,#117835,#117836,#117837,#117838,#117839,#117840,#117841,#117842,
#117843,#117844,#117845,#117846,#117847,#117848,#117849,#117850,#117851,
#117852,#117853,#117854,#117855,#117856,#117857,#117858,#117859,#117860,
#117861,#117862,#117863,#117864,#117865,#117866,#117867,#117868,#117869,
#117870,#117871,#117872,#117873,#117874,#117875,#117876,#117877,#117878,
#117879,#117880,#117881,#117882,#117883,#117884,#117885,#117886,#117887,
#117888,#117889,#117890,#117891,#117892,#117893,#117894,#117895,#117896,
#117897,#117898,#117899,#117900,#117901,#117902,#117903,#117904,#117905,
#117906,#117907,#117908,#117909,#117910,#117911,#117912,#117913,#117914,
#117915,#117916,#117917,#117918,#117919,#117920,#117921,#117922,#117923,
#117924,#117925,#117926,#117927,#117928,#117929,#117930,#117931,#117932,
#117933,#117934,#117935,#117936,#117937,#117938,#117939,#117940,#117941,
#117942,#117943,#117944,#117945,#117946,#117947,#117948,#117949,#117950,
#117951,#117952,#117953,#117954,#117955,#117956,#117957,#117958,#117959,
#117960,#117961,#117962,#117963,#117964,#117965,#117966,#117967,#117968,
#117969,#117970,#117971,#117972,#117973,#117974,#117975,#117976,#117977,
#117978,#117979,#117980,#117981,#117982,#117983,#117984,#117985,#117986,
#117987,#117988,#117989,#117990,#117991,#117992,#117993,#117994,#117995,
#117996,#117997,#117998,#117999,#118000,#118001,#118002,#118003,#118004,
#118005,#118006,#118007,#118008,#118009,#118010,#118011,#118012,#118013,
#118014,#118015,#118016,#118017,#118018,#118019,#118020,#118021),
 .UNSPECIFIED.,.F.,.F.,(4,3,3,3,3,3,3,3,3,3,3,3,3,3,3,3,3,3,3,3,3,3,3,3,
3,3,3,3,3,3,3,3,3,3,3,3,3,3,3,3,3,3,3,3,3,3,3,3,3,3,3,3,3,3,3,3,3,3,3,3,
3,3,3,3,3,3,3,3,3,3,3,3,3,4),(1385.44236023311,1385.52976718702,1385.61728932258,
1385.70501835267,1385.79285658942,1385.8808961999,1385.94214563955,1386.0258843514,
1386.10951986276,1386.19307230616,1386.27656174201,1386.36001569263,1386.44345218647,
1386.52688929623,1386.61034509115,1386.69388958388,1386.77747866682,1386.86120193437,
1386.94188165027,1387.02562036212,1387.10925587348,1387.19280831688,1387.27629775273,
1387.35975170335,1387.44318819719,1387.52662530695,1387.61008110187,1387.6936255946,
1387.77721467754,1387.86093794509,1387.94161766099,1388.02535637284,1388.1089918842,
1388.1925443276,1388.27603376345,1388.35948771407,1388.44292420791,1388.52636131767,
1388.60981711259,1388.69336160532,1388.77695068826,1388.86067395581,1388.94135367171,
1389.02509238356,1389.10872789492,1389.19228033832,1389.27576977417,1389.35922372479,
1389.44266021863,1389.52609732839,1389.6095531233,1389.69309761603,1389.77668669898,
1389.86040996653,1389.94108968243,1390.02482839428,1390.10846390564,1390.19201634904,
1390.27550578489,1390.35895973551,1390.44239622935,1390.52583333911,1390.60928913403,
1390.69283362676,1390.7764227097,1390.86014597725,1390.94082569315,1391.02339322003,
1391.10586410619,1391.18825752044,1391.27058911472,1391.35288481146,1391.43517301765,
1391.47402012541),.UNSPECIFIED.);
#932=B_SPLINE_CURVE_WITH_KNOTS('',3,(#118022,#118023,#118024,#118025,#118026,
#118027,#118028,#118029,#118030,#118031),.UNSPECIFIED.,.F.,.F.,(4,3,3,4),
(1385.19203220808,1385.27963097554,1385.3670679702,1385.44236023309),
 .UNSPECIFIED.);
#933=B_SPLINE_CURVE_WITH_KNOTS('',3,(#118033,#118034,#118035,#118036,#118037,
#118038,#118039,#118040,#118041,#118042),.UNSPECIFIED.,.F.,.F.,(4,3,3,4),
(1385.19097775405,1385.25270024855,1385.37628043219,1385.44236023309),
 .UNSPECIFIED.);
#934=B_SPLINE_CURVE_WITH_KNOTS('',3,(#118043,#118044,#118045,#118046,#118047,
#118048,#118049,#118050,#118051,#118052,#118053,#118054,#118055,#118056,
#118057,#118058,#118059,#118060,#118061,#118062,#118063,#118064,#118065,
#118066,#118067,#118068,#118069,#118070,#118071,#118072,#118073,#118074,
#118075,#118076,#118077,#118078,#118079,#118080,#118081,#118082,#118083,
#118084,#118085,#118086,#118087,#118088,#118089,#118090,#118091,#118092,
#118093,#118094,#118095,#118096,#118097,#118098,#118099,#118100,#118101,
#118102,#118103,#118104,#118105,#118106,#118107,#118108,#118109,#118110,
#118111,#118112,#118113,#118114,#118115,#118116,#118117,#118118,#118119,
#118120,#118121,#118122,#118123,#118124,#118125,#118126,#118127,#118128,
#118129,#118130,#118131,#118132,#118133,#118134,#118135,#118136,#118137,
#118138,#118139,#118140,#118141,#118142,#118143,#118144,#118145,#118146,
#118147,#118148,#118149,#118150,#118151,#118152,#118153,#118154,#118155,
#118156,#118157,#118158,#118159,#118160,#118161,#118162,#118163,#118164,
#118165,#118166,#118167,#118168,#118169,#118170,#118171,#118172,#118173,
#118174,#118175,#118176,#118177,#118178,#118179,#118180,#118181,#118182,
#118183,#118184,#118185,#118186,#118187,#118188,#118189,#118190,#118191,
#118192,#118193,#118194,#118195,#118196,#118197,#118198,#118199,#118200,
#118201,#118202,#118203,#118204,#118205,#118206,#118207,#118208,#118209,
#118210,#118211,#118212,#118213,#118214,#118215,#118216,#118217,#118218,
#118219,#118220,#118221,#118222,#118223,#118224,#118225,#118226,#118227,
#118228,#118229,#118230,#118231,#118232,#118233,#118234,#118235,#118236,
#118237,#118238,#118239,#118240,#118241,#118242,#118243,#118244,#118245,
#118246,#118247,#118248,#118249,#118250,#118251,#118252,#118253,#118254,
#118255,#118256,#118257,#118258,#118259,#118260,#118261,#118262),
 .UNSPECIFIED.,.F.,.F.,(4,3,3,3,3,3,3,3,3,3,3,3,3,3,3,3,3,3,3,3,3,3,3,3,
3,3,3,3,3,3,3,3,3,3,3,3,3,3,3,3,3,3,3,3,3,3,3,3,3,3,3,3,3,3,3,3,3,3,3,3,
3,3,3,3,3,3,3,3,3,3,3,3,3,4),(1385.44236023322,1385.52472586569,1385.60701959995,
1385.68926698294,1385.77149079538,1385.85371006574,1385.93594381662,1386.0182603123,
1386.10061943005,1386.18310618992,1386.25243625927,1386.33617497112,1386.41981048248,
1386.50336292588,1386.58685236173,1386.67030631235,1386.75374280619,1386.83717991595,
1386.92063571087,1387.0041802036,1387.08776928654,1387.17149255409,1387.25217226999,
1387.33591098184,1387.4195464932,1387.5030989366,1387.58658837245,1387.67004232307,
1387.75347881691,1387.83691592667,1387.92037172159,1388.00391621431,1388.08750529726,
1388.17122856481,1388.25190828071,1388.33564699256,1388.41928250392,1388.50283494732,
1388.58632438317,1388.66977833379,1388.75321482763,1388.83665193739,1388.92010773231,
1389.00365222504,1389.08724130798,1389.17096457553,1389.25164429143,1389.33538300328,
1389.41901851464,1389.50257095804,1389.58606039389,1389.66951434451,1389.75295083835,
1389.83638794811,1389.91984374303,1390.00338823576,1390.0869773187,1390.17070058625,
1390.25138030215,1390.335119014,1390.41875452536,1390.50230696876,1390.58579640461,
1390.66925035523,1390.75268684907,1390.83612395883,1390.91957975375,1391.00312424648,
1391.08671332942,1391.17043659697,1391.25111631287,1391.34024896678,1391.4291696579,
1391.47524121817),.UNSPECIFIED.);
#935=B_SPLINE_CURVE_WITH_KNOTS('',3,(#118268,#118269,#118270,#118271,#118272,
#118273,#118274,#118275,#118276,#118277,#118278,#118279,#118280,#118281,
#118282,#118283,#118284,#118285,#118286,#118287,#118288,#118289,#118290,
#118291,#118292,#118293,#118294,#118295,#118296,#118297,#118298,#118299,
#118300,#118301,#118302,#118303,#118304,#118305,#118306,#118307,#118308,
#118309,#118310,#118311,#118312,#118313,#118314,#118315,#118316,#118317,
#118318,#118319,#118320,#118321,#118322,#118323,#118324,#118325,#118326,
#118327,#118328,#118329,#118330,#118331,#118332,#118333,#118334,#118335,
#118336,#118337,#118338,#118339,#118340,#118341,#118342,#118343,#118344,
#118345,#118346,#118347,#118348,#118349,#118350,#118351,#118352,#118353,
#118354,#118355,#118356,#118357,#118358,#118359,#118360,#118361,#118362,
#118363,#118364,#118365,#118366,#118367,#118368,#118369,#118370,#118371,
#118372,#118373,#118374,#118375,#118376,#118377,#118378,#118379,#118380,
#118381,#118382,#118383,#118384,#118385,#118386,#118387,#118388,#118389,
#118390,#118391,#118392,#118393,#118394,#118395,#118396,#118397,#118398,
#118399,#118400,#118401,#118402,#118403,#118404,#118405,#118406,#118407,
#118408,#118409,#118410,#118411,#118412,#118413,#118414,#118415,#118416,
#118417,#118418,#118419,#118420,#118421,#118422,#118423,#118424,#118425,
#118426,#118427,#118428,#118429,#118430,#118431,#118432,#118433,#118434,
#118435,#118436,#118437,#118438,#118439,#118440,#118441,#118442,#118443,
#118444,#118445,#118446,#118447,#118448,#118449,#118450,#118451,#118452,
#118453,#118454,#118455,#118456,#118457,#118458,#118459,#118460,#118461,
#118462,#118463,#118464,#118465,#118466,#118467,#118468,#118469,#118470,
#118471,#118472,#118473,#118474,#118475,#118476,#118477,#118478,#118479,
#118480,#118481,#118482,#118483,#118484),.UNSPECIFIED.,.F.,.F.,(4,3,3,3,
3,3,3,3,3,3,3,3,3,3,3,3,3,3,3,3,3,3,3,3,3,3,3,3,3,3,3,3,3,3,3,3,3,3,3,3,
3,3,3,3,3,3,3,3,3,3,3,3,3,3,3,3,3,3,3,3,3,3,3,3,3,3,3,3,3,3,3,3,4),(1391.72554554027,
1391.84155713252,1391.94056170387,1392.02430041572,1392.10793592708,1392.19148837048,
1392.27497780633,1392.35843175695,1392.44186825079,1392.52530536055,1392.60876115547,
1392.6923056482,1392.77589473114,1392.85961799869,1392.94029771459,1393.02403642644,
1393.1076719378,1393.1912243812,1393.27471381705,1393.35816776767,1393.44160426151,
1393.52504137127,1393.60849716619,1393.69204165892,1393.77563074186,1393.85935400942,
1393.94003372531,1394.02377243716,1394.10740794852,1394.19096039192,1394.27444982777,
1394.35790377839,1394.44134027223,1394.52477738199,1394.60823317691,1394.69177766964,
1394.77536675258,1394.85909002013,1394.93976973603,1395.02350844788,1395.10714395924,
1395.19069640264,1395.27418583849,1395.35763978911,1395.44107628295,1395.52451339271,
1395.60796918763,1395.69151368036,1395.7751027633,1395.85882603085,1395.93950574675,
1396.0232444586,1396.10687996996,1396.19043241336,1396.27392184921,1396.35737579983,
1396.44081229367,1396.52424940343,1396.60770519834,1396.69124969107,1396.77483877401,
1396.85856204157,1396.93924175747,1397.02299139418,1397.10663543065,1397.19017882089,
1397.27366514828,1397.35711253246,1397.44053906297,1397.52398987096,1397.60745144848,
1397.69098429292,1397.75707412262),.UNSPECIFIED.);
#936=B_SPLINE_CURVE_WITH_KNOTS('',3,(#118485,#118486,#118487,#118488,#118489,
#118490,#118491,#118492,#118493,#118494),.UNSPECIFIED.,.F.,.F.,(4,3,3,4),
(1391.47402012541,1391.55633938637,1391.64094246326,1391.72554554016),
 .UNSPECIFIED.);
#937=B_SPLINE_CURVE_WITH_KNOTS('',3,(#118496,#118497,#118498,#118499,#118500,
#118501,#118502,#118503,#118504,#118505),.UNSPECIFIED.,.F.,.F.,(4,3,3,4),
(1391.47524121817,1391.56388883391,1391.65232526733,1391.72554554016),
 .UNSPECIFIED.);
#938=B_SPLINE_CURVE_WITH_KNOTS('',3,(#118506,#118507,#118508,#118509,#118510,
#118511,#118512,#118513,#118514,#118515,#118516,#118517,#118518,#118519,
#118520,#118521,#118522,#118523,#118524,#118525,#118526,#118527,#118528,
#118529,#118530,#118531,#118532,#118533,#118534,#118535,#118536,#118537,
#118538,#118539,#118540,#118541,#118542,#118543,#118544,#118545,#118546,
#118547,#118548,#118549,#118550,#118551,#118552,#118553,#118554,#118555,
#118556,#118557,#118558,#118559,#118560,#118561,#118562,#118563,#118564,
#118565,#118566,#118567,#118568,#118569,#118570,#118571,#118572,#118573,
#118574,#118575,#118576,#118577,#118578,#118579,#118580,#118581,#118582,
#118583,#118584,#118585,#118586,#118587,#118588,#118589,#118590,#118591,
#118592,#118593,#118594,#118595,#118596,#118597,#118598,#118599,#118600,
#118601,#118602,#118603,#118604,#118605,#118606,#118607,#118608,#118609,
#118610,#118611,#118612,#118613,#118614,#118615,#118616,#118617,#118618,
#118619,#118620,#118621,#118622,#118623,#118624,#118625,#118626,#118627,
#118628,#118629,#118630,#118631,#118632,#118633,#118634,#118635,#118636,
#118637,#118638,#118639,#118640,#118641,#118642,#118643,#118644,#118645,
#118646,#118647,#118648,#118649,#118650,#118651,#118652,#118653,#118654,
#118655,#118656,#118657,#118658,#118659,#118660,#118661,#118662,#118663,
#118664,#118665,#118666,#118667,#118668,#118669,#118670,#118671,#118672,
#118673,#118674,#118675,#118676,#118677,#118678,#118679,#118680,#118681,
#118682,#118683,#118684,#118685,#118686,#118687,#118688,#118689,#118690,
#118691,#118692,#118693,#118694,#118695,#118696,#118697,#118698,#118699,
#118700,#118701,#118702,#118703,#118704,#118705,#118706,#118707,#118708,
#118709,#118710,#118711,#118712,#118713,#118714,#118715,#118716,#118717,
#118718,#118719,#118720,#118721,#118722,#118723,#118724,#118725),
 .UNSPECIFIED.,.F.,.F.,(4,3,3,3,3,3,3,3,3,3,3,3,3,3,3,3,3,3,3,3,3,3,3,3,
3,3,3,3,3,3,3,3,3,3,3,3,3,3,3,3,3,3,3,3,3,3,3,3,3,3,3,3,3,3,3,3,3,3,3,3,
3,3,3,3,3,3,3,3,3,3,3,3,3,4),(1391.72554554027,1391.81208339403,1391.89870567794,
1391.98674233935,1392.07363086768,1392.16224159564,1392.25085232359,1392.33459103544,
1392.4182265468,1392.5017789902,1392.58526842605,1392.66872237667,1392.75215887051,
1392.83559598027,1392.91905177519,1393.00259626792,1393.08618535086,1393.16990861841,
1393.25058833431,1393.33432704616,1393.41796255752,1393.50151500092,1393.58500443677,
1393.66845838739,1393.75189488123,1393.83533199099,1393.9187877859,1394.00233227863,
1394.08592136157,1394.16964462913,1394.25032434503,1394.33406305688,1394.41769856824,
1394.50125101164,1394.58474044749,1394.66819439811,1394.75163089195,1394.83506800171,
1394.91852379663,1395.00206828936,1395.0856573723,1395.16938063986,1395.25006035575,
1395.3337990676,1395.41743457896,1395.50098702236,1395.58447645821,1395.66793040883,
1395.75136690267,1395.83480401243,1395.91825980735,1396.00180430008,1396.08539338302,
1396.16911665058,1396.24979636647,1396.33353507832,1396.41717058968,1396.50072303308,
1396.58421246893,1396.66766641955,1396.75110291339,1396.83454002315,1396.91799581807,
1397.0015403108,1397.08512939374,1397.16885266129,1397.24953237719,1397.33223473028,
1397.41483932488,1397.50045997667,1397.5829190073,1397.66534185076,1397.74775086179,
1397.75732193205),.UNSPECIFIED.);
#939=B_SPLINE_CURVE_WITH_KNOTS('',3,(#118731,#118732,#118733,#118734,#118735,
#118736,#118737,#118738,#118739,#118740,#118741,#118742,#118743,#118744,
#118745,#118746,#118747,#118748,#118749,#118750,#118751,#118752,#118753,
#118754,#118755,#118756,#118757,#118758,#118759,#118760,#118761,#118762,
#118763,#118764,#118765,#118766,#118767,#118768,#118769,#118770,#118771,
#118772,#118773,#118774,#118775,#118776,#118777,#118778,#118779,#118780,
#118781,#118782,#118783,#118784,#118785,#118786,#118787,#118788,#118789,
#118790,#118791,#118792,#118793,#118794,#118795,#118796,#118797,#118798,
#118799,#118800,#118801,#118802,#118803,#118804,#118805,#118806,#118807,
#118808,#118809,#118810,#118811,#118812,#118813,#118814,#118815,#118816,
#118817,#118818,#118819,#118820,#118821,#118822,#118823,#118824,#118825,
#118826,#118827,#118828,#118829,#118830,#118831,#118832,#118833,#118834,
#118835,#118836,#118837,#118838,#118839,#118840,#118841,#118842,#118843,
#118844,#118845,#118846,#118847,#118848,#118849,#118850,#118851,#118852,
#118853,#118854,#118855,#118856,#118857,#118858,#118859,#118860,#118861,
#118862,#118863,#118864,#118865,#118866,#118867,#118868,#118869,#118870,
#118871,#118872,#118873,#118874,#118875,#118876,#118877,#118878,#118879,
#118880,#118881,#118882,#118883,#118884,#118885,#118886,#118887,#118888,
#118889,#118890,#118891,#118892,#118893,#118894,#118895,#118896,#118897,
#118898,#118899,#118900,#118901,#118902,#118903,#118904,#118905,#118906,
#118907,#118908,#118909,#118910,#118911,#118912,#118913,#118914,#118915,
#118916,#118917,#118918,#118919,#118920,#118921,#118922,#118923,#118924,
#118925,#118926,#118927,#118928,#118929,#118930,#118931,#118932,#118933,
#118934,#118935,#118936,#118937,#118938,#118939,#118940,#118941,#118942,
#118943,#118944,#118945,#118946,#118947,#118948,#118949,#118950,#118951,
#118952,#118953),.UNSPECIFIED.,.F.,.F.,(4,3,3,3,3,3,3,3,3,3,3,3,3,3,3,3,
3,3,3,3,3,3,3,3,3,3,3,3,3,3,3,3,3,3,3,3,3,3,3,3,3,3,3,3,3,3,3,3,3,3,3,3,
3,3,3,3,3,3,3,3,3,3,3,3,3,3,3,3,3,3,3,3,3,3,4),(1398.00873084757,1398.09161469114,
1398.17440099707,1398.25711065912,1398.34231104909,1398.42493873814,1398.50755742297,
1398.59018586339,1398.67284282351,1398.75559073286,1398.83839338335,1398.92131105705,
1398.93871377891,1399.02245249076,1399.10608800212,1399.18964044552,1399.27312988137,
1399.35658383199,1399.44002032583,1399.52345743559,1399.6069132305,1399.69045772323,
1399.77404680618,1399.85777007373,1399.93844978963,1400.02218850148,1400.10582401284,
1400.18937645624,1400.27286589209,1400.35631984271,1400.43975633655,1400.52319344631,
1400.60664924123,1400.69019373396,1400.7737828169,1400.85750608446,1400.93818580035,
1401.0219245122,1401.10556002356,1401.18911246696,1401.27260190281,1401.35605585343,
1401.43949234727,1401.52292945703,1401.60638525194,1401.68992974467,1401.77351882761,
1401.85724209517,1401.93792181107,1402.02166052292,1402.10529603428,1402.18884847768,
1402.27233791353,1402.35579186415,1402.43922835799,1402.52266546775,1402.60612126267,
1402.6896657554,1402.77325483834,1402.85697810589,1402.93765782179,1403.02139653364,
1403.105032045,1403.1885844884,1403.27207392425,1403.35552787487,1403.43896436871,
1403.52240147847,1403.60585727339,1403.68940176612,1403.77299084906,1403.85671411662,
1403.93739383251,1404.03402820369,1404.04140044517),.UNSPECIFIED.);
#940=B_SPLINE_CURVE_WITH_KNOTS('',3,(#118954,#118955,#118956,#118957,#118958,
#118959,#118960,#118961,#118962,#118963,#118964,#118965,#118966),
 .UNSPECIFIED.,.F.,.F.,(4,3,3,3,4),(1397.75707412262,1397.84070997716,1397.92446166817,
1397.93897776819,1398.00873084745),.UNSPECIFIED.);
#941=B_SPLINE_CURVE_WITH_KNOTS('',3,(#118968,#118969,#118970,#118971,#118972,
#118973,#118974,#118975,#118976,#118977),.UNSPECIFIED.,.F.,.F.,(4,3,3,4),
(1397.75732193205,1397.83975643715,1397.9242436423,1398.00873084745),
 .UNSPECIFIED.);
#942=B_SPLINE_CURVE_WITH_KNOTS('',3,(#118978,#118979,#118980,#118981,#118982,
#118983,#118984,#118985,#118986,#118987,#118988,#118989,#118990,#118991,
#118992,#118993,#118994,#118995,#118996,#118997,#118998,#118999,#119000,
#119001,#119002,#119003,#119004,#119005,#119006,#119007,#119008,#119009,
#119010,#119011,#119012,#119013,#119014,#119015,#119016,#119017,#119018,
#119019,#119020,#119021,#119022,#119023,#119024,#119025,#119026,#119027,
#119028,#119029,#119030,#119031,#119032,#119033,#119034,#119035,#119036,
#119037,#119038,#119039,#119040,#119041,#119042,#119043,#119044,#119045,
#119046,#119047,#119048,#119049,#119050,#119051,#119052,#119053,#119054,
#119055,#119056,#119057,#119058,#119059,#119060,#119061,#119062,#119063,
#119064,#119065,#119066,#119067,#119068,#119069,#119070,#119071,#119072,
#119073,#119074,#119075,#119076,#119077,#119078,#119079,#119080,#119081,
#119082,#119083,#119084,#119085,#119086,#119087,#119088,#119089,#119090,
#119091,#119092,#119093,#119094,#119095,#119096,#119097,#119098,#119099,
#119100,#119101,#119102,#119103,#119104,#119105,#119106,#119107,#119108,
#119109,#119110,#119111,#119112,#119113,#119114,#119115,#119116,#119117,
#119118,#119119,#119120,#119121,#119122,#119123,#119124,#119125,#119126,
#119127,#119128,#119129,#119130,#119131,#119132,#119133,#119134,#119135,
#119136,#119137,#119138,#119139,#119140,#119141,#119142,#119143,#119144,
#119145,#119146,#119147,#119148,#119149,#119150,#119151,#119152,#119153,
#119154,#119155,#119156,#119157,#119158,#119159,#119160,#119161,#119162,
#119163,#119164,#119165,#119166,#119167,#119168,#119169,#119170,#119171,
#119172,#119173,#119174,#119175,#119176,#119177,#119178,#119179,#119180,
#119181,#119182,#119183,#119184,#119185,#119186,#119187,#119188,#119189,
#119190,#119191,#119192,#119193,#119194,#119195,#119196,#119197),
 .UNSPECIFIED.,.F.,.F.,(4,3,3,3,3,3,3,3,3,3,3,3,3,3,3,3,3,3,3,3,3,3,3,3,
3,3,3,3,3,3,3,3,3,3,3,3,3,3,3,3,3,3,3,3,3,3,3,3,3,3,3,3,3,3,3,3,3,3,3,3,
3,3,3,3,3,3,3,3,3,3,3,3,3,4),(1398.00873084761,1398.11756456005,1398.22916845252,
1398.24926838791,1398.33300709976,1398.41664261112,1398.50019505452,1398.58368449037,
1398.66713844099,1398.75057493483,1398.83401204459,1398.91746783951,1399.00101233224,
1399.08460141518,1399.16832468273,1399.24900439863,1399.33274311048,1399.41637862184,
1399.49993106524,1399.58342050109,1399.66687445171,1399.75031094555,1399.83374805531,
1399.91720385023,1400.00074834295,1400.0843374259,1400.16806069345,1400.24874040935,
1400.3324791212,1400.41611463256,1400.49966707596,1400.58315651181,1400.66661046243,
1400.75004695627,1400.83348406603,1400.91693986095,1401.00048435368,1401.08407343662,
1401.16779670417,1401.24847642007,1401.33221513192,1401.41585064328,1401.49940308668,
1401.58289252253,1401.66634647315,1401.74978296699,1401.83322007675,1401.91667587167,
1402.0002203644,1402.08380944734,1402.16753271489,1402.24821243079,1402.33195114264,
1402.415586654,1402.4991390974,1402.58262853325,1402.66608248387,1402.74951897771,
1402.83295608747,1402.91641188239,1402.99995637512,1403.08354545806,1403.16726872562,
1403.24794844151,1403.33169972974,1403.41534508081,1403.49888897681,1403.58237533228,
1403.66582226773,1403.74924787314,1403.83269310383,1403.91614891234,1403.99966484341,
1404.04024993874),.UNSPECIFIED.);
#943=B_SPLINE_CURVE_WITH_KNOTS('',3,(#119203,#119204,#119205,#119206,#119207,
#119208,#119209,#119210,#119211,#119212,#119213,#119214,#119215,#119216,
#119217,#119218,#119219,#119220,#119221,#119222,#119223,#119224,#119225,
#119226,#119227,#119228,#119229,#119230,#119231,#119232,#119233,#119234,
#119235,#119236,#119237,#119238,#119239,#119240,#119241,#119242,#119243,
#119244,#119245,#119246,#119247,#119248,#119249,#119250,#119251,#119252,
#119253,#119254,#119255,#119256,#119257,#119258,#119259,#119260,#119261,
#119262,#119263,#119264,#119265,#119266,#119267,#119268,#119269,#119270,
#119271,#119272,#119273,#119274,#119275,#119276,#119277,#119278,#119279,
#119280,#119281,#119282,#119283,#119284,#119285,#119286,#119287,#119288,
#119289,#119290,#119291,#119292,#119293,#119294,#119295,#119296,#119297,
#119298,#119299,#119300,#119301,#119302,#119303,#119304,#119305,#119306,
#119307,#119308,#119309,#119310,#119311,#119312,#119313,#119314,#119315,
#119316,#119317,#119318,#119319,#119320,#119321,#119322,#119323,#119324,
#119325,#119326,#119327,#119328,#119329,#119330,#119331,#119332,#119333,
#119334,#119335,#119336,#119337,#119338,#119339,#119340,#119341,#119342,
#119343,#119344,#119345,#119346,#119347,#119348,#119349,#119350,#119351,
#119352,#119353,#119354,#119355,#119356,#119357,#119358,#119359,#119360,
#119361,#119362,#119363,#119364,#119365,#119366,#119367,#119368,#119369,
#119370,#119371,#119372,#119373,#119374,#119375,#119376,#119377,#119378,
#119379,#119380,#119381,#119382,#119383,#119384,#119385,#119386,#119387,
#119388,#119389,#119390,#119391,#119392,#119393,#119394,#119395,#119396,
#119397,#119398,#119399,#119400,#119401,#119402,#119403,#119404,#119405,
#119406,#119407,#119408,#119409,#119410,#119411,#119412,#119413,#119414,
#119415,#119416,#119417,#119418,#119419,#119420,#119421,#119422),
 .UNSPECIFIED.,.F.,.F.,(4,3,3,3,3,3,3,3,3,3,3,3,3,3,3,3,3,3,3,3,3,3,3,3,
3,3,3,3,3,3,3,3,3,3,3,3,3,3,3,3,3,3,3,3,3,3,3,3,3,3,3,3,3,3,3,3,3,3,3,3,
3,3,3,3,3,3,3,3,3,3,3,3,3,4),(1404.29191615463,1404.37562428831,1404.4593290263,
1404.54304803957,1404.62679900449,1404.7106527483,1404.79456200366,1404.87860831265,
1404.93712984323,1405.02086855508,1405.10450406644,1405.18805650984,1405.27154594569,
1405.35499989631,1405.43843639015,1405.52187349991,1405.60532929482,1405.68887378755,
1405.7724628705,1405.85618613805,1405.93686585395,1406.0206045658,1406.10424007716,
1406.18779252056,1406.27128195641,1406.35473590703,1406.43817240087,1406.52160951063,
1406.60506530555,1406.68860979828,1406.77219888122,1406.85592214878,1406.93660186467,
1407.02034057652,1407.10397608788,1407.18752853128,1407.27101796713,1407.35447191775,
1407.43790841159,1407.52134552135,1407.60480131627,1407.688345809,1407.77193489194,
1407.85565815949,1407.93633787539,1408.02007658724,1408.1037120986,1408.187264542,
1408.27075397785,1408.35420792847,1408.43764442231,1408.52108153207,1408.60453732698,
1408.68808181971,1408.77167090265,1408.85539417021,1408.93607388611,1409.01981259796,
1409.10344810932,1409.18700055272,1409.27048998857,1409.35394393919,1409.43738043303,
1409.52081754279,1409.60427333771,1409.68781783044,1409.77140691338,1409.85513018094,
1409.93580989683,1410.01998705489,1410.10402428112,1410.18798093152,1410.2718608454,
1410.32430278068),.UNSPECIFIED.);
#944=B_SPLINE_CURVE_WITH_KNOTS('',3,(#119423,#119424,#119425,#119426,#119427,
#119428,#119429,#119430,#119431,#119432),.UNSPECIFIED.,.F.,.F.,(4,3,3,4),
(1404.04140044517,1404.13747352714,1404.23285921852,1404.29191615443),
 .UNSPECIFIED.);
#945=B_SPLINE_CURVE_WITH_KNOTS('',3,(#119434,#119435,#119436,#119437,#119438,
#119439,#119440,#119441,#119442,#119443,#119444,#119445,#119446),
 .UNSPECIFIED.,.F.,.F.,(4,3,3,3,4),(1404.04024993874,1404.12386652121,1404.20760574971,
1404.24768445223,1404.29191615463),.UNSPECIFIED.);
#946=B_SPLINE_CURVE_WITH_KNOTS('',3,(#119447,#119448,#119449,#119450,#119451,
#119452,#119453,#119454,#119455,#119456,#119457,#119458,#119459,#119460,
#119461,#119462,#119463,#119464,#119465,#119466,#119467,#119468,#119469,
#119470,#119471,#119472,#119473,#119474,#119475,#119476,#119477,#119478,
#119479,#119480,#119481,#119482,#119483,#119484,#119485,#119486,#119487,
#119488,#119489,#119490,#119491,#119492,#119493,#119494,#119495,#119496,
#119497,#119498,#119499,#119500,#119501,#119502,#119503,#119504,#119505,
#119506,#119507,#119508,#119509,#119510,#119511,#119512,#119513,#119514,
#119515,#119516,#119517,#119518,#119519,#119520,#119521,#119522,#119523,
#119524,#119525,#119526,#119527,#119528,#119529,#119530,#119531,#119532,
#119533,#119534,#119535,#119536,#119537,#119538,#119539,#119540,#119541,
#119542,#119543,#119544,#119545,#119546,#119547,#119548,#119549,#119550,
#119551,#119552,#119553,#119554,#119555,#119556,#119557,#119558,#119559,
#119560,#119561,#119562,#119563,#119564,#119565,#119566,#119567,#119568,
#119569,#119570,#119571,#119572,#119573,#119574,#119575,#119576,#119577,
#119578,#119579,#119580,#119581,#119582,#119583,#119584,#119585,#119586,
#119587,#119588,#119589,#119590,#119591,#119592,#119593,#119594,#119595,
#119596,#119597,#119598,#119599,#119600,#119601,#119602,#119603,#119604,
#119605,#119606,#119607,#119608,#119609,#119610,#119611,#119612,#119613,
#119614,#119615,#119616,#119617,#119618,#119619,#119620,#119621,#119622,
#119623,#119624,#119625,#119626,#119627,#119628,#119629,#119630,#119631,
#119632,#119633,#119634,#119635,#119636,#119637,#119638,#119639,#119640,
#119641,#119642,#119643,#119644,#119645,#119646,#119647,#119648,#119649,
#119650,#119651,#119652,#119653,#119654,#119655,#119656,#119657,#119658,
#119659,#119660,#119661,#119662,#119663,#119664,#119665,#119666),
 .UNSPECIFIED.,.F.,.F.,(4,3,3,3,3,3,3,3,3,3,3,3,3,3,3,3,3,3,3,3,3,3,3,3,
3,3,3,3,3,3,3,3,3,3,3,3,3,3,3,3,3,3,3,3,3,3,3,3,3,3,3,3,3,3,3,3,3,3,3,3,
3,3,3,3,3,3,3,3,3,3,3,3,3,4),(1404.29191615481,1404.37506475554,1404.45811270144,
1404.54108068674,1404.62398932894,1404.70686775223,1404.78973305654,1404.87260381792,
1404.95549861295,1405.03848303953,1405.1215178224,1405.20467492572,1405.24742046295,
1405.3311591748,1405.41479468616,1405.49834712956,1405.58183656541,1405.66529051603,
1405.74872700987,1405.83216411963,1405.91561991455,1405.99916440728,1406.08275349022,
1406.16647675777,1406.24715647367,1406.33089518552,1406.41453069688,1406.49808314028,
1406.58157257613,1406.66502652675,1406.74846302059,1406.83190013035,1406.91535592527,
1406.998900418,1407.08248950094,1407.16621276849,1407.24689248439,1407.33063119624,
1407.4142667076,1407.497819151,1407.58130858685,1407.66476253747,1407.74819903131,
1407.83163614107,1407.91509193599,1407.99863642872,1408.08222551166,1408.16594877921,
1408.24662849511,1408.33036720696,1408.41400271832,1408.49755516172,1408.58104459757,
1408.66449854819,1408.74793504203,1408.83137215179,1408.91482794671,1408.99837243944,
1409.08196152238,1409.16568478993,1409.24636450583,1409.33010321768,1409.41373872904,
1409.49729117244,1409.58078060829,1409.66423455891,1409.74767105275,1409.83110816251,
1409.91456395743,1409.99810845016,1410.0816975331,1410.16542080065,1410.24610051655,
1410.3244751935),.UNSPECIFIED.);
#947=B_SPLINE_CURVE_WITH_KNOTS('',3,(#119672,#119673,#119674,#119675,#119676,
#119677,#119678,#119679,#119680,#119681,#119682,#119683,#119684,#119685,
#119686,#119687,#119688,#119689,#119690,#119691,#119692,#119693,#119694,
#119695,#119696,#119697,#119698,#119699,#119700,#119701,#119702,#119703,
#119704,#119705,#119706,#119707,#119708,#119709,#119710,#119711,#119712,
#119713,#119714,#119715,#119716,#119717,#119718,#119719,#119720,#119721,
#119722,#119723,#119724,#119725,#119726,#119727,#119728,#119729,#119730,
#119731,#119732,#119733,#119734,#119735,#119736,#119737,#119738,#119739,
#119740,#119741,#119742,#119743,#119744,#119745,#119746,#119747,#119748,
#119749,#119750,#119751,#119752,#119753,#119754,#119755,#119756,#119757,
#119758,#119759,#119760,#119761,#119762,#119763,#119764,#119765,#119766,
#119767,#119768,#119769,#119770,#119771,#119772,#119773,#119774,#119775,
#119776,#119777,#119778,#119779,#119780,#119781,#119782,#119783,#119784,
#119785,#119786,#119787,#119788,#119789,#119790,#119791,#119792,#119793,
#119794,#119795,#119796,#119797,#119798,#119799,#119800,#119801,#119802,
#119803,#119804,#119805,#119806,#119807,#119808,#119809,#119810,#119811,
#119812,#119813,#119814,#119815,#119816,#119817,#119818,#119819,#119820,
#119821,#119822,#119823,#119824,#119825,#119826,#119827,#119828,#119829,
#119830,#119831,#119832,#119833,#119834,#119835,#119836,#119837,#119838,
#119839,#119840,#119841,#119842,#119843,#119844,#119845,#119846,#119847,
#119848,#119849,#119850,#119851,#119852,#119853,#119854,#119855,#119856,
#119857,#119858,#119859,#119860,#119861,#119862,#119863,#119864,#119865,
#119866,#119867,#119868,#119869,#119870,#119871,#119872,#119873,#119874,
#119875,#119876,#119877,#119878,#119879,#119880,#119881,#119882,#119883,
#119884,#119885,#119886,#119887,#119888),.UNSPECIFIED.,.F.,.F.,(4,3,3,3,
3,3,3,3,3,3,3,3,3,3,3,3,3,3,3,3,3,3,3,3,3,3,3,3,3,3,3,3,3,3,3,3,3,3,3,3,
3,3,3,3,3,3,3,3,3,3,3,3,3,3,3,3,3,3,3,3,3,3,3,3,3,3,3,3,3,3,3,3,4),(1410.57510146201,
1410.67010500045,1410.76553206136,1410.86152504162,1410.93554590755,1411.0192846194,
1411.10292013076,1411.18647257416,1411.26996201001,1411.35341596063,1411.43685245447,
1411.52028956423,1411.60374535915,1411.68728985187,1411.77087893482,1411.85460220237,
1411.93528191827,1412.01902063012,1412.10265614148,1412.18620858488,1412.26969802073,
1412.35315197135,1412.43658846519,1412.52002557495,1412.60348136987,1412.6870258626,
1412.77061494554,1412.8543382131,1412.93501792899,1413.01875664084,1413.1023921522,
1413.1859445956,1413.26943403145,1413.35288798207,1413.43632447591,1413.51976158567,
1413.60321738059,1413.68676187332,1413.77035095626,1413.85407422381,1413.93475393971,
1414.01849265156,1414.10212816292,1414.18568060632,1414.26917004217,1414.35262399279,
1414.43606048663,1414.51949759639,1414.6029533913,1414.68649788403,1414.77008696697,
1414.85381023453,1414.93448995043,1415.01822866228,1415.10186417364,1415.18541661704,
1415.26890605289,1415.35236000351,1415.43579649735,1415.51923360711,1415.60268940203,
1415.68623389476,1415.7698229777,1415.85354624526,1415.93422596115,1416.01825423227,
1416.10099893318,1416.18366832812,1416.26628131214,1416.35132401664,1416.43389281429,
1416.52017247222,1416.60645213015),.UNSPECIFIED.);
#948=B_SPLINE_CURVE_WITH_KNOTS('',3,(#119889,#119890,#119891,#119892,#119893,
#119894,#119895,#119896,#119897,#119898),.UNSPECIFIED.,.F.,.F.,(4,3,3,4),
(1410.32430278068,1410.40811390766,1410.49192260022,1410.57510146181),
 .UNSPECIFIED.);
#949=B_SPLINE_CURVE_WITH_KNOTS('',3,(#119900,#119901,#119902,#119903,#119904,
#119905,#119906,#119907,#119908,#119909),.UNSPECIFIED.,.F.,.F.,(4,3,3,4),
(1410.3244751935,1410.42295017058,1410.52052586119,1410.57510146163),
 .UNSPECIFIED.);
#950=B_SPLINE_CURVE_WITH_KNOTS('',3,(#119910,#119911,#119912,#119913,#119914,
#119915,#119916,#119917,#119918,#119919,#119920,#119921,#119922,#119923,
#119924,#119925,#119926,#119927,#119928,#119929,#119930,#119931,#119932,
#119933,#119934,#119935,#119936,#119937,#119938,#119939,#119940,#119941,
#119942,#119943,#119944,#119945,#119946,#119947,#119948,#119949,#119950,
#119951,#119952,#119953,#119954,#119955,#119956,#119957,#119958,#119959,
#119960,#119961,#119962,#119963,#119964,#119965,#119966,#119967,#119968,
#119969,#119970,#119971,#119972,#119973,#119974,#119975,#119976,#119977,
#119978,#119979,#119980,#119981,#119982,#119983,#119984,#119985,#119986,
#119987,#119988,#119989,#119990,#119991,#119992,#119993,#119994,#119995,
#119996,#119997,#119998,#119999,#120000,#120001,#120002,#120003,#120004,
#120005,#120006,#120007,#120008,#120009,#120010,#120011,#120012,#120013,
#120014,#120015,#120016,#120017,#120018,#120019,#120020,#120021,#120022,
#120023,#120024,#120025,#120026,#120027,#120028,#120029,#120030,#120031,
#120032,#120033,#120034,#120035,#120036,#120037,#120038,#120039,#120040,
#120041,#120042,#120043,#120044,#120045,#120046,#120047,#120048,#120049,
#120050,#120051,#120052,#120053,#120054,#120055,#120056,#120057,#120058,
#120059,#120060,#120061,#120062,#120063,#120064,#120065,#120066,#120067,
#120068,#120069,#120070,#120071,#120072,#120073,#120074,#120075,#120076,
#120077,#120078,#120079,#120080,#120081,#120082,#120083,#120084,#120085,
#120086,#120087,#120088,#120089,#120090,#120091,#120092,#120093,#120094,
#120095,#120096,#120097,#120098,#120099,#120100,#120101,#120102,#120103,
#120104,#120105,#120106,#120107,#120108,#120109,#120110,#120111,#120112,
#120113,#120114,#120115,#120116,#120117,#120118,#120119,#120120,#120121,
#120122,#120123,#120124,#120125,#120126,#120127,#120128,#120129),
 .UNSPECIFIED.,.F.,.F.,(4,3,3,3,3,3,3,3,3,3,3,3,3,3,3,3,3,3,3,3,3,3,3,3,
3,3,3,3,3,3,3,3,3,3,3,3,3,3,3,3,3,3,3,3,3,3,3,3,3,3,3,3,3,3,3,3,3,3,3,3,
3,3,3,3,3,3,3,3,3,3,3,3,3,4),(1410.57510146181,1410.65894334499,1410.74225529584,
1410.82557017512,1410.9089061093,1410.9931387138,1411.07661585494,1411.1612261911,
1411.24583652727,1411.32957523912,1411.41321075048,1411.49676319388,1411.58025262973,
1411.66370658035,1411.74714307419,1411.83058018395,1411.91403597887,1411.9975804716,
1412.08116955454,1412.16489282209,1412.24557253799,1412.32931124984,1412.4129467612,
1412.4964992046,1412.57998864045,1412.66344259107,1412.74687908491,1412.83031619467,
1412.91377198959,1412.99731648232,1413.08090556526,1413.16462883281,1413.24530854871,
1413.32904726056,1413.41268277192,1413.49623521532,1413.57972465117,1413.66317860179,
1413.74661509563,1413.83005220539,1413.91350800031,1413.99705249304,1414.08064157598,
1414.16436484353,1414.24504455943,1414.32878327128,1414.41241878264,1414.49597122604,
1414.57946066189,1414.66291461251,1414.74635110635,1414.82978821611,1414.91324401103,
1414.99678850376,1415.0803775867,1415.16410085425,1415.24478057015,1415.328519282,
1415.41215479336,1415.49570723676,1415.57919667261,1415.66265062323,1415.74608711707,
1415.82952422683,1415.91298002175,1415.99652451447,1416.08011359742,1416.16383686497,
1416.24451658087,1416.32920862088,1416.41375449164,1416.49821554759,1416.5825919458,
1416.60760743314),.UNSPECIFIED.);
#951=B_SPLINE_CURVE_WITH_KNOTS('',3,(#120135,#120136,#120137,#120138,#120139,
#120140,#120141,#120142,#120143,#120144,#120145,#120146,#120147,#120148,
#120149,#120150,#120151,#120152,#120153,#120154,#120155,#120156,#120157,
#120158,#120159,#120160,#120161,#120162,#120163,#120164,#120165,#120166,
#120167,#120168,#120169,#120170,#120171,#120172,#120173,#120174,#120175,
#120176,#120177,#120178,#120179,#120180,#120181,#120182,#120183,#120184,
#120185,#120186,#120187,#120188,#120189,#120190,#120191,#120192,#120193,
#120194,#120195,#120196,#120197,#120198,#120199,#120200,#120201,#120202,
#120203,#120204,#120205,#120206,#120207,#120208,#120209,#120210,#120211,
#120212,#120213,#120214,#120215,#120216,#120217,#120218,#120219,#120220,
#120221,#120222,#120223,#120224,#120225,#120226,#120227,#120228,#120229,
#120230,#120231,#120232,#120233,#120234,#120235,#120236,#120237,#120238,
#120239,#120240,#120241,#120242,#120243,#120244,#120245,#120246,#120247,
#120248,#120249,#120250,#120251,#120252,#120253,#120254,#120255,#120256,
#120257,#120258,#120259,#120260,#120261,#120262,#120263,#120264,#120265,
#120266,#120267,#120268,#120269,#120270,#120271,#120272,#120273,#120274,
#120275,#120276,#120277,#120278,#120279,#120280,#120281,#120282,#120283,
#120284,#120285,#120286,#120287,#120288,#120289,#120290,#120291,#120292,
#120293,#120294,#120295,#120296,#120297,#120298,#120299,#120300,#120301,
#120302,#120303,#120304,#120305,#120306,#120307,#120308,#120309,#120310,
#120311,#120312,#120313,#120314,#120315,#120316,#120317,#120318,#120319,
#120320,#120321,#120322,#120323,#120324,#120325,#120326,#120327,#120328,
#120329,#120330,#120331,#120332,#120333,#120334,#120335,#120336,#120337,
#120338,#120339,#120340,#120341,#120342,#120343,#120344,#120345,#120346,
#120347,#120348,#120349,#120350,#120351,#120352,#120353,#120354),
 .UNSPECIFIED.,.F.,.F.,(4,3,3,3,3,3,3,3,3,3,3,3,3,3,3,3,3,3,3,3,3,3,3,3,
3,3,3,3,3,3,3,3,3,3,3,3,3,3,3,3,3,3,3,3,3,3,3,3,3,3,3,3,3,3,3,3,3,3,3,3,
3,3,3,3,3,3,3,3,3,3,3,3,3,4),(1416.85828676899,1416.93396197187,1417.01770068372,
1417.10133619508,1417.18488863848,1417.26837807433,1417.35183202495,1417.43526851879,
1417.51870562855,1417.60216142347,1417.6857059162,1417.76929499914,1417.8530182667,
1417.93369798259,1418.01743669444,1418.1010722058,1418.1846246492,1418.26811408505,
1418.35156803567,1418.43500452951,1418.51844163927,1418.60189743419,1418.68544192692,
1418.76903100986,1418.85275427742,1418.93343399331,1419.01717270516,1419.10080821652,
1419.18436065992,1419.26785009577,1419.35130404639,1419.43474054023,1419.51817764999,
1419.60163344491,1419.68517793764,1419.76876702058,1419.85249028813,1419.93317000403,
1420.01690871588,1420.10054422724,1420.18409667064,1420.26758610649,1420.35104005711,
1420.43447655095,1420.51791366071,1420.60136945563,1420.68491394836,1420.7685030313,
1420.85222629885,1420.93290601475,1421.0166447266,1421.10028023796,1421.18383268136,
1421.26732211721,1421.35077606783,1421.43421256167,1421.51764967143,1421.60110546634,
1421.68464995907,1421.76823904201,1421.85196230957,1421.93264202547,1422.01638314035,
1422.10002049812,1422.18357423364,1422.26706440912,1422.35051630726,1422.4339499617,
1422.51738344462,1422.60083482409,1422.68436422929,1422.76793789954,1422.85162109986,
1422.89017552255),.UNSPECIFIED.);
#952=B_SPLINE_CURVE_WITH_KNOTS('',3,(#120355,#120356,#120357,#120358,#120359,
#120360,#120361,#120362,#120363,#120364),.UNSPECIFIED.,.F.,.F.,(4,3,3,4),
(1416.60645213015,1416.68913802073,1416.7737123948,1416.85828676886),
 .UNSPECIFIED.);
#953=B_SPLINE_CURVE_WITH_KNOTS('',3,(#120366,#120367,#120368,#120369,#120370,
#120371,#120372,#120373,#120374,#120375),.UNSPECIFIED.,.F.,.F.,(4,3,3,4),
(1416.60760743314,1416.69191056942,1416.77619079502,1416.85828676899),
 .UNSPECIFIED.);
#954=B_SPLINE_CURVE_WITH_KNOTS('',3,(#120376,#120377,#120378,#120379,#120380,
#120381,#120382,#120383,#120384,#120385,#120386,#120387,#120388,#120389,
#120390,#120391,#120392,#120393,#120394,#120395,#120396,#120397,#120398,
#120399,#120400,#120401,#120402,#120403,#120404,#120405,#120406,#120407,
#120408,#120409,#120410,#120411,#120412,#120413,#120414,#120415,#120416,
#120417,#120418,#120419,#120420,#120421,#120422,#120423,#120424,#120425,
#120426,#120427,#120428,#120429,#120430,#120431,#120432,#120433,#120434,
#120435,#120436,#120437,#120438,#120439,#120440,#120441,#120442,#120443,
#120444,#120445,#120446,#120447,#120448,#120449,#120450,#120451,#120452,
#120453,#120454,#120455,#120456,#120457,#120458,#120459,#120460,#120461,
#120462,#120463,#120464,#120465,#120466,#120467,#120468,#120469,#120470,
#120471,#120472,#120473,#120474,#120475,#120476,#120477,#120478,#120479,
#120480,#120481,#120482,#120483,#120484,#120485,#120486,#120487,#120488,
#120489,#120490,#120491,#120492,#120493,#120494,#120495,#120496,#120497,
#120498,#120499,#120500,#120501,#120502,#120503,#120504,#120505,#120506,
#120507,#120508,#120509,#120510,#120511,#120512,#120513,#120514,#120515,
#120516,#120517,#120518,#120519,#120520,#120521,#120522,#120523,#120524,
#120525,#120526,#120527,#120528,#120529,#120530,#120531,#120532,#120533,
#120534,#120535,#120536,#120537,#120538,#120539,#120540,#120541,#120542,
#120543,#120544,#120545,#120546,#120547,#120548,#120549,#120550,#120551,
#120552,#120553,#120554,#120555,#120556,#120557,#120558,#120559,#120560,
#120561,#120562,#120563,#120564,#120565,#120566,#120567,#120568,#120569,
#120570,#120571,#120572,#120573,#120574,#120575,#120576,#120577,#120578,
#120579,#120580,#120581,#120582,#120583,#120584,#120585,#120586,#120587,
#120588,#120589,#120590,#120591,#120592),.UNSPECIFIED.,.F.,.F.,(4,3,3,3,
3,3,3,3,3,3,3,3,3,3,3,3,3,3,3,3,3,3,3,3,3,3,3,3,3,3,3,3,3,3,3,3,3,3,3,3,
3,3,3,3,3,3,3,3,3,3,3,3,3,3,3,3,3,3,3,3,3,3,3,3,3,3,3,3,3,3,3,3,4),(1416.85828676918,
1416.95477822478,1417.04830595778,1417.14627927468,1417.24425259159,1417.32799130344,
1417.4116268148,1417.4951792582,1417.57866869405,1417.66212264467,1417.74555913851,
1417.82899624827,1417.91245204319,1417.99599653592,1418.07958561886,1418.16330888641,
1418.24398860231,1418.32772731416,1418.41136282552,1418.49491526892,1418.57840470477,
1418.66185865539,1418.74529514923,1418.82873225899,1418.91218805391,1418.99573254664,
1419.07932162958,1419.16304489713,1419.24372461303,1419.32746332488,1419.41109883624,
1419.49465127964,1419.57814071549,1419.66159466611,1419.74503115995,1419.82846826971,
1419.91192406463,1419.99546855736,1420.0790576403,1420.16278090785,1420.24346062375,
1420.3271993356,1420.41083484696,1420.49438729036,1420.57787672621,1420.66133067683,
1420.74476717067,1420.82820428043,1420.91166007535,1420.99520456808,1421.07879365102,
1421.16251691857,1421.24319663447,1421.32693534632,1421.41057085768,1421.49412330108,
1421.57761273693,1421.66106668755,1421.74450318139,1421.82794029115,1421.91139608607,
1421.9949405788,1422.07852966174,1422.16225292929,1422.24293264519,1422.32559622083,
1422.40816522113,1422.490658732,1422.57309577088,1422.6555052585,1422.73789637857,
1422.82031610301,1422.88963902832),.UNSPECIFIED.);
#955=B_SPLINE_CURVE_WITH_KNOTS('',3,(#120598,#120599,#120600,#120601,#120602,
#120603,#120604,#120605,#120606,#120607,#120608,#120609,#120610,#120611,
#120612,#120613,#120614,#120615,#120616,#120617,#120618,#120619,#120620,
#120621,#120622,#120623,#120624,#120625,#120626,#120627,#120628,#120629,
#120630,#120631,#120632,#120633,#120634,#120635,#120636,#120637,#120638,
#120639,#120640,#120641,#120642,#120643,#120644,#120645,#120646,#120647,
#120648,#120649,#120650,#120651,#120652,#120653,#120654,#120655,#120656,
#120657,#120658,#120659,#120660,#120661,#120662,#120663,#120664,#120665,
#120666,#120667,#120668,#120669,#120670,#120671,#120672,#120673,#120674,
#120675,#120676,#120677,#120678,#120679,#120680,#120681,#120682,#120683,
#120684,#120685,#120686,#120687,#120688,#120689,#120690,#120691,#120692,
#120693,#120694,#120695,#120696,#120697,#120698,#120699,#120700,#120701,
#120702,#120703,#120704,#120705,#120706,#120707,#120708,#120709,#120710,
#120711,#120712,#120713,#120714,#120715,#120716,#120717,#120718,#120719,
#120720,#120721,#120722,#120723,#120724,#120725,#120726,#120727,#120728,
#120729,#120730,#120731,#120732,#120733,#120734,#120735,#120736,#120737,
#120738,#120739,#120740,#120741,#120742,#120743,#120744,#120745,#120746,
#120747,#120748,#120749,#120750,#120751,#120752,#120753,#120754,#120755,
#120756,#120757,#120758,#120759,#120760,#120761,#120762,#120763,#120764,
#120765,#120766,#120767,#120768,#120769,#120770,#120771,#120772,#120773,
#120774,#120775,#120776,#120777,#120778,#120779,#120780,#120781,#120782,
#120783,#120784,#120785,#120786,#120787,#120788,#120789,#120790,#120791,
#120792,#120793,#120794,#120795,#120796,#120797,#120798,#120799,#120800,
#120801,#120802,#120803,#120804,#120805,#120806,#120807,#120808,#120809,
#120810,#120811,#120812,#120813,#120814,#120815,#120816,#120817),
 .UNSPECIFIED.,.F.,.F.,(4,3,3,3,3,3,3,3,3,3,3,3,3,3,3,3,3,3,3,3,3,3,3,3,
3,3,3,3,3,3,3,3,3,3,3,3,3,3,3,3,3,3,3,3,3,3,3,3,3,3,3,3,3,3,3,3,3,3,3,3,
3,3,3,3,3,3,3,3,3,3,3,3,3,4),(1423.14147207631,1423.22386678623,1423.30619520945,
1423.38848470131,1423.47075562151,1423.55302696428,1423.63531772196,1423.71769400858,
1423.80011729223,1423.88266299128,1423.93211404692,1424.01585275877,1424.09948827013,
1424.18304071353,1424.26653014938,1424.3499841,1424.43342059384,1424.5168577036,
1424.60031349852,1424.68385799124,1424.76744707419,1424.85117034174,1424.93185005764,
1425.01558876949,1425.09922428085,1425.18277672425,1425.2662661601,1425.34972011072,
1425.43315660456,1425.51659371432,1425.60004950923,1425.68359400196,1425.7671830849,
1425.85090635246,1425.93158606836,1426.01532478021,1426.09896029157,1426.18251273497,
1426.26600217082,1426.34945612144,1426.43289261528,1426.51632972504,1426.59978551996,
1426.68333001269,1426.76691909563,1426.85064236319,1426.93132207908,1427.01506079093,
1427.09869630229,1427.18224874569,1427.26573818154,1427.34919213216,1427.432628626,
1427.51606573576,1427.59952153068,1427.68306602341,1427.76665510635,1427.85037837391,
1427.9310580898,1428.01479680165,1428.09843231301,1428.18198475641,1428.26547419226,
1428.34892814288,1428.43236463672,1428.51580174648,1428.5992575414,1428.68280203413,
1428.76639111707,1428.85011438462,1428.93079410052,1429.01909172383,1429.10718968499,
1429.17433711171),.UNSPECIFIED.);
#956=B_SPLINE_CURVE_WITH_KNOTS('',3,(#120818,#120819,#120820,#120821,#120822,
#120823,#120824,#120825,#120826,#120827),.UNSPECIFIED.,.F.,.F.,(4,3,3,4),
(1422.89017552255,1422.93237803619,1423.04995135785,1423.14147207617),
 .UNSPECIFIED.);
#957=B_SPLINE_CURVE_WITH_KNOTS('',3,(#120829,#120830,#120831,#120832,#120833,
#120834,#120835,#120836,#120837,#120838),.UNSPECIFIED.,.F.,.F.,(4,3,3,4),
(1422.88963902832,1422.97213368162,1423.05680287883,1423.14147207603),
 .UNSPECIFIED.);
#958=B_SPLINE_CURVE_WITH_KNOTS('',3,(#120839,#120840,#120841,#120842,#120843,
#120844,#120845,#120846,#120847,#120848,#120849,#120850,#120851,#120852,
#120853,#120854,#120855,#120856,#120857,#120858,#120859,#120860,#120861,
#120862,#120863,#120864,#120865,#120866,#120867,#120868,#120869,#120870,
#120871,#120872,#120873,#120874,#120875,#120876,#120877,#120878,#120879,
#120880,#120881,#120882,#120883,#120884,#120885,#120886,#120887,#120888,
#120889,#120890,#120891,#120892,#120893,#120894,#120895,#120896,#120897,
#120898,#120899,#120900,#120901,#120902,#120903,#120904,#120905,#120906,
#120907,#120908,#120909,#120910,#120911,#120912,#120913,#120914,#120915,
#120916,#120917,#120918,#120919,#120920,#120921,#120922,#120923,#120924,
#120925,#120926,#120927,#120928,#120929,#120930,#120931,#120932,#120933,
#120934,#120935,#120936,#120937,#120938,#120939,#120940,#120941,#120942,
#120943,#120944,#120945,#120946,#120947,#120948,#120949,#120950,#120951,
#120952,#120953,#120954,#120955,#120956,#120957,#120958,#120959,#120960,
#120961,#120962,#120963,#120964,#120965,#120966,#120967,#120968,#120969,
#120970,#120971,#120972,#120973,#120974,#120975,#120976,#120977,#120978,
#120979,#120980,#120981,#120982,#120983,#120984,#120985,#120986,#120987,
#120988,#120989,#120990,#120991,#120992,#120993,#120994,#120995,#120996,
#120997,#120998,#120999,#121000,#121001,#121002,#121003,#121004,#121005,
#121006,#121007,#121008,#121009,#121010,#121011,#121012,#121013,#121014,
#121015,#121016,#121017,#121018,#121019,#121020,#121021,#121022,#121023,
#121024,#121025,#121026,#121027,#121028,#121029,#121030,#121031,#121032,
#121033,#121034,#121035,#121036,#121037,#121038,#121039,#121040,#121041,
#121042,#121043,#121044,#121045,#121046,#121047,#121048,#121049,#121050,
#121051,#121052,#121053,#121054,#121055),.UNSPECIFIED.,.F.,.F.,(4,3,3,3,
3,3,3,3,3,3,3,3,3,3,3,3,3,3,3,3,3,3,3,3,3,3,3,3,3,3,3,3,3,3,3,3,3,3,3,3,
3,3,3,3,3,3,3,3,3,3,3,3,3,3,3,3,3,3,3,3,3,3,3,3,3,3,3,3,3,3,3,3,4),(1423.14147207617,
1423.24266865591,1423.32640736776,1423.41004287912,1423.49359532252,1423.57708475837,
1423.66053870899,1423.74397520283,1423.82741231259,1423.91086810751,1423.99441260024,
1424.07800168318,1424.16172495074,1424.24240466663,1424.32614337848,1424.40977888984,
1424.49333133324,1424.57682076909,1424.66027471971,1424.74371121355,1424.82714832331,
1424.91060411823,1424.99414861096,1425.0777376939,1425.16146096146,1425.24214067735,
1425.3258793892,1425.40951490056,1425.49306734396,1425.57655677981,1425.66001073043,
1425.74344722427,1425.82688433403,1425.91034012894,1425.99388462167,1426.07747370462,
1426.16119697217,1426.24187668807,1426.32561539992,1426.40925091128,1426.49280335468,
1426.57629279053,1426.65974674115,1426.74318323499,1426.82662034475,1426.91007613967,
1426.9936206324,1427.07720971534,1427.1609329829,1427.24161269879,1427.32535141064,
1427.408986922,1427.4925393654,1427.57602880125,1427.65948275187,1427.74291924571,
1427.82635635547,1427.90981215039,1427.99335664312,1428.07694572606,1428.16066899361,
1428.24134870951,1428.32509132268,1428.40872984063,1428.49228439967,1428.57740517497,
1428.66085544328,1428.74428734301,1428.82771894588,1428.91410185992,1428.9976247119,
1429.08543765696,1429.17325060202),.UNSPECIFIED.);
#959=B_SPLINE_CURVE_WITH_KNOTS('',3,(#121061,#121062,#121063,#121064,#121065,
#121066,#121067,#121068,#121069,#121070,#121071,#121072,#121073,#121074,
#121075,#121076,#121077,#121078,#121079,#121080,#121081,#121082,#121083,
#121084,#121085,#121086,#121087,#121088,#121089,#121090,#121091,#121092,
#121093,#121094,#121095,#121096,#121097,#121098,#121099,#121100,#121101,
#121102,#121103,#121104,#121105,#121106,#121107,#121108,#121109,#121110,
#121111,#121112,#121113,#121114,#121115,#121116,#121117,#121118,#121119,
#121120,#121121,#121122,#121123,#121124,#121125,#121126,#121127,#121128,
#121129,#121130,#121131,#121132,#121133,#121134,#121135,#121136,#121137,
#121138,#121139,#121140,#121141,#121142,#121143,#121144,#121145,#121146,
#121147,#121148,#121149,#121150,#121151,#121152,#121153,#121154,#121155,
#121156,#121157,#121158,#121159,#121160,#121161,#121162,#121163,#121164,
#121165,#121166,#121167,#121168,#121169,#121170,#121171,#121172,#121173,
#121174,#121175,#121176,#121177,#121178,#121179,#121180,#121181,#121182,
#121183,#121184,#121185,#121186,#121187,#121188,#121189,#121190,#121191,
#121192,#121193,#121194,#121195,#121196,#121197,#121198,#121199,#121200,
#121201,#121202,#121203,#121204,#121205,#121206,#121207,#121208,#121209,
#121210,#121211,#121212,#121213,#121214,#121215,#121216,#121217,#121218,
#121219,#121220,#121221,#121222,#121223,#121224,#121225,#121226,#121227,
#121228,#121229,#121230,#121231,#121232,#121233,#121234,#121235,#121236,
#121237,#121238,#121239,#121240,#121241,#121242,#121243,#121244,#121245,
#121246,#121247,#121248,#121249,#121250,#121251,#121252,#121253,#121254,
#121255,#121256,#121257,#121258,#121259,#121260,#121261,#121262,#121263,
#121264,#121265,#121266,#121267,#121268,#121269,#121270,#121271,#121272,
#121273,#121274,#121275,#121276,#121277,#121278,#121279,#121280),
 .UNSPECIFIED.,.F.,.F.,(4,3,3,3,3,3,3,3,3,3,3,3,3,3,3,3,3,3,3,3,3,3,3,3,
3,3,3,3,3,3,3,3,3,3,3,3,3,3,3,3,3,3,3,3,3,3,3,3,3,3,3,3,3,3,3,3,3,3,3,3,
3,3,3,3,3,3,3,3,3,3,3,3,3,4),(1429.42465738335,1429.51184693731,1429.59914373417,
1429.6866395601,1429.77423939675,1429.86203908662,1429.93053011124,1430.01426882309,
1430.09790433445,1430.18145677785,1430.2649462137,1430.34840016431,1430.43183665816,
1430.51527376791,1430.59872956283,1430.68227405556,1430.7658631385,1430.84958640606,
1430.93026612196,1431.01400483381,1431.09764034517,1431.18119278857,1431.26468222442,
1431.34813617504,1431.43157266888,1431.51500977864,1431.59846557356,1431.68201006629,
1431.76559914923,1431.84932241678,1431.93000213268,1432.01374084453,1432.09737635589,
1432.18092879929,1432.26441823514,1432.34787218576,1432.4313086796,1432.51474578936,
1432.59820158428,1432.68174607701,1432.76533515995,1432.84905842751,1432.9297381434,
1433.01347685525,1433.09711236661,1433.18066481001,1433.26415424586,1433.34760819648,
1433.43104469032,1433.51448180008,1433.597937595,1433.68148208772,1433.76507117067,
1433.84879443822,1433.92947415412,1434.01321286597,1434.09684837733,1434.18040082073,
1434.26389025658,1434.3473442072,1434.43078070104,1434.5142178108,1434.59767360572,
1434.68121809845,1434.76480718139,1434.84853044895,1434.92921016484,1435.01180452316,
1435.09430200276,1435.17672175617,1435.25907889747,1435.34139995451,1435.42371181849,
1435.45634400191),.UNSPECIFIED.);
#960=B_SPLINE_CURVE_WITH_KNOTS('',3,(#121281,#121282,#121283,#121284,#121285,
#121286,#121287,#121288,#121289,#121290),.UNSPECIFIED.,.F.,.F.,(4,3,3,4),
(1429.17433711171,1429.26217368456,1429.3498375818,1429.42465738322),
 .UNSPECIFIED.);
#961=B_SPLINE_CURVE_WITH_KNOTS('',3,(#121292,#121293,#121294,#121295,#121296,
#121297,#121298,#121299,#121300,#121301),.UNSPECIFIED.,.F.,.F.,(4,3,3,4),
(1429.17325060202,1429.24108472023,1429.36688712493,1429.42465738335),
 .UNSPECIFIED.);
#962=B_SPLINE_CURVE_WITH_KNOTS('',3,(#121302,#121303,#121304,#121305,#121306,
#121307,#121308,#121309,#121310,#121311,#121312,#121313,#121314,#121315,
#121316,#121317,#121318,#121319,#121320,#121321,#121322,#121323,#121324,
#121325,#121326,#121327,#121328,#121329,#121330,#121331,#121332,#121333,
#121334,#121335,#121336,#121337,#121338,#121339,#121340,#121341,#121342,
#121343,#121344,#121345,#121346,#121347,#121348,#121349,#121350,#121351,
#121352,#121353,#121354,#121355,#121356,#121357,#121358,#121359,#121360,
#121361,#121362,#121363,#121364,#121365,#121366,#121367,#121368,#121369,
#121370,#121371,#121372,#121373,#121374,#121375,#121376,#121377,#121378,
#121379,#121380,#121381,#121382,#121383,#121384,#121385,#121386,#121387,
#121388,#121389,#121390,#121391,#121392,#121393,#121394,#121395,#121396,
#121397,#121398,#121399,#121400,#121401,#121402,#121403,#121404,#121405,
#121406,#121407,#121408,#121409,#121410,#121411,#121412,#121413,#121414,
#121415,#121416,#121417,#121418,#121419,#121420,#121421,#121422,#121423,
#121424,#121425,#121426,#121427,#121428,#121429,#121430,#121431,#121432,
#121433,#121434,#121435,#121436,#121437,#121438,#121439,#121440,#121441,
#121442,#121443,#121444,#121445,#121446,#121447,#121448,#121449,#121450,
#121451,#121452,#121453,#121454,#121455,#121456,#121457,#121458,#121459,
#121460,#121461,#121462,#121463,#121464,#121465,#121466,#121467,#121468,
#121469,#121470,#121471,#121472,#121473,#121474,#121475,#121476,#121477,
#121478,#121479,#121480,#121481,#121482,#121483,#121484,#121485,#121486,
#121487,#121488,#121489,#121490,#121491,#121492,#121493,#121494,#121495,
#121496,#121497,#121498,#121499,#121500,#121501,#121502,#121503,#121504,
#121505,#121506,#121507,#121508,#121509,#121510,#121511,#121512,#121513,
#121514,#121515,#121516,#121517,#121518,#121519,#121520,#121521),
 .UNSPECIFIED.,.F.,.F.,(4,3,3,3,3,3,3,3,3,3,3,3,3,3,3,3,3,3,3,3,3,3,3,3,
3,3,3,3,3,3,3,3,3,3,3,3,3,3,3,3,3,3,3,3,3,3,3,3,3,3,3,3,3,3,3,3,3,3,3,3,
3,3,3,3,3,3,3,3,3,3,3,3,3,4),(1429.4246573835,1429.50702048783,1429.58931001852,
1429.67155095664,1429.75376682562,1429.83597666066,1429.91819948982,1430.0005042299,
1430.08285026655,1430.16532564741,1430.24082073095,1430.3245594428,1430.40819495416,
1430.49174739756,1430.57523683341,1430.65869078403,1430.74212727787,1430.82556438763,
1430.90902018255,1430.99256467528,1431.07615375822,1431.15987702578,1431.24055674167,
1431.32429545352,1431.40793096488,1431.49148340828,1431.57497284413,1431.65842679475,
1431.74186328859,1431.82530039835,1431.90875619327,1431.992300686,1432.07588976894,
1432.1596130365,1432.24029275239,1432.32403146424,1432.4076669756,1432.491219419,
1432.57470885485,1432.65816280547,1432.74159929931,1432.82503640907,1432.90849220399,
1432.99203669672,1433.07562577966,1433.15934904721,1433.24002876311,1433.32376747496,
1433.40740298632,1433.49095542972,1433.57444486557,1433.65789881619,1433.74133531003,
1433.82477241979,1433.90822821471,1433.99177270744,1434.07536179038,1434.15908505794,
1434.23976477383,1434.32350348568,1434.40713899704,1434.49069144044,1434.57418087629,
1434.6576348269,1434.74107132075,1434.8245084305,1434.90796422542,1434.99150871815,
1435.07509780109,1435.15882106865,1435.23950078455,1435.32891254343,1435.41810836263,
1435.45754054782),.UNSPECIFIED.);
#963=B_SPLINE_CURVE_WITH_KNOTS('',3,(#121527,#121528,#121529,#121530,#121531,
#121532,#121533,#121534,#121535,#121536,#121537,#121538,#121539,#121540,
#121541,#121542,#121543,#121544,#121545,#121546,#121547,#121548,#121549,
#121550,#121551,#121552,#121553,#121554,#121555,#121556,#121557,#121558,
#121559,#121560,#121561,#121562,#121563,#121564,#121565,#121566,#121567,
#121568,#121569,#121570,#121571,#121572,#121573,#121574,#121575,#121576,
#121577,#121578,#121579,#121580,#121581,#121582,#121583,#121584,#121585,
#121586,#121587,#121588,#121589,#121590,#121591,#121592,#121593,#121594,
#121595,#121596,#121597,#121598,#121599,#121600,#121601,#121602,#121603,
#121604,#121605,#121606,#121607,#121608,#121609,#121610,#121611,#121612,
#121613,#121614,#121615,#121616,#121617,#121618,#121619,#121620,#121621,
#121622,#121623,#121624,#121625,#121626,#121627,#121628,#121629,#121630,
#121631,#121632,#121633,#121634,#121635,#121636,#121637,#121638,#121639,
#121640,#121641,#121642,#121643,#121644,#121645,#121646,#121647,#121648,
#121649,#121650,#121651,#121652,#121653,#121654,#121655,#121656,#121657,
#121658,#121659,#121660,#121661,#121662,#121663,#121664,#121665,#121666,
#121667,#121668,#121669,#121670,#121671,#121672,#121673,#121674,#121675,
#121676,#121677,#121678,#121679,#121680,#121681,#121682,#121683,#121684,
#121685,#121686,#121687,#121688,#121689,#121690,#121691,#121692,#121693,
#121694,#121695,#121696,#121697,#121698,#121699,#121700,#121701,#121702,
#121703,#121704,#121705,#121706,#121707,#121708,#121709,#121710,#121711,
#121712,#121713,#121714,#121715,#121716,#121717,#121718,#121719,#121720,
#121721,#121722,#121723,#121724,#121725,#121726,#121727,#121728,#121729,
#121730,#121731,#121732,#121733,#121734,#121735,#121736,#121737,#121738,
#121739,#121740,#121741,#121742,#121743),.UNSPECIFIED.,.F.,.F.,(4,3,3,3,
3,3,3,3,3,3,3,3,3,3,3,3,3,3,3,3,3,3,3,3,3,3,3,3,3,3,3,3,3,3,3,3,3,3,3,3,
3,3,3,3,3,3,3,3,3,3,3,3,3,3,3,3,3,3,3,3,3,3,3,3,3,3,3,3,3,3,3,3,4),(1435.70784269053,
1435.82235604207,1435.92894617556,1436.01268488741,1436.09632039877,1436.17987284217,
1436.26336227802,1436.34681622863,1436.43025272248,1436.51368983223,1436.59714562715,
1436.68069011988,1436.76427920282,1436.84800247038,1436.92868218628,1437.01242089813,
1437.09605640949,1437.17960885289,1437.26309828874,1437.34655223936,1437.4299887332,
1437.51342584296,1437.59688163788,1437.68042613061,1437.76401521355,1437.8477384811,
1437.928418197,1438.01215690885,1438.09579242021,1438.17934486361,1438.26283429946,
1438.34628825008,1438.42972474392,1438.51316185368,1438.5966176486,1438.68016214133,
1438.76375122427,1438.84747449183,1438.92815420772,1439.01189291957,1439.09552843093,
1439.17908087433,1439.26257031018,1439.3460242608,1439.42946075464,1439.5128978644,
1439.59635365932,1439.67989815205,1439.76348723499,1439.84721050254,1439.92789021844,
1440.01162893029,1440.09526444165,1440.17881688505,1440.2623063209,1440.34576027152,
1440.42919676536,1440.51263387512,1440.59608967004,1440.67963416277,1440.76322324571,
1440.84694651326,1440.92762622916,1441.01137625723,1441.09502060469,1441.17856410501,
1441.26205042852,1441.34549769506,1441.42892399429,1441.51237342932,1441.59583358817,
1441.67936222842,1441.73936764326),.UNSPECIFIED.);
#964=B_SPLINE_CURVE_WITH_KNOTS('',3,(#121744,#121745,#121746,#121747,#121748,
#121749,#121750,#121751,#121752,#121753),.UNSPECIFIED.,.F.,.F.,(4,3,3,4),
(1435.45634400191,1435.53868546224,1435.62326407632,1435.70784269039),
 .UNSPECIFIED.);
#965=B_SPLINE_CURVE_WITH_KNOTS('',3,(#121755,#121756,#121757,#121758,#121759,
#121760,#121761,#121762,#121763,#121764),.UNSPECIFIED.,.F.,.F.,(4,3,3,4),
(1435.45754054782,1435.54645941689,1435.63515374008,1435.7078426904),
 .UNSPECIFIED.);
#966=B_SPLINE_CURVE_WITH_KNOTS('',3,(#121765,#121766,#121767,#121768,#121769,
#121770,#121771,#121772,#121773,#121774,#121775,#121776,#121777,#121778,
#121779,#121780,#121781,#121782,#121783,#121784,#121785,#121786,#121787,
#121788,#121789,#121790,#121791,#121792,#121793,#121794,#121795,#121796,
#121797,#121798,#121799,#121800,#121801,#121802,#121803,#121804,#121805,
#121806,#121807,#121808,#121809,#121810,#121811,#121812,#121813,#121814,
#121815,#121816,#121817,#121818,#121819,#121820,#121821,#121822,#121823,
#121824,#121825,#121826,#121827,#121828,#121829,#121830,#121831,#121832,
#121833,#121834,#121835,#121836,#121837,#121838,#121839,#121840,#121841,
#121842,#121843,#121844,#121845,#121846,#121847,#121848,#121849,#121850,
#121851,#121852,#121853,#121854,#121855,#121856,#121857,#121858,#121859,
#121860,#121861,#121862,#121863,#121864,#121865,#121866,#121867,#121868,
#121869,#121870,#121871,#121872,#121873,#121874,#121875,#121876,#121877,
#121878,#121879,#121880,#121881,#121882,#121883,#121884,#121885,#121886,
#121887,#121888,#121889,#121890,#121891,#121892,#121893,#121894,#121895,
#121896,#121897,#121898,#121899,#121900,#121901,#121902,#121903,#121904,
#121905,#121906,#121907,#121908,#121909,#121910,#121911,#121912,#121913,
#121914,#121915,#121916,#121917,#121918,#121919,#121920,#121921,#121922,
#121923,#121924,#121925,#121926,#121927,#121928,#121929,#121930,#121931,
#121932,#121933,#121934,#121935,#121936,#121937,#121938,#121939,#121940,
#121941,#121942,#121943,#121944,#121945,#121946,#121947,#121948,#121949,
#121950,#121951,#121952,#121953,#121954,#121955,#121956,#121957,#121958,
#121959,#121960,#121961,#121962,#121963,#121964,#121965,#121966,#121967,
#121968,#121969,#121970,#121971,#121972,#121973,#121974,#121975,#121976,
#121977,#121978,#121979,#121980,#121981),.UNSPECIFIED.,.F.,.F.,(4,3,3,3,
3,3,3,3,3,3,3,3,3,3,3,3,3,3,3,3,3,3,3,3,3,3,3,3,3,3,3,3,3,3,3,3,3,3,3,3,
3,3,3,3,3,3,3,3,3,3,3,3,3,3,3,3,3,3,3,3,3,3,3,3,3,3,3,3,3,3,3,3,4),(1435.70784269053,
1435.79418909534,1435.8806134886,1435.97026931526,1436.05695086,1436.14809382764,
1436.23923679527,1436.32297550712,1436.40661101849,1436.49016346189,1436.57365289774,
1436.65710684835,1436.7405433422,1436.82398045196,1436.90743624688,1436.99098073961,
1437.07456982255,1437.15829309011,1437.23897280599,1437.32271151783,1437.4063470292,
1437.4898994726,1437.57338890845,1437.65684285906,1437.74027935291,1437.82371646266,
1437.90717225758,1437.99071675031,1438.07430583325,1438.15802910081,1438.23870881671,
1438.32244752856,1438.40608303993,1438.48963548333,1438.57312491918,1438.6565788698,
1438.74001536364,1438.8234524734,1438.90690826832,1438.99045276105,1439.07404184399,
1439.15776511155,1439.23844482744,1439.32218353929,1439.40581905065,1439.48937149405,
1439.57286092991,1439.65631488052,1439.73975137437,1439.82318848412,1439.90664427904,
1439.99018877177,1440.07377785471,1440.15750112227,1440.23818083816,1440.32191955001,
1440.40555506137,1440.48910750477,1440.57259694062,1440.65605089123,1440.73948738508,
1440.82292449483,1440.90638028975,1440.98992478248,1441.07351386542,1441.15723713298,
1441.23791684888,1441.32066010468,1441.40330528578,1441.48739106607,1441.56989035993,
1441.65476938343,1441.73964840693),.UNSPECIFIED.);
#967=B_SPLINE_CURVE_WITH_KNOTS('',3,(#121987,#121988,#121989,#121990,#121991,
#121992,#121993,#121994,#121995,#121996,#121997,#121998,#121999,#122000,
#122001,#122002,#122003,#122004,#122005,#122006,#122007,#122008,#122009,
#122010,#122011,#122012,#122013,#122014,#122015,#122016,#122017,#122018,
#122019,#122020,#122021,#122022,#122023,#122024,#122025,#122026,#122027,
#122028,#122029,#122030,#122031,#122032,#122033,#122034,#122035,#122036,
#122037,#122038,#122039,#122040,#122041,#122042,#122043,#122044,#122045,
#122046,#122047,#122048,#122049,#122050,#122051,#122052,#122053,#122054,
#122055,#122056,#122057,#122058,#122059,#122060,#122061,#122062,#122063,
#122064,#122065,#122066,#122067,#122068,#122069,#122070,#122071,#122072,
#122073,#122074,#122075,#122076,#122077,#122078,#122079,#122080,#122081,
#122082,#122083,#122084,#122085,#122086,#122087,#122088,#122089,#122090,
#122091,#122092,#122093,#122094,#122095,#122096,#122097,#122098,#122099,
#122100,#122101,#122102,#122103,#122104,#122105,#122106,#122107,#122108,
#122109,#122110,#122111,#122112,#122113,#122114,#122115,#122116,#122117,
#122118,#122119,#122120,#122121,#122122,#122123,#122124,#122125,#122126,
#122127,#122128,#122129,#122130,#122131,#122132,#122133,#122134,#122135,
#122136,#122137,#122138,#122139,#122140,#122141,#122142,#122143,#122144,
#122145,#122146,#122147,#122148,#122149,#122150,#122151,#122152,#122153,
#122154,#122155,#122156,#122157,#122158,#122159,#122160,#122161,#122162,
#122163,#122164,#122165,#122166,#122167,#122168,#122169,#122170,#122171,
#122172,#122173,#122174,#122175,#122176,#122177,#122178,#122179,#122180,
#122181,#122182,#122183,#122184,#122185,#122186,#122187,#122188,#122189,
#122190,#122191,#122192,#122193,#122194,#122195,#122196,#122197,#122198,
#122199,#122200,#122201,#122202,#122203,#122204,#122205,#122206),
 .UNSPECIFIED.,.F.,.F.,(4,3,3,3,3,3,3,3,3,3,3,3,3,3,3,3,3,3,3,3,3,3,3,3,
3,3,3,3,3,3,3,3,3,3,3,3,3,3,3,3,3,3,3,3,3,3,3,3,3,3,3,3,3,3,3,3,3,3,3,3,
3,3,3,3,3,3,3,3,3,3,3,3,3,4),(1441.99102799783,1442.07397001655,1442.15681366223,
1442.23957978767,1442.32551959554,1442.40820144904,1442.49087354865,1442.5735546158,
1442.65626337548,1442.73906287441,1442.82191629707,1442.90488611973,1442.9270982506,
1443.01083696245,1443.09447247381,1443.17802491721,1443.26151435306,1443.34496830368,
1443.42840479752,1443.51184190728,1443.5952977022,1443.67884219493,1443.76243127787,
1443.84615454542,1443.92683426132,1444.01057297317,1444.09420848453,1444.17776092793,
1444.26125036378,1444.3447043144,1444.42814080824,1444.511577918,1444.59503371292,
1444.67857820565,1444.76216728859,1444.84589055615,1444.92657027204,1445.01030898389,
1445.09394449525,1445.17749693865,1445.2609863745,1445.34444032512,1445.42787681896,
1445.51131392872,1445.59476972363,1445.67831421636,1445.7619032993,1445.84562656686,
1445.92630628276,1446.01004499461,1446.09368050597,1446.17723294937,1446.26072238522,
1446.34417633584,1446.42761282968,1446.51104993944,1446.59450573436,1446.67805022709,
1446.76163931003,1446.84536257758,1446.92604229348,1447.00978100533,1447.09341651669,
1447.17696896009,1447.26045839594,1447.34391234655,1447.4273488404,1447.51078595016,
1447.59424174507,1447.6777862378,1447.76137532074,1447.8450985883,1447.9257783042,
1448.0236730871),.UNSPECIFIED.);
#968=B_SPLINE_CURVE_WITH_KNOTS('',3,(#122207,#122208,#122209,#122210,#122211,
#122212,#122213,#122214,#122215,#122216,#122217,#122218,#122219),
 .UNSPECIFIED.,.F.,.F.,(4,3,3,3,4),(1441.73936764326,1441.82299876243,1441.9067473108,
1441.92736223988,1441.99102799771),.UNSPECIFIED.);
#969=B_SPLINE_CURVE_WITH_KNOTS('',3,(#122221,#122222,#122223,#122224,#122225,
#122226,#122227,#122228,#122229,#122230),.UNSPECIFIED.,.F.,.F.,(4,3,3,4),
(1441.73964840693,1441.82211908339,1441.90657354055,1441.99102799771),
 .UNSPECIFIED.);
#970=B_SPLINE_CURVE_WITH_KNOTS('',3,(#122231,#122232,#122233,#122234,#122235,
#122236,#122237,#122238,#122239,#122240,#122241,#122242,#122243,#122244,
#122245,#122246,#122247,#122248,#122249,#122250,#122251,#122252,#122253,
#122254,#122255,#122256,#122257,#122258,#122259,#122260,#122261,#122262,
#122263,#122264,#122265,#122266,#122267,#122268,#122269,#122270,#122271,
#122272,#122273,#122274,#122275,#122276,#122277,#122278,#122279,#122280,
#122281,#122282,#122283,#122284,#122285,#122286,#122287,#122288,#122289,
#122290,#122291,#122292,#122293,#122294,#122295,#122296,#122297,#122298,
#122299,#122300,#122301,#122302,#122303,#122304,#122305,#122306,#122307,
#122308,#122309,#122310,#122311,#122312,#122313,#122314,#122315,#122316,
#122317,#122318,#122319,#122320,#122321,#122322,#122323,#122324,#122325,
#122326,#122327,#122328,#122329,#122330,#122331,#122332,#122333,#122334,
#122335,#122336,#122337,#122338,#122339,#122340,#122341,#122342,#122343,
#122344,#122345,#122346,#122347,#122348,#122349,#122350,#122351,#122352,
#122353,#122354,#122355,#122356,#122357,#122358,#122359,#122360,#122361,
#122362,#122363,#122364,#122365,#122366,#122367,#122368,#122369,#122370,
#122371,#122372,#122373,#122374,#122375,#122376,#122377,#122378,#122379,
#122380,#122381,#122382,#122383,#122384,#122385,#122386,#122387,#122388,
#122389,#122390,#122391,#122392,#122393,#122394,#122395,#122396,#122397,
#122398,#122399,#122400,#122401,#122402,#122403,#122404,#122405,#122406,
#122407,#122408,#122409,#122410,#122411,#122412,#122413,#122414,#122415,
#122416,#122417,#122418,#122419,#122420,#122421,#122422,#122423,#122424,
#122425,#122426,#122427,#122428,#122429,#122430,#122431,#122432,#122433,
#122434,#122435,#122436,#122437,#122438,#122439,#122440,#122441,#122442,
#122443,#122444,#122445,#122446,#122447,#122448,#122449,#122450),
 .UNSPECIFIED.,.F.,.F.,(4,3,3,3,3,3,3,3,3,3,3,3,3,3,3,3,3,3,3,3,3,3,3,3,
3,3,3,3,3,3,3,3,3,3,3,3,3,3,3,3,3,3,3,3,3,3,3,3,3,3,3,3,3,3,3,3,3,3,3,3,
3,3,3,3,3,3,3,3,3,3,3,3,3,4),(1441.99102799785,1442.09882248263,1442.20915371554,
1442.2376528596,1442.32139157145,1442.40502708281,1442.48857952621,1442.57206896206,
1442.65552291267,1442.73895940652,1442.82239651628,1442.90585231119,1442.98939680392,
1443.07298588686,1443.15670915442,1443.23738887032,1443.32112758217,1443.40476309353,
1443.48831553693,1443.57180497278,1443.6552589234,1443.73869541724,1443.822132527,
1443.90558832192,1443.98913281465,1444.07272189759,1444.15644516514,1444.23712488104,
1444.32086359289,1444.40449910425,1444.48805154765,1444.5715409835,1444.65499493412,
1444.73843142796,1444.82186853772,1444.90532433264,1444.98886882536,1445.07245790831,
1445.15618117586,1445.23686089176,1445.32059960361,1445.40423511497,1445.48778755837,
1445.57127699422,1445.65473094484,1445.73816743868,1445.82160454844,1445.90506034336,
1445.98860483609,1446.07219391903,1446.15591718658,1446.23659690248,1446.32033561433,
1446.40397112569,1446.48752356909,1446.57101300494,1446.65446695556,1446.7379034494,
1446.82134055916,1446.90479635408,1446.98834084681,1447.07192992975,1447.1556531973,
1447.2363329132,1447.32008459951,1447.40789239756,1447.49143313082,1447.57491711298,
1447.65836246294,1447.74178726958,1447.82523138041,1447.90868683001,1447.99219954226,
1448.02254698393),.UNSPECIFIED.);
#971=B_SPLINE_CURVE_WITH_KNOTS('',3,(#122456,#122457,#122458,#122459,#122460,
#122461,#122462,#122463,#122464,#122465,#122466,#122467,#122468,#122469,
#122470,#122471,#122472,#122473,#122474,#122475,#122476,#122477,#122478,
#122479,#122480,#122481,#122482,#122483,#122484,#122485,#122486,#122487,
#122488,#122489,#122490,#122491,#122492,#122493,#122494,#122495,#122496,
#122497,#122498,#122499,#122500,#122501,#122502,#122503,#122504,#122505,
#122506,#122507,#122508,#122509,#122510,#122511,#122512,#122513,#122514,
#122515,#122516,#122517,#122518,#122519,#122520,#122521,#122522,#122523,
#122524,#122525,#122526,#122527,#122528,#122529,#122530,#122531,#122532,
#122533,#122534,#122535,#122536,#122537,#122538,#122539,#122540,#122541,
#122542,#122543,#122544,#122545,#122546,#122547,#122548,#122549,#122550,
#122551,#122552,#122553,#122554,#122555,#122556,#122557,#122558,#122559,
#122560,#122561,#122562,#122563,#122564,#122565,#122566,#122567,#122568,
#122569,#122570,#122571,#122572,#122573,#122574,#122575,#122576,#122577,
#122578,#122579,#122580,#122581,#122582,#122583,#122584,#122585,#122586,
#122587,#122588,#122589,#122590,#122591,#122592,#122593,#122594,#122595,
#122596,#122597,#122598,#122599,#122600,#122601,#122602,#122603,#122604,
#122605,#122606,#122607,#122608,#122609,#122610,#122611,#122612,#122613,
#122614,#122615,#122616,#122617,#122618,#122619,#122620,#122621,#122622,
#122623,#122624,#122625,#122626,#122627,#122628,#122629,#122630,#122631,
#122632,#122633,#122634,#122635,#122636,#122637,#122638,#122639,#122640,
#122641,#122642,#122643,#122644,#122645,#122646,#122647,#122648,#122649,
#122650,#122651,#122652,#122653,#122654,#122655,#122656,#122657,#122658,
#122659,#122660,#122661,#122662,#122663,#122664,#122665,#122666,#122667,
#122668,#122669,#122670,#122671,#122672,#122673,#122674,#122675),
 .UNSPECIFIED.,.F.,.F.,(4,3,3,3,3,3,3,3,3,3,3,3,3,3,3,3,3,3,3,3,3,3,3,3,
3,3,3,3,3,3,3,3,3,3,3,3,3,3,3,3,3,3,3,3,3,3,3,3,3,3,3,3,3,3,3,3,3,3,3,3,
3,3,3,3,3,3,3,3,3,3,3,3,3,4),(1448.27421330489,1448.35782433656,1448.44142899155,
1448.52504506398,1448.60869035153,1448.69243622458,1448.77623540817,1448.8601726709,
1448.92551431492,1449.00925302677,1449.09288853813,1449.17644098153,1449.25993041738,
1449.343384368,1449.42682086184,1449.5102579716,1449.59371376652,1449.67725825924,
1449.76084734219,1449.84457060974,1449.92525032564,1450.00898903749,1450.09262454885,
1450.17617699225,1450.2596664281,1450.34312037872,1450.42655687256,1450.50999398232,
1450.59344977724,1450.67699426997,1450.76058335291,1450.84430662046,1450.92498633636,
1451.00872504821,1451.09236055957,1451.17591300297,1451.25940243882,1451.34285638944,
1451.42629288328,1451.50972999304,1451.59318578796,1451.67673028069,1451.76031936363,
1451.84404263118,1451.92472234708,1452.00846105893,1452.09209657029,1452.17564901369,
1452.25913844954,1452.34259240016,1452.426028894,1452.50946600376,1452.59292179867,
1452.6764662914,1452.76005537434,1452.8437786419,1452.9244583578,1453.00819706965,
1453.09183258101,1453.17538502441,1453.25887446026,1453.34232841088,1453.42576490472,
1453.50920201448,1453.5926578094,1453.67620230213,1453.75979138507,1453.84351465263,
1453.92419436852,1454.00848723102,1454.09263873748,1454.17670875473,1454.26070005874,
1454.30662927058),.UNSPECIFIED.);
#972=B_SPLINE_CURVE_WITH_KNOTS('',3,(#122676,#122677,#122678,#122679,#122680,
#122681,#122682,#122683,#122684,#122685),.UNSPECIFIED.,.F.,.F.,(4,3,3,4),
(1448.0236730871,1448.12028229969,1448.21615954937,1448.27421330469),
 .UNSPECIFIED.);
#973=B_SPLINE_CURVE_WITH_KNOTS('',3,(#122687,#122688,#122689,#122690,#122691,
#122692,#122693,#122694,#122695,#122696,#122697,#122698,#122699),
 .UNSPECIFIED.,.F.,.F.,(4,3,3,3,4),(1448.02254698393,1448.10615919498,1448.18989572745,
1448.23606892392,1448.27421330489),.UNSPECIFIED.);
#974=B_SPLINE_CURVE_WITH_KNOTS('',3,(#122700,#122701,#122702,#122703,#122704,
#122705,#122706,#122707,#122708,#122709,#122710,#122711,#122712,#122713,
#122714,#122715,#122716,#122717,#122718,#122719,#122720,#122721,#122722,
#122723,#122724,#122725,#122726,#122727,#122728,#122729,#122730,#122731,
#122732,#122733,#122734,#122735,#122736,#122737,#122738,#122739,#122740,
#122741,#122742,#122743,#122744,#122745,#122746,#122747,#122748,#122749,
#122750,#122751,#122752,#122753,#122754,#122755,#122756,#122757,#122758,
#122759,#122760,#122761,#122762,#122763,#122764,#122765,#122766,#122767,
#122768,#122769,#122770,#122771,#122772,#122773,#122774,#122775,#122776,
#122777,#122778,#122779,#122780,#122781,#122782,#122783,#122784,#122785,
#122786,#122787,#122788,#122789,#122790,#122791,#122792,#122793,#122794,
#122795,#122796,#122797,#122798,#122799,#122800,#122801,#122802,#122803,
#122804,#122805,#122806,#122807,#122808,#122809,#122810,#122811,#122812,
#122813,#122814,#122815,#122816,#122817,#122818,#122819,#122820,#122821,
#122822,#122823,#122824,#122825,#122826,#122827,#122828,#122829,#122830,
#122831,#122832,#122833,#122834,#122835,#122836,#122837,#122838,#122839,
#122840,#122841,#122842,#122843,#122844,#122845,#122846,#122847,#122848,
#122849,#122850,#122851,#122852,#122853,#122854,#122855,#122856,#122857,
#122858,#122859,#122860,#122861,#122862,#122863,#122864,#122865,#122866,
#122867,#122868,#122869,#122870,#122871,#122872,#122873,#122874,#122875,
#122876,#122877,#122878,#122879,#122880,#122881,#122882,#122883,#122884,
#122885,#122886,#122887,#122888,#122889,#122890,#122891,#122892,#122893,
#122894,#122895,#122896,#122897,#122898,#122899,#122900,#122901,#122902,
#122903,#122904,#122905,#122906,#122907,#122908,#122909,#122910,#122911,
#122912,#122913,#122914,#122915,#122916,#122917,#122918,#122919),
 .UNSPECIFIED.,.F.,.F.,(4,3,3,3,3,3,3,3,3,3,3,3,3,3,3,3,3,3,3,3,3,3,3,3,
3,3,3,3,3,3,3,3,3,3,3,3,3,3,3,3,3,3,3,3,3,3,3,3,3,3,3,3,3,3,3,3,3,3,3,3,
3,3,3,3,3,3,3,3,3,3,3,3,3,4),(1448.27421330505,1448.35743318097,1448.4405518179,
1448.52358985075,1448.60656783825,1448.68951465084,1448.77244760275,1448.85538521634,
1448.93834601377,1449.02139624031,1449.10449595701,1449.18771960852,1449.23580493464,
1449.31954364649,1449.40317915785,1449.48673160125,1449.5702210371,1449.65367498772,
1449.73711148156,1449.82054859132,1449.90400438624,1449.98754887897,1450.07113796191,
1450.15486122947,1450.23554094536,1450.31927965721,1450.40291516857,1450.48646761197,
1450.56995704782,1450.65341099844,1450.73684749228,1450.82028460204,1450.90374039696,
1450.98728488969,1451.07087397263,1451.15459724018,1451.23527695608,1451.31901566793,
1451.40265117929,1451.48620362269,1451.56969305854,1451.65314700916,1451.736583503,
1451.82002061276,1451.90347640768,1451.98702090041,1452.07060998335,1452.1543332509,
1452.2350129668,1452.31875167865,1452.40238719001,1452.48593963341,1452.56942906926,
1452.65288301988,1452.73631951372,1452.81975662348,1452.9032124184,1452.98675691113,
1453.07034599407,1453.15406926163,1453.23474897752,1453.31848768937,1453.40212320073,
1453.48567564413,1453.56916507998,1453.6526190306,1453.73605552444,1453.8194926342,
1453.90294842912,1453.98649292185,1454.07008200479,1454.15380527234,1454.23448498824,
1454.30674307549),.UNSPECIFIED.);
#975=B_SPLINE_CURVE_WITH_KNOTS('',3,(#122925,#122926,#122927,#122928,#122929,
#122930,#122931,#122932,#122933,#122934,#122935,#122936,#122937,#122938,
#122939,#122940,#122941,#122942,#122943,#122944,#122945,#122946,#122947,
#122948,#122949,#122950,#122951,#122952,#122953,#122954,#122955,#122956,
#122957,#122958,#122959,#122960,#122961,#122962,#122963,#122964,#122965,
#122966,#122967,#122968,#122969,#122970,#122971,#122972,#122973,#122974,
#122975,#122976,#122977,#122978,#122979,#122980,#122981,#122982,#122983,
#122984,#122985,#122986,#122987,#122988,#122989,#122990,#122991,#122992,
#122993,#122994,#122995,#122996,#122997,#122998,#122999,#123000,#123001,
#123002,#123003,#123004,#123005,#123006,#123007,#123008,#123009,#123010,
#123011,#123012,#123013,#123014,#123015,#123016,#123017,#123018,#123019,
#123020,#123021,#123022,#123023,#123024,#123025,#123026,#123027,#123028,
#123029,#123030,#123031,#123032,#123033,#123034,#123035,#123036,#123037,
#123038,#123039,#123040,#123041,#123042,#123043,#123044,#123045,#123046,
#123047,#123048,#123049,#123050,#123051,#123052,#123053,#123054,#123055,
#123056,#123057,#123058,#123059,#123060,#123061,#123062,#123063,#123064,
#123065,#123066,#123067,#123068,#123069,#123070,#123071,#123072,#123073,
#123074,#123075,#123076,#123077,#123078,#123079,#123080,#123081,#123082,
#123083,#123084,#123085,#123086,#123087,#123088,#123089,#123090,#123091,
#123092,#123093,#123094,#123095,#123096,#123097,#123098,#123099,#123100,
#123101,#123102,#123103,#123104,#123105,#123106,#123107,#123108,#123109,
#123110,#123111,#123112,#123113,#123114,#123115,#123116,#123117,#123118,
#123119,#123120,#123121,#123122,#123123,#123124,#123125,#123126,#123127,
#123128,#123129,#123130,#123131,#123132,#123133,#123134,#123135,#123136,
#123137,#123138,#123139,#123140,#123141),.UNSPECIFIED.,.F.,.F.,(4,3,3,3,
3,3,3,3,3,3,3,3,3,3,3,3,3,3,3,3,3,3,3,3,3,3,3,3,3,3,3,3,3,3,3,3,3,3,3,3,
3,3,3,3,3,3,3,3,3,3,3,3,3,3,3,3,3,3,3,3,3,3,3,3,3,3,3,3,3,3,3,3,4),(1454.55739861227,
1454.65194746431,1454.74689204477,1454.84238116431,1454.92393037924,1455.00766909109,
1455.09130460245,1455.17485704585,1455.2583464817,1455.34180043232,1455.42523692616,
1455.50867403592,1455.59212983084,1455.67567432356,1455.75926340651,1455.84298667406,
1455.92366638996,1456.00740510181,1456.09104061317,1456.17459305657,1456.25808249242,
1456.34153644304,1456.42497293688,1456.50841004664,1456.59186584156,1456.67541033429,
1456.75899941723,1456.84272268479,1456.92340240068,1457.00714111253,1457.09077662389,
1457.17432906729,1457.25781850314,1457.34127245376,1457.4247089476,1457.50814605736,
1457.59160185228,1457.67514634501,1457.75873542795,1457.8424586955,1457.9231384114,
1458.00687712325,1458.09051263461,1458.17406507801,1458.25755451386,1458.34100846448,
1458.42444495832,1458.50788206808,1458.591337863,1458.67488235572,1458.75847143867,
1458.84219470622,1458.92287442212,1459.00661313397,1459.09024864533,1459.17380108873,
1459.25729052458,1459.3407444752,1459.42418096904,1459.5076180788,1459.59107387372,
1459.67461836645,1459.75820744939,1459.84193071695,1459.92261043284,1460.00587749695,
1460.08857547718,1460.17119802281,1460.25376406267,1460.33750978343,1460.4200311627,
1460.5043890542,1460.5887469457),.UNSPECIFIED.);
#976=B_SPLINE_CURVE_WITH_KNOTS('',3,(#123142,#123143,#123144,#123145,#123146,
#123147,#123148,#123149,#123150,#123151),.UNSPECIFIED.,.F.,.F.,(4,3,3,4),
(1454.30662927058,1454.3905507352,1454.47446510851,1454.55739861207),
 .UNSPECIFIED.);
#977=B_SPLINE_CURVE_WITH_KNOTS('',3,(#123153,#123154,#123155,#123156,#123157,
#123158,#123159,#123160,#123161,#123162),.UNSPECIFIED.,.F.,.F.,(4,3,3,4),
(1454.30674307549,1454.40585639479,1454.50400867407,1454.55739861189),
 .UNSPECIFIED.);
#978=B_SPLINE_CURVE_WITH_KNOTS('',3,(#123163,#123164,#123165,#123166,#123167,
#123168,#123169,#123170,#123171,#123172,#123173,#123174,#123175,#123176,
#123177,#123178,#123179,#123180,#123181,#123182,#123183,#123184,#123185,
#123186,#123187,#123188,#123189,#123190,#123191,#123192,#123193,#123194,
#123195,#123196,#123197,#123198,#123199,#123200,#123201,#123202,#123203,
#123204,#123205,#123206,#123207,#123208,#123209,#123210,#123211,#123212,
#123213,#123214,#123215,#123216,#123217,#123218,#123219,#123220,#123221,
#123222,#123223,#123224,#123225,#123226,#123227,#123228,#123229,#123230,
#123231,#123232,#123233,#123234,#123235,#123236,#123237,#123238,#123239,
#123240,#123241,#123242,#123243,#123244,#123245,#123246,#123247,#123248,
#123249,#123250,#123251,#123252,#123253,#123254,#123255,#123256,#123257,
#123258,#123259,#123260,#123261,#123262,#123263,#123264,#123265,#123266,
#123267,#123268,#123269,#123270,#123271,#123272,#123273,#123274,#123275,
#123276,#123277,#123278,#123279,#123280,#123281,#123282,#123283,#123284,
#123285,#123286,#123287,#123288,#123289,#123290,#123291,#123292,#123293,
#123294,#123295,#123296,#123297,#123298,#123299,#123300,#123301,#123302,
#123303,#123304,#123305,#123306,#123307,#123308,#123309,#123310,#123311,
#123312,#123313,#123314,#123315,#123316,#123317,#123318,#123319,#123320,
#123321,#123322,#123323,#123324,#123325,#123326,#123327,#123328,#123329,
#123330,#123331,#123332,#123333,#123334,#123335,#123336,#123337,#123338,
#123339,#123340,#123341,#123342,#123343,#123344,#123345,#123346,#123347,
#123348,#123349,#123350,#123351,#123352,#123353,#123354,#123355,#123356,
#123357,#123358,#123359,#123360,#123361,#123362,#123363,#123364,#123365,
#123366,#123367,#123368,#123369,#123370,#123371,#123372,#123373,#123374,
#123375,#123376,#123377,#123378,#123379,#123380,#123381,#123382),
 .UNSPECIFIED.,.F.,.F.,(4,3,3,3,3,3,3,3,3,3,3,3,3,3,3,3,3,3,3,3,3,3,3,3,
3,3,3,3,3,3,3,3,3,3,3,3,3,3,3,3,3,3,3,3,3,3,3,3,3,3,3,3,3,3,3,3,3,3,3,3,
3,3,3,3,3,3,3,3,3,3,3,3,3,4),(1454.55739861207,1454.64200141043,1454.72522978866,
1454.80845873658,1454.89170646772,1454.97733510053,1455.06072123565,1455.1474711173,
1455.23422099896,1455.31795971081,1455.40159522217,1455.48514766557,1455.56863710142,
1455.65209105204,1455.73552754588,1455.81896465564,1455.90242045056,1455.98596494329,
1456.06955402623,1456.15327729378,1456.23395700968,1456.31769572153,1456.40133123289,
1456.48488367629,1456.56837311214,1456.65182706276,1456.7352635566,1456.81870066636,
1456.90215646127,1456.985700954,1457.06929003695,1457.1530133045,1457.2336930204,
1457.31743173225,1457.40106724361,1457.48461968701,1457.56810912286,1457.65156307348,
1457.73499956732,1457.81843667708,1457.901892472,1457.98543696473,1458.06902604767,
1458.15274931522,1458.23342903112,1458.31716774297,1458.40080325433,1458.48435569773,
1458.56784513358,1458.6512990842,1458.73473557804,1458.8181726878,1458.90162848272,
1458.98517297545,1459.06876205839,1459.15248532595,1459.23316504184,1459.31690375369,
1459.40053926505,1459.48409170845,1459.5675811443,1459.65103509492,1459.73447158876,
1459.81790869852,1459.90136449344,1459.98490898617,1460.06849806911,1460.15222133666,
1460.23290105256,1460.32215865567,1460.40683272219,1460.49142158211,1460.57592537746,
1460.58993146501),.UNSPECIFIED.);
#979=B_SPLINE_CURVE_WITH_KNOTS('',3,(#123388,#123389,#123390,#123391,#123392,
#123393,#123394,#123395,#123396,#123397,#123398,#123399,#123400,#123401,
#123402,#123403,#123404,#123405,#123406,#123407,#123408,#123409,#123410,
#123411,#123412,#123413,#123414,#123415,#123416,#123417,#123418,#123419,
#123420,#123421,#123422,#123423,#123424,#123425,#123426,#123427,#123428,
#123429,#123430,#123431,#123432,#123433,#123434,#123435,#123436,#123437,
#123438,#123439,#123440,#123441,#123442,#123443,#123444,#123445,#123446,
#123447,#123448,#123449,#123450,#123451,#123452,#123453,#123454,#123455,
#123456,#123457,#123458,#123459,#123460,#123461,#123462,#123463,#123464,
#123465,#123466,#123467,#123468,#123469,#123470,#123471,#123472,#123473,
#123474,#123475,#123476,#123477,#123478,#123479,#123480,#123481,#123482,
#123483,#123484,#123485,#123486,#123487,#123488,#123489,#123490,#123491,
#123492,#123493,#123494,#123495,#123496,#123497,#123498,#123499,#123500,
#123501,#123502,#123503,#123504,#123505,#123506,#123507,#123508,#123509,
#123510,#123511,#123512,#123513,#123514,#123515,#123516,#123517,#123518,
#123519,#123520,#123521,#123522,#123523,#123524,#123525,#123526,#123527,
#123528,#123529,#123530,#123531,#123532,#123533,#123534,#123535,#123536,
#123537,#123538,#123539,#123540,#123541,#123542,#123543,#123544,#123545,
#123546,#123547,#123548,#123549,#123550,#123551,#123552,#123553,#123554,
#123555,#123556,#123557,#123558,#123559,#123560,#123561,#123562,#123563,
#123564,#123565,#123566,#123567,#123568,#123569,#123570,#123571,#123572,
#123573,#123574,#123575,#123576,#123577,#123578,#123579,#123580,#123581,
#123582,#123583,#123584,#123585,#123586,#123587,#123588,#123589,#123590,
#123591,#123592,#123593,#123594,#123595,#123596,#123597,#123598,#123599,
#123600,#123601,#123602,#123603,#123604,#123605,#123606,#123607),
 .UNSPECIFIED.,.F.,.F.,(4,3,3,3,3,3,3,3,3,3,3,3,3,3,3,3,3,3,3,3,3,3,3,3,
3,3,3,3,3,3,3,3,3,3,3,3,3,3,3,3,3,3,3,3,3,3,3,3,3,3,3,3,3,3,3,3,3,3,3,3,
3,3,3,3,3,3,3,3,3,3,3,3,3,4),(1460.84058391925,1460.92234644356,1461.00608515541,
1461.08972066677,1461.17327311017,1461.25676254602,1461.34021649664,1461.42365299048,
1461.50709010024,1461.59054589516,1461.67409038789,1461.75767947083,1461.84140273838,
1461.92208245428,1462.00582116613,1462.08945667749,1462.17300912089,1462.25649855674,
1462.33995250736,1462.4233890012,1462.50682611096,1462.59028190588,1462.67382639861,
1462.75741548155,1462.84113874911,1462.921818465,1463.00555717685,1463.08919268821,
1463.17274513161,1463.25623456746,1463.33968851808,1463.42312501192,1463.50656212168,
1463.5900179166,1463.67356240933,1463.75715149227,1463.84087475982,1463.92155447572,
1464.00529318757,1464.08892869893,1464.17248114233,1464.25597057818,1464.3394245288,
1464.42286102264,1464.5062981324,1464.58975392732,1464.67329842005,1464.75688750299,
1464.84061077054,1464.92129048644,1465.00502919829,1465.08866470965,1465.17221715305,
1465.2557065889,1465.33916053952,1465.42259703336,1465.50603414312,1465.58948993803,
1465.67303443076,1465.7566235137,1465.84034678126,1465.92102649716,1466.00476796687,
1466.08840559879,1466.17195952814,1466.25952013355,1466.34297044609,1466.42640328248,
1466.50983671436,1466.59328880972,1466.67681791279,1466.76039202568,1466.84407147563,
1466.87244437141),.UNSPECIFIED.);
#980=B_SPLINE_CURVE_WITH_KNOTS('',3,(#123608,#123609,#123610,#123611,#123612,
#123613,#123614,#123615,#123616,#123617),.UNSPECIFIED.,.F.,.F.,(4,3,3,4),
(1460.5887469457,1460.67138214754,1460.75598303333,1460.84058391912),
 .UNSPECIFIED.);
#981=B_SPLINE_CURVE_WITH_KNOTS('',3,(#123619,#123620,#123621,#123622,#123623,
#123624,#123625,#123626,#123627,#123628),.UNSPECIFIED.,.F.,.F.,(4,3,3,4),
(1460.58993146501,1460.67436365968,1460.75876766208,1460.84058391925),
 .UNSPECIFIED.);
#982=B_SPLINE_CURVE_WITH_KNOTS('',3,(#123629,#123630,#123631,#123632,#123633,
#123634,#123635,#123636,#123637,#123638,#123639,#123640,#123641,#123642,
#123643,#123644,#123645,#123646,#123647,#123648,#123649,#123650,#123651,
#123652,#123653,#123654,#123655,#123656,#123657,#123658,#123659,#123660,
#123661,#123662,#123663,#123664,#123665,#123666,#123667,#123668,#123669,
#123670,#123671,#123672,#123673,#123674,#123675,#123676,#123677,#123678,
#123679,#123680,#123681,#123682,#123683,#123684,#123685,#123686,#123687,
#123688,#123689,#123690,#123691,#123692,#123693,#123694,#123695,#123696,
#123697,#123698,#123699,#123700,#123701,#123702,#123703,#123704,#123705,
#123706,#123707,#123708,#123709,#123710,#123711,#123712,#123713,#123714,
#123715,#123716,#123717,#123718,#123719,#123720,#123721,#123722,#123723,
#123724,#123725,#123726,#123727,#123728,#123729,#123730,#123731,#123732,
#123733,#123734,#123735,#123736,#123737,#123738,#123739,#123740,#123741,
#123742,#123743,#123744,#123745,#123746,#123747,#123748,#123749,#123750,
#123751,#123752,#123753,#123754,#123755,#123756,#123757,#123758,#123759,
#123760,#123761,#123762,#123763,#123764,#123765,#123766,#123767,#123768,
#123769,#123770,#123771,#123772,#123773,#123774,#123775,#123776,#123777,
#123778,#123779,#123780,#123781,#123782,#123783,#123784,#123785,#123786,
#123787,#123788,#123789,#123790,#123791,#123792,#123793,#123794,#123795,
#123796,#123797,#123798,#123799,#123800,#123801,#123802,#123803,#123804,
#123805,#123806,#123807,#123808,#123809,#123810,#123811,#123812,#123813,
#123814,#123815,#123816,#123817,#123818,#123819,#123820,#123821,#123822,
#123823,#123824,#123825,#123826,#123827,#123828,#123829,#123830,#123831,
#123832,#123833,#123834,#123835,#123836,#123837,#123838,#123839,#123840,
#123841,#123842,#123843,#123844,#123845,#123846,#123847,#123848),
 .UNSPECIFIED.,.F.,.F.,(4,3,3,3,3,3,3,3,3,3,3,3,3,3,3,3,3,3,3,3,3,3,3,3,
3,3,3,3,3,3,3,3,3,3,3,3,3,3,3,3,3,3,3,3,3,3,3,3,3,3,3,3,3,3,3,3,3,3,3,3,
3,3,3,3,3,3,3,3,3,3,3,3,3,4),(1460.84058391944,1460.93315405195,1461.02625537987,
1461.11963264212,1461.21335570444,1461.23263706328,1461.31637577513,1461.40001128649,
1461.48356372989,1461.56705316574,1461.65050711636,1461.7339436102,1461.81738071996,
1461.90083651488,1461.98438100761,1462.06797009055,1462.1516933581,1462.232373074,
1462.31611178585,1462.39974729721,1462.48329974061,1462.56678917646,1462.65024312708,
1462.73367962092,1462.81711673068,1462.9005725256,1462.98411701832,1463.06770610127,
1463.15142936882,1463.23210908472,1463.31584779657,1463.39948330793,1463.48303575133,
1463.56652518718,1463.6499791378,1463.73341563164,1463.8168527414,1463.90030853632,
1463.98385302905,1464.06744211199,1464.15116537954,1464.23184509544,1464.31558380729,
1464.39921931865,1464.48277176205,1464.5662611979,1464.64971514852,1464.73315164236,
1464.81658875212,1464.90004454704,1464.98358903977,1465.06717812271,1465.15090139026,
1465.23158110616,1465.31531981801,1465.39895532937,1465.48250777277,1465.56599720862,
1465.64945115924,1465.73288765308,1465.81632476284,1465.89978055776,1465.98332505049,
1466.06691413343,1466.15063740098,1466.23131711688,1466.31394700638,1466.39648229565,
1466.47894209376,1466.56134544058,1466.64372069725,1466.72607768958,1466.80846141686,
1466.8719408414),.UNSPECIFIED.);
#983=B_SPLINE_CURVE_WITH_KNOTS('',3,(#123854,#123855,#123856,#123857,#123858,
#123859,#123860,#123861,#123862,#123863,#123864,#123865,#123866,#123867,
#123868,#123869,#123870,#123871,#123872,#123873,#123874,#123875,#123876,
#123877,#123878,#123879,#123880,#123881,#123882,#123883,#123884,#123885,
#123886,#123887,#123888,#123889,#123890,#123891,#123892,#123893,#123894,
#123895,#123896,#123897,#123898,#123899,#123900,#123901,#123902,#123903,
#123904,#123905,#123906,#123907,#123908,#123909,#123910,#123911,#123912,
#123913,#123914,#123915,#123916,#123917,#123918,#123919,#123920,#123921,
#123922,#123923,#123924,#123925,#123926,#123927,#123928,#123929,#123930,
#123931,#123932,#123933,#123934,#123935,#123936,#123937,#123938,#123939,
#123940,#123941,#123942,#123943,#123944,#123945,#123946,#123947,#123948,
#123949,#123950,#123951,#123952,#123953,#123954,#123955,#123956,#123957,
#123958,#123959,#123960,#123961,#123962,#123963,#123964,#123965,#123966,
#123967,#123968,#123969,#123970,#123971,#123972,#123973,#123974,#123975,
#123976,#123977,#123978,#123979,#123980,#123981,#123982,#123983,#123984,
#123985,#123986,#123987,#123988,#123989,#123990,#123991,#123992,#123993,
#123994,#123995,#123996,#123997,#123998,#123999,#124000,#124001,#124002,
#124003,#124004,#124005,#124006,#124007,#124008,#124009,#124010,#124011,
#124012,#124013,#124014,#124015,#124016,#124017,#124018,#124019,#124020,
#124021,#124022,#124023,#124024,#124025,#124026,#124027,#124028,#124029,
#124030,#124031,#124032,#124033,#124034,#124035,#124036,#124037,#124038,
#124039,#124040,#124041,#124042,#124043,#124044,#124045,#124046,#124047,
#124048,#124049,#124050,#124051,#124052,#124053,#124054,#124055,#124056,
#124057,#124058,#124059,#124060,#124061,#124062,#124063,#124064,#124065,
#124066,#124067,#124068,#124069,#124070,#124071,#124072,#124073),
 .UNSPECIFIED.,.F.,.F.,(4,3,3,3,3,3,3,3,3,3,3,3,3,3,3,3,3,3,3,3,3,3,3,3,
3,3,3,3,3,3,3,3,3,3,3,3,3,3,3,3,3,3,3,3,3,3,3,3,3,3,3,3,3,3,3,3,3,3,3,3,
3,3,3,3,3,3,3,3,3,3,3,3,3,4),(1467.12376922661,1467.20615137202,1467.28846542945,
1467.37073818782,1467.45299077312,1467.53524219248,1467.61751144987,1467.69986534415,
1467.78226484149,1467.86478835703,1467.9204985186,1468.00423723045,1468.08787274181,
1468.17142518521,1468.25491462106,1468.33836857168,1468.42180506552,1468.50524217528,
1468.5886979702,1468.67224246292,1468.75583154587,1468.83955481342,1468.92023452932,
1469.00397324117,1469.08760875253,1469.17116119593,1469.25465063178,1469.3381045824,
1469.42154107624,1469.504978186,1469.58843398092,1469.67197847365,1469.75556755659,
1469.83929082415,1469.91997054004,1470.00370925189,1470.08734476325,1470.17089720665,
1470.2543866425,1470.33784059312,1470.42127708696,1470.50471419672,1470.58816999164,
1470.67171448437,1470.75530356731,1470.83902683487,1470.91970655076,1471.00344526261,
1471.08708077397,1471.17063321737,1471.25412265322,1471.33757660384,1471.42101309768,
1471.50445020744,1471.58790600235,1471.67145049508,1471.75503957802,1471.83876284558,
1471.91944256148,1472.00318127333,1472.08681678469,1472.17036922809,1472.25385866394,
1472.33731261456,1472.4207491084,1472.50418621816,1472.58764201308,1472.67118650581,
1472.75477558875,1472.83849885631,1472.9191785722,1473.00772889966,1473.09607576719,
1473.15664071279),.UNSPECIFIED.);
#984=B_SPLINE_CURVE_WITH_KNOTS('',3,(#124074,#124075,#124076,#124077,#124078,
#124079,#124080,#124081,#124082,#124083),.UNSPECIFIED.,.F.,.F.,(4,3,3,4),
(1466.87244437141,1466.92076250788,1467.04006077289,1467.12376922643),
 .UNSPECIFIED.);
#985=B_SPLINE_CURVE_WITH_KNOTS('',3,(#124085,#124086,#124087,#124088,#124089,
#124090,#124091,#124092,#124093,#124094),.UNSPECIFIED.,.F.,.F.,(4,3,3,4),
(1466.8719408414,1466.9543981102,1467.03908366825,1467.12376922629),
 .UNSPECIFIED.);
#986=B_SPLINE_CURVE_WITH_KNOTS('',3,(#124095,#124096,#124097,#124098,#124099,
#124100,#124101,#124102,#124103,#124104,#124105,#124106,#124107,#124108,
#124109,#124110,#124111,#124112,#124113,#124114,#124115,#124116,#124117,
#124118,#124119,#124120,#124121,#124122,#124123,#124124,#124125,#124126,
#124127,#124128,#124129,#124130,#124131,#124132,#124133,#124134,#124135,
#124136,#124137,#124138,#124139,#124140,#124141,#124142,#124143,#124144,
#124145,#124146,#124147,#124148,#124149,#124150,#124151,#124152,#124153,
#124154,#124155,#124156,#124157,#124158,#124159,#124160,#124161,#124162,
#124163,#124164,#124165,#124166,#124167,#124168,#124169,#124170,#124171,
#124172,#124173,#124174,#124175,#124176,#124177,#124178,#124179,#124180,
#124181,#124182,#124183,#124184,#124185,#124186,#124187,#124188,#124189,
#124190,#124191,#124192,#124193,#124194,#124195,#124196,#124197,#124198,
#124199,#124200,#124201,#124202,#124203,#124204,#124205,#124206,#124207,
#124208,#124209,#124210,#124211,#124212,#124213,#124214,#124215,#124216,
#124217,#124218,#124219,#124220,#124221,#124222,#124223,#124224,#124225,
#124226,#124227,#124228,#124229,#124230,#124231,#124232,#124233,#124234,
#124235,#124236,#124237,#124238,#124239,#124240,#124241,#124242,#124243,
#124244,#124245,#124246,#124247,#124248,#124249,#124250,#124251,#124252,
#124253,#124254,#124255,#124256,#124257,#124258,#124259,#124260,#124261,
#124262,#124263,#124264,#124265,#124266,#124267,#124268,#124269,#124270,
#124271,#124272,#124273,#124274,#124275,#124276,#124277,#124278,#124279,
#124280,#124281,#124282,#124283,#124284,#124285,#124286,#124287,#124288,
#124289,#124290,#124291,#124292,#124293,#124294,#124295,#124296,#124297,
#124298,#124299,#124300,#124301,#124302,#124303,#124304,#124305,#124306,
#124307,#124308,#124309,#124310,#124311),.UNSPECIFIED.,.F.,.F.,(4,3,3,3,
3,3,3,3,3,3,3,3,3,3,3,3,3,3,3,3,3,3,3,3,3,3,3,3,3,3,3,3,3,3,3,3,3,3,3,3,
3,3,3,3,3,3,3,3,3,3,3,3,3,3,3,3,3,3,3,3,3,3,3,3,3,3,3,3,3,3,3,3,4),(1467.12376922643,
1467.2310531276,1467.31479183945,1467.39842735081,1467.48197979421,1467.56546923006,
1467.64892318068,1467.73235967452,1467.81579678428,1467.8992525792,1467.98279707193,
1468.06638615487,1468.15010942242,1468.23078913832,1468.31452785017,1468.39816336153,
1468.48171580493,1468.56520524078,1468.6486591914,1468.73209568524,1468.815532795,
1468.89898858992,1468.98253308265,1469.06612216559,1469.14984543314,1469.23052514904,
1469.31426386089,1469.39789937225,1469.48145181565,1469.5649412515,1469.64839520212,
1469.73183169596,1469.81526880572,1469.89872460064,1469.98226909337,1470.06585817631,
1470.14958144386,1470.23026115976,1470.31399987161,1470.39763538297,1470.48118782637,
1470.56467726222,1470.64813121284,1470.73156770668,1470.81500481644,1470.89846061136,
1470.98200510409,1471.06559418703,1471.14931745458,1471.22999717048,1471.31373588233,
1471.39737139369,1471.48092383709,1471.56441327294,1471.64786722356,1471.7313037174,
1471.81474082716,1471.89819662208,1471.98174111481,1472.06533019775,1472.1490534653,
1472.2297331812,1472.31347615588,1472.39711495474,1472.48066971443,1472.56502658325,
1472.64847685927,1472.73190848728,1472.81533953906,1472.90038582054,1472.98390578302,
1473.06971522401,1473.15552466501),.UNSPECIFIED.);
#987=B_SPLINE_CURVE_WITH_KNOTS('',3,(#124317,#124318,#124319,#124320,#124321,
#124322,#124323,#124324,#124325,#124326,#124327,#124328,#124329,#124330,
#124331,#124332,#124333,#124334,#124335,#124336,#124337,#124338,#124339,
#124340,#124341,#124342,#124343,#124344,#124345,#124346,#124347,#124348,
#124349,#124350,#124351,#124352,#124353,#124354,#124355,#124356,#124357,
#124358,#124359,#124360,#124361,#124362,#124363,#124364,#124365,#124366,
#124367,#124368,#124369,#124370,#124371,#124372,#124373,#124374,#124375,
#124376,#124377,#124378,#124379,#124380,#124381,#124382,#124383,#124384,
#124385,#124386,#124387,#124388,#124389,#124390,#124391,#124392,#124393,
#124394,#124395,#124396,#124397,#124398,#124399,#124400,#124401,#124402,
#124403,#124404,#124405,#124406,#124407,#124408,#124409,#124410,#124411,
#124412,#124413,#124414,#124415,#124416,#124417,#124418,#124419,#124420,
#124421,#124422,#124423,#124424,#124425,#124426,#124427,#124428,#124429,
#124430,#124431,#124432,#124433,#124434,#124435,#124436,#124437,#124438,
#124439,#124440,#124441,#124442,#124443,#124444,#124445,#124446,#124447,
#124448,#124449,#124450,#124451,#124452,#124453,#124454,#124455,#124456,
#124457,#124458,#124459,#124460,#124461,#124462,#124463,#124464,#124465,
#124466,#124467,#124468,#124469,#124470,#124471,#124472,#124473,#124474,
#124475,#124476,#124477,#124478,#124479,#124480,#124481,#124482,#124483,
#124484,#124485,#124486,#124487,#124488,#124489,#124490,#124491,#124492,
#124493,#124494,#124495,#124496,#124497,#124498,#124499,#124500,#124501,
#124502,#124503,#124504,#124505,#124506,#124507,#124508,#124509,#124510,
#124511,#124512,#124513,#124514,#124515,#124516,#124517,#124518,#124519,
#124520,#124521,#124522,#124523,#124524,#124525,#124526,#124527,#124528,
#124529,#124530,#124531,#124532,#124533,#124534,#124535,#124536),
 .UNSPECIFIED.,.F.,.F.,(4,3,3,3,3,3,3,3,3,3,3,3,3,3,3,3,3,3,3,3,3,3,3,3,
3,3,3,3,3,3,3,3,3,3,3,3,3,3,3,3,3,3,3,3,3,3,3,3,3,3,3,3,3,3,3,3,3,3,3,3,
3,3,3,3,3,3,3,3,3,3,3,3,3,4),(1473.40695453361,1473.49393313965,1473.5810114473,
1473.66828127154,1473.75565011186,1473.8432173964,1473.91891458292,1474.00265329477,
1474.08628880613,1474.16984124953,1474.25333068538,1474.336784636,1474.42022112984,
1474.5036582396,1474.58711403452,1474.67065852724,1474.75424761019,1474.83797087774,
1474.91865059364,1475.00238930549,1475.08602481685,1475.16957726025,1475.2530666961,
1475.33652064672,1475.41995714056,1475.50339425032,1475.58685004524,1475.67039453797,
1475.75398362091,1475.83770688847,1475.91838660436,1476.00212531621,1476.08576082757,
1476.16931327097,1476.25280270682,1476.33625665744,1476.41969315128,1476.50313026104,
1476.58658605596,1476.67013054869,1476.75371963163,1476.83744289918,1476.91812261508,
1477.00186132693,1477.08549683829,1477.16904928169,1477.25253871754,1477.33599266816,
1477.419429162,1477.50286627176,1477.58632206667,1477.6698665594,1477.75345564234,
1477.8371789099,1477.9178586258,1478.00159733765,1478.08523284901,1478.16878529241,
1478.25227472826,1478.33572867888,1478.41916517272,1478.50260228248,1478.5860580774,
1478.66960257013,1478.75319165307,1478.83691492063,1478.91759463652,1479.00021914845,
1479.08274652633,1479.16519590404,1479.24758186863,1479.32993154163,1479.41227038175,
1479.43866858093),.UNSPECIFIED.);
#988=B_SPLINE_CURVE_WITH_KNOTS('',3,(#124537,#124538,#124539,#124540,#124541,
#124542,#124543,#124544,#124545,#124546),.UNSPECIFIED.,.F.,.F.,(4,3,3,4),
(1473.15664071279,1473.24472264985,1473.3326204829,1473.40695453349),
 .UNSPECIFIED.);
#989=B_SPLINE_CURVE_WITH_KNOTS('',3,(#124548,#124549,#124550,#124551,#124552,
#124553,#124554,#124555,#124556,#124557),.UNSPECIFIED.,.F.,.F.,(4,3,3,4),
(1473.15552466501,1473.22946919192,1473.35769273628,1473.40695453361),
 .UNSPECIFIED.);
#990=B_SPLINE_CURVE_WITH_KNOTS('',3,(#124558,#124559,#124560,#124561,#124562,
#124563,#124564,#124565,#124566,#124567,#124568,#124569,#124570,#124571,
#124572,#124573,#124574,#124575,#124576,#124577,#124578,#124579,#124580,
#124581,#124582,#124583,#124584,#124585,#124586,#124587,#124588,#124589,
#124590,#124591,#124592,#124593,#124594,#124595,#124596,#124597,#124598,
#124599,#124600,#124601,#124602,#124603,#124604,#124605,#124606,#124607,
#124608,#124609,#124610,#124611,#124612,#124613,#124614,#124615,#124616,
#124617,#124618,#124619,#124620,#124621,#124622,#124623,#124624,#124625,
#124626,#124627,#124628,#124629,#124630,#124631,#124632,#124633,#124634,
#124635,#124636,#124637,#124638,#124639,#124640,#124641,#124642,#124643,
#124644,#124645,#124646,#124647,#124648,#124649,#124650,#124651,#124652,
#124653,#124654,#124655,#124656,#124657,#124658,#124659,#124660,#124661,
#124662,#124663,#124664,#124665,#124666,#124667,#124668,#124669,#124670,
#124671,#124672,#124673,#124674,#124675,#124676,#124677,#124678,#124679,
#124680,#124681,#124682,#124683,#124684,#124685,#124686,#124687,#124688,
#124689,#124690,#124691,#124692,#124693,#124694,#124695,#124696,#124697,
#124698,#124699,#124700,#124701,#124702,#124703,#124704,#124705,#124706,
#124707,#124708,#124709,#124710,#124711,#124712,#124713,#124714,#124715,
#124716,#124717,#124718,#124719,#124720,#124721,#124722,#124723,#124724,
#124725,#124726,#124727,#124728,#124729,#124730,#124731,#124732,#124733,
#124734,#124735,#124736,#124737,#124738,#124739,#124740,#124741,#124742,
#124743,#124744,#124745,#124746,#124747,#124748,#124749,#124750,#124751,
#124752,#124753,#124754,#124755,#124756,#124757,#124758,#124759,#124760,
#124761,#124762,#124763,#124764,#124765,#124766,#124767,#124768,#124769,
#124770,#124771,#124772,#124773,#124774,#124775,#124776,#124777),
 .UNSPECIFIED.,.F.,.F.,(4,3,3,3,3,3,3,3,3,3,3,3,3,3,3,3,3,3,3,3,3,3,3,3,
3,3,3,3,3,3,3,3,3,3,3,3,3,3,3,3,3,3,3,3,3,3,3,3,3,3,3,3,3,3,3,3,3,3,3,3,
3,3,3,3,3,3,3,3,3,3,3,3,3,4),(1473.40695453377,1473.4893182278,1473.57160671137,
1473.65384440038,1473.73605555324,1473.81825920997,1473.90047440225,1473.98277068985,
1474.06510696983,1474.14757432633,1474.22920520264,1474.31294391449,1474.39657942585,
1474.48013186925,1474.5636213051,1474.64707525572,1474.73051174956,1474.81394885932,
1474.89740465424,1474.98094914697,1475.06453822991,1475.14826149746,1475.22894121336,
1475.31267992521,1475.39631543657,1475.47986787997,1475.56335731582,1475.64681126644,
1475.73024776028,1475.81368487004,1475.89714066496,1475.98068515769,1476.06427424063,
1476.14799750818,1476.22867722408,1476.31241593593,1476.39605144729,1476.47960389069,
1476.56309332654,1476.64654727716,1476.729983771,1476.81342088076,1476.89687667568,
1476.98042116841,1477.06401025135,1477.1477335189,1477.2284132348,1477.31215194665,
1477.39578745801,1477.47933990141,1477.56282933726,1477.64628328788,1477.72971978172,
1477.81315689148,1477.8966126864,1477.98015717913,1478.06374626207,1478.14746952962,
1478.22814924552,1478.31188795737,1478.39552346873,1478.47907591213,1478.56256534798,
1478.6460192986,1478.72945579244,1478.8128929022,1478.89634869712,1478.97989318985,
1479.06348227279,1479.14720554034,1479.22788525624,1479.31758500425,1479.40706476103,
1479.43983851051),.UNSPECIFIED.);
#991=B_SPLINE_CURVE_WITH_KNOTS('',3,(#124783,#124784,#124785,#124786,#124787,
#124788,#124789,#124790,#124791,#124792,#124793,#124794,#124795,#124796,
#124797,#124798,#124799,#124800,#124801,#124802,#124803,#124804,#124805,
#124806,#124807,#124808,#124809,#124810,#124811,#124812,#124813,#124814,
#124815,#124816,#124817,#124818,#124819,#124820,#124821,#124822,#124823,
#124824,#124825,#124826,#124827,#124828,#124829,#124830,#124831,#124832,
#124833,#124834,#124835,#124836,#124837,#124838,#124839,#124840,#124841,
#124842,#124843,#124844,#124845,#124846,#124847,#124848,#124849,#124850,
#124851,#124852,#124853,#124854,#124855,#124856,#124857,#124858,#124859,
#124860,#124861,#124862,#124863,#124864,#124865,#124866,#124867,#124868,
#124869,#124870,#124871,#124872,#124873,#124874,#124875,#124876,#124877,
#124878,#124879,#124880,#124881,#124882,#124883,#124884,#124885,#124886,
#124887,#124888,#124889,#124890,#124891,#124892,#124893,#124894,#124895,
#124896,#124897,#124898,#124899,#124900,#124901,#124902,#124903,#124904,
#124905,#124906,#124907,#124908,#124909,#124910,#124911,#124912,#124913,
#124914,#124915,#124916,#124917,#124918,#124919,#124920,#124921,#124922,
#124923,#124924,#124925,#124926,#124927,#124928,#124929,#124930,#124931,
#124932,#124933,#124934,#124935,#124936,#124937,#124938,#124939,#124940,
#124941,#124942,#124943,#124944,#124945,#124946,#124947,#124948,#124949,
#124950,#124951,#124952,#124953,#124954,#124955,#124956,#124957,#124958,
#124959,#124960,#124961,#124962,#124963,#124964,#124965,#124966,#124967,
#124968,#124969,#124970,#124971,#124972,#124973,#124974,#124975,#124976,
#124977,#124978,#124979,#124980,#124981,#124982,#124983,#124984,#124985,
#124986,#124987,#124988,#124989,#124990,#124991,#124992,#124993,#124994,
#124995,#124996,#124997,#124998,#124999),.UNSPECIFIED.,.F.,.F.,(4,3,3,3,
3,3,3,3,3,3,3,3,3,3,3,3,3,3,3,3,3,3,3,3,3,3,3,3,3,3,3,3,3,3,3,3,3,3,3,3,
3,3,3,3,3,3,3,3,3,3,3,3,3,3,3,3,3,3,3,3,3,3,3,3,3,3,3,3,3,3,3,3,4),(1479.69013984079,
1479.80373524402,1479.91733064724,1480.00106935909,1480.08470487045,1480.16825731385,
1480.2517467497,1480.33520070032,1480.41863719416,1480.50207430392,1480.58553009884,
1480.66907459157,1480.75266367451,1480.83638694206,1480.91706665796,1481.00080536981,
1481.08444088117,1481.16799332457,1481.25148276042,1481.33493671104,1481.41837320488,
1481.50181031464,1481.58526610956,1481.66881060229,1481.75239968523,1481.83612295279,
1481.91680266868,1482.00054138053,1482.08417689189,1482.16772933529,1482.25121877114,
1482.33467272176,1482.4181092156,1482.50154632536,1482.58500212028,1482.66854661301,
1482.75213569595,1482.8358589635,1482.9165386794,1483.00027739125,1483.08391290261,
1483.16746534601,1483.25095478186,1483.33440873248,1483.41784522632,1483.50128233608,
1483.584738131,1483.66828262373,1483.75187170667,1483.83559497422,1483.91627469012,
1484.00001340197,1484.08364891333,1484.16720135673,1484.25069079258,1484.33414474319,
1484.41758123704,1484.5010183468,1484.58447414171,1484.66801863444,1484.75160771738,
1484.83533098494,1484.91601070084,1484.99976112188,1485.08340578193,1485.16694939894,
1485.25043572519,1485.33388288075,1485.41730895535,1485.50075704418,1485.58421581109,
1485.66774035371,1485.72166203219),.UNSPECIFIED.);
#992=B_SPLINE_CURVE_WITH_KNOTS('',3,(#125000,#125001,#125002,#125003,#125004,
#125005,#125006,#125007,#125008,#125009),.UNSPECIFIED.,.F.,.F.,(4,3,3,4),
(1479.43866858093,1479.52103553806,1479.60558768936,1479.69013984066),
 .UNSPECIFIED.);
#993=B_SPLINE_CURVE_WITH_KNOTS('',3,(#125011,#125012,#125013,#125014,#125015,
#125016,#125017,#125018,#125019,#125020),.UNSPECIFIED.,.F.,.F.,(4,3,3,4),
(1479.43983851051,1479.52903735213,1479.61799758571,1479.69013984063),
 .UNSPECIFIED.);
#994=B_SPLINE_CURVE_WITH_KNOTS('',3,(#125021,#125022,#125023,#125024,#125025,
#125026,#125027,#125028,#125029,#125030,#125031,#125032,#125033,#125034,
#125035,#125036,#125037,#125038,#125039,#125040,#125041,#125042,#125043,
#125044,#125045,#125046,#125047,#125048,#125049,#125050,#125051,#125052,
#125053,#125054,#125055,#125056,#125057,#125058,#125059,#125060,#125061,
#125062,#125063,#125064,#125065,#125066,#125067,#125068,#125069,#125070,
#125071,#125072,#125073,#125074,#125075,#125076,#125077,#125078,#125079,
#125080,#125081,#125082,#125083,#125084,#125085,#125086,#125087,#125088,
#125089,#125090,#125091,#125092,#125093,#125094,#125095,#125096,#125097,
#125098,#125099,#125100,#125101,#125102,#125103,#125104,#125105,#125106,
#125107,#125108,#125109,#125110,#125111,#125112,#125113,#125114,#125115,
#125116,#125117,#125118,#125119,#125120,#125121,#125122,#125123,#125124,
#125125,#125126,#125127,#125128,#125129,#125130,#125131,#125132,#125133,
#125134,#125135,#125136,#125137,#125138,#125139,#125140,#125141,#125142,
#125143,#125144,#125145,#125146,#125147,#125148,#125149,#125150,#125151,
#125152,#125153,#125154,#125155,#125156,#125157,#125158,#125159,#125160,
#125161,#125162,#125163,#125164,#125165,#125166,#125167,#125168,#125169,
#125170,#125171,#125172,#125173,#125174,#125175,#125176,#125177,#125178,
#125179,#125180,#125181,#125182,#125183,#125184,#125185,#125186,#125187,
#125188,#125189,#125190,#125191,#125192,#125193,#125194,#125195,#125196,
#125197,#125198,#125199,#125200,#125201,#125202,#125203,#125204,#125205,
#125206,#125207,#125208,#125209,#125210,#125211,#125212,#125213,#125214,
#125215,#125216,#125217,#125218,#125219,#125220,#125221,#125222,#125223,
#125224,#125225,#125226,#125227,#125228,#125229,#125230,#125231,#125232,
#125233,#125234,#125235,#125236,#125237,#125238,#125239,#125240),
 .UNSPECIFIED.,.F.,.F.,(4,3,3,3,3,3,3,3,3,3,3,3,3,3,3,3,3,3,3,3,3,3,3,3,
3,3,3,3,3,3,3,3,3,3,3,3,3,3,3,3,3,3,3,3,3,3,3,3,3,3,3,3,3,3,3,3,3,3,3,3,
3,3,3,3,3,3,3,3,3,3,3,3,3,4),(1479.69013984079,1479.77630058833,1479.86253318071,
1479.94885023975,1480.03532621794,1480.1218940574,1480.20861921668,1480.22762126696,
1480.31135997881,1480.39499549017,1480.47854793357,1480.56203736942,1480.64549132004,
1480.72892781388,1480.81236492364,1480.89582071856,1480.97936521129,1481.06295429423,
1481.14667756178,1481.22735727768,1481.31109598953,1481.39473150089,1481.47828394429,
1481.56177338014,1481.64522733076,1481.7286638246,1481.81210093436,1481.89555672928,
1481.97910122201,1482.06269030495,1482.1464135725,1482.2270932884,1482.31083200025,
1482.39446751161,1482.47801995501,1482.56150939086,1482.64496334148,1482.72839983532,
1482.81183694508,1482.89529274,1482.97883723273,1483.06242631567,1483.14614958322,
1483.22682929912,1483.31056801097,1483.39420352233,1483.47775596573,1483.56124540158,
1483.6446993522,1483.72813584604,1483.8115729558,1483.89502875072,1483.97857324344,
1484.06216232639,1484.14588559394,1484.22656530984,1484.31030402169,1484.39393953305,
1484.47749197645,1484.5609814123,1484.64443536292,1484.72787185676,1484.81130896652,
1484.89476476144,1484.97830925417,1485.06189833711,1485.14562160467,1485.22630132056,
1485.3090888973,1485.39177806216,1485.47437529998,1485.5569182117,1485.63944678899,
1485.72197536628),.UNSPECIFIED.);
#995=B_SPLINE_CURVE_WITH_KNOTS('',3,(#125246,#125247,#125248,#125249,#125250,
#125251,#125252,#125253,#125254,#125255),.UNSPECIFIED.,.F.,.F.,(4,1,1,1,
1,1,1,4),(1485.97333225685,1486.91548272228,1487.915218733,1488.91495474372,
1489.91469075444,1490.91442676516,1491.91416277588,1492.00598701905),
 .UNSPECIFIED.);
#996=B_SPLINE_CURVE_WITH_KNOTS('',3,(#125256,#125257,#125258,#125259,#125260,
#125261,#125262,#125263,#125264,#125265,#125266,#125267,#125268),
 .UNSPECIFIED.,.F.,.F.,(4,3,3,3,4),(1485.72166203219,1485.80528850285,1485.88903401518,
1485.91574671156,1485.97332514797),.UNSPECIFIED.);
#997=B_SPLINE_CURVE_WITH_KNOTS('',3,(#125270,#125271,#125272,#125273,#125274,
#125275,#125276,#125277,#125278,#125279),.UNSPECIFIED.,.F.,.F.,(4,3,3,4),
(1485.72197536628,1485.80448560964,1485.8889053788,1485.97332514797),
 .UNSPECIFIED.);
#998=B_SPLINE_CURVE_WITH_KNOTS('',3,(#125280,#125281,#125282,#125283,#125284,
#125285,#125286,#125287,#125288,#125289,#125290,#125291,#125292,#125293,
#125294,#125295,#125296,#125297,#125298,#125299,#125300,#125301,#125302,
#125303,#125304,#125305,#125306,#125307,#125308,#125309,#125310,#125311,
#125312,#125313,#125314,#125315,#125316,#125317,#125318,#125319,#125320,
#125321,#125322,#125323,#125324,#125325,#125326,#125327,#125328,#125329,
#125330,#125331,#125332,#125333,#125334,#125335,#125336,#125337,#125338,
#125339,#125340,#125341,#125342,#125343,#125344,#125345,#125346,#125347,
#125348,#125349,#125350,#125351,#125352,#125353,#125354,#125355,#125356,
#125357,#125358,#125359,#125360,#125361,#125362,#125363,#125364,#125365,
#125366,#125367,#125368,#125369,#125370,#125371,#125372,#125373,#125374,
#125375,#125376,#125377,#125378,#125379,#125380,#125381,#125382,#125383,
#125384,#125385,#125386,#125387,#125388,#125389,#125390,#125391,#125392,
#125393,#125394,#125395,#125396,#125397,#125398,#125399,#125400,#125401,
#125402,#125403,#125404,#125405,#125406,#125407,#125408,#125409,#125410,
#125411,#125412,#125413,#125414,#125415,#125416,#125417,#125418,#125419,
#125420,#125421,#125422,#125423,#125424,#125425,#125426,#125427,#125428,
#125429,#125430,#125431,#125432,#125433,#125434,#125435,#125436,#125437,
#125438,#125439,#125440,#125441,#125442,#125443,#125444,#125445,#125446,
#125447,#125448,#125449,#125450,#125451,#125452,#125453,#125454,#125455,
#125456,#125457,#125458,#125459,#125460,#125461,#125462,#125463,#125464,
#125465,#125466,#125467,#125468,#125469,#125470,#125471,#125472,#125473,
#125474,#125475,#125476,#125477,#125478,#125479,#125480,#125481,#125482,
#125483,#125484,#125485,#125486,#125487,#125488,#125489,#125490,#125491,
#125492,#125493,#125494,#125495,#125496,#125497,#125498,#125499),
 .UNSPECIFIED.,.F.,.F.,(4,3,3,3,3,3,3,3,3,3,3,3,3,3,3,3,3,3,3,3,3,3,3,3,
3,3,3,3,3,3,3,3,3,3,3,3,3,3,3,3,3,3,3,3,3,3,3,3,3,3,3,3,3,3,3,3,3,3,3,3,
3,3,3,3,3,3,3,3,3,3,3,3,3,4),(1485.97332514817,1486.08013280166,1486.18927155072,
1486.22603733128,1486.30977604313,1486.39341155449,1486.47696399789,1486.56045343374,
1486.64390738436,1486.7273438782,1486.81078098796,1486.89423678288,1486.97778127561,
1487.06137035855,1487.1450936261,1487.225773342,1487.30951205385,1487.39314756521,
1487.47670000861,1487.56018944446,1487.64364339508,1487.72707988892,1487.81051699868,
1487.8939727936,1487.97751728633,1488.06110636927,1488.14482963682,1488.22550935272,
1488.30924806457,1488.39288357593,1488.47643601933,1488.55992545518,1488.6433794058,
1488.72681589964,1488.8102530094,1488.89370880432,1488.97725329705,1489.06084237999,
1489.14456564755,1489.22524536344,1489.30898407529,1489.39261958665,1489.47617203005,
1489.5596614659,1489.64311541652,1489.72655191036,1489.80998902012,1489.89344481504,
1489.97698930776,1490.06057839071,1490.14430165826,1490.22498137416,1490.30872008601,
1490.39235559737,1490.47590804077,1490.55939747662,1490.64285142724,1490.72628792108,
1490.80972503084,1490.89318082576,1490.97672531848,1491.06031440143,1491.14403766898,
1491.22471738488,1491.30846947086,1491.39551639012,1491.47905786342,1491.56254230654,
1491.64598783891,1491.72941254974,1491.81285539563,1491.89630938701,1491.97981837138,
1492.00484482495),.UNSPECIFIED.);
#999=B_SPLINE_CURVE_WITH_KNOTS('',3,(#125505,#125506,#125507,#125508,#125509,
#125510,#125511,#125512,#125513,#125514),.UNSPECIFIED.,.F.,.F.,(4,1,1,1,
1,1,1,4),(1492.25651045514,1492.9138987866,1493.91363479732,1494.91337080804,
1495.91310681876,1496.91284282948,1497.9125788402,1498.28924643674),
 .UNSPECIFIED.);
#1000=B_SPLINE_CURVE_WITH_KNOTS('',3,(#125515,#125516,#125517,#125518),
 .UNSPECIFIED.,.F.,.F.,(4,4),(1492.00598701905,1492.25651045514),
 .UNSPECIFIED.);
#1001=B_SPLINE_CURVE_WITH_KNOTS('',3,(#125520,#125521,#125522,#125523,#125524,
#125525,#125526,#125527,#125528,#125529,#125530,#125531,#125532),
 .UNSPECIFIED.,.F.,.F.,(4,3,3,3,4),(1492.00484482495,1492.08845275128,1492.17218669413,
1492.2244533956,1492.25651045515),.UNSPECIFIED.);
#1002=B_SPLINE_CURVE_WITH_KNOTS('',3,(#125533,#125534,#125535,#125536,#125537,
#125538,#125539,#125540,#125541,#125542,#125543,#125544,#125545,#125546,
#125547,#125548,#125549,#125550,#125551,#125552,#125553,#125554,#125555,
#125556,#125557,#125558,#125559,#125560,#125561,#125562,#125563,#125564,
#125565,#125566,#125567,#125568,#125569,#125570,#125571,#125572,#125573,
#125574,#125575,#125576,#125577,#125578,#125579,#125580,#125581,#125582,
#125583,#125584,#125585,#125586,#125587,#125588,#125589,#125590,#125591,
#125592,#125593,#125594,#125595,#125596,#125597,#125598,#125599,#125600,
#125601,#125602,#125603,#125604,#125605,#125606,#125607,#125608,#125609,
#125610,#125611,#125612,#125613,#125614,#125615,#125616,#125617,#125618,
#125619,#125620,#125621,#125622,#125623,#125624,#125625,#125626,#125627,
#125628,#125629,#125630,#125631,#125632,#125633,#125634,#125635,#125636,
#125637,#125638,#125639,#125640,#125641,#125642,#125643,#125644,#125645,
#125646,#125647,#125648,#125649,#125650,#125651,#125652,#125653,#125654,
#125655,#125656,#125657,#125658,#125659,#125660,#125661,#125662,#125663,
#125664,#125665,#125666,#125667,#125668,#125669,#125670,#125671,#125672,
#125673,#125674,#125675,#125676,#125677,#125678,#125679,#125680,#125681,
#125682,#125683,#125684,#125685,#125686,#125687,#125688,#125689,#125690,
#125691,#125692,#125693,#125694,#125695,#125696,#125697,#125698,#125699,
#125700,#125701,#125702,#125703,#125704,#125705,#125706,#125707,#125708,
#125709,#125710,#125711,#125712,#125713,#125714,#125715,#125716,#125717,
#125718,#125719,#125720,#125721,#125722,#125723,#125724,#125725,#125726,
#125727,#125728,#125729,#125730,#125731,#125732,#125733,#125734,#125735,
#125736,#125737,#125738,#125739,#125740,#125741,#125742,#125743,#125744,
#125745,#125746,#125747,#125748,#125749,#125750,#125751,#125752),
 .UNSPECIFIED.,.F.,.F.,(4,3,3,3,3,3,3,3,3,3,3,3,3,3,3,3,3,3,3,3,3,3,3,3,
3,3,3,3,3,3,3,3,3,3,3,3,3,3,3,3,3,3,3,3,3,3,3,3,3,3,3,3,3,3,3,3,3,3,3,3,
3,3,3,3,3,3,3,3,3,3,3,3,3,4),(1492.25651045529,1492.33980475775,1492.42299730472,
1492.50610866675,1492.58915933873,1492.67217794586,1492.75518199317,1492.83818994494,
1492.92122026463,1493.00433983238,1493.08750804642,1493.1708018184,1493.22418940632,
1493.30792811817,1493.39156362953,1493.47511607293,1493.55860550878,1493.6420594594,
1493.72549595324,1493.808933063,1493.89238885792,1493.97593335065,1494.05952243359,
1494.14324570114,1494.22392541704,1494.30766412889,1494.39129964025,1494.47485208365,
1494.5583415195,1494.64179547012,1494.72523196396,1494.80866907372,1494.89212486864,
1494.97566936137,1495.05925844431,1495.14298171187,1495.22366142776,1495.30740013961,
1495.39103565097,1495.47458809437,1495.55807753022,1495.64153148084,1495.72496797468,
1495.80840508444,1495.89186087936,1495.97540537209,1496.05899445503,1496.14271772258,
1496.22339743848,1496.30713615033,1496.39077166169,1496.47432410509,1496.55781354094,
1496.64126749156,1496.7247039854,1496.80814109516,1496.89159689008,1496.9751413828,
1497.05873046575,1497.1424537333,1497.2231334492,1497.30687216105,1497.39050767241,
1497.47406011581,1497.55754955166,1497.64100350227,1497.72443999612,1497.80787710587,
1497.89133290079,1497.97487739352,1498.05846647646,1498.14218974402,1498.22286945992,
1498.28900992258),.UNSPECIFIED.);
#1003=B_SPLINE_CURVE_WITH_KNOTS('',3,(#125758,#125759,#125760,#125761,#125762,
#125763,#125764,#125765,#125766,#125767,#125768,#125769,#125770,#125771,
#125772,#125773,#125774,#125775,#125776,#125777,#125778,#125779,#125780,
#125781,#125782,#125783,#125784,#125785,#125786,#125787,#125788,#125789,
#125790,#125791,#125792,#125793,#125794,#125795,#125796,#125797,#125798,
#125799,#125800,#125801,#125802,#125803,#125804,#125805,#125806,#125807,
#125808,#125809,#125810,#125811,#125812,#125813,#125814,#125815,#125816,
#125817,#125818,#125819,#125820,#125821,#125822,#125823,#125824,#125825,
#125826,#125827,#125828,#125829,#125830,#125831,#125832,#125833,#125834,
#125835,#125836,#125837,#125838,#125839,#125840,#125841,#125842,#125843,
#125844,#125845,#125846,#125847,#125848,#125849,#125850,#125851,#125852,
#125853,#125854,#125855,#125856,#125857,#125858,#125859,#125860,#125861,
#125862,#125863,#125864,#125865,#125866,#125867,#125868,#125869,#125870,
#125871,#125872,#125873,#125874,#125875,#125876,#125877,#125878,#125879,
#125880,#125881,#125882,#125883,#125884,#125885,#125886,#125887,#125888,
#125889,#125890,#125891,#125892,#125893,#125894,#125895,#125896,#125897,
#125898,#125899,#125900,#125901,#125902,#125903,#125904,#125905,#125906,
#125907,#125908,#125909,#125910,#125911,#125912,#125913,#125914,#125915,
#125916,#125917,#125918,#125919,#125920,#125921,#125922,#125923,#125924,
#125925,#125926,#125927,#125928,#125929,#125930,#125931,#125932,#125933,
#125934,#125935,#125936,#125937,#125938,#125939,#125940,#125941,#125942,
#125943,#125944,#125945,#125946,#125947,#125948,#125949,#125950,#125951,
#125952,#125953,#125954,#125955,#125956,#125957,#125958,#125959,#125960,
#125961,#125962,#125963,#125964,#125965,#125966,#125967,#125968,#125969,
#125970,#125971,#125972,#125973,#125974),.UNSPECIFIED.,.F.,.F.,(4,3,3,3,
3,3,3,3,3,3,3,3,3,3,3,3,3,3,3,3,3,3,3,3,3,3,3,3,3,3,3,3,3,3,3,3,3,3,3,3,
3,3,3,3,3,3,3,3,3,3,3,3,3,3,3,3,3,3,3,3,3,3,3,3,3,3,3,3,3,3,3,3,4),(1498.53969576232,
1498.63380533641,1498.72828492247,1498.82328898073,1498.91231485092,1498.99605356277,
1499.07968907413,1499.16324151753,1499.24673095338,1499.33018490399,1499.41362139784,
1499.4970585076,1499.58051430251,1499.66405879524,1499.74764787818,1499.83137114574,
1499.91205086164,1499.99578957349,1500.07942508486,1500.16297752826,1500.24646696411,
1500.32992091473,1500.41335740858,1500.49679451833,1500.58025031325,1500.66379480598,
1500.74738388893,1500.83110715649,1500.91178687237,1500.99552558422,1501.07916109558,
1501.16271353898,1501.24620297483,1501.32965692545,1501.41309341929,1501.49653052905,
1501.57998632397,1501.6635308167,1501.74711989964,1501.8308431672,1501.91152288309,
1501.99526159493,1502.0788971063,1502.1624495497,1502.24593898555,1502.32939293616,
1502.41282943001,1502.49626653976,1502.57972233468,1502.66326682741,1502.74685591035,
1502.8305791779,1502.91125889381,1502.99499760566,1503.07863311703,1503.16218556043,
1503.24567499628,1503.32912894689,1503.41256544074,1503.4960025505,1503.57945834542,
1503.66300283815,1503.74659192109,1503.83031518865,1503.91099490453,1503.99374376682,
1504.0763980856,1504.15897688734,1504.24149913172,1504.32399495184,1504.4064721317,
1504.48898209449,1504.57104348731),.UNSPECIFIED.);
#1004=B_SPLINE_CURVE_WITH_KNOTS('',3,(#125975,#125976,#125977,#125978),
 .UNSPECIFIED.,.F.,.F.,(4,4),(1498.28924643674,1498.53969576232),
 .UNSPECIFIED.);
#1005=B_SPLINE_CURVE_WITH_KNOTS('',3,(#125980,#125981,#125982,#125983,#125984,
#125985,#125986,#125987,#125988,#125989),.UNSPECIFIED.,.F.,.F.,(4,3,3,4),
(1498.28900992258,1498.38879043601,1498.48754282435,1498.53969576216),
 .UNSPECIFIED.);
#1006=B_SPLINE_CURVE_WITH_KNOTS('',3,(#125990,#125991,#125992,#125993,#125994,
#125995,#125996,#125997,#125998,#125999,#126000,#126001,#126002,#126003,
#126004,#126005,#126006,#126007,#126008,#126009,#126010,#126011,#126012,
#126013,#126014,#126015,#126016,#126017,#126018,#126019,#126020,#126021,
#126022,#126023,#126024,#126025,#126026,#126027,#126028,#126029,#126030,
#126031,#126032,#126033,#126034,#126035,#126036,#126037,#126038,#126039,
#126040,#126041,#126042,#126043,#126044,#126045,#126046,#126047,#126048,
#126049,#126050,#126051,#126052,#126053,#126054,#126055,#126056,#126057,
#126058,#126059,#126060,#126061,#126062,#126063,#126064,#126065,#126066,
#126067,#126068,#126069,#126070,#126071,#126072,#126073,#126074,#126075,
#126076,#126077,#126078,#126079,#126080,#126081,#126082,#126083,#126084,
#126085,#126086,#126087,#126088,#126089,#126090,#126091,#126092,#126093,
#126094,#126095,#126096,#126097,#126098,#126099,#126100,#126101,#126102,
#126103,#126104,#126105,#126106,#126107,#126108,#126109,#126110,#126111,
#126112,#126113,#126114,#126115,#126116,#126117,#126118,#126119,#126120,
#126121,#126122,#126123,#126124,#126125,#126126,#126127,#126128,#126129,
#126130,#126131,#126132,#126133,#126134,#126135,#126136,#126137,#126138,
#126139,#126140,#126141,#126142,#126143,#126144,#126145,#126146,#126147,
#126148,#126149,#126150,#126151,#126152,#126153,#126154,#126155,#126156,
#126157,#126158,#126159,#126160,#126161,#126162,#126163,#126164,#126165,
#126166,#126167,#126168,#126169,#126170,#126171,#126172,#126173,#126174,
#126175,#126176,#126177,#126178,#126179,#126180,#126181,#126182,#126183,
#126184,#126185,#126186,#126187,#126188,#126189,#126190,#126191,#126192,
#126193,#126194,#126195,#126196,#126197,#126198,#126199,#126200,#126201,
#126202,#126203,#126204,#126205,#126206,#126207,#126208,#126209,#126210,
#126211,#126212),.UNSPECIFIED.,.F.,.F.,(4,3,3,3,3,3,3,3,3,3,3,3,3,3,3,3,
3,3,3,3,3,3,3,3,3,3,3,3,3,3,3,3,3,3,3,3,3,3,3,3,3,3,3,3,3,3,3,3,3,3,3,3,
3,3,3,3,3,3,3,3,3,3,3,3,3,3,3,3,3,3,3,3,3,3,4),(1498.53969576233,1498.62505947587,
1498.70820805334,1498.79135490896,1498.87451833665,1498.96154012015,1499.04483918337,
1499.12819845884,1499.21167592631,1499.22260547064,1499.30634418249,1499.38997969385,
1499.47353213725,1499.55702157311,1499.64047552372,1499.72391201757,1499.80734912732,
1499.89080492224,1499.97434941497,1500.05793849791,1500.14166176547,1500.22234148136,
1500.30608019321,1500.38971570457,1500.47326814797,1500.55675758382,1500.64021153444,
1500.72364802828,1500.80708513804,1500.89054093296,1500.97408542569,1501.05767450863,
1501.14139777619,1501.22207749208,1501.30581620393,1501.38945171529,1501.47300415869,
1501.55649359454,1501.63994754516,1501.723384039,1501.80682114876,1501.89027694367,
1501.9738214364,1502.05741051934,1502.1411337869,1502.2218135028,1502.30555221465,
1502.38918772601,1502.47274016941,1502.55622960526,1502.63968355588,1502.72312004972,
1502.80655715948,1502.8900129544,1502.97355744713,1503.05714653007,1503.14086979762,
1503.22154951352,1503.30528822537,1503.38892373673,1503.47247618013,1503.55596561598,
1503.63941956659,1503.72285606044,1503.80629317019,1503.88974896511,1503.97329345784,
1504.05688254078,1504.14060580834,1504.22128552424,1504.3090278421,1504.39384146299,
1504.47856831567,1504.56320793387,1504.57225479568),.UNSPECIFIED.);
#1007=B_SPLINE_CURVE_WITH_KNOTS('',3,(#126218,#126219,#126220,#126221,#126222,
#126223,#126224,#126225,#126226,#126227,#126228,#126229,#126230,#126231,
#126232,#126233,#126234,#126235,#126236,#126237,#126238,#126239,#126240,
#126241,#126242,#126243,#126244,#126245,#126246,#126247,#126248,#126249,
#126250,#126251,#126252,#126253,#126254,#126255,#126256,#126257,#126258,
#126259,#126260,#126261,#126262,#126263,#126264,#126265,#126266,#126267,
#126268,#126269,#126270,#126271,#126272,#126273,#126274,#126275,#126276,
#126277,#126278,#126279,#126280,#126281,#126282,#126283,#126284,#126285,
#126286,#126287,#126288,#126289,#126290,#126291,#126292,#126293,#126294,
#126295,#126296,#126297,#126298,#126299,#126300,#126301,#126302,#126303,
#126304,#126305,#126306,#126307,#126308,#126309,#126310,#126311,#126312,
#126313,#126314,#126315,#126316,#126317,#126318,#126319,#126320,#126321,
#126322,#126323,#126324,#126325,#126326,#126327,#126328,#126329,#126330,
#126331,#126332,#126333,#126334,#126335,#126336,#126337,#126338,#126339,
#126340,#126341,#126342,#126343,#126344,#126345,#126346,#126347,#126348,
#126349,#126350,#126351,#126352,#126353,#126354,#126355,#126356,#126357,
#126358,#126359,#126360,#126361,#126362,#126363,#126364,#126365,#126366,
#126367,#126368,#126369,#126370,#126371,#126372,#126373,#126374,#126375,
#126376,#126377,#126378,#126379,#126380,#126381,#126382,#126383,#126384,
#126385,#126386,#126387,#126388,#126389,#126390,#126391,#126392,#126393,
#126394,#126395,#126396,#126397,#126398,#126399,#126400,#126401,#126402,
#126403,#126404,#126405,#126406,#126407,#126408,#126409,#126410,#126411,
#126412,#126413,#126414,#126415,#126416,#126417,#126418,#126419,#126420,
#126421,#126422,#126423,#126424,#126425,#126426,#126427,#126428,#126429,
#126430,#126431,#126432,#126433,#126434,#126435,#126436,#126437),
 .UNSPECIFIED.,.F.,.F.,(4,3,3,3,3,3,3,3,3,3,3,3,3,3,3,3,3,3,3,3,3,3,3,3,
3,3,3,3,3,3,3,3,3,3,3,3,3,3,3,3,3,3,3,3,3,3,3,3,3,3,3,3,3,3,3,3,3,3,3,3,
3,3,3,3,3,3,3,3,3,3,3,3,3,4),(1504.8228810695,1504.91073091525,1504.9944696271,
1505.07810513846,1505.16165758186,1505.24514701771,1505.32860096832,1505.41203746217,
1505.49547457192,1505.57893036684,1505.66247485957,1505.74606394251,1505.82978721006,
1505.91046692597,1505.99420563782,1506.07784114918,1506.16139359258,1506.24488302843,
1506.32833697905,1506.41177347289,1506.49521058265,1506.57866637757,1506.6622108703,
1506.74579995324,1506.82952322079,1506.91020293669,1506.99394164854,1507.0775771599,
1507.1611296033,1507.24461903915,1507.32807298977,1507.41150948361,1507.49494659337,
1507.57840238829,1507.66194688102,1507.74553596396,1507.82925923151,1507.90993894741,
1507.99367765926,1508.07731317062,1508.16086561402,1508.24435504987,1508.32780900049,
1508.41124549433,1508.49468260409,1508.57813839901,1508.66168289173,1508.74527197468,
1508.82899524223,1508.90967495813,1508.99341366998,1509.07704918134,1509.16060162474,
1509.24409106059,1509.32754501121,1509.41098150505,1509.49441861481,1509.57787440973,
1509.66141890246,1509.7450079854,1509.82873125295,1509.90941096885,1509.99315279498,
1510.07679070267,1510.16034482747,1510.24714103562,1510.33059132302,1510.41402385468,
1510.49745670225,1510.58090793355,1510.66443464419,1510.74800616879,1510.83168005567,
1510.85471449263),.UNSPECIFIED.);
#1008=B_SPLINE_CURVE_WITH_KNOTS('',3,(#126438,#126439,#126440,#126441,#126442,
#126443,#126444,#126445,#126446,#126447),.UNSPECIFIED.,.F.,.F.,(4,3,3,4),
(1504.57104348731,1504.65363118549,1504.73825612743,1504.82288106937),
 .UNSPECIFIED.);
#1009=B_SPLINE_CURVE_WITH_KNOTS('',3,(#126449,#126450,#126451,#126452,#126453,
#126454,#126455,#126456,#126457,#126458),.UNSPECIFIED.,.F.,.F.,(4,3,3,4),
(1504.57225479568,1504.65682073549,1504.74135303069,1504.82288106951),
 .UNSPECIFIED.);
#1010=B_SPLINE_CURVE_WITH_KNOTS('',3,(#126459,#126460,#126461,#126462,#126463,
#126464,#126465,#126466,#126467,#126468,#126469,#126470,#126471,#126472,
#126473,#126474,#126475,#126476,#126477,#126478,#126479,#126480,#126481,
#126482,#126483,#126484,#126485,#126486,#126487,#126488,#126489,#126490,
#126491,#126492,#126493,#126494,#126495,#126496,#126497,#126498,#126499,
#126500,#126501,#126502,#126503,#126504,#126505,#126506,#126507,#126508,
#126509,#126510,#126511,#126512,#126513,#126514,#126515,#126516,#126517,
#126518,#126519,#126520,#126521,#126522,#126523,#126524,#126525,#126526,
#126527,#126528,#126529,#126530,#126531,#126532,#126533,#126534,#126535,
#126536,#126537,#126538,#126539,#126540,#126541,#126542,#126543,#126544,
#126545,#126546,#126547,#126548,#126549,#126550,#126551,#126552,#126553,
#126554,#126555,#126556,#126557,#126558,#126559,#126560,#126561,#126562,
#126563,#126564,#126565,#126566,#126567,#126568,#126569,#126570,#126571,
#126572,#126573,#126574,#126575,#126576,#126577,#126578,#126579,#126580,
#126581,#126582,#126583,#126584,#126585,#126586,#126587,#126588,#126589,
#126590,#126591,#126592,#126593,#126594,#126595,#126596,#126597,#126598,
#126599,#126600,#126601,#126602,#126603,#126604,#126605,#126606,#126607,
#126608,#126609,#126610,#126611,#126612,#126613,#126614,#126615,#126616,
#126617,#126618,#126619,#126620,#126621,#126622,#126623,#126624,#126625,
#126626,#126627,#126628,#126629,#126630,#126631,#126632,#126633,#126634,
#126635,#126636,#126637,#126638,#126639,#126640,#126641,#126642,#126643,
#126644,#126645,#126646,#126647,#126648,#126649,#126650,#126651,#126652,
#126653,#126654,#126655,#126656,#126657,#126658,#126659,#126660,#126661,
#126662,#126663,#126664,#126665,#126666,#126667,#126668,#126669,#126670,
#126671,#126672,#126673,#126674,#126675,#126676,#126677,#126678),
 .UNSPECIFIED.,.F.,.F.,(4,3,3,3,3,3,3,3,3,3,3,3,3,3,3,3,3,3,3,3,3,3,3,3,
3,3,3,3,3,3,3,3,3,3,3,3,3,3,3,3,3,3,3,3,3,3,3,3,3,3,3,3,3,3,3,3,3,3,3,3,
3,3,3,3,3,3,3,3,3,3,3,3,3,4),(1504.82288106969,1504.91507842316,1505.00777905537,
1505.1007403094,1505.19403937815,1505.22102153496,1505.30476024681,1505.38839575818,
1505.47194820158,1505.55543763743,1505.63889158805,1505.7223280819,1505.80576519166,
1505.88922098658,1505.97276547931,1506.05635456225,1506.14007782982,1506.22075754568,
1506.30449625753,1506.38813176889,1506.47168421229,1506.55517364814,1506.63862759876,
1506.7220640926,1506.80550120236,1506.88895699728,1506.97250149001,1507.05609057295,
1507.13981384051,1507.2204935564,1507.30423226825,1507.38786777961,1507.47142022301,
1507.55490965886,1507.63836360947,1507.72180010332,1507.80523721307,1507.88869300799,
1507.97223750072,1508.05582658366,1508.13954985122,1508.22022956712,1508.30396827897,
1508.38760379033,1508.47115623373,1508.55464566958,1508.6380996202,1508.72153611404,
1508.8049732238,1508.88842901872,1508.97197351145,1509.05556259439,1509.13928586195,
1509.21996557784,1509.30370428969,1509.38733980105,1509.47089224445,1509.5543816803,
1509.63783563091,1509.72127212476,1509.80470923451,1509.88816502943,1509.97170952216,
1510.0552986051,1510.13902187266,1510.21970158856,1510.30230103997,1510.38480585915,
1510.46723517599,1510.54960805049,1510.63195228182,1510.71427833871,1510.796629289,
1510.85424422661),.UNSPECIFIED.);
#1011=B_SPLINE_CURVE_WITH_KNOTS('',3,(#126684,#126685,#126686,#126687,#126688,
#126689,#126690,#126691,#126692,#126693,#126694,#126695,#126696,#126697,
#126698,#126699,#126700,#126701,#126702,#126703,#126704,#126705,#126706,
#126707,#126708,#126709,#126710,#126711,#126712,#126713,#126714,#126715,
#126716,#126717,#126718,#126719,#126720,#126721,#126722,#126723,#126724,
#126725,#126726,#126727,#126728,#126729,#126730,#126731,#126732,#126733,
#126734,#126735,#126736,#126737,#126738,#126739,#126740,#126741,#126742,
#126743,#126744,#126745,#126746,#126747,#126748,#126749,#126750,#126751,
#126752,#126753,#126754,#126755,#126756,#126757,#126758,#126759,#126760,
#126761,#126762,#126763,#126764,#126765,#126766,#126767,#126768,#126769,
#126770,#126771,#126772,#126773,#126774,#126775,#126776,#126777,#126778,
#126779,#126780,#126781,#126782,#126783,#126784,#126785,#126786,#126787,
#126788,#126789,#126790,#126791,#126792,#126793,#126794,#126795,#126796,
#126797,#126798,#126799,#126800,#126801,#126802,#126803,#126804,#126805,
#126806,#126807,#126808,#126809,#126810,#126811,#126812,#126813,#126814,
#126815,#126816,#126817,#126818,#126819,#126820,#126821,#126822,#126823,
#126824,#126825,#126826,#126827,#126828,#126829,#126830,#126831,#126832,
#126833,#126834,#126835,#126836,#126837,#126838,#126839,#126840,#126841,
#126842,#126843,#126844,#126845,#126846,#126847,#126848,#126849,#126850,
#126851,#126852,#126853,#126854,#126855,#126856,#126857,#126858,#126859,
#126860,#126861,#126862,#126863,#126864,#126865,#126866,#126867,#126868,
#126869,#126870,#126871,#126872,#126873,#126874,#126875,#126876,#126877,
#126878,#126879,#126880,#126881,#126882,#126883,#126884,#126885,#126886,
#126887,#126888,#126889,#126890,#126891,#126892,#126893,#126894,#126895,
#126896,#126897,#126898,#126899,#126900,#126901,#126902,#126903),
 .UNSPECIFIED.,.F.,.F.,(4,3,3,3,3,3,3,3,3,3,3,3,3,3,3,3,3,3,3,3,3,3,3,3,
3,3,3,3,3,3,3,3,3,3,3,3,3,3,3,3,3,3,3,3,3,3,3,3,3,3,3,3,3,3,3,3,3,3,3,3,
3,3,3,3,3,3,3,3,3,3,3,3,3,4),(1511.10606637679,1511.18843911631,1511.27074200656,
1511.3530012699,1511.4352387914,1511.51747358911,1511.59972467661,1511.68205952719,
1511.76443860843,1511.84694334215,1511.90888299029,1511.99262170214,1512.0762572135,
1512.1598096569,1512.24329909275,1512.32675304336,1512.41018953721,1512.49362664696,
1512.57708244188,1512.66062693461,1512.74421601755,1512.8279392851,1512.90861900101,
1512.99235771286,1513.07599322422,1513.15954566762,1513.24303510347,1513.32648905408,
1513.40992554793,1513.49336265768,1513.5768184526,1513.66036294533,1513.74395202827,
1513.82767529583,1513.90835501173,1513.99209372358,1514.07572923494,1514.15928167834,
1514.24277111419,1514.32622506481,1514.40966155865,1514.49309866841,1514.57655446333,
1514.66009895606,1514.743688039,1514.82741130656,1514.90809102245,1514.9918297343,
1515.07546524566,1515.15901768906,1515.24250712491,1515.32596107553,1515.40939756937,
1515.49283467913,1515.57629047405,1515.65983496678,1515.74342404972,1515.82714731727,
1515.90782703317,1515.99156574502,1516.07520125639,1516.15875369978,1516.24224313564,
1516.32569708625,1516.4091335801,1516.49257068986,1516.57602648477,1516.6595709775,
1516.74316006045,1516.826883328,1516.90756304389,1516.99637404297,1517.08497773719,
1517.13894299318),.UNSPECIFIED.);
#1012=B_SPLINE_CURVE_WITH_KNOTS('',3,(#126904,#126905,#126906,#126907,#126908,
#126909,#126910,#126911,#126912,#126913),.UNSPECIFIED.,.F.,.F.,(4,3,3,4),
(1510.85471449263,1510.90914697957,1511.03030619401,1511.10606637668),
 .UNSPECIFIED.);
#1013=B_SPLINE_CURVE_WITH_KNOTS('',3,(#126915,#126916,#126917,#126918,#126919,
#126920,#126921,#126922,#126923,#126924),.UNSPECIFIED.,.F.,.F.,(4,3,3,4),
(1510.85424422661,1510.93666726909,1511.02136682282,1511.10606637655),
 .UNSPECIFIED.);
#1014=B_SPLINE_CURVE_WITH_KNOTS('',3,(#126925,#126926,#126927,#126928,#126929,
#126930,#126931,#126932,#126933,#126934,#126935,#126936,#126937,#126938,
#126939,#126940,#126941,#126942,#126943,#126944,#126945,#126946,#126947,
#126948,#126949,#126950,#126951,#126952,#126953,#126954,#126955,#126956,
#126957,#126958,#126959,#126960,#126961,#126962,#126963,#126964,#126965,
#126966,#126967,#126968,#126969,#126970,#126971,#126972,#126973,#126974,
#126975,#126976,#126977,#126978,#126979,#126980,#126981,#126982,#126983,
#126984,#126985,#126986,#126987,#126988,#126989,#126990,#126991,#126992,
#126993,#126994,#126995,#126996,#126997,#126998,#126999,#127000,#127001,
#127002,#127003,#127004,#127005,#127006,#127007,#127008,#127009,#127010,
#127011,#127012,#127013,#127014,#127015,#127016,#127017,#127018,#127019,
#127020,#127021,#127022,#127023,#127024,#127025,#127026,#127027,#127028,
#127029,#127030,#127031,#127032,#127033,#127034,#127035,#127036,#127037,
#127038,#127039,#127040,#127041,#127042,#127043,#127044,#127045,#127046,
#127047,#127048,#127049,#127050,#127051,#127052,#127053,#127054,#127055,
#127056,#127057,#127058,#127059,#127060,#127061,#127062,#127063,#127064,
#127065,#127066,#127067,#127068,#127069,#127070,#127071,#127072,#127073,
#127074,#127075,#127076,#127077,#127078,#127079,#127080,#127081,#127082,
#127083,#127084,#127085,#127086,#127087,#127088,#127089,#127090,#127091,
#127092,#127093,#127094,#127095,#127096,#127097,#127098,#127099,#127100,
#127101,#127102,#127103,#127104,#127105,#127106,#127107,#127108,#127109,
#127110,#127111,#127112,#127113,#127114,#127115,#127116,#127117,#127118,
#127119,#127120,#127121,#127122,#127123,#127124,#127125,#127126,#127127,
#127128,#127129,#127130,#127131,#127132,#127133,#127134,#127135,#127136,
#127137,#127138,#127139,#127140,#127141),.UNSPECIFIED.,.F.,.F.,(4,3,3,3,
3,3,3,3,3,3,3,3,3,3,3,3,3,3,3,3,3,3,3,3,3,3,3,3,3,3,3,3,3,3,3,3,3,3,3,3,
3,3,3,3,3,3,3,3,3,3,3,3,3,3,3,3,3,3,3,3,3,3,3,3,3,3,3,3,3,3,3,3,4),(1511.10606637669,
1511.21943759928,1511.30317631113,1511.38681182249,1511.47036426589,1511.55385370175,
1511.63730765236,1511.72074414621,1511.80418125596,1511.88763705088,1511.97118154361,
1512.05477062655,1512.13849389411,1512.21917361,1512.30291232185,1512.38654783321,
1512.47010027661,1512.55358971246,1512.63704366307,1512.72048015692,1512.80391726667,
1512.88737306159,1512.97091755432,1513.05450663726,1513.13822990481,1513.21890962072,
1513.30264833257,1513.38628384394,1513.46983628734,1513.5533257232,1513.63677967381,
1513.72021616766,1513.80365327742,1513.88710907234,1513.97065356507,1514.05424264802,
1514.13796591558,1514.21864563145,1514.30238434329,1514.38601985466,1514.46957229805,
1514.5530617339,1514.63651568451,1514.71995217836,1514.80338928811,1514.88684508302,
1514.97038957575,1515.05397865869,1515.13770192624,1515.21838164216,1515.30212035401,
1515.38575586537,1515.46930830877,1515.55279774463,1515.63625169524,1515.71968818909,
1515.80312529884,1515.88658109376,1515.97012558649,1516.05371466943,1516.13743793699,
1516.21811765289,1516.30186099068,1516.38550007206,1516.46905503402,1516.5526481454,
1516.63609843941,1516.71952980604,1516.8029603171,1516.8866702191,1516.97018733186,
1517.05399362848,1517.1377999251),.UNSPECIFIED.);
#1015=B_SPLINE_CURVE_WITH_KNOTS('',3,(#127147,#127148,#127149,#127150,#127151,
#127152,#127153,#127154,#127155,#127156,#127157,#127158,#127159,#127160,
#127161,#127162,#127163,#127164,#127165,#127166,#127167,#127168,#127169,
#127170,#127171,#127172,#127173,#127174,#127175,#127176,#127177,#127178,
#127179,#127180,#127181,#127182,#127183,#127184,#127185,#127186,#127187,
#127188,#127189,#127190,#127191,#127192,#127193,#127194,#127195,#127196,
#127197,#127198,#127199,#127200,#127201,#127202,#127203,#127204,#127205,
#127206,#127207,#127208,#127209,#127210,#127211,#127212,#127213,#127214,
#127215,#127216,#127217,#127218,#127219,#127220,#127221,#127222,#127223,
#127224,#127225,#127226,#127227,#127228,#127229,#127230,#127231,#127232,
#127233,#127234,#127235,#127236,#127237,#127238,#127239,#127240,#127241,
#127242,#127243,#127244,#127245,#127246,#127247,#127248,#127249,#127250,
#127251,#127252,#127253,#127254,#127255,#127256,#127257,#127258,#127259,
#127260,#127261,#127262,#127263,#127264,#127265,#127266,#127267,#127268,
#127269,#127270,#127271,#127272,#127273,#127274,#127275,#127276,#127277,
#127278,#127279,#127280,#127281,#127282,#127283,#127284,#127285,#127286,
#127287,#127288,#127289,#127290,#127291,#127292,#127293,#127294,#127295,
#127296,#127297,#127298,#127299,#127300,#127301,#127302,#127303,#127304,
#127305,#127306,#127307,#127308,#127309,#127310,#127311,#127312,#127313,
#127314,#127315,#127316,#127317,#127318,#127319,#127320,#127321,#127322,
#127323,#127324,#127325,#127326,#127327,#127328,#127329,#127330,#127331,
#127332,#127333,#127334,#127335,#127336,#127337,#127338,#127339,#127340,
#127341,#127342,#127343,#127344,#127345,#127346,#127347,#127348,#127349,
#127350,#127351,#127352,#127353,#127354,#127355,#127356,#127357,#127358,
#127359,#127360,#127361,#127362,#127363,#127364,#127365,#127366),
 .UNSPECIFIED.,.F.,.F.,(4,3,3,3,3,3,3,3,3,3,3,3,3,3,3,3,3,3,3,3,3,3,3,3,
3,3,3,3,3,3,3,3,3,3,3,3,3,3,3,3,3,3,3,3,3,3,3,3,3,3,3,3,3,3,3,3,3,3,3,3,
3,3,3,3,3,3,3,3,3,3,3,3,3,4),(1517.38925168386,1517.47602562373,1517.56289209464,
1517.64994290237,1517.73708792198,1517.82443009038,1517.90729905461,1517.99103776646,
1518.07467327782,1518.15822572122,1518.24171515707,1518.32516910769,1518.40860560153,
1518.49204271129,1518.57549850621,1518.65904299894,1518.74263208188,1518.82635534944,
1518.90703506533,1518.99077377718,1519.07440928854,1519.15796173194,1519.24145116779,
1519.32490511841,1519.40834161225,1519.49177872201,1519.57523451692,1519.65877900965,
1519.74236809259,1519.82609136015,1519.90677107605,1519.9905097879,1520.07414529926,
1520.15769774266,1520.24118717851,1520.32464112913,1520.40807762297,1520.49151473273,
1520.57497052765,1520.65851502038,1520.74210410332,1520.82582737088,1520.90650708677,
1520.99024579862,1521.07388130998,1521.15743375338,1521.24092318923,1521.32437713985,
1521.40781363369,1521.49125074345,1521.57470653837,1521.6582510311,1521.74184011404,
1521.8255633816,1521.90624309749,1521.98998180934,1522.0736173207,1522.1571697641,
1522.24065919995,1522.32411315057,1522.40754964441,1522.49098675417,1522.57444254909,
1522.65798704182,1522.74157612476,1522.82529939231,1522.90597910821,1522.98863711599,
1523.07119771625,1523.15368002176,1523.23609810398,1523.31847966571,1523.40084881881,
1523.42099381078),.UNSPECIFIED.);
#1016=B_SPLINE_CURVE_WITH_KNOTS('',3,(#127367,#127368,#127369,#127370,#127371,
#127372,#127373,#127374,#127375,#127376),.UNSPECIFIED.,.F.,.F.,(4,3,3,4),
(1517.13894299318,1517.22727810457,1517.31541712171,1517.38925168369),
 .UNSPECIFIED.);
#1017=B_SPLINE_CURVE_WITH_KNOTS('',3,(#127378,#127379,#127380,#127381,#127382,
#127383,#127384,#127385,#127386,#127387),.UNSPECIFIED.,.F.,.F.,(4,3,3,4),
(1517.1377999251,1517.21785366361,1517.34872141794,1517.38925168387),
 .UNSPECIFIED.);
#1018=B_SPLINE_CURVE_WITH_KNOTS('',3,(#127388,#127389,#127390,#127391,#127392,
#127393,#127394,#127395,#127396,#127397,#127398,#127399,#127400,#127401,
#127402,#127403,#127404,#127405,#127406,#127407,#127408,#127409,#127410,
#127411,#127412,#127413,#127414,#127415,#127416,#127417,#127418,#127419,
#127420,#127421,#127422,#127423,#127424,#127425,#127426,#127427,#127428,
#127429,#127430,#127431,#127432,#127433,#127434,#127435,#127436,#127437,
#127438,#127439,#127440,#127441,#127442,#127443,#127444,#127445,#127446,
#127447,#127448,#127449,#127450,#127451,#127452,#127453,#127454,#127455,
#127456,#127457,#127458,#127459,#127460,#127461,#127462,#127463,#127464,
#127465,#127466,#127467,#127468,#127469,#127470,#127471,#127472,#127473,
#127474,#127475,#127476,#127477,#127478,#127479,#127480,#127481,#127482,
#127483,#127484,#127485,#127486,#127487,#127488,#127489,#127490,#127491,
#127492,#127493,#127494,#127495,#127496,#127497,#127498,#127499,#127500,
#127501,#127502,#127503,#127504,#127505,#127506,#127507,#127508,#127509,
#127510,#127511,#127512,#127513,#127514,#127515,#127516,#127517,#127518,
#127519,#127520,#127521,#127522,#127523,#127524,#127525,#127526,#127527,
#127528,#127529,#127530,#127531,#127532,#127533,#127534,#127535,#127536,
#127537,#127538,#127539,#127540,#127541,#127542,#127543,#127544,#127545,
#127546,#127547,#127548,#127549,#127550,#127551,#127552,#127553,#127554,
#127555,#127556,#127557,#127558,#127559,#127560,#127561,#127562,#127563,
#127564,#127565,#127566,#127567,#127568,#127569,#127570,#127571,#127572,
#127573,#127574,#127575,#127576,#127577,#127578,#127579,#127580,#127581,
#127582,#127583,#127584,#127585,#127586,#127587,#127588,#127589,#127590,
#127591,#127592,#127593,#127594,#127595,#127596,#127597,#127598,#127599,
#127600,#127601,#127602,#127603,#127604,#127605,#127606,#127607),
 .UNSPECIFIED.,.F.,.F.,(4,3,3,3,3,3,3,3,3,3,3,3,3,3,3,3,3,3,3,3,3,3,3,3,
3,3,3,3,3,3,3,3,3,3,3,3,3,3,3,3,3,3,3,3,3,3,3,3,3,3,3,3,3,3,3,3,3,3,3,3,
3,3,3,3,3,3,3,3,3,3,3,3,3,4),(1517.38925168405,1517.47161907531,1517.55390965771,
1517.63686965979,1517.71907915193,1517.80127988251,1517.88349088499,1517.96701558232,
1518.04934654739,1518.13346811086,1518.21758967433,1518.30132838618,1518.38496389754,
1518.46851634094,1518.55200577679,1518.63545972741,1518.71889622125,1518.80233333101,
1518.88578912593,1518.96933361866,1519.0529227016,1519.13664596916,1519.21732568505,
1519.3010643969,1519.38469990826,1519.46825235166,1519.55174178751,1519.63519573813,
1519.71863223197,1519.80206934173,1519.88552513665,1519.96906962938,1520.05265871232,
1520.13638197987,1520.21706169577,1520.30080040762,1520.38443591898,1520.46798836238,
1520.55147779823,1520.63493174885,1520.71836824269,1520.80180535245,1520.88526114737,
1520.9688056401,1521.05239472304,1521.13611799059,1521.21679770649,1521.30053641834,
1521.3841719297,1521.4677243731,1521.55121380895,1521.63466775957,1521.71810425341,
1521.80154136317,1521.88499715809,1521.96854165082,1522.05213073376,1522.13585400131,
1522.21653371721,1522.30027242906,1522.38390794042,1522.46746038382,1522.55094981967,
1522.63440377029,1522.71784026413,1522.80127737389,1522.88473316881,1522.96827766154,
1523.05186674448,1523.13559001203,1523.21626972793,1523.30626667354,1523.39603949157,
1523.42213509551),.UNSPECIFIED.);
#1019=B_SPLINE_CURVE_WITH_KNOTS('',3,(#127613,#127614,#127615,#127616,#127617,
#127618,#127619,#127620,#127621,#127622,#127623,#127624,#127625,#127626,
#127627,#127628,#127629,#127630,#127631,#127632,#127633,#127634,#127635,
#127636,#127637,#127638,#127639,#127640,#127641,#127642,#127643,#127644,
#127645,#127646,#127647,#127648,#127649,#127650,#127651,#127652,#127653,
#127654,#127655,#127656,#127657,#127658,#127659,#127660,#127661,#127662,
#127663,#127664,#127665,#127666,#127667,#127668,#127669,#127670,#127671,
#127672,#127673,#127674,#127675,#127676,#127677,#127678,#127679,#127680,
#127681,#127682,#127683,#127684,#127685,#127686,#127687,#127688,#127689,
#127690,#127691,#127692,#127693,#127694,#127695,#127696,#127697,#127698,
#127699,#127700,#127701,#127702,#127703,#127704,#127705,#127706,#127707,
#127708,#127709,#127710,#127711,#127712,#127713,#127714,#127715,#127716,
#127717,#127718,#127719,#127720,#127721,#127722,#127723,#127724,#127725,
#127726,#127727,#127728,#127729,#127730,#127731,#127732,#127733,#127734,
#127735,#127736,#127737,#127738,#127739,#127740,#127741,#127742,#127743,
#127744,#127745,#127746,#127747,#127748,#127749,#127750,#127751,#127752,
#127753,#127754,#127755,#127756,#127757,#127758,#127759,#127760,#127761,
#127762,#127763,#127764,#127765,#127766,#127767,#127768,#127769,#127770,
#127771,#127772,#127773,#127774,#127775,#127776,#127777,#127778,#127779,
#127780,#127781,#127782,#127783,#127784,#127785,#127786,#127787,#127788,
#127789,#127790,#127791,#127792,#127793,#127794,#127795,#127796,#127797,
#127798,#127799,#127800,#127801,#127802,#127803,#127804,#127805,#127806,
#127807,#127808,#127809,#127810,#127811,#127812,#127813,#127814,#127815,
#127816,#127817,#127818,#127819,#127820,#127821,#127822,#127823,#127824,
#127825,#127826,#127827,#127828,#127829,#127830,#127831,#127832),
 .UNSPECIFIED.,.F.,.F.,(4,3,3,3,3,3,3,3,3,3,3,3,3,3,3,3,3,3,3,3,3,3,3,3,
3,3,3,3,3,3,3,3,3,3,3,3,3,3,3,3,3,3,3,3,3,3,3,3,3,3,3,3,3,3,3,3,3,3,3,3,
3,3,3,3,3,3,3,3,3,3,3,3,3,4),(1523.67243699115,1523.78258462893,1523.89582452207,
1523.90571511893,1523.98945383078,1524.07308934214,1524.15664178554,1524.24013122139,
1524.32358517201,1524.40702166585,1524.49045877561,1524.57391457053,1524.65745906326,
1524.7410481462,1524.82477141375,1524.90545112965,1524.9891898415,1525.07282535286,
1525.15637779626,1525.23986723211,1525.32332118273,1525.40675767657,1525.49019478633,
1525.57365058124,1525.65719507397,1525.74078415691,1525.82450742447,1525.90518714037,
1525.98892585222,1526.07256136358,1526.15611380698,1526.23960324283,1526.32305719345,
1526.40649368729,1526.48993079705,1526.57338659197,1526.6569310847,1526.74052016764,
1526.82424343519,1526.90492315109,1526.98866186294,1527.0722973743,1527.1558498177,
1527.23933925355,1527.32279320417,1527.40622969801,1527.48966680777,1527.57312260269,
1527.65666709542,1527.74025617836,1527.82397944591,1527.90465916181,1527.98839787366,
1528.07203338502,1528.15558582842,1528.23907526427,1528.32252921489,1528.40596570873,
1528.48940281849,1528.57285861341,1528.65640310614,1528.73999218908,1528.82371545664,
1528.90439517253,1528.98814598813,1529.0717909624,1529.1553347027,1529.23882103833,
1529.32226808954,1529.40569394618,1529.48914071552,1529.5725981172,1529.65611866871,
1529.70395727207),.UNSPECIFIED.);
#1020=B_SPLINE_CURVE_WITH_KNOTS('',3,(#127833,#127834,#127835,#127836,#127837,
#127838,#127839,#127840,#127841,#127842),.UNSPECIFIED.,.F.,.F.,(4,3,3,4),
(1523.42099381078,1523.50338958302,1523.58791328703,1523.67243699104),
 .UNSPECIFIED.);
#1021=B_SPLINE_CURVE_WITH_KNOTS('',3,(#127844,#127845,#127846,#127847,#127848,
#127849,#127850,#127851,#127852,#127853),.UNSPECIFIED.,.F.,.F.,(4,3,3,4),
(1523.42213509551,1523.51162295178,1523.60085738858,1523.67243699087),
 .UNSPECIFIED.);
#1022=B_SPLINE_CURVE_WITH_KNOTS('',3,(#127854,#127855,#127856,#127857,#127858,
#127859,#127860,#127861,#127862,#127863,#127864,#127865,#127866,#127867,
#127868,#127869,#127870,#127871,#127872,#127873,#127874,#127875,#127876,
#127877,#127878,#127879,#127880,#127881,#127882,#127883,#127884,#127885,
#127886,#127887,#127888,#127889,#127890,#127891,#127892,#127893,#127894,
#127895,#127896,#127897,#127898,#127899,#127900,#127901,#127902,#127903,
#127904,#127905,#127906,#127907,#127908,#127909,#127910,#127911,#127912,
#127913,#127914,#127915,#127916,#127917,#127918,#127919,#127920,#127921,
#127922,#127923,#127924,#127925,#127926,#127927,#127928,#127929,#127930,
#127931,#127932,#127933,#127934,#127935,#127936,#127937,#127938,#127939,
#127940,#127941,#127942,#127943,#127944,#127945,#127946,#127947,#127948,
#127949,#127950,#127951,#127952,#127953,#127954,#127955,#127956,#127957,
#127958,#127959,#127960,#127961,#127962,#127963,#127964,#127965,#127966,
#127967,#127968,#127969,#127970,#127971,#127972,#127973,#127974,#127975,
#127976,#127977,#127978,#127979,#127980,#127981,#127982,#127983,#127984,
#127985,#127986,#127987,#127988,#127989,#127990,#127991,#127992,#127993,
#127994,#127995,#127996,#127997,#127998,#127999,#128000,#128001,#128002,
#128003,#128004,#128005,#128006,#128007,#128008,#128009,#128010,#128011,
#128012,#128013,#128014,#128015,#128016,#128017,#128018,#128019,#128020,
#128021,#128022,#128023,#128024,#128025,#128026,#128027,#128028,#128029,
#128030,#128031,#128032,#128033,#128034,#128035,#128036,#128037,#128038,
#128039,#128040,#128041,#128042,#128043,#128044,#128045,#128046,#128047,
#128048,#128049,#128050,#128051,#128052,#128053,#128054,#128055,#128056,
#128057,#128058,#128059,#128060,#128061,#128062,#128063,#128064,#128065,
#128066,#128067,#128068,#128069,#128070,#128071,#128072,#128073),
 .UNSPECIFIED.,.F.,.F.,(4,3,3,3,3,3,3,3,3,3,3,3,3,3,3,3,3,3,3,3,3,3,3,3,
3,3,3,3,3,3,3,3,3,3,3,3,3,3,3,3,3,3,3,3,3,3,3,3,3,3,3,3,3,3,3,3,3,3,3,3,
3,3,3,3,3,3,3,3,3,3,3,3,3,4),(1523.67243699105,1523.75841773458,1523.8444644582,
1523.93059030503,1524.01687033097,1524.10323851992,1524.18976393114,1524.21600573865,
1524.2997444505,1524.38337996186,1524.46693240526,1524.55042184111,1524.63387579173,
1524.71731228557,1524.80074939533,1524.88420519025,1524.96774968298,1525.05133876592,
1525.13506203347,1525.21574174937,1525.29948046122,1525.38311597258,1525.46666841598,
1525.55015785183,1525.63361180245,1525.71704829629,1525.80048540605,1525.88394120097,
1525.96748569369,1526.05107477664,1526.13479804419,1526.21547776009,1526.29921647194,
1526.3828519833,1526.4664044267,1526.54989386255,1526.63334781317,1526.71678430701,
1526.80022141677,1526.88367721169,1526.96722170441,1527.05081078736,1527.13453405491,
1527.21521377081,1527.29895248266,1527.38258799402,1527.46614043742,1527.54962987327,
1527.63308382389,1527.71652031773,1527.79995742749,1527.88341322241,1527.96695771514,
1528.05054679808,1528.13427006563,1528.21494978153,1528.29868849338,1528.38232400474,
1528.46587644814,1528.54936588399,1528.63281983461,1528.71625632845,1528.79969343821,
1528.88314923313,1528.96669372586,1529.0502828088,1529.13400607636,1529.21468579225,
1529.29752113583,1529.3802577084,1529.46290141179,1529.54549048635,1529.62805090444,
1529.7043027577),.UNSPECIFIED.);
#1023=B_SPLINE_CURVE_WITH_KNOTS('',3,(#128079,#128080,#128081,#128082,#128083,
#128084,#128085,#128086,#128087,#128088,#128089,#128090,#128091,#128092,
#128093,#128094,#128095,#128096,#128097,#128098,#128099,#128100,#128101,
#128102,#128103,#128104,#128105,#128106,#128107,#128108,#128109,#128110,
#128111,#128112,#128113,#128114,#128115,#128116,#128117,#128118,#128119,
#128120,#128121,#128122,#128123,#128124,#128125,#128126,#128127,#128128,
#128129,#128130,#128131,#128132,#128133,#128134,#128135,#128136,#128137,
#128138,#128139,#128140,#128141,#128142,#128143,#128144,#128145,#128146,
#128147,#128148,#128149,#128150,#128151,#128152,#128153,#128154,#128155,
#128156,#128157,#128158,#128159,#128160,#128161,#128162,#128163,#128164,
#128165,#128166,#128167,#128168,#128169,#128170,#128171,#128172,#128173,
#128174,#128175,#128176,#128177,#128178,#128179,#128180,#128181,#128182,
#128183,#128184,#128185,#128186,#128187,#128188,#128189,#128190,#128191,
#128192,#128193,#128194,#128195,#128196,#128197,#128198,#128199,#128200,
#128201,#128202,#128203,#128204,#128205,#128206,#128207,#128208,#128209,
#128210,#128211,#128212,#128213,#128214,#128215,#128216,#128217,#128218,
#128219,#128220,#128221,#128222,#128223,#128224,#128225,#128226,#128227,
#128228,#128229,#128230,#128231,#128232,#128233,#128234,#128235,#128236,
#128237,#128238,#128239,#128240,#128241,#128242,#128243,#128244,#128245,
#128246,#128247,#128248,#128249,#128250,#128251,#128252,#128253,#128254,
#128255,#128256,#128257,#128258,#128259,#128260,#128261,#128262,#128263,
#128264,#128265,#128266,#128267,#128268,#128269,#128270,#128271,#128272,
#128273,#128274,#128275,#128276,#128277,#128278,#128279,#128280,#128281,
#128282,#128283,#128284,#128285,#128286,#128287,#128288,#128289,#128290,
#128291,#128292,#128293,#128294,#128295,#128296,#128297,#128298),
 .UNSPECIFIED.,.F.,.F.,(4,3,3,3,3,3,3,3,3,3,3,3,3,3,3,3,3,3,3,3,3,3,3,3,
3,3,3,3,3,3,3,3,3,3,3,3,3,3,3,3,3,3,3,3,3,3,3,3,3,3,3,3,3,3,3,3,3,3,3,3,
3,3,3,3,3,3,3,3,3,3,3,3,3,4),(1529.95562229842,1530.03869000497,1530.12165783729,
1530.2045465541,1530.28737683683,1530.37017812198,1530.4529672259,1530.53576278341,
1530.6185834307,1530.70149397743,1530.78445594191,1530.86753831501,1530.90386719397,
1530.98760590582,1531.07124141718,1531.15479386058,1531.23828329643,1531.32173724705,
1531.40517374089,1531.48861085065,1531.57206664557,1531.6556111383,1531.73920022124,
1531.82292348879,1531.90360320469,1531.98734191654,1532.0709774279,1532.1545298713,
1532.23801930715,1532.32147325777,1532.40490975161,1532.48834686137,1532.57180265629,
1532.65534714902,1532.73893623196,1532.82265949951,1532.90333921541,1532.98707792726,
1533.07071343862,1533.15426588202,1533.23775531787,1533.32120926849,1533.40464576233,
1533.48808287209,1533.57153866701,1533.65508315974,1533.73867224268,1533.82239551023,
1533.90307522613,1533.98681393798,1534.07044944934,1534.15400189274,1534.23749132859,
1534.32094527921,1534.40438177305,1534.48781888281,1534.57127467773,1534.65481917046,
1534.7384082534,1534.82213152096,1534.90281123685,1534.9865499487,1535.07018546006,
1535.15373790346,1535.23722733931,1535.32068128993,1535.40411778377,1535.48755489353,
1535.57101068844,1535.65455518117,1535.73814426412,1535.82186753167,1535.90254724757,
1535.98821483034),.UNSPECIFIED.);
#1024=B_SPLINE_CURVE_WITH_KNOTS('',3,(#128299,#128300,#128301,#128302,#128303,
#128304,#128305,#128306,#128307,#128308,#128309,#128310,#128311),
 .UNSPECIFIED.,.F.,.F.,(4,3,3,3,4),(1529.70395727207,1529.78757918107,1529.87132176391,
1529.90413118325,1529.95562229822),.UNSPECIFIED.);
#1025=B_SPLINE_CURVE_WITH_KNOTS('',3,(#128313,#128314,#128315,#128316,#128317,
#128318,#128319,#128320,#128321,#128322),.UNSPECIFIED.,.F.,.F.,(4,3,3,4),
(1529.7043027577,1529.78685599116,1529.87123914469,1529.95562229823),
 .UNSPECIFIED.);
#1026=B_SPLINE_CURVE_WITH_KNOTS('',3,(#128323,#128324,#128325,#128326,#128327,
#128328,#128329,#128330,#128331,#128332,#128333,#128334,#128335,#128336,
#128337,#128338,#128339,#128340,#128341,#128342,#128343,#128344,#128345,
#128346,#128347,#128348,#128349,#128350,#128351,#128352,#128353,#128354,
#128355,#128356,#128357,#128358,#128359,#128360,#128361,#128362,#128363,
#128364,#128365,#128366,#128367,#128368,#128369,#128370,#128371,#128372,
#128373,#128374,#128375,#128376,#128377,#128378,#128379,#128380,#128381,
#128382,#128383,#128384,#128385,#128386,#128387,#128388,#128389,#128390,
#128391,#128392,#128393,#128394,#128395,#128396,#128397,#128398,#128399,
#128400,#128401,#128402,#128403,#128404,#128405,#128406,#128407,#128408,
#128409,#128410,#128411,#128412,#128413,#128414,#128415,#128416,#128417,
#128418,#128419,#128420,#128421,#128422,#128423,#128424,#128425,#128426,
#128427,#128428,#128429,#128430,#128431,#128432,#128433,#128434,#128435,
#128436,#128437,#128438,#128439,#128440,#128441,#128442,#128443,#128444,
#128445,#128446,#128447,#128448,#128449,#128450,#128451,#128452,#128453,
#128454,#128455,#128456,#128457,#128458,#128459,#128460,#128461,#128462,
#128463,#128464,#128465,#128466,#128467,#128468,#128469,#128470,#128471,
#128472,#128473,#128474,#128475,#128476,#128477,#128478,#128479,#128480,
#128481,#128482,#128483,#128484,#128485,#128486,#128487,#128488,#128489,
#128490,#128491,#128492,#128493,#128494,#128495,#128496,#128497,#128498,
#128499,#128500,#128501,#128502,#128503,#128504,#128505,#128506,#128507,
#128508,#128509,#128510,#128511,#128512,#128513,#128514,#128515,#128516,
#128517,#128518,#128519,#128520,#128521,#128522,#128523,#128524,#128525,
#128526,#128527,#128528,#128529,#128530,#128531,#128532,#128533,#128534,
#128535,#128536,#128537,#128538,#128539,#128540,#128541,#128542),
 .UNSPECIFIED.,.F.,.F.,(4,3,3,3,3,3,3,3,3,3,3,3,3,3,3,3,3,3,3,3,3,3,3,3,
3,3,3,3,3,3,3,3,3,3,3,3,3,3,3,3,3,3,3,3,3,3,3,3,3,3,3,3,3,3,3,3,3,3,3,3,
3,3,3,3,3,3,3,3,3,3,3,3,3,4),(1529.95562229836,1530.06149157749,1530.16950984213,
1530.21442180297,1530.29816051482,1530.38179602618,1530.46534846958,1530.54883790543,
1530.63229185605,1530.71572834989,1530.79916545965,1530.88262125457,1530.9661657473,
1531.04975483024,1531.13347809779,1531.21415781369,1531.29789652554,1531.3815320369,
1531.4650844803,1531.54857391615,1531.63202786677,1531.71546436061,1531.79890147037,
1531.88235726529,1531.96590175802,1532.04949084096,1532.13321410851,1532.21389382441,
1532.29763253626,1532.38126804762,1532.46482049102,1532.54830992687,1532.63176387749,
1532.71520037133,1532.79863748109,1532.88209327601,1532.96563776874,1533.04922685168,
1533.13295011923,1533.21362983513,1533.29736854698,1533.38100405834,1533.46455650174,
1533.54804593759,1533.63149988821,1533.71493638205,1533.79837349181,1533.88182928673,
1533.96537377946,1534.0489628624,1534.13268612995,1534.21336584585,1534.2971045577,
1534.38074006906,1534.46429251246,1534.54778194831,1534.63123589893,1534.71467239277,
1534.79810950253,1534.88156529745,1534.96510979018,1535.04869887312,1535.13242214067,
1535.21310185657,1535.29685434383,1535.38314048142,1535.46668270487,1535.55016761907,
1535.63361334401,1535.71703796925,1535.80047957901,1535.88393214105,1535.96743749394,
1535.98714344461),.UNSPECIFIED.);
#1027=B_SPLINE_CURVE_WITH_KNOTS('',3,(#128548,#128549,#128550,#128551,#128552,
#128553,#128554,#128555,#128556,#128557,#128558,#128559,#128560,#128561,
#128562,#128563,#128564,#128565,#128566,#128567,#128568,#128569,#128570,
#128571,#128572,#128573,#128574,#128575,#128576,#128577,#128578,#128579,
#128580,#128581,#128582,#128583,#128584,#128585,#128586,#128587,#128588,
#128589,#128590,#128591,#128592,#128593,#128594,#128595,#128596,#128597,
#128598,#128599,#128600,#128601,#128602,#128603,#128604,#128605,#128606,
#128607,#128608,#128609,#128610,#128611,#128612,#128613,#128614,#128615,
#128616,#128617,#128618,#128619,#128620,#128621,#128622,#128623,#128624,
#128625,#128626,#128627,#128628,#128629,#128630,#128631,#128632,#128633,
#128634,#128635,#128636,#128637,#128638,#128639,#128640,#128641,#128642,
#128643,#128644,#128645,#128646,#128647,#128648,#128649,#128650,#128651,
#128652,#128653,#128654,#128655,#128656,#128657,#128658,#128659,#128660,
#128661,#128662,#128663,#128664,#128665,#128666,#128667,#128668,#128669,
#128670,#128671,#128672,#128673,#128674,#128675,#128676,#128677,#128678,
#128679,#128680,#128681,#128682,#128683,#128684,#128685,#128686,#128687,
#128688,#128689,#128690,#128691,#128692,#128693,#128694,#128695,#128696,
#128697,#128698,#128699,#128700,#128701,#128702,#128703,#128704,#128705,
#128706,#128707,#128708,#128709,#128710,#128711,#128712,#128713,#128714,
#128715,#128716,#128717,#128718,#128719,#128720,#128721,#128722,#128723,
#128724,#128725,#128726,#128727,#128728,#128729,#128730,#128731,#128732,
#128733,#128734,#128735,#128736,#128737,#128738,#128739,#128740,#128741,
#128742,#128743,#128744,#128745,#128746,#128747,#128748,#128749,#128750,
#128751,#128752,#128753,#128754,#128755,#128756,#128757,#128758,#128759,
#128760,#128761,#128762,#128763,#128764,#128765,#128766,#128767),
 .UNSPECIFIED.,.F.,.F.,(4,3,3,3,3,3,3,3,3,3,3,3,3,3,3,3,3,3,3,3,3,3,3,3,
3,3,3,3,3,3,3,3,3,3,3,3,3,3,3,3,3,3,3,3,3,3,3,3,3,3,3,3,3,3,3,3,3,3,3,3,
3,3,3,3,3,3,3,3,3,3,3,3,3,4),(1536.2388076054,1536.32223627499,1536.40565287209,
1536.48907540985,1536.5725219015,1536.65606475899,1536.7396566576,1536.82338883274,
1536.90228325829,1536.98602197014,1537.0696574815,1537.1532099249,1537.23669936075,
1537.32015331137,1537.40358980521,1537.48702691497,1537.57048270989,1537.65402720262,
1537.73761628556,1537.82133955312,1537.90201926901,1537.98575798086,1538.06939349222,
1538.15294593562,1538.23643537147,1538.31988932209,1538.40332581593,1538.48676292569,
1538.57021872061,1538.65376321333,1538.73735229628,1538.82107556383,1538.90175527973,
1538.98549399158,1539.06912950294,1539.15268194634,1539.23617138219,1539.31962533281,
1539.40306182665,1539.48649893641,1539.56995473132,1539.65349922405,1539.737088307,
1539.82081157455,1539.90149129045,1539.9852300023,1540.06886551366,1540.15241795706,
1540.23590739291,1540.31936134353,1540.40279783737,1540.48623494713,1540.56969074205,
1540.65323523478,1540.73682431772,1540.82054758528,1540.90122730117,1540.98496601302,
1541.06860152438,1541.15215396778,1541.23564340363,1541.31909735425,1541.40253384809,
1541.48597095785,1541.56942675276,1541.65297124549,1541.73656032843,1541.82028359599,
1541.90096331189,1541.98550083738,1542.06989404209,1542.15420375164,1542.23843095987,
1542.27128066288),.UNSPECIFIED.);
#1028=B_SPLINE_CURVE_WITH_KNOTS('',3,(#128768,#128769,#128770,#128771,#128772,
#128773,#128774,#128775,#128776,#128777),.UNSPECIFIED.,.F.,.F.,(4,3,3,4),
(1535.98821483034,1536.08596364199,1536.18288058848,1536.23880760521),
 .UNSPECIFIED.);
#1029=B_SPLINE_CURVE_WITH_KNOTS('',3,(#128779,#128780,#128781,#128782,#128783,
#128784,#128785,#128786,#128787,#128788,#128789,#128790,#128791),
 .UNSPECIFIED.,.F.,.F.,(4,3,3,3,4),(1535.98714344461,1536.07074717287,1536.15447863248,
1536.21283786729,1536.23880760541),.UNSPECIFIED.);
#1030=B_SPLINE_CURVE_WITH_KNOTS('',3,(#128792,#128793,#128794,#128795,#128796,
#128797,#128798,#128799,#128800,#128801,#128802,#128803,#128804,#128805,
#128806,#128807,#128808,#128809,#128810,#128811,#128812,#128813,#128814,
#128815,#128816,#128817,#128818,#128819,#128820,#128821,#128822,#128823,
#128824,#128825,#128826,#128827,#128828,#128829,#128830,#128831,#128832,
#128833,#128834,#128835,#128836,#128837,#128838,#128839,#128840,#128841,
#128842,#128843,#128844,#128845,#128846,#128847,#128848,#128849,#128850,
#128851,#128852,#128853,#128854,#128855,#128856,#128857,#128858,#128859,
#128860,#128861,#128862,#128863,#128864,#128865,#128866,#128867,#128868,
#128869,#128870,#128871,#128872,#128873,#128874,#128875,#128876,#128877,
#128878,#128879,#128880,#128881,#128882,#128883,#128884,#128885,#128886,
#128887,#128888,#128889,#128890,#128891,#128892,#128893,#128894,#128895,
#128896,#128897,#128898,#128899,#128900,#128901,#128902,#128903,#128904,
#128905,#128906,#128907,#128908,#128909,#128910,#128911,#128912,#128913,
#128914,#128915,#128916,#128917,#128918,#128919,#128920,#128921,#128922,
#128923,#128924,#128925,#128926,#128927,#128928,#128929,#128930,#128931,
#128932,#128933,#128934,#128935,#128936,#128937,#128938,#128939,#128940,
#128941,#128942,#128943,#128944,#128945,#128946,#128947,#128948,#128949,
#128950,#128951,#128952,#128953,#128954,#128955,#128956,#128957,#128958,
#128959,#128960,#128961,#128962,#128963,#128964,#128965,#128966,#128967,
#128968,#128969,#128970,#128971,#128972,#128973,#128974,#128975,#128976,
#128977,#128978,#128979,#128980,#128981,#128982,#128983,#128984,#128985,
#128986,#128987,#128988,#128989,#128990,#128991,#128992,#128993,#128994,
#128995,#128996,#128997,#128998,#128999,#129000,#129001,#129002,#129003,
#129004,#129005,#129006,#129007,#129008,#129009,#129010,#129011),
 .UNSPECIFIED.,.F.,.F.,(4,3,3,3,3,3,3,3,3,3,3,3,3,3,3,3,3,3,3,3,3,3,3,3,
3,3,3,3,3,3,3,3,3,3,3,3,3,3,3,3,3,3,3,3,3,3,3,3,3,3,3,3,3,3,3,3,3,3,3,3,
3,3,3,3,3,3,3,3,3,3,3,3,3,4),(1536.23880760553,1536.32217949724,1536.40544918826,
1536.48863717929,1536.57176389602,1536.65485772805,1536.73793634554,1536.82101815004,
1536.90412154168,1536.98731402283,1537.07055432919,1537.15392182379,1537.21257387801,
1537.29631258986,1537.37994810122,1537.46350054462,1537.54698998047,1537.63044393109,
1537.71388042493,1537.79731753469,1537.88077332961,1537.96431782234,1538.04790690528,
1538.13163017283,1538.21230988873,1538.29604860058,1538.37968411194,1538.46323655534,
1538.54672599119,1538.63017994181,1538.71361643565,1538.79705354541,1538.88050934033,
1538.96405383306,1539.047642916,1539.13136618355,1539.21204589945,1539.2957846113,
1539.37942012266,1539.46297256606,1539.54646200191,1539.62991595253,1539.71335244637,
1539.79678955613,1539.88024535105,1539.96378984378,1540.04737892672,1540.13110219427,
1540.21178191017,1540.29552062202,1540.37915613338,1540.46270857678,1540.54619801263,
1540.62965196325,1540.71308845709,1540.79652556685,1540.87998136177,1540.96352585449,
1541.04711493744,1541.13083820499,1541.21151792089,1541.29525663274,1541.3788921441,
1541.4624445875,1541.54593402335,1541.62938797397,1541.71282446781,1541.79626157757,
1541.87971737249,1541.96326186522,1542.04685094816,1542.13057421572,1542.21125393161,
1542.27127577894),.UNSPECIFIED.);
#1031=B_SPLINE_CURVE_WITH_KNOTS('',3,(#129017,#129018,#129019,#129020,#129021,
#129022,#129023,#129024,#129025,#129026,#129027,#129028,#129029,#129030,
#129031,#129032,#129033,#129034,#129035,#129036,#129037,#129038,#129039,
#129040,#129041,#129042,#129043,#129044,#129045,#129046,#129047,#129048,
#129049,#129050,#129051,#129052,#129053,#129054,#129055,#129056,#129057,
#129058,#129059,#129060,#129061,#129062,#129063,#129064,#129065,#129066,
#129067,#129068,#129069,#129070,#129071,#129072,#129073,#129074,#129075,
#129076,#129077,#129078,#129079,#129080,#129081,#129082,#129083,#129084,
#129085,#129086,#129087,#129088,#129089,#129090,#129091,#129092,#129093,
#129094,#129095,#129096,#129097,#129098,#129099,#129100,#129101,#129102,
#129103,#129104,#129105,#129106,#129107,#129108,#129109,#129110,#129111,
#129112,#129113,#129114,#129115,#129116,#129117,#129118,#129119,#129120,
#129121,#129122,#129123,#129124,#129125,#129126,#129127,#129128,#129129,
#129130,#129131,#129132,#129133,#129134,#129135,#129136,#129137,#129138,
#129139,#129140,#129141,#129142,#129143,#129144,#129145,#129146,#129147,
#129148,#129149,#129150,#129151,#129152,#129153,#129154,#129155,#129156,
#129157,#129158,#129159,#129160,#129161,#129162,#129163,#129164,#129165,
#129166,#129167,#129168,#129169,#129170,#129171,#129172,#129173,#129174,
#129175,#129176,#129177,#129178,#129179,#129180,#129181,#129182,#129183,
#129184,#129185,#129186,#129187,#129188,#129189,#129190,#129191,#129192,
#129193,#129194,#129195,#129196,#129197,#129198,#129199,#129200,#129201,
#129202,#129203,#129204,#129205,#129206,#129207,#129208,#129209,#129210,
#129211,#129212,#129213,#129214,#129215,#129216,#129217,#129218,#129219,
#129220,#129221,#129222,#129223,#129224,#129225,#129226,#129227,#129228,
#129229,#129230,#129231,#129232,#129233),.UNSPECIFIED.,.F.,.F.,(4,3,3,3,
3,3,3,3,3,3,3,3,3,3,3,3,3,3,3,3,3,3,3,3,3,3,3,3,3,3,3,3,3,3,3,3,3,3,3,3,
3,3,3,3,3,3,3,3,3,3,3,3,3,3,3,3,3,3,3,3,3,3,3,3,3,3,3,3,3,3,3,3,4),(1542.52199291277,
1542.61666951523,1542.71070417245,1542.80570174753,1542.90069932261,1542.98443803446,
1543.06807354582,1543.15162598922,1543.23511542507,1543.31856937569,1543.40200586953,
1543.48544297929,1543.56889877421,1543.65244326694,1543.73603234988,1543.81975561743,
1543.90043533333,1543.98417404518,1544.06780955654,1544.15136199994,1544.23485143579,
1544.31830538641,1544.40174188025,1544.48517899001,1544.56863478492,1544.65217927765,
1544.73576836059,1544.81949162815,1544.90017134405,1544.9839100559,1545.06754556726,
1545.15109801066,1545.23458744651,1545.31804139713,1545.40147789097,1545.48491500073,
1545.56837079565,1545.65191528838,1545.73550437132,1545.81922763887,1545.89990735477,
1545.98364606662,1546.06728157798,1546.15083402138,1546.23432345723,1546.31777740785,
1546.40121390169,1546.48465101145,1546.56810680637,1546.6516512991,1546.73524038204,
1546.81896364959,1546.89964336549,1546.98338207734,1547.0670175887,1547.1505700321,
1547.23405946795,1547.31751341857,1547.40094991241,1547.48438702217,1547.56784281709,
1547.65138730982,1547.73497639276,1547.81869966031,1547.89937937621,1547.98208738707,
1548.0647008436,1548.14723880089,1548.22972024646,1548.31217476354,1548.39461077265,
1548.47707764694,1548.55334172014),.UNSPECIFIED.);
#1032=B_SPLINE_CURVE_WITH_KNOTS('',3,(#129234,#129235,#129236,#129237,#129238,
#129239,#129240,#129241,#129242,#129243),.UNSPECIFIED.,.F.,.F.,(4,3,3,4),
(1542.27128066288,1542.35543589376,1542.43957430175,1542.52199291258),
 .UNSPECIFIED.);
#1033=B_SPLINE_CURVE_WITH_KNOTS('',3,(#129245,#129246,#129247,#129248,#129249,
#129250,#129251,#129252,#129253,#129254),.UNSPECIFIED.,.F.,.F.,(4,3,3,4),
(1542.27127577894,1542.37175444285,1542.47113194599,1542.52199291243),
 .UNSPECIFIED.);
#1034=B_SPLINE_CURVE_WITH_KNOTS('',3,(#129255,#129256,#129257,#129258,#129259,
#129260,#129261,#129262,#129263,#129264,#129265,#129266,#129267,#129268,
#129269,#129270,#129271,#129272,#129273,#129274,#129275,#129276,#129277,
#129278,#129279,#129280,#129281,#129282,#129283,#129284,#129285,#129286,
#129287,#129288,#129289,#129290,#129291,#129292,#129293,#129294,#129295,
#129296,#129297,#129298,#129299,#129300,#129301,#129302,#129303,#129304,
#129305,#129306,#129307,#129308,#129309,#129310,#129311,#129312,#129313,
#129314,#129315,#129316,#129317,#129318,#129319,#129320,#129321,#129322,
#129323,#129324,#129325,#129326,#129327,#129328,#129329,#129330,#129331,
#129332,#129333,#129334,#129335,#129336,#129337,#129338,#129339,#129340,
#129341,#129342,#129343,#129344,#129345,#129346,#129347,#129348,#129349,
#129350,#129351,#129352,#129353,#129354,#129355,#129356,#129357,#129358,
#129359,#129360,#129361,#129362,#129363,#129364,#129365,#129366,#129367,
#129368,#129369,#129370,#129371,#129372,#129373,#129374,#129375,#129376,
#129377,#129378,#129379,#129380,#129381,#129382,#129383,#129384,#129385,
#129386,#129387,#129388,#129389,#129390,#129391,#129392,#129393,#129394,
#129395,#129396,#129397,#129398,#129399,#129400,#129401,#129402,#129403,
#129404,#129405,#129406,#129407,#129408,#129409,#129410,#129411,#129412,
#129413,#129414,#129415,#129416,#129417,#129418,#129419,#129420,#129421,
#129422,#129423,#129424,#129425,#129426,#129427,#129428,#129429,#129430,
#129431,#129432,#129433,#129434,#129435,#129436,#129437,#129438,#129439,
#129440,#129441,#129442,#129443,#129444,#129445,#129446,#129447,#129448,
#129449,#129450,#129451,#129452,#129453,#129454,#129455,#129456,#129457,
#129458,#129459,#129460,#129461,#129462,#129463,#129464,#129465,#129466,
#129467,#129468,#129469,#129470,#129471,#129472,#129473,#129474),
 .UNSPECIFIED.,.F.,.F.,(4,3,3,3,3,3,3,3,3,3,3,3,3,3,3,3,3,3,3,3,3,3,3,3,
3,3,3,3,3,3,3,3,3,3,3,3,3,3,3,3,3,3,3,3,3,3,3,3,3,3,3,3,3,3,3,3,3,3,3,3,
3,3,3,3,3,3,3,3,3,3,3,3,3,4),(1542.52199291259,1542.60811754131,1542.69119004247,
1542.77425859425,1542.85734156487,1542.94045732878,1543.02367001644,1543.10694044436,
1543.19033106149,1543.21098994233,1543.29472865418,1543.37836416554,1543.46191660894,
1543.54540604479,1543.62885999541,1543.71229648925,1543.79573359901,1543.87918939393,
1543.96273388666,1544.0463229696,1544.13004623715,1544.21072595305,1544.2944646649,
1544.37810017626,1544.46165261966,1544.54514205551,1544.62859600613,1544.71203249997,
1544.79546960973,1544.87892540465,1544.96246989738,1545.04605898032,1545.12978224787,
1545.21046196377,1545.29420067562,1545.37783618698,1545.46138863038,1545.54487806623,
1545.62833201685,1545.71176851069,1545.79520562045,1545.87866141537,1545.9622059081,
1546.04579499104,1546.12951825859,1546.21019797449,1546.29393668634,1546.3775721977,
1546.4611246411,1546.54461407695,1546.62806802757,1546.71150452141,1546.79494163117,
1546.87839742609,1546.96194191882,1547.04553100176,1547.12925426931,1547.20993398521,
1547.29367269706,1547.37730820842,1547.46086065182,1547.54435008767,1547.62780403829,
1547.71124053213,1547.79467764189,1547.87813343681,1547.96167792954,1548.04526701248,
1548.12899028003,1548.20966999593,1548.29589684262,1548.38085486658,1548.46771612463,
1548.55457738268),.UNSPECIFIED.);
#1035=B_SPLINE_CURVE_WITH_KNOTS('',3,(#129480,#129481,#129482,#129483,#129484,
#129485,#129486,#129487,#129488,#129489,#129490,#129491,#129492,#129493,
#129494,#129495,#129496,#129497,#129498,#129499,#129500,#129501,#129502,
#129503,#129504,#129505,#129506,#129507,#129508,#129509,#129510,#129511,
#129512,#129513,#129514,#129515,#129516,#129517,#129518,#129519,#129520,
#129521,#129522,#129523,#129524,#129525,#129526,#129527,#129528,#129529,
#129530,#129531,#129532,#129533,#129534,#129535,#129536,#129537,#129538,
#129539,#129540,#129541,#129542,#129543,#129544,#129545,#129546,#129547,
#129548,#129549,#129550,#129551,#129552,#129553,#129554,#129555,#129556,
#129557,#129558,#129559,#129560,#129561,#129562,#129563,#129564,#129565,
#129566,#129567,#129568,#129569,#129570,#129571,#129572,#129573,#129574,
#129575,#129576,#129577,#129578,#129579,#129580,#129581,#129582,#129583,
#129584,#129585,#129586,#129587,#129588,#129589,#129590,#129591,#129592,
#129593,#129594,#129595,#129596,#129597,#129598,#129599,#129600,#129601,
#129602,#129603,#129604,#129605,#129606,#129607,#129608,#129609,#129610,
#129611,#129612,#129613,#129614,#129615,#129616,#129617,#129618,#129619,
#129620,#129621,#129622,#129623,#129624,#129625,#129626,#129627,#129628,
#129629,#129630,#129631,#129632,#129633,#129634,#129635,#129636,#129637,
#129638,#129639,#129640,#129641,#129642,#129643,#129644,#129645,#129646,
#129647,#129648,#129649,#129650,#129651,#129652,#129653,#129654,#129655,
#129656,#129657,#129658,#129659,#129660,#129661,#129662,#129663,#129664,
#129665,#129666,#129667,#129668,#129669,#129670,#129671,#129672,#129673,
#129674,#129675,#129676,#129677,#129678,#129679,#129680,#129681,#129682,
#129683,#129684,#129685,#129686,#129687,#129688,#129689,#129690,#129691,
#129692,#129693,#129694,#129695,#129696,#129697,#129698,#129699),
 .UNSPECIFIED.,.F.,.F.,(4,3,3,3,3,3,3,3,3,3,3,3,3,3,3,3,3,3,3,3,3,3,3,3,
3,3,3,3,3,3,3,3,3,3,3,3,3,3,3,3,3,3,3,3,3,3,3,3,3,3,3,3,3,3,3,3,3,3,3,3,
3,3,3,3,3,3,3,3,3,3,3,3,3,4),(1548.80517821976,1548.89911538693,1548.98285409878,
1549.06648961014,1549.15004205354,1549.23353148939,1549.31698544001,1549.40042193385,
1549.48385904361,1549.56731483853,1549.65085933126,1549.7344484142,1549.81817168175,
1549.89885139765,1549.9825901095,1550.06622562086,1550.14977806426,1550.23326750011,
1550.31672145073,1550.40015794457,1550.48359505433,1550.56705084925,1550.65059534197,
1550.73418442492,1550.81790769247,1550.89858740837,1550.98232612022,1551.06596163158,
1551.14951407498,1551.23300351083,1551.31645746145,1551.39989395529,1551.48333106505,
1551.56678685997,1551.6503313527,1551.73392043564,1551.81764370319,1551.89832341909,
1551.98206213094,1552.0656976423,1552.1492500857,1552.23273952155,1552.31619347217,
1552.39962996601,1552.48306707577,1552.56652287069,1552.65006736342,1552.73365644636,
1552.81737971391,1552.89805942981,1552.98179814166,1553.06543365302,1553.14898609642,
1553.23247553227,1553.31592948289,1553.39936597673,1553.48280308649,1553.56625888141,
1553.64980337414,1553.73339245708,1553.81711572463,1553.89779544053,1553.98153762467,
1554.06517580973,1554.14873013162,1554.23476209869,1554.31821237126,1554.40164460853,
1554.4850768822,1554.56852725991,1554.65205160752,1554.73562057329,1554.81928899481,
1554.83698586821),.UNSPECIFIED.);
#1036=B_SPLINE_CURVE_WITH_KNOTS('',3,(#129700,#129701,#129702,#129703,#129704,
#129705,#129706,#129707,#129708,#129709),.UNSPECIFIED.,.F.,.F.,(4,3,3,4),
(1548.55334172014,1548.63588509157,1548.7205316556,1548.80517821963),
 .UNSPECIFIED.);
#1037=B_SPLINE_CURVE_WITH_KNOTS('',3,(#129711,#129712,#129713,#129714,#129715,
#129716,#129717,#129718,#129719,#129720),.UNSPECIFIED.,.F.,.F.,(4,3,3,4),
(1548.55457738268,1548.63928184855,1548.72394703715,1548.80517821977),
 .UNSPECIFIED.);
#1038=B_SPLINE_CURVE_WITH_KNOTS('',3,(#129721,#129722,#129723,#129724,#129725,
#129726,#129727,#129728,#129729,#129730,#129731,#129732,#129733,#129734,
#129735,#129736,#129737,#129738,#129739,#129740,#129741,#129742,#129743,
#129744,#129745,#129746,#129747,#129748,#129749,#129750,#129751,#129752,
#129753,#129754,#129755,#129756,#129757,#129758,#129759,#129760,#129761,
#129762,#129763,#129764,#129765,#129766,#129767,#129768,#129769,#129770,
#129771,#129772,#129773,#129774,#129775,#129776,#129777,#129778,#129779,
#129780,#129781,#129782,#129783,#129784,#129785,#129786,#129787,#129788,
#129789,#129790,#129791,#129792,#129793,#129794,#129795,#129796,#129797,
#129798,#129799,#129800,#129801,#129802,#129803,#129804,#129805,#129806,
#129807,#129808,#129809,#129810,#129811,#129812,#129813,#129814,#129815,
#129816,#129817,#129818,#129819,#129820,#129821,#129822,#129823,#129824,
#129825,#129826,#129827,#129828,#129829,#129830,#129831,#129832,#129833,
#129834,#129835,#129836,#129837,#129838,#129839,#129840,#129841,#129842,
#129843,#129844,#129845,#129846,#129847,#129848,#129849,#129850,#129851,
#129852,#129853,#129854,#129855,#129856,#129857,#129858,#129859,#129860,
#129861,#129862,#129863,#129864,#129865,#129866,#129867,#129868,#129869,
#129870,#129871,#129872,#129873,#129874,#129875,#129876,#129877,#129878,
#129879,#129880,#129881,#129882,#129883,#129884,#129885,#129886,#129887,
#129888,#129889,#129890,#129891,#129892,#129893,#129894,#129895,#129896,
#129897,#129898,#129899,#129900,#129901,#129902,#129903,#129904,#129905,
#129906,#129907,#129908,#129909,#129910,#129911,#129912,#129913,#129914,
#129915,#129916,#129917,#129918,#129919,#129920,#129921,#129922,#129923,
#129924,#129925,#129926,#129927,#129928,#129929,#129930,#129931,#129932,
#129933,#129934,#129935,#129936,#129937,#129938,#129939,#129940),
 .UNSPECIFIED.,.F.,.F.,(4,3,3,3,3,3,3,3,3,3,3,3,3,3,3,3,3,3,3,3,3,3,3,3,
3,3,3,3,3,3,3,3,3,3,3,3,3,3,3,3,3,3,3,3,3,3,3,3,3,3,3,3,3,3,3,3,3,3,3,3,
3,3,3,3,3,3,3,3,3,3,3,3,3,4),(1548.80517821995,1548.89701446912,1548.98932787598,
1549.08188752032,1549.17477730635,1549.20940600665,1549.2931447185,1549.37678022986,
1549.46033267326,1549.54382210911,1549.62727605973,1549.71071255357,1549.79414966333,
1549.87760545825,1549.96114995098,1550.04473903392,1550.12846230147,1550.20914201737,
1550.29288072922,1550.37651624058,1550.46006868398,1550.54355811983,1550.62701207045,
1550.71044856429,1550.79388567405,1550.87734146897,1550.9608859617,1551.04447504464,
1551.12819831219,1551.20887802809,1551.29261673994,1551.3762522513,1551.4598046947,
1551.54329413055,1551.62674808117,1551.71018457501,1551.79362168477,1551.87707747969,
1551.96062197242,1552.04421105536,1552.12793432291,1552.20861403881,1552.29235275066,
1552.37598826202,1552.45954070542,1552.54303014127,1552.62648409189,1552.70992058573,
1552.79335769549,1552.87681349041,1552.96035798314,1553.04394706608,1553.12767033363,
1553.20835004953,1553.29208876138,1553.37572427274,1553.45927671614,1553.54276615199,
1553.62622010261,1553.70965659645,1553.79309370621,1553.87654950113,1553.96009399386,
1554.0436830768,1554.12740634436,1554.20808606025,1554.29065831141,1554.37313589082,
1554.4555379469,1554.53788355755,1554.62019995884,1554.70249826221,1554.78481964865,
1554.83654914438),.UNSPECIFIED.);
#1039=B_SPLINE_CURVE_WITH_KNOTS('',3,(#129946,#129947,#129948,#129949,#129950,
#129951,#129952,#129953,#129954,#129955,#129956,#129957,#129958,#129959,
#129960,#129961,#129962,#129963,#129964,#129965,#129966,#129967,#129968,
#129969,#129970,#129971,#129972,#129973,#129974,#129975,#129976,#129977,
#129978,#129979,#129980,#129981,#129982,#129983,#129984,#129985,#129986,
#129987,#129988,#129989,#129990,#129991,#129992,#129993,#129994,#129995,
#129996,#129997,#129998,#129999,#130000,#130001,#130002,#130003,#130004,
#130005,#130006,#130007,#130008,#130009,#130010,#130011,#130012,#130013,
#130014,#130015,#130016,#130017,#130018,#130019,#130020,#130021,#130022,
#130023,#130024,#130025,#130026,#130027,#130028,#130029,#130030,#130031,
#130032,#130033,#130034,#130035,#130036,#130037,#130038,#130039,#130040,
#130041,#130042,#130043,#130044,#130045,#130046,#130047,#130048,#130049,
#130050,#130051,#130052,#130053,#130054,#130055,#130056,#130057,#130058,
#130059,#130060,#130061,#130062,#130063,#130064,#130065,#130066,#130067,
#130068,#130069,#130070,#130071,#130072,#130073,#130074,#130075,#130076,
#130077,#130078,#130079,#130080,#130081,#130082,#130083,#130084,#130085,
#130086,#130087,#130088,#130089,#130090,#130091,#130092,#130093,#130094,
#130095,#130096,#130097,#130098,#130099,#130100,#130101,#130102,#130103,
#130104,#130105,#130106,#130107,#130108,#130109,#130110,#130111,#130112,
#130113,#130114,#130115,#130116,#130117,#130118,#130119,#130120,#130121,
#130122,#130123,#130124,#130125,#130126,#130127,#130128,#130129,#130130,
#130131,#130132,#130133,#130134,#130135,#130136,#130137,#130138,#130139,
#130140,#130141,#130142,#130143,#130144,#130145,#130146,#130147,#130148,
#130149,#130150,#130151,#130152,#130153,#130154,#130155,#130156,#130157,
#130158,#130159,#130160,#130161,#130162,#130163,#130164,#130165),
 .UNSPECIFIED.,.F.,.F.,(4,3,3,3,3,3,3,3,3,3,3,3,3,3,3,3,3,3,3,3,3,3,3,3,
3,3,3,3,3,3,3,3,3,3,3,3,3,3,3,3,3,3,3,3,3,3,3,3,3,3,3,3,3,3,3,3,3,3,3,3,
3,3,3,3,3,3,3,3,3,3,3,3,3,4),(1555.08836352707,1555.17073000522,1555.25302491221,
1555.33527390402,1555.41749961745,1555.4997210795,1555.58195731147,1555.6642764509,
1555.74663847006,1555.82912780712,1555.89726746197,1555.98100617382,1556.06464168518,
1556.14819412858,1556.23168356443,1556.31513751505,1556.39857400889,1556.48201111865,
1556.56546691357,1556.64901140629,1556.73260048924,1556.81632375679,1556.89700347269,
1556.98074218454,1557.0643776959,1557.1479301393,1557.23141957515,1557.31487352577,
1557.39831001961,1557.48174712937,1557.56520292428,1557.64874741701,1557.73233649995,
1557.81605976751,1557.89673948341,1557.98047819526,1558.06411370662,1558.14766615002,
1558.23115558587,1558.31460953649,1558.39804603033,1558.48148314009,1558.56493893501,
1558.64848342774,1558.73207251068,1558.81579577824,1558.89647549413,1558.98021420598,
1559.06384971734,1559.14740216074,1559.23089159659,1559.31434554721,1559.39778204105,
1559.48121915081,1559.56467494573,1559.64821943846,1559.7318085214,1559.81553178895,
1559.89621150485,1559.9799502167,1560.06358572806,1560.14713817146,1560.23062760731,
1560.31408155793,1560.39751805177,1560.48095516153,1560.56441095645,1560.64795544918,
1560.73154453212,1560.81526779967,1560.89594751557,1560.9850274229,1561.07389612539,
1561.12124393646),.UNSPECIFIED.);
#1040=B_SPLINE_CURVE_WITH_KNOTS('',3,(#130166,#130167,#130168,#130169,#130170,
#130171,#130172,#130173,#130174,#130175),.UNSPECIFIED.,.F.,.F.,(4,3,3,4),
(1554.83698586821,1554.89753145125,1555.0207046782,1555.08836352694),
 .UNSPECIFIED.);
#1041=B_SPLINE_CURVE_WITH_KNOTS('',3,(#130177,#130178,#130179,#130180,#130181,
#130182,#130183,#130184,#130185,#130186),.UNSPECIFIED.,.F.,.F.,(4,3,3,4),
(1554.83654914438,1554.9189411152,1555.00365232101,1555.08836352682),
 .UNSPECIFIED.);
#1042=B_SPLINE_CURVE_WITH_KNOTS('',3,(#130187,#130188,#130189,#130190,#130191,
#130192,#130193,#130194,#130195,#130196,#130197,#130198,#130199,#130200,
#130201,#130202,#130203,#130204,#130205,#130206,#130207,#130208,#130209,
#130210,#130211,#130212,#130213,#130214,#130215,#130216,#130217,#130218,
#130219,#130220,#130221,#130222,#130223,#130224,#130225,#130226,#130227,
#130228,#130229,#130230,#130231,#130232,#130233,#130234,#130235,#130236,
#130237,#130238,#130239,#130240,#130241,#130242,#130243,#130244,#130245,
#130246,#130247,#130248,#130249,#130250,#130251,#130252,#130253,#130254,
#130255,#130256,#130257,#130258,#130259,#130260,#130261,#130262,#130263,
#130264,#130265,#130266,#130267,#130268,#130269,#130270,#130271,#130272,
#130273,#130274,#130275,#130276,#130277,#130278,#130279,#130280,#130281,
#130282,#130283,#130284,#130285,#130286,#130287,#130288,#130289,#130290,
#130291,#130292,#130293,#130294,#130295,#130296,#130297,#130298,#130299,
#130300,#130301,#130302,#130303,#130304,#130305,#130306,#130307,#130308,
#130309,#130310,#130311,#130312,#130313,#130314,#130315,#130316,#130317,
#130318,#130319,#130320,#130321,#130322,#130323,#130324,#130325,#130326,
#130327,#130328,#130329,#130330,#130331,#130332,#130333,#130334,#130335,
#130336,#130337,#130338,#130339,#130340,#130341,#130342,#130343,#130344,
#130345,#130346,#130347,#130348,#130349,#130350,#130351,#130352,#130353,
#130354,#130355,#130356,#130357,#130358,#130359,#130360,#130361,#130362,
#130363,#130364,#130365,#130366,#130367,#130368,#130369,#130370,#130371,
#130372,#130373,#130374,#130375,#130376,#130377,#130378,#130379,#130380,
#130381,#130382,#130383,#130384,#130385,#130386,#130387,#130388,#130389,
#130390,#130391,#130392,#130393,#130394,#130395,#130396,#130397,#130398,
#130399,#130400,#130401,#130402,#130403),.UNSPECIFIED.,.F.,.F.,(4,3,3,3,
3,3,3,3,3,3,3,3,3,3,3,3,3,3,3,3,3,3,3,3,3,3,3,3,3,3,3,3,3,3,3,3,3,3,3,3,
3,3,3,3,3,3,3,3,3,3,3,3,3,3,3,3,3,3,3,3,3,3,3,3,3,3,3,3,3,3,3,3,4),(1555.08836352695,
1555.20782207097,1555.29156078282,1555.37519629418,1555.45874873758,1555.54223817343,
1555.62569212405,1555.70912861789,1555.79256572765,1555.87602152257,1555.9595660153,
1556.04315509824,1556.12687836579,1556.20755808169,1556.29129679354,1556.3749323049,
1556.4584847483,1556.54197418415,1556.62542813477,1556.70886462861,1556.79230173837,
1556.87575753329,1556.95930202602,1557.04289110896,1557.12661437651,1557.20729409241,
1557.29103280426,1557.37466831562,1557.45822075902,1557.54171019487,1557.62516414549,
1557.70860063933,1557.79203774909,1557.87549354401,1557.95903803674,1558.04262711968,
1558.12635038723,1558.20703010313,1558.29076881498,1558.37440432634,1558.45795676974,
1558.54144620559,1558.62490015621,1558.70833665005,1558.79177375981,1558.87522955473,
1558.95877404746,1559.0423631304,1559.12608639796,1559.20676611385,1559.2905048257,
1559.37414033706,1559.45769278046,1559.54118221631,1559.62463616693,1559.70807266077,
1559.79150977053,1559.87496556544,1559.95851005817,1560.04209914112,1560.12582240867,
1560.20650212457,1560.29024582706,1560.37388519256,1560.4574403584,1560.54092761122,
1560.62437771144,1560.70780874742,1560.79123879095,1560.87472614777,1560.95824120661,
1561.04186108123,1561.12007636444),.UNSPECIFIED.);
#1043=B_SPLINE_CURVE_WITH_KNOTS('',3,(#130409,#130410,#130411,#130412,#130413,
#130414,#130415,#130416,#130417,#130418,#130419,#130420,#130421,#130422,
#130423,#130424,#130425,#130426,#130427,#130428,#130429,#130430,#130431,
#130432,#130433,#130434,#130435,#130436,#130437,#130438,#130439,#130440,
#130441,#130442,#130443,#130444,#130445,#130446,#130447,#130448,#130449,
#130450,#130451,#130452,#130453,#130454,#130455,#130456,#130457,#130458,
#130459,#130460,#130461,#130462,#130463,#130464,#130465,#130466,#130467,
#130468,#130469,#130470,#130471,#130472,#130473,#130474,#130475,#130476,
#130477,#130478,#130479,#130480,#130481,#130482,#130483,#130484,#130485,
#130486,#130487,#130488,#130489,#130490,#130491,#130492,#130493,#130494,
#130495,#130496,#130497,#130498,#130499,#130500,#130501,#130502,#130503,
#130504,#130505,#130506,#130507,#130508,#130509,#130510,#130511,#130512,
#130513,#130514,#130515,#130516,#130517,#130518,#130519,#130520,#130521,
#130522,#130523,#130524,#130525,#130526,#130527,#130528,#130529,#130530,
#130531,#130532,#130533,#130534,#130535,#130536,#130537,#130538,#130539,
#130540,#130541,#130542,#130543,#130544,#130545,#130546,#130547,#130548,
#130549,#130550,#130551,#130552,#130553,#130554,#130555,#130556,#130557,
#130558,#130559,#130560,#130561,#130562,#130563,#130564,#130565,#130566,
#130567,#130568,#130569,#130570,#130571,#130572,#130573,#130574,#130575,
#130576,#130577,#130578,#130579,#130580,#130581,#130582,#130583,#130584,
#130585,#130586,#130587,#130588,#130589,#130590,#130591,#130592,#130593,
#130594,#130595,#130596,#130597,#130598,#130599,#130600,#130601,#130602,
#130603,#130604,#130605,#130606,#130607,#130608,#130609,#130610,#130611,
#130612,#130613,#130614,#130615,#130616,#130617,#130618,#130619,#130620,
#130621,#130622,#130623,#130624,#130625,#130626,#130627,#130628),
 .UNSPECIFIED.,.F.,.F.,(4,3,3,3,3,3,3,3,3,3,3,3,3,3,3,3,3,3,3,3,3,3,3,3,
3,3,3,3,3,3,3,3,3,3,3,3,3,3,3,3,3,3,3,3,3,3,3,3,3,3,3,3,3,3,3,3,3,3,3,3,
3,3,3,3,3,3,3,3,3,3,3,3,3,4),(1561.37154883412,1561.45812422767,1561.54478532766,
1561.63250987732,1561.71943900516,1561.80756126572,1561.89568352629,1561.97942223814,
1562.0630577495,1562.1466101929,1562.23009962875,1562.31355357937,1562.39699007321,
1562.48042718297,1562.56388297789,1562.64742747061,1562.73101655356,1562.81473982111,
1562.89541953701,1562.97915824886,1563.06279376022,1563.14634620362,1563.22983563947,
1563.31328959009,1563.39672608393,1563.48016319369,1563.56361898861,1563.64716348134,
1563.73075256428,1563.81447583183,1563.89515554773,1563.97889425958,1564.06252977094,
1564.14608221434,1564.22957165019,1564.31302560081,1564.39646209465,1564.47989920441,
1564.56335499933,1564.64689949206,1564.730488575,1564.81421184255,1564.89489155845,
1564.9786302703,1565.06226578166,1565.14581822506,1565.22930766091,1565.31276161153,
1565.39619810537,1565.47963521513,1565.56309101005,1565.64663550278,1565.73022458572,
1565.81394785327,1565.89462756917,1565.97836628102,1566.06200179238,1566.14555423578,
1566.22904367163,1566.31249762225,1566.39593411609,1566.47937122585,1566.56282702076,
1566.64637151349,1566.72996059643,1566.81368386399,1566.89436357989,1566.97705844757,
1567.0596556153,1567.14557162137,1567.22802328557,1567.31043887618,1567.39284094755,
1567.40331963956),.UNSPECIFIED.);
#1044=B_SPLINE_CURVE_WITH_KNOTS('',3,(#130629,#130630,#130631,#130632,#130633,
#130634,#130635,#130636,#130637,#130638),.UNSPECIFIED.,.F.,.F.,(4,3,3,4),
(1561.12124393646,1561.20984029863,1561.29822797538,1561.37154883401),
 .UNSPECIFIED.);
#1045=B_SPLINE_CURVE_WITH_KNOTS('',3,(#130640,#130641,#130642,#130643,#130644,
#130645,#130646,#130647,#130648,#130649),.UNSPECIFIED.,.F.,.F.,(4,3,3,4),
(1561.12007636444,1561.20623813529,1561.33999744342,1561.37154883413),
 .UNSPECIFIED.);
#1046=B_SPLINE_CURVE_WITH_KNOTS('',3,(#130650,#130651,#130652,#130653,#130654,
#130655,#130656,#130657,#130658,#130659,#130660,#130661,#130662,#130663,
#130664,#130665,#130666,#130667,#130668,#130669,#130670,#130671,#130672,
#130673,#130674,#130675,#130676,#130677,#130678,#130679,#130680,#130681,
#130682,#130683,#130684,#130685,#130686,#130687,#130688,#130689,#130690,
#130691,#130692,#130693,#130694,#130695,#130696,#130697,#130698,#130699,
#130700,#130701,#130702,#130703,#130704,#130705,#130706,#130707,#130708,
#130709,#130710,#130711,#130712,#130713,#130714,#130715,#130716,#130717,
#130718,#130719,#130720,#130721,#130722,#130723,#130724,#130725,#130726,
#130727,#130728,#130729,#130730,#130731,#130732,#130733,#130734,#130735,
#130736,#130737,#130738,#130739,#130740,#130741,#130742,#130743,#130744,
#130745,#130746,#130747,#130748,#130749,#130750,#130751,#130752,#130753,
#130754,#130755,#130756,#130757,#130758,#130759,#130760,#130761,#130762,
#130763,#130764,#130765,#130766,#130767,#130768,#130769,#130770,#130771,
#130772,#130773,#130774,#130775,#130776,#130777,#130778,#130779,#130780,
#130781,#130782,#130783,#130784,#130785,#130786,#130787,#130788,#130789,
#130790,#130791,#130792,#130793,#130794,#130795,#130796,#130797,#130798,
#130799,#130800,#130801,#130802,#130803,#130804,#130805,#130806,#130807,
#130808,#130809,#130810,#130811,#130812,#130813,#130814,#130815,#130816,
#130817,#130818,#130819,#130820,#130821,#130822,#130823,#130824,#130825,
#130826,#130827,#130828,#130829,#130830,#130831,#130832,#130833,#130834,
#130835,#130836,#130837,#130838,#130839,#130840,#130841,#130842,#130843,
#130844,#130845,#130846,#130847,#130848,#130849,#130850,#130851,#130852,
#130853,#130854,#130855,#130856,#130857,#130858,#130859,#130860,#130861,
#130862,#130863,#130864,#130865,#130866,#130867,#130868,#130869),
 .UNSPECIFIED.,.F.,.F.,(4,3,3,3,3,3,3,3,3,3,3,3,3,3,3,3,3,3,3,3,3,3,3,3,
3,3,3,3,3,3,3,3,3,3,3,3,3,3,3,3,3,3,3,3,3,3,3,3,3,3,3,3,3,3,3,3,3,3,3,3,
3,3,3,3,3,3,3,3,3,3,3,3,3,4),(1561.37154883432,1561.45392302127,1561.53621883923,
1561.61993825257,1561.70214926038,1561.78435027844,1561.86656034019,1561.95141379164,
1562.03374277032,1562.11985845817,1562.20597414601,1562.28971285786,1562.37334836922,
1562.45690081262,1562.54039024847,1562.62384419909,1562.70728069294,1562.79071780269,
1562.87417359761,1562.95771809034,1563.04130717328,1563.12503044084,1563.20571015673,
1563.28944886858,1563.37308437994,1563.45663682334,1563.54012625919,1563.62358020981,
1563.70701670366,1563.79045381341,1563.87390960833,1563.95745410106,1564.041043184,
1564.12476645156,1564.20544616745,1564.2891848793,1564.37282039066,1564.45637283406,
1564.53986226991,1564.62331622053,1564.70675271437,1564.79018982413,1564.87364561904,
1564.95719011177,1565.04077919471,1565.12450246227,1565.20518217817,1565.28892089002,
1565.37255640138,1565.45610884478,1565.53959828063,1565.62305223125,1565.70648872509,
1565.78992583485,1565.87338162976,1565.95692612249,1566.04051520543,1566.12423847299,
1566.20491818889,1566.28865690074,1566.3722924121,1566.4558448555,1566.53933429135,
1566.62278824196,1566.70622473581,1566.78966184557,1566.87311764048,1566.95666213321,
1567.04025121615,1567.12397448371,1567.20465419961,1567.29495789568,1567.38503323209,
1567.40443029398),.UNSPECIFIED.);
#1047=B_SPLINE_CURVE_WITH_KNOTS('',3,(#130875,#130876,#130877,#130878,#130879,
#130880,#130881,#130882,#130883,#130884,#130885,#130886,#130887,#130888,
#130889,#130890,#130891,#130892,#130893,#130894,#130895,#130896,#130897,
#130898,#130899,#130900,#130901,#130902,#130903,#130904,#130905,#130906,
#130907,#130908,#130909,#130910,#130911,#130912,#130913,#130914,#130915,
#130916,#130917,#130918,#130919,#130920,#130921,#130922,#130923,#130924,
#130925,#130926,#130927,#130928,#130929,#130930,#130931,#130932,#130933,
#130934,#130935,#130936,#130937,#130938,#130939,#130940,#130941,#130942,
#130943,#130944,#130945,#130946,#130947,#130948,#130949,#130950,#130951,
#130952,#130953,#130954,#130955,#130956,#130957,#130958,#130959,#130960,
#130961,#130962,#130963,#130964,#130965,#130966,#130967,#130968,#130969,
#130970,#130971,#130972,#130973,#130974,#130975,#130976,#130977,#130978,
#130979,#130980,#130981,#130982,#130983,#130984,#130985,#130986,#130987,
#130988,#130989,#130990,#130991,#130992,#130993,#130994,#130995,#130996,
#130997,#130998,#130999,#131000,#131001,#131002,#131003,#131004,#131005,
#131006,#131007,#131008,#131009,#131010,#131011,#131012,#131013,#131014,
#131015,#131016,#131017,#131018,#131019,#131020,#131021,#131022,#131023,
#131024,#131025,#131026,#131027,#131028,#131029,#131030,#131031,#131032,
#131033,#131034,#131035,#131036,#131037,#131038,#131039,#131040,#131041,
#131042,#131043,#131044,#131045,#131046,#131047,#131048,#131049,#131050,
#131051,#131052,#131053,#131054,#131055,#131056,#131057,#131058,#131059,
#131060,#131061,#131062,#131063,#131064,#131065,#131066,#131067,#131068,
#131069,#131070,#131071,#131072,#131073,#131074,#131075,#131076,#131077,
#131078,#131079,#131080,#131081,#131082,#131083,#131084,#131085,#131086,
#131087,#131088,#131089,#131090,#131091,#131092,#131093,#131094),
 .UNSPECIFIED.,.F.,.F.,(4,3,3,3,3,3,3,3,3,3,3,3,3,3,3,3,3,3,3,3,3,3,3,3,
3,3,3,3,3,3,3,3,3,3,3,3,3,3,3,3,3,3,3,3,3,3,3,3,3,3,3,3,3,3,3,3,3,3,3,3,
3,3,3,3,3,3,3,3,3,3,3,3,3,4),(1567.65473414144,1567.76377432732,1567.87563324908,
1567.89409959061,1567.97783830246,1568.06147381383,1568.14502625723,1568.22851569308,
1568.3119696437,1568.39540613755,1568.4788432473,1568.56229904222,1568.64584353496,
1568.7294326179,1568.81315588546,1568.89383560133,1568.97757431318,1569.06120982454,
1569.14476226794,1569.22825170379,1569.31170565441,1569.39514214825,1569.47857925801,
1569.56203505292,1569.64557954565,1569.7291686286,1569.81289189615,1569.89357161205,
1569.9773103239,1570.06094583526,1570.14449827866,1570.22798771451,1570.31144166512,
1570.39487815897,1570.47831526873,1570.56177106364,1570.64531555637,1570.72890463931,
1570.81262790687,1570.89330762277,1570.97704633462,1571.06068184598,1571.14423428938,
1571.22772372523,1571.31117767585,1571.39461416969,1571.47805127945,1571.56150707437,
1571.6450515671,1571.72864065004,1571.8123639176,1571.89304363349,1571.97678234534,
1572.0604178567,1572.1439703001,1572.22745973595,1572.31091368657,1572.39435018041,
1572.47778729017,1572.56124308509,1572.64478757782,1572.72837666076,1572.81209992831,
1572.89277964421,1572.97653085598,1573.06017614605,1573.14372001628,1573.22720636791,
1573.3106533214,1573.39407896674,1573.47752444329,1573.56098050646,1573.64449717329,
1573.68625334563),.UNSPECIFIED.);
#1048=B_SPLINE_CURVE_WITH_KNOTS('',3,(#131095,#131096,#131097,#131098,#131099,
#131100,#131101,#131102,#131103,#131104),.UNSPECIFIED.,.F.,.F.,(4,3,3,4),
(1567.40331963956,1567.48574756764,1567.57024085447,1567.6547341413),
 .UNSPECIFIED.);
#1049=B_SPLINE_CURVE_WITH_KNOTS('',3,(#131106,#131107,#131108,#131109,#131110,
#131111,#131112,#131113,#131114,#131115),.UNSPECIFIED.,.F.,.F.,(4,3,3,4),
(1567.40443029398,1567.49421655057,1567.58373377193,1567.65473414121),
 .UNSPECIFIED.);
#1050=B_SPLINE_CURVE_WITH_KNOTS('',3,(#131116,#131117,#131118,#131119,#131120,
#131121,#131122,#131123,#131124,#131125,#131126,#131127,#131128,#131129,
#131130,#131131,#131132,#131133,#131134,#131135,#131136,#131137,#131138,
#131139,#131140,#131141,#131142,#131143,#131144,#131145,#131146,#131147,
#131148,#131149,#131150,#131151,#131152,#131153,#131154,#131155,#131156,
#131157,#131158,#131159,#131160,#131161,#131162,#131163,#131164,#131165,
#131166,#131167,#131168,#131169,#131170,#131171,#131172,#131173,#131174,
#131175,#131176,#131177,#131178,#131179,#131180,#131181,#131182,#131183,
#131184,#131185,#131186,#131187,#131188,#131189,#131190,#131191,#131192,
#131193,#131194,#131195,#131196,#131197,#131198,#131199,#131200,#131201,
#131202,#131203,#131204,#131205,#131206,#131207,#131208,#131209,#131210,
#131211,#131212,#131213,#131214,#131215,#131216,#131217,#131218,#131219,
#131220,#131221,#131222,#131223,#131224,#131225,#131226,#131227,#131228,
#131229,#131230,#131231,#131232,#131233,#131234,#131235,#131236,#131237,
#131238,#131239,#131240,#131241,#131242,#131243,#131244,#131245,#131246,
#131247,#131248,#131249,#131250,#131251,#131252,#131253,#131254,#131255,
#131256,#131257,#131258,#131259,#131260,#131261,#131262,#131263,#131264,
#131265,#131266,#131267,#131268,#131269,#131270,#131271,#131272,#131273,
#131274,#131275,#131276,#131277,#131278,#131279,#131280,#131281,#131282,
#131283,#131284,#131285,#131286,#131287,#131288,#131289,#131290,#131291,
#131292,#131293,#131294,#131295,#131296,#131297,#131298,#131299,#131300,
#131301,#131302,#131303,#131304,#131305,#131306,#131307,#131308,#131309,
#131310,#131311,#131312,#131313,#131314,#131315,#131316,#131317,#131318,
#131319,#131320,#131321,#131322,#131323,#131324,#131325,#131326,#131327,
#131328,#131329,#131330,#131331,#131332,#131333,#131334,#131335),
 .UNSPECIFIED.,.F.,.F.,(4,3,3,3,3,3,3,3,3,3,3,3,3,3,3,3,3,3,3,3,3,3,3,3,
3,3,3,3,3,3,3,3,3,3,3,3,3,3,3,3,3,3,3,3,3,3,3,3,3,3,3,3,3,3,3,3,3,3,3,3,
3,3,3,3,3,3,3,3,3,3,3,3,3,4),(1567.65473414131,1567.74054040221,1567.82640703948,
1567.91234767549,1567.99843792169,1568.08461274297,1568.17094473813,1568.20439021033,
1568.28812892218,1568.37176443355,1568.45531687695,1568.5388063128,1568.62226026341,
1568.70569675726,1568.78913386702,1568.87258966194,1568.95613415467,1569.03972323761,
1569.12344650517,1569.20412622105,1569.2878649329,1569.37150044426,1569.45505288766,
1569.53854232351,1569.62199627413,1569.70543276797,1569.78886987773,1569.87232567265,
1569.95587016538,1570.03945924832,1570.12318251588,1570.20386223177,1570.28760094362,
1570.37123645498,1570.45478889838,1570.53827833423,1570.62173228484,1570.70516877869,
1570.78860588845,1570.87206168336,1570.95560617609,1571.03919525903,1571.12291852659,
1571.20359824249,1571.28733695434,1571.3709724657,1571.4545249091,1571.53801434495,
1571.62146829557,1571.70490478941,1571.78834189917,1571.87179769409,1571.95534218682,
1572.03893126976,1572.12265453732,1572.20333425321,1572.28707296506,1572.37070847642,
1572.45426091982,1572.53775035567,1572.62120430628,1572.70464080013,1572.78807790988,
1572.8715337048,1572.95507819753,1573.03866728047,1573.12239054803,1573.20307026393,
1573.28595684986,1573.36874428265,1573.45143789125,1573.53407654318,1573.61668446351,
1573.68663052872),.UNSPECIFIED.);
#1051=B_SPLINE_CURVE_WITH_KNOTS('',3,(#131341,#131342,#131343,#131344,#131345,
#131346,#131347,#131348,#131349,#131350,#131351,#131352,#131353,#131354,
#131355,#131356,#131357,#131358,#131359,#131360,#131361,#131362,#131363,
#131364,#131365,#131366,#131367,#131368,#131369,#131370,#131371,#131372,
#131373,#131374,#131375,#131376,#131377,#131378,#131379,#131380,#131381,
#131382,#131383,#131384,#131385,#131386,#131387,#131388,#131389,#131390,
#131391,#131392,#131393,#131394,#131395,#131396,#131397,#131398,#131399,
#131400,#131401,#131402,#131403,#131404,#131405,#131406,#131407,#131408,
#131409,#131410,#131411,#131412,#131413,#131414,#131415,#131416,#131417,
#131418,#131419,#131420,#131421,#131422,#131423,#131424,#131425,#131426,
#131427,#131428,#131429,#131430,#131431,#131432,#131433,#131434,#131435,
#131436,#131437,#131438,#131439,#131440,#131441,#131442,#131443,#131444,
#131445,#131446,#131447,#131448,#131449,#131450,#131451,#131452,#131453,
#131454,#131455,#131456,#131457,#131458,#131459,#131460,#131461,#131462,
#131463,#131464,#131465,#131466,#131467,#131468,#131469,#131470,#131471,
#131472,#131473,#131474,#131475,#131476,#131477,#131478,#131479,#131480,
#131481,#131482,#131483,#131484,#131485,#131486,#131487,#131488,#131489,
#131490,#131491,#131492,#131493,#131494,#131495,#131496,#131497,#131498,
#131499,#131500,#131501,#131502,#131503,#131504,#131505,#131506,#131507,
#131508,#131509,#131510,#131511,#131512,#131513,#131514,#131515,#131516,
#131517,#131518,#131519,#131520,#131521,#131522,#131523,#131524,#131525,
#131526,#131527,#131528,#131529,#131530,#131531,#131532,#131533,#131534,
#131535,#131536,#131537,#131538,#131539,#131540,#131541,#131542,#131543,
#131544,#131545,#131546,#131547,#131548,#131549,#131550,#131551,#131552,
#131553,#131554,#131555,#131556,#131557,#131558,#131559,#131560),
 .UNSPECIFIED.,.F.,.F.,(4,3,3,3,3,3,3,3,3,3,3,3,3,3,3,3,3,3,3,3,3,3,3,3,
3,3,3,3,3,3,3,3,3,3,3,3,3,3,3,3,3,3,3,3,3,3,3,3,3,3,3,3,3,3,3,3,3,3,3,3,
3,3,3,3,3,3,3,3,3,3,3,3,3,4),(1573.93791944867,1574.0210546865,1574.10408938948,
1574.18704426269,1574.2699399344,1574.35280557854,1574.43565825124,1574.51851653844,
1574.60139902671,1574.68437118786,1574.7673938746,1574.85053857207,1574.89225166565,
1574.9759903775,1575.05962588886,1575.14317833226,1575.22666776811,1575.31012171873,
1575.39355821257,1575.47699532233,1575.56045111725,1575.64399560998,1575.72758469292,
1575.81130796048,1575.89198767637,1575.97572638821,1576.05936189958,1576.14291434298,
1576.22640377883,1576.30985772944,1576.39329422329,1576.47673133304,1576.56018712796,
1576.64373162069,1576.72732070363,1576.81104397118,1576.89172368709,1576.97546239894,
1577.05909791031,1577.14265035371,1577.22613978956,1577.30959374018,1577.39303023403,
1577.47646734378,1577.5599231387,1577.64346763143,1577.72705671438,1577.81077998194,
1577.89145969782,1577.97519840967,1578.05883392103,1578.14238636443,1578.22587580028,
1578.3093297509,1578.39276624475,1578.4762033545,1578.55965914942,1578.64320364215,
1578.72679272509,1578.81051599265,1578.89119570854,1578.97493442039,1579.05856993175,
1579.14212237515,1579.225611811,1579.30906576162,1579.39250225546,1579.47593936522,
1579.55939516013,1579.64293965286,1579.7265287358,1579.81025200336,1579.89093171926,
1579.97048400051),.UNSPECIFIED.);
#1052=B_SPLINE_CURVE_WITH_KNOTS('',3,(#131561,#131562,#131563,#131564,#131565,
#131566,#131567,#131568,#131569,#131570,#131571,#131572,#131573),
 .UNSPECIFIED.,.F.,.F.,(4,3,3,3,4),(1573.68625334563,1573.76987077976,1573.8536105396,
1573.89251565493,1573.93791944848),.UNSPECIFIED.);
#1053=B_SPLINE_CURVE_WITH_KNOTS('',3,(#131575,#131576,#131577,#131578,#131579,
#131580,#131581,#131582,#131583,#131584),.UNSPECIFIED.,.F.,.F.,(4,3,3,4),
(1573.68663052872,1573.76923020489,1573.85357482669,1573.93791944849),
 .UNSPECIFIED.);
#1054=B_SPLINE_CURVE_WITH_KNOTS('',3,(#131585,#131586,#131587,#131588,#131589,
#131590,#131591,#131592,#131593,#131594,#131595,#131596,#131597,#131598,
#131599,#131600,#131601,#131602,#131603,#131604,#131605,#131606,#131607,
#131608,#131609,#131610,#131611,#131612,#131613,#131614,#131615,#131616,
#131617,#131618,#131619,#131620,#131621,#131622,#131623,#131624,#131625,
#131626,#131627,#131628,#131629,#131630,#131631,#131632,#131633,#131634,
#131635,#131636,#131637,#131638,#131639,#131640,#131641,#131642,#131643,
#131644,#131645,#131646,#131647,#131648,#131649,#131650,#131651,#131652,
#131653,#131654,#131655,#131656,#131657,#131658,#131659,#131660,#131661,
#131662,#131663,#131664,#131665,#131666,#131667,#131668,#131669,#131670,
#131671,#131672,#131673,#131674,#131675,#131676,#131677,#131678,#131679,
#131680,#131681,#131682,#131683,#131684,#131685,#131686,#131687,#131688,
#131689,#131690,#131691,#131692,#131693,#131694,#131695,#131696,#131697,
#131698,#131699,#131700,#131701,#131702,#131703,#131704,#131705,#131706,
#131707,#131708,#131709,#131710,#131711,#131712,#131713,#131714,#131715,
#131716,#131717,#131718,#131719,#131720,#131721,#131722,#131723,#131724,
#131725,#131726,#131727,#131728,#131729,#131730,#131731,#131732,#131733,
#131734,#131735,#131736,#131737,#131738,#131739,#131740,#131741,#131742,
#131743,#131744,#131745,#131746,#131747,#131748,#131749,#131750,#131751,
#131752,#131753,#131754,#131755,#131756,#131757,#131758,#131759,#131760,
#131761,#131762,#131763,#131764,#131765,#131766,#131767,#131768,#131769,
#131770,#131771,#131772,#131773,#131774,#131775,#131776,#131777,#131778,
#131779,#131780,#131781,#131782,#131783,#131784,#131785,#131786,#131787,
#131788,#131789,#131790,#131791,#131792,#131793,#131794,#131795,#131796,
#131797,#131798,#131799,#131800,#131801,#131802,#131803,#131804),
 .UNSPECIFIED.,.F.,.F.,(4,3,3,3,3,3,3,3,3,3,3,3,3,3,3,3,3,3,3,3,3,3,3,3,
3,3,3,3,3,3,3,3,3,3,3,3,3,3,3,3,3,3,3,3,3,3,3,3,3,3,3,3,3,3,3,3,3,3,3,3,
3,3,3,3,3,3,3,3,3,3,3,3,3,4),(1573.93791944865,1574.04289524923,1574.14985801462,
1574.20280627465,1574.2865449865,1574.37018049786,1574.45373294126,1574.53722237712,
1574.62067632773,1574.70411282158,1574.78754993133,1574.87100572625,1574.95455021898,
1575.03813930192,1575.12186256948,1575.20254228537,1575.28628099722,1575.36991650858,
1575.45346895198,1575.53695838783,1575.62041233845,1575.70384883229,1575.78728594205,
1575.87074173697,1575.9542862297,1576.03787531264,1576.12159858019,1576.20227829609,
1576.28601700794,1576.3696525193,1576.4532049627,1576.53669439855,1576.62014834917,
1576.70358484301,1576.78702195277,1576.87047774769,1576.95402224041,1577.03761132336,
1577.12133459091,1577.20201430681,1577.28575301866,1577.36938853002,1577.45294097342,
1577.53643040927,1577.61988435989,1577.70332085373,1577.78675796349,1577.87021375841,
1577.95375825114,1578.03734733408,1578.12107060163,1578.20175031753,1578.28548902938,
1578.36912454074,1578.45267698414,1578.53616641999,1578.61962037061,1578.70305686445,
1578.78649397421,1578.86994976913,1578.95349426186,1579.0370833448,1579.12080661235,
1579.20148632825,1579.28523921838,1579.3707646693,1579.45430765298,1579.5377930484,
1579.62123897607,1579.70828993847,1579.79173047179,1579.87518246829,1579.95868485598,
1579.96944282568),.UNSPECIFIED.);
#1055=B_SPLINE_CURVE_WITH_KNOTS('',3,(#131810,#131811,#131812,#131813,#131814,
#131815,#131816,#131817,#131818,#131819,#131820,#131821,#131822,#131823,
#131824,#131825,#131826,#131827,#131828,#131829,#131830,#131831,#131832,
#131833,#131834,#131835,#131836,#131837,#131838,#131839,#131840,#131841,
#131842,#131843,#131844,#131845,#131846,#131847,#131848,#131849,#131850,
#131851,#131852,#131853,#131854,#131855,#131856,#131857,#131858,#131859,
#131860,#131861,#131862,#131863,#131864,#131865,#131866,#131867,#131868,
#131869,#131870,#131871,#131872,#131873,#131874,#131875,#131876,#131877,
#131878,#131879,#131880,#131881,#131882,#131883,#131884,#131885,#131886,
#131887,#131888,#131889,#131890,#131891,#131892,#131893,#131894,#131895,
#131896,#131897,#131898,#131899,#131900,#131901,#131902,#131903,#131904,
#131905,#131906,#131907,#131908,#131909,#131910,#131911,#131912,#131913,
#131914,#131915,#131916,#131917,#131918,#131919,#131920,#131921,#131922,
#131923,#131924,#131925,#131926,#131927,#131928,#131929,#131930,#131931,
#131932,#131933,#131934,#131935,#131936,#131937,#131938,#131939,#131940,
#131941,#131942,#131943,#131944,#131945,#131946,#131947,#131948,#131949,
#131950,#131951,#131952,#131953,#131954,#131955,#131956,#131957,#131958,
#131959,#131960,#131961,#131962,#131963,#131964,#131965,#131966,#131967,
#131968,#131969,#131970,#131971,#131972,#131973,#131974,#131975,#131976,
#131977,#131978,#131979,#131980,#131981,#131982,#131983,#131984,#131985,
#131986,#131987,#131988,#131989,#131990,#131991,#131992,#131993,#131994,
#131995,#131996,#131997,#131998,#131999,#132000,#132001,#132002,#132003,
#132004,#132005,#132006,#132007,#132008,#132009,#132010,#132011,#132012,
#132013,#132014,#132015,#132016,#132017,#132018,#132019,#132020,#132021,
#132022,#132023,#132024,#132025,#132026,#132027,#132028,#132029),
 .UNSPECIFIED.,.F.,.F.,(4,3,3,3,3,3,3,3,3,3,3,3,3,3,3,3,3,3,3,3,3,3,3,3,
3,3,3,3,3,3,3,3,3,3,3,3,3,3,3,3,3,3,3,3,3,3,3,3,3,3,3,3,3,3,3,3,3,3,3,3,
3,3,3,3,3,3,3,3,3,3,3,3,3,4),(1580.22110475566,1580.30480012745,1580.38812860707,
1580.4714604773,1580.55481384701,1580.63877731776,1580.72227243822,1580.8064700841,
1580.89066772998,1580.97440644183,1581.05804195319,1581.14159439659,1581.22508383244,
1581.30853778306,1581.3919742769,1581.47541138666,1581.55886718158,1581.64241167431,
1581.72600075725,1581.80972402481,1581.8904037407,1581.97414245255,1582.05777796391,
1582.14133040731,1582.22481984316,1582.30827379378,1582.39171028762,1582.47514739738,
1582.55860319229,1582.64214768502,1582.72573676796,1582.80946003552,1582.89013975142,
1582.97387846327,1583.05751397463,1583.14106641803,1583.22455585388,1583.3080098045,
1583.39144629834,1583.4748834081,1583.55833920302,1583.64188369575,1583.72547277869,
1583.80919604624,1583.88987576214,1583.97361447399,1584.05724998535,1584.14080242875,
1584.2242918646,1584.30774581522,1584.39118230906,1584.47461941882,1584.55807521374,
1584.64161970647,1584.72520878941,1584.80893205697,1584.88961177286,1584.97335048471,
1585.05698599607,1585.14053843947,1585.22402787532,1585.30748182594,1585.39091831978,
1585.47435542954,1585.55781122445,1585.64135571718,1585.72494480013,1585.80866806768,
1585.88934778358,1585.97401443131,1586.05853521259,1586.14297139875,1586.22732327027,
1586.25360547416),.UNSPECIFIED.);
#1056=B_SPLINE_CURVE_WITH_KNOTS('',3,(#132030,#132031,#132032,#132033,#132034,
#132035,#132036,#132037,#132038,#132039),.UNSPECIFIED.,.F.,.F.,(4,3,3,4),
(1579.97048400051,1580.06883921701,1580.1663064719,1580.22110475548),
 .UNSPECIFIED.);
#1057=B_SPLINE_CURVE_WITH_KNOTS('',3,(#132041,#132042,#132043,#132044,#132045,
#132046,#132047,#132048,#132049,#132050,#132051,#132052,#132053),
 .UNSPECIFIED.,.F.,.F.,(4,3,3,3,4),(1579.96944282568,1580.0530424425,1580.1367715252,
1580.20122233897,1580.22110475567),.UNSPECIFIED.);
#1058=B_SPLINE_CURVE_WITH_KNOTS('',3,(#132054,#132055,#132056,#132057,#132058,
#132059,#132060,#132061,#132062,#132063,#132064,#132065,#132066,#132067,
#132068,#132069,#132070,#132071,#132072,#132073,#132074,#132075,#132076,
#132077,#132078,#132079,#132080,#132081,#132082,#132083,#132084,#132085,
#132086,#132087,#132088,#132089,#132090,#132091,#132092,#132093,#132094,
#132095,#132096,#132097,#132098,#132099,#132100,#132101,#132102,#132103,
#132104,#132105,#132106,#132107,#132108,#132109,#132110,#132111,#132112,
#132113,#132114,#132115,#132116,#132117,#132118,#132119,#132120,#132121,
#132122,#132123,#132124,#132125,#132126,#132127,#132128,#132129,#132130,
#132131,#132132,#132133,#132134,#132135,#132136,#132137,#132138,#132139,
#132140,#132141,#132142,#132143,#132144,#132145,#132146,#132147,#132148,
#132149,#132150,#132151,#132152,#132153,#132154,#132155,#132156,#132157,
#132158,#132159,#132160,#132161,#132162,#132163,#132164,#132165,#132166,
#132167,#132168,#132169,#132170,#132171,#132172,#132173,#132174,#132175,
#132176,#132177,#132178,#132179,#132180,#132181,#132182,#132183,#132184,
#132185,#132186,#132187,#132188,#132189,#132190,#132191,#132192,#132193,
#132194,#132195,#132196,#132197,#132198,#132199,#132200,#132201,#132202,
#132203,#132204,#132205,#132206,#132207,#132208,#132209,#132210,#132211,
#132212,#132213,#132214,#132215,#132216,#132217,#132218,#132219,#132220,
#132221,#132222,#132223,#132224,#132225,#132226,#132227,#132228,#132229,
#132230,#132231,#132232,#132233,#132234,#132235,#132236,#132237,#132238,
#132239,#132240,#132241,#132242,#132243,#132244,#132245,#132246,#132247,
#132248,#132249,#132250,#132251,#132252,#132253,#132254,#132255,#132256,
#132257,#132258,#132259,#132260,#132261,#132262,#132263,#132264,#132265,
#132266,#132267,#132268,#132269,#132270,#132271,#132272,#132273),
 .UNSPECIFIED.,.F.,.F.,(4,3,3,3,3,3,3,3,3,3,3,3,3,3,3,3,3,3,3,3,3,3,3,3,
3,3,3,3,3,3,3,3,3,3,3,3,3,3,3,3,3,3,3,3,3,3,3,3,3,3,3,3,3,3,3,3,3,3,3,3,
3,3,3,3,3,3,3,3,3,3,3,3,3,4),(1580.22110475585,1580.30455741131,1580.38790749604,
1580.47117543512,1580.55438157929,1580.63755409332,1580.72071078458,1580.80386998686,
1580.88705003199,1580.97031903189,1581.05363505913,1581.13707991054,1581.20095834969,
1581.28469706154,1581.3683325729,1581.4518850163,1581.53537445215,1581.61882840277,
1581.70226489661,1581.78570200637,1581.86915780128,1581.95270229401,1582.03629137695,
1582.12001464451,1582.20069436041,1582.28443307226,1582.36806858362,1582.45162102702,
1582.53511046287,1582.61856441349,1582.70200090733,1582.78543801709,1582.86889381201,
1582.95243830474,1583.03602738768,1583.11975065524,1583.20043037113,1583.28416908298,
1583.36780459434,1583.45135703774,1583.53484647359,1583.61830042421,1583.70173691805,
1583.78517402781,1583.86862982273,1583.95217431546,1584.0357633984,1584.11948666596,
1584.20016638185,1584.2839050937,1584.36754060506,1584.45109304846,1584.53458248431,
1584.61803643492,1584.70147292877,1584.78491003853,1584.86836583344,1584.95191032617,
1585.03549940911,1585.11922267667,1585.19990239257,1585.28364110442,1585.36727661578,
1585.45082905918,1585.53431849503,1585.61777244565,1585.70120893949,1585.78464604925,
1585.86810184417,1585.9516463369,1586.03523541984,1586.1189586874,1586.19963840329,
1586.25354069145),.UNSPECIFIED.);
#1059=B_SPLINE_CURVE_WITH_KNOTS('',3,(#132279,#132280,#132281,#132282,#132283,
#132284,#132285,#132286,#132287,#132288,#132289,#132290,#132291,#132292,
#132293,#132294,#132295,#132296,#132297,#132298,#132299,#132300,#132301,
#132302,#132303,#132304,#132305,#132306,#132307,#132308,#132309,#132310,
#132311,#132312,#132313,#132314,#132315,#132316,#132317,#132318,#132319,
#132320,#132321,#132322,#132323,#132324,#132325,#132326,#132327,#132328,
#132329,#132330,#132331,#132332,#132333,#132334,#132335,#132336,#132337,
#132338,#132339,#132340,#132341,#132342,#132343,#132344,#132345,#132346,
#132347,#132348,#132349,#132350,#132351,#132352,#132353,#132354,#132355,
#132356,#132357,#132358,#132359,#132360,#132361,#132362,#132363,#132364,
#132365,#132366,#132367,#132368,#132369,#132370,#132371,#132372,#132373,
#132374,#132375,#132376,#132377,#132378,#132379,#132380,#132381,#132382,
#132383,#132384,#132385,#132386,#132387,#132388,#132389,#132390,#132391,
#132392,#132393,#132394,#132395,#132396,#132397,#132398,#132399,#132400,
#132401,#132402,#132403,#132404,#132405,#132406,#132407,#132408,#132409,
#132410,#132411,#132412,#132413,#132414,#132415,#132416,#132417,#132418,
#132419,#132420,#132421,#132422,#132423,#132424,#132425,#132426,#132427,
#132428,#132429,#132430,#132431,#132432,#132433,#132434,#132435,#132436,
#132437,#132438,#132439,#132440,#132441,#132442,#132443,#132444,#132445,
#132446,#132447,#132448,#132449,#132450,#132451,#132452,#132453,#132454,
#132455,#132456,#132457,#132458,#132459,#132460,#132461,#132462,#132463,
#132464,#132465,#132466,#132467,#132468,#132469,#132470,#132471,#132472,
#132473,#132474,#132475,#132476,#132477,#132478,#132479,#132480,#132481,
#132482,#132483,#132484,#132485,#132486,#132487,#132488,#132489,#132490,
#132491,#132492,#132493,#132494,#132495),.UNSPECIFIED.,.F.,.F.,(4,3,3,3,
3,3,3,3,3,3,3,3,3,3,3,3,3,3,3,3,3,3,3,3,3,3,3,3,3,3,3,3,3,3,3,3,3,3,3,3,
3,3,3,3,3,3,3,3,3,3,3,3,3,3,3,3,3,3,3,3,3,3,3,3,3,3,3,3,3,3,3,3,4),(1586.50429006303,
1586.60048849585,1586.69409668971,1586.79159024201,1586.8890837943,1586.97282250615,
1587.05645801751,1587.14001046091,1587.22349989676,1587.30695384738,1587.39039034122,
1587.47382745098,1587.5572832459,1587.64082773863,1587.72441682157,1587.80814008913,
1587.88881980502,1587.97255851687,1588.05619402823,1588.13974647163,1588.22323590748,
1588.3066898581,1588.39012635194,1588.4735634617,1588.55701925661,1588.64056374934,
1588.72415283228,1588.80787609984,1588.88855581574,1588.97229452759,1589.05593003895,
1589.13948248235,1589.2229719182,1589.30642586882,1589.38986236266,1589.47329947242,
1589.55675526734,1589.64029976007,1589.72388884301,1589.80761211056,1589.88829182646,
1589.97203053831,1590.05566604967,1590.13921849307,1590.22270792892,1590.30616187954,
1590.38959837338,1590.47303548314,1590.55649127806,1590.64003577079,1590.72362485373,
1590.80734812129,1590.88802783718,1590.97176654903,1591.05540206039,1591.13895450379,
1591.22244393964,1591.30589789026,1591.3893343841,1591.47277149386,1591.55622728877,
1591.6397717815,1591.72336086445,1591.807084132,1591.8877638479,1591.97043428355,
1592.05301014788,1592.13551052206,1592.21795441894,1592.3003708666,1592.38276892532,
1592.46519595126,1592.53564160811),.UNSPECIFIED.);
#1060=B_SPLINE_CURVE_WITH_KNOTS('',3,(#132496,#132497,#132498,#132499,#132500,
#132501,#132502,#132503,#132504,#132505),.UNSPECIFIED.,.F.,.F.,(4,3,3,4),
(1586.25360547416,1586.33788429121,1586.42214119569,1586.50429006284),
 .UNSPECIFIED.);
#1061=B_SPLINE_CURVE_WITH_KNOTS('',3,(#132507,#132508,#132509,#132510,#132511,
#132512,#132513,#132514,#132515,#132516),.UNSPECIFIED.,.F.,.F.,(4,3,3,4),
(1586.25354069145,1586.35475079831,1586.45478004659,1586.5042900627),
 .UNSPECIFIED.);
#1062=B_SPLINE_CURVE_WITH_KNOTS('',3,(#132517,#132518,#132519,#132520,#132521,
#132522,#132523,#132524,#132525,#132526,#132527,#132528,#132529,#132530,
#132531,#132532,#132533,#132534,#132535,#132536,#132537,#132538,#132539,
#132540,#132541,#132542,#132543,#132544,#132545,#132546,#132547,#132548,
#132549,#132550,#132551,#132552,#132553,#132554,#132555,#132556,#132557,
#132558,#132559,#132560,#132561,#132562,#132563,#132564,#132565,#132566,
#132567,#132568,#132569,#132570,#132571,#132572,#132573,#132574,#132575,
#132576,#132577,#132578,#132579,#132580,#132581,#132582,#132583,#132584,
#132585,#132586,#132587,#132588,#132589,#132590,#132591,#132592,#132593,
#132594,#132595,#132596,#132597,#132598,#132599,#132600,#132601,#132602,
#132603,#132604,#132605,#132606,#132607,#132608,#132609,#132610,#132611,
#132612,#132613,#132614,#132615,#132616,#132617,#132618,#132619,#132620,
#132621,#132622,#132623,#132624,#132625,#132626,#132627,#132628,#132629,
#132630,#132631,#132632,#132633,#132634,#132635,#132636,#132637,#132638,
#132639,#132640,#132641,#132642,#132643,#132644,#132645,#132646,#132647,
#132648,#132649,#132650,#132651,#132652,#132653,#132654,#132655,#132656,
#132657,#132658,#132659,#132660,#132661,#132662,#132663,#132664,#132665,
#132666,#132667,#132668,#132669,#132670,#132671,#132672,#132673,#132674,
#132675,#132676,#132677,#132678,#132679,#132680,#132681,#132682,#132683,
#132684,#132685,#132686,#132687,#132688,#132689,#132690,#132691,#132692,
#132693,#132694,#132695,#132696,#132697,#132698,#132699,#132700,#132701,
#132702,#132703,#132704,#132705,#132706,#132707,#132708,#132709,#132710,
#132711,#132712,#132713,#132714,#132715,#132716,#132717,#132718,#132719,
#132720,#132721,#132722,#132723,#132724,#132725,#132726,#132727,#132728,
#132729,#132730,#132731,#132732,#132733,#132734,#132735,#132736),
 .UNSPECIFIED.,.F.,.F.,(4,3,3,3,3,3,3,3,3,3,3,3,3,3,3,3,3,3,3,3,3,3,3,3,
3,3,3,3,3,3,3,3,3,3,3,3,3,3,3,3,3,3,3,3,3,3,3,3,3,3,3,3,3,3,3,3,3,3,3,3,
3,3,3,3,3,3,3,3,3,3,3,3,3,4),(1586.50429006285,1586.59117560675,1586.67417571087,
1586.75716969916,1586.84017600843,1586.92321308047,1587.00634564545,1587.08953426791,
1587.17284408563,1587.19937441401,1587.28311312586,1587.36674863722,1587.45030108062,
1587.53379051647,1587.61724446709,1587.70068096093,1587.78411807069,1587.8675738656,
1587.95111835833,1588.03470744127,1588.11843070883,1588.19911042473,1588.28284913658,
1588.36648464794,1588.45003709134,1588.53352652719,1588.61698047781,1588.70041697165,
1588.78385408141,1588.86730987633,1588.95085436906,1589.034443452,1589.11816671956,
1589.19884643545,1589.2825851473,1589.36622065866,1589.44977310206,1589.53326253791,
1589.61671648853,1589.70015298237,1589.78359009213,1589.86704588705,1589.95059037978,
1590.03417946272,1590.11790273027,1590.19858244617,1590.28232115802,1590.36595666938,
1590.44950911278,1590.53299854863,1590.61645249924,1590.69988899309,1590.78332610285,
1590.86678189776,1590.95032639049,1591.03391547343,1591.11763874099,1591.19831845689,
1591.28205716874,1591.3656926801,1591.4492451235,1591.53273455935,1591.61618850997,
1591.69962500381,1591.78306211357,1591.86651790849,1591.95006240122,1592.03365148416,
1592.11737475172,1592.19805446761,1592.28326590893,1592.36837271544,1592.45336110949,
1592.53689918447),.UNSPECIFIED.);
#1063=B_SPLINE_CURVE_WITH_KNOTS('',3,(#132742,#132743,#132744,#132745,#132746,
#132747,#132748,#132749,#132750,#132751,#132752,#132753,#132754,#132755,
#132756,#132757,#132758,#132759,#132760,#132761,#132762,#132763,#132764,
#132765,#132766,#132767,#132768,#132769,#132770,#132771,#132772,#132773,
#132774,#132775,#132776,#132777,#132778,#132779,#132780,#132781,#132782,
#132783,#132784,#132785,#132786,#132787,#132788,#132789,#132790,#132791,
#132792,#132793,#132794,#132795,#132796,#132797,#132798,#132799,#132800,
#132801,#132802,#132803,#132804,#132805,#132806,#132807,#132808,#132809,
#132810,#132811,#132812,#132813,#132814,#132815,#132816,#132817,#132818,
#132819,#132820,#132821,#132822,#132823,#132824,#132825,#132826,#132827,
#132828,#132829,#132830,#132831,#132832,#132833,#132834,#132835,#132836,
#132837,#132838,#132839,#132840,#132841,#132842,#132843,#132844,#132845,
#132846,#132847,#132848,#132849,#132850,#132851,#132852,#132853,#132854,
#132855,#132856,#132857,#132858,#132859,#132860,#132861,#132862,#132863,
#132864,#132865,#132866,#132867,#132868,#132869,#132870,#132871,#132872,
#132873,#132874,#132875,#132876,#132877,#132878,#132879,#132880,#132881,
#132882,#132883,#132884,#132885,#132886,#132887,#132888,#132889,#132890,
#132891,#132892,#132893,#132894,#132895,#132896,#132897,#132898,#132899,
#132900,#132901,#132902,#132903,#132904,#132905,#132906,#132907,#132908,
#132909,#132910,#132911,#132912,#132913,#132914,#132915,#132916,#132917,
#132918,#132919,#132920,#132921,#132922,#132923,#132924,#132925,#132926,
#132927,#132928,#132929,#132930,#132931,#132932,#132933,#132934,#132935,
#132936,#132937,#132938,#132939,#132940,#132941,#132942,#132943,#132944,
#132945,#132946,#132947,#132948,#132949,#132950,#132951,#132952,#132953,
#132954,#132955,#132956,#132957,#132958,#132959,#132960,#132961),
 .UNSPECIFIED.,.F.,.F.,(4,3,3,3,3,3,3,3,3,3,3,3,3,3,3,3,3,3,3,3,3,3,3,3,
3,3,3,3,3,3,3,3,3,3,3,3,3,3,3,3,3,3,3,3,3,3,3,3,3,3,3,3,3,3,3,3,3,3,3,3,
3,3,3,3,3,3,3,3,3,3,3,3,3,4),(1592.78747537002,1592.88749985862,1592.97123857047,
1593.05487408183,1593.13842652523,1593.22191596108,1593.3053699117,1593.38880640554,
1593.4722435153,1593.55569931022,1593.63924380295,1593.72283288589,1593.80655615344,
1593.88723586934,1593.97097458119,1594.05461009255,1594.13816253595,1594.2216519718,
1594.30510592242,1594.38854241626,1594.47197952602,1594.55543532093,1594.63897981366,
1594.7225688966,1594.80629216416,1594.88697188006,1594.97071059191,1595.05434610327,
1595.13789854667,1595.22138798252,1595.30484193314,1595.38827842698,1595.47171553674,
1595.55517133166,1595.63871582439,1595.72230490733,1595.80602817488,1595.88670789078,
1595.97044660263,1596.05408211399,1596.13763455739,1596.22112399324,1596.30457794386,
1596.3880144377,1596.47145154746,1596.55490734238,1596.63845183511,1596.72204091805,
1596.8057641856,1596.8864439015,1596.97018261335,1597.05381812471,1597.13737056811,
1597.22086000396,1597.30431395458,1597.38775044842,1597.47118755818,1597.5546433531,
1597.63818784583,1597.72177692877,1597.80550019633,1597.88617991222,1597.96992245597,
1598.05356092002,1598.13711544061,1598.22238332056,1598.30583358857,1598.3892655418,
1598.47269725198,1598.55933755903,1598.64286097195,1598.726429428,1598.8100938485,
1598.81925848019),.UNSPECIFIED.);
#1064=B_SPLINE_CURVE_WITH_KNOTS('',3,(#132962,#132963,#132964,#132965,#132966,
#132967,#132968,#132969,#132970,#132971),.UNSPECIFIED.,.F.,.F.,(4,3,3,4),
(1592.53564160811,1592.61814382261,1592.70280959625,1592.78747536988),
 .UNSPECIFIED.);
#1065=B_SPLINE_CURVE_WITH_KNOTS('',3,(#132973,#132974,#132975,#132976,#132977,
#132978,#132979,#132980,#132981,#132982),.UNSPECIFIED.,.F.,.F.,(4,3,3,4),
(1592.53689918447,1592.62174705618,1592.70654982744,1592.78747537003),
 .UNSPECIFIED.);
#1066=B_SPLINE_CURVE_WITH_KNOTS('',3,(#132983,#132984,#132985,#132986,#132987,
#132988,#132989,#132990,#132991,#132992,#132993,#132994,#132995,#132996,
#132997,#132998,#132999,#133000,#133001,#133002,#133003,#133004,#133005,
#133006,#133007,#133008,#133009,#133010,#133011,#133012,#133013,#133014,
#133015,#133016,#133017,#133018,#133019,#133020,#133021,#133022,#133023,
#133024,#133025,#133026,#133027,#133028,#133029,#133030,#133031,#133032,
#133033,#133034,#133035,#133036,#133037,#133038,#133039,#133040,#133041,
#133042,#133043,#133044,#133045,#133046,#133047,#133048,#133049,#133050,
#133051,#133052,#133053,#133054,#133055,#133056,#133057,#133058,#133059,
#133060,#133061,#133062,#133063,#133064,#133065,#133066,#133067,#133068,
#133069,#133070,#133071,#133072,#133073,#133074,#133075,#133076,#133077,
#133078,#133079,#133080,#133081,#133082,#133083,#133084,#133085,#133086,
#133087,#133088,#133089,#133090,#133091,#133092,#133093,#133094,#133095,
#133096,#133097,#133098,#133099,#133100,#133101,#133102,#133103,#133104,
#133105,#133106,#133107,#133108,#133109,#133110,#133111,#133112,#133113,
#133114,#133115,#133116,#133117,#133118,#133119,#133120,#133121,#133122,
#133123,#133124,#133125,#133126,#133127,#133128,#133129,#133130,#133131,
#133132,#133133,#133134,#133135,#133136,#133137,#133138,#133139,#133140,
#133141,#133142,#133143,#133144,#133145,#133146,#133147,#133148,#133149,
#133150,#133151,#133152,#133153,#133154,#133155,#133156,#133157,#133158,
#133159,#133160,#133161,#133162,#133163,#133164,#133165,#133166,#133167,
#133168,#133169,#133170,#133171,#133172,#133173,#133174,#133175,#133176,
#133177,#133178,#133179,#133180,#133181,#133182,#133183,#133184,#133185,
#133186,#133187,#133188,#133189,#133190,#133191,#133192,#133193,#133194,
#133195,#133196,#133197,#133198,#133199,#133200,#133201,#133202),
 .UNSPECIFIED.,.F.,.F.,(4,3,3,3,3,3,3,3,3,3,3,3,3,3,3,3,3,3,3,3,3,3,3,3,
3,3,3,3,3,3,3,3,3,3,3,3,3,3,3,3,3,3,3,3,3,3,3,3,3,3,3,3,3,3,3,3,3,3,3,3,
3,3,3,3,3,3,3,3,3,3,3,3,3,4),(1592.7874753702,1592.87896172744,1592.9709007737,
1593.06307252995,1593.15556706926,1593.19779047834,1593.28152919019,1593.36516470155,
1593.44871714495,1593.5322065808,1593.61566053142,1593.69909702526,1593.78253413502,
1593.86598992994,1593.94953442267,1594.03312350561,1594.11684677316,1594.19752648906,
1594.28126520091,1594.36490071227,1594.44845315567,1594.53194259152,1594.61539654214,
1594.69883303598,1594.78227014574,1594.86572594066,1594.94927043339,1595.03285951633,
1595.11658278388,1595.19726249978,1595.28100121163,1595.36463672299,1595.44818916639,
1595.53167860224,1595.61513255286,1595.6985690467,1595.78200615646,1595.86546195138,
1595.94900644411,1596.03259552705,1596.1163187946,1596.1969985105,1596.28073722235,
1596.36437273371,1596.44792517711,1596.53141461296,1596.61486856358,1596.69830505742,
1596.78174216718,1596.8651979621,1596.94874245483,1597.03233153777,1597.11605480532,
1597.19673452122,1597.28047323307,1597.36410874443,1597.44766118783,1597.53115062368,
1597.6146045743,1597.69804106814,1597.7814781779,1597.86493397282,1597.94847846555,
1598.03206754849,1598.11579081604,1598.19647053194,1598.27901881213,1598.36147237307,
1598.44385037954,1598.52617192518,1598.60846368296,1598.6907374058,1598.77303243584,
1598.81885555413),.UNSPECIFIED.);
#1067=B_SPLINE_CURVE_WITH_KNOTS('',3,(#133208,#133209,#133210,#133211,#133212,
#133213,#133214,#133215,#133216,#133217,#133218,#133219,#133220,#133221,
#133222,#133223,#133224,#133225,#133226,#133227,#133228,#133229,#133230,
#133231,#133232,#133233,#133234,#133235,#133236,#133237,#133238,#133239,
#133240,#133241,#133242,#133243,#133244,#133245,#133246,#133247,#133248,
#133249,#133250,#133251,#133252,#133253,#133254,#133255,#133256,#133257,
#133258,#133259,#133260,#133261,#133262,#133263,#133264,#133265,#133266,
#133267,#133268,#133269,#133270,#133271,#133272,#133273,#133274,#133275,
#133276,#133277,#133278,#133279,#133280,#133281,#133282,#133283,#133284,
#133285,#133286,#133287,#133288,#133289,#133290,#133291,#133292,#133293,
#133294,#133295,#133296,#133297,#133298,#133299,#133300,#133301,#133302,
#133303,#133304,#133305,#133306,#133307,#133308,#133309,#133310,#133311,
#133312,#133313,#133314,#133315,#133316,#133317,#133318,#133319,#133320,
#133321,#133322,#133323,#133324,#133325,#133326,#133327,#133328,#133329,
#133330,#133331,#133332,#133333,#133334,#133335,#133336,#133337,#133338,
#133339,#133340,#133341,#133342,#133343,#133344,#133345,#133346,#133347,
#133348,#133349,#133350,#133351,#133352,#133353,#133354,#133355,#133356,
#133357,#133358,#133359,#133360,#133361,#133362,#133363,#133364,#133365,
#133366,#133367,#133368,#133369,#133370,#133371,#133372,#133373,#133374,
#133375,#133376,#133377,#133378,#133379,#133380,#133381,#133382,#133383,
#133384,#133385,#133386,#133387,#133388,#133389,#133390,#133391,#133392,
#133393,#133394,#133395,#133396,#133397,#133398,#133399,#133400,#133401,
#133402,#133403,#133404,#133405,#133406,#133407,#133408,#133409,#133410,
#133411,#133412,#133413,#133414,#133415,#133416,#133417,#133418,#133419,
#133420,#133421,#133422,#133423,#133424,#133425,#133426,#133427),
 .UNSPECIFIED.,.F.,.F.,(4,3,3,3,3,3,3,3,3,3,3,3,3,3,3,3,3,3,3,3,3,3,3,3,
3,3,3,3,3,3,3,3,3,3,3,3,3,3,3,3,3,3,3,3,3,3,3,3,3,3,3,3,3,3,3,3,3,3,3,3,
3,3,3,3,3,3,3,3,3,3,3,3,3,4),(1599.07066067734,1599.15302402575,1599.23531412012,
1599.3175560504,1599.39977319763,1599.48198459586,1599.56420927224,1599.64651601869,
1599.72886431527,1599.81134162596,1599.88565193366,1599.96939064551,1600.05302615687,
1600.13657860027,1600.22006803612,1600.30352198674,1600.38695848058,1600.47039559034,
1600.55385138526,1600.63739587799,1600.72098496093,1600.80470822849,1600.88538794438,
1600.96912665623,1601.05276216759,1601.13631461099,1601.21980404684,1601.30325799746,
1601.3866944913,1601.47013160106,1601.55358739598,1601.6371318887,1601.72072097165,
1601.8044442392,1601.8851239551,1601.96886266695,1602.05249817831,1602.13605062171,
1602.21954005756,1602.30299400818,1602.38643050202,1602.46986761178,1602.5533234067,
1602.63686789943,1602.72045698237,1602.80418024992,1602.88485996582,1602.96859867767,
1603.05223418903,1603.13578663243,1603.21927606828,1603.3027300189,1603.38616651274,
1603.4696036225,1603.55305941742,1603.63660391015,1603.72019299309,1603.80391626064,
1603.88459597654,1603.96833468839,1604.05197019975,1604.13552264315,1604.219012079,
1604.30246602962,1604.38590252346,1604.46933963322,1604.55279542814,1604.63633992087,
1604.71992900381,1604.80365227136,1604.88433198726,1604.97368932459,1605.06283149349,
1605.10354352794),.UNSPECIFIED.);
#1068=B_SPLINE_CURVE_WITH_KNOTS('',3,(#133428,#133429,#133430,#133431,#133432,
#133433,#133434,#133435,#133436,#133437),.UNSPECIFIED.,.F.,.F.,(4,3,3,4),
(1598.81925848019,1598.88591592294,1599.01127570596,1599.0706606772),
 .UNSPECIFIED.);
#1069=B_SPLINE_CURVE_WITH_KNOTS('',3,(#133439,#133440,#133441,#133442,#133443,
#133444,#133445,#133446,#133447,#133448),.UNSPECIFIED.,.F.,.F.,(4,3,3,4),
(1598.81885555413,1598.90121960559,1598.98594014133,1599.07066067708),
 .UNSPECIFIED.);
#1070=B_SPLINE_CURVE_WITH_KNOTS('',3,(#133449,#133450,#133451,#133452,#133453,
#133454,#133455,#133456,#133457,#133458,#133459,#133460,#133461,#133462,
#133463,#133464,#133465,#133466,#133467,#133468,#133469,#133470,#133471,
#133472,#133473,#133474,#133475,#133476,#133477,#133478,#133479,#133480,
#133481,#133482,#133483,#133484,#133485,#133486,#133487,#133488,#133489,
#133490,#133491,#133492,#133493,#133494,#133495,#133496,#133497,#133498,
#133499,#133500,#133501,#133502,#133503,#133504,#133505,#133506,#133507,
#133508,#133509,#133510,#133511,#133512,#133513,#133514,#133515,#133516,
#133517,#133518,#133519,#133520,#133521,#133522,#133523,#133524,#133525,
#133526,#133527,#133528,#133529,#133530,#133531,#133532,#133533,#133534,
#133535,#133536,#133537,#133538,#133539,#133540,#133541,#133542,#133543,
#133544,#133545,#133546,#133547,#133548,#133549,#133550,#133551,#133552,
#133553,#133554,#133555,#133556,#133557,#133558,#133559,#133560,#133561,
#133562,#133563,#133564,#133565,#133566,#133567,#133568,#133569,#133570,
#133571,#133572,#133573,#133574,#133575,#133576,#133577,#133578,#133579,
#133580,#133581,#133582,#133583,#133584,#133585,#133586,#133587,#133588,
#133589,#133590,#133591,#133592,#133593,#133594,#133595,#133596,#133597,
#133598,#133599,#133600,#133601,#133602,#133603,#133604,#133605,#133606,
#133607,#133608,#133609,#133610,#133611,#133612,#133613,#133614,#133615,
#133616,#133617,#133618,#133619,#133620,#133621,#133622,#133623,#133624,
#133625,#133626,#133627,#133628,#133629,#133630,#133631,#133632,#133633,
#133634,#133635,#133636,#133637,#133638,#133639,#133640,#133641,#133642,
#133643,#133644,#133645,#133646,#133647,#133648,#133649,#133650,#133651,
#133652,#133653,#133654,#133655,#133656,#133657,#133658,#133659,#133660,
#133661,#133662,#133663,#133664,#133665),.UNSPECIFIED.,.F.,.F.,(4,3,3,3,
3,3,3,3,3,3,3,3,3,3,3,3,3,3,3,3,3,3,3,3,3,3,3,3,3,3,3,3,3,3,3,3,3,3,3,3,
3,3,3,3,3,3,3,3,3,3,3,3,3,3,3,3,3,3,3,3,3,3,3,3,3,3,3,3,3,3,3,3,4),(1599.07066067721,
1599.19620654266,1599.27994525451,1599.36358076587,1599.44713320927,1599.53062264512,
1599.61407659574,1599.69751308958,1599.78095019934,1599.86440599426,1599.94795048699,
1600.03153956993,1600.11526283748,1600.19594255338,1600.27968126523,1600.36331677659,
1600.44686921999,1600.53035865584,1600.61381260646,1600.6972491003,1600.78068621006,
1600.86414200498,1600.94768649771,1601.03127558065,1601.1149988482,1601.1956785641,
1601.27941727595,1601.36305278731,1601.44660523071,1601.53009466656,1601.61354861718,
1601.69698511102,1601.78042222078,1601.8638780157,1601.94742250843,1602.03101159137,
1602.11473485892,1602.19541457482,1602.27915328667,1602.36278879803,1602.44634124143,
1602.52983067728,1602.6132846279,1602.69672112174,1602.7801582315,1602.86361402642,
1602.94715851915,1603.03074760209,1603.11447086964,1603.19515058554,1603.27888929739,
1603.36252480875,1603.44607725215,1603.529566688,1603.61302063862,1603.69645713246,
1603.77989424222,1603.86335003713,1603.94689452986,1604.03048361281,1604.11420688036,
1604.19488659626,1604.27863066505,1604.36227031628,1604.44582568764,1604.52931283193,
1604.61276270963,1604.69619340916,1604.77962300226,1604.86310851884,1604.9466216911,
1605.03023631808,1605.10235396521),.UNSPECIFIED.);
#1071=B_SPLINE_CURVE_WITH_KNOTS('',3,(#133671,#133672,#133673,#133674,#133675,
#133676,#133677,#133678,#133679,#133680,#133681,#133682,#133683,#133684,
#133685,#133686,#133687,#133688,#133689,#133690,#133691,#133692,#133693,
#133694,#133695,#133696,#133697,#133698,#133699,#133700,#133701,#133702,
#133703,#133704,#133705,#133706,#133707,#133708,#133709,#133710,#133711,
#133712,#133713,#133714,#133715,#133716,#133717,#133718,#133719,#133720,
#133721,#133722,#133723,#133724,#133725,#133726,#133727,#133728,#133729,
#133730,#133731,#133732,#133733,#133734,#133735,#133736,#133737,#133738,
#133739,#133740,#133741,#133742,#133743,#133744,#133745,#133746,#133747,
#133748,#133749,#133750,#133751,#133752,#133753,#133754,#133755,#133756,
#133757,#133758,#133759,#133760,#133761,#133762,#133763,#133764,#133765,
#133766,#133767,#133768,#133769,#133770,#133771,#133772,#133773,#133774,
#133775,#133776,#133777,#133778,#133779,#133780,#133781,#133782,#133783,
#133784,#133785,#133786,#133787,#133788,#133789,#133790,#133791,#133792,
#133793,#133794,#133795,#133796,#133797,#133798,#133799,#133800,#133801,
#133802,#133803,#133804,#133805,#133806,#133807,#133808,#133809,#133810,
#133811,#133812,#133813,#133814,#133815,#133816,#133817,#133818,#133819,
#133820,#133821,#133822,#133823,#133824,#133825,#133826,#133827,#133828,
#133829,#133830,#133831,#133832,#133833,#133834,#133835,#133836,#133837,
#133838,#133839,#133840,#133841,#133842,#133843,#133844,#133845,#133846,
#133847,#133848,#133849,#133850,#133851,#133852,#133853,#133854,#133855,
#133856,#133857,#133858,#133859,#133860,#133861,#133862,#133863,#133864,
#133865,#133866,#133867,#133868,#133869,#133870,#133871,#133872,#133873,
#133874,#133875,#133876,#133877,#133878,#133879,#133880,#133881,#133882,
#133883,#133884,#133885,#133886,#133887),.UNSPECIFIED.,.F.,.F.,(4,3,3,3,
3,3,3,3,3,3,3,3,3,3,3,3,3,3,3,3,3,3,3,3,3,3,3,3,3,3,3,3,3,3,3,3,3,3,3,3,
3,3,3,3,3,3,3,3,3,3,3,3,3,3,3,3,3,3,3,3,3,3,3,3,3,3,3,3,3,3,3,3,4),(1605.35384598438,
1605.44022879737,1605.52669081532,1605.61603511099,1605.70275600956,1605.79341200377,
1605.88406799798,1605.96780670983,1606.05144222119,1606.13499466459,1606.21848410044,
1606.30193805106,1606.3853745449,1606.46881165466,1606.55226744958,1606.63581194231,
1606.71940102525,1606.80312429281,1606.8838040087,1606.96754272055,1607.05117823191,
1607.13473067531,1607.21822011116,1607.30167406178,1607.38511055562,1607.46854766538,
1607.5520034603,1607.63554795302,1607.71913703597,1607.80286030352,1607.88354001942,
1607.96727873127,1608.05091424263,1608.13446668603,1608.21795612188,1608.3014100725,
1608.38484656634,1608.4682836761,1608.55173947102,1608.63528396375,1608.71887304669,
1608.80259631424,1608.88327603014,1608.96701474199,1609.05065025335,1609.13420269675,
1609.2176921326,1609.30114608322,1609.38458257706,1609.46801968682,1609.55147548174,
1609.63501997447,1609.71860905741,1609.80233232497,1609.88301204086,1609.96675075271,
1610.05038626407,1610.13393870747,1610.21742814332,1610.30088209394,1610.38431858778,
1610.46775569754,1610.55121149246,1610.63475598519,1610.71834506813,1610.80206833568,
1610.88274805158,1610.96548316682,1611.04812026984,1611.13250170617,1611.21499298543,
1611.30031950029,1611.38564601516),.UNSPECIFIED.);
#1072=B_SPLINE_CURVE_WITH_KNOTS('',3,(#133888,#133889,#133890,#133891,#133892,
#133893,#133894,#133895,#133896,#133897),.UNSPECIFIED.,.F.,.F.,(4,3,3,4),
(1605.10354352794,1605.19240950004,1605.28105355217,1605.35384598424),
 .UNSPECIFIED.);
#1073=B_SPLINE_CURVE_WITH_KNOTS('',3,(#133899,#133900,#133901,#133902,#133903,
#133904,#133905,#133906,#133907,#133908,#133909,#133910,#133911),
 .UNSPECIFIED.,.F.,.F.,(4,3,3,3,4),(1605.10235396521,1605.18610885268,1605.19462260698,
1605.33154122428,1605.35384598439),.UNSPECIFIED.);
#1074=B_SPLINE_CURVE_WITH_KNOTS('',3,(#133912,#133913,#133914,#133915,#133916,
#133917,#133918,#133919,#133920,#133921,#133922,#133923,#133924,#133925,
#133926,#133927,#133928,#133929,#133930,#133931,#133932,#133933,#133934,
#133935,#133936,#133937,#133938,#133939,#133940,#133941,#133942,#133943,
#133944,#133945,#133946,#133947,#133948,#133949,#133950,#133951,#133952,
#133953,#133954,#133955,#133956,#133957,#133958,#133959,#133960,#133961,
#133962,#133963,#133964,#133965,#133966,#133967,#133968,#133969,#133970,
#133971,#133972,#133973,#133974,#133975,#133976,#133977,#133978,#133979,
#133980,#133981,#133982,#133983,#133984,#133985,#133986,#133987,#133988,
#133989,#133990,#133991,#133992,#133993,#133994,#133995,#133996,#133997,
#133998,#133999,#134000,#134001,#134002,#134003,#134004,#134005,#134006,
#134007,#134008,#134009,#134010,#134011,#134012,#134013,#134014,#134015,
#134016,#134017,#134018,#134019,#134020,#134021,#134022,#134023,#134024,
#134025,#134026,#134027,#134028,#134029,#134030,#134031,#134032,#134033,
#134034,#134035,#134036,#134037,#134038,#134039,#134040,#134041,#134042,
#134043,#134044,#134045,#134046,#134047,#134048,#134049,#134050,#134051,
#134052,#134053,#134054,#134055,#134056,#134057,#134058,#134059,#134060,
#134061,#134062,#134063,#134064,#134065,#134066,#134067,#134068,#134069,
#134070,#134071,#134072,#134073,#134074,#134075,#134076,#134077,#134078,
#134079,#134080,#134081,#134082,#134083,#134084,#134085,#134086,#134087,
#134088,#134089,#134090,#134091,#134092,#134093,#134094,#134095,#134096,
#134097,#134098,#134099,#134100,#134101,#134102,#134103,#134104,#134105,
#134106,#134107,#134108,#134109,#134110,#134111,#134112,#134113,#134114,
#134115,#134116,#134117,#134118,#134119,#134120,#134121,#134122,#134123,
#134124,#134125,#134126,#134127,#134128,#134129,#134130,#134131,#134132,
#134133,#134134),.UNSPECIFIED.,.F.,.F.,(4,3,3,3,3,3,3,3,3,3,3,3,3,3,3,3,
3,3,3,3,3,3,3,3,3,3,3,3,3,3,3,3,3,3,3,3,3,3,3,3,3,3,3,3,3,3,3,3,3,3,3,3,
3,3,3,3,3,3,3,3,3,3,3,3,3,3,3,3,3,3,3,3,3,3,4),(1605.35384598449,1605.43623005758,
1605.51853423986,1605.60301228709,1605.68522798814,1605.76743249965,1605.84964485315,
1605.93582329429,1606.01815352553,1606.10053836855,1606.18303538978,1606.1943586177,
1606.27809732955,1606.36173284091,1606.44528528431,1606.52877472016,1606.61222867078,
1606.69566516462,1606.77910227438,1606.8625580693,1606.94610256203,1607.02969164497,
1607.11341491252,1607.19409462842,1607.27783334027,1607.36146885163,1607.44502129503,
1607.52851073088,1607.6119646815,1607.69540117534,1607.7788382851,1607.86229408002,
1607.94583857275,1608.02942765569,1608.11315092324,1608.19383063914,1608.27756935099,
1608.36120486235,1608.44475730575,1608.5282467416,1608.61170069222,1608.69513718606,
1608.77857429582,1608.86203009074,1608.94557458347,1609.02916366641,1609.11288693397,
1609.19356664986,1609.27730536171,1609.36094087307,1609.44449331647,1609.52798275232,
1609.61143670294,1609.69487319678,1609.77831030654,1609.86176610146,1609.94531059419,
1610.02889967713,1610.11262294469,1610.19330266058,1610.27704137243,1610.36067688379,
1610.44422932719,1610.52771876304,1610.61117271366,1610.6946092075,1610.77804631726,
1610.86150211217,1610.9450466049,1611.02863568784,1611.1123589554,1611.1930386713,
1611.28365903689,1611.37404670308,1611.386724099),.UNSPECIFIED.);
#1075=B_SPLINE_CURVE_WITH_KNOTS('',3,(#134140,#134141,#134142,#134143,#134144,
#134145,#134146,#134147,#134148,#134149,#134150,#134151,#134152,#134153,
#134154,#134155,#134156,#134157,#134158,#134159,#134160,#134161,#134162,
#134163,#134164,#134165,#134166,#134167,#134168,#134169,#134170,#134171,
#134172,#134173,#134174,#134175,#134176,#134177,#134178,#134179,#134180,
#134181,#134182,#134183,#134184,#134185,#134186,#134187,#134188,#134189,
#134190,#134191,#134192,#134193,#134194,#134195,#134196,#134197,#134198,
#134199,#134200,#134201,#134202,#134203,#134204,#134205,#134206,#134207,
#134208,#134209,#134210,#134211,#134212,#134213,#134214,#134215,#134216,
#134217,#134218,#134219,#134220,#134221,#134222,#134223,#134224,#134225,
#134226,#134227,#134228,#134229,#134230,#134231,#134232,#134233,#134234,
#134235,#134236,#134237,#134238,#134239,#134240,#134241,#134242,#134243,
#134244,#134245,#134246,#134247,#134248,#134249,#134250,#134251,#134252,
#134253,#134254,#134255,#134256,#134257,#134258,#134259,#134260,#134261,
#134262,#134263,#134264,#134265,#134266,#134267,#134268,#134269,#134270,
#134271,#134272,#134273,#134274,#134275,#134276,#134277,#134278,#134279,
#134280,#134281,#134282,#134283,#134284,#134285,#134286,#134287,#134288,
#134289,#134290,#134291,#134292,#134293,#134294,#134295,#134296,#134297,
#134298,#134299,#134300,#134301,#134302,#134303,#134304,#134305,#134306,
#134307,#134308,#134309,#134310,#134311,#134312,#134313,#134314,#134315,
#134316,#134317,#134318,#134319,#134320,#134321,#134322,#134323,#134324,
#134325,#134326,#134327,#134328,#134329,#134330,#134331,#134332,#134333,
#134334,#134335,#134336,#134337,#134338,#134339,#134340,#134341,#134342,
#134343,#134344,#134345,#134346,#134347,#134348,#134349,#134350,#134351,
#134352,#134353,#134354,#134355,#134356,#134357,#134358,#134359),
 .UNSPECIFIED.,.F.,.F.,(4,3,3,3,3,3,3,3,3,3,3,3,3,3,3,3,3,3,3,3,3,3,3,3,
3,3,3,3,3,3,3,3,3,3,3,3,3,3,3,3,3,3,3,3,3,3,3,3,3,3,3,3,3,3,3,3,3,3,3,3,
3,3,3,3,3,3,3,3,3,3,3,3,3,4),(1611.63703129169,1611.74502167405,1611.85559144508,
1611.8824840623,1611.96622277415,1612.04985828551,1612.13341072891,1612.21690016476,
1612.30035411538,1612.38379060922,1612.46722771898,1612.5506835139,1612.63422800663,
1612.71781708957,1612.80154035712,1612.88222007302,1612.96595878487,1613.04959429623,
1613.13314673963,1613.21663617548,1613.3000901261,1613.38352661994,1613.4669637297,
1613.55041952462,1613.63396401734,1613.71755310029,1613.80127636784,1613.88195608374,
1613.96569479559,1614.04933030695,1614.13288275035,1614.2163721862,1614.29982613682,
1614.38326263066,1614.46669974042,1614.55015553534,1614.63370002806,1614.71728911101,
1614.80101237856,1614.88169209446,1614.96543080631,1615.04906631767,1615.13261876107,
1615.21610819692,1615.29956214754,1615.38299864138,1615.46643575114,1615.54989154606,
1615.63343603879,1615.71702512173,1615.80074838928,1615.88142810518,1615.96516681703,
1616.04880232839,1616.13235477179,1616.21584420764,1616.29929815826,1616.3827346521,
1616.46617176186,1616.54962755678,1616.63317204951,1616.71676113245,1616.8004844,
1616.8811641159,1616.96491572543,1617.05287003921,1617.13641063114,1617.2198945257,
1617.3033398417,1617.38676466796,1617.47020902566,1617.55366475935,1617.63717820047,
1617.66855023561),.UNSPECIFIED.);
#1076=B_SPLINE_CURVE_WITH_KNOTS('',3,(#134360,#134361,#134362,#134363,#134364,
#134365,#134366,#134367,#134368,#134369),.UNSPECIFIED.,.F.,.F.,(4,3,3,4),
(1611.38564601516,1611.46810946382,1611.55257037769,1611.63703129156),
 .UNSPECIFIED.);
#1077=B_SPLINE_CURVE_WITH_KNOTS('',3,(#134371,#134372,#134373,#134374,#134375,
#134376,#134377,#134378,#134379,#134380),.UNSPECIFIED.,.F.,.F.,(4,3,3,4),
(1611.386724099,1611.47681850758,1611.56662740094,1611.63703129145),
 .UNSPECIFIED.);
#1078=B_SPLINE_CURVE_WITH_KNOTS('',3,(#134381,#134382,#134383,#134384,#134385,
#134386,#134387,#134388,#134389,#134390,#134391,#134392,#134393,#134394,
#134395,#134396,#134397,#134398,#134399,#134400,#134401,#134402,#134403,
#134404,#134405,#134406,#134407,#134408,#134409,#134410,#134411,#134412,
#134413,#134414,#134415,#134416,#134417,#134418,#134419,#134420,#134421,
#134422,#134423,#134424,#134425,#134426,#134427,#134428,#134429,#134430,
#134431,#134432,#134433,#134434,#134435,#134436,#134437,#134438,#134439,
#134440,#134441,#134442,#134443,#134444,#134445,#134446,#134447,#134448,
#134449,#134450,#134451,#134452,#134453,#134454,#134455,#134456,#134457,
#134458,#134459,#134460,#134461,#134462,#134463,#134464,#134465,#134466,
#134467,#134468,#134469,#134470,#134471,#134472,#134473,#134474,#134475,
#134476,#134477,#134478,#134479,#134480,#134481,#134482,#134483,#134484,
#134485,#134486,#134487,#134488,#134489,#134490,#134491,#134492,#134493,
#134494,#134495,#134496,#134497,#134498,#134499,#134500,#134501,#134502,
#134503,#134504,#134505,#134506,#134507,#134508,#134509,#134510,#134511,
#134512,#134513,#134514,#134515,#134516,#134517,#134518,#134519,#134520,
#134521,#134522,#134523,#134524,#134525,#134526,#134527,#134528,#134529,
#134530,#134531,#134532,#134533,#134534,#134535,#134536,#134537,#134538,
#134539,#134540,#134541,#134542,#134543,#134544,#134545,#134546,#134547,
#134548,#134549,#134550,#134551,#134552,#134553,#134554,#134555,#134556,
#134557,#134558,#134559,#134560,#134561,#134562,#134563,#134564,#134565,
#134566,#134567,#134568,#134569,#134570,#134571,#134572,#134573,#134574,
#134575,#134576,#134577,#134578,#134579,#134580,#134581,#134582,#134583,
#134584,#134585,#134586,#134587,#134588,#134589,#134590,#134591,#134592,
#134593,#134594,#134595,#134596,#134597,#134598,#134599,#134600),
 .UNSPECIFIED.,.F.,.F.,(4,3,3,3,3,3,3,3,3,3,3,3,3,3,3,3,3,3,3,3,3,3,3,3,
3,3,3,3,3,3,3,3,3,3,3,3,3,3,3,3,3,3,3,3,3,3,3,3,3,3,3,3,3,3,3,3,3,3,3,3,
3,3,3,3,3,3,3,3,3,3,3,3,3,4),(1611.63703129156,1611.7226684655,1611.80836065655,
1611.8941219279,1611.98002840369,1612.06601597233,1612.1521607194,1612.19277468202,
1612.27651339387,1612.36014890523,1612.44370134863,1612.52719078448,1612.6106447351,
1612.69408122894,1612.7775183387,1612.86097413362,1612.94451862635,1613.02810770929,
1613.11183097685,1613.19251069274,1613.27624940459,1613.35988491595,1613.44343735935,
1613.5269267952,1613.61038074582,1613.69381723966,1613.77725434942,1613.86071014433,
1613.94425463706,1614.02784372,1614.11156698756,1614.19224670346,1614.27598541531,
1614.35962092667,1614.44317337007,1614.52666280592,1614.61011675654,1614.69355325038,
1614.77699036014,1614.86044615506,1614.94399064779,1615.02757973073,1615.11130299828,
1615.19198271418,1615.27572142603,1615.35935693739,1615.44290938079,1615.52639881664,
1615.60985276726,1615.6932892611,1615.77672637086,1615.86018216578,1615.94372665851,
1616.02731574145,1616.11103900901,1616.1917187249,1616.27545743675,1616.35909294811,
1616.44264539151,1616.52613482736,1616.60958877798,1616.69302527182,1616.77646238158,
1616.8599181765,1616.94346266922,1617.02705175217,1617.11077501972,1617.19145473562,
1617.27439607099,1617.35723784698,1617.4399848302,1617.52267650246,1617.60533543112,
1617.66895862687),.UNSPECIFIED.);
#1079=B_SPLINE_CURVE_WITH_KNOTS('',3,(#134606,#134607,#134608,#134609,#134610,
#134611,#134612,#134613,#134614,#134615,#134616,#134617,#134618,#134619,
#134620,#134621,#134622,#134623,#134624,#134625,#134626,#134627,#134628,
#134629,#134630,#134631,#134632,#134633,#134634,#134635,#134636,#134637,
#134638,#134639,#134640,#134641,#134642,#134643,#134644,#134645,#134646,
#134647,#134648,#134649,#134650,#134651,#134652,#134653,#134654,#134655,
#134656,#134657,#134658,#134659,#134660,#134661,#134662,#134663,#134664,
#134665,#134666,#134667,#134668,#134669,#134670,#134671,#134672,#134673,
#134674,#134675,#134676,#134677,#134678,#134679,#134680,#134681,#134682,
#134683,#134684,#134685,#134686,#134687,#134688,#134689,#134690,#134691,
#134692,#134693,#134694,#134695,#134696,#134697,#134698,#134699,#134700,
#134701,#134702,#134703,#134704,#134705,#134706,#134707,#134708,#134709,
#134710,#134711,#134712,#134713,#134714,#134715,#134716,#134717,#134718,
#134719,#134720,#134721,#134722,#134723,#134724,#134725,#134726,#134727,
#134728,#134729,#134730,#134731,#134732,#134733,#134734,#134735,#134736,
#134737,#134738,#134739,#134740,#134741,#134742,#134743,#134744,#134745,
#134746,#134747,#134748,#134749,#134750,#134751,#134752,#134753,#134754,
#134755,#134756,#134757,#134758,#134759,#134760,#134761,#134762,#134763,
#134764,#134765,#134766,#134767,#134768,#134769,#134770,#134771,#134772,
#134773,#134774,#134775,#134776,#134777,#134778,#134779,#134780,#134781,
#134782,#134783,#134784,#134785,#134786,#134787,#134788,#134789,#134790,
#134791,#134792,#134793,#134794,#134795,#134796,#134797,#134798,#134799,
#134800,#134801,#134802,#134803,#134804,#134805,#134806,#134807,#134808,
#134809,#134810,#134811,#134812,#134813,#134814,#134815,#134816,#134817,
#134818,#134819,#134820,#134821,#134822,#134823,#134824,#134825),
 .UNSPECIFIED.,.F.,.F.,(4,3,3,3,3,3,3,3,3,3,3,3,3,3,3,3,3,3,3,3,3,3,3,3,
3,3,3,3,3,3,3,3,3,3,3,3,3,3,3,3,3,3,3,3,3,3,3,3,3,3,3,3,3,3,3,3,3,3,3,3,
3,3,3,3,3,3,3,3,3,3,3,3,3,4),(1617.92021659891,1618.00342250642,1618.08652728227,
1618.16955157317,1618.25251594955,1618.33544933007,1618.41836898947,1618.50129346078,
1618.58424127696,1618.6672785596,1618.75036549745,1618.83357605855,1618.88063613734,
1618.96437484919,1619.04801036055,1619.13156280395,1619.2150522398,1619.29850619042,
1619.38194268426,1619.46537979402,1619.54883558894,1619.63238008167,1619.71596916461,
1619.79969243216,1619.88037214806,1619.96411085991,1620.04774637127,1620.13129881467,
1620.21478825052,1620.29824220114,1620.38167869498,1620.46511580474,1620.54857159966,
1620.63211609239,1620.71570517533,1620.79942844288,1620.88010815878,1620.96384687063,
1621.04748238199,1621.13103482539,1621.21452426124,1621.29797821186,1621.3814147057,
1621.46485181546,1621.54830761038,1621.63185210311,1621.71544118605,1621.7991644536,
1621.8798441695,1621.96358288135,1622.04721839271,1622.13077083611,1622.21426027196,
1622.29771422258,1622.38115071642,1622.46458782618,1622.5480436211,1622.63158811383,
1622.71517719677,1622.79890046433,1622.87958018022,1622.96331889207,1623.04695440343,
1623.13050684683,1623.21399628268,1623.2974502333,1623.38088672714,1623.4643238369,
1623.54777963182,1623.63132412455,1623.71491320749,1623.79863647504,1623.87931619094,
1623.9527520866),.UNSPECIFIED.);
#1080=B_SPLINE_CURVE_WITH_KNOTS('',3,(#134826,#134827,#134828,#134829,#134830,
#134831,#134832,#134833,#134834,#134835,#134836,#134837,#134838),
 .UNSPECIFIED.,.F.,.F.,(4,3,3,3,4),(1617.66855023561,1617.75216328162,1617.83590032492,
1617.88090012662,1617.92021659874),.UNSPECIFIED.);
#1081=B_SPLINE_CURVE_WITH_KNOTS('',3,(#134840,#134841,#134842,#134843,#134844,
#134845,#134846,#134847,#134848,#134849),.UNSPECIFIED.,.F.,.F.,(4,3,3,4),
(1617.66895862687,1617.75160822956,1617.83591241415,1617.92021659874),
 .UNSPECIFIED.);
#1082=B_SPLINE_CURVE_WITH_KNOTS('',3,(#134850,#134851,#134852,#134853,#134854,
#134855,#134856,#134857,#134858,#134859,#134860,#134861,#134862,#134863,
#134864,#134865,#134866,#134867,#134868,#134869,#134870,#134871,#134872,
#134873,#134874,#134875,#134876,#134877,#134878,#134879,#134880,#134881,
#134882,#134883,#134884,#134885,#134886,#134887,#134888,#134889,#134890,
#134891,#134892,#134893,#134894,#134895,#134896,#134897,#134898,#134899,
#134900,#134901,#134902,#134903,#134904,#134905,#134906,#134907,#134908,
#134909,#134910,#134911,#134912,#134913,#134914,#134915,#134916,#134917,
#134918,#134919,#134920,#134921,#134922,#134923,#134924,#134925,#134926,
#134927,#134928,#134929,#134930,#134931,#134932,#134933,#134934,#134935,
#134936,#134937,#134938,#134939,#134940,#134941,#134942,#134943,#134944,
#134945,#134946,#134947,#134948,#134949,#134950,#134951,#134952,#134953,
#134954,#134955,#134956,#134957,#134958,#134959,#134960,#134961,#134962,
#134963,#134964,#134965,#134966,#134967,#134968,#134969,#134970,#134971,
#134972,#134973,#134974,#134975,#134976,#134977,#134978,#134979,#134980,
#134981,#134982,#134983,#134984,#134985,#134986,#134987,#134988,#134989,
#134990,#134991,#134992,#134993,#134994,#134995,#134996,#134997,#134998,
#134999,#135000,#135001,#135002,#135003,#135004,#135005,#135006,#135007,
#135008,#135009,#135010,#135011,#135012,#135013,#135014,#135015,#135016,
#135017,#135018,#135019,#135020,#135021,#135022,#135023,#135024,#135025,
#135026,#135027,#135028,#135029,#135030,#135031,#135032,#135033,#135034,
#135035,#135036,#135037,#135038,#135039,#135040,#135041,#135042,#135043,
#135044,#135045,#135046,#135047,#135048,#135049,#135050,#135051,#135052,
#135053,#135054,#135055,#135056,#135057,#135058,#135059,#135060,#135061,
#135062,#135063,#135064,#135065,#135066),.UNSPECIFIED.,.F.,.F.,(4,3,3,3,
3,3,3,3,3,3,3,3,3,3,3,3,3,3,3,3,3,3,3,3,3,3,3,3,3,3,3,3,3,3,3,3,3,3,3,3,
3,3,3,3,3,3,3,3,3,3,3,3,3,3,3,3,3,3,3,3,3,3,3,3,3,3,3,3,3,3,3,3,4),(1617.92021659892,
1618.02434059583,1618.13030678927,1618.19119074634,1618.27492945819,1618.35856496955,
1618.44211741295,1618.5256068488,1618.60906079941,1618.69249729326,1618.77593440302,
1618.85939019793,1618.94293469066,1619.0265237736,1619.11024704116,1619.19092675706,
1619.27466546891,1619.35830098027,1619.44185342367,1619.52534285952,1619.60879681014,
1619.69223330398,1619.77567041374,1619.85912620866,1619.94267070138,1620.02625978433,
1620.10998305188,1620.19066276778,1620.27440147963,1620.35803699099,1620.44158943439,
1620.52507887024,1620.60853282086,1620.6919693147,1620.77540642446,1620.85886221938,
1620.94240671211,1621.02599579505,1621.10971906261,1621.1903987785,1621.27413749035,
1621.35777300171,1621.44132544511,1621.52481488096,1621.60826883158,1621.69170532542,
1621.77514243518,1621.8585982301,1621.94214272282,1622.02573180577,1622.10945507332,
1622.19013478922,1622.27387350107,1622.35750901243,1622.44106145583,1622.52455089168,
1622.6080048423,1622.69144133614,1622.7748784459,1622.85833424082,1622.94187873355,
1623.02546781649,1623.10919108405,1623.18987079994,1623.27362409456,1623.35838895161,
1623.44193270565,1623.5254185924,1623.60886473297,1623.69458428748,1623.77802358541,
1623.86488326821,1623.95174295101),.UNSPECIFIED.);
#1083=B_SPLINE_CURVE_WITH_KNOTS('',3,(#135072,#135073,#135074,#135075,#135076,
#135077,#135078,#135079,#135080,#135081,#135082,#135083,#135084,#135085,
#135086,#135087,#135088,#135089,#135090,#135091,#135092,#135093,#135094,
#135095,#135096,#135097,#135098,#135099,#135100,#135101,#135102,#135103,
#135104,#135105,#135106,#135107,#135108,#135109,#135110,#135111,#135112,
#135113,#135114,#135115,#135116,#135117,#135118,#135119,#135120,#135121,
#135122,#135123,#135124,#135125,#135126,#135127,#135128,#135129,#135130,
#135131,#135132,#135133,#135134,#135135,#135136,#135137,#135138,#135139,
#135140,#135141,#135142,#135143,#135144,#135145,#135146,#135147,#135148,
#135149,#135150,#135151,#135152,#135153,#135154,#135155,#135156,#135157,
#135158,#135159,#135160,#135161,#135162,#135163,#135164,#135165,#135166,
#135167,#135168,#135169,#135170,#135171,#135172,#135173,#135174,#135175,
#135176,#135177,#135178,#135179,#135180,#135181,#135182,#135183,#135184,
#135185,#135186,#135187,#135188,#135189,#135190,#135191,#135192,#135193,
#135194,#135195,#135196,#135197,#135198,#135199,#135200,#135201,#135202,
#135203,#135204,#135205,#135206,#135207,#135208,#135209,#135210,#135211,
#135212,#135213,#135214,#135215,#135216,#135217,#135218,#135219,#135220,
#135221,#135222,#135223,#135224,#135225,#135226,#135227,#135228,#135229,
#135230,#135231,#135232,#135233,#135234,#135235,#135236,#135237,#135238,
#135239,#135240,#135241,#135242,#135243,#135244,#135245,#135246,#135247,
#135248,#135249,#135250,#135251,#135252,#135253,#135254,#135255,#135256,
#135257,#135258,#135259,#135260,#135261,#135262,#135263,#135264,#135265,
#135266,#135267,#135268,#135269,#135270,#135271,#135272,#135273,#135274,
#135275,#135276,#135277,#135278,#135279,#135280,#135281,#135282,#135283,
#135284,#135285,#135286,#135287,#135288,#135289,#135290,#135291),
 .UNSPECIFIED.,.F.,.F.,(4,3,3,3,3,3,3,3,3,3,3,3,3,3,3,3,3,3,3,3,3,3,3,3,
3,3,3,3,3,3,3,3,3,3,3,3,3,3,3,3,3,3,3,3,3,3,3,3,3,3,3,3,3,3,3,3,3,3,3,3,
3,3,3,3,3,3,3,3,3,3,3,3,3,4),(1624.20340190592,1624.28785819289,1624.371102368,
1624.45434756165,1624.53761197112,1624.62297202876,1624.70637537919,1624.79271379042,
1624.87905220166,1624.96279091351,1625.04642642487,1625.12997886827,1625.21346830412,
1625.29692225474,1625.38035874858,1625.46379585834,1625.54725165326,1625.63079614599,
1625.71438522893,1625.79810849648,1625.87878821238,1625.96252692423,1626.04616243559,
1626.12971487899,1626.21320431484,1626.29665826546,1626.3800947593,1626.46353186906,
1626.54698766398,1626.63053215671,1626.71412123965,1626.79784450721,1626.8785242231,
1626.96226293495,1627.04589844631,1627.12945088971,1627.21294032556,1627.29639427618,
1627.37983077002,1627.46326787978,1627.5467236747,1627.63026816742,1627.71385725037,
1627.79758051792,1627.87826023382,1627.96199894567,1628.04563445703,1628.12918690043,
1628.21267633628,1628.2961302869,1628.37956678074,1628.4630038905,1628.54645968542,
1628.63000417815,1628.71359326109,1628.79731652864,1628.87799624454,1628.96173495639,
1629.04537046775,1629.12892291115,1629.212412347,1629.29586629762,1629.37930279146,
1629.46273990122,1629.54619569613,1629.62974018886,1629.7133292718,1629.79705253936,
1629.87773225526,1629.96253266822,1630.04718562312,1630.13175281295,1630.21623392709,
1630.23592963608),.UNSPECIFIED.);
#1084=B_SPLINE_CURVE_WITH_KNOTS('',3,(#135292,#135293,#135294,#135295,#135296,
#135297,#135298,#135299,#135300,#135301),.UNSPECIFIED.,.F.,.F.,(4,3,3,4),
(1623.9527520866,1624.05174031403,1624.1497797886,1624.20340190574),
 .UNSPECIFIED.);
#1085=B_SPLINE_CURVE_WITH_KNOTS('',3,(#135303,#135304,#135305,#135306,#135307,
#135308,#135309,#135310,#135311,#135312,#135313,#135314,#135315),
 .UNSPECIFIED.,.F.,.F.,(4,3,3,3,4),(1623.95174295101,1624.03533854297,1624.11906535509,
1624.18960681066,1624.20340190592),.UNSPECIFIED.);
#1086=B_SPLINE_CURVE_WITH_KNOTS('',3,(#135316,#135317,#135318,#135319,#135320,
#135321,#135322,#135323,#135324,#135325,#135326,#135327,#135328,#135329,
#135330,#135331,#135332,#135333,#135334,#135335,#135336,#135337,#135338,
#135339,#135340,#135341,#135342,#135343,#135344,#135345,#135346,#135347,
#135348,#135349,#135350,#135351,#135352,#135353,#135354,#135355,#135356,
#135357,#135358,#135359,#135360,#135361,#135362,#135363,#135364,#135365,
#135366,#135367,#135368,#135369,#135370,#135371,#135372,#135373,#135374,
#135375,#135376,#135377,#135378,#135379,#135380,#135381,#135382,#135383,
#135384,#135385,#135386,#135387,#135388,#135389,#135390,#135391,#135392,
#135393,#135394,#135395,#135396,#135397,#135398,#135399,#135400,#135401,
#135402,#135403,#135404,#135405,#135406,#135407,#135408,#135409,#135410,
#135411,#135412,#135413,#135414,#135415,#135416,#135417,#135418,#135419,
#135420,#135421,#135422,#135423,#135424,#135425,#135426,#135427,#135428,
#135429,#135430,#135431,#135432,#135433,#135434,#135435,#135436,#135437,
#135438,#135439,#135440,#135441,#135442,#135443,#135444,#135445,#135446,
#135447,#135448,#135449,#135450,#135451,#135452,#135453,#135454,#135455,
#135456,#135457,#135458,#135459,#135460,#135461,#135462,#135463,#135464,
#135465,#135466,#135467,#135468,#135469,#135470,#135471,#135472,#135473,
#135474,#135475,#135476,#135477,#135478,#135479,#135480,#135481,#135482,
#135483,#135484,#135485,#135486,#135487,#135488,#135489,#135490,#135491,
#135492,#135493,#135494,#135495,#135496,#135497,#135498,#135499,#135500,
#135501,#135502,#135503,#135504,#135505,#135506,#135507,#135508,#135509,
#135510,#135511,#135512,#135513,#135514,#135515,#135516,#135517,#135518,
#135519,#135520,#135521,#135522,#135523,#135524,#135525,#135526,#135527,
#135528,#135529,#135530,#135531,#135532,#135533,#135534,#135535),
 .UNSPECIFIED.,.F.,.F.,(4,3,3,3,3,3,3,3,3,3,3,3,3,3,3,3,3,3,3,3,3,3,3,3,
3,3,3,3,3,3,3,3,3,3,3,3,3,3,3,3,3,3,3,3,3,3,3,3,3,3,3,3,3,3,3,3,3,3,3,3,
3,3,3,3,3,3,3,3,3,3,3,3,3,4),(1624.20340190605,1624.28693851179,1624.37037225623,
1624.45372348263,1624.53701246057,1624.62026714213,1624.70350544141,1624.78674561904,
1624.87000593319,1624.95335509251,1625.03675050512,1625.12027638167,1625.18934282138,
1625.27308153323,1625.35671704459,1625.44026948799,1625.52375892384,1625.60721287446,
1625.6906493683,1625.77408647806,1625.85754227297,1625.9410867657,1626.02467584864,
1626.1083991162,1626.1890788321,1626.27281754395,1626.35645305531,1626.44000549871,
1626.52349493456,1626.60694888517,1626.69038537902,1626.77382248878,1626.85727828369,
1626.94082277642,1627.02441185936,1627.10813512692,1627.18881484282,1627.27255355467,
1627.35618906603,1627.43974150943,1627.52323094528,1627.6066848959,1627.69012138974,
1627.7735584995,1627.85701429442,1627.94055878715,1628.02414787009,1628.10787113765,
1628.18855085354,1628.27228956539,1628.35592507675,1628.43947752015,1628.522966956,
1628.60642090662,1628.68985740046,1628.77329451022,1628.85675030514,1628.94029479787,
1629.02388388081,1629.10760714836,1629.18828686426,1629.27202557611,1629.35566108747,
1629.43921353087,1629.52270296673,1629.60615691734,1629.68959341119,1629.77303052094,
1629.85648631586,1629.94003080859,1630.02361989153,1630.10734315909,1630.18802287498,
1630.23580470972),.UNSPECIFIED.);
#1087=B_SPLINE_CURVE_WITH_KNOTS('',3,(#135541,#135542,#135543,#135544,#135545,
#135546,#135547,#135548,#135549,#135550,#135551,#135552,#135553,#135554,
#135555,#135556,#135557,#135558,#135559,#135560,#135561,#135562,#135563,
#135564,#135565,#135566,#135567,#135568,#135569,#135570,#135571,#135572,
#135573,#135574,#135575,#135576,#135577,#135578,#135579,#135580,#135581,
#135582,#135583,#135584,#135585,#135586,#135587,#135588,#135589,#135590,
#135591,#135592,#135593,#135594,#135595,#135596,#135597,#135598,#135599,
#135600,#135601,#135602,#135603,#135604,#135605,#135606,#135607,#135608,
#135609,#135610,#135611,#135612,#135613,#135614,#135615,#135616,#135617,
#135618,#135619,#135620,#135621,#135622,#135623,#135624,#135625,#135626,
#135627,#135628,#135629,#135630,#135631,#135632,#135633,#135634,#135635,
#135636,#135637,#135638,#135639,#135640,#135641,#135642,#135643,#135644,
#135645,#135646,#135647,#135648,#135649,#135650,#135651,#135652,#135653,
#135654,#135655,#135656,#135657,#135658,#135659,#135660,#135661,#135662,
#135663,#135664,#135665,#135666,#135667,#135668,#135669,#135670,#135671,
#135672,#135673,#135674,#135675,#135676,#135677,#135678,#135679,#135680,
#135681,#135682,#135683,#135684,#135685,#135686,#135687,#135688,#135689,
#135690,#135691,#135692,#135693,#135694,#135695,#135696,#135697,#135698,
#135699,#135700,#135701,#135702,#135703,#135704,#135705,#135706,#135707,
#135708,#135709,#135710,#135711,#135712,#135713,#135714,#135715,#135716,
#135717,#135718,#135719,#135720,#135721,#135722,#135723,#135724,#135725,
#135726,#135727,#135728,#135729,#135730,#135731,#135732,#135733,#135734,
#135735,#135736,#135737,#135738,#135739,#135740,#135741,#135742,#135743,
#135744,#135745,#135746,#135747,#135748,#135749,#135750,#135751,#135752,
#135753,#135754,#135755,#135756,#135757,#135758,#135759,#135760),
 .UNSPECIFIED.,.F.,.F.,(4,3,3,3,3,3,3,3,3,3,3,3,3,3,3,3,3,3,3,3,3,3,3,3,
3,3,3,3,3,3,3,3,3,3,3,3,3,3,3,3,3,3,3,3,3,3,3,3,3,3,3,3,3,3,3,3,3,3,3,3,
3,3,3,3,3,3,3,3,3,3,3,3,3,4),(1630.48658721329,1630.57923050421,1630.67241058499,
1630.76586966149,1630.85967611113,1630.87746826598,1630.96120697783,1631.0448424892,
1631.1283949326,1631.21188436845,1631.29533831906,1631.37877481291,1631.46221192267,
1631.54566771758,1631.62921221032,1631.71280129326,1631.79652456082,1631.8772042767,
1631.96094298855,1632.04457849991,1632.12813094331,1632.21162037916,1632.29507432978,
1632.37851082362,1632.46194793338,1632.5454037283,1632.62894822102,1632.71253730397,
1632.79626057152,1632.87694028742,1632.96067899927,1633.04431451063,1633.12786695403,
1633.21135638988,1633.2948103405,1633.37824683434,1633.4616839441,1633.54513973901,
1633.62868423174,1633.71227331469,1633.79599658224,1633.87667629814,1633.96041500999,
1634.04405052135,1634.12760296475,1634.2110924006,1634.29454635122,1634.37798284506,
1634.46141995482,1634.54487574974,1634.62842024247,1634.71200932541,1634.79573259296,
1634.87641230886,1634.96015102071,1635.04378653207,1635.12733897547,1635.21082841132,
1635.29428236194,1635.37771885578,1635.46115596554,1635.54461176045,1635.62815625318,
1635.71174533612,1635.79546860368,1635.87614831958,1635.95878444239,1636.0413259703,
1636.1237920081,1636.20620159154,1636.28858318972,1636.37094650471,1636.45333691255,
1636.51794311402),.UNSPECIFIED.);
#1088=B_SPLINE_CURVE_WITH_KNOTS('',3,(#135761,#135762,#135763,#135764,#135765,
#135766,#135767,#135768,#135769,#135770),.UNSPECIFIED.,.F.,.F.,(4,3,3,4),
(1630.23592963608,1630.32033661955,1630.40471644067,1630.4865872131),
 .UNSPECIFIED.);
#1089=B_SPLINE_CURVE_WITH_KNOTS('',3,(#135772,#135773,#135774,#135775,#135776,
#135777,#135778,#135779,#135780,#135781),.UNSPECIFIED.,.F.,.F.,(4,3,3,4),
(1630.23580470972,1630.33778215448,1630.43849155912,1630.48658721296),
 .UNSPECIFIED.);
#1090=B_SPLINE_CURVE_WITH_KNOTS('',3,(#135782,#135783,#135784,#135785,#135786,
#135787,#135788,#135789,#135790,#135791,#135792,#135793,#135794,#135795,
#135796,#135797,#135798,#135799,#135800,#135801,#135802,#135803,#135804,
#135805,#135806,#135807,#135808,#135809,#135810,#135811,#135812,#135813,
#135814,#135815,#135816,#135817,#135818,#135819,#135820,#135821,#135822,
#135823,#135824,#135825,#135826,#135827,#135828,#135829,#135830,#135831,
#135832,#135833,#135834,#135835,#135836,#135837,#135838,#135839,#135840,
#135841,#135842,#135843,#135844,#135845,#135846,#135847,#135848,#135849,
#135850,#135851,#135852,#135853,#135854,#135855,#135856,#135857,#135858,
#135859,#135860,#135861,#135862,#135863,#135864,#135865,#135866,#135867,
#135868,#135869,#135870,#135871,#135872,#135873,#135874,#135875,#135876,
#135877,#135878,#135879,#135880,#135881,#135882,#135883,#135884,#135885,
#135886,#135887,#135888,#135889,#135890,#135891,#135892,#135893,#135894,
#135895,#135896,#135897,#135898,#135899,#135900,#135901,#135902,#135903,
#135904,#135905,#135906,#135907,#135908,#135909,#135910,#135911,#135912,
#135913,#135914,#135915,#135916,#135917,#135918,#135919,#135920,#135921,
#135922,#135923,#135924,#135925,#135926,#135927,#135928,#135929,#135930,
#135931,#135932,#135933,#135934,#135935,#135936,#135937,#135938,#135939,
#135940,#135941,#135942,#135943,#135944,#135945,#135946,#135947,#135948,
#135949,#135950,#135951,#135952,#135953,#135954,#135955,#135956,#135957,
#135958,#135959,#135960,#135961,#135962,#135963,#135964,#135965,#135966,
#135967,#135968,#135969,#135970,#135971,#135972,#135973,#135974,#135975,
#135976,#135977,#135978,#135979,#135980,#135981,#135982,#135983,#135984,
#135985,#135986,#135987,#135988,#135989,#135990,#135991,#135992,#135993,
#135994,#135995,#135996,#135997,#135998,#135999,#136000,#136001),
 .UNSPECIFIED.,.F.,.F.,(4,3,3,3,3,3,3,3,3,3,3,3,3,3,3,3,3,3,3,3,3,3,3,3,
3,3,3,3,3,3,3,3,3,3,3,3,3,3,3,3,3,3,3,3,3,3,3,3,3,3,3,3,3,3,3,3,3,3,3,3,
3,3,3,3,3,3,3,3,3,3,3,3,3,4),(1630.4865872131,1630.56954378974,1630.65247615085,
1630.73539924177,1630.8183315628,1630.90129161728,1630.9843453147,1631.06745247754,
1631.15068316703,1631.1877588857,1631.27149759755,1631.35513310891,1631.43868555231,
1631.52217498816,1631.60562893877,1631.68906543262,1631.77250254237,1631.85595833729,
1631.93950283002,1632.02309191296,1632.10681518052,1632.18749489642,1632.27123360827,
1632.35486911963,1632.43842156303,1632.52191099888,1632.6053649495,1632.68880144334,
1632.7722385531,1632.85569434801,1632.93923884074,1633.02282792368,1633.10655119124,
1633.18723090714,1633.27096961899,1633.35460513035,1633.43815757375,1633.5216470096,
1633.60510096022,1633.68853745406,1633.77197456382,1633.85543035874,1633.93897485147,
1634.02256393441,1634.10628720197,1634.18696691786,1634.27070562971,1634.35434114107,
1634.43789358447,1634.52138302032,1634.60483697094,1634.68827346478,1634.77171057454,
1634.85516636946,1634.93871086218,1635.02229994513,1635.10602321268,1635.18670292858,
1635.27044164043,1635.35407715179,1635.43762959519,1635.52111903104,1635.60457298166,
1635.6880094755,1635.77144658526,1635.85490238018,1635.93844687291,1636.02203595585,
1636.10575922341,1636.1864389393,1636.27180414311,1636.35706341973,1636.44220161961,
1636.51922016046),.UNSPECIFIED.);
#1091=B_SPLINE_CURVE_WITH_KNOTS('',3,(#136007,#136008,#136009,#136010,#136011,
#136012,#136013,#136014,#136015,#136016,#136017,#136018,#136019,#136020,
#136021,#136022,#136023,#136024,#136025,#136026,#136027,#136028,#136029,
#136030,#136031,#136032,#136033,#136034,#136035,#136036,#136037,#136038,
#136039,#136040,#136041,#136042,#136043,#136044,#136045,#136046,#136047,
#136048,#136049,#136050,#136051,#136052,#136053,#136054,#136055,#136056,
#136057,#136058,#136059,#136060,#136061,#136062,#136063,#136064,#136065,
#136066,#136067,#136068,#136069,#136070,#136071,#136072,#136073,#136074,
#136075,#136076,#136077,#136078,#136079,#136080,#136081,#136082,#136083,
#136084,#136085,#136086,#136087,#136088,#136089,#136090,#136091,#136092,
#136093,#136094,#136095,#136096,#136097,#136098,#136099,#136100,#136101,
#136102,#136103,#136104,#136105,#136106,#136107,#136108,#136109,#136110,
#136111,#136112,#136113,#136114,#136115,#136116,#136117,#136118,#136119,
#136120,#136121,#136122,#136123,#136124,#136125,#136126,#136127,#136128,
#136129,#136130,#136131,#136132,#136133,#136134,#136135,#136136,#136137,
#136138,#136139,#136140,#136141,#136142,#136143,#136144,#136145,#136146,
#136147,#136148,#136149,#136150,#136151,#136152,#136153,#136154,#136155,
#136156,#136157,#136158,#136159,#136160,#136161,#136162,#136163,#136164,
#136165,#136166,#136167,#136168,#136169,#136170,#136171,#136172,#136173,
#136174,#136175,#136176,#136177,#136178,#136179,#136180,#136181,#136182,
#136183,#136184,#136185,#136186,#136187,#136188,#136189,#136190,#136191,
#136192,#136193,#136194,#136195,#136196,#136197,#136198,#136199,#136200,
#136201,#136202,#136203,#136204,#136205,#136206,#136207,#136208,#136209,
#136210,#136211,#136212,#136213,#136214,#136215,#136216,#136217,#136218,
#136219,#136220,#136221,#136222,#136223),.UNSPECIFIED.,.F.,.F.,(4,3,3,3,
3,3,3,3,3,3,3,3,3,3,3,3,3,3,3,3,3,3,3,3,3,3,3,3,3,3,3,3,3,3,3,3,3,3,3,3,
3,3,3,3,3,3,3,3,3,3,3,3,3,3,3,3,3,3,3,3,3,3,3,3,3,3,3,3,3,3,3,3,4),(1636.76977252028,
1636.8758843303,1636.95962304215,1637.04325855351,1637.12681099691,1637.21030043276,
1637.29375438338,1637.37719087722,1637.46062798698,1637.5440837819,1637.62762827463,
1637.71121735757,1637.79494062513,1637.87562034102,1637.95935905287,1638.04299456423,
1638.12654700763,1638.21003644348,1638.2934903941,1638.37692688794,1638.4603639977,
1638.54381979262,1638.62736428535,1638.71095336829,1638.79467663584,1638.87535635174,
1638.95909506359,1639.04273057495,1639.12628301835,1639.2097724542,1639.29322640482,
1639.37666289866,1639.46010000842,1639.54355580334,1639.62710029607,1639.71068937901,
1639.79441264657,1639.87509236246,1639.95883107431,1640.04246658567,1640.12601902907,
1640.20950846492,1640.29296241554,1640.37639890938,1640.45983601914,1640.54329181406,
1640.62683630679,1640.71042538973,1640.79414865728,1640.87482837318,1640.95856708503,
1641.04220259639,1641.12575503979,1641.20924447564,1641.29269842626,1641.3761349201,
1641.45957202986,1641.54302782478,1641.62657231751,1641.71016140045,1641.793884668,
1641.8745643839,1641.95830728885,1642.0419460335,1642.12550075442,1642.21000469894,
1642.29345497268,1642.37688665221,1642.46031780929,1642.54562143462,1642.62914195036,
1642.71533713049,1642.80153231061),.UNSPECIFIED.);
#1092=B_SPLINE_CURVE_WITH_KNOTS('',3,(#136224,#136225,#136226,#136227,#136228,
#136229,#136230,#136231,#136232,#136233),.UNSPECIFIED.,.F.,.F.,(4,3,3,4),
(1636.51794311402,1636.60040733544,1636.68508992779,1636.76977252014),
 .UNSPECIFIED.);
#1093=B_SPLINE_CURVE_WITH_KNOTS('',3,(#136235,#136236,#136237,#136238,#136239,
#136240,#136241,#136242,#136243,#136244),.UNSPECIFIED.,.F.,.F.,(4,3,3,4),
(1636.51922016046,1636.6042164217,1636.68916155776,1636.76977252028),
 .UNSPECIFIED.);
#1094=B_SPLINE_CURVE_WITH_KNOTS('',3,(#136245,#136246,#136247,#136248,#136249,
#136250,#136251,#136252,#136253,#136254,#136255,#136256,#136257,#136258,
#136259,#136260,#136261,#136262,#136263,#136264,#136265,#136266,#136267,
#136268,#136269,#136270,#136271,#136272,#136273,#136274,#136275,#136276,
#136277,#136278,#136279,#136280,#136281,#136282,#136283,#136284,#136285,
#136286,#136287,#136288,#136289,#136290,#136291,#136292,#136293,#136294,
#136295,#136296,#136297,#136298,#136299,#136300,#136301,#136302,#136303,
#136304,#136305,#136306,#136307,#136308,#136309,#136310,#136311,#136312,
#136313,#136314,#136315,#136316,#136317,#136318,#136319,#136320,#136321,
#136322,#136323,#136324,#136325,#136326,#136327,#136328,#136329,#136330,
#136331,#136332,#136333,#136334,#136335,#136336,#136337,#136338,#136339,
#136340,#136341,#136342,#136343,#136344,#136345,#136346,#136347,#136348,
#136349,#136350,#136351,#136352,#136353,#136354,#136355,#136356,#136357,
#136358,#136359,#136360,#136361,#136362,#136363,#136364,#136365,#136366,
#136367,#136368,#136369,#136370,#136371,#136372,#136373,#136374,#136375,
#136376,#136377,#136378,#136379,#136380,#136381,#136382,#136383,#136384,
#136385,#136386,#136387,#136388,#136389,#136390,#136391,#136392,#136393,
#136394,#136395,#136396,#136397,#136398,#136399,#136400,#136401,#136402,
#136403,#136404,#136405,#136406,#136407,#136408,#136409,#136410,#136411,
#136412,#136413,#136414,#136415,#136416,#136417,#136418,#136419,#136420,
#136421,#136422,#136423,#136424,#136425,#136426,#136427,#136428,#136429,
#136430,#136431,#136432,#136433,#136434,#136435,#136436,#136437,#136438,
#136439,#136440,#136441,#136442,#136443,#136444,#136445,#136446,#136447,
#136448,#136449,#136450,#136451,#136452,#136453,#136454,#136455,#136456,
#136457,#136458,#136459,#136460,#136461,#136462,#136463,#136464),
 .UNSPECIFIED.,.F.,.F.,(4,3,3,3,3,3,3,3,3,3,3,3,3,3,3,3,3,3,3,3,3,3,3,3,
3,3,3,3,3,3,3,3,3,3,3,3,3,3,3,3,3,3,3,3,3,3,3,3,3,3,3,3,3,3,3,3,3,3,3,3,
3,3,3,3,3,3,3,3,3,3,3,3,3,4),(1636.76977252044,1636.86091976418,1636.95249675115,
1637.04429371243,1637.13640641277,1637.18617495002,1637.26991366186,1637.35354917323,
1637.43710161663,1637.52059105248,1637.60404500309,1637.68748149694,1637.77091860669,
1637.85437440161,1637.93791889433,1638.02150797727,1638.10523124483,1638.18591096074,
1638.26964967259,1638.35328518395,1638.43683762735,1638.5203270632,1638.60378101382,
1638.68721750766,1638.77065461742,1638.85411041234,1638.93765490507,1639.02124398801,
1639.10496725556,1639.18564697146,1639.26938568331,1639.35302119467,1639.43657363807,
1639.52006307392,1639.60351702454,1639.68695351838,1639.77039062814,1639.85384642306,
1639.93739091579,1640.02097999873,1640.10470326629,1640.18538298218,1640.26912169403,
1640.35275720539,1640.43630964879,1640.51979908464,1640.60325303526,1640.6866895291,
1640.77012663886,1640.85358243378,1640.93712692651,1641.02071600945,1641.104439277,
1641.1851189929,1641.26885770475,1641.35249321611,1641.43604565951,1641.51953509536,
1641.60298904598,1641.68642553982,1641.76986264958,1641.8533184445,1641.93686293723,
1642.02045202017,1642.10417528773,1642.18485500362,1642.26738253516,1642.34981529156,
1642.43217245181,1642.51447312317,1642.59674341669,1642.67899572452,1642.76126760122,
1642.80116341428),.UNSPECIFIED.);
#1095=B_SPLINE_CURVE_WITH_KNOTS('',3,(#136470,#136471,#136472,#136473,#136474,
#136475,#136476,#136477,#136478,#136479,#136480,#136481,#136482,#136483,
#136484,#136485,#136486,#136487,#136488,#136489,#136490,#136491,#136492,
#136493,#136494,#136495,#136496,#136497,#136498,#136499,#136500,#136501,
#136502,#136503,#136504,#136505,#136506,#136507,#136508,#136509,#136510,
#136511,#136512,#136513,#136514,#136515,#136516,#136517,#136518,#136519,
#136520,#136521,#136522,#136523,#136524,#136525,#136526,#136527,#136528,
#136529,#136530,#136531,#136532,#136533,#136534,#136535,#136536,#136537,
#136538,#136539,#136540,#136541,#136542,#136543,#136544,#136545,#136546,
#136547,#136548,#136549,#136550,#136551,#136552,#136553,#136554,#136555,
#136556,#136557,#136558,#136559,#136560,#136561,#136562,#136563,#136564,
#136565,#136566,#136567,#136568,#136569,#136570,#136571,#136572,#136573,
#136574,#136575,#136576,#136577,#136578,#136579,#136580,#136581,#136582,
#136583,#136584,#136585,#136586,#136587,#136588,#136589,#136590,#136591,
#136592,#136593,#136594,#136595,#136596,#136597,#136598,#136599,#136600,
#136601,#136602,#136603,#136604,#136605,#136606,#136607,#136608,#136609,
#136610,#136611,#136612,#136613,#136614,#136615,#136616,#136617,#136618,
#136619,#136620,#136621,#136622,#136623,#136624,#136625,#136626,#136627,
#136628,#136629,#136630,#136631,#136632,#136633,#136634,#136635,#136636,
#136637,#136638,#136639,#136640,#136641,#136642,#136643,#136644,#136645,
#136646,#136647,#136648,#136649,#136650,#136651,#136652,#136653,#136654,
#136655,#136656,#136657,#136658,#136659,#136660,#136661,#136662,#136663,
#136664,#136665,#136666,#136667,#136668,#136669,#136670,#136671,#136672,
#136673,#136674,#136675,#136676,#136677,#136678,#136679,#136680,#136681,
#136682,#136683,#136684,#136685,#136686,#136687,#136688,#136689),
 .UNSPECIFIED.,.F.,.F.,(4,3,3,3,3,3,3,3,3,3,3,3,3,3,3,3,3,3,3,3,3,3,3,3,
3,3,3,3,3,3,3,3,3,3,3,3,3,3,3,3,3,3,3,3,3,3,3,3,3,3,3,3,3,3,3,3,3,3,3,3,
3,3,3,3,3,3,3,3,3,3,3,3,3,4),(1643.05295782762,1643.13532116623,1643.21760960656,
1643.29984767325,1643.38205948382,1643.4642640775,1643.54648048541,1643.62877814426,
1643.71111604496,1643.79358468629,1643.87403640534,1643.95777511719,1644.04141062855,
1644.12496307195,1644.2084525078,1644.29190645842,1644.37534295227,1644.45878006202,
1644.54223585694,1644.62578034967,1644.70936943261,1644.79309270017,1644.87377241606,
1644.95751112791,1645.04114663927,1645.12469908267,1645.20818851852,1645.29164246914,
1645.37507896298,1645.45851607274,1645.54197186766,1645.62551636039,1645.70910544333,
1645.79282871089,1645.87350842678,1645.95724713863,1646.04088264999,1646.12443509339,
1646.20792452924,1646.29137847986,1646.3748149737,1646.45825208346,1646.54170787837,
1646.6252523711,1646.70884145404,1646.7925647216,1646.8732444375,1646.95698314935,
1647.04061866071,1647.12417110411,1647.20766053996,1647.29111449058,1647.37455098442,
1647.45798809418,1647.5414438891,1647.62498838183,1647.70857746477,1647.79230073233,
1647.87298044822,1647.95671916007,1648.04035467143,1648.12390711483,1648.20739655068,
1648.29085050129,1648.37428699514,1648.45772410489,1648.54117989981,1648.62472439254,
1648.70831347548,1648.79203674304,1648.87271645894,1648.96236005017,1649.05178443656,
1649.08584175472),.UNSPECIFIED.);
#1096=B_SPLINE_CURVE_WITH_KNOTS('',3,(#136690,#136691,#136692,#136693,#136694,
#136695,#136696,#136697,#136698,#136699),.UNSPECIFIED.,.F.,.F.,(4,3,3,4),
(1642.80153231061,1642.87430039462,1643.00204117945,1643.05295782746),
 .UNSPECIFIED.);
#1097=B_SPLINE_CURVE_WITH_KNOTS('',3,(#136701,#136702,#136703,#136704,#136705,
#136706,#136707,#136708,#136709,#136710),.UNSPECIFIED.,.F.,.F.,(4,3,3,4),
(1642.80116341428,1642.88350269748,1642.96823026241,1643.05295782733),
 .UNSPECIFIED.);
#1098=B_SPLINE_CURVE_WITH_KNOTS('',3,(#136711,#136712,#136713,#136714,#136715,
#136716,#136717,#136718,#136719,#136720,#136721,#136722,#136723,#136724,
#136725,#136726,#136727,#136728,#136729,#136730,#136731,#136732,#136733,
#136734,#136735,#136736,#136737,#136738,#136739,#136740,#136741,#136742,
#136743,#136744,#136745,#136746,#136747,#136748,#136749,#136750,#136751,
#136752,#136753,#136754,#136755,#136756,#136757,#136758,#136759,#136760,
#136761,#136762,#136763,#136764,#136765,#136766,#136767,#136768,#136769,
#136770,#136771,#136772,#136773,#136774,#136775,#136776,#136777,#136778,
#136779,#136780,#136781,#136782,#136783,#136784,#136785,#136786,#136787,
#136788,#136789,#136790,#136791,#136792,#136793,#136794,#136795,#136796,
#136797,#136798,#136799,#136800,#136801,#136802,#136803,#136804,#136805,
#136806,#136807,#136808,#136809,#136810,#136811,#136812,#136813,#136814,
#136815,#136816,#136817,#136818,#136819,#136820,#136821,#136822,#136823,
#136824,#136825,#136826,#136827,#136828,#136829,#136830,#136831,#136832,
#136833,#136834,#136835,#136836,#136837,#136838,#136839,#136840,#136841,
#136842,#136843,#136844,#136845,#136846,#136847,#136848,#136849,#136850,
#136851,#136852,#136853,#136854,#136855,#136856,#136857,#136858,#136859,
#136860,#136861,#136862,#136863,#136864,#136865,#136866,#136867,#136868,
#136869,#136870,#136871,#136872,#136873,#136874,#136875,#136876,#136877,
#136878,#136879,#136880,#136881,#136882,#136883,#136884,#136885,#136886,
#136887,#136888,#136889,#136890,#136891,#136892,#136893,#136894,#136895,
#136896,#136897,#136898,#136899,#136900,#136901,#136902,#136903,#136904,
#136905,#136906,#136907,#136908,#136909,#136910,#136911,#136912,#136913,
#136914,#136915,#136916,#136917,#136918,#136919,#136920,#136921,#136922,
#136923,#136924,#136925,#136926,#136927),.UNSPECIFIED.,.F.,.F.,(4,3,3,3,
3,3,3,3,3,3,3,3,3,3,3,3,3,3,3,3,3,3,3,3,3,3,3,3,3,3,3,3,3,3,3,3,3,3,3,3,
3,3,3,3,3,3,3,3,3,3,3,3,3,3,3,3,3,3,3,3,3,3,3,3,3,3,3,3,3,3,3,3,4),(1643.05295782746,
1643.18459101434,1643.26832972619,1643.35196523755,1643.43551768095,1643.5190071168,
1643.60246106742,1643.68589756126,1643.76933467102,1643.85279046593,1643.93633495866,
1644.01992404161,1644.10364730916,1644.18432702506,1644.26806573691,1644.35170124827,
1644.43525369167,1644.51874312752,1644.60219707814,1644.68563357198,1644.76907068174,
1644.85252647666,1644.93607096939,1645.01966005233,1645.10338331988,1645.18406303578,
1645.26780174763,1645.35143725899,1645.43498970239,1645.51847913824,1645.60193308886,
1645.6853695827,1645.76880669246,1645.85226248738,1645.93580698011,1646.01939606305,
1646.1031193306,1646.1837990465,1646.26753775835,1646.35117326971,1646.43472571311,
1646.51821514896,1646.60166909958,1646.68510559342,1646.76854270318,1646.8519984981,
1646.93554299083,1647.01913207377,1647.10285534132,1647.18353505722,1647.26727376907,
1647.35090928043,1647.43446172383,1647.51795115968,1647.6014051103,1647.68484160414,
1647.7682787139,1647.85173450882,1647.93527900155,1648.01886808449,1648.10259135205,
1648.18327106794,1648.26701550462,1648.35065544319,1648.4342110217,1648.51769806414,
1648.60114772603,1648.68457809583,1648.76800724526,1648.85149094862,1648.93500226131,
1649.01861174798,1649.08463270961),.UNSPECIFIED.);
#1099=B_SPLINE_CURVE_WITH_KNOTS('',3,(#136933,#136934,#136935,#136936,#136937,
#136938,#136939,#136940,#136941,#136942,#136943,#136944,#136945,#136946,
#136947,#136948,#136949,#136950,#136951,#136952,#136953,#136954,#136955,
#136956,#136957,#136958,#136959,#136960,#136961,#136962,#136963,#136964,
#136965,#136966,#136967,#136968,#136969,#136970,#136971,#136972,#136973,
#136974,#136975,#136976,#136977,#136978,#136979,#136980,#136981,#136982,
#136983,#136984,#136985,#136986,#136987,#136988,#136989,#136990,#136991,
#136992,#136993,#136994,#136995,#136996,#136997,#136998,#136999,#137000,
#137001,#137002,#137003,#137004,#137005,#137006,#137007,#137008,#137009,
#137010,#137011,#137012,#137013,#137014,#137015,#137016,#137017,#137018,
#137019,#137020,#137021,#137022,#137023,#137024,#137025,#137026,#137027,
#137028,#137029,#137030,#137031,#137032,#137033,#137034,#137035,#137036,
#137037,#137038,#137039,#137040,#137041,#137042,#137043,#137044,#137045,
#137046,#137047,#137048,#137049,#137050,#137051,#137052,#137053,#137054,
#137055,#137056,#137057,#137058,#137059,#137060,#137061,#137062,#137063,
#137064,#137065,#137066,#137067,#137068,#137069,#137070,#137071,#137072,
#137073,#137074,#137075,#137076,#137077,#137078,#137079,#137080,#137081,
#137082,#137083,#137084,#137085,#137086,#137087,#137088,#137089,#137090,
#137091,#137092,#137093,#137094,#137095,#137096,#137097,#137098,#137099,
#137100,#137101,#137102,#137103,#137104,#137105,#137106,#137107,#137108,
#137109,#137110,#137111,#137112,#137113,#137114,#137115,#137116,#137117,
#137118,#137119,#137120,#137121,#137122,#137123,#137124,#137125,#137126,
#137127,#137128,#137129,#137130,#137131,#137132,#137133,#137134,#137135,
#137136,#137137,#137138,#137139,#137140,#137141,#137142,#137143,#137144,
#137145,#137146,#137147,#137148,#137149,#137150,#137151,#137152),
 .UNSPECIFIED.,.F.,.F.,(4,3,3,3,3,3,3,3,3,3,3,3,3,3,3,3,3,3,3,3,3,3,3,3,
3,3,3,3,3,3,3,3,3,3,3,3,3,3,3,3,3,3,3,3,3,3,3,3,3,3,3,3,3,3,3,3,3,3,3,3,
3,3,3,3,3,3,3,3,3,3,3,3,3,4),(1649.33614313464,1649.42233918616,1649.50860824319,
1649.59496282204,1649.68147725306,1649.7680842705,1649.85484863182,1649.87245246966,
1649.95619118151,1650.03982669287,1650.12337913627,1650.20686857212,1650.29032252274,
1650.37375901658,1650.45719612634,1650.54065192126,1650.62419641398,1650.70778549693,
1650.79150876448,1650.87218848038,1650.95592719223,1651.03956270359,1651.12311514699,
1651.20660458284,1651.29005853346,1651.3734950273,1651.45693213706,1651.54038793198,
1651.62393242471,1651.70752150765,1651.79124477521,1651.8719244911,1651.95566320295,
1652.03929871431,1652.12285115771,1652.20634059356,1652.28979454418,1652.37323103802,
1652.45666814778,1652.5401239427,1652.62366843543,1652.70725751837,1652.79098078592,
1652.87166050182,1652.95539921367,1653.03903472503,1653.12258716843,1653.20607660428,
1653.2895305549,1653.37296704874,1653.4564041585,1653.53985995341,1653.62340444614,
1653.70699352908,1653.79071679664,1653.87139651254,1653.95513522439,1654.03877073575,
1654.12232317915,1654.205812615,1654.28926656562,1654.37270305946,1654.45614016922,
1654.53959596414,1654.62314045687,1654.70672953981,1654.79045280737,1654.87113252326,
1654.95391129918,1655.03659172981,1655.11943701868,1655.20197128938,1655.28497208733,
1655.36797288529),.UNSPECIFIED.);
#1100=B_SPLINE_CURVE_WITH_KNOTS('',3,(#137153,#137154,#137155,#137156,#137157,
#137158,#137159,#137160,#137161,#137162),.UNSPECIFIED.,.F.,.F.,(4,3,3,4),
(1649.08584175472,1649.17498599602,1649.26389439352,1649.33614313448),
 .UNSPECIFIED.);
#1101=B_SPLINE_CURVE_WITH_KNOTS('',3,(#137164,#137165,#137166,#137167,#137168,
#137169,#137170,#137171,#137172,#137173,#137174,#137175,#137176),
 .UNSPECIFIED.,.F.,.F.,(4,3,3,3,4),(1649.08463270961,1649.16838434476,1649.18300707866,
1649.32336075287,1649.33614313464),.UNSPECIFIED.);
#1102=B_SPLINE_CURVE_WITH_KNOTS('',3,(#137177,#137178,#137179,#137180,#137181,
#137182,#137183,#137184,#137185,#137186,#137187,#137188,#137189,#137190,
#137191,#137192,#137193,#137194,#137195,#137196,#137197,#137198,#137199,
#137200,#137201,#137202,#137203,#137204,#137205,#137206,#137207,#137208,
#137209,#137210,#137211,#137212,#137213,#137214,#137215,#137216,#137217,
#137218,#137219,#137220,#137221,#137222,#137223,#137224,#137225,#137226,
#137227,#137228,#137229,#137230,#137231,#137232,#137233,#137234,#137235,
#137236,#137237,#137238,#137239,#137240,#137241,#137242,#137243,#137244,
#137245,#137246,#137247,#137248,#137249,#137250,#137251,#137252,#137253,
#137254,#137255,#137256,#137257,#137258,#137259,#137260,#137261,#137262,
#137263,#137264,#137265,#137266,#137267,#137268,#137269,#137270,#137271,
#137272,#137273,#137274,#137275,#137276,#137277,#137278,#137279,#137280,
#137281,#137282,#137283,#137284,#137285,#137286,#137287,#137288,#137289,
#137290,#137291,#137292,#137293,#137294,#137295,#137296,#137297,#137298,
#137299,#137300,#137301,#137302,#137303,#137304,#137305,#137306,#137307,
#137308,#137309,#137310,#137311,#137312,#137313,#137314,#137315,#137316,
#137317,#137318,#137319,#137320,#137321,#137322,#137323,#137324,#137325,
#137326,#137327,#137328,#137329,#137330,#137331,#137332,#137333,#137334,
#137335,#137336,#137337,#137338,#137339,#137340,#137341,#137342,#137343,
#137344,#137345,#137346,#137347,#137348,#137349,#137350,#137351,#137352,
#137353,#137354,#137355,#137356,#137357,#137358,#137359,#137360,#137361,
#137362,#137363,#137364,#137365,#137366,#137367,#137368,#137369,#137370,
#137371,#137372,#137373,#137374,#137375,#137376,#137377,#137378,#137379,
#137380,#137381,#137382,#137383,#137384,#137385,#137386,#137387,#137388,
#137389,#137390,#137391,#137392,#137393,#137394,#137395,#137396),
 .UNSPECIFIED.,.F.,.F.,(4,3,3,3,3,3,3,3,3,3,3,3,3,3,3,3,3,3,3,3,3,3,3,3,
3,3,3,3,3,3,3,3,3,3,3,3,3,3,3,3,3,3,3,3,3,3,3,3,3,3,3,3,3,3,3,3,3,3,3,3,
3,3,3,3,3,3,3,3,3,3,3,3,3,4),(1649.33614313475,1649.4185401776,1649.5008558462,
1649.5860917516,1649.66831531826,1649.75052652388,1649.83274439629,1649.91498796673,
1649.99731983084,1650.07970441643,1650.16220352253,1650.18274308938,1650.26648180123,
1650.35011731259,1650.43366975599,1650.51715919184,1650.60061314246,1650.6840496363,
1650.76748674606,1650.85094254098,1650.93448703371,1651.01807611665,1651.1017993842,
1651.1824791001,1651.26621781195,1651.34985332331,1651.43340576671,1651.51689520256,
1651.60034915318,1651.68378564702,1651.76722275678,1651.8506785517,1651.93422304442,
1652.01781212737,1652.10153539492,1652.18221511082,1652.26595382267,1652.34958933403,
1652.43314177743,1652.51663121328,1652.6000851639,1652.68352165774,1652.7669587675,
1652.85041456242,1652.93395905515,1653.01754813809,1653.10127140564,1653.18195112154,
1653.26568983339,1653.34932534475,1653.43287778815,1653.516367224,1653.59982117462,
1653.68325766846,1653.76669477822,1653.85015057314,1653.93369506587,1654.01728414881,
1654.10100741636,1654.18168713226,1654.26542584411,1654.34906135547,1654.43261379887,
1654.51610323472,1654.59955718534,1654.68299367918,1654.76643078894,1654.84988658386,
1654.93343107659,1655.01702015953,1655.10074342709,1655.18142314298,1655.27521982429,
1655.3690165056),.UNSPECIFIED.);
#1103=B_SPLINE_CURVE_WITH_KNOTS('',3,(#137402,#137403,#137404,#137405,#137406,
#137407,#137408,#137409,#137410,#137411,#137412,#137413,#137414,#137415,
#137416,#137417,#137418,#137419,#137420,#137421,#137422,#137423,#137424,
#137425,#137426,#137427,#137428,#137429,#137430,#137431,#137432,#137433,
#137434,#137435,#137436,#137437,#137438,#137439,#137440,#137441,#137442,
#137443,#137444,#137445,#137446,#137447,#137448,#137449,#137450,#137451,
#137452,#137453,#137454,#137455,#137456,#137457,#137458,#137459,#137460,
#137461,#137462,#137463,#137464,#137465,#137466,#137467,#137468,#137469,
#137470,#137471,#137472,#137473,#137474,#137475,#137476,#137477,#137478,
#137479,#137480,#137481,#137482,#137483,#137484,#137485,#137486,#137487,
#137488,#137489,#137490,#137491,#137492,#137493,#137494,#137495,#137496,
#137497,#137498,#137499,#137500,#137501,#137502,#137503,#137504,#137505,
#137506,#137507,#137508,#137509,#137510,#137511,#137512,#137513,#137514,
#137515,#137516,#137517,#137518,#137519,#137520,#137521,#137522,#137523,
#137524,#137525,#137526,#137527,#137528,#137529,#137530,#137531,#137532,
#137533,#137534,#137535,#137536,#137537,#137538,#137539,#137540,#137541,
#137542,#137543,#137544,#137545,#137546,#137547,#137548,#137549,#137550,
#137551,#137552,#137553,#137554,#137555,#137556,#137557,#137558,#137559,
#137560,#137561,#137562,#137563,#137564,#137565,#137566,#137567,#137568,
#137569,#137570,#137571,#137572,#137573,#137574,#137575,#137576,#137577,
#137578,#137579,#137580,#137581,#137582,#137583,#137584,#137585,#137586,
#137587,#137588,#137589,#137590,#137591,#137592,#137593,#137594,#137595,
#137596,#137597,#137598,#137599,#137600,#137601,#137602,#137603,#137604,
#137605,#137606,#137607,#137608,#137609,#137610,#137611,#137612,#137613,
#137614,#137615,#137616,#137617,#137618,#137619,#137620,#137621),
 .UNSPECIFIED.,.F.,.F.,(4,3,3,3,3,3,3,3,3,3,3,3,3,3,3,3,3,3,3,3,3,3,3,3,
3,3,3,3,3,3,3,3,3,3,3,3,3,3,3,3,3,3,3,3,3,3,3,3,3,3,3,3,3,3,3,3,3,3,3,3,
3,3,3,3,3,3,3,3,3,3,3,3,3,4),(1655.61932844201,1655.72632222295,1655.83568474814,
1655.87086853399,1655.95460724584,1656.0382427572,1656.1217952006,1656.20528463645,
1656.28873858707,1656.37217508092,1656.45561219067,1656.53906798559,1656.62261247832,
1656.70620156126,1656.78992482882,1656.8706045447,1656.95434325655,1657.03797876791,
1657.12153121131,1657.20502064716,1657.28847459778,1657.37191109162,1657.45534820138,
1657.5388039963,1657.62234848903,1657.70593757197,1657.78966083952,1657.87034055543,
1657.95407926728,1658.03771477864,1658.12126722204,1658.2047566579,1658.28821060851,
1658.37164710236,1658.45508421211,1658.53854000703,1658.62208449976,1658.7056735827,
1658.78939685026,1658.87007656615,1658.953815278,1659.03745078936,1659.12100323276,
1659.20449266861,1659.28794661923,1659.37138311307,1659.45482022283,1659.53827601774,
1659.62182051047,1659.70540959341,1659.78913286097,1659.86981257687,1659.95355128872,
1660.03718680008,1660.12073924348,1660.20422867933,1660.28768262995,1660.37111912379,
1660.45455623355,1660.53801202847,1660.6215565212,1660.70514560414,1660.78886887169,
1660.86954858759,1660.95330059649,1661.04049401252,1661.12403534255,1661.20751969612,
1661.29096519257,1661.37438992107,1661.45783300827,1661.54128727818,1661.62479697284,
1661.65084792474),.UNSPECIFIED.);
#1104=B_SPLINE_CURVE_WITH_KNOTS('',3,(#137622,#137623,#137624,#137625,#137626,
#137627,#137628,#137629,#137630,#137631),.UNSPECIFIED.,.F.,.F.,(4,3,3,4),
(1655.36797288529,1655.45047524496,1655.53490184339,1655.61932844182),
 .UNSPECIFIED.);
#1105=B_SPLINE_CURVE_WITH_KNOTS('',3,(#137633,#137634,#137635,#137636,#137637,
#137638,#137639,#137640,#137641,#137642),.UNSPECIFIED.,.F.,.F.,(4,3,3,4),
(1655.3690165056,1655.45942920808,1655.5495389858,1655.61932844169),
 .UNSPECIFIED.);
#1106=B_SPLINE_CURVE_WITH_KNOTS('',3,(#137643,#137644,#137645,#137646,#137647,
#137648,#137649,#137650,#137651,#137652,#137653,#137654,#137655,#137656,
#137657,#137658,#137659,#137660,#137661,#137662,#137663,#137664,#137665,
#137666,#137667,#137668,#137669,#137670,#137671,#137672,#137673,#137674,
#137675,#137676,#137677,#137678,#137679,#137680,#137681,#137682,#137683,
#137684,#137685,#137686,#137687,#137688,#137689,#137690,#137691,#137692,
#137693,#137694,#137695,#137696,#137697,#137698,#137699,#137700,#137701,
#137702,#137703,#137704,#137705,#137706,#137707,#137708,#137709,#137710,
#137711,#137712,#137713,#137714,#137715,#137716,#137717,#137718,#137719,
#137720,#137721,#137722,#137723,#137724,#137725,#137726,#137727,#137728,
#137729,#137730,#137731,#137732,#137733,#137734,#137735,#137736,#137737,
#137738,#137739,#137740,#137741,#137742,#137743,#137744,#137745,#137746,
#137747,#137748,#137749,#137750,#137751,#137752,#137753,#137754,#137755,
#137756,#137757,#137758,#137759,#137760,#137761,#137762,#137763,#137764,
#137765,#137766,#137767,#137768,#137769,#137770,#137771,#137772,#137773,
#137774,#137775,#137776,#137777,#137778,#137779,#137780,#137781,#137782,
#137783,#137784,#137785,#137786,#137787,#137788,#137789,#137790,#137791,
#137792,#137793,#137794,#137795,#137796,#137797,#137798,#137799,#137800,
#137801,#137802,#137803,#137804,#137805,#137806,#137807,#137808,#137809,
#137810,#137811,#137812,#137813,#137814,#137815,#137816,#137817,#137818,
#137819,#137820,#137821,#137822,#137823,#137824,#137825,#137826,#137827,
#137828,#137829,#137830,#137831,#137832,#137833,#137834,#137835,#137836,
#137837,#137838,#137839,#137840,#137841,#137842,#137843,#137844,#137845,
#137846,#137847,#137848,#137849,#137850,#137851,#137852,#137853,#137854,
#137855,#137856,#137857,#137858,#137859,#137860,#137861,#137862),
 .UNSPECIFIED.,.F.,.F.,(4,3,3,3,3,3,3,3,3,3,3,3,3,3,3,3,3,3,3,3,3,3,3,3,
3,3,3,3,3,3,3,3,3,3,3,3,3,3,3,3,3,3,3,3,3,3,3,3,3,3,3,3,3,3,3,3,3,3,3,3,
3,3,3,3,3,3,3,3,3,3,3,3,3,4),(1655.61932844182,1655.70480180458,1655.79032505431,
1655.87591265975,1655.96164121957,1656.04744749123,1656.13341100218,1656.1811591537,
1656.26489786555,1656.34853337691,1656.43208582031,1656.51557525616,1656.59902920678,
1656.68246570062,1656.76590281038,1656.8493586053,1656.93290309803,1657.01649218097,
1657.10021544852,1657.18089516442,1657.26463387627,1657.34826938763,1657.43182183103,
1657.51531126688,1657.5987652175,1657.68220171134,1657.7656388211,1657.84909461602,
1657.93263910875,1658.01622819169,1658.09995145924,1658.18063117514,1658.26436988699,
1658.34800539835,1658.43155784175,1658.5150472776,1658.59850122822,1658.68193772206,
1658.76537483182,1658.84883062674,1658.93237511947,1659.01596420241,1659.09968746996,
1659.18036718586,1659.26410589771,1659.34774140907,1659.43129385247,1659.51478328832,
1659.59823723894,1659.68167373278,1659.76511084254,1659.84856663746,1659.93211113019,
1660.01570021313,1660.09942348068,1660.18010319658,1660.26384190843,1660.34747741979,
1660.43102986319,1660.51451929904,1660.59797324966,1660.6814097435,1660.76484685326,
1660.84830264818,1660.9318471409,1661.01543622385,1661.0991594914,1661.1798392073,
1661.26283883278,1661.34573846742,1661.42854232631,1661.51129049212,1661.59400396625,
1661.65128699969),.UNSPECIFIED.);
#1107=B_SPLINE_CURVE_WITH_KNOTS('',3,(#137868,#137869,#137870,#137871,#137872,
#137873,#137874,#137875,#137876,#137877,#137878,#137879,#137880,#137881,
#137882,#137883,#137884,#137885,#137886,#137887,#137888,#137889,#137890,
#137891,#137892,#137893,#137894,#137895,#137896,#137897,#137898,#137899,
#137900,#137901,#137902,#137903,#137904,#137905,#137906,#137907,#137908,
#137909,#137910,#137911,#137912,#137913,#137914,#137915,#137916,#137917,
#137918,#137919,#137920,#137921,#137922,#137923,#137924,#137925,#137926,
#137927,#137928,#137929,#137930,#137931,#137932,#137933,#137934,#137935,
#137936,#137937,#137938,#137939,#137940,#137941,#137942,#137943,#137944,
#137945,#137946,#137947,#137948,#137949,#137950,#137951,#137952,#137953,
#137954,#137955,#137956,#137957,#137958,#137959,#137960,#137961,#137962,
#137963,#137964,#137965,#137966,#137967,#137968,#137969,#137970,#137971,
#137972,#137973,#137974,#137975,#137976,#137977,#137978,#137979,#137980,
#137981,#137982,#137983,#137984,#137985,#137986,#137987,#137988,#137989,
#137990,#137991,#137992,#137993,#137994,#137995,#137996,#137997,#137998,
#137999,#138000,#138001,#138002,#138003,#138004,#138005,#138006,#138007,
#138008,#138009,#138010,#138011,#138012,#138013,#138014,#138015,#138016,
#138017,#138018,#138019,#138020,#138021,#138022,#138023,#138024,#138025,
#138026,#138027,#138028,#138029,#138030,#138031,#138032,#138033,#138034,
#138035,#138036,#138037,#138038,#138039,#138040,#138041,#138042,#138043,
#138044,#138045,#138046,#138047,#138048,#138049,#138050,#138051,#138052,
#138053,#138054,#138055,#138056,#138057,#138058,#138059,#138060,#138061,
#138062,#138063,#138064,#138065,#138066,#138067,#138068,#138069,#138070,
#138071,#138072,#138073,#138074,#138075,#138076,#138077,#138078,#138079,
#138080,#138081,#138082,#138083,#138084,#138085,#138086,#138087),
 .UNSPECIFIED.,.F.,.F.,(4,3,3,3,3,3,3,3,3,3,3,3,3,3,3,3,3,3,3,3,3,3,3,3,
3,3,3,3,3,3,3,3,3,3,3,3,3,3,3,3,3,3,3,3,3,3,3,3,3,3,3,3,3,3,3,3,3,3,3,3,
3,3,3,3,3,3,3,3,3,3,3,3,3,4),(1661.90251374915,1661.98579347555,1662.06897154049,
1662.15206852732,1662.23510494363,1662.31810946112,1662.40109955002,1662.48409368614,
1662.56711034459,1662.65021628424,1662.73337103092,1662.8166510224,1662.86902060903,
1662.95275932088,1663.03639483224,1663.11994727564,1663.20343671149,1663.2868906621,
1663.37032715595,1663.4537642657,1663.53722006062,1663.62076455335,1663.70435363629,
1663.78807690385,1663.86875661975,1663.9524953316,1664.03613084297,1664.11968328637,
1664.20317272222,1664.28662667284,1664.37006316668,1664.45350027644,1664.53695607136,
1664.62050056409,1664.70408964703,1664.78781291459,1664.86849263047,1664.95223134231,
1665.03586685368,1665.11941929708,1665.20290873293,1665.28636268354,1665.36979917739,
1665.45323628714,1665.53669208206,1665.62023657478,1665.70382565772,1665.78754892528,
1665.86822864119,1665.95196735303,1666.0356028644,1666.11915530779,1666.20264474364,
1666.28609869425,1666.36953518809,1666.45297229784,1666.53642809275,1666.61997258548,
1666.70356166842,1666.78728493597,1666.86796465191,1666.95170336377,1667.03533887515,
1667.11889131856,1667.20238075443,1667.28583470505,1667.36927119891,1667.45270830868,
1667.53616410361,1667.61970859635,1667.70329767931,1667.78702094688,1667.86770066263,
1667.93501912961),.UNSPECIFIED.);
#1108=B_SPLINE_CURVE_WITH_KNOTS('',3,(#138088,#138089,#138090,#138091,#138092,
#138093,#138094,#138095,#138096,#138097,#138098,#138099,#138100),
 .UNSPECIFIED.,.F.,.F.,(4,3,3,3,4),(1661.65084792474,1661.73445666934,1661.81819110253,
1661.86928459831,1661.902513749),.UNSPECIFIED.);
#1109=B_SPLINE_CURVE_WITH_KNOTS('',3,(#138102,#138103,#138104,#138105,#138106,
#138107,#138108,#138109,#138110,#138111),.UNSPECIFIED.,.F.,.F.,(4,3,3,4),
(1661.65128699969,1661.73399004573,1661.81825189737,1661.902513749),
 .UNSPECIFIED.);
#1110=B_SPLINE_CURVE_WITH_KNOTS('',3,(#138112,#138113,#138114,#138115,#138116,
#138117,#138118,#138119,#138120,#138121,#138122,#138123,#138124,#138125,
#138126,#138127,#138128,#138129,#138130,#138131,#138132,#138133,#138134,
#138135,#138136,#138137,#138138,#138139,#138140,#138141,#138142,#138143,
#138144,#138145,#138146,#138147,#138148,#138149,#138150,#138151,#138152,
#138153,#138154,#138155,#138156,#138157,#138158,#138159,#138160,#138161,
#138162,#138163,#138164,#138165,#138166,#138167,#138168,#138169,#138170,
#138171,#138172,#138173,#138174,#138175,#138176,#138177,#138178,#138179,
#138180,#138181,#138182,#138183,#138184,#138185,#138186,#138187,#138188,
#138189,#138190,#138191,#138192,#138193,#138194,#138195,#138196,#138197,
#138198,#138199,#138200,#138201,#138202,#138203,#138204,#138205,#138206,
#138207,#138208,#138209,#138210,#138211,#138212,#138213,#138214,#138215,
#138216,#138217,#138218,#138219,#138220,#138221,#138222,#138223,#138224,
#138225,#138226,#138227,#138228,#138229,#138230,#138231,#138232,#138233,
#138234,#138235,#138236,#138237,#138238,#138239,#138240,#138241,#138242,
#138243,#138244,#138245,#138246,#138247,#138248,#138249,#138250,#138251,
#138252,#138253,#138254,#138255,#138256,#138257,#138258,#138259,#138260,
#138261,#138262,#138263,#138264,#138265,#138266,#138267,#138268,#138269,
#138270,#138271,#138272,#138273,#138274,#138275,#138276,#138277,#138278,
#138279,#138280,#138281,#138282,#138283,#138284,#138285,#138286,#138287,
#138288,#138289,#138290,#138291,#138292,#138293,#138294,#138295,#138296,
#138297,#138298,#138299,#138300,#138301,#138302,#138303,#138304,#138305,
#138306,#138307,#138308,#138309,#138310,#138311,#138312,#138313,#138314,
#138315,#138316,#138317,#138318,#138319,#138320,#138321,#138322,#138323,
#138324,#138325,#138326,#138327,#138328),.UNSPECIFIED.,.F.,.F.,(4,3,3,3,
3,3,3,3,3,3,3,3,3,3,3,3,3,3,3,3,3,3,3,3,3,3,3,3,3,3,3,3,3,3,3,3,3,3,3,3,
3,3,3,3,3,3,3,3,3,3,3,3,3,3,3,3,3,3,3,3,3,3,3,3,3,3,3,3,3,3,3,3,4),(1661.9025137491,
1662.00582469911,1662.11084798141,1662.17957521802,1662.26331392987,1662.34694944123,
1662.43050188463,1662.51399132048,1662.5974452711,1662.68088176494,1662.7643188747,
1662.84777466962,1662.93131916235,1663.01490824529,1663.09863151284,1663.17931122874,
1663.26304994059,1663.34668545195,1663.43023789535,1663.5137273312,1663.59718128182,
1663.68061777566,1663.76405488542,1663.84751068034,1663.93105517306,1664.01464425601,
1664.09836752356,1664.17904723946,1664.26278595131,1664.34642146267,1664.42997390607,
1664.51346334192,1664.59691729254,1664.68035378638,1664.76379089614,1664.84724669106,
1664.93079118379,1665.01438026673,1665.09810353429,1665.17878325018,1665.26252196203,
1665.34615747339,1665.42970991679,1665.51319935264,1665.59665330326,1665.6800897971,
1665.76352690686,1665.84698270178,1665.93052719451,1666.01411627745,1666.097839545,
1666.1785192609,1666.26225797275,1666.34589348411,1666.42944592751,1666.51293536336,
1666.59638931397,1666.67982580782,1666.76326291757,1666.84671871249,1666.93026320522,
1667.01385228816,1667.09757555572,1667.17825527162,1667.26200897232,1667.34601332621,
1667.42955786069,1667.51304424891,1667.59649061251,1667.68087891024,1667.76431701185,
1667.84918040764,1667.93404380343),.UNSPECIFIED.);
#1111=B_SPLINE_CURVE_WITH_KNOTS('',3,(#138334,#138335,#138336,#138337,#138338,
#138339,#138340,#138341,#138342,#138343,#138344,#138345,#138346,#138347,
#138348,#138349,#138350,#138351,#138352,#138353,#138354,#138355,#138356,
#138357,#138358,#138359,#138360,#138361,#138362,#138363,#138364,#138365,
#138366,#138367,#138368,#138369,#138370,#138371,#138372,#138373,#138374,
#138375,#138376,#138377,#138378,#138379,#138380,#138381,#138382,#138383,
#138384,#138385,#138386,#138387,#138388,#138389,#138390,#138391,#138392,
#138393,#138394,#138395,#138396,#138397,#138398,#138399,#138400,#138401,
#138402,#138403,#138404,#138405,#138406,#138407,#138408,#138409,#138410,
#138411,#138412,#138413,#138414,#138415,#138416,#138417,#138418,#138419,
#138420,#138421,#138422,#138423,#138424,#138425,#138426,#138427,#138428,
#138429,#138430,#138431,#138432,#138433,#138434,#138435,#138436,#138437,
#138438,#138439,#138440,#138441,#138442,#138443,#138444,#138445,#138446,
#138447,#138448,#138449,#138450,#138451,#138452,#138453,#138454,#138455,
#138456,#138457,#138458,#138459,#138460,#138461,#138462,#138463,#138464,
#138465,#138466,#138467,#138468,#138469,#138470,#138471,#138472,#138473,
#138474,#138475,#138476,#138477,#138478,#138479,#138480,#138481,#138482,
#138483,#138484,#138485,#138486,#138487,#138488,#138489,#138490,#138491,
#138492,#138493,#138494,#138495,#138496,#138497,#138498,#138499,#138500,
#138501,#138502,#138503,#138504,#138505,#138506,#138507,#138508,#138509,
#138510,#138511,#138512,#138513,#138514,#138515,#138516,#138517,#138518,
#138519,#138520,#138521,#138522,#138523,#138524,#138525,#138526,#138527,
#138528,#138529,#138530,#138531,#138532,#138533,#138534,#138535,#138536,
#138537,#138538,#138539,#138540,#138541,#138542,#138543,#138544,#138545,
#138546,#138547,#138548,#138549,#138550,#138551,#138552,#138553,#138554,
#138555,#138556),.UNSPECIFIED.,.F.,.F.,(4,3,3,3,3,3,3,3,3,3,3,3,3,3,3,3,
3,3,3,3,3,3,3,3,3,3,3,3,3,3,3,3,3,3,3,3,3,3,3,3,3,3,3,3,3,3,3,3,3,3,3,3,
3,3,3,3,3,3,3,3,3,3,3,3,3,3,3,3,3,3,3,3,3,3,4),(1668.18569905618,1668.27091625833,
1668.35407991018,1668.43724227634,1668.52042163574,1668.60717539514,1668.69049092051,
1668.77386693529,1668.85736103574,1668.86743667335,1668.95117538517,1669.03481089652,
1669.11836333989,1669.20185277572,1669.28530672631,1669.36874322014,1669.45218032987,
1669.53563612476,1669.61918061747,1669.70276970039,1669.78649296792,1669.86717268407,
1669.950911396,1670.03454690746,1670.11809935095,1670.20158878688,1670.28504273759,
1670.36847923152,1670.45191634136,1670.53537213637,1670.61891662918,1670.70250571221,
1670.78622897985,1670.86690869479,1670.95064740654,1671.03428291781,1671.11783536111,
1671.20132479686,1671.28477874738,1671.36821524113,1671.45165235079,1671.53510814561,
1671.61865263825,1671.7022417211,1671.78596498857,1671.86664470551,1671.95038341724,
1672.0340189285,1672.11757137178,1672.20106080752,1672.28451475802,1672.36795125175,
1672.45138836139,1672.53484415619,1672.6183886488,1672.70197773162,1672.78570099906,
1672.86638071623,1672.95011942866,1673.0337549406,1673.11730738458,1673.20079682102,
1673.28425077221,1673.36768726663,1673.45112437697,1673.53458017246,1673.61812466576,
1673.70171374926,1673.78543701737,1673.86611672695,1673.95415082145,1674.03893719653,
1674.12363710965,1674.20825020537,1674.21825310493),.UNSPECIFIED.);
#1112=B_SPLINE_CURVE_WITH_KNOTS('',3,(#138557,#138558,#138559,#138560,#138561,
#138562,#138563,#138564,#138565,#138566),.UNSPECIFIED.,.F.,.F.,(4,3,3,4),
(1667.93501912961,1668.03466883892,1668.13330378235,1668.18569905601),
 .UNSPECIFIED.);
#1113=B_SPLINE_CURVE_WITH_KNOTS('',3,(#138568,#138569,#138570,#138571,#138572,
#138573,#138574,#138575,#138576,#138577,#138578,#138579,#138580),
 .UNSPECIFIED.,.F.,.F.,(4,3,3,3,4),(1667.93404380343,1668.01763545707,1668.10136010487,
1668.17799128234,1668.18569905618),.UNSPECIFIED.);
#1114=B_SPLINE_CURVE_WITH_KNOTS('',3,(#138581,#138582,#138583,#138584,#138585,
#138586,#138587,#138588,#138589,#138590,#138591,#138592,#138593,#138594,
#138595,#138596,#138597,#138598,#138599,#138600,#138601,#138602,#138603,
#138604,#138605,#138606,#138607,#138608,#138609,#138610,#138611,#138612,
#138613,#138614,#138615,#138616,#138617,#138618,#138619,#138620,#138621,
#138622,#138623,#138624,#138625,#138626,#138627,#138628,#138629,#138630,
#138631,#138632,#138633,#138634,#138635,#138636,#138637,#138638,#138639,
#138640,#138641,#138642,#138643,#138644,#138645,#138646,#138647,#138648,
#138649,#138650,#138651,#138652,#138653,#138654,#138655,#138656,#138657,
#138658,#138659,#138660,#138661,#138662,#138663,#138664,#138665,#138666,
#138667,#138668,#138669,#138670,#138671,#138672,#138673,#138674,#138675,
#138676,#138677,#138678,#138679,#138680,#138681,#138682,#138683,#138684,
#138685,#138686,#138687,#138688,#138689,#138690,#138691,#138692,#138693,
#138694,#138695,#138696,#138697,#138698,#138699,#138700,#138701,#138702,
#138703,#138704,#138705,#138706,#138707,#138708,#138709,#138710,#138711,
#138712,#138713,#138714,#138715,#138716,#138717,#138718,#138719,#138720,
#138721,#138722,#138723,#138724,#138725,#138726,#138727,#138728,#138729,
#138730,#138731,#138732,#138733,#138734,#138735,#138736,#138737,#138738,
#138739,#138740,#138741,#138742,#138743,#138744,#138745,#138746,#138747,
#138748,#138749,#138750,#138751,#138752,#138753,#138754,#138755,#138756,
#138757,#138758,#138759,#138760,#138761,#138762,#138763,#138764,#138765,
#138766,#138767,#138768,#138769,#138770,#138771,#138772,#138773,#138774,
#138775,#138776,#138777,#138778,#138779,#138780,#138781,#138782,#138783,
#138784,#138785,#138786,#138787,#138788,#138789,#138790,#138791,#138792,
#138793,#138794,#138795,#138796,#138797,#138798,#138799,#138800),
 .UNSPECIFIED.,.F.,.F.,(4,3,3,3,3,3,3,3,3,3,3,3,3,3,3,3,3,3,3,3,3,3,3,3,
3,3,3,3,3,3,3,3,3,3,3,3,3,3,3,3,3,3,3,3,3,3,3,3,3,3,3,3,3,3,3,3,3,3,3,3,
3,3,3,3,3,3,3,3,3,3,3,3,3,4),(1668.18569905633,1668.26932281117,1668.35284349824,
1668.43628137236,1668.51965661534,1668.60299698004,1668.6863204541,1668.76964521919,
1668.85298945409,1668.93642245116,1669.01990095181,1669.10351155826,1669.17772729307,
1669.26146600491,1669.34510151628,1669.42865395967,1669.51214339552,1669.59559734613,
1669.67903383997,1669.76247094972,1669.84592674463,1669.92947123736,1670.0130603203,
1670.09678358785,1670.17746330379,1670.26120201565,1670.34483752703,1670.42838997044,
1670.5118794063,1670.59533335693,1670.67876985079,1670.76220696056,1670.84566275549,
1670.92920724823,1671.01279633118,1671.09651959875,1671.17719931451,1671.26093802634,
1671.3445735377,1671.42812598109,1671.51161541693,1671.59506936753,1671.67850586136,
1671.76194297111,1671.84539876602,1671.92894325873,1672.01253234166,1672.09625560921,
1672.17693532523,1672.26067403705,1672.3443095484,1672.42786199177,1672.5113514276,
1672.59480537819,1672.67824187202,1672.76167898175,1672.84513477664,1672.92867926935,
1673.01226835227,1673.0959916198,1673.17667133595,1673.26041004788,1673.34404555934,
1673.42759800283,1673.51108743876,1673.59454138947,1673.6779778834,1673.76141499324,
1673.84487078825,1673.92841528106,1674.01200436409,1674.09572763173,1674.17640734667,
1674.21806788616),.UNSPECIFIED.);
#1115=B_SPLINE_CURVE_WITH_KNOTS('',3,(#138806,#138807,#138808,#138809,#138810,
#138811,#138812,#138813,#138814,#138815,#138816,#138817,#138818,#138819,
#138820,#138821,#138822,#138823,#138824,#138825,#138826,#138827,#138828,
#138829,#138830,#138831,#138832,#138833,#138834,#138835,#138836,#138837,
#138838,#138839,#138840,#138841,#138842,#138843,#138844,#138845,#138846,
#138847,#138848,#138849,#138850,#138851,#138852,#138853,#138854,#138855,
#138856,#138857,#138858,#138859,#138860,#138861,#138862,#138863,#138864,
#138865,#138866,#138867,#138868,#138869,#138870,#138871,#138872,#138873,
#138874,#138875,#138876,#138877,#138878,#138879,#138880,#138881,#138882,
#138883,#138884,#138885,#138886,#138887,#138888,#138889,#138890,#138891,
#138892,#138893,#138894,#138895,#138896,#138897,#138898,#138899,#138900,
#138901,#138902,#138903,#138904,#138905,#138906,#138907,#138908,#138909,
#138910,#138911,#138912,#138913,#138914,#138915,#138916,#138917,#138918,
#138919,#138920,#138921,#138922,#138923,#138924,#138925,#138926,#138927,
#138928,#138929,#138930,#138931,#138932,#138933,#138934,#138935,#138936,
#138937,#138938,#138939,#138940,#138941,#138942,#138943,#138944,#138945,
#138946,#138947,#138948,#138949,#138950,#138951,#138952,#138953,#138954,
#138955,#138956,#138957,#138958,#138959,#138960,#138961,#138962,#138963,
#138964,#138965,#138966,#138967,#138968,#138969,#138970,#138971,#138972,
#138973,#138974,#138975,#138976,#138977,#138978,#138979,#138980,#138981,
#138982,#138983,#138984,#138985,#138986,#138987,#138988,#138989,#138990,
#138991,#138992,#138993,#138994,#138995,#138996,#138997,#138998,#138999,
#139000,#139001,#139002,#139003,#139004,#139005,#139006,#139007,#139008,
#139009,#139010,#139011,#139012,#139013,#139014,#139015,#139016,#139017,
#139018,#139019,#139020,#139021,#139022,#139023,#139024,#139025),
 .UNSPECIFIED.,.F.,.F.,(4,3,3,3,3,3,3,3,3,3,3,3,3,3,3,3,3,3,3,3,3,3,3,3,
3,3,3,3,3,3,3,3,3,3,3,3,3,3,3,3,3,3,3,3,3,3,3,3,3,3,3,3,3,3,3,3,3,3,3,3,
3,3,3,3,3,3,3,3,3,3,3,3,3,4),(1674.46888436354,1674.56115257197,1674.65392929022,
1674.74696950423,1674.84034904643,1674.86585273767,1674.94959144905,1675.03322695995,
1675.11677940287,1675.20026883823,1675.28372278835,1675.36715928169,1675.45059639094,
1675.53405218535,1675.61759667757,1675.70118575999,1675.78490902703,1675.86558874839,
1675.94932746398,1676.0329629791,1676.11651542627,1676.20000486588,1676.28345882025,
1676.36689531785,1676.45033243134,1676.53378822999,1676.6173327264,1676.70092181301,
1676.78464508417,1676.86532475911,1676.94906346497,1677.03269897035,1677.11625140778,
1677.19974083768,1677.2831947824,1677.36663127038,1677.4500683743,1677.53352416343,
1677.61706865047,1677.70065772776,1677.78438098981,1677.86506076983,1677.94879948055,
1678.03243499074,1678.11598743291,1678.19947686748,1678.28293081675,1678.3663673092,
1678.44980441753,1678.53326021097,1678.61680470218,1678.70039378357,1678.78411704954,
1678.86479678055,1678.94853551605,1679.03217105115,1679.11572351834,1679.19921297802,
1679.28266695241,1679.36610347002,1679.44954060348,1679.53299642204,1679.61654093816,
1679.7001300444,1679.78385333486,1679.86453279127,1679.9471378052,1680.02964819366,
1680.11208308275,1680.19446152879,1680.27681143944,1680.35914315951,1680.44150012559,
1680.50024617582),.UNSPECIFIED.);
#1116=B_SPLINE_CURVE_WITH_KNOTS('',3,(#139026,#139027,#139028,#139029,#139030,
#139031,#139032,#139033,#139034,#139035),.UNSPECIFIED.,.F.,.F.,(4,3,3,4),
(1674.21825310493,1674.30279292267,1674.38730015935,1674.46888436336),
 .UNSPECIFIED.);
#1117=B_SPLINE_CURVE_WITH_KNOTS('',3,(#139037,#139038,#139039,#139040,#139041,
#139042,#139043,#139044,#139045,#139046),.UNSPECIFIED.,.F.,.F.,(4,3,3,4),
(1674.21806788616,1674.32085147138,1674.4222713986,1674.46888436323),
 .UNSPECIFIED.);
#1118=B_SPLINE_CURVE_WITH_KNOTS('',3,(#139047,#139048,#139049,#139050,#139051,
#139052,#139053,#139054,#139055,#139056,#139057,#139058,#139059,#139060,
#139061,#139062,#139063,#139064,#139065,#139066,#139067,#139068,#139069,
#139070,#139071,#139072,#139073,#139074,#139075,#139076,#139077,#139078,
#139079,#139080,#139081,#139082,#139083,#139084,#139085,#139086,#139087,
#139088,#139089,#139090,#139091,#139092,#139093,#139094,#139095,#139096,
#139097,#139098,#139099,#139100,#139101,#139102,#139103,#139104,#139105,
#139106,#139107,#139108,#139109,#139110,#139111,#139112,#139113,#139114,
#139115,#139116,#139117,#139118,#139119,#139120,#139121,#139122,#139123,
#139124,#139125,#139126,#139127,#139128,#139129,#139130,#139131,#139132,
#139133,#139134,#139135,#139136,#139137,#139138,#139139,#139140,#139141,
#139142,#139143,#139144,#139145,#139146,#139147,#139148,#139149,#139150,
#139151,#139152,#139153,#139154,#139155,#139156,#139157,#139158,#139159,
#139160,#139161,#139162,#139163,#139164,#139165,#139166,#139167,#139168,
#139169,#139170,#139171,#139172,#139173,#139174,#139175,#139176,#139177,
#139178,#139179,#139180,#139181,#139182,#139183,#139184,#139185,#139186,
#139187,#139188,#139189,#139190,#139191,#139192,#139193,#139194,#139195,
#139196,#139197,#139198,#139199,#139200,#139201,#139202,#139203,#139204,
#139205,#139206,#139207,#139208,#139209,#139210,#139211,#139212,#139213,
#139214,#139215,#139216,#139217,#139218,#139219,#139220,#139221,#139222,
#139223,#139224,#139225,#139226,#139227,#139228,#139229,#139230,#139231,
#139232,#139233,#139234,#139235,#139236,#139237,#139238,#139239,#139240,
#139241,#139242,#139243,#139244,#139245,#139246,#139247,#139248,#139249,
#139250,#139251,#139252,#139253,#139254,#139255,#139256,#139257,#139258,
#139259,#139260,#139261,#139262,#139263,#139264,#139265,#139266),
 .UNSPECIFIED.,.F.,.F.,(4,3,3,3,3,3,3,3,3,3,3,3,3,3,3,3,3,3,3,3,3,3,3,3,
3,3,3,3,3,3,3,3,3,3,3,3,3,3,3,3,3,3,3,3,3,3,3,3,3,3,3,3,3,3,3,3,3,3,3,3,
3,3,3,3,3,3,3,3,3,3,3,3,3,4),(1674.46888436336,1674.55177946142,1674.63464698122,
1674.71750299009,1674.80036604691,1674.88325471219,1674.96623556418,1675.04926809218,
1675.13242546003,1675.17614335739,1675.25988206912,1675.34351758038,1675.42707002366,
1675.5105594594,1675.5940134099,1675.67744990363,1675.76088701327,1675.84434280807,
1675.92788730068,1676.0114763835,1676.09519965094,1676.17587936811,1676.25961808053,
1676.34325359248,1676.42680603646,1676.5102954729,1676.59374942409,1676.67718591851,
1676.76062302885,1676.84407882434,1676.92762331763,1677.01121240114,1677.09493566925,
1677.17561537883,1677.25935408989,1677.34298960048,1677.42654204309,1677.51003147817,
1677.59348542801,1677.67692192109,1677.76035903009,1677.84381482425,1677.92735931624,
1678.01094839845,1678.09467166529,1678.17535138955,1678.25909010093,1678.34272561183,
1678.42627805475,1678.50976749011,1678.59322144023,1678.67665793357,1678.76009504282,
1678.84355083723,1678.92709532945,1679.01068441187,1679.09440767892,1679.17508740027,
1679.25882611586,1679.34246163098,1679.42601407815,1679.50950351776,1679.59295747213,
1679.67639396973,1679.75983108322,1679.84328688186,1679.92683137828,1680.01042046489,
1680.09414373605,1680.17482341099,1680.26034755561,1680.34576440261,1680.43105754023,
1680.50154027024),.UNSPECIFIED.);
#1119=B_SPLINE_CURVE_WITH_KNOTS('',3,(#139272,#139273,#139274,#139275,#139276,
#139277,#139278,#139279,#139280,#139281,#139282,#139283,#139284,#139285,
#139286,#139287,#139288,#139289,#139290,#139291,#139292,#139293,#139294,
#139295,#139296,#139297,#139298,#139299,#139300,#139301,#139302,#139303,
#139304,#139305,#139306,#139307,#139308,#139309,#139310,#139311,#139312,
#139313,#139314,#139315,#139316,#139317,#139318,#139319,#139320,#139321,
#139322,#139323,#139324,#139325,#139326,#139327,#139328,#139329,#139330,
#139331,#139332,#139333,#139334,#139335,#139336,#139337,#139338,#139339,
#139340,#139341,#139342,#139343,#139344,#139345,#139346,#139347,#139348,
#139349,#139350,#139351,#139352,#139353,#139354,#139355,#139356,#139357,
#139358,#139359,#139360,#139361,#139362,#139363,#139364,#139365,#139366,
#139367,#139368,#139369,#139370,#139371,#139372,#139373,#139374,#139375,
#139376,#139377,#139378,#139379,#139380,#139381,#139382,#139383,#139384,
#139385,#139386,#139387,#139388,#139389,#139390,#139391,#139392,#139393,
#139394,#139395,#139396,#139397,#139398,#139399,#139400,#139401,#139402,
#139403,#139404,#139405,#139406,#139407,#139408,#139409,#139410,#139411,
#139412,#139413,#139414,#139415,#139416,#139417,#139418,#139419,#139420,
#139421,#139422,#139423,#139424,#139425,#139426,#139427,#139428,#139429,
#139430,#139431,#139432,#139433,#139434,#139435,#139436,#139437,#139438,
#139439,#139440,#139441,#139442,#139443,#139444,#139445,#139446,#139447,
#139448,#139449,#139450,#139451,#139452,#139453,#139454,#139455,#139456,
#139457,#139458,#139459,#139460,#139461,#139462,#139463,#139464,#139465,
#139466,#139467,#139468,#139469,#139470,#139471,#139472,#139473,#139474,
#139475,#139476,#139477,#139478,#139479,#139480,#139481,#139482,#139483,
#139484,#139485,#139486,#139487,#139488),.UNSPECIFIED.,.F.,.F.,(4,3,3,3,
3,3,3,3,3,3,3,3,3,3,3,3,3,3,3,3,3,3,3,3,3,3,3,3,3,3,3,3,3,3,3,3,3,3,3,3,
3,3,3,3,3,3,3,3,3,3,3,3,3,3,3,3,3,3,3,3,3,3,3,3,3,3,3,3,3,3,3,3,4),(1680.75206967054,
1680.86426880199,1680.94800751987,1681.03164303693,1681.11519548569,1681.19868492656,
1681.28213888166,1681.36557537968,1681.44901249328,1681.53246829172,1681.61601278743,
1681.69960187308,1681.78332514284,1681.86400481271,1681.94774367009,1682.03137932759,
1682.11493191756,1682.19842150028,1682.28187559768,1682.36531223825,1682.44874949452,
1682.53220543561,1682.61575007314,1682.69933930037,1682.78306270987,1682.86374082343,
1682.94747921671,1683.03111440949,1683.11466653459,1683.19815565276,1683.28160928774,
1683.36504546723,1683.4484822642,1683.5319377482,1683.6154819347,1683.69907071347,
1683.78279368346,1683.86347683415,1683.94721567741,1684.0308513181,1684.11440388863,
1684.19789344933,1684.28134752089,1684.36478413332,1684.44822135917,1684.53167726761,
1684.61522186917,1684.69881105857,1684.78253442747,1684.86321284487,1684.94695242428,
1685.03058880757,1685.11414212632,1685.19763243999,1685.28108726909,1685.3645246417,
1685.44796262968,1685.53141930143,1685.61496466385,1685.69855461397,1685.78227873561,
1685.86294885559,1685.94668988417,1686.03032667021,1686.11387935293,1686.19762019608,
1686.2810682586,1686.36449745582,1686.44792586159,1686.53189592071,1686.61541141165,
1686.69960875486,1686.78380609807),.UNSPECIFIED.);
#1120=B_SPLINE_CURVE_WITH_KNOTS('',3,(#139489,#139490,#139491,#139492,#139493,
#139494,#139495,#139496,#139497,#139498),.UNSPECIFIED.,.F.,.F.,(4,3,3,4),
(1680.50024617582,1680.58267551838,1680.66737259439,1680.7520696704),
 .UNSPECIFIED.);
#1121=B_SPLINE_CURVE_WITH_KNOTS('',3,(#139500,#139501,#139502,#139503,#139504,
#139505,#139506,#139507,#139508,#139509),.UNSPECIFIED.,.F.,.F.,(4,3,3,4),
(1680.50154027024,1680.58669000473,1680.67178237626,1680.75206967054),
 .UNSPECIFIED.);
#1122=B_SPLINE_CURVE_WITH_KNOTS('',3,(#139510,#139511,#139512,#139513,#139514,
#139515,#139516,#139517,#139518,#139519,#139520,#139521,#139522,#139523,
#139524,#139525,#139526,#139527,#139528,#139529,#139530,#139531,#139532,
#139533,#139534,#139535,#139536,#139537,#139538,#139539,#139540,#139541,
#139542,#139543,#139544,#139545,#139546,#139547,#139548,#139549,#139550,
#139551,#139552,#139553,#139554,#139555,#139556,#139557,#139558,#139559,
#139560,#139561,#139562,#139563,#139564,#139565,#139566,#139567,#139568,
#139569,#139570,#139571,#139572,#139573,#139574,#139575,#139576,#139577,
#139578,#139579,#139580,#139581,#139582,#139583,#139584,#139585,#139586,
#139587,#139588,#139589,#139590,#139591,#139592,#139593,#139594,#139595,
#139596,#139597,#139598,#139599,#139600,#139601,#139602,#139603,#139604,
#139605,#139606,#139607,#139608,#139609,#139610,#139611,#139612,#139613,
#139614,#139615,#139616,#139617,#139618,#139619,#139620,#139621,#139622,
#139623,#139624,#139625,#139626,#139627,#139628,#139629,#139630,#139631,
#139632,#139633,#139634,#139635,#139636,#139637,#139638,#139639,#139640,
#139641,#139642,#139643,#139644,#139645,#139646,#139647,#139648,#139649,
#139650,#139651,#139652,#139653,#139654,#139655,#139656,#139657,#139658,
#139659,#139660,#139661,#139662,#139663,#139664,#139665,#139666,#139667,
#139668,#139669,#139670,#139671,#139672,#139673,#139674,#139675,#139676,
#139677,#139678,#139679,#139680,#139681,#139682,#139683,#139684,#139685,
#139686,#139687,#139688,#139689,#139690,#139691,#139692,#139693,#139694,
#139695,#139696,#139697,#139698,#139699,#139700,#139701,#139702,#139703,
#139704,#139705,#139706,#139707,#139708,#139709,#139710,#139711,#139712,
#139713,#139714,#139715,#139716,#139717,#139718,#139719,#139720,#139721,
#139722,#139723,#139724,#139725,#139726,#139727,#139728,#139729),
 .UNSPECIFIED.,.F.,.F.,(4,3,3,3,3,3,3,3,3,3,3,3,3,3,3,3,3,3,3,3,3,3,3,3,
3,3,3,3,3,3,3,3,3,3,3,3,3,3,3,3,3,3,3,3,3,3,3,3,3,3,3,3,3,3,3,3,3,3,3,3,
3,3,3,3,3,3,3,3,3,3,3,3,3,4),(1680.75206967069,1680.84288816935,1680.93411487138,
1681.02554954485,1681.11729322716,1681.17455942171,1681.25829813243,1681.34193364261,
1681.42548608478,1681.50897551935,1681.59242946861,1681.67586596107,1681.75930306939,
1681.84275886284,1681.92630335404,1682.00989243543,1682.09361570139,1682.17429543243,
1682.25803416793,1682.34166970303,1682.42522217022,1682.5087116299,1682.59216560429,
1682.6756021219,1682.75903925536,1682.84249507392,1682.92603959004,1683.00962869628,
1683.09335198674,1683.17403144315,1683.25777011073,1683.34140557785,1683.42495797707,
1683.50844736885,1683.59190127572,1683.67533772603,1683.75877479249,1683.84223054439,
1683.9257749948,1684.00936403572,1684.09308726221,1684.17376745387,1684.25750617175,
1684.34114168881,1684.42469413757,1684.50818357844,1684.59163753354,1684.67507403155,
1684.75851114516,1684.84196694359,1684.92551143931,1685.00910052496,1685.09282379471,
1685.17350346459,1685.25724232197,1685.34087797947,1685.42443056944,1685.50792015216,
1685.59137424956,1685.67481089013,1685.7582481464,1685.84170408749,1685.92524872503,
1686.00883795226,1686.09256136176,1686.17323947531,1686.25574915047,1686.33816398583,
1686.42050317268,1686.50278583004,1686.58503751018,1686.6672712406,1686.74952284399,
1686.7834725217),.UNSPECIFIED.);
#1123=B_SPLINE_CURVE_WITH_KNOTS('',3,(#139735,#139736,#139737,#139738,#139739,
#139740,#139741,#139742,#139743,#139744,#139745,#139746,#139747,#139748,
#139749,#139750,#139751,#139752,#139753,#139754,#139755,#139756,#139757,
#139758,#139759,#139760,#139761,#139762,#139763,#139764,#139765,#139766,
#139767,#139768,#139769,#139770,#139771,#139772,#139773,#139774,#139775,
#139776,#139777,#139778,#139779,#139780,#139781,#139782,#139783,#139784,
#139785,#139786,#139787,#139788,#139789,#139790,#139791,#139792,#139793,
#139794,#139795,#139796,#139797,#139798,#139799,#139800,#139801,#139802,
#139803,#139804,#139805,#139806,#139807,#139808,#139809,#139810,#139811,
#139812,#139813,#139814,#139815,#139816,#139817,#139818,#139819,#139820,
#139821,#139822,#139823,#139824,#139825,#139826,#139827,#139828,#139829,
#139830,#139831,#139832,#139833,#139834,#139835,#139836,#139837,#139838,
#139839,#139840,#139841,#139842,#139843,#139844,#139845,#139846,#139847,
#139848,#139849,#139850,#139851,#139852,#139853,#139854,#139855,#139856,
#139857,#139858,#139859,#139860,#139861,#139862,#139863,#139864,#139865,
#139866,#139867,#139868,#139869,#139870,#139871,#139872,#139873,#139874,
#139875,#139876,#139877,#139878,#139879,#139880,#139881,#139882,#139883,
#139884,#139885,#139886,#139887,#139888,#139889,#139890,#139891,#139892,
#139893,#139894,#139895,#139896,#139897,#139898,#139899,#139900,#139901,
#139902,#139903,#139904,#139905,#139906,#139907,#139908,#139909,#139910,
#139911,#139912,#139913,#139914,#139915,#139916,#139917,#139918,#139919,
#139920,#139921,#139922,#139923,#139924,#139925,#139926,#139927,#139928,
#139929,#139930,#139931,#139932,#139933,#139934,#139935,#139936,#139937,
#139938,#139939,#139940,#139941,#139942,#139943,#139944,#139945,#139946,
#139947,#139948,#139949,#139950,#139951,#139952,#139953,#139954),
 .UNSPECIFIED.,.F.,.F.,(4,3,3,3,3,3,3,3,3,3,3,3,3,3,3,3,3,3,3,3,3,3,3,3,
3,3,3,3,3,3,3,3,3,3,3,3,3,3,3,3,3,3,3,3,3,3,3,3,3,3,3,3,3,3,3,3,3,3,3,3,
3,3,3,3,3,3,3,3,3,3,3,3,3,4),(1687.0352549779,1687.11762183547,1687.19991216208,
1687.28272575145,1687.36493564271,1687.44713698684,1687.52934881702,1687.61261683202,
1687.69494876307,1687.77868482005,1687.86242087703,1687.94616455657,1688.02980506654,
1688.11336253391,1688.19685701369,1688.28031602056,1688.36375757747,1688.44719975227,
1688.5306606094,1688.61421013112,1688.69780423297,1688.78153245111,1688.86215688775,
1688.94588019747,1689.02950028853,1689.11303730936,1689.19651133616,1689.27994995193,
1689.36337115805,1689.44679304129,1689.53023368507,1689.61376323092,1689.69733745427,
1689.78104616198,1689.86189289847,1689.94564535982,1690.02929454784,1690.11286058205,
1690.19636350991,1690.27983075653,1690.3632804255,1690.44673057771,1690.53019927051,
1690.61375636118,1690.69735789888,1690.78109325142,1690.86162890919,1690.94539453213,
1691.02905716924,1691.11263692238,1691.19615382169,1691.27963537068,1691.36309954086,
1691.44656437829,1691.5300479256,1691.61362005147,1691.69723674639,1691.7809873084,
1691.86136491991,1691.94499994849,1692.02853160577,1692.11198013047,1692.19536568823,
1692.27871618166,1692.36204948573,1692.44538376701,1692.52873718895,1692.61218060301,
1692.69566914794,1692.77929382412,1692.86110093063,1692.9513655271,1693.04140261296,
1693.06812991347),.UNSPECIFIED.);
#1124=B_SPLINE_CURVE_WITH_KNOTS('',3,(#139955,#139956,#139957,#139958,#139959,
#139960,#139961,#139962,#139963,#139964),.UNSPECIFIED.,.F.,.F.,(4,3,3,4),
(1686.78380609807,1686.86268486631,1686.99306837669,1687.03525497772),
 .UNSPECIFIED.);
#1125=B_SPLINE_CURVE_WITH_KNOTS('',3,(#139966,#139967,#139968,#139969,#139970,
#139971,#139972,#139973,#139974,#139975),.UNSPECIFIED.,.F.,.F.,(4,3,3,4),
(1686.7834725217,1686.86578987103,1686.95052242432,1687.0352549776),
 .UNSPECIFIED.);
#1126=B_SPLINE_CURVE_WITH_KNOTS('',3,(#139976,#139977,#139978,#139979,#139980,
#139981,#139982,#139983,#139984,#139985,#139986,#139987,#139988,#139989,
#139990,#139991,#139992,#139993,#139994,#139995,#139996,#139997,#139998,
#139999,#140000,#140001,#140002,#140003,#140004,#140005,#140006,#140007,
#140008,#140009,#140010,#140011,#140012,#140013,#140014,#140015,#140016,
#140017,#140018,#140019,#140020,#140021,#140022,#140023,#140024,#140025,
#140026,#140027,#140028,#140029,#140030,#140031,#140032,#140033,#140034,
#140035,#140036,#140037,#140038,#140039,#140040,#140041,#140042,#140043,
#140044,#140045,#140046,#140047,#140048,#140049,#140050,#140051,#140052,
#140053,#140054,#140055,#140056,#140057,#140058,#140059,#140060,#140061,
#140062,#140063,#140064,#140065,#140066,#140067,#140068,#140069,#140070,
#140071,#140072,#140073,#140074,#140075,#140076,#140077,#140078,#140079,
#140080,#140081,#140082,#140083,#140084,#140085,#140086,#140087,#140088,
#140089,#140090,#140091,#140092,#140093,#140094,#140095,#140096,#140097,
#140098,#140099,#140100,#140101,#140102,#140103,#140104,#140105,#140106,
#140107,#140108,#140109,#140110,#140111,#140112,#140113,#140114,#140115,
#140116,#140117,#140118,#140119,#140120,#140121,#140122,#140123,#140124,
#140125,#140126,#140127,#140128,#140129,#140130,#140131,#140132,#140133,
#140134,#140135,#140136,#140137,#140138,#140139,#140140,#140141,#140142,
#140143,#140144,#140145,#140146,#140147,#140148,#140149,#140150,#140151,
#140152,#140153,#140154,#140155,#140156,#140157,#140158,#140159,#140160,
#140161,#140162,#140163,#140164,#140165,#140166,#140167,#140168,#140169,
#140170,#140171,#140172,#140173,#140174,#140175,#140176,#140177,#140178,
#140179,#140180,#140181,#140182,#140183,#140184,#140185,#140186,#140187,
#140188,#140189,#140190,#140191,#140192),.UNSPECIFIED.,.F.,.F.,(4,3,3,3,
3,3,3,3,3,3,3,3,3,3,3,3,3,3,3,3,3,3,3,3,3,3,3,3,3,3,3,3,3,3,3,3,3,3,3,3,
3,3,3,3,3,3,3,3,3,3,3,3,3,3,3,3,3,3,3,3,3,3,3,3,3,3,3,3,3,3,3,3,4),(1687.03525497772,
1687.17297548603,1687.25671432929,1687.34034996998,1687.42390254051,1687.50739210121,
1687.59084617277,1687.67428278519,1687.75772001105,1687.84117591948,1687.92472052105,
1688.00830971045,1688.09203307935,1688.17271149675,1688.25645107616,1688.34008745945,
1688.4236407782,1688.50713109187,1688.59058592097,1688.67402329358,1688.75746128155,
1688.84091795331,1688.92446331573,1689.00805326585,1689.09177738749,1689.17244750747,
1689.25618398008,1689.33981725074,1689.42336745426,1689.50685465334,1689.59030637971,
1689.6737406572,1689.75717556056,1689.84062916108,1689.9241714907,1690.00775842411,
1690.0914795871,1690.17218351819,1690.25592370815,1690.33956068508,1690.42311458017,
1690.5066054525,1690.59006081169,1690.67349869696,1690.75693717979,1690.84039432818,
1690.92394013598,1691.00753051519,1691.09125503391,1691.17191952891,1691.25566320845,
1691.33930371841,1691.42286118579,1691.50635566557,1691.58981467244,1691.67325622935,
1691.75669840415,1691.84015926128,1691.923708783,1692.00730288485,1692.09103110299,
1692.17165553963,1692.25538494486,1692.33900975173,1692.42255011458,1692.5060216795,
1692.5894557807,1692.67287052082,1692.75628398561,1692.83975081521,1692.92324528107,
1693.00683495087,1693.06690371234),.UNSPECIFIED.);
#1127=B_SPLINE_CURVE_WITH_KNOTS('',3,(#140196,#140197,#140198,#140199,#140200,
#140201,#140202,#140203,#140204,#140205,#140206,#140207,#140208,#140209,
#140210,#140211,#140212,#140213,#140214,#140215,#140216,#140217,#140218,
#140219,#140220,#140221,#140222,#140223,#140224,#140225,#140226,#140227,
#140228,#140229,#140230,#140231,#140232,#140233,#140234,#140235,#140236,
#140237,#140238,#140239,#140240,#140241,#140242,#140243,#140244,#140245,
#140246,#140247,#140248,#140249,#140250,#140251,#140252,#140253,#140254,
#140255,#140256,#140257,#140258,#140259,#140260,#140261,#140262,#140263,
#140264,#140265,#140266,#140267,#140268,#140269,#140270,#140271,#140272,
#140273,#140274),.UNSPECIFIED.,.F.,.F.,(4,3,3,3,3,3,3,3,3,3,3,3,3,3,3,3,
3,3,3,3,3,3,3,3,3,3,4),(-4.09254174884206,-3.99894404288052,-3.91885449630764,
-3.83885809227166,-3.75893744803051,-3.67907523956829,-3.59925418855671,
-3.51944544555752,-3.43963967421031,-3.35982126989644,-3.27997462355469,
-3.20004057373489,-3.1200573453262,-3.03996113306838,-2.99920803216039,
-2.9207016395211,-2.84228988317914,-2.76395413880008,-2.68567586928874,
-2.60742974348718,-2.52919913889701,-2.45096738081357,-2.37271779450763,
-2.29438746102101,-2.21601536556249,-2.13752365119797,-2.07058826465548),
 .UNSPECIFIED.);
#1128=B_SPLINE_CURVE_WITH_KNOTS('',3,(#140278,#140279,#140280,#140281,#140282,
#140283,#140284,#140285,#140286,#140287,#140288,#140289,#140290,#140291,
#140292,#140293,#140294,#140295,#140296,#140297,#140298,#140299,#140300,
#140301,#140302,#140303,#140304,#140305,#140306,#140307,#140308,#140309,
#140310,#140311,#140312,#140313,#140314,#140315,#140316,#140317,#140318,
#140319,#140320),.UNSPECIFIED.,.F.,.F.,(4,3,3,3,3,3,3,3,3,3,3,3,3,3,4),
(0.,0.0935817941909758,0.187331892979243,0.281085442661883,0.374720077979815,
0.468011049746007,0.499868005357902,0.579828600624018,0.659779162846936,
0.739735219717809,0.819740648566051,0.899775729107479,0.979885236083813,
0.999736010719684,1.11885509353369),.UNSPECIFIED.);
#1129=B_SPLINE_CURVE_WITH_KNOTS('',3,(#140322,#140323,#140324,#140325,#140326,
#140327,#140328,#140329,#140330,#140331,#140332,#140333,#140334,#140335,
#140336,#140337,#140338,#140339,#140340,#140341,#140342,#140343,#140344,
#140345,#140346,#140347,#140348,#140349,#140350,#140351,#140352,#140353,
#140354,#140355,#140356,#140357,#140358,#140359,#140360,#140361,#140362,
#140363,#140364,#140365,#140366,#140367,#140368,#140369,#140370,#140371,
#140372,#140373,#140374,#140375,#140376,#140377,#140378,#140379,#140380,
#140381,#140382,#140383,#140384,#140385,#140386,#140387,#140388,#140389,
#140390,#140391,#140392,#140393,#140394,#140395,#140396,#140397,#140398,
#140399,#140400,#140401,#140402,#140403,#140404,#140405,#140406,#140407,
#140408,#140409,#140410,#140411,#140412,#140413,#140414,#140415,#140416,
#140417,#140418,#140419,#140420,#140421,#140422,#140423,#140424,#140425,
#140426,#140427,#140428,#140429,#140430,#140431,#140432,#140433,#140434,
#140435,#140436,#140437,#140438,#140439,#140440,#140441,#140442,#140443,
#140444,#140445,#140446,#140447,#140448,#140449,#140450,#140451,#140452,
#140453,#140454,#140455,#140456,#140457,#140458,#140459,#140460,#140461,
#140462,#140463,#140464,#140465,#140466,#140467,#140468,#140469,#140470,
#140471,#140472,#140473,#140474,#140475,#140476,#140477,#140478,#140479,
#140480,#140481,#140482,#140483,#140484,#140485,#140486,#140487,#140488,
#140489,#140490,#140491,#140492,#140493,#140494,#140495,#140496,#140497,
#140498,#140499,#140500,#140501,#140502,#140503,#140504,#140505,#140506,
#140507,#140508,#140509,#140510,#140511,#140512,#140513,#140514,#140515,
#140516,#140517,#140518,#140519,#140520,#140521,#140522,#140523,#140524,
#140525,#140526,#140527,#140528,#140529,#140530,#140531,#140532,#140533,
#140534,#140535,#140536,#140537,#140538,#140539,#140540,#140541,#140542,
#140543,#140544,#140545,#140546,#140547,#140548,#140549,#140550,#140551,
#140552,#140553,#140554,#140555,#140556,#140557,#140558,#140559,#140560,
#140561,#140562,#140563,#140564,#140565),.UNSPECIFIED.,.F.,.F.,(4,3,3,3,
3,3,3,3,3,3,3,3,3,3,3,3,3,3,3,3,3,3,3,3,3,3,3,3,3,3,3,3,3,3,3,3,3,3,3,3,
3,3,3,3,3,3,3,3,3,3,3,3,3,3,3,3,3,3,3,3,3,3,3,3,3,3,3,3,3,3,3,3,3,3,3,3,
3,3,3,3,3,4),(1.11885509365316,1.19890412789216,1.27889220714027,1.35883652401209,
1.43891596119061,1.518840493998,1.59877521794939,1.6787356591488,1.75891974972165,
1.83901897528853,1.919249023072,1.99947202144022,2.07876788808251,2.15796183556404,
2.23707201384114,2.31611649693057,2.39511330010876,2.4740904982881,2.55306021205585,
2.63203868968195,2.71104218287401,2.79013230483545,2.86926983209992,2.94852490788452,
2.99920803216035,3.07930247080208,3.15930292307334,3.23922677491295,3.31909135287532,
3.39891393720777,3.47872295966545,3.55852823188179,3.6383453584131,3.71818994778447,
3.79812076697098,3.8781000941454,3.95819139359745,3.99894404288049,4.07900057834142,
4.15896436952754,4.23885283571627,4.31868333758502,4.39847319032814,4.47825161765034,
4.55802762890995,4.63781686288743,4.71763496319276,4.79754158030628,4.87749796878064,
4.95756851179511,4.99868005360062,5.07854379860577,5.15831194592404,5.23800211985226,
5.31763188244565,5.39721874739824,5.47679146185666,5.5563600875881,5.63594043642507,
5.71554832432581,5.79524375880277,5.87498809798384,5.95484705923799,5.99841606432075,
6.07839930855999,6.15828820346944,6.23810025063035,6.31785289130088,6.39756351983018,
6.4772609324546,6.55695482576828,6.63666090658931,6.71639488600397,6.79621632762634,
6.87608681649885,6.9560710618768,6.99815207504088,7.08687973637244,7.1752513055744,
7.26339298300667,7.35115912867321,7.40204018020966),.UNSPECIFIED.);
#1130=B_SPLINE_CURVE_WITH_KNOTS('',3,(#140567,#140568,#140569,#140570,#140571,
#140572,#140573,#140574,#140575,#140576),.UNSPECIFIED.,.F.,.F.,(4,1,1,1,
1,1,1,4),(7.40204040069455,7.99788808576102,8.99762409648117,9.99736010720132,
10.9970961179215,11.9968321286416,12.9965681393618,13.6852257078742),
 .UNSPECIFIED.);
#1131=B_SPLINE_CURVE_WITH_KNOTS('',3,(#140578,#140579,#140580,#140581,#140582,
#140583,#140584,#140585,#140586,#140587,#140588,#140589,#140590,#140591,
#140592,#140593,#140594,#140595,#140596,#140597,#140598,#140599,#140600,
#140601,#140602,#140603,#140604,#140605,#140606,#140607,#140608,#140609,
#140610,#140611,#140612,#140613,#140614,#140615,#140616,#140617,#140618,
#140619,#140620,#140621,#140622,#140623,#140624,#140625,#140626,#140627,
#140628,#140629,#140630,#140631,#140632,#140633,#140634,#140635,#140636,
#140637,#140638,#140639,#140640,#140641,#140642,#140643,#140644,#140645,
#140646,#140647,#140648,#140649,#140650,#140651,#140652,#140653,#140654,
#140655,#140656,#140657,#140658,#140659,#140660,#140661,#140662,#140663,
#140664,#140665,#140666,#140667,#140668,#140669,#140670,#140671,#140672,
#140673,#140674,#140675,#140676,#140677,#140678,#140679,#140680,#140681,
#140682,#140683,#140684,#140685,#140686,#140687,#140688,#140689,#140690,
#140691,#140692,#140693,#140694,#140695,#140696,#140697,#140698,#140699,
#140700,#140701,#140702,#140703,#140704,#140705,#140706,#140707,#140708,
#140709,#140710,#140711,#140712,#140713,#140714,#140715,#140716,#140717,
#140718,#140719,#140720,#140721,#140722,#140723,#140724,#140725,#140726,
#140727,#140728,#140729,#140730,#140731,#140732,#140733,#140734,#140735,
#140736,#140737,#140738,#140739,#140740,#140741,#140742,#140743,#140744,
#140745,#140746,#140747,#140748,#140749,#140750,#140751,#140752,#140753,
#140754,#140755,#140756,#140757,#140758,#140759,#140760,#140761,#140762,
#140763,#140764,#140765,#140766,#140767,#140768,#140769,#140770,#140771,
#140772,#140773,#140774,#140775,#140776,#140777,#140778,#140779,#140780,
#140781,#140782,#140783,#140784,#140785,#140786,#140787,#140788,#140789,
#140790,#140791,#140792,#140793,#140794,#140795,#140796,#140797,#140798,
#140799,#140800,#140801,#140802,#140803,#140804,#140805,#140806,#140807,
#140808,#140809,#140810,#140811,#140812,#140813,#140814,#140815,#140816,
#140817,#140818,#140819,#140820,#140821,#140822,#140823,#140824),
 .UNSPECIFIED.,.F.,.F.,(4,3,3,3,3,3,3,3,3,3,3,3,3,3,3,3,3,3,3,3,3,3,3,3,
3,3,3,3,3,3,3,3,3,3,3,3,3,3,3,3,3,3,3,3,3,3,3,3,3,3,3,3,3,3,3,3,3,3,3,3,
3,3,3,3,3,3,3,3,3,3,3,3,3,3,3,3,3,3,3,3,3,3,4),(13.6852259127505,13.7801099435782,
13.8756905427146,13.9720376507108,13.9963041500819,14.0762611679736,14.1561236791645,
14.2359092120701,14.3156352344774,14.3953191670501,14.4749898540935,14.5546570063244,
14.6343363539807,14.7140436316013,14.7938385549703,14.8736825899846,14.9536407114316,
14.996040160802,15.0759975957193,15.1558605290186,15.2356464886784,15.3153729420553,
15.3950573093886,15.4747284354873,15.5543960293979,15.6340758209858,15.7137835444186,
15.7935789142272,15.8734233967061,15.9533819633687,15.9957761715221,16.075733473648,
16.1555962732271,16.2353820983737,16.3151084165785,16.3947926482139,16.4744636382654,
16.5541310959256,16.6338107511781,16.7135183383086,16.7933135725563,16.873157919691,
16.9531163525208,16.9955121822422,17.0754694434268,17.1553322011706,17.2351179836328,
17.314844258348,17.3945284457316,17.4741993905267,17.5538668023107,17.633546411104,
17.713253951229,17.7930491378706,17.8728934369877,17.9528518215654,17.9952481929623,
18.0752055148322,18.1550683340336,18.2348541786619,18.3145805161891,18.3942647669683,
18.4739357758324,18.5536032520972,18.6332829257289,18.7129905309957,18.7927857829151,
18.8726301474848,18.9525885972255,18.9949842036824,19.0745911127166,19.1541037254495,
19.2335398970435,19.3129174188851,19.3948541184062,19.4741786590968,19.5535018339292,
19.6328396635326,19.7122081748832,19.7916638055052,19.8711715970075,19.9507856857916,
19.9684110150538),.UNSPECIFIED.);
#1132=B_SPLINE_CURVE_WITH_KNOTS('',3,(#140826,#140827,#140828,#140829,#140830,
#140831,#140832,#140833,#140834,#140835,#140836,#140837),.UNSPECIFIED.,
 .F.,.F.,(4,2,1,1,1,1,1,1,4),(19.9684110150538,19.9947202144025,20.9944562251227,
21.9941922358428,22.9939282465629,23.9936642572831,24.9934002680032,25.9931362787233,
26.2515963222334),.UNSPECIFIED.);
#1133=B_SPLINE_CURVE_WITH_KNOTS('',3,(#140839,#140840,#140841,#140842,#140843,
#140844,#140845,#140846,#140847,#140848),.UNSPECIFIED.,.F.,.F.,(4,1,1,1,
1,1,1,4),(26.2515963222334,26.9928722894435,27.9926083001636,28.9923443108837,
29.9920803216039,30.991816332324,31.9915523430441,32.534781629413),
 .UNSPECIFIED.);
#1134=B_SPLINE_CURVE_WITH_KNOTS('',3,(#140850,#140851,#140852,#140853,#140854,
#140855,#140856,#140857,#140858,#140859),.UNSPECIFIED.,.F.,.F.,(4,1,1,1,
1,1,1,4),(32.534781629413,32.9912883537643,33.9910243644844,34.9907603752045,
35.9904963859246,36.9902323966447,37.9899684073648,38.8179669365925),
 .UNSPECIFIED.);
#1135=B_SPLINE_CURVE_WITH_KNOTS('',3,(#140861,#140862,#140863,#140864,#140865,
#140866,#140867,#140868,#140869,#140870,#140871),.UNSPECIFIED.,.F.,.F.,
(4,1,1,1,1,1,1,1,4),(38.8179669365925,38.9897044180849,39.9894404288051,
40.9891764395252,41.9889124502454,42.9886484609655,43.9883844716856,44.9881204824058,
45.1011522437721),.UNSPECIFIED.);
#1136=B_SPLINE_CURVE_WITH_KNOTS('',3,(#140873,#140874,#140875,#140876,#140877,
#140878,#140879,#140880,#140881,#140882),.UNSPECIFIED.,.F.,.F.,(4,1,1,1,
1,1,1,4),(45.1011522437721,45.9878564931259,46.9875925038461,47.9873285145662,
48.9870645252863,49.9868005360065,50.9865365467266,51.3843375509517),
 .UNSPECIFIED.);
#1137=B_SPLINE_CURVE_WITH_KNOTS('',3,(#140884,#140885,#140886,#140887,#140888,
#140889,#140890,#140891,#140892,#140893),.UNSPECIFIED.,.F.,.F.,(4,1,1,1,
1,1,1,4),(51.3843375509517,51.9862725574467,52.9860085681668,53.9857445788869,
54.985480589607,55.9852166003271,56.9849526110472,57.6675228581313),
 .UNSPECIFIED.);
#1138=B_SPLINE_CURVE_WITH_KNOTS('',3,(#140895,#140896,#140897,#140898,#140899,
#140900,#140901,#140902,#140903,#140904),.UNSPECIFIED.,.F.,.F.,(4,1,1,1,
1,1,1,4),(57.6675228581313,57.9846886217673,58.9844246324875,59.9841606432076,
60.9838966539278,61.983632664648,62.9833686753681,63.9507037176747),
 .UNSPECIFIED.);
#1139=B_SPLINE_CURVE_WITH_KNOTS('',3,(#140906,#140907,#140908,#140909,#140910,
#140911,#140912,#140913,#140914,#140915,#140916,#140917,#140918,#140919,
#140920,#140921,#140922,#140923,#140924,#140925,#140926,#140927,#140928,
#140929,#140930,#140931,#140932,#140933,#140934,#140935,#140936,#140937,
#140938,#140939,#140940,#140941,#140942,#140943,#140944,#140945,#140946,
#140947,#140948,#140949,#140950,#140951,#140952,#140953,#140954,#140955,
#140956,#140957,#140958,#140959,#140960,#140961,#140962,#140963,#140964,
#140965,#140966,#140967,#140968,#140969,#140970,#140971,#140972,#140973,
#140974,#140975,#140976,#140977,#140978,#140979,#140980,#140981,#140982,
#140983,#140984,#140985,#140986,#140987,#140988,#140989,#140990,#140991,
#140992,#140993,#140994,#140995,#140996,#140997,#140998,#140999,#141000,
#141001,#141002,#141003,#141004,#141005,#141006,#141007,#141008,#141009,
#141010,#141011,#141012,#141013,#141014,#141015,#141016,#141017,#141018,
#141019,#141020,#141021,#141022,#141023,#141024,#141025,#141026,#141027,
#141028,#141029,#141030,#141031,#141032,#141033,#141034,#141035,#141036,
#141037,#141038,#141039,#141040,#141041,#141042,#141043,#141044,#141045,
#141046,#141047,#141048,#141049,#141050,#141051,#141052,#141053,#141054,
#141055,#141056,#141057,#141058,#141059,#141060,#141061,#141062,#141063,
#141064,#141065,#141066,#141067,#141068,#141069,#141070,#141071,#141072,
#141073,#141074,#141075,#141076,#141077,#141078,#141079,#141080,#141081,
#141082,#141083,#141084,#141085,#141086,#141087,#141088,#141089,#141090,
#141091,#141092,#141093,#141094,#141095,#141096,#141097,#141098,#141099,
#141100,#141101,#141102,#141103,#141104,#141105,#141106,#141107,#141108,
#141109,#141110,#141111,#141112,#141113,#141114,#141115,#141116,#141117,
#141118,#141119,#141120,#141121,#141122,#141123,#141124,#141125,#141126,
#141127,#141128,#141129,#141130,#141131,#141132,#141133,#141134,#141135,
#141136,#141137,#141138,#141139,#141140,#141141,#141142,#141143,#141144,
#141145,#141146,#141147,#141148,#141149,#141150,#141151,#141152),
 .UNSPECIFIED.,.F.,.F.,(4,3,3,3,3,3,3,3,3,3,3,3,3,3,3,3,3,3,3,3,3,3,3,3,
3,3,3,3,3,3,3,3,3,3,3,3,3,3,3,3,3,3,3,3,3,3,3,3,3,3,3,3,3,3,3,3,3,3,3,3,
3,3,3,3,3,3,3,3,3,3,3,3,3,3,3,3,3,3,3,3,3,3,4),(63.9507081653109,63.9831046860883,
64.0630619862195,64.142924783462,64.2227106059338,64.3024369211289,64.382121149423,
64.4617921356438,64.5414595891696,64.621139239986,64.7008468223806,64.7806420514561,
64.8604863931635,64.9404448202108,64.9828406968084,65.0627979969396,65.1426607941822,
65.2224466166541,65.3021729318493,65.3818571601433,65.4615281463642,65.5411955998901,
65.6208752507066,65.7005828331011,65.7803780621766,65.8602224038843,65.9401808309317,
65.9825767075286,66.0625340076599,66.1423968049025,66.2221826273744,66.3019089425698,
66.381593170864,66.461264157085,66.540931610611,66.6206112614275,66.7003188438221,
66.7801140728977,66.8599584146054,66.9399168416528,66.9823127182487,67.0622700183799,
67.1421328156224,67.2219186380942,67.3016449532894,67.3813291815834,67.4610001678043,
67.5406676213301,67.6203472721465,67.700054854541,67.7798500836165,67.8596944253241,
67.9396528523714,67.9820487289688,68.0620060291001,68.1418688263428,68.2216546488147,
68.30138096401,68.381065192304,68.460736178525,68.540403632051,68.6200832828675,
68.6997908652621,68.7795860943376,68.8594304360453,68.9393888630927,68.9817847396889,
69.0617420398201,69.1416048370627,69.2213906595346,69.3011169747299,69.3808012030239,
69.4604721892448,69.5401396427707,69.6198192935872,69.6995268759819,69.7793221050574,
69.8591664467649,69.9391248738123,69.981520750409,70.0859426319418,70.1882149143938,
70.2338934108873),.UNSPECIFIED.);
#1140=B_SPLINE_CURVE_WITH_KNOTS('',3,(#141154,#141155,#141156,#141157,#141158,
#141159,#141160,#141161,#141162,#141163),.UNSPECIFIED.,.F.,.F.,(4,1,1,1,
1,1,1,4),(70.2338934724905,70.9812567611292,71.9809927718493,72.9807287825695,
73.9804647932896,74.9802008040097,75.9799368147299,76.5170787796701),
 .UNSPECIFIED.);
#1141=B_SPLINE_CURVE_WITH_KNOTS('',3,(#141165,#141166,#141167,#141168,#141169,
#141170,#141171,#141172,#141173,#141174,#141175,#141176,#141177,#141178,
#141179,#141180,#141181,#141182,#141183,#141184,#141185,#141186,#141187,
#141188,#141189,#141190,#141191,#141192,#141193,#141194,#141195,#141196,
#141197,#141198,#141199,#141200,#141201,#141202,#141203,#141204,#141205,
#141206,#141207,#141208,#141209,#141210,#141211,#141212,#141213,#141214,
#141215,#141216,#141217,#141218,#141219,#141220,#141221,#141222,#141223,
#141224,#141225,#141226,#141227,#141228,#141229,#141230,#141231,#141232,
#141233,#141234,#141235,#141236,#141237,#141238,#141239,#141240,#141241,
#141242,#141243,#141244,#141245,#141246,#141247,#141248,#141249,#141250,
#141251,#141252,#141253,#141254,#141255,#141256,#141257,#141258,#141259,
#141260,#141261,#141262,#141263,#141264,#141265,#141266,#141267,#141268,
#141269,#141270,#141271,#141272,#141273,#141274,#141275,#141276,#141277,
#141278,#141279,#141280,#141281,#141282,#141283,#141284,#141285,#141286,
#141287,#141288,#141289,#141290,#141291,#141292,#141293,#141294,#141295,
#141296,#141297,#141298,#141299,#141300,#141301,#141302,#141303,#141304,
#141305,#141306,#141307,#141308,#141309,#141310,#141311,#141312,#141313,
#141314,#141315,#141316,#141317,#141318,#141319,#141320,#141321,#141322,
#141323,#141324,#141325,#141326,#141327,#141328,#141329,#141330,#141331,
#141332,#141333,#141334,#141335,#141336,#141337,#141338,#141339,#141340,
#141341,#141342,#141343,#141344,#141345,#141346,#141347,#141348,#141349,
#141350,#141351,#141352,#141353,#141354,#141355,#141356,#141357,#141358,
#141359,#141360,#141361,#141362,#141363,#141364,#141365,#141366,#141367,
#141368,#141369,#141370,#141371,#141372,#141373,#141374,#141375,#141376,
#141377,#141378,#141379,#141380,#141381,#141382,#141383,#141384,#141385,
#141386,#141387,#141388,#141389,#141390,#141391,#141392,#141393,#141394,
#141395,#141396,#141397,#141398,#141399,#141400,#141401,#141402,#141403,
#141404,#141405,#141406,#141407,#141408,#141409,#141410,#141411),
 .UNSPECIFIED.,.F.,.F.,(4,3,3,3,3,3,3,3,3,3,3,3,3,3,3,3,3,3,3,3,3,3,3,3,
3,3,3,3,3,3,3,3,3,3,3,3,3,3,3,3,3,3,3,3,3,3,3,3,3,3,3,3,3,3,3,3,3,3,3,3,
3,3,3,3,3,3,3,3,3,3,3,3,3,3,3,3,3,3,3,3,3,3,4),(76.5170789829915,76.6019516902264,
76.6869832338072,76.7722619244241,76.8576735508233,76.9432918856119,76.97967282545,
77.0596301255811,77.1394929228235,77.2192787452951,77.2990050604903,77.3786892887841,
77.4583602750048,77.5380277285305,77.6177073793468,77.6974149617411,77.7772101908165,
77.8570545325239,77.9370129595711,77.9794088361701,78.0593661363013,78.1392289335439,
78.2190147560157,78.298741071211,78.3784252995052,78.4580962857261,78.537763739252,
78.6174433900685,78.6971509724629,78.7769462015385,78.8567905432461,78.9367489702935,
78.9791448468902,79.0591021470215,79.1389649442642,79.2187507667361,79.2984770819315,
79.3781613102257,79.4578322964467,79.5374997499727,79.6171794007892,79.6968869831838,
79.7766822122594,79.8565265539671,79.9364849810146,79.9788808576104,80.0588381577416,
80.1387009549841,80.2184867774559,80.2982130926512,80.3778973209452,80.4575683071661,
80.537235760692,80.6169154115085,80.696622993903,80.7764182229785,80.856262564686,
80.9362209917334,80.9786168683304,81.0585741684617,81.1384369657043,81.2182227881762,
81.2979491033716,81.3776333316657,81.4573043178867,81.5369717714127,81.6166514222292,
81.6963590046238,81.7761542336994,81.8559985754071,81.9359570024545,81.9783528790506,
82.0571196435331,82.1357922323713,82.2143891387368,82.2929249535672,82.37142792239,
82.4499146286459,82.5284016410875,82.6069360191478,82.6854971762447,82.764138078185,
82.8002640868496),.UNSPECIFIED.);
#1142=B_SPLINE_CURVE_WITH_KNOTS('',3,(#141413,#141414,#141415,#141416,#141417,
#141418,#141419,#141420,#141421,#141422,#141423),.UNSPECIFIED.,.F.,.F.,
(4,1,1,1,1,1,1,1,4),(82.8002640868496,82.9780888897707,83.9778249004908,
84.977560911211,85.9772969219311,86.9770329326513,87.9767689433714,88.9765049540916,
89.0834493940292),.UNSPECIFIED.);
#1143=B_SPLINE_CURVE_WITH_KNOTS('',3,(#141425,#141426,#141427,#141428,#141429,
#141430,#141431,#141432,#141433,#141434),.UNSPECIFIED.,.F.,.F.,(4,1,1,1,
1,1,1,4),(89.0834493940292,89.9762409648117,90.9759769755319,91.975712986252,
92.9754489969721,93.9751850076922,94.9749210184123,95.3666347012089),
 .UNSPECIFIED.);
#1144=B_SPLINE_CURVE_WITH_KNOTS('',3,(#141436,#141437,#141438,#141439,#141440,
#141441,#141442,#141443,#141444,#141445),.UNSPECIFIED.,.F.,.F.,(4,1,1,1,
1,1,1,4),(95.3666347012089,95.9746570291324,96.9743930398526,97.9741290505727,
98.9738650612928,99.973601072013,100.973337082733,101.649820008388),
 .UNSPECIFIED.);
#1145=B_SPLINE_CURVE_WITH_KNOTS('',3,(#141447,#141448,#141449,#141450,#141451,
#141452,#141453,#141454,#141455,#141456),.UNSPECIFIED.,.F.,.F.,(4,1,1,1,
1,1,1,4),(101.649820008388,101.973073093453,102.972809104173,103.972545114893,
104.972281125613,105.972017136334,106.971753147054,107.93300001923),
 .UNSPECIFIED.);
#1146=B_SPLINE_CURVE_WITH_KNOTS('',3,(#141458,#141459,#141460,#141461,#141462,
#141463,#141464,#141465,#141466,#141467,#141468,#141469,#141470,#141471,
#141472,#141473,#141474,#141475,#141476,#141477,#141478,#141479,#141480,
#141481,#141482,#141483,#141484,#141485,#141486,#141487,#141488,#141489,
#141490,#141491,#141492,#141493,#141494,#141495,#141496,#141497,#141498,
#141499,#141500,#141501,#141502,#141503,#141504,#141505,#141506,#141507,
#141508,#141509,#141510,#141511,#141512,#141513,#141514,#141515,#141516,
#141517,#141518,#141519,#141520,#141521,#141522,#141523,#141524,#141525,
#141526,#141527,#141528,#141529,#141530,#141531,#141532,#141533,#141534,
#141535,#141536,#141537,#141538,#141539,#141540,#141541,#141542,#141543,
#141544,#141545,#141546,#141547,#141548,#141549,#141550,#141551,#141552,
#141553,#141554,#141555,#141556,#141557,#141558,#141559,#141560,#141561,
#141562,#141563,#141564,#141565,#141566,#141567,#141568,#141569,#141570,
#141571,#141572,#141573,#141574,#141575,#141576,#141577,#141578,#141579,
#141580,#141581,#141582,#141583,#141584,#141585,#141586,#141587,#141588,
#141589,#141590,#141591,#141592,#141593,#141594,#141595,#141596,#141597,
#141598,#141599,#141600,#141601,#141602,#141603,#141604,#141605,#141606,
#141607,#141608,#141609,#141610,#141611,#141612,#141613,#141614,#141615,
#141616,#141617,#141618,#141619,#141620,#141621,#141622,#141623,#141624,
#141625,#141626,#141627,#141628,#141629,#141630,#141631,#141632,#141633,
#141634,#141635,#141636,#141637,#141638,#141639,#141640,#141641,#141642,
#141643,#141644,#141645,#141646,#141647,#141648,#141649,#141650,#141651,
#141652,#141653,#141654,#141655,#141656,#141657,#141658,#141659,#141660,
#141661,#141662,#141663,#141664,#141665,#141666,#141667,#141668,#141669,
#141670,#141671,#141672,#141673,#141674,#141675,#141676,#141677,#141678,
#141679,#141680,#141681,#141682,#141683,#141684,#141685,#141686,#141687,
#141688,#141689,#141690,#141691,#141692,#141693,#141694,#141695,#141696,
#141697,#141698,#141699,#141700,#141701,#141702,#141703,#141704),
 .UNSPECIFIED.,.F.,.F.,(4,3,3,3,3,3,3,3,3,3,3,3,3,3,3,3,3,3,3,3,3,3,3,3,
3,3,3,3,3,3,3,3,3,3,3,3,3,3,3,3,3,3,3,3,3,3,3,3,3,3,3,3,3,3,3,3,3,3,3,3,
3,3,3,3,3,3,3,3,3,3,3,3,3,3,3,3,3,3,3,3,3,3,4),(107.933005315568,107.971489157774,
108.051446457905,108.131309255148,108.21109507762,108.290821392815,108.370505621109,
108.45017660733,108.529844060856,108.609523711672,108.689231294067,108.769026523142,
108.84887086485,108.928829291897,108.971225168494,109.051182468625,109.131045265868,
109.21083108834,109.290557403535,109.370241631829,109.44991261805,109.529580071576,
109.609259722392,109.688967304787,109.768762533862,109.84860687557,109.928565302617,
109.970961179214,110.050918479345,110.130781276588,110.21056709906,110.290293414255,
110.369977642549,110.44964862877,110.529316082296,110.608995733112,110.688703315507,
110.768498544582,110.84834288629,110.928301313337,110.970697189934,111.050654490065,
111.130517287308,111.210303109779,111.290029424975,111.369713653269,111.449384639489,
111.529052093015,111.608731743832,111.688439326226,111.768234555301,111.848078897009,
111.928037324056,111.970433200654,112.050390500785,112.130253298028,112.2100391205,
112.289765435696,112.36944966399,112.449120650211,112.528788103737,112.608467754554,
112.688175336949,112.767970566025,112.847814907733,112.92777333478,112.970169211375,
113.050126511506,113.129989308749,113.209775131221,113.289501446416,113.36918567471,
113.448856660931,113.528524114457,113.608203765274,113.687911347668,113.767706576744,
113.847550918451,113.927509345499,113.969905222095,114.075449330656,114.17864104367,
114.216190536642),.UNSPECIFIED.);
#1147=B_SPLINE_CURVE_WITH_KNOTS('',3,(#141706,#141707,#141708,#141709,#141710,
#141711,#141712,#141713,#141714,#141715),.UNSPECIFIED.,.F.,.F.,(4,1,1,1,
1,1,1,4),(114.216190622748,114.969641232815,115.969377243535,116.969113254255,
117.968849264975,118.968585275695,119.968321286416,120.499375929927),
 .UNSPECIFIED.);
#1148=B_SPLINE_CURVE_WITH_KNOTS('',3,(#141717,#141718,#141719,#141720,#141721,
#141722,#141723,#141724,#141725,#141726),.UNSPECIFIED.,.F.,.F.,(4,1,1,1,
1,1,1,4),(120.499375929927,120.968057297136,121.967793307856,122.967529318576,
123.967265329296,124.967001340016,125.966737350736,126.782556444121),
 .UNSPECIFIED.);
#1149=B_SPLINE_CURVE_WITH_KNOTS('',3,(#141728,#141729,#141730,#141731,#141732,
#141733,#141734,#141735,#141736,#141737,#141738,#141739,#141740,#141741,
#141742,#141743,#141744,#141745,#141746,#141747,#141748,#141749,#141750,
#141751,#141752,#141753,#141754,#141755,#141756,#141757,#141758,#141759,
#141760,#141761,#141762,#141763,#141764,#141765,#141766,#141767,#141768,
#141769,#141770,#141771,#141772,#141773,#141774,#141775,#141776,#141777,
#141778,#141779,#141780,#141781,#141782,#141783,#141784,#141785,#141786,
#141787,#141788,#141789,#141790,#141791,#141792,#141793,#141794,#141795,
#141796,#141797,#141798,#141799,#141800,#141801,#141802,#141803,#141804,
#141805,#141806,#141807,#141808,#141809,#141810,#141811,#141812,#141813,
#141814,#141815,#141816,#141817,#141818,#141819,#141820,#141821,#141822,
#141823,#141824,#141825,#141826,#141827,#141828,#141829,#141830,#141831,
#141832,#141833,#141834,#141835,#141836,#141837,#141838,#141839,#141840,
#141841,#141842,#141843,#141844,#141845,#141846,#141847,#141848,#141849,
#141850,#141851,#141852,#141853,#141854,#141855,#141856,#141857,#141858,
#141859,#141860,#141861,#141862,#141863,#141864,#141865,#141866,#141867,
#141868,#141869,#141870,#141871,#141872,#141873,#141874,#141875,#141876,
#141877,#141878,#141879,#141880,#141881,#141882,#141883,#141884,#141885,
#141886,#141887,#141888,#141889,#141890,#141891,#141892,#141893,#141894,
#141895,#141896,#141897,#141898,#141899,#141900,#141901,#141902,#141903,
#141904,#141905,#141906,#141907,#141908,#141909,#141910,#141911,#141912,
#141913,#141914,#141915,#141916,#141917,#141918,#141919,#141920,#141921,
#141922,#141923,#141924,#141925,#141926,#141927,#141928,#141929,#141930,
#141931,#141932,#141933,#141934,#141935,#141936,#141937,#141938,#141939,
#141940,#141941,#141942,#141943,#141944,#141945,#141946,#141947,#141948,
#141949,#141950,#141951,#141952,#141953,#141954,#141955,#141956,#141957,
#141958,#141959,#141960,#141961,#141962,#141963,#141964,#141965,#141966,
#141967,#141968,#141969,#141970,#141971),.UNSPECIFIED.,.F.,.F.,(4,3,3,3,
3,3,3,3,3,3,3,3,3,3,3,3,3,3,3,3,3,3,3,3,3,3,3,3,3,3,3,3,3,3,3,3,3,3,3,3,
3,3,3,3,3,3,3,3,3,3,3,3,3,3,3,3,3,3,3,3,3,3,3,3,3,3,3,3,3,3,3,3,3,3,3,3,
3,3,3,3,3,4),(126.782561237107,126.902559628464,126.966473361456,127.046430661588,
127.126293458831,127.206079281303,127.285805596499,127.365489824793,127.445160811014,
127.524828264541,127.604507915357,127.684215497752,127.764010726828,127.843855068536,
127.923813495584,127.966209372176,128.046166672307,128.12602946955,128.205815292022,
128.285541607217,128.365225835512,128.444896821733,128.524564275259,128.604243926075,
128.68395150847,128.763746737546,128.843591079253,128.923549506301,128.965945382897,
129.045902683028,129.125765480271,129.205551302743,129.285277617938,129.364961846232,
129.444632832453,129.524300285979,129.603979936795,129.68368751919,129.763482748265,
129.843327089973,129.92328551702,129.965681393617,130.045638693748,130.125501490991,
130.205287313463,130.285013628658,130.364697856952,130.444368843173,130.524036296699,
130.603715947515,130.68342352991,130.763218758985,130.843063100693,130.92302152774,
130.965417404337,131.045374704468,131.125237501711,131.205023324183,131.284749639378,
131.364433867672,131.444104853893,131.523772307419,131.603451958235,131.68315954063,
131.762954769705,131.842799111413,131.92275753846,131.965153415057,132.045110715188,
132.124973512431,132.204759334903,132.284485650098,132.364169878393,132.443840864614,
132.52350831814,132.603187968956,132.682895551351,132.762690780427,132.842535122134,
132.922493549182,132.964889425777,133.065746544286),.UNSPECIFIED.);
#1150=B_SPLINE_CURVE_WITH_KNOTS('',3,(#141973,#141974,#141975,#141976,#141977,
#141978,#141979,#141980,#141981,#141982),.UNSPECIFIED.,.F.,.F.,(4,1,1,1,
1,1,1,4),(133.065755642825,133.964625436497,134.964361447218,135.964097457938,
136.963833468658,137.963569479378,138.963305490098,139.34892440658),
 .UNSPECIFIED.);
#1151=B_SPLINE_CURVE_WITH_KNOTS('',3,(#141984,#141985,#141986,#141987,#141988,
#141989,#141990,#141991,#141992,#141993,#141994,#141995,#141996,#141997,
#141998,#141999,#142000,#142001,#142002,#142003,#142004,#142005,#142006,
#142007,#142008,#142009,#142010,#142011,#142012,#142013,#142014,#142015,
#142016,#142017,#142018,#142019,#142020,#142021,#142022,#142023,#142024,
#142025,#142026,#142027,#142028,#142029,#142030,#142031,#142032,#142033,
#142034,#142035,#142036,#142037,#142038,#142039,#142040,#142041,#142042,
#142043,#142044,#142045,#142046,#142047,#142048,#142049,#142050,#142051,
#142052,#142053,#142054,#142055,#142056,#142057,#142058,#142059,#142060,
#142061,#142062,#142063,#142064,#142065,#142066,#142067,#142068,#142069,
#142070,#142071,#142072,#142073,#142074,#142075,#142076,#142077,#142078,
#142079,#142080,#142081,#142082,#142083,#142084,#142085,#142086,#142087,
#142088,#142089,#142090,#142091,#142092,#142093,#142094,#142095,#142096,
#142097,#142098,#142099,#142100,#142101,#142102,#142103,#142104,#142105,
#142106,#142107,#142108,#142109,#142110,#142111,#142112,#142113,#142114,
#142115,#142116,#142117,#142118,#142119,#142120,#142121,#142122,#142123,
#142124,#142125,#142126,#142127,#142128,#142129,#142130,#142131,#142132,
#142133,#142134,#142135,#142136,#142137,#142138,#142139,#142140,#142141,
#142142,#142143,#142144,#142145,#142146,#142147,#142148,#142149,#142150,
#142151,#142152,#142153,#142154,#142155,#142156,#142157,#142158,#142159,
#142160,#142161,#142162,#142163,#142164,#142165,#142166,#142167,#142168,
#142169,#142170,#142171,#142172,#142173,#142174,#142175,#142176,#142177,
#142178,#142179,#142180,#142181,#142182,#142183,#142184,#142185,#142186,
#142187,#142188,#142189,#142190,#142191,#142192,#142193,#142194,#142195,
#142196,#142197,#142198,#142199,#142200,#142201,#142202,#142203,#142204,
#142205,#142206,#142207,#142208,#142209,#142210,#142211,#142212,#142213,
#142214,#142215,#142216,#142217,#142218,#142219,#142220,#142221,#142222,
#142223,#142224,#142225,#142226,#142227,#142228,#142229,#142230),
 .UNSPECIFIED.,.F.,.F.,(4,3,3,3,3,3,3,3,3,3,3,3,3,3,3,3,3,3,3,3,3,3,3,3,
3,3,3,3,3,3,3,3,3,3,3,3,3,3,3,3,3,3,3,3,3,3,3,3,3,3,3,3,3,3,3,3,3,3,3,3,
3,3,3,3,3,3,3,3,3,3,3,3,3,3,3,3,3,3,3,3,3,3,4),(139.348931851466,139.429394985958,
139.509870031329,139.590371667878,139.670914589187,139.751564232921,139.832272604219,
139.913111307842,139.963041500818,140.042998800949,140.122861598192,140.202647420663,
140.282373735859,140.362057964153,140.441728950374,140.521396403899,140.601076054716,
140.68078363711,140.760578866186,140.840423207893,140.92038163494,140.962777511538,
141.042734811669,141.122597608912,141.202383431384,141.282109746579,141.361793974873,
141.441464961094,141.52113241462,141.600812065436,141.680519647831,141.760314876907,
141.840159218614,141.920117645662,141.962513522258,142.042470822389,142.122333619632,
142.202119442103,142.281845757298,142.361529985591,142.441200971812,142.520868425338,
142.600548076154,142.680255658548,142.760050887624,142.839895229331,142.919853656379,
142.962249532978,143.04220683311,143.122069630352,143.201855452824,143.28158176802,
143.361265996314,143.440936982535,143.520604436061,143.600284086878,143.679991669273,
143.759786898348,143.839631240056,143.919589667104,143.961985543699,144.04194284383,
144.121805641073,144.201591463546,144.281317778741,144.361002007036,144.440672993257,
144.520340446783,144.6000200976,144.679727679994,144.75952290907,144.839367250778,
144.919325677825,144.961721554419,145.045521004947,145.125273005645,145.204950022292,
145.284567928792,145.364142558629,145.443696576801,145.523238805001,145.602799540725,
145.632117158645),.UNSPECIFIED.);
#1152=B_SPLINE_CURVE_WITH_KNOTS('',3,(#142232,#142233,#142234,#142235,#142236,
#142237,#142238,#142239,#142240,#142241),.UNSPECIFIED.,.F.,.F.,(4,1,1,1,
1,1,1,4),(145.632124439118,145.961457565139,146.961193575859,147.960929586579,
148.960665597299,149.960401608019,150.960137618739,151.915296521168),
 .UNSPECIFIED.);
#1153=B_SPLINE_CURVE_WITH_KNOTS('',3,(#142243,#142244,#142245,#142246,#142247,
#142248,#142249,#142250,#142251,#142252,#142253,#142254,#142255,#142256,
#142257,#142258,#142259,#142260,#142261,#142262,#142263,#142264,#142265,
#142266,#142267,#142268,#142269,#142270,#142271,#142272,#142273,#142274,
#142275,#142276,#142277,#142278,#142279,#142280,#142281,#142282,#142283,
#142284,#142285,#142286,#142287,#142288,#142289,#142290,#142291,#142292,
#142293,#142294,#142295,#142296,#142297,#142298,#142299,#142300,#142301,
#142302,#142303,#142304,#142305,#142306,#142307,#142308,#142309,#142310,
#142311,#142312,#142313,#142314,#142315,#142316,#142317,#142318,#142319,
#142320,#142321,#142322,#142323,#142324,#142325,#142326,#142327,#142328,
#142329,#142330,#142331,#142332,#142333,#142334,#142335,#142336,#142337,
#142338,#142339,#142340,#142341,#142342,#142343,#142344,#142345,#142346,
#142347,#142348,#142349,#142350,#142351,#142352,#142353,#142354,#142355,
#142356,#142357,#142358,#142359,#142360,#142361,#142362,#142363,#142364,
#142365,#142366,#142367,#142368,#142369,#142370,#142371,#142372,#142373,
#142374,#142375,#142376,#142377,#142378,#142379,#142380,#142381,#142382,
#142383,#142384,#142385,#142386,#142387,#142388,#142389,#142390,#142391,
#142392,#142393,#142394,#142395,#142396,#142397,#142398,#142399,#142400,
#142401,#142402,#142403,#142404,#142405,#142406,#142407,#142408,#142409,
#142410,#142411,#142412,#142413,#142414,#142415,#142416,#142417,#142418,
#142419,#142420,#142421,#142422,#142423,#142424,#142425,#142426,#142427,
#142428,#142429,#142430,#142431,#142432,#142433,#142434,#142435,#142436,
#142437,#142438,#142439,#142440,#142441,#142442,#142443,#142444,#142445,
#142446,#142447,#142448,#142449,#142450,#142451,#142452,#142453,#142454,
#142455,#142456,#142457,#142458,#142459,#142460,#142461,#142462,#142463,
#142464,#142465,#142466,#142467,#142468,#142469,#142470,#142471,#142472,
#142473,#142474,#142475,#142476,#142477,#142478,#142479,#142480,#142481,
#142482,#142483,#142484,#142485,#142486,#142487,#142488,#142489),
 .UNSPECIFIED.,.F.,.F.,(4,3,3,3,3,3,3,3,3,3,3,3,3,3,3,3,3,3,3,3,3,3,3,3,
3,3,3,3,3,3,3,3,3,3,3,3,3,3,3,3,3,3,3,3,3,3,3,3,3,3,3,3,3,3,3,3,3,3,3,3,
3,3,3,3,3,3,3,3,3,3,3,3,3,3,3,3,3,3,3,3,3,3,4),(151.915302465825,151.95987362946,
152.039830929591,152.119693726834,152.199479549306,152.279205864501,152.358890092795,
152.438561079015,152.518228532541,152.597908183358,152.677615765752,152.757410994827,
152.837255336535,152.917213763582,152.95960964018,153.039566940311,153.119429737554,
153.199215560026,153.278941875221,153.358626103515,153.438297089736,153.517964543262,
153.597644194079,153.677351776473,153.757147005549,153.836991347256,153.916949774304,
153.9593456509,154.039302951031,154.119165748274,154.198951570746,154.278677885941,
154.358362114235,154.438033100456,154.517700553982,154.597380204798,154.677087787193,
154.756883016268,154.836727357976,154.916685785023,154.95908166162,155.039038961751,
155.118901758994,155.198687581466,155.278413896661,155.358098124955,155.437769111176,
155.517436564702,155.597116215519,155.676823797913,155.756619026989,155.836463368696,
155.916421795744,155.95881767234,156.038774972471,156.118637769714,156.198423592186,
156.278149907381,156.357834135675,156.437505121896,156.517172575422,156.596852226238,
156.676559808633,156.756355037708,156.836199379416,156.916157806463,156.95855368306,
157.038510983191,157.118373780434,157.198159602905,157.2778859181,157.357570146394,
157.437241132615,157.516908586141,157.596588236957,157.676295819352,157.756091048427,
157.835935390135,157.915893817182,157.95828969378,158.065027953602,158.16918115264,
158.198487725055),.UNSPECIFIED.);
#1154=B_SPLINE_CURVE_WITH_KNOTS('',3,(#142491,#142492,#142493,#142494,#142495,
#142496,#142497,#142498,#142499,#142500),.UNSPECIFIED.,.F.,.F.,(4,1,1,1,
1,1,1,4),(158.198487773005,158.958025704501,159.957761715221,160.957497725941,
161.957233736661,162.956969747381,163.956705758101,164.481673080184),
 .UNSPECIFIED.);
#1155=B_SPLINE_CURVE_WITH_KNOTS('',3,(#142502,#142503,#142504,#142505,#142506,
#142507,#142508,#142509,#142510,#142511),.UNSPECIFIED.,.F.,.F.,(4,1,1,1,
1,1,1,4),(164.481673080184,164.956441768821,165.956177779541,166.955913790262,
167.955649800982,168.955385811702,169.955121822422,170.76485415669),
 .UNSPECIFIED.);
#1156=B_SPLINE_CURVE_WITH_KNOTS('',3,(#142513,#142514,#142515,#142516,#142517,
#142518,#142519,#142520,#142521,#142522,#142523,#142524,#142525,#142526,
#142527,#142528,#142529,#142530,#142531,#142532,#142533,#142534,#142535,
#142536,#142537,#142538,#142539,#142540,#142541,#142542,#142543,#142544,
#142545,#142546,#142547,#142548,#142549,#142550,#142551,#142552,#142553,
#142554,#142555,#142556,#142557,#142558,#142559,#142560,#142561,#142562,
#142563,#142564,#142565,#142566,#142567,#142568,#142569,#142570,#142571,
#142572,#142573,#142574,#142575,#142576,#142577,#142578,#142579,#142580,
#142581,#142582,#142583,#142584,#142585,#142586,#142587,#142588,#142589,
#142590,#142591,#142592,#142593,#142594,#142595,#142596,#142597,#142598,
#142599,#142600,#142601,#142602,#142603,#142604,#142605,#142606,#142607,
#142608,#142609,#142610,#142611,#142612,#142613,#142614,#142615,#142616,
#142617,#142618,#142619,#142620,#142621,#142622,#142623,#142624,#142625,
#142626,#142627,#142628,#142629,#142630,#142631,#142632,#142633,#142634,
#142635,#142636,#142637,#142638,#142639,#142640,#142641,#142642,#142643,
#142644,#142645,#142646,#142647,#142648,#142649,#142650,#142651,#142652,
#142653,#142654,#142655,#142656,#142657,#142658,#142659,#142660,#142661,
#142662,#142663,#142664,#142665,#142666,#142667,#142668,#142669,#142670,
#142671,#142672,#142673,#142674,#142675,#142676,#142677,#142678,#142679,
#142680,#142681,#142682,#142683,#142684,#142685,#142686,#142687,#142688,
#142689,#142690,#142691,#142692,#142693,#142694,#142695,#142696,#142697,
#142698,#142699,#142700,#142701,#142702,#142703,#142704,#142705,#142706,
#142707,#142708,#142709,#142710,#142711,#142712,#142713,#142714,#142715,
#142716,#142717,#142718,#142719,#142720,#142721,#142722,#142723,#142724,
#142725,#142726,#142727,#142728,#142729,#142730,#142731,#142732,#142733,
#142734,#142735,#142736,#142737,#142738,#142739,#142740,#142741,#142742,
#142743,#142744,#142745,#142746,#142747,#142748,#142749,#142750,#142751,
#142752,#142753,#142754,#142755,#142756),.UNSPECIFIED.,.F.,.F.,(4,3,3,3,
3,3,3,3,3,3,3,3,3,3,3,3,3,3,3,3,3,3,3,3,3,3,3,3,3,3,3,3,3,3,3,3,3,3,3,3,
3,3,3,3,3,3,3,3,3,3,3,3,3,3,3,3,3,3,3,3,3,3,3,3,3,3,3,3,3,3,3,3,3,3,3,3,
3,3,3,3,3,4),(170.764858387364,170.882744850471,170.954857833142,171.034815133274,
171.114677930517,171.194463752989,171.274190068185,171.353874296479,171.433545282701,
171.513212736227,171.592892387044,171.672599969439,171.752395198515,171.832239540223,
171.912197967271,171.954593843862,172.034551143993,172.114413941236,172.194199763708,
172.273926078903,172.353610307197,172.433281293418,172.512948746943,172.59262839776,
172.672335980154,172.75213120923,172.831975550937,172.911933977985,172.954329854582,
173.034287154713,173.114149951956,173.193935774427,173.273662089622,173.353346317916,
173.433017304137,173.512684757663,173.592364408479,173.672071990873,173.751867219949,
173.831711561656,173.911669988704,173.954065865302,174.034023165433,174.113885962676,
174.193671785148,174.273398100344,174.353082328638,174.432753314859,174.512420768386,
174.592100419202,174.671808001597,174.751603230673,174.831447572381,174.911405999428,
174.953801876023,175.033759176154,175.113621973397,175.193407795869,175.273134111064,
175.352818339358,175.432489325579,175.512156779105,175.591836429922,175.671544012316,
175.751339241392,175.8311835831,175.911142010147,175.953537886743,176.033495186874,
176.113357984117,176.193143806589,176.272870121784,176.352554350078,176.432225336299,
176.511892789825,176.591572440641,176.671280023036,176.751075252111,176.830919593819,
176.910878020866,176.953273897463,177.048043694543),.UNSPECIFIED.);
#1157=B_SPLINE_CURVE_WITH_KNOTS('',3,(#142758,#142759,#142760,#142761,#142762,
#142763,#142764,#142765,#142766,#142767),.UNSPECIFIED.,.F.,.F.,(4,1,1,1,
1,1,1,4),(177.048052727997,177.953009908183,178.952745918903,179.952481929623,
180.952217940343,181.951953951063,182.951689961784,183.33122142995),
 .UNSPECIFIED.);
#1158=B_SPLINE_CURVE_WITH_KNOTS('',3,(#142769,#142770,#142771,#142772,#142773,
#142774,#142775,#142776,#142777,#142778,#142779,#142780,#142781,#142782,
#142783,#142784,#142785,#142786,#142787,#142788,#142789,#142790,#142791,
#142792,#142793,#142794,#142795,#142796,#142797,#142798,#142799,#142800,
#142801,#142802,#142803,#142804,#142805,#142806,#142807,#142808,#142809,
#142810,#142811,#142812,#142813,#142814,#142815,#142816,#142817,#142818,
#142819,#142820,#142821,#142822,#142823,#142824,#142825,#142826,#142827,
#142828,#142829,#142830,#142831,#142832,#142833,#142834,#142835,#142836,
#142837,#142838,#142839,#142840,#142841,#142842,#142843,#142844,#142845,
#142846,#142847,#142848,#142849,#142850,#142851,#142852,#142853,#142854,
#142855,#142856,#142857,#142858,#142859,#142860,#142861,#142862,#142863,
#142864,#142865,#142866,#142867,#142868,#142869,#142870,#142871,#142872,
#142873,#142874,#142875,#142876,#142877,#142878,#142879,#142880,#142881,
#142882,#142883,#142884,#142885,#142886,#142887,#142888,#142889,#142890,
#142891,#142892,#142893,#142894,#142895,#142896,#142897,#142898,#142899,
#142900,#142901,#142902,#142903,#142904,#142905,#142906,#142907,#142908,
#142909,#142910,#142911,#142912,#142913,#142914,#142915,#142916,#142917,
#142918,#142919,#142920,#142921,#142922,#142923,#142924,#142925,#142926,
#142927,#142928,#142929,#142930,#142931,#142932,#142933,#142934,#142935,
#142936,#142937,#142938,#142939,#142940,#142941,#142942,#142943,#142944,
#142945,#142946,#142947,#142948,#142949,#142950,#142951,#142952,#142953,
#142954,#142955,#142956,#142957,#142958,#142959,#142960,#142961,#142962,
#142963,#142964,#142965,#142966,#142967,#142968,#142969,#142970,#142971,
#142972,#142973,#142974,#142975,#142976,#142977,#142978,#142979,#142980,
#142981,#142982,#142983,#142984,#142985,#142986,#142987,#142988,#142989,
#142990,#142991,#142992,#142993,#142994,#142995,#142996,#142997,#142998,
#142999,#143000,#143001,#143002,#143003,#143004,#143005,#143006,#143007,
#143008,#143009,#143010,#143011,#143012,#143013,#143014,#143015),
 .UNSPECIFIED.,.F.,.F.,(4,3,3,3,3,3,3,3,3,3,3,3,3,3,3,3,3,3,3,3,3,3,3,3,
3,3,3,3,3,3,3,3,3,3,3,3,3,3,3,3,3,3,3,3,3,3,3,3,3,3,3,3,3,3,3,3,3,3,3,3,
3,3,3,3,3,3,3,3,3,3,3,3,3,3,3,3,3,3,3,3,3,3,4),(183.331229001723,183.411579138959,
183.49193796612,183.572320324641,183.65274106719,183.733266169438,183.81384773384,
183.894560468422,183.951425972504,184.031383272635,184.111246069878,184.191031892349,
184.270758207545,184.350442435838,184.430113422059,184.509780875585,184.589460526401,
184.669168108795,184.748963337871,184.828807679578,184.908766106625,184.951161983224,
185.031119283355,185.110982080598,185.190767903069,185.270494218265,185.350178446559,
185.42984943278,185.509516886306,185.589196537122,185.668904119517,185.748699348592,
185.8285436903,185.908502117347,185.950897993944,186.030855294075,186.110718091318,
186.190503913789,186.270230228985,186.349914457279,186.4295854435,186.509252897026,
186.588932547842,186.668640130237,186.748435359312,186.82827970102,186.908238128067,
186.950634004664,187.030591304795,187.110454102038,187.190239924509,187.269966239705,
187.349650467998,187.429321454219,187.508988907745,187.588668558562,187.668376140956,
187.748171370032,187.82801571174,187.907974138787,187.950370015384,188.030327315515,
188.110190112758,188.189975935229,188.269702250425,188.349386478719,188.42905746494,
188.508724918465,188.588404569282,188.668112151676,188.747907380752,188.82775172246,
188.907710149507,188.950106026104,189.033144561454,189.112986258176,189.192752007562,
189.272457603206,189.352118797911,189.431757014182,189.511382385588,189.591023092393,
189.614414308902),.UNSPECIFIED.);
#1159=B_SPLINE_CURVE_WITH_KNOTS('',3,(#143017,#143018,#143019,#143020,#143021,
#143022,#143023,#143024,#143025,#143026),.UNSPECIFIED.,.F.,.F.,(4,1,1,1,
1,1,1,4),(189.614421781537,189.949842036824,190.949578047545,191.949314058265,
192.949050068985,193.948786079705,194.948522090425,195.897599616082),
 .UNSPECIFIED.);
#1160=B_SPLINE_CURVE_WITH_KNOTS('',3,(#143028,#143029,#143030,#143031,#143032,
#143033,#143034,#143035,#143036,#143037,#143038,#143039),.UNSPECIFIED.,
 .F.,.F.,(4,2,1,1,1,1,1,1,4),(195.897599616082,195.948258101145,196.947994111865,
197.947730122585,198.947466133306,199.947202144026,200.946938154746,201.946674165466,
202.180784923262),.UNSPECIFIED.);
#1161=B_SPLINE_CURVE_WITH_KNOTS('',3,(#143041,#143042,#143043,#143044,#143045,
#143046,#143047,#143048,#143049,#143050),.UNSPECIFIED.,.F.,.F.,(4,1,1,1,
1,1,1,4),(202.180784923262,202.946410176186,203.946146186906,204.945882197626,
205.945618208347,206.945354219067,207.945090229787,208.463970230441),
 .UNSPECIFIED.);
#1162=B_SPLINE_CURVE_WITH_KNOTS('',3,(#143052,#143053,#143054,#143055,#143056,
#143057,#143058,#143059,#143060,#143061),.UNSPECIFIED.,.F.,.F.,(4,1,1,1,
1,1,1,4),(208.463970230441,208.944826240507,209.944562251227,210.944298261947,
211.944034272667,212.943770283387,213.943506294108,214.747151886774),
 .UNSPECIFIED.);
#1163=B_SPLINE_CURVE_WITH_KNOTS('',3,(#143063,#143064,#143065,#143066,#143067,
#143068,#143069,#143070,#143071,#143072,#143073,#143074,#143075,#143076,
#143077,#143078,#143079,#143080,#143081,#143082,#143083,#143084,#143085,
#143086,#143087,#143088,#143089,#143090,#143091,#143092,#143093,#143094,
#143095,#143096,#143097,#143098,#143099,#143100,#143101,#143102,#143103,
#143104,#143105,#143106,#143107,#143108,#143109,#143110,#143111,#143112,
#143113,#143114,#143115,#143116,#143117,#143118,#143119,#143120,#143121,
#143122,#143123,#143124,#143125,#143126,#143127,#143128,#143129,#143130,
#143131,#143132,#143133,#143134,#143135,#143136,#143137,#143138,#143139,
#143140,#143141,#143142,#143143,#143144,#143145,#143146,#143147,#143148,
#143149,#143150,#143151,#143152,#143153,#143154,#143155,#143156,#143157,
#143158,#143159,#143160,#143161,#143162,#143163,#143164,#143165,#143166,
#143167,#143168,#143169,#143170,#143171,#143172,#143173,#143174,#143175,
#143176,#143177,#143178,#143179,#143180,#143181,#143182,#143183,#143184,
#143185,#143186,#143187,#143188,#143189,#143190,#143191,#143192,#143193,
#143194,#143195,#143196,#143197,#143198,#143199,#143200,#143201,#143202,
#143203,#143204,#143205,#143206,#143207,#143208,#143209,#143210,#143211,
#143212,#143213,#143214,#143215,#143216,#143217,#143218,#143219,#143220,
#143221,#143222,#143223,#143224,#143225,#143226,#143227,#143228,#143229,
#143230,#143231,#143232,#143233,#143234,#143235,#143236,#143237,#143238,
#143239,#143240,#143241,#143242,#143243,#143244,#143245,#143246,#143247,
#143248,#143249,#143250,#143251,#143252,#143253,#143254,#143255,#143256,
#143257,#143258,#143259,#143260,#143261,#143262,#143263,#143264,#143265,
#143266,#143267,#143268,#143269,#143270,#143271,#143272,#143273,#143274,
#143275,#143276,#143277,#143278,#143279,#143280,#143281,#143282,#143283,
#143284,#143285,#143286,#143287,#143288,#143289,#143290,#143291,#143292,
#143293,#143294,#143295,#143296,#143297,#143298,#143299,#143300,#143301,
#143302,#143303,#143304,#143305,#143306),.UNSPECIFIED.,.F.,.F.,(4,3,3,3,
3,3,3,3,3,3,3,3,3,3,3,3,3,3,3,3,3,3,3,3,3,3,3,3,3,3,3,3,3,3,3,3,3,3,3,3,
3,3,3,3,3,3,3,3,3,3,3,3,3,3,3,3,3,3,3,3,3,3,3,3,3,3,3,3,3,3,3,3,3,3,3,3,
3,3,3,3,3,4),(214.747155537621,214.863097551269,214.943242304828,215.02319960496,
215.103062402203,215.182848224675,215.262574539871,215.342258768165,215.421929754386,
215.501597207913,215.581276858729,215.660984441124,215.7407796702,215.820624011908,
215.900582438956,215.942978315548,216.022935615679,216.102798412922,216.182584235393,
216.262310550589,216.341994778883,216.421665765104,216.501333218629,216.581012869446,
216.66072045184,216.740515680916,216.820360022623,216.900318449671,216.942714326268,
217.022671626399,217.102534423642,217.182320246114,217.262046561309,217.341730789603,
217.421401775824,217.50106922935,217.580748880166,217.660456462561,217.740251691636,
217.820096033344,217.900054460391,217.942450336988,218.022407637119,218.102270434362,
218.182056256834,218.261782572029,218.341466800323,218.421137786544,218.50080524007,
218.580484890887,218.660192473281,218.739987702357,218.819832044064,218.899790471112,
218.942186347708,219.022143647839,219.102006445082,219.181792267553,219.261518582749,
219.341202811043,219.420873797263,219.500541250789,219.580220901606,219.659928484,
219.739723713076,219.819568054783,219.89952648183,219.941922358428,220.02187965856,
220.101742455802,220.181528278274,220.26125459347,220.340938821764,220.420609807986,
220.500277261512,220.579956912329,220.659664494723,220.739459723799,220.819304065507,
220.899262492555,220.941658369149,221.0303408448),.UNSPECIFIED.);
#1164=B_SPLINE_CURVE_WITH_KNOTS('',3,(#143308,#143309,#143310,#143311,#143312,
#143313,#143314,#143315,#143316,#143317),.UNSPECIFIED.,.F.,.F.,(4,1,1,1,
1,1,1,4),(221.030349614055,221.941394379869,222.941130390589,223.940866401309,
224.940602412029,225.940338422749,226.940074433469,227.313518490426),
 .UNSPECIFIED.);
#1165=B_SPLINE_CURVE_WITH_KNOTS('',3,(#143319,#143320,#143321,#143322,#143323,
#143324,#143325,#143326,#143327,#143328,#143329,#143330,#143331,#143332,
#143333,#143334,#143335,#143336,#143337,#143338,#143339,#143340,#143341,
#143342,#143343,#143344,#143345,#143346,#143347,#143348,#143349,#143350,
#143351,#143352,#143353,#143354,#143355,#143356,#143357,#143358,#143359,
#143360,#143361,#143362,#143363,#143364,#143365,#143366,#143367,#143368,
#143369,#143370,#143371,#143372,#143373,#143374,#143375,#143376,#143377,
#143378,#143379,#143380,#143381,#143382,#143383,#143384,#143385,#143386,
#143387,#143388,#143389,#143390,#143391,#143392,#143393,#143394,#143395,
#143396,#143397,#143398,#143399,#143400,#143401,#143402,#143403,#143404,
#143405,#143406,#143407,#143408,#143409,#143410,#143411,#143412,#143413,
#143414,#143415,#143416,#143417,#143418,#143419,#143420,#143421,#143422,
#143423,#143424,#143425,#143426,#143427,#143428,#143429,#143430,#143431,
#143432,#143433,#143434,#143435,#143436,#143437,#143438,#143439,#143440,
#143441,#143442,#143443,#143444,#143445,#143446,#143447,#143448,#143449,
#143450,#143451,#143452,#143453,#143454,#143455,#143456,#143457,#143458,
#143459,#143460,#143461,#143462,#143463,#143464,#143465,#143466,#143467,
#143468,#143469,#143470,#143471,#143472,#143473,#143474,#143475,#143476,
#143477,#143478,#143479,#143480,#143481,#143482,#143483,#143484,#143485,
#143486,#143487,#143488,#143489,#143490,#143491,#143492,#143493,#143494,
#143495,#143496,#143497,#143498,#143499,#143500,#143501,#143502,#143503,
#143504,#143505,#143506,#143507,#143508,#143509,#143510,#143511,#143512,
#143513,#143514,#143515,#143516,#143517,#143518,#143519,#143520,#143521,
#143522,#143523,#143524,#143525,#143526,#143527,#143528,#143529,#143530,
#143531,#143532,#143533,#143534,#143535,#143536,#143537,#143538,#143539,
#143540,#143541,#143542,#143543,#143544,#143545,#143546,#143547,#143548,
#143549,#143550,#143551,#143552,#143553,#143554,#143555,#143556,#143557,
#143558,#143559,#143560,#143561,#143562,#143563,#143564,#143565),
 .UNSPECIFIED.,.F.,.F.,(4,3,3,3,3,3,3,3,3,3,3,3,3,3,3,3,3,3,3,3,3,3,3,3,
3,3,3,3,3,3,3,3,3,3,3,3,3,3,3,3,3,3,3,3,3,3,3,3,3,3,3,3,3,3,3,3,3,3,3,3,
3,3,3,3,3,3,3,3,3,3,3,3,3,3,3,3,3,3,3,3,3,3,4),(227.31352615198,227.393767393133,
227.474014212927,227.554281601494,227.634584558287,227.714989577679,227.795448844244,
227.876040164136,227.939810444189,228.01976774432,228.099630541563,228.179416364034,
228.25914267923,228.338826907524,228.418497893745,228.49816534727,228.577844998087,
228.657552580481,228.737347809557,228.817192151264,228.897150578312,228.939546454909,
229.01950375504,229.099366552283,229.179152374755,229.258878689951,229.338562918246,
229.418233904467,229.497901357993,229.577581008809,229.657288591204,229.73708382028,
229.816928161988,229.896886589035,229.93928246563,230.019239765761,230.099102563004,
230.178888385476,230.258614700671,230.338298928965,230.417969915187,230.497637368713,
230.577317019529,230.657024601924,230.736819831,230.816664172707,230.896622599755,
230.93901847635,231.018975776481,231.098838573724,231.178624396195,231.25835071139,
231.338034939684,231.417705925905,231.497373379431,231.577053030248,231.656760612642,
231.736555841717,231.816400183424,231.896358610472,231.93875448707,232.018711787201,
232.098574584444,232.178360406916,232.258086722111,232.337770950405,232.417441936626,
232.497109390152,232.576789040969,232.656496623363,232.736291852439,232.816136194146,
232.896094621194,232.93849049779,233.020768117961,233.100703328103,233.18056158131,
233.260358584177,233.340110002069,233.419836019979,233.499548074529,233.579272327654,
233.596711459159),.UNSPECIFIED.);
#1166=B_SPLINE_CURVE_WITH_KNOTS('',3,(#143567,#143568,#143569,#143570,#143571,
#143572,#143573,#143574,#143575,#143576),.UNSPECIFIED.,.F.,.F.,(4,1,1,1,
1,1,1,4),(233.596719085091,233.93822650851,234.93796251923,235.93769852995,
236.937434540671,237.937170551391,238.936906562111,239.879896766339),
 .UNSPECIFIED.);
#1167=B_SPLINE_CURVE_WITH_KNOTS('',3,(#143578,#143579,#143580,#143581,#143582,
#143583,#143584,#143585,#143586,#143587,#143588,#143589),.UNSPECIFIED.,
 .F.,.F.,(4,2,1,1,1,1,1,1,4),(239.879896766339,239.936642572831,240.936378583551,
241.936114594271,242.935850604991,243.935586615712,244.935322626432,245.935058637152,
246.163082073519),.UNSPECIFIED.);
#1168=B_SPLINE_CURVE_WITH_KNOTS('',3,(#143591,#143592,#143593,#143594,#143595,
#143596,#143597,#143598,#143599,#143600,#143601,#143602,#143603,#143604,
#143605,#143606,#143607,#143608,#143609,#143610,#143611,#143612,#143613,
#143614,#143615,#143616,#143617,#143618,#143619,#143620,#143621,#143622,
#143623,#143624,#143625,#143626,#143627,#143628,#143629,#143630,#143631,
#143632,#143633,#143634,#143635,#143636,#143637,#143638,#143639,#143640,
#143641,#143642,#143643,#143644,#143645,#143646,#143647,#143648,#143649,
#143650,#143651,#143652,#143653,#143654,#143655,#143656,#143657,#143658,
#143659,#143660,#143661,#143662,#143663,#143664,#143665,#143666,#143667,
#143668,#143669,#143670,#143671,#143672,#143673,#143674,#143675,#143676,
#143677,#143678,#143679,#143680,#143681,#143682,#143683,#143684,#143685,
#143686,#143687,#143688,#143689,#143690,#143691,#143692,#143693,#143694,
#143695,#143696,#143697,#143698,#143699,#143700,#143701,#143702,#143703,
#143704,#143705,#143706,#143707,#143708,#143709,#143710,#143711,#143712,
#143713,#143714,#143715,#143716,#143717,#143718,#143719,#143720,#143721,
#143722,#143723,#143724,#143725,#143726,#143727,#143728,#143729,#143730,
#143731,#143732,#143733,#143734,#143735,#143736,#143737,#143738,#143739,
#143740,#143741,#143742,#143743,#143744,#143745,#143746,#143747,#143748,
#143749,#143750,#143751,#143752,#143753,#143754,#143755,#143756,#143757,
#143758,#143759,#143760,#143761,#143762,#143763,#143764,#143765,#143766,
#143767,#143768,#143769,#143770,#143771,#143772,#143773,#143774,#143775,
#143776,#143777,#143778,#143779,#143780,#143781,#143782,#143783,#143784,
#143785,#143786,#143787,#143788,#143789,#143790,#143791,#143792,#143793,
#143794,#143795,#143796,#143797,#143798,#143799,#143800,#143801,#143802,
#143803,#143804,#143805,#143806,#143807,#143808,#143809,#143810,#143811,
#143812,#143813,#143814,#143815,#143816,#143817,#143818,#143819,#143820,
#143821,#143822,#143823,#143824,#143825,#143826,#143827,#143828,#143829,
#143830,#143831,#143832,#143833,#143834,#143835,#143836,#143837),
 .UNSPECIFIED.,.F.,.F.,(4,3,3,3,3,3,3,3,3,3,3,3,3,3,3,3,3,3,3,3,3,3,3,3,
3,3,3,3,3,3,3,3,3,3,3,3,3,3,3,3,3,3,3,3,3,3,3,3,3,3,3,3,3,3,3,3,3,3,3,3,
3,3,3,3,3,3,3,3,3,3,3,3,3,3,3,3,3,3,3,3,3,3,4),(246.163082073519,246.241812808052,
246.320488022863,246.399133213762,246.477764257754,246.55639764423,246.635049862504,
246.713782865171,246.792558235773,246.871451270532,246.934794647872,247.014751948003,
247.094614745246,247.174400567718,247.254126882913,247.333811111207,247.413482097428,
247.493149550953,247.57282920177,247.652536784164,247.73233201324,247.812176354948,
247.892134781995,247.934530658592,248.014487958723,248.094350755966,248.174136578438,
248.253862893633,248.333547121927,248.413218108148,248.492885561674,248.57256521249,
248.652272794885,248.73206802396,248.811912365668,248.891870792716,248.934266669312,
249.014223969443,249.094086766686,249.173872589157,249.253598904353,249.333283132647,
249.412954118868,249.492621572393,249.57230122321,249.652008805604,249.73180403468,
249.811648376387,249.891606803435,249.934002680032,250.013959980163,250.093822777406,
250.173608599878,250.253334915073,250.333019143366,250.412690129587,250.492357583113,
250.572037233929,250.651744816324,250.7315400454,250.811384387107,250.891342814154,
250.933738690752,251.013695990883,251.093558788126,251.173344610597,251.253070925793,
251.332755154087,251.412426140308,251.492093593834,251.57177324465,251.651480827045,
251.73127605612,251.811120397828,251.891078824876,251.933474701472,252.017082946527,
252.100559235755,252.186986271991,252.270183268191,252.353287967343,252.436284943832,
252.446267380698),.UNSPECIFIED.);
#1169=B_SPLINE_CURVE_WITH_KNOTS('',3,(#143839,#143840,#143841,#143842,#143843,
#143844,#143845,#143846,#143847,#143848,#143849,#143850,#143851,#143852,
#143853,#143854,#143855,#143856,#143857,#143858,#143859,#143860,#143861,
#143862,#143863,#143864,#143865,#143866,#143867,#143868,#143869,#143870,
#143871,#143872,#143873,#143874,#143875,#143876,#143877,#143878,#143879,
#143880,#143881,#143882,#143883,#143884,#143885,#143886,#143887,#143888,
#143889,#143890,#143891,#143892,#143893,#143894,#143895,#143896,#143897,
#143898,#143899,#143900,#143901,#143902,#143903,#143904,#143905,#143906,
#143907,#143908,#143909,#143910,#143911,#143912,#143913,#143914,#143915,
#143916,#143917,#143918,#143919,#143920,#143921,#143922,#143923,#143924,
#143925,#143926,#143927,#143928,#143929,#143930,#143931,#143932,#143933,
#143934,#143935,#143936,#143937,#143938,#143939,#143940,#143941,#143942,
#143943,#143944,#143945,#143946,#143947,#143948,#143949,#143950,#143951,
#143952,#143953,#143954,#143955,#143956,#143957,#143958,#143959,#143960,
#143961,#143962,#143963,#143964,#143965,#143966,#143967,#143968,#143969,
#143970,#143971,#143972,#143973,#143974,#143975,#143976,#143977,#143978,
#143979,#143980,#143981,#143982,#143983,#143984,#143985,#143986,#143987,
#143988,#143989,#143990,#143991,#143992,#143993,#143994,#143995,#143996,
#143997,#143998,#143999,#144000,#144001,#144002,#144003,#144004,#144005,
#144006,#144007,#144008,#144009,#144010,#144011,#144012,#144013,#144014,
#144015,#144016,#144017,#144018,#144019,#144020,#144021,#144022,#144023,
#144024,#144025,#144026,#144027,#144028,#144029,#144030,#144031,#144032,
#144033,#144034,#144035,#144036,#144037,#144038,#144039,#144040,#144041,
#144042,#144043,#144044,#144045,#144046,#144047,#144048,#144049,#144050,
#144051,#144052,#144053,#144054,#144055,#144056,#144057,#144058,#144059,
#144060,#144061,#144062,#144063,#144064,#144065,#144066,#144067,#144068,
#144069,#144070,#144071,#144072,#144073,#144074,#144075,#144076,#144077,
#144078,#144079,#144080,#144081,#144082),.UNSPECIFIED.,.F.,.F.,(4,3,3,3,
3,3,3,3,3,3,3,3,3,3,3,3,3,3,3,3,3,3,3,3,3,3,3,3,3,3,3,3,3,3,3,3,3,3,3,3,
3,3,3,3,3,3,3,3,3,3,3,3,3,3,3,3,3,3,3,3,3,3,3,3,3,3,3,3,3,3,3,3,3,3,3,3,
3,3,3,3,3,4),(252.446267380839,252.530186188249,252.614226469652,252.698477120877,
252.782837309082,252.867396283387,252.933210712193,253.013168012324,253.093030809567,
253.172816632039,253.252542947234,253.332227175528,253.411898161749,253.491565615275,
253.571245266091,253.650952848486,253.730748077561,253.810592419269,253.890550846316,
253.932946722913,254.012904023044,254.092766820287,254.172552642759,254.252278957954,
254.331963186248,254.411634172469,254.491301625995,254.570981276811,254.650688859206,
254.730484088281,254.810328429989,254.890286857036,254.932682733633,255.012640033764,
255.092502831007,255.172288653479,255.252014968674,255.331699196968,255.411370183189,
255.491037636715,255.570717287531,255.650424869926,255.730220099001,255.810064440709,
255.890022867756,255.932418744353,256.012376044484,256.092238841727,256.172024664199,
256.251750979394,256.331435207688,256.411106193909,256.490773647435,256.570453298251,
256.650160880646,256.729956109722,256.809800451429,256.889758878476,256.932154755073,
257.012112055204,257.091974852447,257.171760674918,257.251486990114,257.331171218408,
257.410842204628,257.490509658154,257.570189308971,257.649896891365,257.729692120441,
257.809536462148,257.889494889195,257.931890765793,258.01070166188,258.08941789444,
258.16942224362,258.24799898334,258.326542478408,258.405069289344,258.486165138977,
258.564734604693,258.647093646286,258.729452687878),.UNSPECIFIED.);
#1170=B_SPLINE_CURVE_WITH_KNOTS('',3,(#144084,#144085,#144086,#144087,#144088,
#144089,#144090,#144091,#144092,#144093,#144094),.UNSPECIFIED.,.F.,.F.,
(4,1,1,1,1,1,1,1,4),(258.729452687878,258.931626776513,259.931362787234,
260.931098797954,261.930834808674,262.930570819394,263.930306830114,264.930042840834,
265.012637995057),.UNSPECIFIED.);
#1171=B_SPLINE_CURVE_WITH_KNOTS('',3,(#144096,#144097,#144098,#144099,#144100,
#144101,#144102,#144103,#144104,#144105),.UNSPECIFIED.,.F.,.F.,(4,1,1,1,
1,1,1,4),(265.012637995057,265.929778851554,266.929514862274,267.929250872995,
268.928986883715,269.928722894435,270.928458905155,271.295823302237),
 .UNSPECIFIED.);
#1172=B_SPLINE_CURVE_WITH_KNOTS('',3,(#144107,#144108,#144109,#144110,#144111,
#144112,#144113,#144114,#144115,#144116),.UNSPECIFIED.,.F.,.F.,(4,1,1,1,
1,1,1,4),(271.295823302237,271.928194915875,272.927930926595,273.927666937315,
274.927402948035,275.927138958756,276.926874969476,277.579008609416),
 .UNSPECIFIED.);
#1173=B_SPLINE_CURVE_WITH_KNOTS('',3,(#144118,#144119,#144120,#144121,#144122,
#144123,#144124,#144125,#144126,#144127,#144128,#144129,#144130,#144131,
#144132,#144133,#144134,#144135,#144136,#144137,#144138,#144139,#144140,
#144141,#144142,#144143,#144144,#144145,#144146,#144147,#144148,#144149,
#144150,#144151,#144152,#144153,#144154,#144155,#144156,#144157,#144158,
#144159,#144160,#144161,#144162,#144163,#144164,#144165,#144166,#144167,
#144168,#144169,#144170,#144171,#144172,#144173,#144174,#144175,#144176,
#144177,#144178,#144179,#144180,#144181,#144182,#144183,#144184,#144185,
#144186,#144187,#144188,#144189,#144190,#144191,#144192,#144193,#144194,
#144195,#144196,#144197,#144198,#144199,#144200,#144201,#144202,#144203,
#144204,#144205,#144206,#144207,#144208,#144209,#144210,#144211,#144212,
#144213,#144214,#144215,#144216,#144217,#144218,#144219,#144220,#144221,
#144222,#144223,#144224,#144225,#144226,#144227,#144228,#144229,#144230,
#144231,#144232,#144233,#144234,#144235,#144236,#144237,#144238,#144239,
#144240,#144241,#144242,#144243,#144244,#144245,#144246,#144247,#144248,
#144249,#144250,#144251,#144252,#144253,#144254,#144255,#144256,#144257,
#144258,#144259,#144260,#144261,#144262,#144263,#144264,#144265,#144266,
#144267,#144268,#144269,#144270,#144271,#144272,#144273,#144274,#144275,
#144276,#144277,#144278,#144279,#144280,#144281,#144282,#144283,#144284,
#144285,#144286,#144287,#144288,#144289,#144290,#144291,#144292,#144293,
#144294,#144295,#144296,#144297,#144298,#144299,#144300,#144301,#144302,
#144303,#144304,#144305,#144306,#144307,#144308,#144309,#144310,#144311,
#144312,#144313,#144314,#144315,#144316,#144317,#144318,#144319,#144320,
#144321,#144322,#144323,#144324,#144325,#144326,#144327,#144328,#144329,
#144330,#144331,#144332,#144333,#144334,#144335,#144336,#144337,#144338,
#144339,#144340,#144341,#144342,#144343,#144344,#144345,#144346,#144347,
#144348,#144349,#144350,#144351,#144352,#144353,#144354,#144355,#144356,
#144357,#144358,#144359,#144360,#144361),.UNSPECIFIED.,.F.,.F.,(4,3,3,3,
3,3,3,3,3,3,3,3,3,3,3,3,3,3,3,3,3,3,3,3,3,3,3,3,3,3,3,3,3,3,3,3,3,3,3,3,
3,3,3,3,3,3,3,3,3,3,3,3,3,3,3,3,3,3,3,3,3,3,3,3,3,3,3,3,3,3,3,3,3,3,3,3,
3,3,3,3,3,4),(277.579008731906,277.670689685924,277.762818730233,277.855534755267,
277.926610980196,278.006568280327,278.086431077569,278.166216900041,278.245943215236,
278.325627443529,278.40529842975,278.484965883276,278.564645534092,278.644353116486,
278.724148345561,278.803992687268,278.883951114315,278.926346990916,279.006304291047,
279.08616708829,279.165952910762,279.245679225957,279.325363454251,279.405034440472,
279.484701893998,279.564381544814,279.644089127209,279.723884356284,279.803728697992,
279.883687125039,279.926083001636,280.006040301767,280.08590309901,280.165688921482,
280.245415236677,280.325099464972,280.404770451193,280.484437904719,280.564117555535,
280.64382513793,280.723620367006,280.803464708713,280.883423135761,280.925819012356,
281.005776312487,281.085639109729,281.165424932201,281.245151247396,281.32483547569,
281.404506461911,281.484173915437,281.563853566253,281.643561148647,281.723356377723,
281.80320071943,281.883159146478,281.925555023076,282.005512323207,282.08537512045,
282.165160942922,282.244887258118,282.324571486412,282.404242472633,282.48390992616,
282.563589576976,282.643297159371,282.723092388447,282.802936730155,282.882895157202,
282.925291033797,283.004516126559,283.083647236245,283.162702529059,283.241700101922,
283.32066381893,283.399610922056,283.478557706701,283.557520465671,283.636559775155,
283.715638650542,283.794832188231,283.862193916596),.UNSPECIFIED.);
#1174=B_SPLINE_CURVE_WITH_KNOTS('',3,(#144363,#144364,#144365,#144366,#144367,
#144368,#144369,#144370,#144371,#144372,#144373,#144374),.UNSPECIFIED.,
 .F.,.F.,(4,2,1,1,1,1,1,1,4),(283.862193916596,283.925027044517,284.924763055237,
285.924499065957,286.924235076677,287.923971087397,288.923707098117,289.923443108837,
290.145379223776),.UNSPECIFIED.);
#1175=B_SPLINE_CURVE_WITH_KNOTS('',3,(#144376,#144377,#144378,#144379,#144380,
#144381,#144382,#144383,#144384,#144385,#144386,#144387,#144388,#144389,
#144390,#144391,#144392,#144393,#144394,#144395,#144396,#144397,#144398,
#144399,#144400,#144401,#144402,#144403,#144404,#144405,#144406,#144407,
#144408,#144409,#144410,#144411,#144412,#144413,#144414,#144415,#144416,
#144417,#144418,#144419,#144420,#144421,#144422,#144423,#144424,#144425,
#144426,#144427,#144428,#144429,#144430,#144431,#144432,#144433,#144434,
#144435,#144436,#144437,#144438,#144439,#144440,#144441,#144442,#144443,
#144444,#144445,#144446,#144447,#144448,#144449,#144450,#144451,#144452,
#144453,#144454,#144455,#144456,#144457,#144458,#144459,#144460,#144461,
#144462,#144463,#144464,#144465,#144466,#144467,#144468,#144469,#144470,
#144471,#144472,#144473,#144474,#144475,#144476,#144477,#144478,#144479,
#144480,#144481,#144482,#144483,#144484,#144485,#144486,#144487,#144488,
#144489,#144490,#144491,#144492,#144493,#144494,#144495,#144496,#144497,
#144498,#144499,#144500,#144501,#144502,#144503,#144504,#144505,#144506,
#144507,#144508,#144509,#144510,#144511,#144512,#144513,#144514,#144515,
#144516,#144517,#144518,#144519,#144520,#144521,#144522,#144523,#144524,
#144525,#144526,#144527,#144528,#144529,#144530,#144531,#144532,#144533,
#144534,#144535,#144536,#144537,#144538,#144539,#144540,#144541,#144542,
#144543,#144544,#144545,#144546,#144547,#144548,#144549,#144550,#144551,
#144552,#144553,#144554,#144555,#144556,#144557,#144558,#144559,#144560,
#144561,#144562,#144563,#144564,#144565,#144566,#144567,#144568,#144569,
#144570,#144571,#144572,#144573,#144574,#144575,#144576,#144577,#144578,
#144579,#144580,#144581,#144582,#144583,#144584,#144585,#144586,#144587,
#144588,#144589,#144590,#144591,#144592,#144593,#144594,#144595,#144596,
#144597,#144598,#144599,#144600,#144601,#144602,#144603,#144604,#144605,
#144606,#144607,#144608,#144609,#144610,#144611,#144612,#144613,#144614,
#144615,#144616,#144617,#144618,#144619),.UNSPECIFIED.,.F.,.F.,(4,3,3,3,
3,3,3,3,3,3,3,3,3,3,3,3,3,3,3,3,3,3,3,3,3,3,3,3,3,3,3,3,3,3,3,3,3,3,3,3,
3,3,3,3,3,3,3,3,3,3,3,3,3,3,3,3,3,3,3,3,3,3,3,3,3,3,3,3,3,3,3,3,3,3,3,3,
3,3,3,3,3,4),(290.145379223776,290.22408848333,290.302740462822,290.381360101647,
290.459964035669,290.538568771433,290.617190814347,290.69589275774,290.774635731816,
290.853497957081,290.923179119557,291.003136419688,291.082999216931,291.162785039403,
291.242511354598,291.322195582892,291.401866569113,291.481534022639,291.561213673455,
291.640921255849,291.720716484925,291.800560826633,291.88051925368,291.922915130277,
292.002872430409,292.082735227652,292.162521050124,292.242247365319,292.321931593614,
292.401602579835,292.481270033361,292.560949684178,292.640657266573,292.720452495648,
292.800296837356,292.880255264404,292.922651140998,293.002608441129,293.082471238372,
293.162257060844,293.241983376039,293.321667604333,293.401338590553,293.481006044079,
293.560685694896,293.640393277291,293.720188506366,293.800032848074,293.879991275121,
293.922387151718,294.002344451849,294.082207249092,294.161993071563,294.241719386759,
294.321403615052,294.401074601273,294.480742054799,294.560421705615,294.640129288009,
294.719924517084,294.799768858792,294.87972728584,294.922123162438,295.002080462569,
295.081943259812,295.161729082284,295.241455397479,295.321139625774,295.400810611995,
295.480478065521,295.560157716337,295.639865298731,295.719660527807,295.799504869514,
295.879463296561,295.921859173158,296.005685485794,296.089376747263,296.174173693186,
296.257577841536,296.343071186246,296.428564530955),.UNSPECIFIED.);
#1176=B_SPLINE_CURVE_WITH_KNOTS('',3,(#144621,#144622,#144623,#144624,#144625,
#144626,#144627,#144628,#144629,#144630,#144631,#144632,#144633,#144634,
#144635,#144636,#144637,#144638,#144639,#144640,#144641,#144642,#144643,
#144644,#144645,#144646,#144647,#144648,#144649,#144650,#144651,#144652,
#144653,#144654,#144655,#144656,#144657,#144658,#144659,#144660,#144661,
#144662,#144663,#144664,#144665,#144666,#144667,#144668,#144669,#144670,
#144671,#144672,#144673,#144674,#144675,#144676,#144677,#144678,#144679,
#144680,#144681,#144682,#144683,#144684,#144685,#144686,#144687,#144688,
#144689,#144690,#144691,#144692,#144693,#144694,#144695,#144696,#144697,
#144698,#144699,#144700,#144701,#144702,#144703,#144704,#144705,#144706,
#144707,#144708,#144709,#144710,#144711,#144712,#144713,#144714,#144715,
#144716,#144717,#144718,#144719,#144720,#144721,#144722,#144723,#144724,
#144725,#144726,#144727,#144728,#144729,#144730,#144731,#144732,#144733,
#144734,#144735,#144736,#144737,#144738,#144739,#144740,#144741,#144742,
#144743,#144744,#144745,#144746,#144747,#144748,#144749,#144750,#144751,
#144752,#144753,#144754,#144755,#144756,#144757,#144758,#144759,#144760,
#144761,#144762,#144763,#144764,#144765,#144766,#144767,#144768,#144769,
#144770,#144771,#144772,#144773,#144774,#144775,#144776,#144777,#144778,
#144779,#144780,#144781,#144782,#144783,#144784,#144785,#144786,#144787,
#144788,#144789,#144790,#144791,#144792,#144793,#144794,#144795,#144796,
#144797,#144798,#144799,#144800,#144801,#144802,#144803,#144804,#144805,
#144806,#144807,#144808,#144809,#144810,#144811,#144812,#144813,#144814,
#144815,#144816,#144817,#144818,#144819,#144820,#144821,#144822,#144823,
#144824,#144825,#144826,#144827,#144828,#144829,#144830,#144831,#144832,
#144833,#144834,#144835,#144836,#144837,#144838,#144839,#144840,#144841,
#144842,#144843,#144844,#144845,#144846,#144847,#144848,#144849,#144850,
#144851,#144852,#144853,#144854,#144855,#144856,#144857,#144858,#144859,
#144860,#144861,#144862,#144863,#144864),.UNSPECIFIED.,.F.,.F.,(4,3,3,3,
3,3,3,3,3,3,3,3,3,3,3,3,3,3,3,3,3,3,3,3,3,3,3,3,3,3,3,3,3,3,3,3,3,3,3,3,
3,3,3,3,3,3,3,3,3,3,3,3,3,3,3,3,3,3,3,3,3,3,3,3,3,3,3,3,3,3,3,3,3,3,3,3,
3,3,3,3,3,4),(296.428564531105,296.512262186977,296.59607320243,296.680086462927,
296.764204012982,296.848518636483,296.921595183878,297.001552484009,297.081415281252,
297.161201103724,297.240927418919,297.320611647213,297.400282633434,297.47995008696,
297.559629737777,297.639337320171,297.719132549247,297.798976890955,297.878935318002,
297.921331194598,298.001288494729,298.081151291972,298.160937114443,298.240663429639,
298.320347657933,298.400018644154,298.47968609768,298.559365748496,298.639073330891,
298.718868559966,298.798712901674,298.878671328721,298.921067205318,299.001024505449,
299.080887302692,299.160673125164,299.240399440359,299.320083668654,299.399754654875,
299.479422108401,299.559101759217,299.638809341612,299.718604570687,299.798448912395,
299.878407339443,299.920803216039,300.00076051617,300.080623313413,300.160409135885,
300.24013545108,300.319819679374,300.399490665595,300.479158119121,300.558837769938,
300.638545352333,300.718340581408,300.798184923116,300.878143350163,300.920539226759,
301.00049652689,301.080359324132,301.160145146604,301.239871461799,301.319555690093,
301.399226676314,301.47889412984,301.558573780656,301.63828136305,301.718076592126,
301.797920933833,301.87787936088,301.920275237479,301.999104940712,302.077839823292,
302.157078575147,302.235673780349,302.314235355996,302.392779852823,302.472522349151,
302.551107246514,302.631428542324,302.711749838135),.UNSPECIFIED.);
#1177=B_SPLINE_CURVE_WITH_KNOTS('',3,(#144866,#144867,#144868,#144869,#144870,
#144871,#144872,#144873,#144874,#144875,#144876),.UNSPECIFIED.,.F.,.F.,
(4,1,1,1,1,1,1,1,4),(302.711749838135,302.920011248199,303.919747258919,
304.919483269639,305.919219280359,306.91895529108,307.9186913018,308.91842731252,
308.994935145314),.UNSPECIFIED.);
#1178=B_SPLINE_CURVE_WITH_KNOTS('',3,(#144878,#144879,#144880,#144881,#144882,
#144883,#144884,#144885,#144886,#144887),.UNSPECIFIED.,.F.,.F.,(4,1,1,1,
1,1,1,4),(308.994935145314,309.91816332324,310.91789933396,311.91763534468,
312.9173713554,313.91710736612,314.916843376841,315.278120452494),
 .UNSPECIFIED.);
#1179=B_SPLINE_CURVE_WITH_KNOTS('',3,(#144889,#144890,#144891,#144892,#144893,
#144894,#144895,#144896,#144897,#144898),.UNSPECIFIED.,.F.,.F.,(4,1,1,1,
1,1,1,4),(315.278120452494,315.916579387561,316.916315398281,317.916051409001,
318.915787419721,319.915523430441,320.915259441161,321.561305759673),
 .UNSPECIFIED.);
#1180=B_SPLINE_CURVE_WITH_KNOTS('',3,(#144900,#144901,#144902,#144903,#144904,
#144905,#144906,#144907,#144908,#144909,#144910,#144911,#144912,#144913,
#144914,#144915,#144916,#144917,#144918,#144919,#144920,#144921,#144922,
#144923,#144924,#144925,#144926,#144927,#144928,#144929,#144930,#144931,
#144932,#144933,#144934,#144935,#144936,#144937,#144938,#144939,#144940,
#144941,#144942,#144943,#144944,#144945,#144946,#144947,#144948,#144949,
#144950,#144951,#144952,#144953,#144954,#144955,#144956,#144957,#144958,
#144959,#144960,#144961,#144962,#144963,#144964,#144965,#144966,#144967,
#144968,#144969,#144970,#144971,#144972,#144973,#144974,#144975,#144976,
#144977,#144978,#144979,#144980,#144981,#144982,#144983,#144984,#144985,
#144986,#144987,#144988,#144989,#144990,#144991,#144992,#144993,#144994,
#144995,#144996,#144997,#144998,#144999,#145000,#145001,#145002,#145003,
#145004,#145005,#145006,#145007,#145008,#145009,#145010,#145011,#145012,
#145013,#145014,#145015,#145016,#145017,#145018,#145019,#145020,#145021,
#145022,#145023,#145024,#145025,#145026,#145027,#145028,#145029,#145030,
#145031,#145032,#145033,#145034,#145035,#145036,#145037,#145038,#145039,
#145040,#145041,#145042,#145043,#145044,#145045,#145046,#145047,#145048,
#145049,#145050,#145051,#145052,#145053,#145054,#145055,#145056,#145057,
#145058,#145059,#145060,#145061,#145062,#145063,#145064,#145065,#145066,
#145067,#145068,#145069,#145070,#145071,#145072,#145073,#145074,#145075,
#145076,#145077,#145078,#145079,#145080,#145081,#145082,#145083,#145084,
#145085,#145086,#145087,#145088,#145089,#145090,#145091,#145092,#145093,
#145094,#145095,#145096,#145097,#145098,#145099,#145100,#145101,#145102,
#145103,#145104,#145105,#145106,#145107,#145108,#145109,#145110,#145111,
#145112,#145113,#145114,#145115,#145116,#145117,#145118,#145119,#145120,
#145121,#145122,#145123,#145124,#145125,#145126,#145127,#145128,#145129,
#145130,#145131,#145132,#145133,#145134,#145135,#145136,#145137,#145138,
#145139,#145140,#145141,#145142,#145143),.UNSPECIFIED.,.F.,.F.,(4,3,3,3,
3,3,3,3,3,3,3,3,3,3,3,3,3,3,3,3,3,3,3,3,3,3,3,3,3,3,3,3,3,3,3,3,3,3,3,3,
3,3,3,3,3,3,3,3,3,3,3,3,3,3,3,3,3,3,3,3,3,3,3,3,3,3,3,3,3,3,3,3,3,3,3,3,
3,3,3,3,3,4),(321.561306006896,321.652519309254,321.744150517988,321.836345229445,
321.914995451882,321.994952752013,322.074815549254,322.154601371726,322.23432768692,
322.314011915214,322.393682901434,322.473350354959,322.553030005775,322.632737588169,
322.712532817243,322.79237715895,322.872335585997,322.914731462602,322.994688762733,
323.074551559976,323.154337382448,323.234063697643,323.313747925937,323.393418912158,
323.473086365684,323.5527660165,323.632473598895,323.71226882797,323.792113169678,
323.872071596725,323.914467473322,323.994424773453,324.074287570696,324.154073393168,
324.233799708364,324.313483936658,324.393154922879,324.472822376405,324.552502027222,
324.632209609616,324.712004838692,324.7918491804,324.871807607447,324.914203484042,
324.994160784173,325.074023581416,325.153809403887,325.233535719083,325.313219947377,
325.392890933597,325.472558387123,325.55223803794,325.631945620334,325.71174084941,
325.791585191117,325.871543618164,325.913939494762,325.993896794893,326.073759592136,
326.153545414608,326.233271729803,326.312955958097,326.392626944318,326.472294397844,
326.55197404866,326.631681631054,326.71147686013,326.791321201837,326.871279628885,
326.913675505482,326.99284839066,327.071927338325,327.150930553951,327.229876172782,
327.308787992154,327.387683355991,327.466578593443,327.545490031237,327.624477289976,
327.703504406966,327.78264369027,327.844491066853),.UNSPECIFIED.);
#1181=B_SPLINE_CURVE_WITH_KNOTS('',3,(#145145,#145146,#145147,#145148,#145149,
#145150,#145151,#145152,#145153,#145154,#145155,#145156),.UNSPECIFIED.,
 .F.,.F.,(4,2,1,1,1,1,1,1,4),(327.844491066853,327.913411516202,328.913147526922,
329.912883537642,330.912619548363,331.912355559083,332.912091569803,333.911827580523,
334.127676374032),.UNSPECIFIED.);
#1182=B_SPLINE_CURVE_WITH_KNOTS('',3,(#145158,#145159,#145160,#145161,#145162,
#145163,#145164,#145165,#145166,#145167),.UNSPECIFIED.,.F.,.F.,(4,1,1,1,
1,1,1,4),(334.127676374032,334.911563591243,335.911299601963,336.911035612683,
337.910771623403,338.910507634124,339.910243644844,340.410861681212),
 .UNSPECIFIED.);
#1183=B_SPLINE_CURVE_WITH_KNOTS('',3,(#145169,#145170,#145171,#145172,#145173,
#145174,#145175,#145176,#145177,#145178),.UNSPECIFIED.,.F.,.F.,(4,1,1,1,
1,1,1,4),(340.410861681212,340.909979655564,341.909715666284,342.909451677004,
343.909187687724,344.908923698445,345.908659709165,346.694046988392),
 .UNSPECIFIED.);
#1184=B_SPLINE_CURVE_WITH_KNOTS('',3,(#145180,#145181,#145182,#145183,#145184,
#145185,#145186,#145187,#145188,#145189,#145190),.UNSPECIFIED.,.F.,.F.,
(4,1,1,1,1,1,1,1,4),(346.694046988392,346.908395719885,347.908131730605,
348.907867741325,349.907603752045,350.907339762765,351.907075773485,352.906811784205,
352.977232295571),.UNSPECIFIED.);
#1185=B_SPLINE_CURVE_WITH_KNOTS('',3,(#145192,#145193,#145194,#145195,#145196,
#145197,#145198,#145199,#145200,#145201,#145202,#145203,#145204,#145205,
#145206,#145207,#145208,#145209,#145210,#145211,#145212,#145213,#145214,
#145215,#145216,#145217,#145218,#145219,#145220,#145221,#145222,#145223,
#145224,#145225,#145226,#145227,#145228,#145229,#145230,#145231,#145232,
#145233,#145234,#145235,#145236,#145237,#145238,#145239,#145240,#145241,
#145242,#145243,#145244,#145245,#145246,#145247,#145248,#145249,#145250,
#145251,#145252,#145253,#145254,#145255,#145256,#145257,#145258,#145259,
#145260,#145261,#145262,#145263,#145264,#145265,#145266,#145267,#145268,
#145269,#145270,#145271,#145272,#145273,#145274,#145275,#145276,#145277,
#145278,#145279,#145280,#145281,#145282,#145283,#145284,#145285,#145286,
#145287,#145288,#145289,#145290,#145291,#145292,#145293,#145294,#145295,
#145296,#145297,#145298,#145299,#145300,#145301,#145302,#145303,#145304,
#145305,#145306,#145307,#145308,#145309,#145310,#145311,#145312,#145313,
#145314,#145315,#145316,#145317,#145318,#145319,#145320,#145321,#145322,
#145323,#145324,#145325,#145326,#145327,#145328,#145329,#145330,#145331,
#145332,#145333,#145334,#145335,#145336,#145337,#145338,#145339,#145340,
#145341,#145342,#145343,#145344,#145345,#145346,#145347,#145348,#145349,
#145350,#145351,#145352,#145353,#145354,#145355,#145356,#145357,#145358,
#145359,#145360,#145361,#145362,#145363,#145364,#145365,#145366,#145367,
#145368,#145369,#145370,#145371,#145372,#145373,#145374,#145375,#145376,
#145377,#145378,#145379,#145380,#145381,#145382,#145383,#145384,#145385,
#145386,#145387,#145388,#145389,#145390,#145391,#145392,#145393,#145394,
#145395,#145396,#145397,#145398,#145399,#145400,#145401,#145402,#145403,
#145404,#145405,#145406,#145407,#145408,#145409,#145410,#145411,#145412,
#145413,#145414,#145415,#145416,#145417,#145418,#145419,#145420,#145421,
#145422,#145423,#145424,#145425,#145426,#145427,#145428,#145429,#145430,
#145431,#145432,#145433,#145434,#145435),.UNSPECIFIED.,.F.,.F.,(4,3,3,3,
3,3,3,3,3,3,3,3,3,3,3,3,3,3,3,3,3,3,3,3,3,3,3,3,3,3,3,3,3,3,3,3,3,3,3,3,
3,3,3,3,3,3,3,3,3,3,3,3,3,3,3,3,3,3,3,3,3,3,3,3,3,3,3,3,3,3,3,3,3,3,3,3,
3,3,3,3,3,4),(352.977232295571,353.056367420751,353.135413276433,353.214388057453,
353.293309892804,353.372204939949,353.451087864685,353.529975002706,353.60888269035,
353.687872640281,353.766906214855,353.846057232216,353.906547794926,353.986505095057,
354.0663678923,354.146153714771,354.225880029967,354.305564258261,354.385235244482,
354.464902698008,354.544582348824,354.624289931219,354.704085160294,354.783929502002,
354.863887929049,354.906283805646,354.986241105777,355.06610390302,355.145889725491,
355.225616040687,355.305300268981,355.384971255202,355.464638708728,355.544318359544,
355.624025941938,355.703821171014,355.783665512722,355.863623939769,355.906019816366,
355.985977116497,356.06583991374,356.145625736211,356.225352051406,356.305036279701,
356.384707265921,356.464374719447,356.544054370264,356.623761952658,356.703557181734,
356.783401523441,356.863359950489,356.905755827086,356.985713127217,357.06557592446,
357.145361746932,357.225088062127,357.304772290421,357.384443276641,357.464110730167,
357.543790380984,357.623497963379,357.703293192455,357.783137534163,357.86309596121,
357.905491837806,357.985449137937,358.06531193518,358.145097757652,358.224824072848,
358.304508301142,358.384179287363,358.463846740889,358.543526391705,358.6232339741,
358.703029203175,358.782873544883,358.86283197193,358.905227848526,358.99728591963,
359.089015060361,359.180096318555,359.260417355136),.UNSPECIFIED.);
#1186=B_SPLINE_CURVE_WITH_KNOTS('',3,(#145437,#145438,#145439,#145440,#145441,
#145442,#145443,#145444,#145445,#145446),.UNSPECIFIED.,.F.,.F.,(4,1,1,1,
1,1,1,4),(359.260417602751,359.904963859246,360.904699869967,361.904435880687,
362.904171891407,363.903907902127,364.903643912847,365.54360290993),
 .UNSPECIFIED.);
#1187=B_SPLINE_CURVE_WITH_KNOTS('',3,(#145448,#145449,#145450,#145451,#145452,
#145453,#145454,#145455,#145456,#145457),.UNSPECIFIED.,.F.,.F.,(4,1,1,1,
1,1,1,4),(365.54360290993,365.903379923567,366.903115934287,367.902851945007,
368.902587955728,369.902323966448,370.902059977168,371.82678821711),
 .UNSPECIFIED.);
#1188=B_SPLINE_CURVE_WITH_KNOTS('',3,(#145459,#145460,#145461,#145462,#145463,
#145464,#145465,#145466,#145467,#145468,#145469,#145470),.UNSPECIFIED.,
 .F.,.F.,(4,2,1,1,1,1,1,1,4),(371.82678821711,371.901795987888,372.901531998608,
373.901268009328,374.901004020048,375.900740030769,376.900476041489,377.900212052209,
378.109973524289),.UNSPECIFIED.);
#1189=B_SPLINE_CURVE_WITH_KNOTS('',3,(#145472,#145473,#145474,#145475,#145476,
#145477,#145478,#145479,#145480,#145481,#145482,#145483,#145484,#145485,
#145486,#145487,#145488,#145489,#145490,#145491,#145492,#145493,#145494,
#145495,#145496,#145497,#145498,#145499,#145500,#145501,#145502,#145503,
#145504,#145505,#145506,#145507,#145508,#145509,#145510,#145511,#145512,
#145513,#145514,#145515,#145516,#145517,#145518,#145519,#145520,#145521,
#145522,#145523,#145524,#145525,#145526,#145527,#145528,#145529,#145530,
#145531,#145532,#145533,#145534,#145535,#145536,#145537,#145538,#145539,
#145540,#145541,#145542,#145543,#145544,#145545,#145546,#145547,#145548,
#145549,#145550,#145551,#145552,#145553,#145554,#145555,#145556,#145557,
#145558,#145559,#145560,#145561,#145562,#145563,#145564,#145565,#145566,
#145567,#145568,#145569,#145570,#145571,#145572,#145573,#145574,#145575,
#145576,#145577,#145578,#145579,#145580,#145581,#145582,#145583,#145584,
#145585,#145586,#145587,#145588,#145589,#145590,#145591,#145592,#145593,
#145594,#145595,#145596,#145597,#145598,#145599,#145600,#145601,#145602,
#145603,#145604,#145605,#145606,#145607,#145608,#145609,#145610,#145611,
#145612,#145613,#145614,#145615,#145616,#145617,#145618,#145619,#145620,
#145621,#145622,#145623,#145624,#145625,#145626,#145627,#145628,#145629,
#145630,#145631,#145632,#145633,#145634,#145635,#145636,#145637,#145638,
#145639,#145640,#145641,#145642,#145643,#145644,#145645,#145646,#145647,
#145648,#145649,#145650,#145651,#145652,#145653,#145654,#145655,#145656,
#145657,#145658,#145659,#145660,#145661,#145662,#145663,#145664,#145665,
#145666,#145667,#145668,#145669,#145670,#145671,#145672,#145673,#145674,
#145675,#145676,#145677,#145678,#145679,#145680,#145681,#145682,#145683,
#145684,#145685,#145686,#145687,#145688,#145689,#145690,#145691,#145692,
#145693,#145694,#145695,#145696,#145697,#145698,#145699,#145700,#145701,
#145702,#145703,#145704,#145705,#145706,#145707,#145708,#145709,#145710,
#145711,#145712,#145713,#145714,#145715),.UNSPECIFIED.,.F.,.F.,(4,3,3,3,
3,3,3,3,3,3,3,3,3,3,3,3,3,3,3,3,3,3,3,3,3,3,3,3,3,3,3,3,3,3,3,3,3,3,3,3,
3,3,3,3,3,3,3,3,3,3,3,3,3,3,3,3,3,3,3,3,3,3,3,3,3,3,3,3,3,3,3,3,3,3,3,3,
3,3,3,3,3,4),(378.109973524289,378.18864901344,378.267263817067,378.3463493478,
378.424908498294,378.503465564377,378.582037077905,378.661514824161,378.740203576295,
378.820075819612,378.899948062929,378.97990536306,379.059768160303,379.139553982774,
379.21928029797,379.298964526263,379.378635512484,379.45830296601,379.537982616827,
379.617690199221,379.697485428297,379.777329770004,379.857288197051,379.899684073649,
379.97964137378,380.059504171023,380.139289993494,380.219016308689,380.298700536984,
380.378371523204,380.45803897673,380.537718627547,380.617426209941,380.697221439016,
380.777065780724,380.857024207772,380.899420084369,380.9793773845,381.059240181743,
381.139026004215,381.21875231941,381.298436547704,381.378107533925,381.457774987451,
381.537454638268,381.617162220663,381.696957449738,381.776801791446,381.856760218493,
381.899156095089,381.97911339522,382.058976192463,382.138762014934,382.21848833013,
382.298172558423,382.377843544645,382.457510998171,382.537190648987,382.616898231381,
382.696693460457,382.776537802164,382.856496229212,382.898892105809,382.97884940594,
383.058712203183,383.138498025655,383.21822434085,383.297908569144,383.377579555365,
383.457247008891,383.536926659707,383.616634242102,383.696429471177,383.776273812885,
383.856232239932,383.898628116529,383.98291122769,384.067052492983,384.151000358076,
384.234834447973,384.318511508669,384.393158831352),.UNSPECIFIED.);
#1190=B_SPLINE_CURVE_WITH_KNOTS('',3,(#145717,#145718,#145719,#145720,#145721,
#145722,#145723,#145724,#145725,#145726,#145727,#145728,#145729,#145730,
#145731,#145732,#145733,#145734,#145735,#145736,#145737,#145738,#145739,
#145740,#145741,#145742,#145743,#145744,#145745,#145746,#145747,#145748,
#145749,#145750,#145751,#145752,#145753,#145754,#145755,#145756,#145757,
#145758,#145759,#145760,#145761,#145762,#145763,#145764,#145765,#145766,
#145767,#145768,#145769,#145770,#145771,#145772,#145773,#145774,#145775,
#145776,#145777,#145778,#145779,#145780,#145781,#145782,#145783,#145784,
#145785,#145786,#145787,#145788,#145789,#145790,#145791,#145792,#145793,
#145794,#145795,#145796,#145797,#145798,#145799,#145800,#145801,#145802,
#145803,#145804,#145805,#145806,#145807,#145808,#145809,#145810,#145811,
#145812,#145813,#145814,#145815,#145816,#145817,#145818,#145819,#145820,
#145821,#145822,#145823,#145824,#145825,#145826,#145827,#145828,#145829,
#145830,#145831,#145832,#145833,#145834,#145835,#145836,#145837,#145838,
#145839,#145840,#145841,#145842,#145843,#145844,#145845,#145846,#145847,
#145848,#145849,#145850,#145851,#145852,#145853,#145854,#145855,#145856,
#145857,#145858,#145859,#145860,#145861,#145862,#145863,#145864,#145865,
#145866,#145867,#145868,#145869,#145870,#145871,#145872,#145873,#145874,
#145875,#145876,#145877,#145878,#145879,#145880,#145881,#145882,#145883,
#145884,#145885,#145886,#145887,#145888,#145889,#145890,#145891,#145892,
#145893,#145894,#145895,#145896,#145897,#145898,#145899,#145900,#145901,
#145902,#145903,#145904,#145905,#145906,#145907,#145908,#145909,#145910,
#145911,#145912,#145913,#145914,#145915,#145916,#145917,#145918,#145919,
#145920,#145921,#145922,#145923,#145924,#145925,#145926,#145927,#145928,
#145929,#145930,#145931,#145932,#145933,#145934,#145935,#145936,#145937,
#145938,#145939,#145940,#145941,#145942,#145943,#145944,#145945,#145946,
#145947,#145948,#145949,#145950,#145951,#145952,#145953,#145954,#145955,
#145956,#145957,#145958,#145959,#145960),.UNSPECIFIED.,.F.,.F.,(4,3,3,3,
3,3,3,3,3,3,3,3,3,3,3,3,3,3,3,3,3,3,3,3,3,3,3,3,3,3,3,3,3,3,3,3,3,3,3,3,
3,3,3,3,3,3,3,3,3,3,3,3,3,3,3,3,3,3,3,3,3,3,3,3,3,3,3,3,3,3,3,3,3,3,3,3,
3,3,3,3,3,4),(384.393158831469,384.476433599377,384.559806737166,384.644446084687,
384.72810202294,384.813233075095,384.89836412725,384.978321427381,385.058184224624,
385.137970047095,385.21769636229,385.297380590584,385.377051576805,385.456719030331,
385.536398681147,385.616106263541,385.695901492617,385.775745834324,385.855704261371,
385.89810013797,385.978057438101,386.057920235344,386.137706057815,386.217432373011,
386.297116601305,386.376787587526,386.456455041052,386.536134691868,386.615842274262,
386.695637503338,386.775481845045,386.855440272093,386.89783614869,386.977793448821,
387.057656246064,387.137442068536,387.217168383731,387.296852612025,387.376523598246,
387.456191051772,387.535870702588,387.615578284983,387.695373514059,387.775217855766,
387.855176282814,387.89757215941,387.977529459541,388.057392256784,388.137178079256,
388.216904394451,388.296588622745,388.376259608966,388.455927062492,388.535606713308,
388.615314295703,388.695109524778,388.774953866486,388.854912293533,388.89730817013,
388.977265470261,389.057128267504,389.136914089976,389.216640405171,389.296324633465,
389.375995619686,389.455663073212,389.535342724028,389.615050306422,389.694845535497,
389.774689877205,389.854648304252,389.89704418085,389.975920919647,390.054702476653,
390.133394158125,390.212035029523,390.290641644439,390.369230528185,390.447844999415,
390.526470395101,390.605166603164,390.676344138649),.UNSPECIFIED.);
#1191=B_SPLINE_CURVE_WITH_KNOTS('',3,(#145962,#145963,#145964,#145965,#145966,
#145967,#145968,#145969,#145970,#145971,#145972),.UNSPECIFIED.,.F.,.F.,
(4,1,1,1,1,1,1,1,4),(390.676344138649,390.89678019157,391.896516202291,
392.896252213011,393.895988223731,394.895724234451,395.895460245171,396.895196255891,
396.959529445828),.UNSPECIFIED.);
#1192=B_SPLINE_CURVE_WITH_KNOTS('',3,(#145974,#145975,#145976,#145977,#145978,
#145979,#145980,#145981,#145982,#145983,#145984,#145985,#145986,#145987,
#145988,#145989,#145990,#145991,#145992,#145993,#145994,#145995,#145996,
#145997,#145998,#145999,#146000,#146001,#146002,#146003,#146004,#146005,
#146006,#146007,#146008,#146009,#146010,#146011,#146012,#146013,#146014,
#146015,#146016,#146017,#146018,#146019,#146020,#146021,#146022,#146023,
#146024,#146025,#146026,#146027,#146028,#146029,#146030,#146031,#146032,
#146033,#146034,#146035,#146036,#146037,#146038,#146039,#146040,#146041,
#146042,#146043,#146044,#146045,#146046,#146047,#146048,#146049,#146050,
#146051,#146052,#146053,#146054,#146055,#146056,#146057,#146058,#146059,
#146060,#146061,#146062,#146063,#146064,#146065,#146066,#146067,#146068,
#146069,#146070,#146071,#146072,#146073,#146074,#146075,#146076,#146077,
#146078,#146079,#146080,#146081,#146082,#146083,#146084,#146085,#146086,
#146087,#146088,#146089,#146090,#146091,#146092,#146093,#146094,#146095,
#146096,#146097,#146098,#146099,#146100,#146101,#146102,#146103,#146104,
#146105,#146106,#146107,#146108,#146109,#146110,#146111,#146112,#146113,
#146114,#146115,#146116,#146117,#146118,#146119,#146120,#146121,#146122,
#146123,#146124,#146125,#146126,#146127,#146128,#146129,#146130,#146131,
#146132,#146133,#146134,#146135,#146136,#146137,#146138,#146139,#146140,
#146141,#146142,#146143,#146144,#146145,#146146,#146147,#146148,#146149,
#146150,#146151,#146152,#146153,#146154,#146155,#146156,#146157,#146158,
#146159,#146160,#146161,#146162,#146163,#146164,#146165,#146166,#146167,
#146168,#146169,#146170,#146171,#146172,#146173,#146174,#146175,#146176,
#146177,#146178,#146179,#146180,#146181,#146182,#146183,#146184,#146185,
#146186,#146187,#146188,#146189,#146190,#146191,#146192,#146193,#146194,
#146195,#146196,#146197,#146198,#146199,#146200,#146201,#146202,#146203,
#146204,#146205,#146206,#146207,#146208,#146209,#146210,#146211,#146212,
#146213,#146214,#146215,#146216,#146217),.UNSPECIFIED.,.F.,.F.,(4,3,3,3,
3,3,3,3,3,3,3,3,3,3,3,3,3,3,3,3,3,3,3,3,3,3,3,3,3,3,3,3,3,3,3,3,3,3,3,3,
3,3,3,3,3,3,3,3,3,3,3,3,3,3,3,3,3,3,3,3,3,3,3,3,3,3,3,3,3,3,3,3,3,3,3,3,
3,3,3,3,3,4),(396.959529445828,397.038719794086,397.117820106619,397.196848542962,
397.275823196973,397.354769946268,397.433703753278,397.512640920773,397.591597751488,
397.670636594479,397.749718202142,397.82891891408,397.894932266611,397.974889566742,
398.054752363985,398.134538186457,398.214264501652,398.293948729946,398.373619716167,
398.453287169693,398.532966820509,398.612674402903,398.692469631979,398.772313973687,
398.852272400734,398.894668277331,398.974625577462,399.054488374705,399.134274197176,
399.214000512371,399.293684740665,399.373355726886,399.453023180412,399.532702831229,
399.612410413623,399.692205642699,399.772049984406,399.852008411453,399.894404288051,
399.974361588182,400.054224385425,400.134010207897,400.213736523093,400.293420751387,
400.373091737608,400.452759191135,400.532438841951,400.612146424346,400.691941653422,
400.77178599513,400.851744422178,400.894140298772,400.974097598903,401.053960396146,
401.133746218618,401.213472533813,401.293156762107,401.372827748328,401.452495201854,
401.53217485267,401.611882435065,401.691677664141,401.771522005849,401.851480432896,
401.893876309492,401.973833609623,402.053696406866,402.133482229338,402.213208544533,
402.292892772827,402.372563759048,402.452231212574,402.53191086339,402.611618445785,
402.69141367486,402.771258016568,402.851216443615,402.893612320212,402.986176437499,
403.078390750204,403.169920872596,403.242714630167),.UNSPECIFIED.);
#1193=B_SPLINE_CURVE_WITH_KNOTS('',3,(#146219,#146220,#146221,#146222,#146223,
#146224,#146225,#146226,#146227,#146228),.UNSPECIFIED.,.F.,.F.,(4,1,1,1,
1,1,1,4),(403.242714753008,403.893348330932,404.893084341652,405.892820352372,
406.892556363092,407.892292373813,408.892028384533,409.525900060187),
 .UNSPECIFIED.);
#1194=B_SPLINE_CURVE_WITH_KNOTS('',3,(#146230,#146231,#146232,#146233,#146234,
#146235,#146236,#146237,#146238,#146239),.UNSPECIFIED.,.F.,.F.,(4,1,1,1,
1,1,1,4),(409.525900060187,409.891764395253,410.891500405973,411.891236416693,
412.890972427413,413.890708438133,414.890444448853,415.809085367367),
 .UNSPECIFIED.);
#1195=B_SPLINE_CURVE_WITH_KNOTS('',3,(#146241,#146242,#146243,#146244,#146245,
#146246,#146247,#146248,#146249,#146250,#146251),.UNSPECIFIED.,.F.,.F.,
(4,1,1,1,1,1,1,1,4),(415.809085367367,415.890180459574,416.889916470294,
417.889652481014,418.889388491734,419.889124502454,420.888860513174,421.888596523894,
422.092270674546),.UNSPECIFIED.);
#1196=B_SPLINE_CURVE_WITH_KNOTS('',3,(#146253,#146254,#146255,#146256,#146257,
#146258,#146259,#146260,#146261,#146262,#146263,#146264,#146265,#146266,
#146267,#146268,#146269,#146270,#146271,#146272,#146273,#146274,#146275,
#146276,#146277,#146278,#146279,#146280,#146281,#146282,#146283,#146284,
#146285,#146286,#146287,#146288,#146289,#146290,#146291,#146292,#146293,
#146294,#146295,#146296,#146297,#146298,#146299,#146300,#146301,#146302,
#146303,#146304,#146305,#146306,#146307,#146308,#146309,#146310,#146311,
#146312,#146313,#146314,#146315,#146316,#146317,#146318,#146319,#146320,
#146321,#146322,#146323,#146324,#146325,#146326,#146327,#146328,#146329,
#146330,#146331,#146332,#146333,#146334,#146335,#146336,#146337,#146338,
#146339,#146340,#146341,#146342,#146343,#146344,#146345,#146346,#146347,
#146348,#146349,#146350,#146351,#146352,#146353,#146354,#146355,#146356,
#146357,#146358,#146359,#146360,#146361,#146362,#146363,#146364,#146365,
#146366,#146367,#146368,#146369,#146370,#146371,#146372,#146373,#146374,
#146375,#146376,#146377,#146378,#146379,#146380,#146381,#146382,#146383,
#146384,#146385,#146386,#146387,#146388,#146389,#146390,#146391,#146392,
#146393,#146394,#146395,#146396,#146397,#146398,#146399,#146400,#146401,
#146402,#146403,#146404,#146405,#146406,#146407,#146408,#146409,#146410,
#146411,#146412,#146413,#146414,#146415,#146416,#146417,#146418,#146419,
#146420,#146421,#146422,#146423,#146424,#146425,#146426,#146427,#146428,
#146429,#146430,#146431,#146432,#146433,#146434,#146435,#146436,#146437,
#146438,#146439,#146440,#146441,#146442,#146443,#146444,#146445,#146446,
#146447,#146448,#146449,#146450,#146451,#146452,#146453,#146454,#146455,
#146456,#146457,#146458,#146459,#146460,#146461,#146462,#146463,#146464,
#146465,#146466,#146467,#146468,#146469,#146470,#146471,#146472,#146473,
#146474,#146475,#146476,#146477,#146478,#146479,#146480,#146481,#146482,
#146483,#146484,#146485,#146486,#146487,#146488,#146489,#146490,#146491,
#146492,#146493,#146494,#146495,#146496),.UNSPECIFIED.,.F.,.F.,(4,3,3,3,
3,3,3,3,3,3,3,3,3,3,3,3,3,3,3,3,3,3,3,3,3,3,3,3,3,3,3,3,3,3,3,3,3,3,3,3,
3,3,3,3,3,3,3,3,3,3,3,3,3,3,3,3,3,3,3,3,3,3,3,3,3,3,3,3,3,3,3,3,3,3,3,3,
3,3,3,3,3,4),(422.092270674546,422.170933835011,422.249534663302,422.329384397216,
422.407925778346,422.486463786289,422.565014963407,422.645844356209,422.72451167452,
422.806422104568,422.888332534615,422.968289834746,423.048152631989,423.12793845446,
423.207664769656,423.287348997949,423.36701998417,423.446687437696,423.526367088512,
423.606074670906,423.685869899982,423.765714241689,423.845672668736,423.888068545335,
423.968025845466,424.047888642709,424.12767446518,424.207400780376,424.28708500867,
424.366755994891,424.446423448417,424.526103099233,424.605810681627,424.685605910703,
424.76545025241,424.845408679457,424.887804556055,424.967761856186,425.047624653429,
425.127410475901,425.207136791096,425.28682101939,425.366492005611,425.446159459137,
425.525839109954,425.605546692348,425.685341921424,425.765186263132,425.845144690179,
425.887540566775,425.967497866906,426.047360664149,426.127146486621,426.206872801816,
426.28655703011,426.366228016331,426.445895469857,426.525575120673,426.605282703068,
426.685077932144,426.764922273852,426.844880700899,426.887276577495,426.967233877626,
427.047096674869,427.12688249734,427.206608812536,427.28629304083,427.365964027051,
427.445631480577,427.525311131393,427.605018713787,427.684813942863,427.76465828457,
427.844616711618,427.887012588215,427.971534865699,428.055911567113,428.14008793926,
428.224145636171,428.308038251325,428.375455981601),.UNSPECIFIED.);
#1197=B_SPLINE_CURVE_WITH_KNOTS('',3,(#146498,#146499,#146500,#146501,#146502,
#146503,#146504,#146505,#146506,#146507,#146508,#146509,#146510,#146511,
#146512,#146513,#146514,#146515,#146516,#146517,#146518,#146519,#146520,
#146521,#146522,#146523,#146524,#146525,#146526,#146527,#146528,#146529,
#146530,#146531,#146532,#146533,#146534,#146535,#146536,#146537,#146538,
#146539,#146540,#146541,#146542,#146543,#146544,#146545,#146546,#146547,
#146548,#146549,#146550,#146551,#146552,#146553,#146554,#146555,#146556,
#146557,#146558,#146559,#146560,#146561,#146562,#146563,#146564,#146565,
#146566,#146567,#146568,#146569,#146570,#146571,#146572,#146573,#146574,
#146575,#146576,#146577,#146578,#146579,#146580,#146581,#146582,#146583,
#146584,#146585,#146586,#146587,#146588,#146589,#146590,#146591,#146592,
#146593,#146594,#146595,#146596,#146597,#146598,#146599,#146600,#146601,
#146602,#146603,#146604,#146605,#146606,#146607,#146608,#146609,#146610,
#146611,#146612,#146613,#146614,#146615,#146616,#146617,#146618,#146619,
#146620,#146621,#146622,#146623,#146624,#146625,#146626,#146627,#146628,
#146629,#146630,#146631,#146632,#146633,#146634,#146635,#146636,#146637,
#146638,#146639,#146640,#146641,#146642,#146643,#146644,#146645,#146646,
#146647,#146648,#146649,#146650,#146651,#146652,#146653,#146654,#146655,
#146656,#146657,#146658,#146659,#146660,#146661,#146662,#146663,#146664,
#146665,#146666,#146667,#146668,#146669,#146670,#146671,#146672,#146673,
#146674,#146675,#146676,#146677,#146678,#146679,#146680,#146681,#146682,
#146683,#146684,#146685,#146686,#146687,#146688,#146689,#146690,#146691,
#146692,#146693,#146694,#146695,#146696,#146697,#146698,#146699,#146700,
#146701,#146702,#146703,#146704,#146705,#146706,#146707,#146708,#146709,
#146710,#146711,#146712,#146713,#146714,#146715,#146716,#146717,#146718,
#146719,#146720,#146721,#146722,#146723,#146724,#146725,#146726,#146727,
#146728,#146729,#146730,#146731,#146732,#146733,#146734,#146735,#146736,
#146737,#146738,#146739,#146740,#146741),.UNSPECIFIED.,.F.,.F.,(4,3,3,3,
3,3,3,3,3,3,3,3,3,3,3,3,3,3,3,3,3,3,3,3,3,3,3,3,3,3,3,3,3,3,3,3,3,3,3,3,
3,3,3,3,3,3,3,3,3,3,3,3,3,3,3,3,3,3,3,3,3,3,3,3,3,3,3,3,3,3,3,3,3,3,3,3,
3,3,3,3,3,4),(428.375455981726,428.458528660149,428.541692777151,428.627956732597,
428.711393977797,428.799071288366,428.886748598935,428.966705899066,429.046568696309,
429.126354518781,429.206080833977,429.285765062272,429.365436048493,429.445103502019,
429.524783152836,429.60449073523,429.684285964306,429.764130306014,429.844088733061,
429.886484609655,429.966441909786,430.046304707029,430.1260905295,430.205816844696,
430.28550107299,430.36517205921,430.444839512736,430.524519163553,430.604226745947,
430.684021975022,430.76386631673,430.843824743777,430.886220620375,430.966177920506,
431.046040717749,431.125826540221,431.205552855417,431.285237083711,431.364908069932,
431.444575523458,431.524255174275,431.60396275667,431.683757985745,431.763602327453,
431.843560754501,431.885956631096,431.965913931227,432.04577672847,432.125562550942,
432.205288866137,432.284973094431,432.364644080652,432.444311534178,432.523991184994,
432.603698767389,432.683493996464,432.763338338172,432.84329676522,432.885692641816,
432.965649941947,433.04551273919,433.125298561661,433.205024876856,433.284709105151,
433.364380091372,433.444047544898,433.523727195714,433.603434778108,433.683230007184,
433.763074348891,433.843032775938,433.885428652536,433.964333652462,434.04314326512,
434.121862540956,434.200530738074,434.279164394412,434.357780019542,434.436419696968,
434.515070068844,434.59378794452,434.658641288905),.UNSPECIFIED.);
#1198=B_SPLINE_CURVE_WITH_KNOTS('',3,(#146743,#146744,#146745,#146746,#146747,
#146748,#146749,#146750,#146751,#146752,#146753),.UNSPECIFIED.,.F.,.F.,
(4,1,1,1,1,1,1,1,4),(434.658641288905,434.885164663256,435.884900673976,
436.884636684696,437.884372695416,438.884108706137,439.883844716857,440.883580727577,
440.941826596085),.UNSPECIFIED.);
#1199=B_SPLINE_CURVE_WITH_KNOTS('',3,(#146755,#146756,#146757,#146758,#146759,
#146760,#146761,#146762,#146763,#146764,#146765,#146766,#146767,#146768,
#146769,#146770,#146771,#146772,#146773,#146774,#146775,#146776,#146777,
#146778,#146779,#146780,#146781,#146782,#146783,#146784,#146785,#146786,
#146787,#146788,#146789,#146790,#146791,#146792,#146793,#146794,#146795,
#146796,#146797,#146798,#146799,#146800,#146801,#146802,#146803,#146804,
#146805,#146806,#146807,#146808,#146809,#146810,#146811,#146812,#146813,
#146814,#146815,#146816,#146817,#146818,#146819,#146820,#146821,#146822,
#146823,#146824,#146825,#146826,#146827,#146828,#146829,#146830,#146831,
#146832,#146833,#146834,#146835,#146836,#146837,#146838,#146839,#146840,
#146841,#146842,#146843,#146844,#146845,#146846,#146847,#146848,#146849,
#146850,#146851,#146852,#146853,#146854,#146855,#146856,#146857,#146858,
#146859,#146860,#146861,#146862,#146863,#146864,#146865,#146866,#146867,
#146868,#146869,#146870,#146871,#146872,#146873,#146874,#146875,#146876,
#146877,#146878,#146879,#146880,#146881,#146882,#146883,#146884,#146885,
#146886,#146887,#146888,#146889,#146890,#146891,#146892,#146893,#146894,
#146895,#146896,#146897,#146898,#146899,#146900,#146901,#146902,#146903,
#146904,#146905,#146906,#146907,#146908,#146909,#146910,#146911,#146912,
#146913,#146914,#146915,#146916,#146917,#146918,#146919,#146920,#146921,
#146922,#146923,#146924,#146925,#146926,#146927,#146928,#146929,#146930,
#146931,#146932,#146933,#146934,#146935,#146936,#146937,#146938,#146939,
#146940,#146941,#146942,#146943,#146944,#146945,#146946,#146947,#146948,
#146949,#146950,#146951,#146952,#146953,#146954,#146955,#146956,#146957,
#146958,#146959,#146960,#146961,#146962,#146963,#146964,#146965,#146966,
#146967,#146968,#146969,#146970,#146971,#146972,#146973,#146974,#146975,
#146976,#146977,#146978,#146979,#146980,#146981,#146982,#146983,#146984,
#146985,#146986,#146987,#146988,#146989,#146990,#146991,#146992,#146993,
#146994,#146995,#146996,#146997,#146998),.UNSPECIFIED.,.F.,.F.,(4,3,3,3,
3,3,3,3,3,3,3,3,3,3,3,3,3,3,3,3,3,3,3,3,3,3,3,3,3,3,3,3,3,3,3,3,3,3,3,3,
3,3,3,3,3,3,3,3,3,3,3,3,3,3,3,3,3,3,3,3,3,3,3,3,3,3,3,3,3,3,3,3,3,3,3,3,
3,3,3,3,3,4),(440.941826596085,441.021075135616,441.100232923846,441.179318081556,
441.258348664094,441.337350274657,441.416338156607,441.495328576932,441.574337801935,
441.65342880663,441.732561735784,441.811815443062,441.883316738297,441.963274038428,
442.043136835671,442.122922658143,442.202648973338,442.282333201632,442.362004187853,
442.441671641379,442.521351292195,442.60105887459,442.680854103665,442.760698445373,
442.84065687242,442.883052749017,442.963010049148,443.042872846391,443.122658668863,
443.202384984058,443.282069212352,443.361740198573,443.441407652099,443.521087302915,
443.60079488531,443.680590114385,443.760434456093,443.84039288314,443.882788759737,
443.962746059868,444.042608857111,444.122394679583,444.202120994778,444.281805223072,
444.361476209293,444.441143662819,444.520823313635,444.60053089603,444.680326125105,
444.760170466813,444.84012889386,444.882524770457,444.962482070588,445.042344867831,
445.122130690303,445.201857005498,445.281541233792,445.361212220013,445.440879673539,
445.520559324355,445.600266906749,445.680062135825,445.759906477532,445.83986490458,
445.882260781177,445.962218081308,446.042080878551,446.121866701023,446.201593016219,
446.281277244513,446.360948230734,446.440615684261,446.520295335077,446.600002917472,
446.679798146548,446.759642488256,446.839600915303,446.881996791898,446.9750868076,
447.06780402742,447.159797907512,447.22501190315),.UNSPECIFIED.);
#1200=B_SPLINE_CURVE_WITH_KNOTS('',3,(#147000,#147001,#147002,#147003,#147004,
#147005,#147006,#147007,#147008,#147009,#147010,#147011,#147012,#147013,
#147014,#147015,#147016,#147017,#147018,#147019,#147020,#147021,#147022,
#147023,#147024,#147025,#147026,#147027,#147028,#147029,#147030,#147031,
#147032,#147033,#147034,#147035,#147036,#147037,#147038,#147039,#147040,
#147041,#147042,#147043,#147044,#147045,#147046,#147047,#147048,#147049,
#147050,#147051,#147052,#147053,#147054,#147055,#147056,#147057,#147058,
#147059,#147060,#147061,#147062,#147063,#147064,#147065,#147066,#147067,
#147068,#147069,#147070,#147071,#147072,#147073,#147074,#147075,#147076,
#147077,#147078,#147079,#147080,#147081,#147082,#147083,#147084,#147085,
#147086,#147087,#147088,#147089,#147090,#147091,#147092,#147093,#147094,
#147095,#147096,#147097,#147098,#147099,#147100,#147101,#147102,#147103,
#147104,#147105,#147106,#147107,#147108,#147109,#147110,#147111,#147112,
#147113,#147114,#147115,#147116,#147117,#147118,#147119,#147120,#147121,
#147122,#147123,#147124,#147125,#147126,#147127,#147128,#147129,#147130,
#147131,#147132,#147133,#147134,#147135,#147136,#147137,#147138,#147139,
#147140,#147141,#147142,#147143,#147144,#147145,#147146,#147147,#147148,
#147149,#147150,#147151,#147152,#147153,#147154,#147155,#147156,#147157,
#147158,#147159,#147160,#147161,#147162,#147163,#147164,#147165,#147166,
#147167,#147168,#147169,#147170,#147171,#147172,#147173,#147174,#147175,
#147176,#147177,#147178,#147179,#147180,#147181,#147182,#147183,#147184,
#147185,#147186,#147187,#147188,#147189,#147190,#147191,#147192,#147193,
#147194,#147195,#147196,#147197,#147198,#147199,#147200,#147201,#147202,
#147203,#147204,#147205,#147206,#147207,#147208,#147209,#147210,#147211,
#147212,#147213,#147214,#147215,#147216,#147217,#147218,#147219,#147220,
#147221,#147222,#147223,#147224,#147225,#147226,#147227,#147228,#147229,
#147230,#147231,#147232,#147233,#147234,#147235,#147236,#147237,#147238,
#147239,#147240,#147241,#147242,#147243,#147244,#147245,#147246),
 .UNSPECIFIED.,.F.,.F.,(4,3,3,3,3,3,3,3,3,3,3,3,3,3,3,3,3,3,3,3,3,3,3,3,
3,3,3,3,3,3,3,3,3,3,3,3,3,3,3,3,3,3,3,3,3,3,3,3,3,3,3,3,3,3,3,3,3,3,3,3,
3,3,3,3,3,3,3,3,3,3,3,3,3,3,3,3,3,3,3,3,3,3,4),(447.225011903265,447.307102015684,
447.386849490768,447.466604468513,447.546382529658,447.630220097898,447.710136669819,
447.790112257442,447.8701997552,447.881732802618,447.961690102749,448.041552899992,
448.121338722464,448.201065037659,448.280749265953,448.360420252173,448.440087705699,
448.519767356516,448.59947493891,448.679270167986,448.759114509693,448.83907293674,
448.881468813338,448.961426113469,449.041288910712,449.121074733183,449.200801048379,
449.280485276673,449.360156262894,449.43982371642,449.519503367236,449.599210949631,
449.679006178707,449.758850520414,449.838808947461,449.881204824058,449.961162124189,
450.041024921432,450.120810743904,450.2005370591,450.280221287394,450.359892273615,
450.439559727141,450.519239377957,450.598946960352,450.678742189427,450.758586531135,
450.838544958183,450.880940834778,450.960898134909,451.040760932152,451.120546754624,
451.200273069819,451.279957298114,451.359628284335,451.439295737861,451.518975388677,
451.598682971072,451.678478200147,451.758322541855,451.838280968902,451.880676845498,
451.960634145629,452.040496942872,452.120282765343,452.200009080539,452.279693308832,
452.359364295054,452.43903174858,452.518711399396,452.598418981791,452.678214210866,
452.758058552574,452.838016979622,452.880412856218,452.960970301763,453.041430143191,
453.121807583264,453.202117770593,453.28237162908,453.362591658213,453.442803262859,
453.508197210444),.UNSPECIFIED.);
#1201=B_SPLINE_CURVE_WITH_KNOTS('',3,(#147248,#147249,#147250,#147251,#147252,
#147253,#147254,#147255,#147256,#147257),.UNSPECIFIED.,.F.,.F.,(4,1,1,1,
1,1,1,4),(453.508204888342,453.880148866938,454.879884877659,455.879620888379,
456.879356899099,457.879092909819,458.878828920539,459.791373789161),
 .UNSPECIFIED.);
#1202=B_SPLINE_CURVE_WITH_KNOTS('',3,(#147259,#147260,#147261,#147262,#147263,
#147264,#147265,#147266,#147267,#147268,#147269,#147270,#147271,#147272,
#147273,#147274,#147275,#147276,#147277,#147278,#147279,#147280,#147281,
#147282,#147283,#147284,#147285,#147286,#147287,#147288,#147289,#147290,
#147291,#147292,#147293,#147294,#147295,#147296,#147297,#147298,#147299,
#147300,#147301,#147302,#147303,#147304,#147305,#147306,#147307,#147308,
#147309,#147310,#147311,#147312,#147313,#147314,#147315,#147316,#147317,
#147318,#147319,#147320,#147321,#147322,#147323,#147324,#147325,#147326,
#147327,#147328,#147329,#147330,#147331,#147332,#147333,#147334,#147335,
#147336,#147337,#147338,#147339,#147340,#147341,#147342,#147343,#147344,
#147345,#147346,#147347,#147348,#147349,#147350,#147351,#147352,#147353,
#147354,#147355,#147356,#147357,#147358,#147359,#147360,#147361,#147362,
#147363,#147364,#147365,#147366,#147367,#147368,#147369,#147370,#147371,
#147372,#147373,#147374,#147375,#147376,#147377,#147378,#147379,#147380,
#147381,#147382,#147383,#147384,#147385,#147386,#147387,#147388,#147389,
#147390,#147391,#147392,#147393,#147394,#147395,#147396,#147397,#147398,
#147399,#147400,#147401,#147402,#147403,#147404,#147405,#147406,#147407,
#147408,#147409,#147410,#147411,#147412,#147413,#147414,#147415,#147416,
#147417,#147418,#147419,#147420,#147421,#147422,#147423,#147424,#147425,
#147426,#147427,#147428,#147429,#147430,#147431,#147432,#147433,#147434,
#147435,#147436,#147437,#147438,#147439,#147440,#147441,#147442,#147443,
#147444,#147445,#147446,#147447,#147448,#147449,#147450,#147451,#147452,
#147453,#147454,#147455,#147456,#147457,#147458,#147459,#147460,#147461,
#147462,#147463,#147464,#147465,#147466,#147467,#147468,#147469,#147470,
#147471,#147472,#147473,#147474,#147475,#147476,#147477,#147478,#147479,
#147480,#147481,#147482,#147483,#147484,#147485,#147486,#147487,#147488,
#147489,#147490,#147491,#147492,#147493,#147494,#147495,#147496,#147497,
#147498,#147499,#147500,#147501,#147502),.UNSPECIFIED.,.F.,.F.,(4,3,3,3,
3,3,3,3,3,3,3,3,3,3,3,3,3,3,3,3,3,3,3,3,3,3,3,3,3,3,3,3,3,3,3,3,3,3,3,3,
3,3,3,3,3,3,3,3,3,3,3,3,3,3,3,3,3,3,3,3,3,3,3,3,3,3,3,3,3,3,3,3,3,3,3,3,
3,3,3,3,3,4),(459.791382517624,459.878564931259,459.95852223139,460.038385028633,
460.118170851104,460.1978971663,460.277581394593,460.357252380814,460.43691983434,
460.516599485156,460.596307067551,460.676102296626,460.755946638334,460.835905065381,
460.878300941979,460.95825824211,461.038121039353,461.117906861825,461.19763317702,
461.277317405314,461.356988391535,461.436655845061,461.516335495877,461.596043078271,
461.675838307347,461.755682649054,461.835641076102,461.878036952699,461.95799425283,
462.037857050073,462.117642872545,462.197369187741,462.277053416035,462.356724402256,
462.436391855782,462.516071506599,462.595779088994,462.675574318069,462.755418659777,
462.835377086825,462.87777296342,462.957730263551,463.037593060794,463.117378883266,
463.197105198461,463.276789426755,463.356460412976,463.436127866502,463.515807517319,
463.595515099713,463.675310328789,463.755154670496,463.835113097544,463.87750897414,
463.957466274271,464.037329071514,464.117114893985,464.196841209181,464.276525437475,
464.356196423695,464.435863877221,464.515543528038,464.595251110432,464.675046339507,
464.754890681215,464.834849108262,464.87724498486,464.957202284991,465.037065082234,
465.116850904706,465.196577219901,465.276261448196,465.355932434417,465.435599887943,
465.515279538759,465.594987121154,465.674782350229,465.754626691937,465.834585118985,
465.87698099558,465.99246734354,466.074567824803),.UNSPECIFIED.);
#1203=B_SPLINE_CURVE_WITH_KNOTS('',3,(#147504,#147505,#147506,#147507,#147508,
#147509,#147510,#147511,#147512,#147513),.UNSPECIFIED.,.F.,.F.,(4,1,1,1,
1,1,1,4),(466.074571330478,466.8767170063,467.87645301702,468.87618902774,
469.875925038461,470.875661049181,471.875397059901,472.357753131983),
 .UNSPECIFIED.);
#1204=B_SPLINE_CURVE_WITH_KNOTS('',3,(#147515,#147516,#147517,#147518,#147519,
#147520,#147521,#147522,#147523,#147524),.UNSPECIFIED.,.F.,.F.,(4,1,1,1,
1,1,1,4),(472.357753131983,472.875133070621,473.874869081341,474.874605092061,
475.874341102781,476.874077113501,477.873813124221,478.640938439162),
 .UNSPECIFIED.);
#1205=B_SPLINE_CURVE_WITH_KNOTS('',3,(#147526,#147527,#147528,#147529,#147530,
#147531,#147532,#147533,#147534,#147535,#147536),.UNSPECIFIED.,.F.,.F.,
(4,1,1,1,1,1,1,1,4),(478.640938439162,478.873549134942,479.873285145662,
480.873021156382,481.872757167102,482.872493177822,483.872229188542,484.871965199263,
484.924123746342),.UNSPECIFIED.);
#1206=B_SPLINE_CURVE_WITH_KNOTS('',3,(#147538,#147539,#147540,#147541,#147542,
#147543,#147544,#147545,#147546,#147547),.UNSPECIFIED.,.F.,.F.,(4,1,1,1,
1,1,1,4),(484.924123746342,485.871701209983,486.871437220703,487.871173231423,
488.870909242143,489.870645252863,490.870381263583,491.207301539485),
 .UNSPECIFIED.);
#1207=B_SPLINE_CURVE_WITH_KNOTS('',3,(#147549,#147550,#147551,#147552,#147553,
#147554,#147555,#147556,#147557,#147558,#147559,#147560,#147561,#147562,
#147563,#147564,#147565,#147566,#147567,#147568,#147569,#147570,#147571,
#147572,#147573,#147574,#147575,#147576,#147577,#147578,#147579,#147580,
#147581,#147582,#147583,#147584,#147585,#147586,#147587,#147588,#147589,
#147590,#147591,#147592,#147593,#147594,#147595,#147596,#147597,#147598,
#147599,#147600,#147601,#147602,#147603,#147604,#147605,#147606,#147607,
#147608,#147609,#147610,#147611,#147612,#147613,#147614,#147615,#147616,
#147617,#147618,#147619,#147620,#147621,#147622,#147623,#147624,#147625,
#147626,#147627,#147628,#147629,#147630,#147631,#147632,#147633,#147634,
#147635,#147636,#147637,#147638,#147639,#147640,#147641,#147642,#147643,
#147644,#147645,#147646,#147647,#147648,#147649,#147650,#147651,#147652,
#147653,#147654,#147655,#147656,#147657,#147658,#147659,#147660,#147661,
#147662,#147663,#147664,#147665,#147666,#147667,#147668,#147669,#147670,
#147671,#147672,#147673,#147674,#147675,#147676,#147677,#147678,#147679,
#147680,#147681,#147682,#147683,#147684,#147685,#147686,#147687,#147688,
#147689,#147690,#147691,#147692,#147693,#147694,#147695,#147696,#147697,
#147698,#147699,#147700,#147701,#147702,#147703,#147704,#147705,#147706,
#147707,#147708,#147709,#147710,#147711,#147712,#147713,#147714,#147715,
#147716,#147717,#147718,#147719,#147720,#147721,#147722,#147723,#147724,
#147725,#147726,#147727,#147728,#147729,#147730,#147731,#147732,#147733,
#147734,#147735,#147736,#147737,#147738,#147739,#147740,#147741,#147742,
#147743,#147744,#147745,#147746,#147747,#147748,#147749,#147750,#147751,
#147752,#147753,#147754,#147755,#147756,#147757,#147758,#147759,#147760,
#147761,#147762,#147763,#147764,#147765,#147766,#147767,#147768,#147769,
#147770,#147771,#147772,#147773,#147774,#147775,#147776,#147777,#147778,
#147779,#147780,#147781,#147782,#147783,#147784,#147785,#147786,#147787,
#147788,#147789,#147790,#147791,#147792,#147793,#147794,#147795),
 .UNSPECIFIED.,.F.,.F.,(4,3,3,3,3,3,3,3,3,3,3,3,3,3,3,3,3,3,3,3,3,3,3,3,
3,3,3,3,3,3,3,3,3,3,3,3,3,3,3,3,3,3,3,3,3,3,3,3,3,3,3,3,3,3,3,3,3,3,3,3,
3,3,3,3,3,3,3,3,3,3,3,3,3,3,3,3,3,3,3,3,3,3,4),(491.207309053522,491.29016008112,
491.36981928176,491.449483679156,491.529168945053,491.608890760716,491.688708275316,
491.768582379995,491.848570368169,491.870117274303,491.950074574434,492.029937371677,
492.109723194149,492.189449509344,492.269133737638,492.348804723859,492.428472177385,
492.508151828201,492.587859410595,492.667654639671,492.747498981378,492.827457408426,
492.869853285023,492.949810585154,493.029673382397,493.109459204869,493.189185520065,
493.268869748359,493.34854073458,493.428208188107,493.507887838923,493.587595421318,
493.667390650394,493.747234992102,493.827193419149,493.869589295744,493.949546595875,
494.029409393118,494.109195215589,494.188921530785,494.268605759078,494.348276745299,
494.427944198825,494.507623849641,494.587331432035,494.667126661111,494.746971002818,
494.826929429866,494.869325306464,494.949282606595,495.029145403838,495.108931226309,
495.188657541505,495.268341769799,495.34801275602,495.427680209546,495.507359860362,
495.587067442756,495.666862671832,495.74670701354,495.826665440587,495.869061317184,
495.949018617315,496.028881414558,496.10866723703,496.188393552226,496.268077780519,
496.347748766741,496.427416220267,496.507095871083,496.586803453478,496.666598682554,
496.746443024261,496.826401451308,496.868797327904,496.949472541059,497.030049103338,
497.110542076934,497.190966469049,497.271331757617,497.351661880682,497.431979636697,
497.490494360701),.UNSPECIFIED.);
#1208=B_SPLINE_CURVE_WITH_KNOTS('',3,(#147797,#147798,#147799,#147800,#147801,
#147802,#147803,#147804,#147805,#147806),.UNSPECIFIED.,.F.,.F.,(4,1,1,1,
1,1,1,4),(497.490501958073,497.868533338624,498.868269349344,499.868005360064,
500.867741370785,501.867477381505,502.867213392225,503.773670660106),
 .UNSPECIFIED.);
#1209=B_SPLINE_CURVE_WITH_KNOTS('',3,(#147808,#147809,#147810,#147811,#147812,
#147813,#147814,#147815,#147816,#147817,#147818,#147819,#147820,#147821,
#147822,#147823,#147824,#147825,#147826,#147827,#147828,#147829,#147830,
#147831,#147832,#147833,#147834,#147835,#147836,#147837,#147838,#147839,
#147840,#147841,#147842,#147843,#147844,#147845,#147846,#147847,#147848,
#147849,#147850,#147851,#147852,#147853,#147854,#147855,#147856,#147857,
#147858,#147859,#147860,#147861,#147862,#147863,#147864,#147865,#147866,
#147867,#147868,#147869,#147870,#147871,#147872,#147873,#147874,#147875,
#147876,#147877,#147878,#147879,#147880,#147881,#147882,#147883,#147884,
#147885,#147886,#147887,#147888,#147889,#147890,#147891,#147892,#147893,
#147894,#147895,#147896,#147897,#147898,#147899,#147900,#147901,#147902,
#147903,#147904,#147905,#147906,#147907,#147908,#147909,#147910,#147911,
#147912,#147913,#147914,#147915,#147916,#147917,#147918,#147919,#147920,
#147921,#147922,#147923,#147924,#147925,#147926,#147927,#147928,#147929,
#147930,#147931,#147932,#147933,#147934,#147935,#147936,#147937,#147938,
#147939,#147940,#147941,#147942,#147943,#147944,#147945,#147946,#147947,
#147948,#147949,#147950,#147951,#147952,#147953,#147954,#147955,#147956,
#147957,#147958,#147959,#147960,#147961,#147962,#147963,#147964,#147965,
#147966,#147967,#147968,#147969,#147970,#147971,#147972,#147973,#147974,
#147975,#147976,#147977,#147978,#147979,#147980,#147981,#147982,#147983,
#147984,#147985,#147986,#147987,#147988,#147989,#147990,#147991,#147992,
#147993,#147994,#147995,#147996,#147997,#147998,#147999,#148000,#148001,
#148002,#148003,#148004,#148005,#148006,#148007,#148008,#148009,#148010,
#148011,#148012,#148013,#148014,#148015,#148016,#148017,#148018,#148019,
#148020,#148021,#148022,#148023,#148024,#148025,#148026,#148027,#148028,
#148029,#148030,#148031,#148032,#148033,#148034,#148035,#148036,#148037,
#148038,#148039,#148040,#148041,#148042,#148043,#148044,#148045,#148046,
#148047,#148048,#148049,#148050,#148051),.UNSPECIFIED.,.F.,.F.,(4,3,3,3,
3,3,3,3,3,3,3,3,3,3,3,3,3,3,3,3,3,3,3,3,3,3,3,3,3,3,3,3,3,3,3,3,3,3,3,3,
3,3,3,3,3,3,3,3,3,3,3,3,3,3,3,3,3,3,3,3,3,3,3,3,3,3,3,3,3,3,3,3,3,3,3,3,
3,3,3,3,3,4),(503.773679667881,503.866949402945,503.946906703076,504.026769500319,
504.106555322791,504.186281637986,504.26596586628,504.345636852501,504.425304306027,
504.504983956843,504.584691539238,504.664486768314,504.744331110021,504.824289537068,
504.866685413665,504.946642713796,505.026505511039,505.106291333511,505.186017648706,
505.265701877,505.345372863221,505.425040316747,505.504719967563,505.584427549958,
505.664222779033,505.744067120741,505.824025547788,505.866421424385,505.946378724516,
506.026241521759,506.106027344231,506.185753659426,506.26543788772,506.345108873941,
506.424776327467,506.504455978284,506.584163560678,506.663958789754,506.743803131461,
506.823761558509,506.866157435105,506.946114735236,507.025977532479,507.105763354951,
507.185489670146,507.26517389844,507.344844884661,507.424512338188,507.504191989004,
507.583899571399,507.663694800474,507.743539142182,507.82349756923,507.865893445826,
507.945850745957,508.0257135432,508.105499365672,508.185225680867,508.264909909161,
508.344580895382,508.424248348908,508.503927999725,508.58363558212,508.663430811195,
508.743275152903,508.82323357995,508.865629456546,508.945586756677,509.02544955392,
509.105235376392,509.184961691587,509.264645919881,509.344316906102,509.423984359628,
509.503664010445,509.583371592839,509.663166821915,509.743011163623,509.82296959067,
509.865365467266,509.982757991064,510.05686497506),.UNSPECIFIED.);
#1210=B_SPLINE_CURVE_WITH_KNOTS('',3,(#148053,#148054,#148055,#148056,#148057,
#148058,#148059,#148060,#148061,#148062),.UNSPECIFIED.,.F.,.F.,(4,1,1,1,
1,1,1,4),(510.056869064338,510.865101477986,511.864837488706,512.864573499426,
513.864309510146,514.864045520866,515.863781531586,516.34005028224),
 .UNSPECIFIED.);
#1211=B_SPLINE_CURVE_WITH_KNOTS('',3,(#148064,#148065,#148066,#148067,#148068,
#148069,#148070,#148071,#148072,#148073),.UNSPECIFIED.,.F.,.F.,(4,1,1,1,
1,1,1,4),(516.34005028224,516.863517542307,517.863253553027,518.862989563747,
519.862725574467,520.862461585187,521.862197595907,522.623235589419),
 .UNSPECIFIED.);
#1212=B_SPLINE_CURVE_WITH_KNOTS('',3,(#148075,#148076,#148077,#148078,#148079,
#148080,#148081,#148082,#148083,#148084,#148085),.UNSPECIFIED.,.F.,.F.,
(4,1,1,1,1,1,1,1,4),(522.623235589419,522.861933606627,523.861669617348,
524.861405628068,525.861141638788,526.860877649508,527.860613660228,528.860349670948,
528.906420896599),.UNSPECIFIED.);
#1213=B_SPLINE_CURVE_WITH_KNOTS('',3,(#148087,#148088,#148089,#148090,#148091,
#148092,#148093,#148094,#148095,#148096),.UNSPECIFIED.,.F.,.F.,(4,1,1,1,
1,1,1,4),(528.906420896599,529.860085681668,530.859821692388,531.859557703109,
532.859293713829,533.859029724549,534.858765735269,535.189598872372),
 .UNSPECIFIED.);
#1214=B_SPLINE_CURVE_WITH_KNOTS('',3,(#148098,#148099,#148100,#148101,#148102,
#148103,#148104,#148105,#148106,#148107,#148108,#148109,#148110,#148111,
#148112,#148113,#148114,#148115,#148116,#148117,#148118,#148119,#148120,
#148121,#148122,#148123,#148124,#148125,#148126,#148127,#148128,#148129,
#148130,#148131,#148132,#148133,#148134,#148135,#148136,#148137,#148138,
#148139,#148140,#148141,#148142,#148143,#148144,#148145,#148146,#148147,
#148148,#148149,#148150,#148151,#148152,#148153,#148154,#148155,#148156,
#148157,#148158,#148159,#148160,#148161,#148162,#148163,#148164,#148165,
#148166,#148167,#148168,#148169,#148170,#148171,#148172,#148173,#148174,
#148175,#148176,#148177,#148178,#148179,#148180,#148181,#148182,#148183,
#148184,#148185,#148186,#148187,#148188,#148189,#148190,#148191,#148192,
#148193,#148194,#148195,#148196,#148197,#148198,#148199,#148200,#148201,
#148202,#148203,#148204,#148205,#148206,#148207,#148208,#148209,#148210,
#148211,#148212,#148213,#148214,#148215,#148216,#148217,#148218,#148219,
#148220,#148221,#148222,#148223,#148224,#148225,#148226,#148227,#148228,
#148229,#148230,#148231,#148232,#148233,#148234,#148235,#148236,#148237,
#148238,#148239,#148240,#148241,#148242,#148243,#148244,#148245,#148246,
#148247,#148248,#148249,#148250,#148251,#148252,#148253,#148254,#148255,
#148256,#148257,#148258,#148259,#148260,#148261,#148262,#148263,#148264,
#148265,#148266,#148267,#148268,#148269,#148270,#148271,#148272,#148273,
#148274,#148275,#148276,#148277,#148278,#148279,#148280,#148281,#148282,
#148283,#148284,#148285,#148286,#148287,#148288,#148289,#148290,#148291,
#148292,#148293,#148294,#148295,#148296,#148297,#148298,#148299,#148300,
#148301,#148302,#148303,#148304,#148305,#148306,#148307,#148308,#148309,
#148310,#148311,#148312,#148313,#148314,#148315,#148316,#148317,#148318,
#148319,#148320,#148321,#148322,#148323,#148324,#148325,#148326,#148327,
#148328,#148329,#148330,#148331,#148332,#148333,#148334,#148335,#148336,
#148337,#148338,#148339,#148340,#148341,#148342,#148343,#148344),
 .UNSPECIFIED.,.F.,.F.,(4,3,3,3,3,3,3,3,3,3,3,3,3,3,3,3,3,3,3,3,3,3,3,3,
3,3,3,3,3,3,3,3,3,3,3,3,3,3,3,3,3,3,3,3,3,3,3,3,3,3,3,3,3,3,3,3,3,3,3,3,
3,3,3,3,3,3,3,3,3,3,3,3,3,3,3,3,3,3,3,3,3,3,4),(535.189606203779,535.273218146555,
535.352792787086,535.432370387379,535.511966703241,535.591597498818,535.671322497607,
535.751102402933,535.83099710307,535.858501745989,535.93845904612,536.018321843363,
536.098107665835,536.17783398103,536.257518209324,536.337189195545,536.416856649071,
536.496536299887,536.576243882282,536.656039111357,536.735883453065,536.815841880112,
536.858237756709,536.93819505684,537.018057854083,537.097843676555,537.17756999175,
537.257254220045,537.336925206266,537.416592659792,537.496272310609,537.575979893003,
537.655775122079,537.735619463787,537.815577890834,537.857973767429,537.93793106756,
538.017793864803,538.097579687275,538.17730600247,538.256990230764,538.336661216985,
538.416328670511,538.496008321327,538.575715903721,538.655511132797,538.735355474505,
538.815313901552,538.857709778149,538.93766707828,539.017529875523,539.097315697994,
539.17704201319,539.256726241484,539.336397227705,539.416064681231,539.495744332047,
539.575451914442,539.655247143517,539.735091485225,539.815049912272,539.857445788869,
539.937403089,540.017265886243,540.097051708715,540.176778023911,540.256462252206,
540.336133238427,540.415800691953,540.49548034277,540.575187925165,540.65498315424,
540.734827495948,540.814785922996,540.85718179959,540.937979098972,541.018676641078,
541.099289335752,541.179832036869,541.260312775082,541.340756917768,541.4211847832,
541.472791510958),.UNSPECIFIED.);
#1215=B_SPLINE_CURVE_WITH_KNOTS('',3,(#148346,#148347,#148348,#148349,#148350,
#148351,#148352,#148353,#148354,#148355),.UNSPECIFIED.,.F.,.F.,(4,1,1,1,
1,1,1,4),(541.472798990514,541.85691781031,542.85665382103,543.85638983175,
544.85612584247,545.85586185319,546.85559786391,547.755967729876),
 .UNSPECIFIED.);
#1216=B_SPLINE_CURVE_WITH_KNOTS('',3,(#148357,#148358,#148359,#148360,#148361,
#148362,#148363,#148364,#148365,#148366,#148367,#148368,#148369,#148370,
#148371,#148372,#148373,#148374,#148375,#148376,#148377,#148378,#148379,
#148380,#148381,#148382,#148383,#148384,#148385,#148386,#148387,#148388,
#148389,#148390,#148391,#148392,#148393,#148394,#148395,#148396,#148397,
#148398,#148399,#148400,#148401,#148402,#148403,#148404,#148405,#148406,
#148407,#148408,#148409,#148410,#148411,#148412,#148413,#148414,#148415,
#148416,#148417,#148418,#148419,#148420,#148421,#148422,#148423,#148424,
#148425,#148426,#148427,#148428,#148429,#148430,#148431,#148432,#148433,
#148434,#148435,#148436,#148437,#148438,#148439,#148440,#148441,#148442,
#148443,#148444,#148445,#148446,#148447,#148448,#148449,#148450,#148451,
#148452,#148453,#148454,#148455,#148456,#148457,#148458,#148459,#148460,
#148461,#148462,#148463,#148464,#148465,#148466,#148467,#148468,#148469,
#148470,#148471,#148472,#148473,#148474,#148475,#148476,#148477,#148478,
#148479,#148480,#148481,#148482,#148483,#148484,#148485,#148486,#148487,
#148488,#148489,#148490,#148491,#148492,#148493,#148494,#148495,#148496,
#148497,#148498,#148499,#148500,#148501,#148502,#148503,#148504,#148505,
#148506,#148507,#148508,#148509,#148510,#148511,#148512,#148513,#148514,
#148515,#148516,#148517,#148518,#148519,#148520,#148521,#148522,#148523,
#148524,#148525,#148526,#148527,#148528,#148529,#148530,#148531,#148532,
#148533,#148534,#148535,#148536,#148537,#148538,#148539,#148540,#148541,
#148542,#148543,#148544,#148545,#148546,#148547,#148548,#148549,#148550,
#148551,#148552,#148553,#148554,#148555,#148556,#148557,#148558,#148559,
#148560,#148561,#148562,#148563,#148564,#148565,#148566,#148567,#148568,
#148569,#148570,#148571,#148572,#148573,#148574,#148575,#148576,#148577,
#148578,#148579,#148580,#148581,#148582,#148583,#148584,#148585,#148586,
#148587,#148588,#148589,#148590,#148591,#148592,#148593,#148594,#148595,
#148596,#148597,#148598,#148599,#148600),.UNSPECIFIED.,.F.,.F.,(4,3,3,3,
3,3,3,3,3,3,3,3,3,3,3,3,3,3,3,3,3,3,3,3,3,3,3,3,3,3,3,3,3,3,3,3,3,3,3,3,
3,3,3,3,3,3,3,3,3,3,3,3,3,3,3,3,3,3,3,3,3,3,3,3,3,3,3,3,3,3,3,3,3,3,3,3,
3,3,3,3,3,4),(547.755976818138,547.85533387463,547.935291174761,548.015153972004,
548.094939794476,548.174666109672,548.254350337966,548.334021324187,548.413688777713,
548.49336842853,548.573076010925,548.65287124,548.732715581708,548.812674008755,
548.855069885351,548.935027185482,549.014889982725,549.094675805197,549.174402120392,
549.254086348686,549.333757334907,549.413424788432,549.493104439249,549.572812021643,
549.652607250719,549.732451592426,549.812410019474,549.854805896071,549.934763196202,
550.014625993445,550.094411815916,550.174138131111,550.253822359405,550.333493345626,
550.413160799152,550.492840449969,550.572548032363,550.652343261439,550.732187603146,
550.812146030193,550.854541906791,550.934499206922,551.014362004165,551.094147826637,
551.173874141832,551.253558370126,551.333229356347,551.412896809873,551.49257646069,
551.572284043085,551.65207927216,551.731923613868,551.811882040915,551.854277917511,
551.934235217642,552.014098014885,552.093883837357,552.173610152552,552.253294380846,
552.332965367067,552.412632820593,552.492312471409,552.572020053803,552.651815282879,
552.731659624587,552.811618051634,552.854013928231,552.933971228362,553.013834025605,
553.093619848077,553.173346163272,553.253030391566,553.332701377787,553.412368831313,
553.492048482129,553.571756064523,553.651551293599,553.731395635307,553.811354062354,
553.853749938951,553.973211235292,554.039162125317),.UNSPECIFIED.);
#1217=B_SPLINE_CURVE_WITH_KNOTS('',3,(#148602,#148603,#148604,#148605,#148606,
#148607,#148608,#148609,#148610,#148611),.UNSPECIFIED.,.F.,.F.,(4,1,1,1,
1,1,1,4),(554.039166781551,554.853485949671,555.853221960391,556.852957971112,
557.852693981832,558.852429992552,559.852166003272,560.322347432497),
 .UNSPECIFIED.);
#1218=B_SPLINE_CURVE_WITH_KNOTS('',3,(#148613,#148614,#148615,#148616,#148617,
#148618,#148619,#148620,#148621,#148622),.UNSPECIFIED.,.F.,.F.,(4,1,1,1,
1,1,1,4),(560.322347432497,560.851902013992,561.851638024712,562.851374035433,
563.851110046153,564.850846056873,565.850582067593,566.605532739676),
 .UNSPECIFIED.);
#1219=B_SPLINE_CURVE_WITH_KNOTS('',3,(#148624,#148625,#148626,#148627,#148628,
#148629,#148630,#148631,#148632,#148633,#148634,#148635,#148636,#148637,
#148638,#148639,#148640,#148641,#148642,#148643,#148644,#148645,#148646,
#148647,#148648,#148649,#148650,#148651,#148652,#148653,#148654,#148655,
#148656,#148657,#148658,#148659,#148660,#148661,#148662,#148663,#148664,
#148665,#148666,#148667,#148668,#148669,#148670,#148671,#148672,#148673,
#148674,#148675,#148676,#148677,#148678,#148679,#148680,#148681,#148682,
#148683,#148684,#148685,#148686,#148687,#148688,#148689,#148690,#148691,
#148692,#148693,#148694,#148695,#148696,#148697,#148698,#148699,#148700,
#148701,#148702,#148703,#148704,#148705,#148706,#148707,#148708,#148709,
#148710,#148711,#148712,#148713,#148714,#148715,#148716,#148717,#148718,
#148719,#148720,#148721,#148722,#148723,#148724,#148725,#148726,#148727,
#148728,#148729,#148730,#148731,#148732,#148733,#148734,#148735,#148736,
#148737,#148738,#148739,#148740,#148741,#148742,#148743,#148744,#148745,
#148746,#148747,#148748,#148749,#148750,#148751,#148752,#148753,#148754,
#148755,#148756,#148757,#148758,#148759,#148760,#148761,#148762,#148763,
#148764,#148765,#148766,#148767,#148768,#148769,#148770,#148771,#148772,
#148773,#148774,#148775,#148776,#148777,#148778,#148779,#148780,#148781,
#148782,#148783,#148784,#148785,#148786,#148787,#148788,#148789,#148790,
#148791,#148792,#148793,#148794,#148795,#148796,#148797,#148798,#148799,
#148800,#148801,#148802,#148803,#148804,#148805,#148806,#148807,#148808,
#148809,#148810,#148811,#148812,#148813,#148814,#148815,#148816,#148817,
#148818,#148819,#148820,#148821,#148822,#148823,#148824,#148825,#148826,
#148827,#148828,#148829,#148830,#148831,#148832,#148833,#148834,#148835,
#148836,#148837,#148838,#148839,#148840,#148841,#148842,#148843,#148844,
#148845,#148846,#148847,#148848,#148849,#148850,#148851,#148852,#148853,
#148854,#148855,#148856,#148857,#148858,#148859,#148860,#148861,#148862,
#148863,#148864,#148865,#148866,#148867,#148868,#148869,#148870),
 .UNSPECIFIED.,.F.,.F.,(4,3,3,3,3,3,3,3,3,3,3,3,3,3,3,3,3,3,3,3,3,3,3,3,
3,3,3,3,3,3,3,3,3,3,3,3,3,3,3,3,3,3,3,3,3,3,3,3,3,3,3,3,3,3,3,3,3,3,3,3,
3,3,3,3,3,3,3,3,3,3,3,3,3,3,3,3,3,3,3,3,3,3,4),(566.60553281651,566.708754002674,
566.814418024236,566.850318078313,566.930275378444,567.010138175686,567.089923998157,
567.169650313352,567.249334541646,567.329005527866,567.408672981392,567.488352632208,
567.568060214602,567.647855443677,567.727699785384,567.807658212431,567.850054089033,
567.930011389164,568.009874186407,568.089660008879,568.169386324074,568.249070552368,
568.328741538589,568.408408992115,568.488088642932,568.567796225326,568.647591454402,
568.727435796109,568.807394223157,568.849790099753,568.929747399884,569.009610197127,
569.089396019599,569.169122334794,569.248806563088,569.328477549309,569.408145002835,
569.487824653652,569.567532236047,569.647327465122,569.72717180683,569.807130233877,
569.849526110473,569.929483410604,570.009346207847,570.089132030318,570.168858345514,
570.248542573808,570.328213560028,570.407881013554,570.487560664371,570.567268246765,
570.64706347584,570.726907817548,570.806866244595,570.849262121193,570.929219421324,
571.009082218567,571.088868041039,571.168594356235,571.248278584529,571.32794957075,
571.407617024276,571.487296675093,571.567004257488,571.646799486564,571.726643828271,
571.806602255319,571.848998131914,571.928955432045,572.008818229288,572.08860405176,
572.168330366955,572.24801459525,572.327685581471,572.407353034997,572.487032685813,
572.566740268208,572.646535497284,572.726379838991,572.806338266039,572.848734142634,
572.888718046856),.UNSPECIFIED.);
#1220=B_SPLINE_CURVE_WITH_KNOTS('',3,(#148872,#148873,#148874,#148875,#148876,
#148877,#148878,#148879,#148880,#148881),.UNSPECIFIED.,.F.,.F.,(4,1,1,1,
1,1,1,4),(572.88872350849,573.848470153354,574.848206164074,575.847942174794,
576.847678185514,577.847414196235,578.847150206955,579.171903354036),
 .UNSPECIFIED.);
#1221=B_SPLINE_CURVE_WITH_KNOTS('',3,(#148883,#148884,#148885,#148886,#148887,
#148888,#148889,#148890,#148891,#148892),.UNSPECIFIED.,.F.,.F.,(4,1,1,1,
1,1,1,4),(579.171903354036,579.846886217675,580.846622228395,581.846358239115,
582.846094249835,583.845830260555,584.845566271275,585.455088661215),
 .UNSPECIFIED.);
#1222=B_SPLINE_CURVE_WITH_KNOTS('',3,(#148894,#148895,#148896,#148897,#148898,
#148899,#148900,#148901,#148902,#148903),.UNSPECIFIED.,.F.,.F.,(4,1,1,1,
1,1,1,4),(585.455088661215,585.845302281995,586.845038292716,587.844774303436,
588.844510314156,589.844246324876,590.843982335596,591.738273968395),
 .UNSPECIFIED.);
#1223=B_SPLINE_CURVE_WITH_KNOTS('',3,(#148905,#148906,#148907,#148908,#148909,
#148910,#148911,#148912,#148913,#148914,#148915,#148916),.UNSPECIFIED.,
 .F.,.F.,(4,2,1,1,1,1,1,1,4),(591.738273968395,591.843718346316,592.843454357036,
593.843190367756,594.842926378477,595.842662389197,596.842398399917,597.842134410637,
598.021459275574),.UNSPECIFIED.);
#1224=B_SPLINE_CURVE_WITH_KNOTS('',3,(#148918,#148919,#148920,#148921,#148922,
#148923,#148924,#148925,#148926,#148927,#148928,#148929,#148930,#148931,
#148932,#148933,#148934,#148935,#148936,#148937,#148938,#148939,#148940,
#148941,#148942,#148943,#148944,#148945,#148946,#148947,#148948,#148949,
#148950,#148951,#148952,#148953,#148954,#148955,#148956,#148957,#148958,
#148959,#148960,#148961,#148962,#148963,#148964,#148965,#148966,#148967,
#148968,#148969,#148970,#148971,#148972,#148973,#148974,#148975,#148976,
#148977,#148978,#148979,#148980,#148981,#148982,#148983,#148984,#148985,
#148986,#148987,#148988,#148989,#148990,#148991,#148992,#148993,#148994,
#148995,#148996,#148997,#148998,#148999,#149000,#149001,#149002,#149003,
#149004,#149005,#149006,#149007,#149008,#149009,#149010,#149011,#149012,
#149013,#149014,#149015,#149016,#149017,#149018,#149019,#149020,#149021,
#149022,#149023,#149024,#149025,#149026,#149027,#149028,#149029,#149030,
#149031,#149032,#149033,#149034,#149035,#149036,#149037,#149038,#149039,
#149040,#149041,#149042,#149043,#149044,#149045,#149046,#149047,#149048,
#149049,#149050,#149051,#149052,#149053,#149054,#149055,#149056,#149057,
#149058,#149059,#149060,#149061,#149062,#149063,#149064,#149065,#149066,
#149067,#149068,#149069,#149070,#149071,#149072,#149073,#149074,#149075,
#149076,#149077,#149078,#149079,#149080,#149081,#149082,#149083,#149084,
#149085,#149086,#149087,#149088,#149089,#149090,#149091,#149092,#149093,
#149094,#149095,#149096,#149097,#149098,#149099,#149100,#149101,#149102,
#149103,#149104,#149105,#149106,#149107,#149108,#149109,#149110,#149111,
#149112,#149113,#149114,#149115,#149116,#149117,#149118,#149119,#149120,
#149121,#149122,#149123,#149124,#149125,#149126,#149127,#149128,#149129,
#149130,#149131,#149132,#149133,#149134,#149135,#149136,#149137,#149138,
#149139,#149140,#149141,#149142,#149143,#149144,#149145,#149146,#149147,
#149148,#149149,#149150,#149151,#149152,#149153,#149154,#149155,#149156,
#149157,#149158,#149159,#149160,#149161,#149162,#149163,#149164),
 .UNSPECIFIED.,.F.,.F.,(4,3,3,3,3,3,3,3,3,3,3,3,3,3,3,3,3,3,3,3,3,3,3,3,
3,3,3,3,3,3,3,3,3,3,3,3,3,3,3,3,3,3,3,3,3,3,3,3,3,3,3,3,3,3,3,3,3,3,3,3,
3,3,3,3,3,3,3,3,3,3,3,3,3,3,3,3,3,3,3,3,3,3,4),(598.021459275574,598.100103166507,
598.178678499566,598.257203660822,598.335705731097,598.414198623025,598.492698903982,
598.571223145469,598.649829847877,598.728483691741,598.807246837996,598.841870421357,
598.921827721488,599.001690518731,599.081476341203,599.161202656398,599.240886884692,
599.320557870912,599.400225324438,599.479904975255,599.55961255765,599.639407786725,
599.719252128433,599.79921055548,599.841606432077,599.921563732208,600.001426529451,
600.081212351923,600.160938667118,600.240622895412,600.320293881633,600.399961335159,
600.479640985975,600.55934856837,600.639143797445,600.718988139153,600.7989465662,
600.841342442797,600.921299742928,601.001162540171,601.080948362644,601.160674677839,
601.240358906133,601.320029892354,601.39969734588,601.479376996697,601.559084579092,
601.638879808168,601.718724149876,601.798682576923,601.841078453518,601.921035753649,
602.000898550892,602.080684373364,602.160410688559,602.240094916853,602.319765903074,
602.3994333566,602.479113007416,602.55882058981,602.638615818886,602.718460160594,
602.798418587641,602.840814464238,602.920771764369,603.000634561611,603.080420384083,
603.160146699278,603.239830927572,603.319501913793,603.399169367319,603.478849018135,
603.558556600529,603.638351829605,603.718196171312,603.798154598359,603.840550474958,
603.926106881067,604.011500138433,604.096661221207,604.181679898875,604.26649877441,
604.304644387162),.UNSPECIFIED.);
#1225=B_SPLINE_CURVE_WITH_KNOTS('',3,(#149166,#149167,#149168,#149169,#149170,
#149171,#149172,#149173,#149174,#149175),.UNSPECIFIED.,.F.,.F.,(4,1,1,1,
1,1,1,4),(604.304644582754,604.840286485678,605.840022496398,606.839758507118,
607.839494517838,608.839230528559,609.838966539279,610.587829889933),
 .UNSPECIFIED.);
#1226=B_SPLINE_CURVE_WITH_KNOTS('',3,(#149177,#149178,#149179,#149180,#149181,
#149182,#149183,#149184,#149185,#149186,#149187,#149188,#149189,#149190,
#149191,#149192,#149193,#149194,#149195,#149196,#149197,#149198,#149199,
#149200,#149201,#149202,#149203,#149204,#149205,#149206,#149207,#149208,
#149209,#149210,#149211,#149212,#149213,#149214,#149215,#149216,#149217,
#149218,#149219,#149220,#149221,#149222,#149223,#149224,#149225,#149226,
#149227,#149228,#149229,#149230,#149231,#149232,#149233,#149234,#149235,
#149236,#149237,#149238,#149239,#149240,#149241,#149242,#149243,#149244,
#149245,#149246,#149247,#149248,#149249,#149250,#149251,#149252,#149253,
#149254,#149255,#149256,#149257,#149258,#149259,#149260,#149261,#149262,
#149263,#149264,#149265,#149266,#149267,#149268,#149269,#149270,#149271,
#149272,#149273,#149274,#149275,#149276,#149277,#149278,#149279,#149280,
#149281,#149282,#149283,#149284,#149285,#149286,#149287,#149288,#149289,
#149290,#149291,#149292,#149293,#149294,#149295,#149296,#149297,#149298,
#149299,#149300,#149301,#149302,#149303,#149304,#149305,#149306,#149307,
#149308,#149309,#149310,#149311,#149312,#149313,#149314,#149315,#149316,
#149317,#149318,#149319,#149320,#149321,#149322,#149323,#149324,#149325,
#149326,#149327,#149328,#149329,#149330,#149331,#149332,#149333,#149334,
#149335,#149336,#149337,#149338,#149339,#149340,#149341,#149342,#149343,
#149344,#149345,#149346,#149347,#149348,#149349,#149350,#149351,#149352,
#149353,#149354,#149355,#149356,#149357,#149358,#149359,#149360,#149361,
#149362,#149363,#149364,#149365,#149366,#149367,#149368,#149369,#149370,
#149371,#149372,#149373,#149374,#149375,#149376,#149377,#149378,#149379,
#149380,#149381,#149382,#149383,#149384,#149385,#149386,#149387,#149388,
#149389,#149390,#149391,#149392,#149393,#149394,#149395,#149396,#149397,
#149398,#149399,#149400,#149401,#149402,#149403,#149404,#149405,#149406,
#149407,#149408,#149409,#149410,#149411,#149412,#149413,#149414,#149415,
#149416,#149417,#149418,#149419,#149420,#149421,#149422,#149423),
 .UNSPECIFIED.,.F.,.F.,(4,3,3,3,3,3,3,3,3,3,3,3,3,3,3,3,3,3,3,3,3,3,3,3,
3,3,3,3,3,3,3,3,3,3,3,3,3,3,3,3,3,3,3,3,3,3,3,3,3,3,3,3,3,3,3,3,3,3,3,3,
3,3,3,3,3,3,3,3,3,3,3,3,3,3,3,3,3,3,3,3,3,3,4),(610.587829947008,610.690094159622,
610.794601151968,610.838702549999,610.91865985013,610.998522647371,611.078308469843,
611.158034785037,611.237719013331,611.317389999551,611.397057453076,611.476737103892,
611.556444686285,611.63623991536,611.716084257067,611.796042684113,611.838438560719,
611.91839586085,611.998258658093,612.078044480565,612.15777079576,612.237455024055,
612.317126010276,612.396793463802,612.476473114618,612.556180697013,612.635975926088,
612.715820267796,612.795778694843,612.838174571439,612.91813187157,612.997994668813,
613.077780491285,613.15750680648,613.237191034775,613.316862020996,613.396529474522,
613.476209125338,613.555916707733,613.635711936808,613.715556278516,613.795514705563,
613.837910582159,613.91786788229,613.997730679533,614.077516502004,614.1572428172,
614.236927045494,614.316598031715,614.39626548524,614.475945136057,614.555652718451,
614.635447947527,614.715292289234,614.795250716281,614.837646592879,614.91760389301,
614.997466690253,615.077252512725,615.15697882792,615.236663056215,615.316334042436,
615.396001495962,615.475681146778,615.555388729173,615.635183958249,615.715028299957,
615.794986727004,615.837382603599,615.91733990373,615.997202700973,616.076988523444,
616.15671483864,616.236399066934,616.316070053155,616.395737506681,616.475417157497,
616.555124739891,616.634919968967,616.714764310675,616.794722737722,616.837118614319,
616.871015197113),.UNSPECIFIED.);
#1227=B_SPLINE_CURVE_WITH_KNOTS('',3,(#149425,#149426,#149427,#149428,#149429,
#149430,#149431,#149432,#149433,#149434),.UNSPECIFIED.,.F.,.F.,(4,1,1,1,
1,1,1,4),(616.871019818576,617.836854625039,618.836590635759,619.83632664648,
620.8360626572,621.83579866792,622.83553467864,623.154200504292),
 .UNSPECIFIED.);
#1228=B_SPLINE_CURVE_WITH_KNOTS('',3,(#149436,#149437,#149438,#149439,#149440,
#149441,#149442,#149443,#149444,#149445),.UNSPECIFIED.,.F.,.F.,(4,1,1,1,
1,1,1,4),(623.154200504292,623.83527068936,624.83500670008,625.834742710801,
626.834478721521,627.834214732241,628.833950742961,629.437385811472),
 .UNSPECIFIED.);
#1229=B_SPLINE_CURVE_WITH_KNOTS('',3,(#149447,#149448,#149449,#149450,#149451,
#149452,#149453,#149454,#149455,#149456),.UNSPECIFIED.,.F.,.F.,(4,1,1,1,
1,1,1,4),(629.437385811472,629.833686753681,630.833422764401,631.833158775121,
632.832894785842,633.832630796561,634.832366807282,635.720571118652),
 .UNSPECIFIED.);
#1230=B_SPLINE_CURVE_WITH_KNOTS('',3,(#149458,#149459,#149460,#149461,#149462,
#149463,#149464,#149465,#149466,#149467,#149468),.UNSPECIFIED.,.F.,.F.,
(4,1,1,1,1,1,1,1,4),(635.720571118652,635.832102818002,636.831838828722,
637.831574839442,638.831310850162,639.831046860882,640.830782871603,641.830518882323,
642.003756425831),.UNSPECIFIED.);
#1231=B_SPLINE_CURVE_WITH_KNOTS('',3,(#149470,#149471,#149472,#149473,#149474,
#149475,#149476,#149477,#149478,#149479,#149480,#149481,#149482,#149483,
#149484,#149485,#149486,#149487,#149488,#149489,#149490,#149491,#149492,
#149493,#149494,#149495,#149496,#149497,#149498,#149499,#149500,#149501,
#149502,#149503,#149504,#149505,#149506,#149507,#149508,#149509,#149510,
#149511,#149512,#149513,#149514,#149515,#149516,#149517,#149518,#149519,
#149520,#149521,#149522,#149523,#149524,#149525,#149526,#149527,#149528,
#149529,#149530,#149531,#149532,#149533,#149534,#149535,#149536,#149537,
#149538,#149539,#149540,#149541,#149542,#149543,#149544,#149545,#149546,
#149547,#149548,#149549,#149550,#149551,#149552,#149553,#149554,#149555,
#149556,#149557,#149558,#149559,#149560,#149561,#149562,#149563,#149564,
#149565,#149566,#149567,#149568,#149569,#149570,#149571,#149572,#149573,
#149574,#149575,#149576,#149577,#149578,#149579,#149580,#149581,#149582,
#149583,#149584,#149585,#149586,#149587,#149588,#149589,#149590,#149591,
#149592,#149593,#149594,#149595,#149596,#149597,#149598,#149599,#149600,
#149601,#149602,#149603,#149604,#149605,#149606,#149607,#149608,#149609,
#149610,#149611,#149612,#149613,#149614,#149615,#149616,#149617,#149618,
#149619,#149620,#149621,#149622,#149623,#149624,#149625,#149626,#149627,
#149628,#149629,#149630,#149631,#149632,#149633,#149634,#149635,#149636,
#149637,#149638,#149639,#149640,#149641,#149642,#149643,#149644,#149645,
#149646,#149647,#149648,#149649,#149650,#149651,#149652,#149653,#149654,
#149655,#149656,#149657,#149658,#149659,#149660,#149661,#149662,#149663,
#149664,#149665,#149666,#149667,#149668,#149669,#149670,#149671,#149672,
#149673,#149674,#149675,#149676,#149677,#149678,#149679,#149680,#149681,
#149682,#149683,#149684,#149685,#149686,#149687,#149688,#149689,#149690,
#149691,#149692,#149693,#149694,#149695,#149696,#149697,#149698,#149699,
#149700,#149701,#149702,#149703,#149704,#149705,#149706,#149707,#149708,
#149709,#149710,#149711,#149712,#149713,#149714,#149715,#149716),
 .UNSPECIFIED.,.F.,.F.,(4,3,3,3,3,3,3,3,3,3,3,3,3,3,3,3,3,3,3,3,3,3,3,3,
3,3,3,3,3,3,3,3,3,3,3,3,3,3,3,3,3,3,3,3,3,3,3,3,3,3,3,3,3,3,3,3,3,3,3,3,
3,3,3,3,3,3,3,3,3,3,3,3,3,3,3,3,3,3,3,3,3,3,4),(642.003756425831,642.082402951354,
642.160979450999,642.239504318118,642.318004216256,642.396493621382,642.474989103083,
642.553507234078,642.632107218901,642.710753169526,642.789509990212,642.830254893043,
642.910212193174,642.990074990417,643.069860812889,643.149587128084,643.229271356378,
643.308942342599,643.388609796125,643.468289446942,643.547997029336,643.627792258412,
643.707636600119,643.787595027166,643.829990903763,643.909948203894,643.989811001137,
644.069596823609,644.149323138804,644.229007367098,644.308678353319,644.388345806845,
644.468025457662,644.547733040056,644.627528269132,644.70737261084,644.787331037887,
644.829726914483,644.909684214614,644.989547011857,645.069332834328,645.149059149524,
645.228743377818,645.308414364038,645.388081817564,645.467761468381,645.547469050775,
645.627264279851,645.707108621558,645.787067048606,645.829462925203,645.909420225334,
645.989283022577,646.069068845049,646.148795160244,646.228479388538,646.308150374759,
646.387817828285,646.467497479101,646.547205061496,646.627000290572,646.706844632279,
646.786803059327,646.829198935923,646.909156236054,646.989019033297,647.068804855769,
647.148531170965,647.228215399259,647.30788638548,647.387553839006,647.467233489822,
647.546941072216,647.626736301292,647.706580642999,647.786539070046,647.828934946643,
647.914770615256,648.000437967126,648.08586396628,648.171140400706,648.256207607788,
648.28694150642),.UNSPECIFIED.);
#1232=B_SPLINE_CURVE_WITH_KNOTS('',3,(#149718,#149719,#149720,#149721,#149722,
#149723,#149724,#149725,#149726,#149727),.UNSPECIFIED.,.F.,.F.,(4,1,1,1,
1,1,1,4),(648.286941733011,648.828670957363,649.828406968084,650.828142978804,
651.827878989524,652.827615000244,653.827351010964,654.57012704019),
 .UNSPECIFIED.);
#1233=B_SPLINE_CURVE_WITH_KNOTS('',3,(#149729,#149730,#149731,#149732,#149733,
#149734,#149735,#149736,#149737,#149738,#149739),.UNSPECIFIED.,.F.,.F.,
(4,1,1,1,1,1,1,1,4),(654.57012704019,654.827087021684,655.826823032404,
656.826559043124,657.826295053845,658.826031064565,659.825767075285,660.825503086005,
660.85331234737),.UNSPECIFIED.);
#1234=B_SPLINE_CURVE_WITH_KNOTS('',3,(#149741,#149742,#149743,#149744,#149745,
#149746,#149747,#149748,#149749,#149750,#149751,#149752,#149753,#149754,
#149755,#149756,#149757,#149758,#149759,#149760,#149761,#149762,#149763,
#149764,#149765,#149766,#149767,#149768,#149769,#149770,#149771,#149772,
#149773,#149774,#149775,#149776,#149777,#149778,#149779,#149780,#149781,
#149782,#149783,#149784,#149785,#149786,#149787,#149788,#149789,#149790,
#149791,#149792,#149793,#149794,#149795,#149796,#149797,#149798,#149799,
#149800,#149801,#149802,#149803,#149804,#149805,#149806,#149807,#149808,
#149809,#149810,#149811,#149812,#149813,#149814,#149815,#149816,#149817,
#149818,#149819,#149820,#149821,#149822,#149823,#149824,#149825,#149826,
#149827,#149828,#149829,#149830,#149831,#149832,#149833,#149834,#149835,
#149836,#149837,#149838,#149839,#149840,#149841,#149842,#149843,#149844,
#149845,#149846,#149847,#149848,#149849,#149850,#149851,#149852,#149853,
#149854,#149855,#149856,#149857,#149858,#149859,#149860,#149861,#149862,
#149863,#149864,#149865,#149866,#149867,#149868,#149869,#149870,#149871,
#149872,#149873,#149874,#149875,#149876,#149877,#149878,#149879,#149880,
#149881,#149882,#149883,#149884,#149885,#149886,#149887,#149888,#149889,
#149890,#149891,#149892,#149893,#149894,#149895,#149896,#149897,#149898,
#149899,#149900,#149901,#149902,#149903,#149904,#149905,#149906,#149907,
#149908,#149909,#149910,#149911,#149912,#149913,#149914,#149915,#149916,
#149917,#149918,#149919,#149920,#149921,#149922,#149923,#149924,#149925,
#149926,#149927,#149928,#149929,#149930,#149931,#149932,#149933,#149934,
#149935,#149936,#149937,#149938,#149939,#149940,#149941,#149942,#149943,
#149944,#149945,#149946,#149947,#149948,#149949,#149950,#149951,#149952,
#149953,#149954,#149955,#149956,#149957,#149958,#149959,#149960,#149961,
#149962,#149963,#149964,#149965,#149966,#149967,#149968,#149969,#149970,
#149971,#149972,#149973,#149974,#149975,#149976,#149977,#149978,#149979,
#149980,#149981,#149982,#149983,#149984,#149985,#149986,#149987),
 .UNSPECIFIED.,.F.,.F.,(4,3,3,3,3,3,3,3,3,3,3,3,3,3,3,3,3,3,3,3,3,3,3,3,
3,3,3,3,3,3,3,3,3,3,3,3,3,3,3,3,3,3,3,3,3,3,3,3,3,3,3,3,3,3,3,3,3,3,3,3,
3,3,3,3,3,3,3,3,3,3,3,3,3,3,3,3,3,3,3,3,3,3,4),(660.85331234737,660.93289668504,
661.012387538856,661.09180277648,661.171160202289,661.252920064094,661.332226639779,
661.411532635294,661.490854085283,661.570207031294,661.649648079436,661.729142021672,
661.808742750969,661.825239096725,661.905196396856,661.985059194099,662.06484501657,
662.144571331765,662.224255560059,662.30392654628,662.383593999806,662.463273650622,
662.542981233017,662.622776462092,662.7026208038,662.782579230847,662.824975107445,
662.904932407576,662.984795204819,663.064581027291,663.144307342487,663.223991570781,
663.303662557002,663.383330010528,663.463009661345,663.542717243739,663.622512472815,
663.702356814523,663.782315241571,663.824711118166,663.904668418297,663.98453121554,
664.064317038012,664.144043353207,664.223727581501,664.303398567722,664.383066021248,
664.462745672064,664.542453254459,664.622248483534,664.702092825242,664.78205125229,
664.824447128886,664.904404429017,664.98426722626,665.064053048731,665.143779363927,
665.223463592221,665.303134578442,665.382802031968,665.462481682784,665.542189265178,
665.621984494254,665.701828835961,665.781787263009,665.824183139606,665.904140439737,
665.98400323698,666.063789059453,666.143515374648,666.223199602942,666.302870589163,
666.382538042689,666.462217693506,666.5419252759,666.621720504976,666.701564846683,
666.781523273731,666.823919150326,666.919981952889,667.01551406519,667.110071646987,
667.136497447219),.UNSPECIFIED.);
#1235=B_SPLINE_CURVE_WITH_KNOTS('',3,(#149989,#149990,#149991,#149992,#149993,
#149994,#149995,#149996,#149997,#149998),.UNSPECIFIED.,.F.,.F.,(4,1,1,1,
1,1,1,4),(667.136497654549,667.823655161046,668.823391171766,669.823127182486,
670.822863193206,671.822599203926,672.822335214646,673.419682961729),
 .UNSPECIFIED.);
#1236=B_SPLINE_CURVE_WITH_KNOTS('',3,(#150000,#150001,#150002,#150003,#150004,
#150005,#150006,#150007,#150008,#150009,#150010,#150011,#150012,#150013,
#150014,#150015,#150016,#150017,#150018,#150019,#150020,#150021,#150022,
#150023,#150024,#150025,#150026,#150027,#150028,#150029,#150030,#150031,
#150032,#150033,#150034,#150035,#150036,#150037,#150038,#150039,#150040,
#150041,#150042,#150043,#150044,#150045,#150046,#150047,#150048,#150049,
#150050,#150051,#150052,#150053,#150054,#150055,#150056,#150057,#150058,
#150059,#150060,#150061,#150062,#150063,#150064,#150065,#150066,#150067,
#150068,#150069,#150070,#150071,#150072,#150073,#150074,#150075,#150076,
#150077,#150078,#150079,#150080,#150081,#150082,#150083,#150084,#150085,
#150086,#150087,#150088,#150089,#150090,#150091,#150092,#150093,#150094,
#150095,#150096,#150097,#150098,#150099,#150100,#150101,#150102,#150103,
#150104,#150105,#150106,#150107,#150108,#150109,#150110,#150111,#150112,
#150113,#150114,#150115,#150116,#150117,#150118,#150119,#150120,#150121,
#150122,#150123,#150124,#150125,#150126,#150127,#150128,#150129,#150130,
#150131,#150132,#150133,#150134,#150135,#150136,#150137,#150138,#150139,
#150140,#150141,#150142,#150143,#150144,#150145,#150146,#150147,#150148,
#150149,#150150,#150151,#150152,#150153,#150154,#150155,#150156,#150157,
#150158,#150159,#150160,#150161,#150162,#150163,#150164,#150165,#150166,
#150167,#150168,#150169,#150170,#150171,#150172,#150173,#150174,#150175,
#150176,#150177,#150178,#150179,#150180,#150181,#150182,#150183,#150184,
#150185,#150186,#150187,#150188,#150189,#150190,#150191,#150192,#150193,
#150194,#150195,#150196,#150197,#150198,#150199,#150200,#150201,#150202,
#150203,#150204,#150205,#150206,#150207,#150208,#150209,#150210,#150211,
#150212,#150213,#150214,#150215,#150216,#150217,#150218,#150219,#150220,
#150221,#150222,#150223,#150224,#150225,#150226,#150227,#150228,#150229,
#150230,#150231,#150232,#150233,#150234,#150235,#150236,#150237,#150238,
#150239,#150240,#150241,#150242,#150243,#150244,#150245,#150246),
 .UNSPECIFIED.,.F.,.F.,(4,3,3,3,3,3,3,3,3,3,3,3,3,3,3,3,3,3,3,3,3,3,3,3,
3,3,3,3,3,3,3,3,3,3,3,3,3,3,3,3,3,3,3,3,3,3,3,3,3,3,3,3,3,3,3,3,3,3,3,3,
3,3,3,3,3,3,3,3,3,3,3,3,3,3,3,3,3,3,3,3,3,3,4),(673.419683183978,673.507475405285,
673.595719432381,673.684192986917,673.772987001415,673.822071225367,673.902028525498,
673.981891322741,674.061677145213,674.141403460408,674.221087688703,674.300758674924,
674.38042612845,674.460105779266,674.539813361661,674.619608590737,674.699452932444,
674.779411359492,674.821807236087,674.901764536218,674.981627333461,675.061413155933,
675.141139471128,675.220823699422,675.300494685643,675.380162139169,675.459841789985,
675.53954937238,675.619344601455,675.699188943163,675.77914737021,675.821543246807,
675.901500546938,675.981363344181,676.061149166653,676.140875481848,676.220559710142,
676.300230696363,676.379898149889,676.459577800705,676.539285383099,676.619080612175,
676.698924953882,676.77888338093,676.821279257527,676.901236557658,676.981099354901,
677.060885177373,677.140611492568,677.220295720862,677.299966707083,677.379634160609,
677.459313811426,677.53902139382,677.618816622896,677.698660964603,677.778619391651,
677.821015268247,677.900972568378,677.980835365621,678.060621188092,678.140347503288,
678.220031731582,678.299702717803,678.379370171329,678.459049822145,678.53875740454,
678.618552633615,678.698396975322,678.77835540237,678.820751278967,678.89962025868,
678.978395497203,679.057095415522,679.137817022195,679.216425133687,679.295017936498,
679.373611941843,679.45592602361,679.534608192868,679.613332891335,679.692148113422,
679.702868268909),.UNSPECIFIED.);
#1237=B_SPLINE_CURVE_WITH_KNOTS('',3,(#150248,#150249,#150250,#150251,#150252,
#150253,#150254,#150255,#150256,#150257,#150258,#150259),.UNSPECIFIED.,
 .F.,.F.,(4,2,1,1,1,1,1,1,4),(679.702868268909,679.820487289687,680.820223300408,
681.819959311128,682.819695321848,683.819431332568,684.819167343288,685.818903354008,
685.986053576088),.UNSPECIFIED.);
#1238=B_SPLINE_CURVE_WITH_KNOTS('',3,(#150261,#150262,#150263,#150264,#150265,
#150266,#150267,#150268,#150269,#150270),.UNSPECIFIED.,.F.,.F.,(4,1,1,1,
1,1,1,4),(685.986053576088,686.818639364728,687.818375375449,688.818111386169,
689.817847396889,690.817583407609,691.817319418329,692.269238883268),
 .UNSPECIFIED.);
#1239=B_SPLINE_CURVE_WITH_KNOTS('',3,(#150272,#150273,#150274,#150275,#150276,
#150277,#150278,#150279,#150280,#150281),.UNSPECIFIED.,.F.,.F.,(4,1,1,1,
1,1,1,4),(692.269238883268,692.817055429049,693.816791439769,694.81652745049,
695.81626346121,696.81599947193,697.81573548265,698.552424190447),
 .UNSPECIFIED.);
#1240=B_SPLINE_CURVE_WITH_KNOTS('',3,(#150283,#150284,#150285,#150286,#150287,
#150288,#150289,#150290,#150291,#150292,#150293),.UNSPECIFIED.,.F.,.F.,
(4,1,1,1,1,1,1,1,4),(698.552424190447,698.81547149337,699.81520750409,700.81494351481,
701.81467952553,702.814415536251,703.814151546971,704.813887557691,704.835609497627),
 .UNSPECIFIED.);
#1241=B_SPLINE_CURVE_WITH_KNOTS('',3,(#150295,#150296,#150297,#150298,#150299,
#150300,#150301,#150302,#150303,#150304,#150305,#150306,#150307,#150308,
#150309,#150310,#150311,#150312,#150313,#150314,#150315,#150316,#150317,
#150318,#150319,#150320,#150321,#150322,#150323,#150324,#150325,#150326,
#150327,#150328,#150329,#150330,#150331,#150332,#150333,#150334,#150335,
#150336,#150337,#150338,#150339,#150340,#150341,#150342,#150343,#150344,
#150345,#150346,#150347,#150348,#150349,#150350,#150351,#150352,#150353,
#150354,#150355,#150356,#150357,#150358,#150359,#150360,#150361,#150362,
#150363,#150364,#150365,#150366,#150367,#150368,#150369,#150370,#150371,
#150372,#150373,#150374,#150375,#150376,#150377,#150378,#150379,#150380,
#150381,#150382,#150383,#150384,#150385,#150386,#150387,#150388,#150389,
#150390,#150391,#150392,#150393,#150394,#150395,#150396,#150397,#150398,
#150399,#150400,#150401,#150402,#150403,#150404,#150405,#150406,#150407,
#150408,#150409,#150410,#150411,#150412,#150413,#150414,#150415,#150416,
#150417,#150418,#150419,#150420,#150421,#150422,#150423,#150424,#150425,
#150426,#150427,#150428,#150429,#150430,#150431,#150432,#150433,#150434,
#150435,#150436,#150437,#150438,#150439,#150440,#150441,#150442,#150443,
#150444,#150445,#150446,#150447,#150448,#150449,#150450,#150451,#150452,
#150453,#150454,#150455,#150456,#150457,#150458,#150459,#150460,#150461,
#150462,#150463,#150464,#150465,#150466,#150467,#150468,#150469,#150470,
#150471,#150472,#150473,#150474,#150475,#150476,#150477,#150478,#150479,
#150480,#150481,#150482,#150483,#150484,#150485,#150486,#150487,#150488,
#150489,#150490,#150491,#150492,#150493,#150494,#150495,#150496,#150497,
#150498,#150499,#150500,#150501,#150502,#150503,#150504,#150505,#150506,
#150507,#150508,#150509,#150510,#150511,#150512,#150513,#150514,#150515,
#150516,#150517,#150518,#150519,#150520,#150521,#150522,#150523,#150524,
#150525,#150526,#150527,#150528,#150529,#150530,#150531,#150532,#150533,
#150534,#150535,#150536,#150537,#150538,#150539,#150540,#150541),
 .UNSPECIFIED.,.F.,.F.,(4,3,3,3,3,3,3,3,3,3,3,3,3,3,3,3,3,3,3,3,3,3,3,3,
3,3,3,3,3,3,3,3,3,3,3,3,3,3,3,3,3,3,3,3,3,3,3,3,3,3,3,3,3,3,3,3,3,3,3,3,
3,3,3,3,3,3,3,3,3,3,3,3,3,3,3,3,3,3,3,3,3,3,4),(704.835609497627,704.915270034789,
704.994836731164,705.074327390111,705.153759752259,705.236242729278,705.315622886734,
705.395001979489,705.474395984204,705.553820883933,705.633333846027,705.712899052128,
705.792572327826,705.813623568411,705.893580868542,705.973443665785,706.053229488257,
706.132955803452,706.212640031746,706.292311017967,706.371978471493,706.451658122309,
706.531365704703,706.611160933779,706.691005275486,706.770963702534,706.813359579131,
706.893316879262,706.973179676505,707.052965498977,707.132691814172,707.212376042466,
707.292047028687,707.371714482213,707.451394133029,707.531101715423,707.610896944499,
707.690741286207,707.770699713254,707.813095589851,707.893052889982,707.972915687225,
708.052701509696,708.132427824892,708.212112053186,708.291783039407,708.371450492933,
708.45113014375,708.530837726144,708.61063295522,708.690477296927,708.770435723975,
708.812831600571,708.892788900702,708.972651697945,709.052437520416,709.132163835612,
709.211848063906,709.291519050127,709.371186503653,709.450866154469,709.530573736864,
709.610368965939,709.690213307647,709.770171734694,709.812567611291,709.892524911422,
709.972387708665,710.052173531137,710.131899846332,710.211584074626,710.291255060847,
710.370922514373,710.45060216519,710.530309747585,710.610104976661,710.689949318368,
710.769907745416,710.812303622012,710.909040597874,711.005203662865,711.100327550192,
711.118794607969),.UNSPECIFIED.);
#1242=B_SPLINE_CURVE_WITH_KNOTS('',3,(#150543,#150544,#150545,#150546,#150547,
#150548,#150549,#150550,#150551,#150552),.UNSPECIFIED.,.F.,.F.,(4,1,1,1,
1,1,1,4),(711.118794804806,711.812039632732,712.811775643452,713.811511654172,
714.811247664892,715.810983675612,716.810719686332,717.401980111986),
 .UNSPECIFIED.);
#1243=B_SPLINE_CURVE_WITH_KNOTS('',3,(#150554,#150555,#150556,#150557,#150558,
#150559,#150560,#150561,#150562,#150563,#150564,#150565,#150566,#150567,
#150568,#150569,#150570,#150571,#150572,#150573,#150574,#150575,#150576,
#150577,#150578,#150579,#150580,#150581,#150582,#150583,#150584,#150585,
#150586,#150587,#150588,#150589,#150590,#150591,#150592,#150593,#150594,
#150595,#150596,#150597,#150598,#150599,#150600,#150601,#150602,#150603,
#150604,#150605,#150606,#150607,#150608,#150609,#150610,#150611,#150612,
#150613,#150614,#150615,#150616,#150617,#150618,#150619,#150620,#150621,
#150622,#150623,#150624,#150625,#150626,#150627,#150628,#150629,#150630,
#150631,#150632,#150633,#150634,#150635,#150636,#150637,#150638,#150639,
#150640,#150641,#150642,#150643,#150644,#150645,#150646,#150647,#150648,
#150649,#150650,#150651,#150652,#150653,#150654,#150655,#150656,#150657,
#150658,#150659,#150660,#150661,#150662,#150663,#150664,#150665,#150666,
#150667,#150668,#150669,#150670,#150671,#150672,#150673,#150674,#150675,
#150676,#150677,#150678,#150679,#150680,#150681,#150682,#150683,#150684,
#150685,#150686,#150687,#150688,#150689,#150690,#150691,#150692,#150693,
#150694,#150695,#150696,#150697,#150698,#150699,#150700,#150701,#150702,
#150703,#150704,#150705,#150706,#150707,#150708,#150709,#150710,#150711,
#150712,#150713,#150714,#150715,#150716,#150717,#150718,#150719,#150720,
#150721,#150722,#150723,#150724,#150725,#150726,#150727,#150728,#150729,
#150730,#150731,#150732,#150733,#150734,#150735,#150736,#150737,#150738,
#150739,#150740,#150741,#150742,#150743,#150744,#150745,#150746,#150747,
#150748,#150749,#150750,#150751,#150752,#150753,#150754,#150755,#150756,
#150757,#150758,#150759,#150760,#150761,#150762,#150763,#150764,#150765,
#150766,#150767,#150768,#150769,#150770,#150771,#150772,#150773,#150774,
#150775,#150776,#150777,#150778,#150779,#150780,#150781,#150782,#150783,
#150784,#150785,#150786,#150787,#150788,#150789,#150790,#150791,#150792,
#150793,#150794,#150795,#150796,#150797),.UNSPECIFIED.,.F.,.F.,(4,3,3,3,
3,3,3,3,3,3,3,3,3,3,3,3,3,3,3,3,3,3,3,3,3,3,3,3,3,3,3,3,3,3,3,3,3,3,3,3,
3,3,3,3,3,3,3,3,3,3,3,3,3,3,3,3,3,3,3,3,3,3,3,3,3,3,3,3,3,3,3,3,3,3,3,3,
3,3,3,3,3,4),(717.401980325962,717.489435265062,717.57731884262,717.665419190297,
717.753832653133,717.810455697052,717.890412997183,717.970275794426,718.050061616897,
718.129787932093,718.209472160386,718.289143146607,718.368810600133,718.448490250949,
718.528197833344,718.607993062419,718.687837404127,718.767795831174,718.810191707772,
718.890149007903,718.970011805146,719.049797627618,719.129523942814,719.209208171108,
719.288879157329,719.368546610855,719.448226261672,719.527933844067,719.607729073142,
719.68757341485,719.767531841898,719.809927718493,719.889885018624,719.969747815867,
720.049533638339,720.129259953534,720.208944181828,720.288615168049,720.368282621575,
720.447962272392,720.527669854787,720.607465083862,720.68730942557,720.767267852618,
720.809663729213,720.889621029344,720.969483826587,721.049269649058,721.128995964253,
721.208680192547,721.288351178768,721.368018632294,721.44769828311,721.527405865505,
721.60720109458,721.687045436287,721.767003863335,721.809399739933,721.889357040064,
721.969219837307,722.049005659779,722.128731974974,722.208416203268,722.288087189489,
722.367754643015,722.447434293831,722.527141876226,722.606937105301,722.686781447009,
722.766739874056,722.809135750653,722.887980746099,722.966731996665,723.0454079396,
723.125377624546,723.203961856065,723.282530646254,723.361100519844,723.442116744675,
723.520772986718,723.602969202942,723.685165419166),.UNSPECIFIED.);
#1244=B_SPLINE_CURVE_WITH_KNOTS('',3,(#150799,#150800,#150801,#150802,#150803,
#150804,#150805,#150806,#150807,#150808,#150809),.UNSPECIFIED.,.F.,.F.,
(4,1,1,1,1,1,1,1,4),(723.685165419166,723.808871761373,724.808607772093,
725.808343782813,726.808079793533,727.807815804254,728.807551814974,729.807287825694,
729.968350726345),.UNSPECIFIED.);
#1245=B_SPLINE_CURVE_WITH_KNOTS('',3,(#150811,#150812,#150813,#150814,#150815,
#150816,#150817,#150818,#150819,#150820),.UNSPECIFIED.,.F.,.F.,(4,1,1,1,
1,1,1,4),(729.968350726345,730.807023836414,731.806759847134,732.806495857854,
733.806231868575,734.805967879295,735.805703890015,736.251536033525),
 .UNSPECIFIED.);
#1246=B_SPLINE_CURVE_WITH_KNOTS('',3,(#150822,#150823,#150824,#150825,#150826,
#150827,#150828,#150829,#150830,#150831),.UNSPECIFIED.,.F.,.F.,(4,1,1,1,
1,1,1,4),(736.251536033525,736.805439900735,737.805175911455,738.804911922175,
739.804647932895,740.804383943615,741.804119954336,742.534721340704),
 .UNSPECIFIED.);
#1247=B_SPLINE_CURVE_WITH_KNOTS('',3,(#150833,#150834,#150835,#150836,#150837,
#150838,#150839,#150840,#150841,#150842,#150843),.UNSPECIFIED.,.F.,.F.,
(4,1,1,1,1,1,1,1,4),(742.534721340704,742.803855965056,743.803591975776,
744.803327986496,745.803063997216,746.802800007936,747.802536018656,748.802272029376,
748.817906647884),.UNSPECIFIED.);
#1248=B_SPLINE_CURVE_WITH_KNOTS('',3,(#150845,#150846,#150847,#150848,#150849,
#150850,#150851,#150852,#150853,#150854,#150855,#150856,#150857,#150858,
#150859,#150860,#150861,#150862,#150863,#150864,#150865,#150866,#150867,
#150868,#150869,#150870,#150871,#150872,#150873,#150874,#150875,#150876,
#150877,#150878,#150879,#150880,#150881,#150882,#150883,#150884,#150885,
#150886,#150887,#150888,#150889,#150890,#150891,#150892,#150893,#150894,
#150895,#150896,#150897,#150898,#150899,#150900,#150901,#150902,#150903,
#150904,#150905,#150906,#150907,#150908,#150909,#150910,#150911,#150912,
#150913,#150914,#150915,#150916,#150917,#150918,#150919,#150920,#150921,
#150922,#150923,#150924,#150925,#150926,#150927,#150928,#150929,#150930,
#150931,#150932,#150933,#150934,#150935,#150936,#150937,#150938,#150939,
#150940,#150941,#150942,#150943,#150944,#150945,#150946,#150947,#150948,
#150949,#150950,#150951,#150952,#150953,#150954,#150955,#150956,#150957,
#150958,#150959,#150960,#150961,#150962,#150963,#150964,#150965,#150966,
#150967,#150968,#150969,#150970,#150971,#150972,#150973,#150974,#150975,
#150976,#150977,#150978,#150979,#150980,#150981,#150982,#150983,#150984,
#150985,#150986,#150987,#150988,#150989,#150990,#150991,#150992,#150993,
#150994,#150995,#150996,#150997,#150998,#150999,#151000,#151001,#151002,
#151003,#151004,#151005,#151006,#151007,#151008,#151009,#151010,#151011,
#151012,#151013,#151014,#151015,#151016,#151017,#151018,#151019,#151020,
#151021,#151022,#151023,#151024,#151025,#151026,#151027,#151028,#151029,
#151030,#151031,#151032,#151033,#151034,#151035,#151036,#151037,#151038,
#151039,#151040,#151041,#151042,#151043,#151044,#151045,#151046,#151047,
#151048,#151049,#151050,#151051,#151052,#151053,#151054,#151055,#151056,
#151057,#151058,#151059,#151060,#151061,#151062,#151063,#151064,#151065,
#151066,#151067,#151068,#151069,#151070,#151071,#151072,#151073,#151074,
#151075,#151076,#151077,#151078,#151079,#151080,#151081,#151082,#151083,
#151084,#151085,#151086,#151087,#151088,#151089,#151090,#151091),
 .UNSPECIFIED.,.F.,.F.,(4,3,3,3,3,3,3,3,3,3,3,3,3,3,3,3,3,3,3,3,3,3,3,3,
3,3,3,3,3,3,3,3,3,3,3,3,3,3,3,3,3,3,3,3,3,3,3,3,3,3,3,3,3,3,3,3,3,3,3,3,
3,3,3,3,3,3,3,3,3,3,3,3,3,3,3,3,3,3,3,3,3,3,4),(748.817906647884,748.897646423686,
748.977292073114,749.056861329939,749.136371865781,749.21957638757,749.299033476738,
749.378489054434,749.457959034762,749.537459337759,749.617047679928,749.696687633192,
749.776436940243,749.802008040097,749.881965340228,749.961828137471,750.041613959943,
750.121340275138,750.201024503432,750.280695489653,750.360362943179,750.440042593995,
750.519750176389,750.599545405465,750.679389747172,750.759348174219,750.801744050817,
750.881701350948,750.961564148191,751.041349970662,751.121076285858,751.200760514152,
751.280431500372,751.360098953898,751.439778604715,751.51948618711,751.599281416185,
751.679125757893,751.75908418494,751.801480061537,751.881437361668,751.961300158911,
752.041085981383,752.120812296578,752.200496524872,752.280167511094,752.35983496462,
752.439514615436,752.519222197831,752.599017426906,752.678861768614,752.758820195662,
752.801216072257,752.881173372388,752.961036169631,753.040821992103,753.120548307298,
753.200232535592,753.279903521813,753.359570975339,753.439250626156,753.51895820855,
753.598753437626,753.678597779333,753.75855620638,753.800952082977,753.880909383108,
753.960772180351,754.040558002822,754.120284318017,754.199968546312,754.279639532533,
754.359306986059,754.438986636875,754.518694219269,754.598489448345,754.678333790053,
754.7582922171,754.800688093697,754.89813020414,754.999610987187,755.095292303198,
755.101091770234),.UNSPECIFIED.);
#1249=B_SPLINE_CURVE_WITH_KNOTS('',3,(#151093,#151094,#151095,#151096,#151097,
#151098,#151099,#151100,#151101,#151102),.UNSPECIFIED.,.F.,.F.,(4,1,1,1,
1,1,1,4),(755.101091955063,755.800424104417,756.800160115137,757.799896125858,
758.799632136578,759.799368147298,760.799104158018,761.384277262243),
 .UNSPECIFIED.);
#1250=B_SPLINE_CURVE_WITH_KNOTS('',3,(#151104,#151105,#151106,#151107,#151108,
#151109,#151110,#151111,#151112,#151113,#151114,#151115,#151116,#151117,
#151118,#151119,#151120,#151121,#151122,#151123,#151124,#151125,#151126,
#151127,#151128,#151129,#151130,#151131,#151132,#151133,#151134,#151135,
#151136,#151137,#151138,#151139,#151140,#151141,#151142,#151143,#151144,
#151145,#151146,#151147,#151148,#151149,#151150,#151151,#151152,#151153,
#151154,#151155,#151156,#151157,#151158,#151159,#151160,#151161,#151162,
#151163,#151164,#151165,#151166,#151167,#151168,#151169,#151170,#151171,
#151172,#151173,#151174,#151175,#151176,#151177,#151178,#151179,#151180,
#151181,#151182,#151183,#151184,#151185,#151186,#151187,#151188,#151189,
#151190,#151191,#151192,#151193,#151194,#151195,#151196,#151197,#151198,
#151199,#151200,#151201,#151202,#151203,#151204,#151205,#151206,#151207,
#151208,#151209,#151210,#151211,#151212,#151213,#151214,#151215,#151216,
#151217,#151218,#151219,#151220,#151221,#151222,#151223,#151224,#151225,
#151226,#151227,#151228,#151229,#151230,#151231,#151232,#151233,#151234,
#151235,#151236,#151237,#151238,#151239,#151240,#151241,#151242,#151243,
#151244,#151245,#151246,#151247,#151248,#151249,#151250,#151251,#151252,
#151253,#151254,#151255,#151256,#151257,#151258,#151259,#151260,#151261,
#151262,#151263,#151264,#151265,#151266,#151267,#151268,#151269,#151270,
#151271,#151272,#151273,#151274,#151275,#151276,#151277,#151278,#151279,
#151280,#151281,#151282,#151283,#151284,#151285,#151286,#151287,#151288,
#151289,#151290,#151291,#151292,#151293,#151294,#151295,#151296,#151297,
#151298,#151299,#151300,#151301,#151302,#151303,#151304,#151305,#151306,
#151307,#151308,#151309,#151310,#151311,#151312,#151313,#151314,#151315,
#151316,#151317,#151318,#151319,#151320,#151321,#151322,#151323,#151324,
#151325,#151326,#151327,#151328,#151329,#151330,#151331,#151332,#151333,
#151334,#151335,#151336,#151337,#151338,#151339,#151340,#151341,#151342,
#151343,#151344,#151345,#151346,#151347),.UNSPECIFIED.,.F.,.F.,(4,3,3,3,
3,3,3,3,3,3,3,3,3,3,3,3,3,3,3,3,3,3,3,3,3,3,3,3,3,3,3,3,3,3,3,3,3,3,3,3,
3,3,3,3,3,3,3,3,3,3,3,3,3,3,3,3,3,3,3,3,3,3,3,3,3,3,3,3,3,3,3,3,3,3,3,3,
3,3,3,3,3,4),(761.384277466923,761.471405537994,761.558940529162,761.646680291344,
761.73472615752,761.798840168738,761.87879746887,761.958660266113,762.038446088585,
762.11817240378,762.197856632075,762.277527618296,762.357195071823,762.436874722639,
762.516582305034,762.59637753411,762.676221875818,762.756180302866,762.798576179458,
762.878533479589,762.958396276832,763.038182099303,763.117908414499,763.197592642792,
763.277263629013,763.356931082539,763.436610733355,763.51631831575,763.596113544825,
763.675957886533,763.75591631358,763.798312190178,763.878269490309,763.958132287552,
764.037918110024,764.117644425219,764.197328653514,764.276999639735,764.356667093261,
764.436346744077,764.516054326472,764.595849555547,764.675693897255,764.755652324303,
764.798048200899,764.87800550103,764.957868298273,765.037654120745,765.117380435941,
765.197064664235,765.276735650456,765.356403103982,765.436082754798,765.515790337193,
765.595585566269,765.675429907976,765.755388335024,765.797784211619,765.87774151175,
765.957604308993,766.037390131464,766.11711644666,766.196800674954,766.276471661175,
766.356139114701,766.435818765517,766.515526347911,766.595321576987,766.675165918694,
766.755124345742,766.797520222339,766.876344312258,766.955074645796,767.033729674355,
767.112946286238,767.191509667396,767.270057457799,767.348606193875,767.428320287762,
767.506953550245,767.587208059834,767.667462569422),.UNSPECIFIED.);
#1251=B_SPLINE_CURVE_WITH_KNOTS('',3,(#151349,#151350,#151351,#151352,#151353,
#151354,#151355,#151356,#151357,#151358,#151359),.UNSPECIFIED.,.F.,.F.,
(4,1,1,1,1,1,1,1,4),(767.667462569422,767.797256233059,768.796992243779,
769.796728254499,770.796464265219,771.79620027594,772.79593628666,773.79567229738,
773.950647876602),.UNSPECIFIED.);
#1252=B_SPLINE_CURVE_WITH_KNOTS('',3,(#151361,#151362,#151363,#151364,#151365,
#151366,#151367,#151368,#151369,#151370),.UNSPECIFIED.,.F.,.F.,(4,1,1,1,
1,1,1,4),(773.950647876602,774.7954083081,775.79514431882,776.79488032954,
777.79461634026,778.79435235098,779.794088361701,780.233828319243),
 .UNSPECIFIED.);
#1253=B_SPLINE_CURVE_WITH_KNOTS('',3,(#151372,#151373,#151374,#151375,#151376,
#151377,#151378,#151379,#151380,#151381,#151382,#151383,#151384,#151385,
#151386,#151387,#151388,#151389,#151390,#151391,#151392,#151393,#151394,
#151395,#151396,#151397,#151398,#151399,#151400,#151401,#151402,#151403,
#151404,#151405,#151406,#151407,#151408,#151409,#151410,#151411,#151412,
#151413,#151414,#151415,#151416,#151417,#151418,#151419,#151420,#151421,
#151422,#151423,#151424,#151425,#151426,#151427,#151428,#151429,#151430,
#151431,#151432,#151433,#151434,#151435,#151436,#151437,#151438,#151439,
#151440,#151441,#151442,#151443,#151444,#151445,#151446,#151447,#151448,
#151449,#151450,#151451,#151452,#151453,#151454,#151455,#151456,#151457,
#151458,#151459,#151460,#151461,#151462,#151463,#151464,#151465,#151466,
#151467,#151468,#151469,#151470,#151471,#151472,#151473,#151474,#151475,
#151476,#151477,#151478,#151479,#151480,#151481,#151482,#151483,#151484,
#151485,#151486,#151487,#151488,#151489,#151490,#151491,#151492,#151493,
#151494,#151495,#151496,#151497,#151498,#151499,#151500,#151501,#151502,
#151503,#151504,#151505,#151506,#151507,#151508,#151509,#151510,#151511,
#151512,#151513,#151514,#151515,#151516,#151517,#151518,#151519,#151520,
#151521,#151522,#151523,#151524,#151525,#151526,#151527,#151528,#151529,
#151530,#151531,#151532,#151533,#151534,#151535,#151536,#151537,#151538,
#151539,#151540,#151541,#151542,#151543,#151544,#151545,#151546,#151547,
#151548,#151549,#151550,#151551,#151552,#151553,#151554,#151555,#151556,
#151557,#151558,#151559,#151560,#151561,#151562,#151563,#151564,#151565,
#151566,#151567,#151568,#151569,#151570,#151571,#151572,#151573,#151574,
#151575,#151576,#151577,#151578,#151579,#151580,#151581,#151582,#151583,
#151584,#151585,#151586,#151587,#151588,#151589,#151590,#151591,#151592,
#151593,#151594,#151595,#151596,#151597,#151598,#151599,#151600,#151601,
#151602,#151603,#151604,#151605,#151606,#151607,#151608,#151609,#151610,
#151611,#151612,#151613,#151614,#151615,#151616,#151617,#151618),
 .UNSPECIFIED.,.F.,.F.,(4,3,3,3,3,3,3,3,3,3,3,3,3,3,3,3,3,3,3,3,3,3,3,3,
3,3,3,3,3,3,3,3,3,3,3,3,3,3,3,3,3,3,3,3,3,3,3,3,3,3,3,3,3,3,3,3,3,3,3,3,
3,3,3,3,3,3,3,3,3,3,3,3,3,3,3,3,3,3,3,3,3,3,4),(780.233833183782,780.315493544815,
780.397200486774,780.478966500679,780.560865346708,780.64283406342,780.724956376328,
780.793824372421,780.873781672552,780.953644469795,781.033430292267,781.113156607462,
781.192840835756,781.272511821977,781.352179275503,781.431858926319,781.511566508713,
781.591361737789,781.671206079497,781.751164506544,781.793560383141,781.873517683272,
781.953380480515,782.033166302987,782.112892618182,782.192576846476,782.272247832697,
782.351915286223,782.43159493704,782.511302519434,782.59109774851,782.670942090218,
782.750900517265,782.793296393861,782.873253693992,782.953116491235,783.032902313706,
783.112628628902,783.192312857196,783.271983843416,783.351651296942,783.431330947759,
783.511038530154,783.590833759229,783.670678100936,783.750636527984,783.793032404581,
783.872989704712,783.952852501955,784.032638324427,784.112364639622,784.192048867916,
784.271719854137,784.351387307663,784.43106695848,784.510774540875,784.59056976995,
784.670414111658,784.750372538705,784.792768415301,784.872725715432,784.952588512675,
785.032374335147,785.112100650342,785.191784878636,785.271455864857,785.351123318383,
785.4308029692,785.510510551594,785.590305780669,785.670150122377,785.750108549425,
785.792504426021,785.871752178378,785.952410467451,786.031464250185,786.110464253903,
786.189426805881,786.271324727151,786.350277412381,786.429238753714,786.508242705639,
786.517018490961),.UNSPECIFIED.);
#1254=B_SPLINE_CURVE_WITH_KNOTS('',3,(#151620,#151621,#151622,#151623,#151624,
#151625,#151626,#151627,#151628,#151629,#151630),.UNSPECIFIED.,.F.,.F.,
(4,1,1,1,1,1,1,1,4),(786.517022438603,786.792240436741,787.791976447461,
788.791712458181,789.791448468902,790.791184479622,791.790920490342,792.790656501062,
792.800203798141),.UNSPECIFIED.);
#1255=B_SPLINE_CURVE_WITH_KNOTS('',3,(#151632,#151633,#151634,#151635,#151636,
#151637,#151638,#151639,#151640,#151641,#151642,#151643,#151644,#151645,
#151646,#151647,#151648,#151649,#151650,#151651,#151652,#151653,#151654,
#151655,#151656,#151657,#151658,#151659,#151660,#151661,#151662,#151663,
#151664,#151665,#151666,#151667,#151668,#151669,#151670,#151671,#151672,
#151673,#151674,#151675,#151676,#151677,#151678,#151679,#151680,#151681,
#151682,#151683,#151684,#151685,#151686,#151687,#151688,#151689,#151690,
#151691,#151692,#151693,#151694,#151695,#151696,#151697,#151698,#151699,
#151700,#151701,#151702,#151703,#151704,#151705,#151706,#151707,#151708,
#151709,#151710,#151711,#151712,#151713,#151714,#151715,#151716,#151717,
#151718,#151719,#151720,#151721,#151722,#151723,#151724,#151725,#151726,
#151727,#151728,#151729,#151730,#151731,#151732,#151733,#151734,#151735,
#151736,#151737,#151738,#151739,#151740,#151741,#151742,#151743,#151744,
#151745,#151746,#151747,#151748,#151749,#151750,#151751,#151752,#151753,
#151754,#151755,#151756,#151757,#151758,#151759,#151760,#151761,#151762,
#151763,#151764,#151765,#151766,#151767,#151768,#151769,#151770,#151771,
#151772,#151773,#151774,#151775,#151776,#151777,#151778,#151779,#151780,
#151781,#151782,#151783,#151784,#151785,#151786,#151787,#151788,#151789,
#151790,#151791,#151792,#151793,#151794,#151795,#151796,#151797,#151798,
#151799,#151800,#151801,#151802,#151803,#151804,#151805,#151806,#151807,
#151808,#151809,#151810,#151811,#151812,#151813,#151814,#151815,#151816,
#151817,#151818,#151819,#151820,#151821,#151822,#151823,#151824,#151825,
#151826,#151827,#151828,#151829,#151830,#151831,#151832,#151833,#151834,
#151835,#151836,#151837,#151838,#151839,#151840,#151841,#151842,#151843,
#151844,#151845,#151846,#151847,#151848,#151849,#151850,#151851,#151852,
#151853,#151854,#151855,#151856,#151857,#151858,#151859,#151860,#151861,
#151862,#151863,#151864,#151865,#151866,#151867,#151868,#151869,#151870,
#151871,#151872,#151873,#151874,#151875),.UNSPECIFIED.,.F.,.F.,(4,3,3,3,
3,3,3,3,3,3,3,3,3,3,3,3,3,3,3,3,3,3,3,3,3,3,3,3,3,3,3,3,3,3,3,3,3,3,3,3,
3,3,3,3,3,3,3,3,3,3,3,3,3,3,3,3,3,3,3,3,3,3,3,3,3,3,3,3,3,3,3,3,3,3,3,3,
3,3,3,3,3,4),(792.800203798141,792.880025863388,792.959753592175,793.039404643025,
793.118996612905,793.198547051178,793.278085018463,793.357620195601,793.437168429199,
793.516745570841,793.596410406403,793.676125453485,793.75595229044,793.790392511782,
793.870349811913,793.950212609156,794.029998431628,794.109724746823,794.189408975117,
794.269079961338,794.348747414864,794.428427065681,794.508134648075,794.587929877151,
794.667774218858,794.747732645906,794.790128522502,794.870085822633,794.949948619876,
795.029734442348,795.109460757543,795.189144985837,795.268815972058,795.348483425584,
795.428163076401,795.507870658795,795.587665887871,795.667510229578,795.747468656626,
795.789864533222,795.869821833353,795.949684630596,796.029470453068,796.109196768264,
796.188880996558,796.268551982779,796.348219436305,796.427899087122,796.507606669517,
796.587401898592,796.6672462403,796.747204667347,796.789600543943,796.869557844074,
796.949420641317,797.029206463789,797.108932778984,797.188617007278,797.268287993499,
797.347955447025,797.427635097842,797.507342680236,797.587137909312,797.66698225102,
797.746940678067,797.789336554663,797.869293854794,797.949156652037,798.028942474509,
798.108668789704,798.188353017998,798.268024004219,798.347691457745,798.427371108561,
798.507078690955,798.586873920031,798.666718261738,798.746676688786,798.789072565383,
798.887253081097,798.985321007094,799.083388933091),.UNSPECIFIED.);
#1256=B_SPLINE_CURVE_WITH_KNOTS('',3,(#151877,#151878,#151879,#151880,#151881,
#151882,#151883,#151884,#151885,#151886),.UNSPECIFIED.,.F.,.F.,(4,1,1,1,
1,1,1,4),(799.08338910532,799.788808576103,800.788544586823,801.788280597543,
802.788016608263,803.787752618983,804.787488629703,805.3665744125),
 .UNSPECIFIED.);
#1257=B_SPLINE_CURVE_WITH_KNOTS('',3,(#151888,#151889,#151890,#151891,#151892,
#151893,#151894,#151895,#151896,#151897),.UNSPECIFIED.,.F.,.F.,(4,1,1,1,
1,1,1,4),(805.3665744125,805.787224640424,806.786960651144,807.786696661864,
808.786432672584,809.786168683304,810.785904694024,811.649759719679),
 .UNSPECIFIED.);
#1258=B_SPLINE_CURVE_WITH_KNOTS('',3,(#151899,#151900,#151901,#151902,#151903,
#151904,#151905,#151906,#151907,#151908,#151909),.UNSPECIFIED.,.F.,.F.,
(4,1,1,1,1,1,1,1,4),(811.649759719679,811.785640704745,812.785376715465,
813.785112726185,814.784848736905,815.784584747625,816.784320758345,817.784056769065,
817.932945026859),.UNSPECIFIED.);
#1259=B_SPLINE_CURVE_WITH_KNOTS('',3,(#151911,#151912,#151913,#151914,#151915,
#151916,#151917,#151918,#151919,#151920),.UNSPECIFIED.,.F.,.F.,(4,1,1,1,
1,1,1,4),(817.932945026859,818.783792779785,819.783528790505,820.783264801226,
821.783000811946,822.782736822666,823.782472833386,824.216125065963),
 .UNSPECIFIED.);
#1260=B_SPLINE_CURVE_WITH_KNOTS('',3,(#151922,#151923,#151924,#151925,#151926,
#151927,#151928,#151929,#151930,#151931,#151932,#151933,#151934,#151935,
#151936,#151937,#151938,#151939,#151940,#151941,#151942,#151943,#151944,
#151945,#151946,#151947,#151948,#151949,#151950,#151951,#151952,#151953,
#151954,#151955,#151956,#151957,#151958,#151959,#151960,#151961,#151962,
#151963,#151964,#151965,#151966,#151967,#151968,#151969,#151970,#151971,
#151972,#151973,#151974,#151975,#151976,#151977,#151978,#151979,#151980,
#151981,#151982,#151983,#151984,#151985,#151986,#151987,#151988,#151989,
#151990,#151991,#151992,#151993,#151994,#151995,#151996,#151997,#151998,
#151999,#152000,#152001,#152002,#152003,#152004,#152005,#152006,#152007,
#152008,#152009,#152010,#152011,#152012,#152013,#152014,#152015,#152016,
#152017,#152018,#152019,#152020,#152021,#152022,#152023,#152024,#152025,
#152026,#152027,#152028,#152029,#152030,#152031,#152032,#152033,#152034,
#152035,#152036,#152037,#152038,#152039,#152040,#152041,#152042,#152043,
#152044,#152045,#152046,#152047,#152048,#152049,#152050,#152051,#152052,
#152053,#152054,#152055,#152056,#152057,#152058,#152059,#152060,#152061,
#152062,#152063,#152064,#152065,#152066,#152067,#152068,#152069,#152070,
#152071,#152072,#152073,#152074,#152075,#152076,#152077,#152078,#152079,
#152080,#152081,#152082,#152083,#152084,#152085,#152086,#152087,#152088,
#152089,#152090,#152091,#152092,#152093,#152094,#152095,#152096,#152097,
#152098,#152099,#152100,#152101,#152102,#152103,#152104,#152105,#152106,
#152107,#152108,#152109,#152110,#152111,#152112,#152113,#152114,#152115,
#152116,#152117,#152118,#152119,#152120,#152121,#152122,#152123,#152124,
#152125,#152126,#152127,#152128,#152129,#152130,#152131,#152132,#152133,
#152134,#152135,#152136,#152137,#152138,#152139,#152140,#152141,#152142,
#152143,#152144,#152145,#152146,#152147,#152148,#152149,#152150,#152151,
#152152,#152153,#152154,#152155,#152156,#152157,#152158,#152159,#152160,
#152161,#152162,#152163,#152164,#152165),.UNSPECIFIED.,.F.,.F.,(4,3,3,3,
3,3,3,3,3,3,3,3,3,3,3,3,3,3,3,3,3,3,3,3,3,3,3,3,3,3,3,3,3,3,3,3,3,3,3,3,
3,3,3,3,3,3,3,3,3,3,3,3,3,3,3,3,3,3,3,3,3,3,3,3,3,3,3,3,3,3,3,3,3,3,3,3,
3,3,3,3,3,4),(824.216130334038,824.297637731403,824.379187162414,824.460791451376,
824.542524682942,824.624324720818,824.706278491386,824.782208844106,824.862166144237,
824.94202894148,825.021814763951,825.101541079147,825.181225307441,825.260896293662,
825.340563747188,825.420243398004,825.499950980398,825.579746209474,825.659590551181,
825.739548978228,825.781944854826,825.861902154957,825.9417649522,826.021550774672,
826.101277089867,826.180961318162,826.260632304382,826.340299757908,826.419979408725,
826.499686991119,826.579482220195,826.659326561903,826.73928498895,826.781680865546,
826.861638165677,826.94150096292,827.021286785392,827.101013100587,827.180697328881,
827.260368315102,827.340035768628,827.419715419444,827.499423001839,827.579218230914,
827.659062572622,827.739020999669,827.781416876266,827.861374176397,827.94123697364,
828.021022796112,828.100749111307,828.180433339602,828.260104325823,828.339771779349,
828.419451430166,828.499159012561,828.578954241637,828.658798583344,828.738757010392,
828.781152886987,828.861110187118,828.940972984361,829.020758806833,829.100485122028,
829.180169350322,829.259840336543,829.339507790069,829.419187440885,829.49889502328,
829.578690252356,829.658534594064,829.738493021111,829.780888897707,829.86019447738,
829.94008462286,830.019195745959,830.098252415943,830.177270921403,830.257782101357,
830.336788066053,830.418051853635,830.499315641218),.UNSPECIFIED.);
#1261=B_SPLINE_CURVE_WITH_KNOTS('',3,(#152167,#152168,#152169,#152170,#152171,
#152172,#152173,#152174,#152175,#152176,#152177),.UNSPECIFIED.,.F.,.F.,
(4,1,1,1,1,1,1,1,4),(830.499320072584,830.780624908427,831.780360919147,
832.780096929867,833.779832940587,834.779568951308,835.779304962028,836.779040972748,
836.782500948398),.UNSPECIFIED.);
#1262=B_SPLINE_CURVE_WITH_KNOTS('',3,(#152179,#152180,#152181,#152182,#152183,
#152184,#152185,#152186,#152187,#152188,#152189,#152190,#152191,#152192,
#152193,#152194,#152195,#152196,#152197,#152198,#152199,#152200,#152201,
#152202,#152203,#152204,#152205,#152206,#152207,#152208,#152209,#152210,
#152211,#152212,#152213,#152214,#152215,#152216,#152217,#152218,#152219,
#152220,#152221,#152222,#152223,#152224,#152225,#152226,#152227,#152228,
#152229,#152230,#152231,#152232,#152233,#152234,#152235,#152236,#152237,
#152238,#152239,#152240,#152241,#152242,#152243,#152244,#152245,#152246,
#152247,#152248,#152249,#152250,#152251,#152252,#152253,#152254,#152255,
#152256,#152257,#152258,#152259,#152260,#152261,#152262,#152263,#152264,
#152265,#152266,#152267,#152268,#152269,#152270,#152271,#152272,#152273,
#152274,#152275,#152276,#152277,#152278,#152279,#152280,#152281,#152282,
#152283,#152284,#152285,#152286,#152287,#152288,#152289,#152290,#152291,
#152292,#152293,#152294,#152295,#152296,#152297,#152298,#152299,#152300,
#152301,#152302,#152303,#152304,#152305,#152306,#152307,#152308,#152309,
#152310,#152311,#152312,#152313,#152314,#152315,#152316,#152317,#152318,
#152319,#152320,#152321,#152322,#152323,#152324,#152325,#152326,#152327,
#152328,#152329,#152330,#152331,#152332,#152333,#152334,#152335,#152336,
#152337,#152338,#152339,#152340,#152341,#152342,#152343,#152344,#152345,
#152346,#152347,#152348,#152349,#152350,#152351,#152352,#152353,#152354,
#152355,#152356,#152357,#152358,#152359,#152360,#152361,#152362,#152363,
#152364,#152365,#152366,#152367,#152368,#152369,#152370,#152371,#152372,
#152373,#152374,#152375,#152376,#152377,#152378,#152379,#152380,#152381,
#152382,#152383,#152384,#152385,#152386,#152387,#152388,#152389,#152390,
#152391,#152392,#152393,#152394,#152395,#152396,#152397,#152398,#152399,
#152400,#152401,#152402,#152403,#152404,#152405,#152406,#152407,#152408,
#152409,#152410,#152411,#152412,#152413,#152414,#152415,#152416,#152417,
#152418,#152419,#152420,#152421,#152422),.UNSPECIFIED.,.F.,.F.,(4,3,3,3,
3,3,3,3,3,3,3,3,3,3,3,3,3,3,3,3,3,3,3,3,3,3,3,3,3,3,3,3,3,3,3,3,3,3,3,3,
3,3,3,3,3,3,3,3,3,3,3,3,3,3,3,3,3,3,3,3,3,3,3,3,3,3,3,3,3,3,3,3,3,3,3,3,
3,3,3,3,3,4),(836.782500948398,836.862408365672,836.942221316432,837.021957377889,
837.101634066293,837.181268850594,837.26089065088,837.340509174496,837.420140195296,
837.499799491666,837.579546446107,837.659342905624,837.739252618905,837.778776983468,
837.858734283599,837.938597080842,838.018382903314,838.098109218509,838.177793446803,
838.257464433024,838.33713188655,838.416811537366,838.49651911976,838.576314348836,
838.656158690544,838.736117117591,838.778512994188,838.858470294319,838.938333091562,
839.018118914034,839.097845229229,839.177529457523,839.257200443744,839.33686789727,
839.416547548087,839.496255130481,839.576050359557,839.655894701264,839.735853128312,
839.778249004908,839.858206305039,839.938069102282,840.017854924754,840.097581239949,
840.177265468243,840.256936454464,840.33660390799,840.416283558806,840.495991141201,
840.575786370276,840.655630711984,840.735589139032,840.777985015628,840.857942315759,
840.937805113002,841.017590935474,841.097317250669,841.177001478963,841.256672465184,
841.33633991871,841.416019569526,841.495727151921,841.575522380996,841.655366722704,
841.735325149751,841.777721026348,841.857678326479,841.937541123722,842.017326946193,
842.097053261388,842.176737489683,842.256408475903,842.336075929429,842.415755580246,
842.49546316264,842.575258391716,842.655102733423,842.735061160471,842.777457037068,
842.876411799539,842.97401212279,843.065686096939),.UNSPECIFIED.);
#1263=B_SPLINE_CURVE_WITH_KNOTS('',3,(#152424,#152425,#152426,#152427,#152428,
#152429,#152430,#152431,#152432,#152433),.UNSPECIFIED.,.F.,.F.,(4,1,1,1,
1,1,1,4),(843.065686255577,843.777193047789,844.776929058509,845.776665069229,
846.776401079949,847.776137090669,848.775873101389,849.348871562757),
 .UNSPECIFIED.);
#1264=B_SPLINE_CURVE_WITH_KNOTS('',3,(#152435,#152436,#152437,#152438,#152439,
#152440,#152441,#152442,#152443,#152444),.UNSPECIFIED.,.F.,.F.,(4,1,1,1,
1,1,1,4),(849.348871562757,849.775609112109,850.77534512283,851.77508113355,
852.77481714427,853.77455315499,854.77428916571,855.632056869936),
 .UNSPECIFIED.);
#1265=B_SPLINE_CURVE_WITH_KNOTS('',3,(#152446,#152447,#152448,#152449,#152450,
#152451,#152452,#152453,#152454,#152455,#152456),.UNSPECIFIED.,.F.,.F.,
(4,1,1,1,1,1,1,1,4),(855.632056869936,855.77402517643,856.77376118715,857.77349719787,
858.773233208591,859.772969219311,860.772705230031,861.772441240751,861.915242177116),
 .UNSPECIFIED.);
#1266=B_SPLINE_CURVE_WITH_KNOTS('',3,(#152458,#152459,#152460,#152461,#152462,
#152463,#152464,#152465,#152466,#152467),.UNSPECIFIED.,.F.,.F.,(4,1,1,1,
1,1,1,4),(861.915242177116,862.772177251471,863.771913262191,864.771649272911,
865.771385283631,866.771121294352,867.770857305072,868.198427484296),
 .UNSPECIFIED.);
#1267=B_SPLINE_CURVE_WITH_KNOTS('',3,(#152469,#152470,#152471,#152472,#152473,
#152474,#152475,#152476,#152477,#152478),.UNSPECIFIED.,.F.,.F.,(4,1,1,1,
1,1,1,4),(868.198427484296,868.770593315792,869.770329326512,870.770065337232,
871.769801347952,872.769537358672,873.769273369393,874.481612791475),
 .UNSPECIFIED.);
#1268=B_SPLINE_CURVE_WITH_KNOTS('',3,(#152480,#152481,#152482,#152483,#152484,
#152485,#152486,#152487,#152488,#152489,#152490,#152491,#152492,#152493,
#152494,#152495,#152496,#152497,#152498,#152499,#152500,#152501,#152502,
#152503,#152504,#152505,#152506,#152507,#152508,#152509,#152510,#152511,
#152512,#152513,#152514,#152515,#152516,#152517,#152518,#152519,#152520,
#152521,#152522,#152523,#152524,#152525,#152526,#152527,#152528,#152529,
#152530,#152531,#152532,#152533,#152534,#152535,#152536,#152537,#152538,
#152539,#152540,#152541,#152542,#152543,#152544,#152545,#152546,#152547,
#152548,#152549,#152550,#152551,#152552,#152553,#152554,#152555,#152556,
#152557,#152558,#152559,#152560,#152561,#152562,#152563,#152564,#152565,
#152566,#152567,#152568,#152569,#152570,#152571,#152572,#152573,#152574,
#152575,#152576,#152577,#152578,#152579,#152580,#152581,#152582,#152583,
#152584,#152585,#152586,#152587,#152588,#152589,#152590,#152591,#152592,
#152593,#152594,#152595,#152596,#152597,#152598,#152599,#152600,#152601,
#152602,#152603,#152604,#152605,#152606,#152607,#152608,#152609,#152610,
#152611,#152612,#152613,#152614,#152615,#152616,#152617,#152618,#152619,
#152620,#152621,#152622,#152623,#152624,#152625,#152626,#152627,#152628,
#152629,#152630,#152631,#152632,#152633,#152634,#152635,#152636,#152637,
#152638,#152639,#152640,#152641,#152642,#152643,#152644,#152645,#152646,
#152647,#152648,#152649,#152650,#152651,#152652,#152653,#152654,#152655,
#152656,#152657,#152658,#152659,#152660,#152661,#152662,#152663,#152664,
#152665,#152666,#152667,#152668,#152669,#152670,#152671,#152672,#152673,
#152674,#152675,#152676,#152677,#152678,#152679,#152680,#152681,#152682,
#152683,#152684,#152685,#152686,#152687,#152688,#152689,#152690,#152691,
#152692,#152693,#152694,#152695,#152696,#152697,#152698,#152699,#152700,
#152701,#152702,#152703,#152704,#152705,#152706,#152707,#152708,#152709,
#152710,#152711,#152712,#152713,#152714,#152715,#152716,#152717,#152718,
#152719,#152720,#152721,#152722,#152723),.UNSPECIFIED.,.F.,.F.,(4,3,3,3,
3,3,3,3,3,3,3,3,3,3,3,3,3,3,3,3,3,3,3,3,3,3,3,3,3,3,3,3,3,3,3,3,3,3,3,3,
3,3,3,3,3,3,3,3,3,3,3,3,3,3,3,3,3,3,3,3,3,3,3,3,3,3,3,3,3,3,3,3,3,3,3,3,
3,3,3,3,3,4),(874.48161294818,874.579018330041,874.677851503058,874.769009380113,
874.848966680244,874.928829477486,875.008615299957,875.088341615152,875.168025843445,
875.247696829666,875.327364283191,875.407043934007,875.486751516401,875.566546745476,
875.646391087183,875.72634951423,875.768745390833,875.848702690964,875.928565488207,
876.008351310679,876.088077625874,876.167761854168,876.247432840389,876.327100293915,
876.406779944732,876.486487527126,876.566282756202,876.646127097909,876.726085524957,
876.768481401553,876.848438701684,876.928301498927,877.008087321399,877.087813636594,
877.167497864888,877.247168851109,877.326836304635,877.406515955452,877.486223537846,
877.566018766922,877.64586310863,877.725821535677,877.768217412273,877.848174712404,
877.928037509647,878.007823332118,878.087549647314,878.167233875608,878.246904861829,
878.326572315354,878.406251966171,878.485959548565,878.565754777641,878.645599119348,
878.725557546396,878.767953422993,878.847910723124,878.927773520367,879.007559342839,
879.087285658034,879.166969886328,879.246640872549,879.326308326075,879.405987976892,
879.485695559286,879.565490788362,879.645335130069,879.725293557117,879.767689433713,
879.847608808449,879.92743369775,880.007181667238,880.086870221649,880.166516818457,
880.246150355548,880.325780545941,880.405423153102,880.485093944973,880.564852380967,
880.644660220934,880.724581505706,880.764798098655),.UNSPECIFIED.);
#1269=B_SPLINE_CURVE_WITH_KNOTS('',3,(#152725,#152726,#152727,#152728,#152729,
#152730,#152731,#152732,#152733,#152734,#152735,#152736,#152737),
 .UNSPECIFIED.,.F.,.F.,(4,3,1,1,1,1,1,1,4),(880.764798098655,880.767425444434,
881.767161455154,882.766897465874,883.766633476594,884.766369487314,885.766105498034,
886.765841508754,887.047978910358),.UNSPECIFIED.);
#1270=B_SPLINE_CURVE_WITH_KNOTS('',3,(#152739,#152740,#152741,#152742,#152743,
#152744,#152745,#152746,#152747,#152748,#152749,#152750,#152751,#152752,
#152753,#152754,#152755,#152756,#152757,#152758,#152759,#152760,#152761,
#152762,#152763,#152764,#152765,#152766,#152767,#152768,#152769,#152770,
#152771,#152772,#152773,#152774,#152775,#152776,#152777,#152778,#152779,
#152780,#152781,#152782,#152783,#152784,#152785,#152786,#152787,#152788,
#152789,#152790,#152791,#152792,#152793,#152794,#152795,#152796,#152797,
#152798,#152799,#152800,#152801,#152802,#152803,#152804,#152805,#152806,
#152807,#152808,#152809,#152810,#152811,#152812,#152813,#152814,#152815,
#152816,#152817,#152818,#152819,#152820,#152821,#152822,#152823,#152824,
#152825,#152826,#152827,#152828,#152829,#152830,#152831,#152832,#152833,
#152834,#152835,#152836,#152837,#152838,#152839,#152840,#152841,#152842,
#152843,#152844,#152845,#152846,#152847,#152848,#152849,#152850,#152851,
#152852,#152853,#152854,#152855,#152856,#152857,#152858,#152859,#152860,
#152861,#152862,#152863,#152864,#152865,#152866,#152867,#152868,#152869,
#152870,#152871,#152872,#152873,#152874,#152875,#152876,#152877,#152878,
#152879,#152880,#152881,#152882,#152883,#152884,#152885,#152886,#152887,
#152888,#152889,#152890,#152891,#152892,#152893,#152894,#152895,#152896,
#152897,#152898,#152899,#152900,#152901,#152902,#152903,#152904,#152905,
#152906,#152907,#152908,#152909,#152910,#152911,#152912,#152913,#152914,
#152915,#152916,#152917,#152918,#152919,#152920,#152921,#152922,#152923,
#152924,#152925,#152926,#152927,#152928,#152929,#152930,#152931,#152932,
#152933,#152934,#152935,#152936,#152937,#152938,#152939,#152940,#152941,
#152942,#152943,#152944,#152945,#152946,#152947,#152948,#152949,#152950,
#152951,#152952,#152953,#152954,#152955,#152956,#152957,#152958,#152959,
#152960,#152961,#152962,#152963,#152964,#152965,#152966,#152967,#152968,
#152969,#152970,#152971,#152972,#152973,#152974,#152975,#152976,#152977,
#152978,#152979,#152980,#152981,#152982),.UNSPECIFIED.,.F.,.F.,(4,3,3,3,
3,3,3,3,3,3,3,3,3,3,3,3,3,3,3,3,3,3,3,3,3,3,3,3,3,3,3,3,3,3,3,3,3,3,3,3,
3,3,3,3,3,3,3,3,3,3,3,3,3,3,3,3,3,3,3,3,3,3,3,3,3,3,3,3,3,3,3,3,3,3,3,3,
3,3,3,3,3,4),(887.047983405834,887.127043212417,887.206860000799,887.28587417662,
887.364889743303,887.443922933897,887.524336580291,887.60349397405,887.684535746762,
887.765577519474,887.845534819605,887.925397616848,888.005183439319,888.084909754515,
888.164593982809,888.24426496903,888.323932422556,888.403612073372,888.483319655766,
888.563114884842,888.642959226549,888.722917653597,888.765313530194,888.845270830325,
888.925133627568,889.00491945004,889.084645765235,889.164329993528,889.244000979749,
889.323668433275,889.403348084091,889.483055666486,889.562850895561,889.642695237269,
889.722653664316,889.765049540914,889.845006841046,889.924869638288,890.00465546076,
890.084381775956,890.16406600425,890.243736990471,890.323404443997,890.403084094814,
890.482791677209,890.562586906284,890.642431247992,890.72238967504,890.764785551635,
890.844742851766,890.924605649009,891.004391471481,891.084117786676,891.16380201497,
891.243473001191,891.323140454717,891.402820105533,891.482527687928,891.562322917003,
891.642167258711,891.722125685758,891.764521562355,891.844478862486,891.924341659729,
892.0041274822,892.083853797395,892.163538025689,892.24320901191,892.322876465436,
892.402556116252,892.482263698646,892.562058927722,892.641903269429,892.721861696477,
892.764257573075,892.846197831132,892.928026862176,893.009757780634,893.091379034572,
893.172936173556,893.254431836687,893.331168713014),.UNSPECIFIED.);
#1271=B_SPLINE_CURVE_WITH_KNOTS('',3,(#152984,#152985,#152986,#152987,#152988,
#152989,#152990,#152991,#152992,#152993),.UNSPECIFIED.,.F.,.F.,(4,1,1,1,
1,1,1,4),(893.331174034399,893.763993583795,894.763729594515,895.763465605235,
896.763201615955,897.762937626676,898.762673637396,899.614354020193),
 .UNSPECIFIED.);
#1272=B_SPLINE_CURVE_WITH_KNOTS('',3,(#152995,#152996,#152997,#152998,#152999,
#153000,#153001,#153002,#153003,#153004,#153005),.UNSPECIFIED.,.F.,.F.,
(4,1,1,1,1,1,1,1,4),(899.614354020193,899.762409648116,900.762145658836,
901.761881669556,902.761617680276,903.761353690997,904.761089701717,905.760825712436,
905.897539327373),.UNSPECIFIED.);
#1273=B_SPLINE_CURVE_WITH_KNOTS('',3,(#153007,#153008,#153009,#153010,#153011,
#153012,#153013,#153014,#153015,#153016),.UNSPECIFIED.,.F.,.F.,(4,1,1,1,
1,1,1,4),(905.897539327373,906.760561723157,907.760297733877,908.760033744597,
909.759769755317,910.759505766037,911.759241776758,912.180724634552),
 .UNSPECIFIED.);
#1274=B_SPLINE_CURVE_WITH_KNOTS('',3,(#153018,#153019,#153020,#153021,#153022,
#153023,#153024,#153025,#153026,#153027),.UNSPECIFIED.,.F.,.F.,(4,1,1,1,
1,1,1,4),(912.180724634552,912.758977787478,913.758713798198,914.758449808918,
915.758185819638,916.757921830358,917.757657841078,918.463909941732),
 .UNSPECIFIED.);
#1275=B_SPLINE_CURVE_WITH_KNOTS('',3,(#153029,#153030,#153031,#153032,#153033,
#153034,#153035,#153036,#153037,#153038,#153039,#153040,#153041,#153042,
#153043,#153044,#153045,#153046,#153047,#153048,#153049,#153050,#153051,
#153052,#153053,#153054,#153055,#153056,#153057,#153058,#153059,#153060,
#153061,#153062,#153063,#153064,#153065,#153066,#153067,#153068,#153069,
#153070,#153071,#153072,#153073,#153074,#153075,#153076,#153077,#153078,
#153079,#153080,#153081,#153082,#153083,#153084,#153085,#153086,#153087,
#153088,#153089,#153090,#153091,#153092,#153093,#153094,#153095,#153096,
#153097,#153098,#153099,#153100,#153101,#153102,#153103,#153104,#153105,
#153106,#153107,#153108,#153109,#153110,#153111,#153112,#153113,#153114,
#153115,#153116,#153117,#153118,#153119,#153120,#153121,#153122,#153123,
#153124,#153125,#153126,#153127,#153128,#153129,#153130,#153131,#153132,
#153133,#153134,#153135,#153136,#153137,#153138,#153139,#153140,#153141,
#153142,#153143,#153144,#153145,#153146,#153147,#153148,#153149,#153150,
#153151,#153152,#153153,#153154,#153155,#153156,#153157,#153158,#153159,
#153160,#153161,#153162,#153163,#153164,#153165,#153166,#153167,#153168,
#153169,#153170,#153171,#153172,#153173,#153174,#153175,#153176,#153177,
#153178,#153179,#153180,#153181,#153182,#153183,#153184,#153185,#153186,
#153187,#153188,#153189,#153190,#153191,#153192,#153193,#153194,#153195,
#153196,#153197,#153198,#153199,#153200,#153201,#153202,#153203,#153204,
#153205,#153206,#153207,#153208,#153209,#153210,#153211,#153212,#153213,
#153214,#153215,#153216,#153217,#153218,#153219,#153220,#153221,#153222,
#153223,#153224,#153225,#153226,#153227,#153228,#153229,#153230,#153231,
#153232,#153233,#153234,#153235,#153236,#153237,#153238,#153239,#153240,
#153241,#153242,#153243,#153244,#153245,#153246,#153247,#153248,#153249,
#153250,#153251,#153252,#153253,#153254,#153255,#153256,#153257,#153258,
#153259,#153260,#153261,#153262,#153263,#153264,#153265,#153266,#153267,
#153268,#153269,#153270,#153271,#153272),.UNSPECIFIED.,.F.,.F.,(4,3,3,3,
3,3,3,3,3,3,3,3,3,3,3,3,3,3,3,3,3,3,3,3,3,3,3,3,3,3,3,3,3,3,3,3,3,3,3,3,
3,3,3,3,3,3,3,3,3,3,3,3,3,3,3,3,3,3,3,3,3,3,3,3,3,3,3,3,3,3,3,3,3,3,3,3,
3,3,3,3,3,4),(918.463910112159,918.560627038663,918.65901044523,918.757393851798,
918.837351151929,918.917213949172,918.996999771644,919.076726086839,919.156410315134,
919.236081301355,919.315748754881,919.395428405697,919.475135988092,919.554931217167,
919.634775558875,919.714733985923,919.757129862518,919.837087162649,919.916949959892,
919.996735782363,920.076462097559,920.156146325852,920.235817312073,920.315484765599,
920.395164416415,920.47487199881,920.554667227885,920.634511569593,920.71446999664,
920.756865873238,920.836823173369,920.916685970612,920.996471793084,921.07619810828,
921.155882336574,921.235553322795,921.315220776321,921.394900427137,921.474608009532,
921.554403238608,921.634247580315,921.714206007363,921.756601883959,921.83655918409,
921.916421981333,921.996207803805,922.075934119001,922.155618347295,922.235289333516,
922.314956787042,922.394636437858,922.474344020253,922.554139249329,922.633983591037,
922.713942018084,922.756337894679,922.83629519481,922.916157992052,922.995943814524,
923.075670129719,923.155354358013,923.235025344234,923.31469279776,923.394372448576,
923.47408003097,923.553875260046,923.633719601753,923.7136780288,923.756073905399,
923.835907939634,923.915647532301,923.995310331492,924.074913923755,924.154475848011,
924.234025104635,924.313571425821,924.393130648538,924.472718614622,924.552394154601,
924.632119742723,924.711957223575,924.747095248912),.UNSPECIFIED.);
#1276=B_SPLINE_CURVE_WITH_KNOTS('',3,(#153274,#153275,#153276,#153277,#153278,
#153279,#153280,#153281,#153282,#153283,#153284,#153285,#153286),
 .UNSPECIFIED.,.F.,.F.,(4,3,1,1,1,1,1,1,4),(924.747095248912,924.755809916119,
925.755545926839,926.755281937559,927.755017948279,928.754753959,929.75448996972,
930.75422598044,931.030276540766),.UNSPECIFIED.);
#1277=B_SPLINE_CURVE_WITH_KNOTS('',3,(#153288,#153289,#153290,#153291,#153292,
#153293,#153294,#153295,#153296,#153297,#153298,#153299,#153300,#153301,
#153302,#153303,#153304,#153305,#153306,#153307,#153308,#153309,#153310,
#153311,#153312,#153313,#153314,#153315,#153316,#153317,#153318,#153319,
#153320,#153321,#153322,#153323,#153324,#153325,#153326,#153327,#153328,
#153329,#153330,#153331,#153332,#153333,#153334,#153335,#153336,#153337,
#153338,#153339,#153340,#153341,#153342,#153343,#153344,#153345,#153346,
#153347,#153348,#153349,#153350,#153351,#153352,#153353,#153354,#153355,
#153356,#153357,#153358,#153359,#153360,#153361,#153362,#153363,#153364,
#153365,#153366,#153367,#153368,#153369,#153370,#153371,#153372,#153373,
#153374,#153375,#153376,#153377,#153378,#153379,#153380,#153381,#153382,
#153383,#153384,#153385,#153386,#153387,#153388,#153389,#153390,#153391,
#153392,#153393,#153394,#153395,#153396,#153397,#153398,#153399,#153400,
#153401,#153402,#153403,#153404,#153405,#153406,#153407,#153408,#153409,
#153410,#153411,#153412,#153413,#153414,#153415,#153416,#153417,#153418,
#153419,#153420,#153421,#153422,#153423,#153424,#153425,#153426,#153427,
#153428,#153429,#153430,#153431,#153432,#153433,#153434,#153435,#153436,
#153437,#153438,#153439,#153440,#153441,#153442,#153443,#153444,#153445,
#153446,#153447,#153448,#153449,#153450,#153451,#153452,#153453,#153454,
#153455,#153456,#153457,#153458,#153459,#153460,#153461,#153462,#153463,
#153464,#153465,#153466,#153467,#153468,#153469,#153470,#153471,#153472,
#153473,#153474,#153475,#153476,#153477,#153478,#153479,#153480,#153481,
#153482,#153483,#153484,#153485,#153486,#153487,#153488,#153489,#153490,
#153491,#153492,#153493,#153494,#153495,#153496,#153497,#153498,#153499,
#153500,#153501,#153502,#153503,#153504,#153505,#153506,#153507,#153508,
#153509,#153510,#153511,#153512,#153513,#153514,#153515,#153516,#153517,
#153518,#153519,#153520,#153521,#153522,#153523,#153524,#153525,#153526,
#153527,#153528,#153529,#153530,#153531),.UNSPECIFIED.,.F.,.F.,(4,3,3,3,
3,3,3,3,3,3,3,3,3,3,3,3,3,3,3,3,3,3,3,3,3,3,3,3,3,3,3,3,3,3,3,3,3,3,3,3,
3,3,3,3,3,3,3,3,3,3,3,3,3,3,3,3,3,3,3,3,3,3,3,3,3,3,3,3,3,3,3,3,3,3,3,3,
3,3,3,3,3,4),(931.030280556091,931.109290663972,931.18987457987,931.268834084094,
931.347793270138,931.426768411011,931.508566806049,931.587664371913,931.670813181537,
931.75396199116,931.833919291291,931.913782088534,931.993567911005,932.0732942262,
932.152978454494,932.232649440715,932.312316894241,932.391996545057,932.471704127452,
932.551499356527,932.631343698235,932.711302125282,932.75369800188,932.833655302011,
932.913518099254,932.993303921726,933.073030236921,933.152714465215,933.232385451436,
933.312052904962,933.391732555778,933.471440138172,933.551235367248,933.631079708955,
933.711038136003,933.7534340126,933.833391312731,933.913254109974,933.993039932446,
934.072766247642,934.152450475936,934.232121462157,934.311788915683,934.3914685665,
934.471176148895,934.55097137797,934.630815719678,934.710774146726,934.753170023321,
934.833127323452,934.912990120695,934.992775943167,935.072502258362,935.152186486656,
935.231857472876,935.311524926402,935.391204577219,935.470912159614,935.550707388689,
935.630551730397,935.710510157445,935.752906034041,935.832863334172,935.912726131415,
935.992511953887,936.072238269082,936.151922497375,936.231593483596,936.311260937122,
936.390940587939,936.470648170334,936.550443399409,936.630287741117,936.710246168164,
936.752642044761,936.83474749776,936.916739891055,936.998632017574,937.080410429156,
937.162122335982,937.243767640152,937.313465863271),.UNSPECIFIED.);
#1278=B_SPLINE_CURVE_WITH_KNOTS('',3,(#153533,#153534,#153535,#153536,#153537,
#153538,#153539,#153540,#153541,#153542),.UNSPECIFIED.,.F.,.F.,(4,1,1,1,
1,1,1,4),(937.3134707844,937.752378055481,938.752114066201,939.751850076921,
940.751586087641,941.751322098361,942.751058109081,943.59665117045),
 .UNSPECIFIED.);
#1279=B_SPLINE_CURVE_WITH_KNOTS('',3,(#153544,#153545,#153546,#153547,#153548,
#153549,#153550,#153551,#153552,#153553,#153554),.UNSPECIFIED.,.F.,.F.,
(4,1,1,1,1,1,1,1,4),(943.59665117045,943.750794119802,944.750530130522,
945.750266141242,946.750002151962,947.749738162682,948.749474173402,949.749210184122,
949.87983647763),.UNSPECIFIED.);
#1280=B_SPLINE_CURVE_WITH_KNOTS('',3,(#153556,#153557,#153558,#153559,#153560,
#153561,#153562,#153563,#153564,#153565,#153566,#153567,#153568,#153569,
#153570,#153571,#153572,#153573,#153574,#153575,#153576,#153577,#153578,
#153579,#153580,#153581,#153582,#153583,#153584,#153585,#153586,#153587,
#153588,#153589,#153590,#153591,#153592,#153593,#153594,#153595,#153596,
#153597,#153598,#153599,#153600,#153601,#153602,#153603,#153604,#153605,
#153606,#153607,#153608,#153609,#153610,#153611,#153612,#153613,#153614,
#153615,#153616,#153617,#153618,#153619,#153620,#153621,#153622,#153623,
#153624,#153625,#153626,#153627,#153628,#153629,#153630,#153631,#153632,
#153633,#153634,#153635,#153636,#153637,#153638,#153639,#153640,#153641,
#153642,#153643,#153644,#153645,#153646,#153647,#153648,#153649,#153650,
#153651,#153652,#153653,#153654,#153655,#153656,#153657,#153658,#153659,
#153660,#153661,#153662,#153663,#153664,#153665,#153666,#153667,#153668,
#153669,#153670,#153671,#153672,#153673,#153674,#153675,#153676,#153677,
#153678,#153679,#153680,#153681,#153682,#153683,#153684,#153685,#153686,
#153687,#153688,#153689,#153690,#153691,#153692,#153693,#153694,#153695,
#153696,#153697,#153698,#153699,#153700,#153701,#153702,#153703,#153704,
#153705,#153706,#153707,#153708,#153709,#153710,#153711,#153712,#153713,
#153714,#153715,#153716,#153717,#153718,#153719,#153720,#153721,#153722,
#153723,#153724,#153725,#153726,#153727,#153728,#153729,#153730,#153731,
#153732,#153733,#153734,#153735,#153736,#153737,#153738,#153739,#153740,
#153741,#153742,#153743,#153744,#153745,#153746,#153747,#153748,#153749,
#153750,#153751,#153752,#153753,#153754,#153755,#153756,#153757,#153758,
#153759,#153760,#153761,#153762,#153763,#153764,#153765,#153766,#153767,
#153768,#153769,#153770,#153771,#153772,#153773,#153774,#153775,#153776,
#153777,#153778,#153779,#153780,#153781,#153782,#153783,#153784,#153785,
#153786,#153787,#153788,#153789,#153790,#153791,#153792,#153793,#153794,
#153795,#153796,#153797,#153798,#153799),.UNSPECIFIED.,.F.,.F.,(4,3,3,3,
3,3,3,3,3,3,3,3,3,3,3,3,3,3,3,3,3,3,3,3,3,3,3,3,3,3,3,3,3,3,3,3,3,3,3,3,
3,3,3,3,3,3,3,3,3,3,3,3,3,3,3,3,3,3,3,3,3,3,3,3,3,3,3,3,3,3,3,3,3,3,3,3,
3,3,3,3,3,4),(949.87983647763,949.958583984239,950.037252173226,950.11585943448,
950.194995279526,950.27354633765,950.352095118929,950.430658160405,950.510230169015,
950.588910166874,950.668928180858,950.748946194843,950.828903494974,950.908766292217,
950.988552114689,951.068278429884,951.147962658178,951.227633644399,951.307301097925,
951.386980748741,951.466688331135,951.546483560211,951.626327901919,951.706286328966,
951.748682205563,951.828639505694,951.908502302937,951.988288125409,952.068014440604,
952.147698668898,952.227369655119,952.307037108645,952.386716759462,952.466424341857,
952.546219570932,952.62606391264,952.706022339687,952.748418216283,952.828375516414,
952.908238313657,952.988024136129,953.067750451324,953.147434679617,953.227105665838,
953.306773119364,953.386452770181,953.466160352575,953.545955581651,953.625799923358,
953.705758350406,953.748154227003,953.828111527134,953.907974324377,953.987760146848,
954.067486462044,954.147170690338,954.22684167656,954.306509130085,954.386188780902,
954.465896363296,954.545691592372,954.62553593408,954.705494361127,954.747890237723,
954.827847537854,954.907710335097,954.987496157569,955.067222472764,955.146906701058,
955.226577687279,955.306245140805,955.385924791622,955.465632374017,955.545427603092,
955.6252719448,955.705230371847,955.747626248443,955.83568619894,955.923413789402,
956.010932353538,956.098105389006,956.163021581478),.UNSPECIFIED.);
#1281=B_SPLINE_CURVE_WITH_KNOTS('',3,(#153801,#153802,#153803,#153804,#153805,
#153806,#153807,#153808,#153809,#153810),.UNSPECIFIED.,.F.,.F.,(4,1,1,1,
1,1,1,4),(956.163021784809,956.747362259163,957.747098269883,958.746834280603,
959.746570291324,960.746306302044,961.746042312764,962.446207091989),
 .UNSPECIFIED.);
#1282=B_SPLINE_CURVE_WITH_KNOTS('',3,(#153812,#153813,#153814,#153815,#153816,
#153817,#153818,#153819,#153820,#153821,#153822,#153823,#153824,#153825,
#153826,#153827,#153828,#153829,#153830,#153831,#153832,#153833,#153834,
#153835,#153836,#153837,#153838,#153839,#153840,#153841,#153842,#153843,
#153844,#153845,#153846,#153847,#153848,#153849,#153850,#153851,#153852,
#153853,#153854,#153855,#153856,#153857,#153858,#153859,#153860,#153861,
#153862,#153863,#153864,#153865,#153866,#153867,#153868,#153869,#153870,
#153871,#153872,#153873,#153874,#153875,#153876,#153877,#153878,#153879,
#153880,#153881,#153882,#153883,#153884,#153885,#153886,#153887,#153888,
#153889,#153890,#153891,#153892,#153893,#153894,#153895,#153896,#153897,
#153898,#153899,#153900,#153901,#153902,#153903,#153904,#153905,#153906,
#153907,#153908,#153909,#153910,#153911,#153912,#153913,#153914,#153915,
#153916,#153917,#153918,#153919,#153920,#153921,#153922,#153923,#153924,
#153925,#153926,#153927,#153928,#153929,#153930,#153931,#153932,#153933,
#153934,#153935,#153936,#153937,#153938,#153939,#153940,#153941,#153942,
#153943,#153944,#153945,#153946,#153947,#153948,#153949,#153950,#153951,
#153952,#153953,#153954,#153955,#153956,#153957,#153958,#153959,#153960,
#153961,#153962,#153963,#153964,#153965,#153966,#153967,#153968,#153969,
#153970,#153971,#153972,#153973,#153974,#153975,#153976,#153977,#153978,
#153979,#153980,#153981,#153982,#153983,#153984,#153985,#153986,#153987,
#153988,#153989,#153990,#153991,#153992,#153993,#153994,#153995,#153996,
#153997,#153998,#153999,#154000,#154001,#154002,#154003,#154004,#154005,
#154006,#154007,#154008,#154009,#154010,#154011,#154012,#154013,#154014,
#154015,#154016,#154017,#154018,#154019,#154020,#154021,#154022,#154023,
#154024,#154025,#154026,#154027,#154028,#154029,#154030,#154031,#154032,
#154033,#154034,#154035,#154036,#154037,#154038,#154039,#154040,#154041,
#154042,#154043,#154044,#154045,#154046,#154047,#154048,#154049,#154050,
#154051,#154052,#154053,#154054,#154055),.UNSPECIFIED.,.F.,.F.,(4,3,3,3,
3,3,3,3,3,3,3,3,3,3,3,3,3,3,3,3,3,3,3,3,3,3,3,3,3,3,3,3,3,3,3,3,3,3,3,3,
3,3,3,3,3,3,3,3,3,3,3,3,3,3,3,3,3,3,3,3,3,3,3,3,3,3,3,3,3,3,3,3,3,3,3,3,
3,3,3,3,3,4),(962.446207275155,962.542264496911,962.644021410198,962.745778323484,
962.825735623615,962.905598420857,962.985384243328,963.065110558523,963.144794786817,
963.224465773037,963.304133226562,963.383812877378,963.463520459772,963.543315688847,
963.623160030554,963.703118457601,963.745514334204,963.825471634335,963.905334431578,
963.985120254049,964.064846569245,964.144530797538,964.224201783759,964.303869237285,
964.383548888101,964.463256470496,964.543051699571,964.622896041279,964.702854468326,
964.745250344924,964.825207645056,964.905070442299,964.984856264771,965.064582579967,
965.144266808261,965.223937794482,965.303605248009,965.383284898825,965.46299248122,
965.542787710296,965.622632052004,965.702590479052,965.744986355645,965.824943655776,
965.904806453018,965.98459227549,966.064318590685,966.144002818979,966.223673805199,
966.303341258725,966.383020909541,966.462728491936,966.542523721011,966.622368062718,
966.702326489765,966.744722366364,966.824679666495,966.904542463738,966.98432828621,
967.064054601406,967.1437388297,967.223409815921,967.303077269447,967.382756920263,
967.462464502658,967.542259731733,967.622104073441,967.702062500489,967.744458377085,
967.824210570906,967.903868370934,967.983449501913,968.062971626318,968.146274222924,
968.22574215201,968.305208295397,968.384688558223,968.464198851361,968.543796861733,
968.623446211697,968.703204821876,968.729392399169),.UNSPECIFIED.);
#1283=B_SPLINE_CURVE_WITH_KNOTS('',3,(#154057,#154058,#154059,#154060,#154061,
#154062,#154063,#154064,#154065,#154066,#154067,#154068),.UNSPECIFIED.,
 .F.,.F.,(4,2,1,1,1,1,1,1,4),(968.729392399169,968.744194387805,969.743930398525,
970.743666409245,971.743402419965,972.743138430685,973.742874441405,974.742610452126,
975.012574196375),.UNSPECIFIED.);
#1284=B_SPLINE_CURVE_WITH_KNOTS('',3,(#154070,#154071,#154072,#154073,#154074,
#154075,#154076,#154077,#154078,#154079,#154080,#154081,#154082,#154083,
#154084,#154085,#154086,#154087,#154088,#154089,#154090,#154091,#154092,
#154093,#154094,#154095,#154096,#154097,#154098,#154099,#154100,#154101,
#154102,#154103,#154104,#154105,#154106,#154107,#154108,#154109,#154110,
#154111,#154112,#154113,#154114,#154115,#154116,#154117,#154118,#154119,
#154120,#154121,#154122,#154123,#154124,#154125,#154126,#154127,#154128,
#154129,#154130,#154131,#154132,#154133,#154134,#154135,#154136,#154137,
#154138,#154139,#154140,#154141,#154142,#154143,#154144,#154145,#154146,
#154147,#154148,#154149,#154150,#154151,#154152,#154153,#154154,#154155,
#154156,#154157,#154158,#154159,#154160,#154161,#154162,#154163,#154164,
#154165,#154166,#154167,#154168,#154169,#154170,#154171,#154172,#154173,
#154174,#154175,#154176,#154177,#154178,#154179,#154180,#154181,#154182,
#154183,#154184,#154185,#154186,#154187,#154188,#154189,#154190,#154191,
#154192,#154193,#154194,#154195,#154196,#154197,#154198,#154199,#154200,
#154201,#154202,#154203,#154204,#154205,#154206,#154207,#154208,#154209,
#154210,#154211,#154212,#154213,#154214,#154215,#154216,#154217,#154218,
#154219,#154220,#154221,#154222,#154223,#154224,#154225,#154226,#154227,
#154228,#154229,#154230,#154231,#154232,#154233,#154234,#154235,#154236,
#154237,#154238,#154239,#154240,#154241,#154242,#154243,#154244,#154245,
#154246,#154247,#154248,#154249,#154250,#154251,#154252,#154253,#154254,
#154255,#154256,#154257,#154258,#154259,#154260,#154261,#154262,#154263,
#154264,#154265,#154266,#154267,#154268,#154269,#154270,#154271,#154272,
#154273,#154274,#154275,#154276,#154277,#154278,#154279,#154280,#154281,
#154282,#154283,#154284,#154285,#154286,#154287,#154288,#154289,#154290,
#154291,#154292,#154293,#154294,#154295,#154296,#154297,#154298,#154299,
#154300,#154301,#154302,#154303,#154304,#154305,#154306,#154307,#154308,
#154309,#154310,#154311,#154312,#154313,#154314,#154315,#154316),
 .UNSPECIFIED.,.F.,.F.,(4,3,3,3,3,3,3,3,3,3,3,3,3,3,3,3,3,3,3,3,3,3,3,3,
3,3,3,3,3,3,3,3,3,3,3,3,3,3,3,3,3,3,3,3,3,3,3,3,3,3,3,3,3,3,3,3,3,3,3,3,
3,3,3,3,3,3,3,3,3,3,3,3,3,3,3,3,3,3,3,3,3,3,4),(975.012577706348,975.091541393563,
975.172892027223,975.251800202913,975.330706392125,975.409626904569,975.488578057374,
975.567616783211,975.646708127336,975.72590644325,975.742346462845,975.822303762976,
975.902166560219,975.981952382691,976.061678697887,976.141362926181,976.221033912402,
976.300701365928,976.380381016745,976.46008859914,976.539883828215,976.619728169923,
976.699686596971,976.742082473566,976.822039773697,976.90190257094,976.981688393412,
977.061414708607,977.141098936901,977.220769923122,977.300437376647,977.380117027464,
977.459824609859,977.539619838934,977.619464180642,977.699422607689,977.741818484286,
977.821775784417,977.90163858166,977.981424404131,978.061150719326,978.14083494762,
978.220505933841,978.300173387367,978.379853038183,978.459560620577,978.539355849653,
978.61920019136,978.699158618407,978.741554495006,978.821511795137,978.90137459238,
978.981160414852,979.060886730047,979.140570958341,979.220241944562,979.299909398088,
979.379589048904,979.459296631298,979.539091860374,979.618936202082,979.69889462913,
979.741290505726,979.821247805857,979.9011106031,979.980896425572,980.060622740767,
980.140306969061,980.219977955282,980.299645408808,980.379325059624,980.459032642019,
980.538827871095,980.618672212802,980.69863063985,980.741026516446,980.823302516335,
980.905463515783,980.987521957406,981.069462465544,981.151333907837,981.233133588715,
981.295763013528),.UNSPECIFIED.);
#1285=B_SPLINE_CURVE_WITH_KNOTS('',3,(#154318,#154319,#154320,#154321,#154322,
#154323,#154324,#154325,#154326,#154327),.UNSPECIFIED.,.F.,.F.,(4,1,1,1,
1,1,1,4),(981.295767365742,981.740762527166,982.740498537887,983.740234548607,
984.739970559327,985.739706570047,986.739442580767,987.578948320707),
 .UNSPECIFIED.);
#1286=B_SPLINE_CURVE_WITH_KNOTS('',3,(#154329,#154330,#154331,#154332,#154333,
#154334,#154335,#154336,#154337,#154338,#154339),.UNSPECIFIED.,.F.,.F.,
(4,1,1,1,1,1,1,1,4),(987.578948320707,987.739178591487,988.738914602207,
989.738650612927,990.738386623648,991.738122634368,992.737858645088,993.737594655808,
993.862133627887),.UNSPECIFIED.);
#1287=B_SPLINE_CURVE_WITH_KNOTS('',3,(#154341,#154342,#154343,#154344,#154345,
#154346,#154347,#154348,#154349,#154350,#154351,#154352,#154353,#154354,
#154355,#154356,#154357,#154358,#154359,#154360,#154361,#154362,#154363,
#154364,#154365,#154366,#154367,#154368,#154369,#154370,#154371,#154372,
#154373,#154374,#154375,#154376,#154377,#154378,#154379,#154380,#154381,
#154382,#154383,#154384,#154385,#154386,#154387,#154388,#154389,#154390,
#154391,#154392,#154393,#154394,#154395,#154396,#154397,#154398,#154399,
#154400,#154401,#154402,#154403,#154404,#154405,#154406,#154407,#154408,
#154409,#154410,#154411,#154412,#154413,#154414,#154415,#154416,#154417,
#154418,#154419,#154420,#154421,#154422,#154423,#154424,#154425,#154426,
#154427,#154428,#154429,#154430,#154431,#154432,#154433,#154434,#154435,
#154436,#154437,#154438,#154439,#154440,#154441,#154442,#154443,#154444,
#154445,#154446,#154447,#154448,#154449,#154450,#154451,#154452,#154453,
#154454,#154455,#154456,#154457,#154458,#154459,#154460,#154461,#154462,
#154463,#154464,#154465,#154466,#154467,#154468,#154469,#154470,#154471,
#154472,#154473,#154474,#154475,#154476,#154477,#154478,#154479,#154480,
#154481,#154482,#154483,#154484,#154485,#154486,#154487,#154488,#154489,
#154490,#154491,#154492,#154493,#154494,#154495,#154496,#154497,#154498,
#154499,#154500,#154501,#154502,#154503,#154504,#154505,#154506,#154507,
#154508,#154509,#154510,#154511,#154512,#154513,#154514,#154515,#154516,
#154517,#154518,#154519,#154520,#154521,#154522,#154523,#154524,#154525,
#154526,#154527,#154528,#154529,#154530,#154531,#154532,#154533,#154534,
#154535,#154536,#154537,#154538,#154539,#154540,#154541,#154542,#154543,
#154544,#154545,#154546,#154547,#154548,#154549,#154550,#154551,#154552,
#154553,#154554,#154555,#154556,#154557,#154558,#154559,#154560,#154561,
#154562,#154563,#154564,#154565,#154566,#154567,#154568,#154569,#154570,
#154571,#154572,#154573,#154574,#154575,#154576,#154577,#154578,#154579,
#154580,#154581,#154582,#154583,#154584),.UNSPECIFIED.,.F.,.F.,(4,3,3,3,
3,3,3,3,3,3,3,3,3,3,3,3,3,3,3,3,3,3,3,3,3,3,3,3,3,3,3,3,3,3,3,3,3,3,3,3,
3,3,3,3,3,3,3,3,3,3,3,3,3,3,3,3,3,3,3,3,3,3,3,3,3,3,3,3,3,3,3,3,3,3,3,3,
3,3,3,3,3,4),(993.862133627887,993.940907294356,994.019600459457,994.098231504359,
994.17811889963,994.256690923096,994.335259715897,994.413841803452,994.494714019221,
994.573412485895,994.655371576211,994.737330666528,994.817287966659,994.897150763902,
994.976936586374,995.056662901569,995.136347129863,995.216018116084,995.29568556961,
995.375365220427,995.455072802822,995.534868031897,995.614712373605,995.694670800652,
995.737066677248,995.817023977379,995.896886774622,995.976672597094,996.056398912289,
996.136083140583,996.215754126804,996.295421580329,996.375101231146,996.45480881354,
996.534604042616,996.614448384323,996.694406811371,996.736802687968,996.816759988099,
996.896622785342,996.976408607813,997.056134923009,997.135819151304,997.215490137525,
997.29515759105,997.374837241867,997.454544824261,997.534340053336,997.614184395044,
997.694142822091,997.736538698688,997.81649599882,997.896358796062,997.976144618534,
998.05587093373,998.135555162024,998.215226148245,998.294893601771,998.374573252588,
998.454280834983,998.534076064059,998.613920405767,998.693878832814,998.736274709409,
998.81623200954,998.896094806782,998.975880629253,999.055606944448,999.135291172742,
999.214962158963,999.294629612488,999.374309263304,999.454016845697,999.533812074773,
999.61365641648,999.693614843527,999.736010720129,999.824431802581,999.912507175443,
1000.00036214251,1000.08785478837,1000.14531872231),.UNSPECIFIED.);
#1288=B_SPLINE_CURVE_WITH_KNOTS('',3,(#154586,#154587,#154588,#154589,#154590,
#154591,#154592,#154593,#154594,#154595),.UNSPECIFIED.,.F.,.F.,(4,1,1,1,
1,1,1,4),(1000.14531893507,1000.73574673085,1001.73548274157,1002.73521875229,
1003.73495476301,1004.73469077373,1005.73442678445,1006.42850424225),
 .UNSPECIFIED.);
#1289=B_SPLINE_CURVE_WITH_KNOTS('',3,(#154597,#154598,#154599,#154600,#154601,
#154602,#154603,#154604,#154605,#154606,#154607,#154608,#154609,#154610,
#154611,#154612,#154613,#154614,#154615,#154616,#154617,#154618,#154619,
#154620,#154621,#154622,#154623,#154624,#154625,#154626,#154627,#154628,
#154629,#154630,#154631,#154632,#154633,#154634,#154635,#154636,#154637,
#154638,#154639,#154640,#154641,#154642,#154643,#154644,#154645,#154646,
#154647,#154648,#154649,#154650,#154651,#154652,#154653,#154654,#154655,
#154656,#154657,#154658,#154659,#154660,#154661,#154662,#154663,#154664,
#154665,#154666,#154667,#154668,#154669,#154670,#154671,#154672,#154673,
#154674,#154675,#154676,#154677,#154678,#154679,#154680,#154681,#154682,
#154683,#154684,#154685,#154686,#154687,#154688,#154689,#154690,#154691,
#154692,#154693,#154694,#154695,#154696,#154697,#154698,#154699,#154700,
#154701,#154702,#154703,#154704,#154705,#154706,#154707,#154708,#154709,
#154710,#154711,#154712,#154713,#154714,#154715,#154716,#154717,#154718,
#154719,#154720,#154721,#154722,#154723,#154724,#154725,#154726,#154727,
#154728,#154729,#154730,#154731,#154732,#154733,#154734,#154735,#154736,
#154737,#154738,#154739,#154740,#154741,#154742,#154743,#154744,#154745,
#154746,#154747,#154748,#154749,#154750,#154751,#154752,#154753,#154754,
#154755,#154756,#154757,#154758,#154759,#154760,#154761,#154762,#154763,
#154764,#154765,#154766,#154767,#154768,#154769,#154770,#154771,#154772,
#154773,#154774,#154775,#154776,#154777,#154778,#154779,#154780,#154781,
#154782,#154783,#154784,#154785,#154786,#154787,#154788,#154789,#154790,
#154791,#154792,#154793,#154794,#154795,#154796,#154797,#154798,#154799,
#154800,#154801,#154802,#154803,#154804,#154805,#154806,#154807,#154808,
#154809,#154810,#154811,#154812,#154813,#154814,#154815,#154816,#154817,
#154818,#154819,#154820,#154821,#154822,#154823,#154824,#154825,#154826,
#154827,#154828,#154829,#154830,#154831,#154832,#154833,#154834,#154835,
#154836,#154837,#154838,#154839,#154840,#154841,#154842,#154843),
 .UNSPECIFIED.,.F.,.F.,(4,3,3,3,3,3,3,3,3,3,3,3,3,3,3,3,3,3,3,3,3,3,3,3,
3,3,3,3,3,3,3,3,3,3,3,3,3,3,3,3,3,3,3,3,3,3,3,3,3,3,3,3,3,3,3,3,3,3,3,3,
3,3,3,3,3,3,3,3,3,3,3,3,3,3,3,3,3,3,3,3,3,3,4),(1006.42850443757,1006.52392891918,
1006.62009994949,1006.71707095298,1006.73416279517,1006.8141200953,1006.89398289255,
1006.97376871502,1007.05349503022,1007.13317925852,1007.21285024474,1007.29251769827,
1007.37219734909,1007.45190493148,1007.53170016056,1007.61154450227,1007.69150292932,
1007.73389880589,1007.81385610602,1007.89371890326,1007.97350472574,1008.05323104093,
1008.13291526922,1008.21258625545,1008.29225370897,1008.37193335979,1008.45164094218,
1008.53143617126,1008.61128051296,1008.69123894001,1008.73363481661,1008.81359211674,
1008.89345491398,1008.97324073645,1009.05296705165,1009.13265127994,1009.21232226616,
1009.29198971969,1009.3716693705,1009.4513769529,1009.53117218197,1009.61101652368,
1009.69097495073,1009.73337082733,1009.81332812746,1009.8931909247,1009.97297674718,
1010.05270306237,1010.13238729067,1010.21205827689,1010.29172573041,1010.37140538123,
1010.45111296362,1010.5309081927,1010.61075253441,1010.69071096146,1010.73310683805,
1010.81306413818,1010.89292693542,1010.97271275789,1011.05243907309,1011.13212330138,
1011.2117942876,1011.29146174113,1011.37114139195,1011.45084897434,1011.53064420341,
1011.61048854512,1011.69044697217,1011.73284284877,1011.81251666311,1011.89209613433,
1011.9715990584,1012.05104316828,1012.13362396592,1012.2130145472,1012.2924035767,
1012.37180702271,1012.45124085961,1012.53076213062,1012.61033519284,1012.69001597921,
1012.71168954943),.UNSPECIFIED.);
#1290=B_SPLINE_CURVE_WITH_KNOTS('',3,(#154845,#154846,#154847,#154848,#154849,
#154850,#154851,#154852,#154853,#154854,#154855,#154856,#154857),
 .UNSPECIFIED.,.F.,.F.,(4,3,1,1,1,1,1,1,4),(1012.71168954943,1012.73257885949,
1013.73231487021,1014.73205088093,1015.73178689165,1016.73152290237,1017.73125891309,
1018.73099492381,1018.99487485661),.UNSPECIFIED.);
#1291=B_SPLINE_CURVE_WITH_KNOTS('',3,(#154859,#154860,#154861,#154862,#154863,
#154864,#154865,#154866,#154867,#154868),.UNSPECIFIED.,.F.,.F.,(4,1,1,1,
1,1,1,4),(1018.99487485661,1019.73073093453,1020.73046694525,1021.73020295597,
1022.72993896669,1023.72967497741,1024.72941098813,1025.27806016378),
 .UNSPECIFIED.);
#1292=B_SPLINE_CURVE_WITH_KNOTS('',3,(#154870,#154871,#154872,#154873,#154874,
#154875,#154876,#154877,#154878,#154879),.UNSPECIFIED.,.F.,.F.,(4,1,1,1,
1,1,1,4),(1025.27806016378,1025.72914699885,1026.72888300957,1027.72861902029,
1028.72835503101,1029.72809104173,1030.72782705245,1031.56124547096),
 .UNSPECIFIED.);
#1293=B_SPLINE_CURVE_WITH_KNOTS('',3,(#154881,#154882,#154883,#154884,#154885,
#154886,#154887,#154888,#154889,#154890,#154891),.UNSPECIFIED.,.F.,.F.,
(4,1,1,1,1,1,1,1,4),(1031.56124547096,1031.72756306317,1032.72729907389,
1033.72703508461,1034.72677109533,1035.72650710605,1036.72624311677,1037.72597912749,
1037.84443077814),.UNSPECIFIED.);
#1294=B_SPLINE_CURVE_WITH_KNOTS('',3,(#154893,#154894,#154895,#154896,#154897,
#154898,#154899,#154900,#154901,#154902,#154903,#154904,#154905,#154906,
#154907,#154908,#154909,#154910,#154911,#154912,#154913,#154914,#154915,
#154916,#154917,#154918,#154919,#154920,#154921,#154922,#154923,#154924,
#154925,#154926,#154927,#154928,#154929,#154930,#154931,#154932,#154933,
#154934,#154935,#154936,#154937,#154938,#154939,#154940,#154941,#154942,
#154943,#154944,#154945,#154946,#154947,#154948,#154949,#154950,#154951,
#154952,#154953,#154954,#154955,#154956,#154957,#154958,#154959,#154960,
#154961,#154962,#154963,#154964,#154965,#154966,#154967,#154968,#154969,
#154970,#154971,#154972,#154973,#154974,#154975,#154976,#154977,#154978,
#154979,#154980,#154981,#154982,#154983,#154984,#154985,#154986,#154987,
#154988,#154989,#154990,#154991,#154992,#154993,#154994,#154995,#154996,
#154997,#154998,#154999,#155000,#155001,#155002,#155003,#155004,#155005,
#155006,#155007,#155008,#155009,#155010,#155011,#155012,#155013,#155014,
#155015,#155016,#155017,#155018,#155019,#155020,#155021,#155022,#155023,
#155024,#155025,#155026,#155027,#155028,#155029,#155030,#155031,#155032,
#155033,#155034,#155035,#155036,#155037,#155038,#155039,#155040,#155041,
#155042,#155043,#155044,#155045,#155046,#155047,#155048,#155049,#155050,
#155051,#155052,#155053,#155054,#155055,#155056,#155057,#155058,#155059,
#155060,#155061,#155062,#155063,#155064,#155065,#155066,#155067,#155068,
#155069,#155070,#155071,#155072,#155073,#155074,#155075,#155076,#155077,
#155078,#155079,#155080,#155081,#155082,#155083,#155084,#155085,#155086,
#155087,#155088,#155089,#155090,#155091,#155092,#155093,#155094,#155095,
#155096,#155097,#155098,#155099,#155100,#155101,#155102,#155103,#155104,
#155105,#155106,#155107,#155108,#155109,#155110,#155111,#155112,#155113,
#155114,#155115,#155116,#155117,#155118,#155119,#155120,#155121,#155122,
#155123,#155124,#155125,#155126,#155127,#155128,#155129,#155130,#155131,
#155132,#155133,#155134,#155135,#155136,#155137,#155138,#155139),
 .UNSPECIFIED.,.F.,.F.,(4,3,3,3,3,3,3,3,3,3,3,3,3,3,3,3,3,3,3,3,3,3,3,3,
3,3,3,3,3,3,3,3,3,3,3,3,3,3,3,3,3,3,3,3,3,3,3,3,3,3,3,3,3,3,3,3,3,3,3,3,
3,3,3,3,3,3,3,3,3,3,3,3,3,3,3,3,3,3,3,3,3,3,4),(1037.84443077814,1037.92323353131,
1038.00195463676,1038.08061246473,1038.16125029891,1038.2398463353,1038.31843821249,
1038.39704244251,1038.47921061644,1038.55793065408,1038.63670281158,1038.71557848102,
1038.72571513821,1038.80567243834,1038.88553523558,1038.96532105806,1039.04504737325,
1039.12473160154,1039.20440258777,1039.28407004129,1039.36374969211,1039.4434572745,
1039.52325250358,1039.60309684529,1039.68305527233,1039.72545114893,1039.80540844906,
1039.8852712463,1039.96505706878,1040.04478338397,1040.12446761226,1040.20413859849,
1040.28380605201,1040.36348570283,1040.44319328522,1040.5229885143,1040.60283285601,
1040.68279128305,1040.72518715965,1040.80514445978,1040.88500725702,1040.9647930795,
1041.04451939469,1041.12420362299,1041.20387460921,1041.28354206273,1041.36322171355,
1041.44292929594,1041.52272452502,1041.60256886673,1041.68252729378,1041.72492317037,
1041.8048804705,1041.88474326774,1041.96452909022,1042.04425540541,1042.12393963371,
1042.20361061993,1042.28327807345,1042.36295772427,1042.44266530666,1042.52246053574,
1042.60230487745,1042.68226330449,1042.72465918109,1042.80461648122,1042.88447927846,
1042.96426510094,1043.04399141613,1043.12367564442,1043.20334663065,1043.28301408417,
1043.36269373499,1043.44240131738,1043.52219654646,1043.60204088816,1043.68199931521,
1043.72439519181,1043.81318968657,1043.90162420445,1043.98982593053,1044.07764761709,
1044.12761586414),.UNSPECIFIED.);
#1295=B_SPLINE_CURVE_WITH_KNOTS('',3,(#155141,#155142,#155143,#155144,#155145,
#155146,#155147,#155148,#155149,#155150),.UNSPECIFIED.,.F.,.F.,(4,1,1,1,
1,1,1,4),(1044.12761608532,1044.72413120253,1045.72386721325,1046.72360322397,
1047.72333923469,1048.72307524541,1049.72281125614,1050.4108013925),
 .UNSPECIFIED.);
#1296=B_SPLINE_CURVE_WITH_KNOTS('',3,(#155152,#155153,#155154,#155155,#155156,
#155157,#155158,#155159,#155160,#155161,#155162,#155163,#155164,#155165,
#155166,#155167,#155168,#155169,#155170,#155171,#155172,#155173,#155174,
#155175,#155176,#155177,#155178,#155179,#155180,#155181,#155182,#155183,
#155184,#155185,#155186,#155187,#155188,#155189,#155190,#155191,#155192,
#155193,#155194,#155195,#155196,#155197,#155198,#155199,#155200,#155201,
#155202,#155203,#155204,#155205,#155206,#155207,#155208,#155209,#155210,
#155211,#155212,#155213,#155214,#155215,#155216,#155217,#155218,#155219,
#155220,#155221,#155222,#155223,#155224,#155225,#155226,#155227,#155228,
#155229,#155230,#155231,#155232,#155233,#155234,#155235,#155236,#155237,
#155238,#155239,#155240,#155241,#155242,#155243,#155244,#155245,#155246,
#155247,#155248,#155249,#155250,#155251,#155252,#155253,#155254,#155255,
#155256,#155257,#155258,#155259,#155260,#155261,#155262,#155263,#155264,
#155265,#155266,#155267,#155268,#155269,#155270,#155271,#155272,#155273,
#155274,#155275,#155276,#155277,#155278,#155279,#155280,#155281,#155282,
#155283,#155284,#155285,#155286,#155287,#155288,#155289,#155290,#155291,
#155292,#155293,#155294,#155295,#155296,#155297,#155298,#155299,#155300,
#155301,#155302,#155303,#155304,#155305,#155306,#155307,#155308,#155309,
#155310,#155311,#155312,#155313,#155314,#155315,#155316,#155317,#155318,
#155319,#155320,#155321,#155322,#155323,#155324,#155325,#155326,#155327,
#155328,#155329,#155330,#155331,#155332,#155333,#155334,#155335,#155336,
#155337,#155338,#155339,#155340,#155341,#155342,#155343,#155344,#155345,
#155346,#155347,#155348,#155349,#155350,#155351,#155352,#155353,#155354,
#155355,#155356,#155357,#155358,#155359,#155360,#155361,#155362,#155363,
#155364,#155365,#155366,#155367,#155368,#155369,#155370,#155371,#155372,
#155373,#155374,#155375,#155376,#155377,#155378,#155379,#155380,#155381,
#155382,#155383,#155384,#155385,#155386,#155387,#155388,#155389,#155390,
#155391,#155392,#155393,#155394,#155395,#155396,#155397,#155398),
 .UNSPECIFIED.,.F.,.F.,(4,3,3,3,3,3,3,3,3,3,3,3,3,3,3,3,3,3,3,3,3,3,3,3,
3,3,3,3,3,3,3,3,3,3,3,3,3,3,3,3,3,3,3,3,3,3,3,3,3,3,3,3,3,3,3,3,3,3,3,3,
3,3,3,3,3,3,3,3,3,3,3,3,3,3,3,3,3,3,3,3,3,3,4),(1050.41080159846,1050.50561867196,
1050.60112629621,1050.69739631959,1050.72254726686,1050.80250456699,1050.88236736423,
1050.9621531867,1051.0418795019,1051.12156373019,1051.20123471641,1051.28090216994,
1051.36058182075,1051.44028940315,1051.52008463222,1051.59992897393,1051.67988740098,
1051.72228327758,1051.80224057771,1051.88210337495,1051.96188919743,1052.04161551262,
1052.12129974091,1052.20097072714,1052.28063818066,1052.36031783148,1052.44002541387,
1052.51982064295,1052.59966498466,1052.6796234117,1052.7220192883,1052.80197658843,
1052.88183938567,1052.96162520815,1053.04135152334,1053.12103575164,1053.20070673786,
1053.28037419138,1053.3600538422,1053.43976142459,1053.51955665367,1053.59940099538,
1053.67935942242,1053.72175529902,1053.80171259915,1053.88157539639,1053.96136121887,
1054.04108753406,1054.12077176236,1054.20044274858,1054.2801102021,1054.35978985292,
1054.43949743531,1054.51929266439,1054.5991370061,1054.67909543314,1054.72149130974,
1054.80144860987,1054.88131140712,1054.96109722959,1055.04082354478,1055.12050777308,
1055.2001787593,1055.27984621283,1055.35952586364,1055.43923344604,1055.51902867512,
1055.59887301682,1055.67883144387,1055.72122732046,1055.80082617924,1055.88033074753,
1055.95975888751,1056.0391283975,1056.12098568527,1056.2003022785,1056.27961752731,
1056.35894745853,1056.43830810537,1056.51775582873,1056.59725575641,1056.67686180204,
1056.69398669968),.UNSPECIFIED.);
#1297=B_SPLINE_CURVE_WITH_KNOTS('',3,(#155400,#155401,#155402,#155403,#155404,
#155405,#155406,#155407,#155408,#155409,#155410,#155411,#155412),
 .UNSPECIFIED.,.F.,.F.,(4,3,1,1,1,1,1,1,4),(1056.69398669968,1056.72096333118,
1057.7206993419,1058.72043535262,1059.72017136334,1060.71990737406,1061.71964338478,
1062.7193793955,1062.97717200686),.UNSPECIFIED.);
#1298=B_SPLINE_CURVE_WITH_KNOTS('',3,(#155414,#155415,#155416,#155417,#155418,
#155419,#155420,#155421,#155422,#155423),.UNSPECIFIED.,.F.,.F.,(4,1,1,1,
1,1,1,4),(1062.97717200686,1063.71911540622,1064.71885141694,1065.71858742766,
1066.71832343838,1067.7180594491,1068.71779545982,1069.26035731404),
 .UNSPECIFIED.);
#1299=B_SPLINE_CURVE_WITH_KNOTS('',3,(#155425,#155426,#155427,#155428,#155429,
#155430,#155431,#155432,#155433,#155434,#155435,#155436,#155437,#155438,
#155439,#155440,#155441,#155442,#155443,#155444,#155445,#155446,#155447,
#155448,#155449,#155450,#155451,#155452,#155453,#155454,#155455,#155456,
#155457,#155458,#155459,#155460,#155461,#155462,#155463,#155464,#155465,
#155466,#155467,#155468,#155469,#155470,#155471,#155472,#155473,#155474,
#155475,#155476,#155477,#155478,#155479,#155480,#155481,#155482,#155483,
#155484,#155485,#155486,#155487,#155488,#155489,#155490,#155491,#155492,
#155493,#155494,#155495,#155496,#155497,#155498,#155499,#155500,#155501,
#155502,#155503,#155504,#155505,#155506,#155507,#155508,#155509,#155510,
#155511,#155512,#155513,#155514,#155515,#155516,#155517,#155518,#155519,
#155520,#155521,#155522,#155523,#155524,#155525,#155526,#155527,#155528,
#155529,#155530,#155531,#155532,#155533,#155534,#155535,#155536,#155537,
#155538,#155539,#155540,#155541,#155542,#155543,#155544,#155545,#155546,
#155547,#155548,#155549,#155550,#155551,#155552,#155553,#155554,#155555,
#155556,#155557,#155558,#155559,#155560,#155561,#155562,#155563,#155564,
#155565,#155566,#155567,#155568,#155569,#155570,#155571,#155572,#155573,
#155574,#155575,#155576,#155577,#155578,#155579,#155580,#155581,#155582,
#155583,#155584,#155585,#155586,#155587,#155588,#155589,#155590,#155591,
#155592,#155593,#155594,#155595,#155596,#155597,#155598,#155599,#155600,
#155601,#155602,#155603,#155604,#155605,#155606,#155607,#155608,#155609,
#155610,#155611,#155612,#155613,#155614,#155615,#155616,#155617,#155618,
#155619,#155620,#155621,#155622,#155623,#155624,#155625,#155626,#155627,
#155628,#155629,#155630,#155631,#155632,#155633,#155634,#155635,#155636,
#155637,#155638,#155639,#155640,#155641,#155642,#155643,#155644,#155645,
#155646,#155647,#155648,#155649,#155650,#155651,#155652,#155653,#155654,
#155655,#155656,#155657,#155658,#155659,#155660,#155661,#155662,#155663,
#155664,#155665,#155666,#155667,#155668,#155669,#155670,#155671),
 .UNSPECIFIED.,.F.,.F.,(4,3,3,3,3,3,3,3,3,3,3,3,3,3,3,3,3,3,3,3,3,3,3,3,
3,3,3,3,3,3,3,3,3,3,3,3,3,3,3,3,3,3,3,3,3,3,3,3,3,3,3,3,3,3,3,3,3,3,3,3,
3,3,3,3,3,3,3,3,3,3,3,3,3,3,3,3,3,3,3,3,3,3,4),(1069.26035754479,1069.34545859664,
1069.43072803692,1069.51625386385,1069.60191842313,1069.6877916665,1069.71753147054,
1069.79748877067,1069.87735156791,1069.95713739038,1070.03686370557,1070.11654793387,
1070.19621892009,1070.27588637361,1070.35556602442,1070.43527360682,1070.51506883589,
1070.5949131776,1070.67487160464,1070.71726748126,1070.79722478139,1070.87708757863,
1070.95687340111,1071.0365997163,1071.11628394459,1071.19595493082,1071.27562238434,
1071.35530203516,1071.43500961755,1071.51480484663,1071.59464918833,1071.67460761538,
1071.71700349198,1071.79696079211,1071.87682358935,1071.95660941183,1072.03633572702,
1072.11601995532,1072.19569094154,1072.27535839506,1072.35503804588,1072.43474562828,
1072.51454085735,1072.59438519906,1072.67434362611,1072.7167395027,1072.79669680283,
1072.87655960007,1072.95634542255,1073.03607173774,1073.11575596603,1073.19542695225,
1073.27509440578,1073.3547740566,1073.43448163899,1073.51427686807,1073.59412120977,
1073.67407963682,1073.71647551342,1073.79643281355,1073.87629561079,1073.95608143327,
1074.03580774846,1074.11549197676,1074.19516296298,1074.27483041651,1074.35451006732,
1074.43421764972,1074.51401287879,1074.5938572205,1074.67381564755,1074.71621152414,
1074.79497519234,1074.87364476551,1074.95223873817,1075.03077190006,1075.10927232987,
1075.18775661242,1075.26624131795,1075.34477454951,1075.42333461854,1075.50197703655,
1075.54354262122),.UNSPECIFIED.);
#1300=B_SPLINE_CURVE_WITH_KNOTS('',3,(#155673,#155674,#155675,#155676,#155677,
#155678,#155679,#155680,#155681,#155682,#155683,#155684),.UNSPECIFIED.,
 .F.,.F.,(4,2,1,1,1,1,1,1,4),(1075.54354262122,1075.71594753486,1076.71568354558,
1077.7154195563,1078.71515556702,1079.71489157774,1080.71462758846,1081.71436359918,
1081.8267279284),.UNSPECIFIED.);
#1301=B_SPLINE_CURVE_WITH_KNOTS('',3,(#155686,#155687,#155688,#155689,#155690,
#155691,#155692,#155693,#155694,#155695),.UNSPECIFIED.,.F.,.F.,(4,1,1,1,
1,1,1,4),(1081.8267279284,1082.7140996099,1083.71383562062,1084.71357163134,
1085.71330764206,1086.71304365278,1087.7127796635,1088.10991323558),
 .UNSPECIFIED.);
#1302=B_SPLINE_CURVE_WITH_KNOTS('',3,(#155697,#155698,#155699,#155700,#155701,
#155702,#155703,#155704,#155705,#155706),.UNSPECIFIED.,.F.,.F.,(4,1,1,1,
1,1,1,4),(1088.10991323558,1088.71251567422,1089.71225168494,1090.71198769566,
1091.71172370638,1092.7114597171,1093.71119572782,1094.39309854276),
 .UNSPECIFIED.);
#1303=B_SPLINE_CURVE_WITH_KNOTS('',3,(#155708,#155709,#155710,#155711,#155712,
#155713,#155714,#155715,#155716,#155717),.UNSPECIFIED.,.F.,.F.,(4,1,1,1,
1,1,1,4),(1094.39309854276,1094.71093173854,1095.71066774926,1096.71040375998,
1097.7101397707,1098.70987578142,1099.70961179214,1100.67627932462),
 .UNSPECIFIED.);
#1304=B_SPLINE_CURVE_WITH_KNOTS('',3,(#155719,#155720,#155721,#155722,#155723,
#155724,#155725,#155726,#155727,#155728,#155729,#155730,#155731,#155732,
#155733,#155734,#155735,#155736,#155737,#155738,#155739,#155740,#155741,
#155742,#155743,#155744,#155745,#155746,#155747,#155748,#155749,#155750,
#155751,#155752,#155753,#155754,#155755,#155756,#155757,#155758,#155759,
#155760,#155761,#155762,#155763,#155764,#155765,#155766,#155767,#155768,
#155769,#155770,#155771,#155772,#155773,#155774,#155775,#155776,#155777,
#155778,#155779,#155780,#155781,#155782,#155783,#155784,#155785,#155786,
#155787,#155788,#155789,#155790,#155791,#155792,#155793,#155794,#155795,
#155796,#155797,#155798,#155799,#155800,#155801,#155802,#155803,#155804,
#155805,#155806,#155807,#155808,#155809,#155810,#155811,#155812,#155813,
#155814,#155815,#155816,#155817,#155818,#155819,#155820,#155821,#155822,
#155823,#155824,#155825,#155826,#155827,#155828,#155829,#155830,#155831,
#155832,#155833,#155834,#155835,#155836,#155837,#155838,#155839,#155840,
#155841,#155842,#155843,#155844,#155845,#155846,#155847,#155848,#155849,
#155850,#155851,#155852,#155853,#155854,#155855,#155856,#155857,#155858,
#155859,#155860,#155861,#155862,#155863,#155864,#155865,#155866,#155867,
#155868,#155869,#155870,#155871,#155872,#155873,#155874,#155875,#155876,
#155877,#155878,#155879,#155880,#155881,#155882,#155883,#155884,#155885,
#155886,#155887,#155888,#155889,#155890,#155891,#155892,#155893,#155894,
#155895,#155896,#155897,#155898,#155899,#155900,#155901,#155902,#155903,
#155904,#155905,#155906,#155907,#155908,#155909,#155910,#155911,#155912,
#155913,#155914,#155915,#155916,#155917,#155918,#155919,#155920,#155921,
#155922,#155923,#155924,#155925,#155926,#155927,#155928,#155929,#155930,
#155931,#155932,#155933,#155934,#155935,#155936,#155937,#155938,#155939,
#155940,#155941,#155942,#155943,#155944,#155945,#155946,#155947,#155948,
#155949,#155950,#155951,#155952,#155953,#155954,#155955,#155956,#155957,
#155958,#155959,#155960,#155961,#155962,#155963,#155964,#155965),
 .UNSPECIFIED.,.F.,.F.,(4,3,3,3,3,3,3,3,3,3,3,3,3,3,3,3,3,3,3,3,3,3,3,3,
3,3,3,3,3,3,3,3,3,3,3,3,3,3,3,3,3,3,3,3,3,3,3,3,3,3,3,3,3,3,3,3,3,3,3,3,
3,3,3,3,3,3,3,3,3,3,3,3,3,3,3,3,3,3,3,3,3,3,4),(1100.67628384994,1100.70934780286,
1100.78930510299,1100.86916790023,1100.94895372271,1101.0286800379,1101.1083642662,
1101.18803525242,1101.26770270594,1101.34738235676,1101.42708993915,1101.50688516823,
1101.58672950994,1101.66668793698,1101.70908381358,1101.78904111371,1101.86890391095,
1101.94868973343,1102.02841604862,1102.10810027692,1102.18777126314,1102.26743871666,
1102.34711836748,1102.42682594987,1102.50662117895,1102.58646552066,1102.6664239477,
1102.7088198243,1102.78877712443,1102.86863992167,1102.94842574415,1103.02815205934,
1103.10783628764,1103.18750727386,1103.26717472738,1103.3468543782,1103.42656196059,
1103.50635718967,1103.58620153138,1103.66615995842,1103.70855583502,1103.78851313515,
1103.86837593239,1103.94816175487,1104.02788807006,1104.10757229835,1104.18724328458,
1104.2669107381,1104.34659038892,1104.42629797131,1104.50609320039,1104.5859375421,
1104.66589596914,1104.70829184574,1104.78824914587,1104.86811194311,1104.94789776559,
1105.02762408078,1105.10730830908,1105.1869792953,1105.26664674882,1105.34632639964,
1105.42603398203,1105.50582921111,1105.58567355282,1105.66563197986,1105.70802785646,
1105.78798515659,1105.86784795383,1105.94763377631,1106.0273600915,1106.10704431979,
1106.18671530602,1106.26638275954,1106.34606241036,1106.42576999275,1106.50556522183,
1106.58540956353,1106.66536799058,1106.70776386718,1106.8123055036,1106.91467660682,
1106.95946909753),.UNSPECIFIED.);
#1305=B_SPLINE_CURVE_WITH_KNOTS('',3,(#155967,#155968,#155969,#155970,#155971,
#155972,#155973,#155974,#155975,#155976),.UNSPECIFIED.,.F.,.F.,(4,1,1,1,
1,1,1,4),(1106.95946915712,1107.7074998779,1108.70723588862,1109.70697189934,
1110.70670791006,1111.70644392078,1112.7061799315,1113.2426544643),
 .UNSPECIFIED.);
#1306=B_SPLINE_CURVE_WITH_KNOTS('',3,(#155978,#155979,#155980,#155981,#155982,
#155983,#155984,#155985,#155986,#155987,#155988,#155989,#155990,#155991,
#155992,#155993,#155994,#155995,#155996,#155997,#155998,#155999,#156000,
#156001,#156002,#156003,#156004,#156005,#156006,#156007,#156008,#156009,
#156010,#156011,#156012,#156013,#156014,#156015,#156016,#156017,#156018,
#156019,#156020,#156021,#156022,#156023,#156024,#156025,#156026,#156027,
#156028,#156029,#156030,#156031,#156032,#156033,#156034,#156035,#156036,
#156037,#156038,#156039,#156040,#156041,#156042,#156043,#156044,#156045,
#156046,#156047,#156048,#156049,#156050,#156051,#156052,#156053,#156054,
#156055,#156056,#156057,#156058,#156059,#156060,#156061,#156062,#156063,
#156064,#156065,#156066,#156067,#156068,#156069,#156070,#156071,#156072,
#156073,#156074,#156075,#156076,#156077,#156078,#156079,#156080,#156081,
#156082,#156083,#156084,#156085,#156086,#156087,#156088,#156089,#156090,
#156091,#156092,#156093,#156094,#156095,#156096,#156097,#156098,#156099,
#156100,#156101,#156102,#156103,#156104,#156105,#156106,#156107,#156108,
#156109,#156110,#156111,#156112,#156113,#156114,#156115,#156116,#156117,
#156118,#156119,#156120,#156121,#156122,#156123,#156124,#156125,#156126,
#156127,#156128,#156129,#156130,#156131,#156132,#156133,#156134,#156135,
#156136,#156137,#156138,#156139,#156140,#156141,#156142,#156143,#156144,
#156145,#156146,#156147,#156148,#156149,#156150,#156151,#156152,#156153,
#156154,#156155,#156156,#156157,#156158,#156159,#156160,#156161,#156162,
#156163,#156164,#156165,#156166,#156167,#156168,#156169,#156170,#156171,
#156172,#156173,#156174,#156175,#156176,#156177,#156178,#156179,#156180,
#156181,#156182,#156183,#156184,#156185,#156186,#156187,#156188,#156189,
#156190,#156191,#156192,#156193,#156194,#156195,#156196,#156197,#156198,
#156199,#156200,#156201,#156202,#156203,#156204,#156205,#156206,#156207,
#156208,#156209,#156210,#156211,#156212,#156213,#156214,#156215,#156216,
#156217,#156218,#156219,#156220,#156221,#156222,#156223,#156224),
 .UNSPECIFIED.,.F.,.F.,(4,3,3,3,3,3,3,3,3,3,3,3,3,3,3,3,3,3,3,3,3,3,3,3,
3,3,3,3,3,3,3,3,3,3,3,3,3,3,3,3,3,3,3,3,3,3,3,3,3,3,3,3,3,3,3,3,3,3,3,3,
3,3,3,3,3,3,3,3,3,3,3,3,3,3,3,3,3,3,3,3,3,3,4),(1113.24265466419,1113.32749967178,
1113.41250237364,1113.49775111346,1113.58313209121,1113.66871953895,1113.70591594222,
1113.78587324235,1113.8657360396,1113.94552186207,1114.02524817726,1114.10493240556,
1114.18460339178,1114.26427084531,1114.34395049612,1114.42365807852,1114.50345330759,
1114.5832976493,1114.66325607635,1114.70565195294,1114.78560925307,1114.86547205031,
1114.94525787279,1115.02498418798,1115.10466841628,1115.1843394025,1115.26400685602,
1115.34368650684,1115.42339408923,1115.50318931831,1115.58303366002,1115.66299208706,
1115.70538796366,1115.78534526379,1115.86520806103,1115.94499388351,1116.0247201987,
1116.10440442699,1116.18407541322,1116.26374286674,1116.34342251756,1116.42313009995,
1116.50292532903,1116.58276967073,1116.66272809778,1116.70512397438,1116.78508127451,
1116.86494407175,1116.94472989423,1117.02445620942,1117.10414043772,1117.18381142394,
1117.26347887746,1117.34315852828,1117.42286611067,1117.50266133975,1117.58250568146,
1117.6624641085,1117.7048599851,1117.78481728523,1117.86468008247,1117.94446590494,
1118.02419222014,1118.10387644843,1118.18354743465,1118.26321488818,1118.342894539,
1118.42260212139,1118.50239735047,1118.58224169217,1118.66220011922,1118.70459599582,
1118.7833633104,1118.86203643875,1118.94063387376,1119.01917018146,1119.09767362819,
1119.17616079713,1119.25464825675,1119.33318293803,1119.41174439006,1119.49038526826,
1119.52583977148),.UNSPECIFIED.);
#1307=B_SPLINE_CURVE_WITH_KNOTS('',3,(#156226,#156227,#156228,#156229,#156230,
#156231,#156232,#156233,#156234,#156235,#156236,#156237),.UNSPECIFIED.,
 .F.,.F.,(4,2,1,1,1,1,1,1,4),(1119.52583977148,1119.70433200654,1120.70406801726,
1121.70380402798,1122.7035400387,1123.70327604942,1124.70301206014,1125.70274807086,
1125.80902507866),.UNSPECIFIED.);
#1308=B_SPLINE_CURVE_WITH_KNOTS('',3,(#156239,#156240,#156241,#156242,#156243,
#156244,#156245,#156246,#156247,#156248),.UNSPECIFIED.,.F.,.F.,(4,1,1,1,
1,1,1,4),(1125.80902507866,1126.70248408158,1127.70222009231,1128.70195610303,
1129.70169211375,1130.70142812447,1131.70116413519,1132.09221038584),
 .UNSPECIFIED.);
#1309=B_SPLINE_CURVE_WITH_KNOTS('',3,(#156250,#156251,#156252,#156253,#156254,
#156255,#156256,#156257,#156258,#156259),.UNSPECIFIED.,.F.,.F.,(4,1,1,1,
1,1,1,4),(1132.09221038584,1132.70090014591,1133.70063615663,1134.70037216735,
1135.70010817807,1136.69984418879,1137.69958019951,1138.37539569302),
 .UNSPECIFIED.);
#1310=B_SPLINE_CURVE_WITH_KNOTS('',3,(#156261,#156262,#156263,#156264,#156265,
#156266,#156267,#156268,#156269,#156270),.UNSPECIFIED.,.F.,.F.,(4,1,1,1,
1,1,1,4),(1138.37539569302,1138.69931621023,1139.69905222095,1140.69878823167,
1141.69852424239,1142.69826025311,1143.69799626383,1144.65857562991),
 .UNSPECIFIED.);
#1311=B_SPLINE_CURVE_WITH_KNOTS('',3,(#156272,#156273,#156274,#156275,#156276,
#156277,#156278,#156279,#156280,#156281,#156282,#156283,#156284,#156285,
#156286,#156287,#156288,#156289,#156290,#156291,#156292,#156293,#156294,
#156295,#156296,#156297,#156298,#156299,#156300,#156301,#156302,#156303,
#156304,#156305,#156306,#156307,#156308,#156309,#156310,#156311,#156312,
#156313,#156314,#156315,#156316,#156317,#156318,#156319,#156320,#156321,
#156322,#156323,#156324,#156325,#156326,#156327,#156328,#156329,#156330,
#156331,#156332,#156333,#156334,#156335,#156336,#156337,#156338,#156339,
#156340,#156341,#156342,#156343,#156344,#156345,#156346,#156347,#156348,
#156349,#156350,#156351,#156352,#156353,#156354,#156355,#156356,#156357,
#156358,#156359,#156360,#156361,#156362,#156363,#156364,#156365,#156366,
#156367,#156368,#156369,#156370,#156371,#156372,#156373,#156374,#156375,
#156376,#156377,#156378,#156379,#156380,#156381,#156382,#156383,#156384,
#156385,#156386,#156387,#156388,#156389,#156390,#156391,#156392,#156393,
#156394,#156395,#156396,#156397,#156398,#156399,#156400,#156401,#156402,
#156403,#156404,#156405,#156406,#156407,#156408,#156409,#156410,#156411,
#156412,#156413,#156414,#156415,#156416,#156417,#156418,#156419,#156420,
#156421,#156422,#156423,#156424,#156425,#156426,#156427,#156428,#156429,
#156430,#156431,#156432,#156433,#156434,#156435,#156436,#156437,#156438,
#156439,#156440,#156441,#156442,#156443,#156444,#156445,#156446,#156447,
#156448,#156449,#156450,#156451,#156452,#156453,#156454,#156455,#156456,
#156457,#156458,#156459,#156460,#156461,#156462,#156463,#156464,#156465,
#156466,#156467,#156468,#156469,#156470,#156471,#156472,#156473,#156474,
#156475,#156476,#156477,#156478,#156479,#156480,#156481,#156482,#156483,
#156484,#156485,#156486,#156487,#156488,#156489,#156490,#156491,#156492,
#156493,#156494,#156495,#156496,#156497,#156498,#156499,#156500,#156501,
#156502,#156503,#156504,#156505,#156506,#156507,#156508,#156509,#156510,
#156511,#156512,#156513,#156514,#156515,#156516,#156517,#156518),
 .UNSPECIFIED.,.F.,.F.,(4,3,3,3,3,3,3,3,3,3,3,3,3,3,3,3,3,3,3,3,3,3,3,3,
3,3,3,3,3,3,3,3,3,3,3,3,3,3,3,3,3,3,3,3,3,3,3,3,3,3,3,3,3,3,3,3,3,3,3,3,
3,3,3,3,3,3,3,3,3,3,3,3,3,3,3,3,3,3,3,3,3,3,4),(1144.6585810002,1144.69773227455,
1144.77768957468,1144.85755237192,1144.93733819439,1145.01706450959,1145.09674873788,
1145.1764197241,1145.25608717763,1145.33576682845,1145.41547441084,1145.49526963992,
1145.57511398162,1145.65507240867,1145.69746828527,1145.7774255854,1145.85728838264,
1145.93707420512,1146.01680052031,1146.09648474861,1146.17615573483,1146.25582318835,
1146.33550283917,1146.41521042156,1146.49500565064,1146.57484999235,1146.65480841939,
1146.69720429599,1146.77716159612,1146.85702439336,1146.93681021584,1147.01653653103,
1147.09622075933,1147.17589174555,1147.25555919907,1147.33523884989,1147.41494643228,
1147.49474166136,1147.57458600307,1147.65454443011,1147.69694030671,1147.77689760684,
1147.85676040408,1147.93654622656,1148.01627254175,1148.09595677005,1148.17562775627,
1148.25529520979,1148.33497486061,1148.414682443,1148.49447767208,1148.57432201379,
1148.65428044083,1148.69667631743,1148.77663361756,1148.8564964148,1148.93628223728,
1149.01600855247,1149.09569278077,1149.17536376699,1149.25503122051,1149.33471087133,
1149.41441845372,1149.4942136828,1149.57405802451,1149.65401645155,1149.69641232815,
1149.77636962828,1149.85623242552,1149.936018248,1150.01574456319,1150.09542879149,
1150.17509977771,1150.25476723123,1150.33444688205,1150.41415446445,1150.49394969352,
1150.57379403523,1150.65375246228,1150.69614833887,1150.80181973241,1150.90511477516,
1150.94176622539),.UNSPECIFIED.);
#1312=B_SPLINE_CURVE_WITH_KNOTS('',3,(#156520,#156521,#156522,#156523,#156524,
#156525,#156526,#156527,#156528,#156529),.UNSPECIFIED.,.F.,.F.,(4,1,1,1,
1,1,1,4),(1150.94176630738,1151.69588434959,1152.69562036031,1153.69535637103,
1154.69509238175,1155.69482839247,1156.69456440319,1157.22495161456),
 .UNSPECIFIED.);
#1313=B_SPLINE_CURVE_WITH_KNOTS('',3,(#156531,#156532,#156533,#156534,#156535,
#156536,#156537,#156538,#156539,#156540),.UNSPECIFIED.,.F.,.F.,(4,1,1,1,
1,1,1,4),(1157.22495161456,1157.69430041391,1158.69403642463,1159.69377243535,
1160.69350844607,1161.69324445679,1162.69298046751,1163.50813218944),
 .UNSPECIFIED.);
#1314=B_SPLINE_CURVE_WITH_KNOTS('',3,(#156542,#156543,#156544,#156545,#156546,
#156547,#156548,#156549,#156550,#156551,#156552,#156553,#156554,#156555,
#156556,#156557,#156558,#156559,#156560,#156561,#156562,#156563,#156564,
#156565,#156566,#156567,#156568,#156569,#156570,#156571,#156572,#156573,
#156574,#156575,#156576,#156577,#156578,#156579,#156580,#156581,#156582,
#156583,#156584,#156585,#156586,#156587,#156588,#156589,#156590,#156591,
#156592,#156593,#156594,#156595,#156596,#156597,#156598,#156599,#156600,
#156601,#156602,#156603,#156604,#156605,#156606,#156607,#156608,#156609,
#156610,#156611,#156612,#156613,#156614,#156615,#156616,#156617,#156618,
#156619,#156620,#156621,#156622,#156623,#156624,#156625,#156626,#156627,
#156628,#156629,#156630,#156631,#156632,#156633,#156634,#156635,#156636,
#156637,#156638,#156639,#156640,#156641,#156642,#156643,#156644,#156645,
#156646,#156647,#156648,#156649,#156650,#156651,#156652,#156653,#156654,
#156655,#156656,#156657,#156658,#156659,#156660,#156661,#156662,#156663,
#156664,#156665,#156666,#156667,#156668,#156669,#156670,#156671,#156672,
#156673,#156674,#156675,#156676,#156677,#156678,#156679,#156680,#156681,
#156682,#156683,#156684,#156685,#156686,#156687,#156688,#156689,#156690,
#156691,#156692,#156693,#156694,#156695,#156696,#156697,#156698,#156699,
#156700,#156701,#156702,#156703,#156704,#156705,#156706,#156707,#156708,
#156709,#156710,#156711,#156712,#156713,#156714,#156715,#156716,#156717,
#156718,#156719,#156720,#156721,#156722,#156723,#156724,#156725,#156726,
#156727,#156728,#156729,#156730,#156731,#156732,#156733,#156734,#156735,
#156736,#156737,#156738,#156739,#156740,#156741,#156742,#156743,#156744,
#156745,#156746,#156747,#156748,#156749,#156750,#156751,#156752,#156753,
#156754,#156755,#156756,#156757,#156758,#156759,#156760,#156761,#156762,
#156763,#156764,#156765,#156766,#156767,#156768,#156769,#156770,#156771,
#156772,#156773,#156774,#156775,#156776,#156777,#156778,#156779,#156780,
#156781,#156782,#156783,#156784,#156785),.UNSPECIFIED.,.F.,.F.,(4,3,3,3,
3,3,3,3,3,3,3,3,3,3,3,3,3,3,3,3,3,3,3,3,3,3,3,3,3,3,3,3,3,3,3,3,3,3,3,3,
3,3,3,3,3,3,3,3,3,3,3,3,3,3,3,3,3,3,3,3,3,3,3,3,3,3,3,3,3,3,3,3,3,3,3,3,
3,3,3,3,3,4),(1163.50813692174,1163.62789494603,1163.69271647823,1163.77267377836,
1163.8525365756,1163.93232239808,1164.01204871327,1164.09173294157,1164.17140392779,
1164.25107138131,1164.33075103213,1164.41045861452,1164.4902538436,1164.57009818531,
1164.65005661236,1164.69245248895,1164.77240978908,1164.85227258632,1164.9320584088,
1165.01178472399,1165.09146895229,1165.17113993851,1165.25080739203,1165.33048704285,
1165.41019462524,1165.48998985432,1165.56983419603,1165.64979262307,1165.69218849967,
1165.7721457998,1165.85200859704,1165.93179441952,1166.01152073471,1166.091204963,
1166.17087594923,1166.25054340275,1166.33022305357,1166.40993063596,1166.48972586504,
1166.56957020674,1166.64952863379,1166.69192451039,1166.77188181052,1166.85174460776,
1166.93153043024,1167.01125674543,1167.09094097373,1167.17061195995,1167.25027941347,
1167.32995906429,1167.40966664668,1167.48946187576,1167.56930621747,1167.64926464451,
1167.69166052111,1167.77161782124,1167.85148061848,1167.93126644096,1168.01099275615,
1168.09067698445,1168.17034797067,1168.25001542419,1168.32969507501,1168.4094026574,
1168.48919788648,1168.56904222819,1168.64900065523,1168.69139653183,1168.77135383196,
1168.8512166292,1168.93100245167,1169.01072876687,1169.09041299516,1169.17008398138,
1169.24975143491,1169.32943108573,1169.40913866812,1169.4889338972,1169.5687782389,
1169.64873666595,1169.69113254255,1169.79132222892),.UNSPECIFIED.);
#1315=B_SPLINE_CURVE_WITH_KNOTS('',3,(#156787,#156788,#156789,#156790,#156791,
#156792,#156793,#156794,#156795,#156796),.UNSPECIFIED.,.F.,.F.,(4,1,1,1,
1,1,1,4),(1169.79133132335,1170.69086855327,1171.69060456399,1172.69034057471,
1173.69007658543,1174.68981259615,1175.68954860687,1176.07450007552),
 .UNSPECIFIED.);
#1316=B_SPLINE_CURVE_WITH_KNOTS('',3,(#156798,#156799,#156800,#156801,#156802,
#156803,#156804,#156805,#156806,#156807,#156808,#156809,#156810,#156811,
#156812,#156813,#156814,#156815,#156816,#156817,#156818,#156819,#156820,
#156821,#156822,#156823,#156824,#156825,#156826,#156827,#156828,#156829,
#156830,#156831,#156832,#156833,#156834,#156835,#156836,#156837,#156838,
#156839,#156840,#156841,#156842,#156843,#156844,#156845,#156846,#156847,
#156848,#156849,#156850,#156851,#156852,#156853,#156854,#156855,#156856,
#156857,#156858,#156859,#156860,#156861,#156862,#156863,#156864,#156865,
#156866,#156867,#156868,#156869,#156870,#156871,#156872,#156873,#156874,
#156875,#156876,#156877,#156878,#156879,#156880,#156881,#156882,#156883,
#156884,#156885,#156886,#156887,#156888,#156889,#156890,#156891,#156892,
#156893,#156894,#156895,#156896,#156897,#156898,#156899,#156900,#156901,
#156902,#156903,#156904,#156905,#156906,#156907,#156908,#156909,#156910,
#156911,#156912,#156913,#156914,#156915,#156916,#156917,#156918,#156919,
#156920,#156921,#156922,#156923,#156924,#156925,#156926,#156927,#156928,
#156929,#156930,#156931,#156932,#156933,#156934,#156935,#156936,#156937,
#156938,#156939,#156940,#156941,#156942,#156943,#156944,#156945,#156946,
#156947,#156948,#156949,#156950,#156951,#156952,#156953,#156954,#156955,
#156956,#156957,#156958,#156959,#156960,#156961,#156962,#156963,#156964,
#156965,#156966,#156967,#156968,#156969,#156970,#156971,#156972,#156973,
#156974,#156975,#156976,#156977,#156978,#156979,#156980,#156981,#156982,
#156983,#156984,#156985,#156986,#156987,#156988,#156989,#156990,#156991,
#156992,#156993,#156994,#156995,#156996,#156997,#156998,#156999,#157000,
#157001,#157002,#157003,#157004,#157005,#157006,#157007,#157008,#157009,
#157010,#157011,#157012,#157013,#157014,#157015,#157016,#157017,#157018,
#157019,#157020,#157021,#157022,#157023,#157024,#157025,#157026,#157027,
#157028,#157029,#157030,#157031,#157032,#157033,#157034,#157035,#157036,
#157037,#157038,#157039,#157040,#157041,#157042,#157043,#157044),
 .UNSPECIFIED.,.F.,.F.,(4,3,3,3,3,3,3,3,3,3,3,3,3,3,3,3,3,3,3,3,3,3,3,3,
3,3,3,3,3,3,3,3,3,3,3,3,3,3,3,3,3,3,3,3,3,3,3,3,3,3,3,3,3,3,3,3,3,3,3,3,
3,3,3,3,3,3,3,3,3,3,3,3,3,3,3,3,3,3,3,3,3,3,4),(1176.0745075361,1176.15495807891,
1176.2354201739,1176.31590851967,1176.39643782787,1176.47707359616,1176.55776784111,
1176.63859250809,1176.68928461759,1176.76924191772,1176.84910471496,1176.92889053744,
1177.00861685263,1177.08830108093,1177.16797206715,1177.24763952067,1177.32731917149,
1177.40702675388,1177.48682198296,1177.56666632467,1177.64662475172,1177.68902062831,
1177.76897792844,1177.84884072568,1177.92862654816,1178.00835286335,1178.08803709165,
1178.16770807787,1178.24737553139,1178.32705518221,1178.4067627646,1178.48655799368,
1178.56640233539,1178.64636076243,1178.68875663903,1178.76871393916,1178.8485767364,
1178.92836255888,1179.00808887407,1179.08777310236,1179.16744408859,1179.24711154211,
1179.32679119293,1179.40649877532,1179.4862940044,1179.56613834611,1179.64609677315,
1179.68849264975,1179.76844994988,1179.84831274712,1179.9280985696,1180.00782488479,
1180.08750911308,1180.16718009931,1180.24684755283,1180.32652720365,1180.40623478604,
1180.48603001512,1180.56587435683,1180.64583278387,1180.68822866047,1180.7681859606,
1180.84804875784,1180.92783458031,1181.00756089551,1181.0872451238,1181.16691611002,
1181.24658356355,1181.32626321437,1181.40597079676,1181.48576602583,1181.56561036754,
1181.64556879459,1181.68796467119,1181.7716806927,1181.85144234334,1181.93112890649,
1182.01075624757,1182.09034019153,1182.16990326689,1182.2494544396,1182.32902377031,
1182.35769284328),.UNSPECIFIED.);
#1317=B_SPLINE_CURVE_WITH_KNOTS('',3,(#157046,#157047,#157048,#157049,#157050,
#157051,#157052,#157053,#157054,#157055),.UNSPECIFIED.,.F.,.F.,(4,1,1,1,
1,1,1,4),(1182.3577001467,1182.68770068191,1183.68743669263,1184.68717270335,
1185.68690871407,1186.68664472479,1187.68638073551,1188.64087815046),
 .UNSPECIFIED.);
#1318=B_SPLINE_CURVE_WITH_KNOTS('',3,(#157057,#157058,#157059,#157060,#157061,
#157062,#157063,#157064,#157065,#157066,#157067,#157068,#157069),
 .UNSPECIFIED.,.F.,.F.,(4,3,1,1,1,1,1,1,4),(1188.64087815046,1188.68611674623,
1189.68585275695,1190.68558876767,1191.68532477839,1192.68506078911,1193.68479679983,
1194.68453281055,1194.92406345764),.UNSPECIFIED.);
#1319=B_SPLINE_CURVE_WITH_KNOTS('',3,(#157071,#157072,#157073,#157074,#157075,
#157076,#157077,#157078,#157079,#157080),.UNSPECIFIED.,.F.,.F.,(4,1,1,1,
1,1,1,4),(1194.92406345764,1195.68426882127,1196.68400483199,1197.68374084271,
1198.68347685343,1199.68321286415,1200.68294887487,1201.20724876482),
 .UNSPECIFIED.);
#1320=B_SPLINE_CURVE_WITH_KNOTS('',3,(#157082,#157083,#157084,#157085,#157086,
#157087,#157088,#157089,#157090,#157091),.UNSPECIFIED.,.F.,.F.,(4,1,1,1,
1,1,1,4),(1201.20724876482,1201.68268488559,1202.68242089631,1203.68215690704,
1204.68189291776,1205.68162892848,1206.6813649392,1207.49042990411),
 .UNSPECIFIED.);
#1321=B_SPLINE_CURVE_WITH_KNOTS('',3,(#157093,#157094,#157095,#157096,#157097,
#157098,#157099,#157100,#157101,#157102,#157103,#157104,#157105,#157106,
#157107,#157108,#157109,#157110,#157111,#157112,#157113,#157114,#157115,
#157116,#157117,#157118,#157119,#157120,#157121,#157122,#157123,#157124,
#157125,#157126,#157127,#157128,#157129,#157130,#157131,#157132,#157133,
#157134,#157135,#157136,#157137,#157138,#157139,#157140,#157141,#157142,
#157143,#157144,#157145,#157146,#157147,#157148,#157149,#157150,#157151,
#157152,#157153,#157154,#157155,#157156,#157157,#157158,#157159,#157160,
#157161,#157162,#157163,#157164,#157165,#157166,#157167,#157168,#157169,
#157170,#157171,#157172,#157173,#157174,#157175,#157176,#157177,#157178,
#157179,#157180,#157181,#157182,#157183,#157184,#157185,#157186,#157187,
#157188,#157189,#157190,#157191,#157192,#157193,#157194,#157195,#157196,
#157197,#157198,#157199,#157200,#157201,#157202,#157203,#157204,#157205,
#157206,#157207,#157208,#157209,#157210,#157211,#157212,#157213,#157214,
#157215,#157216,#157217,#157218,#157219,#157220,#157221,#157222,#157223,
#157224,#157225,#157226,#157227,#157228,#157229,#157230,#157231,#157232,
#157233,#157234,#157235,#157236,#157237,#157238,#157239,#157240,#157241,
#157242,#157243,#157244,#157245,#157246,#157247,#157248,#157249,#157250,
#157251,#157252,#157253,#157254,#157255,#157256,#157257,#157258,#157259,
#157260,#157261,#157262,#157263,#157264,#157265,#157266,#157267,#157268,
#157269,#157270,#157271,#157272,#157273,#157274,#157275,#157276,#157277,
#157278,#157279,#157280,#157281,#157282,#157283,#157284,#157285,#157286,
#157287,#157288,#157289,#157290,#157291,#157292,#157293,#157294,#157295,
#157296,#157297,#157298,#157299,#157300,#157301,#157302,#157303,#157304,
#157305,#157306,#157307,#157308,#157309,#157310,#157311,#157312,#157313,
#157314,#157315,#157316,#157317,#157318,#157319,#157320,#157321,#157322,
#157323,#157324,#157325,#157326,#157327,#157328,#157329,#157330,#157331,
#157332,#157333,#157334,#157335,#157336),.UNSPECIFIED.,.F.,.F.,(4,3,3,3,
3,3,3,3,3,3,3,3,3,3,3,3,3,3,3,3,3,3,3,3,3,3,3,3,3,3,3,3,3,3,3,3,3,3,3,3,
3,3,3,3,3,3,3,3,3,3,3,3,3,3,3,3,3,3,3,3,3,3,3,3,3,3,3,3,3,3,3,3,3,3,3,3,
3,3,3,3,3,4),(1207.490434072,1207.6080995271,1207.68110094992,1207.76105825005,
1207.84092104729,1207.92070686976,1208.00043318496,1208.08011741325,1208.15978839947,
1208.239455853,1208.31913550382,1208.39884308621,1208.47863831529,1208.55848265699,
1208.63844108404,1208.68083696064,1208.76079426077,1208.84065705801,1208.92044288049,
1209.00016919568,1209.07985342397,1209.1595244102,1209.23919186372,1209.31887151454,
1209.39857909693,1209.47837432601,1209.55821866772,1209.63817709476,1209.68057297136,
1209.76053027149,1209.84039306873,1209.92017889121,1209.9999052064,1210.0795894347,
1210.15926042092,1210.23892787444,1210.31860752526,1210.39831510765,1210.47811033673,
1210.55795467844,1210.63791310548,1210.68030898208,1210.76026628221,1210.84012907945,
1210.91991490193,1210.99964121712,1211.07932544542,1211.15899643164,1211.23866388516,
1211.31834353598,1211.39805111837,1211.47784634745,1211.55769068916,1211.6376491162,
1211.6800449928,1211.76000229293,1211.83986509017,1211.91965091265,1211.99937722784,
1212.07906145614,1212.15873244236,1212.23839989588,1212.3180795467,1212.39778712909,
1212.47758235817,1212.55742669988,1212.63738512692,1212.67978100352,1212.75973830365,
1212.83960110089,1212.91938692337,1212.99911323856,1213.07879746686,1213.15846845308,
1213.2381359066,1213.31781555742,1213.39752313982,1213.47731836889,1213.5571627106,
1213.63712113765,1213.67951701424,1213.77361937918),.UNSPECIFIED.);
#1322=B_SPLINE_CURVE_WITH_KNOTS('',3,(#157338,#157339,#157340,#157341,#157342,
#157343,#157344,#157345,#157346,#157347),.UNSPECIFIED.,.F.,.F.,(4,1,1,1,
1,1,1,4),(1213.77362840169,1214.67925302496,1215.67898903568,1216.6787250464,
1217.67846105712,1218.67819706784,1219.67793307856,1220.05679710292),
 .UNSPECIFIED.);
#1323=B_SPLINE_CURVE_WITH_KNOTS('',3,(#157349,#157350,#157351,#157352,#157353,
#157354,#157355,#157356,#157357,#157358,#157359,#157360,#157361,#157362,
#157363,#157364,#157365,#157366,#157367,#157368,#157369,#157370,#157371,
#157372,#157373,#157374,#157375,#157376,#157377,#157378,#157379,#157380,
#157381,#157382,#157383,#157384,#157385,#157386,#157387,#157388,#157389,
#157390,#157391,#157392,#157393,#157394,#157395,#157396,#157397,#157398,
#157399,#157400,#157401,#157402,#157403,#157404,#157405,#157406,#157407,
#157408,#157409,#157410,#157411,#157412,#157413,#157414,#157415,#157416,
#157417,#157418,#157419,#157420,#157421,#157422,#157423,#157424,#157425,
#157426,#157427,#157428,#157429,#157430,#157431,#157432,#157433,#157434,
#157435,#157436,#157437,#157438,#157439,#157440,#157441,#157442,#157443,
#157444,#157445,#157446,#157447,#157448,#157449,#157450,#157451,#157452,
#157453,#157454,#157455,#157456,#157457,#157458,#157459,#157460,#157461,
#157462,#157463,#157464,#157465,#157466,#157467,#157468,#157469,#157470,
#157471,#157472,#157473,#157474,#157475,#157476,#157477,#157478,#157479,
#157480,#157481,#157482,#157483,#157484,#157485,#157486,#157487,#157488,
#157489,#157490,#157491,#157492,#157493,#157494,#157495,#157496,#157497,
#157498,#157499,#157500,#157501,#157502,#157503,#157504,#157505,#157506,
#157507,#157508,#157509,#157510,#157511,#157512,#157513,#157514,#157515,
#157516,#157517,#157518,#157519,#157520,#157521,#157522,#157523,#157524,
#157525,#157526,#157527,#157528,#157529,#157530,#157531,#157532,#157533,
#157534,#157535,#157536,#157537,#157538,#157539,#157540,#157541,#157542,
#157543,#157544,#157545,#157546,#157547,#157548,#157549,#157550,#157551,
#157552,#157553,#157554,#157555,#157556,#157557,#157558,#157559,#157560,
#157561,#157562,#157563,#157564,#157565,#157566,#157567,#157568,#157569,
#157570,#157571,#157572,#157573,#157574,#157575,#157576,#157577,#157578,
#157579,#157580,#157581,#157582,#157583,#157584,#157585,#157586,#157587,
#157588,#157589,#157590,#157591,#157592,#157593,#157594,#157595),
 .UNSPECIFIED.,.F.,.F.,(4,3,3,3,3,3,3,3,3,3,3,3,3,3,3,3,3,3,3,3,3,3,3,3,
3,3,3,3,3,3,3,3,3,3,3,3,3,3,3,3,3,3,3,3,3,3,3,3,3,3,3,3,3,3,3,3,3,3,3,3,
3,3,3,3,3,3,3,3,3,3,3,3,3,3,3,3,3,3,3,3,3,3,4),(1220.05680468636,1220.13714268496,
1220.21748902712,1220.29785857117,1220.37826618643,1220.45877790638,1220.5393458432,
1220.62004504479,1220.67766908928,1220.75762638941,1220.83748918665,1220.91727500912,
1220.99700132432,1221.07668555261,1221.15635653883,1221.23602399236,1221.31570364318,
1221.39541122557,1221.47520645465,1221.55505079635,1221.6350092234,1221.6774051,
1221.75736240013,1221.83722519737,1221.91701101985,1221.99673733504,1222.07642156333,
1222.15609254956,1222.23576000308,1222.3154396539,1222.39514723629,1222.47494246537,
1222.55478680708,1222.63474523412,1222.67714111072,1222.75709841085,1222.83696120809,
1222.91674703057,1222.99647334576,1223.07615757405,1223.15582856028,1223.2354960138,
1223.31517566462,1223.39488324701,1223.47467847609,1223.5545228178,1223.63448124484,
1223.67687712144,1223.75683442157,1223.83669721881,1223.91648304129,1223.99620935648,
1224.07589358478,1224.155564571,1224.23523202452,1224.31491167534,1224.39461925773,
1224.47441448681,1224.55425882852,1224.63421725556,1224.67661313216,1224.75657043229,
1224.83643322953,1224.91621905201,1224.9959453672,1225.0756295955,1225.15530058172,
1225.23496803524,1225.31464768606,1225.39435526845,1225.47415049753,1225.55399483924,
1225.63395326628,1225.67634914288,1225.75930424921,1225.83915601167,1225.9189317184,
1225.9986471538,1226.07831806141,1226.15796572783,1226.23760042992,1226.31725012176,
1226.33998999354),.UNSPECIFIED.);
#1324=B_SPLINE_CURVE_WITH_KNOTS('',3,(#157597,#157598,#157599,#157600,#157601,
#157602,#157603,#157604,#157605,#157606),.UNSPECIFIED.,.F.,.F.,(4,1,1,1,
1,1,1,4),(1226.33999748489,1226.6760851536,1227.67582116432,1228.67555717504,
1229.67529318576,1230.67502919648,1231.6747652072,1232.62317530072),
 .UNSPECIFIED.);
#1325=B_SPLINE_CURVE_WITH_KNOTS('',3,(#157608,#157609,#157610,#157611,#157612,
#157613,#157614,#157615,#157616,#157617,#157618,#157619),.UNSPECIFIED.,
 .F.,.F.,(4,2,1,1,1,1,1,1,4),(1232.62317530072,1232.67450121792,1233.67423722864,
1234.67397323936,1235.67370925008,1236.6734452608,1237.67318127152,1238.67291728224,
1238.9063606079),.UNSPECIFIED.);
#1326=B_SPLINE_CURVE_WITH_KNOTS('',3,(#157621,#157622,#157623,#157624,#157625,
#157626,#157627,#157628,#157629,#157630),.UNSPECIFIED.,.F.,.F.,(4,1,1,1,
1,1,1,4),(1238.9063606079,1239.67265329296,1240.67238930368,1241.6721253144,
1242.67186132512,1243.67159733584,1244.67133334656,1245.18954591508),
 .UNSPECIFIED.);
#1327=B_SPLINE_CURVE_WITH_KNOTS('',3,(#157632,#157633,#157634,#157635,#157636,
#157637,#157638,#157639,#157640,#157641),.UNSPECIFIED.,.F.,.F.,(4,1,1,1,
1,1,1,4),(1245.18954591508,1245.67106935728,1246.670805368,1247.67054137872,
1248.67027738944,1249.67001340016,1250.66974941088,1251.4727276359),
 .UNSPECIFIED.);
#1328=B_SPLINE_CURVE_WITH_KNOTS('',3,(#157643,#157644,#157645,#157646,#157647,
#157648,#157649,#157650,#157651,#157652,#157653,#157654,#157655,#157656,
#157657,#157658,#157659,#157660,#157661,#157662,#157663,#157664,#157665,
#157666,#157667,#157668,#157669,#157670,#157671,#157672,#157673,#157674,
#157675,#157676,#157677,#157678,#157679,#157680,#157681,#157682,#157683,
#157684,#157685,#157686,#157687,#157688,#157689,#157690,#157691,#157692,
#157693,#157694,#157695,#157696,#157697,#157698,#157699,#157700,#157701,
#157702,#157703,#157704,#157705,#157706,#157707,#157708,#157709,#157710,
#157711,#157712,#157713,#157714,#157715,#157716,#157717,#157718,#157719,
#157720,#157721,#157722,#157723,#157724,#157725,#157726,#157727,#157728,
#157729,#157730,#157731,#157732,#157733,#157734,#157735,#157736,#157737,
#157738,#157739,#157740,#157741,#157742,#157743,#157744,#157745,#157746,
#157747,#157748,#157749,#157750,#157751,#157752,#157753,#157754,#157755,
#157756,#157757,#157758,#157759,#157760,#157761,#157762,#157763,#157764,
#157765,#157766,#157767,#157768,#157769,#157770,#157771,#157772,#157773,
#157774,#157775,#157776,#157777,#157778,#157779,#157780,#157781,#157782,
#157783,#157784,#157785,#157786,#157787,#157788,#157789,#157790,#157791,
#157792,#157793,#157794,#157795,#157796,#157797,#157798,#157799,#157800,
#157801,#157802,#157803,#157804,#157805,#157806,#157807,#157808,#157809,
#157810,#157811,#157812,#157813,#157814,#157815,#157816,#157817,#157818,
#157819,#157820,#157821,#157822,#157823,#157824,#157825,#157826,#157827,
#157828,#157829,#157830,#157831,#157832,#157833,#157834,#157835,#157836,
#157837,#157838,#157839,#157840,#157841,#157842,#157843,#157844,#157845,
#157846,#157847,#157848,#157849,#157850,#157851,#157852,#157853,#157854,
#157855,#157856,#157857,#157858,#157859,#157860,#157861,#157862,#157863,
#157864,#157865,#157866,#157867,#157868,#157869,#157870,#157871,#157872,
#157873,#157874,#157875,#157876,#157877,#157878,#157879,#157880,#157881,
#157882,#157883,#157884,#157885,#157886),.UNSPECIFIED.,.F.,.F.,(4,3,3,3,
3,3,3,3,3,3,3,3,3,3,3,3,3,3,3,3,3,3,3,3,3,3,3,3,3,3,3,3,3,3,3,3,3,3,3,3,
3,3,3,3,3,3,3,3,3,3,3,3,3,3,3,3,3,3,3,3,3,3,3,3,3,3,3,3,3,3,3,3,3,3,3,3,
3,3,3,3,3,4),(1251.47273122226,1251.58846939653,1251.6694854216,1251.74944272173,
1251.82930551897,1251.90909134145,1251.98881765664,1252.06850188494,1252.14817287116,
1252.22784032468,1252.3075199755,1252.3872275579,1252.46702278697,1252.54686712868,
1252.62682555573,1252.66922143232,1252.74917873245,1252.82904152969,1252.90882735217,
1252.98855366736,1253.06823789566,1253.14790888188,1253.2275763354,1253.30725598622,
1253.38696356861,1253.46675879769,1253.5466031394,1253.62656156644,1253.66895744304,
1253.74891474317,1253.82877754041,1253.90856336289,1253.98828967808,1254.06797390637,
1254.1476448926,1254.22731234612,1254.30699199694,1254.38669957933,1254.46649480841,
1254.54633915012,1254.62629757716,1254.66869345376,1254.74865075389,1254.82851355113,
1254.90829937361,1254.9880256888,1255.06770991709,1255.14738090332,1255.22704835684,
1255.30672800766,1255.38643559005,1255.46623081913,1255.54607516084,1255.62603358788,
1255.66842946448,1255.74838676461,1255.82824956185,1255.90803538433,1255.98776169952,
1256.06744592781,1256.14711691404,1256.22678436756,1256.30646401838,1256.38617160077,
1256.46596682985,1256.54581117156,1256.6257695986,1256.6681654752,1256.74812277533,
1256.82798557257,1256.90777139504,1256.98749771024,1257.06718193853,1257.14685292475,
1257.22652037828,1257.30620002909,1257.38590761149,1257.46570284056,1257.54554718227,
1257.62550560931,1257.66790148592,1257.75591652944),.UNSPECIFIED.);
#1329=B_SPLINE_CURVE_WITH_KNOTS('',3,(#157888,#157889,#157890,#157891,#157892,
#157893,#157894,#157895,#157896,#157897),.UNSPECIFIED.,.F.,.F.,(4,1,1,1,
1,1,1,4),(1257.75592528103,1258.66763749664,1259.66737350736,1260.66710951808,
1261.6668455288,1262.66658153952,1263.66631755024,1264.03909416751),
 .UNSPECIFIED.);
#1330=B_SPLINE_CURVE_WITH_KNOTS('',3,(#157899,#157900,#157901,#157902,#157903,
#157904,#157905,#157906,#157907,#157908,#157909,#157910,#157911,#157912,
#157913,#157914,#157915,#157916,#157917,#157918,#157919,#157920,#157921,
#157922,#157923,#157924,#157925,#157926,#157927,#157928,#157929,#157930,
#157931,#157932,#157933,#157934,#157935,#157936,#157937,#157938,#157939,
#157940,#157941,#157942,#157943,#157944,#157945,#157946,#157947,#157948,
#157949,#157950,#157951,#157952,#157953,#157954,#157955,#157956,#157957,
#157958,#157959,#157960,#157961,#157962,#157963,#157964,#157965,#157966,
#157967,#157968,#157969,#157970,#157971,#157972,#157973,#157974,#157975,
#157976,#157977,#157978,#157979,#157980,#157981,#157982,#157983,#157984,
#157985,#157986,#157987,#157988,#157989,#157990,#157991,#157992,#157993,
#157994,#157995,#157996,#157997,#157998,#157999,#158000,#158001,#158002,
#158003,#158004,#158005,#158006,#158007,#158008,#158009,#158010,#158011,
#158012,#158013,#158014,#158015,#158016,#158017,#158018,#158019,#158020,
#158021,#158022,#158023,#158024,#158025,#158026,#158027,#158028,#158029,
#158030,#158031,#158032,#158033,#158034,#158035,#158036,#158037,#158038,
#158039,#158040,#158041,#158042,#158043,#158044,#158045,#158046,#158047,
#158048,#158049,#158050,#158051,#158052,#158053,#158054,#158055,#158056,
#158057,#158058,#158059,#158060,#158061,#158062,#158063,#158064,#158065,
#158066,#158067,#158068,#158069,#158070,#158071,#158072,#158073,#158074,
#158075,#158076,#158077,#158078,#158079,#158080,#158081,#158082,#158083,
#158084,#158085,#158086,#158087,#158088,#158089,#158090,#158091,#158092,
#158093,#158094,#158095,#158096,#158097,#158098,#158099,#158100,#158101,
#158102,#158103,#158104,#158105,#158106,#158107,#158108,#158109,#158110,
#158111,#158112,#158113,#158114,#158115,#158116,#158117,#158118,#158119,
#158120,#158121,#158122,#158123,#158124,#158125,#158126,#158127,#158128,
#158129,#158130,#158131,#158132,#158133,#158134,#158135,#158136,#158137,
#158138,#158139,#158140,#158141,#158142,#158143,#158144,#158145),
 .UNSPECIFIED.,.F.,.F.,(4,3,3,3,3,3,3,3,3,3,3,3,3,3,3,3,3,3,3,3,3,3,3,3,
3,3,3,3,3,3,3,3,3,3,3,3,3,3,3,3,3,3,3,3,3,3,3,3,3,3,3,3,3,3,3,3,3,3,3,3,
3,3,3,3,3,3,3,3,3,3,3,3,3,3,3,3,3,3,3,3,3,3,4),(1264.03910183662,1264.11933138465,
1264.1995661766,1264.27982121819,1264.36011152426,1264.44050364496,1264.52094977296,
1264.60152805393,1264.66605356096,1264.74601086109,1264.82587365834,1264.90565948081,
1264.985385796,1265.0650700243,1265.14474101052,1265.22440846405,1265.30408811487,
1265.38379569726,1265.46359092634,1265.54343526805,1265.62339369509,1265.66578957168,
1265.74574687181,1265.82560966905,1265.90539549153,1265.98512180672,1266.06480603502,
1266.14447702124,1266.22414447476,1266.30382412558,1266.38353170798,1266.46332693705,
1266.54317127876,1266.62312970581,1266.6655255824,1266.74548288253,1266.82534567977,
1266.90513150224,1266.98485781744,1267.06454204573,1267.14421303195,1267.22388048548,
1267.3035601363,1267.38326771869,1267.46306294777,1267.54290728947,1267.62286571652,
1267.66526159312,1267.74521889325,1267.82508169049,1267.90486751297,1267.98459382816,
1268.06427805645,1268.14394904268,1268.2236164962,1268.30329614702,1268.38300372941,
1268.46279895849,1268.5426433002,1268.62260172724,1268.66499760384,1268.74495490397,
1268.82481770121,1268.90460352368,1268.98432983888,1269.06401406717,1269.14368505339,
1269.22335250692,1269.30303215773,1269.38273974013,1269.4625349692,1269.54237931091,
1269.62233773796,1269.66473361456,1269.74692780571,1269.82687350363,1269.90674213099,
1269.98654938442,1270.07048382426,1270.15021860611,1270.2299400296,1270.3096734261,
1270.3222871438),.UNSPECIFIED.);
#1331=B_SPLINE_CURVE_WITH_KNOTS('',3,(#158147,#158148,#158149,#158150,#158151,
#158152,#158153,#158154,#158155,#158156,#158157),.UNSPECIFIED.,.F.,.F.,
(4,2,1,1,1,1,1,4),(1270.32229478416,1270.66446962528,1271.664205636,1272.66394164672,
1273.66367765744,1274.66341366816,1275.66314967888,1276.60547245098),
 .UNSPECIFIED.);
#1332=B_SPLINE_CURVE_WITH_KNOTS('',3,(#158159,#158160,#158161,#158162,#158163,
#158164,#158165,#158166,#158167,#158168,#158169,#158170,#158171),
 .UNSPECIFIED.,.F.,.F.,(4,3,1,1,1,1,1,1,4),(1276.60547245098,1276.6628856896,
1277.66262170032,1278.66235771104,1279.66209372177,1280.66182973249,1281.66156574321,
1282.66130175393,1282.88865775816),.UNSPECIFIED.);
#1333=B_SPLINE_CURVE_WITH_KNOTS('',3,(#158173,#158174,#158175,#158176,#158177,
#158178,#158179,#158180,#158181,#158182,#158183,#158184,#158185,#158186,
#158187,#158188,#158189,#158190,#158191,#158192,#158193,#158194,#158195,
#158196,#158197,#158198,#158199,#158200,#158201,#158202,#158203,#158204,
#158205,#158206,#158207,#158208,#158209,#158210,#158211,#158212,#158213,
#158214,#158215,#158216,#158217,#158218,#158219,#158220,#158221,#158222,
#158223,#158224,#158225,#158226,#158227,#158228,#158229,#158230,#158231,
#158232,#158233,#158234,#158235,#158236,#158237,#158238,#158239,#158240,
#158241,#158242,#158243,#158244,#158245,#158246,#158247,#158248,#158249,
#158250,#158251,#158252,#158253,#158254,#158255,#158256,#158257,#158258,
#158259,#158260,#158261,#158262,#158263,#158264,#158265,#158266,#158267,
#158268,#158269,#158270,#158271,#158272,#158273,#158274,#158275,#158276,
#158277,#158278,#158279,#158280,#158281,#158282,#158283,#158284,#158285,
#158286,#158287,#158288,#158289,#158290,#158291,#158292,#158293,#158294,
#158295,#158296,#158297,#158298,#158299,#158300,#158301,#158302,#158303,
#158304,#158305,#158306,#158307,#158308,#158309,#158310,#158311,#158312,
#158313,#158314,#158315,#158316,#158317,#158318,#158319,#158320,#158321,
#158322,#158323,#158324,#158325,#158326,#158327,#158328,#158329,#158330,
#158331,#158332,#158333,#158334,#158335,#158336,#158337,#158338,#158339,
#158340,#158341,#158342,#158343,#158344,#158345,#158346,#158347,#158348,
#158349,#158350,#158351,#158352,#158353,#158354,#158355,#158356,#158357,
#158358,#158359,#158360,#158361,#158362,#158363,#158364,#158365,#158366,
#158367,#158368,#158369,#158370,#158371,#158372,#158373,#158374,#158375,
#158376,#158377,#158378,#158379,#158380,#158381,#158382,#158383,#158384,
#158385,#158386,#158387,#158388,#158389,#158390,#158391,#158392,#158393,
#158394,#158395,#158396,#158397,#158398,#158399,#158400,#158401,#158402,
#158403,#158404,#158405,#158406,#158407,#158408,#158409,#158410,#158411,
#158412,#158413,#158414,#158415,#158416,#158417,#158418,#158419),
 .UNSPECIFIED.,.F.,.F.,(4,3,3,3,3,3,3,3,3,3,3,3,3,3,3,3,3,3,3,3,3,3,3,3,
3,3,3,3,3,3,3,3,3,3,3,3,3,3,3,3,3,3,3,3,3,3,3,3,3,3,3,3,3,3,3,3,3,3,3,3,
3,3,3,3,3,3,3,3,3,3,3,3,3,3,3,3,3,3,3,3,3,3,4),(1282.88865775816,1282.96738598792,
1283.04605850303,1283.12470073832,1283.20332865433,1283.28195874242,1283.36060749377,
1283.43933693173,1283.51810858998,1283.59699808486,1283.66103776465,1283.74099506478,
1283.82085786202,1283.9006436845,1283.98036999969,1284.06005422798,1284.13972521421,
1284.21939266773,1284.29907231855,1284.37877990094,1284.45857513002,1284.53841947172,
1284.61837789877,1284.66077377537,1284.7407310755,1284.82059387274,1284.90037969522,
1284.98010601041,1285.0597902387,1285.13946122493,1285.21912867845,1285.29880832927,
1285.37851591166,1285.45831114074,1285.53815548244,1285.61811390949,1285.66050978609,
1285.74046708622,1285.82032988346,1285.90011570594,1285.97984202113,1286.05952624943,
1286.13919723565,1286.21886468917,1286.29854433999,1286.37825192238,1286.45804715146,
1286.53789149317,1286.61784992022,1286.66024579681,1286.74020309694,1286.82006589418,
1286.89985171666,1286.97957803185,1287.05926226015,1287.13893324637,1287.21860069989,
1287.29828035071,1287.3779879331,1287.45778316218,1287.53762750389,1287.61758593093,
1287.65998180753,1287.73993910766,1287.8198019049,1287.89958772738,1287.97931404257,
1288.05899827086,1288.13866925708,1288.21833671061,1288.29801636143,1288.37772394382,
1288.4575191729,1288.53736351461,1288.61732194165,1288.65971781825,1288.7433496464,
1288.8268491885,1288.91309765771,1288.99631706811,1289.07944368197,1289.16246189708,
1289.17184306534),.UNSPECIFIED.);
#1334=B_SPLINE_CURVE_WITH_KNOTS('',3,(#158421,#158422,#158423,#158424,#158425,
#158426,#158427,#158428,#158429,#158430,#158431,#158432,#158433,#158434,
#158435,#158436,#158437,#158438,#158439,#158440,#158441,#158442,#158443,
#158444,#158445,#158446,#158447,#158448,#158449,#158450,#158451,#158452,
#158453,#158454,#158455,#158456,#158457,#158458,#158459,#158460,#158461,
#158462,#158463,#158464,#158465,#158466,#158467,#158468,#158469,#158470,
#158471,#158472,#158473,#158474,#158475,#158476,#158477,#158478,#158479,
#158480,#158481,#158482,#158483,#158484,#158485,#158486,#158487,#158488,
#158489,#158490,#158491,#158492,#158493,#158494,#158495,#158496,#158497,
#158498,#158499,#158500,#158501,#158502,#158503,#158504,#158505,#158506,
#158507,#158508,#158509,#158510,#158511,#158512,#158513,#158514,#158515,
#158516,#158517,#158518,#158519,#158520,#158521,#158522,#158523,#158524,
#158525,#158526,#158527,#158528,#158529,#158530,#158531,#158532,#158533,
#158534,#158535,#158536,#158537,#158538,#158539,#158540,#158541,#158542,
#158543,#158544,#158545,#158546,#158547,#158548,#158549,#158550,#158551,
#158552,#158553,#158554,#158555,#158556,#158557,#158558,#158559,#158560,
#158561,#158562,#158563,#158564,#158565,#158566,#158567,#158568,#158569,
#158570,#158571,#158572,#158573,#158574,#158575,#158576,#158577,#158578,
#158579,#158580,#158581,#158582,#158583,#158584,#158585,#158586,#158587,
#158588,#158589,#158590,#158591,#158592,#158593,#158594,#158595,#158596,
#158597,#158598,#158599,#158600,#158601,#158602,#158603,#158604,#158605,
#158606,#158607,#158608,#158609,#158610,#158611,#158612,#158613,#158614,
#158615,#158616,#158617,#158618,#158619,#158620,#158621,#158622,#158623,
#158624,#158625,#158626,#158627,#158628,#158629,#158630,#158631,#158632,
#158633,#158634,#158635,#158636,#158637,#158638,#158639,#158640,#158641,
#158642,#158643,#158644,#158645,#158646,#158647,#158648,#158649,#158650,
#158651,#158652,#158653,#158654,#158655,#158656,#158657,#158658,#158659,
#158660,#158661,#158662,#158663,#158664),.UNSPECIFIED.,.F.,.F.,(4,3,3,3,
3,3,3,3,3,3,3,3,3,3,3,3,3,3,3,3,3,3,3,3,3,3,3,3,3,3,3,3,3,3,3,3,3,3,3,3,
3,3,3,3,3,3,3,3,3,3,3,3,3,3,3,3,3,3,3,3,3,3,3,3,3,3,3,3,3,3,3,3,3,3,3,3,
3,3,3,3,3,4),(1289.17184306547,1289.25573730055,1289.33975209835,1289.423976356,
1289.50830956445,1289.59284136574,1289.65945382897,1289.7394111291,1289.81927392634,
1289.89905974882,1289.97878606401,1290.05847029231,1290.13814127853,1290.21780873205,
1290.29748838287,1290.37719596526,1290.45699119434,1290.53683553605,1290.61679396309,
1290.65918983969,1290.73914713982,1290.81900993706,1290.89879575954,1290.97852207473,
1291.05820630303,1291.13787728925,1291.21754474277,1291.29722439359,1291.37693197598,
1291.45672720506,1291.53657154677,1291.61652997381,1291.65892585041,1291.73888315054,
1291.81874594778,1291.89853177026,1291.97825808545,1292.05794231375,1292.13761329997,
1292.21728075349,1292.29696040431,1292.3766679867,1292.45646321578,1292.53630755749,
1292.61626598453,1292.65866186113,1292.73861916126,1292.8184819585,1292.89826778098,
1292.97799409617,1293.05767832447,1293.13734931069,1293.21701676421,1293.29669641503,
1293.37640399742,1293.4561992265,1293.53604356821,1293.61600199525,1293.65839787185,
1293.73835517198,1293.81821796922,1293.8980037917,1293.97773010689,1294.05741433518,
1294.1370853214,1294.21675277493,1294.29643242575,1294.37614000814,1294.45593523722,
1294.53577957892,1294.61573800597,1294.65813388257,1294.73694668814,1294.81566481368,
1294.89558525854,1294.97416387267,1295.05270920096,1295.13123780294,1295.21218544533,
1295.29075645646,1295.37289241449,1295.45502837252),.UNSPECIFIED.);
#1335=B_SPLINE_CURVE_WITH_KNOTS('',3,(#158666,#158667,#158668,#158669,#158670,
#158671,#158672,#158673,#158674,#158675,#158676),.UNSPECIFIED.,.F.,.F.,
(4,1,1,1,1,1,1,1,4),(1295.45502837252,1295.65786989329,1296.65760590401,
1297.65734191473,1298.65707792545,1299.65681393617,1300.65654994689,1301.65628595761,
1301.7382136797),.UNSPECIFIED.);
#1336=B_SPLINE_CURVE_WITH_KNOTS('',3,(#158678,#158679,#158680,#158681,#158682,
#158683,#158684,#158685,#158686,#158687),.UNSPECIFIED.,.F.,.F.,(4,1,1,1,
1,1,1,4),(1301.7382136797,1302.65602196833,1303.65575797905,1304.65549398977,
1305.65523000049,1306.65496601121,1307.65470202193,1308.02139898688),
 .UNSPECIFIED.);
#1337=B_SPLINE_CURVE_WITH_KNOTS('',3,(#158689,#158690,#158691,#158692,#158693,
#158694,#158695,#158696,#158697,#158698),.UNSPECIFIED.,.F.,.F.,(4,1,1,1,
1,1,1,4),(1308.02139898688,1308.65443803265,1309.65417404337,1310.65391005409,
1311.65364606481,1312.65338207553,1313.65311808625,1314.30458429405),
 .UNSPECIFIED.);
#1338=B_SPLINE_CURVE_WITH_KNOTS('',3,(#158700,#158701,#158702,#158703,#158704,
#158705,#158706,#158707,#158708,#158709,#158710,#158711,#158712,#158713,
#158714,#158715,#158716,#158717,#158718,#158719,#158720,#158721,#158722,
#158723,#158724,#158725,#158726,#158727,#158728,#158729,#158730,#158731,
#158732,#158733,#158734,#158735,#158736,#158737,#158738,#158739,#158740,
#158741,#158742,#158743,#158744,#158745,#158746,#158747,#158748,#158749,
#158750,#158751,#158752,#158753,#158754,#158755,#158756,#158757,#158758,
#158759,#158760,#158761,#158762,#158763,#158764,#158765,#158766,#158767,
#158768,#158769,#158770,#158771,#158772,#158773,#158774,#158775,#158776,
#158777,#158778,#158779,#158780,#158781,#158782,#158783,#158784,#158785,
#158786,#158787,#158788,#158789,#158790,#158791,#158792,#158793,#158794,
#158795,#158796,#158797,#158798,#158799,#158800,#158801,#158802,#158803,
#158804,#158805,#158806,#158807,#158808,#158809,#158810,#158811,#158812,
#158813,#158814,#158815,#158816,#158817,#158818,#158819,#158820,#158821,
#158822,#158823,#158824,#158825,#158826,#158827,#158828,#158829,#158830,
#158831,#158832,#158833,#158834,#158835,#158836,#158837,#158838,#158839,
#158840,#158841,#158842,#158843,#158844,#158845,#158846,#158847,#158848,
#158849,#158850,#158851,#158852,#158853,#158854,#158855,#158856,#158857,
#158858,#158859,#158860,#158861,#158862,#158863,#158864,#158865,#158866,
#158867,#158868,#158869,#158870,#158871,#158872,#158873,#158874,#158875,
#158876,#158877,#158878,#158879,#158880,#158881,#158882,#158883,#158884,
#158885,#158886,#158887,#158888,#158889,#158890,#158891,#158892,#158893,
#158894,#158895,#158896,#158897,#158898,#158899,#158900,#158901,#158902,
#158903,#158904,#158905,#158906,#158907,#158908,#158909,#158910,#158911,
#158912,#158913,#158914,#158915,#158916,#158917,#158918,#158919,#158920,
#158921,#158922,#158923,#158924,#158925,#158926,#158927,#158928,#158929,
#158930,#158931,#158932,#158933,#158934,#158935,#158936,#158937,#158938,
#158939,#158940,#158941,#158942,#158943),.UNSPECIFIED.,.F.,.F.,(4,3,3,3,
3,3,3,3,3,3,3,3,3,3,3,3,3,3,3,3,3,3,3,3,3,3,3,3,3,3,3,3,3,3,3,3,3,3,3,3,
3,3,3,3,3,3,3,3,3,3,3,3,3,3,3,3,3,3,3,3,3,3,3,3,3,3,3,3,3,3,3,3,3,3,3,3,
3,3,3,3,3,4),(1314.3045844167,1314.39621327382,1314.48828678864,1314.58094463404,
1314.65285409697,1314.7328113971,1314.81267419434,1314.89246001681,1314.972186332,
1315.05187056029,1315.13154154651,1315.21120900003,1315.29088865084,1315.37059623324,
1315.45039146231,1315.53023580401,1315.61019423106,1315.65259010769,1315.73254740782,
1315.81241020506,1315.89219602754,1315.97192234273,1316.05160657102,1316.13127755725,
1316.21094501077,1316.29062466159,1316.37033224398,1316.45012747306,1316.52997181476,
1316.60993024181,1316.65232611841,1316.73228341854,1316.81214621579,1316.89193203826,
1316.97165835345,1317.05134258175,1317.13101356797,1317.2106810215,1317.29036067231,
1317.37006825471,1317.44986348379,1317.52970782549,1317.60966625254,1317.65206212913,
1317.73201942926,1317.8118822265,1317.89166804897,1317.97139436417,1318.05107859246,
1318.13074957868,1318.21041703221,1318.29009668303,1318.36980426542,1318.44959949449,
1318.5294438362,1318.60940226325,1318.65179813985,1318.73175543998,1318.81161823722,
1318.8914040597,1318.97113037489,1319.05081460319,1319.13048558941,1319.21015304293,
1319.28983269375,1319.36954027615,1319.44933550522,1319.52917984693,1319.60913827398,
1319.65153415057,1319.73075336223,1319.80987859597,1319.88892802244,1319.96791974293,
1320.04687761498,1320.12581889128,1320.20475987108,1320.28371685104,1320.36275030379,
1320.44182335561,1320.52101079753,1320.58776960123),.UNSPECIFIED.);
#1339=B_SPLINE_CURVE_WITH_KNOTS('',3,(#158945,#158946,#158947,#158948,#158949,
#158950,#158951,#158952,#158953,#158954,#158955,#158956,#158957),
 .UNSPECIFIED.,.F.,.F.,(4,3,1,1,1,1,1,1,4),(1320.58776960123,1320.65127016129,
1321.65100617201,1322.65074218273,1323.65047819345,1324.65021420417,1325.64995021489,
1326.64968622561,1326.87095490841),.UNSPECIFIED.);
#1340=B_SPLINE_CURVE_WITH_KNOTS('',3,(#158959,#158960,#158961,#158962,#158963,
#158964,#158965,#158966,#158967,#158968,#158969,#158970,#158971,#158972,
#158973,#158974,#158975,#158976,#158977,#158978,#158979,#158980,#158981,
#158982,#158983,#158984,#158985,#158986,#158987,#158988,#158989,#158990,
#158991,#158992,#158993,#158994,#158995,#158996,#158997,#158998,#158999,
#159000,#159001,#159002,#159003,#159004,#159005,#159006,#159007,#159008,
#159009,#159010,#159011,#159012,#159013,#159014,#159015,#159016,#159017,
#159018,#159019,#159020,#159021,#159022,#159023,#159024,#159025,#159026,
#159027,#159028,#159029,#159030,#159031,#159032,#159033,#159034,#159035,
#159036,#159037,#159038,#159039,#159040,#159041,#159042,#159043,#159044,
#159045,#159046,#159047,#159048,#159049,#159050,#159051,#159052,#159053,
#159054,#159055,#159056,#159057,#159058,#159059,#159060,#159061,#159062,
#159063,#159064,#159065,#159066,#159067,#159068,#159069,#159070,#159071,
#159072,#159073,#159074,#159075,#159076,#159077,#159078,#159079,#159080,
#159081,#159082,#159083,#159084,#159085,#159086,#159087,#159088,#159089,
#159090,#159091,#159092,#159093,#159094,#159095,#159096,#159097,#159098,
#159099,#159100,#159101,#159102,#159103,#159104,#159105,#159106,#159107,
#159108,#159109,#159110,#159111,#159112,#159113,#159114,#159115,#159116,
#159117,#159118,#159119,#159120,#159121,#159122,#159123,#159124,#159125,
#159126,#159127,#159128,#159129,#159130,#159131,#159132,#159133,#159134,
#159135,#159136,#159137,#159138,#159139,#159140,#159141,#159142,#159143,
#159144,#159145,#159146,#159147,#159148,#159149,#159150,#159151,#159152,
#159153,#159154,#159155,#159156,#159157,#159158,#159159,#159160,#159161,
#159162,#159163,#159164,#159165,#159166,#159167,#159168,#159169,#159170,
#159171,#159172,#159173,#159174,#159175,#159176,#159177,#159178,#159179,
#159180,#159181,#159182,#159183,#159184,#159185,#159186,#159187,#159188,
#159189,#159190,#159191,#159192,#159193,#159194,#159195,#159196,#159197,
#159198,#159199,#159200,#159201,#159202),.UNSPECIFIED.,.F.,.F.,(4,3,3,3,
3,3,3,3,3,3,3,3,3,3,3,3,3,3,3,3,3,3,3,3,3,3,3,3,3,3,3,3,3,3,3,3,3,3,3,3,
3,3,3,3,3,3,3,3,3,3,3,3,3,3,3,3,3,3,3,3,3,3,3,3,3,3,3,3,3,3,3,3,3,3,3,3,
3,3,3,3,3,4),(1326.87095490841,1326.94966200019,1327.02831162128,1327.10692865002,
1327.18552980509,1327.26413159478,1327.34275052616,1327.42144926218,1327.50018888353,
1327.579047932,1327.64942223633,1327.72937953646,1327.8092423337,1327.88902815617,
1327.96875447137,1328.04843869966,1328.12810968588,1328.20777713941,1328.28745679023,
1328.36716437262,1328.4469596017,1328.5268039434,1328.60676237045,1328.64915824705,
1328.72911554718,1328.80897834442,1328.88876416689,1328.96849048209,1329.04817471038,
1329.1278456966,1329.20751315013,1329.28719280095,1329.36690038334,1329.44669561241,
1329.52653995412,1329.60649838117,1329.64889425777,1329.7288515579,1329.80871435514,
1329.88850017762,1329.96822649281,1330.04791072111,1330.12758170733,1330.20724916085,
1330.28692881167,1330.36663639406,1330.44643162314,1330.52627596485,1330.60623439189,
1330.64863026849,1330.72858756862,1330.80845036586,1330.88823618834,1330.96796250353,
1331.04764673182,1331.12731771805,1331.20698517157,1331.28666482239,1331.36637240478,
1331.44616763386,1331.52601197557,1331.60597040261,1331.64836627921,1331.72832357934,
1331.80818637658,1331.88797219906,1331.96769851425,1332.04738274255,1332.12705372877,
1332.20672118229,1332.28640083311,1332.36610841551,1332.44590364458,1332.52574798629,
1332.60570641334,1332.64810228993,1332.73195292313,1332.81566815408,1332.90028616946,
1332.98371340598,1333.06892681078,1333.15414021559),.UNSPECIFIED.);
#1341=B_SPLINE_CURVE_WITH_KNOTS('',3,(#159204,#159205,#159206,#159207,#159208,
#159209,#159210,#159211,#159212,#159213,#159214,#159215,#159216,#159217,
#159218,#159219,#159220,#159221,#159222,#159223,#159224,#159225,#159226,
#159227,#159228,#159229,#159230,#159231,#159232,#159233,#159234,#159235,
#159236,#159237,#159238,#159239,#159240,#159241,#159242,#159243,#159244,
#159245,#159246,#159247,#159248,#159249,#159250,#159251,#159252,#159253,
#159254,#159255,#159256,#159257,#159258,#159259,#159260,#159261,#159262,
#159263,#159264,#159265,#159266,#159267,#159268,#159269,#159270,#159271,
#159272,#159273,#159274,#159275,#159276,#159277,#159278,#159279,#159280,
#159281,#159282,#159283,#159284,#159285,#159286,#159287,#159288,#159289,
#159290,#159291,#159292,#159293,#159294,#159295,#159296,#159297,#159298,
#159299,#159300,#159301,#159302,#159303,#159304,#159305,#159306,#159307,
#159308,#159309,#159310,#159311,#159312,#159313,#159314,#159315,#159316,
#159317,#159318,#159319,#159320,#159321,#159322,#159323,#159324,#159325,
#159326,#159327,#159328,#159329,#159330,#159331,#159332,#159333,#159334,
#159335,#159336,#159337,#159338,#159339,#159340,#159341,#159342,#159343,
#159344,#159345,#159346,#159347,#159348,#159349,#159350,#159351,#159352,
#159353,#159354,#159355,#159356,#159357,#159358,#159359,#159360,#159361,
#159362,#159363,#159364,#159365,#159366,#159367,#159368,#159369,#159370,
#159371,#159372,#159373,#159374,#159375,#159376,#159377,#159378,#159379,
#159380,#159381,#159382,#159383,#159384,#159385,#159386,#159387,#159388,
#159389,#159390,#159391,#159392,#159393,#159394,#159395,#159396,#159397,
#159398,#159399,#159400,#159401,#159402,#159403,#159404,#159405,#159406,
#159407,#159408,#159409,#159410,#159411,#159412,#159413,#159414,#159415,
#159416,#159417,#159418,#159419,#159420,#159421,#159422,#159423,#159424,
#159425,#159426,#159427,#159428,#159429,#159430,#159431,#159432,#159433,
#159434,#159435,#159436,#159437,#159438,#159439,#159440,#159441,#159442,
#159443,#159444,#159445,#159446,#159447),.UNSPECIFIED.,.F.,.F.,(4,3,3,3,
3,3,3,3,3,3,3,3,3,3,3,3,3,3,3,3,3,3,3,3,3,3,3,3,3,3,3,3,3,3,3,3,3,3,3,3,
3,3,3,3,3,3,3,3,3,3,3,3,3,3,3,3,3,3,3,3,3,3,3,3,3,3,3,3,3,3,3,3,3,3,3,3,
3,3,3,3,3,4),(1333.15414021572,1333.23781402459,1333.32160032962,1333.40558801224,
1333.48967942233,1333.57396772497,1333.64783830065,1333.72779560078,1333.80765839802,
1333.88744422049,1333.96717053569,1334.04685476398,1334.1265257502,1334.20619320373,
1334.28587285454,1334.36558043693,1334.44537566601,1334.52522000772,1334.60517843476,
1334.64757431137,1334.7275316115,1334.80739440874,1334.88718023122,1334.96690654641,
1335.0465907747,1335.12626176093,1335.20592921445,1335.28560886527,1335.36531644766,
1335.44511167674,1335.52495601845,1335.60491444549,1335.64731032209,1335.72726762222,
1335.80713041946,1335.88691624194,1335.96664255713,1336.04632678543,1336.12599777165,
1336.20566522517,1336.28534487599,1336.36505245839,1336.44484768746,1336.52469202917,
1336.60465045622,1336.64704633281,1336.72700363294,1336.80686643018,1336.88665225266,
1336.96637856785,1337.04606279614,1337.12573378236,1337.20540123589,1337.28508088671,
1337.3647884691,1337.44458369818,1337.52442803988,1337.60438646693,1337.64678234353,
1337.72673964366,1337.8066024409,1337.88638826338,1337.96611457857,1338.04579880687,
1338.12546979309,1338.20513724661,1338.28481689743,1338.36452447983,1338.4443197089,
1338.52416405061,1338.60412247766,1338.64651835425,1338.72535031001,1338.80408742697,
1338.88324218894,1338.9618396062,1339.04040335043,1339.11894997117,1339.19854385907,
1339.27713063129,1339.35722807703,1339.43732552277),.UNSPECIFIED.);
#1342=B_SPLINE_CURVE_WITH_KNOTS('',3,(#159449,#159450,#159451,#159452,#159453,
#159454,#159455,#159456,#159457,#159458,#159459),.UNSPECIFIED.,.F.,.F.,
(4,1,1,1,1,1,1,1,4),(1339.43732552277,1339.64625436497,1340.64599037569,
1341.64572638641,1342.64546239713,1343.64519840785,1344.64493441857,1345.64467042929,
1345.72051082995),.UNSPECIFIED.);
#1343=B_SPLINE_CURVE_WITH_KNOTS('',3,(#159461,#159462,#159463,#159464,#159465,
#159466,#159467,#159468,#159469,#159470),.UNSPECIFIED.,.F.,.F.,(4,1,1,1,
1,1,1,4),(1345.72051082995,1346.64440644001,1347.64414245073,1348.64387846145,
1349.64361447217,1350.64335048289,1351.64308649361,1352.00369613713),
 .UNSPECIFIED.);
#1344=B_SPLINE_CURVE_WITH_KNOTS('',3,(#159472,#159473,#159474,#159475,#159476,
#159477,#159478,#159479,#159480,#159481),.UNSPECIFIED.,.F.,.F.,(4,1,1,1,
1,1,1,4),(1352.00369613713,1352.64282250433,1353.64255851505,1354.64229452577,
1355.64203053649,1356.64176654721,1357.64150255794,1358.28688144431),
 .UNSPECIFIED.);
#1345=B_SPLINE_CURVE_WITH_KNOTS('',3,(#159483,#159484,#159485,#159486,#159487,
#159488,#159489,#159490,#159491,#159492,#159493,#159494,#159495,#159496,
#159497,#159498,#159499,#159500,#159501,#159502,#159503,#159504,#159505,
#159506,#159507,#159508,#159509,#159510,#159511,#159512,#159513,#159514,
#159515,#159516,#159517,#159518,#159519,#159520,#159521,#159522,#159523,
#159524,#159525,#159526,#159527,#159528,#159529,#159530,#159531,#159532,
#159533,#159534,#159535,#159536,#159537,#159538,#159539,#159540,#159541,
#159542,#159543,#159544,#159545,#159546,#159547,#159548,#159549,#159550,
#159551,#159552,#159553,#159554,#159555,#159556,#159557,#159558,#159559,
#159560,#159561,#159562,#159563,#159564,#159565,#159566,#159567,#159568,
#159569,#159570,#159571,#159572,#159573,#159574,#159575,#159576,#159577,
#159578,#159579,#159580,#159581,#159582,#159583,#159584,#159585,#159586,
#159587,#159588,#159589,#159590,#159591,#159592,#159593,#159594,#159595,
#159596,#159597,#159598,#159599,#159600,#159601,#159602,#159603,#159604,
#159605,#159606,#159607,#159608,#159609,#159610,#159611,#159612,#159613,
#159614,#159615,#159616,#159617,#159618,#159619,#159620,#159621,#159622,
#159623,#159624,#159625,#159626,#159627,#159628,#159629,#159630,#159631,
#159632,#159633,#159634,#159635,#159636,#159637,#159638,#159639,#159640,
#159641,#159642,#159643,#159644,#159645,#159646,#159647,#159648,#159649,
#159650,#159651,#159652,#159653,#159654,#159655,#159656,#159657,#159658,
#159659,#159660,#159661,#159662,#159663,#159664,#159665,#159666,#159667,
#159668,#159669,#159670,#159671,#159672,#159673,#159674,#159675,#159676,
#159677,#159678,#159679,#159680,#159681,#159682,#159683,#159684,#159685,
#159686,#159687,#159688,#159689,#159690,#159691,#159692,#159693,#159694,
#159695,#159696,#159697,#159698,#159699,#159700,#159701,#159702,#159703,
#159704,#159705,#159706,#159707,#159708,#159709,#159710,#159711,#159712,
#159713,#159714,#159715,#159716,#159717,#159718,#159719,#159720,#159721,
#159722,#159723,#159724,#159725,#159726),.UNSPECIFIED.,.F.,.F.,(4,3,3,3,
3,3,3,3,3,3,3,3,3,3,3,3,3,3,3,3,3,3,3,3,3,3,3,3,3,3,3,3,3,3,3,3,3,3,3,3,
3,3,3,3,3,3,3,3,3,3,3,3,3,3,3,3,3,3,3,3,3,3,3,3,3,3,3,3,3,3,3,3,3,3,3,3,
3,3,3,3,3,4),(1358.28688169172,1358.37804472668,1358.46962250677,1358.56176130781,
1358.64123856866,1358.72119586879,1358.80105866603,1358.8808444885,1358.9605708037,
1359.04025503199,1359.11992601821,1359.19959347174,1359.27927312255,1359.35898070495,
1359.43877593402,1359.51862027573,1359.59857870278,1359.64097457938,1359.72093187951,
1359.80079467675,1359.88058049923,1359.96030681442,1360.03999104272,1360.11966202894,
1360.19932948246,1360.27900913328,1360.35871671567,1360.43851194475,1360.51835628646,
1360.5983147135,1360.6407105901,1360.72066789023,1360.80053068747,1360.88031650995,
1360.96004282514,1361.03972705343,1361.11939803966,1361.19906549318,1361.278745144,
1361.35845272639,1361.43824795547,1361.51809229718,1361.59805072422,1361.64044660082,
1361.72040390095,1361.80026669819,1361.88005252067,1361.95977883586,1362.03946306416,
1362.11913405038,1362.1988015039,1362.27848115472,1362.35818873711,1362.43798396619,
1362.5178283079,1362.59778673494,1362.64018261154,1362.72013991167,1362.80000270892,
1362.87978853139,1362.95951484658,1363.03919907488,1363.1188700611,1363.19853751463,
1363.27821716544,1363.35792474784,1363.43771997692,1363.51756431862,1363.59752274567,
1363.63991862226,1363.71908597835,1363.79815940171,1363.87715710195,1363.95609721831,
1364.03500353988,1364.11389342232,1364.19278319829,1364.27168919809,1364.35067093608,
1364.429692563,1364.50882608086,1364.57006675149),.UNSPECIFIED.);
#1346=B_SPLINE_CURVE_WITH_KNOTS('',3,(#159728,#159729,#159730,#159731,#159732,
#159733,#159734,#159735,#159736,#159737,#159738,#159739,#159740),
 .UNSPECIFIED.,.F.,.F.,(4,3,1,1,1,1,1,1,4),(1364.57006675149,1364.63965463298,
1365.6393906437,1366.63912665442,1367.63886266514,1368.63859867586,1369.63833468658,
1370.6380706973,1370.85325205867),.UNSPECIFIED.);
#1347=B_SPLINE_CURVE_WITH_KNOTS('',3,(#159742,#159743,#159744,#159745,#159746,
#159747,#159748,#159749,#159750,#159751),.UNSPECIFIED.,.F.,.F.,(4,1,1,1,
1,1,1,4),(1370.85325205867,1371.63780670802,1372.63754271874,1373.63727872946,
1374.63701474018,1375.6367507509,1376.63648676162,1377.13643736585),
 .UNSPECIFIED.);
#1348=B_SPLINE_CURVE_WITH_KNOTS('',3,(#159753,#159754,#159755,#159756,#159757,
#159758,#159759,#159760,#159761,#159762),.UNSPECIFIED.,.F.,.F.,(4,1,1,1,
1,1,1,4),(1377.13643736585,1377.63622277234,1378.63595878306,1379.63569479378,
1380.6354308045,1381.63516681522,1382.63490282594,1383.41962267303),
 .UNSPECIFIED.);
#1349=B_SPLINE_CURVE_WITH_KNOTS('',3,(#159764,#159765,#159766,#159767,#159768,
#159769,#159770,#159771,#159772,#159773,#159774,#159775),.UNSPECIFIED.,
 .F.,.F.,(4,2,1,1,1,1,1,1,4),(1383.41962267303,1383.63463883666,1384.63437484738,
1385.6341108581,1386.63384686882,1387.63358287954,1388.63331889026,1389.63305490098,
1389.70280798021),.UNSPECIFIED.);
#1350=B_SPLINE_CURVE_WITH_KNOTS('',3,(#159777,#159778,#159779,#159780,#159781,
#159782,#159783,#159784,#159785,#159786,#159787,#159788,#159789,#159790,
#159791,#159792,#159793,#159794,#159795,#159796,#159797,#159798,#159799,
#159800,#159801,#159802,#159803,#159804,#159805,#159806,#159807,#159808,
#159809,#159810,#159811,#159812,#159813,#159814,#159815,#159816,#159817,
#159818,#159819,#159820,#159821,#159822,#159823,#159824,#159825,#159826,
#159827,#159828,#159829,#159830,#159831,#159832,#159833,#159834,#159835,
#159836,#159837,#159838,#159839,#159840,#159841,#159842,#159843,#159844,
#159845,#159846,#159847,#159848,#159849,#159850,#159851,#159852,#159853,
#159854,#159855,#159856,#159857,#159858,#159859,#159860,#159861,#159862,
#159863,#159864,#159865,#159866,#159867,#159868,#159869,#159870,#159871,
#159872,#159873,#159874,#159875,#159876,#159877,#159878,#159879,#159880,
#159881,#159882,#159883,#159884,#159885,#159886,#159887,#159888,#159889,
#159890,#159891,#159892,#159893,#159894,#159895,#159896,#159897,#159898,
#159899,#159900,#159901,#159902,#159903,#159904,#159905,#159906,#159907,
#159908,#159909,#159910,#159911,#159912,#159913,#159914,#159915,#159916,
#159917,#159918,#159919,#159920,#159921,#159922,#159923,#159924,#159925,
#159926,#159927,#159928,#159929,#159930,#159931,#159932,#159933,#159934,
#159935,#159936,#159937,#159938,#159939,#159940,#159941,#159942,#159943,
#159944,#159945,#159946,#159947,#159948,#159949,#159950,#159951,#159952,
#159953,#159954,#159955,#159956,#159957,#159958,#159959,#159960,#159961,
#159962,#159963,#159964,#159965,#159966,#159967,#159968,#159969,#159970,
#159971,#159972,#159973,#159974,#159975,#159976,#159977,#159978,#159979,
#159980,#159981,#159982,#159983,#159984,#159985,#159986,#159987,#159988,
#159989,#159990,#159991,#159992,#159993,#159994,#159995,#159996,#159997,
#159998,#159999,#160000,#160001,#160002,#160003,#160004,#160005,#160006,
#160007,#160008,#160009,#160010,#160011,#160012,#160013,#160014,#160015,
#160016,#160017,#160018,#160019,#160020),.UNSPECIFIED.,.F.,.F.,(4,3,3,3,
3,3,3,3,3,3,3,3,3,3,3,3,3,3,3,3,3,3,3,3,3,3,3,3,3,3,3,3,3,3,3,3,3,3,3,3,
3,3,3,3,3,3,3,3,3,3,3,3,3,3,3,3,3,3,3,3,3,3,3,3,3,3,3,3,3,3,3,3,3,3,3,3,
3,3,3,3,3,4),(1389.70280798021,1389.78194901558,1389.86100069503,1389.9399812097,
1390.01890868487,1390.09780924709,1390.17669759541,1390.25559006204,1390.33450297977,
1390.41349813155,1390.49253681273,1390.57169311822,1390.6327909117,1390.71274821183,
1390.79261100907,1390.87239683154,1390.95212314674,1391.03180737503,1391.11147836125,
1391.19114581478,1391.2708254656,1391.35053304799,1391.43032827707,1391.51017261877,
1391.59013104582,1391.63252692242,1391.71248422255,1391.79234701979,1391.87213284226,
1391.95185915746,1392.03154338575,1392.11121437197,1392.1908818255,1392.27056147632,
1392.35026905871,1392.43006428779,1392.50990862949,1392.58986705654,1392.63226293314,
1392.71222023327,1392.79208303051,1392.87186885299,1392.95159516818,1393.03127939647,
1393.1109503827,1393.19061783622,1393.27029748704,1393.35000506943,1393.42980029851,
1393.50964464022,1393.58960306726,1393.63199894386,1393.71195624399,1393.79181904123,
1393.87160486371,1393.9513311789,1394.0310154072,1394.11068639342,1394.19035384694,
1394.27003349776,1394.34974108015,1394.42953630923,1394.50938065094,1394.58933907798,
1394.63173495458,1394.71169225471,1394.79155505195,1394.87134087443,1394.95106718962,
1395.03075141792,1395.11042240414,1395.19008985766,1395.26976950848,1395.34947709088,
1395.42927231995,1395.50911666166,1395.58907508871,1395.6314709653,1395.72358358603,
1395.8153650835,1395.90649484727,1395.98599303994),.UNSPECIFIED.);
#1351=B_SPLINE_CURVE_WITH_KNOTS('',3,(#160022,#160023,#160024,#160025,#160026,
#160027,#160028,#160029,#160030,#160031),.UNSPECIFIED.,.F.,.F.,(4,1,1,1,
1,1,1,4),(1395.98599328739,1396.63120697602,1397.63094298674,1398.63067899746,
1399.63041500818,1400.6301510189,1401.62988702962,1402.26917859457),
 .UNSPECIFIED.);
#1352=B_SPLINE_CURVE_WITH_KNOTS('',3,(#160033,#160034,#160035,#160036,#160037,
#160038,#160039,#160040,#160041,#160042),.UNSPECIFIED.,.F.,.F.,(4,1,1,1,
1,1,1,4),(1402.26917859457,1402.62962304034,1403.62935905106,1404.62909506178,
1405.6288310725,1406.62856708322,1407.62830309394,1408.55236390175),
 .UNSPECIFIED.);
#1353=B_SPLINE_CURVE_WITH_KNOTS('',3,(#160044,#160045,#160046,#160047,#160048,
#160049,#160050,#160051,#160052,#160053,#160054,#160055),.UNSPECIFIED.,
 .F.,.F.,(4,2,1,1,1,1,1,1,4),(1408.55236390175,1408.62803910466,1409.62777511538,
1410.6275111261,1411.62724713682,1412.62698314754,1413.62671915826,1414.62645516898,
1414.83554920893),.UNSPECIFIED.);
#1354=B_SPLINE_CURVE_WITH_KNOTS('',3,(#160057,#160058,#160059,#160060,#160061,
#160062,#160063,#160064,#160065,#160066,#160067,#160068,#160069,#160070,
#160071,#160072,#160073,#160074,#160075,#160076,#160077,#160078,#160079,
#160080,#160081,#160082,#160083,#160084,#160085,#160086,#160087,#160088,
#160089,#160090,#160091,#160092,#160093,#160094,#160095,#160096,#160097,
#160098,#160099,#160100,#160101,#160102,#160103,#160104,#160105,#160106,
#160107,#160108,#160109,#160110,#160111,#160112,#160113,#160114,#160115,
#160116,#160117,#160118,#160119,#160120,#160121,#160122,#160123,#160124,
#160125,#160126,#160127,#160128,#160129,#160130,#160131,#160132,#160133,
#160134,#160135,#160136,#160137,#160138,#160139,#160140,#160141,#160142,
#160143,#160144,#160145,#160146,#160147,#160148,#160149,#160150,#160151,
#160152,#160153,#160154,#160155,#160156,#160157,#160158,#160159,#160160,
#160161,#160162,#160163,#160164,#160165,#160166,#160167,#160168,#160169,
#160170,#160171,#160172,#160173,#160174,#160175,#160176,#160177,#160178,
#160179,#160180,#160181,#160182,#160183,#160184,#160185,#160186,#160187,
#160188,#160189,#160190,#160191,#160192,#160193,#160194,#160195,#160196,
#160197,#160198,#160199,#160200,#160201,#160202,#160203,#160204,#160205,
#160206,#160207,#160208,#160209,#160210,#160211,#160212,#160213,#160214,
#160215,#160216,#160217,#160218,#160219,#160220,#160221,#160222,#160223,
#160224,#160225,#160226,#160227,#160228,#160229,#160230,#160231,#160232,
#160233,#160234,#160235,#160236,#160237,#160238,#160239,#160240,#160241,
#160242,#160243,#160244,#160245,#160246,#160247,#160248,#160249,#160250,
#160251,#160252,#160253,#160254,#160255,#160256,#160257,#160258,#160259,
#160260,#160261,#160262,#160263,#160264,#160265,#160266,#160267,#160268,
#160269,#160270,#160271,#160272,#160273,#160274,#160275,#160276,#160277,
#160278,#160279,#160280,#160281,#160282,#160283,#160284,#160285,#160286,
#160287,#160288,#160289,#160290,#160291,#160292,#160293,#160294,#160295,
#160296,#160297,#160298,#160299,#160300),.UNSPECIFIED.,.F.,.F.,(4,3,3,3,
3,3,3,3,3,3,3,3,3,3,3,3,3,3,3,3,3,3,3,3,3,3,3,3,3,3,3,3,3,3,3,3,3,3,3,3,
3,3,3,3,3,3,3,3,3,3,3,3,3,3,3,3,3,3,3,3,3,3,3,3,3,3,3,3,3,3,3,3,3,3,3,3,
3,3,3,3,3,4),(1414.83554920893,1414.91422319859,1414.99283632039,1415.0720056778,
1415.15056272849,1415.22911755209,1415.3076866817,1415.3873128062,1415.46599905401,
1415.54609511686,1415.6261911797,1415.70614847983,1415.78601127707,1415.86579709955,
1415.94552341474,1416.02520764304,1416.10487862926,1416.18454608278,1416.2642257336,
1416.34393331599,1416.42372854507,1416.50357288678,1416.58353131382,1416.62592719042,
1416.70588449055,1416.78574728779,1416.86553311027,1416.94525942546,1417.02494365375,
1417.10461463998,1417.1842820935,1417.26396174432,1417.34366932671,1417.42346455579,
1417.5033088975,1417.58326732454,1417.62566320114,1417.70562050127,1417.78548329851,
1417.86526912099,1417.94499543618,1418.02467966447,1418.1043506507,1418.18401810422,
1418.26369775504,1418.34340533743,1418.42320056651,1418.50304490822,1418.58300333526,
1418.62539921186,1418.70535651199,1418.78521930923,1418.86500513171,1418.9447314469,
1419.0244156752,1419.10408666142,1419.18375411494,1419.26343376576,1419.34314134815,
1419.42293657723,1419.50278091894,1419.58273934598,1419.62513522258,1419.70509252271,
1419.78495531995,1419.86474114243,1419.94446745762,1420.02415168591,1420.10382267214,
1420.18349012566,1420.26316977648,1420.34287735887,1420.42267258795,1420.50251692965,
1420.5824753567,1420.6248712333,1420.70918020921,1420.79334694167,1420.8773195318,
1420.96117782697,1421.0448782206,1421.11873451598),.UNSPECIFIED.);
#1355=B_SPLINE_CURVE_WITH_KNOTS('',3,(#160302,#160303,#160304,#160305,#160306,
#160307,#160308,#160309,#160310,#160311,#160312,#160313,#160314,#160315,
#160316,#160317,#160318,#160319,#160320,#160321,#160322,#160323,#160324,
#160325,#160326,#160327,#160328,#160329,#160330,#160331,#160332,#160333,
#160334,#160335,#160336,#160337,#160338,#160339,#160340,#160341,#160342,
#160343,#160344,#160345,#160346,#160347,#160348,#160349,#160350,#160351,
#160352,#160353,#160354,#160355,#160356,#160357,#160358,#160359,#160360,
#160361,#160362,#160363,#160364,#160365,#160366,#160367,#160368,#160369,
#160370,#160371,#160372,#160373,#160374,#160375,#160376,#160377,#160378,
#160379,#160380,#160381,#160382,#160383,#160384,#160385,#160386,#160387,
#160388,#160389,#160390,#160391,#160392,#160393,#160394,#160395,#160396,
#160397,#160398,#160399,#160400,#160401,#160402,#160403,#160404,#160405,
#160406,#160407,#160408,#160409,#160410,#160411,#160412,#160413,#160414,
#160415,#160416,#160417,#160418,#160419,#160420,#160421,#160422,#160423,
#160424,#160425,#160426,#160427,#160428,#160429,#160430,#160431,#160432,
#160433,#160434,#160435,#160436,#160437,#160438,#160439,#160440,#160441,
#160442,#160443,#160444,#160445,#160446,#160447,#160448,#160449,#160450,
#160451,#160452,#160453,#160454,#160455,#160456,#160457,#160458,#160459,
#160460,#160461,#160462,#160463,#160464,#160465,#160466,#160467,#160468,
#160469,#160470,#160471,#160472,#160473,#160474,#160475,#160476,#160477,
#160478,#160479,#160480,#160481,#160482,#160483,#160484,#160485,#160486,
#160487,#160488,#160489,#160490,#160491,#160492,#160493,#160494,#160495,
#160496,#160497,#160498,#160499,#160500,#160501,#160502,#160503,#160504,
#160505,#160506,#160507,#160508,#160509,#160510,#160511,#160512,#160513,
#160514,#160515,#160516,#160517,#160518,#160519,#160520,#160521,#160522,
#160523,#160524,#160525,#160526,#160527,#160528,#160529,#160530,#160531,
#160532,#160533,#160534,#160535,#160536,#160537,#160538,#160539,#160540,
#160541,#160542,#160543,#160544,#160545),.UNSPECIFIED.,.F.,.F.,(4,3,3,3,
3,3,3,3,3,3,3,3,3,3,3,3,3,3,3,3,3,3,3,3,3,3,3,3,3,3,3,3,3,3,3,3,3,3,3,3,
3,3,3,3,3,3,3,3,3,3,3,3,3,3,3,3,3,3,3,3,3,3,3,3,3,3,3,3,3,3,3,3,3,3,3,3,
3,3,3,3,3,4),(1421.11873451611,1421.20198682774,1421.28533673185,1421.37015435989,
1421.45378598796,1421.53919661599,1421.62460724402,1421.70456454415,1421.78442734139,
1421.86421316387,1421.94393947906,1422.02362370736,1422.10329469358,1422.1829621471,
1422.26264179792,1422.34234938032,1422.42214460939,1422.5019889511,1422.58194737815,
1422.62434325474,1422.70430055487,1422.78416335211,1422.86394917459,1422.94367548978,
1423.02335971808,1423.1030307043,1423.18269815782,1423.26237780864,1423.34208539104,
1423.42188062011,1423.50172496182,1423.58168338887,1423.62407926546,1423.70403656559,
1423.78389936283,1423.8636851853,1423.9434115005,1424.02309572879,1424.10276671501,
1424.18243416854,1424.26211381936,1424.34182140175,1424.42161663083,1424.50146097253,
1424.58141939958,1424.62381527618,1424.70377257631,1424.78363537355,1424.86342119603,
1424.94314751122,1425.02283173951,1425.10250272574,1425.18217017926,1425.26184983008,
1425.34155741247,1425.42135264155,1425.50119698326,1425.5811554103,1425.6235512869,
1425.70350858703,1425.78337138427,1425.86315720674,1425.94288352194,1426.02256775023,
1426.10223873645,1426.18190618998,1426.2615858408,1426.34129342319,1426.42108865227,
1426.50093299397,1426.58089142102,1426.62328729762,1426.7021669801,1426.78095145909,
1426.85964601321,1426.93828972882,1427.01689915789,1427.09549082411,1427.17410791049,
1427.2527358973,1427.33143433151,1427.40191982329),.UNSPECIFIED.);
#1356=B_SPLINE_CURVE_WITH_KNOTS('',3,(#160547,#160548,#160549,#160550,#160551,
#160552,#160553,#160554,#160555,#160556,#160557),.UNSPECIFIED.,.F.,.F.,
(4,1,1,1,1,1,1,1,4),(1427.40191982329,1427.62302330834,1428.62275931906,
1429.62249532978,1430.6222313405,1431.62196735122,1432.62170336194,1433.62143937266,
1433.68510513047),.UNSPECIFIED.);
#1357=B_SPLINE_CURVE_WITH_KNOTS('',3,(#160559,#160560,#160561,#160562,#160563,
#160564,#160565,#160566,#160567,#160568,#160569,#160570,#160571,#160572,
#160573,#160574,#160575,#160576,#160577,#160578,#160579,#160580,#160581,
#160582,#160583,#160584,#160585,#160586,#160587,#160588,#160589,#160590,
#160591,#160592,#160593,#160594,#160595,#160596,#160597,#160598,#160599,
#160600,#160601,#160602,#160603,#160604,#160605,#160606,#160607,#160608,
#160609,#160610,#160611,#160612,#160613,#160614,#160615,#160616,#160617,
#160618,#160619,#160620,#160621,#160622,#160623,#160624,#160625,#160626,
#160627,#160628,#160629,#160630,#160631,#160632,#160633,#160634,#160635,
#160636,#160637,#160638,#160639,#160640,#160641,#160642,#160643,#160644,
#160645,#160646,#160647,#160648,#160649,#160650,#160651,#160652,#160653,
#160654,#160655,#160656,#160657,#160658,#160659,#160660,#160661,#160662,
#160663,#160664,#160665,#160666,#160667,#160668,#160669,#160670,#160671,
#160672,#160673,#160674,#160675,#160676,#160677,#160678,#160679,#160680,
#160681,#160682,#160683,#160684,#160685,#160686,#160687,#160688,#160689,
#160690,#160691,#160692,#160693,#160694,#160695,#160696,#160697,#160698,
#160699,#160700,#160701,#160702,#160703,#160704,#160705,#160706,#160707,
#160708,#160709,#160710,#160711,#160712,#160713,#160714,#160715,#160716,
#160717,#160718,#160719,#160720,#160721,#160722,#160723,#160724,#160725,
#160726,#160727,#160728,#160729,#160730,#160731,#160732,#160733,#160734,
#160735,#160736,#160737,#160738,#160739,#160740,#160741,#160742,#160743,
#160744,#160745,#160746,#160747,#160748,#160749,#160750,#160751,#160752,
#160753,#160754,#160755,#160756,#160757,#160758,#160759,#160760,#160761,
#160762,#160763,#160764,#160765,#160766,#160767,#160768,#160769,#160770,
#160771,#160772,#160773,#160774,#160775,#160776,#160777,#160778,#160779,
#160780,#160781,#160782,#160783,#160784,#160785,#160786,#160787,#160788,
#160789,#160790,#160791,#160792,#160793,#160794,#160795,#160796,#160797,
#160798,#160799,#160800,#160801,#160802),.UNSPECIFIED.,.F.,.F.,(4,3,3,3,
3,3,3,3,3,3,3,3,3,3,3,3,3,3,3,3,3,3,3,3,3,3,3,3,3,3,3,3,3,3,3,3,3,3,3,3,
3,3,3,3,3,3,3,3,3,3,3,3,3,3,3,3,3,3,3,3,3,3,3,3,3,3,3,3,3,3,3,3,3,3,3,3,
3,3,3,3,3,4),(1433.68510513047,1433.76430171396,1433.84340818076,1433.92244268633,
1434.00142332046,1434.08037593041,1434.1593155102,1434.23825835883,1434.31722077516,
1434.3962651774,1434.47535225123,1434.55455861227,1434.62117538338,1434.70113268351,
1434.78099548076,1434.86078130323,1434.94050761843,1435.02019184673,1435.09986283295,
1435.17953028648,1435.2592099373,1435.33891751969,1435.41871274877,1435.49855709048,
1435.57851551753,1435.62091139411,1435.70086869424,1435.78073149149,1435.86051731396,
1435.94024362915,1436.01992785745,1436.09959884367,1436.1792662972,1436.25894594801,
1436.33865353041,1436.41844875948,1436.49829310119,1436.57825152824,1436.62064740483,
1436.70060470496,1436.7804675022,1436.86025332467,1436.93997963987,1437.01966386816,
1437.09933485438,1437.1790023079,1437.25868195872,1437.33838954111,1437.41818477019,
1437.49802911189,1437.57798753894,1437.62038341555,1437.70034071568,1437.78020351292,
1437.8599893354,1437.93971565059,1438.01939987889,1438.09907086511,1438.17873831863,
1438.25841796945,1438.33812555185,1438.41792078092,1438.49776512263,1438.57772354968,
1438.62011942627,1438.7000767264,1438.77993952365,1438.85972534612,1438.93945166132,
1439.01913588961,1439.09880687583,1439.17847432936,1439.25815398018,1439.33786156257,
1439.41765679165,1439.49750113336,1439.57745956041,1439.61985543699,1439.71247622588,
1439.80474479726,1439.89632503004,1439.96829031496),.UNSPECIFIED.);
#1358=B_SPLINE_CURVE_WITH_KNOTS('',3,(#160804,#160805,#160806,#160807,#160808,
#160809,#160810,#160811,#160812,#160813),.UNSPECIFIED.,.F.,.F.,(4,1,1,1,
1,1,1,4),(1439.96829043765,1440.61959144771,1441.61932745843,1442.61906346915,
1443.61879947987,1444.61853549059,1445.61827150131,1446.25147574483),
 .UNSPECIFIED.);
#1359=B_SPLINE_CURVE_WITH_KNOTS('',3,(#160815,#160816,#160817,#160818,#160819,
#160820,#160821,#160822,#160823,#160824),.UNSPECIFIED.,.F.,.F.,(4,1,1,1,
1,1,1,4),(1446.25147574483,1446.61800751203,1447.61774352275,1448.61747953347,
1449.61721554419,1450.61695155491,1451.61668756563,1452.53466105201),
 .UNSPECIFIED.);
#1360=B_SPLINE_CURVE_WITH_KNOTS('',3,(#160826,#160827,#160828,#160829,#160830,
#160831,#160832,#160833,#160834,#160835,#160836,#160837),.UNSPECIFIED.,
 .F.,.F.,(4,2,1,1,1,1,1,1,4),(1452.53466105201,1452.61642357635,1453.61615958707,
1454.61589559779,1455.61563160851,1456.61536761923,1457.61510362995,1458.61483964067,
1458.81784635919),.UNSPECIFIED.);
#1361=B_SPLINE_CURVE_WITH_KNOTS('',3,(#160839,#160840,#160841,#160842,#160843,
#160844,#160845,#160846,#160847,#160848,#160849,#160850,#160851,#160852,
#160853,#160854,#160855,#160856,#160857,#160858,#160859,#160860,#160861,
#160862,#160863,#160864,#160865,#160866,#160867,#160868,#160869,#160870,
#160871,#160872,#160873,#160874,#160875,#160876,#160877,#160878,#160879,
#160880,#160881,#160882,#160883,#160884,#160885,#160886,#160887,#160888,
#160889,#160890,#160891,#160892,#160893,#160894,#160895,#160896,#160897,
#160898,#160899,#160900,#160901,#160902,#160903,#160904,#160905,#160906,
#160907,#160908,#160909,#160910,#160911,#160912,#160913,#160914,#160915,
#160916,#160917,#160918,#160919,#160920,#160921,#160922,#160923,#160924,
#160925,#160926,#160927,#160928,#160929,#160930,#160931,#160932,#160933,
#160934,#160935,#160936,#160937,#160938,#160939,#160940,#160941,#160942,
#160943,#160944,#160945,#160946,#160947,#160948,#160949,#160950,#160951,
#160952,#160953,#160954,#160955,#160956,#160957,#160958,#160959,#160960,
#160961,#160962,#160963,#160964,#160965,#160966,#160967,#160968,#160969,
#160970,#160971,#160972,#160973,#160974,#160975,#160976,#160977,#160978,
#160979,#160980,#160981,#160982,#160983,#160984,#160985,#160986,#160987,
#160988,#160989,#160990,#160991,#160992,#160993,#160994,#160995,#160996,
#160997,#160998,#160999,#161000,#161001,#161002,#161003,#161004,#161005,
#161006,#161007,#161008,#161009,#161010,#161011,#161012,#161013,#161014,
#161015,#161016,#161017,#161018,#161019,#161020,#161021,#161022,#161023,
#161024,#161025,#161026,#161027,#161028,#161029,#161030,#161031,#161032,
#161033,#161034,#161035,#161036,#161037,#161038,#161039,#161040,#161041,
#161042,#161043,#161044,#161045,#161046,#161047,#161048,#161049,#161050,
#161051,#161052,#161053,#161054,#161055,#161056,#161057,#161058,#161059,
#161060,#161061,#161062,#161063,#161064,#161065,#161066,#161067,#161068,
#161069,#161070,#161071,#161072,#161073,#161074,#161075,#161076,#161077,
#161078,#161079,#161080,#161081,#161082),.UNSPECIFIED.,.F.,.F.,(4,3,3,3,
3,3,3,3,3,3,3,3,3,3,3,3,3,3,3,3,3,3,3,3,3,3,3,3,3,3,3,3,3,3,3,3,3,3,3,3,
3,3,3,3,3,3,3,3,3,3,3,3,3,3,3,3,3,3,3,3,3,3,3,3,3,3,3,3,3,3,3,3,3,3,3,3,
3,3,3,3,3,4),(1458.81784635919,1458.89650835172,1458.97510783377,1459.05504131097,
1459.13358093235,1459.21211704093,1459.29066618012,1459.37164354793,1459.45030870812,
1459.53244217975,1459.61457565139,1459.69453295152,1459.77439574876,1459.85418157123,
1459.93390788643,1460.01359211472,1460.09326310094,1460.17293055447,1460.25261020528,
1460.33231778768,1460.41211301675,1460.49195735846,1460.57191578551,1460.61431166211,
1460.69426896224,1460.77413175948,1460.85391758195,1460.93364389715,1461.01332812544,
1461.09299911166,1461.17266656519,1461.25234621601,1461.3320537984,1461.41184902748,
1461.49169336918,1461.57165179623,1461.61404767283,1461.69400497296,1461.7738677702,
1461.85365359268,1461.93337990787,1462.01306413617,1462.09273512239,1462.17240257591,
1462.25208222673,1462.33178980913,1462.4115850382,1462.49142937991,1462.57138780696,
1462.61378368355,1462.69374098368,1462.77360378092,1462.8533896034,1462.93311591859,
1463.01280014688,1463.09247113311,1463.17213858663,1463.25181823745,1463.33152581984,
1463.41132104892,1463.49116539063,1463.57112381767,1463.61351969427,1463.6934769944,
1463.77333979164,1463.85312561412,1463.93285192931,1464.01253615761,1464.09220714383,
1464.17187459735,1464.25155424817,1464.33126183057,1464.41105705964,1464.49090140135,
1464.5708598284,1464.61325570499,1464.69780465656,1464.7822076085,1464.86640944893,
1464.95049205445,1465.03440868174,1465.10103166624),.UNSPECIFIED.);
#1362=B_SPLINE_CURVE_WITH_KNOTS('',3,(#161084,#161085,#161086,#161087,#161088,
#161089,#161090,#161091,#161092,#161093,#161094,#161095,#161096,#161097,
#161098,#161099,#161100,#161101,#161102,#161103,#161104,#161105,#161106,
#161107,#161108,#161109,#161110,#161111,#161112,#161113,#161114,#161115,
#161116,#161117,#161118,#161119,#161120,#161121,#161122,#161123,#161124,
#161125,#161126,#161127,#161128,#161129,#161130,#161131,#161132,#161133,
#161134,#161135,#161136,#161137,#161138,#161139,#161140,#161141,#161142,
#161143,#161144,#161145,#161146,#161147,#161148,#161149,#161150,#161151,
#161152,#161153,#161154,#161155,#161156,#161157,#161158,#161159,#161160,
#161161,#161162,#161163,#161164,#161165,#161166,#161167,#161168,#161169,
#161170,#161171,#161172,#161173,#161174,#161175,#161176,#161177,#161178,
#161179,#161180,#161181,#161182,#161183,#161184,#161185,#161186,#161187,
#161188,#161189,#161190,#161191,#161192,#161193,#161194,#161195,#161196,
#161197,#161198,#161199,#161200,#161201,#161202,#161203,#161204,#161205,
#161206,#161207,#161208,#161209,#161210,#161211,#161212,#161213,#161214,
#161215,#161216,#161217,#161218,#161219,#161220,#161221,#161222,#161223,
#161224,#161225,#161226,#161227,#161228,#161229,#161230,#161231,#161232,
#161233,#161234,#161235,#161236,#161237,#161238,#161239,#161240,#161241,
#161242,#161243,#161244,#161245,#161246,#161247,#161248,#161249,#161250,
#161251,#161252,#161253,#161254,#161255,#161256,#161257,#161258,#161259,
#161260,#161261,#161262,#161263,#161264,#161265,#161266,#161267,#161268,
#161269,#161270,#161271,#161272,#161273,#161274,#161275,#161276,#161277,
#161278,#161279,#161280,#161281,#161282,#161283,#161284,#161285,#161286,
#161287,#161288,#161289,#161290,#161291,#161292,#161293,#161294,#161295,
#161296,#161297,#161298,#161299,#161300,#161301,#161302,#161303,#161304,
#161305,#161306,#161307,#161308,#161309,#161310,#161311,#161312,#161313,
#161314,#161315,#161316,#161317,#161318,#161319,#161320,#161321,#161322,
#161323,#161324,#161325,#161326,#161327,#161328,#161329,#161330),
 .UNSPECIFIED.,.F.,.F.,(4,3,3,3,3,3,3,3,3,3,3,3,3,3,3,3,3,3,3,3,3,3,3,3,
3,3,3,3,3,3,3,3,3,3,3,3,3,3,3,3,3,3,3,3,3,3,3,3,3,3,3,3,3,3,3,3,3,3,3,3,
3,3,3,3,3,3,3,3,3,3,3,3,3,3,3,3,3,3,3,3,3,3,4),(1465.10103166637,1465.18408255591,
1465.26722414529,1465.3536660379,1465.43707971455,1465.52059140623,1465.60425622782,
1465.61299171571,1465.69294901584,1465.77281181308,1465.85259763555,1465.93232395075,
1466.01200817904,1466.09167916526,1466.17134661879,1466.25102626961,1466.330733852,
1466.41052908107,1466.49037342278,1466.57033184983,1466.61272772643,1466.69268502656,
1466.7725478238,1466.85233364628,1466.93205996147,1467.01174418976,1467.09141517599,
1467.17108262951,1467.25076228033,1467.33046986272,1467.4102650918,1467.49010943351,
1467.57006786055,1467.61246373715,1467.69242103728,1467.77228383452,1467.852069657,
1467.93179597219,1468.01148020049,1468.09115118671,1468.17081864023,1468.25049829105,
1468.33020587345,1468.41000110252,1468.48984544423,1468.56980387128,1468.61219974787,
1468.692157048,1468.77201984524,1468.85180566772,1468.93153198291,1469.01121621121,
1469.09088719743,1469.17055465095,1469.25023430177,1469.32994188416,1469.40973711324,
1469.48958145495,1469.56953988199,1469.61193575859,1469.69189305872,1469.77175585596,
1469.85154167844,1469.93126799363,1470.01095222192,1470.09062320815,1470.17029066167,
1470.24997031249,1470.32967789488,1470.40947312396,1470.48931746567,1470.56927589271,
1470.61167176931,1470.69058006137,1470.76939294258,1470.84811543483,1470.92678681762,
1471.00542362705,1471.08404237083,1471.16268499734,1471.24133829156,1471.32005872964,
1471.38421697355),.UNSPECIFIED.);
#1363=B_SPLINE_CURVE_WITH_KNOTS('',3,(#161332,#161333,#161334,#161335,#161336,
#161337,#161338,#161339,#161340,#161341,#161342),.UNSPECIFIED.,.F.,.F.,
(4,1,1,1,1,1,1,1,4),(1471.38421697355,1471.61140778003,1472.61114379075,
1473.61087980147,1474.61061581219,1475.61035182291,1476.61008783363,1477.60982384435,
1477.66740228073),.UNSPECIFIED.);
#1364=B_SPLINE_CURVE_WITH_KNOTS('',3,(#161344,#161345,#161346,#161347,#161348,
#161349,#161350,#161351,#161352,#161353,#161354,#161355,#161356,#161357,
#161358,#161359,#161360,#161361,#161362,#161363,#161364,#161365,#161366,
#161367,#161368,#161369,#161370,#161371,#161372,#161373,#161374,#161375,
#161376,#161377,#161378,#161379,#161380,#161381,#161382,#161383,#161384,
#161385,#161386,#161387,#161388,#161389,#161390,#161391,#161392,#161393,
#161394,#161395,#161396,#161397,#161398,#161399,#161400,#161401,#161402,
#161403,#161404,#161405,#161406,#161407,#161408,#161409,#161410,#161411,
#161412,#161413,#161414,#161415,#161416,#161417,#161418,#161419,#161420,
#161421,#161422,#161423,#161424,#161425,#161426,#161427,#161428,#161429,
#161430,#161431,#161432,#161433,#161434,#161435,#161436,#161437,#161438,
#161439,#161440,#161441,#161442,#161443,#161444,#161445,#161446,#161447,
#161448,#161449,#161450,#161451,#161452,#161453,#161454,#161455,#161456,
#161457,#161458,#161459,#161460,#161461,#161462,#161463,#161464,#161465,
#161466,#161467,#161468,#161469,#161470,#161471,#161472,#161473,#161474,
#161475,#161476,#161477,#161478,#161479,#161480,#161481,#161482,#161483,
#161484,#161485,#161486,#161487,#161488,#161489,#161490,#161491,#161492,
#161493,#161494,#161495,#161496,#161497,#161498,#161499,#161500,#161501,
#161502,#161503,#161504,#161505,#161506,#161507,#161508,#161509,#161510,
#161511,#161512,#161513,#161514,#161515,#161516,#161517,#161518,#161519,
#161520,#161521,#161522,#161523,#161524,#161525,#161526,#161527,#161528,
#161529,#161530,#161531,#161532,#161533,#161534,#161535,#161536,#161537,
#161538,#161539,#161540,#161541,#161542,#161543,#161544,#161545,#161546,
#161547,#161548,#161549,#161550,#161551,#161552,#161553,#161554,#161555,
#161556,#161557,#161558,#161559,#161560,#161561,#161562,#161563,#161564,
#161565,#161566,#161567,#161568,#161569,#161570,#161571,#161572,#161573,
#161574,#161575,#161576,#161577,#161578,#161579,#161580,#161581,#161582,
#161583,#161584,#161585,#161586,#161587),.UNSPECIFIED.,.F.,.F.,(4,3,3,3,
3,3,3,3,3,3,3,3,3,3,3,3,3,3,3,3,3,3,3,3,3,3,3,3,3,3,3,3,3,3,3,3,3,3,3,3,
3,3,3,3,3,3,3,3,3,3,3,3,3,3,3,3,3,3,3,3,3,3,3,3,3,3,3,3,3,3,3,3,3,3,3,3,
3,3,3,3,3,4),(1477.66740228073,1477.74665738145,1477.82582165558,1477.90491321944,
1477.98395012394,1478.06295794255,1478.14195194843,1478.22094840445,1478.29996357275,
1478.37906049634,1478.45819925348,1478.53745897297,1478.60955985507,1478.6895171552,
1478.76937995244,1478.84916577492,1478.92889209011,1479.00857631841,1479.08824730463,
1479.16791475815,1479.24759440897,1479.32730199136,1479.40709722044,1479.48694156215,
1479.5668999892,1479.60929586579,1479.68925316592,1479.76911596316,1479.84890178564,
1479.92862810083,1480.00831232913,1480.08798331535,1480.16765076887,1480.24733041969,
1480.32703800208,1480.40683323116,1480.48667757287,1480.56663599991,1480.60903187651,
1480.68898917664,1480.76885197388,1480.84863779636,1480.92836411155,1481.00804833985,
1481.08771932607,1481.16738677959,1481.24706643041,1481.3267740128,1481.40656924188,
1481.48641358358,1481.56637201063,1481.60876788723,1481.68872518736,1481.7685879846,
1481.84837380708,1481.92810012227,1482.00778435057,1482.08745533679,1482.16712279031,
1482.24680244113,1482.32651002352,1482.4063052526,1482.48614959431,1482.56610802135,
1482.60850389795,1482.68846119808,1482.76832399532,1482.8481098178,1482.92783613299,
1483.00752036128,1483.0871913475,1483.16685880103,1483.24653845185,1483.32624603424,
1483.40604126332,1483.48588560502,1483.56584403207,1483.60823990867,1483.70138884274,
1483.79416232008,1483.8862079791,1483.9505875878),.UNSPECIFIED.);
#1365=B_SPLINE_CURVE_WITH_KNOTS('',3,(#161589,#161590,#161591,#161592,#161593,
#161594,#161595,#161596,#161597,#161598,#161599,#161600,#161601,#161602,
#161603,#161604,#161605,#161606,#161607,#161608,#161609,#161610,#161611,
#161612,#161613,#161614,#161615,#161616,#161617,#161618,#161619,#161620,
#161621,#161622,#161623,#161624,#161625,#161626,#161627,#161628,#161629,
#161630,#161631,#161632,#161633,#161634,#161635,#161636,#161637,#161638,
#161639,#161640,#161641,#161642,#161643,#161644,#161645,#161646,#161647,
#161648,#161649,#161650,#161651,#161652,#161653,#161654,#161655,#161656,
#161657,#161658,#161659,#161660,#161661,#161662,#161663,#161664,#161665,
#161666,#161667,#161668,#161669,#161670,#161671,#161672,#161673,#161674,
#161675,#161676,#161677,#161678,#161679,#161680,#161681,#161682,#161683,
#161684,#161685,#161686,#161687,#161688,#161689,#161690,#161691,#161692,
#161693,#161694,#161695,#161696,#161697,#161698,#161699,#161700,#161701,
#161702,#161703,#161704,#161705,#161706,#161707,#161708,#161709,#161710,
#161711,#161712,#161713,#161714,#161715,#161716,#161717,#161718,#161719,
#161720,#161721,#161722,#161723,#161724,#161725,#161726,#161727,#161728,
#161729,#161730,#161731,#161732,#161733,#161734,#161735,#161736,#161737,
#161738,#161739,#161740,#161741,#161742,#161743,#161744,#161745,#161746,
#161747,#161748,#161749,#161750,#161751,#161752,#161753,#161754,#161755,
#161756,#161757,#161758,#161759,#161760,#161761,#161762,#161763,#161764,
#161765,#161766,#161767,#161768,#161769,#161770,#161771,#161772,#161773,
#161774,#161775,#161776,#161777,#161778,#161779,#161780,#161781,#161782,
#161783,#161784,#161785,#161786,#161787,#161788,#161789,#161790,#161791,
#161792,#161793,#161794,#161795,#161796,#161797,#161798,#161799,#161800,
#161801,#161802,#161803,#161804,#161805,#161806,#161807,#161808,#161809,
#161810,#161811,#161812,#161813,#161814,#161815,#161816,#161817,#161818,
#161819,#161820,#161821,#161822,#161823,#161824,#161825,#161826,#161827,
#161828,#161829,#161830,#161831,#161832,#161833,#161834,#161835),
 .UNSPECIFIED.,.F.,.F.,(4,3,3,3,3,3,3,3,3,3,3,3,3,3,3,3,3,3,3,3,3,3,3,3,
3,3,3,3,3,3,3,3,3,3,3,3,3,3,3,3,3,3,3,3,3,3,3,3,3,3,3,3,3,3,3,3,3,3,3,3,
3,3,3,3,3,3,3,3,3,3,3,3,3,3,3,3,3,3,3,3,3,3,4),(1483.95058758791,1484.03276112934,
1484.11249874285,1484.19224360271,1484.27201130001,1484.35600245486,1484.43590835349,
1484.5158731071,1484.59594982076,1484.60797591939,1484.68793321952,1484.76779601676,
1484.84758183924,1484.92730815443,1485.00699238273,1485.08666336895,1485.16633082247,
1485.24601047329,1485.32571805569,1485.40551328476,1485.48535762647,1485.56531605352,
1485.60771193011,1485.68766923024,1485.76753202748,1485.84731784996,1485.92704416515,
1486.00672839345,1486.08639937967,1486.16606683319,1486.24574648401,1486.3254540664,
1486.40524929548,1486.48509363719,1486.56505206424,1486.60744794083,1486.68740524096,
1486.7672680382,1486.84705386067,1486.92678017587,1487.00646440416,1487.08613539038,
1487.16580284391,1487.24548249473,1487.32519007712,1487.40498530619,1487.4848296479,
1487.56478807495,1487.60718395155,1487.68714125168,1487.76700404892,1487.8467898714,
1487.92651618659,1488.00620041488,1488.08587140111,1488.16553885463,1488.24521850545,
1488.32492608784,1488.40472131692,1488.48456565863,1488.56452408567,1488.60691996227,
1488.6868772624,1488.76674005964,1488.84652588211,1488.92625219731,1489.0059364256,
1489.08560741182,1489.16527486535,1489.24495451617,1489.32466209856,1489.40445732764,
1489.48430166934,1489.56426009639,1489.60665597299,1489.68722612258,1489.7676985561,
1489.84808846144,1489.92841097225,1490.00867685395,1490.08890876417,1490.16913181602,
1490.23377289509),.UNSPECIFIED.);
#1366=B_SPLINE_CURVE_WITH_KNOTS('',3,(#161837,#161838,#161839,#161840,#161841,
#161842,#161843,#161844,#161845,#161846),.UNSPECIFIED.,.F.,.F.,(4,1,1,1,
1,1,1,4),(1490.233780566,1490.60639198371,1491.60612799443,1492.60586400515,
1493.60560001587,1494.60533602659,1495.60507203731,1496.5169494552),
 .UNSPECIFIED.);
#1367=B_SPLINE_CURVE_WITH_KNOTS('',3,(#161848,#161849,#161850,#161851,#161852,
#161853,#161854,#161855,#161856,#161857,#161858,#161859,#161860,#161861,
#161862,#161863,#161864,#161865,#161866,#161867,#161868,#161869,#161870,
#161871,#161872,#161873,#161874,#161875,#161876,#161877,#161878,#161879,
#161880,#161881,#161882,#161883,#161884,#161885,#161886,#161887,#161888,
#161889,#161890,#161891,#161892,#161893,#161894,#161895,#161896,#161897,
#161898,#161899,#161900,#161901,#161902,#161903,#161904,#161905,#161906,
#161907,#161908,#161909,#161910,#161911,#161912,#161913,#161914,#161915,
#161916,#161917,#161918,#161919,#161920,#161921,#161922,#161923,#161924,
#161925,#161926,#161927,#161928,#161929,#161930,#161931,#161932,#161933,
#161934,#161935,#161936,#161937,#161938,#161939,#161940,#161941,#161942,
#161943,#161944,#161945,#161946,#161947,#161948,#161949,#161950,#161951,
#161952,#161953,#161954,#161955,#161956,#161957,#161958,#161959,#161960,
#161961,#161962,#161963,#161964,#161965,#161966,#161967,#161968,#161969,
#161970,#161971,#161972,#161973,#161974,#161975,#161976,#161977,#161978,
#161979,#161980,#161981,#161982,#161983,#161984,#161985,#161986,#161987,
#161988,#161989,#161990,#161991,#161992,#161993,#161994,#161995,#161996,
#161997,#161998,#161999,#162000,#162001,#162002,#162003,#162004,#162005,
#162006,#162007,#162008,#162009,#162010,#162011,#162012,#162013,#162014,
#162015,#162016,#162017,#162018,#162019,#162020,#162021,#162022,#162023,
#162024,#162025,#162026,#162027,#162028,#162029,#162030,#162031,#162032,
#162033,#162034,#162035,#162036,#162037,#162038,#162039,#162040,#162041,
#162042,#162043,#162044,#162045,#162046,#162047,#162048,#162049,#162050,
#162051,#162052,#162053,#162054,#162055,#162056,#162057,#162058,#162059,
#162060,#162061,#162062,#162063,#162064,#162065,#162066,#162067,#162068,
#162069,#162070,#162071,#162072,#162073,#162074,#162075,#162076,#162077,
#162078,#162079,#162080,#162081,#162082,#162083,#162084,#162085,#162086,
#162087,#162088,#162089,#162090,#162091),.UNSPECIFIED.,.F.,.F.,(4,3,3,3,
3,3,3,3,3,3,3,3,3,3,3,3,3,3,3,3,3,3,3,3,3,3,3,3,3,3,3,3,3,3,3,3,3,3,3,3,
3,3,3,3,3,3,3,3,3,3,3,3,3,3,3,3,3,3,3,3,3,3,3,3,3,3,3,3,3,3,3,3,3,3,3,3,
3,3,3,3,3,4),(1496.51695820227,1496.60480804803,1496.68476534816,1496.7646281454,
1496.84441396788,1496.92414028307,1497.00382451137,1497.08349549759,1497.16316295111,
1497.24284260193,1497.32255018433,1497.4023454134,1497.48218975511,1497.56214818216,
1497.60454405875,1497.68450135888,1497.76436415612,1497.8441499786,1497.92387629379,
1498.00356052209,1498.08323150831,1498.16289896183,1498.24257861265,1498.32228619504,
1498.40208142412,1498.48192576583,1498.56188419287,1498.60428006947,1498.6842373696,
1498.76410016684,1498.84388598932,1498.92361230451,1499.00329653281,1499.08296751903,
1499.16263497255,1499.24231462337,1499.32202220576,1499.40181743484,1499.48166177655,
1499.56162020359,1499.60401608019,1499.68397338032,1499.76383617756,1499.84362200004,
1499.92334831523,1500.00303254352,1500.08270352975,1500.16237098327,1500.24205063409,
1500.32175821648,1500.40155344556,1500.48139778726,1500.56135621431,1500.60375209091,
1500.68370939104,1500.76357218828,1500.84335801076,1500.92308432595,1501.00276855425,
1501.08243954047,1501.16210699399,1501.24178664481,1501.3214942272,1501.40128945628,
1501.48113379799,1501.56109222503,1501.60348810163,1501.68344540176,1501.763308199,
1501.84309402147,1501.92282033667,1502.00250456496,1502.08217555118,1502.16184300471,
1502.24152265552,1502.32123023792,1502.40102546699,1502.4808698087,1502.56082823575,
1502.60322411235,1502.71891210661,1502.80014350945),.UNSPECIFIED.);
#1368=B_SPLINE_CURVE_WITH_KNOTS('',3,(#162093,#162094,#162095,#162096,#162097,
#162098,#162099,#162100,#162101,#162102),.UNSPECIFIED.,.F.,.F.,(4,1,1,1,
1,1,1,4),(1502.80014707982,1503.60296012307,1504.60269613379,1505.60243214451,
1506.60216815523,1507.60190416595,1508.60164017667,1509.08332881663),
 .UNSPECIFIED.);
#1369=B_SPLINE_CURVE_WITH_KNOTS('',3,(#162104,#162105,#162106,#162107,#162108,
#162109,#162110,#162111,#162112,#162113),.UNSPECIFIED.,.F.,.F.,(4,1,1,1,
1,1,1,4),(1509.08332881663,1509.60137618739,1510.60111219811,1511.60084820883,
1512.60058421955,1513.60032023027,1514.60005624099,1515.36651412381),
 .UNSPECIFIED.);
#1370=B_SPLINE_CURVE_WITH_KNOTS('',3,(#162115,#162116,#162117,#162118,#162119,
#162120,#162121,#162122,#162123,#162124,#162125,#162126),.UNSPECIFIED.,
 .F.,.F.,(4,2,1,1,1,1,1,1,4),(1515.36651412381,1515.59979225171,1516.59952826244,
1517.59926427316,1518.59900028388,1519.5987362946,1520.59847230532,1521.59820831604,
1521.64969943099),.UNSPECIFIED.);
#1371=B_SPLINE_CURVE_WITH_KNOTS('',3,(#162128,#162129,#162130,#162131,#162132,
#162133,#162134,#162135,#162136,#162137),.UNSPECIFIED.,.F.,.F.,(4,1,1,1,
1,1,1,4),(1521.64969943099,1522.59794432676,1523.59768033748,1524.5974163482,
1525.59715235892,1526.59688836964,1527.59662438036,1527.93287724226),
 .UNSPECIFIED.);
#1372=B_SPLINE_CURVE_WITH_KNOTS('',3,(#162139,#162140,#162141,#162142,#162143,
#162144,#162145,#162146,#162147,#162148,#162149,#162150,#162151,#162152,
#162153,#162154,#162155,#162156,#162157,#162158,#162159,#162160,#162161,
#162162,#162163,#162164,#162165,#162166,#162167,#162168,#162169,#162170,
#162171,#162172,#162173,#162174,#162175,#162176,#162177,#162178,#162179,
#162180,#162181,#162182,#162183,#162184,#162185,#162186,#162187,#162188,
#162189,#162190,#162191,#162192,#162193,#162194,#162195,#162196,#162197,
#162198,#162199,#162200,#162201,#162202,#162203,#162204,#162205,#162206,
#162207,#162208,#162209,#162210,#162211,#162212,#162213,#162214,#162215,
#162216,#162217,#162218,#162219,#162220,#162221,#162222,#162223,#162224,
#162225,#162226,#162227,#162228,#162229,#162230,#162231,#162232,#162233,
#162234,#162235,#162236,#162237,#162238,#162239,#162240,#162241,#162242,
#162243,#162244,#162245,#162246,#162247,#162248,#162249,#162250,#162251,
#162252,#162253,#162254,#162255,#162256,#162257,#162258,#162259,#162260,
#162261,#162262,#162263,#162264,#162265,#162266,#162267,#162268,#162269,
#162270,#162271,#162272,#162273,#162274,#162275,#162276,#162277,#162278,
#162279,#162280,#162281,#162282,#162283,#162284,#162285,#162286,#162287,
#162288,#162289,#162290,#162291,#162292,#162293,#162294,#162295,#162296,
#162297,#162298,#162299,#162300,#162301,#162302,#162303,#162304,#162305,
#162306,#162307,#162308,#162309,#162310,#162311,#162312,#162313,#162314,
#162315,#162316,#162317,#162318,#162319,#162320,#162321,#162322,#162323,
#162324,#162325,#162326,#162327,#162328,#162329,#162330,#162331,#162332,
#162333,#162334,#162335,#162336,#162337,#162338,#162339,#162340,#162341,
#162342,#162343,#162344,#162345,#162346,#162347,#162348,#162349,#162350,
#162351,#162352,#162353,#162354,#162355,#162356,#162357,#162358,#162359,
#162360,#162361,#162362,#162363,#162364,#162365,#162366,#162367,#162368,
#162369,#162370,#162371,#162372,#162373,#162374,#162375,#162376,#162377,
#162378,#162379,#162380,#162381,#162382,#162383,#162384,#162385),
 .UNSPECIFIED.,.F.,.F.,(4,3,3,3,3,3,3,3,3,3,3,3,3,3,3,3,3,3,3,3,3,3,3,3,
3,3,3,3,3,3,3,3,3,3,3,3,3,3,3,3,3,3,3,3,3,3,3,3,3,3,3,3,3,3,3,3,3,3,3,3,
3,3,3,3,3,3,3,3,3,3,3,3,3,3,3,3,3,3,3,3,3,3,4),(1527.93288473817,1528.01581919478,
1528.09546894363,1528.17512364067,1528.25479896718,1528.33451061385,1528.41431779342,
1528.49418137679,1528.57415894196,1528.59636039108,1528.67631769121,1528.75618048845,
1528.83596631093,1528.91569262612,1528.99537685441,1529.07504784064,1529.15471529416,
1529.23439494498,1529.31410252737,1529.39389775645,1529.47374209815,1529.5537005252,
1529.5960964018,1529.67605370193,1529.75591649917,1529.83570232165,1529.91542863684,
1529.99511286513,1530.07478385136,1530.15445130488,1530.2341309557,1530.31383853809,
1530.39363376717,1530.47347810887,1530.55343653592,1530.59583241252,1530.67578971265,
1530.75565250989,1530.83543833237,1530.91516464756,1530.99484887586,1531.07451986208,
1531.1541873156,1531.23386696642,1531.31357454882,1531.39336977789,1531.4732141196,
1531.55317254665,1531.59556842324,1531.67552572337,1531.75538852061,1531.83517434309,
1531.91490065828,1531.99458488658,1532.0742558728,1532.15392332632,1532.23360297714,
1532.31331055953,1532.39310578861,1532.47295013032,1532.55290855736,1532.59530443396,
1532.67526173409,1532.75512453133,1532.83491035381,1532.914636669,1532.9943208973,
1533.07399188352,1533.15365933704,1533.23333898786,1533.31304657025,1533.39284179933,
1533.47268614104,1533.55264456808,1533.59504044468,1533.67572883148,1533.75631844907,
1533.83682434353,1533.91726150585,1533.99763925535,1534.07798168726,1534.15831132183,
1534.21607004535),.UNSPECIFIED.);
#1373=B_SPLINE_CURVE_WITH_KNOTS('',3,(#162387,#162388,#162389,#162390,#162391,
#162392,#162393,#162394,#162395,#162396),.UNSPECIFIED.,.F.,.F.,(4,1,1,1,
1,1,1,4),(1534.21607763161,1534.5947764554,1535.59451246612,1536.59424847684,
1537.59398448756,1538.59372049828,1539.593456509,1540.49924633286),
 .UNSPECIFIED.);
#1374=B_SPLINE_CURVE_WITH_KNOTS('',3,(#162398,#162399,#162400,#162401,#162402,
#162403,#162404,#162405,#162406,#162407,#162408,#162409,#162410,#162411,
#162412,#162413,#162414,#162415,#162416,#162417,#162418,#162419,#162420,
#162421,#162422,#162423,#162424,#162425,#162426,#162427,#162428,#162429,
#162430,#162431,#162432,#162433,#162434,#162435,#162436,#162437,#162438,
#162439,#162440,#162441,#162442,#162443,#162444,#162445,#162446,#162447,
#162448,#162449,#162450,#162451,#162452,#162453,#162454,#162455,#162456,
#162457,#162458,#162459,#162460,#162461,#162462,#162463,#162464,#162465,
#162466,#162467,#162468,#162469,#162470,#162471,#162472,#162473,#162474,
#162475,#162476,#162477,#162478,#162479,#162480,#162481,#162482,#162483,
#162484,#162485,#162486,#162487,#162488,#162489,#162490,#162491,#162492,
#162493,#162494,#162495,#162496,#162497,#162498,#162499,#162500,#162501,
#162502,#162503,#162504,#162505,#162506,#162507,#162508,#162509,#162510,
#162511,#162512,#162513,#162514,#162515,#162516,#162517,#162518,#162519,
#162520,#162521,#162522,#162523,#162524,#162525,#162526,#162527,#162528,
#162529,#162530,#162531,#162532,#162533,#162534,#162535,#162536,#162537,
#162538,#162539,#162540,#162541,#162542,#162543,#162544,#162545,#162546,
#162547,#162548,#162549,#162550,#162551,#162552,#162553,#162554,#162555,
#162556,#162557,#162558,#162559,#162560,#162561,#162562,#162563,#162564,
#162565,#162566,#162567,#162568,#162569,#162570,#162571,#162572,#162573,
#162574,#162575,#162576,#162577,#162578,#162579,#162580,#162581,#162582,
#162583,#162584,#162585,#162586,#162587,#162588,#162589,#162590,#162591,
#162592,#162593,#162594,#162595,#162596,#162597,#162598,#162599,#162600,
#162601,#162602,#162603,#162604,#162605,#162606,#162607,#162608,#162609,
#162610,#162611,#162612,#162613,#162614,#162615,#162616,#162617,#162618,
#162619,#162620,#162621,#162622,#162623,#162624,#162625,#162626,#162627,
#162628,#162629,#162630,#162631,#162632,#162633,#162634,#162635,#162636,
#162637,#162638,#162639,#162640,#162641),.UNSPECIFIED.,.F.,.F.,(4,3,3,3,
3,3,3,3,3,3,3,3,3,3,3,3,3,3,3,3,3,3,3,3,3,3,3,3,3,3,3,3,3,3,3,3,3,3,3,3,
3,3,3,3,3,3,3,3,3,3,3,3,3,3,3,3,3,3,3,3,3,3,3,3,3,3,3,3,3,3,3,3,3,3,3,3,
3,3,3,3,3,4),(1540.49925535253,1540.59319251972,1540.67314981985,1540.75301261709,
1540.83279843957,1540.91252475476,1540.99220898306,1541.07187996928,1541.1515474228,
1541.23122707362,1541.31093465601,1541.39072988509,1541.4705742268,1541.55053265384,
1541.59292853044,1541.67288583057,1541.75274862781,1541.83253445029,1541.91226076548,
1541.99194499378,1542.07161598,1542.15128343352,1542.23096308434,1542.31067066673,
1542.39046589581,1542.47031023752,1542.55026866456,1542.59266454116,1542.67262184129,
1542.75248463853,1542.83227046101,1542.9119967762,1542.9916810045,1543.07135199072,
1543.15101944424,1543.23069909506,1543.31040667745,1543.39020190653,1543.47004624824,
1543.55000467528,1543.59240055188,1543.67235785201,1543.75222064925,1543.83200647173,
1543.91173278692,1543.99141701522,1544.07108800144,1544.15075545496,1544.23043510578,
1544.31014268817,1544.38993791725,1544.46978225896,1544.549740686,1544.5921365626,
1544.67209386273,1544.75195665997,1544.83174248245,1544.91146879764,1544.99115302593,
1545.07082401216,1545.15049146568,1545.2301711165,1545.30987869889,1545.38967392797,
1545.46951826968,1545.54947669672,1545.59187257332,1545.67182987345,1545.75169267069,
1545.83147849316,1545.91120480836,1545.99088903665,1546.07056002287,1546.1502274764,
1546.22990712722,1546.30961470961,1546.38940993869,1546.46925428039,1546.54921270744,
1546.59160858404,1546.70921964393,1546.78244065971),.UNSPECIFIED.);
#1375=B_SPLINE_CURVE_WITH_KNOTS('',3,(#162643,#162644,#162645,#162646,#162647,
#162648,#162649,#162650,#162651,#162652),.UNSPECIFIED.,.F.,.F.,(4,1,1,1,
1,1,1,4),(1546.78244481203,1547.59134459476,1548.59108060548,1549.5908166162,
1550.59055262692,1551.59028863764,1552.59002464836,1553.06562596689),
 .UNSPECIFIED.);
#1376=B_SPLINE_CURVE_WITH_KNOTS('',3,(#162654,#162655,#162656,#162657,#162658,
#162659,#162660,#162661,#162662,#162663),.UNSPECIFIED.,.F.,.F.,(4,1,1,1,
1,1,1,4),(1553.06562596689,1553.58976065908,1554.5894966698,1555.58923268052,
1556.58896869124,1557.58870470196,1558.58844071268,1559.34881127407),
 .UNSPECIFIED.);
#1377=B_SPLINE_CURVE_WITH_KNOTS('',3,(#162665,#162666,#162667,#162668,#162669,
#162670,#162671,#162672,#162673,#162674,#162675,#162676),.UNSPECIFIED.,
 .F.,.F.,(4,2,1,1,1,1,1,1,4),(1559.34881127407,1559.5881767234,1560.58791273412,
1561.58764874484,1562.58738475556,1563.58712076628,1564.586856777,1565.58659278772,
1565.63199658125),.UNSPECIFIED.);
#1378=B_SPLINE_CURVE_WITH_KNOTS('',3,(#162678,#162679,#162680,#162681,#162682,
#162683,#162684,#162685,#162686,#162687),.UNSPECIFIED.,.F.,.F.,(4,1,1,1,
1,1,1,4),(1565.63199658125,1566.58632879844,1567.58606480916,1568.58580081988,
1569.5855368306,1570.58527284132,1571.58500885204,1571.9151745794),
 .UNSPECIFIED.);
#1379=B_SPLINE_CURVE_WITH_KNOTS('',3,(#162689,#162690,#162691,#162692,#162693,
#162694,#162695,#162696,#162697,#162698,#162699,#162700,#162701,#162702,
#162703,#162704,#162705,#162706,#162707,#162708,#162709,#162710,#162711,
#162712,#162713,#162714,#162715,#162716,#162717,#162718,#162719,#162720,
#162721,#162722,#162723,#162724,#162725,#162726,#162727,#162728,#162729,
#162730,#162731,#162732,#162733,#162734,#162735,#162736,#162737,#162738,
#162739,#162740,#162741,#162742,#162743,#162744,#162745,#162746,#162747,
#162748,#162749,#162750,#162751,#162752,#162753,#162754,#162755,#162756,
#162757,#162758,#162759,#162760,#162761,#162762,#162763,#162764,#162765,
#162766,#162767,#162768,#162769,#162770,#162771,#162772,#162773,#162774,
#162775,#162776,#162777,#162778,#162779,#162780,#162781,#162782,#162783,
#162784,#162785,#162786,#162787,#162788,#162789,#162790,#162791,#162792,
#162793,#162794,#162795,#162796,#162797,#162798,#162799,#162800,#162801,
#162802,#162803,#162804,#162805,#162806,#162807,#162808,#162809,#162810,
#162811,#162812,#162813,#162814,#162815,#162816,#162817,#162818,#162819,
#162820,#162821,#162822,#162823,#162824,#162825,#162826,#162827,#162828,
#162829,#162830,#162831,#162832,#162833,#162834,#162835,#162836,#162837,
#162838,#162839,#162840,#162841,#162842,#162843,#162844,#162845,#162846,
#162847,#162848,#162849,#162850,#162851,#162852,#162853,#162854,#162855,
#162856,#162857,#162858,#162859,#162860,#162861,#162862,#162863,#162864,
#162865,#162866,#162867,#162868,#162869,#162870,#162871,#162872,#162873,
#162874,#162875,#162876,#162877,#162878,#162879,#162880,#162881,#162882,
#162883,#162884,#162885,#162886,#162887,#162888,#162889,#162890,#162891,
#162892,#162893,#162894,#162895,#162896,#162897,#162898,#162899,#162900,
#162901,#162902,#162903,#162904,#162905,#162906,#162907,#162908,#162909,
#162910,#162911,#162912,#162913,#162914,#162915,#162916,#162917,#162918,
#162919,#162920,#162921,#162922,#162923,#162924,#162925,#162926,#162927,
#162928,#162929,#162930,#162931,#162932,#162933,#162934,#162935),
 .UNSPECIFIED.,.F.,.F.,(4,3,3,3,3,3,3,3,3,3,3,3,3,3,3,3,3,3,3,3,3,3,3,3,
3,3,3,3,3,3,3,3,3,3,3,3,3,3,3,3,3,3,3,3,3,3,3,3,3,3,3,3,3,3,3,3,3,3,3,3,
3,3,3,3,3,3,3,3,3,3,3,3,3,3,3,3,3,3,3,3,3,3,4),(1571.91518188843,1571.99887726022,
1572.07844285309,1572.1580111645,1572.23759795907,1572.31721900964,1572.39693410193,
1572.47670391825,1572.55658863134,1572.58474486276,1572.66470216289,1572.74456496014,
1572.82435078261,1572.9040770978,1572.9837613261,1573.06343231232,1573.14309976585,
1573.22277941667,1573.30248699906,1573.38228222814,1573.46212656985,1573.5420849969,
1573.58448087348,1573.66443817361,1573.74430097085,1573.82408679333,1573.90381310852,
1573.98349733682,1574.06316832304,1574.14283577656,1574.22251542738,1574.30222300978,
1574.38201823885,1574.46186258056,1574.54182100761,1574.5842168842,1574.66417418433,
1574.74403698157,1574.82382280404,1574.90354911924,1574.98323334753,1575.06290433375,
1575.14257178728,1575.2222514381,1575.30195902049,1575.38175424957,1575.46159859127,
1575.54155701832,1575.58395289492,1575.66391019505,1575.74377299229,1575.82355881477,
1575.90328512996,1575.98296935825,1576.06264034448,1576.142307798,1576.22198744882,
1576.30169503121,1576.38149026029,1576.461334602,1576.54129302904,1576.58368890564,
1576.66364620577,1576.74350900301,1576.82329482548,1576.90302114068,1576.98270536897,
1577.06237635519,1577.14204380872,1577.22172345953,1577.30143104193,1577.381226271,
1577.46107061271,1577.54102903976,1577.58342491636,1577.66423586784,1577.74494693697,
1577.82557301612,1577.90612894158,1577.98662258522,1578.06707947055,1578.1475196518,
1578.19836719561),.UNSPECIFIED.);
#1380=B_SPLINE_CURVE_WITH_KNOTS('',3,(#162937,#162938,#162939,#162940,#162941,
#162942,#162943,#162944,#162945,#162946),.UNSPECIFIED.,.F.,.F.,(4,1,1,1,
1,1,1,4),(1578.19837466001,1578.58316092708,1579.5828969378,1580.58263294852,
1581.58236895924,1582.58210496996,1583.58184098068,1584.4815434095),
 .UNSPECIFIED.);
#1381=B_SPLINE_CURVE_WITH_KNOTS('',3,(#162948,#162949,#162950,#162951,#162952,
#162953,#162954,#162955,#162956,#162957,#162958,#162959,#162960,#162961,
#162962,#162963,#162964,#162965,#162966,#162967,#162968,#162969,#162970,
#162971,#162972,#162973,#162974,#162975,#162976,#162977,#162978,#162979,
#162980,#162981,#162982,#162983,#162984,#162985,#162986,#162987,#162988,
#162989,#162990,#162991,#162992,#162993,#162994,#162995,#162996,#162997,
#162998,#162999,#163000,#163001,#163002,#163003,#163004,#163005,#163006,
#163007,#163008,#163009,#163010,#163011,#163012,#163013,#163014,#163015,
#163016,#163017,#163018,#163019,#163020,#163021,#163022,#163023,#163024,
#163025,#163026,#163027,#163028,#163029,#163030,#163031,#163032,#163033,
#163034,#163035,#163036,#163037,#163038,#163039,#163040,#163041,#163042,
#163043,#163044,#163045,#163046,#163047,#163048,#163049,#163050,#163051,
#163052,#163053,#163054,#163055,#163056,#163057,#163058,#163059,#163060,
#163061,#163062,#163063,#163064,#163065,#163066,#163067,#163068,#163069,
#163070,#163071,#163072,#163073,#163074,#163075,#163076,#163077,#163078,
#163079,#163080,#163081,#163082,#163083,#163084,#163085,#163086,#163087,
#163088,#163089,#163090,#163091,#163092,#163093,#163094,#163095,#163096,
#163097,#163098,#163099,#163100,#163101,#163102,#163103,#163104,#163105,
#163106,#163107,#163108,#163109,#163110,#163111,#163112,#163113,#163114,
#163115,#163116,#163117,#163118,#163119,#163120,#163121,#163122,#163123,
#163124,#163125,#163126,#163127,#163128,#163129,#163130,#163131,#163132,
#163133,#163134,#163135,#163136,#163137,#163138,#163139,#163140,#163141,
#163142,#163143,#163144,#163145,#163146,#163147,#163148,#163149,#163150,
#163151,#163152,#163153,#163154,#163155,#163156,#163157,#163158,#163159,
#163160,#163161,#163162,#163163,#163164,#163165,#163166,#163167,#163168,
#163169,#163170,#163171,#163172,#163173,#163174,#163175,#163176,#163177,
#163178,#163179,#163180,#163181,#163182,#163183,#163184,#163185,#163186,
#163187,#163188,#163189,#163190,#163191),.UNSPECIFIED.,.F.,.F.,(4,3,3,3,
3,3,3,3,3,3,3,3,3,3,3,3,3,3,3,3,3,3,3,3,3,3,3,3,3,3,3,3,3,3,3,3,3,3,3,3,
3,3,3,3,3,3,3,3,3,3,3,3,3,3,3,3,3,3,3,3,3,3,3,3,3,3,3,3,3,3,3,3,3,3,3,3,
3,3,3,3,3,4),(1584.48155250279,1584.5815769914,1584.66153429153,1584.74139708877,
1584.82118291125,1584.90090922644,1584.98059345474,1585.06026444096,1585.13993189449,
1585.2196115453,1585.2993191277,1585.37911435677,1585.45895869848,1585.53891712553,
1585.58131300212,1585.66127030225,1585.74113309949,1585.82091892197,1585.90064523716,
1585.98032946546,1586.06000045168,1586.1396679052,1586.21934755602,1586.29905513841,
1586.37885036749,1586.4586947092,1586.53865313624,1586.58104901284,1586.66100631297,
1586.74086911021,1586.82065493269,1586.90038124788,1586.98006547618,1587.0597364624,
1587.13940391592,1587.21908356674,1587.29879114913,1587.37858637821,1587.45843071992,
1587.53838914696,1587.58078502356,1587.66074232369,1587.74060512093,1587.82039094341,
1587.9001172586,1587.97980148689,1588.05947247312,1588.13913992664,1588.21881957746,
1588.29852715985,1588.37832238893,1588.45816673064,1588.53812515768,1588.58052103428,
1588.66047833441,1588.74034113165,1588.82012695413,1588.89985326932,1588.97953749762,
1589.05920848384,1589.13887593736,1589.21855558818,1589.29826317057,1589.37805839965,
1589.45790274136,1589.5378611684,1589.580257045,1589.66021434513,1589.74007714237,
1589.81986296484,1589.89958928003,1589.97927350833,1590.05894449455,1590.13861194807,
1590.21829159889,1590.29799918128,1590.37779441035,1590.45763875206,1590.53759717911,
1590.57999305572,1590.69969193202,1590.76473780997),.UNSPECIFIED.);
#1382=B_SPLINE_CURVE_WITH_KNOTS('',3,(#163193,#163194,#163195,#163196,#163197,
#163198,#163199,#163200,#163201,#163202),.UNSPECIFIED.,.F.,.F.,(4,1,1,1,
1,1,1,4),(1590.7647425272,1591.57972906644,1592.57946507717,1593.57920108788,
1594.57893709861,1595.57867310933,1596.57840912005,1597.04792311715),
 .UNSPECIFIED.);
#1383=B_SPLINE_CURVE_WITH_KNOTS('',3,(#163204,#163205,#163206,#163207,#163208,
#163209,#163210,#163211,#163212,#163213),.UNSPECIFIED.,.F.,.F.,(4,1,1,1,
1,1,1,4),(1597.04792311715,1597.57814513077,1598.57788114149,1599.57761715221,
1600.57735316293,1601.57708917365,1602.57682518437,1603.33110842433),
 .UNSPECIFIED.);
#1384=B_SPLINE_CURVE_WITH_KNOTS('',3,(#163215,#163216,#163217,#163218,#163219,
#163220,#163221,#163222,#163223,#163224,#163225,#163226,#163227,#163228,
#163229,#163230,#163231,#163232,#163233,#163234,#163235,#163236,#163237,
#163238,#163239,#163240,#163241,#163242,#163243,#163244,#163245,#163246,
#163247,#163248,#163249,#163250,#163251,#163252,#163253,#163254,#163255,
#163256,#163257,#163258,#163259,#163260,#163261,#163262,#163263,#163264,
#163265,#163266,#163267,#163268,#163269,#163270,#163271,#163272,#163273,
#163274,#163275,#163276,#163277,#163278,#163279,#163280,#163281,#163282,
#163283,#163284,#163285,#163286,#163287,#163288,#163289,#163290,#163291,
#163292,#163293,#163294,#163295,#163296,#163297,#163298,#163299,#163300,
#163301,#163302,#163303,#163304,#163305,#163306,#163307,#163308,#163309,
#163310,#163311,#163312,#163313,#163314,#163315,#163316,#163317,#163318,
#163319,#163320,#163321,#163322,#163323,#163324,#163325,#163326,#163327,
#163328,#163329,#163330,#163331,#163332,#163333,#163334,#163335,#163336,
#163337,#163338,#163339,#163340,#163341,#163342,#163343,#163344,#163345,
#163346,#163347,#163348,#163349,#163350,#163351,#163352,#163353,#163354,
#163355,#163356,#163357,#163358,#163359,#163360,#163361,#163362,#163363,
#163364,#163365,#163366,#163367,#163368,#163369,#163370,#163371,#163372,
#163373,#163374,#163375,#163376,#163377,#163378,#163379,#163380,#163381,
#163382,#163383,#163384,#163385,#163386,#163387,#163388,#163389,#163390,
#163391,#163392,#163393,#163394,#163395,#163396,#163397,#163398,#163399,
#163400,#163401,#163402,#163403,#163404,#163405,#163406,#163407,#163408,
#163409,#163410,#163411,#163412,#163413,#163414,#163415,#163416,#163417,
#163418,#163419,#163420,#163421,#163422,#163423,#163424,#163425,#163426,
#163427,#163428,#163429,#163430,#163431,#163432,#163433,#163434,#163435,
#163436,#163437,#163438,#163439,#163440,#163441,#163442,#163443,#163444,
#163445,#163446,#163447,#163448,#163449,#163450,#163451,#163452,#163453,
#163454,#163455,#163456,#163457,#163458,#163459,#163460,#163461),
 .UNSPECIFIED.,.F.,.F.,(4,3,3,3,3,3,3,3,3,3,3,3,3,3,3,3,3,3,3,3,3,3,3,3,
3,3,3,3,3,3,3,3,3,3,3,3,3,3,3,3,3,3,3,3,3,3,3,3,3,3,3,3,3,3,3,3,3,3,3,3,
3,3,3,3,3,3,3,3,3,3,3,3,3,3,3,3,3,3,3,3,3,3,4),(1603.3311085053,1603.43422233826,
1603.53975581896,1603.57656119509,1603.65651849522,1603.73638129247,1603.81616711494,
1603.89589343014,1603.97557765843,1604.05524864465,1604.13491609818,1604.214595749,
1604.29430333139,1604.37409856047,1604.45394290218,1604.53390132923,1604.57629720581,
1604.65625450594,1604.73611730318,1604.81590312566,1604.89562944085,1604.97531366914,
1605.05498465537,1605.13465210889,1605.21433175971,1605.2940393421,1605.37383457118,
1605.45367891289,1605.53363733993,1605.57603321653,1605.65599051666,1605.7358533139,
1605.81563913638,1605.89536545157,1605.97504967986,1606.05472066609,1606.13438811961,
1606.21406777043,1606.29377535282,1606.3735705819,1606.45341492361,1606.53337335065,
1606.57576922725,1606.65572652738,1606.73558932462,1606.8153751471,1606.89510146229,
1606.97478569059,1607.05445667681,1607.13412413033,1607.21380378115,1607.29351136354,
1607.37330659262,1607.45315093433,1607.53310936137,1607.57550523797,1607.6554625381,
1607.73532533534,1607.81511115782,1607.89483747301,1607.97452170131,1608.05419268753,
1608.13386014105,1608.21353979187,1608.29324737426,1608.37304260334,1608.45288694505,
1608.53284537209,1608.57524124869,1608.65519854882,1608.73506134606,1608.81484716853,
1608.89457348373,1608.97425771202,1609.05392869824,1609.13359615177,1609.21327580259,
1609.29298338498,1609.37277861405,1609.45262295576,1609.53258138281,1609.57497725941,
1609.61429373151),.UNSPECIFIED.);
#1385=B_SPLINE_CURVE_WITH_KNOTS('',3,(#163463,#163464,#163465,#163466,#163467,
#163468,#163469,#163470,#163471,#163472),.UNSPECIFIED.,.F.,.F.,(4,1,1,1,
1,1,1,4),(1609.61429912006,1610.57471327013,1611.57444928085,1612.57418529157,
1613.57392130229,1614.57365731301,1615.57339332373,1615.89747903868),
 .UNSPECIFIED.);
#1386=B_SPLINE_CURVE_WITH_KNOTS('',3,(#163474,#163475,#163476,#163477,#163478,
#163479,#163480,#163481,#163482,#163483),.UNSPECIFIED.,.F.,.F.,(4,1,1,1,
1,1,1,4),(1615.89747903868,1616.57312933445,1617.57286534517,1618.57260135589,
1619.57233736661,1620.57207337733,1621.57180938805,1622.18066434587),
 .UNSPECIFIED.);
#1387=B_SPLINE_CURVE_WITH_KNOTS('',3,(#163485,#163486,#163487,#163488,#163489,
#163490,#163491,#163492,#163493,#163494),.UNSPECIFIED.,.F.,.F.,(4,1,1,1,
1,1,1,4),(1622.18066434587,1622.57154539877,1623.57128140949,1624.57101742021,
1625.57075343093,1626.57048944165,1627.57022545237,1628.46384965304),
 .UNSPECIFIED.);
#1388=B_SPLINE_CURVE_WITH_KNOTS('',3,(#163496,#163497,#163498,#163499,#163500,
#163501,#163502,#163503,#163504,#163505,#163506,#163507,#163508),
 .UNSPECIFIED.,.F.,.F.,(4,3,1,1,1,1,1,1,4),(1628.46384965304,1628.56996146309,
1629.56969747381,1630.56943348453,1631.56916949525,1632.56890550597,1633.56864151669,
1634.56837752741,1634.74703496022),.UNSPECIFIED.);
#1389=B_SPLINE_CURVE_WITH_KNOTS('',3,(#163510,#163511,#163512,#163513,#163514,
#163515,#163516,#163517,#163518,#163519,#163520,#163521,#163522,#163523,
#163524,#163525,#163526,#163527,#163528,#163529,#163530,#163531,#163532,
#163533,#163534,#163535,#163536,#163537,#163538,#163539,#163540,#163541,
#163542,#163543,#163544,#163545,#163546,#163547,#163548,#163549,#163550,
#163551,#163552,#163553,#163554,#163555,#163556,#163557,#163558,#163559,
#163560,#163561,#163562,#163563,#163564,#163565,#163566,#163567,#163568,
#163569,#163570,#163571,#163572,#163573,#163574,#163575,#163576,#163577,
#163578,#163579,#163580,#163581,#163582,#163583,#163584,#163585,#163586,
#163587,#163588,#163589,#163590,#163591,#163592,#163593,#163594,#163595,
#163596,#163597,#163598,#163599,#163600,#163601,#163602,#163603,#163604,
#163605,#163606,#163607,#163608,#163609,#163610,#163611,#163612,#163613,
#163614,#163615,#163616,#163617,#163618,#163619,#163620,#163621,#163622,
#163623,#163624,#163625,#163626,#163627,#163628,#163629,#163630,#163631,
#163632,#163633,#163634,#163635,#163636,#163637,#163638,#163639,#163640,
#163641,#163642,#163643,#163644,#163645,#163646,#163647,#163648,#163649,
#163650,#163651,#163652,#163653,#163654,#163655,#163656,#163657,#163658,
#163659,#163660,#163661,#163662,#163663,#163664,#163665,#163666,#163667,
#163668,#163669,#163670,#163671,#163672,#163673,#163674,#163675,#163676,
#163677,#163678,#163679,#163680,#163681,#163682,#163683,#163684,#163685,
#163686,#163687,#163688,#163689,#163690,#163691,#163692,#163693,#163694,
#163695,#163696,#163697,#163698,#163699,#163700,#163701,#163702,#163703,
#163704,#163705,#163706,#163707,#163708,#163709,#163710,#163711,#163712,
#163713,#163714,#163715,#163716,#163717,#163718,#163719,#163720,#163721,
#163722,#163723,#163724,#163725,#163726,#163727,#163728,#163729,#163730,
#163731,#163732,#163733,#163734,#163735,#163736,#163737,#163738,#163739,
#163740,#163741,#163742,#163743,#163744,#163745,#163746,#163747,#163748,
#163749,#163750,#163751,#163752,#163753,#163754,#163755,#163756),
 .UNSPECIFIED.,.F.,.F.,(4,3,3,3,3,3,3,3,3,3,3,3,3,3,3,3,3,3,3,3,3,3,3,3,
3,3,3,3,3,3,3,3,3,3,3,3,3,3,3,3,3,3,3,3,3,3,3,3,3,3,3,3,3,3,3,3,3,3,3,3,
3,3,3,3,3,3,3,3,3,3,3,3,3,3,3,3,3,3,3,3,3,3,4),(1634.74703496022,1634.82567899522,
1634.90425430968,1634.98277929056,1635.06128097298,1635.13977333159,1635.21827293407,
1635.29679635215,1635.37540216393,1635.45405498737,1635.53281728381,1635.56811353813,
1635.64807083826,1635.7279336355,1635.80771945798,1635.88744577317,1635.96713000146,
1636.04680098768,1636.12646844121,1636.20614809203,1636.28585567442,1636.36565090349,
1636.4454952452,1636.52545367225,1636.56784954885,1636.64780684898,1636.72766964622,
1636.80745546869,1636.88718178389,1636.96686601218,1637.0465369984,1637.12620445193,
1637.20588410275,1637.28559168514,1637.36538691421,1637.44523125592,1637.52518968297,
1637.56758555957,1637.6475428597,1637.72740565694,1637.80719147942,1637.88691779461,
1637.96660202291,1638.04627300913,1638.12594046265,1638.20562011347,1638.28532769587,
1638.36512292494,1638.44496726665,1638.5249256937,1638.56732157029,1638.64727887042,
1638.72714166766,1638.80692749014,1638.88665380533,1638.96633803363,1639.04600901985,
1639.12567647337,1639.20535612419,1639.28506370658,1639.36485893566,1639.44470327737,
1639.52466170441,1639.56705758101,1639.64701488114,1639.72687767838,1639.80666350086,
1639.88638981605,1639.96607404435,1640.04574503057,1640.12541248409,1640.20509213491,
1640.2847997173,1640.36459494638,1640.44443928809,1640.52439771513,1640.56679359173,
1640.65238019264,1640.73780309498,1640.82299284296,1640.90803942774,1640.99288519324,
1641.03022006836),.UNSPECIFIED.);
#1390=B_SPLINE_CURVE_WITH_KNOTS('',3,(#163758,#163759,#163760,#163761,#163762,
#163763,#163764,#163765,#163766,#163767),.UNSPECIFIED.,.F.,.F.,(4,1,1,1,
1,1,1,4),(1641.0302202674,1641.56652960245,1642.56626561317,1643.56600162389,
1644.56573763461,1645.56547364533,1646.56520965605,1647.31340557458),
 .UNSPECIFIED.);
#1391=B_SPLINE_CURVE_WITH_KNOTS('',3,(#163769,#163770,#163771,#163772,#163773,
#163774,#163775,#163776,#163777,#163778,#163779,#163780,#163781,#163782,
#163783,#163784,#163785,#163786,#163787,#163788,#163789,#163790,#163791,
#163792,#163793,#163794,#163795,#163796,#163797,#163798,#163799,#163800,
#163801,#163802,#163803,#163804,#163805,#163806,#163807,#163808,#163809,
#163810,#163811,#163812,#163813,#163814,#163815,#163816,#163817,#163818,
#163819,#163820,#163821,#163822,#163823,#163824,#163825,#163826,#163827,
#163828,#163829,#163830,#163831,#163832,#163833,#163834,#163835,#163836,
#163837,#163838,#163839,#163840,#163841,#163842,#163843,#163844,#163845,
#163846,#163847,#163848,#163849,#163850,#163851,#163852,#163853,#163854,
#163855,#163856,#163857,#163858,#163859,#163860,#163861,#163862,#163863,
#163864,#163865,#163866,#163867,#163868,#163869,#163870,#163871,#163872,
#163873,#163874,#163875,#163876,#163877,#163878,#163879,#163880,#163881,
#163882,#163883,#163884,#163885,#163886,#163887,#163888,#163889,#163890,
#163891,#163892,#163893,#163894,#163895,#163896,#163897,#163898,#163899,
#163900,#163901,#163902,#163903,#163904,#163905,#163906,#163907,#163908,
#163909,#163910,#163911,#163912,#163913,#163914,#163915,#163916,#163917,
#163918,#163919,#163920,#163921,#163922,#163923,#163924,#163925,#163926,
#163927,#163928,#163929,#163930,#163931,#163932,#163933,#163934,#163935,
#163936,#163937,#163938,#163939,#163940,#163941,#163942,#163943,#163944,
#163945,#163946,#163947,#163948,#163949,#163950,#163951,#163952,#163953,
#163954,#163955,#163956,#163957,#163958,#163959,#163960,#163961,#163962,
#163963,#163964,#163965,#163966,#163967,#163968,#163969,#163970,#163971,
#163972,#163973,#163974,#163975,#163976,#163977,#163978,#163979,#163980,
#163981,#163982,#163983,#163984,#163985,#163986,#163987,#163988,#163989,
#163990,#163991,#163992,#163993,#163994,#163995,#163996,#163997,#163998,
#163999,#164000,#164001,#164002,#164003,#164004,#164005,#164006,#164007,
#164008,#164009,#164010,#164011,#164012,#164013,#164014,#164015),
 .UNSPECIFIED.,.F.,.F.,(4,3,3,3,3,3,3,3,3,3,3,3,3,3,3,3,3,3,3,3,3,3,3,3,
3,3,3,3,3,3,3,3,3,3,3,3,3,3,3,3,3,3,3,3,3,3,3,3,3,3,3,3,3,3,3,3,3,3,3,3,
3,3,3,3,3,3,3,3,3,3,3,3,3,3,3,3,3,3,3,3,3,3,4),(1647.31340563367,1647.41556786862,
1647.51995242576,1647.56494566677,1647.6449029669,1647.72476576414,1647.80455158661,
1647.8842779018,1647.9639621301,1648.04363311632,1648.12330056984,1648.20298022065,
1648.28268780305,1648.36248303212,1648.44232737383,1648.52228580087,1648.56468167749,
1648.64463897762,1648.72450177486,1648.80428759734,1648.88401391253,1648.96369814083,
1649.04336912705,1649.12303658057,1649.20271623139,1649.28242381378,1649.36221904286,
1649.44206338457,1649.52202181161,1649.56441768821,1649.64437498834,1649.72423778558,
1649.80402360806,1649.88374992325,1649.96343415155,1650.04310513777,1650.12277259129,
1650.20245224211,1650.28215982451,1650.36195505358,1650.44179939529,1650.52175782234,
1650.56415369893,1650.64411099906,1650.7239737963,1650.80375961878,1650.88348593397,
1650.96317016226,1651.04284114849,1651.12250860201,1651.20218825283,1651.28189583522,
1651.3616910643,1651.44153540601,1651.52149383305,1651.56388970965,1651.64384700978,
1651.72370980702,1651.8034956295,1651.88322194469,1651.96290617298,1652.04257715921,
1652.12224461273,1652.20192426355,1652.28163184594,1652.36142707502,1652.44127141673,
1652.52122984377,1652.56362572037,1652.6435830205,1652.72344581774,1652.80323164022,
1652.88295795541,1652.96264218371,1653.04231316993,1653.12198062346,1653.20166027427,
1653.28136785667,1653.36116308574,1653.44100742745,1653.5209658545,1653.56336173109,
1653.59659088176),.UNSPECIFIED.);
#1392=B_SPLINE_CURVE_WITH_KNOTS('',3,(#164017,#164018,#164019,#164020,#164021,
#164022,#164023,#164024,#164025,#164026),.UNSPECIFIED.,.F.,.F.,(4,1,1,1,
1,1,1,4),(1653.59659542634,1654.56309774181,1655.56283375253,1656.56256976325,
1657.56230577397,1658.56204178469,1659.56177779541,1659.87977618894),
 .UNSPECIFIED.);
#1393=B_SPLINE_CURVE_WITH_KNOTS('',3,(#164028,#164029,#164030,#164031,#164032,
#164033,#164034,#164035,#164036,#164037),.UNSPECIFIED.,.F.,.F.,(4,1,1,1,
1,1,1,4),(1659.87977618894,1660.56151380613,1661.56124981685,1662.56098582757,
1663.56072183829,1664.56045784901,1665.56019385973,1666.16296149612),
 .UNSPECIFIED.);
#1394=B_SPLINE_CURVE_WITH_KNOTS('',3,(#164039,#164040,#164041,#164042,#164043,
#164044,#164045,#164046,#164047,#164048),.UNSPECIFIED.,.F.,.F.,(4,1,1,1,
1,1,1,4),(1666.16296149612,1666.55992987046,1667.55966588118,1668.55940189189,
1669.55913790262,1670.55887391334,1671.55860992406,1672.4461468033),
 .UNSPECIFIED.);
#1395=B_SPLINE_CURVE_WITH_KNOTS('',3,(#164050,#164051,#164052,#164053,#164054,
#164055,#164056,#164057,#164058,#164059,#164060,#164061,#164062),
 .UNSPECIFIED.,.F.,.F.,(4,3,1,1,1,1,1,1,4),(1672.4461468033,1672.55834593478,
1673.5580819455,1674.55781795622,1675.55755396694,1676.55728997766,1677.55702598838,
1678.5567619991,1678.72933211048),.UNSPECIFIED.);
#1396=B_SPLINE_CURVE_WITH_KNOTS('',3,(#164064,#164065,#164066,#164067,#164068,
#164069,#164070,#164071,#164072,#164073),.UNSPECIFIED.,.F.,.F.,(4,1,1,1,
1,1,1,4),(1678.72933211048,1679.55649800982,1680.55623402054,1681.55597003126,
1682.55570604198,1683.5554420527,1684.55517806342,1685.01251361461),
 .UNSPECIFIED.);
#1397=B_SPLINE_CURVE_WITH_KNOTS('',3,(#164075,#164076,#164077,#164078,#164079,
#164080,#164081,#164082,#164083,#164084,#164085,#164086,#164087,#164088,
#164089,#164090,#164091,#164092,#164093,#164094,#164095,#164096,#164097,
#164098,#164099,#164100,#164101,#164102,#164103,#164104,#164105,#164106,
#164107,#164108,#164109,#164110,#164111,#164112,#164113,#164114,#164115,
#164116,#164117,#164118,#164119,#164120,#164121,#164122,#164123,#164124,
#164125,#164126,#164127,#164128,#164129,#164130,#164131,#164132,#164133,
#164134,#164135,#164136,#164137,#164138,#164139,#164140,#164141,#164142,
#164143,#164144,#164145,#164146,#164147,#164148,#164149,#164150,#164151,
#164152,#164153,#164154,#164155,#164156,#164157,#164158,#164159,#164160,
#164161,#164162,#164163,#164164,#164165,#164166,#164167,#164168,#164169,
#164170,#164171),.UNSPECIFIED.,.F.,.F.,(4,3,3,3,3,3,3,3,3,3,3,3,3,3,3,3,
3,3,3,3,3,3,3,3,3,3,3,3,3,3,3,3,4),(1685.01251741766,1685.09464503513,1685.1768300882,
1685.25908398026,1685.34147773866,1685.42394791456,1685.50656741574,1685.55491407414,
1685.63500362071,1685.71500002474,1685.79492066898,1685.87478287743,1685.95460392844,
1686.03441267143,1686.11421844278,1686.19403684709,1686.27388349342,1686.35381754324,
1686.43380077164,1686.5138969839,1686.55465008485,1686.63315643435,1686.71156815778,
1686.78990387943,1686.86818213634,1686.94642830235,1687.02465896155,1687.10289078865,
1687.18114045841,1687.25947107649,1687.3378434626,1687.41633594072,1687.48405392823),
 .UNSPECIFIED.);
#1398=B_SPLINE_CURVE_WITH_KNOTS('',3,(#164175,#164176,#164177,#164178,#164179,
#164180,#164181,#164182,#164183,#164184,#164185,#164186,#164187,#164188,
#164189,#164190,#164191,#164192,#164193,#164194,#164195,#164196,#164197,
#164198,#164199,#164200,#164201,#164202,#164203,#164204,#164205,#164206,
#164207,#164208,#164209,#164210,#164211,#164212,#164213,#164214,#164215,
#164216,#164217,#164218,#164219,#164220,#164221,#164222,#164223,#164224,
#164225,#164226,#164227,#164228,#164229,#164230,#164231,#164232,#164233,
#164234,#164235),.UNSPECIFIED.,.F.,.F.,(4,3,3,3,3,3,3,3,3,3,3,3,3,3,3,3,
3,3,3,3,4),(-1689.55385811702,-1689.46027632283,-1689.36652622404,-1689.27277267436,
-1689.17913803904,-1689.08584706727,-1689.05399011166,-1688.97402951639,
-1688.89407895417,-1688.8141228973,-1688.73411746845,-1688.65408238791,
-1688.57397288094,-1688.5541221063,-1688.47204820899,-1688.39005270228,
-1688.30812304275,-1688.22625402995,-1688.14442248704,-1688.0626097839,
-1687.98620407297),.UNSPECIFIED.);
#1399=B_SPLINE_CURVE_WITH_KNOTS('',3,(#164237,#164238,#164239,#164240,#164241,
#164242,#164243,#164244,#164245,#164246),.UNSPECIFIED.,.F.,.F.,(4,1,1,1,
1,1,1,4),(-1687.98619636525,-1687.55438609558,-1686.55465008486,-1685.55491407414,
-1684.55517806342,-1683.5554420527,-1682.55570604198,-1681.70301876581),
 .UNSPECIFIED.);
#1400=B_SPLINE_CURVE_WITH_KNOTS('',3,(#164248,#164249,#164250,#164251,#164252,
#164253,#164254,#164255,#164256,#164257,#164258),.UNSPECIFIED.,.F.,.F.,
(4,1,1,1,1,1,1,1,4),(-1681.70301876581,-1681.55597003126,-1680.55623402054,
-1679.55649800982,-1678.5567619991,-1677.55702598838,-1676.55728997766,
-1675.55755396694,-1675.41983345863),.UNSPECIFIED.);
#1401=B_SPLINE_CURVE_WITH_KNOTS('',3,(#164260,#164261,#164262,#164263,#164264,
#164265,#164266,#164267,#164268,#164269),.UNSPECIFIED.,.F.,.F.,(4,1,1,1,
1,1,1,4),(-1675.41983345863,-1674.55781795622,-1673.5580819455,-1672.55834593478,
-1671.55860992406,-1670.55887391334,-1669.55913790262,-1669.13664815145),
 .UNSPECIFIED.);
#1402=B_SPLINE_CURVE_WITH_KNOTS('',3,(#164271,#164272,#164273,#164274,#164275,
#164276,#164277,#164278,#164279,#164280),.UNSPECIFIED.,.F.,.F.,(4,1,1,1,
1,1,1,4),(-1669.13664815145,-1668.5594018919,-1667.55966588118,-1666.55992987046,
-1665.56019385974,-1664.56045784902,-1663.5607218383,-1662.85346284427),
 .UNSPECIFIED.);
#1403=B_SPLINE_CURVE_WITH_KNOTS('',3,(#164282,#164283,#164284,#164285,#164286,
#164287,#164288,#164289,#164290,#164291,#164292,#164293,#164294,#164295,
#164296,#164297,#164298,#164299,#164300,#164301,#164302,#164303,#164304,
#164305,#164306,#164307,#164308,#164309,#164310,#164311,#164312,#164313,
#164314,#164315,#164316,#164317,#164318,#164319,#164320,#164321,#164322,
#164323,#164324,#164325,#164326,#164327,#164328,#164329,#164330,#164331,
#164332,#164333,#164334,#164335,#164336,#164337,#164338,#164339,#164340,
#164341,#164342,#164343,#164344,#164345,#164346,#164347,#164348,#164349,
#164350,#164351,#164352,#164353,#164354,#164355,#164356,#164357,#164358,
#164359,#164360,#164361,#164362,#164363,#164364,#164365,#164366,#164367,
#164368,#164369,#164370,#164371,#164372,#164373,#164374,#164375,#164376,
#164377,#164378,#164379,#164380,#164381,#164382,#164383,#164384,#164385,
#164386,#164387,#164388,#164389,#164390,#164391,#164392,#164393,#164394,
#164395,#164396,#164397,#164398,#164399,#164400,#164401,#164402,#164403,
#164404,#164405,#164406,#164407,#164408,#164409,#164410,#164411,#164412,
#164413,#164414,#164415,#164416,#164417,#164418,#164419,#164420,#164421,
#164422,#164423,#164424,#164425,#164426,#164427,#164428,#164429,#164430,
#164431,#164432,#164433,#164434,#164435,#164436,#164437,#164438,#164439,
#164440,#164441,#164442,#164443,#164444,#164445,#164446,#164447,#164448,
#164449,#164450,#164451,#164452,#164453,#164454,#164455,#164456,#164457,
#164458,#164459,#164460,#164461,#164462,#164463,#164464,#164465,#164466,
#164467,#164468,#164469,#164470,#164471,#164472,#164473,#164474,#164475,
#164476,#164477,#164478,#164479,#164480,#164481,#164482,#164483,#164484,
#164485,#164486,#164487,#164488,#164489,#164490,#164491,#164492,#164493,
#164494,#164495,#164496,#164497,#164498,#164499,#164500,#164501,#164502,
#164503,#164504,#164505,#164506,#164507,#164508,#164509,#164510,#164511,
#164512,#164513,#164514,#164515,#164516,#164517,#164518,#164519,#164520,
#164521,#164522,#164523,#164524,#164525),.UNSPECIFIED.,.F.,.F.,(4,3,3,3,
3,3,3,3,3,3,3,3,3,3,3,3,3,3,3,3,3,3,3,3,3,3,3,3,3,3,3,3,3,3,3,3,3,3,3,3,
3,3,3,3,3,3,3,3,3,3,3,3,3,3,3,3,3,3,3,3,3,3,3,3,3,3,3,3,3,3,3,3,3,3,3,3,
3,3,3,3,3,4),(-1662.85346267605,-1662.75663390855,-1662.65845502116,-1662.56098582758,
-1662.48102852737,-1662.40116573004,-1662.32137990749,-1662.24165359221,
-1662.16196936383,-1662.08229837752,-1662.00263092391,-1661.92295127301,
-1661.84324369053,-1661.76344846137,-1661.68360411957,-1661.60364569244,
-1661.56124981686,-1661.48129251675,-1661.40142971953,-1661.32164389708,
-1661.24191758191,-1661.16223335364,-1661.08256236744,-1661.00289491393,
-1660.92321526314,-1660.84350768077,-1660.76371245171,-1660.68386811003,
-1660.603909683,-1660.56151380614,-1660.48155650602,-1660.40169370879,-1660.32190788633,
-1660.24218157114,-1660.16249734286,-1660.08282635665,-1660.00315890313,
-1659.92347925233,-1659.84377166994,-1659.76397644088,-1659.68413209918,
-1659.60417367215,-1659.56177779542,-1659.48182049528,-1659.40195769802,
-1659.32217187554,-1659.24244556033,-1659.16276133202,-1659.08309034579,
-1659.00342289225,-1658.92374324142,-1658.84403565902,-1658.76424042993,
-1658.68439608821,-1658.60443766115,-1658.5620417847,-1658.48208448457,
-1658.40222168733,-1658.32243586487,-1658.24270954968,-1658.16302532139,
-1658.08335433517,-1658.00368688165,-1657.92400723084,-1657.84429964845,
-1657.76450441937,-1657.68466007767,-1657.60470165063,-1657.56230577398,
-1657.48245786639,-1657.40270440793,-1657.32302776372,-1657.24341036034,
-1657.16383467191,-1657.08427171309,-1657.00471175588,-1656.92513897508,
-1656.84553754071,-1656.76584851481,-1656.68610954442,-1656.60625841833,
-1656.57027753709),.UNSPECIFIED.);
#1404=B_SPLINE_CURVE_WITH_KNOTS('',3,(#164527,#164528,#164529,#164530,#164531,
#164532,#164533,#164534,#164535,#164536,#164537,#164538,#164539),
 .UNSPECIFIED.,.F.,.F.,(4,3,1,1,1,1,1,1,4),(-1656.57027753709,-1656.56256976326,
-1655.56283375254,-1654.56309774182,-1653.5633617311,-1652.56362572038,
-1651.56388970966,-1650.56415369894,-1650.28709632645),.UNSPECIFIED.);
#1405=B_SPLINE_CURVE_WITH_KNOTS('',3,(#164541,#164542,#164543,#164544,#164545,
#164546,#164547,#164548,#164549,#164550,#164551,#164552,#164553,#164554,
#164555,#164556,#164557,#164558,#164559,#164560,#164561,#164562,#164563,
#164564,#164565,#164566,#164567,#164568,#164569,#164570,#164571,#164572,
#164573,#164574,#164575,#164576,#164577,#164578,#164579,#164580,#164581,
#164582,#164583,#164584,#164585,#164586,#164587,#164588,#164589,#164590,
#164591,#164592,#164593,#164594,#164595,#164596,#164597,#164598,#164599,
#164600,#164601,#164602,#164603,#164604,#164605,#164606,#164607,#164608,
#164609,#164610,#164611,#164612,#164613,#164614,#164615,#164616,#164617,
#164618,#164619,#164620,#164621,#164622,#164623,#164624,#164625,#164626,
#164627,#164628,#164629,#164630,#164631,#164632,#164633,#164634,#164635,
#164636,#164637,#164638,#164639,#164640,#164641,#164642,#164643,#164644,
#164645,#164646,#164647,#164648,#164649,#164650,#164651,#164652,#164653,
#164654,#164655,#164656,#164657,#164658,#164659,#164660,#164661,#164662,
#164663,#164664,#164665,#164666,#164667,#164668,#164669,#164670,#164671,
#164672,#164673,#164674,#164675,#164676,#164677,#164678,#164679,#164680,
#164681,#164682,#164683,#164684,#164685,#164686,#164687,#164688,#164689,
#164690,#164691,#164692,#164693,#164694,#164695,#164696,#164697,#164698,
#164699,#164700,#164701,#164702,#164703,#164704,#164705,#164706,#164707,
#164708,#164709,#164710,#164711,#164712,#164713,#164714,#164715,#164716,
#164717,#164718,#164719,#164720,#164721,#164722,#164723,#164724,#164725,
#164726,#164727,#164728,#164729,#164730,#164731,#164732,#164733,#164734,
#164735,#164736,#164737,#164738,#164739,#164740,#164741,#164742,#164743,
#164744,#164745,#164746,#164747,#164748,#164749,#164750,#164751,#164752,
#164753,#164754,#164755,#164756,#164757,#164758,#164759,#164760,#164761,
#164762,#164763,#164764,#164765,#164766,#164767,#164768,#164769,#164770,
#164771,#164772,#164773,#164774,#164775,#164776,#164777,#164778,#164779,
#164780,#164781,#164782,#164783,#164784),.UNSPECIFIED.,.F.,.F.,(4,3,3,3,
3,3,3,3,3,3,3,3,3,3,3,3,3,3,3,3,3,3,3,3,3,3,3,3,3,3,3,3,3,3,3,3,3,3,3,3,
3,3,3,3,3,3,3,3,3,3,3,3,3,3,3,3,3,3,3,3,3,3,3,3,3,3,3,3,3,3,3,3,3,3,3,3,
3,3,3,3,3,4),(-1650.28709222991,-1650.20807412853,-1650.1276170735,-1650.04864875777,
-1649.9696804804,-1649.89069597473,-1649.8091264031,-1649.73001917906,-1649.64721843364,
-1649.56441768822,-1649.48446038809,-1649.40459759084,-1649.32481176837,
-1649.24508545318,-1649.16540122488,-1649.08573023866,-1649.00606278513,
-1648.92638313432,-1648.84667555192,-1648.76688032284,-1648.68703598114,
-1648.60707755409,-1648.5646816775,-1648.48472437737,-1648.40486158013,
-1648.32507575765,-1648.24534944246,-1648.16566521416,-1648.08599422794,
-1648.00632677442,-1647.9266471236,-1647.8469395412,-1647.76714431213,-1647.68729997042,
-1647.60734154337,-1647.56494566678,-1647.48498836665,-1647.40512556941,
-1647.32533974694,-1647.24561343174,-1647.16592920345,-1647.08625821723,
-1647.0065907637,-1646.92691111288,-1646.84720353049,-1646.76740830141,
-1646.68756395971,-1646.60760553266,-1646.56520965606,-1646.48525235593,
-1646.40538955869,-1646.32560373621,-1646.24587742102,-1646.16619319272,
-1646.0865222065,-1646.00685475298,-1645.92717510216,-1645.84746751977,
-1645.76767229069,-1645.68782794898,-1645.60786952194,-1645.56547364534,
-1645.48551634521,-1645.40565354797,-1645.3258677255,-1645.2461414103,-1645.16645718201,
-1645.08678619579,-1645.00711874226,-1644.92743909145,-1644.84773150905,
-1644.76793627998,-1644.68809193827,-1644.60813351122,-1644.56573763462,
-1644.48365987216,-1644.40169485898,-1644.31982974707,-1644.23807766884,
-1644.1563916886,-1644.07477146095,-1644.00390692273),.UNSPECIFIED.);
#1406=B_SPLINE_CURVE_WITH_KNOTS('',3,(#164786,#164787,#164788,#164789,#164790,
#164791,#164792,#164793,#164794,#164795),.UNSPECIFIED.,.F.,.F.,(4,1,1,1,
1,1,1,4),(-1644.00390193375,-1643.5660016239,-1642.56626561318,-1641.56652960246,
-1640.56679359174,-1639.56705758102,-1638.56732157029,-1637.72072161555),
 .UNSPECIFIED.);
#1407=B_SPLINE_CURVE_WITH_KNOTS('',3,(#164797,#164798,#164799,#164800,#164801,
#164802,#164803,#164804,#164805,#164806,#164807,#164808),.UNSPECIFIED.,
 .F.,.F.,(4,2,1,1,1,1,1,1,4),(-1637.72072161555,-1637.56758555957,-1636.56784954885,
-1635.56811353813,-1634.56837752741,-1633.56864151669,-1632.56890550597,
-1631.56916949525,-1631.43753630837),.UNSPECIFIED.);
#1408=B_SPLINE_CURVE_WITH_KNOTS('',3,(#164810,#164811,#164812,#164813,#164814,
#164815,#164816,#164817,#164818,#164819),.UNSPECIFIED.,.F.,.F.,(4,1,1,1,
1,1,1,4),(-1631.43753630837,-1630.56943348453,-1629.56969747381,-1628.56996146309,
-1627.57022545237,-1626.57048944165,-1625.57075343093,-1625.15435100119),
 .UNSPECIFIED.);
#1409=B_SPLINE_CURVE_WITH_KNOTS('',3,(#164821,#164822,#164823,#164824,#164825,
#164826,#164827,#164828,#164829,#164830),.UNSPECIFIED.,.F.,.F.,(4,1,1,1,
1,1,1,4),(-1625.15435100119,-1624.57101742021,-1623.57128140949,-1622.57154539877,
-1621.57180938805,-1620.57207337733,-1619.57233736661,-1618.87116569401),
 .UNSPECIFIED.);
#1410=B_SPLINE_CURVE_WITH_KNOTS('',3,(#164832,#164833,#164834,#164835,#164836,
#164837,#164838,#164839,#164840,#164841,#164842,#164843,#164844,#164845,
#164846,#164847,#164848,#164849,#164850,#164851,#164852,#164853,#164854,
#164855,#164856,#164857,#164858,#164859,#164860,#164861,#164862,#164863,
#164864,#164865,#164866,#164867,#164868,#164869,#164870,#164871,#164872,
#164873,#164874,#164875,#164876,#164877,#164878,#164879,#164880,#164881,
#164882,#164883,#164884,#164885,#164886,#164887,#164888,#164889,#164890,
#164891,#164892,#164893,#164894,#164895,#164896,#164897,#164898,#164899,
#164900,#164901,#164902,#164903,#164904,#164905,#164906,#164907,#164908,
#164909,#164910,#164911,#164912,#164913,#164914,#164915,#164916,#164917,
#164918,#164919,#164920,#164921,#164922,#164923,#164924,#164925,#164926,
#164927,#164928,#164929,#164930,#164931,#164932,#164933,#164934,#164935,
#164936,#164937,#164938,#164939,#164940,#164941,#164942,#164943,#164944,
#164945,#164946,#164947,#164948,#164949,#164950,#164951,#164952,#164953,
#164954,#164955,#164956,#164957,#164958,#164959,#164960,#164961,#164962,
#164963,#164964,#164965,#164966,#164967,#164968,#164969,#164970,#164971,
#164972,#164973,#164974,#164975,#164976,#164977,#164978,#164979,#164980,
#164981,#164982,#164983,#164984,#164985,#164986,#164987,#164988,#164989,
#164990,#164991,#164992,#164993,#164994,#164995,#164996,#164997,#164998,
#164999,#165000,#165001,#165002,#165003,#165004,#165005,#165006,#165007,
#165008,#165009,#165010,#165011,#165012,#165013,#165014,#165015,#165016,
#165017,#165018,#165019,#165020,#165021,#165022,#165023,#165024,#165025,
#165026,#165027,#165028,#165029,#165030,#165031,#165032,#165033,#165034,
#165035,#165036,#165037,#165038,#165039,#165040,#165041,#165042,#165043,
#165044,#165045,#165046,#165047,#165048,#165049,#165050,#165051,#165052,
#165053,#165054,#165055,#165056,#165057,#165058,#165059,#165060,#165061,
#165062,#165063,#165064,#165065,#165066,#165067,#165068,#165069,#165070,
#165071,#165072,#165073,#165074,#165075),.UNSPECIFIED.,.F.,.F.,(4,3,3,3,
3,3,3,3,3,3,3,3,3,3,3,3,3,3,3,3,3,3,3,3,3,3,3,3,3,3,3,3,3,3,3,3,3,3,3,3,
3,3,3,3,3,3,3,3,3,3,3,3,3,3,3,3,3,3,3,3,3,3,3,3,3,3,3,3,3,3,3,3,3,3,3,3,
3,3,3,3,3,4),(-1618.87116551288,-1618.77500107763,-1618.67380121676,-1618.57260135589,
-1618.49264405576,-1618.41278125852,-1618.33299543604,-1618.25326912085,
-1618.17358489255,-1618.09391390633,-1618.01424645281,-1617.93456680199,
-1617.8548592196,-1617.77506399052,-1617.69521964881,-1617.61526122176,
-1617.57286534517,-1617.49290804504,-1617.4130452478,-1617.33325942532,
-1617.25353311013,-1617.17384888183,-1617.09417789561,-1617.01451044209,
-1616.93483079127,-1616.85512320888,-1616.7753279798,-1616.69548363809,
-1616.61552521105,-1616.57312933445,-1616.49317203432,-1616.41330923708,
-1616.3335234146,-1616.25379709941,-1616.17411287111,-1616.09444188489,
-1616.01477443137,-1615.93509478055,-1615.85538719816,-1615.77559196908,
-1615.69574762737,-1615.61578920033,-1615.57339332373,-1615.4934360236,
-1615.41357322636,-1615.33378740389,-1615.25406108869,-1615.1743768604,
-1615.09470587418,-1615.01503842065,-1614.93535876983,-1614.85565118744,
-1614.77585595836,-1614.69601161666,-1614.61605318961,-1614.57365731301,
-1614.49370001288,-1614.41383721564,-1614.33405139316,-1614.25432507797,
-1614.17464084968,-1614.09496986345,-1614.01530240993,-1613.93562275911,
-1613.85591517672,-1613.77611994764,-1613.69627560593,-1613.61631717889,
-1613.57392130229,-1613.4941558113,-1613.41448472223,-1613.33489032263,
-1613.2553549622,-1613.17193314028,-1613.09245209091,-1613.01297286857,
-1612.93347957904,-1612.85395632244,-1612.77434530931,-1612.69468303516,
-1612.61491125407,-1612.58798038683),.UNSPECIFIED.);
#1411=B_SPLINE_CURVE_WITH_KNOTS('',3,(#165077,#165078,#165079,#165080,#165081,
#165082,#165083,#165084,#165085,#165086,#165087,#165088,#165089),
 .UNSPECIFIED.,.F.,.F.,(4,3,1,1,1,1,1,1,4),(-1612.58798038683,-1612.57418529157,
-1611.57444928085,-1610.57471327013,-1609.57497725941,-1608.57524124869,
-1607.57550523797,-1606.57576922725,-1606.30479867486),.UNSPECIFIED.);
#1412=B_SPLINE_CURVE_WITH_KNOTS('',3,(#165091,#165092,#165093,#165094,#165095,
#165096,#165097,#165098,#165099,#165100,#165101,#165102,#165103,#165104,
#165105,#165106,#165107,#165108,#165109,#165110,#165111,#165112,#165113,
#165114,#165115,#165116,#165117,#165118,#165119,#165120,#165121,#165122,
#165123,#165124,#165125,#165126,#165127,#165128,#165129,#165130,#165131,
#165132,#165133,#165134,#165135,#165136,#165137,#165138,#165139,#165140,
#165141,#165142,#165143,#165144,#165145,#165146,#165147,#165148,#165149,
#165150,#165151,#165152,#165153,#165154,#165155,#165156,#165157,#165158,
#165159,#165160,#165161,#165162,#165163,#165164,#165165,#165166,#165167,
#165168,#165169,#165170,#165171,#165172,#165173,#165174,#165175,#165176,
#165177,#165178,#165179,#165180,#165181,#165182,#165183,#165184,#165185,
#165186,#165187,#165188,#165189,#165190,#165191,#165192,#165193,#165194,
#165195,#165196,#165197,#165198,#165199,#165200,#165201,#165202,#165203,
#165204,#165205,#165206,#165207,#165208,#165209,#165210,#165211,#165212,
#165213,#165214,#165215,#165216,#165217,#165218,#165219,#165220,#165221,
#165222,#165223,#165224,#165225,#165226,#165227,#165228,#165229,#165230,
#165231,#165232,#165233,#165234,#165235,#165236,#165237,#165238,#165239,
#165240,#165241,#165242,#165243,#165244,#165245,#165246,#165247,#165248,
#165249,#165250,#165251,#165252,#165253,#165254,#165255,#165256,#165257,
#165258,#165259,#165260,#165261,#165262,#165263,#165264,#165265,#165266,
#165267,#165268,#165269,#165270,#165271,#165272,#165273,#165274,#165275,
#165276,#165277,#165278,#165279,#165280,#165281,#165282,#165283,#165284,
#165285,#165286,#165287,#165288,#165289,#165290,#165291,#165292,#165293,
#165294,#165295,#165296,#165297,#165298,#165299,#165300,#165301,#165302,
#165303,#165304,#165305,#165306,#165307,#165308,#165309,#165310,#165311,
#165312,#165313,#165314,#165315,#165316,#165317,#165318,#165319,#165320,
#165321,#165322,#165323,#165324,#165325,#165326,#165327,#165328,#165329,
#165330,#165331,#165332,#165333,#165334,#165335,#165336,#165337),
 .UNSPECIFIED.,.F.,.F.,(4,3,3,3,3,3,3,3,3,3,3,3,3,3,3,3,3,3,3,3,3,3,3,3,
3,3,3,3,3,3,3,3,3,3,3,3,3,3,3,3,3,3,3,3,3,3,3,3,3,3,3,3,3,3,3,3,3,3,3,3,
3,3,3,3,3,3,3,3,3,3,3,3,3,3,3,3,3,3,3,3,3,3,4),(-1606.30479507965,-1606.22582393907,
-1606.14460009875,-1606.06568366228,-1605.98676893908,-1605.90783962531,
-1605.82488802311,-1605.7458377603,-1605.66673391448,-1605.58752429386,
-1605.57603321653,-1605.4960759164,-1605.41621311916,-1605.33642729668,
-1605.25670098149,-1605.17701675319,-1605.09734576697,-1605.01767831345,
-1604.93799866263,-1604.85829108023,-1604.77849585116,-1604.69865150945,
-1604.6186930824,-1604.57629720581,-1604.49633990568,-1604.41647710844,
-1604.33669128596,-1604.25696497077,-1604.17728074247,-1604.09760975625,
-1604.01794230273,-1603.93826265191,-1603.85855506952,-1603.77875984044,
-1603.69891549873,-1603.61895707168,-1603.57656119509,-1603.49660389496,
-1603.41674109772,-1603.33695527524,-1603.25722896005,-1603.17754473176,
-1603.09787374553,-1603.01820629201,-1602.93852664119,-1602.8588190588,
-1602.77902382972,-1602.69917948802,-1602.61922106097,-1602.57682518437,
-1602.49686788424,-1602.417005087,-1602.33721926452,-1602.25749294933,-1602.17780872103,
-1602.09813773481,-1602.01847028129,-1601.93879063047,-1601.85908304808,
-1601.779287819,-1601.69944347729,-1601.61948505025,-1601.57708917365,-1601.49713187352,
-1601.41726907628,-1601.33748325381,-1601.25775693861,-1601.17807271032,
-1601.0984017241,-1601.01873427057,-1600.93905461975,-1600.85934703736,
-1600.77955180829,-1600.69970746658,-1600.61974903953,-1600.57735316293,
-1600.49510574788,-1600.41297300452,-1600.33094243016,-1600.24902907937,
-1600.16718435843,-1600.08541054314,-1600.02160977247),.UNSPECIFIED.);
#1413=B_SPLINE_CURVE_WITH_KNOTS('',3,(#165339,#165340,#165341,#165342,#165343,
#165344,#165345,#165346,#165347,#165348),.UNSPECIFIED.,.F.,.F.,(4,1,1,1,
1,1,1,4),(-1600.02160535103,-1599.57761715221,-1598.57788114149,-1597.57814513077,
-1596.57840912005,-1595.57867310933,-1594.57893709861,-1593.73842446529),
 .UNSPECIFIED.);
#1414=B_SPLINE_CURVE_WITH_KNOTS('',3,(#165350,#165351,#165352,#165353,#165354,
#165355,#165356,#165357,#165358,#165359,#165360,#165361),.UNSPECIFIED.,
 .F.,.F.,(4,2,1,1,1,1,1,1,4),(-1593.73842446529,-1593.57920108789,-1592.57946507717,
-1591.57972906645,-1590.57999305573,-1589.58025704501,-1588.58052103429,
-1587.58078502357,-1587.45523915811),.UNSPECIFIED.);
#1415=B_SPLINE_CURVE_WITH_KNOTS('',3,(#165363,#165364,#165365,#165366,#165367,
#165368,#165369,#165370,#165371,#165372,#165373,#165374,#165375,#165376,
#165377,#165378,#165379,#165380,#165381,#165382,#165383,#165384,#165385,
#165386,#165387,#165388,#165389,#165390,#165391,#165392,#165393,#165394,
#165395,#165396,#165397,#165398,#165399,#165400,#165401,#165402,#165403,
#165404,#165405,#165406,#165407,#165408,#165409,#165410,#165411,#165412,
#165413,#165414,#165415,#165416,#165417,#165418,#165419,#165420,#165421,
#165422,#165423,#165424,#165425,#165426,#165427,#165428,#165429,#165430,
#165431,#165432,#165433,#165434,#165435,#165436,#165437,#165438,#165439,
#165440,#165441,#165442,#165443,#165444,#165445,#165446,#165447,#165448,
#165449,#165450,#165451,#165452,#165453,#165454,#165455,#165456,#165457,
#165458,#165459,#165460,#165461,#165462,#165463,#165464,#165465,#165466,
#165467,#165468,#165469,#165470,#165471,#165472,#165473,#165474,#165475,
#165476,#165477,#165478,#165479,#165480,#165481,#165482,#165483,#165484,
#165485,#165486,#165487,#165488,#165489,#165490,#165491,#165492,#165493,
#165494,#165495,#165496,#165497,#165498,#165499,#165500,#165501,#165502,
#165503,#165504,#165505,#165506,#165507,#165508,#165509,#165510,#165511,
#165512,#165513,#165514,#165515,#165516,#165517,#165518,#165519,#165520,
#165521,#165522,#165523,#165524,#165525,#165526,#165527,#165528,#165529,
#165530,#165531,#165532,#165533,#165534,#165535,#165536,#165537,#165538,
#165539,#165540,#165541,#165542,#165543,#165544,#165545,#165546,#165547,
#165548,#165549,#165550,#165551,#165552,#165553,#165554,#165555,#165556,
#165557,#165558,#165559,#165560,#165561,#165562,#165563,#165564,#165565,
#165566,#165567,#165568,#165569,#165570,#165571,#165572,#165573,#165574,
#165575,#165576,#165577,#165578,#165579,#165580,#165581,#165582,#165583,
#165584,#165585,#165586,#165587,#165588,#165589,#165590,#165591,#165592,
#165593,#165594,#165595,#165596,#165597,#165598,#165599,#165600,#165601,
#165602,#165603,#165604,#165605,#165606),.UNSPECIFIED.,.F.,.F.,(4,3,3,3,
3,3,3,3,3,3,3,3,3,3,3,3,3,3,3,3,3,3,3,3,3,3,3,3,3,3,3,3,3,3,3,3,3,3,3,3,
3,3,3,3,3,3,3,3,3,3,3,3,3,3,3,3,3,3,3,3,3,3,3,3,3,3,3,3,3,3,3,3,3,3,3,3,
3,3,3,3,3,4),(-1587.45523915811,-1587.37647002073,-1587.29778119148,-1587.21915428759,
-1587.13939112825,-1587.06082278289,-1586.98225751216,-1586.9036787886,
-1586.82302134466,-1586.74432614687,-1586.66268757986,-1586.58104901285,
-1586.50109171272,-1586.42122891548,-1586.341443093,-1586.26171677781,-1586.18203254951,
-1586.10236156329,-1586.02269410977,-1585.94301445895,-1585.86330687656,
-1585.78351164748,-1585.70366730577,-1585.62370887872,-1585.58131300213,
-1585.501355702,-1585.42149290476,-1585.34170708228,-1585.26198076709,-1585.18229653879,
-1585.10262555257,-1585.02295809905,-1584.94327844823,-1584.86357086583,
-1584.78377563676,-1584.70393129505,-1584.623972868,-1584.58157699141,-1584.50161969128,
-1584.42175689404,-1584.34197107156,-1584.26224475637,-1584.18256052808,
-1584.10288954185,-1584.02322208833,-1583.94354243751,-1583.86383485512,
-1583.78403962604,-1583.70419528433,-1583.62423685729,-1583.58184098069,
-1583.50188368056,-1583.42202088332,-1583.34223506084,-1583.26250874565,
-1583.18282451735,-1583.10315353113,-1583.02348607761,-1582.94380642679,
-1582.8640988444,-1582.78430361532,-1582.70445927361,-1582.62450084657,
-1582.58210496997,-1582.50214766984,-1582.4222848726,-1582.34249905013,
-1582.26277273493,-1582.18308850664,-1582.10341752042,-1582.02375006689,
-1581.94407041608,-1581.86436283369,-1581.78456760461,-1581.7047232629,
-1581.62476483586,-1581.58236895925,-1581.49400844408,-1581.4059913693,
-1581.31819275127,-1581.23075361509,-1581.1720540622),.UNSPECIFIED.);
#1416=B_SPLINE_CURVE_WITH_KNOTS('',3,(#165608,#165609,#165610,#165611,#165612,
#165613,#165614,#165615,#165616,#165617),.UNSPECIFIED.,.F.,.F.,(4,1,1,1,
1,1,1,4),(-1581.17205385093,-1580.58263294853,-1579.58289693781,-1578.58316092709,
-1577.58342491637,-1576.58368890565,-1575.58395289493,-1574.88886854375),
 .UNSPECIFIED.);
#1417=B_SPLINE_CURVE_WITH_KNOTS('',3,(#165619,#165620,#165621,#165622,#165623,
#165624,#165625,#165626,#165627,#165628,#165629,#165630,#165631,#165632,
#165633,#165634,#165635,#165636,#165637,#165638,#165639,#165640,#165641,
#165642,#165643,#165644,#165645,#165646,#165647,#165648,#165649,#165650,
#165651,#165652,#165653,#165654,#165655,#165656,#165657,#165658,#165659,
#165660,#165661,#165662,#165663,#165664,#165665,#165666,#165667,#165668,
#165669,#165670,#165671,#165672,#165673,#165674,#165675,#165676,#165677,
#165678,#165679,#165680,#165681,#165682,#165683,#165684,#165685,#165686,
#165687,#165688,#165689,#165690,#165691,#165692,#165693,#165694,#165695,
#165696,#165697,#165698,#165699,#165700,#165701,#165702,#165703,#165704,
#165705,#165706,#165707,#165708,#165709,#165710,#165711,#165712,#165713,
#165714,#165715,#165716,#165717,#165718,#165719,#165720,#165721,#165722,
#165723,#165724,#165725,#165726,#165727,#165728,#165729,#165730,#165731,
#165732,#165733,#165734,#165735,#165736,#165737,#165738,#165739,#165740,
#165741,#165742,#165743,#165744,#165745,#165746,#165747,#165748,#165749,
#165750,#165751,#165752,#165753,#165754,#165755,#165756,#165757,#165758,
#165759,#165760,#165761,#165762,#165763,#165764,#165765,#165766,#165767,
#165768,#165769,#165770,#165771,#165772,#165773,#165774,#165775,#165776,
#165777,#165778,#165779,#165780,#165781,#165782,#165783,#165784,#165785,
#165786,#165787,#165788,#165789,#165790,#165791,#165792,#165793,#165794,
#165795,#165796,#165797,#165798,#165799,#165800,#165801,#165802,#165803,
#165804,#165805,#165806,#165807,#165808,#165809,#165810,#165811,#165812,
#165813,#165814,#165815,#165816,#165817,#165818,#165819,#165820,#165821,
#165822,#165823,#165824,#165825,#165826,#165827,#165828,#165829,#165830,
#165831,#165832,#165833,#165834,#165835,#165836,#165837,#165838,#165839,
#165840,#165841,#165842,#165843,#165844,#165845,#165846,#165847,#165848,
#165849,#165850,#165851,#165852,#165853,#165854,#165855,#165856,#165857,
#165858,#165859,#165860,#165861,#165862,#165863,#165864,#165865),
 .UNSPECIFIED.,.F.,.F.,(4,3,3,3,3,3,3,3,3,3,3,3,3,3,3,3,3,3,3,3,3,3,3,3,
3,3,3,3,3,3,3,3,3,3,3,3,3,3,3,3,3,3,3,3,3,3,3,3,3,3,3,3,3,3,3,3,3,3,3,3,
3,3,3,3,3,3,3,3,3,3,3,3,3,3,3,3,3,3,3,3,3,3,4),(-1574.8888683503,-1574.7933409988,
-1574.69705729338,-1574.59996713565,-1574.58421688421,-1574.50425958408,
-1574.42439678684,-1574.34461096436,-1574.26488464917,-1574.18520042087,
-1574.10552943465,-1574.02586198112,-1573.94618233031,-1573.86647474791,
-1573.78667951884,-1573.70683517713,-1573.62687675008,-1573.58448087349,
-1573.50452357336,-1573.42466077612,-1573.34487495364,-1573.26514863845,
-1573.18546441015,-1573.10579342393,-1573.02612597041,-1572.94644631959,
-1572.8667387372,-1572.78694350812,-1572.70709916641,-1572.62714073936,
-1572.58474486277,-1572.50478756264,-1572.4249247654,-1572.34513894292,
-1572.26541262773,-1572.18572839943,-1572.10605741321,-1572.02638995969,
-1571.94671030887,-1571.86700272648,-1571.7872074974,-1571.70736315569,
-1571.62740472865,-1571.58500885205,-1571.50505155192,-1571.42518875468,
-1571.3454029322,-1571.26567661701,-1571.18599238872,-1571.10632140249,
-1571.02665394897,-1570.94697429815,-1570.86726671576,-1570.78747148668,
-1570.70762714498,-1570.62766871793,-1570.58527284133,-1570.5053155412,
-1570.42545274396,-1570.34566692149,-1570.26594060629,-1570.186256378,-1570.10658539178,
-1570.02691793825,-1569.94723828744,-1569.86753070504,-1569.78773547597,
-1569.70789113426,-1569.62793270722,-1569.58553683061,-1569.50585028896,
-1569.42625809896,-1569.34674247608,-1569.26728569865,-1569.18458539089,
-1569.1051822485,-1569.02578069471,-1568.94636477135,-1568.86691851423,
-1568.78738477088,-1568.70779930831,-1568.62810586245,-1568.60568323657),
 .UNSPECIFIED.);
#1418=B_SPLINE_CURVE_WITH_KNOTS('',3,(#165867,#165868,#165869,#165870,#165871,
#165872,#165873,#165874,#165875,#165876,#165877,#165878,#165879),
 .UNSPECIFIED.,.F.,.F.,(4,3,1,1,1,1,1,1,4),(-1568.60568323657,-1568.58580081989,
-1567.58606480917,-1566.58632879845,-1565.58659278773,-1564.58685677701,
-1563.58712076629,-1562.58738475557,-1562.32249792939),.UNSPECIFIED.);
#1419=B_SPLINE_CURVE_WITH_KNOTS('',3,(#165881,#165882,#165883,#165884,#165885,
#165886,#165887,#165888,#165889,#165890),.UNSPECIFIED.,.F.,.F.,(4,1,1,1,
1,1,1,4),(-1562.32249792939,-1561.58764874484,-1560.58791273412,-1559.5881767234,
-1558.58844071268,-1557.58870470196,-1556.58896869124,-1556.03931262221),
 .UNSPECIFIED.);
#1420=B_SPLINE_CURVE_WITH_KNOTS('',3,(#165892,#165893,#165894,#165895,#165896,
#165897,#165898,#165899,#165900,#165901),.UNSPECIFIED.,.F.,.F.,(4,1,1,1,
1,1,1,4),(-1556.03931262221,-1555.58923268052,-1554.5894966698,-1553.58976065908,
-1552.59002464836,-1551.59028863764,-1550.59055262692,-1549.75612731503),
 .UNSPECIFIED.);
#1421=B_SPLINE_CURVE_WITH_KNOTS('',3,(#165903,#165904,#165905,#165906,#165907,
#165908,#165909,#165910,#165911,#165912,#165913,#165914),.UNSPECIFIED.,
 .F.,.F.,(4,2,1,1,1,1,1,1,4),(-1549.75612731503,-1549.5908166162,-1548.59108060548,
-1547.59134459476,-1546.59160858404,-1545.59187257332,-1544.5921365626,
-1543.59240055188,-1543.47294200786),.UNSPECIFIED.);
#1422=B_SPLINE_CURVE_WITH_KNOTS('',3,(#165916,#165917,#165918,#165919,#165920,
#165921,#165922,#165923,#165924,#165925,#165926,#165927,#165928,#165929,
#165930,#165931,#165932,#165933,#165934,#165935,#165936,#165937,#165938,
#165939,#165940,#165941,#165942,#165943,#165944,#165945,#165946,#165947,
#165948,#165949,#165950,#165951,#165952,#165953,#165954,#165955,#165956,
#165957,#165958,#165959,#165960,#165961,#165962,#165963,#165964,#165965,
#165966,#165967,#165968,#165969,#165970,#165971,#165972,#165973,#165974,
#165975,#165976,#165977,#165978,#165979,#165980,#165981,#165982,#165983,
#165984,#165985,#165986,#165987,#165988,#165989,#165990,#165991,#165992,
#165993,#165994,#165995,#165996,#165997,#165998,#165999,#166000,#166001,
#166002,#166003,#166004,#166005,#166006,#166007,#166008,#166009,#166010,
#166011,#166012,#166013,#166014,#166015,#166016,#166017,#166018,#166019,
#166020,#166021,#166022,#166023,#166024,#166025,#166026,#166027,#166028,
#166029,#166030,#166031,#166032,#166033,#166034,#166035,#166036,#166037,
#166038,#166039,#166040,#166041,#166042,#166043,#166044,#166045,#166046,
#166047,#166048,#166049,#166050,#166051,#166052,#166053,#166054,#166055,
#166056,#166057,#166058,#166059,#166060,#166061,#166062,#166063,#166064,
#166065,#166066,#166067,#166068,#166069,#166070,#166071,#166072,#166073,
#166074,#166075,#166076,#166077,#166078,#166079,#166080,#166081,#166082,
#166083,#166084,#166085,#166086,#166087,#166088,#166089,#166090,#166091,
#166092,#166093,#166094,#166095,#166096,#166097,#166098,#166099,#166100,
#166101,#166102,#166103,#166104,#166105,#166106,#166107,#166108,#166109,
#166110,#166111,#166112,#166113,#166114,#166115,#166116,#166117,#166118,
#166119,#166120,#166121,#166122,#166123,#166124,#166125,#166126,#166127,
#166128,#166129,#166130,#166131,#166132,#166133,#166134,#166135,#166136,
#166137,#166138,#166139,#166140,#166141,#166142,#166143,#166144,#166145,
#166146,#166147,#166148,#166149,#166150,#166151,#166152,#166153,#166154,
#166155,#166156,#166157,#166158,#166159,#166160,#166161,#166162),
 .UNSPECIFIED.,.F.,.F.,(4,3,3,3,3,3,3,3,3,3,3,3,3,3,3,3,3,3,3,3,3,3,3,3,
3,3,3,3,3,3,3,3,3,3,3,3,3,3,3,3,3,3,3,3,3,3,3,3,3,3,3,3,3,3,3,3,3,3,3,3,
3,3,3,3,3,3,3,3,3,3,3,3,3,3,3,3,3,3,3,3,3,3,4),(-1543.47294200786,-1543.39414426789,
-1543.31542798864,-1543.2367747979,-1543.15626101581,-1543.07766916188,
-1542.99908131531,-1542.92048096174,-1542.8385268566,-1542.75981060134,
-1542.68104212033,-1542.60217029467,-1542.59266454116,-1542.51270724103,
-1542.43284444379,-1542.35305862132,-1542.27333230612,-1542.19364807783,
-1542.11397709161,-1542.03430963808,-1541.95462998727,-1541.87492240487,
-1541.7951271758,-1541.71528283409,-1541.63532440704,-1541.59292853044,
-1541.51297123031,-1541.43310843307,-1541.3533226106,-1541.2735962954,-1541.19391206711,
-1541.11424108089,-1541.03457362736,-1540.95489397655,-1540.87518639415,
-1540.79539116508,-1540.71554682337,-1540.63558839632,-1540.59319251972,
-1540.51323521959,-1540.43337242235,-1540.35358659987,-1540.27386028468,
-1540.19417605638,-1540.11450507016,-1540.03483761664,-1539.95515796582,
-1539.87545038342,-1539.79565515435,-1539.71581081264,-1539.63585238559,
-1539.593456509,-1539.51349920887,-1539.43363641163,-1539.35385058915,-1539.27412427396,
-1539.19444004567,-1539.11476905944,-1539.03510160592,-1538.9554219551,
-1538.87571437271,-1538.79591914363,-1538.71607480192,-1538.63611637488,
-1538.59372049828,-1538.51376319815,-1538.4339004009,-1538.35411457843,
-1538.27438826324,-1538.19470403494,-1538.11503304872,-1538.03536559519,
-1537.95568594437,-1537.87597836198,-1537.7961831329,-1537.71633879119,
-1537.63638036415,-1537.59398448756,-1537.50525262927,-1537.4168783209,
-1537.32873468176,-1537.24096808399,-1537.18975692054),.UNSPECIFIED.);
#1423=B_SPLINE_CURVE_WITH_KNOTS('',3,(#166164,#166165,#166166,#166167,#166168,
#166169,#166170,#166171,#166172,#166173),.UNSPECIFIED.,.F.,.F.,(4,1,1,1,
1,1,1,4),(-1537.18975670068,-1536.59424847684,-1535.59451246612,-1534.5947764554,
-1533.59504044468,-1532.59530443396,-1531.59556842324,-1530.9065713935),
 .UNSPECIFIED.);
#1424=B_SPLINE_CURVE_WITH_KNOTS('',3,(#166175,#166176,#166177,#166178,#166179,
#166180,#166181,#166182,#166183,#166184,#166185,#166186,#166187,#166188,
#166189,#166190,#166191,#166192,#166193,#166194,#166195,#166196,#166197,
#166198,#166199,#166200,#166201,#166202,#166203,#166204,#166205,#166206,
#166207,#166208,#166209,#166210,#166211,#166212,#166213,#166214,#166215,
#166216,#166217,#166218,#166219,#166220,#166221,#166222,#166223,#166224,
#166225,#166226,#166227,#166228,#166229,#166230,#166231,#166232,#166233,
#166234,#166235,#166236,#166237,#166238,#166239,#166240,#166241,#166242,
#166243,#166244,#166245,#166246,#166247,#166248,#166249,#166250,#166251,
#166252,#166253,#166254,#166255,#166256,#166257,#166258,#166259,#166260,
#166261,#166262,#166263,#166264,#166265,#166266,#166267,#166268,#166269,
#166270,#166271,#166272,#166273,#166274,#166275,#166276,#166277,#166278,
#166279,#166280,#166281,#166282,#166283,#166284,#166285,#166286,#166287,
#166288,#166289,#166290,#166291,#166292,#166293,#166294,#166295,#166296,
#166297,#166298,#166299,#166300,#166301,#166302,#166303,#166304,#166305,
#166306,#166307,#166308,#166309,#166310,#166311,#166312,#166313,#166314,
#166315,#166316,#166317,#166318,#166319,#166320,#166321,#166322,#166323,
#166324,#166325,#166326,#166327,#166328,#166329,#166330,#166331,#166332,
#166333,#166334,#166335,#166336,#166337,#166338,#166339,#166340,#166341,
#166342,#166343,#166344,#166345,#166346,#166347,#166348,#166349,#166350,
#166351,#166352,#166353,#166354,#166355,#166356,#166357,#166358,#166359,
#166360,#166361,#166362,#166363,#166364,#166365,#166366,#166367,#166368,
#166369,#166370,#166371,#166372,#166373,#166374,#166375,#166376,#166377,
#166378,#166379,#166380,#166381,#166382,#166383,#166384,#166385,#166386,
#166387,#166388,#166389,#166390,#166391,#166392,#166393,#166394,#166395,
#166396,#166397,#166398,#166399,#166400,#166401,#166402,#166403,#166404,
#166405,#166406,#166407,#166408,#166409,#166410,#166411,#166412,#166413,
#166414,#166415,#166416,#166417,#166418,#166419,#166420,#166421),
 .UNSPECIFIED.,.F.,.F.,(4,3,3,3,3,3,3,3,3,3,3,3,3,3,3,3,3,3,3,3,3,3,3,3,
3,3,3,3,3,3,3,3,3,3,3,3,3,3,3,3,3,3,3,3,3,3,3,3,3,3,3,3,3,3,3,3,3,3,3,3,
3,3,3,3,3,3,3,3,3,3,3,3,3,3,3,3,3,3,3,3,3,3,4),(-1530.90657118922,-1530.81165532923,
-1530.71604002867,-1530.61965629758,-1530.59583241252,-1530.51587511239,
-1530.43601231515,-1530.35622649269,-1530.27650017749,-1530.1968159492,
-1530.11714496299,-1530.03747750946,-1529.95779785865,-1529.87809027626,
-1529.79829504719,-1529.71845070549,-1529.63849227844,-1529.5960964018,
-1529.51613910167,-1529.43627630443,-1529.35649048195,-1529.27676416676,
-1529.19707993846,-1529.11740895224,-1529.03774149872,-1528.9580618479,
-1528.87835426551,-1528.79855903643,-1528.71871469472,-1528.63875626768,
-1528.59636039108,-1528.51640309095,-1528.4365402937,-1528.35675447123,
-1528.27702815604,-1528.19734392774,-1528.11767294152,-1528.03800548799,
-1527.95832583718,-1527.87861825478,-1527.7988230257,-1527.718978684,-1527.63902025695,
-1527.59662438036,-1527.51666708023,-1527.43680428299,-1527.35701846052,
-1527.27729214532,-1527.19760791703,-1527.11793693081,-1527.03826947728,
-1526.95858982647,-1526.87888224407,-1526.799087015,-1526.71924267329,-1526.63928424624,
-1526.59688836964,-1526.51693106951,-1526.43706827227,-1526.35728244979,
-1526.2775561346,-1526.1978719063,-1526.11820092008,-1526.03853346655,-1525.95885381574,
-1525.87914623334,-1525.79935100427,-1525.71950666256,-1525.63954823551,
-1525.59715235892,-1525.5175413367,-1525.43802461378,-1525.35858433859,
-1525.27920272328,-1525.19722564366,-1525.11789704264,-1525.03856981854,
-1524.95922795393,-1524.87985542501,-1524.8003957555,-1524.72088394743,
-1524.64126575125,-1524.62338608632),.UNSPECIFIED.);
#1425=B_SPLINE_CURVE_WITH_KNOTS('',3,(#166423,#166424,#166425,#166426,#166427,
#166428,#166429,#166430,#166431,#166432,#166433,#166434,#166435),
 .UNSPECIFIED.,.F.,.F.,(4,3,1,1,1,1,1,1,4),(-1524.62338608632,-1524.5974163482,
-1523.59768033748,-1522.59794432676,-1521.59820831604,-1520.59847230532,
-1519.5987362946,-1518.59900028388,-1518.34020077914),.UNSPECIFIED.);
#1426=B_SPLINE_CURVE_WITH_KNOTS('',3,(#166437,#166438,#166439,#166440,#166441,
#166442,#166443,#166444,#166445,#166446),.UNSPECIFIED.,.F.,.F.,(4,1,1,1,
1,1,1,4),(-1518.34020077914,-1517.59926427316,-1516.59952826244,-1515.59979225172,
-1514.600056241,-1513.60032023028,-1512.60058421956,-1512.05701547196),
 .UNSPECIFIED.);
#1427=B_SPLINE_CURVE_WITH_KNOTS('',3,(#166448,#166449,#166450,#166451,#166452,
#166453,#166454,#166455,#166456,#166457),.UNSPECIFIED.,.F.,.F.,(4,1,1,1,
1,1,1,4),(-1512.05701547196,-1511.60084820884,-1510.60111219812,-1509.6013761874,
-1508.60164017668,-1507.60190416596,-1506.60216815524,-1505.77383016478),
 .UNSPECIFIED.);
#1428=B_SPLINE_CURVE_WITH_KNOTS('',3,(#166459,#166460,#166461,#166462,#166463,
#166464,#166465,#166466,#166467,#166468,#166469,#166470),.UNSPECIFIED.,
 .F.,.F.,(4,2,1,1,1,1,1,1,4),(-1505.77383016478,-1505.60243214452,-1504.6026961338,
-1503.60296012308,-1502.60322411236,-1501.60348810164,-1500.60375209092,
-1499.6040160802,-1499.4906448576),.UNSPECIFIED.);
#1429=B_SPLINE_CURVE_WITH_KNOTS('',3,(#166472,#166473,#166474,#166475,#166476,
#166477,#166478,#166479,#166480,#166481),.UNSPECIFIED.,.F.,.F.,(4,1,1,1,
1,1,1,4),(-1499.4906448576,-1498.60428006948,-1497.60454405876,-1496.60480804804,
-1495.60507203732,-1494.6053360266,-1493.60560001588,-1493.20745955042),
 .UNSPECIFIED.);
#1430=B_SPLINE_CURVE_WITH_KNOTS('',3,(#166483,#166484,#166485,#166486,#166487,
#166488,#166489,#166490,#166491,#166492),.UNSPECIFIED.,.F.,.F.,(4,1,1,1,
1,1,1,4),(-1493.20745955042,-1492.60586400516,-1491.60612799444,-1490.60639198372,
-1489.606655973,-1488.60691996228,-1487.60718395156,-1486.92427424324),
 .UNSPECIFIED.);
#1431=B_SPLINE_CURVE_WITH_KNOTS('',3,(#166494,#166495,#166496,#166497,#166498,
#166499,#166500,#166501,#166502,#166503,#166504),.UNSPECIFIED.,.F.,.F.,
(4,2,1,1,1,1,1,4),(-1486.92427424324,-1486.60744794083,-1485.60771193012,
-1484.60797591939,-1483.60823990867,-1482.60850389795,-1481.60876788723,
-1480.64109334394),.UNSPECIFIED.);
#1432=B_SPLINE_CURVE_WITH_KNOTS('',3,(#166506,#166507,#166508,#166509,#166510,
#166511,#166512,#166513,#166514,#166515,#166516,#166517,#166518,#166519,
#166520,#166521,#166522,#166523,#166524,#166525,#166526,#166527,#166528,
#166529,#166530,#166531,#166532,#166533,#166534,#166535,#166536,#166537,
#166538,#166539,#166540,#166541,#166542,#166543,#166544,#166545,#166546,
#166547,#166548,#166549,#166550,#166551,#166552,#166553,#166554,#166555,
#166556,#166557,#166558,#166559,#166560,#166561,#166562,#166563,#166564,
#166565,#166566,#166567,#166568,#166569,#166570,#166571,#166572,#166573,
#166574,#166575,#166576,#166577,#166578,#166579,#166580,#166581,#166582,
#166583,#166584,#166585,#166586,#166587,#166588,#166589,#166590,#166591,
#166592,#166593,#166594,#166595,#166596,#166597,#166598,#166599,#166600,
#166601,#166602,#166603,#166604,#166605,#166606,#166607,#166608,#166609,
#166610,#166611,#166612,#166613,#166614,#166615,#166616,#166617,#166618,
#166619,#166620,#166621,#166622,#166623,#166624,#166625,#166626,#166627,
#166628,#166629,#166630,#166631,#166632,#166633,#166634,#166635,#166636,
#166637,#166638,#166639,#166640,#166641,#166642,#166643,#166644,#166645,
#166646,#166647,#166648,#166649,#166650,#166651,#166652,#166653,#166654,
#166655,#166656,#166657,#166658,#166659,#166660,#166661,#166662,#166663,
#166664,#166665,#166666,#166667,#166668,#166669,#166670,#166671,#166672,
#166673,#166674,#166675,#166676,#166677,#166678,#166679,#166680,#166681,
#166682,#166683,#166684,#166685,#166686,#166687,#166688,#166689,#166690,
#166691,#166692,#166693,#166694,#166695,#166696,#166697,#166698,#166699,
#166700,#166701,#166702,#166703,#166704,#166705,#166706,#166707,#166708,
#166709,#166710,#166711,#166712,#166713,#166714,#166715,#166716,#166717,
#166718,#166719,#166720,#166721,#166722,#166723,#166724,#166725,#166726,
#166727,#166728,#166729,#166730,#166731,#166732,#166733,#166734,#166735,
#166736,#166737,#166738,#166739,#166740,#166741,#166742,#166743,#166744,
#166745,#166746,#166747,#166748,#166749,#166750,#166751,#166752),
 .UNSPECIFIED.,.F.,.F.,(4,3,3,3,3,3,3,3,3,3,3,3,3,3,3,3,3,3,3,3,3,3,3,3,
3,3,3,3,3,3,3,3,3,3,3,3,3,3,3,3,3,3,3,3,3,3,3,3,3,3,3,3,3,3,3,3,3,3,3,3,
3,3,3,3,3,3,3,3,3,3,3,3,3,3,3,3,3,3,3,3,3,3,4),(-1480.64108893606,-1480.60903187651,
-1480.52907457638,-1480.44921177914,-1480.36942595667,-1480.28969964147,
-1480.21001541318,-1480.13034442696,-1480.05067697343,-1479.97099732262,
-1479.89128974022,-1479.81149451115,-1479.73165016944,-1479.6516917424,
-1479.60929586579,-1479.52933856566,-1479.44947576842,-1479.36968994594,
-1479.28996363075,-1479.21027940245,-1479.13060841623,-1479.05094096271,
-1478.97126131189,-1478.8915537295,-1478.81175850042,-1478.73191415871,
-1478.65195573167,-1478.60955985507,-1478.52960255494,-1478.4497397577,
-1478.36995393522,-1478.29022762003,-1478.21054339173,-1478.13087240551,
-1478.05120495199,-1477.97152530117,-1477.89181771878,-1477.8120224897,
-1477.73217814799,-1477.65221972095,-1477.60982384435,-1477.52986654422,
-1477.45000374698,-1477.3702179245,-1477.29049160931,-1477.21080738102,
-1477.13113639479,-1477.05146894127,-1476.97178929045,-1476.89208170806,
-1476.81228647898,-1476.73244213728,-1476.65248371023,-1476.61008783363,
-1476.5301305335,-1476.45026773626,-1476.37048191378,-1476.29075559859,
-1476.21107137029,-1476.13140038407,-1476.05173293055,-1475.97205327973,
-1475.89234569734,-1475.81255046826,-1475.73270612655,-1475.65274769951,
-1475.61035182291,-1475.53039452278,-1475.45053172553,-1475.37074590306,
-1475.29101958787,-1475.21133535957,-1475.13166437335,-1475.05199691982,
-1474.972317269,-1474.89260968661,-1474.81281445753,-1474.73297011582,-1474.65301168878,
-1474.61061581219,-1474.50625453886,-1474.40403233292,-1474.3579036915),
 .UNSPECIFIED.);
#1433=B_SPLINE_CURVE_WITH_KNOTS('',3,(#166754,#166755,#166756,#166757,#166758,
#166759,#166760,#166761,#166762,#166763),.UNSPECIFIED.,.F.,.F.,(4,1,1,1,
1,1,1,4),(-1474.35790362888,-1473.61087980147,-1472.61114379075,-1471.61140778003,
-1470.61167176931,-1469.61193575859,-1468.61219974787,-1468.0747183217),
 .UNSPECIFIED.);
#1434=B_SPLINE_CURVE_WITH_KNOTS('',3,(#166765,#166766,#166767,#166768,#166769,
#166770,#166771,#166772,#166773,#166774,#166775,#166776,#166777,#166778,
#166779,#166780,#166781,#166782,#166783,#166784,#166785,#166786,#166787,
#166788,#166789,#166790,#166791,#166792,#166793,#166794,#166795,#166796,
#166797,#166798,#166799,#166800,#166801,#166802,#166803,#166804,#166805,
#166806,#166807,#166808,#166809,#166810,#166811,#166812,#166813,#166814,
#166815,#166816,#166817,#166818,#166819,#166820,#166821,#166822,#166823,
#166824,#166825,#166826,#166827,#166828,#166829,#166830,#166831,#166832,
#166833,#166834,#166835,#166836,#166837,#166838,#166839,#166840,#166841,
#166842,#166843,#166844,#166845,#166846,#166847,#166848,#166849,#166850,
#166851,#166852,#166853,#166854,#166855,#166856,#166857,#166858,#166859,
#166860,#166861,#166862,#166863,#166864,#166865,#166866,#166867,#166868,
#166869,#166870,#166871,#166872,#166873,#166874,#166875,#166876,#166877,
#166878,#166879,#166880,#166881,#166882,#166883,#166884,#166885,#166886,
#166887,#166888,#166889,#166890,#166891,#166892,#166893,#166894,#166895,
#166896,#166897,#166898,#166899,#166900,#166901,#166902,#166903,#166904,
#166905,#166906,#166907,#166908,#166909,#166910,#166911,#166912,#166913,
#166914,#166915,#166916,#166917,#166918,#166919,#166920,#166921,#166922,
#166923,#166924,#166925,#166926,#166927,#166928,#166929,#166930,#166931,
#166932,#166933,#166934,#166935,#166936,#166937,#166938,#166939,#166940,
#166941,#166942,#166943,#166944,#166945,#166946,#166947,#166948,#166949,
#166950,#166951,#166952,#166953,#166954,#166955,#166956,#166957,#166958,
#166959,#166960,#166961,#166962,#166963,#166964,#166965,#166966,#166967,
#166968,#166969,#166970,#166971,#166972,#166973,#166974,#166975,#166976,
#166977,#166978,#166979,#166980,#166981,#166982,#166983,#166984,#166985,
#166986,#166987,#166988,#166989,#166990,#166991,#166992,#166993,#166994,
#166995,#166996,#166997,#166998,#166999,#167000,#167001,#167002,#167003,
#167004,#167005,#167006,#167007,#167008,#167009,#167010,#167011),
 .UNSPECIFIED.,.F.,.F.,(4,3,3,3,3,3,3,3,3,3,3,3,3,3,3,3,3,3,3,3,3,3,3,3,
3,3,3,3,3,3,3,3,3,3,3,3,3,3,3,3,3,3,3,3,3,3,3,3,3,3,3,3,3,3,3,3,3,3,3,3,
3,3,3,3,3,3,3,3,3,3,3,3,3,3,3,3,3,3,3,3,3,3,4),(-1468.07471811664,-1467.98983128614,
-1467.9047850356,-1467.81949107158,-1467.73406381551,-1467.64842972939,
-1467.61246373715,-1467.53250643702,-1467.45264363978,-1467.37285781731,
-1467.29313150212,-1467.21344727382,-1467.1337762876,-1467.05410883408,
-1466.97442918327,-1466.89472160087,-1466.8149263718,-1466.73508203009,
-1466.65512360305,-1466.61272772643,-1466.5327704263,-1466.45290762906,
-1466.37312180658,-1466.29339549139,-1466.2137112631,-1466.13404027688,
-1466.05437282335,-1465.97469317253,-1465.89498559014,-1465.81519036106,
-1465.73534601936,-1465.65538759231,-1465.61299171571,-1465.53303441558,
-1465.45317161834,-1465.37338579586,-1465.29365948067,-1465.21397525237,
-1465.13430426615,-1465.05463681262,-1464.97495716181,-1464.89524957941,
-1464.81545435034,-1464.73561000863,-1464.65565158158,-1464.61325570499,
-1464.53329840486,-1464.45343560762,-1464.37364978514,-1464.29392346995,
-1464.21423924166,-1464.13456825544,-1464.05490080191,-1463.97522115109,
-1463.8955135687,-1463.81571833962,-1463.73587399792,-1463.65591557087,
-1463.61351969427,-1463.53356239414,-1463.4536995969,-1463.37391377442,
-1463.29418745923,-1463.21450323093,-1463.13483224471,-1463.05516479119,
-1462.97548514037,-1462.89577755797,-1462.8159823289,-1462.73613798719,
-1462.65617956014,-1462.61378368355,-1462.53501718464,-1462.45634485605,
-1462.37774820447,-1462.29921262633,-1462.22070988667,-1462.14222340191,
-1462.06373660319,-1461.98520236571,-1461.90664134508,-1461.82800041734,
-1461.79153301452),.UNSPECIFIED.);
#1435=B_SPLINE_CURVE_WITH_KNOTS('',3,(#167013,#167014,#167015,#167016,#167017,
#167018,#167019,#167020,#167021,#167022,#167023,#167024),.UNSPECIFIED.,
 .F.,.F.,(4,2,1,1,1,1,1,1,4),(-1461.79153301452,-1461.61404767283,-1460.61431166211,
-1459.61457565139,-1458.61483964067,-1457.61510362995,-1456.61536761923,
-1455.61563160851,-1455.50834770734),.UNSPECIFIED.);
#1436=B_SPLINE_CURVE_WITH_KNOTS('',3,(#167026,#167027,#167028,#167029,#167030,
#167031,#167032,#167033,#167034,#167035),.UNSPECIFIED.,.F.,.F.,(4,1,1,1,
1,1,1,4),(-1455.50834770734,-1454.61589559779,-1453.61615958707,-1452.61642357635,
-1451.61668756563,-1450.61695155491,-1449.61721554419,-1449.22516240016),
 .UNSPECIFIED.);
#1437=B_SPLINE_CURVE_WITH_KNOTS('',3,(#167037,#167038,#167039,#167040,#167041,
#167042,#167043,#167044,#167045,#167046),.UNSPECIFIED.,.F.,.F.,(4,1,1,1,
1,1,1,4),(-1449.22516240016,-1448.61747953347,-1447.61774352275,-1446.61800751203,
-1445.61827150131,-1444.61853549059,-1443.61879947987,-1442.94197709298),
 .UNSPECIFIED.);
#1438=B_SPLINE_CURVE_WITH_KNOTS('',3,(#167048,#167049,#167050,#167051,#167052,
#167053,#167054,#167055,#167056,#167057),.UNSPECIFIED.,.F.,.F.,(4,1,1,1,
1,1,1,4),(-1442.94197709298,-1442.61906346915,-1441.61932745843,-1440.61959144771,
-1439.61985543699,-1438.62011942627,-1437.62038341555,-1436.65879704426),
 .UNSPECIFIED.);
#1439=B_SPLINE_CURVE_WITH_KNOTS('',3,(#167059,#167060,#167061,#167062,#167063,
#167064,#167065,#167066,#167067,#167068,#167069,#167070,#167071,#167072,
#167073,#167074,#167075,#167076,#167077,#167078,#167079,#167080,#167081,
#167082,#167083,#167084,#167085,#167086,#167087,#167088,#167089,#167090,
#167091,#167092,#167093,#167094,#167095,#167096,#167097,#167098,#167099,
#167100,#167101,#167102,#167103,#167104,#167105,#167106,#167107,#167108,
#167109,#167110,#167111,#167112,#167113,#167114,#167115,#167116,#167117,
#167118,#167119,#167120,#167121,#167122,#167123,#167124,#167125,#167126,
#167127,#167128,#167129,#167130,#167131,#167132,#167133,#167134,#167135,
#167136,#167137,#167138,#167139,#167140,#167141,#167142,#167143,#167144,
#167145,#167146,#167147,#167148,#167149,#167150,#167151,#167152,#167153,
#167154,#167155,#167156,#167157,#167158,#167159,#167160,#167161,#167162,
#167163,#167164,#167165,#167166,#167167,#167168,#167169,#167170,#167171,
#167172,#167173,#167174,#167175,#167176,#167177,#167178,#167179,#167180,
#167181,#167182,#167183,#167184,#167185,#167186,#167187,#167188,#167189,
#167190,#167191,#167192,#167193,#167194,#167195,#167196,#167197,#167198,
#167199,#167200,#167201,#167202,#167203,#167204,#167205,#167206,#167207,
#167208,#167209,#167210,#167211,#167212,#167213,#167214,#167215,#167216,
#167217,#167218,#167219,#167220,#167221,#167222,#167223,#167224,#167225,
#167226,#167227,#167228,#167229,#167230,#167231,#167232,#167233,#167234,
#167235,#167236,#167237,#167238,#167239,#167240,#167241,#167242,#167243,
#167244,#167245,#167246,#167247,#167248,#167249,#167250,#167251,#167252,
#167253,#167254,#167255,#167256,#167257,#167258,#167259,#167260,#167261,
#167262,#167263,#167264,#167265,#167266,#167267,#167268,#167269,#167270,
#167271,#167272,#167273,#167274,#167275,#167276,#167277,#167278,#167279,
#167280,#167281,#167282,#167283,#167284,#167285,#167286,#167287,#167288,
#167289,#167290,#167291,#167292,#167293,#167294,#167295,#167296,#167297,
#167298,#167299,#167300,#167301,#167302,#167303,#167304,#167305),
 .UNSPECIFIED.,.F.,.F.,(4,3,3,3,3,3,3,3,3,3,3,3,3,3,3,3,3,3,3,3,3,3,3,3,
3,3,3,3,3,3,3,3,3,3,3,3,3,3,3,3,3,3,3,3,3,3,3,3,3,3,3,3,3,3,3,3,3,3,3,3,
3,3,3,3,3,3,3,3,3,3,3,3,3,3,3,3,3,3,3,3,3,3,4),(-1436.6587917858,-1436.62064740483,
-1436.5406901047,-1436.46082730746,-1436.38104148498,-1436.30131516979,
-1436.22163094149,-1436.14195995527,-1436.06229250175,-1435.98261285093,
-1435.90290526854,-1435.82311003946,-1435.74326569775,-1435.66330727071,
-1435.62091139411,-1435.54095409398,-1435.46109129674,-1435.38130547426,
-1435.30157915907,-1435.22189493077,-1435.14222394455,-1435.06255649103,
-1434.98287684021,-1434.90316925782,-1434.82337402874,-1434.74352968703,
-1434.66357125999,-1434.62117538339,-1434.54121808326,-1434.46135528602,
-1434.38156946354,-1434.30184314835,-1434.22215892005,-1434.14248793383,
-1434.06282048031,-1433.98314082949,-1433.9034332471,-1433.82363801802,
-1433.74379367631,-1433.66383524926,-1433.62143937267,-1433.54148207254,
-1433.4616192753,-1433.38183345282,-1433.30210713763,-1433.22242290934,
-1433.14275192312,-1433.06308446959,-1432.98340481877,-1432.90369723638,
-1432.8239020073,-1432.7440576656,-1432.66409923855,-1432.62170336195,-1432.54174606182,
-1432.46188326458,-1432.3820974421,-1432.30237112691,-1432.22268689861,
-1432.14301591239,-1432.06334845887,-1431.98366880805,-1431.90396122566,
-1431.82416599658,-1431.74432165487,-1431.66436322783,-1431.62196735123,
-1431.5420100511,-1431.46214725386,-1431.38236143138,-1431.30263511619,
-1431.2229508879,-1431.14327990167,-1431.06361244815,-1430.98393279733,
-1430.90422521494,-1430.82442998586,-1430.74458564415,-1430.66462721711,
-1430.62223134051,-1430.51675163816,-1430.41361228529,-1430.37560656682),
 .UNSPECIFIED.);
#1440=B_SPLINE_CURVE_WITH_KNOTS('',3,(#167307,#167308,#167309,#167310,#167311,
#167312,#167313,#167314,#167315,#167316),.UNSPECIFIED.,.F.,.F.,(4,1,1,1,
1,1,1,4),(-1430.37560647862,-1429.62249532979,-1428.62275931907,-1427.62302330835,
-1426.62328729763,-1425.62355128691,-1424.62381527619,-1424.09242117144),
 .UNSPECIFIED.);
#1441=B_SPLINE_CURVE_WITH_KNOTS('',3,(#167318,#167319,#167320,#167321,#167322,
#167323,#167324,#167325,#167326,#167327),.UNSPECIFIED.,.F.,.F.,(4,1,1,1,
1,1,1,4),(-1424.09242117144,-1423.62407926547,-1422.62434325475,-1421.62460724403,
-1420.62487123331,-1419.62513522259,-1418.62539921187,-1417.80924068802),
 .UNSPECIFIED.);
#1442=B_SPLINE_CURVE_WITH_KNOTS('',3,(#167329,#167330,#167331,#167332,#167333,
#167334,#167335,#167336,#167337,#167338,#167339,#167340,#167341,#167342,
#167343,#167344,#167345,#167346,#167347,#167348,#167349,#167350,#167351,
#167352,#167353,#167354,#167355,#167356,#167357,#167358,#167359,#167360,
#167361,#167362,#167363,#167364,#167365,#167366,#167367,#167368,#167369,
#167370,#167371,#167372,#167373,#167374,#167375,#167376,#167377,#167378,
#167379,#167380,#167381,#167382,#167383,#167384,#167385,#167386,#167387,
#167388,#167389,#167390,#167391,#167392,#167393,#167394,#167395,#167396,
#167397,#167398,#167399,#167400,#167401,#167402,#167403,#167404,#167405,
#167406,#167407,#167408,#167409,#167410,#167411,#167412,#167413,#167414,
#167415,#167416,#167417,#167418,#167419,#167420,#167421,#167422,#167423,
#167424,#167425,#167426,#167427,#167428,#167429,#167430,#167431,#167432,
#167433,#167434,#167435,#167436,#167437,#167438,#167439,#167440,#167441,
#167442,#167443,#167444,#167445,#167446,#167447,#167448,#167449,#167450,
#167451,#167452,#167453,#167454,#167455,#167456,#167457,#167458,#167459,
#167460,#167461,#167462,#167463,#167464,#167465,#167466,#167467,#167468,
#167469,#167470,#167471,#167472,#167473,#167474,#167475,#167476,#167477,
#167478,#167479,#167480,#167481,#167482,#167483,#167484,#167485,#167486,
#167487,#167488,#167489,#167490,#167491,#167492,#167493,#167494,#167495,
#167496,#167497,#167498,#167499,#167500,#167501,#167502,#167503,#167504,
#167505,#167506,#167507,#167508,#167509,#167510,#167511,#167512,#167513,
#167514,#167515,#167516,#167517,#167518,#167519,#167520,#167521,#167522,
#167523,#167524,#167525,#167526,#167527,#167528,#167529,#167530,#167531,
#167532,#167533,#167534,#167535,#167536,#167537,#167538,#167539,#167540,
#167541,#167542,#167543,#167544,#167545,#167546,#167547,#167548,#167549,
#167550,#167551,#167552,#167553,#167554,#167555,#167556,#167557,#167558,
#167559,#167560,#167561,#167562,#167563,#167564,#167565,#167566,#167567,
#167568,#167569,#167570,#167571,#167572),.UNSPECIFIED.,.F.,.F.,(4,3,3,3,
3,3,3,3,3,3,3,3,3,3,3,3,3,3,3,3,3,3,3,3,3,3,3,3,3,3,3,3,3,3,3,3,3,3,3,3,
3,3,3,3,3,3,3,3,3,3,3,3,3,3,3,3,3,3,3,3,3,3,3,3,3,3,3,3,3,3,3,3,3,3,3,3,
3,3,3,3,3,4),(-1417.80923586426,-1417.689114353,-1417.62566320115,-1417.54570590102,
-1417.46584310378,-1417.3860572813,-1417.30633096611,-1417.22664673781,
-1417.14697575159,-1417.06730829807,-1416.98762864725,-1416.90792106486,
-1416.82812583578,-1416.74828149407,-1416.66832306702,-1416.62592719043,
-1416.5459698903,-1416.46610709306,-1416.38632127058,-1416.30659495539,
-1416.22691072709,-1416.14723974087,-1416.06757228735,-1415.98789263653,
-1415.90818505414,-1415.82838982506,-1415.74854548335,-1415.66858705631,
-1415.62619117971,-1415.54623387958,-1415.46637108234,-1415.38658525986,
-1415.30685894467,-1415.22717471637,-1415.14750373015,-1415.06783627663,
-1414.98815662581,-1414.90844904342,-1414.82865381434,-1414.74880947263,
-1414.66885104559,-1414.62645516899,-1414.54649786886,-1414.46663507162,
-1414.38684924914,-1414.30712293395,-1414.22743870566,-1414.14776771943,
-1414.06810026591,-1413.98842061509,-1413.9087130327,-1413.82891780362,
-1413.74907346191,-1413.66911503487,-1413.62671915827,-1413.54676185814,
-1413.4668990609,-1413.38711323842,-1413.30738692323,-1413.22770269494,
-1413.14803170871,-1413.06836425519,-1412.98868460437,-1412.90897702198,
-1412.8291817929,-1412.74933745119,-1412.66937902415,-1412.62698314755,
-1412.54702584742,-1412.46716305018,-1412.38737722771,-1412.30765091251,
-1412.22796668422,-1412.148295698,-1412.06862824447,-1411.98894859366,-1411.90924101126,
-1411.82944578219,-1411.74960144048,-1411.66964301343,-1411.62724713683,
-1411.52605055708),.UNSPECIFIED.);
#1443=B_SPLINE_CURVE_WITH_KNOTS('',3,(#167574,#167575,#167576,#167577,#167578,
#167579,#167580,#167581,#167582,#167583),.UNSPECIFIED.,.F.,.F.,(4,1,1,1,
1,1,1,4),(-1411.52604145674,-1410.62751112611,-1409.62777511538,-1408.62803910466,
-1407.62830309394,-1406.62856708322,-1405.6288310725,-1405.24287268663),
 .UNSPECIFIED.);
#1444=B_SPLINE_CURVE_WITH_KNOTS('',3,(#167585,#167586,#167587,#167588,#167589,
#167590,#167591,#167592,#167593,#167594,#167595,#167596,#167597,#167598,
#167599,#167600,#167601,#167602,#167603,#167604,#167605,#167606,#167607,
#167608,#167609,#167610,#167611,#167612,#167613,#167614,#167615,#167616,
#167617,#167618,#167619,#167620,#167621,#167622,#167623,#167624,#167625,
#167626,#167627,#167628,#167629,#167630,#167631,#167632,#167633,#167634,
#167635,#167636,#167637,#167638,#167639,#167640,#167641,#167642,#167643,
#167644,#167645,#167646,#167647,#167648,#167649,#167650,#167651,#167652,
#167653,#167654,#167655,#167656,#167657,#167658,#167659,#167660,#167661,
#167662,#167663,#167664,#167665,#167666,#167667,#167668,#167669,#167670,
#167671,#167672,#167673,#167674,#167675,#167676,#167677,#167678,#167679,
#167680,#167681,#167682,#167683,#167684,#167685,#167686,#167687,#167688,
#167689,#167690,#167691,#167692,#167693,#167694,#167695,#167696,#167697,
#167698,#167699,#167700,#167701,#167702,#167703,#167704,#167705,#167706,
#167707,#167708,#167709,#167710,#167711,#167712,#167713,#167714,#167715,
#167716,#167717,#167718,#167719,#167720,#167721,#167722,#167723,#167724,
#167725,#167726,#167727,#167728,#167729,#167730,#167731,#167732,#167733,
#167734,#167735,#167736,#167737,#167738,#167739,#167740,#167741,#167742,
#167743,#167744,#167745,#167746,#167747,#167748,#167749,#167750,#167751,
#167752,#167753,#167754,#167755,#167756,#167757,#167758,#167759,#167760,
#167761,#167762,#167763,#167764,#167765,#167766,#167767,#167768,#167769,
#167770,#167771,#167772,#167773,#167774,#167775,#167776,#167777,#167778,
#167779,#167780,#167781,#167782,#167783,#167784,#167785,#167786,#167787,
#167788,#167789,#167790,#167791,#167792,#167793,#167794,#167795,#167796,
#167797,#167798,#167799,#167800,#167801,#167802,#167803,#167804,#167805,
#167806,#167807,#167808,#167809,#167810,#167811,#167812,#167813,#167814,
#167815,#167816,#167817,#167818,#167819,#167820,#167821,#167822,#167823,
#167824,#167825,#167826,#167827,#167828,#167829,#167830,#167831),
 .UNSPECIFIED.,.F.,.F.,(4,3,3,3,3,3,3,3,3,3,3,3,3,3,3,3,3,3,3,3,3,3,3,3,
3,3,3,3,3,3,3,3,3,3,3,3,3,3,3,3,3,3,3,3,3,3,3,3,3,3,3,3,3,3,3,3,3,3,3,3,
3,3,3,3,3,3,3,3,3,3,3,3,3,3,3,3,3,3,3,3,3,3,4),(-1405.2428652499,-1405.16239569195,
-1405.08191404014,-1405.00140562355,-1404.92085575786,-1404.840199036,-1404.75948345872,
-1404.67863759454,-1404.62909506178,-1404.54913776165,-1404.46927496441,
-1404.38948914194,-1404.30976282674,-1404.23007859845,-1404.15040761223,
-1404.0707401587,-1403.99106050789,-1403.9113529255,-1403.83155769642,-1403.75171335471,
-1403.67175492767,-1403.62935905106,-1403.54940175093,-1403.46953895369,
-1403.38975313121,-1403.31002681602,-1403.23034258773,-1403.1506716015,
-1403.07100414798,-1402.99132449716,-1402.91161691477,-1402.83182168569,
-1402.75197734399,-1402.67201891694,-1402.62962304034,-1402.54966574021,
-1402.46980294297,-1402.39001712049,-1402.3102908053,-1402.230606577,-1402.15093559078,
-1402.07126813726,-1401.99158848644,-1401.91188090405,-1401.83208567497,
-1401.75224133326,-1401.67228290621,-1401.62988702962,-1401.54992972949,
-1401.47006693225,-1401.39028110977,-1401.31055479458,-1401.23087056629,
-1401.15119958006,-1401.07153212654,-1400.99185247572,-1400.91214489333,
-1400.83234966425,-1400.75250532255,-1400.6725468955,-1400.6301510189,-1400.55019371877,
-1400.47033092153,-1400.39054509905,-1400.31081878386,-1400.23113455556,
-1400.15146356934,-1400.07179611582,-1399.992116465,-1399.9124088826,-1399.83261365353,
-1399.75276931182,-1399.67281088477,-1399.63041500818,-1399.546573125,-1399.46682601498,
-1399.38715383661,-1399.30754071169,-1399.22797080243,-1399.14842137439,
-1399.0688836793,-1398.98932729873,-1398.95967994272),.UNSPECIFIED.);
#1445=B_SPLINE_CURVE_WITH_KNOTS('',3,(#167833,#167834,#167835,#167836,#167837,
#167838,#167839,#167840,#167841,#167842),.UNSPECIFIED.,.F.,.F.,(4,1,1,1,
1,1,1,4),(-1398.9596726741,-1398.63067899746,-1397.63094298674,-1396.63120697602,
-1395.6314709653,-1394.63173495458,-1393.63199894386,-1392.67650054561),
 .UNSPECIFIED.);
#1446=B_SPLINE_CURVE_WITH_KNOTS('',3,(#167844,#167845,#167846,#167847,#167848,
#167849,#167850,#167851,#167852,#167853,#167854,#167855,#167856,#167857,
#167858,#167859,#167860,#167861,#167862,#167863,#167864,#167865,#167866,
#167867,#167868,#167869,#167870,#167871,#167872,#167873,#167874,#167875,
#167876,#167877,#167878,#167879,#167880,#167881,#167882,#167883,#167884,
#167885,#167886,#167887,#167888,#167889,#167890,#167891,#167892,#167893,
#167894,#167895,#167896,#167897,#167898,#167899,#167900,#167901,#167902,
#167903,#167904,#167905,#167906,#167907,#167908,#167909,#167910,#167911,
#167912,#167913,#167914,#167915,#167916,#167917,#167918,#167919,#167920,
#167921,#167922,#167923,#167924,#167925,#167926,#167927,#167928,#167929,
#167930,#167931,#167932,#167933,#167934,#167935,#167936,#167937,#167938,
#167939,#167940,#167941,#167942,#167943,#167944,#167945,#167946,#167947,
#167948,#167949,#167950,#167951,#167952,#167953,#167954,#167955,#167956,
#167957,#167958,#167959,#167960,#167961,#167962,#167963,#167964,#167965,
#167966,#167967,#167968,#167969,#167970,#167971,#167972,#167973,#167974,
#167975,#167976,#167977,#167978,#167979,#167980,#167981,#167982,#167983,
#167984,#167985,#167986,#167987,#167988,#167989,#167990,#167991,#167992,
#167993,#167994,#167995,#167996,#167997,#167998,#167999,#168000,#168001,
#168002,#168003,#168004,#168005,#168006,#168007,#168008,#168009,#168010,
#168011,#168012,#168013,#168014,#168015,#168016,#168017,#168018,#168019,
#168020,#168021,#168022,#168023,#168024,#168025,#168026,#168027,#168028,
#168029,#168030,#168031,#168032,#168033,#168034,#168035,#168036,#168037,
#168038,#168039,#168040,#168041,#168042,#168043,#168044,#168045,#168046,
#168047,#168048,#168049,#168050,#168051,#168052,#168053,#168054,#168055,
#168056,#168057,#168058,#168059,#168060,#168061,#168062,#168063,#168064,
#168065,#168066,#168067,#168068,#168069,#168070,#168071,#168072,#168073,
#168074,#168075,#168076,#168077,#168078,#168079,#168080,#168081,#168082,
#168083,#168084,#168085,#168086,#168087,#168088,#168089,#168090),
 .UNSPECIFIED.,.F.,.F.,(4,3,3,3,3,3,3,3,3,3,3,3,3,3,3,3,3,3,3,3,3,3,3,3,
3,3,3,3,3,3,3,3,3,3,3,3,3,3,3,3,3,3,3,3,3,3,3,3,3,3,3,3,3,3,3,3,3,3,3,3,
3,3,3,3,3,3,3,3,3,3,3,3,3,3,3,3,3,3,3,3,3,3,4),(-1392.67649463554,-1392.63226293314,
-1392.55230563301,-1392.47244283577,-1392.3926570133,-1392.3129306981,-1392.23324646981,
-1392.15357548359,-1392.07390803006,-1391.99422837924,-1391.91452079685,
-1391.83472556777,-1391.75488122607,-1391.67492279902,-1391.63252692242,
-1391.55256962229,-1391.47270682505,-1391.39292100257,-1391.31319468738,
-1391.23351045909,-1391.15383947286,-1391.07417201934,-1390.99449236852,
-1390.91478478613,-1390.83498955705,-1390.75514521534,-1390.6751867883,
-1390.6327909117,-1390.55283361157,-1390.47297081433,-1390.39318499185,
-1390.31345867666,-1390.23377444837,-1390.15410346214,-1390.07443600862,
-1389.9947563578,-1389.91504877541,-1389.83525354633,-1389.75540920462,
-1389.67545077758,-1389.63305490098,-1389.55309760085,-1389.47323480361,
-1389.39344898113,-1389.31372266594,-1389.23403843764,-1389.15436745142,
-1389.0746999979,-1388.99502034708,-1388.91531276469,-1388.83551753561,
-1388.7556731939,-1388.67571476686,-1388.63331889026,-1388.55336159013,
-1388.47349879289,-1388.39371297041,-1388.31398665522,-1388.23430242692,
-1388.1546314407,-1388.07496398718,-1387.99528433636,-1387.91557675397,
-1387.83578152489,-1387.75593718318,-1387.67597875614,-1387.63358287954,
-1387.55362557941,-1387.47376278217,-1387.39397695969,-1387.3142506445,
-1387.2345664162,-1387.15489542998,-1387.07522797646,-1386.99554832564,
-1386.91584074324,-1386.83604551417,-1386.75620117246,-1386.67624274541,
-1386.63384686882,-1386.52717722615,-1386.42307878727,-1386.39330937843),
 .UNSPECIFIED.);
#1447=B_SPLINE_CURVE_WITH_KNOTS('',3,(#168092,#168093,#168094,#168095,#168096,
#168097,#168098,#168099,#168100,#168101),.UNSPECIFIED.,.F.,.F.,(4,1,1,1,
1,1,1,4),(-1386.39330932836,-1385.6341108581,-1384.63437484738,-1383.63463883666,
-1382.63490282594,-1381.63516681522,-1380.6354308045,-1380.11012402118),
 .UNSPECIFIED.);
#1448=B_SPLINE_CURVE_WITH_KNOTS('',3,(#168103,#168104,#168105,#168106,#168107,
#168108,#168109,#168110,#168111,#168112),.UNSPECIFIED.,.F.,.F.,(4,1,1,1,
1,1,1,4),(-1380.11012402118,-1379.63569479378,-1378.63595878306,-1377.63622277234,
-1376.63648676162,-1375.6367507509,-1374.63701474018,-1373.82694297653),
 .UNSPECIFIED.);
#1449=B_SPLINE_CURVE_WITH_KNOTS('',3,(#168114,#168115,#168116,#168117,#168118,
#168119,#168120,#168121,#168122,#168123,#168124,#168125,#168126,#168127,
#168128,#168129,#168130,#168131,#168132,#168133,#168134,#168135,#168136,
#168137,#168138,#168139,#168140,#168141,#168142,#168143,#168144,#168145,
#168146,#168147,#168148,#168149,#168150,#168151,#168152,#168153,#168154,
#168155,#168156,#168157,#168158,#168159,#168160,#168161,#168162,#168163,
#168164,#168165,#168166,#168167,#168168,#168169,#168170,#168171,#168172,
#168173,#168174,#168175,#168176,#168177,#168178,#168179,#168180,#168181,
#168182,#168183,#168184,#168185,#168186,#168187,#168188,#168189,#168190,
#168191,#168192,#168193,#168194,#168195,#168196,#168197,#168198,#168199,
#168200,#168201,#168202,#168203,#168204,#168205,#168206,#168207,#168208,
#168209,#168210,#168211,#168212,#168213,#168214,#168215,#168216,#168217,
#168218,#168219,#168220,#168221,#168222,#168223,#168224,#168225,#168226,
#168227,#168228,#168229,#168230,#168231,#168232,#168233,#168234,#168235,
#168236,#168237,#168238,#168239,#168240,#168241,#168242,#168243,#168244,
#168245,#168246,#168247,#168248,#168249,#168250,#168251,#168252,#168253,
#168254,#168255,#168256,#168257,#168258,#168259,#168260,#168261,#168262,
#168263,#168264,#168265,#168266,#168267,#168268,#168269,#168270,#168271,
#168272,#168273,#168274,#168275,#168276,#168277,#168278,#168279,#168280,
#168281,#168282,#168283,#168284,#168285,#168286,#168287,#168288,#168289,
#168290,#168291,#168292,#168293,#168294,#168295,#168296,#168297,#168298,
#168299,#168300,#168301,#168302,#168303,#168304,#168305,#168306,#168307,
#168308,#168309,#168310,#168311,#168312,#168313,#168314,#168315,#168316,
#168317,#168318,#168319,#168320,#168321,#168322,#168323,#168324,#168325,
#168326,#168327,#168328,#168329,#168330,#168331,#168332,#168333,#168334,
#168335,#168336,#168337,#168338,#168339,#168340,#168341,#168342,#168343,
#168344,#168345,#168346,#168347,#168348,#168349,#168350,#168351,#168352,
#168353,#168354,#168355,#168356,#168357),.UNSPECIFIED.,.F.,.F.,(4,3,3,3,
3,3,3,3,3,3,3,3,3,3,3,3,3,3,3,3,3,3,3,3,3,3,3,3,3,3,3,3,3,3,3,3,3,3,3,3,
3,3,3,3,3,3,3,3,3,3,3,3,3,3,3,3,3,3,3,3,3,3,3,3,3,3,3,3,3,3,3,3,3,3,3,3,
3,3,3,3,3,4),(-1373.826938714,-1373.70893907459,-1373.63727872946,-1373.55732142933,
-1373.47745863208,-1373.39767280961,-1373.31794649442,-1373.23826226612,
-1373.1585912799,-1373.07892382637,-1372.99924417556,-1372.91953659316,
-1372.83974136408,-1372.75989702238,-1372.67993859533,-1372.63754271874,
-1372.55758541861,-1372.47772262137,-1372.39793679889,-1372.3182104837,
-1372.23852625541,-1372.15885526918,-1372.07918781566,-1371.99950816484,
-1371.91980058245,-1371.84000535337,-1371.76016101166,-1371.68020258462,
-1371.63780670802,-1371.55784940789,-1371.47798661065,-1371.39820078817,
-1371.31847447298,-1371.23879024469,-1371.15911925846,-1371.07945180494,
-1370.99977215412,-1370.92006457173,-1370.84026934265,-1370.76042500095,
-1370.6804665739,-1370.6380706973,-1370.55811339717,-1370.47825059993,-1370.39846477745,
-1370.31873846226,-1370.23905423396,-1370.15938324774,-1370.07971579422,
-1370.0000361434,-1369.92032856101,-1369.84053333193,-1369.76068899022,
-1369.68073056317,-1369.63833468658,-1369.55837738645,-1369.47851458921,
-1369.39872876673,-1369.31900245154,-1369.23931822325,-1369.15964723702,
-1369.0799797835,-1369.00030013268,-1368.92059255029,-1368.84079732121,
-1368.7609529795,-1368.68099455246,-1368.63859867586,-1368.55864137573,
-1368.47877857849,-1368.39899275602,-1368.31926644082,-1368.23958221253,
-1368.15991122631,-1368.08024377278,-1368.00056412196,-1367.92085653957,
-1367.84106131049,-1367.76121696879,-1367.68125854174,-1367.63886266514,
-1367.54375340682),.UNSPECIFIED.);
#1450=B_SPLINE_CURVE_WITH_KNOTS('',3,(#168359,#168360,#168361,#168362,#168363,
#168364,#168365,#168366,#168367,#168368),.UNSPECIFIED.,.F.,.F.,(4,1,1,1,
1,1,1,4),(-1367.54374436809,-1366.63912665442,-1365.6393906437,-1364.63965463298,
-1363.63991862226,-1362.64018261154,-1361.64044660082,-1361.26057566531),
 .UNSPECIFIED.);
#1451=B_SPLINE_CURVE_WITH_KNOTS('',3,(#168370,#168371,#168372,#168373,#168374,
#168375,#168376,#168377,#168378,#168379,#168380,#168381,#168382,#168383,
#168384,#168385,#168386,#168387,#168388,#168389,#168390,#168391,#168392,
#168393,#168394,#168395,#168396,#168397,#168398,#168399,#168400,#168401,
#168402,#168403,#168404,#168405,#168406,#168407,#168408,#168409,#168410,
#168411,#168412,#168413,#168414,#168415,#168416,#168417,#168418,#168419,
#168420,#168421,#168422,#168423,#168424,#168425,#168426,#168427,#168428,
#168429,#168430,#168431,#168432,#168433,#168434,#168435,#168436,#168437,
#168438,#168439,#168440,#168441,#168442,#168443,#168444,#168445,#168446,
#168447,#168448,#168449,#168450,#168451,#168452,#168453,#168454,#168455,
#168456,#168457,#168458,#168459,#168460,#168461,#168462,#168463,#168464,
#168465,#168466,#168467,#168468,#168469,#168470,#168471,#168472,#168473,
#168474,#168475,#168476,#168477,#168478,#168479,#168480,#168481,#168482,
#168483,#168484,#168485,#168486,#168487,#168488,#168489,#168490,#168491,
#168492,#168493,#168494,#168495,#168496,#168497,#168498,#168499,#168500,
#168501,#168502,#168503,#168504,#168505,#168506,#168507,#168508,#168509,
#168510,#168511,#168512,#168513,#168514,#168515,#168516,#168517,#168518,
#168519,#168520,#168521,#168522,#168523,#168524,#168525,#168526,#168527,
#168528,#168529,#168530,#168531,#168532,#168533,#168534,#168535,#168536,
#168537,#168538,#168539,#168540,#168541,#168542,#168543,#168544,#168545,
#168546,#168547,#168548,#168549,#168550,#168551,#168552,#168553,#168554,
#168555,#168556,#168557,#168558,#168559,#168560,#168561,#168562,#168563,
#168564,#168565,#168566,#168567,#168568,#168569,#168570,#168571,#168572,
#168573,#168574,#168575,#168576,#168577,#168578,#168579,#168580,#168581,
#168582,#168583,#168584,#168585,#168586,#168587,#168588,#168589,#168590,
#168591,#168592,#168593,#168594,#168595,#168596,#168597,#168598,#168599,
#168600,#168601,#168602,#168603,#168604,#168605,#168606,#168607,#168608,
#168609,#168610,#168611,#168612,#168613,#168614,#168615,#168616),
 .UNSPECIFIED.,.F.,.F.,(4,3,3,3,3,3,3,3,3,3,3,3,3,3,3,3,3,3,3,3,3,3,3,3,
3,3,3,3,3,3,3,3,3,3,3,3,3,3,3,3,3,3,3,3,3,3,3,3,3,3,3,3,3,3,3,3,3,3,3,3,
3,3,3,3,3,3,3,3,3,3,3,3,3,3,3,3,3,3,3,3,3,3,4),(-1361.26056809964,-1361.18021176969,
-1361.09984657315,-1361.01945767722,-1360.93903023779,-1360.85849830864,
-1360.77790979235,-1360.69719015379,-1360.6407105901,-1360.56075328997,
-1360.48089049273,-1360.40110467025,-1360.32137835506,-1360.24169412676,
-1360.16202314054,-1360.08235568702,-1360.0026760362,-1359.9229684538,-1359.84317322473,
-1359.76332888302,-1359.68337045597,-1359.64097457938,-1359.56101727925,
-1359.48115448201,-1359.40136865953,-1359.32164234434,-1359.24195811604,
-1359.16228712982,-1359.0826196763,-1359.00294002548,-1358.92323244309,
-1358.84343721401,-1358.7635928723,-1358.68363444525,-1358.64123856866,
-1358.56128126853,-1358.48141847129,-1358.40163264881,-1358.32190633362,
-1358.24222210533,-1358.1625511191,-1358.08288366558,-1358.00320401476,
-1357.92349643237,-1357.84370120329,-1357.76385686159,-1357.68389843454,
-1357.64150255794,-1357.56154525781,-1357.48168246057,-1357.40189663809,
-1357.3221703229,-1357.24248609461,-1357.16281510838,-1357.08314765486,
-1357.00346800404,-1356.92376042165,-1356.84396519257,-1356.76412085086,
-1356.68416242382,-1356.64176654722,-1356.56180924709,-1356.48194644985,
-1356.40216062738,-1356.32243431218,-1356.24275008389,-1356.16307909767,
-1356.08341164414,-1356.00373199333,-1355.92402441093,-1355.84422918186,
-1355.76438484015,-1355.6844264131,-1355.6420305365,-1355.55894956849,-1355.47911297368,
-1355.39935227128,-1355.31965166306,-1355.23999539154,-1355.16036196506,
-1355.08074132298,-1355.00110516955,-1354.97738279246),.UNSPECIFIED.);
#1452=B_SPLINE_CURVE_WITH_KNOTS('',3,(#168618,#168619,#168620,#168621,#168622,
#168623,#168624,#168625,#168626,#168627),.UNSPECIFIED.,.F.,.F.,(4,1,1,1,
1,1,1,4),(-1354.97737532952,-1354.64229452578,-1353.64255851506,-1352.64282250434,
-1351.64308649362,-1350.6433504829,-1349.64361447218,-1348.69419748528),
 .UNSPECIFIED.);
#1453=B_SPLINE_CURVE_WITH_KNOTS('',3,(#168629,#168630,#168631,#168632,#168633,
#168634,#168635,#168636,#168637,#168638,#168639,#168640,#168641),
 .UNSPECIFIED.,.F.,.F.,(4,3,1,1,1,1,1,1,4),(-1348.69419748528,-1348.64387846146,
-1347.64414245074,-1346.64440644002,-1345.6446704293,-1344.64493441858,
-1343.64519840786,-1342.64546239714,-1342.4110121781),.UNSPECIFIED.);
#1454=B_SPLINE_CURVE_WITH_KNOTS('',3,(#168643,#168644,#168645,#168646,#168647,
#168648,#168649,#168650,#168651,#168652),.UNSPECIFIED.,.F.,.F.,(4,1,1,1,
1,1,1,4),(-1342.4110121781,-1341.64572638642,-1340.6459903757,-1339.64625436498,
-1338.64651835426,-1337.64678234354,-1336.64704633282,-1336.12782687092),
 .UNSPECIFIED.);
#1455=B_SPLINE_CURVE_WITH_KNOTS('',3,(#168654,#168655,#168656,#168657,#168658,
#168659,#168660,#168661,#168662,#168663),.UNSPECIFIED.,.F.,.F.,(4,1,1,1,
1,1,1,4),(-1336.12782687092,-1335.6473103221,-1334.64757431137,-1333.64783830065,
-1332.64810228993,-1331.64836627921,-1330.64863026849,-1329.84464524732),
 .UNSPECIFIED.);
#1456=B_SPLINE_CURVE_WITH_KNOTS('',3,(#168665,#168666,#168667,#168668,#168669,
#168670,#168671,#168672,#168673,#168674,#168675,#168676,#168677,#168678,
#168679,#168680,#168681,#168682,#168683,#168684,#168685,#168686,#168687,
#168688,#168689,#168690,#168691,#168692,#168693,#168694,#168695,#168696,
#168697,#168698,#168699,#168700,#168701,#168702,#168703,#168704,#168705,
#168706,#168707,#168708,#168709,#168710,#168711,#168712,#168713,#168714,
#168715,#168716,#168717,#168718,#168719,#168720,#168721,#168722,#168723,
#168724,#168725,#168726,#168727,#168728,#168729,#168730,#168731,#168732,
#168733,#168734,#168735,#168736,#168737,#168738,#168739,#168740,#168741,
#168742,#168743,#168744,#168745,#168746,#168747,#168748,#168749,#168750,
#168751,#168752,#168753,#168754,#168755,#168756,#168757,#168758,#168759,
#168760,#168761,#168762,#168763,#168764,#168765,#168766,#168767,#168768,
#168769,#168770,#168771,#168772,#168773,#168774,#168775,#168776,#168777,
#168778,#168779,#168780,#168781,#168782,#168783,#168784,#168785,#168786,
#168787,#168788,#168789,#168790,#168791,#168792,#168793,#168794,#168795,
#168796,#168797,#168798,#168799,#168800,#168801,#168802,#168803,#168804,
#168805,#168806,#168807,#168808,#168809,#168810,#168811,#168812,#168813,
#168814,#168815,#168816,#168817,#168818,#168819,#168820,#168821,#168822,
#168823,#168824,#168825,#168826,#168827,#168828,#168829,#168830,#168831,
#168832,#168833,#168834,#168835,#168836,#168837,#168838,#168839,#168840,
#168841,#168842,#168843,#168844,#168845,#168846,#168847,#168848,#168849,
#168850,#168851,#168852,#168853,#168854,#168855,#168856,#168857,#168858,
#168859,#168860,#168861,#168862,#168863,#168864,#168865,#168866,#168867,
#168868,#168869,#168870,#168871,#168872,#168873,#168874,#168875,#168876,
#168877,#168878,#168879,#168880,#168881,#168882,#168883,#168884,#168885,
#168886,#168887,#168888,#168889,#168890,#168891,#168892,#168893,#168894,
#168895,#168896,#168897,#168898,#168899,#168900,#168901,#168902,#168903,
#168904,#168905,#168906,#168907,#168908),.UNSPECIFIED.,.F.,.F.,(4,3,3,3,
3,3,3,3,3,3,3,3,3,3,3,3,3,3,3,3,3,3,3,3,3,3,3,3,3,3,3,3,3,3,3,3,3,3,3,3,
3,3,3,3,3,3,3,3,3,3,3,3,3,3,3,3,3,3,3,3,3,3,3,3,3,3,3,3,3,3,3,3,3,3,3,3,
3,3,3,3,3,4),(-1329.84464156374,-1329.72859519301,-1329.64889425777,-1329.56893695764,
-1329.4890741604,-1329.40928833792,-1329.32956202273,-1329.24987779444,
-1329.17020680821,-1329.09053935469,-1329.01085970387,-1328.93115212148,
-1328.8513568924,-1328.7715125507,-1328.69155412365,-1328.64915824705,-1328.56920094692,
-1328.48933814968,-1328.4095523272,-1328.32982601201,-1328.25014178372,
-1328.17047079749,-1328.09080334397,-1328.01112369315,-1327.93141611076,
-1327.85162088168,-1327.77177653997,-1327.69181811293,-1327.64942223633,
-1327.5694649362,-1327.48960213896,-1327.40981631648,-1327.33009000129,
-1327.250405773,-1327.17073478677,-1327.09106733325,-1327.01138768243,-1326.93168010004,
-1326.85188487096,-1326.77204052925,-1326.69208210221,-1326.64968622561,
-1326.56972892548,-1326.48986612824,-1326.41008030576,-1326.33035399057,
-1326.25066976227,-1326.17099877605,-1326.09133132253,-1326.01165167171,
-1325.93194408932,-1325.85214886024,-1325.77230451853,-1325.69234609149,
-1325.64995021489,-1325.56999291476,-1325.49013011752,-1325.41034429504,
-1325.33061797985,-1325.25093375156,-1325.17126276533,-1325.09159531181,
-1325.01191566099,-1324.9322080786,-1324.85241284952,-1324.77256850782,
-1324.69261008077,-1324.65021420417,-1324.57025690404,-1324.4903941068,
-1324.41060828432,-1324.33088196913,-1324.25119774083,-1324.17152675461,
-1324.09185930109,-1324.01217965027,-1323.93247206787,-1323.8526768388,
-1323.77283249709,-1323.69287407004,-1323.65047819345,-1323.56145625656),
 .UNSPECIFIED.);
#1457=B_SPLINE_CURVE_WITH_KNOTS('',3,(#168910,#168911,#168912,#168913,#168914,
#168915,#168916,#168917,#168918,#168919),.UNSPECIFIED.,.F.,.F.,(4,1,1,1,
1,1,1,4),(-1323.56144747861,-1322.65074218273,-1321.65100617201,-1320.65127016129,
-1319.65153415057,-1318.65179813985,-1317.65206212913,-1317.27827860692),
 .UNSPECIFIED.);
#1458=B_SPLINE_CURVE_WITH_KNOTS('',3,(#168921,#168922,#168923,#168924,#168925,
#168926,#168927,#168928,#168929,#168930,#168931,#168932,#168933,#168934,
#168935,#168936,#168937,#168938,#168939,#168940,#168941,#168942,#168943,
#168944,#168945,#168946,#168947,#168948,#168949,#168950,#168951,#168952,
#168953,#168954,#168955,#168956,#168957,#168958,#168959,#168960,#168961,
#168962,#168963,#168964,#168965,#168966,#168967,#168968,#168969,#168970,
#168971,#168972,#168973,#168974,#168975,#168976,#168977,#168978,#168979,
#168980,#168981,#168982,#168983,#168984,#168985,#168986,#168987,#168988,
#168989,#168990,#168991,#168992,#168993,#168994,#168995,#168996,#168997,
#168998,#168999,#169000,#169001,#169002,#169003,#169004,#169005,#169006,
#169007,#169008,#169009,#169010,#169011,#169012,#169013,#169014,#169015,
#169016,#169017,#169018,#169019,#169020,#169021,#169022,#169023,#169024,
#169025,#169026,#169027,#169028,#169029,#169030,#169031,#169032,#169033,
#169034,#169035,#169036,#169037,#169038,#169039,#169040,#169041,#169042,
#169043,#169044,#169045,#169046,#169047,#169048,#169049,#169050,#169051,
#169052,#169053,#169054,#169055,#169056,#169057,#169058,#169059,#169060,
#169061,#169062,#169063,#169064,#169065,#169066,#169067,#169068,#169069,
#169070,#169071,#169072,#169073,#169074,#169075,#169076,#169077,#169078,
#169079,#169080,#169081,#169082,#169083,#169084,#169085,#169086,#169087,
#169088,#169089,#169090,#169091,#169092,#169093,#169094,#169095,#169096,
#169097,#169098,#169099,#169100,#169101,#169102,#169103,#169104,#169105,
#169106,#169107,#169108,#169109,#169110,#169111,#169112,#169113,#169114,
#169115,#169116,#169117,#169118,#169119,#169120,#169121,#169122,#169123,
#169124,#169125,#169126,#169127,#169128,#169129,#169130,#169131,#169132,
#169133,#169134,#169135,#169136,#169137,#169138,#169139,#169140,#169141,
#169142,#169143,#169144,#169145,#169146,#169147,#169148,#169149,#169150,
#169151,#169152,#169153,#169154,#169155,#169156,#169157,#169158,#169159,
#169160,#169161,#169162,#169163,#169164,#169165,#169166,#169167),
 .UNSPECIFIED.,.F.,.F.,(4,3,3,3,3,3,3,3,3,3,3,3,3,3,3,3,3,3,3,3,3,3,3,3,
3,3,3,3,3,3,3,3,3,3,3,3,3,3,3,3,3,3,3,3,3,3,3,3,3,3,3,3,3,3,3,3,3,3,3,3,
3,3,3,3,3,3,3,3,3,3,3,3,3,3,3,3,3,3,3,3,3,3,4),(-1317.27827094938,-1317.19802374242,
-1317.11777078609,-1317.03749709826,-1316.95718768734,-1316.8767760874,
-1316.79631011808,-1316.71571214589,-1316.65232611841,-1316.57236881828,
-1316.49250602104,-1316.41272019856,-1316.33299388337,-1316.25330965508,
-1316.17363866885,-1316.09397121533,-1316.01429156451,-1315.93458398212,
-1315.85478875304,-1315.77494441134,-1315.69498598429,-1315.65259010769,
-1315.57263280756,-1315.49277001032,-1315.41298418785,-1315.33325787265,
-1315.25357364436,-1315.17390265814,-1315.09423520461,-1315.01455555379,
-1314.9348479714,-1314.85505274232,-1314.77520840062,-1314.69524997357,
-1314.65285409697,-1314.57289679684,-1314.4930339996,-1314.41324817712,
-1314.33352186193,-1314.25383763363,-1314.17416664741,-1314.09449919389,
-1314.01481954307,-1313.93511196068,-1313.8553167316,-1313.77547238989,
-1313.69551396285,-1313.65311808625,-1313.57316078612,-1313.49329798888,
-1313.4135121664,-1313.33378585121,-1313.25410162291,-1313.17443063669,
-1313.09476318317,-1313.01508353235,-1312.93537594996,-1312.85558072088,
-1312.77573637917,-1312.69577795213,-1312.65338207553,-1312.5734247754,
-1312.49356197816,-1312.41377615568,-1312.33404984049,-1312.2543656122,
-1312.17469462597,-1312.09502717245,-1312.01534752163,-1311.93563993924,
-1311.85584471016,-1311.77600036845,-1311.69604194141,-1311.65364606481,
-1311.57132601198,-1311.49139611813,-1311.41154312364,-1311.3317513169,
-1311.25200502747,-1311.17228400148,-1311.09257687473,-1311.01285737541,
-1310.9950856422),.UNSPECIFIED.);
#1459=B_SPLINE_CURVE_WITH_KNOTS('',3,(#169169,#169170,#169171,#169172,#169173,
#169174,#169175,#169176,#169177,#169178),.UNSPECIFIED.,.F.,.F.,(4,1,1,1,
1,1,1,4),(-1310.99507802379,-1310.65391005409,-1309.65417404337,-1308.65443803265,
-1307.65470202193,-1306.65496601121,-1305.65523000049,-1304.71190033502),
 .UNSPECIFIED.);
#1460=B_SPLINE_CURVE_WITH_KNOTS('',3,(#169180,#169181,#169182,#169183,#169184,
#169185,#169186,#169187,#169188,#169189,#169190,#169191),.UNSPECIFIED.,
 .F.,.F.,(4,2,1,1,1,1,1,1,4),(-1304.71190033502,-1304.65549398977,-1303.65575797905,
-1302.65602196833,-1301.65628595761,-1300.65654994689,-1299.65681393617,
-1298.65707792545,-1298.42871502784),.UNSPECIFIED.);
#1461=B_SPLINE_CURVE_WITH_KNOTS('',3,(#169193,#169194,#169195,#169196,#169197,
#169198,#169199,#169200,#169201,#169202,#169203,#169204,#169205,#169206,
#169207,#169208,#169209,#169210,#169211,#169212,#169213,#169214,#169215,
#169216,#169217,#169218,#169219,#169220,#169221,#169222,#169223,#169224,
#169225,#169226,#169227,#169228,#169229,#169230,#169231,#169232,#169233,
#169234,#169235,#169236,#169237,#169238,#169239,#169240,#169241,#169242,
#169243,#169244,#169245,#169246,#169247,#169248,#169249,#169250,#169251,
#169252,#169253,#169254,#169255,#169256,#169257,#169258,#169259,#169260,
#169261,#169262,#169263,#169264,#169265,#169266,#169267,#169268,#169269,
#169270,#169271,#169272,#169273,#169274,#169275,#169276,#169277,#169278,
#169279,#169280,#169281,#169282,#169283,#169284,#169285,#169286,#169287,
#169288,#169289,#169290,#169291,#169292,#169293,#169294,#169295,#169296,
#169297,#169298,#169299,#169300,#169301,#169302,#169303,#169304,#169305,
#169306,#169307,#169308,#169309,#169310,#169311,#169312,#169313,#169314,
#169315,#169316,#169317,#169318,#169319,#169320,#169321,#169322,#169323,
#169324,#169325,#169326,#169327,#169328,#169329,#169330,#169331,#169332,
#169333,#169334,#169335,#169336,#169337,#169338,#169339,#169340,#169341,
#169342,#169343,#169344,#169345,#169346,#169347,#169348,#169349,#169350,
#169351,#169352,#169353,#169354,#169355,#169356,#169357,#169358,#169359,
#169360,#169361,#169362,#169363,#169364,#169365,#169366,#169367,#169368,
#169369,#169370,#169371,#169372,#169373,#169374,#169375,#169376,#169377,
#169378,#169379,#169380,#169381,#169382,#169383,#169384,#169385,#169386,
#169387,#169388,#169389,#169390,#169391,#169392,#169393,#169394,#169395,
#169396,#169397,#169398,#169399,#169400,#169401,#169402,#169403,#169404,
#169405,#169406,#169407,#169408,#169409,#169410,#169411,#169412,#169413,
#169414,#169415,#169416,#169417,#169418,#169419,#169420,#169421,#169422,
#169423,#169424,#169425,#169426,#169427,#169428,#169429,#169430,#169431,
#169432,#169433,#169434,#169435,#169436,#169437,#169438,#169439),
 .UNSPECIFIED.,.F.,.F.,(4,3,3,3,3,3,3,3,3,3,3,3,3,3,3,3,3,3,3,3,3,3,3,3,
3,3,3,3,3,3,3,3,3,3,3,3,3,3,3,3,3,3,3,3,3,3,3,3,3,3,3,3,3,3,3,3,3,3,3,3,
3,3,3,3,3,3,3,3,3,3,3,3,3,3,3,3,3,3,3,3,3,3,4),(-1298.42871502784,-1298.34998300514,
-1298.27130640284,-1298.19265969411,-1298.11402704446,-1298.03539196553,
-1297.95673796895,-1297.87800313816,-1297.79922586424,-1297.72033101374,
-1297.65734191473,-1297.5773846146,-1297.49752181736,-1297.41773599488,
-1297.33800967969,-1297.25832545139,-1297.17865446517,-1297.09898701165,
-1297.01930736083,-1296.93959977843,-1296.85980454936,-1296.77996020765,
-1296.7000017806,-1296.65760590401,-1296.57764860388,-1296.49778580664,
-1296.41799998416,-1296.33827366897,-1296.25858944067,-1296.17891845445,
-1296.09925100093,-1296.01957135011,-1295.93986376772,-1295.86006853864,
-1295.78022419693,-1295.70026576988,-1295.65786989329,-1295.57791259316,
-1295.49804979592,-1295.41826397344,-1295.33853765825,-1295.25885342996,
-1295.17918244374,-1295.09951499021,-1295.01983533939,-1294.940127757,-1294.86033252792,
-1294.78048818622,-1294.70052975917,-1294.65813388257,-1294.57817658244,
-1294.4983137852,-1294.41852796272,-1294.33880164753,-1294.25911741924,
-1294.17944643301,-1294.09977897949,-1294.02009932867,-1293.94039174628,
-1293.8605965172,-1293.78075217549,-1293.70079374845,-1293.65839787185,
-1293.57844057172,-1293.49857777448,-1293.41879195201,-1293.33906563681,
-1293.25938140852,-1293.1797104223,-1293.10004296877,-1293.02036331796,
-1292.94065573556,-1292.86086050649,-1292.78101616478,-1292.70105773773,
-1292.65866186113,-1292.57506558009,-1292.49160108778,-1292.405083246,-1292.32189762189,
-1292.23880404213,-1292.15581784198,-1292.14552972066),.UNSPECIFIED.);
#1462=B_SPLINE_CURVE_WITH_KNOTS('',3,(#169441,#169442,#169443,#169444,#169445,
#169446,#169447,#169448,#169449,#169450,#169451,#169452,#169453,#169454,
#169455,#169456,#169457,#169458,#169459,#169460,#169461,#169462,#169463,
#169464,#169465,#169466,#169467,#169468,#169469,#169470,#169471,#169472,
#169473,#169474,#169475,#169476,#169477,#169478,#169479,#169480,#169481,
#169482,#169483,#169484,#169485,#169486,#169487,#169488,#169489,#169490,
#169491,#169492,#169493,#169494,#169495,#169496,#169497,#169498,#169499,
#169500,#169501,#169502,#169503,#169504,#169505,#169506,#169507,#169508,
#169509,#169510,#169511,#169512,#169513,#169514,#169515,#169516,#169517,
#169518,#169519,#169520,#169521,#169522,#169523,#169524,#169525,#169526,
#169527,#169528,#169529,#169530,#169531,#169532,#169533,#169534,#169535,
#169536,#169537,#169538,#169539,#169540,#169541,#169542,#169543,#169544,
#169545,#169546,#169547,#169548,#169549,#169550,#169551,#169552,#169553,
#169554,#169555,#169556,#169557,#169558,#169559,#169560,#169561,#169562,
#169563,#169564,#169565,#169566,#169567,#169568,#169569,#169570,#169571,
#169572,#169573,#169574,#169575,#169576,#169577,#169578,#169579,#169580,
#169581,#169582,#169583,#169584,#169585,#169586,#169587,#169588,#169589,
#169590,#169591,#169592,#169593,#169594,#169595,#169596,#169597,#169598,
#169599,#169600,#169601,#169602,#169603,#169604,#169605,#169606,#169607,
#169608,#169609,#169610,#169611,#169612,#169613,#169614,#169615,#169616,
#169617,#169618,#169619,#169620,#169621,#169622,#169623,#169624,#169625,
#169626,#169627,#169628,#169629,#169630,#169631,#169632,#169633,#169634,
#169635,#169636,#169637,#169638,#169639,#169640,#169641,#169642,#169643,
#169644,#169645,#169646,#169647,#169648,#169649,#169650,#169651,#169652,
#169653,#169654,#169655,#169656,#169657,#169658,#169659,#169660,#169661,
#169662,#169663,#169664,#169665,#169666,#169667,#169668,#169669,#169670,
#169671,#169672,#169673,#169674,#169675,#169676,#169677,#169678,#169679,
#169680,#169681,#169682,#169683,#169684),.UNSPECIFIED.,.F.,.F.,(4,3,3,3,
3,3,3,3,3,3,3,3,3,3,3,3,3,3,3,3,3,3,3,3,3,3,3,3,3,3,3,3,3,3,3,3,3,3,3,3,
3,3,3,3,3,3,3,3,3,3,3,3,3,3,3,3,3,3,3,3,3,3,3,3,3,3,3,3,3,3,3,3,3,3,3,3,
3,3,3,3,3,4),(-1292.14552972052,-1292.06159838444,-1291.9775451088,-1291.89328099867,
-1291.80890705239,-1291.72433422119,-1291.65892585041,-1291.57896855028,
-1291.49910575303,-1291.41931993056,-1291.33959361536,-1291.25990938707,
-1291.18023840085,-1291.10057094732,-1291.0208912965,-1290.94118371411,
-1290.86138848503,-1290.78154414332,-1290.70158571627,-1290.65918983969,
-1290.57923253956,-1290.49936974232,-1290.41958391984,-1290.33985760465,
-1290.26017337635,-1290.18050239013,-1290.10083493661,-1290.02115528579,
-1289.9414477034,-1289.86165247432,-1289.78180813261,-1289.70184970556,
-1289.65945382897,-1289.57949652884,-1289.4996337316,-1289.41984790912,
-1289.34012159393,-1289.26043736564,-1289.18076637942,-1289.10109892589,
-1289.02141927507,-1288.94171169268,-1288.8619164636,-1288.7820721219,-1288.70211369485,
-1288.65971781825,-1288.57976051812,-1288.49989772088,-1288.4201118984,
-1288.34038558321,-1288.26070135491,-1288.18103036869,-1288.10136291517,
-1288.02168326435,-1287.94197568196,-1287.86218045288,-1287.78233611117,
-1287.70237768413,-1287.65998180753,-1287.5800245074,-1287.50016171016,
-1287.42037588769,-1287.34064957249,-1287.2609653442,-1287.18129435798,
-1287.10162690445,-1287.02194725364,-1286.94223967124,-1286.86244444217,
-1286.78260010046,-1286.70264167341,-1286.66024579681,-1286.5814358575,
-1286.5027205734,-1286.42267355341,-1286.34409775286,-1286.2655551761,-1286.18702926213,
-1286.10585804997,-1286.02728935643,-1285.94481688495,-1285.86234441348),
 .UNSPECIFIED.);
#1463=B_SPLINE_CURVE_WITH_KNOTS('',3,(#169686,#169687,#169688,#169689,#169690,
#169691,#169692,#169693,#169694,#169695,#169696,#169697),.UNSPECIFIED.,
 .F.,.F.,(4,2,1,1,1,1,1,1,4),(-1285.86234441348,-1285.66050978609,-1284.66077377537,
-1283.66103776465,-1282.66130175393,-1281.66156574321,-1280.66182973249,
-1279.66209372177,-1279.5791591063),.UNSPECIFIED.);
#1464=B_SPLINE_CURVE_WITH_KNOTS('',3,(#169699,#169700,#169701,#169702,#169703,
#169704,#169705,#169706,#169707,#169708),.UNSPECIFIED.,.F.,.F.,(4,1,1,1,
1,1,1,4),(-1279.5791591063,-1278.66235771105,-1277.66262170033,-1276.66288568961,
-1275.66314967889,-1274.66341366817,-1273.66367765745,-1273.29597379912),
 .UNSPECIFIED.);
#1465=B_SPLINE_CURVE_WITH_KNOTS('',3,(#169710,#169711,#169712,#169713,#169714,
#169715,#169716,#169717,#169718,#169719),.UNSPECIFIED.,.F.,.F.,(4,1,1,1,
1,1,1,4),(-1273.29597379912,-1272.66394164673,-1271.66420563601,-1270.66446962529,
-1269.66473361457,-1268.66499760385,-1267.66526159313,-1267.01278849194),
 .UNSPECIFIED.);
#1466=B_SPLINE_CURVE_WITH_KNOTS('',3,(#169721,#169722,#169723,#169724,#169725,
#169726,#169727,#169728,#169729,#169730,#169731,#169732,#169733,#169734,
#169735,#169736,#169737,#169738,#169739,#169740,#169741,#169742,#169743,
#169744,#169745,#169746,#169747,#169748,#169749,#169750,#169751,#169752,
#169753,#169754,#169755,#169756,#169757,#169758,#169759,#169760,#169761,
#169762,#169763,#169764,#169765,#169766,#169767,#169768,#169769,#169770,
#169771,#169772,#169773,#169774,#169775,#169776,#169777,#169778,#169779,
#169780,#169781,#169782,#169783,#169784,#169785,#169786,#169787,#169788,
#169789,#169790,#169791,#169792,#169793,#169794,#169795,#169796,#169797,
#169798,#169799,#169800,#169801,#169802,#169803,#169804,#169805,#169806,
#169807,#169808,#169809,#169810,#169811,#169812,#169813,#169814,#169815,
#169816,#169817,#169818,#169819,#169820,#169821,#169822,#169823,#169824,
#169825,#169826,#169827,#169828,#169829,#169830,#169831,#169832,#169833,
#169834,#169835,#169836,#169837,#169838,#169839,#169840,#169841,#169842,
#169843,#169844,#169845,#169846,#169847,#169848,#169849,#169850,#169851,
#169852,#169853,#169854,#169855,#169856,#169857,#169858,#169859,#169860,
#169861,#169862,#169863,#169864,#169865,#169866,#169867,#169868,#169869,
#169870,#169871,#169872,#169873,#169874,#169875,#169876,#169877,#169878,
#169879,#169880,#169881,#169882,#169883,#169884,#169885,#169886,#169887,
#169888,#169889,#169890,#169891,#169892,#169893,#169894,#169895,#169896,
#169897,#169898,#169899,#169900,#169901,#169902,#169903,#169904,#169905,
#169906,#169907,#169908,#169909,#169910,#169911,#169912,#169913,#169914,
#169915,#169916,#169917,#169918,#169919,#169920,#169921,#169922,#169923,
#169924,#169925,#169926,#169927,#169928,#169929,#169930,#169931,#169932,
#169933,#169934,#169935,#169936,#169937,#169938,#169939,#169940,#169941,
#169942,#169943,#169944,#169945,#169946,#169947,#169948,#169949,#169950,
#169951,#169952,#169953,#169954,#169955,#169956,#169957,#169958,#169959,
#169960,#169961,#169962,#169963,#169964),.UNSPECIFIED.,.F.,.F.,(4,3,3,3,
3,3,3,3,3,3,3,3,3,3,3,3,3,3,3,3,3,3,3,3,3,3,3,3,3,3,3,3,3,3,3,3,3,3,3,3,
3,3,3,3,3,3,3,3,3,3,3,3,3,3,3,3,3,3,3,3,3,3,3,3,3,3,3,3,3,3,3,3,3,3,3,3,
3,3,3,3,3,4),(-1267.01278836953,-1266.92108083957,-1266.8289234614,-1266.73617774725,
-1266.66552558241,-1266.58556828228,-1266.50570548503,-1266.42591966256,
-1266.34619334737,-1266.26650911907,-1266.18683813285,-1266.10717067932,
-1266.02749102851,-1265.94778344611,-1265.86798821703,-1265.78814387533,
-1265.70818544828,-1265.66578957169,-1265.58583227156,-1265.50596947432,
-1265.42618365184,-1265.34645733665,-1265.26677310836,-1265.18710212213,
-1265.10743466861,-1265.02775501779,-1264.9480474354,-1264.86825220632,
-1264.78840786461,-1264.70844943757,-1264.66605356097,-1264.58609626084,
-1264.5062334636,-1264.42644764112,-1264.34672132593,-1264.26703709764,
-1264.18736611141,-1264.10769865789,-1264.02801900707,-1263.94831142468,
-1263.8685161956,-1263.78867185389,-1263.70871342685,-1263.66631755025,
-1263.58636025012,-1263.50649745288,-1263.4267116304,-1263.34698531521,
-1263.26730108691,-1263.18763010069,-1263.10796264717,-1263.02828299635,
-1262.94857541396,-1262.86878018488,-1262.78893584317,-1262.70897741613,
-1262.66658153953,-1262.5866242394,-1262.50676144216,-1262.42697561969,
-1262.34724930449,-1262.2675650762,-1262.18789408998,-1262.10822663645,
-1262.02854698564,-1261.94883940325,-1261.86904417417,-1261.78919983246,
-1261.70924140542,-1261.66684552881,-1261.58761743001,-1261.50848331692,
-1261.42942502562,-1261.35042446142,-1261.27145775696,-1261.19250767568,
-1261.11355792414,-1261.03459221153,-1260.95554990908,-1260.87646805771,
-1260.79727140574,-1260.72960318476),.UNSPECIFIED.);
#1467=B_SPLINE_CURVE_WITH_KNOTS('',3,(#169966,#169967,#169968,#169969,#169970,
#169971,#169972,#169973,#169974,#169975,#169976,#169977,#169978),
 .UNSPECIFIED.,.F.,.F.,(4,3,1,1,1,1,1,1,4),(-1260.72960318476,-1260.66710951809,
-1259.66737350737,-1258.66763749665,-1257.66790148592,-1256.6681654752,
-1255.66842946448,-1254.66869345376,-1254.44641787758),.UNSPECIFIED.);
#1468=B_SPLINE_CURVE_WITH_KNOTS('',3,(#169980,#169981,#169982,#169983,#169984,
#169985,#169986,#169987,#169988,#169989,#169990,#169991,#169992,#169993,
#169994,#169995,#169996,#169997,#169998,#169999,#170000,#170001,#170002,
#170003,#170004,#170005,#170006,#170007,#170008,#170009,#170010,#170011,
#170012,#170013,#170014,#170015,#170016,#170017,#170018,#170019,#170020,
#170021,#170022,#170023,#170024,#170025,#170026,#170027,#170028,#170029,
#170030,#170031,#170032,#170033,#170034,#170035,#170036,#170037,#170038,
#170039,#170040,#170041,#170042,#170043,#170044,#170045,#170046,#170047,
#170048,#170049,#170050,#170051,#170052,#170053,#170054,#170055,#170056,
#170057,#170058,#170059,#170060,#170061,#170062,#170063,#170064,#170065,
#170066,#170067,#170068,#170069,#170070,#170071,#170072,#170073,#170074,
#170075,#170076,#170077,#170078,#170079,#170080,#170081,#170082,#170083,
#170084,#170085,#170086,#170087,#170088,#170089,#170090,#170091,#170092,
#170093,#170094,#170095,#170096,#170097,#170098,#170099,#170100,#170101,
#170102,#170103,#170104,#170105,#170106,#170107,#170108,#170109,#170110,
#170111,#170112,#170113,#170114,#170115,#170116,#170117,#170118,#170119,
#170120,#170121,#170122,#170123,#170124,#170125,#170126,#170127,#170128,
#170129,#170130,#170131,#170132,#170133,#170134,#170135,#170136,#170137,
#170138,#170139,#170140,#170141,#170142,#170143,#170144,#170145,#170146,
#170147,#170148,#170149,#170150,#170151,#170152,#170153,#170154,#170155,
#170156,#170157,#170158,#170159,#170160,#170161,#170162,#170163,#170164,
#170165,#170166,#170167,#170168,#170169,#170170,#170171,#170172,#170173,
#170174,#170175,#170176,#170177,#170178,#170179,#170180,#170181,#170182,
#170183,#170184,#170185,#170186,#170187,#170188,#170189,#170190,#170191,
#170192,#170193,#170194,#170195,#170196,#170197,#170198,#170199,#170200,
#170201,#170202,#170203,#170204,#170205,#170206,#170207,#170208,#170209,
#170210,#170211,#170212,#170213,#170214,#170215,#170216,#170217,#170218,
#170219,#170220,#170221,#170222,#170223),.UNSPECIFIED.,.F.,.F.,(4,3,3,3,
3,3,3,3,3,3,3,3,3,3,3,3,3,3,3,3,3,3,3,3,3,3,3,3,3,3,3,3,3,3,3,3,3,3,3,3,
3,3,3,3,3,3,3,3,3,3,3,3,3,3,3,3,3,3,3,3,3,3,3,3,3,3,3,3,3,3,3,3,3,3,3,3,
3,3,3,3,3,4),(-1254.44641787758,-1254.36770750134,-1254.28905430803,-1254.21043332721,
-1254.13182796515,-1254.05322171621,-1253.97459807584,-1253.89589448617,
-1253.81714979179,-1253.73828593555,-1253.66895744304,-1253.58900014291,
-1253.50913734567,-1253.42935152319,-1253.349625208,-1253.26994097971,-1253.19026999348,
-1253.11060253996,-1253.03092288914,-1252.95121530675,-1252.87142007767,
-1252.79157573596,-1252.71161730892,-1252.66922143232,-1252.58926413219,
-1252.50940133495,-1252.42961551247,-1252.34988919728,-1252.27020496899,
-1252.19053398276,-1252.11086652924,-1252.03118687842,-1251.95147929603,
-1251.87168406695,-1251.79183972524,-1251.7118812982,-1251.6694854216,-1251.58952812147,
-1251.50966532423,-1251.42987950175,-1251.35015318656,-1251.27046895826,
-1251.19079797204,-1251.11113051852,-1251.0314508677,-1250.95174328531,
-1250.87194805623,-1250.79210371452,-1250.71214528748,-1250.66974941088,
-1250.58979211075,-1250.50992931351,-1250.43014349103,-1250.35041717584,
-1250.27073294755,-1250.19106196132,-1250.1113945078,-1250.03171485698,
-1249.95200727459,-1249.87221204551,-1249.7923677038,-1249.71240927676,
-1249.67001340016,-1249.59005610003,-1249.51019330279,-1249.43040748032,
-1249.35068116512,-1249.27099693683,-1249.19132595061,-1249.11165849708,
-1249.03197884626,-1248.95227126387,-1248.87247603479,-1248.79263169309,
-1248.71267326604,-1248.67027738944,-1248.58646341498,-1248.50278431403,
-1248.41789637812,-1248.3345039439,-1248.24886825715,-1248.1632325704),
 .UNSPECIFIED.);
#1469=B_SPLINE_CURVE_WITH_KNOTS('',3,(#170225,#170226,#170227,#170228,#170229,
#170230,#170231,#170232,#170233,#170234,#170235,#170236,#170237,#170238,
#170239,#170240,#170241,#170242,#170243,#170244,#170245,#170246,#170247,
#170248,#170249,#170250,#170251,#170252,#170253,#170254,#170255,#170256,
#170257,#170258,#170259,#170260,#170261,#170262,#170263,#170264,#170265,
#170266,#170267,#170268,#170269,#170270,#170271,#170272,#170273,#170274,
#170275,#170276,#170277,#170278,#170279,#170280,#170281,#170282,#170283,
#170284,#170285,#170286,#170287,#170288,#170289,#170290,#170291,#170292,
#170293,#170294,#170295,#170296,#170297,#170298,#170299,#170300,#170301,
#170302,#170303,#170304,#170305,#170306,#170307,#170308,#170309,#170310,
#170311,#170312,#170313,#170314,#170315,#170316,#170317,#170318,#170319,
#170320,#170321,#170322,#170323,#170324,#170325,#170326,#170327,#170328,
#170329,#170330,#170331,#170332,#170333,#170334,#170335,#170336,#170337,
#170338,#170339,#170340,#170341,#170342,#170343,#170344,#170345,#170346,
#170347,#170348,#170349,#170350,#170351,#170352,#170353,#170354,#170355,
#170356,#170357,#170358,#170359,#170360,#170361,#170362,#170363,#170364,
#170365,#170366,#170367,#170368,#170369,#170370,#170371,#170372,#170373,
#170374,#170375,#170376,#170377,#170378,#170379,#170380,#170381,#170382,
#170383,#170384,#170385,#170386,#170387,#170388,#170389,#170390,#170391,
#170392,#170393,#170394,#170395,#170396,#170397,#170398,#170399,#170400,
#170401,#170402,#170403,#170404,#170405,#170406,#170407,#170408,#170409,
#170410,#170411,#170412,#170413,#170414,#170415,#170416,#170417,#170418,
#170419,#170420,#170421,#170422,#170423,#170424,#170425,#170426,#170427,
#170428,#170429,#170430,#170431,#170432,#170433,#170434,#170435,#170436,
#170437,#170438,#170439,#170440,#170441,#170442,#170443,#170444,#170445,
#170446,#170447,#170448,#170449,#170450,#170451,#170452,#170453,#170454,
#170455,#170456,#170457,#170458,#170459,#170460,#170461,#170462,#170463,
#170464,#170465,#170466,#170467,#170468),.UNSPECIFIED.,.F.,.F.,(4,3,3,3,
3,3,3,3,3,3,3,3,3,3,3,3,3,3,3,3,3,3,3,3,3,3,3,3,3,3,3,3,3,3,3,3,3,3,3,3,
3,3,3,3,3,3,3,3,3,3,3,3,3,3,3,3,3,3,3,3,3,3,3,3,3,3,3,3,3,3,3,3,3,3,3,3,
3,3,3,3,3,4),(-1248.16323257024,-1248.07952275549,-1247.99569914006,-1247.91167283667,
-1247.82754195684,-1247.74321391104,-1247.67054137872,-1247.59058407859,
-1247.51072128135,-1247.43093545887,-1247.35120914368,-1247.27152491538,
-1247.19185392916,-1247.11218647564,-1247.03250682482,-1246.95279924242,
-1246.87300401335,-1246.79315967164,-1246.71320124459,-1246.670805368,-1246.59084806787,
-1246.51098527063,-1246.43119944815,-1246.35147313296,-1246.27178890466,
-1246.19211791844,-1246.11245046492,-1246.0327708141,-1245.95306323171,
-1245.87326800263,-1245.79342366092,-1245.71346523388,-1245.67106935728,
-1245.59111205715,-1245.51124925991,-1245.43146343743,-1245.35173712224,
-1245.27205289395,-1245.19238190772,-1245.1127144542,-1245.03303480338,
-1244.95332722099,-1244.87353199191,-1244.7936876502,-1244.71372922316,
-1244.67133334656,-1244.59137604643,-1244.51151324919,-1244.43172742671,
-1244.35200111152,-1244.27231688323,-1244.192645897,-1244.11297844348,-1244.03329879266,
-1243.95359121027,-1243.87379598119,-1243.79395163948,-1243.71399321244,
-1243.67159733584,-1243.59164003571,-1243.51177723847,-1243.43199141599,
-1243.3522651008,-1243.27258087251,-1243.19290988628,-1243.11324243276,
-1243.03356278194,-1242.95385519955,-1242.87405997047,-1242.79421562877,
-1242.71425720172,-1242.67186132512,-1242.59303275308,-1242.51429899253,
-1242.43501752637,-1242.35642343201,-1242.27786294518,-1242.19931951457,
-1242.11950145173,-1242.04091749406,-1241.96048237864,-1241.88004726322),
 .UNSPECIFIED.);
#1470=B_SPLINE_CURVE_WITH_KNOTS('',3,(#170470,#170471,#170472,#170473,#170474,
#170475,#170476,#170477,#170478,#170479,#170480,#170481),.UNSPECIFIED.,
 .F.,.F.,(4,2,1,1,1,1,1,1,4),(-1241.88004726322,-1241.6721253144,-1240.67238930368,
-1239.67265329296,-1238.67291728224,-1237.67318127152,-1236.6734452608,
-1235.67370925008,-1235.59686195605),.UNSPECIFIED.);
#1471=B_SPLINE_CURVE_WITH_KNOTS('',3,(#170483,#170484,#170485,#170486,#170487,
#170488,#170489,#170490,#170491,#170492),.UNSPECIFIED.,.F.,.F.,(4,1,1,1,
1,1,1,4),(-1235.59686195605,-1234.67397323936,-1233.67423722864,-1232.67450121792,
-1231.6747652072,-1230.67502919648,-1229.67529318576,-1229.31367664887),
 .UNSPECIFIED.);
#1472=B_SPLINE_CURVE_WITH_KNOTS('',3,(#170494,#170495,#170496,#170497,#170498,
#170499,#170500,#170501,#170502,#170503),.UNSPECIFIED.,.F.,.F.,(4,1,1,1,
1,1,1,4),(-1229.31367664887,-1228.67555717504,-1227.67582116432,-1226.6760851536,
-1225.67634914288,-1224.67661313216,-1223.67687712144,-1223.03049134169),
 .UNSPECIFIED.);
#1473=B_SPLINE_CURVE_WITH_KNOTS('',3,(#170505,#170506,#170507,#170508,#170509,
#170510,#170511,#170512,#170513,#170514,#170515,#170516,#170517,#170518,
#170519,#170520,#170521,#170522,#170523,#170524,#170525,#170526,#170527,
#170528,#170529,#170530,#170531,#170532,#170533,#170534,#170535,#170536,
#170537,#170538,#170539,#170540,#170541,#170542,#170543,#170544,#170545,
#170546,#170547,#170548,#170549,#170550,#170551,#170552,#170553,#170554,
#170555,#170556,#170557,#170558,#170559,#170560,#170561,#170562,#170563,
#170564,#170565,#170566,#170567,#170568,#170569,#170570,#170571,#170572,
#170573,#170574,#170575,#170576,#170577,#170578,#170579,#170580,#170581,
#170582,#170583,#170584,#170585,#170586,#170587,#170588,#170589,#170590,
#170591,#170592,#170593,#170594,#170595,#170596,#170597,#170598,#170599,
#170600,#170601,#170602,#170603,#170604,#170605,#170606,#170607,#170608,
#170609,#170610,#170611,#170612,#170613,#170614,#170615,#170616,#170617,
#170618,#170619,#170620,#170621,#170622,#170623,#170624,#170625,#170626,
#170627,#170628,#170629,#170630,#170631,#170632,#170633,#170634,#170635,
#170636,#170637,#170638,#170639,#170640,#170641,#170642,#170643,#170644,
#170645,#170646,#170647,#170648,#170649,#170650,#170651,#170652,#170653,
#170654,#170655,#170656,#170657,#170658,#170659,#170660,#170661,#170662,
#170663,#170664,#170665,#170666,#170667,#170668,#170669,#170670,#170671,
#170672,#170673,#170674,#170675,#170676,#170677,#170678,#170679,#170680,
#170681,#170682,#170683,#170684,#170685,#170686,#170687,#170688,#170689,
#170690,#170691,#170692,#170693,#170694,#170695,#170696,#170697,#170698,
#170699,#170700,#170701,#170702,#170703,#170704,#170705,#170706,#170707,
#170708,#170709,#170710,#170711,#170712,#170713,#170714,#170715,#170716,
#170717,#170718,#170719,#170720,#170721,#170722,#170723,#170724,#170725,
#170726,#170727,#170728,#170729,#170730,#170731,#170732,#170733,#170734,
#170735,#170736,#170737,#170738,#170739,#170740,#170741,#170742,#170743,
#170744,#170745,#170746,#170747,#170748),.UNSPECIFIED.,.F.,.F.,(4,3,3,3,
3,3,3,3,3,3,3,3,3,3,3,3,3,3,3,3,3,3,3,3,3,3,3,3,3,3,3,3,3,3,3,3,3,3,3,3,
3,3,3,3,3,3,3,3,3,3,3,3,3,3,3,3,3,3,3,3,3,3,3,3,3,3,3,3,3,3,3,3,3,3,3,3,
3,3,3,3,3,4),(-1223.03049109457,-1222.93925215063,-1222.84759368162,-1222.75537044079,
-1222.67714111072,-1222.59718381059,-1222.51732101335,-1222.43753519088,
-1222.35780887569,-1222.2781246474,-1222.19845366118,-1222.11878620766,
-1222.03910655684,-1221.95939897445,-1221.87960374538,-1221.79975940368,
-1221.71980097663,-1221.6774051,-1221.59744779987,-1221.51758500263,-1221.43779918015,
-1221.35807286496,-1221.27838863667,-1221.19871765044,-1221.11905019692,
-1221.0393705461,-1220.95966296371,-1220.87986773463,-1220.80002339292,
-1220.72006496588,-1220.67766908928,-1220.59771178915,-1220.51784899191,
-1220.43806316943,-1220.35833685424,-1220.27865262594,-1220.19898163972,
-1220.11931418619,-1220.03963453538,-1219.95992695298,-1219.88013172391,
-1219.8002873822,-1219.72032895515,-1219.67793307856,-1219.59797577843,
-1219.51811298119,-1219.43832715872,-1219.35860084352,-1219.27891661523,
-1219.19924562901,-1219.11957817548,-1219.03989852466,-1218.96019094227,
-1218.88039571319,-1218.80055137149,-1218.72059294444,-1218.67819706784,
-1218.59823976771,-1218.51837697047,-1218.43859114799,-1218.3588648328,
-1218.2791806045,-1218.19950961828,-1218.11984216476,-1218.04016251394,
-1217.96045493154,-1217.88065970247,-1217.80081536076,-1217.72085693371,
-1217.67846105712,-1217.59928534504,-1217.52020357293,-1217.44119753742,
-1217.36224910532,-1217.28333447517,-1217.20443630897,-1217.12553827937,
-1217.04662406147,-1216.96763398074,-1216.88860405746,-1216.80946182794,
-1216.74730603451),.UNSPECIFIED.);
#1474=B_SPLINE_CURVE_WITH_KNOTS('',3,(#170750,#170751,#170752,#170753,#170754,
#170755,#170756,#170757,#170758,#170759,#170760,#170761,#170762),
 .UNSPECIFIED.,.F.,.F.,(4,3,1,1,1,1,1,1,4),(-1216.74730603451,-1216.6787250464,
-1215.67898903568,-1214.67925302496,-1213.67951701424,-1212.67978100352,
-1211.6800449928,-1210.68030898208,-1210.46412072733),.UNSPECIFIED.);
#1475=B_SPLINE_CURVE_WITH_KNOTS('',3,(#170764,#170765,#170766,#170767,#170768,
#170769,#170770,#170771,#170772,#170773),.UNSPECIFIED.,.F.,.F.,(4,1,1,1,
1,1,1,4),(-1210.46412072733,-1209.68057297136,-1208.68083696064,-1207.68110094992,
-1206.6813649392,-1205.68162892848,-1204.68189291776,-1204.18093542015),
 .UNSPECIFIED.);
#1476=B_SPLINE_CURVE_WITH_KNOTS('',3,(#170775,#170776,#170777,#170778,#170779,
#170780,#170781,#170782,#170783,#170784),.UNSPECIFIED.,.F.,.F.,(4,1,1,1,
1,1,1,4),(-1204.18093542015,-1203.68215690704,-1202.68242089632,-1201.6826848856,
-1200.68294887488,-1199.68321286416,-1198.68347685344,-1197.89775011297),
 .UNSPECIFIED.);
#1477=B_SPLINE_CURVE_WITH_KNOTS('',3,(#170786,#170787,#170788,#170789,#170790,
#170791,#170792,#170793,#170794,#170795,#170796),.UNSPECIFIED.,.F.,.F.,
(4,1,1,1,1,1,1,1,4),(-1197.89775011297,-1197.68374084272,-1196.684004832,
-1195.68426882128,-1194.68453281056,-1193.68479679984,-1192.68506078912,
-1191.6853247784,-1191.61456480579),.UNSPECIFIED.);
#1478=B_SPLINE_CURVE_WITH_KNOTS('',3,(#170798,#170799,#170800,#170801,#170802,
#170803,#170804,#170805,#170806,#170807,#170808,#170809,#170810,#170811,
#170812,#170813,#170814,#170815,#170816,#170817,#170818,#170819,#170820,
#170821,#170822,#170823,#170824,#170825,#170826,#170827,#170828,#170829,
#170830,#170831,#170832,#170833,#170834,#170835,#170836,#170837,#170838,
#170839,#170840,#170841,#170842,#170843,#170844,#170845,#170846,#170847,
#170848,#170849,#170850,#170851,#170852,#170853,#170854,#170855,#170856,
#170857,#170858,#170859,#170860,#170861,#170862,#170863,#170864,#170865,
#170866,#170867,#170868,#170869,#170870,#170871,#170872,#170873,#170874,
#170875,#170876,#170877,#170878,#170879,#170880,#170881,#170882,#170883,
#170884,#170885,#170886,#170887,#170888,#170889,#170890,#170891,#170892,
#170893,#170894,#170895,#170896,#170897,#170898,#170899,#170900,#170901,
#170902,#170903,#170904,#170905,#170906,#170907,#170908,#170909,#170910,
#170911,#170912,#170913,#170914,#170915,#170916,#170917,#170918,#170919,
#170920,#170921,#170922,#170923,#170924,#170925,#170926,#170927,#170928,
#170929,#170930,#170931,#170932,#170933,#170934,#170935,#170936,#170937,
#170938,#170939,#170940,#170941,#170942,#170943,#170944,#170945,#170946,
#170947,#170948,#170949,#170950,#170951,#170952,#170953,#170954,#170955,
#170956,#170957,#170958,#170959,#170960,#170961,#170962,#170963,#170964,
#170965,#170966,#170967,#170968,#170969,#170970,#170971,#170972,#170973,
#170974,#170975,#170976,#170977,#170978,#170979,#170980,#170981,#170982,
#170983,#170984,#170985,#170986,#170987,#170988,#170989,#170990,#170991,
#170992,#170993,#170994,#170995,#170996,#170997,#170998,#170999,#171000,
#171001,#171002,#171003,#171004,#171005,#171006,#171007,#171008,#171009,
#171010,#171011,#171012,#171013,#171014,#171015,#171016,#171017,#171018,
#171019,#171020,#171021,#171022,#171023,#171024,#171025,#171026,#171027,
#171028,#171029,#171030,#171031,#171032,#171033,#171034,#171035,#171036,
#171037,#171038,#171039,#171040,#171041),.UNSPECIFIED.,.F.,.F.,(4,3,3,3,
3,3,3,3,3,3,3,3,3,3,3,3,3,3,3,3,3,3,3,3,3,3,3,3,3,3,3,3,3,3,3,3,3,3,3,3,
3,3,3,3,3,3,3,3,3,3,3,3,3,3,3,3,3,3,3,3,3,3,3,3,3,3,3,3,3,3,3,3,3,3,3,3,
3,3,3,3,3,4),(-1191.61456480579,-1191.53543267293,-1191.45638976538,-1191.37741788645,
-1191.29849890527,-1191.21960664864,-1191.14072646774,-1191.0618420251,
-1190.98293698261,-1190.90394966339,-1190.824918671,-1190.74577032809,-1190.68558876768,
-1190.60563146755,-1190.52576867031,-1190.44598284783,-1190.36625653264,
-1190.28657230435,-1190.20690131812,-1190.1272338646,-1190.04755421378,
-1189.96784663139,-1189.88805140231,-1189.8082070606,-1189.72824863356,
-1189.68585275696,-1189.60589545683,-1189.52603265959,-1189.44624683711,
-1189.36652052192,-1189.28683629362,-1189.2071653074,-1189.12749785388,
-1189.04781820306,-1188.96811062067,-1188.88831539159,-1188.80847104988,
-1188.72851262284,-1188.68611674624,-1188.60615944611,-1188.52629664887,
-1188.44651082639,-1188.3667845112,-1188.2871002829,-1188.20742929668,-1188.12776184316,
-1188.04808219234,-1187.96837460995,-1187.88857938087,-1187.80873503916,
-1187.72877661212,-1187.68638073552,-1187.60642343539,-1187.52656063815,
-1187.44677481567,-1187.36704850048,-1187.28736427218,-1187.20769328596,
-1187.12802583244,-1187.04834618162,-1186.96863859923,-1186.88884337015,
-1186.80899902844,-1186.7290406014,-1186.6866447248,-1186.60668742467,-1186.52682462743,
-1186.44703880496,-1186.36731248976,-1186.28762826147,-1186.20795727525,
-1186.12828982172,-1186.04861017091,-1185.96890258851,-1185.88910735944,
-1185.80926301773,-1185.72930459068,-1185.68690871408,-1185.59487830074,
-1185.50317571114,-1185.41211905715,-1185.3313797463),.UNSPECIFIED.);
#1479=B_SPLINE_CURVE_WITH_KNOTS('',3,(#171043,#171044,#171045,#171046,#171047,
#171048,#171049,#171050,#171051,#171052),.UNSPECIFIED.,.F.,.F.,(4,1,1,1,
1,1,1,4),(-1185.33137949861,-1184.68717270336,-1183.68743669263,-1182.68770068191,
-1181.6879646712,-1180.68822866048,-1179.68849264975,-1179.04819419143),
 .UNSPECIFIED.);
#1480=B_SPLINE_CURVE_WITH_KNOTS('',3,(#171054,#171055,#171056,#171057,#171058,
#171059,#171060,#171061,#171062,#171063),.UNSPECIFIED.,.F.,.F.,(4,1,1,1,
1,1,1,4),(-1179.04819419143,-1178.68875663903,-1177.68902062831,-1176.68928461759,
-1175.68954860687,-1174.68981259615,-1173.69007658543,-1172.76500888425),
 .UNSPECIFIED.);
#1481=B_SPLINE_CURVE_WITH_KNOTS('',3,(#171065,#171066,#171067,#171068,#171069,
#171070,#171071,#171072,#171073,#171074,#171075,#171076,#171077),
 .UNSPECIFIED.,.F.,.F.,(4,3,1,1,1,1,1,1,4),(-1172.76500888425,-1172.69034057471,
-1171.69060456399,-1170.69086855327,-1169.69113254255,-1168.69139653183,
-1167.69166052111,-1166.69192451039,-1166.48182357707),.UNSPECIFIED.);
#1482=B_SPLINE_CURVE_WITH_KNOTS('',3,(#171079,#171080,#171081,#171082,#171083,
#171084,#171085,#171086,#171087,#171088,#171089,#171090,#171091,#171092,
#171093,#171094,#171095,#171096,#171097,#171098,#171099,#171100,#171101,
#171102,#171103,#171104,#171105,#171106,#171107,#171108,#171109,#171110,
#171111,#171112,#171113,#171114,#171115,#171116,#171117,#171118,#171119,
#171120,#171121,#171122,#171123,#171124,#171125,#171126,#171127,#171128,
#171129,#171130,#171131,#171132,#171133,#171134,#171135,#171136,#171137,
#171138,#171139,#171140,#171141,#171142,#171143,#171144,#171145,#171146,
#171147,#171148,#171149,#171150,#171151,#171152,#171153,#171154,#171155,
#171156,#171157,#171158,#171159,#171160,#171161,#171162,#171163,#171164,
#171165,#171166,#171167,#171168,#171169,#171170,#171171,#171172,#171173,
#171174,#171175,#171176,#171177,#171178,#171179,#171180,#171181,#171182,
#171183,#171184,#171185,#171186,#171187,#171188,#171189,#171190,#171191,
#171192,#171193,#171194,#171195,#171196,#171197,#171198,#171199,#171200,
#171201,#171202,#171203,#171204,#171205,#171206,#171207,#171208,#171209,
#171210,#171211,#171212,#171213,#171214,#171215,#171216,#171217,#171218,
#171219,#171220,#171221,#171222,#171223,#171224,#171225,#171226,#171227,
#171228,#171229,#171230,#171231,#171232,#171233,#171234,#171235,#171236,
#171237,#171238,#171239,#171240,#171241,#171242,#171243,#171244,#171245,
#171246,#171247,#171248,#171249,#171250,#171251,#171252,#171253,#171254,
#171255,#171256,#171257,#171258,#171259,#171260,#171261,#171262,#171263,
#171264,#171265,#171266,#171267,#171268,#171269,#171270,#171271,#171272,
#171273,#171274,#171275,#171276,#171277,#171278,#171279,#171280,#171281,
#171282,#171283,#171284,#171285,#171286,#171287,#171288,#171289,#171290,
#171291,#171292,#171293,#171294,#171295,#171296,#171297,#171298,#171299,
#171300,#171301,#171302,#171303,#171304,#171305,#171306,#171307,#171308,
#171309,#171310,#171311,#171312,#171313,#171314,#171315,#171316,#171317,
#171318,#171319,#171320,#171321,#171322),.UNSPECIFIED.,.F.,.F.,(4,3,3,3,
3,3,3,3,3,3,3,3,3,3,3,3,3,3,3,3,3,3,3,3,3,3,3,3,3,3,3,3,3,3,3,3,3,3,3,3,
3,3,3,3,3,3,3,3,3,3,3,3,3,3,3,3,3,3,3,3,3,3,3,3,3,3,3,3,3,3,3,3,3,3,3,3,
3,3,3,3,3,4),(-1166.48182357707,-1166.40314731128,-1166.32453163811,-1166.2454887458,
-1166.16692851299,-1166.08837029189,-1166.00979755129,-1165.93039528838,
-1165.85170524793,-1165.7719468738,-1165.69218849967,-1165.61223119954,
-1165.5323684023,-1165.45258257983,-1165.37285626463,-1165.29317203634,
-1165.21350105012,-1165.13383359659,-1165.05415394577,-1164.97444636338,
-1164.89465113431,-1164.8148067926,-1164.73484836555,-1164.69245248895,
-1164.61249518882,-1164.53263239158,-1164.4528465691,-1164.37312025391,
-1164.29343602562,-1164.2137650394,-1164.13409758587,-1164.05441793505,
-1163.97471035266,-1163.89491512358,-1163.81507078188,-1163.73511235483,
-1163.69271647823,-1163.6127591781,-1163.53289638086,-1163.45311055838,
-1163.37338424319,-1163.29370001489,-1163.21402902867,-1163.13436157515,
-1163.05468192433,-1162.97497434194,-1162.89517911286,-1162.81533477115,
-1162.7353763441,-1162.69298046751,-1162.61302316738,-1162.53316037014,
-1162.45337454766,-1162.37364823247,-1162.29396400417,-1162.21429301795,
-1162.13462556443,-1162.05494591361,-1161.97523833122,-1161.89544310214,
-1161.81559876043,-1161.73564033339,-1161.69324445679,-1161.61328715666,
-1161.53342435941,-1161.45363853694,-1161.37391222175,-1161.29422799345,
-1161.21455700723,-1161.1348895537,-1161.05520990289,-1160.97550232049,
-1160.89570709142,-1160.81586274971,-1160.73590432266,-1160.69350844607,
-1160.60923845646,-1160.52511011155,-1160.44117479101,-1160.35735298291,
-1160.2736877613,-1160.19863827),.UNSPECIFIED.);
#1483=B_SPLINE_CURVE_WITH_KNOTS('',3,(#171324,#171325,#171326,#171327,#171328,
#171329,#171330,#171331,#171332,#171333,#171334,#171335,#171336,#171337,
#171338,#171339,#171340,#171341,#171342,#171343,#171344,#171345,#171346,
#171347,#171348,#171349,#171350,#171351,#171352,#171353,#171354,#171355,
#171356,#171357,#171358,#171359,#171360,#171361,#171362,#171363,#171364,
#171365,#171366,#171367,#171368,#171369,#171370,#171371,#171372,#171373,
#171374,#171375,#171376,#171377,#171378,#171379,#171380,#171381,#171382,
#171383,#171384,#171385,#171386,#171387,#171388,#171389,#171390,#171391,
#171392,#171393,#171394,#171395,#171396,#171397,#171398,#171399,#171400,
#171401,#171402,#171403,#171404,#171405,#171406,#171407,#171408,#171409,
#171410,#171411,#171412,#171413,#171414,#171415,#171416,#171417,#171418,
#171419,#171420,#171421,#171422,#171423,#171424,#171425,#171426,#171427,
#171428,#171429,#171430,#171431,#171432,#171433,#171434,#171435,#171436,
#171437,#171438,#171439,#171440,#171441,#171442,#171443,#171444,#171445,
#171446,#171447,#171448,#171449,#171450,#171451,#171452,#171453,#171454,
#171455,#171456,#171457,#171458,#171459,#171460,#171461,#171462,#171463,
#171464,#171465,#171466,#171467,#171468,#171469,#171470,#171471,#171472,
#171473,#171474,#171475,#171476,#171477,#171478,#171479,#171480,#171481,
#171482,#171483,#171484,#171485,#171486,#171487,#171488,#171489,#171490,
#171491,#171492,#171493,#171494,#171495,#171496,#171497,#171498,#171499,
#171500,#171501,#171502,#171503,#171504,#171505,#171506,#171507,#171508,
#171509,#171510,#171511,#171512,#171513,#171514,#171515,#171516,#171517,
#171518,#171519,#171520,#171521,#171522,#171523,#171524,#171525,#171526,
#171527,#171528,#171529,#171530,#171531,#171532,#171533,#171534,#171535,
#171536,#171537,#171538,#171539,#171540,#171541,#171542,#171543,#171544,
#171545,#171546,#171547,#171548,#171549,#171550,#171551,#171552,#171553,
#171554,#171555,#171556,#171557,#171558,#171559,#171560,#171561,#171562,
#171563,#171564,#171565,#171566,#171567),.UNSPECIFIED.,.F.,.F.,(4,3,3,3,
3,3,3,3,3,3,3,3,3,3,3,3,3,3,3,3,3,3,3,3,3,3,3,3,3,3,3,3,3,3,3,3,3,3,3,3,
3,3,3,3,3,3,3,3,3,3,3,3,3,3,3,3,3,3,3,3,3,3,3,3,3,3,3,3,3,3,3,3,3,3,3,3,
3,3,3,3,3,4),(-1160.19863826989,-1160.11535205206,-1160.03196706726,-1159.94741840929,
-1159.86375007496,-1159.77876125516,-1159.69377243535,-1159.61381513522,
-1159.53395233798,-1159.45416651551,-1159.37444020032,-1159.29475597202,
-1159.2150849858,-1159.13541753228,-1159.05573788146,-1158.97603029907,
-1158.89623507,-1158.81639072829,-1158.73643230125,-1158.69403642463,-1158.6140791245,
-1158.53421632726,-1158.45443050478,-1158.37470418959,-1158.2950199613,
-1158.21534897507,-1158.13568152155,-1158.05600187073,-1157.97629428834,
-1157.89649905926,-1157.81665471755,-1157.73669629051,-1157.69430041391,
-1157.61434311378,-1157.53448031654,-1157.45469449406,-1157.37496817887,
-1157.29528395057,-1157.21561296435,-1157.13594551083,-1157.05626586001,
-1156.97655827761,-1156.89676304854,-1156.81691870683,-1156.73696027978,
-1156.69456440319,-1156.61460710306,-1156.53474430582,-1156.45495848335,
-1156.37523216815,-1156.29554793986,-1156.21587695364,-1156.13620950011,
-1156.05652984929,-1155.9768222669,-1155.89702703782,-1155.81718269612,
-1155.73722426907,-1155.69482839247,-1155.61487109234,-1155.5350082951,
-1155.45522247262,-1155.37549615743,-1155.29581192913,-1155.21614094291,
-1155.13647348939,-1155.05679383857,-1154.97708625617,-1154.8972910271,
-1154.81744668539,-1154.73748825834,-1154.69509238175,-1154.61621712552,
-1154.53743704012,-1154.45874680529,-1154.38010736615,-1154.30150216832,
-1154.22291468565,-1154.1443015305,-1154.06567743878,-1153.98698234884,
-1153.91545296271),.UNSPECIFIED.);
#1484=B_SPLINE_CURVE_WITH_KNOTS('',3,(#171569,#171570,#171571,#171572,#171573,
#171574,#171575,#171576,#171577,#171578,#171579,#171580),.UNSPECIFIED.,
 .F.,.F.,(4,2,1,1,1,1,1,1,4),(-1153.91545296271,-1153.69535637103,-1152.69562036031,
-1151.69588434959,-1150.69614833887,-1149.69641232815,-1148.69667631743,
-1147.69694030671,-1147.63226765553),.UNSPECIFIED.);
#1485=B_SPLINE_CURVE_WITH_KNOTS('',3,(#171582,#171583,#171584,#171585,#171586,
#171587,#171588,#171589,#171590,#171591,#171592,#171593,#171594,#171595,
#171596,#171597,#171598,#171599,#171600,#171601,#171602,#171603,#171604,
#171605,#171606,#171607,#171608,#171609,#171610,#171611,#171612,#171613,
#171614,#171615,#171616,#171617,#171618,#171619,#171620,#171621,#171622,
#171623,#171624,#171625,#171626,#171627,#171628,#171629,#171630,#171631,
#171632,#171633,#171634,#171635,#171636,#171637,#171638,#171639,#171640,
#171641,#171642,#171643,#171644,#171645,#171646,#171647,#171648,#171649,
#171650,#171651,#171652,#171653,#171654,#171655,#171656,#171657,#171658,
#171659,#171660,#171661,#171662,#171663,#171664,#171665,#171666,#171667,
#171668,#171669,#171670,#171671,#171672,#171673,#171674,#171675,#171676,
#171677,#171678,#171679,#171680,#171681,#171682,#171683,#171684,#171685,
#171686,#171687,#171688,#171689,#171690,#171691,#171692,#171693,#171694,
#171695,#171696,#171697,#171698,#171699,#171700,#171701,#171702,#171703,
#171704,#171705,#171706,#171707,#171708,#171709,#171710,#171711,#171712,
#171713,#171714,#171715,#171716,#171717,#171718,#171719,#171720,#171721,
#171722,#171723,#171724,#171725,#171726,#171727,#171728,#171729,#171730,
#171731,#171732,#171733,#171734,#171735,#171736,#171737,#171738,#171739,
#171740,#171741,#171742,#171743,#171744,#171745,#171746,#171747,#171748,
#171749,#171750,#171751,#171752,#171753,#171754,#171755,#171756,#171757,
#171758,#171759,#171760,#171761,#171762,#171763,#171764,#171765,#171766,
#171767,#171768,#171769,#171770,#171771,#171772,#171773,#171774,#171775,
#171776,#171777,#171778,#171779,#171780,#171781,#171782,#171783,#171784,
#171785,#171786,#171787,#171788,#171789,#171790,#171791,#171792,#171793,
#171794,#171795,#171796,#171797,#171798,#171799,#171800,#171801,#171802,
#171803,#171804,#171805,#171806,#171807,#171808,#171809,#171810,#171811,
#171812,#171813,#171814,#171815,#171816,#171817,#171818,#171819,#171820,
#171821,#171822,#171823,#171824,#171825),.UNSPECIFIED.,.F.,.F.,(4,3,3,3,
3,3,3,3,3,3,3,3,3,3,3,3,3,3,3,3,3,3,3,3,3,3,3,3,3,3,3,3,3,3,3,3,3,3,3,3,
3,3,3,3,3,3,3,3,3,3,3,3,3,3,3,3,3,3,3,3,3,3,3,3,3,3,3,3,3,3,3,3,3,3,3,3,
3,3,3,3,3,4),(-1147.63226765553,-1147.55308046487,-1147.47398326853,-1147.3949579049,
-1147.31598627808,-1147.23704249499,-1147.15811160934,-1147.07917731644,
-1147.00022331162,-1146.92118728103,-1146.84210843834,-1146.76291058435,
-1146.69720429599,-1146.61724699586,-1146.53738419862,-1146.45759837614,
-1146.37787206095,-1146.29818783266,-1146.21851684644,-1146.13884939291,
-1146.05916974209,-1145.9794621597,-1145.89966693062,-1145.81982258892,
-1145.73986416187,-1145.69746828527,-1145.61751098514,-1145.5376481879,
-1145.45786236543,-1145.37813605023,-1145.29845182194,-1145.21878083572,
-1145.13911338219,-1145.05943373137,-1144.97972614898,-1144.8999309199,
-1144.8200865782,-1144.74012815115,-1144.69773227455,-1144.61777497442,
-1144.53791217718,-1144.4581263547,-1144.37840003951,-1144.29871581122,
-1144.21904482499,-1144.13937737147,-1144.05969772065,-1143.97999013826,
-1143.90019490918,-1143.82035056747,-1143.74039214043,-1143.69799626383,
-1143.6180389637,-1143.53817616646,-1143.45839034398,-1143.37866402879,
-1143.29897980049,-1143.21930881427,-1143.13964136075,-1143.05996170993,
-1142.98025412754,-1142.90045889846,-1142.82061455675,-1142.74065612971,
-1142.69826025311,-1142.61830295298,-1142.53844015574,-1142.45865433326,
-1142.37892801807,-1142.29924378977,-1142.21957280355,-1142.13990535003,
-1142.06022569921,-1141.98051811681,-1141.90072288774,-1141.82087854603,
-1141.74092011898,-1141.69852424239,-1141.6059888571,-1141.51380205893,
-1141.42229735434,-1141.34908247127),.UNSPECIFIED.);
#1486=B_SPLINE_CURVE_WITH_KNOTS('',3,(#171827,#171828,#171829,#171830,#171831,
#171832,#171833,#171834,#171835,#171836),.UNSPECIFIED.,.F.,.F.,(4,1,1,1,
1,1,1,4),(-1141.34908234835,-1140.69878823167,-1139.69905222095,-1138.69931621023,
-1137.69958019951,-1136.69984418879,-1135.70010817807,-1135.06589704117),
 .UNSPECIFIED.);
#1487=B_SPLINE_CURVE_WITH_KNOTS('',3,(#171838,#171839,#171840,#171841,#171842,
#171843,#171844,#171845,#171846,#171847),.UNSPECIFIED.,.F.,.F.,(4,1,1,1,
1,1,1,4),(-1135.06589704117,-1134.70037216735,-1133.70063615663,-1132.70090014591,
-1131.70116413519,-1130.70142812447,-1129.70169211375,-1128.78271173399),
 .UNSPECIFIED.);
#1488=B_SPLINE_CURVE_WITH_KNOTS('',3,(#171849,#171850,#171851,#171852,#171853,
#171854,#171855,#171856,#171857,#171858,#171859,#171860),.UNSPECIFIED.,
 .F.,.F.,(4,2,1,1,1,1,1,1,4),(-1128.78271173399,-1128.70195610303,-1127.70222009231,
-1126.70248408159,-1125.70274807087,-1124.70301206015,-1123.70327604943,
-1122.70354003871,-1122.49952642681),.UNSPECIFIED.);
#1489=B_SPLINE_CURVE_WITH_KNOTS('',3,(#171862,#171863,#171864,#171865,#171866,
#171867,#171868,#171869,#171870,#171871,#171872,#171873,#171874,#171875,
#171876,#171877,#171878,#171879,#171880,#171881,#171882,#171883,#171884,
#171885,#171886,#171887,#171888,#171889,#171890,#171891,#171892,#171893,
#171894,#171895,#171896,#171897,#171898,#171899,#171900,#171901,#171902,
#171903,#171904,#171905,#171906,#171907,#171908,#171909,#171910,#171911,
#171912,#171913,#171914,#171915,#171916,#171917,#171918,#171919,#171920,
#171921,#171922,#171923,#171924,#171925,#171926,#171927,#171928,#171929,
#171930,#171931,#171932,#171933,#171934,#171935,#171936,#171937,#171938,
#171939,#171940,#171941,#171942,#171943,#171944,#171945,#171946,#171947,
#171948,#171949,#171950,#171951,#171952,#171953,#171954,#171955,#171956,
#171957,#171958,#171959,#171960,#171961,#171962,#171963,#171964,#171965,
#171966,#171967,#171968,#171969,#171970,#171971,#171972,#171973,#171974,
#171975,#171976,#171977,#171978,#171979,#171980,#171981,#171982,#171983,
#171984,#171985,#171986,#171987,#171988,#171989,#171990,#171991,#171992,
#171993,#171994,#171995,#171996,#171997,#171998,#171999,#172000,#172001,
#172002,#172003,#172004,#172005,#172006,#172007,#172008,#172009,#172010,
#172011,#172012,#172013,#172014,#172015,#172016,#172017,#172018,#172019,
#172020,#172021,#172022,#172023,#172024,#172025,#172026,#172027,#172028,
#172029,#172030,#172031,#172032,#172033,#172034,#172035,#172036,#172037,
#172038,#172039,#172040,#172041,#172042,#172043,#172044,#172045,#172046,
#172047,#172048,#172049,#172050,#172051,#172052,#172053,#172054,#172055,
#172056,#172057,#172058,#172059,#172060,#172061,#172062,#172063,#172064,
#172065,#172066,#172067,#172068,#172069,#172070,#172071,#172072,#172073,
#172074,#172075,#172076,#172077,#172078,#172079,#172080,#172081,#172082,
#172083,#172084,#172085,#172086,#172087,#172088,#172089,#172090,#172091,
#172092,#172093,#172094,#172095,#172096,#172097,#172098,#172099,#172100,
#172101,#172102,#172103,#172104,#172105),.UNSPECIFIED.,.F.,.F.,(4,3,3,3,
3,3,3,3,3,3,3,3,3,3,3,3,3,3,3,3,3,3,3,3,3,3,3,3,3,3,3,3,3,3,3,3,3,3,3,3,
3,3,3,3,3,3,3,3,3,3,3,3,3,3,3,3,3,3,3,3,3,3,3,3,3,3,3,3,3,3,3,3,3,3,3,3,
3,3,3,3,3,4),(-1122.49952642681,-1122.42086265841,-1122.34226113132,-1122.26245399341,
-1122.18391170298,-1122.10537271461,-1122.02682048646,-1121.94606637184,
-1121.86739794136,-1121.78560098468,-1121.70380402799,-1121.62384672786,
-1121.54398393062,-1121.46419810814,-1121.38447179295,-1121.30478756465,
-1121.22511657843,-1121.14544912491,-1121.06576947409,-1120.9860618917,
-1120.90626666262,-1120.82642232091,-1120.74646389386,-1120.70406801727,
-1120.62411071714,-1120.5442479199,-1120.46446209742,-1120.38473578223,
-1120.30505155393,-1120.22538056771,-1120.14571311419,-1120.06603346337,
-1119.98632588098,-1119.9065306519,-1119.82668631019,-1119.74672788314,
-1119.70433200655,-1119.62437470642,-1119.54451190918,-1119.4647260867,
-1119.38499977151,-1119.30531554322,-1119.22564455699,-1119.14597710347,
-1119.06629745265,-1118.98658987026,-1118.90679464118,-1118.82695029948,
-1118.74699187243,-1118.70459599583,-1118.6246386957,-1118.54477589846,
-1118.46499007598,-1118.38526376079,-1118.3055795325,-1118.22590854627,
-1118.14624109275,-1118.06656144193,-1117.98685385954,-1117.90705863046,
-1117.82721428875,-1117.74725586171,-1117.70485998511,-1117.62490268498,
-1117.54503988774,-1117.46525406527,-1117.38552775007,-1117.30584352178,
-1117.22617253556,-1117.14650508203,-1117.06682543121,-1116.98711784882,
-1116.90732261974,-1116.82747827804,-1116.74751985099,-1116.70512397439,
-1116.620615229,-1116.53625184539,-1116.45208839494,-1116.36804333682,-1116.28416290556,
-1116.21634111975),.UNSPECIFIED.);
#1490=B_SPLINE_CURVE_WITH_KNOTS('',3,(#172107,#172108,#172109,#172110,#172111,
#172112,#172113,#172114,#172115,#172116,#172117,#172118,#172119,#172120,
#172121,#172122,#172123,#172124,#172125,#172126,#172127,#172128,#172129,
#172130,#172131,#172132,#172133,#172134,#172135,#172136,#172137,#172138,
#172139,#172140,#172141,#172142,#172143,#172144,#172145,#172146,#172147,
#172148,#172149,#172150,#172151,#172152,#172153,#172154,#172155,#172156,
#172157,#172158,#172159,#172160,#172161,#172162,#172163,#172164,#172165,
#172166,#172167,#172168,#172169,#172170,#172171,#172172,#172173,#172174,
#172175,#172176,#172177,#172178,#172179,#172180,#172181,#172182,#172183,
#172184,#172185,#172186,#172187,#172188,#172189,#172190,#172191,#172192,
#172193,#172194,#172195,#172196,#172197,#172198,#172199,#172200,#172201,
#172202,#172203,#172204,#172205,#172206,#172207,#172208,#172209,#172210,
#172211,#172212,#172213,#172214,#172215,#172216,#172217,#172218,#172219,
#172220,#172221,#172222,#172223,#172224,#172225,#172226,#172227,#172228,
#172229,#172230,#172231,#172232,#172233,#172234,#172235,#172236,#172237,
#172238,#172239,#172240,#172241,#172242,#172243,#172244,#172245,#172246,
#172247,#172248,#172249,#172250,#172251,#172252,#172253,#172254,#172255,
#172256,#172257,#172258,#172259,#172260,#172261,#172262,#172263,#172264,
#172265,#172266,#172267,#172268,#172269,#172270,#172271,#172272,#172273,
#172274,#172275,#172276,#172277,#172278,#172279,#172280,#172281,#172282,
#172283,#172284,#172285,#172286,#172287,#172288,#172289,#172290,#172291,
#172292,#172293,#172294,#172295,#172296,#172297,#172298,#172299,#172300,
#172301,#172302,#172303,#172304,#172305,#172306,#172307,#172308,#172309,
#172310,#172311,#172312,#172313,#172314,#172315,#172316,#172317,#172318,
#172319,#172320,#172321,#172322,#172323,#172324,#172325,#172326,#172327,
#172328,#172329,#172330,#172331,#172332,#172333,#172334,#172335,#172336,
#172337,#172338,#172339,#172340,#172341,#172342,#172343,#172344,#172345,
#172346,#172347,#172348,#172349,#172350),.UNSPECIFIED.,.F.,.F.,(4,3,3,3,
3,3,3,3,3,3,3,3,3,3,3,3,3,3,3,3,3,3,3,3,3,3,3,3,3,3,3,3,3,3,3,3,3,3,3,3,
3,3,3,3,3,3,3,3,3,3,3,3,3,3,3,3,3,3,3,3,3,3,3,3,3,3,3,3,3,3,3,3,3,3,3,3,
3,3,3,3,3,4),(-1116.21634111963,-1116.13325733148,-1116.05008172745,-1115.96390828651,
-1115.8804590234,-1115.79292349354,-1115.70538796367,-1115.62543066354,
-1115.54556786629,-1115.46578204382,-1115.38605572863,-1115.30637150033,
-1115.22670051411,-1115.14703306058,-1115.06735340976,-1114.98764582737,
-1114.90785059829,-1114.82800625658,-1114.74804782954,-1114.70565195295,
-1114.62569465282,-1114.54583185558,-1114.4660460331,-1114.38631971791,
-1114.30663548961,-1114.22696450339,-1114.14729704987,-1114.06761739905,
-1113.98790981666,-1113.90811458758,-1113.82827024587,-1113.74831181882,
-1113.70591594223,-1113.6259586421,-1113.54609584486,-1113.46631002239,
-1113.38658370719,-1113.3068994789,-1113.22722849268,-1113.14756103915,
-1113.06788138833,-1112.98817380594,-1112.90837857687,-1112.82853423516,
-1112.74857580811,-1112.70617993151,-1112.62622263138,-1112.54635983414,
-1112.46657401166,-1112.38684769647,-1112.30716346817,-1112.22749248195,
-1112.14782502843,-1112.06814537761,-1111.98843779522,-1111.90864256614,
-1111.82879822443,-1111.74883979739,-1111.70644392079,-1111.62648662066,
-1111.54662382342,-1111.46683800095,-1111.38711168575,-1111.30742745746,
-1111.22775647124,-1111.14808901771,-1111.0684093669,-1110.9887017845,-1110.90890655543,
-1110.82906221372,-1110.74910378667,-1110.70670791007,-1110.62780456985,
-1110.54899660499,-1110.47027895055,-1110.39161235929,-1110.31298029234,
-1110.23436623922,-1110.15572804764,-1110.07707914813,-1109.99836256153,
-1109.93315581245),.UNSPECIFIED.);
#1491=B_SPLINE_CURVE_WITH_KNOTS('',3,(#172352,#172353,#172354,#172355,#172356,
#172357,#172358,#172359,#172360,#172361,#172362,#172363),.UNSPECIFIED.,
 .F.,.F.,(4,2,1,1,1,1,1,1,4),(-1109.93315581245,-1109.70697189935,-1108.70723588863,
-1107.70749987791,-1106.70776386719,-1105.70802785646,-1104.70829184574,
-1103.70855583502,-1103.64997050527),.UNSPECIFIED.);
#1492=B_SPLINE_CURVE_WITH_KNOTS('',3,(#172365,#172366,#172367,#172368,#172369,
#172370,#172371,#172372,#172373,#172374,#172375,#172376,#172377,#172378,
#172379,#172380,#172381,#172382,#172383,#172384,#172385,#172386,#172387,
#172388,#172389,#172390,#172391,#172392,#172393,#172394,#172395,#172396,
#172397,#172398,#172399,#172400,#172401,#172402,#172403,#172404,#172405,
#172406,#172407,#172408,#172409,#172410,#172411,#172412,#172413,#172414,
#172415,#172416,#172417,#172418,#172419,#172420,#172421,#172422,#172423,
#172424,#172425,#172426,#172427,#172428,#172429,#172430,#172431,#172432,
#172433,#172434,#172435,#172436,#172437,#172438,#172439,#172440,#172441,
#172442,#172443,#172444,#172445,#172446,#172447,#172448,#172449,#172450,
#172451,#172452,#172453,#172454,#172455,#172456,#172457,#172458,#172459,
#172460,#172461,#172462,#172463,#172464,#172465,#172466,#172467,#172468,
#172469,#172470,#172471,#172472,#172473,#172474,#172475,#172476,#172477,
#172478,#172479,#172480,#172481,#172482,#172483,#172484,#172485,#172486,
#172487,#172488,#172489,#172490,#172491,#172492,#172493,#172494,#172495,
#172496,#172497,#172498,#172499,#172500,#172501,#172502,#172503,#172504,
#172505,#172506,#172507,#172508,#172509,#172510,#172511,#172512,#172513,
#172514,#172515,#172516,#172517,#172518,#172519,#172520,#172521,#172522,
#172523,#172524,#172525,#172526,#172527,#172528,#172529,#172530,#172531,
#172532,#172533,#172534,#172535,#172536,#172537,#172538,#172539,#172540,
#172541,#172542,#172543,#172544,#172545,#172546,#172547,#172548,#172549,
#172550,#172551,#172552,#172553,#172554,#172555,#172556,#172557,#172558,
#172559,#172560,#172561,#172562,#172563,#172564,#172565,#172566,#172567,
#172568,#172569,#172570,#172571,#172572,#172573,#172574,#172575,#172576,
#172577,#172578,#172579,#172580,#172581,#172582,#172583,#172584,#172585,
#172586,#172587,#172588,#172589,#172590,#172591,#172592,#172593,#172594,
#172595,#172596,#172597,#172598,#172599,#172600,#172601,#172602,#172603,
#172604,#172605,#172606,#172607,#172608),.UNSPECIFIED.,.F.,.F.,(4,3,3,3,
3,3,3,3,3,3,3,3,3,3,3,3,3,3,3,3,3,3,3,3,3,3,3,3,3,3,3,3,3,3,3,3,3,3,3,3,
3,3,3,3,3,3,3,3,3,3,3,3,3,3,3,3,3,3,3,3,3,3,3,3,3,3,3,3,3,3,3,3,3,3,3,3,
3,3,3,3,3,4),(-1103.64997050527,-1103.57072528908,-1103.49157078566,-1103.41248887196,
-1103.33346149041,-1103.25446302266,-1103.17547824058,-1103.0964908751,
-1103.01748465782,-1102.93839664834,-1102.85926666808,-1102.78001600334,
-1102.7088198243,-1102.62886252417,-1102.54899972693,-1102.46921390445,
-1102.38948758926,-1102.30980336097,-1102.23013237475,-1102.15046492122,
-1102.0707852704,-1101.99107768801,-1101.91128245893,-1101.83143811723,
-1101.75147969018,-1101.70908381358,-1101.62912651345,-1101.54926371621,
-1101.46947789373,-1101.38975157854,-1101.31006735025,-1101.23039636403,
-1101.1507289105,-1101.07104925968,-1100.99134167729,-1100.91154644821,
-1100.83170210651,-1100.75174367946,-1100.70934780286,-1100.62939050273,
-1100.54952770549,-1100.46974188301,-1100.39001556782,-1100.31033133952,
-1100.2306603533,-1100.15099289978,-1100.07131324896,-1099.99160566657,
-1099.91181043749,-1099.83196609578,-1099.75200766874,-1099.70961179214,
-1099.62965449201,-1099.54979169477,-1099.47000587229,-1099.3902795571,
-1099.3105953288,-1099.23092434258,-1099.15125688906,-1099.07157723824,
-1098.99186965585,-1098.91207442677,-1098.83223008506,-1098.75227165802,
-1098.70987578142,-1098.62991848129,-1098.55005568404,-1098.47026986157,
-1098.39054354638,-1098.31085931808,-1098.23118833186,-1098.15152087833,
-1098.07184122752,-1097.99213364512,-1097.91233841605,-1097.83249407434,
-1097.75253564729,-1097.7101397707,-1097.61707962411,-1097.52439093108,
-1097.43242331425,-1097.36678531938),.UNSPECIFIED.);
#1493=B_SPLINE_CURVE_WITH_KNOTS('',3,(#172610,#172611,#172612,#172613,#172614,
#172615,#172616,#172617,#172618,#172619),.UNSPECIFIED.,.F.,.F.,(4,1,1,1,
1,1,1,4),(-1097.36678519809,-1096.71040375998,-1095.71066774926,-1094.71093173854,
-1093.71119572782,-1092.7114597171,-1091.71172370638,-1091.08359989091),
 .UNSPECIFIED.);
#1494=B_SPLINE_CURVE_WITH_KNOTS('',3,(#172621,#172622,#172623,#172624,#172625,
#172626,#172627,#172628,#172629,#172630),.UNSPECIFIED.,.F.,.F.,(4,1,1,1,
1,1,1,4),(-1091.08359989091,-1090.71198769566,-1089.71225168494,-1088.71251567422,
-1087.7127796635,-1086.71304365278,-1085.71330764206,-1084.80042330243),
 .UNSPECIFIED.);
#1495=B_SPLINE_CURVE_WITH_KNOTS('',3,(#172632,#172633,#172634,#172635,#172636,
#172637,#172638,#172639,#172640,#172641,#172642,#172643,#172644,#172645,
#172646,#172647,#172648,#172649,#172650,#172651,#172652,#172653,#172654,
#172655,#172656,#172657,#172658,#172659,#172660,#172661,#172662,#172663,
#172664,#172665,#172666,#172667,#172668,#172669,#172670,#172671,#172672,
#172673,#172674,#172675,#172676,#172677,#172678,#172679,#172680,#172681,
#172682,#172683,#172684,#172685,#172686,#172687,#172688,#172689,#172690,
#172691,#172692,#172693,#172694,#172695,#172696,#172697,#172698,#172699,
#172700,#172701,#172702,#172703,#172704,#172705,#172706,#172707,#172708,
#172709,#172710,#172711,#172712,#172713,#172714,#172715,#172716,#172717,
#172718,#172719,#172720,#172721,#172722,#172723,#172724,#172725,#172726,
#172727,#172728,#172729,#172730,#172731,#172732,#172733,#172734,#172735,
#172736,#172737,#172738,#172739,#172740,#172741,#172742,#172743,#172744,
#172745,#172746,#172747,#172748,#172749,#172750,#172751,#172752,#172753,
#172754,#172755,#172756,#172757,#172758,#172759,#172760,#172761,#172762,
#172763,#172764,#172765,#172766,#172767,#172768,#172769,#172770,#172771,
#172772,#172773,#172774,#172775,#172776,#172777,#172778,#172779,#172780,
#172781,#172782,#172783,#172784,#172785,#172786,#172787,#172788,#172789,
#172790,#172791,#172792,#172793,#172794,#172795,#172796,#172797,#172798,
#172799,#172800,#172801,#172802,#172803,#172804,#172805,#172806,#172807,
#172808,#172809,#172810,#172811,#172812,#172813,#172814,#172815,#172816,
#172817,#172818,#172819,#172820,#172821,#172822,#172823,#172824,#172825,
#172826,#172827,#172828,#172829,#172830,#172831,#172832,#172833,#172834,
#172835,#172836,#172837,#172838,#172839,#172840,#172841,#172842,#172843,
#172844,#172845,#172846,#172847,#172848,#172849,#172850,#172851,#172852,
#172853,#172854,#172855,#172856,#172857,#172858,#172859,#172860,#172861,
#172862,#172863,#172864,#172865,#172866,#172867,#172868,#172869,#172870,
#172871,#172872,#172873,#172874,#172875),.UNSPECIFIED.,.F.,.F.,(4,3,3,3,
3,3,3,3,3,3,3,3,3,3,3,3,3,3,3,3,3,3,3,3,3,3,3,3,3,3,3,3,3,3,3,3,3,3,3,3,
3,3,3,3,3,3,3,3,3,3,3,3,3,3,3,3,3,3,3,3,3,3,3,3,3,3,3,3,3,3,3,3,3,3,3,3,
3,3,3,3,3,4),(-1084.80041458373,-1084.71357163134,-1084.63361433121,-1084.55375153397,
-1084.47396571149,-1084.3942393963,-1084.31455516801,-1084.23488418178,
-1084.15521672826,-1084.07553707744,-1083.99582949505,-1083.91603426597,
-1083.83618992427,-1083.75623149722,-1083.71383562062,-1083.63387832049,
-1083.55401552325,-1083.47422970077,-1083.39450338558,-1083.31481915728,
-1083.23514817106,-1083.15548071754,-1083.07580106672,-1082.99609348433,
-1082.91629825525,-1082.83645391354,-1082.7564954865,-1082.7140996099,-1082.63414230977,
-1082.55427951253,-1082.47449369005,-1082.39476737486,-1082.31508314657,
-1082.23541216034,-1082.15574470682,-1082.076065056,-1081.99635747361,-1081.91656224453,
-1081.83671790283,-1081.75675947578,-1081.71436359918,-1081.63440629905,
-1081.55454350181,-1081.47475767933,-1081.39503136414,-1081.31534713584,
-1081.23567614962,-1081.1560086961,-1081.07632904528,-1080.99662146289,
-1080.91682623381,-1080.8369818921,-1080.75702346506,-1080.71462758846,
-1080.63467028833,-1080.55480749109,-1080.47502166861,-1080.39529535342,
-1080.31561112513,-1080.2359401389,-1080.15627268538,-1080.07659303456,
-1079.99688545217,-1079.91709022309,-1079.83724588138,-1079.75728745434,
-1079.71489157774,-1079.63493427761,-1079.55507148037,-1079.47528565789,
-1079.3955593427,-1079.3158751144,-1079.23620412818,-1079.15653667466,-1079.07685702384,
-1078.99714944145,-1078.91735421237,-1078.83750987066,-1078.75755144361,
-1078.71515556702,-1078.59977111222,-1078.51722927655),.UNSPECIFIED.);
#1496=B_SPLINE_CURVE_WITH_KNOTS('',3,(#172877,#172878,#172879,#172880,#172881,
#172882,#172883,#172884,#172885,#172886),.UNSPECIFIED.,.F.,.F.,(4,1,1,1,
1,1,1,4),(-1078.51722580384,-1077.7154195563,-1076.71568354558,-1075.71594753486,
-1074.71621152414,-1073.71647551342,-1072.7167395027,-1072.23404396937),
 .UNSPECIFIED.);
#1497=B_SPLINE_CURVE_WITH_KNOTS('',3,(#172888,#172889,#172890,#172891,#172892,
#172893,#172894,#172895,#172896,#172897),.UNSPECIFIED.,.F.,.F.,(4,1,1,1,
1,1,1,4),(-1072.23404396937,-1071.71700349198,-1070.71726748126,-1069.71753147054,
-1068.71779545982,-1067.7180594491,-1066.71832343838,-1065.95085866219),
 .UNSPECIFIED.);
#1498=B_SPLINE_CURVE_WITH_KNOTS('',3,(#172899,#172900,#172901,#172902,#172903,
#172904,#172905,#172906,#172907,#172908,#172909),.UNSPECIFIED.,.F.,.F.,
(4,1,1,1,1,1,1,1,4),(-1065.95085866219,-1065.71858742766,-1064.71885141694,
-1063.71911540622,-1062.7193793955,-1061.71964338478,-1060.71990737406,
-1059.72017136334,-1059.66767335501),.UNSPECIFIED.);
#1499=B_SPLINE_CURVE_WITH_KNOTS('',3,(#172911,#172912,#172913,#172914,#172915,
#172916,#172917,#172918,#172919,#172920),.UNSPECIFIED.,.F.,.F.,(4,1,1,1,
1,1,1,4),(-1059.66767335501,-1058.72043535262,-1057.7206993419,-1056.72096333118,
-1055.72122732046,-1054.72149130974,-1053.72175529902,-1053.38449557091),
 .UNSPECIFIED.);
#1500=B_SPLINE_CURVE_WITH_KNOTS('',3,(#172922,#172923,#172924,#172925,#172926,
#172927,#172928,#172929,#172930,#172931,#172932,#172933,#172934,#172935,
#172936,#172937,#172938,#172939,#172940,#172941,#172942,#172943,#172944,
#172945,#172946,#172947,#172948,#172949,#172950,#172951,#172952,#172953,
#172954,#172955,#172956,#172957,#172958,#172959,#172960,#172961,#172962,
#172963,#172964,#172965,#172966,#172967,#172968,#172969,#172970,#172971,
#172972,#172973,#172974,#172975,#172976,#172977,#172978,#172979,#172980,
#172981,#172982,#172983,#172984,#172985,#172986,#172987,#172988,#172989,
#172990,#172991,#172992,#172993,#172994,#172995,#172996,#172997,#172998,
#172999,#173000,#173001,#173002,#173003,#173004,#173005,#173006,#173007,
#173008,#173009,#173010,#173011,#173012,#173013,#173014,#173015,#173016,
#173017,#173018,#173019,#173020,#173021,#173022,#173023,#173024,#173025,
#173026,#173027,#173028,#173029,#173030,#173031,#173032,#173033,#173034,
#173035,#173036,#173037,#173038,#173039,#173040,#173041,#173042,#173043,
#173044,#173045,#173046,#173047,#173048,#173049,#173050,#173051,#173052,
#173053,#173054,#173055,#173056,#173057,#173058,#173059,#173060,#173061,
#173062,#173063,#173064,#173065,#173066,#173067,#173068,#173069,#173070,
#173071,#173072,#173073,#173074,#173075,#173076,#173077,#173078,#173079,
#173080,#173081,#173082,#173083,#173084,#173085,#173086,#173087,#173088,
#173089,#173090,#173091,#173092,#173093,#173094,#173095,#173096,#173097,
#173098,#173099,#173100,#173101,#173102,#173103,#173104,#173105,#173106,
#173107,#173108,#173109,#173110,#173111,#173112,#173113,#173114,#173115,
#173116,#173117,#173118,#173119,#173120,#173121,#173122,#173123,#173124,
#173125,#173126,#173127,#173128,#173129,#173130,#173131,#173132,#173133,
#173134,#173135,#173136,#173137,#173138,#173139,#173140,#173141,#173142,
#173143,#173144,#173145,#173146,#173147,#173148,#173149,#173150,#173151,
#173152,#173153,#173154,#173155,#173156,#173157,#173158,#173159,#173160,
#173161,#173162,#173163,#173164,#173165,#173166,#173167,#173168),
 .UNSPECIFIED.,.F.,.F.,(4,3,3,3,3,3,3,3,3,3,3,3,3,3,3,3,3,3,3,3,3,3,3,3,
3,3,3,3,3,3,3,3,3,3,3,3,3,3,3,3,3,3,3,3,3,3,3,3,3,3,3,3,3,3,3,3,3,3,3,3,
3,3,3,3,3,3,3,3,3,3,3,3,3,3,3,3,3,3,3,3,3,3,4),(-1053.38448804783,-1053.30167945289,
-1053.22201542787,-1053.14234607935,-1053.06265574047,-1052.9829287348,
-1052.90310594554,-1052.82322647131,-1052.74323316342,-1052.7220192883,
-1052.64206198817,-1052.56219919093,-1052.48241336845,-1052.40268705326,
-1052.32300282496,-1052.24333183874,-1052.16366438522,-1052.0839847344,
-1052.004277152,-1051.92448192293,-1051.84463758122,-1051.76467915417,-1051.72228327758,
-1051.64232597745,-1051.56246318021,-1051.48267735773,-1051.40295104254,
-1051.32326681424,-1051.24359582802,-1051.1639283745,-1051.08424872368,
-1051.00454114129,-1050.92474591221,-1050.8449015705,-1050.76494314345,
-1050.72254726686,-1050.64258996673,-1050.56272716949,-1050.48294134702,
-1050.40321503182,-1050.32353080353,-1050.24385981731,-1050.16419236378,
-1050.08451271296,-1050.00480513057,-1049.92500990149,-1049.84516555979,
-1049.76520713274,-1049.72281125614,-1049.64285395601,-1049.56299115877,
-1049.48320533629,-1049.4034790211,-1049.32379479281,-1049.24412380658,
-1049.16445635306,-1049.08477670224,-1049.00506911985,-1048.92527389077,
-1048.84542954906,-1048.76547112202,-1048.72307524542,-1048.64311794529,
-1048.56325514805,-1048.48346932558,-1048.40374301038,-1048.32405878209,
-1048.24438779587,-1048.16472034234,-1048.08504069153,-1048.00533310913,
-1047.92553788006,-1047.84569353835,-1047.7657351113,-1047.7233392347,-1047.64267070184,
-1047.56210075995,-1047.48161433869,-1047.40119642267,-1047.32083745328,
-1047.24051357248,-1047.16020183974,-1047.10130274065),.UNSPECIFIED.);
#1501=B_SPLINE_CURVE_WITH_KNOTS('',3,(#173170,#173171,#173172,#173173,#173174,
#173175,#173176,#173177,#173178,#173179),.UNSPECIFIED.,.F.,.F.,(4,1,1,1,
1,1,1,4),(-1047.1012951378,-1046.72360322398,-1045.72386721326,-1044.72413120254,
-1043.72439519182,-1042.7246591811,-1041.72492317038,-1040.8181264349),
 .UNSPECIFIED.);
#1502=B_SPLINE_CURVE_WITH_KNOTS('',3,(#173181,#173182,#173183,#173184,#173185,
#173186,#173187,#173188,#173189,#173190,#173191,#173192,#173193,#173194,
#173195,#173196,#173197,#173198,#173199,#173200,#173201,#173202,#173203,
#173204,#173205,#173206,#173207,#173208,#173209,#173210,#173211,#173212,
#173213,#173214,#173215,#173216,#173217,#173218,#173219,#173220,#173221,
#173222,#173223,#173224,#173225,#173226,#173227,#173228,#173229,#173230,
#173231,#173232,#173233,#173234,#173235,#173236,#173237,#173238,#173239,
#173240,#173241,#173242,#173243,#173244,#173245,#173246,#173247,#173248,
#173249,#173250,#173251,#173252,#173253,#173254,#173255,#173256,#173257,
#173258,#173259,#173260,#173261,#173262,#173263,#173264,#173265,#173266,
#173267,#173268,#173269,#173270,#173271,#173272,#173273,#173274,#173275,
#173276,#173277,#173278,#173279,#173280,#173281,#173282,#173283,#173284,
#173285,#173286,#173287,#173288,#173289,#173290,#173291,#173292,#173293,
#173294,#173295,#173296,#173297,#173298,#173299,#173300,#173301,#173302,
#173303,#173304,#173305,#173306,#173307,#173308,#173309,#173310,#173311,
#173312,#173313,#173314,#173315,#173316,#173317,#173318,#173319,#173320,
#173321,#173322,#173323,#173324,#173325,#173326,#173327,#173328,#173329,
#173330,#173331,#173332,#173333,#173334,#173335,#173336,#173337,#173338,
#173339,#173340,#173341,#173342,#173343,#173344,#173345,#173346,#173347,
#173348,#173349,#173350,#173351,#173352,#173353,#173354,#173355,#173356,
#173357,#173358,#173359,#173360,#173361,#173362,#173363,#173364,#173365,
#173366,#173367,#173368,#173369,#173370,#173371,#173372,#173373,#173374,
#173375,#173376,#173377,#173378,#173379,#173380,#173381,#173382,#173383,
#173384,#173385,#173386,#173387,#173388,#173389,#173390,#173391,#173392,
#173393,#173394,#173395,#173396,#173397,#173398,#173399,#173400,#173401,
#173402,#173403,#173404,#173405,#173406,#173407,#173408,#173409,#173410,
#173411,#173412,#173413,#173414,#173415,#173416,#173417,#173418,#173419,
#173420,#173421,#173422,#173423,#173424),.UNSPECIFIED.,.F.,.F.,(4,3,3,3,
3,3,3,3,3,3,3,3,3,3,3,3,3,3,3,3,3,3,3,3,3,3,3,3,3,3,3,3,3,3,3,3,3,3,3,3,
3,3,3,3,3,3,3,3,3,3,3,3,3,3,3,3,3,3,3,3,3,3,3,3,3,3,3,3,3,3,3,3,3,3,3,3,
3,3,3,3,3,4),(-1040.81811743347,-1040.72518715966,-1040.64522985953,-1040.56536706229,
-1040.48558123981,-1040.40585492462,-1040.32617069632,-1040.2464997101,
-1040.16683225657,-1040.08715260576,-1040.00744502336,-1039.92764979429,
-1039.84780545258,-1039.76784702553,-1039.72545114894,-1039.64549384881,
-1039.56563105157,-1039.48584522909,-1039.4061189139,-1039.3264346856,-1039.24676369938,
-1039.16709624586,-1039.08741659504,-1039.00770901265,-1038.92791378357,
-1038.84806944186,-1038.76811101482,-1038.72571513822,-1038.64575783809,
-1038.56589504085,-1038.48610921837,-1038.40638290318,-1038.32669867489,
-1038.24702768866,-1038.16736023514,-1038.08768058432,-1038.00797300193,
-1037.92817777285,-1037.84833343114,-1037.7683750041,-1037.7259791275,-1037.64602182737,
-1037.56615903013,-1037.48637320765,-1037.40664689246,-1037.32696266416,
-1037.24729167794,-1037.16762422442,-1037.0879445736,-1037.00823699121,
-1036.92844176213,-1036.84859742042,-1036.76863899338,-1036.72624311678,
-1036.64628581665,-1036.56642301941,-1036.48663719693,-1036.40691088174,
-1036.32722665344,-1036.24755566722,-1036.1678882137,-1036.08820856288,
-1036.00850098049,-1035.92870575141,-1035.8488614097,-1035.76890298266,
-1035.72650710606,-1035.64654980593,-1035.56668700869,-1035.48690118622,
-1035.40717487102,-1035.32749064273,-1035.24781965651,-1035.16815220299,
-1035.08847255217,-1035.00876496978,-1034.9289697407,-1034.849125399,-1034.76916697195,
-1034.72677109534,-1034.60948897058,-1034.53493212629),.UNSPECIFIED.);
#1503=B_SPLINE_CURVE_WITH_KNOTS('',3,(#173426,#173427,#173428,#173429,#173430,
#173431,#173432,#173433,#173434,#173435),.UNSPECIFIED.,.F.,.F.,(4,1,1,1,
1,1,1,4),(-1034.53492806915,-1033.72703508462,-1032.7272990739,-1031.72756306318,
-1030.72782705246,-1029.72809104174,-1028.72835503102,-1028.25174681911),
 .UNSPECIFIED.);
#1504=B_SPLINE_CURVE_WITH_KNOTS('',3,(#173437,#173438,#173439,#173440,#173441,
#173442,#173443,#173444,#173445,#173446),.UNSPECIFIED.,.F.,.F.,(4,1,1,1,
1,1,1,4),(-1028.25174681911,-1027.72861902029,-1026.72888300957,-1025.72914699885,
-1024.72941098813,-1023.72967497741,-1022.72993896669,-1021.96856151193),
 .UNSPECIFIED.);
#1505=B_SPLINE_CURVE_WITH_KNOTS('',3,(#173448,#173449,#173450,#173451,#173452,
#173453,#173454,#173455,#173456,#173457,#173458),.UNSPECIFIED.,.F.,.F.,
(4,1,1,1,1,1,1,1,4),(-1021.96856151193,-1021.73020295597,-1020.73046694525,
-1019.73073093453,-1018.73099492381,-1017.73125891309,-1016.73152290237,
-1015.73178689165,-1015.68537620475),.UNSPECIFIED.);
#1506=B_SPLINE_CURVE_WITH_KNOTS('',3,(#173460,#173461,#173462,#173463,#173464,
#173465,#173466,#173467,#173468,#173469),.UNSPECIFIED.,.F.,.F.,(4,1,1,1,
1,1,1,4),(-1015.68537620475,-1014.73205088093,-1013.73231487021,-1012.73257885949,
-1011.73284284877,-1010.73310683805,-1009.73337082733,-1009.40219824018),
 .UNSPECIFIED.);
#1507=B_SPLINE_CURVE_WITH_KNOTS('',3,(#173471,#173472,#173473,#173474,#173475,
#173476,#173477,#173478,#173479,#173480,#173481,#173482,#173483,#173484,
#173485,#173486,#173487,#173488,#173489,#173490,#173491,#173492,#173493,
#173494,#173495,#173496,#173497,#173498,#173499,#173500,#173501,#173502,
#173503,#173504,#173505,#173506,#173507,#173508,#173509,#173510,#173511,
#173512,#173513,#173514,#173515,#173516,#173517,#173518,#173519,#173520,
#173521,#173522,#173523,#173524,#173525,#173526,#173527,#173528,#173529,
#173530,#173531,#173532,#173533,#173534,#173535,#173536,#173537,#173538,
#173539,#173540,#173541,#173542,#173543,#173544,#173545,#173546,#173547,
#173548,#173549,#173550,#173551,#173552,#173553,#173554,#173555,#173556,
#173557,#173558,#173559,#173560,#173561,#173562,#173563,#173564,#173565,
#173566,#173567,#173568,#173569,#173570,#173571,#173572,#173573,#173574,
#173575,#173576,#173577,#173578,#173579,#173580,#173581,#173582,#173583,
#173584,#173585,#173586,#173587,#173588,#173589,#173590,#173591,#173592,
#173593,#173594,#173595,#173596,#173597,#173598,#173599,#173600,#173601,
#173602,#173603,#173604,#173605,#173606,#173607,#173608,#173609,#173610,
#173611,#173612,#173613,#173614,#173615,#173616,#173617,#173618,#173619,
#173620,#173621,#173622,#173623,#173624,#173625,#173626,#173627,#173628,
#173629,#173630,#173631,#173632,#173633,#173634,#173635,#173636,#173637,
#173638,#173639,#173640,#173641,#173642,#173643,#173644,#173645,#173646,
#173647,#173648,#173649,#173650,#173651,#173652,#173653,#173654,#173655,
#173656,#173657,#173658,#173659,#173660,#173661,#173662,#173663,#173664,
#173665,#173666,#173667,#173668,#173669,#173670,#173671,#173672,#173673,
#173674,#173675,#173676,#173677,#173678,#173679,#173680,#173681,#173682,
#173683,#173684,#173685,#173686,#173687,#173688,#173689,#173690,#173691,
#173692,#173693,#173694,#173695,#173696,#173697,#173698,#173699,#173700,
#173701,#173702,#173703,#173704,#173705,#173706,#173707,#173708,#173709,
#173710,#173711,#173712,#173713,#173714,#173715,#173716,#173717),
 .UNSPECIFIED.,.F.,.F.,(4,3,3,3,3,3,3,3,3,3,3,3,3,3,3,3,3,3,3,3,3,3,3,3,
3,3,3,3,3,3,3,3,3,3,3,3,3,3,3,3,3,3,3,3,3,3,3,3,3,3,3,3,3,3,3,3,3,3,3,3,
3,3,3,3,3,3,3,3,3,3,3,3,3,3,3,3,3,3,3,3,3,3,4),(-1009.40219089757,-1009.31862138745,
-1009.23904212832,-1009.15945978643,-1009.0798586105,-1009.00022284082,
-1008.92049278562,-1008.84070773089,-1008.76080793305,-1008.73363481661,
-1008.65367751648,-1008.57381471924,-1008.49402889676,-1008.41430258157,
-1008.33461835327,-1008.25494736705,-1008.17527991353,-1008.09560026271,
-1008.01589268032,-1007.93609745124,-1007.85625310953,-1007.77629468249,
-1007.73389880589,-1007.65394150576,-1007.57407870852,-1007.49429288604,
-1007.41456657085,-1007.33488234256,-1007.25521135633,-1007.17554390281,
-1007.09586425199,-1007.0161566696,-1006.93636144052,-1006.85651709881,
-1006.77655867177,-1006.73416279517,-1006.65420549504,-1006.5743426978,
-1006.49455687532,-1006.41483056013,-1006.33514633183,-1006.25547534561,
-1006.17580789209,-1006.09612824127,-1006.01642065888,-1005.9366254298,
-1005.85678108809,-1005.77682266105,-1005.73442678445,-1005.65446948432,
-1005.57460668708,-1005.4948208646,-1005.41509454941,-1005.33541032112,
-1005.25573933489,-1005.17607188137,-1005.09639223055,-1005.01668464816,
-1004.93688941908,-1004.85704507737,-1004.77708665033,-1004.73469077373,
-1004.6547334736,-1004.57487067636,-1004.49508485389,-1004.41535853869,
-1004.3356743104,-1004.25600332418,-1004.17633587065,-1004.09665621983,
-1004.01694863744,-1003.93715340836,-1003.85730906666,-1003.77735063961,
-1003.73495476301,-1003.65416438689,-1003.57347370472,-1003.49286779783,
-1003.41233180347,-1003.33185761023,-1003.25141993018,-1003.17099831016,
-1003.11900559039),.UNSPECIFIED.);
#1508=B_SPLINE_CURVE_WITH_KNOTS('',3,(#173719,#173720,#173721,#173722,#173723,
#173724,#173725,#173726,#173727,#173728),.UNSPECIFIED.,.F.,.F.,(4,1,1,1,
1,1,1,4),(-1003.1189981033,-1002.73521875229,-1001.73548274157,-1000.73574673085,
-999.736010720131,-998.736274709411,-997.736538698691,-996.835829368632),
 .UNSPECIFIED.);
#1509=B_SPLINE_CURVE_WITH_KNOTS('',3,(#173730,#173731,#173732,#173733,#173734,
#173735,#173736,#173737,#173738,#173739,#173740,#173741,#173742,#173743,
#173744,#173745,#173746,#173747,#173748,#173749,#173750,#173751,#173752,
#173753,#173754,#173755,#173756,#173757,#173758,#173759,#173760,#173761,
#173762,#173763,#173764,#173765,#173766,#173767,#173768,#173769,#173770,
#173771,#173772,#173773,#173774,#173775,#173776,#173777,#173778,#173779,
#173780,#173781,#173782,#173783,#173784,#173785,#173786,#173787,#173788,
#173789,#173790,#173791,#173792,#173793,#173794,#173795,#173796,#173797,
#173798,#173799,#173800,#173801,#173802,#173803,#173804,#173805,#173806,
#173807,#173808,#173809,#173810,#173811,#173812,#173813,#173814,#173815,
#173816,#173817,#173818,#173819,#173820,#173821,#173822,#173823,#173824,
#173825,#173826,#173827,#173828,#173829,#173830,#173831,#173832,#173833,
#173834,#173835,#173836,#173837,#173838,#173839,#173840,#173841,#173842,
#173843,#173844,#173845,#173846,#173847,#173848,#173849,#173850,#173851,
#173852,#173853,#173854,#173855,#173856,#173857,#173858,#173859,#173860,
#173861,#173862,#173863,#173864,#173865,#173866,#173867,#173868,#173869,
#173870,#173871,#173872,#173873,#173874,#173875,#173876,#173877,#173878,
#173879,#173880,#173881,#173882,#173883,#173884,#173885,#173886,#173887,
#173888,#173889,#173890,#173891,#173892,#173893,#173894,#173895,#173896,
#173897,#173898,#173899,#173900,#173901,#173902,#173903,#173904,#173905,
#173906,#173907,#173908,#173909,#173910,#173911,#173912,#173913,#173914,
#173915,#173916,#173917,#173918,#173919,#173920,#173921,#173922,#173923,
#173924,#173925,#173926,#173927,#173928,#173929,#173930,#173931,#173932,
#173933,#173934,#173935,#173936,#173937,#173938,#173939,#173940,#173941,
#173942,#173943,#173944,#173945,#173946,#173947,#173948,#173949,#173950,
#173951,#173952,#173953,#173954,#173955,#173956,#173957,#173958,#173959,
#173960,#173961,#173962,#173963,#173964,#173965,#173966,#173967,#173968,
#173969,#173970,#173971,#173972,#173973),.UNSPECIFIED.,.F.,.F.,(4,3,3,3,
3,3,3,3,3,3,3,3,3,3,3,3,3,3,3,3,3,3,3,3,3,3,3,3,3,3,3,3,3,3,3,3,3,3,3,3,
3,3,3,3,3,3,3,3,3,3,3,3,3,3,3,3,3,3,3,3,3,3,3,3,3,3,3,3,3,3,3,3,3,3,3,3,
3,3,3,3,3,4),(-996.835820283214,-996.736802687971,-996.656845387839,-996.576982590595,
-996.497196768122,-996.417470452926,-996.337786224631,-996.258115238409,
-996.178447784882,-996.098768134065,-996.019060551669,-995.939265322593,
-995.859420980884,-995.779462553835,-995.737066677251,-995.65710937712,
-995.577246579877,-995.497460757405,-995.41773444221,-995.338050213916,
-995.258379227695,-995.178711774169,-995.099032123353,-995.019324540959,
-994.939529311883,-994.859684970175,-994.779726543128,-994.73733066653,
-994.657373366399,-994.577510569156,-994.497724746684,-994.417998431489,
-994.338314203195,-994.258643216974,-994.178975763448,-994.099296112632,
-994.019588530237,-993.939793301162,-993.859948959454,-993.779990532407,
-993.73759465581,-993.657637355679,-993.577774558436,-993.497988735965,
-993.418262420769,-993.338578192475,-993.258907206254,-993.179239752729,
-993.099560101912,-993.019852519518,-992.940057290442,-992.860212948735,
-992.780254521687,-992.73785864509,-992.657901344959,-992.578038547716,
-992.498252725244,-992.418526410049,-992.338842181755,-992.259171195534,
-992.179503742008,-992.099824091192,-992.020116508798,-991.940321279722,
-991.860476938015,-991.780518510967,-991.73812263437,-991.658165334239,
-991.578302536996,-991.498516714524,-991.418790399329,-991.339106171035,
-991.259435184814,-991.179767731288,-991.100088080471,-991.020380498077,
-990.940585269001,-990.860740927293,-990.780782500246,-990.73838662365,
-990.619045316449,-990.552634976034),.UNSPECIFIED.);
#1510=B_SPLINE_CURVE_WITH_KNOTS('',3,(#173975,#173976,#173977,#173978,#173979,
#173980,#173981,#173982,#173983,#173984),.UNSPECIFIED.,.F.,.F.,(4,1,1,1,
1,1,1,4),(-990.552630350918,-989.73865061293,-988.73891460221,-987.739178591489,
-986.739442580769,-985.739706570049,-984.739970559329,-984.269449668855),
 .UNSPECIFIED.);
#1511=B_SPLINE_CURVE_WITH_KNOTS('',3,(#173986,#173987,#173988,#173989,#173990,
#173991,#173992,#173993,#173994,#173995),.UNSPECIFIED.,.F.,.F.,(4,1,1,1,
1,1,1,4),(-984.269449668855,-983.740234548609,-982.740498537889,-981.740762527169,
-980.741026516449,-979.741290505728,-978.741554495008,-977.986264361675),
 .UNSPECIFIED.);
#1512=B_SPLINE_CURVE_WITH_KNOTS('',3,(#173997,#173998,#173999,#174000,#174001,
#174002,#174003,#174004,#174005,#174006,#174007,#174008,#174009,#174010,
#174011,#174012,#174013,#174014,#174015,#174016,#174017,#174018,#174019,
#174020,#174021,#174022,#174023,#174024,#174025,#174026,#174027,#174028,
#174029,#174030,#174031,#174032,#174033,#174034,#174035,#174036,#174037,
#174038,#174039,#174040,#174041,#174042,#174043,#174044,#174045,#174046,
#174047,#174048,#174049,#174050,#174051,#174052,#174053,#174054,#174055,
#174056,#174057,#174058,#174059,#174060,#174061,#174062,#174063,#174064,
#174065,#174066,#174067,#174068,#174069,#174070,#174071,#174072,#174073,
#174074,#174075,#174076,#174077,#174078,#174079,#174080,#174081,#174082,
#174083,#174084,#174085,#174086,#174087,#174088,#174089,#174090,#174091,
#174092,#174093,#174094,#174095,#174096,#174097,#174098,#174099,#174100,
#174101,#174102,#174103,#174104,#174105,#174106,#174107,#174108,#174109,
#174110,#174111,#174112,#174113,#174114,#174115,#174116,#174117,#174118,
#174119,#174120,#174121,#174122,#174123,#174124,#174125,#174126,#174127,
#174128,#174129,#174130,#174131,#174132,#174133,#174134,#174135,#174136,
#174137,#174138,#174139,#174140,#174141,#174142,#174143,#174144,#174145,
#174146,#174147,#174148,#174149,#174150,#174151,#174152,#174153,#174154,
#174155,#174156,#174157,#174158,#174159,#174160,#174161,#174162,#174163,
#174164,#174165,#174166,#174167,#174168,#174169,#174170,#174171,#174172,
#174173,#174174,#174175,#174176,#174177,#174178,#174179,#174180,#174181,
#174182,#174183,#174184,#174185,#174186,#174187,#174188,#174189,#174190,
#174191,#174192,#174193,#174194,#174195,#174196,#174197,#174198,#174199,
#174200,#174201,#174202,#174203,#174204,#174205,#174206,#174207,#174208,
#174209,#174210,#174211,#174212,#174213,#174214,#174215,#174216,#174217,
#174218,#174219,#174220,#174221,#174222,#174223,#174224,#174225,#174226,
#174227,#174228,#174229,#174230,#174231,#174232,#174233,#174234,#174235,
#174236,#174237,#174238,#174239,#174240,#174241,#174242,#174243),
 .UNSPECIFIED.,.F.,.F.,(4,3,3,3,3,3,3,3,3,3,3,3,3,3,3,3,3,3,3,3,3,3,3,3,
3,3,3,3,3,3,3,3,3,3,3,3,3,3,3,3,3,3,3,3,3,3,3,3,3,3,3,3,3,3,3,3,3,3,3,3,
3,3,3,3,3,3,3,3,3,3,3,3,3,3,3,3,3,3,3,3,3,3,4),(-977.986264286946,-977.882988264251,
-977.777257487168,-977.741818484288,-977.661861184157,-977.581998386914,
-977.502212564442,-977.422486249247,-977.342802020953,-977.263131034732,
-977.183463581206,-977.103783930389,-977.024076347995,-976.944281118919,
-976.864436777212,-976.784478350164,-976.742082473568,-976.662125173437,
-976.582262376194,-976.502476553722,-976.422750238527,-976.343066010233,
-976.263395024012,-976.183727570486,-976.10404791967,-976.024340337275,
-975.9445451082,-975.864700766492,-975.784742339445,-975.742346462848,-975.662389162717,
-975.582526365474,-975.502740543002,-975.423014227807,-975.343329999513,
-975.263659013292,-975.183991559766,-975.104311908949,-975.024604326555,
-974.944809097479,-974.864964755772,-974.785006328724,-974.742610452128,
-974.662653151997,-974.582790354754,-974.503004532282,-974.423278217087,
-974.343593988793,-974.263923002572,-974.184255549046,-974.10457589823,
-974.024868315835,-973.94507308676,-973.865228745052,-973.785270318005,
-973.742874441408,-973.662917141277,-973.583054344035,-973.503268521563,
-973.423542206368,-973.343857978074,-973.264186991853,-973.184519538327,
-973.104839887511,-973.025132305117,-972.945337076041,-972.865492734334,
-972.785534307287,-972.743138430688,-972.663181130556,-972.583318333313,
-972.503532510841,-972.423806195645,-972.344121967351,-972.26445098113,
-972.184783527603,-972.105103876787,-972.025396294392,-971.945601065316,
-971.865756723608,-971.78579829656,-971.743402419967,-971.703079054496),
 .UNSPECIFIED.);
#1513=B_SPLINE_CURVE_WITH_KNOTS('',3,(#174245,#174246,#174247,#174248,#174249,
#174250,#174251,#174252,#174253,#174254),.UNSPECIFIED.,.F.,.F.,(4,1,1,1,
1,1,1,4),(-971.703073555962,-970.743666409247,-969.743930398527,-968.744194387807,
-967.744458377087,-966.744722366367,-965.744986355647,-965.419893747316),
 .UNSPECIFIED.);
#1514=B_SPLINE_CURVE_WITH_KNOTS('',3,(#174256,#174257,#174258,#174259,#174260,
#174261,#174262,#174263,#174264,#174265),.UNSPECIFIED.,.F.,.F.,(4,1,1,1,
1,1,1,4),(-965.419893747316,-964.745250344926,-963.745514334207,-962.745778323486,
-961.746042312766,-960.746306302046,-959.746570291326,-959.136708440137),
 .UNSPECIFIED.);
#1515=B_SPLINE_CURVE_WITH_KNOTS('',3,(#174267,#174268,#174269,#174270,#174271,
#174272,#174273,#174274,#174275,#174276),.UNSPECIFIED.,.F.,.F.,(4,1,1,1,
1,1,1,4),(-959.136708440137,-958.746834280606,-957.747098269886,-956.747362259165,
-955.747626248445,-954.747890237725,-953.748154227005,-952.853523132957),
 .UNSPECIFIED.);
#1516=B_SPLINE_CURVE_WITH_KNOTS('',3,(#174278,#174279,#174280,#174281,#174282,
#174283,#174284,#174285,#174286,#174287,#174288),.UNSPECIFIED.,.F.,.F.,
(4,1,1,1,1,1,1,1,4),(-952.853523132957,-952.748418216285,-951.748682205565,
-950.748946194845,-949.749210184125,-948.749474173404,-947.749738162684,
-946.750002151964,-946.570337825777),.UNSPECIFIED.);
#1517=B_SPLINE_CURVE_WITH_KNOTS('',3,(#174290,#174291,#174292,#174293,#174294,
#174295,#174296,#174297,#174298,#174299,#174300,#174301,#174302,#174303,
#174304,#174305,#174306,#174307,#174308,#174309,#174310,#174311,#174312,
#174313,#174314,#174315,#174316,#174317,#174318,#174319,#174320,#174321,
#174322,#174323,#174324,#174325,#174326,#174327,#174328,#174329,#174330,
#174331,#174332,#174333,#174334,#174335,#174336,#174337,#174338,#174339,
#174340,#174341,#174342,#174343,#174344,#174345,#174346,#174347,#174348,
#174349,#174350,#174351,#174352,#174353,#174354,#174355,#174356,#174357,
#174358,#174359,#174360,#174361,#174362,#174363,#174364,#174365,#174366,
#174367,#174368,#174369,#174370,#174371,#174372,#174373,#174374,#174375,
#174376,#174377,#174378,#174379,#174380,#174381,#174382,#174383,#174384,
#174385,#174386,#174387,#174388,#174389,#174390,#174391,#174392,#174393,
#174394,#174395,#174396,#174397,#174398,#174399,#174400,#174401,#174402,
#174403,#174404,#174405,#174406,#174407,#174408,#174409,#174410,#174411,
#174412,#174413,#174414,#174415,#174416,#174417,#174418,#174419,#174420,
#174421,#174422,#174423,#174424,#174425,#174426,#174427,#174428,#174429,
#174430,#174431,#174432,#174433,#174434,#174435,#174436,#174437,#174438,
#174439,#174440,#174441,#174442,#174443,#174444,#174445,#174446,#174447,
#174448,#174449,#174450,#174451,#174452,#174453,#174454,#174455,#174456,
#174457,#174458,#174459,#174460,#174461,#174462,#174463,#174464,#174465,
#174466,#174467,#174468,#174469,#174470,#174471,#174472,#174473,#174474,
#174475,#174476,#174477,#174478,#174479,#174480,#174481,#174482,#174483,
#174484,#174485,#174486,#174487,#174488,#174489,#174490,#174491,#174492,
#174493,#174494,#174495,#174496,#174497,#174498,#174499,#174500,#174501,
#174502,#174503,#174504,#174505,#174506,#174507,#174508,#174509,#174510,
#174511,#174512,#174513,#174514,#174515,#174516,#174517,#174518,#174519,
#174520,#174521,#174522,#174523,#174524,#174525,#174526,#174527,#174528,
#174529,#174530,#174531,#174532,#174533,#174534,#174535,#174536),
 .UNSPECIFIED.,.F.,.F.,(4,3,3,3,3,3,3,3,3,3,3,3,3,3,3,3,3,3,3,3,3,3,3,3,
3,3,3,3,3,3,3,3,3,3,3,3,3,3,3,3,3,3,3,3,3,3,3,3,3,3,3,3,3,3,3,3,3,3,3,3,
3,3,3,3,3,3,3,3,3,3,3,3,3,3,3,3,3,3,3,3,3,3,4),(-946.570337825777,-946.49169399442,
-946.413118638042,-946.334593371033,-946.256091089334,-946.177597911869,
-946.099097271433,-946.020572596639,-945.941965426675,-945.863311049155,
-945.7845474559,-945.750266141244,-945.670308841113,-945.59044604387,-945.510660221398,
-945.430933906203,-945.351249677909,-945.271578691688,-945.191911238163,
-945.112231587346,-945.032524004952,-944.952728775876,-944.872884434168,
-944.792926007121,-944.750530130524,-944.670572830393,-944.59071003315,
-944.510924210678,-944.431197895483,-944.351513667189,-944.271842680968,
-944.192175227442,-944.112495576626,-944.032787994232,-943.952992765156,
-943.873148423448,-943.793189996401,-943.750794119804,-943.670836819673,
-943.59097402243,-943.511188199958,-943.431461884764,-943.351777656469,
-943.272106670248,-943.192439216723,-943.112759565906,-943.033051983512,
-942.953256754436,-942.873412412728,-942.793453985681,-942.751058109084,
-942.671100808953,-942.59123801171,-942.511452189238,-942.431725874042,
-942.352041645748,-942.272370659527,-942.192703206002,-942.113023555185,
-942.033315972791,-941.953520743716,-941.873676402008,-941.793717974961,
-941.751322098364,-941.671364798233,-941.59150200099,-941.511716178518,
-941.431989863322,-941.352305635028,-941.272634648806,-941.19296719528,
-941.113287544464,-941.033579962069,-940.953784732993,-940.873940391285,
-940.793981964238,-940.751586087643,-940.666044999251,-940.580666781501,
-940.495520242455,-940.410515725407,-940.325710494659,-940.287152712433),
 .UNSPECIFIED.);
#1518=B_SPLINE_CURVE_WITH_KNOTS('',3,(#174538,#174539,#174540,#174541,#174542,
#174543,#174544,#174545,#174546,#174547),.UNSPECIFIED.,.F.,.F.,(4,1,1,1,
1,1,1,4),(-940.287152518598,-939.751850076923,-938.752114066203,-937.752378055483,
-936.752642044763,-935.752906034043,-934.753170023323,-934.003967211418),
 .UNSPECIFIED.);
#1519=B_SPLINE_CURVE_WITH_KNOTS('',3,(#174549,#174550,#174551,#174552,#174553,
#174554,#174555,#174556,#174557,#174558,#174559,#174560,#174561,#174562,
#174563,#174564,#174565,#174566,#174567,#174568,#174569,#174570,#174571,
#174572,#174573,#174574,#174575,#174576,#174577,#174578,#174579,#174580,
#174581,#174582,#174583,#174584,#174585,#174586,#174587,#174588,#174589,
#174590,#174591,#174592,#174593,#174594,#174595,#174596,#174597,#174598,
#174599,#174600,#174601,#174602,#174603,#174604,#174605,#174606,#174607,
#174608,#174609,#174610,#174611,#174612,#174613,#174614,#174615,#174616,
#174617,#174618,#174619,#174620,#174621,#174622,#174623,#174624,#174625,
#174626,#174627,#174628,#174629,#174630,#174631,#174632,#174633,#174634,
#174635,#174636,#174637,#174638,#174639,#174640,#174641,#174642,#174643,
#174644,#174645,#174646,#174647,#174648,#174649,#174650,#174651,#174652,
#174653,#174654,#174655,#174656,#174657,#174658,#174659,#174660,#174661,
#174662,#174663,#174664,#174665,#174666,#174667,#174668,#174669,#174670,
#174671,#174672,#174673,#174674,#174675,#174676,#174677,#174678,#174679,
#174680,#174681,#174682,#174683,#174684,#174685,#174686,#174687,#174688,
#174689,#174690,#174691,#174692,#174693,#174694,#174695,#174696,#174697,
#174698,#174699,#174700,#174701,#174702,#174703,#174704,#174705,#174706,
#174707,#174708,#174709,#174710,#174711,#174712,#174713,#174714,#174715,
#174716,#174717,#174718,#174719,#174720,#174721,#174722,#174723,#174724,
#174725,#174726,#174727,#174728,#174729,#174730,#174731,#174732,#174733,
#174734,#174735,#174736,#174737,#174738,#174739,#174740,#174741,#174742,
#174743,#174744,#174745,#174746,#174747,#174748,#174749,#174750,#174751,
#174752,#174753,#174754,#174755,#174756,#174757,#174758,#174759,#174760,
#174761,#174762,#174763,#174764,#174765,#174766,#174767,#174768,#174769,
#174770,#174771,#174772,#174773,#174774,#174775,#174776,#174777,#174778,
#174779,#174780,#174781,#174782,#174783,#174784,#174785,#174786,#174787,
#174788,#174789,#174790,#174791,#174792,#174793,#174794,#174795),
 .UNSPECIFIED.,.F.,.F.,(4,3,3,3,3,3,3,3,3,3,3,3,3,3,3,3,3,3,3,3,3,3,3,3,
3,3,3,3,3,3,3,3,3,3,3,3,3,3,3,3,3,3,3,3,3,3,3,3,3,3,3,3,3,3,3,3,3,3,3,3,
3,3,3,3,3,3,3,3,3,3,3,3,3,3,3,3,3,3,3,3,3,3,4),(-934.003967155371,-933.901650858112,
-933.797081270037,-933.753434012602,-933.673476712471,-933.593613915228,
-933.513828092756,-933.434101777561,-933.354417549267,-933.274746563046,
-933.19507910952,-933.115399458704,-933.035691876309,-932.955896647234,
-932.876052305526,-932.796093878479,-932.753698001882,-932.673740701751,
-932.593877904508,-932.514092082036,-932.434365766841,-932.354681538547,
-932.275010552326,-932.1953430988,-932.115663447983,-932.035955865589,-931.956160636513,
-931.876316294806,-931.796357867758,-931.753961991162,-931.674004691031,
-931.594141893788,-931.514356071316,-931.434629756121,-931.354945527827,
-931.275274541606,-931.19560708808,-931.115927437264,-931.036219854869,
-930.956424625794,-930.876580284086,-930.796621857039,-930.754225980442,
-930.674268680311,-930.594405883068,-930.514620060596,-930.434893745401,
-930.355209517107,-930.275538530886,-930.19587107736,-930.116191426543,
-930.036483844149,-929.956688615073,-929.876844273366,-929.796885846318,
-929.754489969722,-929.674532669591,-929.594669872348,-929.514884049876,
-929.435157734681,-929.355473506387,-929.275802520166,-929.19613506664,
-929.116455415824,-929.036747833429,-928.956952604354,-928.877108262646,
-928.797149835599,-928.754753959002,-928.674796658871,-928.594933861628,
-928.515148039157,-928.435421723961,-928.355737495667,-928.276066509446,
-928.19639905592,-928.116719405104,-928.037011822709,-927.957216593634,
-927.877372251926,-927.797413824879,-927.755017948282,-927.720781904239),
 .UNSPECIFIED.);
#1520=B_SPLINE_CURVE_WITH_KNOTS('',3,(#174797,#174798,#174799,#174800,#174801,
#174802,#174803,#174804,#174805,#174806),.UNSPECIFIED.,.F.,.F.,(4,1,1,1,
1,1,1,4),(-927.720777243923,-926.755281937562,-925.755545926841,-924.755809916121,
-923.756073905401,-922.756337894681,-921.756601883961,-921.437596597059),
 .UNSPECIFIED.);
#1521=B_SPLINE_CURVE_WITH_KNOTS('',3,(#174808,#174809,#174810,#174811,#174812,
#174813,#174814,#174815,#174816,#174817),.UNSPECIFIED.,.F.,.F.,(4,1,1,1,
1,1,1,4),(-921.437596597059,-920.756865873241,-919.757129862521,-918.7573938518,
-917.75765784108,-916.75792183036,-915.75818581964,-915.15441128988),
 .UNSPECIFIED.);
#1522=B_SPLINE_CURVE_WITH_KNOTS('',3,(#174819,#174820,#174821,#174822,#174823,
#174824,#174825,#174826,#174827,#174828),.UNSPECIFIED.,.F.,.F.,(4,1,1,1,
1,1,1,4),(-915.15441128988,-914.75844980892,-913.7587137982,-912.75897778748,
-911.75924177676,-910.75950576604,-909.759769755319,-908.8712259827),
 .UNSPECIFIED.);
#1523=B_SPLINE_CURVE_WITH_KNOTS('',3,(#174830,#174831,#174832,#174833,#174834,
#174835,#174836,#174837,#174838,#174839,#174840),.UNSPECIFIED.,.F.,.F.,
(4,1,1,1,1,1,1,1,4),(-908.8712259827,-908.760033744599,-907.760297733879,
-906.760561723159,-905.760825712439,-904.761089701719,-903.761353690998,
-902.761617680278,-902.588040675521),.UNSPECIFIED.);
#1524=B_SPLINE_CURVE_WITH_KNOTS('',3,(#174842,#174843,#174844,#174845,#174846,
#174847,#174848,#174849,#174850,#174851,#174852,#174853,#174854,#174855,
#174856,#174857,#174858,#174859,#174860,#174861,#174862,#174863,#174864,
#174865,#174866,#174867,#174868,#174869,#174870,#174871,#174872,#174873,
#174874,#174875,#174876,#174877,#174878,#174879,#174880,#174881,#174882,
#174883,#174884,#174885,#174886,#174887,#174888,#174889,#174890,#174891,
#174892,#174893,#174894,#174895,#174896,#174897,#174898,#174899,#174900,
#174901,#174902,#174903,#174904,#174905,#174906,#174907,#174908,#174909,
#174910,#174911,#174912,#174913,#174914,#174915,#174916,#174917,#174918,
#174919,#174920,#174921,#174922,#174923,#174924,#174925,#174926,#174927,
#174928,#174929,#174930,#174931,#174932,#174933,#174934,#174935,#174936,
#174937,#174938,#174939,#174940,#174941,#174942,#174943,#174944,#174945,
#174946,#174947,#174948,#174949,#174950,#174951,#174952,#174953,#174954,
#174955,#174956,#174957,#174958,#174959,#174960,#174961,#174962,#174963,
#174964,#174965,#174966,#174967,#174968,#174969,#174970,#174971,#174972,
#174973,#174974,#174975,#174976,#174977,#174978,#174979,#174980,#174981,
#174982,#174983,#174984,#174985,#174986,#174987,#174988,#174989,#174990,
#174991,#174992,#174993,#174994,#174995,#174996,#174997,#174998,#174999,
#175000,#175001,#175002,#175003,#175004,#175005,#175006,#175007,#175008,
#175009,#175010,#175011,#175012,#175013,#175014,#175015,#175016,#175017,
#175018,#175019,#175020,#175021,#175022,#175023,#175024,#175025,#175026,
#175027,#175028,#175029,#175030,#175031,#175032,#175033,#175034,#175035,
#175036,#175037,#175038,#175039,#175040,#175041,#175042,#175043,#175044,
#175045,#175046,#175047,#175048,#175049,#175050,#175051,#175052,#175053,
#175054,#175055,#175056,#175057,#175058,#175059,#175060,#175061,#175062,
#175063,#175064,#175065,#175066,#175067,#175068,#175069,#175070,#175071,
#175072,#175073,#175074,#175075,#175076,#175077,#175078,#175079,#175080,
#175081,#175082,#175083,#175084,#175085,#175086,#175087,#175088),
 .UNSPECIFIED.,.F.,.F.,(4,3,3,3,3,3,3,3,3,3,3,3,3,3,3,3,3,3,3,3,3,3,3,3,
3,3,3,3,3,3,3,3,3,3,3,3,3,3,3,3,3,3,3,3,3,3,3,3,3,3,3,3,3,3,3,3,3,3,3,3,
3,3,3,3,3,3,3,3,3,3,3,3,3,3,3,3,3,3,3,3,3,3,4),(-902.588040675521,-902.509394374953,
-902.430818019321,-902.352293215628,-902.273793277036,-902.195303758856,
-902.116808091585,-902.03828970253,-901.959689426147,-901.881043118882,
-901.802286029661,-901.761881669558,-901.681924369427,-901.602061572184,
-901.522275749713,-901.442549434517,-901.362865206223,-901.283194220002,
-901.203526766476,-901.12384711566,-901.044139533266,-900.96434430419,-900.884499962482,
-900.804541535435,-900.762145658838,-900.682188358707,-900.602325561464,
-900.522539738992,-900.442813423797,-900.363129195503,-900.283458209282,
-900.203790755757,-900.12411110494,-900.044403522546,-899.96460829347,-899.884763951762,
-899.804805524715,-899.762409648118,-899.682452347987,-899.602589550744,
-899.522803728272,-899.443077413077,-899.363393184783,-899.283722198563,
-899.204054745037,-899.12437509422,-899.044667511825,-898.96487228275,-898.885027941042,
-898.805069513995,-898.762673637398,-898.682716337267,-898.602853540024,
-898.523067717552,-898.443341402357,-898.363657174063,-898.283986187842,
-898.204318734316,-898.1246390835,-898.044931501105,-897.965136272029,-897.885291930322,
-897.805333503274,-897.762937626678,-897.682980326547,-897.603117529304,
-897.523331706833,-897.443605391638,-897.363921163344,-897.284250177123,
-897.204582723597,-897.124903072781,-897.045195490386,-896.965400261311,
-896.885555919603,-896.805597492556,-896.763201615958,-896.677381751715,
-896.591729906743,-896.506318888007,-896.421057019866,-896.336003844487,
-896.30485559323),.UNSPECIFIED.);
#1525=B_SPLINE_CURVE_WITH_KNOTS('',3,(#175090,#175091,#175092,#175093,#175094,
#175095,#175096,#175097,#175098,#175099),.UNSPECIFIED.,.F.,.F.,(4,1,1,1,
1,1,1,4),(-896.304855368341,-895.763465605238,-894.763729594517,-893.763993583797,
-892.764257573077,-891.764521562357,-890.764785551637,-890.021670061161),
 .UNSPECIFIED.);
#1526=B_SPLINE_CURVE_WITH_KNOTS('',3,(#175101,#175102,#175103,#175104,#175105,
#175106,#175107,#175108,#175109,#175110,#175111,#175112,#175113,#175114,
#175115,#175116,#175117,#175118,#175119,#175120,#175121,#175122,#175123,
#175124,#175125,#175126,#175127,#175128,#175129,#175130,#175131,#175132,
#175133,#175134,#175135,#175136,#175137,#175138,#175139,#175140,#175141,
#175142,#175143,#175144,#175145,#175146,#175147,#175148,#175149,#175150,
#175151,#175152,#175153,#175154,#175155,#175156,#175157,#175158,#175159,
#175160,#175161,#175162,#175163,#175164,#175165,#175166,#175167,#175168,
#175169,#175170,#175171,#175172,#175173,#175174,#175175,#175176,#175177,
#175178,#175179,#175180,#175181,#175182,#175183,#175184,#175185,#175186,
#175187,#175188,#175189,#175190,#175191,#175192,#175193,#175194,#175195,
#175196,#175197,#175198,#175199,#175200,#175201,#175202,#175203,#175204,
#175205,#175206,#175207,#175208,#175209,#175210,#175211,#175212,#175213,
#175214,#175215,#175216,#175217,#175218,#175219,#175220,#175221,#175222,
#175223,#175224,#175225,#175226,#175227,#175228,#175229,#175230,#175231,
#175232,#175233,#175234,#175235,#175236,#175237,#175238,#175239,#175240,
#175241,#175242,#175243,#175244,#175245,#175246,#175247,#175248,#175249,
#175250,#175251,#175252,#175253,#175254,#175255,#175256,#175257,#175258,
#175259,#175260,#175261,#175262,#175263,#175264,#175265,#175266,#175267,
#175268,#175269,#175270,#175271,#175272,#175273,#175274,#175275,#175276,
#175277,#175278,#175279,#175280,#175281,#175282,#175283,#175284,#175285,
#175286,#175287,#175288,#175289,#175290,#175291,#175292,#175293,#175294,
#175295,#175296,#175297,#175298,#175299,#175300,#175301,#175302,#175303,
#175304,#175305,#175306,#175307,#175308,#175309,#175310,#175311,#175312,
#175313,#175314,#175315,#175316,#175317,#175318,#175319,#175320,#175321,
#175322,#175323,#175324,#175325,#175326,#175327,#175328,#175329,#175330,
#175331,#175332,#175333,#175334,#175335,#175336,#175337,#175338,#175339,
#175340,#175341,#175342,#175343,#175344,#175345,#175346,#175347),
 .UNSPECIFIED.,.F.,.F.,(4,3,3,3,3,3,3,3,3,3,3,3,3,3,3,3,3,3,3,3,3,3,3,3,
3,3,3,3,3,3,3,3,3,3,3,3,3,3,3,3,3,3,3,3,3,3,3,3,3,3,3,3,3,3,3,3,3,3,3,3,
3,3,3,3,3,3,3,3,3,3,3,3,3,3,3,3,3,3,3,3,3,3,4),(-890.021669986904,-889.920265842706,
-889.816786494554,-889.765049540917,-889.685092240785,-889.605229443542,
-889.52544362107,-889.445717305874,-889.366033077579,-889.286362091358,
-889.206694637831,-889.127014987014,-889.047307404619,-888.967512175543,
-888.887667833835,-888.807709406787,-888.765313530197,-888.685356230066,
-888.605493432823,-888.525707610351,-888.445981295155,-888.366297066861,
-888.28662608064,-888.206958627114,-888.127278976297,-888.047571393903,
-887.967776164827,-887.887931823119,-887.807973396071,-887.765577519476,
-887.685620219345,-887.605757422102,-887.52597159963,-887.446245284435,
-887.366561056141,-887.28689006992,-887.207222616394,-887.127542965578,
-887.047835383184,-886.968040154108,-886.888195812401,-886.808237385353,
-886.765841508756,-886.685884208625,-886.606021411382,-886.526235588911,
-886.446509273715,-886.366825045421,-886.287154059201,-886.207486605675,
-886.127806954858,-886.048099372464,-885.968304143389,-885.888459801681,
-885.808501374634,-885.766105498036,-885.686148197905,-885.606285400662,
-885.52649957819,-885.446773262995,-885.367089034701,-885.28741804848,-885.207750594954,
-885.128070944137,-885.048363361743,-884.968568132667,-884.888723790959,
-884.808765363912,-884.766369487316,-884.686412187185,-884.606549389942,
-884.52676356747,-884.447037252275,-884.367353023981,-884.28768203776,-884.208014584234,
-884.128334933417,-884.048627351023,-883.968832121947,-883.888987780239,
-883.809029353192,-883.766633476596,-883.738484753982),.UNSPECIFIED.);
#1527=B_SPLINE_CURVE_WITH_KNOTS('',3,(#175349,#175350,#175351,#175352,#175353,
#175354,#175355,#175356,#175357,#175358,#175359,#175360,#175361,#175362,
#175363,#175364,#175365,#175366,#175367,#175368,#175369,#175370,#175371,
#175372,#175373,#175374,#175375,#175376,#175377,#175378,#175379,#175380,
#175381,#175382,#175383,#175384,#175385,#175386,#175387,#175388,#175389,
#175390,#175391,#175392,#175393,#175394,#175395,#175396,#175397,#175398,
#175399,#175400,#175401,#175402,#175403,#175404,#175405,#175406,#175407,
#175408,#175409,#175410,#175411,#175412,#175413,#175414,#175415,#175416,
#175417,#175418,#175419,#175420,#175421,#175422,#175423,#175424,#175425,
#175426,#175427,#175428,#175429,#175430,#175431,#175432,#175433,#175434,
#175435,#175436,#175437,#175438,#175439,#175440,#175441,#175442,#175443,
#175444,#175445,#175446,#175447,#175448,#175449,#175450,#175451,#175452,
#175453,#175454,#175455,#175456,#175457,#175458,#175459,#175460,#175461,
#175462,#175463,#175464,#175465,#175466,#175467,#175468,#175469,#175470,
#175471,#175472,#175473,#175474,#175475,#175476,#175477,#175478,#175479,
#175480,#175481,#175482,#175483,#175484,#175485,#175486,#175487,#175488,
#175489,#175490,#175491,#175492,#175493,#175494,#175495,#175496,#175497,
#175498,#175499,#175500,#175501,#175502,#175503,#175504,#175505,#175506,
#175507,#175508,#175509,#175510,#175511,#175512,#175513,#175514,#175515,
#175516,#175517,#175518,#175519,#175520,#175521,#175522,#175523,#175524,
#175525,#175526,#175527,#175528,#175529,#175530,#175531,#175532,#175533,
#175534,#175535,#175536,#175537,#175538,#175539,#175540,#175541,#175542,
#175543,#175544,#175545,#175546,#175547,#175548,#175549,#175550,#175551,
#175552,#175553,#175554,#175555,#175556,#175557,#175558,#175559,#175560,
#175561,#175562,#175563,#175564,#175565,#175566,#175567,#175568,#175569,
#175570,#175571,#175572,#175573,#175574,#175575,#175576,#175577,#175578,
#175579,#175580,#175581,#175582,#175583,#175584,#175585,#175586,#175587,
#175588,#175589,#175590,#175591,#175592,#175593,#175594,#175595),
 .UNSPECIFIED.,.F.,.F.,(4,3,3,3,3,3,3,3,3,3,3,3,3,3,3,3,3,3,3,3,3,3,3,3,
3,3,3,3,3,3,3,3,3,3,3,3,3,3,3,3,3,3,3,3,3,3,3,3,3,3,3,3,3,3,3,3,3,3,3,3,
3,3,3,3,3,3,3,3,3,3,3,3,3,3,3,3,3,3,3,3,3,3,4),(-883.73848475388,-883.658904576264,
-883.579417860576,-883.500006735715,-883.420653393899,-883.338933902896,
-883.259631332509,-883.180329314193,-883.1010118102,-883.021662775846,-882.942225636669,
-882.862735566645,-882.783138781002,-882.766897465876,-882.686940165745,
-882.607077368502,-882.52729154603,-882.447565230835,-882.367881002541,
-882.28821001632,-882.208542562794,-882.128862911978,-882.049155329583,
-881.969360100508,-881.8895157588,-881.809557331752,-881.767161455156,-881.687204155025,
-881.607341357782,-881.527555535311,-881.447829220115,-881.368144991821,
-881.2884740056,-881.208806552074,-881.129126901258,-881.049419318863,-880.969624089788,
-880.889779748081,-880.809821321033,-880.767425444436,-880.687468144304,
-880.607605347062,-880.52781952459,-880.448093209394,-880.368408981099,
-880.288737994878,-880.209070541352,-880.129390890535,-880.04968330814,
-879.969888079065,-879.890043737357,-879.810085310309,-879.767689433715,
-879.687732133584,-879.607869336341,-879.528083513869,-879.448357198674,
-879.36867297038,-879.289001984159,-879.209334530633,-879.129654879816,
-879.049947297422,-878.970152068346,-878.890307726639,-878.810349299592,
-878.767953422995,-878.687996122864,-878.608133325622,-878.52834750315,
-878.448621187955,-878.368936959661,-878.28926597344,-878.209598519914,
-878.129918869098,-878.050211286704,-877.970416057628,-877.890571715921,
-877.810613288874,-877.768217412275,-877.672191336738,-877.576693682037,
-877.482167121906,-877.455299654684),.UNSPECIFIED.);
#1528=B_SPLINE_CURVE_WITH_KNOTS('',3,(#175597,#175598,#175599,#175600,#175601,
#175602,#175603,#175604,#175605,#175606),.UNSPECIFIED.,.F.,.F.,(4,1,1,1,
1,1,1,4),(-877.455299446802,-876.768481401555,-875.768745390835,-874.769009380115,
-873.769273369395,-872.769537358675,-871.769801347954,-871.172114139623),
 .UNSPECIFIED.);
#1529=B_SPLINE_CURVE_WITH_KNOTS('',3,(#175608,#175609,#175610,#175611,#175612,
#175613,#175614,#175615,#175616,#175617,#175618,#175619,#175620,#175621,
#175622,#175623,#175624,#175625,#175626,#175627,#175628,#175629,#175630,
#175631,#175632,#175633,#175634,#175635,#175636,#175637,#175638,#175639,
#175640,#175641,#175642,#175643,#175644,#175645,#175646,#175647,#175648,
#175649,#175650,#175651,#175652,#175653,#175654,#175655,#175656,#175657,
#175658,#175659,#175660,#175661,#175662,#175663,#175664,#175665,#175666,
#175667,#175668,#175669,#175670,#175671,#175672,#175673,#175674,#175675,
#175676,#175677,#175678,#175679,#175680,#175681,#175682,#175683,#175684,
#175685,#175686,#175687,#175688,#175689,#175690,#175691,#175692,#175693,
#175694,#175695,#175696,#175697,#175698,#175699,#175700,#175701,#175702,
#175703,#175704,#175705,#175706,#175707,#175708,#175709,#175710,#175711,
#175712,#175713,#175714,#175715,#175716,#175717,#175718,#175719,#175720,
#175721,#175722,#175723,#175724,#175725,#175726,#175727,#175728,#175729,
#175730,#175731,#175732,#175733,#175734,#175735,#175736,#175737,#175738,
#175739,#175740,#175741,#175742,#175743,#175744,#175745,#175746,#175747,
#175748,#175749,#175750,#175751,#175752,#175753,#175754,#175755,#175756,
#175757,#175758,#175759,#175760,#175761,#175762,#175763,#175764,#175765,
#175766,#175767,#175768,#175769,#175770,#175771,#175772,#175773,#175774,
#175775,#175776,#175777,#175778,#175779,#175780,#175781,#175782,#175783,
#175784,#175785,#175786,#175787,#175788,#175789,#175790,#175791,#175792,
#175793,#175794,#175795,#175796,#175797,#175798,#175799,#175800,#175801,
#175802,#175803,#175804,#175805,#175806,#175807,#175808,#175809,#175810,
#175811,#175812,#175813,#175814,#175815,#175816,#175817,#175818,#175819,
#175820,#175821,#175822,#175823,#175824,#175825,#175826,#175827,#175828,
#175829,#175830,#175831,#175832,#175833,#175834,#175835,#175836,#175837,
#175838,#175839,#175840,#175841,#175842,#175843,#175844,#175845,#175846,
#175847,#175848,#175849,#175850,#175851,#175852,#175853,#175854),
 .UNSPECIFIED.,.F.,.F.,(4,3,3,3,3,3,3,3,3,3,3,3,3,3,3,3,3,3,3,3,3,3,3,3,
3,3,3,3,3,3,3,3,3,3,3,3,3,3,3,3,3,3,3,3,3,3,3,3,3,3,3,3,3,3,3,3,3,3,3,3,
3,3,3,3,3,3,3,3,3,3,3,3,3,3,3,3,3,3,3,3,3,3,4),(-871.172113916944,-871.084302572035,
-870.996038084311,-870.907543334164,-870.818727704578,-870.770065337234,
-870.690108037103,-870.610245239861,-870.530459417389,-870.450733102194,
-870.371048873901,-870.29137788768,-870.211710434154,-870.132030783338,
-870.052323200944,-869.972527971869,-869.892683630162,-869.812725203114,
-869.770329326514,-869.690372026383,-869.61050922914,-869.530723406668,
-869.450997091473,-869.371312863179,-869.291641876958,-869.211974423432,
-869.132294772616,-869.052587190221,-868.972791961146,-868.892947619438,
-868.812989192391,-868.770593315794,-868.690636015663,-868.61077321842,
-868.530987395948,-868.451261080753,-868.371576852459,-868.291905866238,
-868.212238412712,-868.132558761895,-868.052851179501,-867.973055950425,
-867.893211608718,-867.81325318167,-867.770857305074,-867.690900004943,
-867.6110372077,-867.531251385228,-867.451525070033,-867.371840841739,-867.292169855518,
-867.212502401992,-867.132822751176,-867.053115168781,-866.973319939706,
-866.893475597998,-866.813517170951,-866.771121294354,-866.691163994223,
-866.61130119698,-866.531515374508,-866.451789059313,-866.372104831019,
-866.292433844798,-866.212766391272,-866.133086740456,-866.053379158062,
-865.973583928986,-865.893739587279,-865.813781160231,-865.771385283634,
-865.692514875663,-865.613738208896,-865.535036863318,-865.454273359459,
-865.375663826956,-865.29706959623,-865.218474156873,-865.136087825765,
-865.057404123793,-864.978677878304,-864.899860992298,-864.888928832443),
 .UNSPECIFIED.);
#1530=B_SPLINE_CURVE_WITH_KNOTS('',3,(#175856,#175857,#175858,#175859,#175860,
#175861,#175862,#175863,#175864,#175865,#175866),.UNSPECIFIED.,.F.,.F.,
(4,1,1,1,1,1,1,1,4),(-864.888928832443,-864.771649272913,-863.771913262193,
-862.772177251473,-861.772441240753,-860.772705230033,-859.772969219313,
-858.773233208593,-858.605743525264),.UNSPECIFIED.);
#1531=B_SPLINE_CURVE_WITH_KNOTS('',3,(#175868,#175869,#175870,#175871,#175872,
#175873,#175874,#175875,#175876,#175877),.UNSPECIFIED.,.F.,.F.,(4,1,1,1,
1,1,1,4),(-858.605743525264,-857.773497197872,-856.773761187152,-855.774025176432,
-854.774289165712,-853.774553154992,-852.774817144272,-852.322558218084),
 .UNSPECIFIED.);
#1532=B_SPLINE_CURVE_WITH_KNOTS('',3,(#175879,#175880,#175881,#175882,#175883,
#175884,#175885,#175886,#175887,#175888),.UNSPECIFIED.,.F.,.F.,(4,1,1,1,
1,1,1,4),(-852.322558218084,-851.775081133552,-850.775345122832,-849.775609112111,
-848.775873101391,-847.776137090671,-846.776401079951,-846.039372910904),
 .UNSPECIFIED.);
#1533=B_SPLINE_CURVE_WITH_KNOTS('',3,(#175890,#175891,#175892,#175893,#175894,
#175895,#175896,#175897,#175898,#175899,#175900),.UNSPECIFIED.,.F.,.F.,
(4,1,1,1,1,1,1,1,4),(-846.039372910904,-845.776665069231,-844.776929058511,
-843.777193047791,-842.777457037071,-841.77772102635,-840.77798501563,-839.77824900491,
-839.756187603725),.UNSPECIFIED.);
#1534=B_SPLINE_CURVE_WITH_KNOTS('',3,(#175902,#175903,#175904,#175905,#175906,
#175907,#175908,#175909,#175910,#175911,#175912,#175913,#175914,#175915,
#175916,#175917,#175918,#175919,#175920,#175921,#175922,#175923,#175924,
#175925,#175926,#175927,#175928,#175929,#175930,#175931,#175932,#175933,
#175934,#175935,#175936,#175937,#175938,#175939,#175940,#175941,#175942,
#175943,#175944,#175945,#175946,#175947,#175948,#175949,#175950,#175951,
#175952,#175953,#175954,#175955,#175956,#175957,#175958,#175959,#175960,
#175961,#175962,#175963,#175964,#175965,#175966,#175967,#175968,#175969,
#175970,#175971,#175972,#175973,#175974,#175975,#175976,#175977,#175978,
#175979,#175980,#175981,#175982,#175983,#175984,#175985,#175986,#175987,
#175988,#175989,#175990,#175991,#175992,#175993,#175994,#175995,#175996,
#175997,#175998,#175999,#176000,#176001,#176002,#176003,#176004,#176005,
#176006,#176007,#176008,#176009,#176010,#176011,#176012,#176013,#176014,
#176015,#176016,#176017,#176018,#176019,#176020,#176021,#176022,#176023,
#176024,#176025,#176026,#176027,#176028,#176029,#176030,#176031,#176032,
#176033,#176034,#176035,#176036,#176037,#176038,#176039,#176040,#176041,
#176042,#176043,#176044,#176045,#176046,#176047,#176048,#176049,#176050,
#176051,#176052,#176053,#176054,#176055,#176056,#176057,#176058,#176059,
#176060,#176061,#176062,#176063,#176064,#176065,#176066,#176067,#176068,
#176069,#176070,#176071,#176072,#176073,#176074,#176075,#176076,#176077,
#176078,#176079,#176080,#176081,#176082,#176083,#176084,#176085,#176086,
#176087,#176088,#176089,#176090,#176091,#176092,#176093,#176094,#176095,
#176096,#176097,#176098,#176099,#176100,#176101,#176102,#176103,#176104,
#176105,#176106,#176107,#176108,#176109,#176110,#176111,#176112,#176113,
#176114,#176115,#176116,#176117,#176118,#176119,#176120,#176121,#176122,
#176123,#176124,#176125,#176126,#176127,#176128,#176129,#176130,#176131,
#176132,#176133,#176134,#176135,#176136,#176137,#176138,#176139,#176140,
#176141,#176142,#176143,#176144,#176145,#176146,#176147,#176148),
 .UNSPECIFIED.,.F.,.F.,(4,3,3,3,3,3,3,3,3,3,3,3,3,3,3,3,3,3,3,3,3,3,3,3,
3,3,3,3,3,3,3,3,3,3,3,3,3,3,3,3,3,3,3,3,3,3,3,3,3,3,3,3,3,3,3,3,3,3,3,3,
3,3,3,3,3,3,3,3,3,3,3,3,3,3,3,3,3,3,3,3,3,3,4),(-839.756187603725,-839.676531395756,
-839.596969010512,-839.517482640912,-839.438054542635,-839.355611849079,
-839.276235882847,-839.196860955274,-839.117471086351,-839.038050289642,
-838.95854142878,-838.878980288109,-838.79931114942,-838.77851299419,-838.698555694059,
-838.618692896816,-838.538907074344,-838.459180759149,-838.379496530855,
-838.299825544634,-838.220158091108,-838.140478440292,-838.060770857898,
-837.980975628822,-837.901131287115,-837.821172860067,-837.77877698347,
-837.698819683339,-837.618956886096,-837.539171063624,-837.459444748429,
-837.379760520135,-837.300089533914,-837.220422080388,-837.140742429571,
-837.061034847177,-836.981239618101,-836.901395276393,-836.821436849346,
-836.77904097275,-836.699083672619,-836.619220875376,-836.539435052904,
-836.459708737709,-836.380024509415,-836.300353523194,-836.220686069668,
-836.141006418851,-836.061298836457,-835.981503607381,-835.901659265674,
-835.821700838626,-835.77930496203,-835.699347661899,-835.619484864656,
-835.539699042185,-835.459972726989,-835.380288498695,-835.300617512474,
-835.220950058948,-835.141270408132,-835.061562825738,-834.981767596663,
-834.901923254955,-834.821964827908,-834.77956895131,-834.699611651178,
-834.619748853936,-834.539963031464,-834.460236716268,-834.380552487973,
-834.300881501752,-834.221214048226,-834.141534397409,-834.061826815015,
-833.982031585939,-833.902187244231,-833.822228817184,-833.779832940589,
-833.683134355094,-833.587007138293,-833.491915336761,-833.473002493996),
 .UNSPECIFIED.);
#1535=B_SPLINE_CURVE_WITH_KNOTS('',3,(#176150,#176151,#176152,#176153,#176154,
#176155,#176156,#176157,#176158,#176159),.UNSPECIFIED.,.F.,.F.,(4,1,1,1,
1,1,1,4),(-833.473002296545,-832.780096929869,-831.780360919149,-830.780624908429,
-829.780888897709,-828.781152886989,-827.781416876269,-827.189816989366),
 .UNSPECIFIED.);
#1536=B_SPLINE_CURVE_WITH_KNOTS('',3,(#176161,#176162,#176163,#176164,#176165,
#176166,#176167,#176168,#176169,#176170,#176171,#176172,#176173,#176174,
#176175,#176176,#176177,#176178,#176179,#176180,#176181,#176182,#176183,
#176184,#176185,#176186,#176187,#176188,#176189,#176190,#176191,#176192,
#176193,#176194,#176195,#176196,#176197,#176198,#176199,#176200,#176201,
#176202,#176203,#176204,#176205,#176206,#176207,#176208,#176209,#176210,
#176211,#176212,#176213,#176214,#176215,#176216,#176217,#176218,#176219,
#176220,#176221,#176222,#176223,#176224,#176225,#176226,#176227,#176228,
#176229,#176230,#176231,#176232,#176233,#176234,#176235,#176236,#176237,
#176238,#176239,#176240,#176241,#176242,#176243,#176244,#176245,#176246,
#176247,#176248,#176249,#176250,#176251,#176252,#176253,#176254,#176255,
#176256,#176257,#176258,#176259,#176260,#176261,#176262,#176263,#176264,
#176265,#176266,#176267,#176268,#176269,#176270,#176271,#176272,#176273,
#176274,#176275,#176276,#176277,#176278,#176279,#176280,#176281,#176282,
#176283,#176284,#176285,#176286,#176287,#176288,#176289,#176290,#176291,
#176292,#176293,#176294,#176295,#176296,#176297,#176298,#176299,#176300,
#176301,#176302,#176303,#176304,#176305,#176306,#176307,#176308,#176309,
#176310,#176311,#176312,#176313,#176314,#176315,#176316,#176317,#176318,
#176319,#176320,#176321,#176322,#176323,#176324,#176325,#176326,#176327,
#176328,#176329,#176330,#176331,#176332,#176333,#176334,#176335,#176336,
#176337,#176338,#176339,#176340,#176341,#176342,#176343,#176344,#176345,
#176346,#176347,#176348,#176349,#176350,#176351,#176352,#176353,#176354,
#176355,#176356,#176357,#176358,#176359,#176360,#176361,#176362,#176363,
#176364,#176365,#176366,#176367,#176368,#176369,#176370,#176371,#176372,
#176373,#176374,#176375,#176376,#176377,#176378,#176379,#176380,#176381,
#176382,#176383,#176384,#176385,#176386,#176387,#176388,#176389,#176390,
#176391,#176392,#176393,#176394,#176395,#176396,#176397,#176398,#176399,
#176400,#176401,#176402,#176403,#176404),.UNSPECIFIED.,.F.,.F.,(4,3,3,3,
3,3,3,3,3,3,3,3,3,3,3,3,3,3,3,3,3,3,3,3,3,3,3,3,3,3,3,3,3,3,3,3,3,3,3,3,
3,3,3,3,3,3,3,3,3,3,3,3,3,3,3,3,3,3,3,3,3,3,3,3,3,3,3,3,3,3,3,3,3,3,3,3,
3,3,3,3,3,4),(-827.189816774901,-827.102343305138,-827.014439944225,-826.926319122299,
-826.837884784447,-826.781680865548,-826.701723565417,-826.621860768175,
-826.542074945703,-826.462348630508,-826.382664402214,-826.302993415994,
-826.223325962468,-826.143646311652,-826.063938729258,-825.984143500182,
-825.904299158475,-825.824340731428,-825.781944854828,-825.701987554697,
-825.622124757454,-825.542338934982,-825.462612619787,-825.382928391493,
-825.303257405272,-825.223589951747,-825.14391030093,-825.064202718536,
-824.98440748946,-824.904563147753,-824.824604720705,-824.782208844108,
-824.702251543977,-824.622388746734,-824.542602924262,-824.462876609067,
-824.383192380772,-824.303521394551,-824.223853941025,-824.144174290209,
-824.064466707814,-823.984671478739,-823.904827137031,-823.824868709983,
-823.782472833388,-823.702515533257,-823.622652736014,-823.542866913542,
-823.463140598347,-823.383456370053,-823.303785383832,-823.224117930306,
-823.14443827949,-823.064730697095,-822.98493546802,-822.905091126312,-822.825132699265,
-822.782736822668,-822.702779522537,-822.622916725294,-822.543130902822,
-822.463404587627,-822.383720359333,-822.304049373112,-822.224381919586,
-822.14470226877,-822.064994686376,-821.9851994573,-821.905355115593,-821.825396688545,
-821.783000811948,-821.704154560128,-821.625402052782,-821.54672485351,
-821.466713207095,-821.388127723732,-821.30955767386,-821.230986533456,
-821.149897820638,-821.071240210406,-820.988935946296,-820.906631682186),
 .UNSPECIFIED.);
#1537=B_SPLINE_CURVE_WITH_KNOTS('',3,(#176406,#176407,#176408,#176409,#176410,
#176411,#176412,#176413,#176414,#176415,#176416),.UNSPECIFIED.,.F.,.F.,
(4,1,1,1,1,1,1,1,4),(-820.906631682186,-820.783264801228,-819.783528790507,
-818.783792779787,-817.784056769067,-816.784320758347,-815.784584747627,
-814.784848736907,-814.623446375007),.UNSPECIFIED.);
#1538=B_SPLINE_CURVE_WITH_KNOTS('',3,(#176418,#176419,#176420,#176421,#176422,
#176423,#176424,#176425,#176426,#176427),.UNSPECIFIED.,.F.,.F.,(4,1,1,1,
1,1,1,4),(-814.623446375007,-813.785112726187,-812.785376715467,-811.785640704747,
-810.785904694026,-809.786168683306,-808.786432672586,-808.340261067827),
 .UNSPECIFIED.);
#1539=B_SPLINE_CURVE_WITH_KNOTS('',3,(#176429,#176430,#176431,#176432,#176433,
#176434,#176435,#176436,#176437,#176438),.UNSPECIFIED.,.F.,.F.,(4,1,1,1,
1,1,1,4),(-808.340261067827,-807.786696661866,-806.786960651146,-805.787224640426,
-804.787488629706,-803.787752618985,-802.788016608265,-802.057075760647),
 .UNSPECIFIED.);
#1540=B_SPLINE_CURVE_WITH_KNOTS('',3,(#176440,#176441,#176442,#176443,#176444,
#176445,#176446,#176447,#176448,#176449,#176450),.UNSPECIFIED.,.F.,.F.,
(4,1,1,1,1,1,1,1,4),(-802.057075760647,-801.788280597545,-800.788544586825,
-799.788808576105,-798.789072565385,-797.789336554665,-796.789600543945,
-795.789864533224,-795.773890453468),.UNSPECIFIED.);
#1541=B_SPLINE_CURVE_WITH_KNOTS('',3,(#176452,#176453,#176454,#176455,#176456,
#176457,#176458,#176459,#176460,#176461,#176462,#176463,#176464,#176465,
#176466,#176467,#176468,#176469,#176470,#176471,#176472,#176473,#176474,
#176475,#176476,#176477,#176478,#176479,#176480,#176481,#176482,#176483,
#176484,#176485,#176486,#176487,#176488,#176489,#176490,#176491,#176492,
#176493,#176494,#176495,#176496,#176497,#176498,#176499,#176500,#176501,
#176502,#176503,#176504,#176505,#176506,#176507,#176508,#176509,#176510,
#176511,#176512,#176513,#176514,#176515,#176516,#176517,#176518,#176519,
#176520,#176521,#176522,#176523,#176524,#176525,#176526,#176527,#176528,
#176529,#176530,#176531,#176532,#176533,#176534,#176535,#176536,#176537,
#176538,#176539,#176540,#176541,#176542,#176543,#176544,#176545,#176546,
#176547,#176548,#176549,#176550,#176551,#176552,#176553,#176554,#176555,
#176556,#176557,#176558,#176559,#176560,#176561,#176562,#176563,#176564,
#176565,#176566,#176567,#176568,#176569,#176570,#176571,#176572,#176573,
#176574,#176575,#176576,#176577,#176578,#176579,#176580,#176581,#176582,
#176583,#176584,#176585,#176586,#176587,#176588,#176589,#176590,#176591,
#176592,#176593,#176594,#176595,#176596,#176597,#176598,#176599,#176600,
#176601,#176602,#176603,#176604,#176605,#176606,#176607,#176608,#176609,
#176610,#176611,#176612,#176613,#176614,#176615,#176616,#176617,#176618,
#176619,#176620,#176621,#176622,#176623,#176624,#176625,#176626,#176627,
#176628,#176629,#176630,#176631,#176632,#176633,#176634,#176635,#176636,
#176637,#176638,#176639,#176640,#176641,#176642,#176643,#176644,#176645,
#176646,#176647,#176648,#176649,#176650,#176651,#176652,#176653,#176654,
#176655,#176656,#176657,#176658,#176659,#176660,#176661,#176662,#176663,
#176664,#176665,#176666,#176667,#176668,#176669,#176670,#176671,#176672,
#176673,#176674,#176675,#176676,#176677,#176678,#176679,#176680,#176681,
#176682,#176683,#176684,#176685,#176686,#176687,#176688,#176689,#176690,
#176691,#176692,#176693,#176694,#176695,#176696,#176697,#176698),
 .UNSPECIFIED.,.F.,.F.,(4,3,3,3,3,3,3,3,3,3,3,3,3,3,3,3,3,3,3,3,3,3,3,3,
3,3,3,3,3,3,3,3,3,3,3,3,3,3,3,3,3,3,3,3,3,3,3,3,3,3,3,3,3,3,3,3,3,3,3,3,
3,3,3,3,3,3,3,3,3,3,3,3,3,3,3,3,3,3,3,3,3,3,4),(-795.773890453468,-795.694155176644,
-795.614514012216,-795.534949222386,-795.455443131542,-795.372278805412,
-795.292826095086,-795.21337487234,-795.133909219456,-795.054413212759,
-794.974829166046,-794.895193473398,-794.815448498595,-794.790128522504,
-794.710171222373,-794.63030842513,-794.550522602658,-794.470796287463,
-794.391112059169,-794.311441072948,-794.231773619423,-794.152093968606,
-794.072386386212,-793.992591157136,-793.912746815429,-793.832788388382,
-793.790392511784,-793.710435211653,-793.63057241441,-793.550786591939,
-793.471060276743,-793.391376048449,-793.311705062228,-793.232037608702,
-793.152357957886,-793.072650375491,-792.992855146416,-792.913010804708,
-792.833052377661,-792.790656501064,-792.710699200933,-792.63083640369,
-792.551050581218,-792.471324266023,-792.391640037729,-792.311969051508,
-792.232301597982,-792.152621947165,-792.072914364771,-791.993119135695,
-791.913274793988,-791.83331636694,-791.790920490344,-791.710963190213,
-791.63110039297,-791.551314570498,-791.471588255303,-791.391904027008,
-791.312233040788,-791.232565587262,-791.152885936445,-791.07317835405,
-790.993383124975,-790.913538783267,-790.83358035622,-790.791184479624,
-790.711227179493,-790.63136438225,-790.551578559778,-790.471852244583,
-790.392168016289,-790.312497030068,-790.232829576543,-790.153149925726,
-790.073442343332,-789.993647114257,-789.913802772549,-789.833844345502,
-789.791448468904,-789.694046533938,-789.592375932863,-789.496729054174,
-789.490705331789),.UNSPECIFIED.);
#1542=B_SPLINE_CURVE_WITH_KNOTS('',3,(#176700,#176701,#176702,#176703,#176704,
#176705,#176706,#176707,#176708,#176709),.UNSPECIFIED.,.F.,.F.,(4,1,1,1,
1,1,1,4),(-789.490705146288,-788.791712458183,-787.791976447463,-786.792240436743,
-785.792504426023,-784.792768415303,-783.793032404583,-783.207519839109),
 .UNSPECIFIED.);
#1543=B_SPLINE_CURVE_WITH_KNOTS('',3,(#176711,#176712,#176713,#176714,#176715,
#176716,#176717,#176718,#176719,#176720,#176721,#176722,#176723,#176724,
#176725,#176726,#176727,#176728,#176729,#176730,#176731,#176732,#176733,
#176734,#176735,#176736,#176737,#176738,#176739,#176740,#176741,#176742,
#176743,#176744,#176745,#176746,#176747,#176748,#176749,#176750,#176751,
#176752,#176753,#176754,#176755,#176756,#176757,#176758,#176759,#176760,
#176761,#176762,#176763,#176764,#176765,#176766,#176767,#176768,#176769,
#176770,#176771,#176772,#176773,#176774,#176775,#176776,#176777,#176778,
#176779,#176780,#176781,#176782,#176783,#176784,#176785,#176786,#176787,
#176788,#176789,#176790,#176791,#176792,#176793,#176794,#176795,#176796,
#176797,#176798,#176799,#176800,#176801,#176802,#176803,#176804,#176805,
#176806,#176807,#176808,#176809,#176810,#176811,#176812,#176813,#176814,
#176815,#176816,#176817,#176818,#176819,#176820,#176821,#176822,#176823,
#176824,#176825,#176826,#176827,#176828,#176829,#176830,#176831,#176832,
#176833,#176834,#176835,#176836,#176837,#176838,#176839,#176840,#176841,
#176842,#176843,#176844,#176845,#176846,#176847,#176848,#176849,#176850,
#176851,#176852,#176853,#176854,#176855,#176856,#176857,#176858,#176859,
#176860,#176861,#176862,#176863,#176864,#176865,#176866,#176867,#176868,
#176869,#176870,#176871,#176872,#176873,#176874,#176875,#176876,#176877,
#176878,#176879,#176880,#176881,#176882,#176883,#176884,#176885,#176886,
#176887,#176888,#176889,#176890,#176891,#176892,#176893,#176894,#176895,
#176896,#176897,#176898,#176899,#176900,#176901,#176902,#176903,#176904,
#176905,#176906,#176907,#176908,#176909,#176910,#176911,#176912,#176913,
#176914,#176915,#176916,#176917,#176918,#176919,#176920,#176921,#176922,
#176923,#176924,#176925,#176926,#176927,#176928,#176929,#176930,#176931,
#176932,#176933,#176934,#176935,#176936,#176937,#176938,#176939,#176940,
#176941,#176942,#176943,#176944,#176945,#176946,#176947,#176948,#176949,
#176950,#176951,#176952,#176953,#176954),.UNSPECIFIED.,.F.,.F.,(4,3,3,3,
3,3,3,3,3,3,3,3,3,3,3,3,3,3,3,3,3,3,3,3,3,3,3,3,3,3,3,3,3,3,3,3,3,3,3,3,
3,3,3,3,3,3,3,3,3,3,3,3,3,3,3,3,3,3,3,3,3,3,3,3,3,3,3,3,3,3,3,3,3,3,3,3,
3,3,3,3,3,4),(-783.207519633885,-783.120373602226,-783.032819475524,-782.94505992763,
-782.856993893478,-782.793296393863,-782.713339093731,-782.633476296488,
-782.553690474016,-782.47396415882,-782.394279930526,-782.314608944304,
-782.234941490778,-782.155261839961,-782.075554257566,-781.99575902849,
-781.915914686782,-781.835956259734,-781.793560383142,-781.713603083011,
-781.633740285768,-781.553954463296,-781.474228148101,-781.394543919807,
-781.314872933586,-781.23520548006,-781.155525829244,-781.075818246849,
-780.996023017774,-780.916178676066,-780.836220249019,-780.793824372422,
-780.713867072291,-780.634004275048,-780.554218452577,-780.474492137382,
-780.394807909087,-780.315136922867,-780.235469469341,-780.155789818525,
-780.07608223613,-779.996287007055,-779.916442665347,-779.8364842383,-779.794088361702,
-779.714131061571,-779.634268264328,-779.554482441856,-779.474756126661,
-779.395071898367,-779.315400912146,-779.23573345862,-779.156053807803,
-779.076346225409,-778.996550996333,-778.916706654626,-778.836748227578,
-778.794352350982,-778.714395050851,-778.634532253608,-778.554746431136,
-778.475020115941,-778.395335887647,-778.315664901426,-778.2359974479,-778.156317797083,
-778.076610214689,-777.996814985613,-777.916970643906,-777.837012216858,
-777.794616340262,-777.715791165492,-777.63705974625,-777.558403631865,
-777.479144994373,-777.400580530135,-777.322031647876,-777.243481811772,
-777.163694991812,-777.085060525394,-777.004697528662,-776.924334531929),
 .UNSPECIFIED.);
#1544=B_SPLINE_CURVE_WITH_KNOTS('',3,(#176956,#176957,#176958,#176959,#176960,
#176961,#176962,#176963,#176964,#176965,#176966),.UNSPECIFIED.,.F.,.F.,
(4,1,1,1,1,1,1,1,4),(-776.924334531929,-776.794880329542,-775.795144318822,
-774.795408308102,-773.795672297381,-772.795936286661,-771.796200275941,
-770.796464265221,-770.64114922475),.UNSPECIFIED.);
#1545=B_SPLINE_CURVE_WITH_KNOTS('',3,(#176968,#176969,#176970,#176971,#176972,
#176973,#176974,#176975,#176976,#176977),.UNSPECIFIED.,.F.,.F.,(4,1,1,1,
1,1,1,4),(-770.64114922475,-769.796728254501,-768.796992243781,-767.797256233061,
-766.79752022234,-765.79778421162,-764.7980482009,-764.357968758915),
 .UNSPECIFIED.);
#1546=B_SPLINE_CURVE_WITH_KNOTS('',3,(#176979,#176980,#176981,#176982,#176983,
#176984,#176985,#176986,#176987,#176988,#176989,#176990,#176991,#176992,
#176993,#176994,#176995,#176996,#176997,#176998,#176999,#177000,#177001,
#177002,#177003,#177004,#177005,#177006,#177007,#177008,#177009,#177010,
#177011,#177012,#177013,#177014,#177015,#177016,#177017,#177018,#177019,
#177020,#177021,#177022,#177023,#177024,#177025,#177026,#177027,#177028,
#177029,#177030,#177031,#177032,#177033,#177034,#177035,#177036,#177037,
#177038,#177039,#177040,#177041,#177042,#177043,#177044,#177045,#177046,
#177047,#177048,#177049,#177050,#177051,#177052,#177053,#177054,#177055,
#177056,#177057,#177058,#177059,#177060,#177061,#177062,#177063,#177064,
#177065,#177066,#177067,#177068,#177069,#177070,#177071,#177072,#177073,
#177074,#177075,#177076,#177077,#177078,#177079,#177080,#177081,#177082,
#177083,#177084,#177085,#177086,#177087,#177088,#177089,#177090,#177091,
#177092,#177093,#177094,#177095,#177096,#177097,#177098,#177099,#177100,
#177101,#177102,#177103,#177104,#177105,#177106,#177107,#177108,#177109,
#177110,#177111,#177112,#177113,#177114,#177115,#177116,#177117,#177118,
#177119,#177120,#177121,#177122,#177123,#177124,#177125,#177126,#177127,
#177128,#177129,#177130,#177131,#177132,#177133,#177134,#177135,#177136,
#177137,#177138,#177139,#177140,#177141,#177142,#177143,#177144,#177145,
#177146,#177147,#177148,#177149,#177150,#177151,#177152,#177153,#177154,
#177155,#177156,#177157,#177158,#177159,#177160,#177161,#177162,#177163,
#177164,#177165,#177166,#177167,#177168,#177169,#177170,#177171,#177172,
#177173,#177174,#177175,#177176,#177177,#177178,#177179,#177180,#177181,
#177182,#177183,#177184,#177185,#177186,#177187,#177188,#177189,#177190,
#177191,#177192,#177193,#177194,#177195,#177196,#177197,#177198,#177199,
#177200,#177201,#177202,#177203,#177204,#177205,#177206,#177207,#177208,
#177209,#177210,#177211,#177212,#177213,#177214,#177215,#177216,#177217,
#177218,#177219,#177220,#177221,#177222,#177223,#177224,#177225),
 .UNSPECIFIED.,.F.,.F.,(4,3,3,3,3,3,3,3,3,3,3,3,3,3,3,3,3,3,3,3,3,3,3,3,
3,3,3,3,3,3,3,3,3,3,3,3,3,3,3,3,3,3,3,3,3,3,3,3,3,3,3,3,3,3,3,3,3,3,3,3,
3,3,3,3,3,3,3,3,3,3,3,3,3,3,3,3,3,3,3,3,3,3,4),(-764.35796391757,-764.276294881444,
-764.19457900503,-764.112803816722,-764.030895575215,-763.948917289433,
-763.866785413175,-763.79831219018,-763.718354890049,-763.638492092806,
-763.558706270334,-763.478979955139,-763.399295726844,-763.319624740623,
-763.239957287097,-763.160277636281,-763.080570053887,-763.000774824811,
-762.920930483103,-762.840972056056,-762.79857617946,-762.718618879329,
-762.638756082086,-762.558970259614,-762.479243944419,-762.399559716125,
-762.319888729904,-762.240221276378,-762.160541625562,-762.080834043167,
-762.001038814092,-761.921194472384,-761.841236045336,-761.79884016874,
-761.718882868609,-761.639020071366,-761.559234248894,-761.479507933699,
-761.399823705405,-761.320152719184,-761.240485265658,-761.160805614842,
-761.081098032448,-761.001302803372,-760.921458461664,-760.841500034617,
-760.79910415802,-760.719146857889,-760.639284060646,-760.559498238175,
-760.479771922979,-760.400087694685,-760.320416708464,-760.240749254938,
-760.161069604121,-760.081362021726,-760.001566792651,-759.921722450943,
-759.841764023896,-759.7993681473,-759.719410847169,-759.639548049926,-759.559762227454,
-759.480035912258,-759.400351683963,-759.320680697742,-759.241013244216,
-759.161333593399,-759.081626011005,-759.00183078193,-758.921986440222,
-758.842028013175,-758.799632136579,-758.720387508559,-758.639686396288,
-758.560635712157,-758.481638770385,-758.402679241637,-758.320704083825,
-758.24175427393,-758.162795757206,-758.083794480984,-758.07477861039),
 .UNSPECIFIED.);
#1547=B_SPLINE_CURVE_WITH_KNOTS('',3,(#177227,#177228,#177229,#177230,#177231,
#177232,#177233,#177234,#177235,#177236,#177237),.UNSPECIFIED.,.F.,.F.,
(4,1,1,1,1,1,1,1,4),(-758.074774690477,-757.799896125859,-756.800160115139,
-755.800424104419,-754.800688093699,-753.800952082979,-752.801216072259,
-751.801480061539,-751.791593303211),.UNSPECIFIED.);
#1548=B_SPLINE_CURVE_WITH_KNOTS('',3,(#177239,#177240,#177241,#177242,#177243,
#177244,#177245,#177246,#177247,#177248,#177249,#177250,#177251,#177252,
#177253,#177254,#177255,#177256,#177257,#177258,#177259,#177260,#177261,
#177262,#177263,#177264,#177265,#177266,#177267,#177268,#177269,#177270,
#177271,#177272,#177273,#177274,#177275,#177276,#177277,#177278,#177279,
#177280,#177281,#177282,#177283,#177284,#177285,#177286,#177287,#177288,
#177289,#177290,#177291,#177292,#177293,#177294,#177295,#177296,#177297,
#177298,#177299,#177300,#177301,#177302,#177303,#177304,#177305,#177306,
#177307,#177308,#177309,#177310,#177311,#177312,#177313,#177314,#177315,
#177316,#177317,#177318,#177319,#177320,#177321,#177322,#177323,#177324,
#177325,#177326,#177327,#177328,#177329,#177330,#177331,#177332,#177333,
#177334,#177335,#177336,#177337,#177338,#177339,#177340,#177341,#177342,
#177343,#177344,#177345,#177346,#177347,#177348,#177349,#177350,#177351,
#177352,#177353,#177354,#177355,#177356,#177357,#177358,#177359,#177360,
#177361,#177362,#177363,#177364,#177365,#177366,#177367,#177368,#177369,
#177370,#177371,#177372,#177373,#177374,#177375,#177376,#177377,#177378,
#177379,#177380,#177381,#177382,#177383,#177384,#177385,#177386,#177387,
#177388,#177389,#177390,#177391,#177392,#177393,#177394,#177395,#177396,
#177397,#177398,#177399,#177400,#177401,#177402,#177403,#177404,#177405,
#177406,#177407,#177408,#177409,#177410,#177411,#177412,#177413,#177414,
#177415,#177416,#177417,#177418,#177419,#177420,#177421,#177422,#177423,
#177424,#177425,#177426,#177427,#177428,#177429,#177430,#177431,#177432,
#177433,#177434,#177435,#177436,#177437,#177438,#177439,#177440,#177441,
#177442,#177443,#177444,#177445,#177446,#177447,#177448,#177449,#177450,
#177451,#177452,#177453,#177454,#177455,#177456,#177457,#177458,#177459,
#177460,#177461,#177462,#177463,#177464,#177465,#177466,#177467,#177468,
#177469,#177470,#177471,#177472,#177473,#177474,#177475,#177476,#177477,
#177478,#177479,#177480,#177481,#177482),.UNSPECIFIED.,.F.,.F.,(4,3,3,3,
3,3,3,3,3,3,3,3,3,3,3,3,3,3,3,3,3,3,3,3,3,3,3,3,3,3,3,3,3,3,3,3,3,3,3,3,
3,3,3,3,3,3,3,3,3,3,3,3,3,3,3,3,3,3,3,3,3,3,3,3,3,3,3,3,3,3,3,3,3,3,3,3,
3,3,3,3,3,4),(-751.791593303211,-751.71177590738,-751.632052838358,-751.552406433267,
-751.472819090824,-751.393273257364,-751.313739864144,-751.23420923262,
-751.15466551229,-751.075092847645,-750.995432486505,-750.915721873857,
-750.835899552971,-750.801744050818,-750.721786750687,-750.641923953444,
-750.562138130972,-750.482411815777,-750.402727587483,-750.323056601262,
-750.243389147736,-750.16370949692,-750.084001914525,-750.00420668545,-749.924362343742,
-749.844403916695,-749.802008040098,-749.722050739967,-749.642187942724,
-749.562402120252,-749.482675805057,-749.402991576763,-749.323320590542,
-749.243653137016,-749.1639734862,-749.084265903805,-749.00447067473,-748.924626333022,
-748.844667905974,-748.802272029378,-748.722314729247,-748.642451932004,
-748.562666109532,-748.482939794337,-748.403255566043,-748.323584579822,
-748.243917126296,-748.16423747548,-748.084529893086,-748.00473466401,-747.924890322302,
-747.844931895255,-747.802536018658,-747.722578718527,-747.642715921284,
-747.562930098813,-747.483203783617,-747.403519555322,-747.323848569101,
-747.244181115575,-747.164501464759,-747.084793882364,-747.004998653289,
-746.925154311582,-746.845195884534,-746.802800007938,-746.722842707807,
-746.642979910564,-746.563194088092,-746.483467772897,-746.403783544603,
-746.324112558383,-746.244445104857,-746.16476545404,-746.085057871645,
-746.005262642569,-745.925418300862,-745.845459873815,-745.803063997218,
-745.704925577428,-745.606666873208,-745.508408168989),.UNSPECIFIED.);
#1549=B_SPLINE_CURVE_WITH_KNOTS('',3,(#177484,#177485,#177486,#177487,#177488,
#177489,#177490,#177491,#177492,#177493),.UNSPECIFIED.,.F.,.F.,(4,1,1,1,
1,1,1,4),(-745.508407996031,-744.803327986498,-743.803591975778,-742.803855965058,
-741.804119954337,-740.804383943617,-739.804647932897,-739.225222688852),
 .UNSPECIFIED.);
#1550=B_SPLINE_CURVE_WITH_KNOTS('',3,(#177495,#177496,#177497,#177498,#177499,
#177500,#177501,#177502,#177503,#177504),.UNSPECIFIED.,.F.,.F.,(4,1,1,1,
1,1,1,4),(-739.225222688852,-738.804911922177,-737.805175911457,-736.805439900736,
-735.805703890017,-734.805967879296,-733.806231868576,-732.942037381672),
 .UNSPECIFIED.);
#1551=B_SPLINE_CURVE_WITH_KNOTS('',3,(#177506,#177507,#177508,#177509,#177510,
#177511,#177512,#177513,#177514,#177515,#177516),.UNSPECIFIED.,.F.,.F.,
(4,1,1,1,1,1,1,1,4),(-732.942037381672,-732.806495857856,-731.806759847136,
-730.807023836416,-729.807287825696,-728.807551814976,-727.807815804255,
-726.808079793535,-726.658852074493),.UNSPECIFIED.);
#1552=B_SPLINE_CURVE_WITH_KNOTS('',3,(#177518,#177519,#177520,#177521,#177522,
#177523,#177524,#177525,#177526,#177527),.UNSPECIFIED.,.F.,.F.,(4,1,1,1,
1,1,1,4),(-726.658852074493,-725.808343782815,-724.808607772095,-723.808871761375,
-722.809135750655,-721.809399739935,-720.809663729215,-720.37567201352),
 .UNSPECIFIED.);
#1553=B_SPLINE_CURVE_WITH_KNOTS('',3,(#177529,#177530,#177531,#177532,#177533,
#177534,#177535,#177536,#177537,#177538,#177539,#177540,#177541,#177542,
#177543,#177544,#177545,#177546,#177547,#177548,#177549,#177550,#177551,
#177552,#177553,#177554,#177555,#177556,#177557,#177558,#177559,#177560,
#177561,#177562,#177563,#177564,#177565,#177566,#177567,#177568,#177569,
#177570,#177571,#177572,#177573,#177574,#177575,#177576,#177577,#177578,
#177579,#177580,#177581,#177582,#177583,#177584,#177585,#177586,#177587,
#177588,#177589,#177590,#177591,#177592,#177593,#177594,#177595,#177596,
#177597,#177598,#177599,#177600,#177601,#177602,#177603,#177604,#177605,
#177606,#177607,#177608,#177609,#177610,#177611,#177612,#177613,#177614,
#177615,#177616,#177617,#177618,#177619,#177620,#177621,#177622,#177623,
#177624,#177625,#177626,#177627,#177628,#177629,#177630,#177631,#177632,
#177633,#177634,#177635,#177636,#177637,#177638,#177639,#177640,#177641,
#177642,#177643,#177644,#177645,#177646,#177647,#177648,#177649,#177650,
#177651,#177652,#177653,#177654,#177655,#177656,#177657,#177658,#177659,
#177660,#177661,#177662,#177663,#177664,#177665,#177666,#177667,#177668,
#177669,#177670,#177671,#177672,#177673,#177674,#177675,#177676,#177677,
#177678,#177679,#177680,#177681,#177682,#177683,#177684,#177685,#177686,
#177687,#177688,#177689,#177690,#177691,#177692,#177693,#177694,#177695,
#177696,#177697,#177698,#177699,#177700,#177701,#177702,#177703,#177704,
#177705,#177706,#177707,#177708,#177709,#177710,#177711,#177712,#177713,
#177714,#177715,#177716,#177717,#177718,#177719,#177720,#177721,#177722,
#177723,#177724,#177725,#177726,#177727,#177728,#177729,#177730,#177731,
#177732,#177733,#177734,#177735,#177736,#177737,#177738,#177739,#177740,
#177741,#177742,#177743,#177744,#177745,#177746,#177747,#177748,#177749,
#177750,#177751,#177752,#177753,#177754,#177755,#177756,#177757,#177758,
#177759,#177760,#177761,#177762,#177763,#177764,#177765,#177766,#177767,
#177768,#177769,#177770,#177771,#177772),.UNSPECIFIED.,.F.,.F.,(4,3,3,3,
3,3,3,3,3,3,3,3,3,3,3,3,3,3,3,3,3,3,3,3,3,3,3,3,3,3,3,3,3,3,3,3,3,3,3,3,
3,3,3,3,3,3,3,3,3,3,3,3,3,3,3,3,3,3,3,3,3,3,3,3,3,3,3,3,3,3,3,3,3,3,3,3,
3,3,3,3,3,4),(-720.375666767313,-720.294150968666,-720.212592887853,-720.130979718437,
-720.049237393192,-719.967428093136,-719.885465069706,-719.809927718494,
-719.729970418363,-719.65010762112,-719.570321798648,-719.490595483453,
-719.410911255159,-719.331240268938,-719.251572815412,-719.171893164596,
-719.092185582201,-719.012390353126,-718.932546011418,-718.852587584371,
-718.810191707774,-718.730234407643,-718.6503716104,-718.570585787928,-718.490859472733,
-718.411175244439,-718.331504258218,-718.251836804692,-718.172157153875,
-718.092449571481,-718.012654342405,-717.932810000698,-717.85285157365,
-717.810455697054,-717.730498396923,-717.65063559968,-717.570849777208,
-717.491123462013,-717.411439233719,-717.331768247498,-717.252100793972,
-717.172421143155,-717.09271356076,-717.012918331685,-716.933073989977,
-716.85311556293,-716.810719686334,-716.730762386203,-716.65089958896,-716.571113766489,
-716.491387451293,-716.411703222999,-716.332032236778,-716.252364783252,
-716.172685132435,-716.09297755004,-716.013182320965,-715.933337979258,
-715.85337955221,-715.810983675614,-715.731026375483,-715.65116357824,-715.571377755768,
-715.491651440573,-715.411967212279,-715.332296226058,-715.252628772532,
-715.172949121715,-715.09324153932,-715.013446310245,-714.933601968538,
-714.85364354149,-714.811247664894,-714.731945400098,-714.652012407602,
-714.572904570939,-714.493851148949,-714.414835850797,-714.334247253131,
-714.255244345521,-714.173862902827,-714.092481460134),.UNSPECIFIED.);
#1554=B_SPLINE_CURVE_WITH_KNOTS('',3,(#177774,#177775,#177776,#177777,#177778,
#177779,#177780,#177781,#177782,#177783,#177784),.UNSPECIFIED.,.F.,.F.,
(4,1,1,1,1,1,1,1,4),(-714.092477055051,-713.811511654174,-712.811775643453,
-711.812039632733,-710.812303622013,-709.812567611293,-708.812831600573,
-707.813095589853,-707.809296152954),.UNSPECIFIED.);
#1555=B_SPLINE_CURVE_WITH_KNOTS('',3,(#177786,#177787,#177788,#177789,#177790,
#177791,#177792,#177793,#177794,#177795,#177796,#177797,#177798,#177799,
#177800,#177801,#177802,#177803,#177804,#177805,#177806,#177807,#177808,
#177809,#177810,#177811,#177812,#177813,#177814,#177815,#177816,#177817,
#177818,#177819,#177820,#177821,#177822,#177823,#177824,#177825,#177826,
#177827,#177828,#177829,#177830,#177831,#177832,#177833,#177834,#177835,
#177836,#177837,#177838,#177839,#177840,#177841,#177842,#177843,#177844,
#177845,#177846,#177847,#177848,#177849,#177850,#177851,#177852,#177853,
#177854,#177855,#177856,#177857,#177858,#177859,#177860,#177861,#177862,
#177863,#177864,#177865,#177866,#177867,#177868,#177869,#177870,#177871,
#177872,#177873,#177874,#177875,#177876,#177877,#177878,#177879,#177880,
#177881,#177882,#177883,#177884,#177885,#177886,#177887,#177888,#177889,
#177890,#177891,#177892,#177893,#177894,#177895,#177896,#177897,#177898,
#177899,#177900,#177901,#177902,#177903,#177904,#177905,#177906,#177907,
#177908,#177909,#177910,#177911,#177912,#177913,#177914,#177915,#177916,
#177917,#177918,#177919,#177920,#177921,#177922,#177923,#177924,#177925,
#177926,#177927,#177928,#177929,#177930,#177931,#177932,#177933,#177934,
#177935,#177936,#177937,#177938,#177939,#177940,#177941,#177942,#177943,
#177944,#177945,#177946,#177947,#177948,#177949,#177950,#177951,#177952,
#177953,#177954,#177955,#177956,#177957,#177958,#177959,#177960,#177961,
#177962,#177963,#177964,#177965,#177966,#177967,#177968,#177969,#177970,
#177971,#177972,#177973,#177974,#177975,#177976,#177977,#177978,#177979,
#177980,#177981,#177982,#177983,#177984,#177985,#177986,#177987,#177988,
#177989,#177990,#177991,#177992,#177993,#177994,#177995,#177996,#177997,
#177998,#177999,#178000,#178001,#178002,#178003,#178004,#178005,#178006,
#178007,#178008,#178009,#178010,#178011,#178012,#178013,#178014,#178015,
#178016,#178017,#178018,#178019,#178020,#178021,#178022,#178023,#178024,
#178025,#178026,#178027,#178028,#178029),.UNSPECIFIED.,.F.,.F.,(4,3,3,3,
3,3,3,3,3,3,3,3,3,3,3,3,3,3,3,3,3,3,3,3,3,3,3,3,3,3,3,3,3,3,3,3,3,3,3,3,
3,3,3,3,3,3,3,3,3,3,3,3,3,3,3,3,3,3,3,3,3,3,3,3,3,3,3,3,3,3,3,3,3,3,3,3,
3,3,3,3,3,4),(-707.809296152954,-707.729393576193,-707.649585460883,-707.56985422511,
-707.490182347959,-707.410552355825,-707.330935321053,-707.251321537018,
-707.171695225664,-707.092040604376,-707.012298323543,-706.932506498773,
-706.852601501857,-706.813359579133,-706.733402279002,-706.653539481759,
-706.573753659287,-706.494027344092,-706.414343115798,-706.334672129577,
-706.255004676051,-706.175325025235,-706.095617442841,-706.015822213765,
-705.935977872058,-705.85601944501,-705.813623568413,-705.733666268282,
-705.653803471039,-705.574017648568,-705.494291333373,-705.414607105079,
-705.334936118858,-705.255268665332,-705.175589014516,-705.095881432121,
-705.016086203046,-704.936241861339,-704.856283434291,-704.813887557693,
-704.733930257561,-704.654067460319,-704.574281637847,-704.494555322651,
-704.414871094357,-704.335200108136,-704.25553265461,-704.175853003793,
-704.096145421398,-704.016350192322,-703.936505850614,-703.856547423567,
-703.814151546972,-703.734194246841,-703.654331449598,-703.574545627126,
-703.494819311931,-703.415135083637,-703.335464097416,-703.25579664389,
-703.176116993074,-703.09640941068,-703.016614181604,-702.936769839897,
-702.856811412849,-702.814415536252,-702.734458236121,-702.654595438879,
-702.574809616407,-702.495083301212,-702.415399072918,-702.335728086698,
-702.256060633172,-702.176380982356,-702.096673399962,-702.016878170886,
-701.937033829179,-701.857075402131,-701.814679525532,-701.71576893031,
-701.618207500733,-701.526111005195),.UNSPECIFIED.);
#1556=B_SPLINE_CURVE_WITH_KNOTS('',3,(#178031,#178032,#178033,#178034,#178035,
#178036,#178037,#178038,#178039,#178040),.UNSPECIFIED.,.F.,.F.,(4,1,1,1,
1,1,1,4),(-701.526110845774,-700.814943514812,-699.815207504092,-698.815471493372,
-697.815735482651,-696.815999471931,-695.816263461211,-695.242925538595),
 .UNSPECIFIED.);
#1557=B_SPLINE_CURVE_WITH_KNOTS('',3,(#178042,#178043,#178044,#178045,#178046,
#178047,#178048,#178049,#178050,#178051),.UNSPECIFIED.,.F.,.F.,(4,1,1,1,
1,1,1,4),(-695.242925538595,-694.816527450491,-693.816791439771,-692.817055429051,
-691.817319418331,-690.817583407611,-689.81784739689,-688.959740231415),
 .UNSPECIFIED.);
#1558=B_SPLINE_CURVE_WITH_KNOTS('',3,(#178053,#178054,#178055,#178056,#178057,
#178058,#178059,#178060,#178061,#178062,#178063),.UNSPECIFIED.,.F.,.F.,
(4,1,1,1,1,1,1,1,4),(-688.959740231415,-688.81811138617,-687.81837537545,
-686.81863936473,-685.81890335401,-684.81916734329,-683.81943133257,-682.81969532185,
-682.676554924236),.UNSPECIFIED.);
#1559=B_SPLINE_CURVE_WITH_KNOTS('',3,(#178065,#178066,#178067,#178068,#178069,
#178070,#178071,#178072,#178073,#178074),.UNSPECIFIED.,.F.,.F.,(4,1,1,1,
1,1,1,4),(-682.676554924236,-681.819959311129,-680.820223300409,-679.820487289689,
-678.820751278969,-677.821015268249,-676.821279257529,-676.393369617056),
 .UNSPECIFIED.);
#1560=B_SPLINE_CURVE_WITH_KNOTS('',3,(#178076,#178077,#178078,#178079,#178080,
#178081,#178082,#178083,#178084,#178085),.UNSPECIFIED.,.F.,.F.,(4,1,1,1,
1,1,1,4),(-676.393369617056,-675.821543246809,-674.821807236089,-673.822071225368,
-672.822335214648,-671.822599203928,-670.822863193208,-670.110184309877),
 .UNSPECIFIED.);
#1561=B_SPLINE_CURVE_WITH_KNOTS('',3,(#178087,#178088,#178089,#178090,#178091,
#178092,#178093,#178094,#178095,#178096,#178097,#178098,#178099,#178100,
#178101,#178102,#178103,#178104,#178105,#178106,#178107,#178108,#178109,
#178110,#178111,#178112,#178113,#178114,#178115,#178116,#178117,#178118,
#178119,#178120,#178121,#178122,#178123,#178124,#178125,#178126,#178127,
#178128,#178129,#178130,#178131,#178132,#178133,#178134,#178135,#178136,
#178137,#178138,#178139,#178140,#178141,#178142,#178143,#178144,#178145,
#178146,#178147,#178148,#178149,#178150,#178151,#178152,#178153,#178154,
#178155,#178156,#178157,#178158,#178159,#178160,#178161,#178162,#178163,
#178164,#178165,#178166,#178167,#178168,#178169,#178170,#178171,#178172,
#178173,#178174,#178175,#178176,#178177,#178178,#178179,#178180,#178181,
#178182,#178183,#178184,#178185,#178186,#178187,#178188,#178189,#178190,
#178191,#178192,#178193,#178194,#178195,#178196,#178197,#178198,#178199,
#178200,#178201,#178202,#178203,#178204,#178205,#178206,#178207,#178208,
#178209,#178210,#178211,#178212,#178213,#178214,#178215,#178216,#178217,
#178218,#178219,#178220,#178221,#178222,#178223,#178224,#178225,#178226,
#178227,#178228,#178229,#178230,#178231,#178232,#178233,#178234,#178235,
#178236,#178237,#178238,#178239,#178240,#178241,#178242,#178243,#178244,
#178245,#178246,#178247,#178248,#178249,#178250,#178251,#178252,#178253,
#178254,#178255,#178256,#178257,#178258,#178259,#178260,#178261,#178262,
#178263,#178264,#178265,#178266,#178267,#178268,#178269,#178270,#178271,
#178272,#178273,#178274,#178275,#178276,#178277,#178278,#178279,#178280,
#178281,#178282,#178283,#178284,#178285,#178286,#178287,#178288,#178289,
#178290,#178291,#178292,#178293,#178294,#178295,#178296,#178297,#178298,
#178299,#178300,#178301,#178302,#178303,#178304,#178305,#178306,#178307,
#178308,#178309,#178310,#178311,#178312,#178313,#178314,#178315,#178316,
#178317,#178318,#178319,#178320,#178321,#178322,#178323,#178324,#178325,
#178326,#178327,#178328,#178329,#178330),.UNSPECIFIED.,.F.,.F.,(4,3,3,3,
3,3,3,3,3,3,3,3,3,3,3,3,3,3,3,3,3,3,3,3,3,3,3,3,3,3,3,3,3,3,3,3,3,3,3,3,
3,3,3,3,3,3,3,3,3,3,3,3,3,3,3,3,3,3,3,3,3,3,3,3,3,3,3,3,3,3,3,3,3,3,3,3,
3,3,3,3,3,4),(-670.110184153965,-670.012739495242,-669.913861623891,-669.823127182488,
-669.743169882357,-669.663307085115,-669.583521262643,-669.503794947448,
-669.424110719154,-669.344439732933,-669.264772279407,-669.185092628591,
-669.105385046197,-669.025589817122,-668.945745475414,-668.865787048367,
-668.823391171768,-668.743433871637,-668.663571074394,-668.583785251923,
-668.504058936727,-668.424374708433,-668.344703722213,-668.265036268687,
-668.18535661787,-668.105649035476,-668.0258538064,-667.946009464693,-667.866051037646,
-667.823655161048,-667.743697860916,-667.663835063674,-667.584049241201,
-667.504322926006,-667.424638697711,-667.34496771149,-667.265300257964,
-667.185620607147,-667.105913024752,-667.026117795676,-666.946273453968,
-666.866315026921,-666.823919150327,-666.743961850196,-666.664099052953,
-666.584313230481,-666.504586915286,-666.424902686992,-666.345231700771,
-666.265564247245,-666.185884596429,-666.106177014035,-666.026381784959,
-665.946537443251,-665.866579016204,-665.824183139607,-665.744225839476,
-665.664363042233,-665.584577219762,-665.504850904567,-665.425166676273,
-665.345495690052,-665.265828236526,-665.18614858571,-665.106441003315,
-665.02664577424,-664.946801432533,-664.866843005485,-664.824447128887,
-664.744522891255,-664.664693141368,-664.584940318383,-664.505246922308,
-664.425595500394,-664.345957161305,-664.266322192653,-664.186674835235,
-664.106999325398,-664.027236170141,-663.947423648092,-663.867497597443,
-663.826999002697),.UNSPECIFIED.);
#1562=B_SPLINE_CURVE_WITH_KNOTS('',3,(#178332,#178333,#178334,#178335,#178336,
#178337,#178338,#178339,#178340,#178341,#178342,#178343),.UNSPECIFIED.,
 .F.,.F.,(4,2,1,1,1,1,1,1,4),(-663.826999002697,-663.824711118167,-662.824975107447,
-661.825239096727,-660.825503086007,-659.825767075287,-658.826031064566,
-657.826295053846,-657.543818216983),.UNSPECIFIED.);
#1563=B_SPLINE_CURVE_WITH_KNOTS('',3,(#178345,#178346,#178347,#178348,#178349,
#178350,#178351,#178352,#178353,#178354,#178355,#178356,#178357,#178358,
#178359,#178360,#178361,#178362,#178363,#178364,#178365,#178366,#178367,
#178368,#178369,#178370,#178371,#178372,#178373,#178374,#178375,#178376,
#178377,#178378,#178379,#178380,#178381,#178382,#178383,#178384,#178385,
#178386,#178387,#178388,#178389,#178390,#178391,#178392,#178393,#178394,
#178395,#178396,#178397,#178398,#178399,#178400,#178401,#178402,#178403,
#178404,#178405,#178406,#178407,#178408,#178409,#178410,#178411,#178412,
#178413,#178414,#178415,#178416,#178417,#178418,#178419,#178420,#178421,
#178422,#178423,#178424,#178425,#178426,#178427,#178428,#178429,#178430,
#178431,#178432,#178433,#178434,#178435,#178436,#178437,#178438,#178439,
#178440,#178441,#178442,#178443,#178444,#178445,#178446,#178447,#178448,
#178449,#178450,#178451,#178452,#178453,#178454,#178455,#178456,#178457,
#178458,#178459,#178460,#178461,#178462,#178463,#178464,#178465,#178466,
#178467,#178468,#178469,#178470,#178471,#178472,#178473,#178474,#178475,
#178476,#178477,#178478,#178479,#178480,#178481,#178482,#178483,#178484,
#178485,#178486,#178487,#178488,#178489,#178490,#178491,#178492,#178493,
#178494,#178495,#178496,#178497,#178498,#178499,#178500,#178501,#178502,
#178503,#178504,#178505,#178506,#178507,#178508,#178509,#178510,#178511,
#178512,#178513,#178514,#178515,#178516,#178517,#178518,#178519,#178520,
#178521,#178522,#178523,#178524,#178525,#178526,#178527,#178528,#178529,
#178530,#178531,#178532,#178533,#178534,#178535,#178536,#178537,#178538,
#178539,#178540,#178541,#178542,#178543,#178544,#178545,#178546,#178547,
#178548,#178549,#178550,#178551,#178552,#178553,#178554,#178555,#178556,
#178557,#178558,#178559,#178560,#178561,#178562,#178563,#178564,#178565,
#178566,#178567,#178568,#178569,#178570,#178571,#178572,#178573,#178574,
#178575,#178576,#178577,#178578,#178579,#178580,#178581,#178582,#178583,
#178584,#178585,#178586,#178587,#178588),.UNSPECIFIED.,.F.,.F.,(4,3,3,3,
3,3,3,3,3,3,3,3,3,3,3,3,3,3,3,3,3,3,3,3,3,3,3,3,3,3,3,3,3,3,3,3,3,3,3,3,
3,3,3,3,3,3,3,3,3,3,3,3,3,3,3,3,3,3,3,3,3,3,3,3,3,3,3,3,3,3,3,3,3,3,3,3,
3,3,3,3,3,4),(-657.543813695517,-657.464751020353,-657.3849770232,-657.305959699517,
-657.226940888437,-657.147904359238,-657.06756803021,-656.988407198372,
-656.907483120749,-656.826559043126,-656.746601742995,-656.666738945752,
-656.58695312328,-656.507226808085,-656.427542579791,-656.34787159357,-656.268204140044,
-656.188524489227,-656.108816906833,-656.029021677757,-655.94917733605,
-655.869218909002,-655.826823032406,-655.746865732275,-655.667002935032,
-655.58721711256,-655.507490797365,-655.42780656907,-655.348135582849,-655.268468129323,
-655.188788478506,-655.109080896112,-655.029285667036,-654.949441325329,
-654.869482898281,-654.827087021686,-654.747129721555,-654.667266924312,
-654.587481101841,-654.507754786645,-654.428070558352,-654.348399572131,
-654.268732118605,-654.189052467789,-654.109344885395,-654.029549656319,
-653.949705314611,-653.869746887564,-653.827351010966,-653.747393710834,
-653.667530913592,-653.58774509112,-653.508018775925,-653.42833454763,-653.348663561409,
-653.268996107883,-653.189316457066,-653.109608874671,-653.029813645595,
-652.949969303887,-652.870010876839,-652.827615000245,-652.747657700114,
-652.667794902871,-652.5880090804,-652.508282765205,-652.428598536911,-652.34892755069,
-652.269260097164,-652.189580446348,-652.109872863953,-652.030077634878,
-651.95023329317,-651.870274866122,-651.827878989526,-651.745947788662,
-651.664127715656,-651.582405638949,-651.500793005596,-651.419244358718,
-651.337756902616,-651.260628388338),.UNSPECIFIED.);
#1564=B_SPLINE_CURVE_WITH_KNOTS('',3,(#178590,#178591,#178592,#178593,#178594,
#178595,#178596,#178597,#178598,#178599),.UNSPECIFIED.,.F.,.F.,(4,1,1,1,
1,1,1,4),(-651.260623045353,-650.828142978805,-649.828406968085,-648.828670957365,
-647.828934946645,-646.829198935925,-645.829462925205,-644.977443081158),
 .UNSPECIFIED.);
#1565=B_SPLINE_CURVE_WITH_KNOTS('',3,(#178601,#178602,#178603,#178604,#178605,
#178606,#178607,#178608,#178609,#178610,#178611),.UNSPECIFIED.,.F.,.F.,
(4,1,1,1,1,1,1,1,4),(-644.977443081158,-644.829726914485,-643.829990903764,
-642.830254893044,-641.830518882324,-640.830782871604,-639.831046860884,
-638.831310850164,-638.694257773979),.UNSPECIFIED.);
#1566=B_SPLINE_CURVE_WITH_KNOTS('',3,(#178613,#178614,#178615,#178616,#178617,
#178618,#178619,#178620,#178621,#178622),.UNSPECIFIED.,.F.,.F.,(4,1,1,1,
1,1,1,4),(-638.694257773979,-637.831574839444,-636.831838828723,-635.832102818003,
-634.832366807283,-633.832630796563,-632.832894785843,-632.411072466799),
 .UNSPECIFIED.);
#1567=B_SPLINE_CURVE_WITH_KNOTS('',3,(#178624,#178625,#178626,#178627,#178628,
#178629,#178630,#178631,#178632,#178633),.UNSPECIFIED.,.F.,.F.,(4,1,1,1,
1,1,1,4),(-632.411072466799,-631.833158775123,-630.833422764403,-629.833686753683,
-628.833950742962,-627.834214732242,-626.834478721522,-626.12788715962),
 .UNSPECIFIED.);
#1568=B_SPLINE_CURVE_WITH_KNOTS('',3,(#178635,#178636,#178637,#178638,#178639,
#178640,#178641,#178642,#178643,#178644,#178645,#178646,#178647,#178648,
#178649,#178650,#178651,#178652,#178653,#178654,#178655,#178656,#178657,
#178658,#178659,#178660,#178661,#178662,#178663,#178664,#178665,#178666,
#178667,#178668,#178669,#178670,#178671,#178672,#178673,#178674,#178675,
#178676,#178677,#178678,#178679,#178680,#178681,#178682,#178683,#178684,
#178685,#178686,#178687,#178688,#178689,#178690,#178691,#178692,#178693,
#178694,#178695,#178696,#178697,#178698,#178699,#178700,#178701,#178702,
#178703,#178704,#178705,#178706,#178707,#178708,#178709,#178710,#178711,
#178712,#178713,#178714,#178715,#178716,#178717,#178718,#178719,#178720,
#178721,#178722,#178723,#178724,#178725,#178726,#178727,#178728,#178729,
#178730,#178731,#178732,#178733,#178734,#178735,#178736,#178737,#178738,
#178739,#178740,#178741,#178742,#178743,#178744,#178745,#178746,#178747,
#178748,#178749,#178750,#178751,#178752,#178753,#178754,#178755,#178756,
#178757,#178758,#178759,#178760,#178761,#178762,#178763,#178764,#178765,
#178766,#178767,#178768,#178769,#178770,#178771,#178772,#178773,#178774,
#178775,#178776,#178777,#178778,#178779,#178780,#178781,#178782,#178783,
#178784,#178785,#178786,#178787,#178788,#178789,#178790,#178791,#178792,
#178793,#178794,#178795,#178796,#178797,#178798,#178799,#178800,#178801,
#178802,#178803,#178804,#178805,#178806,#178807,#178808,#178809,#178810,
#178811,#178812,#178813,#178814,#178815,#178816,#178817,#178818,#178819,
#178820,#178821,#178822,#178823,#178824,#178825,#178826,#178827,#178828,
#178829,#178830,#178831,#178832,#178833,#178834,#178835,#178836,#178837,
#178838,#178839,#178840,#178841,#178842,#178843,#178844,#178845,#178846,
#178847,#178848,#178849,#178850,#178851,#178852,#178853,#178854,#178855,
#178856,#178857,#178858,#178859,#178860,#178861,#178862,#178863,#178864,
#178865,#178866,#178867,#178868,#178869,#178870,#178871,#178872,#178873,
#178874,#178875,#178876,#178877,#178878),.UNSPECIFIED.,.F.,.F.,(4,3,3,3,
3,3,3,3,3,3,3,3,3,3,3,3,3,3,3,3,3,3,3,3,3,3,3,3,3,3,3,3,3,3,3,3,3,3,3,3,
3,3,3,3,3,3,3,3,3,3,3,3,3,3,3,3,3,3,3,3,3,3,3,3,3,3,3,3,3,3,3,3,3,3,3,3,
3,3,3,3,3,4),(-626.127886989932,-626.031132445784,-625.932937578293,-625.834742710802,
-625.754785410671,-625.674922613429,-625.595136790957,-625.515410475762,
-625.435726247468,-625.356055261248,-625.276387807722,-625.196708156906,
-625.117000574512,-625.037205345437,-624.95736100373,-624.877402576683,
-624.835006700082,-624.755049399951,-624.675186602708,-624.595400780236,
-624.515674465041,-624.435990236747,-624.356319250526,-624.276651797,-624.196972146184,
-624.117264563789,-624.037469334714,-623.957624993006,-623.877666565959,
-623.835270689362,-623.755313389231,-623.675450591988,-623.595664769516,
-623.515938454321,-623.436254226027,-623.356583239806,-623.27691578628,
-623.197236135464,-623.117528553069,-623.037733323994,-622.957888982286,
-622.877930555239,-622.835534678642,-622.755577378511,-622.675714581268,
-622.595928758796,-622.5162024436,-622.436518215306,-622.356847229085,-622.277179775559,
-622.197500124743,-622.117792542348,-622.037997313272,-621.958152971564,
-621.878194544517,-621.835798667921,-621.75584136779,-621.675978570547,
-621.596192748075,-621.51646643288,-621.436782204585,-621.357111218364,
-621.277443764838,-621.197764114022,-621.118056531627,-621.038261302552,
-620.958416960844,-620.878458533796,-620.836062657201,-620.756223956451,
-620.676479699828,-620.596812243681,-620.517204005867,-620.437637451845,
-620.358083586226,-620.278532678271,-620.198968894966,-620.119376398451,
-620.039696321836,-619.959966231899,-619.880124160307,-619.84470185244),
 .UNSPECIFIED.);
#1569=B_SPLINE_CURVE_WITH_KNOTS('',3,(#178880,#178881,#178882,#178883,#178884,
#178885,#178886,#178887,#178888,#178889,#178890,#178891),.UNSPECIFIED.,
 .F.,.F.,(4,2,1,1,1,1,1,1,4),(-619.84470185244,-619.836326646481,-618.836590635761,
-617.836854625041,-616.837118614321,-615.837382603601,-614.837646592881,
-613.83791058216,-613.561520588044),.UNSPECIFIED.);
#1570=B_SPLINE_CURVE_WITH_KNOTS('',3,(#178893,#178894,#178895,#178896,#178897,
#178898,#178899,#178900,#178901,#178902,#178903,#178904,#178905,#178906,
#178907,#178908,#178909,#178910,#178911,#178912,#178913,#178914,#178915,
#178916,#178917,#178918,#178919,#178920,#178921,#178922,#178923,#178924,
#178925,#178926,#178927,#178928,#178929,#178930,#178931,#178932,#178933,
#178934,#178935,#178936,#178937,#178938,#178939,#178940,#178941,#178942,
#178943,#178944,#178945,#178946,#178947,#178948,#178949,#178950,#178951,
#178952,#178953,#178954,#178955,#178956,#178957,#178958,#178959,#178960,
#178961,#178962,#178963,#178964,#178965,#178966,#178967,#178968,#178969,
#178970,#178971,#178972,#178973,#178974,#178975,#178976,#178977,#178978,
#178979,#178980,#178981,#178982,#178983,#178984,#178985,#178986,#178987,
#178988,#178989,#178990,#178991,#178992,#178993,#178994,#178995,#178996,
#178997,#178998,#178999,#179000,#179001,#179002,#179003,#179004,#179005,
#179006,#179007,#179008,#179009,#179010,#179011,#179012,#179013,#179014,
#179015,#179016,#179017,#179018,#179019,#179020,#179021,#179022,#179023,
#179024,#179025,#179026,#179027,#179028,#179029,#179030,#179031,#179032,
#179033,#179034,#179035,#179036,#179037,#179038,#179039,#179040,#179041,
#179042,#179043,#179044,#179045,#179046,#179047,#179048,#179049,#179050,
#179051,#179052,#179053,#179054,#179055,#179056,#179057,#179058,#179059,
#179060,#179061,#179062,#179063,#179064,#179065,#179066,#179067,#179068,
#179069,#179070,#179071,#179072,#179073,#179074,#179075,#179076,#179077,
#179078,#179079,#179080,#179081,#179082,#179083,#179084,#179085,#179086,
#179087,#179088,#179089,#179090,#179091,#179092,#179093,#179094,#179095,
#179096,#179097,#179098,#179099,#179100,#179101,#179102,#179103,#179104,
#179105,#179106,#179107,#179108,#179109,#179110,#179111,#179112,#179113,
#179114,#179115,#179116,#179117,#179118,#179119,#179120,#179121,#179122,
#179123,#179124,#179125,#179126,#179127,#179128,#179129,#179130,#179131,
#179132,#179133,#179134,#179135,#179136),.UNSPECIFIED.,.F.,.F.,(4,3,3,3,
3,3,3,3,3,3,3,3,3,3,3,3,3,3,3,3,3,3,3,3,3,3,3,3,3,3,3,3,3,3,3,3,3,3,3,3,
3,3,3,3,3,3,3,3,3,3,3,3,3,3,3,3,3,3,3,3,3,3,3,3,3,3,3,3,3,3,3,3,3,3,3,3,
3,3,3,3,3,4),(-613.56151654526,-613.482503752502,-613.401962604869,-613.323000140188,
-613.244037899469,-613.165059611842,-613.083338351741,-613.004237540242,
-612.921206055841,-612.83817457144,-612.758217271309,-612.678354474066,
-612.598568651595,-612.518842336399,-612.439158108106,-612.359487121885,
-612.279819668359,-612.200140017542,-612.120432435148,-612.040637206073,
-611.960792864365,-611.880834437318,-611.83843856072,-611.758481260589,
-611.678618463346,-611.598832640874,-611.519106325679,-611.439422097385,
-611.359751111164,-611.280083657638,-611.200404006821,-611.120696424427,
-611.040901195352,-610.961056853644,-610.881098426597,-610.83870255,-610.758745249869,
-610.678882452626,-610.599096630154,-610.519370314959,-610.439686086665,
-610.360015100444,-610.280347646918,-610.200667996101,-610.120960413707,
-610.041165184631,-609.961320842923,-609.881362415876,-609.83896653928,
-609.759009239149,-609.679146441906,-609.599360619435,-609.519634304239,
-609.439950075945,-609.360279089724,-609.280611636198,-609.200931985382,
-609.121224402987,-609.041429173912,-608.961584832204,-608.881626405157,
-608.83923052856,-608.759273228429,-608.679410431186,-608.599624608714,
-608.519898293519,-608.440214065225,-608.360543079004,-608.280875625478,
-608.201195974662,-608.121488392268,-608.041693163193,-607.961848821485,
-607.881890394438,-607.83949451784,-607.757398416682,-607.675415270246,
-607.593532266941,-607.511762748388,-607.430059596932,-607.34842276145,
-607.278331238081),.UNSPECIFIED.);
#1571=B_SPLINE_CURVE_WITH_KNOTS('',3,(#179138,#179139,#179140,#179141,#179142,
#179143,#179144,#179145,#179146,#179147),.UNSPECIFIED.,.F.,.F.,(4,1,1,1,
1,1,1,4),(-607.278326294004,-606.839758507119,-605.840022496399,-604.840286485679,
-603.840550474959,-602.840814464239,-601.841078453519,-600.995145930901),
 .UNSPECIFIED.);
#1572=B_SPLINE_CURVE_WITH_KNOTS('',3,(#179149,#179150,#179151,#179152,#179153,
#179154,#179155,#179156,#179157,#179158,#179159),.UNSPECIFIED.,.F.,.F.,
(4,1,1,1,1,1,1,1,4),(-600.995145930901,-600.841342442799,-599.841606432079,
-598.841870421359,-597.842134410638,-596.842398399918,-595.842662389198,
-594.842926378478,-594.711960623722),.UNSPECIFIED.);
#1573=B_SPLINE_CURVE_WITH_KNOTS('',3,(#179161,#179162,#179163,#179164,#179165,
#179166,#179167,#179168,#179169,#179170,#179171,#179172,#179173,#179174,
#179175,#179176,#179177,#179178,#179179,#179180,#179181,#179182,#179183,
#179184,#179185,#179186,#179187,#179188,#179189,#179190,#179191,#179192,
#179193,#179194,#179195,#179196,#179197,#179198,#179199,#179200,#179201,
#179202,#179203,#179204,#179205,#179206,#179207,#179208,#179209,#179210,
#179211,#179212,#179213,#179214,#179215,#179216,#179217,#179218,#179219,
#179220,#179221,#179222,#179223,#179224,#179225,#179226,#179227,#179228,
#179229,#179230,#179231,#179232,#179233,#179234,#179235,#179236,#179237,
#179238,#179239,#179240,#179241,#179242,#179243,#179244,#179245,#179246,
#179247,#179248,#179249,#179250,#179251,#179252,#179253,#179254,#179255,
#179256,#179257,#179258,#179259,#179260,#179261,#179262,#179263,#179264,
#179265,#179266,#179267,#179268,#179269,#179270,#179271,#179272,#179273,
#179274,#179275,#179276,#179277,#179278,#179279,#179280,#179281,#179282,
#179283,#179284,#179285,#179286,#179287,#179288,#179289,#179290,#179291,
#179292,#179293,#179294,#179295,#179296,#179297,#179298,#179299,#179300,
#179301,#179302,#179303,#179304,#179305,#179306,#179307,#179308,#179309,
#179310,#179311,#179312,#179313,#179314,#179315,#179316,#179317,#179318,
#179319,#179320,#179321,#179322,#179323,#179324,#179325,#179326,#179327,
#179328,#179329,#179330,#179331,#179332,#179333,#179334,#179335,#179336,
#179337,#179338,#179339,#179340,#179341,#179342,#179343,#179344,#179345,
#179346,#179347,#179348,#179349,#179350,#179351,#179352,#179353,#179354,
#179355,#179356,#179357,#179358,#179359,#179360,#179361,#179362,#179363,
#179364,#179365,#179366,#179367,#179368,#179369,#179370,#179371,#179372,
#179373,#179374,#179375,#179376,#179377,#179378,#179379,#179380,#179381,
#179382,#179383,#179384,#179385,#179386,#179387,#179388,#179389,#179390,
#179391,#179392,#179393,#179394,#179395,#179396,#179397,#179398,#179399,
#179400,#179401,#179402,#179403,#179404),.UNSPECIFIED.,.F.,.F.,(4,3,3,3,
3,3,3,3,3,3,3,3,3,3,3,3,3,3,3,3,3,3,3,3,3,3,3,3,3,3,3,3,3,3,3,3,3,3,3,3,
3,3,3,3,3,3,3,3,3,3,3,3,3,3,3,3,3,3,3,3,3,3,3,3,3,3,3,3,3,3,3,3,3,3,3,3,
3,3,3,3,3,4),(-594.711960623722,-594.633214489757,-594.554547606313,-594.475941583082,
-594.396847681166,-594.318297702532,-594.239749946813,-594.161187876371,
-594.081688499218,-594.003009440059,-593.923099903909,-593.843190367758,
-593.763233067627,-593.683370270384,-593.603584447913,-593.523858132717,
-593.444173904423,-593.364502918202,-593.284835464676,-593.20515581386,
-593.125448231465,-593.04565300239,-592.965808660682,-592.885850233635,
-592.843454357038,-592.763497056907,-592.683634259664,-592.603848437192,
-592.524122121997,-592.444437893703,-592.364766907482,-592.285099453956,
-592.20541980314,-592.125712220745,-592.045916991669,-591.966072649962,
-591.886114222915,-591.843718346318,-591.763761046187,-591.683898248944,
-591.604112426473,-591.524386111277,-591.444701882984,-591.365030896763,
-591.285363443237,-591.205683792421,-591.125976210027,-591.046180980951,
-590.966336639243,-590.886378212196,-590.843982335598,-590.764025035466,
-590.684162238224,-590.604376415752,-590.524650100556,-590.444965872261,
-590.36529488604,-590.285627432514,-590.205947781697,-590.126240199303,
-590.046444970227,-589.966600628519,-589.886642201472,-589.844246324877,
-589.764289024746,-589.684426227503,-589.604640405031,-589.524914089836,
-589.445229861541,-589.36555887532,-589.285891421794,-589.206211770978,
-589.126504188583,-589.046708959508,-588.9668646178,-588.886906190753,-588.844510314157,
-588.756470151581,-588.668761629949,-588.581261527724,-588.494106043377,
-588.428775519318),.UNSPECIFIED.);
#1574=B_SPLINE_CURVE_WITH_KNOTS('',3,(#179406,#179407,#179408,#179409,#179410,
#179411,#179412,#179413,#179414,#179415),.UNSPECIFIED.,.F.,.F.,(4,1,1,1,
1,1,1,4),(-588.428775316542,-587.844774303437,-586.845038292717,-585.845302281997,
-584.845566271277,-583.845830260557,-582.846094249836,-582.145590009363),
 .UNSPECIFIED.);
#1575=B_SPLINE_CURVE_WITH_KNOTS('',3,(#179417,#179418,#179419,#179420,#179421,
#179422,#179423,#179424,#179425,#179426,#179427,#179428,#179429,#179430,
#179431,#179432,#179433,#179434,#179435,#179436,#179437,#179438,#179439,
#179440,#179441,#179442,#179443,#179444,#179445,#179446,#179447,#179448,
#179449,#179450,#179451,#179452,#179453,#179454,#179455,#179456,#179457,
#179458,#179459,#179460,#179461,#179462,#179463,#179464,#179465,#179466,
#179467,#179468,#179469,#179470,#179471,#179472,#179473,#179474,#179475,
#179476,#179477,#179478,#179479,#179480,#179481,#179482,#179483,#179484,
#179485,#179486,#179487,#179488,#179489,#179490,#179491,#179492,#179493,
#179494,#179495,#179496,#179497,#179498,#179499,#179500,#179501,#179502,
#179503,#179504,#179505,#179506,#179507,#179508,#179509,#179510,#179511,
#179512,#179513,#179514,#179515,#179516,#179517,#179518,#179519,#179520,
#179521,#179522,#179523,#179524,#179525,#179526,#179527,#179528,#179529,
#179530,#179531,#179532,#179533,#179534,#179535,#179536,#179537,#179538,
#179539,#179540,#179541,#179542,#179543,#179544,#179545,#179546,#179547,
#179548,#179549,#179550,#179551,#179552,#179553,#179554,#179555,#179556,
#179557,#179558,#179559,#179560,#179561,#179562,#179563,#179564,#179565,
#179566,#179567,#179568,#179569,#179570,#179571,#179572,#179573,#179574,
#179575,#179576,#179577,#179578,#179579,#179580,#179581,#179582,#179583,
#179584,#179585,#179586,#179587,#179588,#179589,#179590,#179591,#179592,
#179593,#179594,#179595,#179596,#179597,#179598,#179599,#179600,#179601,
#179602,#179603,#179604,#179605,#179606,#179607,#179608,#179609,#179610,
#179611,#179612,#179613,#179614,#179615,#179616,#179617,#179618,#179619,
#179620,#179621,#179622,#179623,#179624,#179625,#179626,#179627,#179628,
#179629,#179630,#179631,#179632,#179633,#179634,#179635,#179636,#179637,
#179638,#179639,#179640,#179641,#179642,#179643,#179644,#179645,#179646,
#179647,#179648,#179649,#179650,#179651,#179652,#179653,#179654,#179655,
#179656,#179657,#179658,#179659,#179660),.UNSPECIFIED.,.F.,.F.,(4,3,3,3,
3,3,3,3,3,3,3,3,3,3,3,3,3,3,3,3,3,3,3,3,3,3,3,3,3,3,3,3,3,3,3,3,3,3,3,3,
3,3,3,3,3,3,3,3,3,3,3,3,3,3,3,3,3,3,3,3,3,3,3,3,3,3,3,3,3,3,3,3,3,3,3,3,
3,3,3,3,3,4),(-582.145589826881,-582.049496542247,-581.947927390681,-581.846358239116,
-581.766400938985,-581.686538141743,-581.606752319271,-581.527026004076,
-581.447341775783,-581.367670789562,-581.288003336036,-581.20832368522,
-581.128616102826,-581.048820873751,-580.968976532043,-580.889018104996,
-580.846622228396,-580.766664928265,-580.686802131022,-580.60701630855,
-580.527289993355,-580.447605765061,-580.36793477884,-580.288267325314,
-580.208587674498,-580.128880092103,-580.049084863028,-579.96924052132,
-579.889282094273,-579.846886217676,-579.766928917545,-579.687066120302,
-579.60728029783,-579.527553982635,-579.447869754341,-579.36819876812,-579.288531314594,
-579.208851663777,-579.129144081383,-579.049348852307,-578.9695045106,-578.889546083552,
-578.847150206956,-578.767192906825,-578.687330109582,-578.60754428711,
-578.527817971915,-578.448133743621,-578.3684627574,-578.288795303875,-578.209115653058,
-578.129408070664,-578.049612841588,-577.969768499881,-577.889810072833,
-577.847414196236,-577.767456896105,-577.687594098862,-577.60780827639,
-577.528081961195,-577.448397732901,-577.36872674668,-577.289059293154,
-577.209379642337,-577.129672059943,-577.049876830867,-576.97003248916,
-576.890074062112,-576.847678185516,-576.767921519313,-576.688259249651,
-576.608673655916,-576.52914707972,-576.445804282528,-576.366331940496,
-576.286861398012,-576.207376753605,-576.127862100087,-576.048259715846,
-575.968606018376,-575.888842977266,-575.862404702183),.UNSPECIFIED.);
#1576=B_SPLINE_CURVE_WITH_KNOTS('',3,(#179662,#179663,#179664,#179665,#179666,
#179667,#179668,#179669,#179670,#179671,#179672,#179673),.UNSPECIFIED.,
 .F.,.F.,(4,2,1,1,1,1,1,1,4),(-575.862404702183,-575.847942174796,-574.848206164075,
-573.848470153355,-572.848734142635,-571.848998131915,-570.849262121195,
-569.849526110475,-569.579222933784),.UNSPECIFIED.);
#1577=B_SPLINE_CURVE_WITH_KNOTS('',3,(#179675,#179676,#179677,#179678,#179679,
#179680,#179681,#179682,#179683,#179684,#179685,#179686,#179687,#179688,
#179689,#179690,#179691,#179692,#179693,#179694,#179695,#179696,#179697,
#179698,#179699,#179700,#179701,#179702,#179703,#179704,#179705,#179706,
#179707,#179708,#179709,#179710,#179711,#179712,#179713,#179714,#179715,
#179716,#179717,#179718,#179719,#179720,#179721,#179722,#179723,#179724,
#179725,#179726,#179727,#179728,#179729,#179730,#179731,#179732,#179733,
#179734,#179735,#179736,#179737,#179738,#179739,#179740,#179741,#179742,
#179743,#179744,#179745,#179746,#179747,#179748,#179749,#179750,#179751,
#179752,#179753,#179754,#179755,#179756,#179757,#179758,#179759,#179760,
#179761,#179762,#179763,#179764,#179765,#179766,#179767,#179768,#179769,
#179770,#179771,#179772,#179773,#179774,#179775,#179776,#179777,#179778,
#179779,#179780,#179781,#179782,#179783,#179784,#179785,#179786,#179787,
#179788,#179789,#179790,#179791,#179792,#179793,#179794,#179795,#179796,
#179797,#179798,#179799,#179800,#179801,#179802,#179803,#179804,#179805,
#179806,#179807,#179808,#179809,#179810,#179811,#179812,#179813,#179814,
#179815,#179816,#179817,#179818,#179819,#179820,#179821,#179822,#179823,
#179824,#179825,#179826,#179827,#179828,#179829,#179830,#179831,#179832,
#179833,#179834,#179835,#179836,#179837,#179838,#179839,#179840,#179841,
#179842,#179843,#179844,#179845,#179846,#179847,#179848,#179849,#179850,
#179851,#179852,#179853,#179854,#179855,#179856,#179857,#179858,#179859,
#179860,#179861,#179862,#179863,#179864,#179865,#179866,#179867,#179868,
#179869,#179870,#179871,#179872,#179873,#179874,#179875,#179876,#179877,
#179878,#179879,#179880,#179881,#179882,#179883,#179884,#179885,#179886,
#179887,#179888,#179889,#179890,#179891,#179892,#179893,#179894,#179895,
#179896,#179897,#179898,#179899,#179900,#179901,#179902,#179903,#179904,
#179905,#179906,#179907,#179908,#179909,#179910,#179911,#179912,#179913,
#179914,#179915,#179916,#179917,#179918,#179919,#179920,#179921),
 .UNSPECIFIED.,.F.,.F.,(4,3,3,3,3,3,3,3,3,3,3,3,3,3,3,3,3,3,3,3,3,3,3,3,
3,3,3,3,3,3,3,3,3,3,3,3,3,3,3,3,3,3,3,3,3,3,3,3,3,3,3,3,3,3,3,3,3,3,3,3,
3,3,3,3,3,3,3,3,3,3,3,3,3,3,3,3,3,3,3,3,3,3,4),(-569.579219395004,-569.500253204918,
-569.418945316773,-569.340034366194,-569.261125310107,-569.182201840767,
-569.099098905514,-569.020054680491,-568.940956990892,-568.86175344233,
-568.849790099755,-568.769832799623,-568.689970002381,-568.610184179909,
-568.530457864713,-568.450773636419,-568.371102650198,-568.291435196672,
-568.211755545855,-568.13204796346,-568.052252734384,-567.972408392676,
-567.892449965629,-567.850054089034,-567.770096788903,-567.69023399166,
-567.610448169188,-567.530721853993,-567.451037625699,-567.371366639478,
-567.291699185952,-567.212019535136,-567.132311952741,-567.052516723666,
-566.972672381958,-566.892713954911,-566.850318078314,-566.770360778183,
-566.69049798094,-566.610712158469,-566.530985843273,-566.451301614979,
-566.371630628758,-566.291963175232,-566.212283524416,-566.132575942021,
-566.052780712946,-565.972936371238,-565.892977944191,-565.850582067594,
-565.770624767463,-565.69076197022,-565.610976147748,-565.531249832553,
-565.451565604259,-565.371894618038,-565.292227164512,-565.212547513696,
-565.132839931302,-565.053044702226,-564.973200360518,-564.893241933471,
-564.850846056874,-564.770888756743,-564.6910259595,-564.611240137028,-564.531513821833,
-564.451829593539,-564.372158607318,-564.292491153792,-564.212811502976,
-564.133103920581,-564.053308691505,-563.973464349798,-563.89350592275,
-563.851110046154,-563.768843700018,-563.686692243135,-563.604643212547,
-563.522711875554,-563.440849456856,-563.359058510945,-563.296034087824),
 .UNSPECIFIED.);
#1578=B_SPLINE_CURVE_WITH_KNOTS('',3,(#179923,#179924,#179925,#179926,#179927,
#179928,#179929,#179930,#179931,#179932),.UNSPECIFIED.,.F.,.F.,(4,1,1,1,
1,1,1,4),(-563.296029712208,-562.851374035434,-561.851638024714,-560.851902013993,
-559.852166003273,-558.852429992553,-557.852693981833,-557.012848780644),
 .UNSPECIFIED.);
#1579=B_SPLINE_CURVE_WITH_KNOTS('',3,(#179934,#179935,#179936,#179937,#179938,
#179939,#179940,#179941,#179942,#179943,#179944),.UNSPECIFIED.,.F.,.F.,
(4,1,1,1,1,1,1,1,4),(-557.012848780644,-556.852957971113,-555.853221960393,
-554.853485949673,-553.853749938953,-552.854013928232,-551.854277917512,
-550.854541906792,-550.729663473465),.UNSPECIFIED.);
#1580=B_SPLINE_CURVE_WITH_KNOTS('',3,(#179946,#179947,#179948,#179949,#179950,
#179951,#179952,#179953,#179954,#179955,#179956,#179957,#179958,#179959,
#179960,#179961,#179962,#179963,#179964,#179965,#179966,#179967,#179968,
#179969,#179970,#179971,#179972,#179973,#179974,#179975,#179976,#179977,
#179978,#179979,#179980,#179981,#179982,#179983,#179984,#179985,#179986,
#179987,#179988,#179989,#179990,#179991,#179992,#179993,#179994,#179995,
#179996,#179997,#179998,#179999,#180000,#180001,#180002,#180003,#180004,
#180005,#180006,#180007,#180008,#180009,#180010,#180011,#180012,#180013,
#180014,#180015,#180016,#180017,#180018,#180019,#180020,#180021,#180022,
#180023,#180024,#180025,#180026,#180027,#180028,#180029,#180030,#180031,
#180032,#180033,#180034,#180035,#180036,#180037,#180038,#180039,#180040,
#180041,#180042,#180043,#180044,#180045,#180046,#180047,#180048,#180049,
#180050,#180051,#180052,#180053,#180054,#180055,#180056,#180057,#180058,
#180059,#180060,#180061,#180062,#180063,#180064,#180065,#180066,#180067,
#180068,#180069,#180070,#180071,#180072,#180073,#180074,#180075,#180076,
#180077,#180078,#180079,#180080,#180081,#180082,#180083,#180084,#180085,
#180086,#180087,#180088,#180089,#180090,#180091,#180092,#180093,#180094,
#180095,#180096,#180097,#180098,#180099,#180100,#180101,#180102,#180103,
#180104,#180105,#180106,#180107,#180108,#180109,#180110,#180111,#180112,
#180113,#180114,#180115,#180116,#180117,#180118,#180119,#180120,#180121,
#180122,#180123,#180124,#180125,#180126,#180127,#180128,#180129,#180130,
#180131,#180132,#180133,#180134,#180135,#180136,#180137,#180138,#180139,
#180140,#180141,#180142,#180143,#180144,#180145,#180146,#180147,#180148,
#180149,#180150,#180151,#180152,#180153,#180154,#180155,#180156,#180157,
#180158,#180159,#180160,#180161,#180162,#180163,#180164,#180165,#180166,
#180167,#180168,#180169,#180170,#180171,#180172,#180173,#180174,#180175,
#180176,#180177,#180178,#180179,#180180,#180181,#180182,#180183,#180184,
#180185,#180186,#180187,#180188,#180189),.UNSPECIFIED.,.F.,.F.,(4,3,3,3,
3,3,3,3,3,3,3,3,3,3,3,3,3,3,3,3,3,3,3,3,3,3,3,3,3,3,3,3,3,3,3,3,3,3,3,3,
3,3,3,3,3,3,3,3,3,3,3,3,3,3,3,3,3,3,3,3,3,3,3,3,3,3,3,3,3,3,3,3,3,3,3,3,
3,3,3,3,3,4),(-550.729663473465,-550.650891342868,-550.572199648605,-550.493570008962,
-550.413724494851,-550.335153720726,-550.256586124739,-550.178005180778,
-550.097205359601,-550.018508004469,-549.93665695027,-549.854805896072,
-549.774848595941,-549.694985798698,-549.615199976226,-549.535473661031,
-549.455789432737,-549.376118446516,-549.29645099299,-549.216771342174,
-549.13706375978,-549.057268530704,-548.977424188996,-548.897465761949,
-548.855069885352,-548.775112585221,-548.695249787978,-548.615463965506,
-548.535737650311,-548.456053422017,-548.376382435796,-548.29671498227,
-548.217035331454,-548.13732774906,-548.057532519984,-547.977688178277,
-547.897729751229,-547.855333874632,-547.775376574501,-547.695513777258,
-547.615727954786,-547.536001639591,-547.456317411296,-547.376646425075,
-547.296978971549,-547.217299320733,-547.137591738338,-547.057796509262,
-546.977952167554,-546.897993740507,-546.855597863912,-546.775640563781,
-546.695777766538,-546.615991944066,-546.536265628871,-546.456581400576,
-546.376910414356,-546.29724296083,-546.217563310013,-546.137855727619,
-546.058060498543,-545.978216156835,-545.898257729788,-545.855861853192,
-545.775904553061,-545.696041755818,-545.616255933346,-545.536529618151,
-545.456845389857,-545.377174403636,-545.29750695011,-545.217827299294,
-545.1381197169,-545.058324487824,-544.978480146117,-544.89852171907,-544.856125842472,
-544.767725216914,-544.679669533128,-544.591833594987,-544.504359017994,
-544.44647837855),.UNSPECIFIED.);
#1581=B_SPLINE_CURVE_WITH_KNOTS('',3,(#180191,#180192,#180193,#180194,#180195,
#180196,#180197,#180198,#180199,#180200),.UNSPECIFIED.,.F.,.F.,(4,1,1,1,
1,1,1,4),(-544.446478166285,-543.856389831751,-542.856653821031,-541.856917810311,
-540.857181799591,-539.857445788871,-538.857709778151,-538.163292859106),
 .UNSPECIFIED.);
#1582=B_SPLINE_CURVE_WITH_KNOTS('',3,(#180202,#180203,#180204,#180205,#180206,
#180207,#180208,#180209,#180210,#180211,#180212,#180213,#180214,#180215,
#180216,#180217,#180218,#180219,#180220,#180221,#180222,#180223,#180224,
#180225,#180226,#180227,#180228,#180229,#180230,#180231,#180232,#180233,
#180234,#180235,#180236,#180237,#180238,#180239,#180240,#180241,#180242,
#180243,#180244,#180245,#180246,#180247,#180248,#180249,#180250,#180251,
#180252,#180253,#180254,#180255,#180256,#180257,#180258,#180259,#180260,
#180261,#180262,#180263,#180264,#180265,#180266,#180267,#180268,#180269,
#180270,#180271,#180272,#180273,#180274,#180275,#180276,#180277,#180278,
#180279,#180280,#180281,#180282,#180283,#180284,#180285,#180286,#180287,
#180288,#180289,#180290,#180291,#180292,#180293,#180294,#180295,#180296,
#180297,#180298,#180299,#180300,#180301,#180302,#180303,#180304,#180305,
#180306,#180307,#180308,#180309,#180310,#180311,#180312,#180313,#180314,
#180315,#180316,#180317,#180318,#180319,#180320,#180321,#180322,#180323,
#180324,#180325,#180326,#180327,#180328,#180329,#180330,#180331,#180332,
#180333,#180334,#180335,#180336,#180337,#180338,#180339,#180340,#180341,
#180342,#180343,#180344,#180345,#180346,#180347,#180348,#180349,#180350,
#180351,#180352,#180353,#180354,#180355,#180356,#180357,#180358,#180359,
#180360,#180361,#180362,#180363,#180364,#180365,#180366,#180367,#180368,
#180369,#180370,#180371,#180372,#180373,#180374,#180375,#180376,#180377,
#180378,#180379,#180380,#180381,#180382,#180383,#180384,#180385,#180386,
#180387,#180388,#180389,#180390,#180391,#180392,#180393,#180394,#180395,
#180396,#180397,#180398,#180399,#180400,#180401,#180402,#180403,#180404,
#180405,#180406,#180407,#180408,#180409,#180410,#180411,#180412,#180413,
#180414,#180415,#180416,#180417,#180418,#180419,#180420,#180421,#180422,
#180423,#180424,#180425,#180426,#180427,#180428,#180429,#180430,#180431,
#180432,#180433,#180434,#180435,#180436,#180437,#180438,#180439,#180440,
#180441,#180442,#180443,#180444,#180445,#180446,#180447,#180448),
 .UNSPECIFIED.,.F.,.F.,(4,3,3,3,3,3,3,3,3,3,3,3,3,3,3,3,3,3,3,3,3,3,3,3,
3,3,3,3,3,3,3,3,3,3,3,3,3,3,3,3,3,3,3,3,3,3,3,3,3,3,3,3,3,3,3,3,3,3,3,3,
3,3,3,3,3,3,3,3,3,3,3,3,3,3,3,3,3,3,3,3,3,3,4),(-538.163292664416,-538.067833579261,
-537.971624657692,-537.874613587217,-537.85797376743,-537.778016467299,
-537.698153670057,-537.618367847586,-537.538641532391,-537.458957304097,
-537.379286317877,-537.299618864351,-537.219939213535,-537.140231631141,
-537.060436402066,-536.980592060359,-536.900633633312,-536.85823775671,
-536.778280456579,-536.698417659336,-536.618631836864,-536.538905521669,
-536.459221293375,-536.379550307154,-536.299882853628,-536.220203202811,
-536.140495620417,-536.060700391342,-535.980856049634,-535.900897622587,
-535.85850174599,-535.778544445859,-535.698681648616,-535.618895826144,
-535.539169510949,-535.459485282654,-535.379814296433,-535.300146842907,
-535.220467192091,-535.140759609696,-535.060964380621,-534.981120038913,
-534.901161611866,-534.85876573527,-534.778808435139,-534.698945637896,
-534.619159815425,-534.539433500229,-534.459749271935,-534.380078285714,
-534.300410832189,-534.220731181372,-534.141023598978,-534.061228369902,
-533.981384028195,-533.901425601147,-533.85902972455,-533.779072424419,
-533.699209627176,-533.619423804704,-533.539697489509,-533.460013261215,
-533.380342274994,-533.300674821468,-533.220995170652,-533.141287588257,
-533.061492359181,-532.981648017474,-532.901689590426,-532.85929371383,
-532.779615619115,-532.700031870406,-532.62052467556,-532.541076305429,
-532.458455211241,-532.37906040542,-532.299667163717,-532.220259521228,
-532.140821507006,-532.061296040865,-531.981718807671,-531.90203376275,
-531.880107551926),.UNSPECIFIED.);
#1583=B_SPLINE_CURVE_WITH_KNOTS('',3,(#180450,#180451,#180452,#180453,#180454,
#180455,#180456,#180457,#180458,#180459,#180460,#180461),.UNSPECIFIED.,
 .F.,.F.,(4,2,1,1,1,1,1,1,4),(-531.880107551926,-531.85955770311,-530.85982169239,
-529.860085681669,-528.860349670949,-527.860613660229,-526.860877649509,
-525.861141638789,-525.596922244747),.UNSPECIFIED.);
#1584=B_SPLINE_CURVE_WITH_KNOTS('',3,(#180463,#180464,#180465,#180466,#180467,
#180468,#180469,#180470,#180471,#180472),.UNSPECIFIED.,.F.,.F.,(4,1,1,1,
1,1,1,4),(-525.596922244747,-524.861405628069,-523.861669617349,-522.861933606629,
-521.862197595908,-520.862461585188,-519.862725574468,-519.313736937567),
 .UNSPECIFIED.);
#1585=B_SPLINE_CURVE_WITH_KNOTS('',3,(#180474,#180475,#180476,#180477,#180478,
#180479,#180480,#180481,#180482,#180483),.UNSPECIFIED.,.F.,.F.,(4,1,1,1,
1,1,1,4),(-519.313736937567,-518.862989563748,-517.863253553028,-516.863517542308,
-515.863781531588,-514.864045520868,-513.864309510147,-513.030551630387),
 .UNSPECIFIED.);
#1586=B_SPLINE_CURVE_WITH_KNOTS('',3,(#180485,#180486,#180487,#180488,#180489,
#180490,#180491,#180492,#180493,#180494,#180495),.UNSPECIFIED.,.F.,.F.,
(4,1,1,1,1,1,1,1,4),(-513.030551630387,-512.864573499427,-511.864837488707,
-510.865101477987,-509.865365467267,-508.865629456547,-507.865893445827,
-506.866157435107,-506.747366323208),.UNSPECIFIED.);
#1587=B_SPLINE_CURVE_WITH_KNOTS('',3,(#180497,#180498,#180499,#180500,#180501,
#180502,#180503,#180504,#180505,#180506,#180507,#180508,#180509,#180510,
#180511,#180512,#180513,#180514,#180515,#180516,#180517,#180518,#180519,
#180520,#180521,#180522,#180523,#180524,#180525,#180526,#180527,#180528,
#180529,#180530,#180531,#180532,#180533,#180534,#180535,#180536,#180537,
#180538,#180539,#180540,#180541,#180542,#180543,#180544,#180545,#180546,
#180547,#180548,#180549,#180550,#180551,#180552,#180553,#180554,#180555,
#180556,#180557,#180558,#180559,#180560,#180561,#180562,#180563,#180564,
#180565,#180566,#180567,#180568,#180569,#180570,#180571,#180572,#180573,
#180574,#180575,#180576,#180577,#180578,#180579,#180580,#180581,#180582,
#180583,#180584,#180585,#180586,#180587,#180588,#180589,#180590,#180591,
#180592,#180593,#180594,#180595,#180596,#180597,#180598,#180599,#180600,
#180601,#180602,#180603,#180604,#180605,#180606,#180607,#180608,#180609,
#180610,#180611,#180612,#180613,#180614,#180615,#180616,#180617,#180618,
#180619,#180620,#180621,#180622,#180623,#180624,#180625,#180626,#180627,
#180628,#180629,#180630,#180631,#180632,#180633,#180634,#180635,#180636,
#180637,#180638,#180639,#180640,#180641,#180642,#180643,#180644,#180645,
#180646,#180647,#180648,#180649,#180650,#180651,#180652,#180653,#180654,
#180655,#180656,#180657,#180658,#180659,#180660,#180661,#180662,#180663,
#180664,#180665,#180666,#180667,#180668,#180669,#180670,#180671,#180672,
#180673,#180674,#180675,#180676,#180677,#180678,#180679,#180680,#180681,
#180682,#180683,#180684,#180685,#180686,#180687,#180688,#180689,#180690,
#180691,#180692,#180693,#180694,#180695,#180696,#180697,#180698,#180699,
#180700,#180701,#180702,#180703,#180704,#180705,#180706,#180707,#180708,
#180709,#180710,#180711,#180712,#180713,#180714,#180715,#180716,#180717,
#180718,#180719,#180720,#180721,#180722,#180723,#180724,#180725,#180726,
#180727,#180728,#180729,#180730,#180731,#180732,#180733,#180734,#180735,
#180736,#180737,#180738,#180739,#180740,#180741,#180742,#180743),
 .UNSPECIFIED.,.F.,.F.,(4,3,3,3,3,3,3,3,3,3,3,3,3,3,3,3,3,3,3,3,3,3,3,3,
3,3,3,3,3,3,3,3,3,3,3,3,3,3,3,3,3,3,3,3,3,3,3,3,3,3,3,3,3,3,3,3,3,3,3,3,
3,3,3,3,3,3,3,3,3,3,3,3,3,3,3,3,3,3,3,3,3,3,4),(-506.747366323208,-506.668565269127,
-506.589845799829,-506.511189544419,-506.430593529415,-506.351998912421,
-506.273408403512,-506.194805489864,-506.112709473494,-506.033990720535,
-505.955219812063,-505.876345448082,-505.866421424386,-505.786464124255,
-505.706601327012,-505.62681550454,-505.547089189345,-505.467404961051,
-505.38773397483,-505.308066521304,-505.228386870488,-505.148679288093,
-505.068884059018,-504.98903971731,-504.909081290263,-504.866685413666,
-504.786728113535,-504.706865316292,-504.627079493821,-504.547353178625,
-504.467668950331,-504.38799796411,-504.308330510585,-504.228650859768,
-504.148943277374,-504.069148048298,-503.989303706591,-503.909345279544,
-503.866949402946,-503.786992102815,-503.707129305572,-503.6273434831,-503.547617167905,
-503.467932939611,-503.38826195339,-503.308594499864,-503.228914849047,
-503.149207266652,-503.069412037577,-502.989567695869,-502.909609268821,
-502.867213392226,-502.787256092095,-502.707393294852,-502.627607472381,
-502.547881157185,-502.468196928891,-502.38852594267,-502.308858489144,
-502.229178838328,-502.149471255933,-502.069676026858,-501.98983168515,
-501.909873258103,-501.867477381506,-501.787520081375,-501.707657284132,
-501.62787146166,-501.548145146465,-501.468460918171,-501.38878993195,-501.309122478424,
-501.229442827608,-501.149735245214,-501.069940016139,-500.990095674431,
-500.910137247384,-500.867741370786,-500.77896803224,-500.6905538493,-500.602371739187,
-500.51456865474,-500.464181236766),.UNSPECIFIED.);
#1588=B_SPLINE_CURVE_WITH_KNOTS('',3,(#180745,#180746,#180747,#180748,#180749,
#180750,#180751,#180752,#180753,#180754),.UNSPECIFIED.,.F.,.F.,(4,1,1,1,
1,1,1,4),(-500.464181016028,-499.868005360066,-498.868269349345,-497.868533338625,
-496.868797327905,-495.869061317185,-494.869325306465,-494.180995708849),
 .UNSPECIFIED.);
#1589=B_SPLINE_CURVE_WITH_KNOTS('',3,(#180756,#180757,#180758,#180759,#180760,
#180761,#180762,#180763,#180764,#180765,#180766,#180767,#180768,#180769,
#180770,#180771,#180772,#180773,#180774,#180775,#180776,#180777,#180778,
#180779,#180780,#180781,#180782,#180783,#180784,#180785,#180786,#180787,
#180788,#180789,#180790,#180791,#180792,#180793,#180794,#180795,#180796,
#180797,#180798,#180799,#180800,#180801,#180802,#180803,#180804,#180805,
#180806,#180807,#180808,#180809,#180810,#180811,#180812,#180813,#180814,
#180815,#180816,#180817,#180818,#180819,#180820,#180821,#180822,#180823,
#180824,#180825,#180826,#180827,#180828,#180829,#180830,#180831,#180832,
#180833,#180834,#180835,#180836,#180837,#180838,#180839,#180840,#180841,
#180842,#180843,#180844,#180845,#180846,#180847,#180848,#180849,#180850,
#180851,#180852,#180853,#180854,#180855,#180856,#180857,#180858,#180859,
#180860,#180861,#180862,#180863,#180864,#180865,#180866,#180867,#180868,
#180869,#180870,#180871,#180872,#180873,#180874,#180875,#180876,#180877,
#180878,#180879,#180880,#180881,#180882,#180883,#180884,#180885,#180886,
#180887,#180888,#180889,#180890,#180891,#180892,#180893,#180894,#180895,
#180896,#180897,#180898,#180899,#180900,#180901,#180902,#180903,#180904,
#180905,#180906,#180907,#180908,#180909,#180910,#180911,#180912,#180913,
#180914,#180915,#180916,#180917,#180918,#180919,#180920,#180921,#180922,
#180923,#180924,#180925,#180926,#180927,#180928,#180929,#180930,#180931,
#180932,#180933,#180934,#180935,#180936,#180937,#180938,#180939,#180940,
#180941,#180942,#180943,#180944,#180945,#180946,#180947,#180948,#180949,
#180950,#180951,#180952,#180953,#180954,#180955,#180956,#180957,#180958,
#180959,#180960,#180961,#180962,#180963,#180964,#180965,#180966,#180967,
#180968,#180969,#180970,#180971,#180972,#180973,#180974,#180975,#180976,
#180977,#180978,#180979,#180980,#180981,#180982,#180983,#180984,#180985,
#180986,#180987,#180988,#180989,#180990,#180991,#180992,#180993,#180994,
#180995,#180996,#180997,#180998,#180999,#181000,#181001,#181002),
 .UNSPECIFIED.,.F.,.F.,(4,3,3,3,3,3,3,3,3,3,3,3,3,3,3,3,3,3,3,3,3,3,3,3,
3,3,3,3,3,3,3,3,3,3,3,3,3,3,3,3,3,3,3,3,3,3,3,3,3,3,3,3,3,3,3,3,3,3,3,3,
3,3,3,3,3,3,3,3,3,3,3,3,3,3,3,3,3,3,3,3,3,3,4),(-494.180995503453,-494.086145198552,
-493.990601361686,-493.894293100197,-493.869589295745,-493.789631995614,
-493.709769198372,-493.6299833759,-493.550257060705,-493.470572832411,-493.390901846191,
-493.311234392665,-493.231554741849,-493.151847159454,-493.072051930379,
-492.992207588672,-492.912249161625,-492.869853285025,-492.789895984894,
-492.710033187651,-492.63024736518,-492.550521049984,-492.470836821691,
-492.39116583547,-492.311498381944,-492.231818731127,-492.152111148733,
-492.072315919658,-491.99247157795,-491.912513150903,-491.870117274305,
-491.790159974173,-491.710297176931,-491.630511354459,-491.550785039263,
-491.471100810969,-491.391429824747,-491.311762371221,-491.232082720404,
-491.15237513801,-491.072579908934,-490.992735567226,-490.912777140178,
-490.870381263584,-490.790423963453,-490.71056116621,-490.630775343738,
-490.551049028543,-490.471364800249,-490.391693814028,-490.312026360502,
-490.232346709686,-490.152639127291,-490.072843898216,-489.992999556508,
-489.913041129461,-489.870645252864,-489.790687952733,-489.71082515549,
-489.631039333019,-489.551313017823,-489.471628789529,-489.391957803309,
-489.312290349783,-489.232610698966,-489.152903116572,-489.073107887497,
-488.993263545789,-488.913305118742,-488.870909242144,-488.791306292984,
-488.711797637287,-488.632365416433,-488.552991835624,-488.471094156379,
-488.391773525049,-488.312454249021,-488.233120304614,-488.153755661784,
-488.074303920618,-487.994799997186,-487.915189864538,-487.897810401669),
 .UNSPECIFIED.);
#1590=B_SPLINE_CURVE_WITH_KNOTS('',3,(#181004,#181005,#181006,#181007,#181008,
#181009,#181010,#181011,#181012,#181013,#181014,#181015),.UNSPECIFIED.,
 .F.,.F.,(4,2,1,1,1,1,1,1,4),(-487.897810401669,-487.871173231424,-486.871437220704,
-485.871701209984,-484.871965199264,-483.872229188543,-482.872493177823,
-481.872757167103,-481.61462509449),.UNSPECIFIED.);
#1591=B_SPLINE_CURVE_WITH_KNOTS('',3,(#181017,#181018,#181019,#181020,#181021,
#181022,#181023,#181024,#181025,#181026),.UNSPECIFIED.,.F.,.F.,(4,1,1,1,
1,1,1,4),(-481.61462509449,-480.873021156383,-479.873285145663,-478.873549134943,
-477.873813124223,-476.874077113502,-475.874341102782,-475.33143978731),
 .UNSPECIFIED.);
#1592=B_SPLINE_CURVE_WITH_KNOTS('',3,(#181028,#181029,#181030,#181031,#181032,
#181033,#181034,#181035,#181036,#181037,#181038,#181039,#181040,#181041,
#181042,#181043,#181044,#181045,#181046,#181047,#181048,#181049,#181050,
#181051,#181052,#181053,#181054,#181055,#181056,#181057,#181058,#181059,
#181060,#181061,#181062,#181063,#181064,#181065,#181066,#181067,#181068,
#181069,#181070,#181071,#181072,#181073,#181074,#181075,#181076,#181077,
#181078,#181079,#181080,#181081,#181082,#181083,#181084,#181085,#181086,
#181087,#181088,#181089,#181090,#181091,#181092,#181093,#181094,#181095,
#181096,#181097,#181098,#181099,#181100,#181101,#181102,#181103,#181104,
#181105,#181106,#181107,#181108,#181109,#181110,#181111,#181112,#181113,
#181114,#181115,#181116,#181117,#181118,#181119,#181120,#181121,#181122,
#181123,#181124,#181125,#181126,#181127,#181128,#181129,#181130,#181131,
#181132,#181133,#181134,#181135,#181136,#181137,#181138,#181139,#181140,
#181141,#181142,#181143,#181144,#181145,#181146,#181147,#181148,#181149,
#181150,#181151,#181152,#181153,#181154,#181155,#181156,#181157,#181158,
#181159,#181160,#181161,#181162,#181163,#181164,#181165,#181166,#181167,
#181168,#181169,#181170,#181171,#181172,#181173,#181174,#181175,#181176,
#181177,#181178,#181179,#181180,#181181,#181182,#181183,#181184,#181185,
#181186,#181187,#181188,#181189,#181190,#181191,#181192,#181193,#181194,
#181195,#181196,#181197,#181198,#181199,#181200,#181201,#181202,#181203,
#181204,#181205,#181206,#181207,#181208,#181209,#181210,#181211,#181212,
#181213,#181214,#181215,#181216,#181217,#181218,#181219,#181220,#181221,
#181222,#181223,#181224,#181225,#181226,#181227,#181228,#181229,#181230,
#181231,#181232,#181233,#181234,#181235,#181236,#181237,#181238,#181239,
#181240,#181241,#181242,#181243,#181244,#181245,#181246,#181247,#181248,
#181249,#181250,#181251,#181252,#181253,#181254,#181255,#181256,#181257,
#181258,#181259,#181260,#181261,#181262,#181263,#181264,#181265,#181266,
#181267,#181268,#181269,#181270,#181271,#181272,#181273,#181274),
 .UNSPECIFIED.,.F.,.F.,(4,3,3,3,3,3,3,3,3,3,3,3,3,3,3,3,3,3,3,3,3,3,3,3,
3,3,3,3,3,3,3,3,3,3,3,3,3,3,3,3,3,3,3,3,3,3,3,3,3,3,3,3,3,3,3,3,3,3,3,3,
3,3,3,3,3,3,3,3,3,3,3,3,3,3,3,3,3,3,3,3,3,3,4),(-475.331439554867,-475.246323996886,
-475.161039435295,-475.075497894197,-474.989817249859,-474.903927795396,
-474.874605092062,-474.794647791931,-474.714784994688,-474.634999172216,
-474.555272857021,-474.475588628726,-474.395917642505,-474.316250188979,
-474.236570538163,-474.156862955768,-474.077067726693,-473.997223384985,
-473.917264957938,-473.874869081342,-473.794911781211,-473.715048983968,
-473.635263161496,-473.555536846301,-473.475852618007,-473.396181631786,
-473.31651417826,-473.236834527444,-473.157126945049,-473.077331715973,
-472.997487374266,-472.917528947218,-472.875133070622,-472.795175770491,
-472.715312973248,-472.635527150776,-472.555800835581,-472.476116607287,
-472.396445621066,-472.31677816754,-472.237098516724,-472.157390934329,
-472.077595705254,-471.997751363546,-471.917792936499,-471.875397059902,
-471.795439759771,-471.715576962528,-471.635791140056,-471.556064824861,
-471.476380596567,-471.396709610346,-471.31704215682,-471.237362506004,
-471.157654923609,-471.077859694534,-470.998015352826,-470.918056925779,
-470.875661049182,-470.795703749051,-470.715840951808,-470.636055129337,
-470.556328814141,-470.476644585847,-470.396973599626,-470.317306146101,
-470.237626495284,-470.15791891289,-470.078123683814,-469.998279342107,
-469.918320915059,-469.875925038462,-469.797161483017,-469.718492017867,
-469.639898148453,-469.561365072808,-469.482864722549,-469.404380512817,
-469.325895873312,-469.247362635622,-469.168802557328,-469.090159966002,
-469.04825448013),.UNSPECIFIED.);
#1593=B_SPLINE_CURVE_WITH_KNOTS('',3,(#181276,#181277,#181278,#181279,#181280,
#181281,#181282,#181283,#181284,#181285,#181286),.UNSPECIFIED.,.F.,.F.,
(4,1,1,1,1,1,1,1,4),(-469.04825448013,-468.876189027742,-467.876453017021,
-466.876717006301,-465.876980995581,-464.877244984861,-463.877508974141,
-462.877772963421,-462.765069172951),.UNSPECIFIED.);
#1594=B_SPLINE_CURVE_WITH_KNOTS('',3,(#181288,#181289,#181290,#181291,#181292,
#181293,#181294,#181295,#181296,#181297),.UNSPECIFIED.,.F.,.F.,(4,1,1,1,
1,1,1,4),(-462.765069172951,-461.878036952701,-460.87830094198,-459.87856493126,
-458.87882892054,-457.87909290982,-456.8793568991,-456.481883865771),
 .UNSPECIFIED.);
#1595=B_SPLINE_CURVE_WITH_KNOTS('',3,(#181299,#181300,#181301,#181302,#181303,
#181304,#181305,#181306,#181307,#181308),.UNSPECIFIED.,.F.,.F.,(4,1,1,1,
1,1,1,4),(-456.481883865771,-455.87962088838,-454.87988487766,-453.88014886694,
-452.880412856219,-451.880676845499,-450.880940834779,-450.198698558592),
 .UNSPECIFIED.);
#1596=B_SPLINE_CURVE_WITH_KNOTS('',3,(#181310,#181311,#181312,#181313,#181314,
#181315,#181316,#181317,#181318,#181319),.UNSPECIFIED.,.F.,.F.,(4,1,1,1,
1,1,1,4),(-450.198698558592,-449.881204824059,-448.881468813339,-447.881732802619,
-446.881996791899,-445.882260781179,-444.882524770458,-443.915517737304),
 .UNSPECIFIED.);
#1597=B_SPLINE_CURVE_WITH_KNOTS('',3,(#181321,#181322,#181323,#181324,#181325,
#181326,#181327,#181328,#181329,#181330,#181331,#181332,#181333,#181334,
#181335,#181336,#181337,#181338,#181339,#181340,#181341,#181342,#181343,
#181344,#181345,#181346,#181347,#181348,#181349,#181350,#181351,#181352,
#181353,#181354,#181355,#181356,#181357,#181358,#181359,#181360,#181361,
#181362,#181363,#181364,#181365,#181366,#181367,#181368,#181369,#181370,
#181371,#181372,#181373,#181374,#181375,#181376,#181377,#181378,#181379,
#181380,#181381,#181382,#181383,#181384,#181385,#181386,#181387,#181388,
#181389,#181390,#181391,#181392,#181393,#181394,#181395,#181396,#181397,
#181398,#181399,#181400,#181401,#181402,#181403,#181404,#181405,#181406,
#181407,#181408,#181409,#181410,#181411,#181412,#181413,#181414,#181415,
#181416,#181417,#181418,#181419,#181420,#181421,#181422,#181423,#181424,
#181425,#181426,#181427,#181428,#181429,#181430,#181431,#181432,#181433,
#181434,#181435,#181436,#181437,#181438,#181439,#181440,#181441,#181442,
#181443,#181444,#181445,#181446,#181447,#181448,#181449,#181450,#181451,
#181452,#181453,#181454,#181455,#181456,#181457,#181458,#181459,#181460,
#181461,#181462,#181463,#181464,#181465,#181466,#181467,#181468,#181469,
#181470,#181471,#181472,#181473,#181474,#181475,#181476,#181477,#181478,
#181479,#181480,#181481,#181482,#181483,#181484,#181485,#181486,#181487,
#181488,#181489,#181490,#181491,#181492,#181493,#181494,#181495,#181496,
#181497,#181498,#181499,#181500,#181501,#181502,#181503,#181504,#181505,
#181506,#181507,#181508,#181509,#181510,#181511,#181512,#181513,#181514,
#181515,#181516,#181517,#181518,#181519,#181520,#181521,#181522,#181523,
#181524,#181525,#181526,#181527,#181528,#181529,#181530,#181531,#181532,
#181533,#181534,#181535,#181536,#181537,#181538,#181539,#181540,#181541,
#181542,#181543,#181544,#181545,#181546,#181547,#181548,#181549,#181550,
#181551,#181552,#181553,#181554,#181555,#181556,#181557,#181558,#181559,
#181560,#181561,#181562,#181563,#181564,#181565,#181566,#181567),
 .UNSPECIFIED.,.F.,.F.,(4,3,3,3,3,3,3,3,3,3,3,3,3,3,3,3,3,3,3,3,3,3,3,3,
3,3,3,3,3,3,3,3,3,3,3,3,3,3,3,3,3,3,3,3,3,3,3,3,3,3,3,3,3,3,3,3,3,3,3,3,
3,3,3,3,3,3,3,3,3,3,3,3,3,3,3,3,3,3,3,3,3,3,4),(-443.915513251412,-443.882788759738,
-443.802831459607,-443.722968662364,-443.643182839892,-443.563456524697,
-443.483772296403,-443.404101310182,-443.324433856656,-443.244754205839,
-443.165046623445,-443.085251394369,-443.005407052661,-442.925448625614,
-442.883052749018,-442.803095448887,-442.723232651644,-442.643446829172,
-442.563720513977,-442.484036285683,-442.404365299462,-442.324697845936,
-442.24501819512,-442.165310612725,-442.085515383649,-442.005671041942,
-441.925712614894,-441.883316738298,-441.803359438167,-441.723496640924,
-441.643710818452,-441.563984503257,-441.484300274963,-441.404629288742,
-441.324961835216,-441.2452821844,-441.165574602005,-441.08577937293,-441.005935031222,
-440.925976604175,-440.883580727578,-440.803623427447,-440.723760630204,
-440.643974807732,-440.564248492537,-440.484564264243,-440.404893278022,
-440.325225824496,-440.245546173679,-440.165838591285,-440.086043362209,
-440.006199020502,-439.926240593454,-439.883844716858,-439.803887416727,
-439.724024619484,-439.644238797013,-439.564512481817,-439.484828253523,
-439.405157267303,-439.325489813777,-439.24581016296,-439.166102580566,
-439.086307351491,-439.006463009783,-438.926504582736,-438.884108706138,
-438.804151406007,-438.724288608764,-438.644502786292,-438.564776471096,
-438.485092242802,-438.405421256581,-438.325753803055,-438.246074152238,
-438.166366569843,-438.086571340767,-438.00672699906,-437.926768572012,
-437.884372695417,-437.779892065321,-437.677571283294,-437.632328004849),
 .UNSPECIFIED.);
#1598=B_SPLINE_CURVE_WITH_KNOTS('',3,(#181569,#181570,#181571,#181572,#181573,
#181574,#181575,#181576,#181577,#181578),.UNSPECIFIED.,.F.,.F.,(4,1,1,1,
1,1,1,4),(-437.632327944233,-436.884636684697,-435.884900673977,-434.885164663257,
-433.885428652537,-432.885692641817,-431.885956631097,-431.349142637053),
 .UNSPECIFIED.);
#1599=B_SPLINE_CURVE_WITH_KNOTS('',3,(#181580,#181581,#181582,#181583,#181584,
#181585,#181586,#181587,#181588,#181589,#181590,#181591,#181592,#181593,
#181594,#181595,#181596,#181597,#181598,#181599,#181600,#181601,#181602,
#181603,#181604,#181605,#181606,#181607,#181608,#181609,#181610,#181611,
#181612,#181613,#181614,#181615,#181616,#181617,#181618,#181619,#181620,
#181621,#181622,#181623,#181624,#181625,#181626,#181627,#181628,#181629,
#181630,#181631,#181632,#181633,#181634,#181635,#181636,#181637,#181638,
#181639,#181640,#181641,#181642,#181643,#181644,#181645,#181646,#181647,
#181648,#181649,#181650,#181651,#181652,#181653,#181654,#181655,#181656,
#181657,#181658,#181659,#181660,#181661,#181662,#181663,#181664,#181665,
#181666,#181667,#181668,#181669,#181670,#181671,#181672,#181673,#181674,
#181675,#181676,#181677,#181678,#181679,#181680,#181681,#181682,#181683,
#181684,#181685,#181686,#181687,#181688,#181689,#181690,#181691,#181692,
#181693,#181694,#181695,#181696,#181697,#181698,#181699,#181700,#181701,
#181702,#181703,#181704,#181705,#181706,#181707,#181708,#181709,#181710,
#181711,#181712,#181713,#181714,#181715,#181716,#181717,#181718,#181719,
#181720,#181721,#181722,#181723,#181724,#181725,#181726,#181727,#181728,
#181729,#181730,#181731,#181732,#181733,#181734,#181735,#181736,#181737,
#181738,#181739,#181740,#181741,#181742,#181743,#181744,#181745,#181746,
#181747,#181748,#181749,#181750,#181751,#181752,#181753,#181754,#181755,
#181756,#181757,#181758,#181759,#181760,#181761,#181762,#181763,#181764,
#181765,#181766,#181767,#181768,#181769,#181770,#181771,#181772,#181773,
#181774,#181775,#181776,#181777,#181778,#181779,#181780,#181781,#181782,
#181783,#181784,#181785,#181786,#181787,#181788,#181789,#181790,#181791,
#181792,#181793,#181794,#181795,#181796,#181797,#181798,#181799,#181800,
#181801,#181802,#181803,#181804,#181805,#181806,#181807,#181808,#181809,
#181810,#181811,#181812,#181813,#181814,#181815,#181816,#181817,#181818,
#181819,#181820,#181821,#181822,#181823,#181824,#181825,#181826),
 .UNSPECIFIED.,.F.,.F.,(4,3,3,3,3,3,3,3,3,3,3,3,3,3,3,3,3,3,3,3,3,3,3,3,
3,3,3,3,3,3,3,3,3,3,3,3,3,3,3,3,3,3,3,3,3,3,3,3,3,3,3,3,3,3,3,3,3,3,3,3,
3,3,3,3,3,3,3,3,3,3,3,3,3,3,3,3,3,3,3,3,3,3,4),(-431.349142435417,-431.264283350958,
-431.179265992277,-431.094002032319,-431.008605479933,-430.923002336439,
-430.886220620377,-430.806263320245,-430.726400523002,-430.64661470053,
-430.566888385334,-430.48720415704,-430.407533170818,-430.327865717292,
-430.248186066475,-430.16847848408,-430.088683255004,-430.008838913296,
-429.928880486248,-429.886484609656,-429.806527309525,-429.726664512282,
-429.64687868981,-429.567152374615,-429.487468146321,-429.4077971601,-429.328129706574,
-429.248450055757,-429.168742473363,-429.088947244287,-429.00910290258,
-428.929144475532,-428.886748598936,-428.806791298805,-428.726928501562,
-428.647142679091,-428.567416363896,-428.487732135602,-428.408061149381,
-428.328393695855,-428.248714045039,-428.169006462644,-428.089211233569,
-428.009366891862,-427.929408464814,-427.887012588216,-427.807055288085,
-427.727192490842,-427.64740666837,-427.567680353175,-427.487996124881,
-427.40832513866,-427.328657685134,-427.248978034317,-427.169270451923,
-427.089475222847,-427.00963088114,-426.929672454092,-426.887276577496,
-426.807319277365,-426.727456480122,-426.64767065765,-426.567944342455,
-426.488260114161,-426.40858912794,-426.328921674414,-426.249242023598,
-426.169534441203,-426.089739212128,-426.009894870421,-425.929936443373,
-425.887540566776,-425.808773536607,-425.730100687268,-425.651503525719,
-425.572967473253,-425.494464274122,-425.41597734501,-425.337490117298,
-425.25895559468,-425.180394297064,-425.101753411262,-425.065957329874),
 .UNSPECIFIED.);
#1600=B_SPLINE_CURVE_WITH_KNOTS('',3,(#181828,#181829,#181830,#181831,#181832,
#181833,#181834,#181835,#181836,#181837,#181838),.UNSPECIFIED.,.F.,.F.,
(4,1,1,1,1,1,1,1,4),(-425.065957329874,-424.887804556056,-423.888068545336,
-422.888332534616,-421.888596523895,-420.888860513175,-419.889124502455,
-418.889388491735,-418.782772022694),.UNSPECIFIED.);
#1601=B_SPLINE_CURVE_WITH_KNOTS('',3,(#181840,#181841,#181842,#181843,#181844,
#181845,#181846,#181847,#181848,#181849),.UNSPECIFIED.,.F.,.F.,(4,1,1,1,
1,1,1,4),(-418.782772022694,-417.889652481015,-416.889916470295,-415.890180459574,
-414.890444448854,-413.890708438134,-412.890972427414,-412.499586715514),
 .UNSPECIFIED.);
#1602=B_SPLINE_CURVE_WITH_KNOTS('',3,(#181851,#181852,#181853,#181854,#181855,
#181856,#181857,#181858,#181859,#181860),.UNSPECIFIED.,.F.,.F.,(4,1,1,1,
1,1,1,4),(-412.499586715514,-411.891236416694,-410.891500405974,-409.891764395254,
-408.892028384534,-407.892292373813,-406.892556363093,-406.216401408335),
 .UNSPECIFIED.);
#1603=B_SPLINE_CURVE_WITH_KNOTS('',3,(#181862,#181863,#181864,#181865,#181866,
#181867,#181868,#181869,#181870,#181871),.UNSPECIFIED.,.F.,.F.,(4,1,1,1,
1,1,1,4),(-406.216401408335,-405.892820352373,-404.893084341653,-403.893348330933,
-402.893612320213,-401.893876309493,-400.894140298773,-399.933221433922),
 .UNSPECIFIED.);
#1604=B_SPLINE_CURVE_WITH_KNOTS('',3,(#181873,#181874,#181875,#181876,#181877,
#181878,#181879,#181880,#181881,#181882,#181883,#181884,#181885,#181886,
#181887,#181888,#181889,#181890,#181891,#181892,#181893,#181894,#181895,
#181896,#181897,#181898,#181899,#181900,#181901,#181902,#181903,#181904,
#181905,#181906,#181907,#181908,#181909,#181910,#181911,#181912,#181913,
#181914,#181915,#181916,#181917,#181918,#181919,#181920,#181921,#181922,
#181923,#181924,#181925,#181926,#181927,#181928,#181929,#181930,#181931,
#181932,#181933,#181934,#181935,#181936,#181937,#181938,#181939,#181940,
#181941,#181942,#181943,#181944,#181945,#181946,#181947,#181948,#181949,
#181950,#181951,#181952,#181953,#181954,#181955,#181956,#181957,#181958,
#181959,#181960,#181961,#181962,#181963,#181964,#181965,#181966,#181967,
#181968,#181969,#181970,#181971,#181972,#181973,#181974,#181975,#181976,
#181977,#181978,#181979,#181980,#181981,#181982,#181983,#181984,#181985,
#181986,#181987,#181988,#181989,#181990,#181991,#181992,#181993,#181994,
#181995,#181996,#181997,#181998,#181999,#182000,#182001,#182002,#182003,
#182004,#182005,#182006,#182007,#182008,#182009,#182010,#182011,#182012,
#182013,#182014,#182015,#182016,#182017,#182018,#182019,#182020,#182021,
#182022,#182023,#182024,#182025,#182026,#182027,#182028,#182029,#182030,
#182031,#182032,#182033,#182034,#182035,#182036,#182037,#182038,#182039,
#182040,#182041,#182042,#182043,#182044,#182045,#182046,#182047,#182048,
#182049,#182050,#182051,#182052,#182053,#182054,#182055,#182056,#182057,
#182058,#182059,#182060,#182061,#182062,#182063,#182064,#182065,#182066,
#182067,#182068,#182069,#182070,#182071,#182072,#182073,#182074,#182075,
#182076,#182077,#182078,#182079,#182080,#182081,#182082,#182083,#182084,
#182085,#182086,#182087,#182088,#182089,#182090,#182091,#182092,#182093,
#182094,#182095,#182096,#182097,#182098,#182099,#182100,#182101,#182102,
#182103,#182104,#182105,#182106,#182107,#182108,#182109,#182110,#182111,
#182112,#182113,#182114,#182115,#182116,#182117,#182118,#182119),
 .UNSPECIFIED.,.F.,.F.,(4,3,3,3,3,3,3,3,3,3,3,3,3,3,3,3,3,3,3,3,3,3,3,3,
3,3,3,3,3,3,3,3,3,3,3,3,3,3,3,3,3,3,3,3,3,3,3,3,3,3,3,3,3,3,3,3,3,3,3,3,
3,3,3,3,3,3,3,3,3,3,3,3,3,3,3,3,3,3,3,3,3,3,4),(-399.933216101155,-399.894404288052,
-399.814446987921,-399.734584190678,-399.654798368206,-399.575072053011,
-399.495387824717,-399.415716838496,-399.33604938497,-399.256369734153,
-399.176662151759,-399.096866922683,-399.017022580976,-398.937064153929,
-398.894668277332,-398.814710977201,-398.734848179958,-398.655062357486,
-398.575336042291,-398.495651813997,-398.415980827776,-398.33631337425,
-398.256633723433,-398.176926141039,-398.097130911963,-398.017286570256,
-397.937328143208,-397.894932266612,-397.814974966481,-397.735112169238,
-397.655326346766,-397.575600031571,-397.495915803277,-397.416244817056,
-397.33657736353,-397.256897712713,-397.177190130319,-397.097394901243,
-397.017550559535,-396.937592132488,-396.895196255892,-396.815238955761,
-396.735376158518,-396.655590336046,-396.575864020851,-396.496179792557,
-396.416508806336,-396.33684135281,-396.257161701994,-396.177454119599,
-396.097658890524,-396.017814548816,-395.937856121769,-395.895460245172,
-395.815502945041,-395.735640147798,-395.655854325326,-395.576128010131,
-395.496443781837,-395.416772795616,-395.33710534209,-395.257425691274,
-395.177718108879,-395.097922879804,-395.018078538096,-394.938120111049,
-394.895724234452,-394.815766934321,-394.735904137078,-394.656118314606,
-394.576391999411,-394.496707771117,-394.417036784896,-394.33736933137,
-394.257689680554,-394.177982098159,-394.098186869083,-394.018342527376,
-393.938384100329,-393.895988223732,-393.790381676865,-393.68713925179,
-393.650030878059),.UNSPECIFIED.);
#1605=B_SPLINE_CURVE_WITH_KNOTS('',3,(#182121,#182122,#182123,#182124,#182125,
#182126,#182127,#182128,#182129,#182130),.UNSPECIFIED.,.F.,.F.,(4,1,1,1,
1,1,1,4),(-393.650030793976,-392.896252213012,-391.896516202291,-390.896780191571,
-389.897044180851,-388.897308170131,-387.897572159411,-387.366845486796),
 .UNSPECIFIED.);
#1606=B_SPLINE_CURVE_WITH_KNOTS('',3,(#182132,#182133,#182134,#182135,#182136,
#182137,#182138,#182139,#182140,#182141),.UNSPECIFIED.,.F.,.F.,(4,1,1,1,
1,1,1,4),(-387.366845486796,-386.897836148691,-385.898100137971,-384.89836412725,
-383.89862811653,-382.89889210581,-381.89915609509,-381.083664942812),
 .UNSPECIFIED.);
#1607=B_SPLINE_CURVE_WITH_KNOTS('',3,(#182143,#182144,#182145,#182146,#182147,
#182148,#182149,#182150,#182151,#182152,#182153,#182154,#182155,#182156,
#182157,#182158,#182159,#182160,#182161,#182162,#182163,#182164,#182165,
#182166,#182167,#182168,#182169,#182170,#182171,#182172,#182173,#182174,
#182175,#182176,#182177,#182178,#182179,#182180,#182181,#182182,#182183,
#182184,#182185,#182186,#182187,#182188,#182189,#182190,#182191,#182192,
#182193,#182194,#182195,#182196,#182197,#182198,#182199,#182200,#182201,
#182202,#182203,#182204,#182205,#182206,#182207,#182208,#182209,#182210,
#182211,#182212,#182213,#182214,#182215,#182216,#182217,#182218,#182219,
#182220,#182221,#182222,#182223,#182224,#182225,#182226,#182227,#182228,
#182229,#182230,#182231,#182232,#182233,#182234,#182235,#182236,#182237,
#182238,#182239,#182240,#182241,#182242,#182243,#182244,#182245,#182246,
#182247,#182248,#182249,#182250,#182251,#182252,#182253,#182254,#182255,
#182256,#182257,#182258,#182259,#182260,#182261,#182262,#182263,#182264,
#182265,#182266,#182267,#182268,#182269,#182270,#182271,#182272,#182273,
#182274,#182275,#182276,#182277,#182278,#182279,#182280,#182281,#182282,
#182283,#182284,#182285,#182286,#182287,#182288,#182289,#182290,#182291,
#182292,#182293,#182294,#182295,#182296,#182297,#182298,#182299,#182300,
#182301,#182302,#182303,#182304,#182305,#182306,#182307,#182308,#182309,
#182310,#182311,#182312,#182313,#182314,#182315,#182316,#182317,#182318,
#182319,#182320,#182321,#182322,#182323,#182324,#182325,#182326,#182327,
#182328,#182329,#182330,#182331,#182332,#182333,#182334,#182335,#182336,
#182337,#182338,#182339,#182340,#182341,#182342,#182343,#182344,#182345,
#182346,#182347,#182348,#182349,#182350,#182351,#182352,#182353,#182354,
#182355,#182356,#182357,#182358,#182359,#182360,#182361,#182362,#182363,
#182364,#182365,#182366,#182367,#182368,#182369,#182370,#182371,#182372,
#182373,#182374,#182375,#182376,#182377,#182378,#182379,#182380,#182381,
#182382,#182383,#182384,#182385,#182386),.UNSPECIFIED.,.F.,.F.,(4,3,3,3,
3,3,3,3,3,3,3,3,3,3,3,3,3,3,3,3,3,3,3,3,3,3,3,3,3,3,3,3,3,3,3,3,3,3,3,3,
3,3,3,3,3,3,3,3,3,3,3,3,3,3,3,3,3,3,3,3,3,3,3,3,3,3,3,3,3,3,3,3,3,3,3,3,
3,3,3,3,3,4),(-381.083660179617,-380.963780184145,-380.89942008437,-380.819462784239,
-380.739599986997,-380.659814164526,-380.580087849331,-380.500403621037,
-380.420732634817,-380.341065181291,-380.261385530475,-380.181677948081,
-380.101882719006,-380.022038377299,-379.942079950252,-379.89968407365,
-379.819726773519,-379.739863976276,-379.660078153804,-379.580351838609,
-379.500667610315,-379.420996624094,-379.341329170568,-379.261649519751,
-379.181941937356,-379.102146708281,-379.022302366573,-378.942343939526,
-378.89994806293,-378.819990762799,-378.740127965556,-378.660342143084,
-378.580615827889,-378.500931599595,-378.421260613374,-378.341593159848,
-378.261913509032,-378.182205926637,-378.102410697561,-378.022566355854,
-377.942607928807,-377.90021205221,-377.820254752079,-377.740391954836,
-377.660606132364,-377.580879817169,-377.501195588874,-377.421524602653,
-377.341857149127,-377.262177498311,-377.182469915916,-377.10267468684,
-377.022830345133,-376.942871918085,-376.900476041489,-376.820518741358,
-376.740655944115,-376.660870121643,-376.581143806448,-376.501459578154,
-376.421788591933,-376.342121138407,-376.26244148759,-376.182733905196,
-376.10293867612,-376.023094334413,-375.943135907365,-375.900740030769,
-375.820782730638,-375.740919933395,-375.661134110923,-375.581407795728,
-375.501723567434,-375.422052581213,-375.342385127687,-375.262705476871,
-375.182997894476,-375.103202665401,-375.023358323693,-374.943399896646,
-374.901004020049,-374.800474872437),.UNSPECIFIED.);
#1608=B_SPLINE_CURVE_WITH_KNOTS('',3,(#182388,#182389,#182390,#182391,#182392,
#182393,#182394,#182395,#182396,#182397),.UNSPECIFIED.,.F.,.F.,(4,1,1,1,
1,1,1,4),(-374.800465775823,-373.901268009329,-372.901531998609,-371.901795987889,
-370.902059977169,-369.902323966449,-368.902587955728,-368.517297017911),
 .UNSPECIFIED.);
#1609=B_SPLINE_CURVE_WITH_KNOTS('',3,(#182399,#182400,#182401,#182402,#182403,
#182404,#182405,#182406,#182407,#182408,#182409,#182410,#182411,#182412,
#182413,#182414,#182415,#182416,#182417,#182418,#182419,#182420,#182421,
#182422,#182423,#182424,#182425,#182426,#182427,#182428,#182429,#182430,
#182431,#182432,#182433,#182434,#182435,#182436,#182437,#182438,#182439,
#182440,#182441,#182442,#182443,#182444,#182445,#182446,#182447,#182448,
#182449,#182450,#182451,#182452,#182453,#182454,#182455,#182456,#182457,
#182458,#182459,#182460,#182461,#182462,#182463,#182464,#182465,#182466,
#182467,#182468,#182469,#182470,#182471,#182472,#182473,#182474,#182475,
#182476,#182477,#182478,#182479,#182480,#182481,#182482,#182483,#182484,
#182485,#182486,#182487,#182488,#182489,#182490,#182491,#182492,#182493,
#182494,#182495,#182496,#182497,#182498,#182499,#182500,#182501,#182502,
#182503,#182504,#182505,#182506,#182507,#182508,#182509,#182510,#182511,
#182512,#182513,#182514,#182515,#182516,#182517,#182518,#182519,#182520,
#182521,#182522,#182523,#182524,#182525,#182526,#182527,#182528,#182529,
#182530,#182531,#182532,#182533,#182534,#182535,#182536,#182537,#182538,
#182539,#182540,#182541,#182542,#182543,#182544,#182545,#182546,#182547,
#182548,#182549,#182550,#182551,#182552,#182553,#182554,#182555,#182556,
#182557,#182558,#182559,#182560,#182561,#182562,#182563,#182564,#182565,
#182566,#182567,#182568,#182569,#182570,#182571,#182572,#182573,#182574,
#182575,#182576,#182577,#182578,#182579,#182580,#182581,#182582,#182583,
#182584,#182585,#182586,#182587,#182588,#182589,#182590,#182591,#182592,
#182593,#182594,#182595,#182596,#182597,#182598,#182599,#182600,#182601,
#182602,#182603,#182604,#182605,#182606,#182607,#182608,#182609,#182610,
#182611,#182612,#182613,#182614,#182615,#182616,#182617,#182618,#182619,
#182620,#182621,#182622,#182623,#182624,#182625,#182626,#182627,#182628,
#182629,#182630,#182631,#182632,#182633,#182634,#182635,#182636,#182637,
#182638,#182639,#182640,#182641,#182642,#182643,#182644,#182645),
 .UNSPECIFIED.,.F.,.F.,(4,3,3,3,3,3,3,3,3,3,3,3,3,3,3,3,3,3,3,3,3,3,3,3,
3,3,3,3,3,3,3,3,3,3,3,3,3,3,3,3,3,3,3,3,3,3,3,3,3,3,3,3,3,3,3,3,3,3,3,3,
3,3,3,3,3,3,3,3,3,3,3,3,3,3,3,3,3,3,3,3,3,3,4),(-368.517289565257,-368.436832624477,
-368.356363949258,-368.275868850284,-368.195332625071,-368.114689806444,
-368.033988383624,-367.953156584468,-367.902851945008,-367.822894644877,
-367.743031847634,-367.663246025162,-367.583519709966,-367.503835481672,
-367.424164495451,-367.344497041925,-367.264817391109,-367.185109808714,
-367.105314579639,-367.025470237931,-366.945511810883,-366.903115934288,
-366.823158634157,-366.743295836914,-366.663510014442,-366.583783699247,
-366.504099470953,-366.424428484732,-366.344761031206,-366.26508138039,
-366.185373797995,-366.10557856892,-366.025734227212,-365.945775800164,
-365.903379923568,-365.823422623437,-365.743559826194,-365.663774003722,
-365.584047688527,-365.504363460234,-365.424692474013,-365.345025020487,
-365.26534536967,-365.185637787276,-365.1058425582,-365.025998216493,-364.946039789446,
-364.903643912848,-364.823686612717,-364.743823815474,-364.664037993002,
-364.584311677807,-364.504627449513,-364.424956463292,-364.345289009766,
-364.265609358949,-364.185901776555,-364.106106547479,-364.026262205772,
-363.946303778725,-363.903907902128,-363.823950601997,-363.744087804754,
-363.664301982283,-363.584575667088,-363.504891438794,-363.425220452573,
-363.345552999047,-363.265873348231,-363.186165765837,-363.106370536762,
-363.026526195054,-362.946567768006,-362.904171891408,-362.820413437242,
-362.740656700297,-362.660974998161,-362.581352461097,-362.501773259803,
-362.422214796349,-362.342668178147,-362.263103224232,-362.234104258078),
 .UNSPECIFIED.);
#1610=B_SPLINE_CURVE_WITH_KNOTS('',3,(#182647,#182648,#182649,#182650,#182651,
#182652,#182653,#182654,#182655,#182656),.UNSPECIFIED.,.F.,.F.,(4,1,1,1,
1,1,1,4),(-362.23409696627,-361.904435880687,-360.904699869967,-359.904963859247,
-358.905227848527,-357.905491837807,-356.905755827087,-355.950918950898),
 .UNSPECIFIED.);
#1611=B_SPLINE_CURVE_WITH_KNOTS('',3,(#182658,#182659,#182660,#182661,#182662,
#182663,#182664,#182665,#182666,#182667,#182668,#182669),.UNSPECIFIED.,
 .F.,.F.,(4,2,1,1,1,1,1,1,4),(-355.950918950898,-355.906019816367,-354.906283805647,
-353.906547794926,-352.906811784206,-351.907075773486,-350.907339762766,
-349.907603752046,-349.667733643719),.UNSPECIFIED.);
#1612=B_SPLINE_CURVE_WITH_KNOTS('',3,(#182671,#182672,#182673,#182674,#182675,
#182676,#182677,#182678,#182679,#182680),.UNSPECIFIED.,.F.,.F.,(4,1,1,1,
1,1,1,4),(-349.667733643719,-348.907867741326,-347.908131730606,-346.908395719885,
-345.908659709165,-344.908923698445,-343.909187687725,-343.384548336539),
 .UNSPECIFIED.);
#1613=B_SPLINE_CURVE_WITH_KNOTS('',3,(#182682,#182683,#182684,#182685,#182686,
#182687,#182688,#182689,#182690,#182691),.UNSPECIFIED.,.F.,.F.,(4,1,1,1,
1,1,1,4),(-343.384548336539,-342.909451677005,-341.909715666285,-340.909979655565,
-339.910243644845,-338.910507634124,-337.910771623404,-337.10136722921),
 .UNSPECIFIED.);
#1614=B_SPLINE_CURVE_WITH_KNOTS('',3,(#182693,#182694,#182695,#182696,#182697,
#182698,#182699,#182700,#182701,#182702,#182703,#182704,#182705,#182706,
#182707,#182708,#182709,#182710,#182711,#182712,#182713,#182714,#182715,
#182716,#182717,#182718,#182719,#182720,#182721,#182722,#182723,#182724,
#182725,#182726,#182727,#182728,#182729,#182730,#182731,#182732,#182733,
#182734,#182735,#182736,#182737,#182738,#182739,#182740,#182741,#182742,
#182743,#182744,#182745,#182746,#182747,#182748,#182749,#182750,#182751,
#182752,#182753,#182754,#182755,#182756,#182757,#182758,#182759,#182760,
#182761,#182762,#182763,#182764,#182765,#182766,#182767,#182768,#182769,
#182770,#182771,#182772,#182773,#182774,#182775,#182776,#182777,#182778,
#182779,#182780,#182781,#182782,#182783,#182784,#182785,#182786,#182787,
#182788,#182789,#182790,#182791,#182792,#182793,#182794,#182795,#182796,
#182797,#182798,#182799,#182800,#182801,#182802,#182803,#182804,#182805,
#182806,#182807,#182808,#182809,#182810,#182811,#182812,#182813,#182814,
#182815,#182816,#182817,#182818,#182819,#182820,#182821,#182822,#182823,
#182824,#182825,#182826,#182827,#182828,#182829,#182830,#182831,#182832,
#182833,#182834,#182835,#182836,#182837,#182838,#182839,#182840,#182841,
#182842,#182843,#182844,#182845,#182846,#182847,#182848,#182849,#182850,
#182851,#182852,#182853,#182854,#182855,#182856,#182857,#182858,#182859,
#182860,#182861,#182862,#182863,#182864,#182865,#182866,#182867,#182868,
#182869,#182870,#182871,#182872,#182873,#182874,#182875,#182876,#182877,
#182878,#182879,#182880,#182881,#182882,#182883,#182884,#182885,#182886,
#182887,#182888,#182889,#182890,#182891,#182892,#182893,#182894,#182895,
#182896,#182897,#182898,#182899,#182900,#182901,#182902,#182903,#182904,
#182905,#182906,#182907,#182908,#182909,#182910,#182911,#182912,#182913,
#182914,#182915,#182916,#182917,#182918,#182919,#182920,#182921,#182922,
#182923,#182924,#182925,#182926,#182927,#182928,#182929,#182930,#182931,
#182932,#182933,#182934,#182935,#182936),.UNSPECIFIED.,.F.,.F.,(4,3,3,3,
3,3,3,3,3,3,3,3,3,3,3,3,3,3,3,3,3,3,3,3,3,3,3,3,3,3,3,3,3,3,3,3,3,3,3,3,
3,3,3,3,3,3,3,3,3,3,3,3,3,3,3,3,3,3,3,3,3,3,3,3,3,3,3,3,3,3,3,3,3,3,3,3,
3,3,3,3,3,4),(-337.10136302936,-336.983585417605,-336.911035612684,-336.831078312553,
-336.751215515311,-336.67142969284,-336.591703377646,-336.512019149352,
-336.432348163132,-336.352680709607,-336.273001058791,-336.193293476397,
-336.113498247322,-336.033653905615,-335.953695478568,-335.911299601964,
-335.831342301833,-335.75147950459,-335.671693682118,-335.591967366923,
-335.512283138629,-335.432612152408,-335.352944698882,-335.273265048065,
-335.19355746567,-335.113762236595,-335.033917894887,-334.95395946784,-334.911563591244,
-334.831606291113,-334.75174349387,-334.671957671398,-334.592231356202,
-334.512547127908,-334.432876141687,-334.353208688161,-334.273529037344,
-334.19382145495,-334.114026225874,-334.034181884166,-333.954223457119,
-333.911827580524,-333.831870280393,-333.752007483151,-333.672221660679,
-333.592495345484,-333.51281111719,-333.433140130969,-333.353472677443,
-333.273793026627,-333.194085444233,-333.114290215158,-333.03444587345,
-332.954487446403,-332.912091569804,-332.832134269673,-332.75227147243,
-332.672485649958,-332.592759334762,-332.513075106468,-332.433404120247,
-332.35373666672,-332.274057015904,-332.194349433509,-332.114554204433,
-332.034709862725,-331.954751435678,-331.912355559083,-331.832398258952,
-331.752535461709,-331.672749639237,-331.593023324042,-331.513339095748,
-331.433668109527,-331.354000656001,-331.274321005184,-331.19461342279,
-331.114818193714,-331.034973852006,-330.955015424959,-330.912619548363,
-330.81817772218),.UNSPECIFIED.);
#1615=B_SPLINE_CURVE_WITH_KNOTS('',3,(#182938,#182939,#182940,#182941,#182942,
#182943,#182944,#182945,#182946,#182947),.UNSPECIFIED.,.F.,.F.,(4,1,1,1,
1,1,1,4),(-330.81816869401,-329.912883537643,-328.913147526923,-327.913411516203,
-326.913675505483,-325.913939494763,-324.914203484043,-324.534999992564),
 .UNSPECIFIED.);
#1616=B_SPLINE_CURVE_WITH_KNOTS('',3,(#182949,#182950,#182951,#182952,#182953,
#182954,#182955,#182956,#182957,#182958,#182959,#182960,#182961,#182962,
#182963,#182964,#182965,#182966,#182967,#182968,#182969,#182970,#182971,
#182972,#182973,#182974,#182975,#182976,#182977,#182978,#182979,#182980,
#182981,#182982,#182983,#182984,#182985,#182986,#182987,#182988,#182989,
#182990,#182991,#182992,#182993,#182994,#182995,#182996,#182997,#182998,
#182999,#183000,#183001,#183002,#183003,#183004,#183005,#183006,#183007,
#183008,#183009,#183010,#183011,#183012,#183013,#183014,#183015,#183016,
#183017,#183018,#183019,#183020,#183021,#183022,#183023,#183024,#183025,
#183026,#183027,#183028,#183029,#183030,#183031,#183032,#183033,#183034,
#183035,#183036,#183037,#183038,#183039,#183040,#183041,#183042,#183043,
#183044,#183045,#183046,#183047,#183048,#183049,#183050,#183051,#183052,
#183053,#183054,#183055,#183056,#183057,#183058,#183059,#183060,#183061,
#183062,#183063,#183064,#183065,#183066,#183067,#183068,#183069,#183070,
#183071,#183072,#183073,#183074,#183075,#183076,#183077,#183078,#183079,
#183080,#183081,#183082,#183083,#183084,#183085,#183086,#183087,#183088,
#183089,#183090,#183091,#183092,#183093,#183094,#183095,#183096,#183097,
#183098,#183099,#183100,#183101,#183102,#183103,#183104,#183105,#183106,
#183107,#183108,#183109,#183110,#183111,#183112,#183113,#183114,#183115,
#183116,#183117,#183118,#183119,#183120,#183121,#183122,#183123,#183124,
#183125,#183126,#183127,#183128,#183129,#183130,#183131,#183132,#183133,
#183134,#183135,#183136,#183137,#183138,#183139,#183140,#183141,#183142,
#183143,#183144,#183145,#183146,#183147,#183148,#183149,#183150,#183151,
#183152,#183153,#183154,#183155,#183156,#183157,#183158,#183159,#183160,
#183161,#183162,#183163,#183164,#183165,#183166,#183167,#183168,#183169,
#183170,#183171,#183172,#183173,#183174,#183175,#183176,#183177,#183178,
#183179,#183180,#183181,#183182,#183183,#183184,#183185,#183186,#183187,
#183188,#183189,#183190,#183191,#183192,#183193,#183194,#183195),
 .UNSPECIFIED.,.F.,.F.,(4,3,3,3,3,3,3,3,3,3,3,3,3,3,3,3,3,3,3,3,3,3,3,3,
3,3,3,3,3,3,3,3,3,3,3,3,3,3,3,3,3,3,3,3,3,3,3,3,3,3,3,3,3,3,3,3,3,3,3,3,
3,3,3,3,3,3,3,3,3,3,3,3,3,3,3,3,3,3,3,3,3,3,4),(-324.534992415001,-324.454648248748,
-324.374295562936,-324.293919507813,-324.213505222498,-324.132986702897,
-324.052411841748,-323.971705764006,-323.914467473322,-323.834510173191,
-323.754647375949,-323.674861553477,-323.595135238282,-323.515451009989,
-323.435780023768,-323.356112570243,-323.276432919427,-323.196725337033,
-323.116930107957,-323.03708576625,-322.957127339203,-322.914731462602,
-322.834774162471,-322.754911365228,-322.675125542756,-322.595399227561,
-322.515714999267,-322.436044013046,-322.35637655952,-322.276696908704,
-322.19698932631,-322.117194097234,-322.037349755527,-321.95739132848,-321.914995451882,
-321.835038151751,-321.755175354508,-321.675389532036,-321.595663216841,
-321.515978988548,-321.436308002326,-321.3566405488,-321.276960897984,-321.197253315588,
-321.117458086513,-321.037613744805,-320.957655317758,-320.915259441162,
-320.835302141031,-320.755439343788,-320.675653521317,-320.595927206121,
-320.516242977827,-320.436571991607,-320.356904538081,-320.277224887264,
-320.197517304869,-320.117722075794,-320.037877734087,-319.957919307039,
-319.915523430442,-319.835566130311,-319.755703333068,-319.675917510597,
-319.596191195401,-319.516506967108,-319.436835980887,-319.357168527361,
-319.277488876545,-319.197781294151,-319.117986065075,-319.038141723368,
-318.95818329632,-318.915787419722,-318.832789880734,-318.752943243527,
-318.67317260685,-318.593462181619,-318.513796219564,-318.434153364985,
-318.354523413875,-318.274878297269,-318.251807107821),.UNSPECIFIED.);
#1617=B_SPLINE_CURVE_WITH_KNOTS('',3,(#183197,#183198,#183199,#183200,#183201,
#183202,#183203,#183204,#183205,#183206),.UNSPECIFIED.,.F.,.F.,(4,1,1,1,
1,1,1,4),(-318.251799625932,-317.916051409002,-316.916315398281,-315.916579387561,
-314.916843376841,-313.917107366121,-312.917371355401,-311.968621800641),
 .UNSPECIFIED.);
#1618=B_SPLINE_CURVE_WITH_KNOTS('',3,(#183208,#183209,#183210,#183211,#183212,
#183213,#183214,#183215,#183216,#183217,#183218,#183219),.UNSPECIFIED.,
 .F.,.F.,(4,2,1,1,1,1,1,1,4),(-311.968621800641,-311.917635344681,-310.917899333961,
-309.918163323241,-308.918427312521,-307.9186913018,-306.91895529108,-305.91921928036,
-305.685436493462),.UNSPECIFIED.);
#1619=B_SPLINE_CURVE_WITH_KNOTS('',3,(#183221,#183222,#183223,#183224,#183225,
#183226,#183227,#183228,#183229,#183230),.UNSPECIFIED.,.F.,.F.,(4,1,1,1,
1,1,1,4),(-305.685436493462,-304.91948326964,-303.91974725892,-302.9200112482,
-301.92027523748,-300.920539226759,-299.920803216039,-299.402251186282),
 .UNSPECIFIED.);
#1620=B_SPLINE_CURVE_WITH_KNOTS('',3,(#183232,#183233,#183234,#183235,#183236,
#183237,#183238,#183239,#183240,#183241),.UNSPECIFIED.,.F.,.F.,(4,1,1,1,
1,1,1,4),(-299.402251186282,-298.921067205319,-297.921331194599,-296.921595183879,
-295.921859173159,-294.922123162439,-293.922387151719,-293.119069498281),
 .UNSPECIFIED.);
#1621=B_SPLINE_CURVE_WITH_KNOTS('',3,(#183243,#183244,#183245,#183246,#183247,
#183248,#183249,#183250,#183251,#183252,#183253,#183254,#183255,#183256,
#183257,#183258,#183259,#183260,#183261,#183262,#183263,#183264,#183265,
#183266,#183267,#183268,#183269,#183270,#183271,#183272,#183273,#183274,
#183275,#183276,#183277,#183278,#183279,#183280,#183281,#183282,#183283,
#183284,#183285,#183286,#183287,#183288,#183289,#183290,#183291,#183292,
#183293,#183294,#183295,#183296,#183297,#183298,#183299,#183300,#183301,
#183302,#183303,#183304,#183305,#183306,#183307,#183308,#183309,#183310,
#183311,#183312,#183313,#183314,#183315,#183316,#183317,#183318,#183319,
#183320,#183321,#183322,#183323,#183324,#183325,#183326,#183327,#183328,
#183329,#183330,#183331,#183332,#183333,#183334,#183335,#183336,#183337,
#183338,#183339,#183340,#183341,#183342,#183343,#183344,#183345,#183346,
#183347,#183348,#183349,#183350,#183351,#183352,#183353,#183354,#183355,
#183356,#183357,#183358,#183359,#183360,#183361,#183362,#183363,#183364,
#183365,#183366,#183367,#183368,#183369,#183370,#183371,#183372,#183373,
#183374,#183375,#183376,#183377,#183378,#183379,#183380,#183381,#183382,
#183383,#183384,#183385,#183386,#183387,#183388,#183389,#183390,#183391,
#183392,#183393,#183394,#183395,#183396,#183397,#183398,#183399,#183400,
#183401,#183402,#183403,#183404,#183405,#183406,#183407,#183408,#183409,
#183410,#183411,#183412,#183413,#183414,#183415,#183416,#183417,#183418,
#183419,#183420,#183421,#183422,#183423,#183424,#183425,#183426,#183427,
#183428,#183429,#183430,#183431,#183432,#183433,#183434,#183435,#183436,
#183437,#183438,#183439,#183440,#183441,#183442,#183443,#183444,#183445,
#183446,#183447,#183448,#183449,#183450,#183451,#183452,#183453,#183454,
#183455,#183456,#183457,#183458,#183459,#183460,#183461,#183462,#183463,
#183464,#183465,#183466,#183467,#183468,#183469,#183470,#183471,#183472,
#183473,#183474,#183475,#183476,#183477,#183478,#183479,#183480,#183481,
#183482,#183483,#183484,#183485,#183486),.UNSPECIFIED.,.F.,.F.,(4,3,3,3,
3,3,3,3,3,3,3,3,3,3,3,3,3,3,3,3,3,3,3,3,3,3,3,3,3,3,3,3,3,3,3,3,3,3,3,3,
3,3,3,3,3,3,3,3,3,3,3,3,3,3,3,3,3,3,3,3,3,3,3,3,3,3,3,3,3,3,3,3,3,3,3,3,
3,3,3,3,3,4),(-293.119065879103,-293.003224251817,-292.922651140998,-292.842693840867,
-292.762831043625,-292.683045221154,-292.603318905959,-292.523634677665,
-292.443963691445,-292.36429623792,-292.284616587104,-292.204909004709,
-292.125113775634,-292.045269433927,-291.965311006881,-291.922915130278,
-291.842957830147,-291.763095032904,-291.683309210432,-291.603582895237,
-291.523898666943,-291.444227680721,-291.364560227196,-291.284880576379,
-291.205172993984,-291.125377764909,-291.045533423201,-290.965574996154,
-290.923179119558,-290.843221819427,-290.763359022184,-290.683573199712,
-290.603846884517,-290.524162656223,-290.444491670002,-290.364824216476,
-290.285144565659,-290.205436983265,-290.125641754189,-290.045797412481,
-289.965838985434,-289.923443108838,-289.843485808707,-289.763623011464,
-289.683837188992,-289.604110873797,-289.524426645503,-289.444755659282,
-289.365088205756,-289.28540855494,-289.205700972545,-289.12590574347,-289.046061401762,
-288.966102974715,-288.923707098118,-288.843749797987,-288.763887000744,
-288.684101178272,-288.604374863077,-288.524690634783,-288.445019648562,
-288.365352195036,-288.28567254422,-288.205964961825,-288.12616973275,-288.046325391042,
-287.966366963995,-287.923971087398,-287.844013787267,-287.764150990024,
-287.684365167553,-287.604638852357,-287.524954624064,-287.445283637843,
-287.365616184317,-287.2859365335,-287.206228951106,-287.12643372203,-287.046589380323,
-286.966630953275,-286.924235076678,-286.835880571923),.UNSPECIFIED.);
#1622=B_SPLINE_CURVE_WITH_KNOTS('',3,(#183488,#183489,#183490,#183491,#183492,
#183493,#183494,#183495,#183496,#183497),.UNSPECIFIED.,.F.,.F.,(4,1,1,1,
1,1,1,4),(-286.835871811251,-285.924499065957,-284.924763055237,-283.925027044517,
-282.925291033797,-281.925555023077,-280.925819012357,-280.552702930068),
 .UNSPECIFIED.);
#1623=B_SPLINE_CURVE_WITH_KNOTS('',3,(#183499,#183500,#183501,#183502,#183503,
#183504,#183505,#183506,#183507,#183508,#183509,#183510,#183511,#183512,
#183513,#183514,#183515,#183516,#183517,#183518,#183519,#183520,#183521,
#183522,#183523,#183524,#183525,#183526,#183527,#183528,#183529,#183530,
#183531,#183532,#183533,#183534,#183535,#183536,#183537,#183538,#183539,
#183540,#183541,#183542,#183543,#183544,#183545,#183546,#183547,#183548,
#183549,#183550,#183551,#183552,#183553,#183554,#183555,#183556,#183557,
#183558,#183559,#183560,#183561,#183562,#183563,#183564,#183565,#183566,
#183567,#183568,#183569,#183570,#183571,#183572,#183573,#183574,#183575,
#183576,#183577,#183578,#183579,#183580,#183581,#183582,#183583,#183584,
#183585,#183586,#183587,#183588,#183589,#183590,#183591,#183592,#183593,
#183594,#183595,#183596,#183597,#183598,#183599,#183600,#183601,#183602,
#183603,#183604,#183605,#183606,#183607,#183608,#183609,#183610,#183611,
#183612,#183613,#183614,#183615,#183616,#183617,#183618,#183619,#183620,
#183621,#183622,#183623,#183624,#183625,#183626,#183627,#183628,#183629,
#183630,#183631,#183632,#183633,#183634,#183635,#183636,#183637,#183638,
#183639,#183640,#183641,#183642,#183643,#183644,#183645,#183646,#183647,
#183648,#183649,#183650,#183651,#183652,#183653,#183654,#183655,#183656,
#183657,#183658,#183659,#183660,#183661,#183662,#183663,#183664,#183665,
#183666,#183667,#183668,#183669,#183670,#183671,#183672,#183673,#183674,
#183675,#183676,#183677,#183678,#183679,#183680,#183681,#183682,#183683,
#183684,#183685,#183686,#183687,#183688,#183689,#183690,#183691,#183692,
#183693,#183694,#183695,#183696,#183697,#183698,#183699,#183700,#183701,
#183702,#183703,#183704,#183705,#183706,#183707,#183708,#183709,#183710,
#183711,#183712,#183713,#183714,#183715,#183716,#183717,#183718,#183719,
#183720,#183721,#183722,#183723,#183724,#183725,#183726,#183727,#183728,
#183729,#183730,#183731,#183732,#183733,#183734,#183735,#183736,#183737,
#183738,#183739,#183740,#183741,#183742,#183743,#183744,#183745),
 .UNSPECIFIED.,.F.,.F.,(4,3,3,3,3,3,3,3,3,3,3,3,3,3,3,3,3,3,3,3,3,3,3,3,
3,3,3,3,3,3,3,3,3,3,3,3,3,3,3,3,3,3,3,3,3,3,3,3,3,3,3,3,3,3,3,3,3,3,3,3,
3,3,3,3,3,3,3,3,3,3,3,3,3,3,3,3,3,3,3,3,3,3,4),(-280.552695264744,-280.472459775551,
-280.392218872353,-280.311957557339,-280.231660823479,-280.151262148967,
-280.070809345223,-279.990224439258,-279.926083001637,-279.846125701506,
-279.766262904263,-279.686477081792,-279.606750766596,-279.527066538302,
-279.447395552081,-279.367728098555,-279.288048447739,-279.208340865344,
-279.128545636268,-279.048701294561,-278.968742867514,-278.926346990917,
-278.846389690786,-278.766526893543,-278.686741071071,-278.607014755875,
-278.527330527581,-278.44765954136,-278.367992087833,-278.288312437017,
-278.208604854622,-278.128809625546,-278.048965283838,-277.969006856791,
-277.926610980196,-277.846653680065,-277.766790882822,-277.68700506035,
-277.607278745154,-277.52759451686,-277.447923530639,-277.368256077113,
-277.288576426296,-277.208868843902,-277.129073614826,-277.049229273118,
-276.96927084607,-276.926874969476,-276.846917669345,-276.767054872103,
-276.687269049631,-276.607542734435,-276.527858506141,-276.44818751992,
-276.368520066394,-276.288840415578,-276.209132833184,-276.129337604108,
-276.0494932624,-275.969534835353,-275.927138958756,-275.847181658625,-275.767318861382,
-275.68753303891,-275.607806723715,-275.528122495421,-275.4484515092,-275.368784055674,
-275.289104404858,-275.209396822464,-275.129601593388,-275.049757251681,
-274.969798824633,-274.927402948036,-274.845166324227,-274.765225966303,
-274.685362621073,-274.605560586828,-274.525804203116,-274.446073351479,
-274.366356525348,-274.286627668652,-274.269509957564),.UNSPECIFIED.);
#1624=B_SPLINE_CURVE_WITH_KNOTS('',3,(#183747,#183748,#183749,#183750,#183751,
#183752,#183753,#183754,#183755,#183756),.UNSPECIFIED.,.F.,.F.,(4,1,1,1,
1,1,1,4),(-274.269502324484,-273.927666937316,-272.927930926596,-271.928194915876,
-270.928458905156,-269.928722894435,-268.928986883715,-267.986324650384),
 .UNSPECIFIED.);
#1625=B_SPLINE_CURVE_WITH_KNOTS('',3,(#183758,#183759,#183760,#183761,#183762,
#183763,#183764,#183765,#183766,#183767,#183768,#183769),.UNSPECIFIED.,
 .F.,.F.,(4,2,1,1,1,1,1,1,4),(-267.986324650384,-267.929250872995,-266.929514862275,
-265.929778851555,-264.930042840835,-263.930306830115,-262.930570819394,
-261.930834808674,-261.703139343205),.UNSPECIFIED.);
#1626=B_SPLINE_CURVE_WITH_KNOTS('',3,(#183771,#183772,#183773,#183774,#183775,
#183776,#183777,#183778,#183779,#183780,#183781,#183782,#183783,#183784,
#183785,#183786,#183787,#183788,#183789,#183790,#183791,#183792,#183793,
#183794,#183795,#183796,#183797,#183798,#183799,#183800,#183801,#183802,
#183803,#183804,#183805,#183806,#183807,#183808,#183809,#183810,#183811,
#183812,#183813,#183814,#183815,#183816,#183817,#183818,#183819,#183820,
#183821,#183822,#183823,#183824,#183825,#183826,#183827,#183828,#183829,
#183830,#183831,#183832,#183833,#183834,#183835,#183836,#183837,#183838,
#183839,#183840,#183841,#183842,#183843,#183844,#183845,#183846,#183847,
#183848,#183849,#183850,#183851,#183852,#183853,#183854,#183855,#183856,
#183857,#183858,#183859,#183860,#183861,#183862,#183863,#183864,#183865,
#183866,#183867,#183868,#183869,#183870,#183871,#183872,#183873,#183874,
#183875,#183876,#183877,#183878,#183879,#183880,#183881,#183882,#183883,
#183884,#183885,#183886,#183887,#183888,#183889,#183890,#183891,#183892,
#183893,#183894,#183895,#183896,#183897,#183898,#183899,#183900,#183901,
#183902,#183903,#183904,#183905,#183906,#183907,#183908,#183909,#183910,
#183911,#183912,#183913,#183914,#183915,#183916,#183917,#183918,#183919,
#183920,#183921,#183922,#183923,#183924,#183925,#183926,#183927,#183928,
#183929,#183930,#183931,#183932,#183933,#183934,#183935,#183936,#183937,
#183938,#183939,#183940,#183941,#183942,#183943,#183944,#183945,#183946,
#183947,#183948,#183949,#183950,#183951,#183952,#183953,#183954,#183955,
#183956,#183957,#183958,#183959,#183960,#183961,#183962,#183963,#183964,
#183965,#183966,#183967,#183968,#183969,#183970,#183971,#183972,#183973,
#183974,#183975,#183976,#183977,#183978,#183979,#183980,#183981,#183982,
#183983,#183984,#183985,#183986,#183987,#183988,#183989,#183990,#183991,
#183992,#183993,#183994,#183995,#183996,#183997,#183998,#183999,#184000,
#184001,#184002,#184003,#184004,#184005,#184006,#184007,#184008,#184009,
#184010,#184011,#184012,#184013,#184014,#184015,#184016,#184017),
 .UNSPECIFIED.,.F.,.F.,(4,3,3,3,3,3,3,3,3,3,3,3,3,3,3,3,3,3,3,3,3,3,3,3,
3,3,3,3,3,3,3,3,3,3,3,3,3,3,3,3,3,3,3,3,3,3,3,3,3,3,3,3,3,3,3,3,3,3,3,3,
3,3,3,3,3,3,3,3,3,3,3,3,3,3,3,3,3,3,3,3,3,3,4),(-261.703139343205,-261.624409844129,
-261.545735960619,-261.467092226832,-261.388462724706,-261.309830963874,
-261.231180454103,-261.152449208019,-261.073675666579,-260.994784376284,
-260.931098797954,-260.851141497823,-260.77127870058,-260.691492878109,
-260.611766562913,-260.53208233462,-260.452411348399,-260.372743894873,
-260.293064244057,-260.213356661662,-260.133561432586,-260.053717090879,
-259.973758663832,-259.931362787234,-259.851405487103,-259.77154268986,
-259.691756867388,-259.612030552193,-259.532346323899,-259.452675337678,
-259.373007884152,-259.293328233336,-259.213620650942,-259.133825421866,
-259.053981080158,-258.974022653111,-258.931626776514,-258.851669476383,
-258.77180667914,-258.692020856668,-258.612294541473,-258.532610313179,
-258.452939326958,-258.373271873432,-258.293592222615,-258.213884640221,
-258.134089411145,-258.054245069438,-257.97428664239,-257.931890765794,
-257.851933465663,-257.77207066842,-257.692284845948,-257.612558530753,
-257.532874302459,-257.453203316238,-257.373535862713,-257.293856211896,
-257.214148629501,-257.134353400426,-257.054509058718,-256.974550631671,
-256.932154755074,-256.852197454943,-256.7723346577,-256.692548835229,-256.612822520034,
-256.533138291739,-256.453467305518,-256.373799851992,-256.294120201176,
-256.214412618781,-256.134617389706,-256.054773047998,-255.974814620951,
-255.932418744354,-255.848798920709,-255.765311214882,-255.678971920168,
-255.595763918918,-255.512648459724,-255.429641055154,-255.419954036025),
 .UNSPECIFIED.);
#1627=B_SPLINE_CURVE_WITH_KNOTS('',3,(#184019,#184020,#184021,#184022,#184023,
#184024,#184025,#184026,#184027,#184028,#184029,#184030,#184031,#184032,
#184033,#184034,#184035,#184036,#184037,#184038,#184039,#184040,#184041,
#184042,#184043,#184044,#184045,#184046,#184047,#184048,#184049,#184050,
#184051,#184052,#184053,#184054,#184055,#184056,#184057,#184058,#184059,
#184060,#184061,#184062,#184063,#184064,#184065,#184066,#184067,#184068,
#184069,#184070,#184071,#184072,#184073,#184074,#184075,#184076,#184077,
#184078,#184079,#184080,#184081,#184082,#184083,#184084,#184085,#184086,
#184087,#184088,#184089,#184090,#184091,#184092,#184093,#184094,#184095,
#184096,#184097,#184098,#184099,#184100,#184101,#184102,#184103,#184104,
#184105,#184106,#184107,#184108,#184109,#184110,#184111,#184112,#184113,
#184114,#184115,#184116,#184117,#184118,#184119,#184120,#184121,#184122,
#184123,#184124,#184125,#184126,#184127,#184128,#184129,#184130,#184131,
#184132,#184133,#184134,#184135,#184136,#184137,#184138,#184139,#184140,
#184141,#184142,#184143,#184144,#184145,#184146,#184147,#184148,#184149,
#184150,#184151,#184152,#184153,#184154,#184155,#184156,#184157,#184158,
#184159,#184160,#184161,#184162,#184163,#184164,#184165,#184166,#184167,
#184168,#184169,#184170,#184171,#184172,#184173,#184174,#184175,#184176,
#184177,#184178,#184179,#184180,#184181,#184182,#184183,#184184,#184185,
#184186,#184187,#184188,#184189,#184190,#184191,#184192,#184193,#184194,
#184195,#184196,#184197,#184198,#184199,#184200,#184201,#184202,#184203,
#184204,#184205,#184206,#184207,#184208,#184209,#184210,#184211,#184212,
#184213,#184214,#184215,#184216,#184217,#184218,#184219,#184220,#184221,
#184222,#184223,#184224,#184225,#184226,#184227,#184228,#184229,#184230,
#184231,#184232,#184233,#184234,#184235,#184236,#184237,#184238,#184239,
#184240,#184241,#184242,#184243,#184244,#184245,#184246,#184247,#184248,
#184249,#184250,#184251,#184252,#184253,#184254,#184255,#184256,#184257,
#184258,#184259,#184260,#184261,#184262),.UNSPECIFIED.,.F.,.F.,(4,3,3,3,
3,3,3,3,3,3,3,3,3,3,3,3,3,3,3,3,3,3,3,3,3,3,3,3,3,3,3,3,3,3,3,3,3,3,3,3,
3,3,3,3,3,3,3,3,3,3,3,3,3,3,3,3,3,3,3,3,3,3,3,3,3,3,3,3,3,3,3,3,3,3,3,3,
3,3,3,3,3,4),(-255.419954035887,-255.336047313209,-255.252019565011,-255.167781894743,
-255.083434975878,-254.99888936605,-254.932682733633,-254.852725433502,
-254.772862636259,-254.693076813787,-254.613350498592,-254.533666270298,
-254.453995284077,-254.374327830551,-254.294648179734,-254.21494059734,
-254.135145368264,-254.055301026557,-253.975342599509,-253.932946722913,
-253.852989422782,-253.773126625539,-253.693340803067,-253.613614487872,
-253.533930259578,-253.454259273357,-253.374591819831,-253.294912169015,
-253.21520458662,-253.135409357545,-253.055565015837,-252.97560658879,-252.933210712193,
-252.853253412062,-252.773390614819,-252.693604792347,-252.613878477152,
-252.534194248858,-252.454523262637,-252.374855809111,-252.295176158294,
-252.2154685759,-252.135673346824,-252.055829005117,-251.975870578069,-251.933474701473,
-251.853517401342,-251.773654604099,-251.693868781627,-251.614142466432,
-251.534458238138,-251.454787251917,-251.375119798391,-251.295440147575,
-251.21573256518,-251.135937336105,-251.056092994397,-250.97613456735,-250.933738690753,
-250.853781390622,-250.773918593379,-250.694132770907,-250.614406455712,
-250.534722227418,-250.455051241197,-250.375383787671,-250.295704136855,
-250.21599655446,-250.136201325385,-250.056356983677,-249.97639855663,-249.934002680033,
-249.855190850333,-249.776473692243,-249.696510571818,-249.617932915645,
-249.539388524333,-249.460860837844,-249.379837810594,-249.30126758998,
-249.219018159413,-249.136768728846),.UNSPECIFIED.);
#1628=B_SPLINE_CURVE_WITH_KNOTS('',3,(#184264,#184265,#184266,#184267,#184268,
#184269,#184270,#184271,#184272,#184273,#184274),.UNSPECIFIED.,.F.,.F.,
(4,1,1,1,1,1,1,1,4),(-249.136768728846,-248.934266669313,-247.934530658593,
-246.934794647872,-245.935058637152,-244.935322626432,-243.935586615712,
-242.935850604992,-242.853583421666),.UNSPECIFIED.);
#1629=B_SPLINE_CURVE_WITH_KNOTS('',3,(#184276,#184277,#184278,#184279,#184280,
#184281,#184282,#184283,#184284,#184285),.UNSPECIFIED.,.F.,.F.,(4,1,1,1,
1,1,1,4),(-242.853583421666,-241.936114594272,-240.936378583552,-239.936642572831,
-238.936906562111,-237.937170551391,-236.937434540671,-236.570398114487),
 .UNSPECIFIED.);
#1630=B_SPLINE_CURVE_WITH_KNOTS('',3,(#184287,#184288,#184289,#184290,#184291,
#184292,#184293,#184294,#184295,#184296),.UNSPECIFIED.,.F.,.F.,(4,1,1,1,
1,1,1,4),(-236.570398114487,-235.937698529951,-234.937962519231,-233.938226508511,
-232.938490497791,-231.93875448707,-230.93901847635,-230.287212807307),
 .UNSPECIFIED.);
#1631=B_SPLINE_CURVE_WITH_KNOTS('',3,(#184298,#184299,#184300,#184301,#184302,
#184303,#184304,#184305,#184306,#184307,#184308,#184309,#184310,#184311,
#184312,#184313,#184314,#184315,#184316,#184317,#184318,#184319,#184320,
#184321,#184322,#184323,#184324,#184325,#184326,#184327,#184328,#184329,
#184330,#184331,#184332,#184333,#184334,#184335,#184336,#184337,#184338,
#184339,#184340,#184341,#184342,#184343,#184344,#184345,#184346,#184347,
#184348,#184349,#184350,#184351,#184352,#184353,#184354,#184355,#184356,
#184357,#184358,#184359,#184360,#184361,#184362,#184363,#184364,#184365,
#184366,#184367,#184368,#184369,#184370,#184371,#184372,#184373,#184374,
#184375,#184376,#184377,#184378,#184379,#184380,#184381,#184382,#184383,
#184384,#184385,#184386,#184387,#184388,#184389,#184390,#184391,#184392,
#184393,#184394,#184395,#184396,#184397,#184398,#184399,#184400,#184401,
#184402,#184403,#184404,#184405,#184406,#184407,#184408,#184409,#184410,
#184411,#184412,#184413,#184414,#184415,#184416,#184417,#184418,#184419,
#184420,#184421,#184422,#184423,#184424,#184425,#184426,#184427,#184428,
#184429,#184430,#184431,#184432,#184433,#184434,#184435,#184436,#184437,
#184438,#184439,#184440,#184441,#184442,#184443,#184444,#184445,#184446,
#184447,#184448,#184449,#184450,#184451,#184452,#184453,#184454,#184455,
#184456,#184457,#184458,#184459,#184460,#184461,#184462,#184463,#184464,
#184465,#184466,#184467,#184468,#184469,#184470,#184471,#184472,#184473,
#184474,#184475,#184476,#184477,#184478,#184479,#184480,#184481,#184482,
#184483,#184484,#184485,#184486,#184487,#184488,#184489,#184490,#184491,
#184492,#184493,#184494,#184495,#184496,#184497,#184498,#184499,#184500,
#184501,#184502,#184503,#184504,#184505,#184506,#184507,#184508,#184509,
#184510,#184511,#184512,#184513,#184514,#184515,#184516,#184517,#184518,
#184519,#184520,#184521,#184522,#184523,#184524,#184525,#184526,#184527,
#184528,#184529,#184530,#184531,#184532,#184533,#184534,#184535,#184536,
#184537,#184538,#184539,#184540,#184541),.UNSPECIFIED.,.F.,.F.,(4,3,3,3,
3,3,3,3,3,3,3,3,3,3,3,3,3,3,3,3,3,3,3,3,3,3,3,3,3,3,3,3,3,3,3,3,3,3,3,3,
3,3,3,3,3,3,3,3,3,3,3,3,3,3,3,3,3,3,3,3,3,3,3,3,3,3,3,3,3,3,3,3,3,3,3,3,
3,3,3,3,3,4),(-230.287212684737,-230.195557356441,-230.103455628521,-230.010768224531,
-229.93928246563,-229.859325165499,-229.779462368256,-229.699676545784,
-229.619950230589,-229.540266002295,-229.460595016074,-229.380927562548,
-229.301247911732,-229.221540329337,-229.141745100262,-229.061900758554,
-228.981942331507,-228.93954645491,-228.859589154779,-228.779726357536,
-228.699940535064,-228.620214219869,-228.540529991575,-228.460859005354,
-228.381191551828,-228.301511901012,-228.221804318617,-228.142009089542,
-228.062164747834,-227.982206320787,-227.93981044419,-227.859853144059,
-227.779990346816,-227.700204524344,-227.620478209149,-227.540793980855,
-227.461122994634,-227.381455541108,-227.301775890292,-227.222068307897,
-227.142273078822,-227.062428737114,-226.982470310067,-226.94007443347,
-226.860117133339,-226.780254336096,-226.700468513624,-226.620742198429,
-226.541057970135,-226.461386983914,-226.381719530388,-226.302039879572,
-226.222332297177,-226.142537068101,-226.062692726394,-225.982734299346,
-225.94033842275,-225.860381122619,-225.780518325376,-225.700732502905,
-225.621006187709,-225.541321959415,-225.461650973195,-225.381983519669,
-225.302303868853,-225.222596286458,-225.142801057383,-225.062956715675,
-224.982998288628,-224.94060241203,-224.861380214033,-224.782251996577,
-224.703199591262,-224.624204899021,-224.545244058955,-224.466299823835,
-224.387355896365,-224.308395981842,-224.229359554931,-224.150283545781,
-224.071093008039,-224.004027500127),.UNSPECIFIED.);
#1632=B_SPLINE_CURVE_WITH_KNOTS('',3,(#184543,#184544,#184545,#184546,#184547,
#184548,#184549,#184550,#184551,#184552,#184553,#184554),.UNSPECIFIED.,
 .F.,.F.,(4,2,1,1,1,1,1,1,4),(-224.004027500127,-223.940866401309,-222.941130390589,
-221.941394379869,-220.941658369149,-219.941922358429,-218.942186347709,
-217.942450336989,-217.720842192948),.UNSPECIFIED.);
#1633=B_SPLINE_CURVE_WITH_KNOTS('',3,(#184556,#184557,#184558,#184559,#184560,
#184561,#184562,#184563,#184564,#184565,#184566,#184567,#184568,#184569,
#184570,#184571,#184572,#184573,#184574,#184575,#184576,#184577,#184578,
#184579,#184580,#184581,#184582,#184583,#184584,#184585,#184586,#184587,
#184588,#184589,#184590,#184591,#184592,#184593,#184594,#184595,#184596,
#184597,#184598,#184599,#184600,#184601,#184602,#184603,#184604,#184605,
#184606,#184607,#184608,#184609,#184610,#184611,#184612,#184613,#184614,
#184615,#184616,#184617,#184618,#184619,#184620,#184621,#184622,#184623,
#184624,#184625,#184626,#184627,#184628,#184629,#184630,#184631,#184632,
#184633,#184634,#184635,#184636,#184637,#184638,#184639,#184640,#184641,
#184642,#184643,#184644,#184645,#184646,#184647,#184648,#184649,#184650,
#184651,#184652,#184653,#184654,#184655,#184656,#184657,#184658,#184659,
#184660,#184661,#184662,#184663,#184664,#184665,#184666,#184667,#184668,
#184669,#184670,#184671,#184672,#184673,#184674,#184675,#184676,#184677,
#184678,#184679,#184680,#184681,#184682,#184683,#184684,#184685,#184686,
#184687,#184688,#184689,#184690,#184691,#184692,#184693,#184694,#184695,
#184696,#184697,#184698,#184699,#184700,#184701,#184702,#184703,#184704,
#184705,#184706,#184707,#184708,#184709,#184710,#184711,#184712,#184713,
#184714,#184715,#184716,#184717,#184718,#184719,#184720,#184721,#184722,
#184723,#184724,#184725,#184726,#184727,#184728,#184729,#184730,#184731,
#184732,#184733,#184734,#184735,#184736,#184737,#184738,#184739,#184740,
#184741,#184742,#184743,#184744,#184745,#184746,#184747,#184748,#184749,
#184750,#184751,#184752,#184753,#184754,#184755,#184756,#184757,#184758,
#184759,#184760,#184761,#184762,#184763,#184764,#184765,#184766,#184767,
#184768,#184769,#184770,#184771,#184772,#184773,#184774,#184775,#184776,
#184777,#184778,#184779,#184780,#184781,#184782,#184783,#184784,#184785,
#184786,#184787,#184788,#184789,#184790,#184791,#184792,#184793,#184794,
#184795,#184796,#184797,#184798,#184799),.UNSPECIFIED.,.F.,.F.,(4,3,3,3,
3,3,3,3,3,3,3,3,3,3,3,3,3,3,3,3,3,3,3,3,3,3,3,3,3,3,3,3,3,3,3,3,3,3,3,3,
3,3,3,3,3,3,3,3,3,3,3,3,3,3,3,3,3,3,3,3,3,3,3,3,3,3,3,3,3,3,3,3,3,3,3,3,
3,3,3,3,3,4),(-217.720842192948,-217.642134003223,-217.563483187297,-217.484864835763,
-217.406262272064,-217.327658988786,-217.249038479712,-217.170338117275,
-217.091596795613,-217.01273613636,-216.942714326268,-216.862757026137,
-216.782894228894,-216.703108406423,-216.623382091228,-216.543697862933,
-216.464026876712,-216.384359423187,-216.30467977237,-216.224972189976,
-216.145176960901,-216.065332619193,-215.985374192146,-215.942978315548,
-215.863021015417,-215.783158218174,-215.703372395702,-215.623646080507,
-215.543961852213,-215.464290865992,-215.384623412466,-215.30494376165,
-215.225236179255,-215.14544095018,-215.065596608472,-214.985638181425,
-214.943242304828,-214.863285004697,-214.783422207454,-214.703636384983,
-214.623910069787,-214.544225841493,-214.464554855272,-214.384887401746,
-214.305207750929,-214.225500168535,-214.14570493946,-214.065860597752,
-213.985902170705,-213.943506294108,-213.863548993977,-213.783686196734,
-213.703900374262,-213.624174059067,-213.544489830773,-213.464818844552,
-213.385151391026,-213.30547174021,-213.225764157815,-213.14596892874,-213.066124587032,
-212.986166159985,-212.943770283388,-212.863812983257,-212.783950186014,
-212.704164363543,-212.624438048348,-212.544753820053,-212.465082833832,
-212.385415380307,-212.30573572949,-212.226028147096,-212.14623291802,-212.066388576313,
-211.986430149266,-211.944034272668,-211.860196019356,-211.77649298943,
-211.691783963515,-211.608368479178,-211.523012682473,-211.437656885768),
 .UNSPECIFIED.);
#1634=B_SPLINE_CURVE_WITH_KNOTS('',3,(#184801,#184802,#184803,#184804,#184805,
#184806,#184807,#184808,#184809,#184810,#184811,#184812,#184813,#184814,
#184815,#184816,#184817,#184818,#184819,#184820,#184821,#184822,#184823,
#184824,#184825,#184826,#184827,#184828,#184829,#184830,#184831,#184832,
#184833,#184834,#184835,#184836,#184837,#184838,#184839,#184840,#184841,
#184842,#184843,#184844,#184845,#184846,#184847,#184848,#184849,#184850,
#184851,#184852,#184853,#184854,#184855,#184856,#184857,#184858,#184859,
#184860,#184861,#184862,#184863,#184864,#184865,#184866,#184867,#184868,
#184869,#184870,#184871,#184872,#184873,#184874,#184875,#184876,#184877,
#184878,#184879,#184880,#184881,#184882,#184883,#184884,#184885,#184886,
#184887,#184888,#184889,#184890,#184891,#184892,#184893,#184894,#184895,
#184896,#184897,#184898,#184899,#184900,#184901,#184902,#184903,#184904,
#184905,#184906,#184907,#184908,#184909,#184910,#184911,#184912,#184913,
#184914,#184915,#184916,#184917,#184918,#184919,#184920,#184921,#184922,
#184923,#184924,#184925,#184926,#184927,#184928,#184929,#184930,#184931,
#184932,#184933,#184934,#184935,#184936,#184937,#184938,#184939,#184940,
#184941,#184942,#184943,#184944,#184945,#184946,#184947,#184948,#184949,
#184950,#184951,#184952,#184953,#184954,#184955,#184956,#184957,#184958,
#184959,#184960,#184961,#184962,#184963,#184964,#184965,#184966,#184967,
#184968,#184969,#184970,#184971,#184972,#184973,#184974,#184975,#184976,
#184977,#184978,#184979,#184980,#184981,#184982,#184983,#184984,#184985,
#184986,#184987,#184988,#184989,#184990,#184991,#184992,#184993,#184994,
#184995,#184996,#184997,#184998,#184999,#185000,#185001,#185002,#185003,
#185004,#185005,#185006,#185007,#185008,#185009,#185010,#185011,#185012,
#185013,#185014,#185015,#185016,#185017,#185018,#185019,#185020,#185021,
#185022,#185023,#185024,#185025,#185026,#185027,#185028,#185029,#185030,
#185031,#185032,#185033,#185034,#185035,#185036,#185037,#185038,#185039,
#185040,#185041,#185042,#185043,#185044),.UNSPECIFIED.,.F.,.F.,(4,3,3,3,
3,3,3,3,3,3,3,3,3,3,3,3,3,3,3,3,3,3,3,3,3,3,3,3,3,3,3,3,3,3,3,3,3,3,3,3,
3,3,3,3,3,3,3,3,3,3,3,3,3,3,3,3,3,3,3,3,3,3,3,3,3,3,3,3,3,3,3,3,3,3,3,3,
3,3,3,3,3,4),(-211.437656885626,-211.353970957782,-211.27017209527,-211.186171414536,
-211.102066720774,-211.017765042623,-210.944298261948,-210.864340961817,
-210.784478164574,-210.704692342102,-210.624966026906,-210.545281798612,
-210.465610812391,-210.385943358865,-210.306263708048,-210.226556125653,
-210.146760896578,-210.06691655487,-209.986958127822,-209.944562251228,
-209.864604951096,-209.784742153854,-209.704956331381,-209.625230016186,
-209.545545787892,-209.46587480167,-209.386207348144,-209.306527697328,
-209.226820114933,-209.147024885857,-209.067180544149,-208.987222117101,
-208.944826240507,-208.864868940376,-208.785006143133,-208.705220320661,
-208.625494005466,-208.545809777172,-208.466138790951,-208.386471337425,
-208.306791686609,-208.227084104215,-208.147288875139,-208.067444533432,
-207.987486106384,-207.945090229787,-207.865132929656,-207.785270132413,
-207.705484309942,-207.625757994746,-207.546073766452,-207.466402780232,
-207.386735326706,-207.307055675889,-207.227348093495,-207.14755286442,
-207.067708522712,-206.987750095665,-206.945354219067,-206.865396918936,
-206.785534121693,-206.705748299221,-206.626021984026,-206.546337755732,
-206.466666769511,-206.386999315985,-206.307319665169,-206.227612082774,
-206.147816853699,-206.067972511991,-205.988014084944,-205.945618208347,
-205.86678740295,-205.788051427103,-205.708853946039,-205.630257658485,
-205.55169502182,-205.473149485886,-205.393480009062,-205.314894194931,
-205.23468288676,-205.154471578589),.UNSPECIFIED.);
#1635=B_SPLINE_CURVE_WITH_KNOTS('',3,(#185046,#185047,#185048,#185049,#185050,
#185051,#185052,#185053,#185054,#185055,#185056),.UNSPECIFIED.,.F.,.F.,
(4,1,1,1,1,1,1,1,4),(-205.154471578589,-204.945882197627,-203.946146186907,
-202.946410176187,-201.946674165466,-200.946938154746,-199.947202144026,
-198.947466133306,-198.871286271409),.UNSPECIFIED.);
#1636=B_SPLINE_CURVE_WITH_KNOTS('',3,(#185058,#185059,#185060,#185061,#185062,
#185063,#185064,#185065,#185066,#185067),.UNSPECIFIED.,.F.,.F.,(4,1,1,1,
1,1,1,4),(-198.871286271409,-197.947730122586,-196.947994111866,-195.948258101146,
-194.948522090426,-193.948786079705,-192.949050068985,-192.58810096423),
 .UNSPECIFIED.);
#1637=B_SPLINE_CURVE_WITH_KNOTS('',3,(#185069,#185070,#185071,#185072,#185073,
#185074,#185075,#185076,#185077,#185078),.UNSPECIFIED.,.F.,.F.,(4,1,1,1,
1,1,1,4),(-192.58810096423,-191.949314058265,-190.949578047545,-189.949842036825,
-188.950106026105,-187.950370015385,-186.950634004665,-186.30491565705),
 .UNSPECIFIED.);
#1638=B_SPLINE_CURVE_WITH_KNOTS('',3,(#185080,#185081,#185082,#185083,#185084,
#185085,#185086,#185087,#185088,#185089,#185090,#185091,#185092,#185093,
#185094,#185095,#185096,#185097,#185098,#185099,#185100,#185101,#185102,
#185103,#185104,#185105,#185106,#185107,#185108,#185109,#185110,#185111,
#185112,#185113,#185114,#185115,#185116,#185117,#185118,#185119,#185120,
#185121,#185122,#185123,#185124,#185125,#185126,#185127,#185128,#185129,
#185130,#185131,#185132,#185133,#185134,#185135,#185136,#185137,#185138,
#185139,#185140,#185141,#185142,#185143,#185144,#185145,#185146,#185147,
#185148,#185149,#185150,#185151,#185152,#185153,#185154,#185155,#185156,
#185157,#185158,#185159,#185160,#185161,#185162,#185163,#185164,#185165,
#185166,#185167,#185168,#185169,#185170,#185171,#185172,#185173,#185174,
#185175,#185176,#185177,#185178,#185179,#185180,#185181,#185182,#185183,
#185184,#185185,#185186,#185187,#185188,#185189,#185190,#185191,#185192,
#185193,#185194,#185195,#185196,#185197,#185198,#185199,#185200,#185201,
#185202,#185203,#185204,#185205,#185206,#185207,#185208,#185209,#185210,
#185211,#185212,#185213,#185214,#185215,#185216,#185217,#185218,#185219,
#185220,#185221,#185222,#185223,#185224,#185225,#185226,#185227,#185228,
#185229,#185230,#185231,#185232,#185233,#185234,#185235,#185236,#185237,
#185238,#185239,#185240,#185241,#185242,#185243,#185244,#185245,#185246,
#185247,#185248,#185249,#185250,#185251,#185252,#185253,#185254,#185255,
#185256,#185257,#185258,#185259,#185260,#185261,#185262,#185263,#185264,
#185265,#185266,#185267,#185268,#185269,#185270,#185271,#185272,#185273,
#185274,#185275,#185276,#185277,#185278,#185279,#185280,#185281,#185282,
#185283,#185284,#185285,#185286,#185287,#185288,#185289,#185290,#185291,
#185292,#185293,#185294,#185295,#185296,#185297,#185298,#185299,#185300,
#185301,#185302,#185303,#185304,#185305,#185306,#185307,#185308,#185309,
#185310,#185311,#185312,#185313,#185314,#185315,#185316,#185317,#185318,
#185319,#185320,#185321,#185322,#185323),.UNSPECIFIED.,.F.,.F.,(4,3,3,3,
3,3,3,3,3,3,3,3,3,3,3,3,3,3,3,3,3,3,3,3,3,3,3,3,3,3,3,3,3,3,3,3,3,3,3,3,
3,3,3,3,3,3,3,3,3,3,3,3,3,3,3,3,3,3,3,3,3,3,3,3,3,3,3,3,3,3,3,3,3,3,3,3,
3,3,3,3,3,4),(-186.304915409735,-186.213726832839,-186.122121906506,-186.0299546992,
-185.950897993944,-185.870940693813,-185.79107789657,-185.711292074098,
-185.631565758903,-185.551881530609,-185.472210544388,-185.392543090862,
-185.312863440046,-185.233155857651,-185.153360628576,-185.073516286868,
-184.993557859821,-184.951161983224,-184.871204683093,-184.79134188585,
-184.711556063378,-184.631829748183,-184.552145519889,-184.472474533668,
-184.392807080142,-184.313127429326,-184.233419846931,-184.153624617856,
-184.073780276148,-183.993821849101,-183.951425972504,-183.871468672373,
-183.79160587513,-183.711820052658,-183.632093737463,-183.552409509169,
-183.472738522948,-183.393071069422,-183.313391418605,-183.233683836211,
-183.153888607135,-183.074044265427,-182.99408583838,-182.951689961784,
-182.871732661653,-182.79186986441,-182.712084041939,-182.632357726743,
-182.552673498449,-182.473002512228,-182.393335058703,-182.313655407886,
-182.233947825492,-182.154152596416,-182.074308254709,-181.994349827661,
-181.951953951064,-181.871996650933,-181.79213385369,-181.712348031218,
-181.632621716023,-181.552937487729,-181.473266501508,-181.393599047982,
-181.313919397166,-181.234211814771,-181.154416585696,-181.074572243988,
-180.994613816941,-180.952217940344,-180.873047776925,-180.793971548658,
-180.714971048043,-180.636028137857,-180.557119024801,-180.478226359198,
-180.399333810161,-180.320425049214,-180.241440507916,-180.162416093261,
-180.083279647565,-180.021730349871),.UNSPECIFIED.);
#1639=B_SPLINE_CURVE_WITH_KNOTS('',3,(#185325,#185326,#185327,#185328,#185329,
#185330,#185331,#185332,#185333,#185334,#185335,#185336),.UNSPECIFIED.,
 .F.,.F.,(4,2,1,1,1,1,1,1,4),(-180.021730349871,-179.952481929624,-178.952745918903,
-177.953009908183,-176.953273897463,-175.953537886743,-174.953801876023,
-173.954065865303,-173.738545042691),.UNSPECIFIED.);
#1640=B_SPLINE_CURVE_WITH_KNOTS('',3,(#185338,#185339,#185340,#185341,#185342,
#185343,#185344,#185345,#185346,#185347),.UNSPECIFIED.,.F.,.F.,(4,1,1,1,
1,1,1,4),(-173.738545042691,-172.954329854583,-171.954593843863,-170.954857833142,
-169.955121822422,-168.955385811702,-167.955649800982,-167.455359735511),
 .UNSPECIFIED.);
#1641=B_SPLINE_CURVE_WITH_KNOTS('',3,(#185349,#185350,#185351,#185352,#185353,
#185354,#185355,#185356,#185357,#185358),.UNSPECIFIED.,.F.,.F.,(4,1,1,1,
1,1,1,4),(-167.455359735511,-166.955913790262,-165.956177779542,-164.956441768822,
-163.956705758101,-162.956969747381,-161.957233736661,-161.172174428332),
 .UNSPECIFIED.);
#1642=B_SPLINE_CURVE_WITH_KNOTS('',3,(#185360,#185361,#185362,#185363,#185364,
#185365,#185366,#185367,#185368,#185369,#185370),.UNSPECIFIED.,.F.,.F.,
(4,1,1,1,1,1,1,1,4),(-161.172174428332,-160.957497725941,-159.957761715221,
-158.958025704501,-157.958289693781,-156.958553683061,-155.95881767234,
-154.95908166162,-154.888989121152),.UNSPECIFIED.);
#1643=B_SPLINE_CURVE_WITH_KNOTS('',3,(#185372,#185373,#185374,#185375,#185376,
#185377,#185378,#185379,#185380,#185381,#185382,#185383,#185384,#185385,
#185386,#185387,#185388,#185389,#185390,#185391,#185392,#185393,#185394,
#185395,#185396,#185397,#185398,#185399,#185400,#185401,#185402,#185403,
#185404,#185405,#185406,#185407,#185408,#185409,#185410,#185411,#185412,
#185413,#185414,#185415,#185416,#185417,#185418,#185419,#185420,#185421,
#185422,#185423,#185424,#185425,#185426,#185427,#185428,#185429,#185430,
#185431,#185432,#185433,#185434,#185435,#185436,#185437,#185438,#185439,
#185440,#185441,#185442,#185443,#185444,#185445,#185446,#185447,#185448,
#185449,#185450,#185451,#185452,#185453,#185454,#185455,#185456,#185457,
#185458,#185459,#185460,#185461,#185462,#185463,#185464,#185465,#185466,
#185467,#185468,#185469,#185470,#185471,#185472,#185473,#185474,#185475,
#185476,#185477,#185478,#185479,#185480,#185481,#185482,#185483,#185484,
#185485,#185486,#185487,#185488,#185489,#185490,#185491,#185492,#185493,
#185494,#185495,#185496,#185497,#185498,#185499,#185500,#185501,#185502,
#185503,#185504,#185505,#185506,#185507,#185508,#185509,#185510,#185511,
#185512,#185513,#185514,#185515,#185516,#185517,#185518,#185519,#185520,
#185521,#185522,#185523,#185524,#185525,#185526,#185527,#185528,#185529,
#185530,#185531,#185532,#185533,#185534,#185535,#185536,#185537,#185538,
#185539,#185540,#185541,#185542,#185543,#185544,#185545,#185546,#185547,
#185548,#185549,#185550,#185551,#185552,#185553,#185554,#185555,#185556,
#185557,#185558,#185559,#185560,#185561,#185562,#185563,#185564,#185565,
#185566,#185567,#185568,#185569,#185570,#185571,#185572,#185573,#185574,
#185575,#185576,#185577,#185578,#185579,#185580,#185581,#185582,#185583,
#185584,#185585,#185586,#185587,#185588,#185589,#185590,#185591,#185592,
#185593,#185594,#185595,#185596,#185597,#185598,#185599,#185600,#185601,
#185602,#185603,#185604,#185605,#185606,#185607,#185608,#185609,#185610,
#185611,#185612,#185613,#185614,#185615),.UNSPECIFIED.,.F.,.F.,(4,3,3,3,
3,3,3,3,3,3,3,3,3,3,3,3,3,3,3,3,3,3,3,3,3,3,3,3,3,3,3,3,3,3,3,3,3,3,3,3,
3,3,3,3,3,3,3,3,3,3,3,3,3,3,3,3,3,3,3,3,3,3,3,3,3,3,3,3,3,3,3,3,3,3,3,3,
3,3,3,3,3,4),(-154.888989121152,-154.809851096199,-154.730802383284,-154.651824789386,
-154.572900187323,-154.494002434836,-154.415116849767,-154.336227098127,
-154.257316845318,-154.178324344123,-154.099288265117,-154.020134654139,
-153.9593456509,-153.879388350769,-153.799525553526,-153.719739731054,-153.640013415859,
-153.560329187565,-153.480658201344,-153.400990747818,-153.321311097002,
-153.241603514607,-153.161808285532,-153.081963943824,-153.002005516777,
-152.95960964018,-152.879652340049,-152.799789542806,-152.720003720334,
-152.640277405139,-152.560593176846,-152.480922190625,-152.401254737099,
-152.321575086282,-152.241867503888,-152.162072274812,-152.082227933105,
-152.002269506057,-151.95987362946,-151.879916329329,-151.800053532086,
-151.720267709614,-151.640541394419,-151.560857166125,-151.481186179904,
-151.401518726378,-151.321839075561,-151.242131493167,-151.162336264091,
-151.082491922383,-151.002533495336,-150.96013761874,-150.880180318609,
-150.800317521366,-150.720531698895,-150.6408053837,-150.561121155404,-150.481450169184,
-150.401782715658,-150.322103064841,-150.242395482447,-150.162600253372,
-150.082755911664,-150.002797484616,-149.96040160802,-149.880444307889,
-149.800581510646,-149.720795688174,-149.641069372979,-149.561385144685,
-149.481714158464,-149.402046704939,-149.322367054122,-149.242659471728,
-149.162864242652,-149.083019900944,-149.003061473897,-148.9606655973,-148.86858074921,
-148.776825906217,-148.68572083433,-148.605804061509),.UNSPECIFIED.);
#1644=B_SPLINE_CURVE_WITH_KNOTS('',3,(#185617,#185618,#185619,#185620,#185621,
#185622,#185623,#185624,#185625,#185626),.UNSPECIFIED.,.F.,.F.,(4,1,1,1,
1,1,1,4),(-148.605803813973,-147.960929586579,-146.961193575859,-145.961457565139,
-144.961721554419,-143.961985543699,-142.962249532979,-142.322618506793),
 .UNSPECIFIED.);
#1645=B_SPLINE_CURVE_WITH_KNOTS('',3,(#185628,#185629,#185630,#185631,#185632,
#185633,#185634,#185635,#185636,#185637),.UNSPECIFIED.,.F.,.F.,(4,1,1,1,
1,1,1,4),(-142.322618506793,-141.962513522259,-140.962777511538,-139.963041500818,
-138.963305490098,-137.963569479378,-136.963833468658,-136.039433199614),
 .UNSPECIFIED.);
#1646=B_SPLINE_CURVE_WITH_KNOTS('',3,(#185639,#185640,#185641,#185642,#185643,
#185644,#185645,#185646,#185647,#185648,#185649),.UNSPECIFIED.,.F.,.F.,
(4,1,1,1,1,1,1,1,4),(-136.039433199614,-135.964097457938,-134.964361447218,
-133.964625436498,-132.964889425777,-131.965153415057,-130.965417404337,
-129.965681393617,-129.756247892434),.UNSPECIFIED.);
#1647=B_SPLINE_CURVE_WITH_KNOTS('',3,(#185651,#185652,#185653,#185654,#185655,
#185656,#185657,#185658,#185659,#185660,#185661,#185662,#185663,#185664,
#185665,#185666,#185667,#185668,#185669,#185670,#185671,#185672,#185673,
#185674,#185675,#185676,#185677,#185678,#185679,#185680,#185681,#185682,
#185683,#185684,#185685,#185686,#185687,#185688,#185689,#185690,#185691,
#185692,#185693,#185694,#185695,#185696,#185697,#185698,#185699,#185700,
#185701,#185702,#185703,#185704,#185705,#185706,#185707,#185708,#185709,
#185710,#185711,#185712,#185713,#185714,#185715,#185716,#185717,#185718,
#185719,#185720,#185721,#185722,#185723,#185724,#185725,#185726,#185727,
#185728,#185729,#185730,#185731,#185732,#185733,#185734,#185735,#185736,
#185737,#185738,#185739,#185740,#185741,#185742,#185743,#185744,#185745,
#185746,#185747,#185748,#185749,#185750,#185751,#185752,#185753,#185754,
#185755,#185756,#185757,#185758,#185759,#185760,#185761,#185762,#185763,
#185764,#185765,#185766,#185767,#185768,#185769,#185770,#185771,#185772,
#185773,#185774,#185775,#185776,#185777,#185778,#185779,#185780,#185781,
#185782,#185783,#185784,#185785,#185786,#185787,#185788,#185789,#185790,
#185791,#185792,#185793,#185794,#185795,#185796,#185797,#185798,#185799,
#185800,#185801,#185802,#185803,#185804,#185805,#185806,#185807,#185808,
#185809,#185810,#185811,#185812,#185813,#185814,#185815,#185816,#185817,
#185818,#185819,#185820,#185821,#185822,#185823,#185824,#185825,#185826,
#185827,#185828,#185829,#185830,#185831,#185832,#185833,#185834,#185835,
#185836,#185837,#185838,#185839,#185840,#185841,#185842,#185843,#185844,
#185845,#185846,#185847,#185848,#185849,#185850,#185851,#185852,#185853,
#185854,#185855,#185856,#185857,#185858,#185859,#185860,#185861,#185862,
#185863,#185864,#185865,#185866,#185867,#185868,#185869,#185870,#185871,
#185872,#185873,#185874,#185875,#185876,#185877,#185878,#185879,#185880,
#185881,#185882,#185883,#185884,#185885,#185886,#185887,#185888,#185889,
#185890,#185891,#185892,#185893,#185894),.UNSPECIFIED.,.F.,.F.,(4,3,3,3,
3,3,3,3,3,3,3,3,3,3,3,3,3,3,3,3,3,3,3,3,3,3,3,3,3,3,3,3,3,3,3,3,3,3,3,3,
3,3,3,3,3,3,3,3,3,3,3,3,3,3,3,3,3,3,3,3,3,3,3,3,3,3,3,3,3,3,3,3,3,3,3,3,
3,3,3,3,3,4),(-129.756247892434,-129.677573144673,-129.598959172096,-129.519832448446,
-129.441274334452,-129.36271837502,-129.28414803768,-129.204597373984,-129.125909857212,
-129.045927620055,-128.965945382897,-128.885988082766,-128.806125285523,
-128.726339463052,-128.646613147856,-128.566928919562,-128.487257933341,
-128.407590479815,-128.327910828999,-128.248203246604,-128.168408017529,
-128.088563675821,-128.008605248774,-127.966209372177,-127.886252072046,
-127.806389274803,-127.726603452331,-127.646877137136,-127.567192908842,
-127.487521922621,-127.407854469095,-127.328174818279,-127.248467235884,
-127.168672006808,-127.088827665101,-127.008869238054,-126.966473361457,
-126.886516061326,-126.806653264083,-126.726867441612,-126.647141126417,
-126.567456898122,-126.487785911901,-126.408118458375,-126.328438807559,
-126.248731225164,-126.168935996089,-126.089091654381,-126.009133227334,
-125.966737350737,-125.886780050606,-125.806917253363,-125.727131430891,
-125.647405115695,-125.567720887402,-125.48804990118,-125.408382447654,
-125.328702796838,-125.248995214444,-125.169199985368,-125.08935564366,
-125.009397216612,-124.967001340016,-124.887044039885,-124.807181242642,
-124.727395420171,-124.647669104975,-124.567984876682,-124.488313890461,
-124.408646436935,-124.328966786118,-124.249259203724,-124.169463974648,
-124.089619632941,-124.009661205894,-123.967265329296,-123.882969519311,
-123.798815750226,-123.714855745484,-123.631009770825,-123.547321253712,
-123.473062585378),.UNSPECIFIED.);
#1648=B_SPLINE_CURVE_WITH_KNOTS('',3,(#185896,#185897,#185898,#185899,#185900,
#185901,#185902,#185903,#185904,#185905,#185906,#185907,#185908,#185909,
#185910,#185911,#185912,#185913,#185914,#185915,#185916,#185917,#185918,
#185919,#185920,#185921,#185922,#185923,#185924,#185925,#185926,#185927,
#185928,#185929,#185930,#185931,#185932,#185933,#185934,#185935,#185936,
#185937,#185938,#185939,#185940,#185941,#185942,#185943,#185944,#185945,
#185946,#185947,#185948,#185949,#185950,#185951,#185952,#185953,#185954,
#185955,#185956,#185957,#185958,#185959,#185960,#185961,#185962,#185963,
#185964,#185965,#185966,#185967,#185968,#185969,#185970,#185971,#185972,
#185973,#185974,#185975,#185976,#185977,#185978,#185979,#185980,#185981,
#185982,#185983,#185984,#185985,#185986,#185987,#185988,#185989,#185990,
#185991,#185992,#185993,#185994,#185995,#185996,#185997,#185998,#185999,
#186000,#186001,#186002,#186003,#186004,#186005,#186006,#186007,#186008,
#186009,#186010,#186011,#186012,#186013,#186014,#186015,#186016,#186017,
#186018,#186019,#186020,#186021,#186022,#186023,#186024,#186025,#186026,
#186027,#186028,#186029,#186030,#186031,#186032,#186033,#186034,#186035,
#186036,#186037,#186038,#186039,#186040,#186041,#186042,#186043,#186044,
#186045,#186046,#186047,#186048,#186049,#186050,#186051,#186052,#186053,
#186054,#186055,#186056,#186057,#186058,#186059,#186060,#186061,#186062,
#186063,#186064,#186065,#186066,#186067,#186068,#186069,#186070,#186071,
#186072,#186073,#186074,#186075,#186076,#186077,#186078,#186079,#186080,
#186081,#186082,#186083,#186084,#186085,#186086,#186087,#186088,#186089,
#186090,#186091,#186092,#186093,#186094,#186095,#186096,#186097,#186098,
#186099,#186100,#186101,#186102,#186103,#186104,#186105,#186106,#186107,
#186108,#186109,#186110,#186111,#186112,#186113,#186114,#186115,#186116,
#186117,#186118,#186119,#186120,#186121,#186122,#186123,#186124,#186125,
#186126,#186127,#186128,#186129,#186130,#186131,#186132,#186133,#186134,
#186135,#186136,#186137,#186138,#186139),.UNSPECIFIED.,.F.,.F.,(4,3,3,3,
3,3,3,3,3,3,3,3,3,3,3,3,3,3,3,3,3,3,3,3,3,3,3,3,3,3,3,3,3,3,3,3,3,3,3,3,
3,3,3,3,3,3,3,3,3,3,3,3,3,3,3,3,3,3,3,3,3,3,3,3,3,3,3,3,3,3,3,3,3,3,3,3,
3,3,3,3,3,4),(-123.473062585254,-123.389798861451,-123.306437150327,-123.22171019239,
-123.138066210288,-123.052797764432,-122.967529318576,-122.887572018445,
-122.807709221202,-122.727923398731,-122.648197083535,-122.568512855241,
-122.48884186902,-122.409174415494,-122.329494764678,-122.249787182283,
-122.169991953208,-122.0901476115,-122.010189184453,-121.967793307856,-121.887836007725,
-121.807973210482,-121.72818738801,-121.648461072815,-121.568776844521,
-121.4891058583,-121.409438404774,-121.329758753957,-121.250051171563,-121.170255942487,
-121.09041160078,-121.010453173732,-120.968057297136,-120.888099997005,
-120.808237199762,-120.728451377291,-120.648725062095,-120.569040833801,
-120.48936984758,-120.409702394055,-120.330022743238,-120.250315160843,
-120.170519931768,-120.09067559006,-120.010717163013,-119.968321286416,
-119.888363986285,-119.808501189042,-119.728715366571,-119.648989051376,
-119.569304823081,-119.48963383686,-119.409966383334,-119.330286732518,
-119.250579150123,-119.170783921048,-119.09093957934,-119.010981152293,
-118.968585275696,-118.888627975565,-118.808765178322,-118.72897935585,
-118.649253040654,-118.56956881236,-118.489897826139,-118.410230372612,
-118.330550721796,-118.250843139401,-118.171047910325,-118.091203568617,
-118.01124514157,-117.968849264975,-117.889971084437,-117.811188096325,
-117.732495007955,-117.653852743602,-117.575244750464,-117.496654504028,
-117.418038752298,-117.339412087883,-117.260714790506,-117.189877278075),
 .UNSPECIFIED.);
#1649=B_SPLINE_CURVE_WITH_KNOTS('',3,(#186141,#186142,#186143,#186144,#186145,
#186146,#186147,#186148,#186149,#186150,#186151),.UNSPECIFIED.,.F.,.F.,
(4,1,1,1,1,1,1,1,4),(-117.189877278075,-116.969113254255,-115.969377243535,
-114.969641232815,-113.969905222095,-112.970169211375,-111.970433200655,
-110.970697189935,-110.906691970895),.UNSPECIFIED.);
#1650=B_SPLINE_CURVE_WITH_KNOTS('',3,(#186153,#186154,#186155,#186156,#186157,
#186158,#186159,#186160,#186161,#186162,#186163,#186164,#186165,#186166,
#186167,#186168,#186169,#186170,#186171,#186172,#186173,#186174,#186175,
#186176,#186177,#186178,#186179,#186180,#186181,#186182,#186183,#186184,
#186185,#186186,#186187,#186188,#186189,#186190,#186191,#186192,#186193,
#186194,#186195,#186196,#186197,#186198,#186199,#186200,#186201,#186202,
#186203,#186204,#186205,#186206,#186207,#186208,#186209,#186210,#186211,
#186212,#186213,#186214,#186215,#186216,#186217,#186218,#186219,#186220,
#186221,#186222,#186223,#186224,#186225,#186226,#186227,#186228,#186229,
#186230,#186231,#186232,#186233,#186234,#186235,#186236,#186237,#186238,
#186239,#186240,#186241,#186242,#186243,#186244,#186245,#186246,#186247,
#186248,#186249,#186250,#186251,#186252,#186253,#186254,#186255,#186256,
#186257,#186258,#186259,#186260,#186261,#186262,#186263,#186264,#186265,
#186266,#186267,#186268,#186269,#186270,#186271,#186272,#186273,#186274,
#186275,#186276,#186277,#186278,#186279,#186280,#186281,#186282,#186283,
#186284,#186285,#186286,#186287,#186288,#186289,#186290,#186291,#186292,
#186293,#186294,#186295,#186296,#186297,#186298,#186299,#186300,#186301,
#186302,#186303,#186304,#186305,#186306,#186307,#186308,#186309,#186310,
#186311,#186312,#186313,#186314,#186315,#186316,#186317,#186318,#186319,
#186320,#186321,#186322,#186323,#186324,#186325,#186326,#186327,#186328,
#186329,#186330,#186331,#186332,#186333,#186334,#186335,#186336,#186337,
#186338,#186339,#186340,#186341,#186342,#186343,#186344,#186345,#186346,
#186347,#186348,#186349,#186350,#186351,#186352,#186353,#186354,#186355,
#186356,#186357,#186358,#186359,#186360,#186361,#186362,#186363,#186364,
#186365,#186366,#186367,#186368,#186369,#186370,#186371,#186372,#186373,
#186374,#186375,#186376,#186377,#186378,#186379,#186380,#186381,#186382,
#186383,#186384,#186385,#186386,#186387,#186388,#186389,#186390,#186391,
#186392,#186393,#186394,#186395,#186396),.UNSPECIFIED.,.F.,.F.,(4,3,3,3,
3,3,3,3,3,3,3,3,3,3,3,3,3,3,3,3,3,3,3,3,3,3,3,3,3,3,3,3,3,3,3,3,3,3,3,3,
3,3,3,3,3,3,3,3,3,3,3,3,3,3,3,3,3,3,3,3,3,3,3,3,3,3,3,3,3,3,3,3,3,3,3,3,
3,3,3,3,3,4),(-110.906691970895,-110.82749856315,-110.748395230993,-110.669363816888,
-110.590386228964,-110.511436604536,-110.432499965624,-110.35356001131,
-110.27460044075,-110.195558870897,-110.116474582147,-110.037271099244,
-109.970961179214,-109.891003879083,-109.81114108184,-109.731355259369,
-109.651628944173,-109.571944715879,-109.492273729658,-109.412606276133,
-109.332926625316,-109.253219042922,-109.173423813846,-109.093579472138,
-109.013621045091,-108.971225168494,-108.891267868363,-108.81140507112,
-108.731619248648,-108.651892933453,-108.572208705159,-108.492537718938,
-108.412870265412,-108.333190614595,-108.253483032201,-108.173687803125,
-108.093843461418,-108.013885034371,-107.971489157774,-107.891531857643,
-107.8116690604,-107.731883237929,-107.652156922733,-107.572472694439,-107.492801708218,
-107.413134254692,-107.333454603876,-107.253747021481,-107.173951792405,
-107.094107450698,-107.01414902365,-106.971753147054,-106.891795846923,
-106.81193304968,-106.732147227209,-106.652420912013,-106.572736683719,
-106.493065697498,-106.413398243972,-106.333718593156,-106.254011010761,
-106.174215781686,-106.094371439978,-106.014413012931,-105.972017136334,
-105.892059836203,-105.81219703896,-105.732411216489,-105.652684901294,
-105.573000672999,-105.493329686778,-105.413662233252,-105.333982582435,
-105.254275000041,-105.174479770965,-105.094635429257,-105.01467700221,
-104.972281125614,-104.879689190256,-104.787448241979,-104.695893518158,
-104.623506786484),.UNSPECIFIED.);
#1651=B_SPLINE_CURVE_WITH_KNOTS('',3,(#186398,#186399,#186400,#186401,#186402,
#186403,#186404,#186405,#186406,#186407),.UNSPECIFIED.,.F.,.F.,(4,1,1,1,
1,1,1,4),(-104.623506663716,-103.972545114894,-102.972809104174,-101.973073093453,
-100.973337082733,-99.9736010720131,-98.973865061293,-98.340321356536),
 .UNSPECIFIED.);
#1652=B_SPLINE_CURVE_WITH_KNOTS('',3,(#186409,#186410,#186411,#186412,#186413,
#186414,#186415,#186416,#186417,#186418),.UNSPECIFIED.,.F.,.F.,(4,1,1,1,
1,1,1,4),(-98.340321356536,-97.9741290505729,-96.9743930398527,-95.9746570291326,
-94.9749210184124,-93.9751850076923,-92.9754489969722,-92.0571360493564),
 .UNSPECIFIED.);
#1653=B_SPLINE_CURVE_WITH_KNOTS('',3,(#186420,#186421,#186422,#186423,#186424,
#186425,#186426,#186427,#186428,#186429,#186430),.UNSPECIFIED.,.F.,.F.,
(4,1,1,1,1,1,1,1,4),(-92.0571360493564,-91.9757129862521,-90.9759769755319,
-89.9762409648118,-88.9765049540917,-87.9767689433716,-86.9770329326514,
-85.9772969219313,-85.7739507421768),.UNSPECIFIED.);
#1654=B_SPLINE_CURVE_WITH_KNOTS('',3,(#186432,#186433,#186434,#186435,#186436,
#186437,#186438,#186439,#186440,#186441,#186442,#186443,#186444,#186445,
#186446,#186447,#186448,#186449,#186450,#186451,#186452,#186453,#186454,
#186455,#186456,#186457,#186458,#186459,#186460,#186461,#186462,#186463,
#186464,#186465,#186466,#186467,#186468,#186469,#186470,#186471,#186472,
#186473,#186474,#186475,#186476,#186477,#186478,#186479,#186480,#186481,
#186482,#186483,#186484,#186485,#186486,#186487,#186488,#186489,#186490,
#186491,#186492,#186493,#186494,#186495,#186496,#186497,#186498,#186499,
#186500,#186501,#186502,#186503,#186504,#186505,#186506,#186507,#186508,
#186509,#186510,#186511,#186512,#186513,#186514,#186515,#186516,#186517,
#186518,#186519,#186520,#186521,#186522,#186523,#186524,#186525,#186526,
#186527,#186528,#186529,#186530,#186531,#186532,#186533,#186534,#186535,
#186536,#186537,#186538,#186539,#186540,#186541,#186542,#186543,#186544,
#186545,#186546,#186547,#186548,#186549,#186550,#186551,#186552,#186553,
#186554,#186555,#186556,#186557,#186558,#186559,#186560,#186561,#186562,
#186563,#186564,#186565,#186566,#186567,#186568,#186569,#186570,#186571,
#186572,#186573,#186574,#186575,#186576,#186577,#186578,#186579,#186580,
#186581,#186582,#186583,#186584,#186585,#186586,#186587,#186588,#186589,
#186590,#186591,#186592,#186593,#186594,#186595,#186596,#186597,#186598,
#186599,#186600,#186601,#186602,#186603,#186604,#186605,#186606,#186607,
#186608,#186609,#186610,#186611,#186612,#186613,#186614,#186615,#186616,
#186617,#186618,#186619,#186620,#186621,#186622,#186623,#186624,#186625,
#186626,#186627,#186628,#186629,#186630,#186631,#186632,#186633,#186634,
#186635,#186636,#186637,#186638,#186639,#186640,#186641,#186642,#186643,
#186644,#186645,#186646,#186647,#186648,#186649,#186650,#186651,#186652,
#186653,#186654,#186655,#186656,#186657,#186658,#186659,#186660,#186661,
#186662,#186663,#186664,#186665,#186666,#186667,#186668,#186669,#186670,
#186671,#186672,#186673,#186674,#186675),.UNSPECIFIED.,.F.,.F.,(4,3,3,3,
3,3,3,3,3,3,3,3,3,3,3,3,3,3,3,3,3,3,3,3,3,3,3,3,3,3,3,3,3,3,3,3,3,3,3,3,
3,3,3,3,3,3,3,3,3,3,3,3,3,3,3,3,3,3,3,3,3,3,3,3,3,3,3,3,3,3,3,3,3,3,3,3,
3,3,3,3,3,4),(-85.7739507421768,-85.6952881601577,-85.616687997987,-85.53679711214,
-85.4582566003864,-85.379719530466,-85.3011693595009,-85.2202672474284,
-85.1416009943376,-85.0595809527744,-84.9775609112112,-84.89760361108,-84.8177408138373,
-84.7379549913655,-84.6582286761703,-84.5785444478759,-84.498873461655,
-84.419206008129,-84.3395263573124,-84.2598187749181,-84.1800235458425,
-84.1001792041348,-84.0202207770874,-83.977824900491,-83.8978676003597,
-83.8180048031171,-83.7382189806452,-83.6584926654501,-83.5788084371562,
-83.4991374509353,-83.4194699974093,-83.3397903465929,-83.2600827641988,
-83.1802875351232,-83.1004431934156,-83.0204847663682,-82.9780888897709,
-82.8981315896397,-82.8182687923971,-82.7384829699253,-82.65875665473,-82.579072426436,
-82.4994014402152,-82.4197339866892,-82.3400543358726,-82.2603467534779,
-82.1805515244024,-82.1007071826946,-82.0207487556472,-81.9783528790508,
-81.8983955789195,-81.818532781677,-81.7387469592052,-81.65902064401,-81.5793364157154,
-81.4996654294946,-81.4199979759686,-81.3403183251522,-81.2606107427579,
-81.1808155136824,-81.100971171975,-81.0210127449277,-80.9786168683306,
-80.8986595681993,-80.818796770957,-80.7390109484849,-80.6592846332902,
-80.5796004049962,-80.4999294187752,-80.4202619652489,-80.3405823144325,
-80.2608747320383,-80.1810795029628,-80.1012351612554,-80.0212767342081,
-79.9788808576105,-79.894345483959,-79.8099558941397,-79.7257670174106,
-79.6416970903594,-79.5577926852418,-79.4907654351257),.UNSPECIFIED.);
#1655=B_SPLINE_CURVE_WITH_KNOTS('',3,(#186677,#186678,#186679,#186680,#186681,
#186682,#186683,#186684,#186685,#186686,#186687,#186688,#186689,#186690,
#186691,#186692,#186693,#186694,#186695,#186696,#186697,#186698,#186699,
#186700,#186701,#186702,#186703,#186704,#186705,#186706,#186707,#186708,
#186709,#186710,#186711,#186712,#186713,#186714,#186715,#186716,#186717,
#186718,#186719,#186720,#186721,#186722,#186723,#186724,#186725,#186726,
#186727,#186728,#186729,#186730,#186731,#186732,#186733,#186734,#186735,
#186736,#186737,#186738,#186739,#186740,#186741,#186742,#186743,#186744,
#186745,#186746,#186747,#186748,#186749,#186750,#186751,#186752,#186753,
#186754,#186755,#186756,#186757,#186758,#186759,#186760,#186761,#186762,
#186763,#186764,#186765,#186766,#186767,#186768,#186769,#186770,#186771,
#186772,#186773,#186774,#186775,#186776,#186777,#186778,#186779,#186780,
#186781,#186782,#186783,#186784,#186785,#186786,#186787,#186788,#186789,
#186790,#186791,#186792,#186793,#186794,#186795,#186796,#186797,#186798,
#186799,#186800,#186801,#186802,#186803,#186804,#186805,#186806,#186807,
#186808,#186809,#186810,#186811,#186812,#186813,#186814,#186815,#186816,
#186817,#186818,#186819,#186820,#186821,#186822,#186823,#186824,#186825,
#186826,#186827,#186828,#186829,#186830,#186831,#186832,#186833,#186834,
#186835,#186836,#186837,#186838,#186839,#186840,#186841,#186842,#186843,
#186844,#186845,#186846,#186847,#186848,#186849,#186850,#186851,#186852,
#186853,#186854,#186855,#186856,#186857,#186858,#186859,#186860,#186861,
#186862,#186863,#186864,#186865,#186866,#186867,#186868,#186869,#186870,
#186871,#186872,#186873,#186874,#186875,#186876,#186877,#186878,#186879,
#186880,#186881,#186882,#186883,#186884,#186885,#186886,#186887,#186888,
#186889,#186890,#186891,#186892,#186893,#186894,#186895,#186896,#186897,
#186898,#186899,#186900,#186901,#186902,#186903,#186904,#186905,#186906,
#186907,#186908,#186909,#186910,#186911,#186912,#186913,#186914,#186915,
#186916,#186917,#186918,#186919,#186920),.UNSPECIFIED.,.F.,.F.,(4,3,3,3,
3,3,3,3,3,3,3,3,3,3,3,3,3,3,3,3,3,3,3,3,3,3,3,3,3,3,3,3,3,3,3,3,3,3,3,3,
3,3,3,3,3,3,3,3,3,3,3,3,3,3,3,3,3,3,3,3,3,3,3,3,3,3,3,3,3,3,3,3,3,3,3,3,
3,3,3,3,3,4),(-79.4907654349973,-79.4077034724819,-79.3245504349086,-79.2381990379041,
-79.1547733841094,-79.0669591154998,-78.9791448468903,-78.8991875467591,
-78.8193247495167,-78.7395389270448,-78.6598126118496,-78.5801283835557,
-78.5004573973348,-78.4207899438089,-78.3411102929926,-78.2614027105983,
-78.1816074815228,-78.101763139815,-78.0218047127677,-77.9794088361702,
-77.8994515360389,-77.8195887387963,-77.7398029163244,-77.6600766011291,
-77.5803923728351,-77.5007213866142,-77.4210539330884,-77.3413742822718,
-77.2616666998774,-77.1818714708018,-77.1020271290941,-77.0220687020468,
-76.9796728254501,-76.8997155253188,-76.819852728076,-76.7400669056043,
-76.6603405904092,-76.5806563621158,-76.5009853758948,-76.4213179223689,
-76.3416382715525,-76.2619306891576,-76.182135460082,-76.1022911183746,
-76.0223326913272,-75.97993681473,-75.8999795145987,-75.820116717356,-75.7403308948843,
-75.6606045796891,-75.5809203513952,-75.5012493651742,-75.4215819116484,
-75.3419022608322,-75.2621946784377,-75.1823994493621,-75.1025551076547,
-75.0225966806073,-74.9802008040098,-74.9002435038785,-74.8203807066359,
-74.7405948841641,-74.6608685689692,-74.5811843406744,-74.5015133544535,
-74.4218459009276,-74.3421662501111,-74.2624586677158,-74.1826634386403,
-74.1028190969327,-74.0228606698853,-73.9804647932897,-73.9015581804217,
-73.8227469663865,-73.7440261147531,-73.6653563569114,-73.5867211558266,
-73.5081040028306,-73.4294628808362,-73.3508110774882,-73.2720919472877,
-73.2075801278176),.UNSPECIFIED.);
#1656=B_SPLINE_CURVE_WITH_KNOTS('',3,(#186922,#186923,#186924,#186925,#186926,
#186927,#186928,#186929,#186930,#186931,#186932),.UNSPECIFIED.,.F.,.F.,
(4,1,1,1,1,1,1,1,4),(-73.2075801278176,-72.9807287825696,-71.9809927718494,
-70.9812567611293,-69.9815207504092,-68.981784739689,-67.9820487289689,
-66.9823127182488,-66.9243948206381),.UNSPECIFIED.);
#1657=B_SPLINE_CURVE_WITH_KNOTS('',3,(#186934,#186935,#186936,#186937,#186938,
#186939,#186940,#186941,#186942,#186943,#186944,#186945,#186946,#186947,
#186948,#186949,#186950,#186951,#186952,#186953,#186954,#186955,#186956,
#186957,#186958,#186959,#186960,#186961,#186962,#186963,#186964,#186965,
#186966,#186967,#186968,#186969,#186970,#186971,#186972,#186973,#186974,
#186975,#186976,#186977,#186978,#186979,#186980,#186981,#186982,#186983,
#186984,#186985,#186986,#186987,#186988,#186989,#186990,#186991,#186992,
#186993,#186994,#186995,#186996,#186997,#186998,#186999,#187000,#187001,
#187002,#187003,#187004,#187005,#187006,#187007,#187008,#187009,#187010,
#187011,#187012,#187013,#187014,#187015,#187016,#187017,#187018,#187019,
#187020,#187021,#187022,#187023,#187024,#187025,#187026,#187027,#187028,
#187029,#187030,#187031,#187032,#187033,#187034,#187035,#187036,#187037,
#187038,#187039,#187040,#187041,#187042,#187043,#187044,#187045,#187046,
#187047,#187048,#187049,#187050,#187051,#187052,#187053,#187054,#187055,
#187056,#187057,#187058,#187059,#187060,#187061,#187062,#187063,#187064,
#187065,#187066,#187067,#187068,#187069,#187070,#187071,#187072,#187073,
#187074,#187075,#187076,#187077,#187078,#187079,#187080,#187081,#187082,
#187083,#187084,#187085,#187086,#187087,#187088,#187089,#187090,#187091,
#187092,#187093,#187094,#187095,#187096,#187097,#187098,#187099,#187100,
#187101,#187102,#187103,#187104,#187105,#187106,#187107,#187108,#187109,
#187110,#187111,#187112,#187113,#187114,#187115,#187116,#187117,#187118,
#187119,#187120,#187121,#187122,#187123,#187124,#187125,#187126,#187127,
#187128,#187129,#187130,#187131,#187132,#187133,#187134,#187135,#187136,
#187137,#187138,#187139,#187140,#187141,#187142,#187143,#187144,#187145,
#187146,#187147,#187148,#187149,#187150,#187151,#187152,#187153,#187154,
#187155,#187156,#187157,#187158,#187159,#187160,#187161,#187162,#187163,
#187164,#187165,#187166,#187167,#187168,#187169,#187170,#187171,#187172,
#187173,#187174,#187175,#187176,#187177),.UNSPECIFIED.,.F.,.F.,(4,3,3,3,
3,3,3,3,3,3,3,3,3,3,3,3,3,3,3,3,3,3,3,3,3,3,3,3,3,3,3,3,3,3,3,3,3,3,3,3,
3,3,3,3,3,3,3,3,3,3,3,3,3,3,3,3,3,3,3,3,3,3,3,3,3,3,3,3,3,3,3,3,3,3,3,3,
3,3,3,3,3,4),(-66.9243948206381,-66.8451430614651,-66.7659820906656,-66.68689378965,
-66.6078601052444,-66.5288554488661,-66.4498645624908,-66.3708711811437,
-66.2918590405673,-66.2127651323194,-66.1336293443134,-66.054372687672,
-65.9825767075287,-65.9026194073974,-65.8227566101546,-65.7429707876828,
-65.6632444724872,-65.5835602441933,-65.5038892579723,-65.4242218044462,
-65.3445421536298,-65.2648345712352,-65.1850393421596,-65.105195000452,
-65.0252365734045,-64.9828406968085,-64.9028833966772,-64.8230205994346,
-64.7432347769627,-64.6635084617673,-64.5838242334732,-64.5041532472523,
-64.4244857937264,-64.3448061429098,-64.2650985605154,-64.1853033314399,
-64.1054589897322,-64.0255005626848,-63.9831046860884,-63.9031473859572,
-63.8232845887147,-63.7434987662427,-63.6637724510475,-63.5840882227535,
-63.5044172365327,-63.4247497830068,-63.3450701321903,-63.2653625497957,
-63.1855673207202,-63.1057229790125,-63.0257645519651,-62.9833686753683,
-62.903411375237,-62.8235485779942,-62.7437627555225,-62.6640364403274,
-62.5843522120328,-62.5046812258119,-62.425013772286,-62.3453341214695,
-62.2656265390753,-62.1858313099998,-62.1059869682922,-62.0260285412449,
-61.9836326646481,-61.9036753645168,-61.823812567274,-61.7440267448023,
-61.6643004296077,-61.5846162013138,-61.5049452150927,-61.4252777615666,
-61.3455981107502,-61.2658905283563,-61.1860952992806,-61.1062509575726,
-61.0262925305251,-60.983896653928,-60.8907777178953,-60.798032881653,-60.7060135811139,
-60.6412095135729),.UNSPECIFIED.);
#1658=B_SPLINE_CURVE_WITH_KNOTS('',3,(#187179,#187180,#187181,#187182,#187183,
#187184,#187185,#187186,#187187,#187188,#187189,#187190,#187191,#187192,
#187193,#187194,#187195,#187196,#187197,#187198,#187199,#187200,#187201,
#187202,#187203,#187204,#187205,#187206,#187207,#187208,#187209,#187210,
#187211,#187212,#187213,#187214,#187215,#187216,#187217,#187218,#187219,
#187220,#187221,#187222,#187223,#187224,#187225,#187226,#187227,#187228,
#187229,#187230,#187231,#187232,#187233,#187234,#187235,#187236,#187237,
#187238,#187239,#187240,#187241,#187242,#187243,#187244,#187245,#187246,
#187247,#187248,#187249,#187250,#187251,#187252,#187253,#187254,#187255,
#187256,#187257,#187258,#187259,#187260,#187261,#187262,#187263,#187264,
#187265,#187266,#187267,#187268,#187269,#187270,#187271,#187272,#187273,
#187274,#187275,#187276,#187277,#187278,#187279,#187280,#187281,#187282,
#187283,#187284,#187285,#187286,#187287,#187288,#187289,#187290,#187291,
#187292,#187293,#187294,#187295,#187296,#187297,#187298,#187299,#187300,
#187301,#187302,#187303,#187304,#187305,#187306,#187307,#187308,#187309,
#187310,#187311,#187312,#187313,#187314,#187315,#187316,#187317,#187318,
#187319,#187320,#187321,#187322,#187323,#187324,#187325,#187326,#187327,
#187328,#187329,#187330,#187331,#187332,#187333,#187334,#187335,#187336,
#187337,#187338,#187339,#187340,#187341,#187342,#187343,#187344,#187345,
#187346,#187347,#187348,#187349,#187350,#187351,#187352,#187353,#187354,
#187355,#187356,#187357,#187358,#187359,#187360,#187361,#187362,#187363,
#187364,#187365,#187366,#187367,#187368,#187369,#187370,#187371,#187372,
#187373,#187374,#187375,#187376,#187377,#187378,#187379,#187380,#187381,
#187382,#187383,#187384,#187385,#187386,#187387,#187388,#187389,#187390,
#187391,#187392,#187393,#187394,#187395,#187396,#187397,#187398,#187399,
#187400,#187401,#187402,#187403,#187404,#187405,#187406,#187407,#187408,
#187409,#187410,#187411,#187412,#187413,#187414,#187415,#187416,#187417,
#187418,#187419,#187420,#187421,#187422,#187423,#187424,#187425),
 .UNSPECIFIED.,.F.,.F.,(4,3,3,3,3,3,3,3,3,3,3,3,3,3,3,3,3,3,3,3,3,3,3,3,
3,3,3,3,3,3,3,3,3,3,3,3,3,3,3,3,3,3,3,3,3,3,3,3,3,3,3,3,3,3,3,3,3,3,3,3,
3,3,3,3,3,3,3,3,3,3,3,3,3,3,3,3,3,3,3,3,3,3,4),(-60.6412095134584,-60.5590784046771,
-60.4793357811508,-60.3995857810152,-60.3198128184427,-60.235899774634,
-60.1559884534018,-60.0760181955046,-59.995936002992,-59.9841606432079,
-59.9042033430767,-59.8243405458341,-59.7445547233624,-59.664828408167,
-59.5851441798728,-59.5054731936519,-59.4258057401261,-59.3461260893097,
-59.2664185069152,-59.1866232778397,-59.106778936132,-59.0268205090847,
-58.9844246324877,-58.9044673323564,-58.8246045351137,-58.7448187126417,
-58.6650923974462,-58.5854081691519,-58.5057371829309,-58.4260697294049,
-58.3463900785883,-58.2666824961936,-58.186887267118,-58.1070429254103,
-58.0270844983627,-57.9846886217676,-57.9047313216364,-57.8248685243939,
-57.7450827019221,-57.6653563867272,-57.5856721584333,-57.5060011722124,
-57.4263337186865,-57.3466540678699,-57.2669464854756,-57.1871512564001,
-57.1073069146926,-57.0273484876453,-56.9849526110475,-56.9049953109163,
-56.8251325136738,-56.7453466912019,-56.6656203760066,-56.5859361477129,
-56.5062651614919,-56.4265977079658,-56.3469180571494,-56.2672104747552,
-56.1874152456796,-56.1075709039718,-56.0276124769243,-55.9852166003274,
-55.9052593001963,-55.8253965029537,-55.7456106804819,-55.665884365286,
-55.5862001369919,-55.506529150771,-55.426861697245,-55.3471820464283,-55.2674744640334,
-55.1876792349578,-55.1078348932506,-55.0278764662033,-54.9854805896072,
-54.9049169077671,-54.8244508849754,-54.7440673257589,-54.6637510888401,
-54.5834913281942,-54.5032654666035,-54.4230482427655,-54.3580242062788),
 .UNSPECIFIED.);
#1659=B_SPLINE_CURVE_WITH_KNOTS('',3,(#187427,#187428,#187429,#187430,#187431,
#187432,#187433,#187434,#187435,#187436),.UNSPECIFIED.,.F.,.F.,(4,1,1,1,
1,1,1,4),(-54.3580165317574,-53.9857445788871,-52.9860085681669,-51.9862725574468,
-50.9865365467267,-49.9868005360066,-48.9870645252864,-48.0748476368028),
 .UNSPECIFIED.);
#1660=B_SPLINE_CURVE_WITH_KNOTS('',3,(#187438,#187439,#187440,#187441,#187442,
#187443,#187444,#187445,#187446,#187447,#187448,#187449,#187450,#187451,
#187452,#187453,#187454,#187455,#187456,#187457,#187458,#187459,#187460,
#187461,#187462,#187463,#187464,#187465,#187466,#187467,#187468,#187469,
#187470,#187471,#187472,#187473,#187474,#187475,#187476,#187477,#187478,
#187479,#187480,#187481,#187482,#187483,#187484,#187485,#187486,#187487,
#187488,#187489,#187490,#187491,#187492,#187493,#187494,#187495,#187496,
#187497,#187498,#187499,#187500,#187501,#187502,#187503,#187504,#187505,
#187506,#187507,#187508,#187509,#187510,#187511,#187512,#187513,#187514,
#187515,#187516,#187517,#187518,#187519,#187520,#187521,#187522,#187523,
#187524,#187525,#187526,#187527,#187528,#187529,#187530,#187531,#187532,
#187533,#187534,#187535,#187536,#187537,#187538,#187539,#187540,#187541,
#187542,#187543,#187544,#187545,#187546,#187547,#187548,#187549,#187550,
#187551,#187552,#187553,#187554,#187555,#187556,#187557,#187558,#187559,
#187560,#187561,#187562,#187563,#187564,#187565,#187566,#187567,#187568,
#187569,#187570,#187571,#187572,#187573,#187574,#187575,#187576,#187577,
#187578,#187579,#187580,#187581,#187582,#187583,#187584,#187585,#187586,
#187587,#187588,#187589,#187590,#187591,#187592,#187593,#187594,#187595,
#187596,#187597,#187598,#187599,#187600,#187601,#187602,#187603,#187604,
#187605,#187606,#187607,#187608,#187609,#187610,#187611,#187612,#187613,
#187614,#187615,#187616,#187617,#187618,#187619,#187620,#187621,#187622,
#187623,#187624,#187625,#187626,#187627,#187628,#187629,#187630,#187631,
#187632,#187633,#187634,#187635,#187636,#187637,#187638,#187639,#187640,
#187641,#187642,#187643,#187644,#187645,#187646,#187647,#187648,#187649,
#187650,#187651,#187652,#187653,#187654,#187655,#187656,#187657,#187658,
#187659,#187660,#187661,#187662,#187663,#187664,#187665,#187666,#187667,
#187668,#187669,#187670,#187671,#187672,#187673,#187674,#187675,#187676,
#187677,#187678,#187679,#187680,#187681),.UNSPECIFIED.,.F.,.F.,(4,3,3,3,
3,3,3,3,3,3,3,3,3,3,3,3,3,3,3,3,3,3,3,3,3,3,3,3,3,3,3,3,3,3,3,3,3,3,3,3,
3,3,3,3,3,3,3,3,3,3,3,3,3,3,3,3,3,3,3,3,3,3,3,3,3,3,3,3,3,3,3,3,3,3,3,3,
3,3,3,3,3,4),(-48.0748388990992,-47.9873285145663,-47.9073712144349,-47.8275084171922,
-47.7477225947202,-47.6679962795249,-47.5883120512307,-47.5086410650096,
-47.4289736114836,-47.3492939606671,-47.2695863782722,-47.1897911491966,
-47.1099468074887,-47.0299883804412,-46.9875925038462,-46.9076352037149,
-46.8277724064724,-46.7479865840006,-46.6682602688053,-46.5885760405113,
-46.5089050542904,-46.4292376007644,-46.3495579499479,-46.2698503675534,
-46.1900551384779,-46.1102107967703,-46.0302523697229,-45.987856493126,
-45.9078991929947,-45.8280363957522,-45.7482505732803,-45.668524258085,
-45.5888400297908,-45.5091690435699,-45.429501590044,-45.3498219392276,
-45.270114356833,-45.1903191277575,-45.1104747860499,-45.0305163590025,
-44.9881204824059,-44.9081631822747,-44.8283003850321,-44.7485145625602,
-44.668788247365,-44.5891040190709,-44.50943303285,-44.4297655793241,-44.3500859285076,
-44.2703783461131,-44.1905831170376,-44.1107387753299,-44.0307803482826,
-43.9883844716858,-43.9084271715545,-43.8285643743119,-43.74877855184,-43.6690522366447,
-43.5893680083507,-43.5096970221298,-43.4300295686039,-43.3503499177874,
-43.2706423353929,-43.1908471063174,-43.1110027646097,-43.0310443375623,
-42.9886484609656,-42.9086911608343,-42.8288283635917,-42.7490425411198,
-42.6693162259245,-42.5896319976304,-42.5099610114094,-42.4302935578836,
-42.3506139070671,-42.2709063246724,-42.1911110955969,-42.1112667538892,
-42.0313083268418,-41.9889124502455,-41.8733272325874,-41.7916535919196),
 .UNSPECIFIED.);
#1661=B_SPLINE_CURVE_WITH_KNOTS('',3,(#187683,#187684,#187685,#187686,#187687,
#187688,#187689,#187690,#187691,#187692),.UNSPECIFIED.,.F.,.F.,(4,1,1,1,
1,1,1,4),(-41.7916500544357,-40.9891764395254,-39.9894404288052,-38.9897044180851,
-37.989968407365,-36.9902323966448,-35.9904963859247,-35.50846828474),
 .UNSPECIFIED.);
#1662=B_SPLINE_CURVE_WITH_KNOTS('',3,(#187694,#187695,#187696,#187697,#187698,
#187699,#187700,#187701,#187702,#187703),.UNSPECIFIED.,.F.,.F.,(4,1,1,1,
1,1,1,4),(-35.50846828474,-34.9907603752046,-33.9910243644845,-32.9912883537643,
-31.9915523430442,-30.9918163323241,-29.9920803216039,-29.2252829775605),
 .UNSPECIFIED.);
#1663=B_SPLINE_CURVE_WITH_KNOTS('',3,(#187705,#187706,#187707,#187708,#187709,
#187710,#187711,#187712,#187713,#187714,#187715),.UNSPECIFIED.,.F.,.F.,
(4,1,1,1,1,1,1,1,4),(-29.2252829775605,-28.9923443108838,-27.9926083001637,
-26.9928722894435,-25.9931362787234,-24.9934002680033,-23.9936642572832,
-22.993928246563,-22.9420976703809),.UNSPECIFIED.);
#1664=B_SPLINE_CURVE_WITH_KNOTS('',3,(#187717,#187718,#187719,#187720,#187721,
#187722,#187723,#187724,#187725,#187726),.UNSPECIFIED.,.F.,.F.,(4,1,1,1,
1,1,1,4),(-22.9420976703809,-21.9941922358429,-20.9944562251228,-19.9947202144026,
-18.9949842036825,-17.9952481929624,-16.9955121822422,-16.6589198685825),
 .UNSPECIFIED.);
#1665=B_SPLINE_CURVE_WITH_KNOTS('',3,(#187728,#187729,#187730,#187731,#187732,
#187733,#187734,#187735,#187736,#187737,#187738,#187739,#187740,#187741,
#187742,#187743,#187744,#187745,#187746,#187747,#187748,#187749,#187750,
#187751,#187752,#187753,#187754,#187755,#187756,#187757,#187758,#187759,
#187760,#187761,#187762,#187763,#187764,#187765,#187766,#187767,#187768,
#187769,#187770,#187771,#187772,#187773,#187774,#187775,#187776,#187777,
#187778,#187779,#187780,#187781,#187782,#187783,#187784,#187785,#187786,
#187787,#187788,#187789,#187790,#187791,#187792,#187793,#187794,#187795,
#187796,#187797,#187798,#187799,#187800,#187801,#187802,#187803,#187804,
#187805,#187806,#187807,#187808,#187809,#187810,#187811,#187812,#187813,
#187814,#187815,#187816,#187817,#187818,#187819,#187820,#187821,#187822,
#187823,#187824,#187825,#187826,#187827,#187828,#187829,#187830,#187831,
#187832,#187833,#187834,#187835,#187836,#187837,#187838,#187839,#187840,
#187841,#187842,#187843,#187844,#187845,#187846,#187847,#187848,#187849,
#187850,#187851,#187852,#187853,#187854,#187855,#187856,#187857,#187858,
#187859,#187860,#187861,#187862,#187863,#187864,#187865,#187866,#187867,
#187868,#187869,#187870,#187871,#187872,#187873,#187874,#187875,#187876,
#187877,#187878,#187879,#187880,#187881,#187882,#187883,#187884,#187885,
#187886,#187887,#187888,#187889,#187890,#187891,#187892,#187893,#187894,
#187895,#187896,#187897,#187898,#187899,#187900,#187901,#187902,#187903,
#187904,#187905,#187906,#187907,#187908,#187909,#187910,#187911,#187912,
#187913,#187914,#187915,#187916,#187917,#187918,#187919,#187920,#187921,
#187922,#187923,#187924,#187925,#187926,#187927,#187928,#187929,#187930,
#187931,#187932,#187933,#187934,#187935,#187936,#187937,#187938,#187939,
#187940,#187941,#187942,#187943,#187944,#187945,#187946,#187947,#187948,
#187949,#187950,#187951,#187952,#187953,#187954,#187955,#187956,#187957,
#187958,#187959,#187960,#187961,#187962,#187963,#187964,#187965,#187966,
#187967,#187968,#187969,#187970,#187971,#187972,#187973,#187974),
 .UNSPECIFIED.,.F.,.F.,(4,3,3,3,3,3,3,3,3,3,3,3,3,3,3,3,3,3,3,3,3,3,3,3,
3,3,3,3,3,3,3,3,3,3,3,3,3,3,3,3,3,3,3,3,3,3,3,3,3,3,3,3,3,3,3,3,3,3,3,3,
3,3,3,3,3,3,3,3,3,3,3,3,3,3,3,3,3,3,3,3,3,3,4),(-16.6589123632013,-16.5760203392414,
-16.4963658357425,-16.4167062586062,-16.3370259313394,-16.257309167994,
-16.1774967883031,-16.0976279107091,-16.0176451019278,-15.9957761715221,
-15.9158187324329,-15.8359557956803,-15.7561698332831,-15.6764433778821,
-15.5967590092361,-15.5170878828934,-15.4374202894017,-15.3577404988956,
-15.2780327772076,-15.198237410145,-15.118392930983,-15.0384343685027,-14.996040160802,
-14.9160831648467,-14.8362206718143,-14.7564351533039,-14.6767091415404,
-14.5970252158687,-14.5173545301081,-14.4376873756752,-14.3580080223317,
-14.278300735536,-14.1985057977278,-14.1186617452726,-14.0387036018344,
-13.9963041500818,-13.9163467244748,-13.8364838036549,-13.7566978595949,
-13.6769714248916,-13.5972870792623,-13.5176159792993,-13.4379484142671,
-13.3582686542674,-13.2785609651013,-13.1987656334396,-13.1189211913599,
-13.0389626682531,-12.9965681393617,-12.9166100108447,-12.8367463812177,
-12.7569597231879,-12.6772325700763,-12.5975475023185,-12.5178756770059,
-12.4382073847008,-12.3585268961407,-12.2788184777613,-12.199022419603,
-12.1191772514785,-12.0392180093319,-11.9968321286416,-11.9168769666291,
-11.8370163088955,-11.7572326253178,-11.6775084464124,-11.5978263498226,
-11.5181574817392,-11.4384921377459,-11.3588145860714,-11.2791090906347,
-11.1993159195183,-11.1194736224419,-11.0395172015575,-10.9970961179214,
-10.9164104612956,-10.8358235390977,-10.7553203015422,-10.6748857539066,
-10.5945105281505,-10.5141705799335,-10.4338432861696,-10.3757270560217),
 .UNSPECIFIED.);
#1666=B_SPLINE_CURVE_WITH_KNOTS('',3,(#187975,#187976,#187977,#187978,#187979,
#187980,#187981,#187982,#187983,#187984),.UNSPECIFIED.,.F.,.F.,(4,1,1,1,
1,1,1,4),(-10.3757194590647,-9.99736010720131,-8.99762409648118,-7.99788808576105,
-6.99815207504092,-5.99841606432079,-4.99868005360065,-4.09255001849307),
 .UNSPECIFIED.);
#1667=B_SPLINE_CURVE_WITH_KNOTS('',3,(#187987,#187988,#187989,#187990,#187991,
#187992,#187993,#187994,#187995,#187996),.UNSPECIFIED.,.F.,.F.,(4,3,3,4),
(1693.06690371234,1693.1506377533,1693.17139155035,1693.3184402849),
 .UNSPECIFIED.);
#1668=B_SPLINE_CURVE_WITH_KNOTS('',3,(#187998,#187999,#188000,#188001,#188002,
#188003,#188004,#188005,#188006,#188007,#188008,#188009,#188010,#188011,
#188012,#188013,#188014,#188015,#188016,#188017,#188018,#188019,#188020,
#188021,#188022,#188023,#188024,#188025,#188026,#188027,#188028,#188029,
#188030,#188031,#188032,#188033,#188034,#188035,#188036,#188037,#188038,
#188039,#188040,#188041,#188042,#188043,#188044,#188045,#188046,#188047,
#188048,#188049,#188050,#188051,#188052,#188053,#188054,#188055,#188056,
#188057,#188058,#188059,#188060,#188061,#188062,#188063,#188064,#188065,
#188066,#188067,#188068,#188069,#188070,#188071,#188072,#188073,#188074,
#188075,#188076,#188077,#188078,#188079,#188080,#188081,#188082,#188083,
#188084,#188085,#188086,#188087,#188088,#188089,#188090,#188091,#188092,
#188093,#188094,#188095,#188096,#188097,#188098,#188099,#188100,#188101,
#188102,#188103,#188104,#188105,#188106,#188107,#188108,#188109,#188110,
#188111,#188112,#188113,#188114,#188115,#188116,#188117,#188118,#188119,
#188120,#188121,#188122,#188123,#188124,#188125,#188126,#188127,#188128,
#188129,#188130,#188131,#188132,#188133,#188134,#188135,#188136,#188137,
#188138,#188139,#188140,#188141,#188142,#188143,#188144,#188145,#188146,
#188147,#188148,#188149,#188150,#188151,#188152,#188153,#188154,#188155,
#188156,#188157,#188158,#188159,#188160,#188161,#188162,#188163,#188164,
#188165,#188166,#188167,#188168,#188169,#188170,#188171,#188172,#188173,
#188174,#188175,#188176,#188177,#188178,#188179,#188180,#188181,#188182,
#188183,#188184,#188185,#188186,#188187,#188188,#188189,#188190,#188191,
#188192,#188193,#188194,#188195,#188196,#188197,#188198,#188199,#188200,
#188201,#188202,#188203,#188204,#188205,#188206,#188207,#188208,#188209,
#188210,#188211),.UNSPECIFIED.,.F.,.F.,(4,3,3,3,3,3,3,3,3,3,3,3,3,3,3,3,
3,3,3,3,3,3,3,3,3,3,3,3,3,3,3,3,3,3,3,3,3,3,3,3,3,3,3,3,3,3,3,3,3,3,3,3,
3,3,3,3,3,3,3,3,3,3,3,3,3,3,3,3,3,3,3,4),(1693.31844028502,1693.4008614421,
1693.48319961379,1693.5691906072,1693.65143266586,1693.73366105159,1693.81589478312,
1693.89815288144,1693.98049848208,1694.0628955963,1694.14540833862,1694.17112756107,
1694.25489318401,1694.33855582112,1694.42213557425,1694.50565247357,1694.58913402256,
1694.67259819274,1694.75606303016,1694.83954657748,1694.92311870335,1695.00673539827,
1695.09048596028,1695.17086357179,1695.25449860037,1695.33803025765,1695.42147878235,
1695.50486434011,1695.58821483354,1695.67154813761,1695.75488241889,1695.83823584083,
1695.92167925488,1696.00516779981,1696.088792476,1696.17059958251,1696.25445516476,
1696.33820713564,1696.42187551199,1696.50548023893,1696.58904810639,1696.67259766383,
1696.75614687949,1696.83971371749,1696.92336695497,1697.00706370128,1697.09089170662,
1697.17033559323,1697.25421280583,1697.33798830632,1697.42168206028,1697.50531396346,
1697.58891161285,1697.6724925293,1697.75607464121,1697.8396758739,1697.92336565213,
1698.00710016425,1698.09096762072,1698.17007160395,1698.25229074706,1698.33440658285,
1698.4164405015,1698.50181651835,1698.58375783067,1698.665686824,1698.74762265115,
1698.82958446971,1698.91163608436,1698.99374084933,1699.0759627348,1699.09944863636),
 .UNSPECIFIED.);
#1669=B_SPLINE_CURVE_WITH_KNOTS('',3,(#188215,#188216,#188217,#188218,#188219,
#188220,#188221,#188222,#188223,#188224,#188225,#188226,#188227,#188228,
#188229,#188230,#188231,#188232,#188233,#188234,#188235,#188236,#188237,
#188238,#188239,#188240,#188241,#188242,#188243,#188244,#188245,#188246,
#188247,#188248,#188249,#188250,#188251,#188252,#188253,#188254,#188255,
#188256,#188257,#188258,#188259,#188260,#188261,#188262,#188263,#188264,
#188265,#188266,#188267,#188268,#188269,#188270,#188271,#188272,#188273,
#188274,#188275,#188276,#188277,#188278,#188279,#188280,#188281,#188282,
#188283,#188284,#188285,#188286,#188287,#188288,#188289,#188290,#188291,
#188292,#188293,#188294,#188295,#188296,#188297,#188298,#188299,#188300,
#188301,#188302,#188303,#188304,#188305,#188306,#188307,#188308,#188309,
#188310,#188311,#188312,#188313,#188314,#188315,#188316,#188317,#188318,
#188319,#188320,#188321,#188322,#188323,#188324,#188325,#188326,#188327,
#188328,#188329,#188330,#188331,#188332,#188333,#188334,#188335,#188336,
#188337,#188338,#188339,#188340,#188341,#188342,#188343,#188344,#188345,
#188346,#188347,#188348,#188349,#188350,#188351,#188352,#188353,#188354,
#188355,#188356,#188357,#188358,#188359,#188360,#188361,#188362,#188363,
#188364,#188365,#188366,#188367,#188368,#188369,#188370,#188371,#188372,
#188373,#188374,#188375,#188376,#188377),.UNSPECIFIED.,.F.,.F.,(4,3,3,3,
3,3,3,3,3,3,3,3,3,3,3,3,3,3,3,3,3,3,3,3,3,3,3,3,3,3,3,3,3,3,3,3,3,3,3,3,
3,3,3,3,3,3,3,3,3,3,3,3,3,3,4),(1693.3184402849,1693.40445195466,1693.49052691538,
1693.57667826784,1693.66297932812,1693.74936613508,1693.8359058484,1693.86083694135,
1693.94471415395,1694.02848965444,1694.1121834084,1694.19581531157,1694.27941296097,
1694.36299387742,1694.44657598933,1694.53017722202,1694.61386700025,1694.69760151237,
1694.78146896884,1694.86057295207,1694.94357842618,1695.02647983489,1695.10929799024,
1695.19205362182,1695.27558553944,1695.35829320941,1695.44100417102,1695.52373709062,
1695.60788005866,1695.69075989804,1695.77553443042,1695.86030896279,1695.94531027662,
1696.03020068413,1696.11499871164,1696.19972280846,1696.2843898248,1696.36902560792,
1696.45364676064,1696.53826987213,1696.62294846804,1696.70765480488,1696.79245608915,
1696.86004497351,1696.94393615237,1697.02775838711,1697.11153137067,1697.19527348557,
1697.27902402691,1697.35991297887,1697.45761556266,1697.55815691806,1697.65637442568,
1697.75807770495,1697.85978098423),.UNSPECIFIED.);
#1670=B_SPLINE_CURVE_WITH_KNOTS('',3,(#188378,#188379,#188380,#188381,#188382,
#188383,#188384,#188385,#188386,#188387),.UNSPECIFIED.,.F.,.F.,(4,3,3,4),
(1693.06812991347,1693.15787446388,1693.24735628336,1693.3184402848),
 .UNSPECIFIED.);
#1671=B_SPLINE_CURVE_WITH_KNOTS('',3,(#188398,#188399,#188400,#188401,#188402,
#188403,#188404,#188405,#188406,#188407,#188408,#188409,#188410,#188411,
#188412,#188413,#188414,#188415,#188416,#188417,#188418,#188419,#188420,
#188421,#188422,#188423,#188424,#188425,#188426,#188427,#188428,#188429,
#188430,#188431,#188432,#188433,#188434,#188435,#188436,#188437,#188438,
#188439,#188440,#188441,#188442,#188443,#188444,#188445,#188446,#188447,
#188448,#188449,#188450,#188451,#188452,#188453,#188454,#188455,#188456,
#188457,#188458,#188459,#188460,#188461,#188462,#188463,#188464,#188465,
#188466,#188467,#188468,#188469,#188470,#188471,#188472,#188473,#188474,
#188475,#188476,#188477,#188478,#188479,#188480,#188481,#188482,#188483,
#188484,#188485,#188486,#188487,#188488,#188489,#188490,#188491,#188492,
#188493,#188494,#188495,#188496,#188497,#188498,#188499,#188500,#188501,
#188502,#188503),.UNSPECIFIED.,.F.,.F.,(4,3,3,3,3,3,3,3,3,3,3,3,3,3,3,3,
3,3,3,3,3,3,3,3,3,3,3,3,3,3,3,3,3,3,3,4),(0.,0.0349249411505533,0.077348853415627,
0.121065958001284,0.164783062586941,0.189329869490245,0.195424600648578,
0.241029503011481,0.286450338806425,0.332357184633421,0.37784421010019,
0.390926586700649,0.397162835114324,0.444154447221939,0.491251570163209,
0.537752846290075,0.557531973039803,0.592379688295695,0.602095847517636,
0.609874760882364,0.656076546176515,0.703084256260691,0.75095048994342,
0.793453887845117,0.814883791466027,0.821323462530115,0.828310165375817,
0.836313695086938,0.885124880906474,0.93393606672601,0.958011516551483,
0.969491304425174,0.977480420947961,1.02729690957154,1.07695759308116,1.1265396653275),
 .UNSPECIFIED.);
#1672=B_SPLINE_CURVE_WITH_KNOTS('',3,(#188504,#188505,#188506,#188507,#188508,
#188509,#188510,#188511,#188512,#188513,#188514,#188515,#188516,#188517,
#188518,#188519,#188520,#188521,#188522,#188523,#188524,#188525,#188526,
#188527,#188528,#188529,#188530,#188531,#188532,#188533,#188534,#188535,
#188536,#188537,#188538,#188539,#188540,#188541,#188542,#188543,#188544,
#188545,#188546,#188547,#188548,#188549,#188550,#188551,#188552,#188553,
#188554,#188555,#188556,#188557,#188558,#188559,#188560,#188561,#188562,
#188563,#188564,#188565,#188566,#188567,#188568,#188569,#188570,#188571,
#188572,#188573,#188574,#188575,#188576,#188577,#188578,#188579,#188580,
#188581,#188582,#188583,#188584,#188585,#188586,#188587,#188588,#188589,
#188590,#188591,#188592,#188593,#188594,#188595,#188596,#188597,#188598,
#188599,#188600,#188601,#188602,#188603,#188604,#188605,#188606,#188607,
#188608,#188609,#188610,#188611,#188612),.UNSPECIFIED.,.F.,.F.,(4,3,3,3,
3,3,3,3,3,3,3,3,3,3,3,3,3,3,3,3,3,3,3,3,3,3,3,3,3,3,3,3,3,3,3,3,4),(0.,
0.041701088542356,0.0909472972506543,0.141057893902492,0.191015907286953,
0.217221518357794,0.225657279792899,0.231692767572414,0.280603377364562,
0.329547178464156,0.377736289482342,0.425495421787918,0.43983668838786,
0.446522460479898,0.452442110700344,0.499701052287928,0.546385278965876,
0.591957470686799,0.610305684420423,0.652878075156173,0.658871161398199,
0.664713829125931,0.71062307702576,0.756799778329133,0.802540179953837,
0.839581075287956,0.858865496482928,0.865300881974491,0.876732522103725,
0.92192199373265,0.966865006644529,0.987435883002153,0.996596083696916,
1.00397196471875,1.04808827133039,1.09146893286586,1.13094109509354),
 .UNSPECIFIED.);
#1673=B_SPLINE_CURVE_WITH_KNOTS('',3,(#195422,#195423,#195424,#195425,#195426,
#195427,#195428,#195429,#195430,#195431,#195432,#195433,#195434,#195435,
#195436,#195437,#195438,#195439,#195440,#195441,#195442,#195443,#195444,
#195445,#195446,#195447,#195448,#195449,#195450,#195451,#195452,#195453,
#195454,#195455,#195456,#195457,#195458,#195459,#195460,#195461,#195462,
#195463,#195464,#195465,#195466,#195467,#195468,#195469,#195470,#195471,
#195472,#195473,#195474,#195475,#195476,#195477,#195478,#195479,#195480,
#195481,#195482,#195483,#195484,#195485,#195486,#195487,#195488,#195489,
#195490,#195491,#195492,#195493,#195494,#195495,#195496,#195497,#195498,
#195499,#195500,#195501,#195502,#195503,#195504,#195505,#195506,#195507,
#195508,#195509,#195510,#195511,#195512,#195513,#195514,#195515,#195516,
#195517,#195518,#195519,#195520,#195521,#195522,#195523,#195524,#195525,
#195526,#195527,#195528,#195529,#195530,#195531,#195532,#195533),
 .UNSPECIFIED.,.F.,.F.,(4,3,3,3,3,3,3,3,3,3,3,3,3,3,3,3,3,3,3,3,3,3,3,3,
3,3,3,3,3,3,3,3,3,3,3,3,3,4),(8.35256518316599E-5,0.041701088540131,0.0910835065821966,
0.141049325530906,0.19113697887595,0.217221517785501,0.225657277714787,
0.231692761965483,0.280603371493228,0.329547172995227,0.377736284294025,
0.425495416317654,0.439836687990196,0.446522457868978,0.452442110036265,
0.499758065245721,0.546067231244348,0.59195747025222,0.610305684420784,
0.643609039131399,0.652878075055363,0.658871161296266,0.664713829119152,
0.710623077230221,0.756799777861816,0.802540179620603,0.839581075225947,
0.858865496404956,0.865300878338205,0.876732522105704,0.921906064998915,
0.966935138622801,0.987435883182548,0.996596084006623,1.00397196652038,
1.04808827280157,1.09146893461145,1.13094109510077),.UNSPECIFIED.);
#1674=B_SPLINE_CURVE_WITH_KNOTS('',3,(#202314,#202315,#202316,#202317,#202318,
#202319,#202320,#202321,#202322,#202323,#202324,#202325,#202326,#202327,
#202328,#202329,#202330,#202331,#202332,#202333,#202334,#202335,#202336,
#202337,#202338,#202339,#202340,#202341,#202342,#202343,#202344,#202345,
#202346,#202347,#202348,#202349,#202350,#202351,#202352,#202353,#202354,
#202355,#202356,#202357,#202358,#202359,#202360,#202361,#202362,#202363,
#202364,#202365,#202366,#202367,#202368,#202369,#202370,#202371,#202372,
#202373,#202374,#202375,#202376,#202377,#202378,#202379,#202380,#202381,
#202382,#202383,#202384,#202385,#202386,#202387,#202388,#202389,#202390,
#202391,#202392,#202393,#202394,#202395,#202396,#202397,#202398,#202399,
#202400,#202401,#202402,#202403,#202404,#202405,#202406,#202407,#202408,
#202409,#202410,#202411,#202412,#202413,#202414,#202415,#202416,#202417,
#202418,#202419),.UNSPECIFIED.,.F.,.F.,(4,3,3,3,3,3,3,3,3,3,3,3,3,3,3,3,
3,3,3,3,3,3,3,3,3,3,3,3,3,3,3,3,3,3,3,4),(0.,0.0349249411503097,0.0774968629053873,
0.120798554477859,0.164983976463475,0.189329869243756,0.195424599752804,
0.241029502145285,0.286450337938425,0.33235718364418,0.377844209322727,
0.390926586284597,0.397162832866434,0.444107542409823,0.491089657327383,
0.537752844152331,0.557531973038066,0.592379688293954,0.602095847495157,
0.609874759394341,0.65562314585235,0.70310861257605,0.75059407929975,0.793453887192463,
0.814883791138819,0.821323461655805,0.828310165215568,0.836313695085176,
0.885124880977893,0.93393606687061,0.958011516677791,0.969491304629128,
0.977480415130059,1.02729689945038,1.07695758373463,1.12653966532806),
 .UNSPECIFIED.);
#1943=SHAPE_REPRESENTATION_RELATIONSHIP('SRR','None',#279302,#1952);
#1952=ADVANCED_BREP_SHAPE_REPRESENTATION('',(#1970),#279258);
#1961=STYLED_ITEM('',(#279355),#1970);
#1970=MANIFOLD_SOLID_BREP('Body1',#14939);
#1987=FACE_BOUND('',#2891,.T.);
#1988=FACE_BOUND('',#2894,.T.);
#2043=PLANE('',#15379);
#2044=PLANE('',#15384);
#2045=PLANE('',#15385);
#2046=PLANE('',#15386);
#2047=PLANE('',#15388);
#2048=PLANE('',#15389);
#2049=PLANE('',#15395);
#2050=PLANE('',#15396);
#2141=FACE_OUTER_BOUND('',#2620,.T.);
#2142=FACE_OUTER_BOUND('',#2621,.T.);
#2143=FACE_OUTER_BOUND('',#2622,.T.);
#2144=FACE_OUTER_BOUND('',#2623,.T.);
#2145=FACE_OUTER_BOUND('',#2624,.T.);
#2146=FACE_OUTER_BOUND('',#2625,.T.);
#2147=FACE_OUTER_BOUND('',#2626,.T.);
#2148=FACE_OUTER_BOUND('',#2627,.T.);
#2149=FACE_OUTER_BOUND('',#2628,.T.);
#2150=FACE_OUTER_BOUND('',#2629,.T.);
#2151=FACE_OUTER_BOUND('',#2630,.T.);
#2152=FACE_OUTER_BOUND('',#2631,.T.);
#2153=FACE_OUTER_BOUND('',#2632,.T.);
#2154=FACE_OUTER_BOUND('',#2633,.T.);
#2155=FACE_OUTER_BOUND('',#2634,.T.);
#2156=FACE_OUTER_BOUND('',#2635,.T.);
#2157=FACE_OUTER_BOUND('',#2636,.T.);
#2158=FACE_OUTER_BOUND('',#2637,.T.);
#2159=FACE_OUTER_BOUND('',#2638,.T.);
#2160=FACE_OUTER_BOUND('',#2639,.T.);
#2161=FACE_OUTER_BOUND('',#2640,.T.);
#2162=FACE_OUTER_BOUND('',#2641,.T.);
#2163=FACE_OUTER_BOUND('',#2642,.T.);
#2164=FACE_OUTER_BOUND('',#2643,.T.);
#2165=FACE_OUTER_BOUND('',#2644,.T.);
#2166=FACE_OUTER_BOUND('',#2645,.T.);
#2167=FACE_OUTER_BOUND('',#2646,.T.);
#2168=FACE_OUTER_BOUND('',#2647,.T.);
#2169=FACE_OUTER_BOUND('',#2648,.T.);
#2170=FACE_OUTER_BOUND('',#2649,.T.);
#2171=FACE_OUTER_BOUND('',#2650,.T.);
#2172=FACE_OUTER_BOUND('',#2651,.T.);
#2173=FACE_OUTER_BOUND('',#2652,.T.);
#2174=FACE_OUTER_BOUND('',#2653,.T.);
#2175=FACE_OUTER_BOUND('',#2654,.T.);
#2176=FACE_OUTER_BOUND('',#2655,.T.);
#2177=FACE_OUTER_BOUND('',#2656,.T.);
#2178=FACE_OUTER_BOUND('',#2657,.T.);
#2179=FACE_OUTER_BOUND('',#2658,.T.);
#2180=FACE_OUTER_BOUND('',#2659,.T.);
#2181=FACE_OUTER_BOUND('',#2660,.T.);
#2182=FACE_OUTER_BOUND('',#2661,.T.);
#2183=FACE_OUTER_BOUND('',#2662,.T.);
#2184=FACE_OUTER_BOUND('',#2663,.T.);
#2185=FACE_OUTER_BOUND('',#2664,.T.);
#2186=FACE_OUTER_BOUND('',#2665,.T.);
#2187=FACE_OUTER_BOUND('',#2666,.T.);
#2188=FACE_OUTER_BOUND('',#2667,.T.);
#2189=FACE_OUTER_BOUND('',#2668,.T.);
#2190=FACE_OUTER_BOUND('',#2669,.T.);
#2191=FACE_OUTER_BOUND('',#2670,.T.);
#2192=FACE_OUTER_BOUND('',#2671,.T.);
#2193=FACE_OUTER_BOUND('',#2672,.T.);
#2194=FACE_OUTER_BOUND('',#2673,.T.);
#2195=FACE_OUTER_BOUND('',#2674,.T.);
#2196=FACE_OUTER_BOUND('',#2675,.T.);
#2197=FACE_OUTER_BOUND('',#2676,.T.);
#2198=FACE_OUTER_BOUND('',#2677,.T.);
#2199=FACE_OUTER_BOUND('',#2678,.T.);
#2200=FACE_OUTER_BOUND('',#2679,.T.);
#2201=FACE_OUTER_BOUND('',#2680,.T.);
#2202=FACE_OUTER_BOUND('',#2681,.T.);
#2203=FACE_OUTER_BOUND('',#2682,.T.);
#2204=FACE_OUTER_BOUND('',#2683,.T.);
#2205=FACE_OUTER_BOUND('',#2684,.T.);
#2206=FACE_OUTER_BOUND('',#2685,.T.);
#2207=FACE_OUTER_BOUND('',#2686,.T.);
#2208=FACE_OUTER_BOUND('',#2687,.T.);
#2209=FACE_OUTER_BOUND('',#2688,.T.);
#2210=FACE_OUTER_BOUND('',#2689,.T.);
#2211=FACE_OUTER_BOUND('',#2690,.T.);
#2212=FACE_OUTER_BOUND('',#2691,.T.);
#2213=FACE_OUTER_BOUND('',#2692,.T.);
#2214=FACE_OUTER_BOUND('',#2693,.T.);
#2215=FACE_OUTER_BOUND('',#2694,.T.);
#2216=FACE_OUTER_BOUND('',#2695,.T.);
#2217=FACE_OUTER_BOUND('',#2696,.T.);
#2218=FACE_OUTER_BOUND('',#2697,.T.);
#2219=FACE_OUTER_BOUND('',#2698,.T.);
#2220=FACE_OUTER_BOUND('',#2699,.T.);
#2221=FACE_OUTER_BOUND('',#2700,.T.);
#2222=FACE_OUTER_BOUND('',#2701,.T.);
#2223=FACE_OUTER_BOUND('',#2702,.T.);
#2224=FACE_OUTER_BOUND('',#2703,.T.);
#2225=FACE_OUTER_BOUND('',#2704,.T.);
#2226=FACE_OUTER_BOUND('',#2705,.T.);
#2227=FACE_OUTER_BOUND('',#2706,.T.);
#2228=FACE_OUTER_BOUND('',#2707,.T.);
#2229=FACE_OUTER_BOUND('',#2708,.T.);
#2230=FACE_OUTER_BOUND('',#2709,.T.);
#2231=FACE_OUTER_BOUND('',#2710,.T.);
#2232=FACE_OUTER_BOUND('',#2711,.T.);
#2233=FACE_OUTER_BOUND('',#2712,.T.);
#2234=FACE_OUTER_BOUND('',#2713,.T.);
#2235=FACE_OUTER_BOUND('',#2714,.T.);
#2236=FACE_OUTER_BOUND('',#2715,.T.);
#2237=FACE_OUTER_BOUND('',#2716,.T.);
#2238=FACE_OUTER_BOUND('',#2717,.T.);
#2239=FACE_OUTER_BOUND('',#2718,.T.);
#2240=FACE_OUTER_BOUND('',#2719,.T.);
#2241=FACE_OUTER_BOUND('',#2720,.T.);
#2242=FACE_OUTER_BOUND('',#2721,.T.);
#2243=FACE_OUTER_BOUND('',#2722,.T.);
#2244=FACE_OUTER_BOUND('',#2723,.T.);
#2245=FACE_OUTER_BOUND('',#2724,.T.);
#2246=FACE_OUTER_BOUND('',#2725,.T.);
#2247=FACE_OUTER_BOUND('',#2726,.T.);
#2248=FACE_OUTER_BOUND('',#2727,.T.);
#2249=FACE_OUTER_BOUND('',#2728,.T.);
#2250=FACE_OUTER_BOUND('',#2729,.T.);
#2251=FACE_OUTER_BOUND('',#2730,.T.);
#2252=FACE_OUTER_BOUND('',#2731,.T.);
#2253=FACE_OUTER_BOUND('',#2732,.T.);
#2254=FACE_OUTER_BOUND('',#2733,.T.);
#2255=FACE_OUTER_BOUND('',#2734,.T.);
#2256=FACE_OUTER_BOUND('',#2735,.T.);
#2257=FACE_OUTER_BOUND('',#2736,.T.);
#2258=FACE_OUTER_BOUND('',#2737,.T.);
#2259=FACE_OUTER_BOUND('',#2738,.T.);
#2260=FACE_OUTER_BOUND('',#2739,.T.);
#2261=FACE_OUTER_BOUND('',#2740,.T.);
#2262=FACE_OUTER_BOUND('',#2741,.T.);
#2263=FACE_OUTER_BOUND('',#2742,.T.);
#2264=FACE_OUTER_BOUND('',#2743,.T.);
#2265=FACE_OUTER_BOUND('',#2744,.T.);
#2266=FACE_OUTER_BOUND('',#2745,.T.);
#2267=FACE_OUTER_BOUND('',#2746,.T.);
#2268=FACE_OUTER_BOUND('',#2747,.T.);
#2269=FACE_OUTER_BOUND('',#2748,.T.);
#2270=FACE_OUTER_BOUND('',#2749,.T.);
#2271=FACE_OUTER_BOUND('',#2750,.T.);
#2272=FACE_OUTER_BOUND('',#2751,.T.);
#2273=FACE_OUTER_BOUND('',#2752,.T.);
#2274=FACE_OUTER_BOUND('',#2753,.T.);
#2275=FACE_OUTER_BOUND('',#2754,.T.);
#2276=FACE_OUTER_BOUND('',#2755,.T.);
#2277=FACE_OUTER_BOUND('',#2756,.T.);
#2278=FACE_OUTER_BOUND('',#2757,.T.);
#2279=FACE_OUTER_BOUND('',#2758,.T.);
#2280=FACE_OUTER_BOUND('',#2759,.T.);
#2281=FACE_OUTER_BOUND('',#2760,.T.);
#2282=FACE_OUTER_BOUND('',#2761,.T.);
#2283=FACE_OUTER_BOUND('',#2762,.T.);
#2284=FACE_OUTER_BOUND('',#2763,.T.);
#2285=FACE_OUTER_BOUND('',#2764,.T.);
#2286=FACE_OUTER_BOUND('',#2765,.T.);
#2287=FACE_OUTER_BOUND('',#2766,.T.);
#2288=FACE_OUTER_BOUND('',#2767,.T.);
#2289=FACE_OUTER_BOUND('',#2768,.T.);
#2290=FACE_OUTER_BOUND('',#2769,.T.);
#2291=FACE_OUTER_BOUND('',#2770,.T.);
#2292=FACE_OUTER_BOUND('',#2771,.T.);
#2293=FACE_OUTER_BOUND('',#2772,.T.);
#2294=FACE_OUTER_BOUND('',#2773,.T.);
#2295=FACE_OUTER_BOUND('',#2774,.T.);
#2296=FACE_OUTER_BOUND('',#2775,.T.);
#2297=FACE_OUTER_BOUND('',#2776,.T.);
#2298=FACE_OUTER_BOUND('',#2777,.T.);
#2299=FACE_OUTER_BOUND('',#2778,.T.);
#2300=FACE_OUTER_BOUND('',#2779,.T.);
#2301=FACE_OUTER_BOUND('',#2780,.T.);
#2302=FACE_OUTER_BOUND('',#2781,.T.);
#2303=FACE_OUTER_BOUND('',#2782,.T.);
#2304=FACE_OUTER_BOUND('',#2783,.T.);
#2305=FACE_OUTER_BOUND('',#2784,.T.);
#2306=FACE_OUTER_BOUND('',#2785,.T.);
#2307=FACE_OUTER_BOUND('',#2786,.T.);
#2308=FACE_OUTER_BOUND('',#2787,.T.);
#2309=FACE_OUTER_BOUND('',#2788,.T.);
#2310=FACE_OUTER_BOUND('',#2789,.T.);
#2311=FACE_OUTER_BOUND('',#2790,.T.);
#2312=FACE_OUTER_BOUND('',#2791,.T.);
#2313=FACE_OUTER_BOUND('',#2792,.T.);
#2314=FACE_OUTER_BOUND('',#2793,.T.);
#2315=FACE_OUTER_BOUND('',#2794,.T.);
#2316=FACE_OUTER_BOUND('',#2795,.T.);
#2317=FACE_OUTER_BOUND('',#2796,.T.);
#2318=FACE_OUTER_BOUND('',#2797,.T.);
#2319=FACE_OUTER_BOUND('',#2798,.T.);
#2320=FACE_OUTER_BOUND('',#2799,.T.);
#2321=FACE_OUTER_BOUND('',#2800,.T.);
#2322=FACE_OUTER_BOUND('',#2801,.T.);
#2323=FACE_OUTER_BOUND('',#2802,.T.);
#2324=FACE_OUTER_BOUND('',#2803,.T.);
#2325=FACE_OUTER_BOUND('',#2804,.T.);
#2326=FACE_OUTER_BOUND('',#2805,.T.);
#2327=FACE_OUTER_BOUND('',#2806,.T.);
#2328=FACE_OUTER_BOUND('',#2807,.T.);
#2329=FACE_OUTER_BOUND('',#2808,.T.);
#2330=FACE_OUTER_BOUND('',#2809,.T.);
#2331=FACE_OUTER_BOUND('',#2810,.T.);
#2332=FACE_OUTER_BOUND('',#2811,.T.);
#2333=FACE_OUTER_BOUND('',#2812,.T.);
#2334=FACE_OUTER_BOUND('',#2813,.T.);
#2335=FACE_OUTER_BOUND('',#2814,.T.);
#2336=FACE_OUTER_BOUND('',#2815,.T.);
#2337=FACE_OUTER_BOUND('',#2816,.T.);
#2338=FACE_OUTER_BOUND('',#2817,.T.);
#2339=FACE_OUTER_BOUND('',#2818,.T.);
#2340=FACE_OUTER_BOUND('',#2819,.T.);
#2341=FACE_OUTER_BOUND('',#2820,.T.);
#2342=FACE_OUTER_BOUND('',#2821,.T.);
#2343=FACE_OUTER_BOUND('',#2822,.T.);
#2344=FACE_OUTER_BOUND('',#2823,.T.);
#2345=FACE_OUTER_BOUND('',#2824,.T.);
#2346=FACE_OUTER_BOUND('',#2825,.T.);
#2347=FACE_OUTER_BOUND('',#2826,.T.);
#2348=FACE_OUTER_BOUND('',#2827,.T.);
#2349=FACE_OUTER_BOUND('',#2828,.T.);
#2350=FACE_OUTER_BOUND('',#2829,.T.);
#2351=FACE_OUTER_BOUND('',#2830,.T.);
#2352=FACE_OUTER_BOUND('',#2831,.T.);
#2353=FACE_OUTER_BOUND('',#2832,.T.);
#2354=FACE_OUTER_BOUND('',#2833,.T.);
#2355=FACE_OUTER_BOUND('',#2834,.T.);
#2356=FACE_OUTER_BOUND('',#2835,.T.);
#2357=FACE_OUTER_BOUND('',#2836,.T.);
#2358=FACE_OUTER_BOUND('',#2837,.T.);
#2359=FACE_OUTER_BOUND('',#2838,.T.);
#2360=FACE_OUTER_BOUND('',#2839,.T.);
#2361=FACE_OUTER_BOUND('',#2840,.T.);
#2362=FACE_OUTER_BOUND('',#2841,.T.);
#2363=FACE_OUTER_BOUND('',#2842,.T.);
#2364=FACE_OUTER_BOUND('',#2843,.T.);
#2365=FACE_OUTER_BOUND('',#2844,.T.);
#2366=FACE_OUTER_BOUND('',#2845,.T.);
#2367=FACE_OUTER_BOUND('',#2846,.T.);
#2368=FACE_OUTER_BOUND('',#2847,.T.);
#2369=FACE_OUTER_BOUND('',#2848,.T.);
#2370=FACE_OUTER_BOUND('',#2849,.T.);
#2371=FACE_OUTER_BOUND('',#2850,.T.);
#2372=FACE_OUTER_BOUND('',#2851,.T.);
#2373=FACE_OUTER_BOUND('',#2852,.T.);
#2374=FACE_OUTER_BOUND('',#2853,.T.);
#2375=FACE_OUTER_BOUND('',#2854,.T.);
#2376=FACE_OUTER_BOUND('',#2855,.T.);
#2377=FACE_OUTER_BOUND('',#2856,.T.);
#2378=FACE_OUTER_BOUND('',#2857,.T.);
#2379=FACE_OUTER_BOUND('',#2858,.T.);
#2380=FACE_OUTER_BOUND('',#2859,.T.);
#2381=FACE_OUTER_BOUND('',#2860,.T.);
#2382=FACE_OUTER_BOUND('',#2861,.T.);
#2383=FACE_OUTER_BOUND('',#2862,.T.);
#2384=FACE_OUTER_BOUND('',#2863,.T.);
#2385=FACE_OUTER_BOUND('',#2864,.T.);
#2386=FACE_OUTER_BOUND('',#2865,.T.);
#2387=FACE_OUTER_BOUND('',#2866,.T.);
#2388=FACE_OUTER_BOUND('',#2867,.T.);
#2389=FACE_OUTER_BOUND('',#2868,.T.);
#2390=FACE_OUTER_BOUND('',#2869,.T.);
#2391=FACE_OUTER_BOUND('',#2870,.T.);
#2392=FACE_OUTER_BOUND('',#2871,.T.);
#2393=FACE_OUTER_BOUND('',#2872,.T.);
#2394=FACE_OUTER_BOUND('',#2873,.T.);
#2395=FACE_OUTER_BOUND('',#2874,.T.);
#2396=FACE_OUTER_BOUND('',#2875,.T.);
#2397=FACE_OUTER_BOUND('',#2876,.T.);
#2398=FACE_OUTER_BOUND('',#2877,.T.);
#2399=FACE_OUTER_BOUND('',#2878,.T.);
#2400=FACE_OUTER_BOUND('',#2879,.T.);
#2401=FACE_OUTER_BOUND('',#2880,.T.);
#2402=FACE_OUTER_BOUND('',#2881,.T.);
#2403=FACE_OUTER_BOUND('',#2882,.T.);
#2404=FACE_OUTER_BOUND('',#2883,.T.);
#2405=FACE_OUTER_BOUND('',#2884,.T.);
#2406=FACE_OUTER_BOUND('',#2885,.T.);
#2407=FACE_OUTER_BOUND('',#2886,.T.);
#2408=FACE_OUTER_BOUND('',#2887,.T.);
#2409=FACE_OUTER_BOUND('',#2888,.T.);
#2410=FACE_OUTER_BOUND('',#2889,.T.);
#2411=FACE_OUTER_BOUND('',#2890,.T.);
#2412=FACE_OUTER_BOUND('',#2892,.T.);
#2413=FACE_OUTER_BOUND('',#2893,.T.);
#2414=FACE_OUTER_BOUND('',#2895,.T.);
#2415=FACE_OUTER_BOUND('',#2896,.T.);
#2416=FACE_OUTER_BOUND('',#2897,.T.);
#2417=FACE_OUTER_BOUND('',#2898,.T.);
#2418=FACE_OUTER_BOUND('',#2899,.T.);
#2419=FACE_OUTER_BOUND('',#2900,.T.);
#2420=FACE_OUTER_BOUND('',#2901,.T.);
#2421=FACE_OUTER_BOUND('',#2902,.T.);
#2422=FACE_OUTER_BOUND('',#2903,.T.);
#2620=EDGE_LOOP('',(#9140,#9141,#9142,#9143));
#2621=EDGE_LOOP('',(#9144,#9145,#9146,#9147,#9148,#9149));
#2622=EDGE_LOOP('',(#9150,#9151,#9152,#9153,#9154,#9155));
#2623=EDGE_LOOP('',(#9156,#9157,#9158,#9159,#9160,#9161));
#2624=EDGE_LOOP('',(#9162,#9163,#9164,#9165,#9166,#9167));
#2625=EDGE_LOOP('',(#9168,#9169,#9170,#9171,#9172,#9173));
#2626=EDGE_LOOP('',(#9174,#9175,#9176,#9177,#9178,#9179));
#2627=EDGE_LOOP('',(#9180,#9181,#9182,#9183,#9184,#9185));
#2628=EDGE_LOOP('',(#9186,#9187,#9188,#9189,#9190,#9191));
#2629=EDGE_LOOP('',(#9192,#9193,#9194,#9195,#9196,#9197));
#2630=EDGE_LOOP('',(#9198,#9199,#9200,#9201,#9202,#9203));
#2631=EDGE_LOOP('',(#9204,#9205,#9206,#9207,#9208,#9209));
#2632=EDGE_LOOP('',(#9210,#9211,#9212,#9213,#9214,#9215));
#2633=EDGE_LOOP('',(#9216,#9217,#9218,#9219,#9220,#9221));
#2634=EDGE_LOOP('',(#9222,#9223,#9224,#9225,#9226,#9227));
#2635=EDGE_LOOP('',(#9228,#9229,#9230,#9231,#9232,#9233));
#2636=EDGE_LOOP('',(#9234,#9235,#9236,#9237,#9238,#9239));
#2637=EDGE_LOOP('',(#9240,#9241,#9242,#9243,#9244,#9245));
#2638=EDGE_LOOP('',(#9246,#9247,#9248,#9249,#9250,#9251));
#2639=EDGE_LOOP('',(#9252,#9253,#9254,#9255,#9256,#9257));
#2640=EDGE_LOOP('',(#9258,#9259,#9260,#9261,#9262,#9263));
#2641=EDGE_LOOP('',(#9264,#9265,#9266,#9267,#9268,#9269));
#2642=EDGE_LOOP('',(#9270,#9271,#9272,#9273,#9274,#9275));
#2643=EDGE_LOOP('',(#9276,#9277,#9278,#9279,#9280,#9281));
#2644=EDGE_LOOP('',(#9282,#9283,#9284,#9285,#9286,#9287));
#2645=EDGE_LOOP('',(#9288,#9289,#9290,#9291,#9292,#9293));
#2646=EDGE_LOOP('',(#9294,#9295,#9296,#9297,#9298,#9299));
#2647=EDGE_LOOP('',(#9300,#9301,#9302,#9303,#9304,#9305));
#2648=EDGE_LOOP('',(#9306,#9307,#9308,#9309,#9310,#9311));
#2649=EDGE_LOOP('',(#9312,#9313,#9314,#9315,#9316,#9317));
#2650=EDGE_LOOP('',(#9318,#9319,#9320,#9321,#9322,#9323));
#2651=EDGE_LOOP('',(#9324,#9325,#9326,#9327,#9328,#9329));
#2652=EDGE_LOOP('',(#9330,#9331,#9332,#9333,#9334,#9335));
#2653=EDGE_LOOP('',(#9336,#9337,#9338,#9339,#9340,#9341));
#2654=EDGE_LOOP('',(#9342,#9343,#9344,#9345,#9346,#9347));
#2655=EDGE_LOOP('',(#9348,#9349,#9350,#9351,#9352,#9353));
#2656=EDGE_LOOP('',(#9354,#9355,#9356,#9357,#9358,#9359));
#2657=EDGE_LOOP('',(#9360,#9361,#9362,#9363,#9364,#9365));
#2658=EDGE_LOOP('',(#9366,#9367,#9368,#9369,#9370,#9371));
#2659=EDGE_LOOP('',(#9372,#9373,#9374,#9375,#9376,#9377));
#2660=EDGE_LOOP('',(#9378,#9379,#9380,#9381,#9382,#9383));
#2661=EDGE_LOOP('',(#9384,#9385,#9386,#9387,#9388,#9389));
#2662=EDGE_LOOP('',(#9390,#9391,#9392,#9393,#9394,#9395));
#2663=EDGE_LOOP('',(#9396,#9397,#9398,#9399,#9400,#9401));
#2664=EDGE_LOOP('',(#9402,#9403,#9404,#9405,#9406,#9407));
#2665=EDGE_LOOP('',(#9408,#9409,#9410,#9411,#9412,#9413));
#2666=EDGE_LOOP('',(#9414,#9415,#9416,#9417,#9418,#9419));
#2667=EDGE_LOOP('',(#9420,#9421,#9422,#9423,#9424,#9425));
#2668=EDGE_LOOP('',(#9426,#9427,#9428,#9429,#9430,#9431));
#2669=EDGE_LOOP('',(#9432,#9433,#9434,#9435,#9436,#9437));
#2670=EDGE_LOOP('',(#9438,#9439,#9440,#9441,#9442,#9443));
#2671=EDGE_LOOP('',(#9444,#9445,#9446,#9447,#9448,#9449));
#2672=EDGE_LOOP('',(#9450,#9451,#9452,#9453,#9454,#9455));
#2673=EDGE_LOOP('',(#9456,#9457,#9458,#9459,#9460,#9461));
#2674=EDGE_LOOP('',(#9462,#9463,#9464,#9465,#9466,#9467));
#2675=EDGE_LOOP('',(#9468,#9469,#9470,#9471,#9472,#9473));
#2676=EDGE_LOOP('',(#9474,#9475,#9476,#9477,#9478,#9479));
#2677=EDGE_LOOP('',(#9480,#9481,#9482,#9483,#9484,#9485));
#2678=EDGE_LOOP('',(#9486,#9487,#9488,#9489,#9490,#9491));
#2679=EDGE_LOOP('',(#9492,#9493,#9494,#9495,#9496,#9497));
#2680=EDGE_LOOP('',(#9498,#9499,#9500,#9501,#9502,#9503));
#2681=EDGE_LOOP('',(#9504,#9505,#9506,#9507,#9508,#9509));
#2682=EDGE_LOOP('',(#9510,#9511,#9512,#9513,#9514,#9515));
#2683=EDGE_LOOP('',(#9516,#9517,#9518,#9519,#9520,#9521));
#2684=EDGE_LOOP('',(#9522,#9523,#9524,#9525,#9526,#9527));
#2685=EDGE_LOOP('',(#9528,#9529,#9530,#9531,#9532,#9533));
#2686=EDGE_LOOP('',(#9534,#9535,#9536,#9537,#9538,#9539));
#2687=EDGE_LOOP('',(#9540,#9541,#9542,#9543,#9544,#9545));
#2688=EDGE_LOOP('',(#9546,#9547,#9548,#9549,#9550,#9551));
#2689=EDGE_LOOP('',(#9552,#9553,#9554,#9555,#9556,#9557));
#2690=EDGE_LOOP('',(#9558,#9559,#9560,#9561,#9562,#9563));
#2691=EDGE_LOOP('',(#9564,#9565,#9566,#9567,#9568,#9569));
#2692=EDGE_LOOP('',(#9570,#9571,#9572,#9573,#9574,#9575));
#2693=EDGE_LOOP('',(#9576,#9577,#9578,#9579,#9580,#9581));
#2694=EDGE_LOOP('',(#9582,#9583,#9584,#9585,#9586,#9587));
#2695=EDGE_LOOP('',(#9588,#9589,#9590,#9591,#9592,#9593));
#2696=EDGE_LOOP('',(#9594,#9595,#9596,#9597,#9598,#9599));
#2697=EDGE_LOOP('',(#9600,#9601,#9602,#9603,#9604,#9605));
#2698=EDGE_LOOP('',(#9606,#9607,#9608,#9609,#9610,#9611));
#2699=EDGE_LOOP('',(#9612,#9613,#9614,#9615,#9616,#9617));
#2700=EDGE_LOOP('',(#9618,#9619,#9620,#9621,#9622,#9623));
#2701=EDGE_LOOP('',(#9624,#9625,#9626,#9627,#9628,#9629));
#2702=EDGE_LOOP('',(#9630,#9631,#9632,#9633,#9634,#9635));
#2703=EDGE_LOOP('',(#9636,#9637,#9638,#9639,#9640,#9641));
#2704=EDGE_LOOP('',(#9642,#9643,#9644,#9645,#9646,#9647));
#2705=EDGE_LOOP('',(#9648,#9649,#9650,#9651,#9652,#9653));
#2706=EDGE_LOOP('',(#9654,#9655,#9656,#9657,#9658,#9659));
#2707=EDGE_LOOP('',(#9660,#9661,#9662,#9663,#9664,#9665));
#2708=EDGE_LOOP('',(#9666,#9667,#9668,#9669,#9670,#9671));
#2709=EDGE_LOOP('',(#9672,#9673,#9674,#9675,#9676,#9677));
#2710=EDGE_LOOP('',(#9678,#9679,#9680,#9681,#9682,#9683));
#2711=EDGE_LOOP('',(#9684,#9685,#9686,#9687,#9688,#9689));
#2712=EDGE_LOOP('',(#9690,#9691,#9692,#9693,#9694,#9695));
#2713=EDGE_LOOP('',(#9696,#9697,#9698,#9699,#9700,#9701));
#2714=EDGE_LOOP('',(#9702,#9703,#9704,#9705,#9706,#9707));
#2715=EDGE_LOOP('',(#9708,#9709,#9710,#9711,#9712,#9713));
#2716=EDGE_LOOP('',(#9714,#9715,#9716,#9717,#9718,#9719));
#2717=EDGE_LOOP('',(#9720,#9721,#9722,#9723,#9724,#9725));
#2718=EDGE_LOOP('',(#9726,#9727,#9728,#9729,#9730,#9731));
#2719=EDGE_LOOP('',(#9732,#9733,#9734,#9735,#9736,#9737));
#2720=EDGE_LOOP('',(#9738,#9739,#9740,#9741,#9742,#9743));
#2721=EDGE_LOOP('',(#9744,#9745,#9746,#9747,#9748,#9749));
#2722=EDGE_LOOP('',(#9750,#9751,#9752,#9753,#9754,#9755));
#2723=EDGE_LOOP('',(#9756,#9757,#9758,#9759,#9760,#9761));
#2724=EDGE_LOOP('',(#9762,#9763,#9764,#9765,#9766,#9767));
#2725=EDGE_LOOP('',(#9768,#9769,#9770,#9771,#9772,#9773));
#2726=EDGE_LOOP('',(#9774,#9775,#9776,#9777,#9778,#9779));
#2727=EDGE_LOOP('',(#9780,#9781,#9782,#9783,#9784,#9785));
#2728=EDGE_LOOP('',(#9786,#9787,#9788,#9789,#9790,#9791));
#2729=EDGE_LOOP('',(#9792,#9793,#9794,#9795,#9796,#9797));
#2730=EDGE_LOOP('',(#9798,#9799,#9800,#9801,#9802,#9803));
#2731=EDGE_LOOP('',(#9804,#9805,#9806,#9807,#9808,#9809));
#2732=EDGE_LOOP('',(#9810,#9811,#9812,#9813,#9814,#9815));
#2733=EDGE_LOOP('',(#9816,#9817,#9818,#9819,#9820,#9821));
#2734=EDGE_LOOP('',(#9822,#9823,#9824,#9825,#9826,#9827));
#2735=EDGE_LOOP('',(#9828,#9829,#9830,#9831,#9832,#9833));
#2736=EDGE_LOOP('',(#9834,#9835,#9836,#9837,#9838,#9839));
#2737=EDGE_LOOP('',(#9840,#9841,#9842,#9843,#9844,#9845));
#2738=EDGE_LOOP('',(#9846,#9847,#9848,#9849,#9850,#9851));
#2739=EDGE_LOOP('',(#9852,#9853,#9854,#9855,#9856,#9857));
#2740=EDGE_LOOP('',(#9858,#9859,#9860,#9861,#9862,#9863));
#2741=EDGE_LOOP('',(#9864,#9865,#9866,#9867,#9868,#9869));
#2742=EDGE_LOOP('',(#9870,#9871,#9872,#9873,#9874,#9875));
#2743=EDGE_LOOP('',(#9876,#9877,#9878,#9879,#9880,#9881));
#2744=EDGE_LOOP('',(#9882,#9883,#9884,#9885,#9886,#9887));
#2745=EDGE_LOOP('',(#9888,#9889,#9890,#9891,#9892,#9893));
#2746=EDGE_LOOP('',(#9894,#9895,#9896,#9897,#9898,#9899));
#2747=EDGE_LOOP('',(#9900,#9901,#9902,#9903,#9904,#9905));
#2748=EDGE_LOOP('',(#9906,#9907,#9908,#9909,#9910,#9911));
#2749=EDGE_LOOP('',(#9912,#9913,#9914,#9915,#9916,#9917));
#2750=EDGE_LOOP('',(#9918,#9919,#9920,#9921,#9922,#9923));
#2751=EDGE_LOOP('',(#9924,#9925,#9926,#9927,#9928,#9929));
#2752=EDGE_LOOP('',(#9930,#9931,#9932,#9933,#9934,#9935));
#2753=EDGE_LOOP('',(#9936,#9937,#9938,#9939,#9940,#9941));
#2754=EDGE_LOOP('',(#9942,#9943,#9944,#9945,#9946,#9947));
#2755=EDGE_LOOP('',(#9948,#9949,#9950,#9951,#9952,#9953));
#2756=EDGE_LOOP('',(#9954,#9955,#9956,#9957,#9958,#9959));
#2757=EDGE_LOOP('',(#9960,#9961,#9962,#9963,#9964,#9965));
#2758=EDGE_LOOP('',(#9966,#9967,#9968,#9969,#9970,#9971));
#2759=EDGE_LOOP('',(#9972,#9973,#9974,#9975,#9976,#9977));
#2760=EDGE_LOOP('',(#9978,#9979,#9980,#9981,#9982,#9983));
#2761=EDGE_LOOP('',(#9984,#9985,#9986,#9987,#9988,#9989));
#2762=EDGE_LOOP('',(#9990,#9991,#9992,#9993,#9994,#9995));
#2763=EDGE_LOOP('',(#9996,#9997,#9998,#9999,#10000,#10001));
#2764=EDGE_LOOP('',(#10002,#10003,#10004,#10005,#10006,#10007));
#2765=EDGE_LOOP('',(#10008,#10009,#10010,#10011,#10012,#10013));
#2766=EDGE_LOOP('',(#10014,#10015,#10016,#10017,#10018,#10019));
#2767=EDGE_LOOP('',(#10020,#10021,#10022,#10023,#10024,#10025));
#2768=EDGE_LOOP('',(#10026,#10027,#10028,#10029,#10030,#10031));
#2769=EDGE_LOOP('',(#10032,#10033,#10034,#10035,#10036,#10037));
#2770=EDGE_LOOP('',(#10038,#10039,#10040,#10041,#10042,#10043));
#2771=EDGE_LOOP('',(#10044,#10045,#10046,#10047,#10048,#10049));
#2772=EDGE_LOOP('',(#10050,#10051,#10052,#10053,#10054,#10055));
#2773=EDGE_LOOP('',(#10056,#10057,#10058,#10059,#10060,#10061));
#2774=EDGE_LOOP('',(#10062,#10063,#10064,#10065,#10066,#10067));
#2775=EDGE_LOOP('',(#10068,#10069,#10070,#10071,#10072,#10073));
#2776=EDGE_LOOP('',(#10074,#10075,#10076,#10077,#10078,#10079));
#2777=EDGE_LOOP('',(#10080,#10081,#10082,#10083,#10084,#10085));
#2778=EDGE_LOOP('',(#10086,#10087,#10088,#10089,#10090,#10091));
#2779=EDGE_LOOP('',(#10092,#10093,#10094,#10095,#10096,#10097));
#2780=EDGE_LOOP('',(#10098,#10099,#10100,#10101,#10102,#10103));
#2781=EDGE_LOOP('',(#10104,#10105,#10106,#10107,#10108,#10109));
#2782=EDGE_LOOP('',(#10110,#10111,#10112,#10113,#10114,#10115));
#2783=EDGE_LOOP('',(#10116,#10117,#10118,#10119,#10120,#10121));
#2784=EDGE_LOOP('',(#10122,#10123,#10124,#10125,#10126,#10127));
#2785=EDGE_LOOP('',(#10128,#10129,#10130,#10131,#10132,#10133));
#2786=EDGE_LOOP('',(#10134,#10135,#10136,#10137,#10138,#10139));
#2787=EDGE_LOOP('',(#10140,#10141,#10142,#10143,#10144,#10145));
#2788=EDGE_LOOP('',(#10146,#10147,#10148,#10149,#10150,#10151));
#2789=EDGE_LOOP('',(#10152,#10153,#10154,#10155,#10156,#10157));
#2790=EDGE_LOOP('',(#10158,#10159,#10160,#10161,#10162,#10163));
#2791=EDGE_LOOP('',(#10164,#10165,#10166,#10167,#10168,#10169));
#2792=EDGE_LOOP('',(#10170,#10171,#10172,#10173,#10174,#10175));
#2793=EDGE_LOOP('',(#10176,#10177,#10178,#10179,#10180,#10181));
#2794=EDGE_LOOP('',(#10182,#10183,#10184,#10185,#10186,#10187));
#2795=EDGE_LOOP('',(#10188,#10189,#10190,#10191,#10192,#10193));
#2796=EDGE_LOOP('',(#10194,#10195,#10196,#10197,#10198,#10199));
#2797=EDGE_LOOP('',(#10200,#10201,#10202,#10203,#10204,#10205));
#2798=EDGE_LOOP('',(#10206,#10207,#10208,#10209,#10210,#10211));
#2799=EDGE_LOOP('',(#10212,#10213,#10214,#10215,#10216,#10217));
#2800=EDGE_LOOP('',(#10218,#10219,#10220,#10221,#10222,#10223));
#2801=EDGE_LOOP('',(#10224,#10225,#10226,#10227,#10228,#10229));
#2802=EDGE_LOOP('',(#10230,#10231,#10232,#10233,#10234,#10235));
#2803=EDGE_LOOP('',(#10236,#10237,#10238,#10239,#10240,#10241));
#2804=EDGE_LOOP('',(#10242,#10243,#10244,#10245,#10246,#10247));
#2805=EDGE_LOOP('',(#10248,#10249,#10250,#10251,#10252,#10253));
#2806=EDGE_LOOP('',(#10254,#10255,#10256,#10257,#10258,#10259));
#2807=EDGE_LOOP('',(#10260,#10261,#10262,#10263,#10264,#10265));
#2808=EDGE_LOOP('',(#10266,#10267,#10268,#10269,#10270,#10271));
#2809=EDGE_LOOP('',(#10272,#10273,#10274,#10275,#10276,#10277));
#2810=EDGE_LOOP('',(#10278,#10279,#10280,#10281,#10282,#10283));
#2811=EDGE_LOOP('',(#10284,#10285,#10286,#10287,#10288,#10289));
#2812=EDGE_LOOP('',(#10290,#10291,#10292,#10293,#10294,#10295));
#2813=EDGE_LOOP('',(#10296,#10297,#10298,#10299,#10300,#10301));
#2814=EDGE_LOOP('',(#10302,#10303,#10304,#10305,#10306,#10307));
#2815=EDGE_LOOP('',(#10308,#10309,#10310,#10311,#10312,#10313));
#2816=EDGE_LOOP('',(#10314,#10315,#10316,#10317,#10318,#10319));
#2817=EDGE_LOOP('',(#10320,#10321,#10322,#10323,#10324,#10325));
#2818=EDGE_LOOP('',(#10326,#10327,#10328,#10329,#10330,#10331));
#2819=EDGE_LOOP('',(#10332,#10333,#10334,#10335,#10336,#10337));
#2820=EDGE_LOOP('',(#10338,#10339,#10340,#10341,#10342,#10343));
#2821=EDGE_LOOP('',(#10344,#10345,#10346,#10347,#10348,#10349));
#2822=EDGE_LOOP('',(#10350,#10351,#10352,#10353,#10354,#10355));
#2823=EDGE_LOOP('',(#10356,#10357,#10358,#10359,#10360,#10361));
#2824=EDGE_LOOP('',(#10362,#10363,#10364,#10365,#10366,#10367));
#2825=EDGE_LOOP('',(#10368,#10369,#10370,#10371,#10372,#10373));
#2826=EDGE_LOOP('',(#10374,#10375,#10376,#10377,#10378,#10379));
#2827=EDGE_LOOP('',(#10380,#10381,#10382,#10383,#10384,#10385));
#2828=EDGE_LOOP('',(#10386,#10387,#10388,#10389,#10390,#10391));
#2829=EDGE_LOOP('',(#10392,#10393,#10394,#10395,#10396,#10397));
#2830=EDGE_LOOP('',(#10398,#10399,#10400,#10401,#10402,#10403));
#2831=EDGE_LOOP('',(#10404,#10405,#10406,#10407,#10408,#10409));
#2832=EDGE_LOOP('',(#10410,#10411,#10412,#10413,#10414,#10415));
#2833=EDGE_LOOP('',(#10416,#10417,#10418,#10419,#10420,#10421));
#2834=EDGE_LOOP('',(#10422,#10423,#10424,#10425,#10426,#10427));
#2835=EDGE_LOOP('',(#10428,#10429,#10430,#10431,#10432,#10433));
#2836=EDGE_LOOP('',(#10434,#10435,#10436,#10437,#10438,#10439));
#2837=EDGE_LOOP('',(#10440,#10441,#10442,#10443,#10444,#10445));
#2838=EDGE_LOOP('',(#10446,#10447,#10448,#10449,#10450,#10451));
#2839=EDGE_LOOP('',(#10452,#10453,#10454,#10455,#10456,#10457));
#2840=EDGE_LOOP('',(#10458,#10459,#10460,#10461,#10462,#10463));
#2841=EDGE_LOOP('',(#10464,#10465,#10466,#10467,#10468,#10469));
#2842=EDGE_LOOP('',(#10470,#10471,#10472,#10473,#10474,#10475));
#2843=EDGE_LOOP('',(#10476,#10477,#10478,#10479,#10480,#10481));
#2844=EDGE_LOOP('',(#10482,#10483,#10484,#10485,#10486,#10487));
#2845=EDGE_LOOP('',(#10488,#10489,#10490,#10491,#10492,#10493));
#2846=EDGE_LOOP('',(#10494,#10495,#10496,#10497,#10498,#10499));
#2847=EDGE_LOOP('',(#10500,#10501,#10502,#10503,#10504,#10505));
#2848=EDGE_LOOP('',(#10506,#10507,#10508,#10509,#10510,#10511));
#2849=EDGE_LOOP('',(#10512,#10513,#10514,#10515,#10516,#10517));
#2850=EDGE_LOOP('',(#10518,#10519,#10520,#10521,#10522,#10523));
#2851=EDGE_LOOP('',(#10524,#10525,#10526,#10527,#10528,#10529));
#2852=EDGE_LOOP('',(#10530,#10531,#10532,#10533,#10534,#10535));
#2853=EDGE_LOOP('',(#10536,#10537,#10538,#10539,#10540,#10541));
#2854=EDGE_LOOP('',(#10542,#10543,#10544,#10545,#10546,#10547));
#2855=EDGE_LOOP('',(#10548,#10549,#10550,#10551,#10552,#10553));
#2856=EDGE_LOOP('',(#10554,#10555,#10556,#10557,#10558,#10559));
#2857=EDGE_LOOP('',(#10560,#10561,#10562,#10563,#10564,#10565));
#2858=EDGE_LOOP('',(#10566,#10567,#10568,#10569,#10570,#10571));
#2859=EDGE_LOOP('',(#10572,#10573,#10574,#10575,#10576,#10577));
#2860=EDGE_LOOP('',(#10578,#10579,#10580,#10581,#10582,#10583));
#2861=EDGE_LOOP('',(#10584,#10585,#10586,#10587,#10588,#10589));
#2862=EDGE_LOOP('',(#10590,#10591,#10592,#10593,#10594,#10595));
#2863=EDGE_LOOP('',(#10596,#10597,#10598,#10599,#10600,#10601));
#2864=EDGE_LOOP('',(#10602,#10603,#10604,#10605,#10606,#10607));
#2865=EDGE_LOOP('',(#10608,#10609,#10610,#10611,#10612,#10613));
#2866=EDGE_LOOP('',(#10614,#10615,#10616,#10617,#10618,#10619));
#2867=EDGE_LOOP('',(#10620,#10621,#10622,#10623,#10624,#10625));
#2868=EDGE_LOOP('',(#10626,#10627,#10628,#10629,#10630,#10631));
#2869=EDGE_LOOP('',(#10632,#10633,#10634,#10635,#10636,#10637));
#2870=EDGE_LOOP('',(#10638,#10639,#10640,#10641,#10642,#10643));
#2871=EDGE_LOOP('',(#10644,#10645,#10646,#10647,#10648,#10649));
#2872=EDGE_LOOP('',(#10650,#10651,#10652,#10653,#10654,#10655));
#2873=EDGE_LOOP('',(#10656,#10657,#10658,#10659,#10660,#10661));
#2874=EDGE_LOOP('',(#10662,#10663,#10664,#10665,#10666,#10667));
#2875=EDGE_LOOP('',(#10668,#10669,#10670,#10671,#10672,#10673));
#2876=EDGE_LOOP('',(#10674,#10675,#10676,#10677,#10678,#10679));
#2877=EDGE_LOOP('',(#10680,#10681,#10682,#10683,#10684,#10685));
#2878=EDGE_LOOP('',(#10686,#10687,#10688,#10689,#10690,#10691));
#2879=EDGE_LOOP('',(#10692,#10693,#10694,#10695,#10696,#10697));
#2880=EDGE_LOOP('',(#10698,#10699,#10700,#10701,#10702,#10703));
#2881=EDGE_LOOP('',(#10704,#10705,#10706,#10707,#10708,#10709));
#2882=EDGE_LOOP('',(#10710,#10711,#10712,#10713,#10714,#10715));
#2883=EDGE_LOOP('',(#10716,#10717,#10718,#10719,#10720,#10721));
#2884=EDGE_LOOP('',(#10722,#10723,#10724,#10725,#10726,#10727));
#2885=EDGE_LOOP('',(#10728,#10729,#10730,#10731,#10732,#10733));
#2886=EDGE_LOOP('',(#10734,#10735,#10736,#10737,#10738,#10739));
#2887=EDGE_LOOP('',(#10740,#10741,#10742,#10743,#10744,#10745));
#2888=EDGE_LOOP('',(#10746,#10747,#10748,#10749,#10750,#10751,#10752,#10753,
#10754,#10755,#10756,#10757,#10758,#10759,#10760,#10761,#10762,#10763,#10764,
#10765,#10766,#10767,#10768,#10769,#10770,#10771,#10772,#10773,#10774,#10775,
#10776,#10777,#10778,#10779,#10780,#10781,#10782,#10783,#10784,#10785,#10786,
#10787,#10788,#10789,#10790,#10791,#10792,#10793,#10794,#10795,#10796,#10797,
#10798,#10799,#10800,#10801,#10802,#10803,#10804,#10805,#10806,#10807,#10808,
#10809,#10810,#10811,#10812,#10813,#10814,#10815,#10816,#10817,#10818,#10819,
#10820,#10821,#10822,#10823,#10824,#10825,#10826,#10827,#10828,#10829,#10830,
#10831,#10832,#10833,#10834,#10835,#10836,#10837,#10838,#10839,#10840,#10841,
#10842,#10843,#10844,#10845,#10846,#10847,#10848,#10849,#10850,#10851,#10852,
#10853,#10854,#10855,#10856,#10857,#10858,#10859,#10860,#10861,#10862,#10863,
#10864,#10865,#10866,#10867,#10868,#10869,#10870,#10871,#10872,#10873,#10874,
#10875,#10876,#10877,#10878,#10879,#10880,#10881,#10882,#10883,#10884,#10885,
#10886,#10887,#10888,#10889,#10890,#10891,#10892,#10893,#10894,#10895,#10896,
#10897,#10898,#10899,#10900,#10901,#10902,#10903,#10904,#10905,#10906,#10907,
#10908,#10909,#10910,#10911,#10912,#10913,#10914,#10915,#10916,#10917,#10918,
#10919,#10920,#10921,#10922,#10923,#10924,#10925,#10926,#10927,#10928,#10929,
#10930,#10931,#10932,#10933,#10934,#10935,#10936,#10937,#10938,#10939,#10940,
#10941,#10942,#10943,#10944,#10945,#10946,#10947,#10948,#10949,#10950,#10951,
#10952,#10953,#10954,#10955,#10956,#10957,#10958,#10959,#10960,#10961,#10962,
#10963,#10964,#10965,#10966,#10967,#10968,#10969,#10970,#10971,#10972,#10973,
#10974,#10975,#10976,#10977,#10978,#10979,#10980,#10981,#10982,#10983,#10984,
#10985,#10986,#10987,#10988,#10989,#10990,#10991,#10992,#10993,#10994,#10995,
#10996,#10997,#10998,#10999,#11000,#11001,#11002,#11003,#11004,#11005,#11006,
#11007,#11008,#11009,#11010,#11011,#11012,#11013,#11014,#11015,#11016,#11017,
#11018,#11019,#11020,#11021,#11022,#11023,#11024,#11025,#11026,#11027,#11028,
#11029,#11030,#11031,#11032,#11033,#11034,#11035,#11036,#11037,#11038,#11039,
#11040,#11041,#11042,#11043,#11044,#11045,#11046,#11047,#11048,#11049,#11050,
#11051,#11052,#11053,#11054,#11055,#11056,#11057,#11058,#11059,#11060,#11061,
#11062,#11063,#11064,#11065,#11066,#11067,#11068,#11069,#11070,#11071,#11072,
#11073,#11074,#11075,#11076,#11077,#11078,#11079,#11080,#11081,#11082,#11083,
#11084,#11085,#11086,#11087,#11088,#11089,#11090,#11091,#11092,#11093,#11094,
#11095,#11096,#11097,#11098,#11099,#11100,#11101,#11102,#11103,#11104,#11105,
#11106,#11107,#11108,#11109,#11110,#11111,#11112,#11113,#11114,#11115,#11116,
#11117,#11118,#11119,#11120,#11121,#11122,#11123,#11124,#11125,#11126,#11127,
#11128,#11129,#11130,#11131,#11132,#11133,#11134,#11135,#11136,#11137,#11138,
#11139,#11140,#11141,#11142,#11143,#11144,#11145,#11146,#11147,#11148,#11149,
#11150,#11151,#11152,#11153,#11154,#11155,#11156,#11157,#11158,#11159,#11160,
#11161,#11162,#11163,#11164,#11165,#11166,#11167,#11168,#11169,#11170,#11171,
#11172,#11173,#11174,#11175,#11176,#11177,#11178,#11179,#11180,#11181,#11182,
#11183,#11184,#11185,#11186,#11187,#11188,#11189,#11190,#11191,#11192,#11193,
#11194,#11195,#11196,#11197,#11198,#11199,#11200,#11201,#11202,#11203,#11204,
#11205,#11206,#11207,#11208,#11209,#11210,#11211,#11212,#11213,#11214,#11215,
#11216,#11217,#11218,#11219,#11220,#11221,#11222,#11223,#11224,#11225,#11226,
#11227,#11228,#11229,#11230,#11231,#11232,#11233,#11234,#11235,#11236,#11237,
#11238,#11239,#11240,#11241,#11242,#11243,#11244,#11245,#11246,#11247,#11248,
#11249,#11250,#11251,#11252,#11253,#11254,#11255,#11256,#11257,#11258,#11259,
#11260,#11261,#11262,#11263,#11264,#11265,#11266,#11267,#11268,#11269,#11270,
#11271,#11272,#11273,#11274,#11275,#11276,#11277,#11278,#11279,#11280,#11281,
#11282,#11283,#11284,#11285,#11286,#11287));
#2889=EDGE_LOOP('',(#11288,#11289,#11290,#11291,#11292,#11293));
#2890=EDGE_LOOP('',(#11294));
#2891=EDGE_LOOP('',(#11295));
#2892=EDGE_LOOP('',(#11296,#11297,#11298,#11299));
#2893=EDGE_LOOP('',(#11300));
#2894=EDGE_LOOP('',(#11301,#11302,#11303,#11304));
#2895=EDGE_LOOP('',(#11305,#11306,#11307,#11308));
#2896=EDGE_LOOP('',(#11309,#11310));
#2897=EDGE_LOOP('',(#11311,#11312,#11313,#11314));
#2898=EDGE_LOOP('',(#11315,#11316,#11317));
#2899=EDGE_LOOP('',(#11318,#11319,#11320,#11321,#11322,#11323,#11324,#11325,
#11326,#11327,#11328,#11329));
#2900=EDGE_LOOP('',(#11330,#11331,#11332,#11333));
#2901=EDGE_LOOP('',(#11334,#11335,#11336,#11337,#11338,#11339,#11340,#11341,
#11342,#11343,#11344,#11345,#11346,#11347,#11348,#11349,#11350,#11351,#11352,
#11353,#11354,#11355,#11356,#11357,#11358,#11359,#11360,#11361,#11362,#11363,
#11364,#11365,#11366,#11367,#11368,#11369,#11370,#11371,#11372,#11373,#11374,
#11375,#11376,#11377,#11378,#11379,#11380,#11381,#11382,#11383,#11384,#11385,
#11386,#11387,#11388,#11389,#11390,#11391,#11392,#11393,#11394,#11395,#11396,
#11397,#11398,#11399,#11400,#11401,#11402,#11403,#11404,#11405,#11406,#11407,
#11408,#11409,#11410,#11411,#11412,#11413,#11414,#11415,#11416,#11417,#11418,
#11419,#11420,#11421,#11422,#11423,#11424,#11425,#11426,#11427,#11428,#11429,
#11430,#11431,#11432,#11433,#11434,#11435,#11436,#11437,#11438,#11439,#11440,
#11441,#11442,#11443,#11444,#11445,#11446,#11447,#11448,#11449,#11450,#11451,
#11452,#11453,#11454,#11455,#11456,#11457,#11458,#11459,#11460,#11461,#11462,
#11463,#11464,#11465,#11466,#11467,#11468,#11469,#11470,#11471,#11472,#11473,
#11474,#11475,#11476,#11477,#11478,#11479,#11480,#11481,#11482,#11483,#11484,
#11485,#11486,#11487,#11488,#11489,#11490,#11491,#11492,#11493,#11494,#11495,
#11496,#11497,#11498,#11499,#11500,#11501,#11502,#11503,#11504,#11505,#11506,
#11507,#11508,#11509,#11510,#11511,#11512,#11513,#11514,#11515,#11516,#11517,
#11518,#11519,#11520,#11521,#11522,#11523,#11524,#11525,#11526,#11527,#11528,
#11529,#11530,#11531,#11532,#11533,#11534,#11535,#11536,#11537,#11538,#11539,
#11540,#11541,#11542,#11543,#11544,#11545,#11546,#11547,#11548,#11549,#11550,
#11551,#11552,#11553,#11554,#11555,#11556,#11557,#11558,#11559,#11560,#11561,
#11562,#11563,#11564,#11565,#11566,#11567,#11568,#11569,#11570,#11571,#11572,
#11573,#11574,#11575,#11576,#11577,#11578,#11579,#11580,#11581,#11582,#11583,
#11584,#11585,#11586,#11587,#11588,#11589,#11590,#11591,#11592,#11593,#11594,
#11595,#11596,#11597,#11598,#11599,#11600,#11601,#11602,#11603,#11604,#11605,
#11606,#11607,#11608,#11609,#11610,#11611,#11612,#11613,#11614,#11615,#11616,
#11617,#11618,#11619,#11620,#11621,#11622,#11623,#11624,#11625,#11626,#11627,
#11628,#11629,#11630,#11631,#11632,#11633,#11634,#11635,#11636,#11637,#11638,
#11639,#11640,#11641,#11642,#11643,#11644,#11645,#11646,#11647,#11648,#11649,
#11650,#11651,#11652,#11653,#11654,#11655,#11656,#11657,#11658,#11659,#11660,
#11661,#11662,#11663,#11664,#11665,#11666,#11667,#11668,#11669,#11670,#11671,
#11672,#11673,#11674,#11675,#11676,#11677,#11678,#11679,#11680,#11681,#11682,
#11683,#11684,#11685,#11686,#11687,#11688,#11689,#11690,#11691,#11692,#11693,
#11694,#11695,#11696,#11697,#11698,#11699,#11700,#11701,#11702,#11703,#11704,
#11705,#11706,#11707,#11708,#11709,#11710,#11711,#11712,#11713,#11714,#11715,
#11716,#11717,#11718,#11719,#11720,#11721,#11722,#11723,#11724,#11725,#11726,
#11727,#11728,#11729,#11730,#11731,#11732,#11733,#11734,#11735,#11736,#11737,
#11738,#11739,#11740,#11741,#11742,#11743,#11744,#11745,#11746,#11747,#11748,
#11749,#11750,#11751,#11752,#11753,#11754,#11755,#11756,#11757,#11758,#11759,
#11760,#11761,#11762,#11763,#11764,#11765,#11766,#11767,#11768,#11769,#11770,
#11771,#11772,#11773,#11774,#11775,#11776,#11777,#11778,#11779,#11780,#11781,
#11782,#11783,#11784,#11785,#11786,#11787,#11788,#11789,#11790,#11791,#11792,
#11793,#11794,#11795,#11796,#11797,#11798,#11799,#11800,#11801,#11802,#11803,
#11804,#11805,#11806,#11807,#11808,#11809,#11810,#11811,#11812,#11813,#11814,
#11815,#11816,#11817,#11818,#11819,#11820,#11821,#11822,#11823,#11824,#11825,
#11826,#11827,#11828,#11829,#11830,#11831,#11832,#11833,#11834,#11835,#11836,
#11837,#11838,#11839,#11840,#11841,#11842,#11843,#11844,#11845,#11846,#11847,
#11848,#11849,#11850,#11851,#11852,#11853,#11854,#11855,#11856,#11857,#11858,
#11859,#11860,#11861,#11862,#11863,#11864,#11865,#11866,#11867,#11868,#11869,
#11870,#11871,#11872,#11873,#11874,#11875,#11876,#11877,#11878,#11879,#11880,
#11881,#11882,#11883,#11884,#11885,#11886,#11887,#11888,#11889,#11890,#11891,
#11892,#11893,#11894,#11895,#11896,#11897,#11898,#11899,#11900,#11901,#11902,
#11903,#11904,#11905,#11906,#11907,#11908,#11909,#11910,#11911,#11912,#11913,
#11914,#11915,#11916,#11917,#11918,#11919,#11920,#11921,#11922,#11923,#11924,
#11925,#11926,#11927,#11928,#11929,#11930,#11931,#11932,#11933,#11934,#11935,
#11936,#11937,#11938,#11939,#11940,#11941,#11942,#11943,#11944,#11945,#11946,
#11947,#11948,#11949,#11950,#11951,#11952,#11953,#11954,#11955,#11956,#11957,
#11958,#11959,#11960,#11961,#11962,#11963,#11964,#11965,#11966,#11967,#11968,
#11969,#11970,#11971,#11972,#11973,#11974,#11975,#11976,#11977,#11978,#11979,
#11980,#11981,#11982,#11983,#11984,#11985,#11986,#11987,#11988,#11989,#11990,
#11991,#11992,#11993,#11994,#11995,#11996,#11997,#11998,#11999,#12000,#12001,
#12002,#12003,#12004,#12005,#12006,#12007,#12008,#12009,#12010,#12011,#12012,
#12013,#12014,#12015,#12016,#12017,#12018,#12019,#12020,#12021,#12022,#12023,
#12024,#12025,#12026,#12027,#12028,#12029,#12030,#12031,#12032,#12033,#12034,
#12035,#12036,#12037,#12038,#12039,#12040,#12041,#12042,#12043,#12044,#12045,
#12046,#12047,#12048,#12049,#12050,#12051,#12052,#12053,#12054,#12055,#12056,
#12057,#12058,#12059,#12060,#12061,#12062,#12063,#12064,#12065,#12066,#12067,
#12068,#12069,#12070,#12071,#12072,#12073,#12074,#12075,#12076,#12077,#12078,
#12079,#12080,#12081,#12082,#12083,#12084,#12085,#12086,#12087,#12088,#12089,
#12090,#12091,#12092,#12093,#12094,#12095,#12096,#12097,#12098,#12099,#12100,
#12101,#12102,#12103,#12104,#12105,#12106,#12107,#12108,#12109,#12110,#12111,
#12112,#12113,#12114,#12115,#12116,#12117,#12118,#12119,#12120,#12121,#12122,
#12123,#12124,#12125,#12126,#12127,#12128,#12129,#12130,#12131,#12132,#12133,
#12134,#12135,#12136,#12137,#12138,#12139,#12140,#12141,#12142));
#2902=EDGE_LOOP('',(#12143,#12144,#12145,#12146,#12147,#12148,#12149,#12150,
#12151,#12152,#12153,#12154,#12155,#12156,#12157,#12158,#12159,#12160,#12161,
#12162,#12163,#12164,#12165,#12166,#12167,#12168,#12169,#12170,#12171,#12172,
#12173,#12174,#12175,#12176,#12177,#12178,#12179,#12180,#12181,#12182,#12183,
#12184,#12185,#12186,#12187,#12188,#12189,#12190,#12191,#12192,#12193,#12194,
#12195,#12196,#12197,#12198,#12199,#12200,#12201,#12202,#12203,#12204,#12205,
#12206,#12207,#12208,#12209,#12210,#12211,#12212,#12213,#12214,#12215,#12216,
#12217,#12218,#12219,#12220,#12221,#12222,#12223,#12224,#12225,#12226,#12227,
#12228,#12229,#12230,#12231,#12232,#12233,#12234,#12235,#12236,#12237,#12238,
#12239,#12240,#12241,#12242,#12243,#12244,#12245,#12246,#12247,#12248,#12249,
#12250,#12251,#12252,#12253,#12254,#12255,#12256,#12257,#12258,#12259,#12260,
#12261,#12262,#12263,#12264,#12265,#12266,#12267,#12268,#12269,#12270,#12271,
#12272,#12273,#12274,#12275,#12276,#12277,#12278,#12279,#12280,#12281,#12282,
#12283,#12284,#12285,#12286,#12287,#12288,#12289,#12290,#12291,#12292,#12293,
#12294,#12295,#12296,#12297,#12298,#12299,#12300,#12301,#12302,#12303,#12304,
#12305,#12306,#12307,#12308,#12309,#12310,#12311,#12312,#12313,#12314,#12315,
#12316,#12317,#12318,#12319,#12320,#12321,#12322,#12323,#12324,#12325,#12326,
#12327,#12328,#12329,#12330,#12331,#12332,#12333,#12334,#12335,#12336,#12337,
#12338,#12339,#12340,#12341,#12342,#12343,#12344,#12345,#12346,#12347,#12348,
#12349,#12350,#12351,#12352,#12353,#12354,#12355,#12356,#12357,#12358,#12359,
#12360,#12361,#12362,#12363,#12364,#12365,#12366,#12367,#12368,#12369,#12370,
#12371,#12372,#12373,#12374,#12375,#12376,#12377,#12378,#12379,#12380,#12381,
#12382,#12383,#12384,#12385,#12386,#12387,#12388,#12389,#12390,#12391,#12392,
#12393,#12394,#12395,#12396,#12397,#12398,#12399,#12400,#12401,#12402,#12403,
#12404,#12405,#12406,#12407,#12408,#12409,#12410,#12411,#12412,#12413,#12414,
#12415,#12416,#12417,#12418,#12419,#12420,#12421,#12422,#12423,#12424,#12425,
#12426,#12427,#12428,#12429,#12430,#12431,#12432,#12433,#12434,#12435,#12436,
#12437,#12438,#12439,#12440,#12441,#12442,#12443,#12444,#12445,#12446,#12447,
#12448,#12449,#12450,#12451,#12452,#12453,#12454,#12455,#12456,#12457,#12458,
#12459,#12460,#12461,#12462,#12463,#12464,#12465,#12466,#12467,#12468,#12469,
#12470,#12471,#12472,#12473,#12474,#12475,#12476,#12477,#12478,#12479,#12480,
#12481,#12482,#12483,#12484,#12485,#12486,#12487,#12488,#12489,#12490,#12491,
#12492,#12493,#12494,#12495,#12496,#12497,#12498,#12499,#12500,#12501,#12502,
#12503,#12504,#12505,#12506,#12507,#12508,#12509,#12510,#12511,#12512,#12513,
#12514,#12515,#12516,#12517,#12518,#12519,#12520,#12521,#12522,#12523,#12524,
#12525,#12526,#12527,#12528,#12529,#12530,#12531,#12532,#12533,#12534,#12535,
#12536,#12537,#12538,#12539,#12540,#12541,#12542,#12543,#12544,#12545,#12546,
#12547,#12548,#12549,#12550,#12551,#12552,#12553,#12554,#12555,#12556,#12557,
#12558,#12559,#12560,#12561,#12562,#12563,#12564,#12565,#12566,#12567,#12568,
#12569,#12570,#12571,#12572,#12573,#12574,#12575,#12576,#12577,#12578,#12579,
#12580,#12581,#12582,#12583,#12584,#12585,#12586,#12587,#12588,#12589,#12590,
#12591,#12592,#12593,#12594,#12595,#12596,#12597,#12598,#12599,#12600,#12601,
#12602,#12603,#12604,#12605,#12606,#12607,#12608,#12609,#12610,#12611,#12612,
#12613,#12614,#12615,#12616,#12617,#12618,#12619,#12620,#12621,#12622,#12623,
#12624,#12625,#12626,#12627,#12628,#12629,#12630,#12631,#12632,#12633,#12634,
#12635,#12636,#12637,#12638,#12639,#12640,#12641,#12642,#12643,#12644,#12645,
#12646,#12647,#12648,#12649,#12650,#12651,#12652,#12653,#12654,#12655,#12656,
#12657,#12658,#12659,#12660,#12661,#12662,#12663,#12664,#12665,#12666,#12667,
#12668,#12669,#12670,#12671,#12672,#12673,#12674,#12675,#12676,#12677,#12678,
#12679,#12680,#12681,#12682,#12683,#12684,#12685,#12686,#12687,#12688,#12689,
#12690,#12691,#12692,#12693,#12694,#12695,#12696,#12697,#12698,#12699,#12700,
#12701,#12702,#12703,#12704,#12705,#12706,#12707,#12708,#12709,#12710,#12711,
#12712,#12713,#12714,#12715,#12716,#12717,#12718,#12719,#12720,#12721,#12722,
#12723,#12724,#12725,#12726,#12727,#12728,#12729,#12730,#12731,#12732,#12733,
#12734,#12735,#12736,#12737,#12738,#12739,#12740,#12741,#12742,#12743,#12744,
#12745,#12746,#12747,#12748,#12749,#12750,#12751,#12752,#12753,#12754,#12755,
#12756,#12757,#12758,#12759,#12760,#12761,#12762,#12763,#12764,#12765,#12766,
#12767,#12768,#12769,#12770,#12771,#12772,#12773,#12774,#12775,#12776,#12777,
#12778,#12779,#12780,#12781,#12782,#12783,#12784,#12785,#12786,#12787,#12788,
#12789,#12790,#12791,#12792,#12793,#12794,#12795,#12796,#12797,#12798,#12799,
#12800,#12801,#12802,#12803,#12804,#12805,#12806,#12807,#12808,#12809,#12810,
#12811,#12812,#12813,#12814,#12815,#12816,#12817,#12818,#12819,#12820,#12821,
#12822,#12823,#12824,#12825,#12826,#12827,#12828,#12829,#12830,#12831,#12832,
#12833,#12834,#12835,#12836,#12837,#12838,#12839,#12840,#12841,#12842,#12843,
#12844,#12845,#12846,#12847,#12848,#12849,#12850,#12851,#12852,#12853,#12854,
#12855,#12856,#12857,#12858,#12859,#12860,#12861,#12862,#12863,#12864,#12865,
#12866,#12867,#12868,#12869,#12870,#12871,#12872,#12873,#12874,#12875,#12876,
#12877,#12878,#12879,#12880,#12881,#12882,#12883,#12884,#12885,#12886,#12887,
#12888,#12889,#12890,#12891,#12892,#12893,#12894,#12895,#12896,#12897,#12898,
#12899,#12900,#12901,#12902,#12903,#12904,#12905,#12906,#12907,#12908,#12909,
#12910,#12911,#12912,#12913,#12914,#12915,#12916,#12917,#12918,#12919,#12920,
#12921,#12922,#12923,#12924,#12925,#12926,#12927,#12928,#12929,#12930,#12931,
#12932,#12933,#12934,#12935,#12936,#12937,#12938,#12939,#12940,#12941,#12942,
#12943,#12944,#12945,#12946,#12947,#12948,#12949,#12950,#12951));
#2903=EDGE_LOOP('',(#12952,#12953,#12954,#12955));
#3156=LINE('',#17633,#3684);
#3157=LINE('',#17963,#3685);
#3158=LINE('',#18429,#3686);
#3159=LINE('',#18895,#3687);
#3160=LINE('',#19364,#3688);
#3161=LINE('',#19830,#3689);
#3162=LINE('',#20296,#3690);
#3163=LINE('',#20762,#3691);
#3164=LINE('',#21225,#3692);
#3165=LINE('',#21691,#3693);
#3166=LINE('',#21947,#3694);
#3167=LINE('',#22200,#3695);
#3168=LINE('',#22660,#3696);
#3169=LINE('',#23126,#3697);
#3170=LINE('',#23592,#3698);
#3171=LINE('',#24055,#3699);
#3172=LINE('',#24521,#3700);
#3173=LINE('',#24987,#3701);
#3174=LINE('',#25453,#3702);
#3175=LINE('',#25922,#3703);
#3176=LINE('',#26388,#3704);
#3177=LINE('',#26854,#3705);
#3178=LINE('',#27317,#3706);
#3179=LINE('',#27789,#3707);
#3180=LINE('',#28255,#3708);
#3181=LINE('',#28721,#3709);
#3182=LINE('',#29193,#3710);
#3183=LINE('',#29659,#3711);
#3184=LINE('',#30122,#3712);
#3185=LINE('',#30585,#3713);
#3186=LINE('',#31057,#3714);
#3187=LINE('',#31523,#3715);
#3188=LINE('',#31986,#3716);
#3189=LINE('',#32455,#3717);
#3190=LINE('',#32921,#3718);
#3191=LINE('',#33384,#3719);
#3192=LINE('',#33847,#3720);
#3193=LINE('',#34316,#3721);
#3194=LINE('',#34782,#3722);
#3195=LINE('',#35245,#3723);
#3196=LINE('',#35711,#3724);
#3197=LINE('',#36177,#3725);
#3198=LINE('',#36640,#3726);
#3199=LINE('',#37103,#3727);
#3200=LINE('',#37572,#3728);
#3201=LINE('',#38038,#3729);
#3202=LINE('',#38501,#3730);
#3203=LINE('',#38967,#3731);
#3204=LINE('',#39433,#3732);
#3205=LINE('',#39896,#3733);
#3206=LINE('',#40365,#3734);
#3207=LINE('',#40834,#3735);
#3208=LINE('',#41300,#3736);
#3209=LINE('',#41763,#3737);
#3210=LINE('',#42229,#3738);
#3211=LINE('',#42695,#3739);
#3212=LINE('',#43158,#3740);
#3213=LINE('',#43630,#3741);
#3214=LINE('',#44099,#3742);
#3215=LINE('',#44562,#3743);
#3216=LINE('',#45025,#3744);
#3217=LINE('',#45491,#3745);
#3218=LINE('',#45957,#3746);
#3219=LINE('',#46417,#3747);
#3220=LINE('',#46886,#3748);
#3221=LINE('',#47355,#3749);
#3222=LINE('',#47818,#3750);
#3223=LINE('',#48284,#3751);
#3224=LINE('',#48747,#3752);
#3225=LINE('',#49213,#3753);
#3226=LINE('',#49676,#3754);
#3227=LINE('',#49935,#3755);
#3228=LINE('',#50188,#3756);
#3229=LINE('',#50648,#3757);
#3230=LINE('',#51114,#3758);
#3231=LINE('',#51577,#3759);
#3232=LINE('',#52043,#3760);
#3233=LINE('',#52509,#3761);
#3234=LINE('',#52978,#3762);
#3235=LINE('',#53447,#3763);
#3236=LINE('',#53910,#3764);
#3237=LINE('',#54376,#3765);
#3238=LINE('',#54839,#3766);
#3239=LINE('',#55305,#3767);
#3240=LINE('',#55771,#3768);
#3241=LINE('',#56240,#3769);
#3242=LINE('',#56709,#3770);
#3243=LINE('',#57172,#3771);
#3244=LINE('',#57638,#3772);
#3245=LINE('',#58101,#3773);
#3246=LINE('',#58570,#3774);
#3247=LINE('',#59036,#3775);
#3248=LINE('',#59502,#3776);
#3249=LINE('',#59971,#3777);
#3250=LINE('',#60437,#3778);
#3251=LINE('',#60900,#3779);
#3252=LINE('',#61363,#3780);
#3253=LINE('',#61832,#3781);
#3254=LINE('',#62298,#3782);
#3255=LINE('',#62764,#3783);
#3256=LINE('',#63236,#3784);
#3257=LINE('',#63702,#3785);
#3258=LINE('',#64165,#3786);
#3259=LINE('',#64628,#3787);
#3260=LINE('',#65094,#3788);
#3261=LINE('',#65560,#3789);
#3262=LINE('',#66026,#3790);
#3263=LINE('',#66495,#3791);
#3264=LINE('',#66961,#3792);
#3265=LINE('',#67424,#3793);
#3266=LINE('',#67887,#3794);
#3267=LINE('',#68353,#3795);
#3268=LINE('',#68819,#3796);
#3269=LINE('',#69285,#3797);
#3270=LINE('',#69754,#3798);
#3271=LINE('',#70220,#3799);
#3272=LINE('',#70683,#3800);
#3273=LINE('',#71152,#3801);
#3274=LINE('',#71618,#3802);
#3275=LINE('',#72081,#3803);
#3276=LINE('',#72547,#3804);
#3277=LINE('',#73016,#3805);
#3278=LINE('',#73482,#3806);
#3279=LINE('',#73945,#3807);
#3280=LINE('',#74414,#3808);
#3281=LINE('',#74880,#3809);
#3282=LINE('',#75343,#3810);
#3283=LINE('',#75809,#3811);
#3284=LINE('',#76278,#3812);
#3285=LINE('',#76744,#3813);
#3286=LINE('',#77204,#3814);
#3287=LINE('',#77670,#3815);
#3288=LINE('',#78136,#3816);
#3289=LINE('',#78599,#3817);
#3290=LINE('',#79065,#3818);
#3291=LINE('',#79534,#3819);
#3292=LINE('',#80000,#3820);
#3293=LINE('',#80460,#3821);
#3294=LINE('',#80926,#3822);
#3295=LINE('',#81392,#3823);
#3296=LINE('',#81855,#3824);
#3297=LINE('',#82114,#3825);
#3298=LINE('',#82365,#3826);
#3299=LINE('',#82825,#3827);
#3300=LINE('',#83285,#3828);
#3301=LINE('',#83751,#3829);
#3302=LINE('',#84217,#3830);
#3303=LINE('',#84680,#3831);
#3304=LINE('',#85149,#3832);
#3305=LINE('',#85615,#3833);
#3306=LINE('',#86084,#3834);
#3307=LINE('',#86550,#3835);
#3308=LINE('',#87016,#3836);
#3309=LINE('',#87482,#3837);
#3310=LINE('',#87945,#3838);
#3311=LINE('',#88414,#3839);
#3312=LINE('',#88880,#3840);
#3313=LINE('',#89349,#3841);
#3314=LINE('',#89815,#3842);
#3315=LINE('',#90278,#3843);
#3316=LINE('',#90744,#3844);
#3317=LINE('',#91207,#3845);
#3318=LINE('',#91676,#3846);
#3319=LINE('',#92142,#3847);
#3320=LINE('',#92611,#3848);
#3321=LINE('',#93077,#3849);
#3322=LINE('',#93540,#3850);
#3323=LINE('',#94006,#3851);
#3324=LINE('',#94472,#3852);
#3325=LINE('',#94941,#3853);
#3326=LINE('',#95407,#3854);
#3327=LINE('',#95870,#3855);
#3328=LINE('',#96336,#3856);
#3329=LINE('',#96799,#3857);
#3330=LINE('',#97265,#3858);
#3331=LINE('',#97731,#3859);
#3332=LINE('',#97990,#3860);
#3333=LINE('',#98450,#3861);
#3334=LINE('',#98916,#3862);
#3335=LINE('',#99382,#3863);
#3336=LINE('',#99845,#3864);
#3337=LINE('',#100311,#3865);
#3338=LINE('',#100777,#3866);
#3339=LINE('',#101243,#3867);
#3340=LINE('',#101712,#3868);
#3341=LINE('',#102178,#3869);
#3342=LINE('',#102641,#3870);
#3343=LINE('',#103104,#3871);
#3344=LINE('',#103576,#3872);
#3345=LINE('',#104042,#3873);
#3346=LINE('',#104508,#3874);
#3347=LINE('',#104980,#3875);
#3348=LINE('',#105446,#3876);
#3349=LINE('',#105909,#3877);
#3350=LINE('',#106372,#3878);
#3351=LINE('',#106844,#3879);
#3352=LINE('',#107310,#3880);
#3353=LINE('',#107773,#3881);
#3354=LINE('',#108242,#3882);
#3355=LINE('',#108708,#3883);
#3356=LINE('',#109171,#3884);
#3357=LINE('',#109634,#3885);
#3358=LINE('',#109893,#3886);
#3359=LINE('',#110353,#3887);
#3360=LINE('',#110816,#3888);
#3361=LINE('',#111282,#3889);
#3362=LINE('',#111748,#3890);
#3363=LINE('',#112211,#3891);
#3364=LINE('',#112674,#3892);
#3365=LINE('',#113143,#3893);
#3366=LINE('',#113609,#3894);
#3367=LINE('',#114072,#3895);
#3368=LINE('',#114538,#3896);
#3369=LINE('',#115004,#3897);
#3370=LINE('',#115467,#3898);
#3371=LINE('',#115936,#3899);
#3372=LINE('',#116405,#3900);
#3373=LINE('',#116871,#3901);
#3374=LINE('',#117334,#3902);
#3375=LINE('',#117800,#3903);
#3376=LINE('',#118266,#3904);
#3377=LINE('',#118729,#3905);
#3378=LINE('',#119201,#3906);
#3379=LINE('',#119670,#3907);
#3380=LINE('',#120133,#3908);
#3381=LINE('',#120596,#3909);
#3382=LINE('',#121059,#3910);
#3383=LINE('',#121525,#3911);
#3384=LINE('',#121985,#3912);
#3385=LINE('',#122454,#3913);
#3386=LINE('',#122923,#3914);
#3387=LINE('',#123386,#3915);
#3388=LINE('',#123852,#3916);
#3389=LINE('',#124315,#3917);
#3390=LINE('',#124781,#3918);
#3391=LINE('',#125244,#3919);
#3392=LINE('',#125503,#3920);
#3393=LINE('',#125756,#3921);
#3394=LINE('',#126216,#3922);
#3395=LINE('',#126682,#3923);
#3396=LINE('',#127145,#3924);
#3397=LINE('',#127611,#3925);
#3398=LINE('',#128077,#3926);
#3399=LINE('',#128546,#3927);
#3400=LINE('',#129015,#3928);
#3401=LINE('',#129478,#3929);
#3402=LINE('',#129944,#3930);
#3403=LINE('',#130407,#3931);
#3404=LINE('',#130873,#3932);
#3405=LINE('',#131339,#3933);
#3406=LINE('',#131808,#3934);
#3407=LINE('',#132277,#3935);
#3408=LINE('',#132740,#3936);
#3409=LINE('',#133206,#3937);
#3410=LINE('',#133669,#3938);
#3411=LINE('',#134138,#3939);
#3412=LINE('',#134604,#3940);
#3413=LINE('',#135070,#3941);
#3414=LINE('',#135539,#3942);
#3415=LINE('',#136005,#3943);
#3416=LINE('',#136468,#3944);
#3417=LINE('',#136931,#3945);
#3418=LINE('',#137400,#3946);
#3419=LINE('',#137866,#3947);
#3420=LINE('',#138332,#3948);
#3421=LINE('',#138804,#3949);
#3422=LINE('',#139270,#3950);
#3423=LINE('',#139733,#3951);
#3424=LINE('',#188395,#3952);
#3425=LINE('',#188616,#3953);
#3426=LINE('',#188618,#3954);
#3427=LINE('',#188620,#3955);
#3428=LINE('',#188621,#3956);
#3429=LINE('',#188627,#3957);
#3430=LINE('',#188629,#3958);
#3431=LINE('',#188631,#3959);
#3432=LINE('',#188632,#3960);
#3433=LINE('',#188638,#3961);
#3684=VECTOR('',#15852,4.91825);
#3685=VECTOR('',#15857,4.91825);
#3686=VECTOR('',#15860,4.91825);
#3687=VECTOR('',#15863,4.91825);
#3688=VECTOR('',#15866,4.91825);
#3689=VECTOR('',#15869,4.91825);
#3690=VECTOR('',#15872,4.91825);
#3691=VECTOR('',#15875,4.91825);
#3692=VECTOR('',#15878,4.91825);
#3693=VECTOR('',#15881,4.91825);
#3694=VECTOR('',#15884,4.91825);
#3695=VECTOR('',#15887,4.91825);
#3696=VECTOR('',#15890,4.91825);
#3697=VECTOR('',#15893,4.91825);
#3698=VECTOR('',#15896,4.91825);
#3699=VECTOR('',#15899,4.91825);
#3700=VECTOR('',#15902,4.91825);
#3701=VECTOR('',#15905,4.91825);
#3702=VECTOR('',#15908,4.91825);
#3703=VECTOR('',#15911,4.91825);
#3704=VECTOR('',#15914,4.91825);
#3705=VECTOR('',#15917,4.91825);
#3706=VECTOR('',#15920,4.91825);
#3707=VECTOR('',#15923,4.91825);
#3708=VECTOR('',#15926,4.91825);
#3709=VECTOR('',#15929,4.91825);
#3710=VECTOR('',#15932,4.91825);
#3711=VECTOR('',#15935,4.91825);
#3712=VECTOR('',#15938,4.91825);
#3713=VECTOR('',#15941,4.91825);
#3714=VECTOR('',#15944,4.91825);
#3715=VECTOR('',#15947,4.91825);
#3716=VECTOR('',#15950,4.91825);
#3717=VECTOR('',#15953,4.91825);
#3718=VECTOR('',#15956,4.91825);
#3719=VECTOR('',#15959,4.91825);
#3720=VECTOR('',#15962,4.91825);
#3721=VECTOR('',#15965,4.91825);
#3722=VECTOR('',#15968,4.91825);
#3723=VECTOR('',#15971,4.91825);
#3724=VECTOR('',#15974,4.91825);
#3725=VECTOR('',#15977,4.91825);
#3726=VECTOR('',#15980,4.91825);
#3727=VECTOR('',#15983,4.91825);
#3728=VECTOR('',#15986,4.91825);
#3729=VECTOR('',#15989,4.91825);
#3730=VECTOR('',#15992,4.91825);
#3731=VECTOR('',#15995,4.91825);
#3732=VECTOR('',#15998,4.91825);
#3733=VECTOR('',#16001,4.91825);
#3734=VECTOR('',#16004,4.91825);
#3735=VECTOR('',#16007,4.91825);
#3736=VECTOR('',#16010,4.91825);
#3737=VECTOR('',#16013,4.91825);
#3738=VECTOR('',#16016,4.91825);
#3739=VECTOR('',#16019,4.91825);
#3740=VECTOR('',#16022,4.91825);
#3741=VECTOR('',#16025,4.91825);
#3742=VECTOR('',#16028,4.91825);
#3743=VECTOR('',#16031,4.91825);
#3744=VECTOR('',#16034,4.91825);
#3745=VECTOR('',#16037,4.91825);
#3746=VECTOR('',#16040,4.91825);
#3747=VECTOR('',#16043,4.91825);
#3748=VECTOR('',#16046,4.91825);
#3749=VECTOR('',#16049,4.91825);
#3750=VECTOR('',#16052,4.91825);
#3751=VECTOR('',#16055,4.91825);
#3752=VECTOR('',#16058,4.91825);
#3753=VECTOR('',#16061,4.91825);
#3754=VECTOR('',#16064,4.91825);
#3755=VECTOR('',#16067,4.91825);
#3756=VECTOR('',#16070,4.91825);
#3757=VECTOR('',#16073,4.91825);
#3758=VECTOR('',#16076,4.91825);
#3759=VECTOR('',#16079,4.91825);
#3760=VECTOR('',#16082,4.91825);
#3761=VECTOR('',#16085,4.91825);
#3762=VECTOR('',#16088,4.91825);
#3763=VECTOR('',#16091,4.91825);
#3764=VECTOR('',#16094,4.91825);
#3765=VECTOR('',#16097,4.91825);
#3766=VECTOR('',#16100,4.91825);
#3767=VECTOR('',#16103,4.91825);
#3768=VECTOR('',#16106,4.91825);
#3769=VECTOR('',#16109,4.91825);
#3770=VECTOR('',#16112,4.91825);
#3771=VECTOR('',#16115,4.91825);
#3772=VECTOR('',#16118,4.91825);
#3773=VECTOR('',#16121,4.91825);
#3774=VECTOR('',#16124,4.91825);
#3775=VECTOR('',#16127,4.91825);
#3776=VECTOR('',#16130,4.91825);
#3777=VECTOR('',#16133,4.91825);
#3778=VECTOR('',#16136,4.91825);
#3779=VECTOR('',#16139,4.91825);
#3780=VECTOR('',#16142,4.91825);
#3781=VECTOR('',#16145,4.91825);
#3782=VECTOR('',#16148,4.91825);
#3783=VECTOR('',#16151,4.91825);
#3784=VECTOR('',#16154,4.91825);
#3785=VECTOR('',#16157,4.91825);
#3786=VECTOR('',#16160,4.91825);
#3787=VECTOR('',#16163,4.91825);
#3788=VECTOR('',#16166,4.91825);
#3789=VECTOR('',#16169,4.91825);
#3790=VECTOR('',#16172,4.91825);
#3791=VECTOR('',#16175,4.91825);
#3792=VECTOR('',#16178,4.91825);
#3793=VECTOR('',#16181,4.91825);
#3794=VECTOR('',#16184,4.91825);
#3795=VECTOR('',#16187,4.91825);
#3796=VECTOR('',#16190,4.91825);
#3797=VECTOR('',#16193,4.91825);
#3798=VECTOR('',#16196,4.91825);
#3799=VECTOR('',#16199,4.91825);
#3800=VECTOR('',#16202,4.91825);
#3801=VECTOR('',#16205,4.91825);
#3802=VECTOR('',#16208,4.91825);
#3803=VECTOR('',#16211,4.91825);
#3804=VECTOR('',#16214,4.91825);
#3805=VECTOR('',#16217,4.91825);
#3806=VECTOR('',#16220,4.91825);
#3807=VECTOR('',#16223,4.91825);
#3808=VECTOR('',#16226,4.91825);
#3809=VECTOR('',#16229,4.91825);
#3810=VECTOR('',#16232,4.91825);
#3811=VECTOR('',#16235,4.91825);
#3812=VECTOR('',#16238,4.91825);
#3813=VECTOR('',#16241,4.91825);
#3814=VECTOR('',#16244,4.91825);
#3815=VECTOR('',#16247,4.91825);
#3816=VECTOR('',#16250,4.91825);
#3817=VECTOR('',#16253,4.91825);
#3818=VECTOR('',#16256,4.91825);
#3819=VECTOR('',#16259,4.91825);
#3820=VECTOR('',#16262,4.91825);
#3821=VECTOR('',#16265,4.91825);
#3822=VECTOR('',#16268,4.91825);
#3823=VECTOR('',#16271,4.91825);
#3824=VECTOR('',#16274,4.91825);
#3825=VECTOR('',#16277,4.91825);
#3826=VECTOR('',#16280,4.91825);
#3827=VECTOR('',#16283,4.91825);
#3828=VECTOR('',#16286,4.91825);
#3829=VECTOR('',#16289,4.91825);
#3830=VECTOR('',#16292,4.91825);
#3831=VECTOR('',#16295,4.91825);
#3832=VECTOR('',#16298,4.91825);
#3833=VECTOR('',#16301,4.91825);
#3834=VECTOR('',#16304,4.91825);
#3835=VECTOR('',#16307,4.91825);
#3836=VECTOR('',#16310,4.91825);
#3837=VECTOR('',#16313,4.91825);
#3838=VECTOR('',#16316,4.91825);
#3839=VECTOR('',#16319,4.91825);
#3840=VECTOR('',#16322,4.91825);
#3841=VECTOR('',#16325,4.91825);
#3842=VECTOR('',#16328,4.91825);
#3843=VECTOR('',#16331,4.91825);
#3844=VECTOR('',#16334,4.91825);
#3845=VECTOR('',#16337,4.91825);
#3846=VECTOR('',#16340,4.91825);
#3847=VECTOR('',#16343,4.91825);
#3848=VECTOR('',#16346,4.91825);
#3849=VECTOR('',#16349,4.91825);
#3850=VECTOR('',#16352,4.91825);
#3851=VECTOR('',#16355,4.91825);
#3852=VECTOR('',#16358,4.91825);
#3853=VECTOR('',#16361,4.91825);
#3854=VECTOR('',#16364,4.91825);
#3855=VECTOR('',#16367,4.91825);
#3856=VECTOR('',#16370,4.91825);
#3857=VECTOR('',#16373,4.91825);
#3858=VECTOR('',#16376,4.91825);
#3859=VECTOR('',#16379,4.91825);
#3860=VECTOR('',#16382,4.91825);
#3861=VECTOR('',#16385,4.91825);
#3862=VECTOR('',#16388,4.91825);
#3863=VECTOR('',#16391,4.91825);
#3864=VECTOR('',#16394,4.91825);
#3865=VECTOR('',#16397,4.91825);
#3866=VECTOR('',#16400,4.91825);
#3867=VECTOR('',#16403,4.91825);
#3868=VECTOR('',#16406,4.91825);
#3869=VECTOR('',#16409,4.91825);
#3870=VECTOR('',#16412,4.91825);
#3871=VECTOR('',#16415,4.91825);
#3872=VECTOR('',#16418,4.91825);
#3873=VECTOR('',#16421,4.91825);
#3874=VECTOR('',#16424,4.91825);
#3875=VECTOR('',#16427,4.91825);
#3876=VECTOR('',#16430,4.91825);
#3877=VECTOR('',#16433,4.91825);
#3878=VECTOR('',#16436,4.91825);
#3879=VECTOR('',#16439,4.91825);
#3880=VECTOR('',#16442,4.91825);
#3881=VECTOR('',#16445,4.91825);
#3882=VECTOR('',#16448,4.91825);
#3883=VECTOR('',#16451,4.91825);
#3884=VECTOR('',#16454,4.91825);
#3885=VECTOR('',#16457,4.91825);
#3886=VECTOR('',#16460,4.91825);
#3887=VECTOR('',#16463,4.91825);
#3888=VECTOR('',#16466,4.91825);
#3889=VECTOR('',#16469,4.91825);
#3890=VECTOR('',#16472,4.91825);
#3891=VECTOR('',#16475,4.91825);
#3892=VECTOR('',#16478,4.91825);
#3893=VECTOR('',#16481,4.91825);
#3894=VECTOR('',#16484,4.91825);
#3895=VECTOR('',#16487,4.91825);
#3896=VECTOR('',#16490,4.91825);
#3897=VECTOR('',#16493,4.91825);
#3898=VECTOR('',#16496,4.91825);
#3899=VECTOR('',#16499,4.91825);
#3900=VECTOR('',#16502,4.91825);
#3901=VECTOR('',#16505,4.91825);
#3902=VECTOR('',#16508,4.91825);
#3903=VECTOR('',#16511,4.91825);
#3904=VECTOR('',#16514,4.91825);
#3905=VECTOR('',#16517,4.91825);
#3906=VECTOR('',#16520,4.91825);
#3907=VECTOR('',#16523,4.91825);
#3908=VECTOR('',#16526,4.91825);
#3909=VECTOR('',#16529,4.91825);
#3910=VECTOR('',#16532,4.91825);
#3911=VECTOR('',#16535,4.91825);
#3912=VECTOR('',#16538,4.91825);
#3913=VECTOR('',#16541,4.91825);
#3914=VECTOR('',#16544,4.91825);
#3915=VECTOR('',#16547,4.91825);
#3916=VECTOR('',#16550,4.91825);
#3917=VECTOR('',#16553,4.91825);
#3918=VECTOR('',#16556,4.91825);
#3919=VECTOR('',#16559,4.91825);
#3920=VECTOR('',#16562,4.91825);
#3921=VECTOR('',#16565,4.91825);
#3922=VECTOR('',#16568,4.91825);
#3923=VECTOR('',#16571,4.91825);
#3924=VECTOR('',#16574,4.91825);
#3925=VECTOR('',#16577,4.91825);
#3926=VECTOR('',#16580,4.91825);
#3927=VECTOR('',#16583,4.91825);
#3928=VECTOR('',#16586,4.91825);
#3929=VECTOR('',#16589,4.91825);
#3930=VECTOR('',#16592,4.91825);
#3931=VECTOR('',#16595,4.91825);
#3932=VECTOR('',#16598,4.91825);
#3933=VECTOR('',#16601,4.91825);
#3934=VECTOR('',#16604,4.91825);
#3935=VECTOR('',#16607,4.91825);
#3936=VECTOR('',#16610,4.91825);
#3937=VECTOR('',#16613,4.91825);
#3938=VECTOR('',#16616,4.91825);
#3939=VECTOR('',#16619,4.91825);
#3940=VECTOR('',#16622,4.91825);
#3941=VECTOR('',#16625,4.91825);
#3942=VECTOR('',#16628,4.91825);
#3943=VECTOR('',#16631,4.91825);
#3944=VECTOR('',#16634,4.91825);
#3945=VECTOR('',#16637,4.91825);
#3946=VECTOR('',#16640,4.91825);
#3947=VECTOR('',#16643,4.91825);
#3948=VECTOR('',#16646,4.91825);
#3949=VECTOR('',#16649,4.91825);
#3950=VECTOR('',#16652,4.91825);
#3951=VECTOR('',#16655,4.91825);
#3952=VECTOR('',#16674,9.);
#3953=VECTOR('',#16681,10.);
#3954=VECTOR('',#16682,10.);
#3955=VECTOR('',#16683,10.);
#3956=VECTOR('',#16684,10.);
#3957=VECTOR('',#16691,10.);
#3958=VECTOR('',#16692,10.);
#3959=VECTOR('',#16693,10.);
#3960=VECTOR('',#16694,10.);
#3961=VECTOR('',#16703,7.);
#4176=CIRCLE('',#15106,4.91825);
#4177=CIRCLE('',#15375,5.91675);
#4178=CIRCLE('',#15376,5.91675);
#4179=CIRCLE('',#15378,4.91825);
#4180=CIRCLE('',#15380,9.);
#4181=CIRCLE('',#15381,7.);
#4182=CIRCLE('',#15383,9.);
#4183=CIRCLE('',#15387,7.);
#4184=CIRCLE('',#15390,7.);
#4185=CIRCLE('',#15391,7.);
#4186=CIRCLE('',#15393,7.);
#4187=CIRCLE('',#15394,7.);
#4356=VERTEX_POINT('',#17631);
#4357=VERTEX_POINT('',#17632);
#4358=VERTEX_POINT('',#17634);
#4359=VERTEX_POINT('',#17822);
#4360=VERTEX_POINT('',#17961);
#4361=VERTEX_POINT('',#17962);
#4362=VERTEX_POINT('',#17964);
#4363=VERTEX_POINT('',#18195);
#4364=VERTEX_POINT('',#18427);
#4365=VERTEX_POINT('',#18428);
#4366=VERTEX_POINT('',#18430);
#4367=VERTEX_POINT('',#18661);
#4368=VERTEX_POINT('',#18893);
#4369=VERTEX_POINT('',#18894);
#4370=VERTEX_POINT('',#18896);
#4371=VERTEX_POINT('',#19130);
#4372=VERTEX_POINT('',#19362);
#4373=VERTEX_POINT('',#19363);
#4374=VERTEX_POINT('',#19365);
#4375=VERTEX_POINT('',#19596);
#4376=VERTEX_POINT('',#19828);
#4377=VERTEX_POINT('',#19829);
#4378=VERTEX_POINT('',#19831);
#4379=VERTEX_POINT('',#20059);
#4380=VERTEX_POINT('',#20294);
#4381=VERTEX_POINT('',#20295);
#4382=VERTEX_POINT('',#20297);
#4383=VERTEX_POINT('',#20528);
#4384=VERTEX_POINT('',#20760);
#4385=VERTEX_POINT('',#20761);
#4386=VERTEX_POINT('',#20763);
#4387=VERTEX_POINT('',#20994);
#4388=VERTEX_POINT('',#21223);
#4389=VERTEX_POINT('',#21224);
#4390=VERTEX_POINT('',#21226);
#4391=VERTEX_POINT('',#21457);
#4392=VERTEX_POINT('',#21689);
#4393=VERTEX_POINT('',#21690);
#4394=VERTEX_POINT('',#21692);
#4395=VERTEX_POINT('',#21923);
#4396=VERTEX_POINT('',#21945);
#4397=VERTEX_POINT('',#21946);
#4398=VERTEX_POINT('',#21948);
#4399=VERTEX_POINT('',#22182);
#4400=VERTEX_POINT('',#22198);
#4401=VERTEX_POINT('',#22199);
#4402=VERTEX_POINT('',#22201);
#4403=VERTEX_POINT('',#22432);
#4404=VERTEX_POINT('',#22658);
#4405=VERTEX_POINT('',#22659);
#4406=VERTEX_POINT('',#22661);
#4407=VERTEX_POINT('',#22892);
#4408=VERTEX_POINT('',#23124);
#4409=VERTEX_POINT('',#23125);
#4410=VERTEX_POINT('',#23127);
#4411=VERTEX_POINT('',#23358);
#4412=VERTEX_POINT('',#23590);
#4413=VERTEX_POINT('',#23591);
#4414=VERTEX_POINT('',#23593);
#4415=VERTEX_POINT('',#23824);
#4416=VERTEX_POINT('',#24053);
#4417=VERTEX_POINT('',#24054);
#4418=VERTEX_POINT('',#24056);
#4419=VERTEX_POINT('',#24287);
#4420=VERTEX_POINT('',#24519);
#4421=VERTEX_POINT('',#24520);
#4422=VERTEX_POINT('',#24522);
#4423=VERTEX_POINT('',#24753);
#4424=VERTEX_POINT('',#24985);
#4425=VERTEX_POINT('',#24986);
#4426=VERTEX_POINT('',#24988);
#4427=VERTEX_POINT('',#25219);
#4428=VERTEX_POINT('',#25451);
#4429=VERTEX_POINT('',#25452);
#4430=VERTEX_POINT('',#25454);
#4431=VERTEX_POINT('',#25688);
#4432=VERTEX_POINT('',#25920);
#4433=VERTEX_POINT('',#25921);
#4434=VERTEX_POINT('',#25923);
#4435=VERTEX_POINT('',#26154);
#4436=VERTEX_POINT('',#26386);
#4437=VERTEX_POINT('',#26387);
#4438=VERTEX_POINT('',#26389);
#4439=VERTEX_POINT('',#26620);
#4440=VERTEX_POINT('',#26852);
#4441=VERTEX_POINT('',#26853);
#4442=VERTEX_POINT('',#26855);
#4443=VERTEX_POINT('',#27086);
#4444=VERTEX_POINT('',#27315);
#4445=VERTEX_POINT('',#27316);
#4446=VERTEX_POINT('',#27318);
#4447=VERTEX_POINT('',#27549);
#4448=VERTEX_POINT('',#27787);
#4449=VERTEX_POINT('',#27788);
#4450=VERTEX_POINT('',#27790);
#4451=VERTEX_POINT('',#28021);
#4452=VERTEX_POINT('',#28253);
#4453=VERTEX_POINT('',#28254);
#4454=VERTEX_POINT('',#28256);
#4455=VERTEX_POINT('',#28487);
#4456=VERTEX_POINT('',#28719);
#4457=VERTEX_POINT('',#28720);
#4458=VERTEX_POINT('',#28722);
#4459=VERTEX_POINT('',#28959);
#4460=VERTEX_POINT('',#29191);
#4461=VERTEX_POINT('',#29192);
#4462=VERTEX_POINT('',#29194);
#4463=VERTEX_POINT('',#29425);
#4464=VERTEX_POINT('',#29657);
#4465=VERTEX_POINT('',#29658);
#4466=VERTEX_POINT('',#29660);
#4467=VERTEX_POINT('',#29888);
#4468=VERTEX_POINT('',#30120);
#4469=VERTEX_POINT('',#30121);
#4470=VERTEX_POINT('',#30123);
#4471=VERTEX_POINT('',#30354);
#4472=VERTEX_POINT('',#30583);
#4473=VERTEX_POINT('',#30584);
#4474=VERTEX_POINT('',#30586);
#4475=VERTEX_POINT('',#30817);
#4476=VERTEX_POINT('',#31055);
#4477=VERTEX_POINT('',#31056);
#4478=VERTEX_POINT('',#31058);
#4479=VERTEX_POINT('',#31289);
#4480=VERTEX_POINT('',#31521);
#4481=VERTEX_POINT('',#31522);
#4482=VERTEX_POINT('',#31524);
#4483=VERTEX_POINT('',#31755);
#4484=VERTEX_POINT('',#31984);
#4485=VERTEX_POINT('',#31985);
#4486=VERTEX_POINT('',#31987);
#4487=VERTEX_POINT('',#32221);
#4488=VERTEX_POINT('',#32453);
#4489=VERTEX_POINT('',#32454);
#4490=VERTEX_POINT('',#32456);
#4491=VERTEX_POINT('',#32687);
#4492=VERTEX_POINT('',#32919);
#4493=VERTEX_POINT('',#32920);
#4494=VERTEX_POINT('',#32922);
#4495=VERTEX_POINT('',#33150);
#4496=VERTEX_POINT('',#33382);
#4497=VERTEX_POINT('',#33383);
#4498=VERTEX_POINT('',#33385);
#4499=VERTEX_POINT('',#33616);
#4500=VERTEX_POINT('',#33845);
#4501=VERTEX_POINT('',#33846);
#4502=VERTEX_POINT('',#33848);
#4503=VERTEX_POINT('',#34079);
#4504=VERTEX_POINT('',#34314);
#4505=VERTEX_POINT('',#34315);
#4506=VERTEX_POINT('',#34317);
#4507=VERTEX_POINT('',#34548);
#4508=VERTEX_POINT('',#34780);
#4509=VERTEX_POINT('',#34781);
#4510=VERTEX_POINT('',#34783);
#4511=VERTEX_POINT('',#35014);
#4512=VERTEX_POINT('',#35243);
#4513=VERTEX_POINT('',#35244);
#4514=VERTEX_POINT('',#35246);
#4515=VERTEX_POINT('',#35477);
#4516=VERTEX_POINT('',#35709);
#4517=VERTEX_POINT('',#35710);
#4518=VERTEX_POINT('',#35712);
#4519=VERTEX_POINT('',#35943);
#4520=VERTEX_POINT('',#36175);
#4521=VERTEX_POINT('',#36176);
#4522=VERTEX_POINT('',#36178);
#4523=VERTEX_POINT('',#36406);
#4524=VERTEX_POINT('',#36638);
#4525=VERTEX_POINT('',#36639);
#4526=VERTEX_POINT('',#36641);
#4527=VERTEX_POINT('',#36872);
#4528=VERTEX_POINT('',#37101);
#4529=VERTEX_POINT('',#37102);
#4530=VERTEX_POINT('',#37104);
#4531=VERTEX_POINT('',#37335);
#4532=VERTEX_POINT('',#37570);
#4533=VERTEX_POINT('',#37571);
#4534=VERTEX_POINT('',#37573);
#4535=VERTEX_POINT('',#37804);
#4536=VERTEX_POINT('',#38036);
#4537=VERTEX_POINT('',#38037);
#4538=VERTEX_POINT('',#38039);
#4539=VERTEX_POINT('',#38270);
#4540=VERTEX_POINT('',#38499);
#4541=VERTEX_POINT('',#38500);
#4542=VERTEX_POINT('',#38502);
#4543=VERTEX_POINT('',#38733);
#4544=VERTEX_POINT('',#38965);
#4545=VERTEX_POINT('',#38966);
#4546=VERTEX_POINT('',#38968);
#4547=VERTEX_POINT('',#39199);
#4548=VERTEX_POINT('',#39431);
#4549=VERTEX_POINT('',#39432);
#4550=VERTEX_POINT('',#39434);
#4551=VERTEX_POINT('',#39662);
#4552=VERTEX_POINT('',#39894);
#4553=VERTEX_POINT('',#39895);
#4554=VERTEX_POINT('',#39897);
#4555=VERTEX_POINT('',#40131);
#4556=VERTEX_POINT('',#40363);
#4557=VERTEX_POINT('',#40364);
#4558=VERTEX_POINT('',#40366);
#4559=VERTEX_POINT('',#40597);
#4560=VERTEX_POINT('',#40832);
#4561=VERTEX_POINT('',#40833);
#4562=VERTEX_POINT('',#40835);
#4563=VERTEX_POINT('',#41066);
#4564=VERTEX_POINT('',#41298);
#4565=VERTEX_POINT('',#41299);
#4566=VERTEX_POINT('',#41301);
#4567=VERTEX_POINT('',#41532);
#4568=VERTEX_POINT('',#41761);
#4569=VERTEX_POINT('',#41762);
#4570=VERTEX_POINT('',#41764);
#4571=VERTEX_POINT('',#41995);
#4572=VERTEX_POINT('',#42227);
#4573=VERTEX_POINT('',#42228);
#4574=VERTEX_POINT('',#42230);
#4575=VERTEX_POINT('',#42461);
#4576=VERTEX_POINT('',#42693);
#4577=VERTEX_POINT('',#42694);
#4578=VERTEX_POINT('',#42696);
#4579=VERTEX_POINT('',#42924);
#4580=VERTEX_POINT('',#43156);
#4581=VERTEX_POINT('',#43157);
#4582=VERTEX_POINT('',#43159);
#4583=VERTEX_POINT('',#43396);
#4584=VERTEX_POINT('',#43628);
#4585=VERTEX_POINT('',#43629);
#4586=VERTEX_POINT('',#43631);
#4587=VERTEX_POINT('',#43862);
#4588=VERTEX_POINT('',#44097);
#4589=VERTEX_POINT('',#44098);
#4590=VERTEX_POINT('',#44100);
#4591=VERTEX_POINT('',#44328);
#4592=VERTEX_POINT('',#44560);
#4593=VERTEX_POINT('',#44561);
#4594=VERTEX_POINT('',#44563);
#4595=VERTEX_POINT('',#44794);
#4596=VERTEX_POINT('',#45023);
#4597=VERTEX_POINT('',#45024);
#4598=VERTEX_POINT('',#45026);
#4599=VERTEX_POINT('',#45257);
#4600=VERTEX_POINT('',#45489);
#4601=VERTEX_POINT('',#45490);
#4602=VERTEX_POINT('',#45492);
#4603=VERTEX_POINT('',#45723);
#4604=VERTEX_POINT('',#45955);
#4605=VERTEX_POINT('',#45956);
#4606=VERTEX_POINT('',#45958);
#4607=VERTEX_POINT('',#46186);
#4608=VERTEX_POINT('',#46415);
#4609=VERTEX_POINT('',#46416);
#4610=VERTEX_POINT('',#46418);
#4611=VERTEX_POINT('',#46652);
#4612=VERTEX_POINT('',#46884);
#4613=VERTEX_POINT('',#46885);
#4614=VERTEX_POINT('',#46887);
#4615=VERTEX_POINT('',#47118);
#4616=VERTEX_POINT('',#47353);
#4617=VERTEX_POINT('',#47354);
#4618=VERTEX_POINT('',#47356);
#4619=VERTEX_POINT('',#47584);
#4620=VERTEX_POINT('',#47816);
#4621=VERTEX_POINT('',#47817);
#4622=VERTEX_POINT('',#47819);
#4623=VERTEX_POINT('',#48050);
#4624=VERTEX_POINT('',#48282);
#4625=VERTEX_POINT('',#48283);
#4626=VERTEX_POINT('',#48285);
#4627=VERTEX_POINT('',#48516);
#4628=VERTEX_POINT('',#48745);
#4629=VERTEX_POINT('',#48746);
#4630=VERTEX_POINT('',#48748);
#4631=VERTEX_POINT('',#48979);
#4632=VERTEX_POINT('',#49211);
#4633=VERTEX_POINT('',#49212);
#4634=VERTEX_POINT('',#49214);
#4635=VERTEX_POINT('',#49442);
#4636=VERTEX_POINT('',#49674);
#4637=VERTEX_POINT('',#49675);
#4638=VERTEX_POINT('',#49677);
#4639=VERTEX_POINT('',#49701);
#4640=VERTEX_POINT('',#49933);
#4641=VERTEX_POINT('',#49934);
#4642=VERTEX_POINT('',#49936);
#4643=VERTEX_POINT('',#49951);
#4644=VERTEX_POINT('',#50186);
#4645=VERTEX_POINT('',#50187);
#4646=VERTEX_POINT('',#50189);
#4647=VERTEX_POINT('',#50411);
#4648=VERTEX_POINT('',#50646);
#4649=VERTEX_POINT('',#50647);
#4650=VERTEX_POINT('',#50649);
#4651=VERTEX_POINT('',#50880);
#4652=VERTEX_POINT('',#51112);
#4653=VERTEX_POINT('',#51113);
#4654=VERTEX_POINT('',#51115);
#4655=VERTEX_POINT('',#51346);
#4656=VERTEX_POINT('',#51575);
#4657=VERTEX_POINT('',#51576);
#4658=VERTEX_POINT('',#51578);
#4659=VERTEX_POINT('',#51809);
#4660=VERTEX_POINT('',#52041);
#4661=VERTEX_POINT('',#52042);
#4662=VERTEX_POINT('',#52044);
#4663=VERTEX_POINT('',#52275);
#4664=VERTEX_POINT('',#52507);
#4665=VERTEX_POINT('',#52508);
#4666=VERTEX_POINT('',#52510);
#4667=VERTEX_POINT('',#52744);
#4668=VERTEX_POINT('',#52976);
#4669=VERTEX_POINT('',#52977);
#4670=VERTEX_POINT('',#52979);
#4671=VERTEX_POINT('',#53210);
#4672=VERTEX_POINT('',#53445);
#4673=VERTEX_POINT('',#53446);
#4674=VERTEX_POINT('',#53448);
#4675=VERTEX_POINT('',#53676);
#4676=VERTEX_POINT('',#53908);
#4677=VERTEX_POINT('',#53909);
#4678=VERTEX_POINT('',#53911);
#4679=VERTEX_POINT('',#54142);
#4680=VERTEX_POINT('',#54374);
#4681=VERTEX_POINT('',#54375);
#4682=VERTEX_POINT('',#54377);
#4683=VERTEX_POINT('',#54608);
#4684=VERTEX_POINT('',#54837);
#4685=VERTEX_POINT('',#54838);
#4686=VERTEX_POINT('',#54840);
#4687=VERTEX_POINT('',#55071);
#4688=VERTEX_POINT('',#55303);
#4689=VERTEX_POINT('',#55304);
#4690=VERTEX_POINT('',#55306);
#4691=VERTEX_POINT('',#55537);
#4692=VERTEX_POINT('',#55769);
#4693=VERTEX_POINT('',#55770);
#4694=VERTEX_POINT('',#55772);
#4695=VERTEX_POINT('',#56006);
#4696=VERTEX_POINT('',#56238);
#4697=VERTEX_POINT('',#56239);
#4698=VERTEX_POINT('',#56241);
#4699=VERTEX_POINT('',#56472);
#4700=VERTEX_POINT('',#56707);
#4701=VERTEX_POINT('',#56708);
#4702=VERTEX_POINT('',#56710);
#4703=VERTEX_POINT('',#56938);
#4704=VERTEX_POINT('',#57170);
#4705=VERTEX_POINT('',#57171);
#4706=VERTEX_POINT('',#57173);
#4707=VERTEX_POINT('',#57404);
#4708=VERTEX_POINT('',#57636);
#4709=VERTEX_POINT('',#57637);
#4710=VERTEX_POINT('',#57639);
#4711=VERTEX_POINT('',#57870);
#4712=VERTEX_POINT('',#58099);
#4713=VERTEX_POINT('',#58100);
#4714=VERTEX_POINT('',#58102);
#4715=VERTEX_POINT('',#58330);
#4716=VERTEX_POINT('',#58568);
#4717=VERTEX_POINT('',#58569);
#4718=VERTEX_POINT('',#58571);
#4719=VERTEX_POINT('',#58802);
#4720=VERTEX_POINT('',#59034);
#4721=VERTEX_POINT('',#59035);
#4722=VERTEX_POINT('',#59037);
#4723=VERTEX_POINT('',#59271);
#4724=VERTEX_POINT('',#59500);
#4725=VERTEX_POINT('',#59501);
#4726=VERTEX_POINT('',#59503);
#4727=VERTEX_POINT('',#59734);
#4728=VERTEX_POINT('',#59969);
#4729=VERTEX_POINT('',#59970);
#4730=VERTEX_POINT('',#59972);
#4731=VERTEX_POINT('',#60203);
#4732=VERTEX_POINT('',#60435);
#4733=VERTEX_POINT('',#60436);
#4734=VERTEX_POINT('',#60438);
#4735=VERTEX_POINT('',#60666);
#4736=VERTEX_POINT('',#60898);
#4737=VERTEX_POINT('',#60899);
#4738=VERTEX_POINT('',#60901);
#4739=VERTEX_POINT('',#61132);
#4740=VERTEX_POINT('',#61361);
#4741=VERTEX_POINT('',#61362);
#4742=VERTEX_POINT('',#61364);
#4743=VERTEX_POINT('',#61595);
#4744=VERTEX_POINT('',#61830);
#4745=VERTEX_POINT('',#61831);
#4746=VERTEX_POINT('',#61833);
#4747=VERTEX_POINT('',#62064);
#4748=VERTEX_POINT('',#62296);
#4749=VERTEX_POINT('',#62297);
#4750=VERTEX_POINT('',#62299);
#4751=VERTEX_POINT('',#62533);
#4752=VERTEX_POINT('',#62762);
#4753=VERTEX_POINT('',#62763);
#4754=VERTEX_POINT('',#62765);
#4755=VERTEX_POINT('',#62999);
#4756=VERTEX_POINT('',#63234);
#4757=VERTEX_POINT('',#63235);
#4758=VERTEX_POINT('',#63237);
#4759=VERTEX_POINT('',#63468);
#4760=VERTEX_POINT('',#63700);
#4761=VERTEX_POINT('',#63701);
#4762=VERTEX_POINT('',#63703);
#4763=VERTEX_POINT('',#63931);
#4764=VERTEX_POINT('',#64163);
#4765=VERTEX_POINT('',#64164);
#4766=VERTEX_POINT('',#64166);
#4767=VERTEX_POINT('',#64397);
#4768=VERTEX_POINT('',#64626);
#4769=VERTEX_POINT('',#64627);
#4770=VERTEX_POINT('',#64629);
#4771=VERTEX_POINT('',#64860);
#4772=VERTEX_POINT('',#65092);
#4773=VERTEX_POINT('',#65093);
#4774=VERTEX_POINT('',#65095);
#4775=VERTEX_POINT('',#65326);
#4776=VERTEX_POINT('',#65558);
#4777=VERTEX_POINT('',#65559);
#4778=VERTEX_POINT('',#65561);
#4779=VERTEX_POINT('',#65795);
#4780=VERTEX_POINT('',#66024);
#4781=VERTEX_POINT('',#66025);
#4782=VERTEX_POINT('',#66027);
#4783=VERTEX_POINT('',#66258);
#4784=VERTEX_POINT('',#66493);
#4785=VERTEX_POINT('',#66494);
#4786=VERTEX_POINT('',#66496);
#4787=VERTEX_POINT('',#66727);
#4788=VERTEX_POINT('',#66959);
#4789=VERTEX_POINT('',#66960);
#4790=VERTEX_POINT('',#66962);
#4791=VERTEX_POINT('',#67190);
#4792=VERTEX_POINT('',#67422);
#4793=VERTEX_POINT('',#67423);
#4794=VERTEX_POINT('',#67425);
#4795=VERTEX_POINT('',#67656);
#4796=VERTEX_POINT('',#67885);
#4797=VERTEX_POINT('',#67886);
#4798=VERTEX_POINT('',#67888);
#4799=VERTEX_POINT('',#68119);
#4800=VERTEX_POINT('',#68351);
#4801=VERTEX_POINT('',#68352);
#4802=VERTEX_POINT('',#68354);
#4803=VERTEX_POINT('',#68585);
#4804=VERTEX_POINT('',#68817);
#4805=VERTEX_POINT('',#68818);
#4806=VERTEX_POINT('',#68820);
#4807=VERTEX_POINT('',#69054);
#4808=VERTEX_POINT('',#69283);
#4809=VERTEX_POINT('',#69284);
#4810=VERTEX_POINT('',#69286);
#4811=VERTEX_POINT('',#69517);
#4812=VERTEX_POINT('',#69752);
#4813=VERTEX_POINT('',#69753);
#4814=VERTEX_POINT('',#69755);
#4815=VERTEX_POINT('',#69986);
#4816=VERTEX_POINT('',#70218);
#4817=VERTEX_POINT('',#70219);
#4818=VERTEX_POINT('',#70221);
#4819=VERTEX_POINT('',#70449);
#4820=VERTEX_POINT('',#70681);
#4821=VERTEX_POINT('',#70682);
#4822=VERTEX_POINT('',#70684);
#4823=VERTEX_POINT('',#70921);
#4824=VERTEX_POINT('',#71150);
#4825=VERTEX_POINT('',#71151);
#4826=VERTEX_POINT('',#71153);
#4827=VERTEX_POINT('',#71384);
#4828=VERTEX_POINT('',#71616);
#4829=VERTEX_POINT('',#71617);
#4830=VERTEX_POINT('',#71619);
#4831=VERTEX_POINT('',#71847);
#4832=VERTEX_POINT('',#72079);
#4833=VERTEX_POINT('',#72080);
#4834=VERTEX_POINT('',#72082);
#4835=VERTEX_POINT('',#72316);
#4836=VERTEX_POINT('',#72545);
#4837=VERTEX_POINT('',#72546);
#4838=VERTEX_POINT('',#72548);
#4839=VERTEX_POINT('',#72779);
#4840=VERTEX_POINT('',#73014);
#4841=VERTEX_POINT('',#73015);
#4842=VERTEX_POINT('',#73017);
#4843=VERTEX_POINT('',#73248);
#4844=VERTEX_POINT('',#73480);
#4845=VERTEX_POINT('',#73481);
#4846=VERTEX_POINT('',#73483);
#4847=VERTEX_POINT('',#73711);
#4848=VERTEX_POINT('',#73943);
#4849=VERTEX_POINT('',#73944);
#4850=VERTEX_POINT('',#73946);
#4851=VERTEX_POINT('',#74180);
#4852=VERTEX_POINT('',#74412);
#4853=VERTEX_POINT('',#74413);
#4854=VERTEX_POINT('',#74415);
#4855=VERTEX_POINT('',#74646);
#4856=VERTEX_POINT('',#74878);
#4857=VERTEX_POINT('',#74879);
#4858=VERTEX_POINT('',#74881);
#4859=VERTEX_POINT('',#75109);
#4860=VERTEX_POINT('',#75341);
#4861=VERTEX_POINT('',#75342);
#4862=VERTEX_POINT('',#75344);
#4863=VERTEX_POINT('',#75578);
#4864=VERTEX_POINT('',#75807);
#4865=VERTEX_POINT('',#75808);
#4866=VERTEX_POINT('',#75810);
#4867=VERTEX_POINT('',#76041);
#4868=VERTEX_POINT('',#76276);
#4869=VERTEX_POINT('',#76277);
#4870=VERTEX_POINT('',#76279);
#4871=VERTEX_POINT('',#76510);
#4872=VERTEX_POINT('',#76742);
#4873=VERTEX_POINT('',#76743);
#4874=VERTEX_POINT('',#76745);
#4875=VERTEX_POINT('',#76973);
#4876=VERTEX_POINT('',#77202);
#4877=VERTEX_POINT('',#77203);
#4878=VERTEX_POINT('',#77205);
#4879=VERTEX_POINT('',#77436);
#4880=VERTEX_POINT('',#77668);
#4881=VERTEX_POINT('',#77669);
#4882=VERTEX_POINT('',#77671);
#4883=VERTEX_POINT('',#77902);
#4884=VERTEX_POINT('',#78134);
#4885=VERTEX_POINT('',#78135);
#4886=VERTEX_POINT('',#78137);
#4887=VERTEX_POINT('',#78365);
#4888=VERTEX_POINT('',#78597);
#4889=VERTEX_POINT('',#78598);
#4890=VERTEX_POINT('',#78600);
#4891=VERTEX_POINT('',#78834);
#4892=VERTEX_POINT('',#79063);
#4893=VERTEX_POINT('',#79064);
#4894=VERTEX_POINT('',#79066);
#4895=VERTEX_POINT('',#79297);
#4896=VERTEX_POINT('',#79532);
#4897=VERTEX_POINT('',#79533);
#4898=VERTEX_POINT('',#79535);
#4899=VERTEX_POINT('',#79766);
#4900=VERTEX_POINT('',#79998);
#4901=VERTEX_POINT('',#79999);
#4902=VERTEX_POINT('',#80001);
#4903=VERTEX_POINT('',#80229);
#4904=VERTEX_POINT('',#80458);
#4905=VERTEX_POINT('',#80459);
#4906=VERTEX_POINT('',#80461);
#4907=VERTEX_POINT('',#80692);
#4908=VERTEX_POINT('',#80924);
#4909=VERTEX_POINT('',#80925);
#4910=VERTEX_POINT('',#80927);
#4911=VERTEX_POINT('',#81158);
#4912=VERTEX_POINT('',#81390);
#4913=VERTEX_POINT('',#81391);
#4914=VERTEX_POINT('',#81393);
#4915=VERTEX_POINT('',#81621);
#4916=VERTEX_POINT('',#81853);
#4917=VERTEX_POINT('',#81854);
#4918=VERTEX_POINT('',#81856);
#4919=VERTEX_POINT('',#82090);
#4920=VERTEX_POINT('',#82112);
#4921=VERTEX_POINT('',#82113);
#4922=VERTEX_POINT('',#82115);
#4923=VERTEX_POINT('',#82346);
#4924=VERTEX_POINT('',#82363);
#4925=VERTEX_POINT('',#82364);
#4926=VERTEX_POINT('',#82366);
#4927=VERTEX_POINT('',#82597);
#4928=VERTEX_POINT('',#82823);
#4929=VERTEX_POINT('',#82824);
#4930=VERTEX_POINT('',#82826);
#4931=VERTEX_POINT('',#83054);
#4932=VERTEX_POINT('',#83283);
#4933=VERTEX_POINT('',#83284);
#4934=VERTEX_POINT('',#83286);
#4935=VERTEX_POINT('',#83517);
#4936=VERTEX_POINT('',#83749);
#4937=VERTEX_POINT('',#83750);
#4938=VERTEX_POINT('',#83752);
#4939=VERTEX_POINT('',#83983);
#4940=VERTEX_POINT('',#84215);
#4941=VERTEX_POINT('',#84216);
#4942=VERTEX_POINT('',#84218);
#4943=VERTEX_POINT('',#84446);
#4944=VERTEX_POINT('',#84678);
#4945=VERTEX_POINT('',#84679);
#4946=VERTEX_POINT('',#84681);
#4947=VERTEX_POINT('',#84915);
#4948=VERTEX_POINT('',#85147);
#4949=VERTEX_POINT('',#85148);
#4950=VERTEX_POINT('',#85150);
#4951=VERTEX_POINT('',#85381);
#4952=VERTEX_POINT('',#85613);
#4953=VERTEX_POINT('',#85614);
#4954=VERTEX_POINT('',#85616);
#4955=VERTEX_POINT('',#85847);
#4956=VERTEX_POINT('',#86082);
#4957=VERTEX_POINT('',#86083);
#4958=VERTEX_POINT('',#86085);
#4959=VERTEX_POINT('',#86316);
#4960=VERTEX_POINT('',#86548);
#4961=VERTEX_POINT('',#86549);
#4962=VERTEX_POINT('',#86551);
#4963=VERTEX_POINT('',#86782);
#4964=VERTEX_POINT('',#87014);
#4965=VERTEX_POINT('',#87015);
#4966=VERTEX_POINT('',#87017);
#4967=VERTEX_POINT('',#87248);
#4968=VERTEX_POINT('',#87480);
#4969=VERTEX_POINT('',#87481);
#4970=VERTEX_POINT('',#87483);
#4971=VERTEX_POINT('',#87711);
#4972=VERTEX_POINT('',#87943);
#4973=VERTEX_POINT('',#87944);
#4974=VERTEX_POINT('',#87946);
#4975=VERTEX_POINT('',#88180);
#4976=VERTEX_POINT('',#88412);
#4977=VERTEX_POINT('',#88413);
#4978=VERTEX_POINT('',#88415);
#4979=VERTEX_POINT('',#88646);
#4980=VERTEX_POINT('',#88878);
#4981=VERTEX_POINT('',#88879);
#4982=VERTEX_POINT('',#88881);
#4983=VERTEX_POINT('',#89112);
#4984=VERTEX_POINT('',#89347);
#4985=VERTEX_POINT('',#89348);
#4986=VERTEX_POINT('',#89350);
#4987=VERTEX_POINT('',#89581);
#4988=VERTEX_POINT('',#89813);
#4989=VERTEX_POINT('',#89814);
#4990=VERTEX_POINT('',#89816);
#4991=VERTEX_POINT('',#90047);
#4992=VERTEX_POINT('',#90276);
#4993=VERTEX_POINT('',#90277);
#4994=VERTEX_POINT('',#90279);
#4995=VERTEX_POINT('',#90510);
#4996=VERTEX_POINT('',#90742);
#4997=VERTEX_POINT('',#90743);
#4998=VERTEX_POINT('',#90745);
#4999=VERTEX_POINT('',#90973);
#5000=VERTEX_POINT('',#91205);
#5001=VERTEX_POINT('',#91206);
#5002=VERTEX_POINT('',#91208);
#5003=VERTEX_POINT('',#91442);
#5004=VERTEX_POINT('',#91674);
#5005=VERTEX_POINT('',#91675);
#5006=VERTEX_POINT('',#91677);
#5007=VERTEX_POINT('',#91908);
#5008=VERTEX_POINT('',#92140);
#5009=VERTEX_POINT('',#92141);
#5010=VERTEX_POINT('',#92143);
#5011=VERTEX_POINT('',#92371);
#5012=VERTEX_POINT('',#92609);
#5013=VERTEX_POINT('',#92610);
#5014=VERTEX_POINT('',#92612);
#5015=VERTEX_POINT('',#92843);
#5016=VERTEX_POINT('',#93075);
#5017=VERTEX_POINT('',#93076);
#5018=VERTEX_POINT('',#93078);
#5019=VERTEX_POINT('',#93309);
#5020=VERTEX_POINT('',#93538);
#5021=VERTEX_POINT('',#93539);
#5022=VERTEX_POINT('',#93541);
#5023=VERTEX_POINT('',#93772);
#5024=VERTEX_POINT('',#94004);
#5025=VERTEX_POINT('',#94005);
#5026=VERTEX_POINT('',#94007);
#5027=VERTEX_POINT('',#94238);
#5028=VERTEX_POINT('',#94470);
#5029=VERTEX_POINT('',#94471);
#5030=VERTEX_POINT('',#94473);
#5031=VERTEX_POINT('',#94707);
#5032=VERTEX_POINT('',#94939);
#5033=VERTEX_POINT('',#94940);
#5034=VERTEX_POINT('',#94942);
#5035=VERTEX_POINT('',#95173);
#5036=VERTEX_POINT('',#95405);
#5037=VERTEX_POINT('',#95406);
#5038=VERTEX_POINT('',#95408);
#5039=VERTEX_POINT('',#95636);
#5040=VERTEX_POINT('',#95868);
#5041=VERTEX_POINT('',#95869);
#5042=VERTEX_POINT('',#95871);
#5043=VERTEX_POINT('',#96102);
#5044=VERTEX_POINT('',#96334);
#5045=VERTEX_POINT('',#96335);
#5046=VERTEX_POINT('',#96337);
#5047=VERTEX_POINT('',#96568);
#5048=VERTEX_POINT('',#96797);
#5049=VERTEX_POINT('',#96798);
#5050=VERTEX_POINT('',#96800);
#5051=VERTEX_POINT('',#97031);
#5052=VERTEX_POINT('',#97263);
#5053=VERTEX_POINT('',#97264);
#5054=VERTEX_POINT('',#97266);
#5055=VERTEX_POINT('',#97497);
#5056=VERTEX_POINT('',#97729);
#5057=VERTEX_POINT('',#97730);
#5058=VERTEX_POINT('',#97732);
#5059=VERTEX_POINT('',#97966);
#5060=VERTEX_POINT('',#97988);
#5061=VERTEX_POINT('',#97989);
#5062=VERTEX_POINT('',#97991);
#5063=VERTEX_POINT('',#98222);
#5064=VERTEX_POINT('',#98448);
#5065=VERTEX_POINT('',#98449);
#5066=VERTEX_POINT('',#98451);
#5067=VERTEX_POINT('',#98682);
#5068=VERTEX_POINT('',#98914);
#5069=VERTEX_POINT('',#98915);
#5070=VERTEX_POINT('',#98917);
#5071=VERTEX_POINT('',#99148);
#5072=VERTEX_POINT('',#99380);
#5073=VERTEX_POINT('',#99381);
#5074=VERTEX_POINT('',#99383);
#5075=VERTEX_POINT('',#99614);
#5076=VERTEX_POINT('',#99843);
#5077=VERTEX_POINT('',#99844);
#5078=VERTEX_POINT('',#99846);
#5079=VERTEX_POINT('',#100077);
#5080=VERTEX_POINT('',#100309);
#5081=VERTEX_POINT('',#100310);
#5082=VERTEX_POINT('',#100312);
#5083=VERTEX_POINT('',#100543);
#5084=VERTEX_POINT('',#100775);
#5085=VERTEX_POINT('',#100776);
#5086=VERTEX_POINT('',#100778);
#5087=VERTEX_POINT('',#101009);
#5088=VERTEX_POINT('',#101241);
#5089=VERTEX_POINT('',#101242);
#5090=VERTEX_POINT('',#101244);
#5091=VERTEX_POINT('',#101478);
#5092=VERTEX_POINT('',#101710);
#5093=VERTEX_POINT('',#101711);
#5094=VERTEX_POINT('',#101713);
#5095=VERTEX_POINT('',#101944);
#5096=VERTEX_POINT('',#102176);
#5097=VERTEX_POINT('',#102177);
#5098=VERTEX_POINT('',#102179);
#5099=VERTEX_POINT('',#102407);
#5100=VERTEX_POINT('',#102639);
#5101=VERTEX_POINT('',#102640);
#5102=VERTEX_POINT('',#102642);
#5103=VERTEX_POINT('',#102873);
#5104=VERTEX_POINT('',#103102);
#5105=VERTEX_POINT('',#103103);
#5106=VERTEX_POINT('',#103105);
#5107=VERTEX_POINT('',#103336);
#5108=VERTEX_POINT('',#103574);
#5109=VERTEX_POINT('',#103575);
#5110=VERTEX_POINT('',#103577);
#5111=VERTEX_POINT('',#103808);
#5112=VERTEX_POINT('',#104040);
#5113=VERTEX_POINT('',#104041);
#5114=VERTEX_POINT('',#104043);
#5115=VERTEX_POINT('',#104274);
#5116=VERTEX_POINT('',#104506);
#5117=VERTEX_POINT('',#104507);
#5118=VERTEX_POINT('',#104509);
#5119=VERTEX_POINT('',#104746);
#5120=VERTEX_POINT('',#104978);
#5121=VERTEX_POINT('',#104979);
#5122=VERTEX_POINT('',#104981);
#5123=VERTEX_POINT('',#105212);
#5124=VERTEX_POINT('',#105444);
#5125=VERTEX_POINT('',#105445);
#5126=VERTEX_POINT('',#105447);
#5127=VERTEX_POINT('',#105675);
#5128=VERTEX_POINT('',#105907);
#5129=VERTEX_POINT('',#105908);
#5130=VERTEX_POINT('',#105910);
#5131=VERTEX_POINT('',#106141);
#5132=VERTEX_POINT('',#106370);
#5133=VERTEX_POINT('',#106371);
#5134=VERTEX_POINT('',#106373);
#5135=VERTEX_POINT('',#106604);
#5136=VERTEX_POINT('',#106842);
#5137=VERTEX_POINT('',#106843);
#5138=VERTEX_POINT('',#106845);
#5139=VERTEX_POINT('',#107076);
#5140=VERTEX_POINT('',#107308);
#5141=VERTEX_POINT('',#107309);
#5142=VERTEX_POINT('',#107311);
#5143=VERTEX_POINT('',#107542);
#5144=VERTEX_POINT('',#107771);
#5145=VERTEX_POINT('',#107772);
#5146=VERTEX_POINT('',#107774);
#5147=VERTEX_POINT('',#108008);
#5148=VERTEX_POINT('',#108240);
#5149=VERTEX_POINT('',#108241);
#5150=VERTEX_POINT('',#108243);
#5151=VERTEX_POINT('',#108474);
#5152=VERTEX_POINT('',#108706);
#5153=VERTEX_POINT('',#108707);
#5154=VERTEX_POINT('',#108709);
#5155=VERTEX_POINT('',#108937);
#5156=VERTEX_POINT('',#109169);
#5157=VERTEX_POINT('',#109170);
#5158=VERTEX_POINT('',#109172);
#5159=VERTEX_POINT('',#109403);
#5160=VERTEX_POINT('',#109632);
#5161=VERTEX_POINT('',#109633);
#5162=VERTEX_POINT('',#109635);
#5163=VERTEX_POINT('',#109656);
#5164=VERTEX_POINT('',#109891);
#5165=VERTEX_POINT('',#109892);
#5166=VERTEX_POINT('',#109894);
#5167=VERTEX_POINT('',#110119);
#5168=VERTEX_POINT('',#110351);
#5169=VERTEX_POINT('',#110352);
#5170=VERTEX_POINT('',#110354);
#5171=VERTEX_POINT('',#110585);
#5172=VERTEX_POINT('',#110814);
#5173=VERTEX_POINT('',#110815);
#5174=VERTEX_POINT('',#110817);
#5175=VERTEX_POINT('',#111048);
#5176=VERTEX_POINT('',#111280);
#5177=VERTEX_POINT('',#111281);
#5178=VERTEX_POINT('',#111283);
#5179=VERTEX_POINT('',#111514);
#5180=VERTEX_POINT('',#111746);
#5181=VERTEX_POINT('',#111747);
#5182=VERTEX_POINT('',#111749);
#5183=VERTEX_POINT('',#111977);
#5184=VERTEX_POINT('',#112209);
#5185=VERTEX_POINT('',#112210);
#5186=VERTEX_POINT('',#112212);
#5187=VERTEX_POINT('',#112443);
#5188=VERTEX_POINT('',#112672);
#5189=VERTEX_POINT('',#112673);
#5190=VERTEX_POINT('',#112675);
#5191=VERTEX_POINT('',#112906);
#5192=VERTEX_POINT('',#113141);
#5193=VERTEX_POINT('',#113142);
#5194=VERTEX_POINT('',#113144);
#5195=VERTEX_POINT('',#113375);
#5196=VERTEX_POINT('',#113607);
#5197=VERTEX_POINT('',#113608);
#5198=VERTEX_POINT('',#113610);
#5199=VERTEX_POINT('',#113841);
#5200=VERTEX_POINT('',#114070);
#5201=VERTEX_POINT('',#114071);
#5202=VERTEX_POINT('',#114073);
#5203=VERTEX_POINT('',#114304);
#5204=VERTEX_POINT('',#114536);
#5205=VERTEX_POINT('',#114537);
#5206=VERTEX_POINT('',#114539);
#5207=VERTEX_POINT('',#114770);
#5208=VERTEX_POINT('',#115002);
#5209=VERTEX_POINT('',#115003);
#5210=VERTEX_POINT('',#115005);
#5211=VERTEX_POINT('',#115233);
#5212=VERTEX_POINT('',#115465);
#5213=VERTEX_POINT('',#115466);
#5214=VERTEX_POINT('',#115468);
#5215=VERTEX_POINT('',#115702);
#5216=VERTEX_POINT('',#115934);
#5217=VERTEX_POINT('',#115935);
#5218=VERTEX_POINT('',#115937);
#5219=VERTEX_POINT('',#116168);
#5220=VERTEX_POINT('',#116403);
#5221=VERTEX_POINT('',#116404);
#5222=VERTEX_POINT('',#116406);
#5223=VERTEX_POINT('',#116637);
#5224=VERTEX_POINT('',#116869);
#5225=VERTEX_POINT('',#116870);
#5226=VERTEX_POINT('',#116872);
#5227=VERTEX_POINT('',#117103);
#5228=VERTEX_POINT('',#117332);
#5229=VERTEX_POINT('',#117333);
#5230=VERTEX_POINT('',#117335);
#5231=VERTEX_POINT('',#117566);
#5232=VERTEX_POINT('',#117798);
#5233=VERTEX_POINT('',#117799);
#5234=VERTEX_POINT('',#117801);
#5235=VERTEX_POINT('',#118032);
#5236=VERTEX_POINT('',#118264);
#5237=VERTEX_POINT('',#118265);
#5238=VERTEX_POINT('',#118267);
#5239=VERTEX_POINT('',#118495);
#5240=VERTEX_POINT('',#118727);
#5241=VERTEX_POINT('',#118728);
#5242=VERTEX_POINT('',#118730);
#5243=VERTEX_POINT('',#118967);
#5244=VERTEX_POINT('',#119199);
#5245=VERTEX_POINT('',#119200);
#5246=VERTEX_POINT('',#119202);
#5247=VERTEX_POINT('',#119433);
#5248=VERTEX_POINT('',#119668);
#5249=VERTEX_POINT('',#119669);
#5250=VERTEX_POINT('',#119671);
#5251=VERTEX_POINT('',#119899);
#5252=VERTEX_POINT('',#120131);
#5253=VERTEX_POINT('',#120132);
#5254=VERTEX_POINT('',#120134);
#5255=VERTEX_POINT('',#120365);
#5256=VERTEX_POINT('',#120594);
#5257=VERTEX_POINT('',#120595);
#5258=VERTEX_POINT('',#120597);
#5259=VERTEX_POINT('',#120828);
#5260=VERTEX_POINT('',#121057);
#5261=VERTEX_POINT('',#121058);
#5262=VERTEX_POINT('',#121060);
#5263=VERTEX_POINT('',#121291);
#5264=VERTEX_POINT('',#121523);
#5265=VERTEX_POINT('',#121524);
#5266=VERTEX_POINT('',#121526);
#5267=VERTEX_POINT('',#121754);
#5268=VERTEX_POINT('',#121983);
#5269=VERTEX_POINT('',#121984);
#5270=VERTEX_POINT('',#121986);
#5271=VERTEX_POINT('',#122220);
#5272=VERTEX_POINT('',#122452);
#5273=VERTEX_POINT('',#122453);
#5274=VERTEX_POINT('',#122455);
#5275=VERTEX_POINT('',#122686);
#5276=VERTEX_POINT('',#122921);
#5277=VERTEX_POINT('',#122922);
#5278=VERTEX_POINT('',#122924);
#5279=VERTEX_POINT('',#123152);
#5280=VERTEX_POINT('',#123384);
#5281=VERTEX_POINT('',#123385);
#5282=VERTEX_POINT('',#123387);
#5283=VERTEX_POINT('',#123618);
#5284=VERTEX_POINT('',#123850);
#5285=VERTEX_POINT('',#123851);
#5286=VERTEX_POINT('',#123853);
#5287=VERTEX_POINT('',#124084);
#5288=VERTEX_POINT('',#124313);
#5289=VERTEX_POINT('',#124314);
#5290=VERTEX_POINT('',#124316);
#5291=VERTEX_POINT('',#124547);
#5292=VERTEX_POINT('',#124779);
#5293=VERTEX_POINT('',#124780);
#5294=VERTEX_POINT('',#124782);
#5295=VERTEX_POINT('',#125010);
#5296=VERTEX_POINT('',#125242);
#5297=VERTEX_POINT('',#125243);
#5298=VERTEX_POINT('',#125245);
#5299=VERTEX_POINT('',#125269);
#5300=VERTEX_POINT('',#125501);
#5301=VERTEX_POINT('',#125502);
#5302=VERTEX_POINT('',#125504);
#5303=VERTEX_POINT('',#125519);
#5304=VERTEX_POINT('',#125754);
#5305=VERTEX_POINT('',#125755);
#5306=VERTEX_POINT('',#125757);
#5307=VERTEX_POINT('',#125979);
#5308=VERTEX_POINT('',#126214);
#5309=VERTEX_POINT('',#126215);
#5310=VERTEX_POINT('',#126217);
#5311=VERTEX_POINT('',#126448);
#5312=VERTEX_POINT('',#126680);
#5313=VERTEX_POINT('',#126681);
#5314=VERTEX_POINT('',#126683);
#5315=VERTEX_POINT('',#126914);
#5316=VERTEX_POINT('',#127143);
#5317=VERTEX_POINT('',#127144);
#5318=VERTEX_POINT('',#127146);
#5319=VERTEX_POINT('',#127377);
#5320=VERTEX_POINT('',#127609);
#5321=VERTEX_POINT('',#127610);
#5322=VERTEX_POINT('',#127612);
#5323=VERTEX_POINT('',#127843);
#5324=VERTEX_POINT('',#128075);
#5325=VERTEX_POINT('',#128076);
#5326=VERTEX_POINT('',#128078);
#5327=VERTEX_POINT('',#128312);
#5328=VERTEX_POINT('',#128544);
#5329=VERTEX_POINT('',#128545);
#5330=VERTEX_POINT('',#128547);
#5331=VERTEX_POINT('',#128778);
#5332=VERTEX_POINT('',#129013);
#5333=VERTEX_POINT('',#129014);
#5334=VERTEX_POINT('',#129016);
#5335=VERTEX_POINT('',#129244);
#5336=VERTEX_POINT('',#129476);
#5337=VERTEX_POINT('',#129477);
#5338=VERTEX_POINT('',#129479);
#5339=VERTEX_POINT('',#129710);
#5340=VERTEX_POINT('',#129942);
#5341=VERTEX_POINT('',#129943);
#5342=VERTEX_POINT('',#129945);
#5343=VERTEX_POINT('',#130176);
#5344=VERTEX_POINT('',#130405);
#5345=VERTEX_POINT('',#130406);
#5346=VERTEX_POINT('',#130408);
#5347=VERTEX_POINT('',#130639);
#5348=VERTEX_POINT('',#130871);
#5349=VERTEX_POINT('',#130872);
#5350=VERTEX_POINT('',#130874);
#5351=VERTEX_POINT('',#131105);
#5352=VERTEX_POINT('',#131337);
#5353=VERTEX_POINT('',#131338);
#5354=VERTEX_POINT('',#131340);
#5355=VERTEX_POINT('',#131574);
#5356=VERTEX_POINT('',#131806);
#5357=VERTEX_POINT('',#131807);
#5358=VERTEX_POINT('',#131809);
#5359=VERTEX_POINT('',#132040);
#5360=VERTEX_POINT('',#132275);
#5361=VERTEX_POINT('',#132276);
#5362=VERTEX_POINT('',#132278);
#5363=VERTEX_POINT('',#132506);
#5364=VERTEX_POINT('',#132738);
#5365=VERTEX_POINT('',#132739);
#5366=VERTEX_POINT('',#132741);
#5367=VERTEX_POINT('',#132972);
#5368=VERTEX_POINT('',#133204);
#5369=VERTEX_POINT('',#133205);
#5370=VERTEX_POINT('',#133207);
#5371=VERTEX_POINT('',#133438);
#5372=VERTEX_POINT('',#133667);
#5373=VERTEX_POINT('',#133668);
#5374=VERTEX_POINT('',#133670);
#5375=VERTEX_POINT('',#133898);
#5376=VERTEX_POINT('',#134136);
#5377=VERTEX_POINT('',#134137);
#5378=VERTEX_POINT('',#134139);
#5379=VERTEX_POINT('',#134370);
#5380=VERTEX_POINT('',#134602);
#5381=VERTEX_POINT('',#134603);
#5382=VERTEX_POINT('',#134605);
#5383=VERTEX_POINT('',#134839);
#5384=VERTEX_POINT('',#135068);
#5385=VERTEX_POINT('',#135069);
#5386=VERTEX_POINT('',#135071);
#5387=VERTEX_POINT('',#135302);
#5388=VERTEX_POINT('',#135537);
#5389=VERTEX_POINT('',#135538);
#5390=VERTEX_POINT('',#135540);
#5391=VERTEX_POINT('',#135771);
#5392=VERTEX_POINT('',#136003);
#5393=VERTEX_POINT('',#136004);
#5394=VERTEX_POINT('',#136006);
#5395=VERTEX_POINT('',#136234);
#5396=VERTEX_POINT('',#136466);
#5397=VERTEX_POINT('',#136467);
#5398=VERTEX_POINT('',#136469);
#5399=VERTEX_POINT('',#136700);
#5400=VERTEX_POINT('',#136929);
#5401=VERTEX_POINT('',#136930);
#5402=VERTEX_POINT('',#136932);
#5403=VERTEX_POINT('',#137163);
#5404=VERTEX_POINT('',#137398);
#5405=VERTEX_POINT('',#137399);
#5406=VERTEX_POINT('',#137401);
#5407=VERTEX_POINT('',#137632);
#5408=VERTEX_POINT('',#137864);
#5409=VERTEX_POINT('',#137865);
#5410=VERTEX_POINT('',#137867);
#5411=VERTEX_POINT('',#138101);
#5412=VERTEX_POINT('',#138330);
#5413=VERTEX_POINT('',#138331);
#5414=VERTEX_POINT('',#138333);
#5415=VERTEX_POINT('',#138567);
#5416=VERTEX_POINT('',#138802);
#5417=VERTEX_POINT('',#138803);
#5418=VERTEX_POINT('',#138805);
#5419=VERTEX_POINT('',#139036);
#5420=VERTEX_POINT('',#139268);
#5421=VERTEX_POINT('',#139269);
#5422=VERTEX_POINT('',#139271);
#5423=VERTEX_POINT('',#139499);
#5424=VERTEX_POINT('',#139731);
#5425=VERTEX_POINT('',#139732);
#5426=VERTEX_POINT('',#139734);
#5427=VERTEX_POINT('',#139965);
#5428=VERTEX_POINT('',#140194);
#5429=VERTEX_POINT('',#140195);
#5430=VERTEX_POINT('',#140275);
#5431=VERTEX_POINT('',#140277);
#5432=VERTEX_POINT('',#140321);
#5433=VERTEX_POINT('',#140566);
#5434=VERTEX_POINT('',#140577);
#5435=VERTEX_POINT('',#140825);
#5436=VERTEX_POINT('',#140838);
#5437=VERTEX_POINT('',#140849);
#5438=VERTEX_POINT('',#140860);
#5439=VERTEX_POINT('',#140872);
#5440=VERTEX_POINT('',#140883);
#5441=VERTEX_POINT('',#140894);
#5442=VERTEX_POINT('',#140905);
#5443=VERTEX_POINT('',#141153);
#5444=VERTEX_POINT('',#141164);
#5445=VERTEX_POINT('',#141412);
#5446=VERTEX_POINT('',#141424);
#5447=VERTEX_POINT('',#141435);
#5448=VERTEX_POINT('',#141446);
#5449=VERTEX_POINT('',#141457);
#5450=VERTEX_POINT('',#141705);
#5451=VERTEX_POINT('',#141716);
#5452=VERTEX_POINT('',#141727);
#5453=VERTEX_POINT('',#141972);
#5454=VERTEX_POINT('',#141983);
#5455=VERTEX_POINT('',#142231);
#5456=VERTEX_POINT('',#142242);
#5457=VERTEX_POINT('',#142490);
#5458=VERTEX_POINT('',#142501);
#5459=VERTEX_POINT('',#142512);
#5460=VERTEX_POINT('',#142757);
#5461=VERTEX_POINT('',#142768);
#5462=VERTEX_POINT('',#143016);
#5463=VERTEX_POINT('',#143027);
#5464=VERTEX_POINT('',#143040);
#5465=VERTEX_POINT('',#143051);
#5466=VERTEX_POINT('',#143062);
#5467=VERTEX_POINT('',#143307);
#5468=VERTEX_POINT('',#143318);
#5469=VERTEX_POINT('',#143566);
#5470=VERTEX_POINT('',#143577);
#5471=VERTEX_POINT('',#143590);
#5472=VERTEX_POINT('',#143838);
#5473=VERTEX_POINT('',#144083);
#5474=VERTEX_POINT('',#144095);
#5475=VERTEX_POINT('',#144106);
#5476=VERTEX_POINT('',#144117);
#5477=VERTEX_POINT('',#144362);
#5478=VERTEX_POINT('',#144375);
#5479=VERTEX_POINT('',#144620);
#5480=VERTEX_POINT('',#144865);
#5481=VERTEX_POINT('',#144877);
#5482=VERTEX_POINT('',#144888);
#5483=VERTEX_POINT('',#144899);
#5484=VERTEX_POINT('',#145144);
#5485=VERTEX_POINT('',#145157);
#5486=VERTEX_POINT('',#145168);
#5487=VERTEX_POINT('',#145179);
#5488=VERTEX_POINT('',#145191);
#5489=VERTEX_POINT('',#145436);
#5490=VERTEX_POINT('',#145447);
#5491=VERTEX_POINT('',#145458);
#5492=VERTEX_POINT('',#145471);
#5493=VERTEX_POINT('',#145716);
#5494=VERTEX_POINT('',#145961);
#5495=VERTEX_POINT('',#145973);
#5496=VERTEX_POINT('',#146218);
#5497=VERTEX_POINT('',#146229);
#5498=VERTEX_POINT('',#146240);
#5499=VERTEX_POINT('',#146252);
#5500=VERTEX_POINT('',#146497);
#5501=VERTEX_POINT('',#146742);
#5502=VERTEX_POINT('',#146754);
#5503=VERTEX_POINT('',#146999);
#5504=VERTEX_POINT('',#147247);
#5505=VERTEX_POINT('',#147258);
#5506=VERTEX_POINT('',#147503);
#5507=VERTEX_POINT('',#147514);
#5508=VERTEX_POINT('',#147525);
#5509=VERTEX_POINT('',#147537);
#5510=VERTEX_POINT('',#147548);
#5511=VERTEX_POINT('',#147796);
#5512=VERTEX_POINT('',#147807);
#5513=VERTEX_POINT('',#148052);
#5514=VERTEX_POINT('',#148063);
#5515=VERTEX_POINT('',#148074);
#5516=VERTEX_POINT('',#148086);
#5517=VERTEX_POINT('',#148097);
#5518=VERTEX_POINT('',#148345);
#5519=VERTEX_POINT('',#148356);
#5520=VERTEX_POINT('',#148601);
#5521=VERTEX_POINT('',#148612);
#5522=VERTEX_POINT('',#148623);
#5523=VERTEX_POINT('',#148871);
#5524=VERTEX_POINT('',#148882);
#5525=VERTEX_POINT('',#148893);
#5526=VERTEX_POINT('',#148904);
#5527=VERTEX_POINT('',#148917);
#5528=VERTEX_POINT('',#149165);
#5529=VERTEX_POINT('',#149176);
#5530=VERTEX_POINT('',#149424);
#5531=VERTEX_POINT('',#149435);
#5532=VERTEX_POINT('',#149446);
#5533=VERTEX_POINT('',#149457);
#5534=VERTEX_POINT('',#149469);
#5535=VERTEX_POINT('',#149717);
#5536=VERTEX_POINT('',#149728);
#5537=VERTEX_POINT('',#149740);
#5538=VERTEX_POINT('',#149988);
#5539=VERTEX_POINT('',#149999);
#5540=VERTEX_POINT('',#150247);
#5541=VERTEX_POINT('',#150260);
#5542=VERTEX_POINT('',#150271);
#5543=VERTEX_POINT('',#150282);
#5544=VERTEX_POINT('',#150294);
#5545=VERTEX_POINT('',#150542);
#5546=VERTEX_POINT('',#150553);
#5547=VERTEX_POINT('',#150798);
#5548=VERTEX_POINT('',#150810);
#5549=VERTEX_POINT('',#150821);
#5550=VERTEX_POINT('',#150832);
#5551=VERTEX_POINT('',#150844);
#5552=VERTEX_POINT('',#151092);
#5553=VERTEX_POINT('',#151103);
#5554=VERTEX_POINT('',#151348);
#5555=VERTEX_POINT('',#151360);
#5556=VERTEX_POINT('',#151371);
#5557=VERTEX_POINT('',#151619);
#5558=VERTEX_POINT('',#151631);
#5559=VERTEX_POINT('',#151876);
#5560=VERTEX_POINT('',#151887);
#5561=VERTEX_POINT('',#151898);
#5562=VERTEX_POINT('',#151910);
#5563=VERTEX_POINT('',#151921);
#5564=VERTEX_POINT('',#152166);
#5565=VERTEX_POINT('',#152178);
#5566=VERTEX_POINT('',#152423);
#5567=VERTEX_POINT('',#152434);
#5568=VERTEX_POINT('',#152445);
#5569=VERTEX_POINT('',#152457);
#5570=VERTEX_POINT('',#152468);
#5571=VERTEX_POINT('',#152479);
#5572=VERTEX_POINT('',#152724);
#5573=VERTEX_POINT('',#152738);
#5574=VERTEX_POINT('',#152983);
#5575=VERTEX_POINT('',#152994);
#5576=VERTEX_POINT('',#153006);
#5577=VERTEX_POINT('',#153017);
#5578=VERTEX_POINT('',#153028);
#5579=VERTEX_POINT('',#153273);
#5580=VERTEX_POINT('',#153287);
#5581=VERTEX_POINT('',#153532);
#5582=VERTEX_POINT('',#153543);
#5583=VERTEX_POINT('',#153555);
#5584=VERTEX_POINT('',#153800);
#5585=VERTEX_POINT('',#153811);
#5586=VERTEX_POINT('',#154056);
#5587=VERTEX_POINT('',#154069);
#5588=VERTEX_POINT('',#154317);
#5589=VERTEX_POINT('',#154328);
#5590=VERTEX_POINT('',#154340);
#5591=VERTEX_POINT('',#154585);
#5592=VERTEX_POINT('',#154596);
#5593=VERTEX_POINT('',#154844);
#5594=VERTEX_POINT('',#154858);
#5595=VERTEX_POINT('',#154869);
#5596=VERTEX_POINT('',#154880);
#5597=VERTEX_POINT('',#154892);
#5598=VERTEX_POINT('',#155140);
#5599=VERTEX_POINT('',#155151);
#5600=VERTEX_POINT('',#155399);
#5601=VERTEX_POINT('',#155413);
#5602=VERTEX_POINT('',#155424);
#5603=VERTEX_POINT('',#155672);
#5604=VERTEX_POINT('',#155685);
#5605=VERTEX_POINT('',#155696);
#5606=VERTEX_POINT('',#155707);
#5607=VERTEX_POINT('',#155718);
#5608=VERTEX_POINT('',#155966);
#5609=VERTEX_POINT('',#155977);
#5610=VERTEX_POINT('',#156225);
#5611=VERTEX_POINT('',#156238);
#5612=VERTEX_POINT('',#156249);
#5613=VERTEX_POINT('',#156260);
#5614=VERTEX_POINT('',#156271);
#5615=VERTEX_POINT('',#156519);
#5616=VERTEX_POINT('',#156530);
#5617=VERTEX_POINT('',#156541);
#5618=VERTEX_POINT('',#156786);
#5619=VERTEX_POINT('',#156797);
#5620=VERTEX_POINT('',#157045);
#5621=VERTEX_POINT('',#157056);
#5622=VERTEX_POINT('',#157070);
#5623=VERTEX_POINT('',#157081);
#5624=VERTEX_POINT('',#157092);
#5625=VERTEX_POINT('',#157337);
#5626=VERTEX_POINT('',#157348);
#5627=VERTEX_POINT('',#157596);
#5628=VERTEX_POINT('',#157607);
#5629=VERTEX_POINT('',#157620);
#5630=VERTEX_POINT('',#157631);
#5631=VERTEX_POINT('',#157642);
#5632=VERTEX_POINT('',#157887);
#5633=VERTEX_POINT('',#157898);
#5634=VERTEX_POINT('',#158146);
#5635=VERTEX_POINT('',#158158);
#5636=VERTEX_POINT('',#158172);
#5637=VERTEX_POINT('',#158420);
#5638=VERTEX_POINT('',#158665);
#5639=VERTEX_POINT('',#158677);
#5640=VERTEX_POINT('',#158688);
#5641=VERTEX_POINT('',#158699);
#5642=VERTEX_POINT('',#158944);
#5643=VERTEX_POINT('',#158958);
#5644=VERTEX_POINT('',#159203);
#5645=VERTEX_POINT('',#159448);
#5646=VERTEX_POINT('',#159460);
#5647=VERTEX_POINT('',#159471);
#5648=VERTEX_POINT('',#159482);
#5649=VERTEX_POINT('',#159727);
#5650=VERTEX_POINT('',#159741);
#5651=VERTEX_POINT('',#159752);
#5652=VERTEX_POINT('',#159763);
#5653=VERTEX_POINT('',#159776);
#5654=VERTEX_POINT('',#160021);
#5655=VERTEX_POINT('',#160032);
#5656=VERTEX_POINT('',#160043);
#5657=VERTEX_POINT('',#160056);
#5658=VERTEX_POINT('',#160301);
#5659=VERTEX_POINT('',#160546);
#5660=VERTEX_POINT('',#160558);
#5661=VERTEX_POINT('',#160803);
#5662=VERTEX_POINT('',#160814);
#5663=VERTEX_POINT('',#160825);
#5664=VERTEX_POINT('',#160838);
#5665=VERTEX_POINT('',#161083);
#5666=VERTEX_POINT('',#161331);
#5667=VERTEX_POINT('',#161343);
#5668=VERTEX_POINT('',#161588);
#5669=VERTEX_POINT('',#161836);
#5670=VERTEX_POINT('',#161847);
#5671=VERTEX_POINT('',#162092);
#5672=VERTEX_POINT('',#162103);
#5673=VERTEX_POINT('',#162114);
#5674=VERTEX_POINT('',#162127);
#5675=VERTEX_POINT('',#162138);
#5676=VERTEX_POINT('',#162386);
#5677=VERTEX_POINT('',#162397);
#5678=VERTEX_POINT('',#162642);
#5679=VERTEX_POINT('',#162653);
#5680=VERTEX_POINT('',#162664);
#5681=VERTEX_POINT('',#162677);
#5682=VERTEX_POINT('',#162688);
#5683=VERTEX_POINT('',#162936);
#5684=VERTEX_POINT('',#162947);
#5685=VERTEX_POINT('',#163192);
#5686=VERTEX_POINT('',#163203);
#5687=VERTEX_POINT('',#163214);
#5688=VERTEX_POINT('',#163462);
#5689=VERTEX_POINT('',#163473);
#5690=VERTEX_POINT('',#163484);
#5691=VERTEX_POINT('',#163495);
#5692=VERTEX_POINT('',#163509);
#5693=VERTEX_POINT('',#163757);
#5694=VERTEX_POINT('',#163768);
#5695=VERTEX_POINT('',#164016);
#5696=VERTEX_POINT('',#164027);
#5697=VERTEX_POINT('',#164038);
#5698=VERTEX_POINT('',#164049);
#5699=VERTEX_POINT('',#164063);
#5700=VERTEX_POINT('',#164074);
#5701=VERTEX_POINT('',#164172);
#5702=VERTEX_POINT('',#164174);
#5703=VERTEX_POINT('',#164236);
#5704=VERTEX_POINT('',#164247);
#5705=VERTEX_POINT('',#164259);
#5706=VERTEX_POINT('',#164270);
#5707=VERTEX_POINT('',#164281);
#5708=VERTEX_POINT('',#164526);
#5709=VERTEX_POINT('',#164540);
#5710=VERTEX_POINT('',#164785);
#5711=VERTEX_POINT('',#164796);
#5712=VERTEX_POINT('',#164809);
#5713=VERTEX_POINT('',#164820);
#5714=VERTEX_POINT('',#164831);
#5715=VERTEX_POINT('',#165076);
#5716=VERTEX_POINT('',#165090);
#5717=VERTEX_POINT('',#165338);
#5718=VERTEX_POINT('',#165349);
#5719=VERTEX_POINT('',#165362);
#5720=VERTEX_POINT('',#165607);
#5721=VERTEX_POINT('',#165618);
#5722=VERTEX_POINT('',#165866);
#5723=VERTEX_POINT('',#165880);
#5724=VERTEX_POINT('',#165891);
#5725=VERTEX_POINT('',#165902);
#5726=VERTEX_POINT('',#165915);
#5727=VERTEX_POINT('',#166163);
#5728=VERTEX_POINT('',#166174);
#5729=VERTEX_POINT('',#166422);
#5730=VERTEX_POINT('',#166436);
#5731=VERTEX_POINT('',#166447);
#5732=VERTEX_POINT('',#166458);
#5733=VERTEX_POINT('',#166471);
#5734=VERTEX_POINT('',#166482);
#5735=VERTEX_POINT('',#166493);
#5736=VERTEX_POINT('',#166505);
#5737=VERTEX_POINT('',#166753);
#5738=VERTEX_POINT('',#166764);
#5739=VERTEX_POINT('',#167012);
#5740=VERTEX_POINT('',#167025);
#5741=VERTEX_POINT('',#167036);
#5742=VERTEX_POINT('',#167047);
#5743=VERTEX_POINT('',#167058);
#5744=VERTEX_POINT('',#167306);
#5745=VERTEX_POINT('',#167317);
#5746=VERTEX_POINT('',#167328);
#5747=VERTEX_POINT('',#167573);
#5748=VERTEX_POINT('',#167584);
#5749=VERTEX_POINT('',#167832);
#5750=VERTEX_POINT('',#167843);
#5751=VERTEX_POINT('',#168091);
#5752=VERTEX_POINT('',#168102);
#5753=VERTEX_POINT('',#168113);
#5754=VERTEX_POINT('',#168358);
#5755=VERTEX_POINT('',#168369);
#5756=VERTEX_POINT('',#168617);
#5757=VERTEX_POINT('',#168628);
#5758=VERTEX_POINT('',#168642);
#5759=VERTEX_POINT('',#168653);
#5760=VERTEX_POINT('',#168664);
#5761=VERTEX_POINT('',#168909);
#5762=VERTEX_POINT('',#168920);
#5763=VERTEX_POINT('',#169168);
#5764=VERTEX_POINT('',#169179);
#5765=VERTEX_POINT('',#169192);
#5766=VERTEX_POINT('',#169440);
#5767=VERTEX_POINT('',#169685);
#5768=VERTEX_POINT('',#169698);
#5769=VERTEX_POINT('',#169709);
#5770=VERTEX_POINT('',#169720);
#5771=VERTEX_POINT('',#169965);
#5772=VERTEX_POINT('',#169979);
#5773=VERTEX_POINT('',#170224);
#5774=VERTEX_POINT('',#170469);
#5775=VERTEX_POINT('',#170482);
#5776=VERTEX_POINT('',#170493);
#5777=VERTEX_POINT('',#170504);
#5778=VERTEX_POINT('',#170749);
#5779=VERTEX_POINT('',#170763);
#5780=VERTEX_POINT('',#170774);
#5781=VERTEX_POINT('',#170785);
#5782=VERTEX_POINT('',#170797);
#5783=VERTEX_POINT('',#171042);
#5784=VERTEX_POINT('',#171053);
#5785=VERTEX_POINT('',#171064);
#5786=VERTEX_POINT('',#171078);
#5787=VERTEX_POINT('',#171323);
#5788=VERTEX_POINT('',#171568);
#5789=VERTEX_POINT('',#171581);
#5790=VERTEX_POINT('',#171826);
#5791=VERTEX_POINT('',#171837);
#5792=VERTEX_POINT('',#171848);
#5793=VERTEX_POINT('',#171861);
#5794=VERTEX_POINT('',#172106);
#5795=VERTEX_POINT('',#172351);
#5796=VERTEX_POINT('',#172364);
#5797=VERTEX_POINT('',#172609);
#5798=VERTEX_POINT('',#172620);
#5799=VERTEX_POINT('',#172631);
#5800=VERTEX_POINT('',#172876);
#5801=VERTEX_POINT('',#172887);
#5802=VERTEX_POINT('',#172898);
#5803=VERTEX_POINT('',#172910);
#5804=VERTEX_POINT('',#172921);
#5805=VERTEX_POINT('',#173169);
#5806=VERTEX_POINT('',#173180);
#5807=VERTEX_POINT('',#173425);
#5808=VERTEX_POINT('',#173436);
#5809=VERTEX_POINT('',#173447);
#5810=VERTEX_POINT('',#173459);
#5811=VERTEX_POINT('',#173470);
#5812=VERTEX_POINT('',#173718);
#5813=VERTEX_POINT('',#173729);
#5814=VERTEX_POINT('',#173974);
#5815=VERTEX_POINT('',#173985);
#5816=VERTEX_POINT('',#173996);
#5817=VERTEX_POINT('',#174244);
#5818=VERTEX_POINT('',#174255);
#5819=VERTEX_POINT('',#174266);
#5820=VERTEX_POINT('',#174277);
#5821=VERTEX_POINT('',#174289);
#5822=VERTEX_POINT('',#174537);
#5823=VERTEX_POINT('',#174548);
#5824=VERTEX_POINT('',#174796);
#5825=VERTEX_POINT('',#174807);
#5826=VERTEX_POINT('',#174818);
#5827=VERTEX_POINT('',#174829);
#5828=VERTEX_POINT('',#174841);
#5829=VERTEX_POINT('',#175089);
#5830=VERTEX_POINT('',#175100);
#5831=VERTEX_POINT('',#175348);
#5832=VERTEX_POINT('',#175596);
#5833=VERTEX_POINT('',#175607);
#5834=VERTEX_POINT('',#175855);
#5835=VERTEX_POINT('',#175867);
#5836=VERTEX_POINT('',#175878);
#5837=VERTEX_POINT('',#175889);
#5838=VERTEX_POINT('',#175901);
#5839=VERTEX_POINT('',#176149);
#5840=VERTEX_POINT('',#176160);
#5841=VERTEX_POINT('',#176405);
#5842=VERTEX_POINT('',#176417);
#5843=VERTEX_POINT('',#176428);
#5844=VERTEX_POINT('',#176439);
#5845=VERTEX_POINT('',#176451);
#5846=VERTEX_POINT('',#176699);
#5847=VERTEX_POINT('',#176710);
#5848=VERTEX_POINT('',#176955);
#5849=VERTEX_POINT('',#176967);
#5850=VERTEX_POINT('',#176978);
#5851=VERTEX_POINT('',#177226);
#5852=VERTEX_POINT('',#177238);
#5853=VERTEX_POINT('',#177483);
#5854=VERTEX_POINT('',#177494);
#5855=VERTEX_POINT('',#177505);
#5856=VERTEX_POINT('',#177517);
#5857=VERTEX_POINT('',#177528);
#5858=VERTEX_POINT('',#177773);
#5859=VERTEX_POINT('',#177785);
#5860=VERTEX_POINT('',#178030);
#5861=VERTEX_POINT('',#178041);
#5862=VERTEX_POINT('',#178052);
#5863=VERTEX_POINT('',#178064);
#5864=VERTEX_POINT('',#178075);
#5865=VERTEX_POINT('',#178086);
#5866=VERTEX_POINT('',#178331);
#5867=VERTEX_POINT('',#178344);
#5868=VERTEX_POINT('',#178589);
#5869=VERTEX_POINT('',#178600);
#5870=VERTEX_POINT('',#178612);
#5871=VERTEX_POINT('',#178623);
#5872=VERTEX_POINT('',#178634);
#5873=VERTEX_POINT('',#178879);
#5874=VERTEX_POINT('',#178892);
#5875=VERTEX_POINT('',#179137);
#5876=VERTEX_POINT('',#179148);
#5877=VERTEX_POINT('',#179160);
#5878=VERTEX_POINT('',#179405);
#5879=VERTEX_POINT('',#179416);
#5880=VERTEX_POINT('',#179661);
#5881=VERTEX_POINT('',#179674);
#5882=VERTEX_POINT('',#179922);
#5883=VERTEX_POINT('',#179933);
#5884=VERTEX_POINT('',#179945);
#5885=VERTEX_POINT('',#180190);
#5886=VERTEX_POINT('',#180201);
#5887=VERTEX_POINT('',#180449);
#5888=VERTEX_POINT('',#180462);
#5889=VERTEX_POINT('',#180473);
#5890=VERTEX_POINT('',#180484);
#5891=VERTEX_POINT('',#180496);
#5892=VERTEX_POINT('',#180744);
#5893=VERTEX_POINT('',#180755);
#5894=VERTEX_POINT('',#181003);
#5895=VERTEX_POINT('',#181016);
#5896=VERTEX_POINT('',#181027);
#5897=VERTEX_POINT('',#181275);
#5898=VERTEX_POINT('',#181287);
#5899=VERTEX_POINT('',#181298);
#5900=VERTEX_POINT('',#181309);
#5901=VERTEX_POINT('',#181320);
#5902=VERTEX_POINT('',#181568);
#5903=VERTEX_POINT('',#181579);
#5904=VERTEX_POINT('',#181827);
#5905=VERTEX_POINT('',#181839);
#5906=VERTEX_POINT('',#181850);
#5907=VERTEX_POINT('',#181861);
#5908=VERTEX_POINT('',#181872);
#5909=VERTEX_POINT('',#182120);
#5910=VERTEX_POINT('',#182131);
#5911=VERTEX_POINT('',#182142);
#5912=VERTEX_POINT('',#182387);
#5913=VERTEX_POINT('',#182398);
#5914=VERTEX_POINT('',#182646);
#5915=VERTEX_POINT('',#182657);
#5916=VERTEX_POINT('',#182670);
#5917=VERTEX_POINT('',#182681);
#5918=VERTEX_POINT('',#182692);
#5919=VERTEX_POINT('',#182937);
#5920=VERTEX_POINT('',#182948);
#5921=VERTEX_POINT('',#183196);
#5922=VERTEX_POINT('',#183207);
#5923=VERTEX_POINT('',#183220);
#5924=VERTEX_POINT('',#183231);
#5925=VERTEX_POINT('',#183242);
#5926=VERTEX_POINT('',#183487);
#5927=VERTEX_POINT('',#183498);
#5928=VERTEX_POINT('',#183746);
#5929=VERTEX_POINT('',#183757);
#5930=VERTEX_POINT('',#183770);
#5931=VERTEX_POINT('',#184018);
#5932=VERTEX_POINT('',#184263);
#5933=VERTEX_POINT('',#184275);
#5934=VERTEX_POINT('',#184286);
#5935=VERTEX_POINT('',#184297);
#5936=VERTEX_POINT('',#184542);
#5937=VERTEX_POINT('',#184555);
#5938=VERTEX_POINT('',#184800);
#5939=VERTEX_POINT('',#185045);
#5940=VERTEX_POINT('',#185057);
#5941=VERTEX_POINT('',#185068);
#5942=VERTEX_POINT('',#185079);
#5943=VERTEX_POINT('',#185324);
#5944=VERTEX_POINT('',#185337);
#5945=VERTEX_POINT('',#185348);
#5946=VERTEX_POINT('',#185359);
#5947=VERTEX_POINT('',#185371);
#5948=VERTEX_POINT('',#185616);
#5949=VERTEX_POINT('',#185627);
#5950=VERTEX_POINT('',#185638);
#5951=VERTEX_POINT('',#185650);
#5952=VERTEX_POINT('',#185895);
#5953=VERTEX_POINT('',#186140);
#5954=VERTEX_POINT('',#186152);
#5955=VERTEX_POINT('',#186397);
#5956=VERTEX_POINT('',#186408);
#5957=VERTEX_POINT('',#186419);
#5958=VERTEX_POINT('',#186431);
#5959=VERTEX_POINT('',#186676);
#5960=VERTEX_POINT('',#186921);
#5961=VERTEX_POINT('',#186933);
#5962=VERTEX_POINT('',#187178);
#5963=VERTEX_POINT('',#187426);
#5964=VERTEX_POINT('',#187437);
#5965=VERTEX_POINT('',#187682);
#5966=VERTEX_POINT('',#187693);
#5967=VERTEX_POINT('',#187704);
#5968=VERTEX_POINT('',#187716);
#5969=VERTEX_POINT('',#187727);
#5970=VERTEX_POINT('',#187986);
#5971=VERTEX_POINT('',#187997);
#5972=VERTEX_POINT('',#188212);
#5973=VERTEX_POINT('',#188214);
#5974=VERTEX_POINT('',#188389);
#5975=VERTEX_POINT('',#188391);
#5976=VERTEX_POINT('',#188394);
#5977=VERTEX_POINT('',#188614);
#5978=VERTEX_POINT('',#188615);
#5979=VERTEX_POINT('',#188617);
#5980=VERTEX_POINT('',#188619);
#5981=VERTEX_POINT('',#188625);
#5982=VERTEX_POINT('',#188626);
#5983=VERTEX_POINT('',#188628);
#5984=VERTEX_POINT('',#188630);
#5985=VERTEX_POINT('',#188634);
#6495=EDGE_CURVE('',#4356,#4357,#3156,.T.);
#6496=EDGE_CURVE('',#4358,#4356,#57,.T.);
#6497=EDGE_CURVE('',#4359,#4358,#4176,.T.);
#6498=EDGE_CURVE('',#4359,#4357,#58,.T.);
#6499=EDGE_CURVE('',#4360,#4361,#3157,.T.);
#6500=EDGE_CURVE('',#4362,#4360,#59,.T.);
#6501=EDGE_CURVE('',#4356,#4362,#60,.T.);
#6502=EDGE_CURVE('',#4357,#4363,#61,.T.);
#6503=EDGE_CURVE('',#4363,#4361,#62,.T.);
#6504=EDGE_CURVE('',#4364,#4365,#3158,.T.);
#6505=EDGE_CURVE('',#4366,#4364,#63,.T.);
#6506=EDGE_CURVE('',#4360,#4366,#64,.T.);
#6507=EDGE_CURVE('',#4361,#4367,#65,.T.);
#6508=EDGE_CURVE('',#4367,#4365,#66,.T.);
#6509=EDGE_CURVE('',#4368,#4369,#3159,.T.);
#6510=EDGE_CURVE('',#4370,#4368,#67,.T.);
#6511=EDGE_CURVE('',#4364,#4370,#68,.T.);
#6512=EDGE_CURVE('',#4365,#4371,#69,.T.);
#6513=EDGE_CURVE('',#4371,#4369,#70,.T.);
#6514=EDGE_CURVE('',#4372,#4373,#3160,.T.);
#6515=EDGE_CURVE('',#4374,#4372,#71,.T.);
#6516=EDGE_CURVE('',#4368,#4374,#72,.T.);
#6517=EDGE_CURVE('',#4369,#4375,#73,.T.);
#6518=EDGE_CURVE('',#4375,#4373,#74,.T.);
#6519=EDGE_CURVE('',#4376,#4377,#3161,.T.);
#6520=EDGE_CURVE('',#4378,#4376,#75,.T.);
#6521=EDGE_CURVE('',#4372,#4378,#76,.T.);
#6522=EDGE_CURVE('',#4373,#4379,#77,.T.);
#6523=EDGE_CURVE('',#4379,#4377,#78,.T.);
#6524=EDGE_CURVE('',#4380,#4381,#3162,.T.);
#6525=EDGE_CURVE('',#4382,#4380,#79,.T.);
#6526=EDGE_CURVE('',#4376,#4382,#80,.T.);
#6527=EDGE_CURVE('',#4377,#4383,#81,.T.);
#6528=EDGE_CURVE('',#4383,#4381,#82,.T.);
#6529=EDGE_CURVE('',#4384,#4385,#3163,.T.);
#6530=EDGE_CURVE('',#4386,#4384,#83,.T.);
#6531=EDGE_CURVE('',#4380,#4386,#84,.T.);
#6532=EDGE_CURVE('',#4381,#4387,#85,.T.);
#6533=EDGE_CURVE('',#4387,#4385,#86,.T.);
#6534=EDGE_CURVE('',#4388,#4389,#3164,.T.);
#6535=EDGE_CURVE('',#4390,#4388,#87,.T.);
#6536=EDGE_CURVE('',#4384,#4390,#88,.T.);
#6537=EDGE_CURVE('',#4385,#4391,#89,.T.);
#6538=EDGE_CURVE('',#4391,#4389,#90,.T.);
#6539=EDGE_CURVE('',#4392,#4393,#3165,.T.);
#6540=EDGE_CURVE('',#4394,#4392,#91,.T.);
#6541=EDGE_CURVE('',#4388,#4394,#92,.T.);
#6542=EDGE_CURVE('',#4389,#4395,#93,.T.);
#6543=EDGE_CURVE('',#4395,#4393,#94,.T.);
#6544=EDGE_CURVE('',#4396,#4397,#3166,.T.);
#6545=EDGE_CURVE('',#4398,#4396,#95,.T.);
#6546=EDGE_CURVE('',#4392,#4398,#96,.T.);
#6547=EDGE_CURVE('',#4393,#4399,#97,.T.);
#6548=EDGE_CURVE('',#4399,#4397,#98,.T.);
#6549=EDGE_CURVE('',#4400,#4401,#3167,.T.);
#6550=EDGE_CURVE('',#4402,#4400,#99,.T.);
#6551=EDGE_CURVE('',#4396,#4402,#100,.T.);
#6552=EDGE_CURVE('',#4397,#4403,#101,.T.);
#6553=EDGE_CURVE('',#4403,#4401,#102,.T.);
#6554=EDGE_CURVE('',#4404,#4405,#3168,.T.);
#6555=EDGE_CURVE('',#4406,#4404,#103,.T.);
#6556=EDGE_CURVE('',#4400,#4406,#104,.T.);
#6557=EDGE_CURVE('',#4401,#4407,#105,.T.);
#6558=EDGE_CURVE('',#4407,#4405,#106,.T.);
#6559=EDGE_CURVE('',#4408,#4409,#3169,.T.);
#6560=EDGE_CURVE('',#4410,#4408,#107,.T.);
#6561=EDGE_CURVE('',#4404,#4410,#108,.T.);
#6562=EDGE_CURVE('',#4405,#4411,#109,.T.);
#6563=EDGE_CURVE('',#4411,#4409,#110,.T.);
#6564=EDGE_CURVE('',#4412,#4413,#3170,.T.);
#6565=EDGE_CURVE('',#4414,#4412,#111,.T.);
#6566=EDGE_CURVE('',#4408,#4414,#112,.T.);
#6567=EDGE_CURVE('',#4409,#4415,#113,.T.);
#6568=EDGE_CURVE('',#4415,#4413,#114,.T.);
#6569=EDGE_CURVE('',#4416,#4417,#3171,.T.);
#6570=EDGE_CURVE('',#4418,#4416,#115,.T.);
#6571=EDGE_CURVE('',#4412,#4418,#116,.T.);
#6572=EDGE_CURVE('',#4413,#4419,#117,.T.);
#6573=EDGE_CURVE('',#4419,#4417,#118,.T.);
#6574=EDGE_CURVE('',#4420,#4421,#3172,.T.);
#6575=EDGE_CURVE('',#4422,#4420,#119,.T.);
#6576=EDGE_CURVE('',#4416,#4422,#120,.T.);
#6577=EDGE_CURVE('',#4417,#4423,#121,.T.);
#6578=EDGE_CURVE('',#4423,#4421,#122,.T.);
#6579=EDGE_CURVE('',#4424,#4425,#3173,.T.);
#6580=EDGE_CURVE('',#4426,#4424,#123,.T.);
#6581=EDGE_CURVE('',#4420,#4426,#124,.T.);
#6582=EDGE_CURVE('',#4421,#4427,#125,.T.);
#6583=EDGE_CURVE('',#4427,#4425,#126,.T.);
#6584=EDGE_CURVE('',#4428,#4429,#3174,.T.);
#6585=EDGE_CURVE('',#4430,#4428,#127,.T.);
#6586=EDGE_CURVE('',#4424,#4430,#128,.T.);
#6587=EDGE_CURVE('',#4425,#4431,#129,.T.);
#6588=EDGE_CURVE('',#4431,#4429,#130,.T.);
#6589=EDGE_CURVE('',#4432,#4433,#3175,.T.);
#6590=EDGE_CURVE('',#4434,#4432,#131,.T.);
#6591=EDGE_CURVE('',#4428,#4434,#132,.T.);
#6592=EDGE_CURVE('',#4429,#4435,#133,.T.);
#6593=EDGE_CURVE('',#4435,#4433,#134,.T.);
#6594=EDGE_CURVE('',#4436,#4437,#3176,.T.);
#6595=EDGE_CURVE('',#4438,#4436,#135,.T.);
#6596=EDGE_CURVE('',#4432,#4438,#136,.T.);
#6597=EDGE_CURVE('',#4433,#4439,#137,.T.);
#6598=EDGE_CURVE('',#4439,#4437,#138,.T.);
#6599=EDGE_CURVE('',#4440,#4441,#3177,.T.);
#6600=EDGE_CURVE('',#4442,#4440,#139,.T.);
#6601=EDGE_CURVE('',#4436,#4442,#140,.T.);
#6602=EDGE_CURVE('',#4437,#4443,#141,.T.);
#6603=EDGE_CURVE('',#4443,#4441,#142,.T.);
#6604=EDGE_CURVE('',#4444,#4445,#3178,.T.);
#6605=EDGE_CURVE('',#4446,#4444,#143,.T.);
#6606=EDGE_CURVE('',#4440,#4446,#144,.T.);
#6607=EDGE_CURVE('',#4441,#4447,#145,.T.);
#6608=EDGE_CURVE('',#4447,#4445,#146,.T.);
#6609=EDGE_CURVE('',#4448,#4449,#3179,.T.);
#6610=EDGE_CURVE('',#4450,#4448,#147,.T.);
#6611=EDGE_CURVE('',#4444,#4450,#148,.T.);
#6612=EDGE_CURVE('',#4445,#4451,#149,.T.);
#6613=EDGE_CURVE('',#4451,#4449,#150,.T.);
#6614=EDGE_CURVE('',#4452,#4453,#3180,.T.);
#6615=EDGE_CURVE('',#4454,#4452,#151,.T.);
#6616=EDGE_CURVE('',#4448,#4454,#152,.T.);
#6617=EDGE_CURVE('',#4449,#4455,#153,.T.);
#6618=EDGE_CURVE('',#4455,#4453,#154,.T.);
#6619=EDGE_CURVE('',#4456,#4457,#3181,.T.);
#6620=EDGE_CURVE('',#4458,#4456,#155,.T.);
#6621=EDGE_CURVE('',#4452,#4458,#156,.T.);
#6622=EDGE_CURVE('',#4453,#4459,#157,.T.);
#6623=EDGE_CURVE('',#4459,#4457,#158,.T.);
#6624=EDGE_CURVE('',#4460,#4461,#3182,.T.);
#6625=EDGE_CURVE('',#4462,#4460,#159,.T.);
#6626=EDGE_CURVE('',#4456,#4462,#160,.T.);
#6627=EDGE_CURVE('',#4457,#4463,#161,.T.);
#6628=EDGE_CURVE('',#4463,#4461,#162,.T.);
#6629=EDGE_CURVE('',#4464,#4465,#3183,.T.);
#6630=EDGE_CURVE('',#4466,#4464,#163,.T.);
#6631=EDGE_CURVE('',#4460,#4466,#164,.T.);
#6632=EDGE_CURVE('',#4461,#4467,#165,.T.);
#6633=EDGE_CURVE('',#4467,#4465,#166,.T.);
#6634=EDGE_CURVE('',#4468,#4469,#3184,.T.);
#6635=EDGE_CURVE('',#4470,#4468,#167,.T.);
#6636=EDGE_CURVE('',#4464,#4470,#168,.T.);
#6637=EDGE_CURVE('',#4465,#4471,#169,.T.);
#6638=EDGE_CURVE('',#4471,#4469,#170,.T.);
#6639=EDGE_CURVE('',#4472,#4473,#3185,.T.);
#6640=EDGE_CURVE('',#4474,#4472,#171,.T.);
#6641=EDGE_CURVE('',#4468,#4474,#172,.T.);
#6642=EDGE_CURVE('',#4469,#4475,#173,.T.);
#6643=EDGE_CURVE('',#4475,#4473,#174,.T.);
#6644=EDGE_CURVE('',#4476,#4477,#3186,.T.);
#6645=EDGE_CURVE('',#4478,#4476,#175,.T.);
#6646=EDGE_CURVE('',#4472,#4478,#176,.T.);
#6647=EDGE_CURVE('',#4473,#4479,#177,.T.);
#6648=EDGE_CURVE('',#4479,#4477,#178,.T.);
#6649=EDGE_CURVE('',#4480,#4481,#3187,.T.);
#6650=EDGE_CURVE('',#4482,#4480,#179,.T.);
#6651=EDGE_CURVE('',#4476,#4482,#180,.T.);
#6652=EDGE_CURVE('',#4477,#4483,#181,.T.);
#6653=EDGE_CURVE('',#4483,#4481,#182,.T.);
#6654=EDGE_CURVE('',#4484,#4485,#3188,.T.);
#6655=EDGE_CURVE('',#4486,#4484,#183,.T.);
#6656=EDGE_CURVE('',#4480,#4486,#184,.T.);
#6657=EDGE_CURVE('',#4481,#4487,#185,.T.);
#6658=EDGE_CURVE('',#4487,#4485,#186,.T.);
#6659=EDGE_CURVE('',#4488,#4489,#3189,.T.);
#6660=EDGE_CURVE('',#4490,#4488,#187,.T.);
#6661=EDGE_CURVE('',#4484,#4490,#188,.T.);
#6662=EDGE_CURVE('',#4485,#4491,#189,.T.);
#6663=EDGE_CURVE('',#4491,#4489,#190,.T.);
#6664=EDGE_CURVE('',#4492,#4493,#3190,.T.);
#6665=EDGE_CURVE('',#4494,#4492,#191,.T.);
#6666=EDGE_CURVE('',#4488,#4494,#192,.T.);
#6667=EDGE_CURVE('',#4489,#4495,#193,.T.);
#6668=EDGE_CURVE('',#4495,#4493,#194,.T.);
#6669=EDGE_CURVE('',#4496,#4497,#3191,.T.);
#6670=EDGE_CURVE('',#4498,#4496,#195,.T.);
#6671=EDGE_CURVE('',#4492,#4498,#196,.T.);
#6672=EDGE_CURVE('',#4493,#4499,#197,.T.);
#6673=EDGE_CURVE('',#4499,#4497,#198,.T.);
#6674=EDGE_CURVE('',#4500,#4501,#3192,.T.);
#6675=EDGE_CURVE('',#4502,#4500,#199,.T.);
#6676=EDGE_CURVE('',#4496,#4502,#200,.T.);
#6677=EDGE_CURVE('',#4497,#4503,#201,.T.);
#6678=EDGE_CURVE('',#4503,#4501,#202,.T.);
#6679=EDGE_CURVE('',#4504,#4505,#3193,.T.);
#6680=EDGE_CURVE('',#4506,#4504,#203,.T.);
#6681=EDGE_CURVE('',#4500,#4506,#204,.T.);
#6682=EDGE_CURVE('',#4501,#4507,#205,.T.);
#6683=EDGE_CURVE('',#4507,#4505,#206,.T.);
#6684=EDGE_CURVE('',#4508,#4509,#3194,.T.);
#6685=EDGE_CURVE('',#4510,#4508,#207,.T.);
#6686=EDGE_CURVE('',#4504,#4510,#208,.T.);
#6687=EDGE_CURVE('',#4505,#4511,#209,.T.);
#6688=EDGE_CURVE('',#4511,#4509,#210,.T.);
#6689=EDGE_CURVE('',#4512,#4513,#3195,.T.);
#6690=EDGE_CURVE('',#4514,#4512,#211,.T.);
#6691=EDGE_CURVE('',#4508,#4514,#212,.T.);
#6692=EDGE_CURVE('',#4509,#4515,#213,.T.);
#6693=EDGE_CURVE('',#4515,#4513,#214,.T.);
#6694=EDGE_CURVE('',#4516,#4517,#3196,.T.);
#6695=EDGE_CURVE('',#4518,#4516,#215,.T.);
#6696=EDGE_CURVE('',#4512,#4518,#216,.T.);
#6697=EDGE_CURVE('',#4513,#4519,#217,.T.);
#6698=EDGE_CURVE('',#4519,#4517,#218,.T.);
#6699=EDGE_CURVE('',#4520,#4521,#3197,.T.);
#6700=EDGE_CURVE('',#4522,#4520,#219,.T.);
#6701=EDGE_CURVE('',#4516,#4522,#220,.T.);
#6702=EDGE_CURVE('',#4517,#4523,#221,.T.);
#6703=EDGE_CURVE('',#4523,#4521,#222,.T.);
#6704=EDGE_CURVE('',#4524,#4525,#3198,.T.);
#6705=EDGE_CURVE('',#4526,#4524,#223,.T.);
#6706=EDGE_CURVE('',#4520,#4526,#224,.T.);
#6707=EDGE_CURVE('',#4521,#4527,#225,.T.);
#6708=EDGE_CURVE('',#4527,#4525,#226,.T.);
#6709=EDGE_CURVE('',#4528,#4529,#3199,.T.);
#6710=EDGE_CURVE('',#4530,#4528,#227,.T.);
#6711=EDGE_CURVE('',#4524,#4530,#228,.T.);
#6712=EDGE_CURVE('',#4525,#4531,#229,.T.);
#6713=EDGE_CURVE('',#4531,#4529,#230,.T.);
#6714=EDGE_CURVE('',#4532,#4533,#3200,.T.);
#6715=EDGE_CURVE('',#4534,#4532,#231,.T.);
#6716=EDGE_CURVE('',#4528,#4534,#232,.T.);
#6717=EDGE_CURVE('',#4529,#4535,#233,.T.);
#6718=EDGE_CURVE('',#4535,#4533,#234,.T.);
#6719=EDGE_CURVE('',#4536,#4537,#3201,.T.);
#6720=EDGE_CURVE('',#4538,#4536,#235,.T.);
#6721=EDGE_CURVE('',#4532,#4538,#236,.T.);
#6722=EDGE_CURVE('',#4533,#4539,#237,.T.);
#6723=EDGE_CURVE('',#4539,#4537,#238,.T.);
#6724=EDGE_CURVE('',#4540,#4541,#3202,.T.);
#6725=EDGE_CURVE('',#4542,#4540,#239,.T.);
#6726=EDGE_CURVE('',#4536,#4542,#240,.T.);
#6727=EDGE_CURVE('',#4537,#4543,#241,.T.);
#6728=EDGE_CURVE('',#4543,#4541,#242,.T.);
#6729=EDGE_CURVE('',#4544,#4545,#3203,.T.);
#6730=EDGE_CURVE('',#4546,#4544,#243,.T.);
#6731=EDGE_CURVE('',#4540,#4546,#244,.T.);
#6732=EDGE_CURVE('',#4541,#4547,#245,.T.);
#6733=EDGE_CURVE('',#4547,#4545,#246,.T.);
#6734=EDGE_CURVE('',#4548,#4549,#3204,.T.);
#6735=EDGE_CURVE('',#4550,#4548,#247,.T.);
#6736=EDGE_CURVE('',#4544,#4550,#248,.T.);
#6737=EDGE_CURVE('',#4545,#4551,#249,.T.);
#6738=EDGE_CURVE('',#4551,#4549,#250,.T.);
#6739=EDGE_CURVE('',#4552,#4553,#3205,.T.);
#6740=EDGE_CURVE('',#4554,#4552,#251,.T.);
#6741=EDGE_CURVE('',#4548,#4554,#252,.T.);
#6742=EDGE_CURVE('',#4549,#4555,#253,.T.);
#6743=EDGE_CURVE('',#4555,#4553,#254,.T.);
#6744=EDGE_CURVE('',#4556,#4557,#3206,.T.);
#6745=EDGE_CURVE('',#4558,#4556,#255,.T.);
#6746=EDGE_CURVE('',#4552,#4558,#256,.T.);
#6747=EDGE_CURVE('',#4553,#4559,#257,.T.);
#6748=EDGE_CURVE('',#4559,#4557,#258,.T.);
#6749=EDGE_CURVE('',#4560,#4561,#3207,.T.);
#6750=EDGE_CURVE('',#4562,#4560,#259,.T.);
#6751=EDGE_CURVE('',#4556,#4562,#260,.T.);
#6752=EDGE_CURVE('',#4557,#4563,#261,.T.);
#6753=EDGE_CURVE('',#4563,#4561,#262,.T.);
#6754=EDGE_CURVE('',#4564,#4565,#3208,.T.);
#6755=EDGE_CURVE('',#4566,#4564,#263,.T.);
#6756=EDGE_CURVE('',#4560,#4566,#264,.T.);
#6757=EDGE_CURVE('',#4561,#4567,#265,.T.);
#6758=EDGE_CURVE('',#4567,#4565,#266,.T.);
#6759=EDGE_CURVE('',#4568,#4569,#3209,.T.);
#6760=EDGE_CURVE('',#4570,#4568,#267,.T.);
#6761=EDGE_CURVE('',#4564,#4570,#268,.T.);
#6762=EDGE_CURVE('',#4565,#4571,#269,.T.);
#6763=EDGE_CURVE('',#4571,#4569,#270,.T.);
#6764=EDGE_CURVE('',#4572,#4573,#3210,.T.);
#6765=EDGE_CURVE('',#4574,#4572,#271,.T.);
#6766=EDGE_CURVE('',#4568,#4574,#272,.T.);
#6767=EDGE_CURVE('',#4569,#4575,#273,.T.);
#6768=EDGE_CURVE('',#4575,#4573,#274,.T.);
#6769=EDGE_CURVE('',#4576,#4577,#3211,.T.);
#6770=EDGE_CURVE('',#4578,#4576,#275,.T.);
#6771=EDGE_CURVE('',#4572,#4578,#276,.T.);
#6772=EDGE_CURVE('',#4573,#4579,#277,.T.);
#6773=EDGE_CURVE('',#4579,#4577,#278,.T.);
#6774=EDGE_CURVE('',#4580,#4581,#3212,.T.);
#6775=EDGE_CURVE('',#4582,#4580,#279,.T.);
#6776=EDGE_CURVE('',#4576,#4582,#280,.T.);
#6777=EDGE_CURVE('',#4577,#4583,#281,.T.);
#6778=EDGE_CURVE('',#4583,#4581,#282,.T.);
#6779=EDGE_CURVE('',#4584,#4585,#3213,.T.);
#6780=EDGE_CURVE('',#4586,#4584,#283,.T.);
#6781=EDGE_CURVE('',#4580,#4586,#284,.T.);
#6782=EDGE_CURVE('',#4581,#4587,#285,.T.);
#6783=EDGE_CURVE('',#4587,#4585,#286,.T.);
#6784=EDGE_CURVE('',#4588,#4589,#3214,.T.);
#6785=EDGE_CURVE('',#4590,#4588,#287,.T.);
#6786=EDGE_CURVE('',#4584,#4590,#288,.T.);
#6787=EDGE_CURVE('',#4585,#4591,#289,.T.);
#6788=EDGE_CURVE('',#4591,#4589,#290,.T.);
#6789=EDGE_CURVE('',#4592,#4593,#3215,.T.);
#6790=EDGE_CURVE('',#4594,#4592,#291,.T.);
#6791=EDGE_CURVE('',#4588,#4594,#292,.T.);
#6792=EDGE_CURVE('',#4589,#4595,#293,.T.);
#6793=EDGE_CURVE('',#4595,#4593,#294,.T.);
#6794=EDGE_CURVE('',#4596,#4597,#3216,.T.);
#6795=EDGE_CURVE('',#4598,#4596,#295,.T.);
#6796=EDGE_CURVE('',#4592,#4598,#296,.T.);
#6797=EDGE_CURVE('',#4593,#4599,#297,.T.);
#6798=EDGE_CURVE('',#4599,#4597,#298,.T.);
#6799=EDGE_CURVE('',#4600,#4601,#3217,.T.);
#6800=EDGE_CURVE('',#4602,#4600,#299,.T.);
#6801=EDGE_CURVE('',#4596,#4602,#300,.T.);
#6802=EDGE_CURVE('',#4597,#4603,#301,.T.);
#6803=EDGE_CURVE('',#4603,#4601,#302,.T.);
#6804=EDGE_CURVE('',#4604,#4605,#3218,.T.);
#6805=EDGE_CURVE('',#4606,#4604,#303,.T.);
#6806=EDGE_CURVE('',#4600,#4606,#304,.T.);
#6807=EDGE_CURVE('',#4601,#4607,#305,.T.);
#6808=EDGE_CURVE('',#4607,#4605,#306,.T.);
#6809=EDGE_CURVE('',#4608,#4609,#3219,.T.);
#6810=EDGE_CURVE('',#4610,#4608,#307,.T.);
#6811=EDGE_CURVE('',#4604,#4610,#308,.T.);
#6812=EDGE_CURVE('',#4605,#4611,#309,.T.);
#6813=EDGE_CURVE('',#4611,#4609,#310,.T.);
#6814=EDGE_CURVE('',#4612,#4613,#3220,.T.);
#6815=EDGE_CURVE('',#4614,#4612,#311,.T.);
#6816=EDGE_CURVE('',#4608,#4614,#312,.T.);
#6817=EDGE_CURVE('',#4609,#4615,#313,.T.);
#6818=EDGE_CURVE('',#4615,#4613,#314,.T.);
#6819=EDGE_CURVE('',#4616,#4617,#3221,.T.);
#6820=EDGE_CURVE('',#4618,#4616,#315,.T.);
#6821=EDGE_CURVE('',#4612,#4618,#316,.T.);
#6822=EDGE_CURVE('',#4613,#4619,#317,.T.);
#6823=EDGE_CURVE('',#4619,#4617,#318,.T.);
#6824=EDGE_CURVE('',#4620,#4621,#3222,.T.);
#6825=EDGE_CURVE('',#4622,#4620,#319,.T.);
#6826=EDGE_CURVE('',#4616,#4622,#320,.T.);
#6827=EDGE_CURVE('',#4617,#4623,#321,.T.);
#6828=EDGE_CURVE('',#4623,#4621,#322,.T.);
#6829=EDGE_CURVE('',#4624,#4625,#3223,.T.);
#6830=EDGE_CURVE('',#4626,#4624,#323,.T.);
#6831=EDGE_CURVE('',#4620,#4626,#324,.T.);
#6832=EDGE_CURVE('',#4621,#4627,#325,.T.);
#6833=EDGE_CURVE('',#4627,#4625,#326,.T.);
#6834=EDGE_CURVE('',#4628,#4629,#3224,.T.);
#6835=EDGE_CURVE('',#4630,#4628,#327,.T.);
#6836=EDGE_CURVE('',#4624,#4630,#328,.T.);
#6837=EDGE_CURVE('',#4625,#4631,#329,.T.);
#6838=EDGE_CURVE('',#4631,#4629,#330,.T.);
#6839=EDGE_CURVE('',#4632,#4633,#3225,.T.);
#6840=EDGE_CURVE('',#4634,#4632,#331,.T.);
#6841=EDGE_CURVE('',#4628,#4634,#332,.T.);
#6842=EDGE_CURVE('',#4629,#4635,#333,.T.);
#6843=EDGE_CURVE('',#4635,#4633,#334,.T.);
#6844=EDGE_CURVE('',#4636,#4637,#3226,.T.);
#6845=EDGE_CURVE('',#4638,#4636,#335,.T.);
#6846=EDGE_CURVE('',#4632,#4638,#336,.T.);
#6847=EDGE_CURVE('',#4633,#4639,#337,.T.);
#6848=EDGE_CURVE('',#4639,#4637,#338,.T.);
#6849=EDGE_CURVE('',#4640,#4641,#3227,.T.);
#6850=EDGE_CURVE('',#4642,#4640,#339,.T.);
#6851=EDGE_CURVE('',#4636,#4642,#340,.T.);
#6852=EDGE_CURVE('',#4637,#4643,#341,.T.);
#6853=EDGE_CURVE('',#4643,#4641,#342,.T.);
#6854=EDGE_CURVE('',#4644,#4645,#3228,.T.);
#6855=EDGE_CURVE('',#4646,#4644,#343,.T.);
#6856=EDGE_CURVE('',#4640,#4646,#344,.T.);
#6857=EDGE_CURVE('',#4641,#4647,#345,.T.);
#6858=EDGE_CURVE('',#4647,#4645,#346,.T.);
#6859=EDGE_CURVE('',#4648,#4649,#3229,.T.);
#6860=EDGE_CURVE('',#4650,#4648,#347,.T.);
#6861=EDGE_CURVE('',#4644,#4650,#348,.T.);
#6862=EDGE_CURVE('',#4645,#4651,#349,.T.);
#6863=EDGE_CURVE('',#4651,#4649,#350,.T.);
#6864=EDGE_CURVE('',#4652,#4653,#3230,.T.);
#6865=EDGE_CURVE('',#4654,#4652,#351,.T.);
#6866=EDGE_CURVE('',#4648,#4654,#352,.T.);
#6867=EDGE_CURVE('',#4649,#4655,#353,.T.);
#6868=EDGE_CURVE('',#4655,#4653,#354,.T.);
#6869=EDGE_CURVE('',#4656,#4657,#3231,.T.);
#6870=EDGE_CURVE('',#4658,#4656,#355,.T.);
#6871=EDGE_CURVE('',#4652,#4658,#356,.T.);
#6872=EDGE_CURVE('',#4653,#4659,#357,.T.);
#6873=EDGE_CURVE('',#4659,#4657,#358,.T.);
#6874=EDGE_CURVE('',#4660,#4661,#3232,.T.);
#6875=EDGE_CURVE('',#4662,#4660,#359,.T.);
#6876=EDGE_CURVE('',#4656,#4662,#360,.T.);
#6877=EDGE_CURVE('',#4657,#4663,#361,.T.);
#6878=EDGE_CURVE('',#4663,#4661,#362,.T.);
#6879=EDGE_CURVE('',#4664,#4665,#3233,.T.);
#6880=EDGE_CURVE('',#4666,#4664,#363,.T.);
#6881=EDGE_CURVE('',#4660,#4666,#364,.T.);
#6882=EDGE_CURVE('',#4661,#4667,#365,.T.);
#6883=EDGE_CURVE('',#4667,#4665,#366,.T.);
#6884=EDGE_CURVE('',#4668,#4669,#3234,.T.);
#6885=EDGE_CURVE('',#4670,#4668,#367,.T.);
#6886=EDGE_CURVE('',#4664,#4670,#368,.T.);
#6887=EDGE_CURVE('',#4665,#4671,#369,.T.);
#6888=EDGE_CURVE('',#4671,#4669,#370,.T.);
#6889=EDGE_CURVE('',#4672,#4673,#3235,.T.);
#6890=EDGE_CURVE('',#4674,#4672,#371,.T.);
#6891=EDGE_CURVE('',#4668,#4674,#372,.T.);
#6892=EDGE_CURVE('',#4669,#4675,#373,.T.);
#6893=EDGE_CURVE('',#4675,#4673,#374,.T.);
#6894=EDGE_CURVE('',#4676,#4677,#3236,.T.);
#6895=EDGE_CURVE('',#4678,#4676,#375,.T.);
#6896=EDGE_CURVE('',#4672,#4678,#376,.T.);
#6897=EDGE_CURVE('',#4673,#4679,#377,.T.);
#6898=EDGE_CURVE('',#4679,#4677,#378,.T.);
#6899=EDGE_CURVE('',#4680,#4681,#3237,.T.);
#6900=EDGE_CURVE('',#4682,#4680,#379,.T.);
#6901=EDGE_CURVE('',#4676,#4682,#380,.T.);
#6902=EDGE_CURVE('',#4677,#4683,#381,.T.);
#6903=EDGE_CURVE('',#4683,#4681,#382,.T.);
#6904=EDGE_CURVE('',#4684,#4685,#3238,.T.);
#6905=EDGE_CURVE('',#4686,#4684,#383,.T.);
#6906=EDGE_CURVE('',#4680,#4686,#384,.T.);
#6907=EDGE_CURVE('',#4681,#4687,#385,.T.);
#6908=EDGE_CURVE('',#4687,#4685,#386,.T.);
#6909=EDGE_CURVE('',#4688,#4689,#3239,.T.);
#6910=EDGE_CURVE('',#4690,#4688,#387,.T.);
#6911=EDGE_CURVE('',#4684,#4690,#388,.T.);
#6912=EDGE_CURVE('',#4685,#4691,#389,.T.);
#6913=EDGE_CURVE('',#4691,#4689,#390,.T.);
#6914=EDGE_CURVE('',#4692,#4693,#3240,.T.);
#6915=EDGE_CURVE('',#4694,#4692,#391,.T.);
#6916=EDGE_CURVE('',#4688,#4694,#392,.T.);
#6917=EDGE_CURVE('',#4689,#4695,#393,.T.);
#6918=EDGE_CURVE('',#4695,#4693,#394,.T.);
#6919=EDGE_CURVE('',#4696,#4697,#3241,.T.);
#6920=EDGE_CURVE('',#4698,#4696,#395,.T.);
#6921=EDGE_CURVE('',#4692,#4698,#396,.T.);
#6922=EDGE_CURVE('',#4693,#4699,#397,.T.);
#6923=EDGE_CURVE('',#4699,#4697,#398,.T.);
#6924=EDGE_CURVE('',#4700,#4701,#3242,.T.);
#6925=EDGE_CURVE('',#4702,#4700,#399,.T.);
#6926=EDGE_CURVE('',#4696,#4702,#400,.T.);
#6927=EDGE_CURVE('',#4697,#4703,#401,.T.);
#6928=EDGE_CURVE('',#4703,#4701,#402,.T.);
#6929=EDGE_CURVE('',#4704,#4705,#3243,.T.);
#6930=EDGE_CURVE('',#4706,#4704,#403,.T.);
#6931=EDGE_CURVE('',#4700,#4706,#404,.T.);
#6932=EDGE_CURVE('',#4701,#4707,#405,.T.);
#6933=EDGE_CURVE('',#4707,#4705,#406,.T.);
#6934=EDGE_CURVE('',#4708,#4709,#3244,.T.);
#6935=EDGE_CURVE('',#4710,#4708,#407,.T.);
#6936=EDGE_CURVE('',#4704,#4710,#408,.T.);
#6937=EDGE_CURVE('',#4705,#4711,#409,.T.);
#6938=EDGE_CURVE('',#4711,#4709,#410,.T.);
#6939=EDGE_CURVE('',#4712,#4713,#3245,.T.);
#6940=EDGE_CURVE('',#4714,#4712,#411,.T.);
#6941=EDGE_CURVE('',#4708,#4714,#412,.T.);
#6942=EDGE_CURVE('',#4709,#4715,#413,.T.);
#6943=EDGE_CURVE('',#4715,#4713,#414,.T.);
#6944=EDGE_CURVE('',#4716,#4717,#3246,.T.);
#6945=EDGE_CURVE('',#4718,#4716,#415,.T.);
#6946=EDGE_CURVE('',#4712,#4718,#416,.T.);
#6947=EDGE_CURVE('',#4713,#4719,#417,.T.);
#6948=EDGE_CURVE('',#4719,#4717,#418,.T.);
#6949=EDGE_CURVE('',#4720,#4721,#3247,.T.);
#6950=EDGE_CURVE('',#4722,#4720,#419,.T.);
#6951=EDGE_CURVE('',#4716,#4722,#420,.T.);
#6952=EDGE_CURVE('',#4717,#4723,#421,.T.);
#6953=EDGE_CURVE('',#4723,#4721,#422,.T.);
#6954=EDGE_CURVE('',#4724,#4725,#3248,.T.);
#6955=EDGE_CURVE('',#4726,#4724,#423,.T.);
#6956=EDGE_CURVE('',#4720,#4726,#424,.T.);
#6957=EDGE_CURVE('',#4721,#4727,#425,.T.);
#6958=EDGE_CURVE('',#4727,#4725,#426,.T.);
#6959=EDGE_CURVE('',#4728,#4729,#3249,.T.);
#6960=EDGE_CURVE('',#4730,#4728,#427,.T.);
#6961=EDGE_CURVE('',#4724,#4730,#428,.T.);
#6962=EDGE_CURVE('',#4725,#4731,#429,.T.);
#6963=EDGE_CURVE('',#4731,#4729,#430,.T.);
#6964=EDGE_CURVE('',#4732,#4733,#3250,.T.);
#6965=EDGE_CURVE('',#4734,#4732,#431,.T.);
#6966=EDGE_CURVE('',#4728,#4734,#432,.T.);
#6967=EDGE_CURVE('',#4729,#4735,#433,.T.);
#6968=EDGE_CURVE('',#4735,#4733,#434,.T.);
#6969=EDGE_CURVE('',#4736,#4737,#3251,.T.);
#6970=EDGE_CURVE('',#4738,#4736,#435,.T.);
#6971=EDGE_CURVE('',#4732,#4738,#436,.T.);
#6972=EDGE_CURVE('',#4733,#4739,#437,.T.);
#6973=EDGE_CURVE('',#4739,#4737,#438,.T.);
#6974=EDGE_CURVE('',#4740,#4741,#3252,.T.);
#6975=EDGE_CURVE('',#4742,#4740,#439,.T.);
#6976=EDGE_CURVE('',#4736,#4742,#440,.T.);
#6977=EDGE_CURVE('',#4737,#4743,#441,.T.);
#6978=EDGE_CURVE('',#4743,#4741,#442,.T.);
#6979=EDGE_CURVE('',#4744,#4745,#3253,.T.);
#6980=EDGE_CURVE('',#4746,#4744,#443,.T.);
#6981=EDGE_CURVE('',#4740,#4746,#444,.T.);
#6982=EDGE_CURVE('',#4741,#4747,#445,.T.);
#6983=EDGE_CURVE('',#4747,#4745,#446,.T.);
#6984=EDGE_CURVE('',#4748,#4749,#3254,.T.);
#6985=EDGE_CURVE('',#4750,#4748,#447,.T.);
#6986=EDGE_CURVE('',#4744,#4750,#448,.T.);
#6987=EDGE_CURVE('',#4745,#4751,#449,.T.);
#6988=EDGE_CURVE('',#4751,#4749,#450,.T.);
#6989=EDGE_CURVE('',#4752,#4753,#3255,.T.);
#6990=EDGE_CURVE('',#4754,#4752,#451,.T.);
#6991=EDGE_CURVE('',#4748,#4754,#452,.T.);
#6992=EDGE_CURVE('',#4749,#4755,#453,.T.);
#6993=EDGE_CURVE('',#4755,#4753,#454,.T.);
#6994=EDGE_CURVE('',#4756,#4757,#3256,.T.);
#6995=EDGE_CURVE('',#4758,#4756,#455,.T.);
#6996=EDGE_CURVE('',#4752,#4758,#456,.T.);
#6997=EDGE_CURVE('',#4753,#4759,#457,.T.);
#6998=EDGE_CURVE('',#4759,#4757,#458,.T.);
#6999=EDGE_CURVE('',#4760,#4761,#3257,.T.);
#7000=EDGE_CURVE('',#4762,#4760,#459,.T.);
#7001=EDGE_CURVE('',#4756,#4762,#460,.T.);
#7002=EDGE_CURVE('',#4757,#4763,#461,.T.);
#7003=EDGE_CURVE('',#4763,#4761,#462,.T.);
#7004=EDGE_CURVE('',#4764,#4765,#3258,.T.);
#7005=EDGE_CURVE('',#4766,#4764,#463,.T.);
#7006=EDGE_CURVE('',#4760,#4766,#464,.T.);
#7007=EDGE_CURVE('',#4761,#4767,#465,.T.);
#7008=EDGE_CURVE('',#4767,#4765,#466,.T.);
#7009=EDGE_CURVE('',#4768,#4769,#3259,.T.);
#7010=EDGE_CURVE('',#4770,#4768,#467,.T.);
#7011=EDGE_CURVE('',#4764,#4770,#468,.T.);
#7012=EDGE_CURVE('',#4765,#4771,#469,.T.);
#7013=EDGE_CURVE('',#4771,#4769,#470,.T.);
#7014=EDGE_CURVE('',#4772,#4773,#3260,.T.);
#7015=EDGE_CURVE('',#4774,#4772,#471,.T.);
#7016=EDGE_CURVE('',#4768,#4774,#472,.T.);
#7017=EDGE_CURVE('',#4769,#4775,#473,.T.);
#7018=EDGE_CURVE('',#4775,#4773,#474,.T.);
#7019=EDGE_CURVE('',#4776,#4777,#3261,.T.);
#7020=EDGE_CURVE('',#4778,#4776,#475,.T.);
#7021=EDGE_CURVE('',#4772,#4778,#476,.T.);
#7022=EDGE_CURVE('',#4773,#4779,#477,.T.);
#7023=EDGE_CURVE('',#4779,#4777,#478,.T.);
#7024=EDGE_CURVE('',#4780,#4781,#3262,.T.);
#7025=EDGE_CURVE('',#4782,#4780,#479,.T.);
#7026=EDGE_CURVE('',#4776,#4782,#480,.T.);
#7027=EDGE_CURVE('',#4777,#4783,#481,.T.);
#7028=EDGE_CURVE('',#4783,#4781,#482,.T.);
#7029=EDGE_CURVE('',#4784,#4785,#3263,.T.);
#7030=EDGE_CURVE('',#4786,#4784,#483,.T.);
#7031=EDGE_CURVE('',#4780,#4786,#484,.T.);
#7032=EDGE_CURVE('',#4781,#4787,#485,.T.);
#7033=EDGE_CURVE('',#4787,#4785,#486,.T.);
#7034=EDGE_CURVE('',#4788,#4789,#3264,.T.);
#7035=EDGE_CURVE('',#4790,#4788,#487,.T.);
#7036=EDGE_CURVE('',#4784,#4790,#488,.T.);
#7037=EDGE_CURVE('',#4785,#4791,#489,.T.);
#7038=EDGE_CURVE('',#4791,#4789,#490,.T.);
#7039=EDGE_CURVE('',#4792,#4793,#3265,.T.);
#7040=EDGE_CURVE('',#4794,#4792,#491,.T.);
#7041=EDGE_CURVE('',#4788,#4794,#492,.T.);
#7042=EDGE_CURVE('',#4789,#4795,#493,.T.);
#7043=EDGE_CURVE('',#4795,#4793,#494,.T.);
#7044=EDGE_CURVE('',#4796,#4797,#3266,.T.);
#7045=EDGE_CURVE('',#4798,#4796,#495,.T.);
#7046=EDGE_CURVE('',#4792,#4798,#496,.T.);
#7047=EDGE_CURVE('',#4793,#4799,#497,.T.);
#7048=EDGE_CURVE('',#4799,#4797,#498,.T.);
#7049=EDGE_CURVE('',#4800,#4801,#3267,.T.);
#7050=EDGE_CURVE('',#4802,#4800,#499,.T.);
#7051=EDGE_CURVE('',#4796,#4802,#500,.T.);
#7052=EDGE_CURVE('',#4797,#4803,#501,.T.);
#7053=EDGE_CURVE('',#4803,#4801,#502,.T.);
#7054=EDGE_CURVE('',#4804,#4805,#3268,.T.);
#7055=EDGE_CURVE('',#4806,#4804,#503,.T.);
#7056=EDGE_CURVE('',#4800,#4806,#504,.T.);
#7057=EDGE_CURVE('',#4801,#4807,#505,.T.);
#7058=EDGE_CURVE('',#4807,#4805,#506,.T.);
#7059=EDGE_CURVE('',#4808,#4809,#3269,.T.);
#7060=EDGE_CURVE('',#4810,#4808,#507,.T.);
#7061=EDGE_CURVE('',#4804,#4810,#508,.T.);
#7062=EDGE_CURVE('',#4805,#4811,#509,.T.);
#7063=EDGE_CURVE('',#4811,#4809,#510,.T.);
#7064=EDGE_CURVE('',#4812,#4813,#3270,.T.);
#7065=EDGE_CURVE('',#4814,#4812,#511,.T.);
#7066=EDGE_CURVE('',#4808,#4814,#512,.T.);
#7067=EDGE_CURVE('',#4809,#4815,#513,.T.);
#7068=EDGE_CURVE('',#4815,#4813,#514,.T.);
#7069=EDGE_CURVE('',#4816,#4817,#3271,.T.);
#7070=EDGE_CURVE('',#4818,#4816,#515,.T.);
#7071=EDGE_CURVE('',#4812,#4818,#516,.T.);
#7072=EDGE_CURVE('',#4813,#4819,#517,.T.);
#7073=EDGE_CURVE('',#4819,#4817,#518,.T.);
#7074=EDGE_CURVE('',#4820,#4821,#3272,.T.);
#7075=EDGE_CURVE('',#4822,#4820,#519,.T.);
#7076=EDGE_CURVE('',#4816,#4822,#520,.T.);
#7077=EDGE_CURVE('',#4817,#4823,#521,.T.);
#7078=EDGE_CURVE('',#4823,#4821,#522,.T.);
#7079=EDGE_CURVE('',#4824,#4825,#3273,.T.);
#7080=EDGE_CURVE('',#4826,#4824,#523,.T.);
#7081=EDGE_CURVE('',#4820,#4826,#524,.T.);
#7082=EDGE_CURVE('',#4821,#4827,#525,.T.);
#7083=EDGE_CURVE('',#4827,#4825,#526,.T.);
#7084=EDGE_CURVE('',#4828,#4829,#3274,.T.);
#7085=EDGE_CURVE('',#4830,#4828,#527,.T.);
#7086=EDGE_CURVE('',#4824,#4830,#528,.T.);
#7087=EDGE_CURVE('',#4825,#4831,#529,.T.);
#7088=EDGE_CURVE('',#4831,#4829,#530,.T.);
#7089=EDGE_CURVE('',#4832,#4833,#3275,.T.);
#7090=EDGE_CURVE('',#4834,#4832,#531,.T.);
#7091=EDGE_CURVE('',#4828,#4834,#532,.T.);
#7092=EDGE_CURVE('',#4829,#4835,#533,.T.);
#7093=EDGE_CURVE('',#4835,#4833,#534,.T.);
#7094=EDGE_CURVE('',#4836,#4837,#3276,.T.);
#7095=EDGE_CURVE('',#4838,#4836,#535,.T.);
#7096=EDGE_CURVE('',#4832,#4838,#536,.T.);
#7097=EDGE_CURVE('',#4833,#4839,#537,.T.);
#7098=EDGE_CURVE('',#4839,#4837,#538,.T.);
#7099=EDGE_CURVE('',#4840,#4841,#3277,.T.);
#7100=EDGE_CURVE('',#4842,#4840,#539,.T.);
#7101=EDGE_CURVE('',#4836,#4842,#540,.T.);
#7102=EDGE_CURVE('',#4837,#4843,#541,.T.);
#7103=EDGE_CURVE('',#4843,#4841,#542,.T.);
#7104=EDGE_CURVE('',#4844,#4845,#3278,.T.);
#7105=EDGE_CURVE('',#4846,#4844,#543,.T.);
#7106=EDGE_CURVE('',#4840,#4846,#544,.T.);
#7107=EDGE_CURVE('',#4841,#4847,#545,.T.);
#7108=EDGE_CURVE('',#4847,#4845,#546,.T.);
#7109=EDGE_CURVE('',#4848,#4849,#3279,.T.);
#7110=EDGE_CURVE('',#4850,#4848,#547,.T.);
#7111=EDGE_CURVE('',#4844,#4850,#548,.T.);
#7112=EDGE_CURVE('',#4845,#4851,#549,.T.);
#7113=EDGE_CURVE('',#4851,#4849,#550,.T.);
#7114=EDGE_CURVE('',#4852,#4853,#3280,.T.);
#7115=EDGE_CURVE('',#4854,#4852,#551,.T.);
#7116=EDGE_CURVE('',#4848,#4854,#552,.T.);
#7117=EDGE_CURVE('',#4849,#4855,#553,.T.);
#7118=EDGE_CURVE('',#4855,#4853,#554,.T.);
#7119=EDGE_CURVE('',#4856,#4857,#3281,.T.);
#7120=EDGE_CURVE('',#4858,#4856,#555,.T.);
#7121=EDGE_CURVE('',#4852,#4858,#556,.T.);
#7122=EDGE_CURVE('',#4853,#4859,#557,.T.);
#7123=EDGE_CURVE('',#4859,#4857,#558,.T.);
#7124=EDGE_CURVE('',#4860,#4861,#3282,.T.);
#7125=EDGE_CURVE('',#4862,#4860,#559,.T.);
#7126=EDGE_CURVE('',#4856,#4862,#560,.T.);
#7127=EDGE_CURVE('',#4857,#4863,#561,.T.);
#7128=EDGE_CURVE('',#4863,#4861,#562,.T.);
#7129=EDGE_CURVE('',#4864,#4865,#3283,.T.);
#7130=EDGE_CURVE('',#4866,#4864,#563,.T.);
#7131=EDGE_CURVE('',#4860,#4866,#564,.T.);
#7132=EDGE_CURVE('',#4861,#4867,#565,.T.);
#7133=EDGE_CURVE('',#4867,#4865,#566,.T.);
#7134=EDGE_CURVE('',#4868,#4869,#3284,.T.);
#7135=EDGE_CURVE('',#4870,#4868,#567,.T.);
#7136=EDGE_CURVE('',#4864,#4870,#568,.T.);
#7137=EDGE_CURVE('',#4865,#4871,#569,.T.);
#7138=EDGE_CURVE('',#4871,#4869,#570,.T.);
#7139=EDGE_CURVE('',#4872,#4873,#3285,.T.);
#7140=EDGE_CURVE('',#4874,#4872,#571,.T.);
#7141=EDGE_CURVE('',#4868,#4874,#572,.T.);
#7142=EDGE_CURVE('',#4869,#4875,#573,.T.);
#7143=EDGE_CURVE('',#4875,#4873,#574,.T.);
#7144=EDGE_CURVE('',#4876,#4877,#3286,.T.);
#7145=EDGE_CURVE('',#4878,#4876,#575,.T.);
#7146=EDGE_CURVE('',#4872,#4878,#576,.T.);
#7147=EDGE_CURVE('',#4873,#4879,#577,.T.);
#7148=EDGE_CURVE('',#4879,#4877,#578,.T.);
#7149=EDGE_CURVE('',#4880,#4881,#3287,.T.);
#7150=EDGE_CURVE('',#4882,#4880,#579,.T.);
#7151=EDGE_CURVE('',#4876,#4882,#580,.T.);
#7152=EDGE_CURVE('',#4877,#4883,#581,.T.);
#7153=EDGE_CURVE('',#4883,#4881,#582,.T.);
#7154=EDGE_CURVE('',#4884,#4885,#3288,.T.);
#7155=EDGE_CURVE('',#4886,#4884,#583,.T.);
#7156=EDGE_CURVE('',#4880,#4886,#584,.T.);
#7157=EDGE_CURVE('',#4881,#4887,#585,.T.);
#7158=EDGE_CURVE('',#4887,#4885,#586,.T.);
#7159=EDGE_CURVE('',#4888,#4889,#3289,.T.);
#7160=EDGE_CURVE('',#4890,#4888,#587,.T.);
#7161=EDGE_CURVE('',#4884,#4890,#588,.T.);
#7162=EDGE_CURVE('',#4885,#4891,#589,.T.);
#7163=EDGE_CURVE('',#4891,#4889,#590,.T.);
#7164=EDGE_CURVE('',#4892,#4893,#3290,.T.);
#7165=EDGE_CURVE('',#4894,#4892,#591,.T.);
#7166=EDGE_CURVE('',#4888,#4894,#592,.T.);
#7167=EDGE_CURVE('',#4889,#4895,#593,.T.);
#7168=EDGE_CURVE('',#4895,#4893,#594,.T.);
#7169=EDGE_CURVE('',#4896,#4897,#3291,.T.);
#7170=EDGE_CURVE('',#4898,#4896,#595,.T.);
#7171=EDGE_CURVE('',#4892,#4898,#596,.T.);
#7172=EDGE_CURVE('',#4893,#4899,#597,.T.);
#7173=EDGE_CURVE('',#4899,#4897,#598,.T.);
#7174=EDGE_CURVE('',#4900,#4901,#3292,.T.);
#7175=EDGE_CURVE('',#4902,#4900,#599,.T.);
#7176=EDGE_CURVE('',#4896,#4902,#600,.T.);
#7177=EDGE_CURVE('',#4897,#4903,#601,.T.);
#7178=EDGE_CURVE('',#4903,#4901,#602,.T.);
#7179=EDGE_CURVE('',#4904,#4905,#3293,.T.);
#7180=EDGE_CURVE('',#4906,#4904,#603,.T.);
#7181=EDGE_CURVE('',#4900,#4906,#604,.T.);
#7182=EDGE_CURVE('',#4901,#4907,#605,.T.);
#7183=EDGE_CURVE('',#4907,#4905,#606,.T.);
#7184=EDGE_CURVE('',#4908,#4909,#3294,.T.);
#7185=EDGE_CURVE('',#4910,#4908,#607,.T.);
#7186=EDGE_CURVE('',#4904,#4910,#608,.T.);
#7187=EDGE_CURVE('',#4905,#4911,#609,.T.);
#7188=EDGE_CURVE('',#4911,#4909,#610,.T.);
#7189=EDGE_CURVE('',#4912,#4913,#3295,.T.);
#7190=EDGE_CURVE('',#4914,#4912,#611,.T.);
#7191=EDGE_CURVE('',#4908,#4914,#612,.T.);
#7192=EDGE_CURVE('',#4909,#4915,#613,.T.);
#7193=EDGE_CURVE('',#4915,#4913,#614,.T.);
#7194=EDGE_CURVE('',#4916,#4917,#3296,.T.);
#7195=EDGE_CURVE('',#4918,#4916,#615,.T.);
#7196=EDGE_CURVE('',#4912,#4918,#616,.T.);
#7197=EDGE_CURVE('',#4913,#4919,#617,.T.);
#7198=EDGE_CURVE('',#4919,#4917,#618,.T.);
#7199=EDGE_CURVE('',#4920,#4921,#3297,.T.);
#7200=EDGE_CURVE('',#4922,#4920,#619,.T.);
#7201=EDGE_CURVE('',#4916,#4922,#620,.T.);
#7202=EDGE_CURVE('',#4917,#4923,#621,.T.);
#7203=EDGE_CURVE('',#4923,#4921,#622,.T.);
#7204=EDGE_CURVE('',#4924,#4925,#3298,.T.);
#7205=EDGE_CURVE('',#4926,#4924,#623,.T.);
#7206=EDGE_CURVE('',#4920,#4926,#624,.T.);
#7207=EDGE_CURVE('',#4921,#4927,#625,.T.);
#7208=EDGE_CURVE('',#4927,#4925,#626,.T.);
#7209=EDGE_CURVE('',#4928,#4929,#3299,.T.);
#7210=EDGE_CURVE('',#4930,#4928,#627,.T.);
#7211=EDGE_CURVE('',#4924,#4930,#628,.T.);
#7212=EDGE_CURVE('',#4925,#4931,#629,.T.);
#7213=EDGE_CURVE('',#4931,#4929,#630,.T.);
#7214=EDGE_CURVE('',#4932,#4933,#3300,.T.);
#7215=EDGE_CURVE('',#4934,#4932,#631,.T.);
#7216=EDGE_CURVE('',#4928,#4934,#632,.T.);
#7217=EDGE_CURVE('',#4929,#4935,#633,.T.);
#7218=EDGE_CURVE('',#4935,#4933,#634,.T.);
#7219=EDGE_CURVE('',#4936,#4937,#3301,.T.);
#7220=EDGE_CURVE('',#4938,#4936,#635,.T.);
#7221=EDGE_CURVE('',#4932,#4938,#636,.T.);
#7222=EDGE_CURVE('',#4933,#4939,#637,.T.);
#7223=EDGE_CURVE('',#4939,#4937,#638,.T.);
#7224=EDGE_CURVE('',#4940,#4941,#3302,.T.);
#7225=EDGE_CURVE('',#4942,#4940,#639,.T.);
#7226=EDGE_CURVE('',#4936,#4942,#640,.T.);
#7227=EDGE_CURVE('',#4937,#4943,#641,.T.);
#7228=EDGE_CURVE('',#4943,#4941,#642,.T.);
#7229=EDGE_CURVE('',#4944,#4945,#3303,.T.);
#7230=EDGE_CURVE('',#4946,#4944,#643,.T.);
#7231=EDGE_CURVE('',#4940,#4946,#644,.T.);
#7232=EDGE_CURVE('',#4941,#4947,#645,.T.);
#7233=EDGE_CURVE('',#4947,#4945,#646,.T.);
#7234=EDGE_CURVE('',#4948,#4949,#3304,.T.);
#7235=EDGE_CURVE('',#4950,#4948,#647,.T.);
#7236=EDGE_CURVE('',#4944,#4950,#648,.T.);
#7237=EDGE_CURVE('',#4945,#4951,#649,.T.);
#7238=EDGE_CURVE('',#4951,#4949,#650,.T.);
#7239=EDGE_CURVE('',#4952,#4953,#3305,.T.);
#7240=EDGE_CURVE('',#4954,#4952,#651,.T.);
#7241=EDGE_CURVE('',#4948,#4954,#652,.T.);
#7242=EDGE_CURVE('',#4949,#4955,#653,.T.);
#7243=EDGE_CURVE('',#4955,#4953,#654,.T.);
#7244=EDGE_CURVE('',#4956,#4957,#3306,.T.);
#7245=EDGE_CURVE('',#4958,#4956,#655,.T.);
#7246=EDGE_CURVE('',#4952,#4958,#656,.T.);
#7247=EDGE_CURVE('',#4953,#4959,#657,.T.);
#7248=EDGE_CURVE('',#4959,#4957,#658,.T.);
#7249=EDGE_CURVE('',#4960,#4961,#3307,.T.);
#7250=EDGE_CURVE('',#4962,#4960,#659,.T.);
#7251=EDGE_CURVE('',#4956,#4962,#660,.T.);
#7252=EDGE_CURVE('',#4957,#4963,#661,.T.);
#7253=EDGE_CURVE('',#4963,#4961,#662,.T.);
#7254=EDGE_CURVE('',#4964,#4965,#3308,.T.);
#7255=EDGE_CURVE('',#4966,#4964,#663,.T.);
#7256=EDGE_CURVE('',#4960,#4966,#664,.T.);
#7257=EDGE_CURVE('',#4961,#4967,#665,.T.);
#7258=EDGE_CURVE('',#4967,#4965,#666,.T.);
#7259=EDGE_CURVE('',#4968,#4969,#3309,.T.);
#7260=EDGE_CURVE('',#4970,#4968,#667,.T.);
#7261=EDGE_CURVE('',#4964,#4970,#668,.T.);
#7262=EDGE_CURVE('',#4965,#4971,#669,.T.);
#7263=EDGE_CURVE('',#4971,#4969,#670,.T.);
#7264=EDGE_CURVE('',#4972,#4973,#3310,.T.);
#7265=EDGE_CURVE('',#4974,#4972,#671,.T.);
#7266=EDGE_CURVE('',#4968,#4974,#672,.T.);
#7267=EDGE_CURVE('',#4969,#4975,#673,.T.);
#7268=EDGE_CURVE('',#4975,#4973,#674,.T.);
#7269=EDGE_CURVE('',#4976,#4977,#3311,.T.);
#7270=EDGE_CURVE('',#4978,#4976,#675,.T.);
#7271=EDGE_CURVE('',#4972,#4978,#676,.T.);
#7272=EDGE_CURVE('',#4973,#4979,#677,.T.);
#7273=EDGE_CURVE('',#4979,#4977,#678,.T.);
#7274=EDGE_CURVE('',#4980,#4981,#3312,.T.);
#7275=EDGE_CURVE('',#4982,#4980,#679,.T.);
#7276=EDGE_CURVE('',#4976,#4982,#680,.T.);
#7277=EDGE_CURVE('',#4977,#4983,#681,.T.);
#7278=EDGE_CURVE('',#4983,#4981,#682,.T.);
#7279=EDGE_CURVE('',#4984,#4985,#3313,.T.);
#7280=EDGE_CURVE('',#4986,#4984,#683,.T.);
#7281=EDGE_CURVE('',#4980,#4986,#684,.T.);
#7282=EDGE_CURVE('',#4981,#4987,#685,.T.);
#7283=EDGE_CURVE('',#4987,#4985,#686,.T.);
#7284=EDGE_CURVE('',#4988,#4989,#3314,.T.);
#7285=EDGE_CURVE('',#4990,#4988,#687,.T.);
#7286=EDGE_CURVE('',#4984,#4990,#688,.T.);
#7287=EDGE_CURVE('',#4985,#4991,#689,.T.);
#7288=EDGE_CURVE('',#4991,#4989,#690,.T.);
#7289=EDGE_CURVE('',#4992,#4993,#3315,.T.);
#7290=EDGE_CURVE('',#4994,#4992,#691,.T.);
#7291=EDGE_CURVE('',#4988,#4994,#692,.T.);
#7292=EDGE_CURVE('',#4989,#4995,#693,.T.);
#7293=EDGE_CURVE('',#4995,#4993,#694,.T.);
#7294=EDGE_CURVE('',#4996,#4997,#3316,.T.);
#7295=EDGE_CURVE('',#4998,#4996,#695,.T.);
#7296=EDGE_CURVE('',#4992,#4998,#696,.T.);
#7297=EDGE_CURVE('',#4993,#4999,#697,.T.);
#7298=EDGE_CURVE('',#4999,#4997,#698,.T.);
#7299=EDGE_CURVE('',#5000,#5001,#3317,.T.);
#7300=EDGE_CURVE('',#5002,#5000,#699,.T.);
#7301=EDGE_CURVE('',#4996,#5002,#700,.T.);
#7302=EDGE_CURVE('',#4997,#5003,#701,.T.);
#7303=EDGE_CURVE('',#5003,#5001,#702,.T.);
#7304=EDGE_CURVE('',#5004,#5005,#3318,.T.);
#7305=EDGE_CURVE('',#5006,#5004,#703,.T.);
#7306=EDGE_CURVE('',#5000,#5006,#704,.T.);
#7307=EDGE_CURVE('',#5001,#5007,#705,.T.);
#7308=EDGE_CURVE('',#5007,#5005,#706,.T.);
#7309=EDGE_CURVE('',#5008,#5009,#3319,.T.);
#7310=EDGE_CURVE('',#5010,#5008,#707,.T.);
#7311=EDGE_CURVE('',#5004,#5010,#708,.T.);
#7312=EDGE_CURVE('',#5005,#5011,#709,.T.);
#7313=EDGE_CURVE('',#5011,#5009,#710,.T.);
#7314=EDGE_CURVE('',#5012,#5013,#3320,.T.);
#7315=EDGE_CURVE('',#5014,#5012,#711,.T.);
#7316=EDGE_CURVE('',#5008,#5014,#712,.T.);
#7317=EDGE_CURVE('',#5009,#5015,#713,.T.);
#7318=EDGE_CURVE('',#5015,#5013,#714,.T.);
#7319=EDGE_CURVE('',#5016,#5017,#3321,.T.);
#7320=EDGE_CURVE('',#5018,#5016,#715,.T.);
#7321=EDGE_CURVE('',#5012,#5018,#716,.T.);
#7322=EDGE_CURVE('',#5013,#5019,#717,.T.);
#7323=EDGE_CURVE('',#5019,#5017,#718,.T.);
#7324=EDGE_CURVE('',#5020,#5021,#3322,.T.);
#7325=EDGE_CURVE('',#5022,#5020,#719,.T.);
#7326=EDGE_CURVE('',#5016,#5022,#720,.T.);
#7327=EDGE_CURVE('',#5017,#5023,#721,.T.);
#7328=EDGE_CURVE('',#5023,#5021,#722,.T.);
#7329=EDGE_CURVE('',#5024,#5025,#3323,.T.);
#7330=EDGE_CURVE('',#5026,#5024,#723,.T.);
#7331=EDGE_CURVE('',#5020,#5026,#724,.T.);
#7332=EDGE_CURVE('',#5021,#5027,#725,.T.);
#7333=EDGE_CURVE('',#5027,#5025,#726,.T.);
#7334=EDGE_CURVE('',#5028,#5029,#3324,.T.);
#7335=EDGE_CURVE('',#5030,#5028,#727,.T.);
#7336=EDGE_CURVE('',#5024,#5030,#728,.T.);
#7337=EDGE_CURVE('',#5025,#5031,#729,.T.);
#7338=EDGE_CURVE('',#5031,#5029,#730,.T.);
#7339=EDGE_CURVE('',#5032,#5033,#3325,.T.);
#7340=EDGE_CURVE('',#5034,#5032,#731,.T.);
#7341=EDGE_CURVE('',#5028,#5034,#732,.T.);
#7342=EDGE_CURVE('',#5029,#5035,#733,.T.);
#7343=EDGE_CURVE('',#5035,#5033,#734,.T.);
#7344=EDGE_CURVE('',#5036,#5037,#3326,.T.);
#7345=EDGE_CURVE('',#5038,#5036,#735,.T.);
#7346=EDGE_CURVE('',#5032,#5038,#736,.T.);
#7347=EDGE_CURVE('',#5033,#5039,#737,.T.);
#7348=EDGE_CURVE('',#5039,#5037,#738,.T.);
#7349=EDGE_CURVE('',#5040,#5041,#3327,.T.);
#7350=EDGE_CURVE('',#5042,#5040,#739,.T.);
#7351=EDGE_CURVE('',#5036,#5042,#740,.T.);
#7352=EDGE_CURVE('',#5037,#5043,#741,.T.);
#7353=EDGE_CURVE('',#5043,#5041,#742,.T.);
#7354=EDGE_CURVE('',#5044,#5045,#3328,.T.);
#7355=EDGE_CURVE('',#5046,#5044,#743,.T.);
#7356=EDGE_CURVE('',#5040,#5046,#744,.T.);
#7357=EDGE_CURVE('',#5041,#5047,#745,.T.);
#7358=EDGE_CURVE('',#5047,#5045,#746,.T.);
#7359=EDGE_CURVE('',#5048,#5049,#3329,.T.);
#7360=EDGE_CURVE('',#5050,#5048,#747,.T.);
#7361=EDGE_CURVE('',#5044,#5050,#748,.T.);
#7362=EDGE_CURVE('',#5045,#5051,#749,.T.);
#7363=EDGE_CURVE('',#5051,#5049,#750,.T.);
#7364=EDGE_CURVE('',#5052,#5053,#3330,.T.);
#7365=EDGE_CURVE('',#5054,#5052,#751,.T.);
#7366=EDGE_CURVE('',#5048,#5054,#752,.T.);
#7367=EDGE_CURVE('',#5049,#5055,#753,.T.);
#7368=EDGE_CURVE('',#5055,#5053,#754,.T.);
#7369=EDGE_CURVE('',#5056,#5057,#3331,.T.);
#7370=EDGE_CURVE('',#5058,#5056,#755,.T.);
#7371=EDGE_CURVE('',#5052,#5058,#756,.T.);
#7372=EDGE_CURVE('',#5053,#5059,#757,.T.);
#7373=EDGE_CURVE('',#5059,#5057,#758,.T.);
#7374=EDGE_CURVE('',#5060,#5061,#3332,.T.);
#7375=EDGE_CURVE('',#5062,#5060,#759,.T.);
#7376=EDGE_CURVE('',#5056,#5062,#760,.T.);
#7377=EDGE_CURVE('',#5057,#5063,#761,.T.);
#7378=EDGE_CURVE('',#5063,#5061,#762,.T.);
#7379=EDGE_CURVE('',#5064,#5065,#3333,.T.);
#7380=EDGE_CURVE('',#5066,#5064,#763,.T.);
#7381=EDGE_CURVE('',#5060,#5066,#764,.T.);
#7382=EDGE_CURVE('',#5061,#5067,#765,.T.);
#7383=EDGE_CURVE('',#5067,#5065,#766,.T.);
#7384=EDGE_CURVE('',#5068,#5069,#3334,.T.);
#7385=EDGE_CURVE('',#5070,#5068,#767,.T.);
#7386=EDGE_CURVE('',#5064,#5070,#768,.T.);
#7387=EDGE_CURVE('',#5065,#5071,#769,.T.);
#7388=EDGE_CURVE('',#5071,#5069,#770,.T.);
#7389=EDGE_CURVE('',#5072,#5073,#3335,.T.);
#7390=EDGE_CURVE('',#5074,#5072,#771,.T.);
#7391=EDGE_CURVE('',#5068,#5074,#772,.T.);
#7392=EDGE_CURVE('',#5069,#5075,#773,.T.);
#7393=EDGE_CURVE('',#5075,#5073,#774,.T.);
#7394=EDGE_CURVE('',#5076,#5077,#3336,.T.);
#7395=EDGE_CURVE('',#5078,#5076,#775,.T.);
#7396=EDGE_CURVE('',#5072,#5078,#776,.T.);
#7397=EDGE_CURVE('',#5073,#5079,#777,.T.);
#7398=EDGE_CURVE('',#5079,#5077,#778,.T.);
#7399=EDGE_CURVE('',#5080,#5081,#3337,.T.);
#7400=EDGE_CURVE('',#5082,#5080,#779,.T.);
#7401=EDGE_CURVE('',#5076,#5082,#780,.T.);
#7402=EDGE_CURVE('',#5077,#5083,#781,.T.);
#7403=EDGE_CURVE('',#5083,#5081,#782,.T.);
#7404=EDGE_CURVE('',#5084,#5085,#3338,.T.);
#7405=EDGE_CURVE('',#5086,#5084,#783,.T.);
#7406=EDGE_CURVE('',#5080,#5086,#784,.T.);
#7407=EDGE_CURVE('',#5081,#5087,#785,.T.);
#7408=EDGE_CURVE('',#5087,#5085,#786,.T.);
#7409=EDGE_CURVE('',#5088,#5089,#3339,.T.);
#7410=EDGE_CURVE('',#5090,#5088,#787,.T.);
#7411=EDGE_CURVE('',#5084,#5090,#788,.T.);
#7412=EDGE_CURVE('',#5085,#5091,#789,.T.);
#7413=EDGE_CURVE('',#5091,#5089,#790,.T.);
#7414=EDGE_CURVE('',#5092,#5093,#3340,.T.);
#7415=EDGE_CURVE('',#5094,#5092,#791,.T.);
#7416=EDGE_CURVE('',#5088,#5094,#792,.T.);
#7417=EDGE_CURVE('',#5089,#5095,#793,.T.);
#7418=EDGE_CURVE('',#5095,#5093,#794,.T.);
#7419=EDGE_CURVE('',#5096,#5097,#3341,.T.);
#7420=EDGE_CURVE('',#5098,#5096,#795,.T.);
#7421=EDGE_CURVE('',#5092,#5098,#796,.T.);
#7422=EDGE_CURVE('',#5093,#5099,#797,.T.);
#7423=EDGE_CURVE('',#5099,#5097,#798,.T.);
#7424=EDGE_CURVE('',#5100,#5101,#3342,.T.);
#7425=EDGE_CURVE('',#5102,#5100,#799,.T.);
#7426=EDGE_CURVE('',#5096,#5102,#800,.T.);
#7427=EDGE_CURVE('',#5097,#5103,#801,.T.);
#7428=EDGE_CURVE('',#5103,#5101,#802,.T.);
#7429=EDGE_CURVE('',#5104,#5105,#3343,.T.);
#7430=EDGE_CURVE('',#5106,#5104,#803,.T.);
#7431=EDGE_CURVE('',#5100,#5106,#804,.T.);
#7432=EDGE_CURVE('',#5101,#5107,#805,.T.);
#7433=EDGE_CURVE('',#5107,#5105,#806,.T.);
#7434=EDGE_CURVE('',#5108,#5109,#3344,.T.);
#7435=EDGE_CURVE('',#5110,#5108,#807,.T.);
#7436=EDGE_CURVE('',#5104,#5110,#808,.T.);
#7437=EDGE_CURVE('',#5105,#5111,#809,.T.);
#7438=EDGE_CURVE('',#5111,#5109,#810,.T.);
#7439=EDGE_CURVE('',#5112,#5113,#3345,.T.);
#7440=EDGE_CURVE('',#5114,#5112,#811,.T.);
#7441=EDGE_CURVE('',#5108,#5114,#812,.T.);
#7442=EDGE_CURVE('',#5109,#5115,#813,.T.);
#7443=EDGE_CURVE('',#5115,#5113,#814,.T.);
#7444=EDGE_CURVE('',#5116,#5117,#3346,.T.);
#7445=EDGE_CURVE('',#5118,#5116,#815,.T.);
#7446=EDGE_CURVE('',#5112,#5118,#816,.T.);
#7447=EDGE_CURVE('',#5113,#5119,#817,.T.);
#7448=EDGE_CURVE('',#5119,#5117,#818,.T.);
#7449=EDGE_CURVE('',#5120,#5121,#3347,.T.);
#7450=EDGE_CURVE('',#5122,#5120,#819,.T.);
#7451=EDGE_CURVE('',#5116,#5122,#820,.T.);
#7452=EDGE_CURVE('',#5117,#5123,#821,.T.);
#7453=EDGE_CURVE('',#5123,#5121,#822,.T.);
#7454=EDGE_CURVE('',#5124,#5125,#3348,.T.);
#7455=EDGE_CURVE('',#5126,#5124,#823,.T.);
#7456=EDGE_CURVE('',#5120,#5126,#824,.T.);
#7457=EDGE_CURVE('',#5121,#5127,#825,.T.);
#7458=EDGE_CURVE('',#5127,#5125,#826,.T.);
#7459=EDGE_CURVE('',#5128,#5129,#3349,.T.);
#7460=EDGE_CURVE('',#5130,#5128,#827,.T.);
#7461=EDGE_CURVE('',#5124,#5130,#828,.T.);
#7462=EDGE_CURVE('',#5125,#5131,#829,.T.);
#7463=EDGE_CURVE('',#5131,#5129,#830,.T.);
#7464=EDGE_CURVE('',#5132,#5133,#3350,.T.);
#7465=EDGE_CURVE('',#5134,#5132,#831,.T.);
#7466=EDGE_CURVE('',#5128,#5134,#832,.T.);
#7467=EDGE_CURVE('',#5129,#5135,#833,.T.);
#7468=EDGE_CURVE('',#5135,#5133,#834,.T.);
#7469=EDGE_CURVE('',#5136,#5137,#3351,.T.);
#7470=EDGE_CURVE('',#5138,#5136,#835,.T.);
#7471=EDGE_CURVE('',#5132,#5138,#836,.T.);
#7472=EDGE_CURVE('',#5133,#5139,#837,.T.);
#7473=EDGE_CURVE('',#5139,#5137,#838,.T.);
#7474=EDGE_CURVE('',#5140,#5141,#3352,.T.);
#7475=EDGE_CURVE('',#5142,#5140,#839,.T.);
#7476=EDGE_CURVE('',#5136,#5142,#840,.T.);
#7477=EDGE_CURVE('',#5137,#5143,#841,.T.);
#7478=EDGE_CURVE('',#5143,#5141,#842,.T.);
#7479=EDGE_CURVE('',#5144,#5145,#3353,.T.);
#7480=EDGE_CURVE('',#5146,#5144,#843,.T.);
#7481=EDGE_CURVE('',#5140,#5146,#844,.T.);
#7482=EDGE_CURVE('',#5141,#5147,#845,.T.);
#7483=EDGE_CURVE('',#5147,#5145,#846,.T.);
#7484=EDGE_CURVE('',#5148,#5149,#3354,.T.);
#7485=EDGE_CURVE('',#5150,#5148,#847,.T.);
#7486=EDGE_CURVE('',#5144,#5150,#848,.T.);
#7487=EDGE_CURVE('',#5145,#5151,#849,.T.);
#7488=EDGE_CURVE('',#5151,#5149,#850,.T.);
#7489=EDGE_CURVE('',#5152,#5153,#3355,.T.);
#7490=EDGE_CURVE('',#5154,#5152,#851,.T.);
#7491=EDGE_CURVE('',#5148,#5154,#852,.T.);
#7492=EDGE_CURVE('',#5149,#5155,#853,.T.);
#7493=EDGE_CURVE('',#5155,#5153,#854,.T.);
#7494=EDGE_CURVE('',#5156,#5157,#3356,.T.);
#7495=EDGE_CURVE('',#5158,#5156,#855,.T.);
#7496=EDGE_CURVE('',#5152,#5158,#856,.T.);
#7497=EDGE_CURVE('',#5153,#5159,#857,.T.);
#7498=EDGE_CURVE('',#5159,#5157,#858,.T.);
#7499=EDGE_CURVE('',#5160,#5161,#3357,.T.);
#7500=EDGE_CURVE('',#5162,#5160,#859,.T.);
#7501=EDGE_CURVE('',#5156,#5162,#860,.T.);
#7502=EDGE_CURVE('',#5157,#5163,#861,.T.);
#7503=EDGE_CURVE('',#5163,#5161,#862,.T.);
#7504=EDGE_CURVE('',#5164,#5165,#3358,.T.);
#7505=EDGE_CURVE('',#5166,#5164,#863,.T.);
#7506=EDGE_CURVE('',#5160,#5166,#864,.T.);
#7507=EDGE_CURVE('',#5161,#5167,#865,.T.);
#7508=EDGE_CURVE('',#5167,#5165,#866,.T.);
#7509=EDGE_CURVE('',#5168,#5169,#3359,.T.);
#7510=EDGE_CURVE('',#5170,#5168,#867,.T.);
#7511=EDGE_CURVE('',#5164,#5170,#868,.T.);
#7512=EDGE_CURVE('',#5165,#5171,#869,.T.);
#7513=EDGE_CURVE('',#5171,#5169,#870,.T.);
#7514=EDGE_CURVE('',#5172,#5173,#3360,.T.);
#7515=EDGE_CURVE('',#5174,#5172,#871,.T.);
#7516=EDGE_CURVE('',#5168,#5174,#872,.T.);
#7517=EDGE_CURVE('',#5169,#5175,#873,.T.);
#7518=EDGE_CURVE('',#5175,#5173,#874,.T.);
#7519=EDGE_CURVE('',#5176,#5177,#3361,.T.);
#7520=EDGE_CURVE('',#5178,#5176,#875,.T.);
#7521=EDGE_CURVE('',#5172,#5178,#876,.T.);
#7522=EDGE_CURVE('',#5173,#5179,#877,.T.);
#7523=EDGE_CURVE('',#5179,#5177,#878,.T.);
#7524=EDGE_CURVE('',#5180,#5181,#3362,.T.);
#7525=EDGE_CURVE('',#5182,#5180,#879,.T.);
#7526=EDGE_CURVE('',#5176,#5182,#880,.T.);
#7527=EDGE_CURVE('',#5177,#5183,#881,.T.);
#7528=EDGE_CURVE('',#5183,#5181,#882,.T.);
#7529=EDGE_CURVE('',#5184,#5185,#3363,.T.);
#7530=EDGE_CURVE('',#5186,#5184,#883,.T.);
#7531=EDGE_CURVE('',#5180,#5186,#884,.T.);
#7532=EDGE_CURVE('',#5181,#5187,#885,.T.);
#7533=EDGE_CURVE('',#5187,#5185,#886,.T.);
#7534=EDGE_CURVE('',#5188,#5189,#3364,.T.);
#7535=EDGE_CURVE('',#5190,#5188,#887,.T.);
#7536=EDGE_CURVE('',#5184,#5190,#888,.T.);
#7537=EDGE_CURVE('',#5185,#5191,#889,.T.);
#7538=EDGE_CURVE('',#5191,#5189,#890,.T.);
#7539=EDGE_CURVE('',#5192,#5193,#3365,.T.);
#7540=EDGE_CURVE('',#5194,#5192,#891,.T.);
#7541=EDGE_CURVE('',#5188,#5194,#892,.T.);
#7542=EDGE_CURVE('',#5189,#5195,#893,.T.);
#7543=EDGE_CURVE('',#5195,#5193,#894,.T.);
#7544=EDGE_CURVE('',#5196,#5197,#3366,.T.);
#7545=EDGE_CURVE('',#5198,#5196,#895,.T.);
#7546=EDGE_CURVE('',#5192,#5198,#896,.T.);
#7547=EDGE_CURVE('',#5193,#5199,#897,.T.);
#7548=EDGE_CURVE('',#5199,#5197,#898,.T.);
#7549=EDGE_CURVE('',#5200,#5201,#3367,.T.);
#7550=EDGE_CURVE('',#5202,#5200,#899,.T.);
#7551=EDGE_CURVE('',#5196,#5202,#900,.T.);
#7552=EDGE_CURVE('',#5197,#5203,#901,.T.);
#7553=EDGE_CURVE('',#5203,#5201,#902,.T.);
#7554=EDGE_CURVE('',#5204,#5205,#3368,.T.);
#7555=EDGE_CURVE('',#5206,#5204,#903,.T.);
#7556=EDGE_CURVE('',#5200,#5206,#904,.T.);
#7557=EDGE_CURVE('',#5201,#5207,#905,.T.);
#7558=EDGE_CURVE('',#5207,#5205,#906,.T.);
#7559=EDGE_CURVE('',#5208,#5209,#3369,.T.);
#7560=EDGE_CURVE('',#5210,#5208,#907,.T.);
#7561=EDGE_CURVE('',#5204,#5210,#908,.T.);
#7562=EDGE_CURVE('',#5205,#5211,#909,.T.);
#7563=EDGE_CURVE('',#5211,#5209,#910,.T.);
#7564=EDGE_CURVE('',#5212,#5213,#3370,.T.);
#7565=EDGE_CURVE('',#5214,#5212,#911,.T.);
#7566=EDGE_CURVE('',#5208,#5214,#912,.T.);
#7567=EDGE_CURVE('',#5209,#5215,#913,.T.);
#7568=EDGE_CURVE('',#5215,#5213,#914,.T.);
#7569=EDGE_CURVE('',#5216,#5217,#3371,.T.);
#7570=EDGE_CURVE('',#5218,#5216,#915,.T.);
#7571=EDGE_CURVE('',#5212,#5218,#916,.T.);
#7572=EDGE_CURVE('',#5213,#5219,#917,.T.);
#7573=EDGE_CURVE('',#5219,#5217,#918,.T.);
#7574=EDGE_CURVE('',#5220,#5221,#3372,.T.);
#7575=EDGE_CURVE('',#5222,#5220,#919,.T.);
#7576=EDGE_CURVE('',#5216,#5222,#920,.T.);
#7577=EDGE_CURVE('',#5217,#5223,#921,.T.);
#7578=EDGE_CURVE('',#5223,#5221,#922,.T.);
#7579=EDGE_CURVE('',#5224,#5225,#3373,.T.);
#7580=EDGE_CURVE('',#5226,#5224,#923,.T.);
#7581=EDGE_CURVE('',#5220,#5226,#924,.T.);
#7582=EDGE_CURVE('',#5221,#5227,#925,.T.);
#7583=EDGE_CURVE('',#5227,#5225,#926,.T.);
#7584=EDGE_CURVE('',#5228,#5229,#3374,.T.);
#7585=EDGE_CURVE('',#5230,#5228,#927,.T.);
#7586=EDGE_CURVE('',#5224,#5230,#928,.T.);
#7587=EDGE_CURVE('',#5225,#5231,#929,.T.);
#7588=EDGE_CURVE('',#5231,#5229,#930,.T.);
#7589=EDGE_CURVE('',#5232,#5233,#3375,.T.);
#7590=EDGE_CURVE('',#5234,#5232,#931,.T.);
#7591=EDGE_CURVE('',#5228,#5234,#932,.T.);
#7592=EDGE_CURVE('',#5229,#5235,#933,.T.);
#7593=EDGE_CURVE('',#5235,#5233,#934,.T.);
#7594=EDGE_CURVE('',#5236,#5237,#3376,.T.);
#7595=EDGE_CURVE('',#5238,#5236,#935,.T.);
#7596=EDGE_CURVE('',#5232,#5238,#936,.T.);
#7597=EDGE_CURVE('',#5233,#5239,#937,.T.);
#7598=EDGE_CURVE('',#5239,#5237,#938,.T.);
#7599=EDGE_CURVE('',#5240,#5241,#3377,.T.);
#7600=EDGE_CURVE('',#5242,#5240,#939,.T.);
#7601=EDGE_CURVE('',#5236,#5242,#940,.T.);
#7602=EDGE_CURVE('',#5237,#5243,#941,.T.);
#7603=EDGE_CURVE('',#5243,#5241,#942,.T.);
#7604=EDGE_CURVE('',#5244,#5245,#3378,.T.);
#7605=EDGE_CURVE('',#5246,#5244,#943,.T.);
#7606=EDGE_CURVE('',#5240,#5246,#944,.T.);
#7607=EDGE_CURVE('',#5241,#5247,#945,.T.);
#7608=EDGE_CURVE('',#5247,#5245,#946,.T.);
#7609=EDGE_CURVE('',#5248,#5249,#3379,.T.);
#7610=EDGE_CURVE('',#5250,#5248,#947,.T.);
#7611=EDGE_CURVE('',#5244,#5250,#948,.T.);
#7612=EDGE_CURVE('',#5245,#5251,#949,.T.);
#7613=EDGE_CURVE('',#5251,#5249,#950,.T.);
#7614=EDGE_CURVE('',#5252,#5253,#3380,.T.);
#7615=EDGE_CURVE('',#5254,#5252,#951,.T.);
#7616=EDGE_CURVE('',#5248,#5254,#952,.T.);
#7617=EDGE_CURVE('',#5249,#5255,#953,.T.);
#7618=EDGE_CURVE('',#5255,#5253,#954,.T.);
#7619=EDGE_CURVE('',#5256,#5257,#3381,.T.);
#7620=EDGE_CURVE('',#5258,#5256,#955,.T.);
#7621=EDGE_CURVE('',#5252,#5258,#956,.T.);
#7622=EDGE_CURVE('',#5253,#5259,#957,.T.);
#7623=EDGE_CURVE('',#5259,#5257,#958,.T.);
#7624=EDGE_CURVE('',#5260,#5261,#3382,.T.);
#7625=EDGE_CURVE('',#5262,#5260,#959,.T.);
#7626=EDGE_CURVE('',#5256,#5262,#960,.T.);
#7627=EDGE_CURVE('',#5257,#5263,#961,.T.);
#7628=EDGE_CURVE('',#5263,#5261,#962,.T.);
#7629=EDGE_CURVE('',#5264,#5265,#3383,.T.);
#7630=EDGE_CURVE('',#5266,#5264,#963,.T.);
#7631=EDGE_CURVE('',#5260,#5266,#964,.T.);
#7632=EDGE_CURVE('',#5261,#5267,#965,.T.);
#7633=EDGE_CURVE('',#5267,#5265,#966,.T.);
#7634=EDGE_CURVE('',#5268,#5269,#3384,.T.);
#7635=EDGE_CURVE('',#5270,#5268,#967,.T.);
#7636=EDGE_CURVE('',#5264,#5270,#968,.T.);
#7637=EDGE_CURVE('',#5265,#5271,#969,.T.);
#7638=EDGE_CURVE('',#5271,#5269,#970,.T.);
#7639=EDGE_CURVE('',#5272,#5273,#3385,.T.);
#7640=EDGE_CURVE('',#5274,#5272,#971,.T.);
#7641=EDGE_CURVE('',#5268,#5274,#972,.T.);
#7642=EDGE_CURVE('',#5269,#5275,#973,.T.);
#7643=EDGE_CURVE('',#5275,#5273,#974,.T.);
#7644=EDGE_CURVE('',#5276,#5277,#3386,.T.);
#7645=EDGE_CURVE('',#5278,#5276,#975,.T.);
#7646=EDGE_CURVE('',#5272,#5278,#976,.T.);
#7647=EDGE_CURVE('',#5273,#5279,#977,.T.);
#7648=EDGE_CURVE('',#5279,#5277,#978,.T.);
#7649=EDGE_CURVE('',#5280,#5281,#3387,.T.);
#7650=EDGE_CURVE('',#5282,#5280,#979,.T.);
#7651=EDGE_CURVE('',#5276,#5282,#980,.T.);
#7652=EDGE_CURVE('',#5277,#5283,#981,.T.);
#7653=EDGE_CURVE('',#5283,#5281,#982,.T.);
#7654=EDGE_CURVE('',#5284,#5285,#3388,.T.);
#7655=EDGE_CURVE('',#5286,#5284,#983,.T.);
#7656=EDGE_CURVE('',#5280,#5286,#984,.T.);
#7657=EDGE_CURVE('',#5281,#5287,#985,.T.);
#7658=EDGE_CURVE('',#5287,#5285,#986,.T.);
#7659=EDGE_CURVE('',#5288,#5289,#3389,.T.);
#7660=EDGE_CURVE('',#5290,#5288,#987,.T.);
#7661=EDGE_CURVE('',#5284,#5290,#988,.T.);
#7662=EDGE_CURVE('',#5285,#5291,#989,.T.);
#7663=EDGE_CURVE('',#5291,#5289,#990,.T.);
#7664=EDGE_CURVE('',#5292,#5293,#3390,.T.);
#7665=EDGE_CURVE('',#5294,#5292,#991,.T.);
#7666=EDGE_CURVE('',#5288,#5294,#992,.T.);
#7667=EDGE_CURVE('',#5289,#5295,#993,.T.);
#7668=EDGE_CURVE('',#5295,#5293,#994,.T.);
#7669=EDGE_CURVE('',#5296,#5297,#3391,.T.);
#7670=EDGE_CURVE('',#5298,#5296,#995,.T.);
#7671=EDGE_CURVE('',#5292,#5298,#996,.T.);
#7672=EDGE_CURVE('',#5293,#5299,#997,.T.);
#7673=EDGE_CURVE('',#5299,#5297,#998,.T.);
#7674=EDGE_CURVE('',#5300,#5301,#3392,.T.);
#7675=EDGE_CURVE('',#5302,#5300,#999,.T.);
#7676=EDGE_CURVE('',#5296,#5302,#1000,.T.);
#7677=EDGE_CURVE('',#5297,#5303,#1001,.T.);
#7678=EDGE_CURVE('',#5303,#5301,#1002,.T.);
#7679=EDGE_CURVE('',#5304,#5305,#3393,.T.);
#7680=EDGE_CURVE('',#5306,#5304,#1003,.T.);
#7681=EDGE_CURVE('',#5300,#5306,#1004,.T.);
#7682=EDGE_CURVE('',#5301,#5307,#1005,.T.);
#7683=EDGE_CURVE('',#5307,#5305,#1006,.T.);
#7684=EDGE_CURVE('',#5308,#5309,#3394,.T.);
#7685=EDGE_CURVE('',#5310,#5308,#1007,.T.);
#7686=EDGE_CURVE('',#5304,#5310,#1008,.T.);
#7687=EDGE_CURVE('',#5305,#5311,#1009,.T.);
#7688=EDGE_CURVE('',#5311,#5309,#1010,.T.);
#7689=EDGE_CURVE('',#5312,#5313,#3395,.T.);
#7690=EDGE_CURVE('',#5314,#5312,#1011,.T.);
#7691=EDGE_CURVE('',#5308,#5314,#1012,.T.);
#7692=EDGE_CURVE('',#5309,#5315,#1013,.T.);
#7693=EDGE_CURVE('',#5315,#5313,#1014,.T.);
#7694=EDGE_CURVE('',#5316,#5317,#3396,.T.);
#7695=EDGE_CURVE('',#5318,#5316,#1015,.T.);
#7696=EDGE_CURVE('',#5312,#5318,#1016,.T.);
#7697=EDGE_CURVE('',#5313,#5319,#1017,.T.);
#7698=EDGE_CURVE('',#5319,#5317,#1018,.T.);
#7699=EDGE_CURVE('',#5320,#5321,#3397,.T.);
#7700=EDGE_CURVE('',#5322,#5320,#1019,.T.);
#7701=EDGE_CURVE('',#5316,#5322,#1020,.T.);
#7702=EDGE_CURVE('',#5317,#5323,#1021,.T.);
#7703=EDGE_CURVE('',#5323,#5321,#1022,.T.);
#7704=EDGE_CURVE('',#5324,#5325,#3398,.T.);
#7705=EDGE_CURVE('',#5326,#5324,#1023,.T.);
#7706=EDGE_CURVE('',#5320,#5326,#1024,.T.);
#7707=EDGE_CURVE('',#5321,#5327,#1025,.T.);
#7708=EDGE_CURVE('',#5327,#5325,#1026,.T.);
#7709=EDGE_CURVE('',#5328,#5329,#3399,.T.);
#7710=EDGE_CURVE('',#5330,#5328,#1027,.T.);
#7711=EDGE_CURVE('',#5324,#5330,#1028,.T.);
#7712=EDGE_CURVE('',#5325,#5331,#1029,.T.);
#7713=EDGE_CURVE('',#5331,#5329,#1030,.T.);
#7714=EDGE_CURVE('',#5332,#5333,#3400,.T.);
#7715=EDGE_CURVE('',#5334,#5332,#1031,.T.);
#7716=EDGE_CURVE('',#5328,#5334,#1032,.T.);
#7717=EDGE_CURVE('',#5329,#5335,#1033,.T.);
#7718=EDGE_CURVE('',#5335,#5333,#1034,.T.);
#7719=EDGE_CURVE('',#5336,#5337,#3401,.T.);
#7720=EDGE_CURVE('',#5338,#5336,#1035,.T.);
#7721=EDGE_CURVE('',#5332,#5338,#1036,.T.);
#7722=EDGE_CURVE('',#5333,#5339,#1037,.T.);
#7723=EDGE_CURVE('',#5339,#5337,#1038,.T.);
#7724=EDGE_CURVE('',#5340,#5341,#3402,.T.);
#7725=EDGE_CURVE('',#5342,#5340,#1039,.T.);
#7726=EDGE_CURVE('',#5336,#5342,#1040,.T.);
#7727=EDGE_CURVE('',#5337,#5343,#1041,.T.);
#7728=EDGE_CURVE('',#5343,#5341,#1042,.T.);
#7729=EDGE_CURVE('',#5344,#5345,#3403,.T.);
#7730=EDGE_CURVE('',#5346,#5344,#1043,.T.);
#7731=EDGE_CURVE('',#5340,#5346,#1044,.T.);
#7732=EDGE_CURVE('',#5341,#5347,#1045,.T.);
#7733=EDGE_CURVE('',#5347,#5345,#1046,.T.);
#7734=EDGE_CURVE('',#5348,#5349,#3404,.T.);
#7735=EDGE_CURVE('',#5350,#5348,#1047,.T.);
#7736=EDGE_CURVE('',#5344,#5350,#1048,.T.);
#7737=EDGE_CURVE('',#5345,#5351,#1049,.T.);
#7738=EDGE_CURVE('',#5351,#5349,#1050,.T.);
#7739=EDGE_CURVE('',#5352,#5353,#3405,.T.);
#7740=EDGE_CURVE('',#5354,#5352,#1051,.T.);
#7741=EDGE_CURVE('',#5348,#5354,#1052,.T.);
#7742=EDGE_CURVE('',#5349,#5355,#1053,.T.);
#7743=EDGE_CURVE('',#5355,#5353,#1054,.T.);
#7744=EDGE_CURVE('',#5356,#5357,#3406,.T.);
#7745=EDGE_CURVE('',#5358,#5356,#1055,.T.);
#7746=EDGE_CURVE('',#5352,#5358,#1056,.T.);
#7747=EDGE_CURVE('',#5353,#5359,#1057,.T.);
#7748=EDGE_CURVE('',#5359,#5357,#1058,.T.);
#7749=EDGE_CURVE('',#5360,#5361,#3407,.T.);
#7750=EDGE_CURVE('',#5362,#5360,#1059,.T.);
#7751=EDGE_CURVE('',#5356,#5362,#1060,.T.);
#7752=EDGE_CURVE('',#5357,#5363,#1061,.T.);
#7753=EDGE_CURVE('',#5363,#5361,#1062,.T.);
#7754=EDGE_CURVE('',#5364,#5365,#3408,.T.);
#7755=EDGE_CURVE('',#5366,#5364,#1063,.T.);
#7756=EDGE_CURVE('',#5360,#5366,#1064,.T.);
#7757=EDGE_CURVE('',#5361,#5367,#1065,.T.);
#7758=EDGE_CURVE('',#5367,#5365,#1066,.T.);
#7759=EDGE_CURVE('',#5368,#5369,#3409,.T.);
#7760=EDGE_CURVE('',#5370,#5368,#1067,.T.);
#7761=EDGE_CURVE('',#5364,#5370,#1068,.T.);
#7762=EDGE_CURVE('',#5365,#5371,#1069,.T.);
#7763=EDGE_CURVE('',#5371,#5369,#1070,.T.);
#7764=EDGE_CURVE('',#5372,#5373,#3410,.T.);
#7765=EDGE_CURVE('',#5374,#5372,#1071,.T.);
#7766=EDGE_CURVE('',#5368,#5374,#1072,.T.);
#7767=EDGE_CURVE('',#5369,#5375,#1073,.T.);
#7768=EDGE_CURVE('',#5375,#5373,#1074,.T.);
#7769=EDGE_CURVE('',#5376,#5377,#3411,.T.);
#7770=EDGE_CURVE('',#5378,#5376,#1075,.T.);
#7771=EDGE_CURVE('',#5372,#5378,#1076,.T.);
#7772=EDGE_CURVE('',#5373,#5379,#1077,.T.);
#7773=EDGE_CURVE('',#5379,#5377,#1078,.T.);
#7774=EDGE_CURVE('',#5380,#5381,#3412,.T.);
#7775=EDGE_CURVE('',#5382,#5380,#1079,.T.);
#7776=EDGE_CURVE('',#5376,#5382,#1080,.T.);
#7777=EDGE_CURVE('',#5377,#5383,#1081,.T.);
#7778=EDGE_CURVE('',#5383,#5381,#1082,.T.);
#7779=EDGE_CURVE('',#5384,#5385,#3413,.T.);
#7780=EDGE_CURVE('',#5386,#5384,#1083,.T.);
#7781=EDGE_CURVE('',#5380,#5386,#1084,.T.);
#7782=EDGE_CURVE('',#5381,#5387,#1085,.T.);
#7783=EDGE_CURVE('',#5387,#5385,#1086,.T.);
#7784=EDGE_CURVE('',#5388,#5389,#3414,.T.);
#7785=EDGE_CURVE('',#5390,#5388,#1087,.T.);
#7786=EDGE_CURVE('',#5384,#5390,#1088,.T.);
#7787=EDGE_CURVE('',#5385,#5391,#1089,.T.);
#7788=EDGE_CURVE('',#5391,#5389,#1090,.T.);
#7789=EDGE_CURVE('',#5392,#5393,#3415,.T.);
#7790=EDGE_CURVE('',#5394,#5392,#1091,.T.);
#7791=EDGE_CURVE('',#5388,#5394,#1092,.T.);
#7792=EDGE_CURVE('',#5389,#5395,#1093,.T.);
#7793=EDGE_CURVE('',#5395,#5393,#1094,.T.);
#7794=EDGE_CURVE('',#5396,#5397,#3416,.T.);
#7795=EDGE_CURVE('',#5398,#5396,#1095,.T.);
#7796=EDGE_CURVE('',#5392,#5398,#1096,.T.);
#7797=EDGE_CURVE('',#5393,#5399,#1097,.T.);
#7798=EDGE_CURVE('',#5399,#5397,#1098,.T.);
#7799=EDGE_CURVE('',#5400,#5401,#3417,.T.);
#7800=EDGE_CURVE('',#5402,#5400,#1099,.T.);
#7801=EDGE_CURVE('',#5396,#5402,#1100,.T.);
#7802=EDGE_CURVE('',#5397,#5403,#1101,.T.);
#7803=EDGE_CURVE('',#5403,#5401,#1102,.T.);
#7804=EDGE_CURVE('',#5404,#5405,#3418,.T.);
#7805=EDGE_CURVE('',#5406,#5404,#1103,.T.);
#7806=EDGE_CURVE('',#5400,#5406,#1104,.T.);
#7807=EDGE_CURVE('',#5401,#5407,#1105,.T.);
#7808=EDGE_CURVE('',#5407,#5405,#1106,.T.);
#7809=EDGE_CURVE('',#5408,#5409,#3419,.T.);
#7810=EDGE_CURVE('',#5410,#5408,#1107,.T.);
#7811=EDGE_CURVE('',#5404,#5410,#1108,.T.);
#7812=EDGE_CURVE('',#5405,#5411,#1109,.T.);
#7813=EDGE_CURVE('',#5411,#5409,#1110,.T.);
#7814=EDGE_CURVE('',#5412,#5413,#3420,.T.);
#7815=EDGE_CURVE('',#5414,#5412,#1111,.T.);
#7816=EDGE_CURVE('',#5408,#5414,#1112,.T.);
#7817=EDGE_CURVE('',#5409,#5415,#1113,.T.);
#7818=EDGE_CURVE('',#5415,#5413,#1114,.T.);
#7819=EDGE_CURVE('',#5416,#5417,#3421,.T.);
#7820=EDGE_CURVE('',#5418,#5416,#1115,.T.);
#7821=EDGE_CURVE('',#5412,#5418,#1116,.T.);
#7822=EDGE_CURVE('',#5413,#5419,#1117,.T.);
#7823=EDGE_CURVE('',#5419,#5417,#1118,.T.);
#7824=EDGE_CURVE('',#5420,#5421,#3422,.T.);
#7825=EDGE_CURVE('',#5422,#5420,#1119,.T.);
#7826=EDGE_CURVE('',#5416,#5422,#1120,.T.);
#7827=EDGE_CURVE('',#5417,#5423,#1121,.T.);
#7828=EDGE_CURVE('',#5423,#5421,#1122,.T.);
#7829=EDGE_CURVE('',#5424,#5425,#3423,.T.);
#7830=EDGE_CURVE('',#5426,#5424,#1123,.T.);
#7831=EDGE_CURVE('',#5420,#5426,#1124,.T.);
#7832=EDGE_CURVE('',#5421,#5427,#1125,.T.);
#7833=EDGE_CURVE('',#5427,#5425,#1126,.T.);
#7834=EDGE_CURVE('',#5428,#5429,#1127,.T.);
#7835=EDGE_CURVE('',#5430,#5429,#4177,.F.);
#7836=EDGE_CURVE('',#5430,#5431,#1128,.T.);
#7837=EDGE_CURVE('',#5431,#5432,#1129,.T.);
#7838=EDGE_CURVE('',#5432,#5433,#1130,.T.);
#7839=EDGE_CURVE('',#5433,#5434,#1131,.T.);
#7840=EDGE_CURVE('',#5434,#5435,#1132,.T.);
#7841=EDGE_CURVE('',#5435,#5436,#1133,.T.);
#7842=EDGE_CURVE('',#5436,#5437,#1134,.T.);
#7843=EDGE_CURVE('',#5437,#5438,#1135,.T.);
#7844=EDGE_CURVE('',#5438,#5439,#1136,.T.);
#7845=EDGE_CURVE('',#5439,#5440,#1137,.T.);
#7846=EDGE_CURVE('',#5440,#5441,#1138,.T.);
#7847=EDGE_CURVE('',#5441,#5442,#1139,.T.);
#7848=EDGE_CURVE('',#5442,#5443,#1140,.T.);
#7849=EDGE_CURVE('',#5443,#5444,#1141,.T.);
#7850=EDGE_CURVE('',#5444,#5445,#1142,.T.);
#7851=EDGE_CURVE('',#5445,#5446,#1143,.T.);
#7852=EDGE_CURVE('',#5446,#5447,#1144,.T.);
#7853=EDGE_CURVE('',#5447,#5448,#1145,.T.);
#7854=EDGE_CURVE('',#5448,#5449,#1146,.T.);
#7855=EDGE_CURVE('',#5449,#5450,#1147,.T.);
#7856=EDGE_CURVE('',#5450,#5451,#1148,.T.);
#7857=EDGE_CURVE('',#5451,#5452,#1149,.T.);
#7858=EDGE_CURVE('',#5452,#5453,#1150,.T.);
#7859=EDGE_CURVE('',#5453,#5454,#1151,.T.);
#7860=EDGE_CURVE('',#5454,#5455,#1152,.T.);
#7861=EDGE_CURVE('',#5455,#5456,#1153,.T.);
#7862=EDGE_CURVE('',#5456,#5457,#1154,.T.);
#7863=EDGE_CURVE('',#5457,#5458,#1155,.T.);
#7864=EDGE_CURVE('',#5458,#5459,#1156,.T.);
#7865=EDGE_CURVE('',#5459,#5460,#1157,.T.);
#7866=EDGE_CURVE('',#5460,#5461,#1158,.T.);
#7867=EDGE_CURVE('',#5461,#5462,#1159,.T.);
#7868=EDGE_CURVE('',#5462,#5463,#1160,.T.);
#7869=EDGE_CURVE('',#5463,#5464,#1161,.T.);
#7870=EDGE_CURVE('',#5464,#5465,#1162,.T.);
#7871=EDGE_CURVE('',#5465,#5466,#1163,.T.);
#7872=EDGE_CURVE('',#5466,#5467,#1164,.T.);
#7873=EDGE_CURVE('',#5467,#5468,#1165,.T.);
#7874=EDGE_CURVE('',#5468,#5469,#1166,.T.);
#7875=EDGE_CURVE('',#5469,#5470,#1167,.T.);
#7876=EDGE_CURVE('',#5470,#5471,#1168,.T.);
#7877=EDGE_CURVE('',#5471,#5472,#1169,.T.);
#7878=EDGE_CURVE('',#5472,#5473,#1170,.T.);
#7879=EDGE_CURVE('',#5473,#5474,#1171,.T.);
#7880=EDGE_CURVE('',#5474,#5475,#1172,.T.);
#7881=EDGE_CURVE('',#5475,#5476,#1173,.T.);
#7882=EDGE_CURVE('',#5476,#5477,#1174,.T.);
#7883=EDGE_CURVE('',#5477,#5478,#1175,.T.);
#7884=EDGE_CURVE('',#5478,#5479,#1176,.T.);
#7885=EDGE_CURVE('',#5479,#5480,#1177,.T.);
#7886=EDGE_CURVE('',#5480,#5481,#1178,.T.);
#7887=EDGE_CURVE('',#5481,#5482,#1179,.T.);
#7888=EDGE_CURVE('',#5482,#5483,#1180,.T.);
#7889=EDGE_CURVE('',#5483,#5484,#1181,.T.);
#7890=EDGE_CURVE('',#5484,#5485,#1182,.T.);
#7891=EDGE_CURVE('',#5485,#5486,#1183,.T.);
#7892=EDGE_CURVE('',#5486,#5487,#1184,.T.);
#7893=EDGE_CURVE('',#5487,#5488,#1185,.T.);
#7894=EDGE_CURVE('',#5488,#5489,#1186,.T.);
#7895=EDGE_CURVE('',#5489,#5490,#1187,.T.);
#7896=EDGE_CURVE('',#5490,#5491,#1188,.T.);
#7897=EDGE_CURVE('',#5491,#5492,#1189,.T.);
#7898=EDGE_CURVE('',#5492,#5493,#1190,.T.);
#7899=EDGE_CURVE('',#5493,#5494,#1191,.T.);
#7900=EDGE_CURVE('',#5494,#5495,#1192,.T.);
#7901=EDGE_CURVE('',#5495,#5496,#1193,.T.);
#7902=EDGE_CURVE('',#5496,#5497,#1194,.T.);
#7903=EDGE_CURVE('',#5497,#5498,#1195,.T.);
#7904=EDGE_CURVE('',#5498,#5499,#1196,.T.);
#7905=EDGE_CURVE('',#5499,#5500,#1197,.T.);
#7906=EDGE_CURVE('',#5500,#5501,#1198,.T.);
#7907=EDGE_CURVE('',#5501,#5502,#1199,.T.);
#7908=EDGE_CURVE('',#5502,#5503,#1200,.T.);
#7909=EDGE_CURVE('',#5503,#5504,#1201,.T.);
#7910=EDGE_CURVE('',#5504,#5505,#1202,.T.);
#7911=EDGE_CURVE('',#5505,#5506,#1203,.T.);
#7912=EDGE_CURVE('',#5506,#5507,#1204,.T.);
#7913=EDGE_CURVE('',#5507,#5508,#1205,.T.);
#7914=EDGE_CURVE('',#5508,#5509,#1206,.T.);
#7915=EDGE_CURVE('',#5509,#5510,#1207,.T.);
#7916=EDGE_CURVE('',#5510,#5511,#1208,.T.);
#7917=EDGE_CURVE('',#5511,#5512,#1209,.T.);
#7918=EDGE_CURVE('',#5512,#5513,#1210,.T.);
#7919=EDGE_CURVE('',#5513,#5514,#1211,.T.);
#7920=EDGE_CURVE('',#5514,#5515,#1212,.T.);
#7921=EDGE_CURVE('',#5515,#5516,#1213,.T.);
#7922=EDGE_CURVE('',#5516,#5517,#1214,.T.);
#7923=EDGE_CURVE('',#5517,#5518,#1215,.T.);
#7924=EDGE_CURVE('',#5518,#5519,#1216,.T.);
#7925=EDGE_CURVE('',#5519,#5520,#1217,.T.);
#7926=EDGE_CURVE('',#5520,#5521,#1218,.T.);
#7927=EDGE_CURVE('',#5521,#5522,#1219,.T.);
#7928=EDGE_CURVE('',#5522,#5523,#1220,.T.);
#7929=EDGE_CURVE('',#5523,#5524,#1221,.T.);
#7930=EDGE_CURVE('',#5524,#5525,#1222,.T.);
#7931=EDGE_CURVE('',#5525,#5526,#1223,.T.);
#7932=EDGE_CURVE('',#5526,#5527,#1224,.T.);
#7933=EDGE_CURVE('',#5527,#5528,#1225,.T.);
#7934=EDGE_CURVE('',#5528,#5529,#1226,.T.);
#7935=EDGE_CURVE('',#5529,#5530,#1227,.T.);
#7936=EDGE_CURVE('',#5530,#5531,#1228,.T.);
#7937=EDGE_CURVE('',#5531,#5532,#1229,.T.);
#7938=EDGE_CURVE('',#5532,#5533,#1230,.T.);
#7939=EDGE_CURVE('',#5533,#5534,#1231,.T.);
#7940=EDGE_CURVE('',#5534,#5535,#1232,.T.);
#7941=EDGE_CURVE('',#5535,#5536,#1233,.T.);
#7942=EDGE_CURVE('',#5536,#5537,#1234,.T.);
#7943=EDGE_CURVE('',#5537,#5538,#1235,.T.);
#7944=EDGE_CURVE('',#5538,#5539,#1236,.T.);
#7945=EDGE_CURVE('',#5539,#5540,#1237,.T.);
#7946=EDGE_CURVE('',#5540,#5541,#1238,.T.);
#7947=EDGE_CURVE('',#5541,#5542,#1239,.T.);
#7948=EDGE_CURVE('',#5542,#5543,#1240,.T.);
#7949=EDGE_CURVE('',#5543,#5544,#1241,.T.);
#7950=EDGE_CURVE('',#5544,#5545,#1242,.T.);
#7951=EDGE_CURVE('',#5545,#5546,#1243,.T.);
#7952=EDGE_CURVE('',#5546,#5547,#1244,.T.);
#7953=EDGE_CURVE('',#5547,#5548,#1245,.T.);
#7954=EDGE_CURVE('',#5548,#5549,#1246,.T.);
#7955=EDGE_CURVE('',#5549,#5550,#1247,.T.);
#7956=EDGE_CURVE('',#5550,#5551,#1248,.T.);
#7957=EDGE_CURVE('',#5551,#5552,#1249,.T.);
#7958=EDGE_CURVE('',#5552,#5553,#1250,.T.);
#7959=EDGE_CURVE('',#5553,#5554,#1251,.T.);
#7960=EDGE_CURVE('',#5554,#5555,#1252,.T.);
#7961=EDGE_CURVE('',#5555,#5556,#1253,.T.);
#7962=EDGE_CURVE('',#5556,#5557,#1254,.T.);
#7963=EDGE_CURVE('',#5557,#5558,#1255,.T.);
#7964=EDGE_CURVE('',#5558,#5559,#1256,.T.);
#7965=EDGE_CURVE('',#5559,#5560,#1257,.T.);
#7966=EDGE_CURVE('',#5560,#5561,#1258,.T.);
#7967=EDGE_CURVE('',#5561,#5562,#1259,.T.);
#7968=EDGE_CURVE('',#5562,#5563,#1260,.T.);
#7969=EDGE_CURVE('',#5563,#5564,#1261,.T.);
#7970=EDGE_CURVE('',#5564,#5565,#1262,.T.);
#7971=EDGE_CURVE('',#5565,#5566,#1263,.T.);
#7972=EDGE_CURVE('',#5566,#5567,#1264,.T.);
#7973=EDGE_CURVE('',#5567,#5568,#1265,.T.);
#7974=EDGE_CURVE('',#5568,#5569,#1266,.T.);
#7975=EDGE_CURVE('',#5569,#5570,#1267,.T.);
#7976=EDGE_CURVE('',#5570,#5571,#1268,.T.);
#7977=EDGE_CURVE('',#5571,#5572,#1269,.T.);
#7978=EDGE_CURVE('',#5572,#5573,#1270,.T.);
#7979=EDGE_CURVE('',#5573,#5574,#1271,.T.);
#7980=EDGE_CURVE('',#5574,#5575,#1272,.T.);
#7981=EDGE_CURVE('',#5575,#5576,#1273,.T.);
#7982=EDGE_CURVE('',#5576,#5577,#1274,.T.);
#7983=EDGE_CURVE('',#5577,#5578,#1275,.T.);
#7984=EDGE_CURVE('',#5578,#5579,#1276,.T.);
#7985=EDGE_CURVE('',#5579,#5580,#1277,.T.);
#7986=EDGE_CURVE('',#5580,#5581,#1278,.T.);
#7987=EDGE_CURVE('',#5581,#5582,#1279,.T.);
#7988=EDGE_CURVE('',#5582,#5583,#1280,.T.);
#7989=EDGE_CURVE('',#5583,#5584,#1281,.T.);
#7990=EDGE_CURVE('',#5584,#5585,#1282,.T.);
#7991=EDGE_CURVE('',#5585,#5586,#1283,.T.);
#7992=EDGE_CURVE('',#5586,#5587,#1284,.T.);
#7993=EDGE_CURVE('',#5587,#5588,#1285,.T.);
#7994=EDGE_CURVE('',#5588,#5589,#1286,.T.);
#7995=EDGE_CURVE('',#5589,#5590,#1287,.T.);
#7996=EDGE_CURVE('',#5590,#5591,#1288,.T.);
#7997=EDGE_CURVE('',#5591,#5592,#1289,.T.);
#7998=EDGE_CURVE('',#5592,#5593,#1290,.T.);
#7999=EDGE_CURVE('',#5593,#5594,#1291,.T.);
#8000=EDGE_CURVE('',#5594,#5595,#1292,.T.);
#8001=EDGE_CURVE('',#5595,#5596,#1293,.T.);
#8002=EDGE_CURVE('',#5596,#5597,#1294,.T.);
#8003=EDGE_CURVE('',#5597,#5598,#1295,.T.);
#8004=EDGE_CURVE('',#5598,#5599,#1296,.T.);
#8005=EDGE_CURVE('',#5599,#5600,#1297,.T.);
#8006=EDGE_CURVE('',#5600,#5601,#1298,.T.);
#8007=EDGE_CURVE('',#5601,#5602,#1299,.T.);
#8008=EDGE_CURVE('',#5602,#5603,#1300,.T.);
#8009=EDGE_CURVE('',#5603,#5604,#1301,.T.);
#8010=EDGE_CURVE('',#5604,#5605,#1302,.T.);
#8011=EDGE_CURVE('',#5605,#5606,#1303,.T.);
#8012=EDGE_CURVE('',#5606,#5607,#1304,.T.);
#8013=EDGE_CURVE('',#5607,#5608,#1305,.T.);
#8014=EDGE_CURVE('',#5608,#5609,#1306,.T.);
#8015=EDGE_CURVE('',#5609,#5610,#1307,.T.);
#8016=EDGE_CURVE('',#5610,#5611,#1308,.T.);
#8017=EDGE_CURVE('',#5611,#5612,#1309,.T.);
#8018=EDGE_CURVE('',#5612,#5613,#1310,.T.);
#8019=EDGE_CURVE('',#5613,#5614,#1311,.T.);
#8020=EDGE_CURVE('',#5614,#5615,#1312,.T.);
#8021=EDGE_CURVE('',#5615,#5616,#1313,.T.);
#8022=EDGE_CURVE('',#5616,#5617,#1314,.T.);
#8023=EDGE_CURVE('',#5617,#5618,#1315,.T.);
#8024=EDGE_CURVE('',#5618,#5619,#1316,.T.);
#8025=EDGE_CURVE('',#5619,#5620,#1317,.T.);
#8026=EDGE_CURVE('',#5620,#5621,#1318,.T.);
#8027=EDGE_CURVE('',#5621,#5622,#1319,.T.);
#8028=EDGE_CURVE('',#5622,#5623,#1320,.T.);
#8029=EDGE_CURVE('',#5623,#5624,#1321,.T.);
#8030=EDGE_CURVE('',#5624,#5625,#1322,.T.);
#8031=EDGE_CURVE('',#5625,#5626,#1323,.T.);
#8032=EDGE_CURVE('',#5626,#5627,#1324,.T.);
#8033=EDGE_CURVE('',#5627,#5628,#1325,.T.);
#8034=EDGE_CURVE('',#5628,#5629,#1326,.T.);
#8035=EDGE_CURVE('',#5629,#5630,#1327,.T.);
#8036=EDGE_CURVE('',#5630,#5631,#1328,.T.);
#8037=EDGE_CURVE('',#5631,#5632,#1329,.T.);
#8038=EDGE_CURVE('',#5632,#5633,#1330,.T.);
#8039=EDGE_CURVE('',#5633,#5634,#1331,.T.);
#8040=EDGE_CURVE('',#5634,#5635,#1332,.T.);
#8041=EDGE_CURVE('',#5635,#5636,#1333,.T.);
#8042=EDGE_CURVE('',#5636,#5637,#1334,.T.);
#8043=EDGE_CURVE('',#5637,#5638,#1335,.T.);
#8044=EDGE_CURVE('',#5638,#5639,#1336,.T.);
#8045=EDGE_CURVE('',#5639,#5640,#1337,.T.);
#8046=EDGE_CURVE('',#5640,#5641,#1338,.T.);
#8047=EDGE_CURVE('',#5641,#5642,#1339,.T.);
#8048=EDGE_CURVE('',#5642,#5643,#1340,.T.);
#8049=EDGE_CURVE('',#5643,#5644,#1341,.T.);
#8050=EDGE_CURVE('',#5644,#5645,#1342,.T.);
#8051=EDGE_CURVE('',#5645,#5646,#1343,.T.);
#8052=EDGE_CURVE('',#5646,#5647,#1344,.T.);
#8053=EDGE_CURVE('',#5647,#5648,#1345,.T.);
#8054=EDGE_CURVE('',#5648,#5649,#1346,.T.);
#8055=EDGE_CURVE('',#5649,#5650,#1347,.T.);
#8056=EDGE_CURVE('',#5650,#5651,#1348,.T.);
#8057=EDGE_CURVE('',#5651,#5652,#1349,.T.);
#8058=EDGE_CURVE('',#5652,#5653,#1350,.T.);
#8059=EDGE_CURVE('',#5653,#5654,#1351,.T.);
#8060=EDGE_CURVE('',#5654,#5655,#1352,.T.);
#8061=EDGE_CURVE('',#5655,#5656,#1353,.T.);
#8062=EDGE_CURVE('',#5656,#5657,#1354,.T.);
#8063=EDGE_CURVE('',#5657,#5658,#1355,.T.);
#8064=EDGE_CURVE('',#5658,#5659,#1356,.T.);
#8065=EDGE_CURVE('',#5659,#5660,#1357,.T.);
#8066=EDGE_CURVE('',#5660,#5661,#1358,.T.);
#8067=EDGE_CURVE('',#5661,#5662,#1359,.T.);
#8068=EDGE_CURVE('',#5662,#5663,#1360,.T.);
#8069=EDGE_CURVE('',#5663,#5664,#1361,.T.);
#8070=EDGE_CURVE('',#5664,#5665,#1362,.T.);
#8071=EDGE_CURVE('',#5665,#5666,#1363,.T.);
#8072=EDGE_CURVE('',#5666,#5667,#1364,.T.);
#8073=EDGE_CURVE('',#5667,#5668,#1365,.T.);
#8074=EDGE_CURVE('',#5668,#5669,#1366,.T.);
#8075=EDGE_CURVE('',#5669,#5670,#1367,.T.);
#8076=EDGE_CURVE('',#5670,#5671,#1368,.T.);
#8077=EDGE_CURVE('',#5671,#5672,#1369,.T.);
#8078=EDGE_CURVE('',#5672,#5673,#1370,.T.);
#8079=EDGE_CURVE('',#5673,#5674,#1371,.T.);
#8080=EDGE_CURVE('',#5674,#5675,#1372,.T.);
#8081=EDGE_CURVE('',#5675,#5676,#1373,.T.);
#8082=EDGE_CURVE('',#5676,#5677,#1374,.T.);
#8083=EDGE_CURVE('',#5677,#5678,#1375,.T.);
#8084=EDGE_CURVE('',#5678,#5679,#1376,.T.);
#8085=EDGE_CURVE('',#5679,#5680,#1377,.T.);
#8086=EDGE_CURVE('',#5680,#5681,#1378,.T.);
#8087=EDGE_CURVE('',#5681,#5682,#1379,.T.);
#8088=EDGE_CURVE('',#5682,#5683,#1380,.T.);
#8089=EDGE_CURVE('',#5683,#5684,#1381,.T.);
#8090=EDGE_CURVE('',#5684,#5685,#1382,.T.);
#8091=EDGE_CURVE('',#5685,#5686,#1383,.T.);
#8092=EDGE_CURVE('',#5686,#5687,#1384,.T.);
#8093=EDGE_CURVE('',#5687,#5688,#1385,.T.);
#8094=EDGE_CURVE('',#5688,#5689,#1386,.T.);
#8095=EDGE_CURVE('',#5689,#5690,#1387,.T.);
#8096=EDGE_CURVE('',#5690,#5691,#1388,.T.);
#8097=EDGE_CURVE('',#5691,#5692,#1389,.T.);
#8098=EDGE_CURVE('',#5692,#5693,#1390,.T.);
#8099=EDGE_CURVE('',#5693,#5694,#1391,.T.);
#8100=EDGE_CURVE('',#5694,#5695,#1392,.T.);
#8101=EDGE_CURVE('',#5695,#5696,#1393,.T.);
#8102=EDGE_CURVE('',#5696,#5697,#1394,.T.);
#8103=EDGE_CURVE('',#5697,#5698,#1395,.T.);
#8104=EDGE_CURVE('',#5698,#5699,#1396,.T.);
#8105=EDGE_CURVE('',#5699,#5700,#1397,.T.);
#8106=EDGE_CURVE('',#5701,#5700,#4178,.T.);
#8107=EDGE_CURVE('',#5701,#5702,#1398,.T.);
#8108=EDGE_CURVE('',#5702,#5703,#1399,.T.);
#8109=EDGE_CURVE('',#5703,#5704,#1400,.T.);
#8110=EDGE_CURVE('',#5704,#5705,#1401,.T.);
#8111=EDGE_CURVE('',#5705,#5706,#1402,.T.);
#8112=EDGE_CURVE('',#5706,#5707,#1403,.T.);
#8113=EDGE_CURVE('',#5707,#5708,#1404,.T.);
#8114=EDGE_CURVE('',#5708,#5709,#1405,.T.);
#8115=EDGE_CURVE('',#5709,#5710,#1406,.T.);
#8116=EDGE_CURVE('',#5710,#5711,#1407,.T.);
#8117=EDGE_CURVE('',#5711,#5712,#1408,.T.);
#8118=EDGE_CURVE('',#5712,#5713,#1409,.T.);
#8119=EDGE_CURVE('',#5713,#5714,#1410,.T.);
#8120=EDGE_CURVE('',#5714,#5715,#1411,.T.);
#8121=EDGE_CURVE('',#5715,#5716,#1412,.T.);
#8122=EDGE_CURVE('',#5716,#5717,#1413,.T.);
#8123=EDGE_CURVE('',#5717,#5718,#1414,.T.);
#8124=EDGE_CURVE('',#5718,#5719,#1415,.T.);
#8125=EDGE_CURVE('',#5719,#5720,#1416,.T.);
#8126=EDGE_CURVE('',#5720,#5721,#1417,.T.);
#8127=EDGE_CURVE('',#5721,#5722,#1418,.T.);
#8128=EDGE_CURVE('',#5722,#5723,#1419,.T.);
#8129=EDGE_CURVE('',#5723,#5724,#1420,.T.);
#8130=EDGE_CURVE('',#5724,#5725,#1421,.T.);
#8131=EDGE_CURVE('',#5725,#5726,#1422,.T.);
#8132=EDGE_CURVE('',#5726,#5727,#1423,.T.);
#8133=EDGE_CURVE('',#5727,#5728,#1424,.T.);
#8134=EDGE_CURVE('',#5728,#5729,#1425,.T.);
#8135=EDGE_CURVE('',#5729,#5730,#1426,.T.);
#8136=EDGE_CURVE('',#5730,#5731,#1427,.T.);
#8137=EDGE_CURVE('',#5731,#5732,#1428,.T.);
#8138=EDGE_CURVE('',#5732,#5733,#1429,.T.);
#8139=EDGE_CURVE('',#5733,#5734,#1430,.T.);
#8140=EDGE_CURVE('',#5734,#5735,#1431,.T.);
#8141=EDGE_CURVE('',#5735,#5736,#1432,.T.);
#8142=EDGE_CURVE('',#5736,#5737,#1433,.T.);
#8143=EDGE_CURVE('',#5737,#5738,#1434,.T.);
#8144=EDGE_CURVE('',#5738,#5739,#1435,.T.);
#8145=EDGE_CURVE('',#5739,#5740,#1436,.T.);
#8146=EDGE_CURVE('',#5740,#5741,#1437,.T.);
#8147=EDGE_CURVE('',#5741,#5742,#1438,.T.);
#8148=EDGE_CURVE('',#5742,#5743,#1439,.T.);
#8149=EDGE_CURVE('',#5743,#5744,#1440,.T.);
#8150=EDGE_CURVE('',#5744,#5745,#1441,.T.);
#8151=EDGE_CURVE('',#5745,#5746,#1442,.T.);
#8152=EDGE_CURVE('',#5746,#5747,#1443,.T.);
#8153=EDGE_CURVE('',#5747,#5748,#1444,.T.);
#8154=EDGE_CURVE('',#5748,#5749,#1445,.T.);
#8155=EDGE_CURVE('',#5749,#5750,#1446,.T.);
#8156=EDGE_CURVE('',#5750,#5751,#1447,.T.);
#8157=EDGE_CURVE('',#5751,#5752,#1448,.T.);
#8158=EDGE_CURVE('',#5752,#5753,#1449,.T.);
#8159=EDGE_CURVE('',#5753,#5754,#1450,.T.);
#8160=EDGE_CURVE('',#5754,#5755,#1451,.T.);
#8161=EDGE_CURVE('',#5755,#5756,#1452,.T.);
#8162=EDGE_CURVE('',#5756,#5757,#1453,.T.);
#8163=EDGE_CURVE('',#5757,#5758,#1454,.T.);
#8164=EDGE_CURVE('',#5758,#5759,#1455,.T.);
#8165=EDGE_CURVE('',#5759,#5760,#1456,.T.);
#8166=EDGE_CURVE('',#5760,#5761,#1457,.T.);
#8167=EDGE_CURVE('',#5761,#5762,#1458,.T.);
#8168=EDGE_CURVE('',#5762,#5763,#1459,.T.);
#8169=EDGE_CURVE('',#5763,#5764,#1460,.T.);
#8170=EDGE_CURVE('',#5764,#5765,#1461,.T.);
#8171=EDGE_CURVE('',#5765,#5766,#1462,.T.);
#8172=EDGE_CURVE('',#5766,#5767,#1463,.T.);
#8173=EDGE_CURVE('',#5767,#5768,#1464,.T.);
#8174=EDGE_CURVE('',#5768,#5769,#1465,.T.);
#8175=EDGE_CURVE('',#5769,#5770,#1466,.T.);
#8176=EDGE_CURVE('',#5770,#5771,#1467,.T.);
#8177=EDGE_CURVE('',#5771,#5772,#1468,.T.);
#8178=EDGE_CURVE('',#5772,#5773,#1469,.T.);
#8179=EDGE_CURVE('',#5773,#5774,#1470,.T.);
#8180=EDGE_CURVE('',#5774,#5775,#1471,.T.);
#8181=EDGE_CURVE('',#5775,#5776,#1472,.T.);
#8182=EDGE_CURVE('',#5776,#5777,#1473,.T.);
#8183=EDGE_CURVE('',#5777,#5778,#1474,.T.);
#8184=EDGE_CURVE('',#5778,#5779,#1475,.T.);
#8185=EDGE_CURVE('',#5779,#5780,#1476,.T.);
#8186=EDGE_CURVE('',#5780,#5781,#1477,.T.);
#8187=EDGE_CURVE('',#5781,#5782,#1478,.T.);
#8188=EDGE_CURVE('',#5782,#5783,#1479,.T.);
#8189=EDGE_CURVE('',#5783,#5784,#1480,.T.);
#8190=EDGE_CURVE('',#5784,#5785,#1481,.T.);
#8191=EDGE_CURVE('',#5785,#5786,#1482,.T.);
#8192=EDGE_CURVE('',#5786,#5787,#1483,.T.);
#8193=EDGE_CURVE('',#5787,#5788,#1484,.T.);
#8194=EDGE_CURVE('',#5788,#5789,#1485,.T.);
#8195=EDGE_CURVE('',#5789,#5790,#1486,.T.);
#8196=EDGE_CURVE('',#5790,#5791,#1487,.T.);
#8197=EDGE_CURVE('',#5791,#5792,#1488,.T.);
#8198=EDGE_CURVE('',#5792,#5793,#1489,.T.);
#8199=EDGE_CURVE('',#5793,#5794,#1490,.T.);
#8200=EDGE_CURVE('',#5794,#5795,#1491,.T.);
#8201=EDGE_CURVE('',#5795,#5796,#1492,.T.);
#8202=EDGE_CURVE('',#5796,#5797,#1493,.T.);
#8203=EDGE_CURVE('',#5797,#5798,#1494,.T.);
#8204=EDGE_CURVE('',#5798,#5799,#1495,.T.);
#8205=EDGE_CURVE('',#5799,#5800,#1496,.T.);
#8206=EDGE_CURVE('',#5800,#5801,#1497,.T.);
#8207=EDGE_CURVE('',#5801,#5802,#1498,.T.);
#8208=EDGE_CURVE('',#5802,#5803,#1499,.T.);
#8209=EDGE_CURVE('',#5803,#5804,#1500,.T.);
#8210=EDGE_CURVE('',#5804,#5805,#1501,.T.);
#8211=EDGE_CURVE('',#5805,#5806,#1502,.T.);
#8212=EDGE_CURVE('',#5806,#5807,#1503,.T.);
#8213=EDGE_CURVE('',#5807,#5808,#1504,.T.);
#8214=EDGE_CURVE('',#5808,#5809,#1505,.T.);
#8215=EDGE_CURVE('',#5809,#5810,#1506,.T.);
#8216=EDGE_CURVE('',#5810,#5811,#1507,.T.);
#8217=EDGE_CURVE('',#5811,#5812,#1508,.T.);
#8218=EDGE_CURVE('',#5812,#5813,#1509,.T.);
#8219=EDGE_CURVE('',#5813,#5814,#1510,.T.);
#8220=EDGE_CURVE('',#5814,#5815,#1511,.T.);
#8221=EDGE_CURVE('',#5815,#5816,#1512,.T.);
#8222=EDGE_CURVE('',#5816,#5817,#1513,.T.);
#8223=EDGE_CURVE('',#5817,#5818,#1514,.T.);
#8224=EDGE_CURVE('',#5818,#5819,#1515,.T.);
#8225=EDGE_CURVE('',#5819,#5820,#1516,.T.);
#8226=EDGE_CURVE('',#5820,#5821,#1517,.T.);
#8227=EDGE_CURVE('',#5821,#5822,#1518,.T.);
#8228=EDGE_CURVE('',#5822,#5823,#1519,.T.);
#8229=EDGE_CURVE('',#5823,#5824,#1520,.T.);
#8230=EDGE_CURVE('',#5824,#5825,#1521,.T.);
#8231=EDGE_CURVE('',#5825,#5826,#1522,.T.);
#8232=EDGE_CURVE('',#5826,#5827,#1523,.T.);
#8233=EDGE_CURVE('',#5827,#5828,#1524,.T.);
#8234=EDGE_CURVE('',#5828,#5829,#1525,.T.);
#8235=EDGE_CURVE('',#5829,#5830,#1526,.T.);
#8236=EDGE_CURVE('',#5830,#5831,#1527,.T.);
#8237=EDGE_CURVE('',#5831,#5832,#1528,.T.);
#8238=EDGE_CURVE('',#5832,#5833,#1529,.T.);
#8239=EDGE_CURVE('',#5833,#5834,#1530,.T.);
#8240=EDGE_CURVE('',#5834,#5835,#1531,.T.);
#8241=EDGE_CURVE('',#5835,#5836,#1532,.T.);
#8242=EDGE_CURVE('',#5836,#5837,#1533,.T.);
#8243=EDGE_CURVE('',#5837,#5838,#1534,.T.);
#8244=EDGE_CURVE('',#5838,#5839,#1535,.T.);
#8245=EDGE_CURVE('',#5839,#5840,#1536,.T.);
#8246=EDGE_CURVE('',#5840,#5841,#1537,.T.);
#8247=EDGE_CURVE('',#5841,#5842,#1538,.T.);
#8248=EDGE_CURVE('',#5842,#5843,#1539,.T.);
#8249=EDGE_CURVE('',#5843,#5844,#1540,.T.);
#8250=EDGE_CURVE('',#5844,#5845,#1541,.T.);
#8251=EDGE_CURVE('',#5845,#5846,#1542,.T.);
#8252=EDGE_CURVE('',#5846,#5847,#1543,.T.);
#8253=EDGE_CURVE('',#5847,#5848,#1544,.T.);
#8254=EDGE_CURVE('',#5848,#5849,#1545,.T.);
#8255=EDGE_CURVE('',#5849,#5850,#1546,.T.);
#8256=EDGE_CURVE('',#5850,#5851,#1547,.T.);
#8257=EDGE_CURVE('',#5851,#5852,#1548,.T.);
#8258=EDGE_CURVE('',#5852,#5853,#1549,.T.);
#8259=EDGE_CURVE('',#5853,#5854,#1550,.T.);
#8260=EDGE_CURVE('',#5854,#5855,#1551,.T.);
#8261=EDGE_CURVE('',#5855,#5856,#1552,.T.);
#8262=EDGE_CURVE('',#5856,#5857,#1553,.T.);
#8263=EDGE_CURVE('',#5857,#5858,#1554,.T.);
#8264=EDGE_CURVE('',#5858,#5859,#1555,.T.);
#8265=EDGE_CURVE('',#5859,#5860,#1556,.T.);
#8266=EDGE_CURVE('',#5860,#5861,#1557,.T.);
#8267=EDGE_CURVE('',#5861,#5862,#1558,.T.);
#8268=EDGE_CURVE('',#5862,#5863,#1559,.T.);
#8269=EDGE_CURVE('',#5863,#5864,#1560,.T.);
#8270=EDGE_CURVE('',#5864,#5865,#1561,.T.);
#8271=EDGE_CURVE('',#5865,#5866,#1562,.T.);
#8272=EDGE_CURVE('',#5866,#5867,#1563,.T.);
#8273=EDGE_CURVE('',#5867,#5868,#1564,.T.);
#8274=EDGE_CURVE('',#5868,#5869,#1565,.T.);
#8275=EDGE_CURVE('',#5869,#5870,#1566,.T.);
#8276=EDGE_CURVE('',#5870,#5871,#1567,.T.);
#8277=EDGE_CURVE('',#5871,#5872,#1568,.T.);
#8278=EDGE_CURVE('',#5872,#5873,#1569,.T.);
#8279=EDGE_CURVE('',#5873,#5874,#1570,.T.);
#8280=EDGE_CURVE('',#5874,#5875,#1571,.T.);
#8281=EDGE_CURVE('',#5875,#5876,#1572,.T.);
#8282=EDGE_CURVE('',#5876,#5877,#1573,.T.);
#8283=EDGE_CURVE('',#5877,#5878,#1574,.T.);
#8284=EDGE_CURVE('',#5878,#5879,#1575,.T.);
#8285=EDGE_CURVE('',#5879,#5880,#1576,.T.);
#8286=EDGE_CURVE('',#5880,#5881,#1577,.T.);
#8287=EDGE_CURVE('',#5881,#5882,#1578,.T.);
#8288=EDGE_CURVE('',#5882,#5883,#1579,.T.);
#8289=EDGE_CURVE('',#5883,#5884,#1580,.T.);
#8290=EDGE_CURVE('',#5884,#5885,#1581,.T.);
#8291=EDGE_CURVE('',#5885,#5886,#1582,.T.);
#8292=EDGE_CURVE('',#5886,#5887,#1583,.T.);
#8293=EDGE_CURVE('',#5887,#5888,#1584,.T.);
#8294=EDGE_CURVE('',#5888,#5889,#1585,.T.);
#8295=EDGE_CURVE('',#5889,#5890,#1586,.T.);
#8296=EDGE_CURVE('',#5890,#5891,#1587,.T.);
#8297=EDGE_CURVE('',#5891,#5892,#1588,.T.);
#8298=EDGE_CURVE('',#5892,#5893,#1589,.T.);
#8299=EDGE_CURVE('',#5893,#5894,#1590,.T.);
#8300=EDGE_CURVE('',#5894,#5895,#1591,.T.);
#8301=EDGE_CURVE('',#5895,#5896,#1592,.T.);
#8302=EDGE_CURVE('',#5896,#5897,#1593,.T.);
#8303=EDGE_CURVE('',#5897,#5898,#1594,.T.);
#8304=EDGE_CURVE('',#5898,#5899,#1595,.T.);
#8305=EDGE_CURVE('',#5899,#5900,#1596,.T.);
#8306=EDGE_CURVE('',#5900,#5901,#1597,.T.);
#8307=EDGE_CURVE('',#5901,#5902,#1598,.T.);
#8308=EDGE_CURVE('',#5902,#5903,#1599,.T.);
#8309=EDGE_CURVE('',#5903,#5904,#1600,.T.);
#8310=EDGE_CURVE('',#5904,#5905,#1601,.T.);
#8311=EDGE_CURVE('',#5905,#5906,#1602,.T.);
#8312=EDGE_CURVE('',#5906,#5907,#1603,.T.);
#8313=EDGE_CURVE('',#5907,#5908,#1604,.T.);
#8314=EDGE_CURVE('',#5908,#5909,#1605,.T.);
#8315=EDGE_CURVE('',#5909,#5910,#1606,.T.);
#8316=EDGE_CURVE('',#5910,#5911,#1607,.T.);
#8317=EDGE_CURVE('',#5911,#5912,#1608,.T.);
#8318=EDGE_CURVE('',#5912,#5913,#1609,.T.);
#8319=EDGE_CURVE('',#5913,#5914,#1610,.T.);
#8320=EDGE_CURVE('',#5914,#5915,#1611,.T.);
#8321=EDGE_CURVE('',#5915,#5916,#1612,.T.);
#8322=EDGE_CURVE('',#5916,#5917,#1613,.T.);
#8323=EDGE_CURVE('',#5917,#5918,#1614,.T.);
#8324=EDGE_CURVE('',#5918,#5919,#1615,.T.);
#8325=EDGE_CURVE('',#5919,#5920,#1616,.T.);
#8326=EDGE_CURVE('',#5920,#5921,#1617,.T.);
#8327=EDGE_CURVE('',#5921,#5922,#1618,.T.);
#8328=EDGE_CURVE('',#5922,#5923,#1619,.T.);
#8329=EDGE_CURVE('',#5923,#5924,#1620,.T.);
#8330=EDGE_CURVE('',#5924,#5925,#1621,.T.);
#8331=EDGE_CURVE('',#5925,#5926,#1622,.T.);
#8332=EDGE_CURVE('',#5926,#5927,#1623,.T.);
#8333=EDGE_CURVE('',#5927,#5928,#1624,.T.);
#8334=EDGE_CURVE('',#5928,#5929,#1625,.T.);
#8335=EDGE_CURVE('',#5929,#5930,#1626,.T.);
#8336=EDGE_CURVE('',#5930,#5931,#1627,.T.);
#8337=EDGE_CURVE('',#5931,#5932,#1628,.T.);
#8338=EDGE_CURVE('',#5932,#5933,#1629,.T.);
#8339=EDGE_CURVE('',#5933,#5934,#1630,.T.);
#8340=EDGE_CURVE('',#5934,#5935,#1631,.T.);
#8341=EDGE_CURVE('',#5935,#5936,#1632,.T.);
#8342=EDGE_CURVE('',#5936,#5937,#1633,.T.);
#8343=EDGE_CURVE('',#5937,#5938,#1634,.T.);
#8344=EDGE_CURVE('',#5938,#5939,#1635,.T.);
#8345=EDGE_CURVE('',#5939,#5940,#1636,.T.);
#8346=EDGE_CURVE('',#5940,#5941,#1637,.T.);
#8347=EDGE_CURVE('',#5941,#5942,#1638,.T.);
#8348=EDGE_CURVE('',#5942,#5943,#1639,.T.);
#8349=EDGE_CURVE('',#5943,#5944,#1640,.T.);
#8350=EDGE_CURVE('',#5944,#5945,#1641,.T.);
#8351=EDGE_CURVE('',#5945,#5946,#1642,.T.);
#8352=EDGE_CURVE('',#5946,#5947,#1643,.T.);
#8353=EDGE_CURVE('',#5947,#5948,#1644,.T.);
#8354=EDGE_CURVE('',#5948,#5949,#1645,.T.);
#8355=EDGE_CURVE('',#5949,#5950,#1646,.T.);
#8356=EDGE_CURVE('',#5950,#5951,#1647,.T.);
#8357=EDGE_CURVE('',#5951,#5952,#1648,.T.);
#8358=EDGE_CURVE('',#5952,#5953,#1649,.T.);
#8359=EDGE_CURVE('',#5953,#5954,#1650,.T.);
#8360=EDGE_CURVE('',#5954,#5955,#1651,.T.);
#8361=EDGE_CURVE('',#5955,#5956,#1652,.T.);
#8362=EDGE_CURVE('',#5956,#5957,#1653,.T.);
#8363=EDGE_CURVE('',#5957,#5958,#1654,.T.);
#8364=EDGE_CURVE('',#5958,#5959,#1655,.T.);
#8365=EDGE_CURVE('',#5959,#5960,#1656,.T.);
#8366=EDGE_CURVE('',#5960,#5961,#1657,.T.);
#8367=EDGE_CURVE('',#5961,#5962,#1658,.T.);
#8368=EDGE_CURVE('',#5962,#5963,#1659,.T.);
#8369=EDGE_CURVE('',#5963,#5964,#1660,.T.);
#8370=EDGE_CURVE('',#5964,#5965,#1661,.T.);
#8371=EDGE_CURVE('',#5965,#5966,#1662,.T.);
#8372=EDGE_CURVE('',#5966,#5967,#1663,.T.);
#8373=EDGE_CURVE('',#5967,#5968,#1664,.T.);
#8374=EDGE_CURVE('',#5968,#5969,#1665,.T.);
#8375=EDGE_CURVE('',#5969,#5428,#1666,.T.);
#8376=EDGE_CURVE('',#5425,#5970,#1667,.T.);
#8377=EDGE_CURVE('',#5970,#5971,#1668,.T.);
#8378=EDGE_CURVE('',#5972,#5971,#4179,.T.);
#8379=EDGE_CURVE('',#5973,#5972,#1669,.T.);
#8380=EDGE_CURVE('',#5424,#5973,#1670,.T.);
#8381=EDGE_CURVE('',#5974,#5974,#4180,.T.);
#8382=EDGE_CURVE('',#5975,#5975,#4181,.T.);
#8383=EDGE_CURVE('',#5974,#5976,#3424,.T.);
#8384=EDGE_CURVE('',#5976,#5976,#4182,.T.);
#8385=EDGE_CURVE('',#4358,#5430,#1671,.T.);
#8386=EDGE_CURVE('',#5429,#4359,#1672,.T.);
#8387=EDGE_CURVE('',#5977,#5978,#3425,.T.);
#8388=EDGE_CURVE('',#5979,#5977,#3426,.T.);
#8389=EDGE_CURVE('',#5979,#5980,#3427,.T.);
#8390=EDGE_CURVE('',#5978,#5980,#3428,.T.);
#8391=EDGE_CURVE('',#5980,#5979,#4183,.T.);
#8392=EDGE_CURVE('',#5981,#5982,#3429,.T.);
#8393=EDGE_CURVE('',#5983,#5981,#3430,.T.);
#8394=EDGE_CURVE('',#5983,#5984,#3431,.T.);
#8395=EDGE_CURVE('',#5982,#5984,#3432,.T.);
#8396=EDGE_CURVE('',#5984,#5985,#4184,.T.);
#8397=EDGE_CURVE('',#5985,#5983,#4185,.T.);
#8398=EDGE_CURVE('',#5985,#5975,#3433,.T.);
#8399=EDGE_CURVE('',#5978,#5981,#4186,.T.);
#8400=EDGE_CURVE('',#5982,#5977,#4187,.T.);
#8401=EDGE_CURVE('',#5700,#5972,#1673,.T.);
#8402=EDGE_CURVE('',#5971,#5701,#1674,.T.);
#9140=ORIENTED_EDGE('',*,*,#6495,.F.);
#9141=ORIENTED_EDGE('',*,*,#6496,.F.);
#9142=ORIENTED_EDGE('',*,*,#6497,.F.);
#9143=ORIENTED_EDGE('',*,*,#6498,.T.);
#9144=ORIENTED_EDGE('',*,*,#6499,.F.);
#9145=ORIENTED_EDGE('',*,*,#6500,.F.);
#9146=ORIENTED_EDGE('',*,*,#6501,.F.);
#9147=ORIENTED_EDGE('',*,*,#6495,.T.);
#9148=ORIENTED_EDGE('',*,*,#6502,.T.);
#9149=ORIENTED_EDGE('',*,*,#6503,.T.);
#9150=ORIENTED_EDGE('',*,*,#6504,.F.);
#9151=ORIENTED_EDGE('',*,*,#6505,.F.);
#9152=ORIENTED_EDGE('',*,*,#6506,.F.);
#9153=ORIENTED_EDGE('',*,*,#6499,.T.);
#9154=ORIENTED_EDGE('',*,*,#6507,.T.);
#9155=ORIENTED_EDGE('',*,*,#6508,.T.);
#9156=ORIENTED_EDGE('',*,*,#6509,.F.);
#9157=ORIENTED_EDGE('',*,*,#6510,.F.);
#9158=ORIENTED_EDGE('',*,*,#6511,.F.);
#9159=ORIENTED_EDGE('',*,*,#6504,.T.);
#9160=ORIENTED_EDGE('',*,*,#6512,.T.);
#9161=ORIENTED_EDGE('',*,*,#6513,.T.);
#9162=ORIENTED_EDGE('',*,*,#6514,.F.);
#9163=ORIENTED_EDGE('',*,*,#6515,.F.);
#9164=ORIENTED_EDGE('',*,*,#6516,.F.);
#9165=ORIENTED_EDGE('',*,*,#6509,.T.);
#9166=ORIENTED_EDGE('',*,*,#6517,.T.);
#9167=ORIENTED_EDGE('',*,*,#6518,.T.);
#9168=ORIENTED_EDGE('',*,*,#6519,.F.);
#9169=ORIENTED_EDGE('',*,*,#6520,.F.);
#9170=ORIENTED_EDGE('',*,*,#6521,.F.);
#9171=ORIENTED_EDGE('',*,*,#6514,.T.);
#9172=ORIENTED_EDGE('',*,*,#6522,.T.);
#9173=ORIENTED_EDGE('',*,*,#6523,.T.);
#9174=ORIENTED_EDGE('',*,*,#6524,.F.);
#9175=ORIENTED_EDGE('',*,*,#6525,.F.);
#9176=ORIENTED_EDGE('',*,*,#6526,.F.);
#9177=ORIENTED_EDGE('',*,*,#6519,.T.);
#9178=ORIENTED_EDGE('',*,*,#6527,.T.);
#9179=ORIENTED_EDGE('',*,*,#6528,.T.);
#9180=ORIENTED_EDGE('',*,*,#6529,.F.);
#9181=ORIENTED_EDGE('',*,*,#6530,.F.);
#9182=ORIENTED_EDGE('',*,*,#6531,.F.);
#9183=ORIENTED_EDGE('',*,*,#6524,.T.);
#9184=ORIENTED_EDGE('',*,*,#6532,.T.);
#9185=ORIENTED_EDGE('',*,*,#6533,.T.);
#9186=ORIENTED_EDGE('',*,*,#6534,.F.);
#9187=ORIENTED_EDGE('',*,*,#6535,.F.);
#9188=ORIENTED_EDGE('',*,*,#6536,.F.);
#9189=ORIENTED_EDGE('',*,*,#6529,.T.);
#9190=ORIENTED_EDGE('',*,*,#6537,.T.);
#9191=ORIENTED_EDGE('',*,*,#6538,.T.);
#9192=ORIENTED_EDGE('',*,*,#6539,.F.);
#9193=ORIENTED_EDGE('',*,*,#6540,.F.);
#9194=ORIENTED_EDGE('',*,*,#6541,.F.);
#9195=ORIENTED_EDGE('',*,*,#6534,.T.);
#9196=ORIENTED_EDGE('',*,*,#6542,.T.);
#9197=ORIENTED_EDGE('',*,*,#6543,.T.);
#9198=ORIENTED_EDGE('',*,*,#6544,.F.);
#9199=ORIENTED_EDGE('',*,*,#6545,.F.);
#9200=ORIENTED_EDGE('',*,*,#6546,.F.);
#9201=ORIENTED_EDGE('',*,*,#6539,.T.);
#9202=ORIENTED_EDGE('',*,*,#6547,.T.);
#9203=ORIENTED_EDGE('',*,*,#6548,.T.);
#9204=ORIENTED_EDGE('',*,*,#6549,.F.);
#9205=ORIENTED_EDGE('',*,*,#6550,.F.);
#9206=ORIENTED_EDGE('',*,*,#6551,.F.);
#9207=ORIENTED_EDGE('',*,*,#6544,.T.);
#9208=ORIENTED_EDGE('',*,*,#6552,.T.);
#9209=ORIENTED_EDGE('',*,*,#6553,.T.);
#9210=ORIENTED_EDGE('',*,*,#6554,.F.);
#9211=ORIENTED_EDGE('',*,*,#6555,.F.);
#9212=ORIENTED_EDGE('',*,*,#6556,.F.);
#9213=ORIENTED_EDGE('',*,*,#6549,.T.);
#9214=ORIENTED_EDGE('',*,*,#6557,.T.);
#9215=ORIENTED_EDGE('',*,*,#6558,.T.);
#9216=ORIENTED_EDGE('',*,*,#6559,.F.);
#9217=ORIENTED_EDGE('',*,*,#6560,.F.);
#9218=ORIENTED_EDGE('',*,*,#6561,.F.);
#9219=ORIENTED_EDGE('',*,*,#6554,.T.);
#9220=ORIENTED_EDGE('',*,*,#6562,.T.);
#9221=ORIENTED_EDGE('',*,*,#6563,.T.);
#9222=ORIENTED_EDGE('',*,*,#6564,.F.);
#9223=ORIENTED_EDGE('',*,*,#6565,.F.);
#9224=ORIENTED_EDGE('',*,*,#6566,.F.);
#9225=ORIENTED_EDGE('',*,*,#6559,.T.);
#9226=ORIENTED_EDGE('',*,*,#6567,.T.);
#9227=ORIENTED_EDGE('',*,*,#6568,.T.);
#9228=ORIENTED_EDGE('',*,*,#6569,.F.);
#9229=ORIENTED_EDGE('',*,*,#6570,.F.);
#9230=ORIENTED_EDGE('',*,*,#6571,.F.);
#9231=ORIENTED_EDGE('',*,*,#6564,.T.);
#9232=ORIENTED_EDGE('',*,*,#6572,.T.);
#9233=ORIENTED_EDGE('',*,*,#6573,.T.);
#9234=ORIENTED_EDGE('',*,*,#6574,.F.);
#9235=ORIENTED_EDGE('',*,*,#6575,.F.);
#9236=ORIENTED_EDGE('',*,*,#6576,.F.);
#9237=ORIENTED_EDGE('',*,*,#6569,.T.);
#9238=ORIENTED_EDGE('',*,*,#6577,.T.);
#9239=ORIENTED_EDGE('',*,*,#6578,.T.);
#9240=ORIENTED_EDGE('',*,*,#6579,.F.);
#9241=ORIENTED_EDGE('',*,*,#6580,.F.);
#9242=ORIENTED_EDGE('',*,*,#6581,.F.);
#9243=ORIENTED_EDGE('',*,*,#6574,.T.);
#9244=ORIENTED_EDGE('',*,*,#6582,.T.);
#9245=ORIENTED_EDGE('',*,*,#6583,.T.);
#9246=ORIENTED_EDGE('',*,*,#6584,.F.);
#9247=ORIENTED_EDGE('',*,*,#6585,.F.);
#9248=ORIENTED_EDGE('',*,*,#6586,.F.);
#9249=ORIENTED_EDGE('',*,*,#6579,.T.);
#9250=ORIENTED_EDGE('',*,*,#6587,.T.);
#9251=ORIENTED_EDGE('',*,*,#6588,.T.);
#9252=ORIENTED_EDGE('',*,*,#6589,.F.);
#9253=ORIENTED_EDGE('',*,*,#6590,.F.);
#9254=ORIENTED_EDGE('',*,*,#6591,.F.);
#9255=ORIENTED_EDGE('',*,*,#6584,.T.);
#9256=ORIENTED_EDGE('',*,*,#6592,.T.);
#9257=ORIENTED_EDGE('',*,*,#6593,.T.);
#9258=ORIENTED_EDGE('',*,*,#6594,.F.);
#9259=ORIENTED_EDGE('',*,*,#6595,.F.);
#9260=ORIENTED_EDGE('',*,*,#6596,.F.);
#9261=ORIENTED_EDGE('',*,*,#6589,.T.);
#9262=ORIENTED_EDGE('',*,*,#6597,.T.);
#9263=ORIENTED_EDGE('',*,*,#6598,.T.);
#9264=ORIENTED_EDGE('',*,*,#6599,.F.);
#9265=ORIENTED_EDGE('',*,*,#6600,.F.);
#9266=ORIENTED_EDGE('',*,*,#6601,.F.);
#9267=ORIENTED_EDGE('',*,*,#6594,.T.);
#9268=ORIENTED_EDGE('',*,*,#6602,.T.);
#9269=ORIENTED_EDGE('',*,*,#6603,.T.);
#9270=ORIENTED_EDGE('',*,*,#6604,.F.);
#9271=ORIENTED_EDGE('',*,*,#6605,.F.);
#9272=ORIENTED_EDGE('',*,*,#6606,.F.);
#9273=ORIENTED_EDGE('',*,*,#6599,.T.);
#9274=ORIENTED_EDGE('',*,*,#6607,.T.);
#9275=ORIENTED_EDGE('',*,*,#6608,.T.);
#9276=ORIENTED_EDGE('',*,*,#6609,.F.);
#9277=ORIENTED_EDGE('',*,*,#6610,.F.);
#9278=ORIENTED_EDGE('',*,*,#6611,.F.);
#9279=ORIENTED_EDGE('',*,*,#6604,.T.);
#9280=ORIENTED_EDGE('',*,*,#6612,.T.);
#9281=ORIENTED_EDGE('',*,*,#6613,.T.);
#9282=ORIENTED_EDGE('',*,*,#6614,.F.);
#9283=ORIENTED_EDGE('',*,*,#6615,.F.);
#9284=ORIENTED_EDGE('',*,*,#6616,.F.);
#9285=ORIENTED_EDGE('',*,*,#6609,.T.);
#9286=ORIENTED_EDGE('',*,*,#6617,.T.);
#9287=ORIENTED_EDGE('',*,*,#6618,.T.);
#9288=ORIENTED_EDGE('',*,*,#6619,.F.);
#9289=ORIENTED_EDGE('',*,*,#6620,.F.);
#9290=ORIENTED_EDGE('',*,*,#6621,.F.);
#9291=ORIENTED_EDGE('',*,*,#6614,.T.);
#9292=ORIENTED_EDGE('',*,*,#6622,.T.);
#9293=ORIENTED_EDGE('',*,*,#6623,.T.);
#9294=ORIENTED_EDGE('',*,*,#6624,.F.);
#9295=ORIENTED_EDGE('',*,*,#6625,.F.);
#9296=ORIENTED_EDGE('',*,*,#6626,.F.);
#9297=ORIENTED_EDGE('',*,*,#6619,.T.);
#9298=ORIENTED_EDGE('',*,*,#6627,.T.);
#9299=ORIENTED_EDGE('',*,*,#6628,.T.);
#9300=ORIENTED_EDGE('',*,*,#6629,.F.);
#9301=ORIENTED_EDGE('',*,*,#6630,.F.);
#9302=ORIENTED_EDGE('',*,*,#6631,.F.);
#9303=ORIENTED_EDGE('',*,*,#6624,.T.);
#9304=ORIENTED_EDGE('',*,*,#6632,.T.);
#9305=ORIENTED_EDGE('',*,*,#6633,.T.);
#9306=ORIENTED_EDGE('',*,*,#6634,.F.);
#9307=ORIENTED_EDGE('',*,*,#6635,.F.);
#9308=ORIENTED_EDGE('',*,*,#6636,.F.);
#9309=ORIENTED_EDGE('',*,*,#6629,.T.);
#9310=ORIENTED_EDGE('',*,*,#6637,.T.);
#9311=ORIENTED_EDGE('',*,*,#6638,.T.);
#9312=ORIENTED_EDGE('',*,*,#6639,.F.);
#9313=ORIENTED_EDGE('',*,*,#6640,.F.);
#9314=ORIENTED_EDGE('',*,*,#6641,.F.);
#9315=ORIENTED_EDGE('',*,*,#6634,.T.);
#9316=ORIENTED_EDGE('',*,*,#6642,.T.);
#9317=ORIENTED_EDGE('',*,*,#6643,.T.);
#9318=ORIENTED_EDGE('',*,*,#6644,.F.);
#9319=ORIENTED_EDGE('',*,*,#6645,.F.);
#9320=ORIENTED_EDGE('',*,*,#6646,.F.);
#9321=ORIENTED_EDGE('',*,*,#6639,.T.);
#9322=ORIENTED_EDGE('',*,*,#6647,.T.);
#9323=ORIENTED_EDGE('',*,*,#6648,.T.);
#9324=ORIENTED_EDGE('',*,*,#6649,.F.);
#9325=ORIENTED_EDGE('',*,*,#6650,.F.);
#9326=ORIENTED_EDGE('',*,*,#6651,.F.);
#9327=ORIENTED_EDGE('',*,*,#6644,.T.);
#9328=ORIENTED_EDGE('',*,*,#6652,.T.);
#9329=ORIENTED_EDGE('',*,*,#6653,.T.);
#9330=ORIENTED_EDGE('',*,*,#6654,.F.);
#9331=ORIENTED_EDGE('',*,*,#6655,.F.);
#9332=ORIENTED_EDGE('',*,*,#6656,.F.);
#9333=ORIENTED_EDGE('',*,*,#6649,.T.);
#9334=ORIENTED_EDGE('',*,*,#6657,.T.);
#9335=ORIENTED_EDGE('',*,*,#6658,.T.);
#9336=ORIENTED_EDGE('',*,*,#6659,.F.);
#9337=ORIENTED_EDGE('',*,*,#6660,.F.);
#9338=ORIENTED_EDGE('',*,*,#6661,.F.);
#9339=ORIENTED_EDGE('',*,*,#6654,.T.);
#9340=ORIENTED_EDGE('',*,*,#6662,.T.);
#9341=ORIENTED_EDGE('',*,*,#6663,.T.);
#9342=ORIENTED_EDGE('',*,*,#6664,.F.);
#9343=ORIENTED_EDGE('',*,*,#6665,.F.);
#9344=ORIENTED_EDGE('',*,*,#6666,.F.);
#9345=ORIENTED_EDGE('',*,*,#6659,.T.);
#9346=ORIENTED_EDGE('',*,*,#6667,.T.);
#9347=ORIENTED_EDGE('',*,*,#6668,.T.);
#9348=ORIENTED_EDGE('',*,*,#6669,.F.);
#9349=ORIENTED_EDGE('',*,*,#6670,.F.);
#9350=ORIENTED_EDGE('',*,*,#6671,.F.);
#9351=ORIENTED_EDGE('',*,*,#6664,.T.);
#9352=ORIENTED_EDGE('',*,*,#6672,.T.);
#9353=ORIENTED_EDGE('',*,*,#6673,.T.);
#9354=ORIENTED_EDGE('',*,*,#6674,.F.);
#9355=ORIENTED_EDGE('',*,*,#6675,.F.);
#9356=ORIENTED_EDGE('',*,*,#6676,.F.);
#9357=ORIENTED_EDGE('',*,*,#6669,.T.);
#9358=ORIENTED_EDGE('',*,*,#6677,.T.);
#9359=ORIENTED_EDGE('',*,*,#6678,.T.);
#9360=ORIENTED_EDGE('',*,*,#6679,.F.);
#9361=ORIENTED_EDGE('',*,*,#6680,.F.);
#9362=ORIENTED_EDGE('',*,*,#6681,.F.);
#9363=ORIENTED_EDGE('',*,*,#6674,.T.);
#9364=ORIENTED_EDGE('',*,*,#6682,.T.);
#9365=ORIENTED_EDGE('',*,*,#6683,.T.);
#9366=ORIENTED_EDGE('',*,*,#6684,.F.);
#9367=ORIENTED_EDGE('',*,*,#6685,.F.);
#9368=ORIENTED_EDGE('',*,*,#6686,.F.);
#9369=ORIENTED_EDGE('',*,*,#6679,.T.);
#9370=ORIENTED_EDGE('',*,*,#6687,.T.);
#9371=ORIENTED_EDGE('',*,*,#6688,.T.);
#9372=ORIENTED_EDGE('',*,*,#6689,.F.);
#9373=ORIENTED_EDGE('',*,*,#6690,.F.);
#9374=ORIENTED_EDGE('',*,*,#6691,.F.);
#9375=ORIENTED_EDGE('',*,*,#6684,.T.);
#9376=ORIENTED_EDGE('',*,*,#6692,.T.);
#9377=ORIENTED_EDGE('',*,*,#6693,.T.);
#9378=ORIENTED_EDGE('',*,*,#6694,.F.);
#9379=ORIENTED_EDGE('',*,*,#6695,.F.);
#9380=ORIENTED_EDGE('',*,*,#6696,.F.);
#9381=ORIENTED_EDGE('',*,*,#6689,.T.);
#9382=ORIENTED_EDGE('',*,*,#6697,.T.);
#9383=ORIENTED_EDGE('',*,*,#6698,.T.);
#9384=ORIENTED_EDGE('',*,*,#6699,.F.);
#9385=ORIENTED_EDGE('',*,*,#6700,.F.);
#9386=ORIENTED_EDGE('',*,*,#6701,.F.);
#9387=ORIENTED_EDGE('',*,*,#6694,.T.);
#9388=ORIENTED_EDGE('',*,*,#6702,.T.);
#9389=ORIENTED_EDGE('',*,*,#6703,.T.);
#9390=ORIENTED_EDGE('',*,*,#6704,.F.);
#9391=ORIENTED_EDGE('',*,*,#6705,.F.);
#9392=ORIENTED_EDGE('',*,*,#6706,.F.);
#9393=ORIENTED_EDGE('',*,*,#6699,.T.);
#9394=ORIENTED_EDGE('',*,*,#6707,.T.);
#9395=ORIENTED_EDGE('',*,*,#6708,.T.);
#9396=ORIENTED_EDGE('',*,*,#6709,.F.);
#9397=ORIENTED_EDGE('',*,*,#6710,.F.);
#9398=ORIENTED_EDGE('',*,*,#6711,.F.);
#9399=ORIENTED_EDGE('',*,*,#6704,.T.);
#9400=ORIENTED_EDGE('',*,*,#6712,.T.);
#9401=ORIENTED_EDGE('',*,*,#6713,.T.);
#9402=ORIENTED_EDGE('',*,*,#6714,.F.);
#9403=ORIENTED_EDGE('',*,*,#6715,.F.);
#9404=ORIENTED_EDGE('',*,*,#6716,.F.);
#9405=ORIENTED_EDGE('',*,*,#6709,.T.);
#9406=ORIENTED_EDGE('',*,*,#6717,.T.);
#9407=ORIENTED_EDGE('',*,*,#6718,.T.);
#9408=ORIENTED_EDGE('',*,*,#6719,.F.);
#9409=ORIENTED_EDGE('',*,*,#6720,.F.);
#9410=ORIENTED_EDGE('',*,*,#6721,.F.);
#9411=ORIENTED_EDGE('',*,*,#6714,.T.);
#9412=ORIENTED_EDGE('',*,*,#6722,.T.);
#9413=ORIENTED_EDGE('',*,*,#6723,.T.);
#9414=ORIENTED_EDGE('',*,*,#6724,.F.);
#9415=ORIENTED_EDGE('',*,*,#6725,.F.);
#9416=ORIENTED_EDGE('',*,*,#6726,.F.);
#9417=ORIENTED_EDGE('',*,*,#6719,.T.);
#9418=ORIENTED_EDGE('',*,*,#6727,.T.);
#9419=ORIENTED_EDGE('',*,*,#6728,.T.);
#9420=ORIENTED_EDGE('',*,*,#6729,.F.);
#9421=ORIENTED_EDGE('',*,*,#6730,.F.);
#9422=ORIENTED_EDGE('',*,*,#6731,.F.);
#9423=ORIENTED_EDGE('',*,*,#6724,.T.);
#9424=ORIENTED_EDGE('',*,*,#6732,.T.);
#9425=ORIENTED_EDGE('',*,*,#6733,.T.);
#9426=ORIENTED_EDGE('',*,*,#6734,.F.);
#9427=ORIENTED_EDGE('',*,*,#6735,.F.);
#9428=ORIENTED_EDGE('',*,*,#6736,.F.);
#9429=ORIENTED_EDGE('',*,*,#6729,.T.);
#9430=ORIENTED_EDGE('',*,*,#6737,.T.);
#9431=ORIENTED_EDGE('',*,*,#6738,.T.);
#9432=ORIENTED_EDGE('',*,*,#6739,.F.);
#9433=ORIENTED_EDGE('',*,*,#6740,.F.);
#9434=ORIENTED_EDGE('',*,*,#6741,.F.);
#9435=ORIENTED_EDGE('',*,*,#6734,.T.);
#9436=ORIENTED_EDGE('',*,*,#6742,.T.);
#9437=ORIENTED_EDGE('',*,*,#6743,.T.);
#9438=ORIENTED_EDGE('',*,*,#6744,.F.);
#9439=ORIENTED_EDGE('',*,*,#6745,.F.);
#9440=ORIENTED_EDGE('',*,*,#6746,.F.);
#9441=ORIENTED_EDGE('',*,*,#6739,.T.);
#9442=ORIENTED_EDGE('',*,*,#6747,.T.);
#9443=ORIENTED_EDGE('',*,*,#6748,.T.);
#9444=ORIENTED_EDGE('',*,*,#6749,.F.);
#9445=ORIENTED_EDGE('',*,*,#6750,.F.);
#9446=ORIENTED_EDGE('',*,*,#6751,.F.);
#9447=ORIENTED_EDGE('',*,*,#6744,.T.);
#9448=ORIENTED_EDGE('',*,*,#6752,.T.);
#9449=ORIENTED_EDGE('',*,*,#6753,.T.);
#9450=ORIENTED_EDGE('',*,*,#6754,.F.);
#9451=ORIENTED_EDGE('',*,*,#6755,.F.);
#9452=ORIENTED_EDGE('',*,*,#6756,.F.);
#9453=ORIENTED_EDGE('',*,*,#6749,.T.);
#9454=ORIENTED_EDGE('',*,*,#6757,.T.);
#9455=ORIENTED_EDGE('',*,*,#6758,.T.);
#9456=ORIENTED_EDGE('',*,*,#6759,.F.);
#9457=ORIENTED_EDGE('',*,*,#6760,.F.);
#9458=ORIENTED_EDGE('',*,*,#6761,.F.);
#9459=ORIENTED_EDGE('',*,*,#6754,.T.);
#9460=ORIENTED_EDGE('',*,*,#6762,.T.);
#9461=ORIENTED_EDGE('',*,*,#6763,.T.);
#9462=ORIENTED_EDGE('',*,*,#6764,.F.);
#9463=ORIENTED_EDGE('',*,*,#6765,.F.);
#9464=ORIENTED_EDGE('',*,*,#6766,.F.);
#9465=ORIENTED_EDGE('',*,*,#6759,.T.);
#9466=ORIENTED_EDGE('',*,*,#6767,.T.);
#9467=ORIENTED_EDGE('',*,*,#6768,.T.);
#9468=ORIENTED_EDGE('',*,*,#6769,.F.);
#9469=ORIENTED_EDGE('',*,*,#6770,.F.);
#9470=ORIENTED_EDGE('',*,*,#6771,.F.);
#9471=ORIENTED_EDGE('',*,*,#6764,.T.);
#9472=ORIENTED_EDGE('',*,*,#6772,.T.);
#9473=ORIENTED_EDGE('',*,*,#6773,.T.);
#9474=ORIENTED_EDGE('',*,*,#6774,.F.);
#9475=ORIENTED_EDGE('',*,*,#6775,.F.);
#9476=ORIENTED_EDGE('',*,*,#6776,.F.);
#9477=ORIENTED_EDGE('',*,*,#6769,.T.);
#9478=ORIENTED_EDGE('',*,*,#6777,.T.);
#9479=ORIENTED_EDGE('',*,*,#6778,.T.);
#9480=ORIENTED_EDGE('',*,*,#6779,.F.);
#9481=ORIENTED_EDGE('',*,*,#6780,.F.);
#9482=ORIENTED_EDGE('',*,*,#6781,.F.);
#9483=ORIENTED_EDGE('',*,*,#6774,.T.);
#9484=ORIENTED_EDGE('',*,*,#6782,.T.);
#9485=ORIENTED_EDGE('',*,*,#6783,.T.);
#9486=ORIENTED_EDGE('',*,*,#6784,.F.);
#9487=ORIENTED_EDGE('',*,*,#6785,.F.);
#9488=ORIENTED_EDGE('',*,*,#6786,.F.);
#9489=ORIENTED_EDGE('',*,*,#6779,.T.);
#9490=ORIENTED_EDGE('',*,*,#6787,.T.);
#9491=ORIENTED_EDGE('',*,*,#6788,.T.);
#9492=ORIENTED_EDGE('',*,*,#6789,.F.);
#9493=ORIENTED_EDGE('',*,*,#6790,.F.);
#9494=ORIENTED_EDGE('',*,*,#6791,.F.);
#9495=ORIENTED_EDGE('',*,*,#6784,.T.);
#9496=ORIENTED_EDGE('',*,*,#6792,.T.);
#9497=ORIENTED_EDGE('',*,*,#6793,.T.);
#9498=ORIENTED_EDGE('',*,*,#6794,.F.);
#9499=ORIENTED_EDGE('',*,*,#6795,.F.);
#9500=ORIENTED_EDGE('',*,*,#6796,.F.);
#9501=ORIENTED_EDGE('',*,*,#6789,.T.);
#9502=ORIENTED_EDGE('',*,*,#6797,.T.);
#9503=ORIENTED_EDGE('',*,*,#6798,.T.);
#9504=ORIENTED_EDGE('',*,*,#6799,.F.);
#9505=ORIENTED_EDGE('',*,*,#6800,.F.);
#9506=ORIENTED_EDGE('',*,*,#6801,.F.);
#9507=ORIENTED_EDGE('',*,*,#6794,.T.);
#9508=ORIENTED_EDGE('',*,*,#6802,.T.);
#9509=ORIENTED_EDGE('',*,*,#6803,.T.);
#9510=ORIENTED_EDGE('',*,*,#6804,.F.);
#9511=ORIENTED_EDGE('',*,*,#6805,.F.);
#9512=ORIENTED_EDGE('',*,*,#6806,.F.);
#9513=ORIENTED_EDGE('',*,*,#6799,.T.);
#9514=ORIENTED_EDGE('',*,*,#6807,.T.);
#9515=ORIENTED_EDGE('',*,*,#6808,.T.);
#9516=ORIENTED_EDGE('',*,*,#6809,.F.);
#9517=ORIENTED_EDGE('',*,*,#6810,.F.);
#9518=ORIENTED_EDGE('',*,*,#6811,.F.);
#9519=ORIENTED_EDGE('',*,*,#6804,.T.);
#9520=ORIENTED_EDGE('',*,*,#6812,.T.);
#9521=ORIENTED_EDGE('',*,*,#6813,.T.);
#9522=ORIENTED_EDGE('',*,*,#6814,.F.);
#9523=ORIENTED_EDGE('',*,*,#6815,.F.);
#9524=ORIENTED_EDGE('',*,*,#6816,.F.);
#9525=ORIENTED_EDGE('',*,*,#6809,.T.);
#9526=ORIENTED_EDGE('',*,*,#6817,.T.);
#9527=ORIENTED_EDGE('',*,*,#6818,.T.);
#9528=ORIENTED_EDGE('',*,*,#6819,.F.);
#9529=ORIENTED_EDGE('',*,*,#6820,.F.);
#9530=ORIENTED_EDGE('',*,*,#6821,.F.);
#9531=ORIENTED_EDGE('',*,*,#6814,.T.);
#9532=ORIENTED_EDGE('',*,*,#6822,.T.);
#9533=ORIENTED_EDGE('',*,*,#6823,.T.);
#9534=ORIENTED_EDGE('',*,*,#6824,.F.);
#9535=ORIENTED_EDGE('',*,*,#6825,.F.);
#9536=ORIENTED_EDGE('',*,*,#6826,.F.);
#9537=ORIENTED_EDGE('',*,*,#6819,.T.);
#9538=ORIENTED_EDGE('',*,*,#6827,.T.);
#9539=ORIENTED_EDGE('',*,*,#6828,.T.);
#9540=ORIENTED_EDGE('',*,*,#6829,.F.);
#9541=ORIENTED_EDGE('',*,*,#6830,.F.);
#9542=ORIENTED_EDGE('',*,*,#6831,.F.);
#9543=ORIENTED_EDGE('',*,*,#6824,.T.);
#9544=ORIENTED_EDGE('',*,*,#6832,.T.);
#9545=ORIENTED_EDGE('',*,*,#6833,.T.);
#9546=ORIENTED_EDGE('',*,*,#6834,.F.);
#9547=ORIENTED_EDGE('',*,*,#6835,.F.);
#9548=ORIENTED_EDGE('',*,*,#6836,.F.);
#9549=ORIENTED_EDGE('',*,*,#6829,.T.);
#9550=ORIENTED_EDGE('',*,*,#6837,.T.);
#9551=ORIENTED_EDGE('',*,*,#6838,.T.);
#9552=ORIENTED_EDGE('',*,*,#6839,.F.);
#9553=ORIENTED_EDGE('',*,*,#6840,.F.);
#9554=ORIENTED_EDGE('',*,*,#6841,.F.);
#9555=ORIENTED_EDGE('',*,*,#6834,.T.);
#9556=ORIENTED_EDGE('',*,*,#6842,.T.);
#9557=ORIENTED_EDGE('',*,*,#6843,.T.);
#9558=ORIENTED_EDGE('',*,*,#6844,.F.);
#9559=ORIENTED_EDGE('',*,*,#6845,.F.);
#9560=ORIENTED_EDGE('',*,*,#6846,.F.);
#9561=ORIENTED_EDGE('',*,*,#6839,.T.);
#9562=ORIENTED_EDGE('',*,*,#6847,.T.);
#9563=ORIENTED_EDGE('',*,*,#6848,.T.);
#9564=ORIENTED_EDGE('',*,*,#6849,.F.);
#9565=ORIENTED_EDGE('',*,*,#6850,.F.);
#9566=ORIENTED_EDGE('',*,*,#6851,.F.);
#9567=ORIENTED_EDGE('',*,*,#6844,.T.);
#9568=ORIENTED_EDGE('',*,*,#6852,.T.);
#9569=ORIENTED_EDGE('',*,*,#6853,.T.);
#9570=ORIENTED_EDGE('',*,*,#6854,.F.);
#9571=ORIENTED_EDGE('',*,*,#6855,.F.);
#9572=ORIENTED_EDGE('',*,*,#6856,.F.);
#9573=ORIENTED_EDGE('',*,*,#6849,.T.);
#9574=ORIENTED_EDGE('',*,*,#6857,.T.);
#9575=ORIENTED_EDGE('',*,*,#6858,.T.);
#9576=ORIENTED_EDGE('',*,*,#6859,.F.);
#9577=ORIENTED_EDGE('',*,*,#6860,.F.);
#9578=ORIENTED_EDGE('',*,*,#6861,.F.);
#9579=ORIENTED_EDGE('',*,*,#6854,.T.);
#9580=ORIENTED_EDGE('',*,*,#6862,.T.);
#9581=ORIENTED_EDGE('',*,*,#6863,.T.);
#9582=ORIENTED_EDGE('',*,*,#6864,.F.);
#9583=ORIENTED_EDGE('',*,*,#6865,.F.);
#9584=ORIENTED_EDGE('',*,*,#6866,.F.);
#9585=ORIENTED_EDGE('',*,*,#6859,.T.);
#9586=ORIENTED_EDGE('',*,*,#6867,.T.);
#9587=ORIENTED_EDGE('',*,*,#6868,.T.);
#9588=ORIENTED_EDGE('',*,*,#6869,.F.);
#9589=ORIENTED_EDGE('',*,*,#6870,.F.);
#9590=ORIENTED_EDGE('',*,*,#6871,.F.);
#9591=ORIENTED_EDGE('',*,*,#6864,.T.);
#9592=ORIENTED_EDGE('',*,*,#6872,.T.);
#9593=ORIENTED_EDGE('',*,*,#6873,.T.);
#9594=ORIENTED_EDGE('',*,*,#6874,.F.);
#9595=ORIENTED_EDGE('',*,*,#6875,.F.);
#9596=ORIENTED_EDGE('',*,*,#6876,.F.);
#9597=ORIENTED_EDGE('',*,*,#6869,.T.);
#9598=ORIENTED_EDGE('',*,*,#6877,.T.);
#9599=ORIENTED_EDGE('',*,*,#6878,.T.);
#9600=ORIENTED_EDGE('',*,*,#6879,.F.);
#9601=ORIENTED_EDGE('',*,*,#6880,.F.);
#9602=ORIENTED_EDGE('',*,*,#6881,.F.);
#9603=ORIENTED_EDGE('',*,*,#6874,.T.);
#9604=ORIENTED_EDGE('',*,*,#6882,.T.);
#9605=ORIENTED_EDGE('',*,*,#6883,.T.);
#9606=ORIENTED_EDGE('',*,*,#6884,.F.);
#9607=ORIENTED_EDGE('',*,*,#6885,.F.);
#9608=ORIENTED_EDGE('',*,*,#6886,.F.);
#9609=ORIENTED_EDGE('',*,*,#6879,.T.);
#9610=ORIENTED_EDGE('',*,*,#6887,.T.);
#9611=ORIENTED_EDGE('',*,*,#6888,.T.);
#9612=ORIENTED_EDGE('',*,*,#6889,.F.);
#9613=ORIENTED_EDGE('',*,*,#6890,.F.);
#9614=ORIENTED_EDGE('',*,*,#6891,.F.);
#9615=ORIENTED_EDGE('',*,*,#6884,.T.);
#9616=ORIENTED_EDGE('',*,*,#6892,.T.);
#9617=ORIENTED_EDGE('',*,*,#6893,.T.);
#9618=ORIENTED_EDGE('',*,*,#6894,.F.);
#9619=ORIENTED_EDGE('',*,*,#6895,.F.);
#9620=ORIENTED_EDGE('',*,*,#6896,.F.);
#9621=ORIENTED_EDGE('',*,*,#6889,.T.);
#9622=ORIENTED_EDGE('',*,*,#6897,.T.);
#9623=ORIENTED_EDGE('',*,*,#6898,.T.);
#9624=ORIENTED_EDGE('',*,*,#6899,.F.);
#9625=ORIENTED_EDGE('',*,*,#6900,.F.);
#9626=ORIENTED_EDGE('',*,*,#6901,.F.);
#9627=ORIENTED_EDGE('',*,*,#6894,.T.);
#9628=ORIENTED_EDGE('',*,*,#6902,.T.);
#9629=ORIENTED_EDGE('',*,*,#6903,.T.);
#9630=ORIENTED_EDGE('',*,*,#6904,.F.);
#9631=ORIENTED_EDGE('',*,*,#6905,.F.);
#9632=ORIENTED_EDGE('',*,*,#6906,.F.);
#9633=ORIENTED_EDGE('',*,*,#6899,.T.);
#9634=ORIENTED_EDGE('',*,*,#6907,.T.);
#9635=ORIENTED_EDGE('',*,*,#6908,.T.);
#9636=ORIENTED_EDGE('',*,*,#6909,.F.);
#9637=ORIENTED_EDGE('',*,*,#6910,.F.);
#9638=ORIENTED_EDGE('',*,*,#6911,.F.);
#9639=ORIENTED_EDGE('',*,*,#6904,.T.);
#9640=ORIENTED_EDGE('',*,*,#6912,.T.);
#9641=ORIENTED_EDGE('',*,*,#6913,.T.);
#9642=ORIENTED_EDGE('',*,*,#6914,.F.);
#9643=ORIENTED_EDGE('',*,*,#6915,.F.);
#9644=ORIENTED_EDGE('',*,*,#6916,.F.);
#9645=ORIENTED_EDGE('',*,*,#6909,.T.);
#9646=ORIENTED_EDGE('',*,*,#6917,.T.);
#9647=ORIENTED_EDGE('',*,*,#6918,.T.);
#9648=ORIENTED_EDGE('',*,*,#6919,.F.);
#9649=ORIENTED_EDGE('',*,*,#6920,.F.);
#9650=ORIENTED_EDGE('',*,*,#6921,.F.);
#9651=ORIENTED_EDGE('',*,*,#6914,.T.);
#9652=ORIENTED_EDGE('',*,*,#6922,.T.);
#9653=ORIENTED_EDGE('',*,*,#6923,.T.);
#9654=ORIENTED_EDGE('',*,*,#6924,.F.);
#9655=ORIENTED_EDGE('',*,*,#6925,.F.);
#9656=ORIENTED_EDGE('',*,*,#6926,.F.);
#9657=ORIENTED_EDGE('',*,*,#6919,.T.);
#9658=ORIENTED_EDGE('',*,*,#6927,.T.);
#9659=ORIENTED_EDGE('',*,*,#6928,.T.);
#9660=ORIENTED_EDGE('',*,*,#6929,.F.);
#9661=ORIENTED_EDGE('',*,*,#6930,.F.);
#9662=ORIENTED_EDGE('',*,*,#6931,.F.);
#9663=ORIENTED_EDGE('',*,*,#6924,.T.);
#9664=ORIENTED_EDGE('',*,*,#6932,.T.);
#9665=ORIENTED_EDGE('',*,*,#6933,.T.);
#9666=ORIENTED_EDGE('',*,*,#6934,.F.);
#9667=ORIENTED_EDGE('',*,*,#6935,.F.);
#9668=ORIENTED_EDGE('',*,*,#6936,.F.);
#9669=ORIENTED_EDGE('',*,*,#6929,.T.);
#9670=ORIENTED_EDGE('',*,*,#6937,.T.);
#9671=ORIENTED_EDGE('',*,*,#6938,.T.);
#9672=ORIENTED_EDGE('',*,*,#6939,.F.);
#9673=ORIENTED_EDGE('',*,*,#6940,.F.);
#9674=ORIENTED_EDGE('',*,*,#6941,.F.);
#9675=ORIENTED_EDGE('',*,*,#6934,.T.);
#9676=ORIENTED_EDGE('',*,*,#6942,.T.);
#9677=ORIENTED_EDGE('',*,*,#6943,.T.);
#9678=ORIENTED_EDGE('',*,*,#6944,.F.);
#9679=ORIENTED_EDGE('',*,*,#6945,.F.);
#9680=ORIENTED_EDGE('',*,*,#6946,.F.);
#9681=ORIENTED_EDGE('',*,*,#6939,.T.);
#9682=ORIENTED_EDGE('',*,*,#6947,.T.);
#9683=ORIENTED_EDGE('',*,*,#6948,.T.);
#9684=ORIENTED_EDGE('',*,*,#6949,.F.);
#9685=ORIENTED_EDGE('',*,*,#6950,.F.);
#9686=ORIENTED_EDGE('',*,*,#6951,.F.);
#9687=ORIENTED_EDGE('',*,*,#6944,.T.);
#9688=ORIENTED_EDGE('',*,*,#6952,.T.);
#9689=ORIENTED_EDGE('',*,*,#6953,.T.);
#9690=ORIENTED_EDGE('',*,*,#6954,.F.);
#9691=ORIENTED_EDGE('',*,*,#6955,.F.);
#9692=ORIENTED_EDGE('',*,*,#6956,.F.);
#9693=ORIENTED_EDGE('',*,*,#6949,.T.);
#9694=ORIENTED_EDGE('',*,*,#6957,.T.);
#9695=ORIENTED_EDGE('',*,*,#6958,.T.);
#9696=ORIENTED_EDGE('',*,*,#6959,.F.);
#9697=ORIENTED_EDGE('',*,*,#6960,.F.);
#9698=ORIENTED_EDGE('',*,*,#6961,.F.);
#9699=ORIENTED_EDGE('',*,*,#6954,.T.);
#9700=ORIENTED_EDGE('',*,*,#6962,.T.);
#9701=ORIENTED_EDGE('',*,*,#6963,.T.);
#9702=ORIENTED_EDGE('',*,*,#6964,.F.);
#9703=ORIENTED_EDGE('',*,*,#6965,.F.);
#9704=ORIENTED_EDGE('',*,*,#6966,.F.);
#9705=ORIENTED_EDGE('',*,*,#6959,.T.);
#9706=ORIENTED_EDGE('',*,*,#6967,.T.);
#9707=ORIENTED_EDGE('',*,*,#6968,.T.);
#9708=ORIENTED_EDGE('',*,*,#6969,.F.);
#9709=ORIENTED_EDGE('',*,*,#6970,.F.);
#9710=ORIENTED_EDGE('',*,*,#6971,.F.);
#9711=ORIENTED_EDGE('',*,*,#6964,.T.);
#9712=ORIENTED_EDGE('',*,*,#6972,.T.);
#9713=ORIENTED_EDGE('',*,*,#6973,.T.);
#9714=ORIENTED_EDGE('',*,*,#6974,.F.);
#9715=ORIENTED_EDGE('',*,*,#6975,.F.);
#9716=ORIENTED_EDGE('',*,*,#6976,.F.);
#9717=ORIENTED_EDGE('',*,*,#6969,.T.);
#9718=ORIENTED_EDGE('',*,*,#6977,.T.);
#9719=ORIENTED_EDGE('',*,*,#6978,.T.);
#9720=ORIENTED_EDGE('',*,*,#6979,.F.);
#9721=ORIENTED_EDGE('',*,*,#6980,.F.);
#9722=ORIENTED_EDGE('',*,*,#6981,.F.);
#9723=ORIENTED_EDGE('',*,*,#6974,.T.);
#9724=ORIENTED_EDGE('',*,*,#6982,.T.);
#9725=ORIENTED_EDGE('',*,*,#6983,.T.);
#9726=ORIENTED_EDGE('',*,*,#6984,.F.);
#9727=ORIENTED_EDGE('',*,*,#6985,.F.);
#9728=ORIENTED_EDGE('',*,*,#6986,.F.);
#9729=ORIENTED_EDGE('',*,*,#6979,.T.);
#9730=ORIENTED_EDGE('',*,*,#6987,.T.);
#9731=ORIENTED_EDGE('',*,*,#6988,.T.);
#9732=ORIENTED_EDGE('',*,*,#6989,.F.);
#9733=ORIENTED_EDGE('',*,*,#6990,.F.);
#9734=ORIENTED_EDGE('',*,*,#6991,.F.);
#9735=ORIENTED_EDGE('',*,*,#6984,.T.);
#9736=ORIENTED_EDGE('',*,*,#6992,.T.);
#9737=ORIENTED_EDGE('',*,*,#6993,.T.);
#9738=ORIENTED_EDGE('',*,*,#6994,.F.);
#9739=ORIENTED_EDGE('',*,*,#6995,.F.);
#9740=ORIENTED_EDGE('',*,*,#6996,.F.);
#9741=ORIENTED_EDGE('',*,*,#6989,.T.);
#9742=ORIENTED_EDGE('',*,*,#6997,.T.);
#9743=ORIENTED_EDGE('',*,*,#6998,.T.);
#9744=ORIENTED_EDGE('',*,*,#6999,.F.);
#9745=ORIENTED_EDGE('',*,*,#7000,.F.);
#9746=ORIENTED_EDGE('',*,*,#7001,.F.);
#9747=ORIENTED_EDGE('',*,*,#6994,.T.);
#9748=ORIENTED_EDGE('',*,*,#7002,.T.);
#9749=ORIENTED_EDGE('',*,*,#7003,.T.);
#9750=ORIENTED_EDGE('',*,*,#7004,.F.);
#9751=ORIENTED_EDGE('',*,*,#7005,.F.);
#9752=ORIENTED_EDGE('',*,*,#7006,.F.);
#9753=ORIENTED_EDGE('',*,*,#6999,.T.);
#9754=ORIENTED_EDGE('',*,*,#7007,.T.);
#9755=ORIENTED_EDGE('',*,*,#7008,.T.);
#9756=ORIENTED_EDGE('',*,*,#7009,.F.);
#9757=ORIENTED_EDGE('',*,*,#7010,.F.);
#9758=ORIENTED_EDGE('',*,*,#7011,.F.);
#9759=ORIENTED_EDGE('',*,*,#7004,.T.);
#9760=ORIENTED_EDGE('',*,*,#7012,.T.);
#9761=ORIENTED_EDGE('',*,*,#7013,.T.);
#9762=ORIENTED_EDGE('',*,*,#7014,.F.);
#9763=ORIENTED_EDGE('',*,*,#7015,.F.);
#9764=ORIENTED_EDGE('',*,*,#7016,.F.);
#9765=ORIENTED_EDGE('',*,*,#7009,.T.);
#9766=ORIENTED_EDGE('',*,*,#7017,.T.);
#9767=ORIENTED_EDGE('',*,*,#7018,.T.);
#9768=ORIENTED_EDGE('',*,*,#7019,.F.);
#9769=ORIENTED_EDGE('',*,*,#7020,.F.);
#9770=ORIENTED_EDGE('',*,*,#7021,.F.);
#9771=ORIENTED_EDGE('',*,*,#7014,.T.);
#9772=ORIENTED_EDGE('',*,*,#7022,.T.);
#9773=ORIENTED_EDGE('',*,*,#7023,.T.);
#9774=ORIENTED_EDGE('',*,*,#7024,.F.);
#9775=ORIENTED_EDGE('',*,*,#7025,.F.);
#9776=ORIENTED_EDGE('',*,*,#7026,.F.);
#9777=ORIENTED_EDGE('',*,*,#7019,.T.);
#9778=ORIENTED_EDGE('',*,*,#7027,.T.);
#9779=ORIENTED_EDGE('',*,*,#7028,.T.);
#9780=ORIENTED_EDGE('',*,*,#7029,.F.);
#9781=ORIENTED_EDGE('',*,*,#7030,.F.);
#9782=ORIENTED_EDGE('',*,*,#7031,.F.);
#9783=ORIENTED_EDGE('',*,*,#7024,.T.);
#9784=ORIENTED_EDGE('',*,*,#7032,.T.);
#9785=ORIENTED_EDGE('',*,*,#7033,.T.);
#9786=ORIENTED_EDGE('',*,*,#7034,.F.);
#9787=ORIENTED_EDGE('',*,*,#7035,.F.);
#9788=ORIENTED_EDGE('',*,*,#7036,.F.);
#9789=ORIENTED_EDGE('',*,*,#7029,.T.);
#9790=ORIENTED_EDGE('',*,*,#7037,.T.);
#9791=ORIENTED_EDGE('',*,*,#7038,.T.);
#9792=ORIENTED_EDGE('',*,*,#7039,.F.);
#9793=ORIENTED_EDGE('',*,*,#7040,.F.);
#9794=ORIENTED_EDGE('',*,*,#7041,.F.);
#9795=ORIENTED_EDGE('',*,*,#7034,.T.);
#9796=ORIENTED_EDGE('',*,*,#7042,.T.);
#9797=ORIENTED_EDGE('',*,*,#7043,.T.);
#9798=ORIENTED_EDGE('',*,*,#7044,.F.);
#9799=ORIENTED_EDGE('',*,*,#7045,.F.);
#9800=ORIENTED_EDGE('',*,*,#7046,.F.);
#9801=ORIENTED_EDGE('',*,*,#7039,.T.);
#9802=ORIENTED_EDGE('',*,*,#7047,.T.);
#9803=ORIENTED_EDGE('',*,*,#7048,.T.);
#9804=ORIENTED_EDGE('',*,*,#7049,.F.);
#9805=ORIENTED_EDGE('',*,*,#7050,.F.);
#9806=ORIENTED_EDGE('',*,*,#7051,.F.);
#9807=ORIENTED_EDGE('',*,*,#7044,.T.);
#9808=ORIENTED_EDGE('',*,*,#7052,.T.);
#9809=ORIENTED_EDGE('',*,*,#7053,.T.);
#9810=ORIENTED_EDGE('',*,*,#7054,.F.);
#9811=ORIENTED_EDGE('',*,*,#7055,.F.);
#9812=ORIENTED_EDGE('',*,*,#7056,.F.);
#9813=ORIENTED_EDGE('',*,*,#7049,.T.);
#9814=ORIENTED_EDGE('',*,*,#7057,.T.);
#9815=ORIENTED_EDGE('',*,*,#7058,.T.);
#9816=ORIENTED_EDGE('',*,*,#7059,.F.);
#9817=ORIENTED_EDGE('',*,*,#7060,.F.);
#9818=ORIENTED_EDGE('',*,*,#7061,.F.);
#9819=ORIENTED_EDGE('',*,*,#7054,.T.);
#9820=ORIENTED_EDGE('',*,*,#7062,.T.);
#9821=ORIENTED_EDGE('',*,*,#7063,.T.);
#9822=ORIENTED_EDGE('',*,*,#7064,.F.);
#9823=ORIENTED_EDGE('',*,*,#7065,.F.);
#9824=ORIENTED_EDGE('',*,*,#7066,.F.);
#9825=ORIENTED_EDGE('',*,*,#7059,.T.);
#9826=ORIENTED_EDGE('',*,*,#7067,.T.);
#9827=ORIENTED_EDGE('',*,*,#7068,.T.);
#9828=ORIENTED_EDGE('',*,*,#7069,.F.);
#9829=ORIENTED_EDGE('',*,*,#7070,.F.);
#9830=ORIENTED_EDGE('',*,*,#7071,.F.);
#9831=ORIENTED_EDGE('',*,*,#7064,.T.);
#9832=ORIENTED_EDGE('',*,*,#7072,.T.);
#9833=ORIENTED_EDGE('',*,*,#7073,.T.);
#9834=ORIENTED_EDGE('',*,*,#7074,.F.);
#9835=ORIENTED_EDGE('',*,*,#7075,.F.);
#9836=ORIENTED_EDGE('',*,*,#7076,.F.);
#9837=ORIENTED_EDGE('',*,*,#7069,.T.);
#9838=ORIENTED_EDGE('',*,*,#7077,.T.);
#9839=ORIENTED_EDGE('',*,*,#7078,.T.);
#9840=ORIENTED_EDGE('',*,*,#7079,.F.);
#9841=ORIENTED_EDGE('',*,*,#7080,.F.);
#9842=ORIENTED_EDGE('',*,*,#7081,.F.);
#9843=ORIENTED_EDGE('',*,*,#7074,.T.);
#9844=ORIENTED_EDGE('',*,*,#7082,.T.);
#9845=ORIENTED_EDGE('',*,*,#7083,.T.);
#9846=ORIENTED_EDGE('',*,*,#7084,.F.);
#9847=ORIENTED_EDGE('',*,*,#7085,.F.);
#9848=ORIENTED_EDGE('',*,*,#7086,.F.);
#9849=ORIENTED_EDGE('',*,*,#7079,.T.);
#9850=ORIENTED_EDGE('',*,*,#7087,.T.);
#9851=ORIENTED_EDGE('',*,*,#7088,.T.);
#9852=ORIENTED_EDGE('',*,*,#7089,.F.);
#9853=ORIENTED_EDGE('',*,*,#7090,.F.);
#9854=ORIENTED_EDGE('',*,*,#7091,.F.);
#9855=ORIENTED_EDGE('',*,*,#7084,.T.);
#9856=ORIENTED_EDGE('',*,*,#7092,.T.);
#9857=ORIENTED_EDGE('',*,*,#7093,.T.);
#9858=ORIENTED_EDGE('',*,*,#7094,.F.);
#9859=ORIENTED_EDGE('',*,*,#7095,.F.);
#9860=ORIENTED_EDGE('',*,*,#7096,.F.);
#9861=ORIENTED_EDGE('',*,*,#7089,.T.);
#9862=ORIENTED_EDGE('',*,*,#7097,.T.);
#9863=ORIENTED_EDGE('',*,*,#7098,.T.);
#9864=ORIENTED_EDGE('',*,*,#7099,.F.);
#9865=ORIENTED_EDGE('',*,*,#7100,.F.);
#9866=ORIENTED_EDGE('',*,*,#7101,.F.);
#9867=ORIENTED_EDGE('',*,*,#7094,.T.);
#9868=ORIENTED_EDGE('',*,*,#7102,.T.);
#9869=ORIENTED_EDGE('',*,*,#7103,.T.);
#9870=ORIENTED_EDGE('',*,*,#7104,.F.);
#9871=ORIENTED_EDGE('',*,*,#7105,.F.);
#9872=ORIENTED_EDGE('',*,*,#7106,.F.);
#9873=ORIENTED_EDGE('',*,*,#7099,.T.);
#9874=ORIENTED_EDGE('',*,*,#7107,.T.);
#9875=ORIENTED_EDGE('',*,*,#7108,.T.);
#9876=ORIENTED_EDGE('',*,*,#7109,.F.);
#9877=ORIENTED_EDGE('',*,*,#7110,.F.);
#9878=ORIENTED_EDGE('',*,*,#7111,.F.);
#9879=ORIENTED_EDGE('',*,*,#7104,.T.);
#9880=ORIENTED_EDGE('',*,*,#7112,.T.);
#9881=ORIENTED_EDGE('',*,*,#7113,.T.);
#9882=ORIENTED_EDGE('',*,*,#7114,.F.);
#9883=ORIENTED_EDGE('',*,*,#7115,.F.);
#9884=ORIENTED_EDGE('',*,*,#7116,.F.);
#9885=ORIENTED_EDGE('',*,*,#7109,.T.);
#9886=ORIENTED_EDGE('',*,*,#7117,.T.);
#9887=ORIENTED_EDGE('',*,*,#7118,.T.);
#9888=ORIENTED_EDGE('',*,*,#7119,.F.);
#9889=ORIENTED_EDGE('',*,*,#7120,.F.);
#9890=ORIENTED_EDGE('',*,*,#7121,.F.);
#9891=ORIENTED_EDGE('',*,*,#7114,.T.);
#9892=ORIENTED_EDGE('',*,*,#7122,.T.);
#9893=ORIENTED_EDGE('',*,*,#7123,.T.);
#9894=ORIENTED_EDGE('',*,*,#7124,.F.);
#9895=ORIENTED_EDGE('',*,*,#7125,.F.);
#9896=ORIENTED_EDGE('',*,*,#7126,.F.);
#9897=ORIENTED_EDGE('',*,*,#7119,.T.);
#9898=ORIENTED_EDGE('',*,*,#7127,.T.);
#9899=ORIENTED_EDGE('',*,*,#7128,.T.);
#9900=ORIENTED_EDGE('',*,*,#7129,.F.);
#9901=ORIENTED_EDGE('',*,*,#7130,.F.);
#9902=ORIENTED_EDGE('',*,*,#7131,.F.);
#9903=ORIENTED_EDGE('',*,*,#7124,.T.);
#9904=ORIENTED_EDGE('',*,*,#7132,.T.);
#9905=ORIENTED_EDGE('',*,*,#7133,.T.);
#9906=ORIENTED_EDGE('',*,*,#7134,.F.);
#9907=ORIENTED_EDGE('',*,*,#7135,.F.);
#9908=ORIENTED_EDGE('',*,*,#7136,.F.);
#9909=ORIENTED_EDGE('',*,*,#7129,.T.);
#9910=ORIENTED_EDGE('',*,*,#7137,.T.);
#9911=ORIENTED_EDGE('',*,*,#7138,.T.);
#9912=ORIENTED_EDGE('',*,*,#7139,.F.);
#9913=ORIENTED_EDGE('',*,*,#7140,.F.);
#9914=ORIENTED_EDGE('',*,*,#7141,.F.);
#9915=ORIENTED_EDGE('',*,*,#7134,.T.);
#9916=ORIENTED_EDGE('',*,*,#7142,.T.);
#9917=ORIENTED_EDGE('',*,*,#7143,.T.);
#9918=ORIENTED_EDGE('',*,*,#7144,.F.);
#9919=ORIENTED_EDGE('',*,*,#7145,.F.);
#9920=ORIENTED_EDGE('',*,*,#7146,.F.);
#9921=ORIENTED_EDGE('',*,*,#7139,.T.);
#9922=ORIENTED_EDGE('',*,*,#7147,.T.);
#9923=ORIENTED_EDGE('',*,*,#7148,.T.);
#9924=ORIENTED_EDGE('',*,*,#7149,.F.);
#9925=ORIENTED_EDGE('',*,*,#7150,.F.);
#9926=ORIENTED_EDGE('',*,*,#7151,.F.);
#9927=ORIENTED_EDGE('',*,*,#7144,.T.);
#9928=ORIENTED_EDGE('',*,*,#7152,.T.);
#9929=ORIENTED_EDGE('',*,*,#7153,.T.);
#9930=ORIENTED_EDGE('',*,*,#7154,.F.);
#9931=ORIENTED_EDGE('',*,*,#7155,.F.);
#9932=ORIENTED_EDGE('',*,*,#7156,.F.);
#9933=ORIENTED_EDGE('',*,*,#7149,.T.);
#9934=ORIENTED_EDGE('',*,*,#7157,.T.);
#9935=ORIENTED_EDGE('',*,*,#7158,.T.);
#9936=ORIENTED_EDGE('',*,*,#7159,.F.);
#9937=ORIENTED_EDGE('',*,*,#7160,.F.);
#9938=ORIENTED_EDGE('',*,*,#7161,.F.);
#9939=ORIENTED_EDGE('',*,*,#7154,.T.);
#9940=ORIENTED_EDGE('',*,*,#7162,.T.);
#9941=ORIENTED_EDGE('',*,*,#7163,.T.);
#9942=ORIENTED_EDGE('',*,*,#7164,.F.);
#9943=ORIENTED_EDGE('',*,*,#7165,.F.);
#9944=ORIENTED_EDGE('',*,*,#7166,.F.);
#9945=ORIENTED_EDGE('',*,*,#7159,.T.);
#9946=ORIENTED_EDGE('',*,*,#7167,.T.);
#9947=ORIENTED_EDGE('',*,*,#7168,.T.);
#9948=ORIENTED_EDGE('',*,*,#7169,.F.);
#9949=ORIENTED_EDGE('',*,*,#7170,.F.);
#9950=ORIENTED_EDGE('',*,*,#7171,.F.);
#9951=ORIENTED_EDGE('',*,*,#7164,.T.);
#9952=ORIENTED_EDGE('',*,*,#7172,.T.);
#9953=ORIENTED_EDGE('',*,*,#7173,.T.);
#9954=ORIENTED_EDGE('',*,*,#7174,.F.);
#9955=ORIENTED_EDGE('',*,*,#7175,.F.);
#9956=ORIENTED_EDGE('',*,*,#7176,.F.);
#9957=ORIENTED_EDGE('',*,*,#7169,.T.);
#9958=ORIENTED_EDGE('',*,*,#7177,.T.);
#9959=ORIENTED_EDGE('',*,*,#7178,.T.);
#9960=ORIENTED_EDGE('',*,*,#7179,.F.);
#9961=ORIENTED_EDGE('',*,*,#7180,.F.);
#9962=ORIENTED_EDGE('',*,*,#7181,.F.);
#9963=ORIENTED_EDGE('',*,*,#7174,.T.);
#9964=ORIENTED_EDGE('',*,*,#7182,.T.);
#9965=ORIENTED_EDGE('',*,*,#7183,.T.);
#9966=ORIENTED_EDGE('',*,*,#7184,.F.);
#9967=ORIENTED_EDGE('',*,*,#7185,.F.);
#9968=ORIENTED_EDGE('',*,*,#7186,.F.);
#9969=ORIENTED_EDGE('',*,*,#7179,.T.);
#9970=ORIENTED_EDGE('',*,*,#7187,.T.);
#9971=ORIENTED_EDGE('',*,*,#7188,.T.);
#9972=ORIENTED_EDGE('',*,*,#7189,.F.);
#9973=ORIENTED_EDGE('',*,*,#7190,.F.);
#9974=ORIENTED_EDGE('',*,*,#7191,.F.);
#9975=ORIENTED_EDGE('',*,*,#7184,.T.);
#9976=ORIENTED_EDGE('',*,*,#7192,.T.);
#9977=ORIENTED_EDGE('',*,*,#7193,.T.);
#9978=ORIENTED_EDGE('',*,*,#7194,.F.);
#9979=ORIENTED_EDGE('',*,*,#7195,.F.);
#9980=ORIENTED_EDGE('',*,*,#7196,.F.);
#9981=ORIENTED_EDGE('',*,*,#7189,.T.);
#9982=ORIENTED_EDGE('',*,*,#7197,.T.);
#9983=ORIENTED_EDGE('',*,*,#7198,.T.);
#9984=ORIENTED_EDGE('',*,*,#7199,.F.);
#9985=ORIENTED_EDGE('',*,*,#7200,.F.);
#9986=ORIENTED_EDGE('',*,*,#7201,.F.);
#9987=ORIENTED_EDGE('',*,*,#7194,.T.);
#9988=ORIENTED_EDGE('',*,*,#7202,.T.);
#9989=ORIENTED_EDGE('',*,*,#7203,.T.);
#9990=ORIENTED_EDGE('',*,*,#7204,.F.);
#9991=ORIENTED_EDGE('',*,*,#7205,.F.);
#9992=ORIENTED_EDGE('',*,*,#7206,.F.);
#9993=ORIENTED_EDGE('',*,*,#7199,.T.);
#9994=ORIENTED_EDGE('',*,*,#7207,.T.);
#9995=ORIENTED_EDGE('',*,*,#7208,.T.);
#9996=ORIENTED_EDGE('',*,*,#7209,.F.);
#9997=ORIENTED_EDGE('',*,*,#7210,.F.);
#9998=ORIENTED_EDGE('',*,*,#7211,.F.);
#9999=ORIENTED_EDGE('',*,*,#7204,.T.);
#10000=ORIENTED_EDGE('',*,*,#7212,.T.);
#10001=ORIENTED_EDGE('',*,*,#7213,.T.);
#10002=ORIENTED_EDGE('',*,*,#7214,.F.);
#10003=ORIENTED_EDGE('',*,*,#7215,.F.);
#10004=ORIENTED_EDGE('',*,*,#7216,.F.);
#10005=ORIENTED_EDGE('',*,*,#7209,.T.);
#10006=ORIENTED_EDGE('',*,*,#7217,.T.);
#10007=ORIENTED_EDGE('',*,*,#7218,.T.);
#10008=ORIENTED_EDGE('',*,*,#7219,.F.);
#10009=ORIENTED_EDGE('',*,*,#7220,.F.);
#10010=ORIENTED_EDGE('',*,*,#7221,.F.);
#10011=ORIENTED_EDGE('',*,*,#7214,.T.);
#10012=ORIENTED_EDGE('',*,*,#7222,.T.);
#10013=ORIENTED_EDGE('',*,*,#7223,.T.);
#10014=ORIENTED_EDGE('',*,*,#7224,.F.);
#10015=ORIENTED_EDGE('',*,*,#7225,.F.);
#10016=ORIENTED_EDGE('',*,*,#7226,.F.);
#10017=ORIENTED_EDGE('',*,*,#7219,.T.);
#10018=ORIENTED_EDGE('',*,*,#7227,.T.);
#10019=ORIENTED_EDGE('',*,*,#7228,.T.);
#10020=ORIENTED_EDGE('',*,*,#7229,.F.);
#10021=ORIENTED_EDGE('',*,*,#7230,.F.);
#10022=ORIENTED_EDGE('',*,*,#7231,.F.);
#10023=ORIENTED_EDGE('',*,*,#7224,.T.);
#10024=ORIENTED_EDGE('',*,*,#7232,.T.);
#10025=ORIENTED_EDGE('',*,*,#7233,.T.);
#10026=ORIENTED_EDGE('',*,*,#7234,.F.);
#10027=ORIENTED_EDGE('',*,*,#7235,.F.);
#10028=ORIENTED_EDGE('',*,*,#7236,.F.);
#10029=ORIENTED_EDGE('',*,*,#7229,.T.);
#10030=ORIENTED_EDGE('',*,*,#7237,.T.);
#10031=ORIENTED_EDGE('',*,*,#7238,.T.);
#10032=ORIENTED_EDGE('',*,*,#7239,.F.);
#10033=ORIENTED_EDGE('',*,*,#7240,.F.);
#10034=ORIENTED_EDGE('',*,*,#7241,.F.);
#10035=ORIENTED_EDGE('',*,*,#7234,.T.);
#10036=ORIENTED_EDGE('',*,*,#7242,.T.);
#10037=ORIENTED_EDGE('',*,*,#7243,.T.);
#10038=ORIENTED_EDGE('',*,*,#7244,.F.);
#10039=ORIENTED_EDGE('',*,*,#7245,.F.);
#10040=ORIENTED_EDGE('',*,*,#7246,.F.);
#10041=ORIENTED_EDGE('',*,*,#7239,.T.);
#10042=ORIENTED_EDGE('',*,*,#7247,.T.);
#10043=ORIENTED_EDGE('',*,*,#7248,.T.);
#10044=ORIENTED_EDGE('',*,*,#7249,.F.);
#10045=ORIENTED_EDGE('',*,*,#7250,.F.);
#10046=ORIENTED_EDGE('',*,*,#7251,.F.);
#10047=ORIENTED_EDGE('',*,*,#7244,.T.);
#10048=ORIENTED_EDGE('',*,*,#7252,.T.);
#10049=ORIENTED_EDGE('',*,*,#7253,.T.);
#10050=ORIENTED_EDGE('',*,*,#7254,.F.);
#10051=ORIENTED_EDGE('',*,*,#7255,.F.);
#10052=ORIENTED_EDGE('',*,*,#7256,.F.);
#10053=ORIENTED_EDGE('',*,*,#7249,.T.);
#10054=ORIENTED_EDGE('',*,*,#7257,.T.);
#10055=ORIENTED_EDGE('',*,*,#7258,.T.);
#10056=ORIENTED_EDGE('',*,*,#7259,.F.);
#10057=ORIENTED_EDGE('',*,*,#7260,.F.);
#10058=ORIENTED_EDGE('',*,*,#7261,.F.);
#10059=ORIENTED_EDGE('',*,*,#7254,.T.);
#10060=ORIENTED_EDGE('',*,*,#7262,.T.);
#10061=ORIENTED_EDGE('',*,*,#7263,.T.);
#10062=ORIENTED_EDGE('',*,*,#7264,.F.);
#10063=ORIENTED_EDGE('',*,*,#7265,.F.);
#10064=ORIENTED_EDGE('',*,*,#7266,.F.);
#10065=ORIENTED_EDGE('',*,*,#7259,.T.);
#10066=ORIENTED_EDGE('',*,*,#7267,.T.);
#10067=ORIENTED_EDGE('',*,*,#7268,.T.);
#10068=ORIENTED_EDGE('',*,*,#7269,.F.);
#10069=ORIENTED_EDGE('',*,*,#7270,.F.);
#10070=ORIENTED_EDGE('',*,*,#7271,.F.);
#10071=ORIENTED_EDGE('',*,*,#7264,.T.);
#10072=ORIENTED_EDGE('',*,*,#7272,.T.);
#10073=ORIENTED_EDGE('',*,*,#7273,.T.);
#10074=ORIENTED_EDGE('',*,*,#7274,.F.);
#10075=ORIENTED_EDGE('',*,*,#7275,.F.);
#10076=ORIENTED_EDGE('',*,*,#7276,.F.);
#10077=ORIENTED_EDGE('',*,*,#7269,.T.);
#10078=ORIENTED_EDGE('',*,*,#7277,.T.);
#10079=ORIENTED_EDGE('',*,*,#7278,.T.);
#10080=ORIENTED_EDGE('',*,*,#7279,.F.);
#10081=ORIENTED_EDGE('',*,*,#7280,.F.);
#10082=ORIENTED_EDGE('',*,*,#7281,.F.);
#10083=ORIENTED_EDGE('',*,*,#7274,.T.);
#10084=ORIENTED_EDGE('',*,*,#7282,.T.);
#10085=ORIENTED_EDGE('',*,*,#7283,.T.);
#10086=ORIENTED_EDGE('',*,*,#7284,.F.);
#10087=ORIENTED_EDGE('',*,*,#7285,.F.);
#10088=ORIENTED_EDGE('',*,*,#7286,.F.);
#10089=ORIENTED_EDGE('',*,*,#7279,.T.);
#10090=ORIENTED_EDGE('',*,*,#7287,.T.);
#10091=ORIENTED_EDGE('',*,*,#7288,.T.);
#10092=ORIENTED_EDGE('',*,*,#7289,.F.);
#10093=ORIENTED_EDGE('',*,*,#7290,.F.);
#10094=ORIENTED_EDGE('',*,*,#7291,.F.);
#10095=ORIENTED_EDGE('',*,*,#7284,.T.);
#10096=ORIENTED_EDGE('',*,*,#7292,.T.);
#10097=ORIENTED_EDGE('',*,*,#7293,.T.);
#10098=ORIENTED_EDGE('',*,*,#7294,.F.);
#10099=ORIENTED_EDGE('',*,*,#7295,.F.);
#10100=ORIENTED_EDGE('',*,*,#7296,.F.);
#10101=ORIENTED_EDGE('',*,*,#7289,.T.);
#10102=ORIENTED_EDGE('',*,*,#7297,.T.);
#10103=ORIENTED_EDGE('',*,*,#7298,.T.);
#10104=ORIENTED_EDGE('',*,*,#7299,.F.);
#10105=ORIENTED_EDGE('',*,*,#7300,.F.);
#10106=ORIENTED_EDGE('',*,*,#7301,.F.);
#10107=ORIENTED_EDGE('',*,*,#7294,.T.);
#10108=ORIENTED_EDGE('',*,*,#7302,.T.);
#10109=ORIENTED_EDGE('',*,*,#7303,.T.);
#10110=ORIENTED_EDGE('',*,*,#7304,.F.);
#10111=ORIENTED_EDGE('',*,*,#7305,.F.);
#10112=ORIENTED_EDGE('',*,*,#7306,.F.);
#10113=ORIENTED_EDGE('',*,*,#7299,.T.);
#10114=ORIENTED_EDGE('',*,*,#7307,.T.);
#10115=ORIENTED_EDGE('',*,*,#7308,.T.);
#10116=ORIENTED_EDGE('',*,*,#7309,.F.);
#10117=ORIENTED_EDGE('',*,*,#7310,.F.);
#10118=ORIENTED_EDGE('',*,*,#7311,.F.);
#10119=ORIENTED_EDGE('',*,*,#7304,.T.);
#10120=ORIENTED_EDGE('',*,*,#7312,.T.);
#10121=ORIENTED_EDGE('',*,*,#7313,.T.);
#10122=ORIENTED_EDGE('',*,*,#7314,.F.);
#10123=ORIENTED_EDGE('',*,*,#7315,.F.);
#10124=ORIENTED_EDGE('',*,*,#7316,.F.);
#10125=ORIENTED_EDGE('',*,*,#7309,.T.);
#10126=ORIENTED_EDGE('',*,*,#7317,.T.);
#10127=ORIENTED_EDGE('',*,*,#7318,.T.);
#10128=ORIENTED_EDGE('',*,*,#7319,.F.);
#10129=ORIENTED_EDGE('',*,*,#7320,.F.);
#10130=ORIENTED_EDGE('',*,*,#7321,.F.);
#10131=ORIENTED_EDGE('',*,*,#7314,.T.);
#10132=ORIENTED_EDGE('',*,*,#7322,.T.);
#10133=ORIENTED_EDGE('',*,*,#7323,.T.);
#10134=ORIENTED_EDGE('',*,*,#7324,.F.);
#10135=ORIENTED_EDGE('',*,*,#7325,.F.);
#10136=ORIENTED_EDGE('',*,*,#7326,.F.);
#10137=ORIENTED_EDGE('',*,*,#7319,.T.);
#10138=ORIENTED_EDGE('',*,*,#7327,.T.);
#10139=ORIENTED_EDGE('',*,*,#7328,.T.);
#10140=ORIENTED_EDGE('',*,*,#7329,.F.);
#10141=ORIENTED_EDGE('',*,*,#7330,.F.);
#10142=ORIENTED_EDGE('',*,*,#7331,.F.);
#10143=ORIENTED_EDGE('',*,*,#7324,.T.);
#10144=ORIENTED_EDGE('',*,*,#7332,.T.);
#10145=ORIENTED_EDGE('',*,*,#7333,.T.);
#10146=ORIENTED_EDGE('',*,*,#7334,.F.);
#10147=ORIENTED_EDGE('',*,*,#7335,.F.);
#10148=ORIENTED_EDGE('',*,*,#7336,.F.);
#10149=ORIENTED_EDGE('',*,*,#7329,.T.);
#10150=ORIENTED_EDGE('',*,*,#7337,.T.);
#10151=ORIENTED_EDGE('',*,*,#7338,.T.);
#10152=ORIENTED_EDGE('',*,*,#7339,.F.);
#10153=ORIENTED_EDGE('',*,*,#7340,.F.);
#10154=ORIENTED_EDGE('',*,*,#7341,.F.);
#10155=ORIENTED_EDGE('',*,*,#7334,.T.);
#10156=ORIENTED_EDGE('',*,*,#7342,.T.);
#10157=ORIENTED_EDGE('',*,*,#7343,.T.);
#10158=ORIENTED_EDGE('',*,*,#7344,.F.);
#10159=ORIENTED_EDGE('',*,*,#7345,.F.);
#10160=ORIENTED_EDGE('',*,*,#7346,.F.);
#10161=ORIENTED_EDGE('',*,*,#7339,.T.);
#10162=ORIENTED_EDGE('',*,*,#7347,.T.);
#10163=ORIENTED_EDGE('',*,*,#7348,.T.);
#10164=ORIENTED_EDGE('',*,*,#7349,.F.);
#10165=ORIENTED_EDGE('',*,*,#7350,.F.);
#10166=ORIENTED_EDGE('',*,*,#7351,.F.);
#10167=ORIENTED_EDGE('',*,*,#7344,.T.);
#10168=ORIENTED_EDGE('',*,*,#7352,.T.);
#10169=ORIENTED_EDGE('',*,*,#7353,.T.);
#10170=ORIENTED_EDGE('',*,*,#7354,.F.);
#10171=ORIENTED_EDGE('',*,*,#7355,.F.);
#10172=ORIENTED_EDGE('',*,*,#7356,.F.);
#10173=ORIENTED_EDGE('',*,*,#7349,.T.);
#10174=ORIENTED_EDGE('',*,*,#7357,.T.);
#10175=ORIENTED_EDGE('',*,*,#7358,.T.);
#10176=ORIENTED_EDGE('',*,*,#7359,.F.);
#10177=ORIENTED_EDGE('',*,*,#7360,.F.);
#10178=ORIENTED_EDGE('',*,*,#7361,.F.);
#10179=ORIENTED_EDGE('',*,*,#7354,.T.);
#10180=ORIENTED_EDGE('',*,*,#7362,.T.);
#10181=ORIENTED_EDGE('',*,*,#7363,.T.);
#10182=ORIENTED_EDGE('',*,*,#7364,.F.);
#10183=ORIENTED_EDGE('',*,*,#7365,.F.);
#10184=ORIENTED_EDGE('',*,*,#7366,.F.);
#10185=ORIENTED_EDGE('',*,*,#7359,.T.);
#10186=ORIENTED_EDGE('',*,*,#7367,.T.);
#10187=ORIENTED_EDGE('',*,*,#7368,.T.);
#10188=ORIENTED_EDGE('',*,*,#7369,.F.);
#10189=ORIENTED_EDGE('',*,*,#7370,.F.);
#10190=ORIENTED_EDGE('',*,*,#7371,.F.);
#10191=ORIENTED_EDGE('',*,*,#7364,.T.);
#10192=ORIENTED_EDGE('',*,*,#7372,.T.);
#10193=ORIENTED_EDGE('',*,*,#7373,.T.);
#10194=ORIENTED_EDGE('',*,*,#7374,.F.);
#10195=ORIENTED_EDGE('',*,*,#7375,.F.);
#10196=ORIENTED_EDGE('',*,*,#7376,.F.);
#10197=ORIENTED_EDGE('',*,*,#7369,.T.);
#10198=ORIENTED_EDGE('',*,*,#7377,.T.);
#10199=ORIENTED_EDGE('',*,*,#7378,.T.);
#10200=ORIENTED_EDGE('',*,*,#7379,.F.);
#10201=ORIENTED_EDGE('',*,*,#7380,.F.);
#10202=ORIENTED_EDGE('',*,*,#7381,.F.);
#10203=ORIENTED_EDGE('',*,*,#7374,.T.);
#10204=ORIENTED_EDGE('',*,*,#7382,.T.);
#10205=ORIENTED_EDGE('',*,*,#7383,.T.);
#10206=ORIENTED_EDGE('',*,*,#7384,.F.);
#10207=ORIENTED_EDGE('',*,*,#7385,.F.);
#10208=ORIENTED_EDGE('',*,*,#7386,.F.);
#10209=ORIENTED_EDGE('',*,*,#7379,.T.);
#10210=ORIENTED_EDGE('',*,*,#7387,.T.);
#10211=ORIENTED_EDGE('',*,*,#7388,.T.);
#10212=ORIENTED_EDGE('',*,*,#7389,.F.);
#10213=ORIENTED_EDGE('',*,*,#7390,.F.);
#10214=ORIENTED_EDGE('',*,*,#7391,.F.);
#10215=ORIENTED_EDGE('',*,*,#7384,.T.);
#10216=ORIENTED_EDGE('',*,*,#7392,.T.);
#10217=ORIENTED_EDGE('',*,*,#7393,.T.);
#10218=ORIENTED_EDGE('',*,*,#7394,.F.);
#10219=ORIENTED_EDGE('',*,*,#7395,.F.);
#10220=ORIENTED_EDGE('',*,*,#7396,.F.);
#10221=ORIENTED_EDGE('',*,*,#7389,.T.);
#10222=ORIENTED_EDGE('',*,*,#7397,.T.);
#10223=ORIENTED_EDGE('',*,*,#7398,.T.);
#10224=ORIENTED_EDGE('',*,*,#7399,.F.);
#10225=ORIENTED_EDGE('',*,*,#7400,.F.);
#10226=ORIENTED_EDGE('',*,*,#7401,.F.);
#10227=ORIENTED_EDGE('',*,*,#7394,.T.);
#10228=ORIENTED_EDGE('',*,*,#7402,.T.);
#10229=ORIENTED_EDGE('',*,*,#7403,.T.);
#10230=ORIENTED_EDGE('',*,*,#7404,.F.);
#10231=ORIENTED_EDGE('',*,*,#7405,.F.);
#10232=ORIENTED_EDGE('',*,*,#7406,.F.);
#10233=ORIENTED_EDGE('',*,*,#7399,.T.);
#10234=ORIENTED_EDGE('',*,*,#7407,.T.);
#10235=ORIENTED_EDGE('',*,*,#7408,.T.);
#10236=ORIENTED_EDGE('',*,*,#7409,.F.);
#10237=ORIENTED_EDGE('',*,*,#7410,.F.);
#10238=ORIENTED_EDGE('',*,*,#7411,.F.);
#10239=ORIENTED_EDGE('',*,*,#7404,.T.);
#10240=ORIENTED_EDGE('',*,*,#7412,.T.);
#10241=ORIENTED_EDGE('',*,*,#7413,.T.);
#10242=ORIENTED_EDGE('',*,*,#7414,.F.);
#10243=ORIENTED_EDGE('',*,*,#7415,.F.);
#10244=ORIENTED_EDGE('',*,*,#7416,.F.);
#10245=ORIENTED_EDGE('',*,*,#7409,.T.);
#10246=ORIENTED_EDGE('',*,*,#7417,.T.);
#10247=ORIENTED_EDGE('',*,*,#7418,.T.);
#10248=ORIENTED_EDGE('',*,*,#7419,.F.);
#10249=ORIENTED_EDGE('',*,*,#7420,.F.);
#10250=ORIENTED_EDGE('',*,*,#7421,.F.);
#10251=ORIENTED_EDGE('',*,*,#7414,.T.);
#10252=ORIENTED_EDGE('',*,*,#7422,.T.);
#10253=ORIENTED_EDGE('',*,*,#7423,.T.);
#10254=ORIENTED_EDGE('',*,*,#7424,.F.);
#10255=ORIENTED_EDGE('',*,*,#7425,.F.);
#10256=ORIENTED_EDGE('',*,*,#7426,.F.);
#10257=ORIENTED_EDGE('',*,*,#7419,.T.);
#10258=ORIENTED_EDGE('',*,*,#7427,.T.);
#10259=ORIENTED_EDGE('',*,*,#7428,.T.);
#10260=ORIENTED_EDGE('',*,*,#7429,.F.);
#10261=ORIENTED_EDGE('',*,*,#7430,.F.);
#10262=ORIENTED_EDGE('',*,*,#7431,.F.);
#10263=ORIENTED_EDGE('',*,*,#7424,.T.);
#10264=ORIENTED_EDGE('',*,*,#7432,.T.);
#10265=ORIENTED_EDGE('',*,*,#7433,.T.);
#10266=ORIENTED_EDGE('',*,*,#7434,.F.);
#10267=ORIENTED_EDGE('',*,*,#7435,.F.);
#10268=ORIENTED_EDGE('',*,*,#7436,.F.);
#10269=ORIENTED_EDGE('',*,*,#7429,.T.);
#10270=ORIENTED_EDGE('',*,*,#7437,.T.);
#10271=ORIENTED_EDGE('',*,*,#7438,.T.);
#10272=ORIENTED_EDGE('',*,*,#7439,.F.);
#10273=ORIENTED_EDGE('',*,*,#7440,.F.);
#10274=ORIENTED_EDGE('',*,*,#7441,.F.);
#10275=ORIENTED_EDGE('',*,*,#7434,.T.);
#10276=ORIENTED_EDGE('',*,*,#7442,.T.);
#10277=ORIENTED_EDGE('',*,*,#7443,.T.);
#10278=ORIENTED_EDGE('',*,*,#7444,.F.);
#10279=ORIENTED_EDGE('',*,*,#7445,.F.);
#10280=ORIENTED_EDGE('',*,*,#7446,.F.);
#10281=ORIENTED_EDGE('',*,*,#7439,.T.);
#10282=ORIENTED_EDGE('',*,*,#7447,.T.);
#10283=ORIENTED_EDGE('',*,*,#7448,.T.);
#10284=ORIENTED_EDGE('',*,*,#7449,.F.);
#10285=ORIENTED_EDGE('',*,*,#7450,.F.);
#10286=ORIENTED_EDGE('',*,*,#7451,.F.);
#10287=ORIENTED_EDGE('',*,*,#7444,.T.);
#10288=ORIENTED_EDGE('',*,*,#7452,.T.);
#10289=ORIENTED_EDGE('',*,*,#7453,.T.);
#10290=ORIENTED_EDGE('',*,*,#7454,.F.);
#10291=ORIENTED_EDGE('',*,*,#7455,.F.);
#10292=ORIENTED_EDGE('',*,*,#7456,.F.);
#10293=ORIENTED_EDGE('',*,*,#7449,.T.);
#10294=ORIENTED_EDGE('',*,*,#7457,.T.);
#10295=ORIENTED_EDGE('',*,*,#7458,.T.);
#10296=ORIENTED_EDGE('',*,*,#7459,.F.);
#10297=ORIENTED_EDGE('',*,*,#7460,.F.);
#10298=ORIENTED_EDGE('',*,*,#7461,.F.);
#10299=ORIENTED_EDGE('',*,*,#7454,.T.);
#10300=ORIENTED_EDGE('',*,*,#7462,.T.);
#10301=ORIENTED_EDGE('',*,*,#7463,.T.);
#10302=ORIENTED_EDGE('',*,*,#7464,.F.);
#10303=ORIENTED_EDGE('',*,*,#7465,.F.);
#10304=ORIENTED_EDGE('',*,*,#7466,.F.);
#10305=ORIENTED_EDGE('',*,*,#7459,.T.);
#10306=ORIENTED_EDGE('',*,*,#7467,.T.);
#10307=ORIENTED_EDGE('',*,*,#7468,.T.);
#10308=ORIENTED_EDGE('',*,*,#7469,.F.);
#10309=ORIENTED_EDGE('',*,*,#7470,.F.);
#10310=ORIENTED_EDGE('',*,*,#7471,.F.);
#10311=ORIENTED_EDGE('',*,*,#7464,.T.);
#10312=ORIENTED_EDGE('',*,*,#7472,.T.);
#10313=ORIENTED_EDGE('',*,*,#7473,.T.);
#10314=ORIENTED_EDGE('',*,*,#7474,.F.);
#10315=ORIENTED_EDGE('',*,*,#7475,.F.);
#10316=ORIENTED_EDGE('',*,*,#7476,.F.);
#10317=ORIENTED_EDGE('',*,*,#7469,.T.);
#10318=ORIENTED_EDGE('',*,*,#7477,.T.);
#10319=ORIENTED_EDGE('',*,*,#7478,.T.);
#10320=ORIENTED_EDGE('',*,*,#7479,.F.);
#10321=ORIENTED_EDGE('',*,*,#7480,.F.);
#10322=ORIENTED_EDGE('',*,*,#7481,.F.);
#10323=ORIENTED_EDGE('',*,*,#7474,.T.);
#10324=ORIENTED_EDGE('',*,*,#7482,.T.);
#10325=ORIENTED_EDGE('',*,*,#7483,.T.);
#10326=ORIENTED_EDGE('',*,*,#7484,.F.);
#10327=ORIENTED_EDGE('',*,*,#7485,.F.);
#10328=ORIENTED_EDGE('',*,*,#7486,.F.);
#10329=ORIENTED_EDGE('',*,*,#7479,.T.);
#10330=ORIENTED_EDGE('',*,*,#7487,.T.);
#10331=ORIENTED_EDGE('',*,*,#7488,.T.);
#10332=ORIENTED_EDGE('',*,*,#7489,.F.);
#10333=ORIENTED_EDGE('',*,*,#7490,.F.);
#10334=ORIENTED_EDGE('',*,*,#7491,.F.);
#10335=ORIENTED_EDGE('',*,*,#7484,.T.);
#10336=ORIENTED_EDGE('',*,*,#7492,.T.);
#10337=ORIENTED_EDGE('',*,*,#7493,.T.);
#10338=ORIENTED_EDGE('',*,*,#7494,.F.);
#10339=ORIENTED_EDGE('',*,*,#7495,.F.);
#10340=ORIENTED_EDGE('',*,*,#7496,.F.);
#10341=ORIENTED_EDGE('',*,*,#7489,.T.);
#10342=ORIENTED_EDGE('',*,*,#7497,.T.);
#10343=ORIENTED_EDGE('',*,*,#7498,.T.);
#10344=ORIENTED_EDGE('',*,*,#7499,.F.);
#10345=ORIENTED_EDGE('',*,*,#7500,.F.);
#10346=ORIENTED_EDGE('',*,*,#7501,.F.);
#10347=ORIENTED_EDGE('',*,*,#7494,.T.);
#10348=ORIENTED_EDGE('',*,*,#7502,.T.);
#10349=ORIENTED_EDGE('',*,*,#7503,.T.);
#10350=ORIENTED_EDGE('',*,*,#7504,.F.);
#10351=ORIENTED_EDGE('',*,*,#7505,.F.);
#10352=ORIENTED_EDGE('',*,*,#7506,.F.);
#10353=ORIENTED_EDGE('',*,*,#7499,.T.);
#10354=ORIENTED_EDGE('',*,*,#7507,.T.);
#10355=ORIENTED_EDGE('',*,*,#7508,.T.);
#10356=ORIENTED_EDGE('',*,*,#7509,.F.);
#10357=ORIENTED_EDGE('',*,*,#7510,.F.);
#10358=ORIENTED_EDGE('',*,*,#7511,.F.);
#10359=ORIENTED_EDGE('',*,*,#7504,.T.);
#10360=ORIENTED_EDGE('',*,*,#7512,.T.);
#10361=ORIENTED_EDGE('',*,*,#7513,.T.);
#10362=ORIENTED_EDGE('',*,*,#7514,.F.);
#10363=ORIENTED_EDGE('',*,*,#7515,.F.);
#10364=ORIENTED_EDGE('',*,*,#7516,.F.);
#10365=ORIENTED_EDGE('',*,*,#7509,.T.);
#10366=ORIENTED_EDGE('',*,*,#7517,.T.);
#10367=ORIENTED_EDGE('',*,*,#7518,.T.);
#10368=ORIENTED_EDGE('',*,*,#7519,.F.);
#10369=ORIENTED_EDGE('',*,*,#7520,.F.);
#10370=ORIENTED_EDGE('',*,*,#7521,.F.);
#10371=ORIENTED_EDGE('',*,*,#7514,.T.);
#10372=ORIENTED_EDGE('',*,*,#7522,.T.);
#10373=ORIENTED_EDGE('',*,*,#7523,.T.);
#10374=ORIENTED_EDGE('',*,*,#7524,.F.);
#10375=ORIENTED_EDGE('',*,*,#7525,.F.);
#10376=ORIENTED_EDGE('',*,*,#7526,.F.);
#10377=ORIENTED_EDGE('',*,*,#7519,.T.);
#10378=ORIENTED_EDGE('',*,*,#7527,.T.);
#10379=ORIENTED_EDGE('',*,*,#7528,.T.);
#10380=ORIENTED_EDGE('',*,*,#7529,.F.);
#10381=ORIENTED_EDGE('',*,*,#7530,.F.);
#10382=ORIENTED_EDGE('',*,*,#7531,.F.);
#10383=ORIENTED_EDGE('',*,*,#7524,.T.);
#10384=ORIENTED_EDGE('',*,*,#7532,.T.);
#10385=ORIENTED_EDGE('',*,*,#7533,.T.);
#10386=ORIENTED_EDGE('',*,*,#7534,.F.);
#10387=ORIENTED_EDGE('',*,*,#7535,.F.);
#10388=ORIENTED_EDGE('',*,*,#7536,.F.);
#10389=ORIENTED_EDGE('',*,*,#7529,.T.);
#10390=ORIENTED_EDGE('',*,*,#7537,.T.);
#10391=ORIENTED_EDGE('',*,*,#7538,.T.);
#10392=ORIENTED_EDGE('',*,*,#7539,.F.);
#10393=ORIENTED_EDGE('',*,*,#7540,.F.);
#10394=ORIENTED_EDGE('',*,*,#7541,.F.);
#10395=ORIENTED_EDGE('',*,*,#7534,.T.);
#10396=ORIENTED_EDGE('',*,*,#7542,.T.);
#10397=ORIENTED_EDGE('',*,*,#7543,.T.);
#10398=ORIENTED_EDGE('',*,*,#7544,.F.);
#10399=ORIENTED_EDGE('',*,*,#7545,.F.);
#10400=ORIENTED_EDGE('',*,*,#7546,.F.);
#10401=ORIENTED_EDGE('',*,*,#7539,.T.);
#10402=ORIENTED_EDGE('',*,*,#7547,.T.);
#10403=ORIENTED_EDGE('',*,*,#7548,.T.);
#10404=ORIENTED_EDGE('',*,*,#7549,.F.);
#10405=ORIENTED_EDGE('',*,*,#7550,.F.);
#10406=ORIENTED_EDGE('',*,*,#7551,.F.);
#10407=ORIENTED_EDGE('',*,*,#7544,.T.);
#10408=ORIENTED_EDGE('',*,*,#7552,.T.);
#10409=ORIENTED_EDGE('',*,*,#7553,.T.);
#10410=ORIENTED_EDGE('',*,*,#7554,.F.);
#10411=ORIENTED_EDGE('',*,*,#7555,.F.);
#10412=ORIENTED_EDGE('',*,*,#7556,.F.);
#10413=ORIENTED_EDGE('',*,*,#7549,.T.);
#10414=ORIENTED_EDGE('',*,*,#7557,.T.);
#10415=ORIENTED_EDGE('',*,*,#7558,.T.);
#10416=ORIENTED_EDGE('',*,*,#7559,.F.);
#10417=ORIENTED_EDGE('',*,*,#7560,.F.);
#10418=ORIENTED_EDGE('',*,*,#7561,.F.);
#10419=ORIENTED_EDGE('',*,*,#7554,.T.);
#10420=ORIENTED_EDGE('',*,*,#7562,.T.);
#10421=ORIENTED_EDGE('',*,*,#7563,.T.);
#10422=ORIENTED_EDGE('',*,*,#7564,.F.);
#10423=ORIENTED_EDGE('',*,*,#7565,.F.);
#10424=ORIENTED_EDGE('',*,*,#7566,.F.);
#10425=ORIENTED_EDGE('',*,*,#7559,.T.);
#10426=ORIENTED_EDGE('',*,*,#7567,.T.);
#10427=ORIENTED_EDGE('',*,*,#7568,.T.);
#10428=ORIENTED_EDGE('',*,*,#7569,.F.);
#10429=ORIENTED_EDGE('',*,*,#7570,.F.);
#10430=ORIENTED_EDGE('',*,*,#7571,.F.);
#10431=ORIENTED_EDGE('',*,*,#7564,.T.);
#10432=ORIENTED_EDGE('',*,*,#7572,.T.);
#10433=ORIENTED_EDGE('',*,*,#7573,.T.);
#10434=ORIENTED_EDGE('',*,*,#7574,.F.);
#10435=ORIENTED_EDGE('',*,*,#7575,.F.);
#10436=ORIENTED_EDGE('',*,*,#7576,.F.);
#10437=ORIENTED_EDGE('',*,*,#7569,.T.);
#10438=ORIENTED_EDGE('',*,*,#7577,.T.);
#10439=ORIENTED_EDGE('',*,*,#7578,.T.);
#10440=ORIENTED_EDGE('',*,*,#7579,.F.);
#10441=ORIENTED_EDGE('',*,*,#7580,.F.);
#10442=ORIENTED_EDGE('',*,*,#7581,.F.);
#10443=ORIENTED_EDGE('',*,*,#7574,.T.);
#10444=ORIENTED_EDGE('',*,*,#7582,.T.);
#10445=ORIENTED_EDGE('',*,*,#7583,.T.);
#10446=ORIENTED_EDGE('',*,*,#7584,.F.);
#10447=ORIENTED_EDGE('',*,*,#7585,.F.);
#10448=ORIENTED_EDGE('',*,*,#7586,.F.);
#10449=ORIENTED_EDGE('',*,*,#7579,.T.);
#10450=ORIENTED_EDGE('',*,*,#7587,.T.);
#10451=ORIENTED_EDGE('',*,*,#7588,.T.);
#10452=ORIENTED_EDGE('',*,*,#7589,.F.);
#10453=ORIENTED_EDGE('',*,*,#7590,.F.);
#10454=ORIENTED_EDGE('',*,*,#7591,.F.);
#10455=ORIENTED_EDGE('',*,*,#7584,.T.);
#10456=ORIENTED_EDGE('',*,*,#7592,.T.);
#10457=ORIENTED_EDGE('',*,*,#7593,.T.);
#10458=ORIENTED_EDGE('',*,*,#7594,.F.);
#10459=ORIENTED_EDGE('',*,*,#7595,.F.);
#10460=ORIENTED_EDGE('',*,*,#7596,.F.);
#10461=ORIENTED_EDGE('',*,*,#7589,.T.);
#10462=ORIENTED_EDGE('',*,*,#7597,.T.);
#10463=ORIENTED_EDGE('',*,*,#7598,.T.);
#10464=ORIENTED_EDGE('',*,*,#7599,.F.);
#10465=ORIENTED_EDGE('',*,*,#7600,.F.);
#10466=ORIENTED_EDGE('',*,*,#7601,.F.);
#10467=ORIENTED_EDGE('',*,*,#7594,.T.);
#10468=ORIENTED_EDGE('',*,*,#7602,.T.);
#10469=ORIENTED_EDGE('',*,*,#7603,.T.);
#10470=ORIENTED_EDGE('',*,*,#7604,.F.);
#10471=ORIENTED_EDGE('',*,*,#7605,.F.);
#10472=ORIENTED_EDGE('',*,*,#7606,.F.);
#10473=ORIENTED_EDGE('',*,*,#7599,.T.);
#10474=ORIENTED_EDGE('',*,*,#7607,.T.);
#10475=ORIENTED_EDGE('',*,*,#7608,.T.);
#10476=ORIENTED_EDGE('',*,*,#7609,.F.);
#10477=ORIENTED_EDGE('',*,*,#7610,.F.);
#10478=ORIENTED_EDGE('',*,*,#7611,.F.);
#10479=ORIENTED_EDGE('',*,*,#7604,.T.);
#10480=ORIENTED_EDGE('',*,*,#7612,.T.);
#10481=ORIENTED_EDGE('',*,*,#7613,.T.);
#10482=ORIENTED_EDGE('',*,*,#7614,.F.);
#10483=ORIENTED_EDGE('',*,*,#7615,.F.);
#10484=ORIENTED_EDGE('',*,*,#7616,.F.);
#10485=ORIENTED_EDGE('',*,*,#7609,.T.);
#10486=ORIENTED_EDGE('',*,*,#7617,.T.);
#10487=ORIENTED_EDGE('',*,*,#7618,.T.);
#10488=ORIENTED_EDGE('',*,*,#7619,.F.);
#10489=ORIENTED_EDGE('',*,*,#7620,.F.);
#10490=ORIENTED_EDGE('',*,*,#7621,.F.);
#10491=ORIENTED_EDGE('',*,*,#7614,.T.);
#10492=ORIENTED_EDGE('',*,*,#7622,.T.);
#10493=ORIENTED_EDGE('',*,*,#7623,.T.);
#10494=ORIENTED_EDGE('',*,*,#7624,.F.);
#10495=ORIENTED_EDGE('',*,*,#7625,.F.);
#10496=ORIENTED_EDGE('',*,*,#7626,.F.);
#10497=ORIENTED_EDGE('',*,*,#7619,.T.);
#10498=ORIENTED_EDGE('',*,*,#7627,.T.);
#10499=ORIENTED_EDGE('',*,*,#7628,.T.);
#10500=ORIENTED_EDGE('',*,*,#7629,.F.);
#10501=ORIENTED_EDGE('',*,*,#7630,.F.);
#10502=ORIENTED_EDGE('',*,*,#7631,.F.);
#10503=ORIENTED_EDGE('',*,*,#7624,.T.);
#10504=ORIENTED_EDGE('',*,*,#7632,.T.);
#10505=ORIENTED_EDGE('',*,*,#7633,.T.);
#10506=ORIENTED_EDGE('',*,*,#7634,.F.);
#10507=ORIENTED_EDGE('',*,*,#7635,.F.);
#10508=ORIENTED_EDGE('',*,*,#7636,.F.);
#10509=ORIENTED_EDGE('',*,*,#7629,.T.);
#10510=ORIENTED_EDGE('',*,*,#7637,.T.);
#10511=ORIENTED_EDGE('',*,*,#7638,.T.);
#10512=ORIENTED_EDGE('',*,*,#7639,.F.);
#10513=ORIENTED_EDGE('',*,*,#7640,.F.);
#10514=ORIENTED_EDGE('',*,*,#7641,.F.);
#10515=ORIENTED_EDGE('',*,*,#7634,.T.);
#10516=ORIENTED_EDGE('',*,*,#7642,.T.);
#10517=ORIENTED_EDGE('',*,*,#7643,.T.);
#10518=ORIENTED_EDGE('',*,*,#7644,.F.);
#10519=ORIENTED_EDGE('',*,*,#7645,.F.);
#10520=ORIENTED_EDGE('',*,*,#7646,.F.);
#10521=ORIENTED_EDGE('',*,*,#7639,.T.);
#10522=ORIENTED_EDGE('',*,*,#7647,.T.);
#10523=ORIENTED_EDGE('',*,*,#7648,.T.);
#10524=ORIENTED_EDGE('',*,*,#7649,.F.);
#10525=ORIENTED_EDGE('',*,*,#7650,.F.);
#10526=ORIENTED_EDGE('',*,*,#7651,.F.);
#10527=ORIENTED_EDGE('',*,*,#7644,.T.);
#10528=ORIENTED_EDGE('',*,*,#7652,.T.);
#10529=ORIENTED_EDGE('',*,*,#7653,.T.);
#10530=ORIENTED_EDGE('',*,*,#7654,.F.);
#10531=ORIENTED_EDGE('',*,*,#7655,.F.);
#10532=ORIENTED_EDGE('',*,*,#7656,.F.);
#10533=ORIENTED_EDGE('',*,*,#7649,.T.);
#10534=ORIENTED_EDGE('',*,*,#7657,.T.);
#10535=ORIENTED_EDGE('',*,*,#7658,.T.);
#10536=ORIENTED_EDGE('',*,*,#7659,.F.);
#10537=ORIENTED_EDGE('',*,*,#7660,.F.);
#10538=ORIENTED_EDGE('',*,*,#7661,.F.);
#10539=ORIENTED_EDGE('',*,*,#7654,.T.);
#10540=ORIENTED_EDGE('',*,*,#7662,.T.);
#10541=ORIENTED_EDGE('',*,*,#7663,.T.);
#10542=ORIENTED_EDGE('',*,*,#7664,.F.);
#10543=ORIENTED_EDGE('',*,*,#7665,.F.);
#10544=ORIENTED_EDGE('',*,*,#7666,.F.);
#10545=ORIENTED_EDGE('',*,*,#7659,.T.);
#10546=ORIENTED_EDGE('',*,*,#7667,.T.);
#10547=ORIENTED_EDGE('',*,*,#7668,.T.);
#10548=ORIENTED_EDGE('',*,*,#7669,.F.);
#10549=ORIENTED_EDGE('',*,*,#7670,.F.);
#10550=ORIENTED_EDGE('',*,*,#7671,.F.);
#10551=ORIENTED_EDGE('',*,*,#7664,.T.);
#10552=ORIENTED_EDGE('',*,*,#7672,.T.);
#10553=ORIENTED_EDGE('',*,*,#7673,.T.);
#10554=ORIENTED_EDGE('',*,*,#7674,.F.);
#10555=ORIENTED_EDGE('',*,*,#7675,.F.);
#10556=ORIENTED_EDGE('',*,*,#7676,.F.);
#10557=ORIENTED_EDGE('',*,*,#7669,.T.);
#10558=ORIENTED_EDGE('',*,*,#7677,.T.);
#10559=ORIENTED_EDGE('',*,*,#7678,.T.);
#10560=ORIENTED_EDGE('',*,*,#7679,.F.);
#10561=ORIENTED_EDGE('',*,*,#7680,.F.);
#10562=ORIENTED_EDGE('',*,*,#7681,.F.);
#10563=ORIENTED_EDGE('',*,*,#7674,.T.);
#10564=ORIENTED_EDGE('',*,*,#7682,.T.);
#10565=ORIENTED_EDGE('',*,*,#7683,.T.);
#10566=ORIENTED_EDGE('',*,*,#7684,.F.);
#10567=ORIENTED_EDGE('',*,*,#7685,.F.);
#10568=ORIENTED_EDGE('',*,*,#7686,.F.);
#10569=ORIENTED_EDGE('',*,*,#7679,.T.);
#10570=ORIENTED_EDGE('',*,*,#7687,.T.);
#10571=ORIENTED_EDGE('',*,*,#7688,.T.);
#10572=ORIENTED_EDGE('',*,*,#7689,.F.);
#10573=ORIENTED_EDGE('',*,*,#7690,.F.);
#10574=ORIENTED_EDGE('',*,*,#7691,.F.);
#10575=ORIENTED_EDGE('',*,*,#7684,.T.);
#10576=ORIENTED_EDGE('',*,*,#7692,.T.);
#10577=ORIENTED_EDGE('',*,*,#7693,.T.);
#10578=ORIENTED_EDGE('',*,*,#7694,.F.);
#10579=ORIENTED_EDGE('',*,*,#7695,.F.);
#10580=ORIENTED_EDGE('',*,*,#7696,.F.);
#10581=ORIENTED_EDGE('',*,*,#7689,.T.);
#10582=ORIENTED_EDGE('',*,*,#7697,.T.);
#10583=ORIENTED_EDGE('',*,*,#7698,.T.);
#10584=ORIENTED_EDGE('',*,*,#7699,.F.);
#10585=ORIENTED_EDGE('',*,*,#7700,.F.);
#10586=ORIENTED_EDGE('',*,*,#7701,.F.);
#10587=ORIENTED_EDGE('',*,*,#7694,.T.);
#10588=ORIENTED_EDGE('',*,*,#7702,.T.);
#10589=ORIENTED_EDGE('',*,*,#7703,.T.);
#10590=ORIENTED_EDGE('',*,*,#7704,.F.);
#10591=ORIENTED_EDGE('',*,*,#7705,.F.);
#10592=ORIENTED_EDGE('',*,*,#7706,.F.);
#10593=ORIENTED_EDGE('',*,*,#7699,.T.);
#10594=ORIENTED_EDGE('',*,*,#7707,.T.);
#10595=ORIENTED_EDGE('',*,*,#7708,.T.);
#10596=ORIENTED_EDGE('',*,*,#7709,.F.);
#10597=ORIENTED_EDGE('',*,*,#7710,.F.);
#10598=ORIENTED_EDGE('',*,*,#7711,.F.);
#10599=ORIENTED_EDGE('',*,*,#7704,.T.);
#10600=ORIENTED_EDGE('',*,*,#7712,.T.);
#10601=ORIENTED_EDGE('',*,*,#7713,.T.);
#10602=ORIENTED_EDGE('',*,*,#7714,.F.);
#10603=ORIENTED_EDGE('',*,*,#7715,.F.);
#10604=ORIENTED_EDGE('',*,*,#7716,.F.);
#10605=ORIENTED_EDGE('',*,*,#7709,.T.);
#10606=ORIENTED_EDGE('',*,*,#7717,.T.);
#10607=ORIENTED_EDGE('',*,*,#7718,.T.);
#10608=ORIENTED_EDGE('',*,*,#7719,.F.);
#10609=ORIENTED_EDGE('',*,*,#7720,.F.);
#10610=ORIENTED_EDGE('',*,*,#7721,.F.);
#10611=ORIENTED_EDGE('',*,*,#7714,.T.);
#10612=ORIENTED_EDGE('',*,*,#7722,.T.);
#10613=ORIENTED_EDGE('',*,*,#7723,.T.);
#10614=ORIENTED_EDGE('',*,*,#7724,.F.);
#10615=ORIENTED_EDGE('',*,*,#7725,.F.);
#10616=ORIENTED_EDGE('',*,*,#7726,.F.);
#10617=ORIENTED_EDGE('',*,*,#7719,.T.);
#10618=ORIENTED_EDGE('',*,*,#7727,.T.);
#10619=ORIENTED_EDGE('',*,*,#7728,.T.);
#10620=ORIENTED_EDGE('',*,*,#7729,.F.);
#10621=ORIENTED_EDGE('',*,*,#7730,.F.);
#10622=ORIENTED_EDGE('',*,*,#7731,.F.);
#10623=ORIENTED_EDGE('',*,*,#7724,.T.);
#10624=ORIENTED_EDGE('',*,*,#7732,.T.);
#10625=ORIENTED_EDGE('',*,*,#7733,.T.);
#10626=ORIENTED_EDGE('',*,*,#7734,.F.);
#10627=ORIENTED_EDGE('',*,*,#7735,.F.);
#10628=ORIENTED_EDGE('',*,*,#7736,.F.);
#10629=ORIENTED_EDGE('',*,*,#7729,.T.);
#10630=ORIENTED_EDGE('',*,*,#7737,.T.);
#10631=ORIENTED_EDGE('',*,*,#7738,.T.);
#10632=ORIENTED_EDGE('',*,*,#7739,.F.);
#10633=ORIENTED_EDGE('',*,*,#7740,.F.);
#10634=ORIENTED_EDGE('',*,*,#7741,.F.);
#10635=ORIENTED_EDGE('',*,*,#7734,.T.);
#10636=ORIENTED_EDGE('',*,*,#7742,.T.);
#10637=ORIENTED_EDGE('',*,*,#7743,.T.);
#10638=ORIENTED_EDGE('',*,*,#7744,.F.);
#10639=ORIENTED_EDGE('',*,*,#7745,.F.);
#10640=ORIENTED_EDGE('',*,*,#7746,.F.);
#10641=ORIENTED_EDGE('',*,*,#7739,.T.);
#10642=ORIENTED_EDGE('',*,*,#7747,.T.);
#10643=ORIENTED_EDGE('',*,*,#7748,.T.);
#10644=ORIENTED_EDGE('',*,*,#7749,.F.);
#10645=ORIENTED_EDGE('',*,*,#7750,.F.);
#10646=ORIENTED_EDGE('',*,*,#7751,.F.);
#10647=ORIENTED_EDGE('',*,*,#7744,.T.);
#10648=ORIENTED_EDGE('',*,*,#7752,.T.);
#10649=ORIENTED_EDGE('',*,*,#7753,.T.);
#10650=ORIENTED_EDGE('',*,*,#7754,.F.);
#10651=ORIENTED_EDGE('',*,*,#7755,.F.);
#10652=ORIENTED_EDGE('',*,*,#7756,.F.);
#10653=ORIENTED_EDGE('',*,*,#7749,.T.);
#10654=ORIENTED_EDGE('',*,*,#7757,.T.);
#10655=ORIENTED_EDGE('',*,*,#7758,.T.);
#10656=ORIENTED_EDGE('',*,*,#7759,.F.);
#10657=ORIENTED_EDGE('',*,*,#7760,.F.);
#10658=ORIENTED_EDGE('',*,*,#7761,.F.);
#10659=ORIENTED_EDGE('',*,*,#7754,.T.);
#10660=ORIENTED_EDGE('',*,*,#7762,.T.);
#10661=ORIENTED_EDGE('',*,*,#7763,.T.);
#10662=ORIENTED_EDGE('',*,*,#7764,.F.);
#10663=ORIENTED_EDGE('',*,*,#7765,.F.);
#10664=ORIENTED_EDGE('',*,*,#7766,.F.);
#10665=ORIENTED_EDGE('',*,*,#7759,.T.);
#10666=ORIENTED_EDGE('',*,*,#7767,.T.);
#10667=ORIENTED_EDGE('',*,*,#7768,.T.);
#10668=ORIENTED_EDGE('',*,*,#7769,.F.);
#10669=ORIENTED_EDGE('',*,*,#7770,.F.);
#10670=ORIENTED_EDGE('',*,*,#7771,.F.);
#10671=ORIENTED_EDGE('',*,*,#7764,.T.);
#10672=ORIENTED_EDGE('',*,*,#7772,.T.);
#10673=ORIENTED_EDGE('',*,*,#7773,.T.);
#10674=ORIENTED_EDGE('',*,*,#7774,.F.);
#10675=ORIENTED_EDGE('',*,*,#7775,.F.);
#10676=ORIENTED_EDGE('',*,*,#7776,.F.);
#10677=ORIENTED_EDGE('',*,*,#7769,.T.);
#10678=ORIENTED_EDGE('',*,*,#7777,.T.);
#10679=ORIENTED_EDGE('',*,*,#7778,.T.);
#10680=ORIENTED_EDGE('',*,*,#7779,.F.);
#10681=ORIENTED_EDGE('',*,*,#7780,.F.);
#10682=ORIENTED_EDGE('',*,*,#7781,.F.);
#10683=ORIENTED_EDGE('',*,*,#7774,.T.);
#10684=ORIENTED_EDGE('',*,*,#7782,.T.);
#10685=ORIENTED_EDGE('',*,*,#7783,.T.);
#10686=ORIENTED_EDGE('',*,*,#7784,.F.);
#10687=ORIENTED_EDGE('',*,*,#7785,.F.);
#10688=ORIENTED_EDGE('',*,*,#7786,.F.);
#10689=ORIENTED_EDGE('',*,*,#7779,.T.);
#10690=ORIENTED_EDGE('',*,*,#7787,.T.);
#10691=ORIENTED_EDGE('',*,*,#7788,.T.);
#10692=ORIENTED_EDGE('',*,*,#7789,.F.);
#10693=ORIENTED_EDGE('',*,*,#7790,.F.);
#10694=ORIENTED_EDGE('',*,*,#7791,.F.);
#10695=ORIENTED_EDGE('',*,*,#7784,.T.);
#10696=ORIENTED_EDGE('',*,*,#7792,.T.);
#10697=ORIENTED_EDGE('',*,*,#7793,.T.);
#10698=ORIENTED_EDGE('',*,*,#7794,.F.);
#10699=ORIENTED_EDGE('',*,*,#7795,.F.);
#10700=ORIENTED_EDGE('',*,*,#7796,.F.);
#10701=ORIENTED_EDGE('',*,*,#7789,.T.);
#10702=ORIENTED_EDGE('',*,*,#7797,.T.);
#10703=ORIENTED_EDGE('',*,*,#7798,.T.);
#10704=ORIENTED_EDGE('',*,*,#7799,.F.);
#10705=ORIENTED_EDGE('',*,*,#7800,.F.);
#10706=ORIENTED_EDGE('',*,*,#7801,.F.);
#10707=ORIENTED_EDGE('',*,*,#7794,.T.);
#10708=ORIENTED_EDGE('',*,*,#7802,.T.);
#10709=ORIENTED_EDGE('',*,*,#7803,.T.);
#10710=ORIENTED_EDGE('',*,*,#7804,.F.);
#10711=ORIENTED_EDGE('',*,*,#7805,.F.);
#10712=ORIENTED_EDGE('',*,*,#7806,.F.);
#10713=ORIENTED_EDGE('',*,*,#7799,.T.);
#10714=ORIENTED_EDGE('',*,*,#7807,.T.);
#10715=ORIENTED_EDGE('',*,*,#7808,.T.);
#10716=ORIENTED_EDGE('',*,*,#7809,.F.);
#10717=ORIENTED_EDGE('',*,*,#7810,.F.);
#10718=ORIENTED_EDGE('',*,*,#7811,.F.);
#10719=ORIENTED_EDGE('',*,*,#7804,.T.);
#10720=ORIENTED_EDGE('',*,*,#7812,.T.);
#10721=ORIENTED_EDGE('',*,*,#7813,.T.);
#10722=ORIENTED_EDGE('',*,*,#7814,.F.);
#10723=ORIENTED_EDGE('',*,*,#7815,.F.);
#10724=ORIENTED_EDGE('',*,*,#7816,.F.);
#10725=ORIENTED_EDGE('',*,*,#7809,.T.);
#10726=ORIENTED_EDGE('',*,*,#7817,.T.);
#10727=ORIENTED_EDGE('',*,*,#7818,.T.);
#10728=ORIENTED_EDGE('',*,*,#7819,.F.);
#10729=ORIENTED_EDGE('',*,*,#7820,.F.);
#10730=ORIENTED_EDGE('',*,*,#7821,.F.);
#10731=ORIENTED_EDGE('',*,*,#7814,.T.);
#10732=ORIENTED_EDGE('',*,*,#7822,.T.);
#10733=ORIENTED_EDGE('',*,*,#7823,.T.);
#10734=ORIENTED_EDGE('',*,*,#7824,.F.);
#10735=ORIENTED_EDGE('',*,*,#7825,.F.);
#10736=ORIENTED_EDGE('',*,*,#7826,.F.);
#10737=ORIENTED_EDGE('',*,*,#7819,.T.);
#10738=ORIENTED_EDGE('',*,*,#7827,.T.);
#10739=ORIENTED_EDGE('',*,*,#7828,.T.);
#10740=ORIENTED_EDGE('',*,*,#7829,.F.);
#10741=ORIENTED_EDGE('',*,*,#7830,.F.);
#10742=ORIENTED_EDGE('',*,*,#7831,.F.);
#10743=ORIENTED_EDGE('',*,*,#7824,.T.);
#10744=ORIENTED_EDGE('',*,*,#7832,.T.);
#10745=ORIENTED_EDGE('',*,*,#7833,.T.);
#10746=ORIENTED_EDGE('',*,*,#7834,.T.);
#10747=ORIENTED_EDGE('',*,*,#7835,.F.);
#10748=ORIENTED_EDGE('',*,*,#7836,.T.);
#10749=ORIENTED_EDGE('',*,*,#7837,.T.);
#10750=ORIENTED_EDGE('',*,*,#7838,.T.);
#10751=ORIENTED_EDGE('',*,*,#7839,.T.);
#10752=ORIENTED_EDGE('',*,*,#7840,.T.);
#10753=ORIENTED_EDGE('',*,*,#7841,.T.);
#10754=ORIENTED_EDGE('',*,*,#7842,.T.);
#10755=ORIENTED_EDGE('',*,*,#7843,.T.);
#10756=ORIENTED_EDGE('',*,*,#7844,.T.);
#10757=ORIENTED_EDGE('',*,*,#7845,.T.);
#10758=ORIENTED_EDGE('',*,*,#7846,.T.);
#10759=ORIENTED_EDGE('',*,*,#7847,.T.);
#10760=ORIENTED_EDGE('',*,*,#7848,.T.);
#10761=ORIENTED_EDGE('',*,*,#7849,.T.);
#10762=ORIENTED_EDGE('',*,*,#7850,.T.);
#10763=ORIENTED_EDGE('',*,*,#7851,.T.);
#10764=ORIENTED_EDGE('',*,*,#7852,.T.);
#10765=ORIENTED_EDGE('',*,*,#7853,.T.);
#10766=ORIENTED_EDGE('',*,*,#7854,.T.);
#10767=ORIENTED_EDGE('',*,*,#7855,.T.);
#10768=ORIENTED_EDGE('',*,*,#7856,.T.);
#10769=ORIENTED_EDGE('',*,*,#7857,.T.);
#10770=ORIENTED_EDGE('',*,*,#7858,.T.);
#10771=ORIENTED_EDGE('',*,*,#7859,.T.);
#10772=ORIENTED_EDGE('',*,*,#7860,.T.);
#10773=ORIENTED_EDGE('',*,*,#7861,.T.);
#10774=ORIENTED_EDGE('',*,*,#7862,.T.);
#10775=ORIENTED_EDGE('',*,*,#7863,.T.);
#10776=ORIENTED_EDGE('',*,*,#7864,.T.);
#10777=ORIENTED_EDGE('',*,*,#7865,.T.);
#10778=ORIENTED_EDGE('',*,*,#7866,.T.);
#10779=ORIENTED_EDGE('',*,*,#7867,.T.);
#10780=ORIENTED_EDGE('',*,*,#7868,.T.);
#10781=ORIENTED_EDGE('',*,*,#7869,.T.);
#10782=ORIENTED_EDGE('',*,*,#7870,.T.);
#10783=ORIENTED_EDGE('',*,*,#7871,.T.);
#10784=ORIENTED_EDGE('',*,*,#7872,.T.);
#10785=ORIENTED_EDGE('',*,*,#7873,.T.);
#10786=ORIENTED_EDGE('',*,*,#7874,.T.);
#10787=ORIENTED_EDGE('',*,*,#7875,.T.);
#10788=ORIENTED_EDGE('',*,*,#7876,.T.);
#10789=ORIENTED_EDGE('',*,*,#7877,.T.);
#10790=ORIENTED_EDGE('',*,*,#7878,.T.);
#10791=ORIENTED_EDGE('',*,*,#7879,.T.);
#10792=ORIENTED_EDGE('',*,*,#7880,.T.);
#10793=ORIENTED_EDGE('',*,*,#7881,.T.);
#10794=ORIENTED_EDGE('',*,*,#7882,.T.);
#10795=ORIENTED_EDGE('',*,*,#7883,.T.);
#10796=ORIENTED_EDGE('',*,*,#7884,.T.);
#10797=ORIENTED_EDGE('',*,*,#7885,.T.);
#10798=ORIENTED_EDGE('',*,*,#7886,.T.);
#10799=ORIENTED_EDGE('',*,*,#7887,.T.);
#10800=ORIENTED_EDGE('',*,*,#7888,.T.);
#10801=ORIENTED_EDGE('',*,*,#7889,.T.);
#10802=ORIENTED_EDGE('',*,*,#7890,.T.);
#10803=ORIENTED_EDGE('',*,*,#7891,.T.);
#10804=ORIENTED_EDGE('',*,*,#7892,.T.);
#10805=ORIENTED_EDGE('',*,*,#7893,.T.);
#10806=ORIENTED_EDGE('',*,*,#7894,.T.);
#10807=ORIENTED_EDGE('',*,*,#7895,.T.);
#10808=ORIENTED_EDGE('',*,*,#7896,.T.);
#10809=ORIENTED_EDGE('',*,*,#7897,.T.);
#10810=ORIENTED_EDGE('',*,*,#7898,.T.);
#10811=ORIENTED_EDGE('',*,*,#7899,.T.);
#10812=ORIENTED_EDGE('',*,*,#7900,.T.);
#10813=ORIENTED_EDGE('',*,*,#7901,.T.);
#10814=ORIENTED_EDGE('',*,*,#7902,.T.);
#10815=ORIENTED_EDGE('',*,*,#7903,.T.);
#10816=ORIENTED_EDGE('',*,*,#7904,.T.);
#10817=ORIENTED_EDGE('',*,*,#7905,.T.);
#10818=ORIENTED_EDGE('',*,*,#7906,.T.);
#10819=ORIENTED_EDGE('',*,*,#7907,.T.);
#10820=ORIENTED_EDGE('',*,*,#7908,.T.);
#10821=ORIENTED_EDGE('',*,*,#7909,.T.);
#10822=ORIENTED_EDGE('',*,*,#7910,.T.);
#10823=ORIENTED_EDGE('',*,*,#7911,.T.);
#10824=ORIENTED_EDGE('',*,*,#7912,.T.);
#10825=ORIENTED_EDGE('',*,*,#7913,.T.);
#10826=ORIENTED_EDGE('',*,*,#7914,.T.);
#10827=ORIENTED_EDGE('',*,*,#7915,.T.);
#10828=ORIENTED_EDGE('',*,*,#7916,.T.);
#10829=ORIENTED_EDGE('',*,*,#7917,.T.);
#10830=ORIENTED_EDGE('',*,*,#7918,.T.);
#10831=ORIENTED_EDGE('',*,*,#7919,.T.);
#10832=ORIENTED_EDGE('',*,*,#7920,.T.);
#10833=ORIENTED_EDGE('',*,*,#7921,.T.);
#10834=ORIENTED_EDGE('',*,*,#7922,.T.);
#10835=ORIENTED_EDGE('',*,*,#7923,.T.);
#10836=ORIENTED_EDGE('',*,*,#7924,.T.);
#10837=ORIENTED_EDGE('',*,*,#7925,.T.);
#10838=ORIENTED_EDGE('',*,*,#7926,.T.);
#10839=ORIENTED_EDGE('',*,*,#7927,.T.);
#10840=ORIENTED_EDGE('',*,*,#7928,.T.);
#10841=ORIENTED_EDGE('',*,*,#7929,.T.);
#10842=ORIENTED_EDGE('',*,*,#7930,.T.);
#10843=ORIENTED_EDGE('',*,*,#7931,.T.);
#10844=ORIENTED_EDGE('',*,*,#7932,.T.);
#10845=ORIENTED_EDGE('',*,*,#7933,.T.);
#10846=ORIENTED_EDGE('',*,*,#7934,.T.);
#10847=ORIENTED_EDGE('',*,*,#7935,.T.);
#10848=ORIENTED_EDGE('',*,*,#7936,.T.);
#10849=ORIENTED_EDGE('',*,*,#7937,.T.);
#10850=ORIENTED_EDGE('',*,*,#7938,.T.);
#10851=ORIENTED_EDGE('',*,*,#7939,.T.);
#10852=ORIENTED_EDGE('',*,*,#7940,.T.);
#10853=ORIENTED_EDGE('',*,*,#7941,.T.);
#10854=ORIENTED_EDGE('',*,*,#7942,.T.);
#10855=ORIENTED_EDGE('',*,*,#7943,.T.);
#10856=ORIENTED_EDGE('',*,*,#7944,.T.);
#10857=ORIENTED_EDGE('',*,*,#7945,.T.);
#10858=ORIENTED_EDGE('',*,*,#7946,.T.);
#10859=ORIENTED_EDGE('',*,*,#7947,.T.);
#10860=ORIENTED_EDGE('',*,*,#7948,.T.);
#10861=ORIENTED_EDGE('',*,*,#7949,.T.);
#10862=ORIENTED_EDGE('',*,*,#7950,.T.);
#10863=ORIENTED_EDGE('',*,*,#7951,.T.);
#10864=ORIENTED_EDGE('',*,*,#7952,.T.);
#10865=ORIENTED_EDGE('',*,*,#7953,.T.);
#10866=ORIENTED_EDGE('',*,*,#7954,.T.);
#10867=ORIENTED_EDGE('',*,*,#7955,.T.);
#10868=ORIENTED_EDGE('',*,*,#7956,.T.);
#10869=ORIENTED_EDGE('',*,*,#7957,.T.);
#10870=ORIENTED_EDGE('',*,*,#7958,.T.);
#10871=ORIENTED_EDGE('',*,*,#7959,.T.);
#10872=ORIENTED_EDGE('',*,*,#7960,.T.);
#10873=ORIENTED_EDGE('',*,*,#7961,.T.);
#10874=ORIENTED_EDGE('',*,*,#7962,.T.);
#10875=ORIENTED_EDGE('',*,*,#7963,.T.);
#10876=ORIENTED_EDGE('',*,*,#7964,.T.);
#10877=ORIENTED_EDGE('',*,*,#7965,.T.);
#10878=ORIENTED_EDGE('',*,*,#7966,.T.);
#10879=ORIENTED_EDGE('',*,*,#7967,.T.);
#10880=ORIENTED_EDGE('',*,*,#7968,.T.);
#10881=ORIENTED_EDGE('',*,*,#7969,.T.);
#10882=ORIENTED_EDGE('',*,*,#7970,.T.);
#10883=ORIENTED_EDGE('',*,*,#7971,.T.);
#10884=ORIENTED_EDGE('',*,*,#7972,.T.);
#10885=ORIENTED_EDGE('',*,*,#7973,.T.);
#10886=ORIENTED_EDGE('',*,*,#7974,.T.);
#10887=ORIENTED_EDGE('',*,*,#7975,.T.);
#10888=ORIENTED_EDGE('',*,*,#7976,.T.);
#10889=ORIENTED_EDGE('',*,*,#7977,.T.);
#10890=ORIENTED_EDGE('',*,*,#7978,.T.);
#10891=ORIENTED_EDGE('',*,*,#7979,.T.);
#10892=ORIENTED_EDGE('',*,*,#7980,.T.);
#10893=ORIENTED_EDGE('',*,*,#7981,.T.);
#10894=ORIENTED_EDGE('',*,*,#7982,.T.);
#10895=ORIENTED_EDGE('',*,*,#7983,.T.);
#10896=ORIENTED_EDGE('',*,*,#7984,.T.);
#10897=ORIENTED_EDGE('',*,*,#7985,.T.);
#10898=ORIENTED_EDGE('',*,*,#7986,.T.);
#10899=ORIENTED_EDGE('',*,*,#7987,.T.);
#10900=ORIENTED_EDGE('',*,*,#7988,.T.);
#10901=ORIENTED_EDGE('',*,*,#7989,.T.);
#10902=ORIENTED_EDGE('',*,*,#7990,.T.);
#10903=ORIENTED_EDGE('',*,*,#7991,.T.);
#10904=ORIENTED_EDGE('',*,*,#7992,.T.);
#10905=ORIENTED_EDGE('',*,*,#7993,.T.);
#10906=ORIENTED_EDGE('',*,*,#7994,.T.);
#10907=ORIENTED_EDGE('',*,*,#7995,.T.);
#10908=ORIENTED_EDGE('',*,*,#7996,.T.);
#10909=ORIENTED_EDGE('',*,*,#7997,.T.);
#10910=ORIENTED_EDGE('',*,*,#7998,.T.);
#10911=ORIENTED_EDGE('',*,*,#7999,.T.);
#10912=ORIENTED_EDGE('',*,*,#8000,.T.);
#10913=ORIENTED_EDGE('',*,*,#8001,.T.);
#10914=ORIENTED_EDGE('',*,*,#8002,.T.);
#10915=ORIENTED_EDGE('',*,*,#8003,.T.);
#10916=ORIENTED_EDGE('',*,*,#8004,.T.);
#10917=ORIENTED_EDGE('',*,*,#8005,.T.);
#10918=ORIENTED_EDGE('',*,*,#8006,.T.);
#10919=ORIENTED_EDGE('',*,*,#8007,.T.);
#10920=ORIENTED_EDGE('',*,*,#8008,.T.);
#10921=ORIENTED_EDGE('',*,*,#8009,.T.);
#10922=ORIENTED_EDGE('',*,*,#8010,.T.);
#10923=ORIENTED_EDGE('',*,*,#8011,.T.);
#10924=ORIENTED_EDGE('',*,*,#8012,.T.);
#10925=ORIENTED_EDGE('',*,*,#8013,.T.);
#10926=ORIENTED_EDGE('',*,*,#8014,.T.);
#10927=ORIENTED_EDGE('',*,*,#8015,.T.);
#10928=ORIENTED_EDGE('',*,*,#8016,.T.);
#10929=ORIENTED_EDGE('',*,*,#8017,.T.);
#10930=ORIENTED_EDGE('',*,*,#8018,.T.);
#10931=ORIENTED_EDGE('',*,*,#8019,.T.);
#10932=ORIENTED_EDGE('',*,*,#8020,.T.);
#10933=ORIENTED_EDGE('',*,*,#8021,.T.);
#10934=ORIENTED_EDGE('',*,*,#8022,.T.);
#10935=ORIENTED_EDGE('',*,*,#8023,.T.);
#10936=ORIENTED_EDGE('',*,*,#8024,.T.);
#10937=ORIENTED_EDGE('',*,*,#8025,.T.);
#10938=ORIENTED_EDGE('',*,*,#8026,.T.);
#10939=ORIENTED_EDGE('',*,*,#8027,.T.);
#10940=ORIENTED_EDGE('',*,*,#8028,.T.);
#10941=ORIENTED_EDGE('',*,*,#8029,.T.);
#10942=ORIENTED_EDGE('',*,*,#8030,.T.);
#10943=ORIENTED_EDGE('',*,*,#8031,.T.);
#10944=ORIENTED_EDGE('',*,*,#8032,.T.);
#10945=ORIENTED_EDGE('',*,*,#8033,.T.);
#10946=ORIENTED_EDGE('',*,*,#8034,.T.);
#10947=ORIENTED_EDGE('',*,*,#8035,.T.);
#10948=ORIENTED_EDGE('',*,*,#8036,.T.);
#10949=ORIENTED_EDGE('',*,*,#8037,.T.);
#10950=ORIENTED_EDGE('',*,*,#8038,.T.);
#10951=ORIENTED_EDGE('',*,*,#8039,.T.);
#10952=ORIENTED_EDGE('',*,*,#8040,.T.);
#10953=ORIENTED_EDGE('',*,*,#8041,.T.);
#10954=ORIENTED_EDGE('',*,*,#8042,.T.);
#10955=ORIENTED_EDGE('',*,*,#8043,.T.);
#10956=ORIENTED_EDGE('',*,*,#8044,.T.);
#10957=ORIENTED_EDGE('',*,*,#8045,.T.);
#10958=ORIENTED_EDGE('',*,*,#8046,.T.);
#10959=ORIENTED_EDGE('',*,*,#8047,.T.);
#10960=ORIENTED_EDGE('',*,*,#8048,.T.);
#10961=ORIENTED_EDGE('',*,*,#8049,.T.);
#10962=ORIENTED_EDGE('',*,*,#8050,.T.);
#10963=ORIENTED_EDGE('',*,*,#8051,.T.);
#10964=ORIENTED_EDGE('',*,*,#8052,.T.);
#10965=ORIENTED_EDGE('',*,*,#8053,.T.);
#10966=ORIENTED_EDGE('',*,*,#8054,.T.);
#10967=ORIENTED_EDGE('',*,*,#8055,.T.);
#10968=ORIENTED_EDGE('',*,*,#8056,.T.);
#10969=ORIENTED_EDGE('',*,*,#8057,.T.);
#10970=ORIENTED_EDGE('',*,*,#8058,.T.);
#10971=ORIENTED_EDGE('',*,*,#8059,.T.);
#10972=ORIENTED_EDGE('',*,*,#8060,.T.);
#10973=ORIENTED_EDGE('',*,*,#8061,.T.);
#10974=ORIENTED_EDGE('',*,*,#8062,.T.);
#10975=ORIENTED_EDGE('',*,*,#8063,.T.);
#10976=ORIENTED_EDGE('',*,*,#8064,.T.);
#10977=ORIENTED_EDGE('',*,*,#8065,.T.);
#10978=ORIENTED_EDGE('',*,*,#8066,.T.);
#10979=ORIENTED_EDGE('',*,*,#8067,.T.);
#10980=ORIENTED_EDGE('',*,*,#8068,.T.);
#10981=ORIENTED_EDGE('',*,*,#8069,.T.);
#10982=ORIENTED_EDGE('',*,*,#8070,.T.);
#10983=ORIENTED_EDGE('',*,*,#8071,.T.);
#10984=ORIENTED_EDGE('',*,*,#8072,.T.);
#10985=ORIENTED_EDGE('',*,*,#8073,.T.);
#10986=ORIENTED_EDGE('',*,*,#8074,.T.);
#10987=ORIENTED_EDGE('',*,*,#8075,.T.);
#10988=ORIENTED_EDGE('',*,*,#8076,.T.);
#10989=ORIENTED_EDGE('',*,*,#8077,.T.);
#10990=ORIENTED_EDGE('',*,*,#8078,.T.);
#10991=ORIENTED_EDGE('',*,*,#8079,.T.);
#10992=ORIENTED_EDGE('',*,*,#8080,.T.);
#10993=ORIENTED_EDGE('',*,*,#8081,.T.);
#10994=ORIENTED_EDGE('',*,*,#8082,.T.);
#10995=ORIENTED_EDGE('',*,*,#8083,.T.);
#10996=ORIENTED_EDGE('',*,*,#8084,.T.);
#10997=ORIENTED_EDGE('',*,*,#8085,.T.);
#10998=ORIENTED_EDGE('',*,*,#8086,.T.);
#10999=ORIENTED_EDGE('',*,*,#8087,.T.);
#11000=ORIENTED_EDGE('',*,*,#8088,.T.);
#11001=ORIENTED_EDGE('',*,*,#8089,.T.);
#11002=ORIENTED_EDGE('',*,*,#8090,.T.);
#11003=ORIENTED_EDGE('',*,*,#8091,.T.);
#11004=ORIENTED_EDGE('',*,*,#8092,.T.);
#11005=ORIENTED_EDGE('',*,*,#8093,.T.);
#11006=ORIENTED_EDGE('',*,*,#8094,.T.);
#11007=ORIENTED_EDGE('',*,*,#8095,.T.);
#11008=ORIENTED_EDGE('',*,*,#8096,.T.);
#11009=ORIENTED_EDGE('',*,*,#8097,.T.);
#11010=ORIENTED_EDGE('',*,*,#8098,.T.);
#11011=ORIENTED_EDGE('',*,*,#8099,.T.);
#11012=ORIENTED_EDGE('',*,*,#8100,.T.);
#11013=ORIENTED_EDGE('',*,*,#8101,.T.);
#11014=ORIENTED_EDGE('',*,*,#8102,.T.);
#11015=ORIENTED_EDGE('',*,*,#8103,.T.);
#11016=ORIENTED_EDGE('',*,*,#8104,.T.);
#11017=ORIENTED_EDGE('',*,*,#8105,.T.);
#11018=ORIENTED_EDGE('',*,*,#8106,.F.);
#11019=ORIENTED_EDGE('',*,*,#8107,.T.);
#11020=ORIENTED_EDGE('',*,*,#8108,.T.);
#11021=ORIENTED_EDGE('',*,*,#8109,.T.);
#11022=ORIENTED_EDGE('',*,*,#8110,.T.);
#11023=ORIENTED_EDGE('',*,*,#8111,.T.);
#11024=ORIENTED_EDGE('',*,*,#8112,.T.);
#11025=ORIENTED_EDGE('',*,*,#8113,.T.);
#11026=ORIENTED_EDGE('',*,*,#8114,.T.);
#11027=ORIENTED_EDGE('',*,*,#8115,.T.);
#11028=ORIENTED_EDGE('',*,*,#8116,.T.);
#11029=ORIENTED_EDGE('',*,*,#8117,.T.);
#11030=ORIENTED_EDGE('',*,*,#8118,.T.);
#11031=ORIENTED_EDGE('',*,*,#8119,.T.);
#11032=ORIENTED_EDGE('',*,*,#8120,.T.);
#11033=ORIENTED_EDGE('',*,*,#8121,.T.);
#11034=ORIENTED_EDGE('',*,*,#8122,.T.);
#11035=ORIENTED_EDGE('',*,*,#8123,.T.);
#11036=ORIENTED_EDGE('',*,*,#8124,.T.);
#11037=ORIENTED_EDGE('',*,*,#8125,.T.);
#11038=ORIENTED_EDGE('',*,*,#8126,.T.);
#11039=ORIENTED_EDGE('',*,*,#8127,.T.);
#11040=ORIENTED_EDGE('',*,*,#8128,.T.);
#11041=ORIENTED_EDGE('',*,*,#8129,.T.);
#11042=ORIENTED_EDGE('',*,*,#8130,.T.);
#11043=ORIENTED_EDGE('',*,*,#8131,.T.);
#11044=ORIENTED_EDGE('',*,*,#8132,.T.);
#11045=ORIENTED_EDGE('',*,*,#8133,.T.);
#11046=ORIENTED_EDGE('',*,*,#8134,.T.);
#11047=ORIENTED_EDGE('',*,*,#8135,.T.);
#11048=ORIENTED_EDGE('',*,*,#8136,.T.);
#11049=ORIENTED_EDGE('',*,*,#8137,.T.);
#11050=ORIENTED_EDGE('',*,*,#8138,.T.);
#11051=ORIENTED_EDGE('',*,*,#8139,.T.);
#11052=ORIENTED_EDGE('',*,*,#8140,.T.);
#11053=ORIENTED_EDGE('',*,*,#8141,.T.);
#11054=ORIENTED_EDGE('',*,*,#8142,.T.);
#11055=ORIENTED_EDGE('',*,*,#8143,.T.);
#11056=ORIENTED_EDGE('',*,*,#8144,.T.);
#11057=ORIENTED_EDGE('',*,*,#8145,.T.);
#11058=ORIENTED_EDGE('',*,*,#8146,.T.);
#11059=ORIENTED_EDGE('',*,*,#8147,.T.);
#11060=ORIENTED_EDGE('',*,*,#8148,.T.);
#11061=ORIENTED_EDGE('',*,*,#8149,.T.);
#11062=ORIENTED_EDGE('',*,*,#8150,.T.);
#11063=ORIENTED_EDGE('',*,*,#8151,.T.);
#11064=ORIENTED_EDGE('',*,*,#8152,.T.);
#11065=ORIENTED_EDGE('',*,*,#8153,.T.);
#11066=ORIENTED_EDGE('',*,*,#8154,.T.);
#11067=ORIENTED_EDGE('',*,*,#8155,.T.);
#11068=ORIENTED_EDGE('',*,*,#8156,.T.);
#11069=ORIENTED_EDGE('',*,*,#8157,.T.);
#11070=ORIENTED_EDGE('',*,*,#8158,.T.);
#11071=ORIENTED_EDGE('',*,*,#8159,.T.);
#11072=ORIENTED_EDGE('',*,*,#8160,.T.);
#11073=ORIENTED_EDGE('',*,*,#8161,.T.);
#11074=ORIENTED_EDGE('',*,*,#8162,.T.);
#11075=ORIENTED_EDGE('',*,*,#8163,.T.);
#11076=ORIENTED_EDGE('',*,*,#8164,.T.);
#11077=ORIENTED_EDGE('',*,*,#8165,.T.);
#11078=ORIENTED_EDGE('',*,*,#8166,.T.);
#11079=ORIENTED_EDGE('',*,*,#8167,.T.);
#11080=ORIENTED_EDGE('',*,*,#8168,.T.);
#11081=ORIENTED_EDGE('',*,*,#8169,.T.);
#11082=ORIENTED_EDGE('',*,*,#8170,.T.);
#11083=ORIENTED_EDGE('',*,*,#8171,.T.);
#11084=ORIENTED_EDGE('',*,*,#8172,.T.);
#11085=ORIENTED_EDGE('',*,*,#8173,.T.);
#11086=ORIENTED_EDGE('',*,*,#8174,.T.);
#11087=ORIENTED_EDGE('',*,*,#8175,.T.);
#11088=ORIENTED_EDGE('',*,*,#8176,.T.);
#11089=ORIENTED_EDGE('',*,*,#8177,.T.);
#11090=ORIENTED_EDGE('',*,*,#8178,.T.);
#11091=ORIENTED_EDGE('',*,*,#8179,.T.);
#11092=ORIENTED_EDGE('',*,*,#8180,.T.);
#11093=ORIENTED_EDGE('',*,*,#8181,.T.);
#11094=ORIENTED_EDGE('',*,*,#8182,.T.);
#11095=ORIENTED_EDGE('',*,*,#8183,.T.);
#11096=ORIENTED_EDGE('',*,*,#8184,.T.);
#11097=ORIENTED_EDGE('',*,*,#8185,.T.);
#11098=ORIENTED_EDGE('',*,*,#8186,.T.);
#11099=ORIENTED_EDGE('',*,*,#8187,.T.);
#11100=ORIENTED_EDGE('',*,*,#8188,.T.);
#11101=ORIENTED_EDGE('',*,*,#8189,.T.);
#11102=ORIENTED_EDGE('',*,*,#8190,.T.);
#11103=ORIENTED_EDGE('',*,*,#8191,.T.);
#11104=ORIENTED_EDGE('',*,*,#8192,.T.);
#11105=ORIENTED_EDGE('',*,*,#8193,.T.);
#11106=ORIENTED_EDGE('',*,*,#8194,.T.);
#11107=ORIENTED_EDGE('',*,*,#8195,.T.);
#11108=ORIENTED_EDGE('',*,*,#8196,.T.);
#11109=ORIENTED_EDGE('',*,*,#8197,.T.);
#11110=ORIENTED_EDGE('',*,*,#8198,.T.);
#11111=ORIENTED_EDGE('',*,*,#8199,.T.);
#11112=ORIENTED_EDGE('',*,*,#8200,.T.);
#11113=ORIENTED_EDGE('',*,*,#8201,.T.);
#11114=ORIENTED_EDGE('',*,*,#8202,.T.);
#11115=ORIENTED_EDGE('',*,*,#8203,.T.);
#11116=ORIENTED_EDGE('',*,*,#8204,.T.);
#11117=ORIENTED_EDGE('',*,*,#8205,.T.);
#11118=ORIENTED_EDGE('',*,*,#8206,.T.);
#11119=ORIENTED_EDGE('',*,*,#8207,.T.);
#11120=ORIENTED_EDGE('',*,*,#8208,.T.);
#11121=ORIENTED_EDGE('',*,*,#8209,.T.);
#11122=ORIENTED_EDGE('',*,*,#8210,.T.);
#11123=ORIENTED_EDGE('',*,*,#8211,.T.);
#11124=ORIENTED_EDGE('',*,*,#8212,.T.);
#11125=ORIENTED_EDGE('',*,*,#8213,.T.);
#11126=ORIENTED_EDGE('',*,*,#8214,.T.);
#11127=ORIENTED_EDGE('',*,*,#8215,.T.);
#11128=ORIENTED_EDGE('',*,*,#8216,.T.);
#11129=ORIENTED_EDGE('',*,*,#8217,.T.);
#11130=ORIENTED_EDGE('',*,*,#8218,.T.);
#11131=ORIENTED_EDGE('',*,*,#8219,.T.);
#11132=ORIENTED_EDGE('',*,*,#8220,.T.);
#11133=ORIENTED_EDGE('',*,*,#8221,.T.);
#11134=ORIENTED_EDGE('',*,*,#8222,.T.);
#11135=ORIENTED_EDGE('',*,*,#8223,.T.);
#11136=ORIENTED_EDGE('',*,*,#8224,.T.);
#11137=ORIENTED_EDGE('',*,*,#8225,.T.);
#11138=ORIENTED_EDGE('',*,*,#8226,.T.);
#11139=ORIENTED_EDGE('',*,*,#8227,.T.);
#11140=ORIENTED_EDGE('',*,*,#8228,.T.);
#11141=ORIENTED_EDGE('',*,*,#8229,.T.);
#11142=ORIENTED_EDGE('',*,*,#8230,.T.);
#11143=ORIENTED_EDGE('',*,*,#8231,.T.);
#11144=ORIENTED_EDGE('',*,*,#8232,.T.);
#11145=ORIENTED_EDGE('',*,*,#8233,.T.);
#11146=ORIENTED_EDGE('',*,*,#8234,.T.);
#11147=ORIENTED_EDGE('',*,*,#8235,.T.);
#11148=ORIENTED_EDGE('',*,*,#8236,.T.);
#11149=ORIENTED_EDGE('',*,*,#8237,.T.);
#11150=ORIENTED_EDGE('',*,*,#8238,.T.);
#11151=ORIENTED_EDGE('',*,*,#8239,.T.);
#11152=ORIENTED_EDGE('',*,*,#8240,.T.);
#11153=ORIENTED_EDGE('',*,*,#8241,.T.);
#11154=ORIENTED_EDGE('',*,*,#8242,.T.);
#11155=ORIENTED_EDGE('',*,*,#8243,.T.);
#11156=ORIENTED_EDGE('',*,*,#8244,.T.);
#11157=ORIENTED_EDGE('',*,*,#8245,.T.);
#11158=ORIENTED_EDGE('',*,*,#8246,.T.);
#11159=ORIENTED_EDGE('',*,*,#8247,.T.);
#11160=ORIENTED_EDGE('',*,*,#8248,.T.);
#11161=ORIENTED_EDGE('',*,*,#8249,.T.);
#11162=ORIENTED_EDGE('',*,*,#8250,.T.);
#11163=ORIENTED_EDGE('',*,*,#8251,.T.);
#11164=ORIENTED_EDGE('',*,*,#8252,.T.);
#11165=ORIENTED_EDGE('',*,*,#8253,.T.);
#11166=ORIENTED_EDGE('',*,*,#8254,.T.);
#11167=ORIENTED_EDGE('',*,*,#8255,.T.);
#11168=ORIENTED_EDGE('',*,*,#8256,.T.);
#11169=ORIENTED_EDGE('',*,*,#8257,.T.);
#11170=ORIENTED_EDGE('',*,*,#8258,.T.);
#11171=ORIENTED_EDGE('',*,*,#8259,.T.);
#11172=ORIENTED_EDGE('',*,*,#8260,.T.);
#11173=ORIENTED_EDGE('',*,*,#8261,.T.);
#11174=ORIENTED_EDGE('',*,*,#8262,.T.);
#11175=ORIENTED_EDGE('',*,*,#8263,.T.);
#11176=ORIENTED_EDGE('',*,*,#8264,.T.);
#11177=ORIENTED_EDGE('',*,*,#8265,.T.);
#11178=ORIENTED_EDGE('',*,*,#8266,.T.);
#11179=ORIENTED_EDGE('',*,*,#8267,.T.);
#11180=ORIENTED_EDGE('',*,*,#8268,.T.);
#11181=ORIENTED_EDGE('',*,*,#8269,.T.);
#11182=ORIENTED_EDGE('',*,*,#8270,.T.);
#11183=ORIENTED_EDGE('',*,*,#8271,.T.);
#11184=ORIENTED_EDGE('',*,*,#8272,.T.);
#11185=ORIENTED_EDGE('',*,*,#8273,.T.);
#11186=ORIENTED_EDGE('',*,*,#8274,.T.);
#11187=ORIENTED_EDGE('',*,*,#8275,.T.);
#11188=ORIENTED_EDGE('',*,*,#8276,.T.);
#11189=ORIENTED_EDGE('',*,*,#8277,.T.);
#11190=ORIENTED_EDGE('',*,*,#8278,.T.);
#11191=ORIENTED_EDGE('',*,*,#8279,.T.);
#11192=ORIENTED_EDGE('',*,*,#8280,.T.);
#11193=ORIENTED_EDGE('',*,*,#8281,.T.);
#11194=ORIENTED_EDGE('',*,*,#8282,.T.);
#11195=ORIENTED_EDGE('',*,*,#8283,.T.);
#11196=ORIENTED_EDGE('',*,*,#8284,.T.);
#11197=ORIENTED_EDGE('',*,*,#8285,.T.);
#11198=ORIENTED_EDGE('',*,*,#8286,.T.);
#11199=ORIENTED_EDGE('',*,*,#8287,.T.);
#11200=ORIENTED_EDGE('',*,*,#8288,.T.);
#11201=ORIENTED_EDGE('',*,*,#8289,.T.);
#11202=ORIENTED_EDGE('',*,*,#8290,.T.);
#11203=ORIENTED_EDGE('',*,*,#8291,.T.);
#11204=ORIENTED_EDGE('',*,*,#8292,.T.);
#11205=ORIENTED_EDGE('',*,*,#8293,.T.);
#11206=ORIENTED_EDGE('',*,*,#8294,.T.);
#11207=ORIENTED_EDGE('',*,*,#8295,.T.);
#11208=ORIENTED_EDGE('',*,*,#8296,.T.);
#11209=ORIENTED_EDGE('',*,*,#8297,.T.);
#11210=ORIENTED_EDGE('',*,*,#8298,.T.);
#11211=ORIENTED_EDGE('',*,*,#8299,.T.);
#11212=ORIENTED_EDGE('',*,*,#8300,.T.);
#11213=ORIENTED_EDGE('',*,*,#8301,.T.);
#11214=ORIENTED_EDGE('',*,*,#8302,.T.);
#11215=ORIENTED_EDGE('',*,*,#8303,.T.);
#11216=ORIENTED_EDGE('',*,*,#8304,.T.);
#11217=ORIENTED_EDGE('',*,*,#8305,.T.);
#11218=ORIENTED_EDGE('',*,*,#8306,.T.);
#11219=ORIENTED_EDGE('',*,*,#8307,.T.);
#11220=ORIENTED_EDGE('',*,*,#8308,.T.);
#11221=ORIENTED_EDGE('',*,*,#8309,.T.);
#11222=ORIENTED_EDGE('',*,*,#8310,.T.);
#11223=ORIENTED_EDGE('',*,*,#8311,.T.);
#11224=ORIENTED_EDGE('',*,*,#8312,.T.);
#11225=ORIENTED_EDGE('',*,*,#8313,.T.);
#11226=ORIENTED_EDGE('',*,*,#8314,.T.);
#11227=ORIENTED_EDGE('',*,*,#8315,.T.);
#11228=ORIENTED_EDGE('',*,*,#8316,.T.);
#11229=ORIENTED_EDGE('',*,*,#8317,.T.);
#11230=ORIENTED_EDGE('',*,*,#8318,.T.);
#11231=ORIENTED_EDGE('',*,*,#8319,.T.);
#11232=ORIENTED_EDGE('',*,*,#8320,.T.);
#11233=ORIENTED_EDGE('',*,*,#8321,.T.);
#11234=ORIENTED_EDGE('',*,*,#8322,.T.);
#11235=ORIENTED_EDGE('',*,*,#8323,.T.);
#11236=ORIENTED_EDGE('',*,*,#8324,.T.);
#11237=ORIENTED_EDGE('',*,*,#8325,.T.);
#11238=ORIENTED_EDGE('',*,*,#8326,.T.);
#11239=ORIENTED_EDGE('',*,*,#8327,.T.);
#11240=ORIENTED_EDGE('',*,*,#8328,.T.);
#11241=ORIENTED_EDGE('',*,*,#8329,.T.);
#11242=ORIENTED_EDGE('',*,*,#8330,.T.);
#11243=ORIENTED_EDGE('',*,*,#8331,.T.);
#11244=ORIENTED_EDGE('',*,*,#8332,.T.);
#11245=ORIENTED_EDGE('',*,*,#8333,.T.);
#11246=ORIENTED_EDGE('',*,*,#8334,.T.);
#11247=ORIENTED_EDGE('',*,*,#8335,.T.);
#11248=ORIENTED_EDGE('',*,*,#8336,.T.);
#11249=ORIENTED_EDGE('',*,*,#8337,.T.);
#11250=ORIENTED_EDGE('',*,*,#8338,.T.);
#11251=ORIENTED_EDGE('',*,*,#8339,.T.);
#11252=ORIENTED_EDGE('',*,*,#8340,.T.);
#11253=ORIENTED_EDGE('',*,*,#8341,.T.);
#11254=ORIENTED_EDGE('',*,*,#8342,.T.);
#11255=ORIENTED_EDGE('',*,*,#8343,.T.);
#11256=ORIENTED_EDGE('',*,*,#8344,.T.);
#11257=ORIENTED_EDGE('',*,*,#8345,.T.);
#11258=ORIENTED_EDGE('',*,*,#8346,.T.);
#11259=ORIENTED_EDGE('',*,*,#8347,.T.);
#11260=ORIENTED_EDGE('',*,*,#8348,.T.);
#11261=ORIENTED_EDGE('',*,*,#8349,.T.);
#11262=ORIENTED_EDGE('',*,*,#8350,.T.);
#11263=ORIENTED_EDGE('',*,*,#8351,.T.);
#11264=ORIENTED_EDGE('',*,*,#8352,.T.);
#11265=ORIENTED_EDGE('',*,*,#8353,.T.);
#11266=ORIENTED_EDGE('',*,*,#8354,.T.);
#11267=ORIENTED_EDGE('',*,*,#8355,.T.);
#11268=ORIENTED_EDGE('',*,*,#8356,.T.);
#11269=ORIENTED_EDGE('',*,*,#8357,.T.);
#11270=ORIENTED_EDGE('',*,*,#8358,.T.);
#11271=ORIENTED_EDGE('',*,*,#8359,.T.);
#11272=ORIENTED_EDGE('',*,*,#8360,.T.);
#11273=ORIENTED_EDGE('',*,*,#8361,.T.);
#11274=ORIENTED_EDGE('',*,*,#8362,.T.);
#11275=ORIENTED_EDGE('',*,*,#8363,.T.);
#11276=ORIENTED_EDGE('',*,*,#8364,.T.);
#11277=ORIENTED_EDGE('',*,*,#8365,.T.);
#11278=ORIENTED_EDGE('',*,*,#8366,.T.);
#11279=ORIENTED_EDGE('',*,*,#8367,.T.);
#11280=ORIENTED_EDGE('',*,*,#8368,.T.);
#11281=ORIENTED_EDGE('',*,*,#8369,.T.);
#11282=ORIENTED_EDGE('',*,*,#8370,.T.);
#11283=ORIENTED_EDGE('',*,*,#8371,.T.);
#11284=ORIENTED_EDGE('',*,*,#8372,.T.);
#11285=ORIENTED_EDGE('',*,*,#8373,.T.);
#11286=ORIENTED_EDGE('',*,*,#8374,.T.);
#11287=ORIENTED_EDGE('',*,*,#8375,.T.);
#11288=ORIENTED_EDGE('',*,*,#7829,.T.);
#11289=ORIENTED_EDGE('',*,*,#8376,.T.);
#11290=ORIENTED_EDGE('',*,*,#8377,.T.);
#11291=ORIENTED_EDGE('',*,*,#8378,.F.);
#11292=ORIENTED_EDGE('',*,*,#8379,.F.);
#11293=ORIENTED_EDGE('',*,*,#8380,.F.);
#11294=ORIENTED_EDGE('',*,*,#8381,.T.);
#11295=ORIENTED_EDGE('',*,*,#8382,.F.);
#11296=ORIENTED_EDGE('',*,*,#8381,.F.);
#11297=ORIENTED_EDGE('',*,*,#8383,.T.);
#11298=ORIENTED_EDGE('',*,*,#8384,.T.);
#11299=ORIENTED_EDGE('',*,*,#8383,.F.);
#11300=ORIENTED_EDGE('',*,*,#8384,.F.);
#11301=ORIENTED_EDGE('',*,*,#8385,.T.);
#11302=ORIENTED_EDGE('',*,*,#7835,.T.);
#11303=ORIENTED_EDGE('',*,*,#8386,.T.);
#11304=ORIENTED_EDGE('',*,*,#6497,.T.);
#11305=ORIENTED_EDGE('',*,*,#8387,.F.);
#11306=ORIENTED_EDGE('',*,*,#8388,.F.);
#11307=ORIENTED_EDGE('',*,*,#8389,.T.);
#11308=ORIENTED_EDGE('',*,*,#8390,.F.);
#11309=ORIENTED_EDGE('',*,*,#8391,.F.);
#11310=ORIENTED_EDGE('',*,*,#8389,.F.);
#11311=ORIENTED_EDGE('',*,*,#8392,.F.);
#11312=ORIENTED_EDGE('',*,*,#8393,.F.);
#11313=ORIENTED_EDGE('',*,*,#8394,.T.);
#11314=ORIENTED_EDGE('',*,*,#8395,.F.);
#11315=ORIENTED_EDGE('',*,*,#8396,.F.);
#11316=ORIENTED_EDGE('',*,*,#8394,.F.);
#11317=ORIENTED_EDGE('',*,*,#8397,.F.);
#11318=ORIENTED_EDGE('',*,*,#8396,.T.);
#11319=ORIENTED_EDGE('',*,*,#8398,.T.);
#11320=ORIENTED_EDGE('',*,*,#8382,.T.);
#11321=ORIENTED_EDGE('',*,*,#8398,.F.);
#11322=ORIENTED_EDGE('',*,*,#8397,.T.);
#11323=ORIENTED_EDGE('',*,*,#8393,.T.);
#11324=ORIENTED_EDGE('',*,*,#8399,.F.);
#11325=ORIENTED_EDGE('',*,*,#8390,.T.);
#11326=ORIENTED_EDGE('',*,*,#8391,.T.);
#11327=ORIENTED_EDGE('',*,*,#8388,.T.);
#11328=ORIENTED_EDGE('',*,*,#8400,.F.);
#11329=ORIENTED_EDGE('',*,*,#8395,.T.);
#11330=ORIENTED_EDGE('',*,*,#8387,.T.);
#11331=ORIENTED_EDGE('',*,*,#8399,.T.);
#11332=ORIENTED_EDGE('',*,*,#8392,.T.);
#11333=ORIENTED_EDGE('',*,*,#8400,.T.);
#11334=ORIENTED_EDGE('',*,*,#8401,.F.);
#11335=ORIENTED_EDGE('',*,*,#8105,.F.);
#11336=ORIENTED_EDGE('',*,*,#8104,.F.);
#11337=ORIENTED_EDGE('',*,*,#8103,.F.);
#11338=ORIENTED_EDGE('',*,*,#8102,.F.);
#11339=ORIENTED_EDGE('',*,*,#8101,.F.);
#11340=ORIENTED_EDGE('',*,*,#8100,.F.);
#11341=ORIENTED_EDGE('',*,*,#8099,.F.);
#11342=ORIENTED_EDGE('',*,*,#8098,.F.);
#11343=ORIENTED_EDGE('',*,*,#8097,.F.);
#11344=ORIENTED_EDGE('',*,*,#8096,.F.);
#11345=ORIENTED_EDGE('',*,*,#8095,.F.);
#11346=ORIENTED_EDGE('',*,*,#8094,.F.);
#11347=ORIENTED_EDGE('',*,*,#8093,.F.);
#11348=ORIENTED_EDGE('',*,*,#8092,.F.);
#11349=ORIENTED_EDGE('',*,*,#8091,.F.);
#11350=ORIENTED_EDGE('',*,*,#8090,.F.);
#11351=ORIENTED_EDGE('',*,*,#8089,.F.);
#11352=ORIENTED_EDGE('',*,*,#8088,.F.);
#11353=ORIENTED_EDGE('',*,*,#8087,.F.);
#11354=ORIENTED_EDGE('',*,*,#8086,.F.);
#11355=ORIENTED_EDGE('',*,*,#8085,.F.);
#11356=ORIENTED_EDGE('',*,*,#8084,.F.);
#11357=ORIENTED_EDGE('',*,*,#8083,.F.);
#11358=ORIENTED_EDGE('',*,*,#8082,.F.);
#11359=ORIENTED_EDGE('',*,*,#8081,.F.);
#11360=ORIENTED_EDGE('',*,*,#8080,.F.);
#11361=ORIENTED_EDGE('',*,*,#8079,.F.);
#11362=ORIENTED_EDGE('',*,*,#8078,.F.);
#11363=ORIENTED_EDGE('',*,*,#8077,.F.);
#11364=ORIENTED_EDGE('',*,*,#8076,.F.);
#11365=ORIENTED_EDGE('',*,*,#8075,.F.);
#11366=ORIENTED_EDGE('',*,*,#8074,.F.);
#11367=ORIENTED_EDGE('',*,*,#8073,.F.);
#11368=ORIENTED_EDGE('',*,*,#8072,.F.);
#11369=ORIENTED_EDGE('',*,*,#8071,.F.);
#11370=ORIENTED_EDGE('',*,*,#8070,.F.);
#11371=ORIENTED_EDGE('',*,*,#8069,.F.);
#11372=ORIENTED_EDGE('',*,*,#8068,.F.);
#11373=ORIENTED_EDGE('',*,*,#8067,.F.);
#11374=ORIENTED_EDGE('',*,*,#8066,.F.);
#11375=ORIENTED_EDGE('',*,*,#8065,.F.);
#11376=ORIENTED_EDGE('',*,*,#8064,.F.);
#11377=ORIENTED_EDGE('',*,*,#8063,.F.);
#11378=ORIENTED_EDGE('',*,*,#8062,.F.);
#11379=ORIENTED_EDGE('',*,*,#8061,.F.);
#11380=ORIENTED_EDGE('',*,*,#8060,.F.);
#11381=ORIENTED_EDGE('',*,*,#8059,.F.);
#11382=ORIENTED_EDGE('',*,*,#8058,.F.);
#11383=ORIENTED_EDGE('',*,*,#8057,.F.);
#11384=ORIENTED_EDGE('',*,*,#8056,.F.);
#11385=ORIENTED_EDGE('',*,*,#8055,.F.);
#11386=ORIENTED_EDGE('',*,*,#8054,.F.);
#11387=ORIENTED_EDGE('',*,*,#8053,.F.);
#11388=ORIENTED_EDGE('',*,*,#8052,.F.);
#11389=ORIENTED_EDGE('',*,*,#8051,.F.);
#11390=ORIENTED_EDGE('',*,*,#8050,.F.);
#11391=ORIENTED_EDGE('',*,*,#8049,.F.);
#11392=ORIENTED_EDGE('',*,*,#8048,.F.);
#11393=ORIENTED_EDGE('',*,*,#8047,.F.);
#11394=ORIENTED_EDGE('',*,*,#8046,.F.);
#11395=ORIENTED_EDGE('',*,*,#8045,.F.);
#11396=ORIENTED_EDGE('',*,*,#8044,.F.);
#11397=ORIENTED_EDGE('',*,*,#8043,.F.);
#11398=ORIENTED_EDGE('',*,*,#8042,.F.);
#11399=ORIENTED_EDGE('',*,*,#8041,.F.);
#11400=ORIENTED_EDGE('',*,*,#8040,.F.);
#11401=ORIENTED_EDGE('',*,*,#8039,.F.);
#11402=ORIENTED_EDGE('',*,*,#8038,.F.);
#11403=ORIENTED_EDGE('',*,*,#8037,.F.);
#11404=ORIENTED_EDGE('',*,*,#8036,.F.);
#11405=ORIENTED_EDGE('',*,*,#8035,.F.);
#11406=ORIENTED_EDGE('',*,*,#8034,.F.);
#11407=ORIENTED_EDGE('',*,*,#8033,.F.);
#11408=ORIENTED_EDGE('',*,*,#8032,.F.);
#11409=ORIENTED_EDGE('',*,*,#8031,.F.);
#11410=ORIENTED_EDGE('',*,*,#8030,.F.);
#11411=ORIENTED_EDGE('',*,*,#8029,.F.);
#11412=ORIENTED_EDGE('',*,*,#8028,.F.);
#11413=ORIENTED_EDGE('',*,*,#8027,.F.);
#11414=ORIENTED_EDGE('',*,*,#8026,.F.);
#11415=ORIENTED_EDGE('',*,*,#8025,.F.);
#11416=ORIENTED_EDGE('',*,*,#8024,.F.);
#11417=ORIENTED_EDGE('',*,*,#8023,.F.);
#11418=ORIENTED_EDGE('',*,*,#8022,.F.);
#11419=ORIENTED_EDGE('',*,*,#8021,.F.);
#11420=ORIENTED_EDGE('',*,*,#8020,.F.);
#11421=ORIENTED_EDGE('',*,*,#8019,.F.);
#11422=ORIENTED_EDGE('',*,*,#8018,.F.);
#11423=ORIENTED_EDGE('',*,*,#8017,.F.);
#11424=ORIENTED_EDGE('',*,*,#8016,.F.);
#11425=ORIENTED_EDGE('',*,*,#8015,.F.);
#11426=ORIENTED_EDGE('',*,*,#8014,.F.);
#11427=ORIENTED_EDGE('',*,*,#8013,.F.);
#11428=ORIENTED_EDGE('',*,*,#8012,.F.);
#11429=ORIENTED_EDGE('',*,*,#8011,.F.);
#11430=ORIENTED_EDGE('',*,*,#8010,.F.);
#11431=ORIENTED_EDGE('',*,*,#8009,.F.);
#11432=ORIENTED_EDGE('',*,*,#8008,.F.);
#11433=ORIENTED_EDGE('',*,*,#8007,.F.);
#11434=ORIENTED_EDGE('',*,*,#8006,.F.);
#11435=ORIENTED_EDGE('',*,*,#8005,.F.);
#11436=ORIENTED_EDGE('',*,*,#8004,.F.);
#11437=ORIENTED_EDGE('',*,*,#8003,.F.);
#11438=ORIENTED_EDGE('',*,*,#8002,.F.);
#11439=ORIENTED_EDGE('',*,*,#8001,.F.);
#11440=ORIENTED_EDGE('',*,*,#8000,.F.);
#11441=ORIENTED_EDGE('',*,*,#7999,.F.);
#11442=ORIENTED_EDGE('',*,*,#7998,.F.);
#11443=ORIENTED_EDGE('',*,*,#7997,.F.);
#11444=ORIENTED_EDGE('',*,*,#7996,.F.);
#11445=ORIENTED_EDGE('',*,*,#7995,.F.);
#11446=ORIENTED_EDGE('',*,*,#7994,.F.);
#11447=ORIENTED_EDGE('',*,*,#7993,.F.);
#11448=ORIENTED_EDGE('',*,*,#7992,.F.);
#11449=ORIENTED_EDGE('',*,*,#7991,.F.);
#11450=ORIENTED_EDGE('',*,*,#7990,.F.);
#11451=ORIENTED_EDGE('',*,*,#7989,.F.);
#11452=ORIENTED_EDGE('',*,*,#7988,.F.);
#11453=ORIENTED_EDGE('',*,*,#7987,.F.);
#11454=ORIENTED_EDGE('',*,*,#7986,.F.);
#11455=ORIENTED_EDGE('',*,*,#7985,.F.);
#11456=ORIENTED_EDGE('',*,*,#7984,.F.);
#11457=ORIENTED_EDGE('',*,*,#7983,.F.);
#11458=ORIENTED_EDGE('',*,*,#7982,.F.);
#11459=ORIENTED_EDGE('',*,*,#7981,.F.);
#11460=ORIENTED_EDGE('',*,*,#7980,.F.);
#11461=ORIENTED_EDGE('',*,*,#7979,.F.);
#11462=ORIENTED_EDGE('',*,*,#7978,.F.);
#11463=ORIENTED_EDGE('',*,*,#7977,.F.);
#11464=ORIENTED_EDGE('',*,*,#7976,.F.);
#11465=ORIENTED_EDGE('',*,*,#7975,.F.);
#11466=ORIENTED_EDGE('',*,*,#7974,.F.);
#11467=ORIENTED_EDGE('',*,*,#7973,.F.);
#11468=ORIENTED_EDGE('',*,*,#7972,.F.);
#11469=ORIENTED_EDGE('',*,*,#7971,.F.);
#11470=ORIENTED_EDGE('',*,*,#7970,.F.);
#11471=ORIENTED_EDGE('',*,*,#7969,.F.);
#11472=ORIENTED_EDGE('',*,*,#7968,.F.);
#11473=ORIENTED_EDGE('',*,*,#7967,.F.);
#11474=ORIENTED_EDGE('',*,*,#7966,.F.);
#11475=ORIENTED_EDGE('',*,*,#7965,.F.);
#11476=ORIENTED_EDGE('',*,*,#7964,.F.);
#11477=ORIENTED_EDGE('',*,*,#7963,.F.);
#11478=ORIENTED_EDGE('',*,*,#7962,.F.);
#11479=ORIENTED_EDGE('',*,*,#7961,.F.);
#11480=ORIENTED_EDGE('',*,*,#7960,.F.);
#11481=ORIENTED_EDGE('',*,*,#7959,.F.);
#11482=ORIENTED_EDGE('',*,*,#7958,.F.);
#11483=ORIENTED_EDGE('',*,*,#7957,.F.);
#11484=ORIENTED_EDGE('',*,*,#7956,.F.);
#11485=ORIENTED_EDGE('',*,*,#7955,.F.);
#11486=ORIENTED_EDGE('',*,*,#7954,.F.);
#11487=ORIENTED_EDGE('',*,*,#7953,.F.);
#11488=ORIENTED_EDGE('',*,*,#7952,.F.);
#11489=ORIENTED_EDGE('',*,*,#7951,.F.);
#11490=ORIENTED_EDGE('',*,*,#7950,.F.);
#11491=ORIENTED_EDGE('',*,*,#7949,.F.);
#11492=ORIENTED_EDGE('',*,*,#7948,.F.);
#11493=ORIENTED_EDGE('',*,*,#7947,.F.);
#11494=ORIENTED_EDGE('',*,*,#7946,.F.);
#11495=ORIENTED_EDGE('',*,*,#7945,.F.);
#11496=ORIENTED_EDGE('',*,*,#7944,.F.);
#11497=ORIENTED_EDGE('',*,*,#7943,.F.);
#11498=ORIENTED_EDGE('',*,*,#7942,.F.);
#11499=ORIENTED_EDGE('',*,*,#7941,.F.);
#11500=ORIENTED_EDGE('',*,*,#7940,.F.);
#11501=ORIENTED_EDGE('',*,*,#7939,.F.);
#11502=ORIENTED_EDGE('',*,*,#7938,.F.);
#11503=ORIENTED_EDGE('',*,*,#7937,.F.);
#11504=ORIENTED_EDGE('',*,*,#7936,.F.);
#11505=ORIENTED_EDGE('',*,*,#7935,.F.);
#11506=ORIENTED_EDGE('',*,*,#7934,.F.);
#11507=ORIENTED_EDGE('',*,*,#7933,.F.);
#11508=ORIENTED_EDGE('',*,*,#7932,.F.);
#11509=ORIENTED_EDGE('',*,*,#7931,.F.);
#11510=ORIENTED_EDGE('',*,*,#7930,.F.);
#11511=ORIENTED_EDGE('',*,*,#7929,.F.);
#11512=ORIENTED_EDGE('',*,*,#7928,.F.);
#11513=ORIENTED_EDGE('',*,*,#7927,.F.);
#11514=ORIENTED_EDGE('',*,*,#7926,.F.);
#11515=ORIENTED_EDGE('',*,*,#7925,.F.);
#11516=ORIENTED_EDGE('',*,*,#7924,.F.);
#11517=ORIENTED_EDGE('',*,*,#7923,.F.);
#11518=ORIENTED_EDGE('',*,*,#7922,.F.);
#11519=ORIENTED_EDGE('',*,*,#7921,.F.);
#11520=ORIENTED_EDGE('',*,*,#7920,.F.);
#11521=ORIENTED_EDGE('',*,*,#7919,.F.);
#11522=ORIENTED_EDGE('',*,*,#7918,.F.);
#11523=ORIENTED_EDGE('',*,*,#7917,.F.);
#11524=ORIENTED_EDGE('',*,*,#7916,.F.);
#11525=ORIENTED_EDGE('',*,*,#7915,.F.);
#11526=ORIENTED_EDGE('',*,*,#7914,.F.);
#11527=ORIENTED_EDGE('',*,*,#7913,.F.);
#11528=ORIENTED_EDGE('',*,*,#7912,.F.);
#11529=ORIENTED_EDGE('',*,*,#7911,.F.);
#11530=ORIENTED_EDGE('',*,*,#7910,.F.);
#11531=ORIENTED_EDGE('',*,*,#7909,.F.);
#11532=ORIENTED_EDGE('',*,*,#7908,.F.);
#11533=ORIENTED_EDGE('',*,*,#7907,.F.);
#11534=ORIENTED_EDGE('',*,*,#7906,.F.);
#11535=ORIENTED_EDGE('',*,*,#7905,.F.);
#11536=ORIENTED_EDGE('',*,*,#7904,.F.);
#11537=ORIENTED_EDGE('',*,*,#7903,.F.);
#11538=ORIENTED_EDGE('',*,*,#7902,.F.);
#11539=ORIENTED_EDGE('',*,*,#7901,.F.);
#11540=ORIENTED_EDGE('',*,*,#7900,.F.);
#11541=ORIENTED_EDGE('',*,*,#7899,.F.);
#11542=ORIENTED_EDGE('',*,*,#7898,.F.);
#11543=ORIENTED_EDGE('',*,*,#7897,.F.);
#11544=ORIENTED_EDGE('',*,*,#7896,.F.);
#11545=ORIENTED_EDGE('',*,*,#7895,.F.);
#11546=ORIENTED_EDGE('',*,*,#7894,.F.);
#11547=ORIENTED_EDGE('',*,*,#7893,.F.);
#11548=ORIENTED_EDGE('',*,*,#7892,.F.);
#11549=ORIENTED_EDGE('',*,*,#7891,.F.);
#11550=ORIENTED_EDGE('',*,*,#7890,.F.);
#11551=ORIENTED_EDGE('',*,*,#7889,.F.);
#11552=ORIENTED_EDGE('',*,*,#7888,.F.);
#11553=ORIENTED_EDGE('',*,*,#7887,.F.);
#11554=ORIENTED_EDGE('',*,*,#7886,.F.);
#11555=ORIENTED_EDGE('',*,*,#7885,.F.);
#11556=ORIENTED_EDGE('',*,*,#7884,.F.);
#11557=ORIENTED_EDGE('',*,*,#7883,.F.);
#11558=ORIENTED_EDGE('',*,*,#7882,.F.);
#11559=ORIENTED_EDGE('',*,*,#7881,.F.);
#11560=ORIENTED_EDGE('',*,*,#7880,.F.);
#11561=ORIENTED_EDGE('',*,*,#7879,.F.);
#11562=ORIENTED_EDGE('',*,*,#7878,.F.);
#11563=ORIENTED_EDGE('',*,*,#7877,.F.);
#11564=ORIENTED_EDGE('',*,*,#7876,.F.);
#11565=ORIENTED_EDGE('',*,*,#7875,.F.);
#11566=ORIENTED_EDGE('',*,*,#7874,.F.);
#11567=ORIENTED_EDGE('',*,*,#7873,.F.);
#11568=ORIENTED_EDGE('',*,*,#7872,.F.);
#11569=ORIENTED_EDGE('',*,*,#7871,.F.);
#11570=ORIENTED_EDGE('',*,*,#7870,.F.);
#11571=ORIENTED_EDGE('',*,*,#7869,.F.);
#11572=ORIENTED_EDGE('',*,*,#7868,.F.);
#11573=ORIENTED_EDGE('',*,*,#7867,.F.);
#11574=ORIENTED_EDGE('',*,*,#7866,.F.);
#11575=ORIENTED_EDGE('',*,*,#7865,.F.);
#11576=ORIENTED_EDGE('',*,*,#7864,.F.);
#11577=ORIENTED_EDGE('',*,*,#7863,.F.);
#11578=ORIENTED_EDGE('',*,*,#7862,.F.);
#11579=ORIENTED_EDGE('',*,*,#7861,.F.);
#11580=ORIENTED_EDGE('',*,*,#7860,.F.);
#11581=ORIENTED_EDGE('',*,*,#7859,.F.);
#11582=ORIENTED_EDGE('',*,*,#7858,.F.);
#11583=ORIENTED_EDGE('',*,*,#7857,.F.);
#11584=ORIENTED_EDGE('',*,*,#7856,.F.);
#11585=ORIENTED_EDGE('',*,*,#7855,.F.);
#11586=ORIENTED_EDGE('',*,*,#7854,.F.);
#11587=ORIENTED_EDGE('',*,*,#7853,.F.);
#11588=ORIENTED_EDGE('',*,*,#7852,.F.);
#11589=ORIENTED_EDGE('',*,*,#7851,.F.);
#11590=ORIENTED_EDGE('',*,*,#7850,.F.);
#11591=ORIENTED_EDGE('',*,*,#7849,.F.);
#11592=ORIENTED_EDGE('',*,*,#7848,.F.);
#11593=ORIENTED_EDGE('',*,*,#7847,.F.);
#11594=ORIENTED_EDGE('',*,*,#7846,.F.);
#11595=ORIENTED_EDGE('',*,*,#7845,.F.);
#11596=ORIENTED_EDGE('',*,*,#7844,.F.);
#11597=ORIENTED_EDGE('',*,*,#7843,.F.);
#11598=ORIENTED_EDGE('',*,*,#7842,.F.);
#11599=ORIENTED_EDGE('',*,*,#7841,.F.);
#11600=ORIENTED_EDGE('',*,*,#7840,.F.);
#11601=ORIENTED_EDGE('',*,*,#7839,.F.);
#11602=ORIENTED_EDGE('',*,*,#7838,.F.);
#11603=ORIENTED_EDGE('',*,*,#7837,.F.);
#11604=ORIENTED_EDGE('',*,*,#7836,.F.);
#11605=ORIENTED_EDGE('',*,*,#8385,.F.);
#11606=ORIENTED_EDGE('',*,*,#6496,.T.);
#11607=ORIENTED_EDGE('',*,*,#6501,.T.);
#11608=ORIENTED_EDGE('',*,*,#6500,.T.);
#11609=ORIENTED_EDGE('',*,*,#6506,.T.);
#11610=ORIENTED_EDGE('',*,*,#6505,.T.);
#11611=ORIENTED_EDGE('',*,*,#6511,.T.);
#11612=ORIENTED_EDGE('',*,*,#6510,.T.);
#11613=ORIENTED_EDGE('',*,*,#6516,.T.);
#11614=ORIENTED_EDGE('',*,*,#6515,.T.);
#11615=ORIENTED_EDGE('',*,*,#6521,.T.);
#11616=ORIENTED_EDGE('',*,*,#6520,.T.);
#11617=ORIENTED_EDGE('',*,*,#6526,.T.);
#11618=ORIENTED_EDGE('',*,*,#6525,.T.);
#11619=ORIENTED_EDGE('',*,*,#6531,.T.);
#11620=ORIENTED_EDGE('',*,*,#6530,.T.);
#11621=ORIENTED_EDGE('',*,*,#6536,.T.);
#11622=ORIENTED_EDGE('',*,*,#6535,.T.);
#11623=ORIENTED_EDGE('',*,*,#6541,.T.);
#11624=ORIENTED_EDGE('',*,*,#6540,.T.);
#11625=ORIENTED_EDGE('',*,*,#6546,.T.);
#11626=ORIENTED_EDGE('',*,*,#6545,.T.);
#11627=ORIENTED_EDGE('',*,*,#6551,.T.);
#11628=ORIENTED_EDGE('',*,*,#6550,.T.);
#11629=ORIENTED_EDGE('',*,*,#6556,.T.);
#11630=ORIENTED_EDGE('',*,*,#6555,.T.);
#11631=ORIENTED_EDGE('',*,*,#6561,.T.);
#11632=ORIENTED_EDGE('',*,*,#6560,.T.);
#11633=ORIENTED_EDGE('',*,*,#6566,.T.);
#11634=ORIENTED_EDGE('',*,*,#6565,.T.);
#11635=ORIENTED_EDGE('',*,*,#6571,.T.);
#11636=ORIENTED_EDGE('',*,*,#6570,.T.);
#11637=ORIENTED_EDGE('',*,*,#6576,.T.);
#11638=ORIENTED_EDGE('',*,*,#6575,.T.);
#11639=ORIENTED_EDGE('',*,*,#6581,.T.);
#11640=ORIENTED_EDGE('',*,*,#6580,.T.);
#11641=ORIENTED_EDGE('',*,*,#6586,.T.);
#11642=ORIENTED_EDGE('',*,*,#6585,.T.);
#11643=ORIENTED_EDGE('',*,*,#6591,.T.);
#11644=ORIENTED_EDGE('',*,*,#6590,.T.);
#11645=ORIENTED_EDGE('',*,*,#6596,.T.);
#11646=ORIENTED_EDGE('',*,*,#6595,.T.);
#11647=ORIENTED_EDGE('',*,*,#6601,.T.);
#11648=ORIENTED_EDGE('',*,*,#6600,.T.);
#11649=ORIENTED_EDGE('',*,*,#6606,.T.);
#11650=ORIENTED_EDGE('',*,*,#6605,.T.);
#11651=ORIENTED_EDGE('',*,*,#6611,.T.);
#11652=ORIENTED_EDGE('',*,*,#6610,.T.);
#11653=ORIENTED_EDGE('',*,*,#6616,.T.);
#11654=ORIENTED_EDGE('',*,*,#6615,.T.);
#11655=ORIENTED_EDGE('',*,*,#6621,.T.);
#11656=ORIENTED_EDGE('',*,*,#6620,.T.);
#11657=ORIENTED_EDGE('',*,*,#6626,.T.);
#11658=ORIENTED_EDGE('',*,*,#6625,.T.);
#11659=ORIENTED_EDGE('',*,*,#6631,.T.);
#11660=ORIENTED_EDGE('',*,*,#6630,.T.);
#11661=ORIENTED_EDGE('',*,*,#6636,.T.);
#11662=ORIENTED_EDGE('',*,*,#6635,.T.);
#11663=ORIENTED_EDGE('',*,*,#6641,.T.);
#11664=ORIENTED_EDGE('',*,*,#6640,.T.);
#11665=ORIENTED_EDGE('',*,*,#6646,.T.);
#11666=ORIENTED_EDGE('',*,*,#6645,.T.);
#11667=ORIENTED_EDGE('',*,*,#6651,.T.);
#11668=ORIENTED_EDGE('',*,*,#6650,.T.);
#11669=ORIENTED_EDGE('',*,*,#6656,.T.);
#11670=ORIENTED_EDGE('',*,*,#6655,.T.);
#11671=ORIENTED_EDGE('',*,*,#6661,.T.);
#11672=ORIENTED_EDGE('',*,*,#6660,.T.);
#11673=ORIENTED_EDGE('',*,*,#6666,.T.);
#11674=ORIENTED_EDGE('',*,*,#6665,.T.);
#11675=ORIENTED_EDGE('',*,*,#6671,.T.);
#11676=ORIENTED_EDGE('',*,*,#6670,.T.);
#11677=ORIENTED_EDGE('',*,*,#6676,.T.);
#11678=ORIENTED_EDGE('',*,*,#6675,.T.);
#11679=ORIENTED_EDGE('',*,*,#6681,.T.);
#11680=ORIENTED_EDGE('',*,*,#6680,.T.);
#11681=ORIENTED_EDGE('',*,*,#6686,.T.);
#11682=ORIENTED_EDGE('',*,*,#6685,.T.);
#11683=ORIENTED_EDGE('',*,*,#6691,.T.);
#11684=ORIENTED_EDGE('',*,*,#6690,.T.);
#11685=ORIENTED_EDGE('',*,*,#6696,.T.);
#11686=ORIENTED_EDGE('',*,*,#6695,.T.);
#11687=ORIENTED_EDGE('',*,*,#6701,.T.);
#11688=ORIENTED_EDGE('',*,*,#6700,.T.);
#11689=ORIENTED_EDGE('',*,*,#6706,.T.);
#11690=ORIENTED_EDGE('',*,*,#6705,.T.);
#11691=ORIENTED_EDGE('',*,*,#6711,.T.);
#11692=ORIENTED_EDGE('',*,*,#6710,.T.);
#11693=ORIENTED_EDGE('',*,*,#6716,.T.);
#11694=ORIENTED_EDGE('',*,*,#6715,.T.);
#11695=ORIENTED_EDGE('',*,*,#6721,.T.);
#11696=ORIENTED_EDGE('',*,*,#6720,.T.);
#11697=ORIENTED_EDGE('',*,*,#6726,.T.);
#11698=ORIENTED_EDGE('',*,*,#6725,.T.);
#11699=ORIENTED_EDGE('',*,*,#6731,.T.);
#11700=ORIENTED_EDGE('',*,*,#6730,.T.);
#11701=ORIENTED_EDGE('',*,*,#6736,.T.);
#11702=ORIENTED_EDGE('',*,*,#6735,.T.);
#11703=ORIENTED_EDGE('',*,*,#6741,.T.);
#11704=ORIENTED_EDGE('',*,*,#6740,.T.);
#11705=ORIENTED_EDGE('',*,*,#6746,.T.);
#11706=ORIENTED_EDGE('',*,*,#6745,.T.);
#11707=ORIENTED_EDGE('',*,*,#6751,.T.);
#11708=ORIENTED_EDGE('',*,*,#6750,.T.);
#11709=ORIENTED_EDGE('',*,*,#6756,.T.);
#11710=ORIENTED_EDGE('',*,*,#6755,.T.);
#11711=ORIENTED_EDGE('',*,*,#6761,.T.);
#11712=ORIENTED_EDGE('',*,*,#6760,.T.);
#11713=ORIENTED_EDGE('',*,*,#6766,.T.);
#11714=ORIENTED_EDGE('',*,*,#6765,.T.);
#11715=ORIENTED_EDGE('',*,*,#6771,.T.);
#11716=ORIENTED_EDGE('',*,*,#6770,.T.);
#11717=ORIENTED_EDGE('',*,*,#6776,.T.);
#11718=ORIENTED_EDGE('',*,*,#6775,.T.);
#11719=ORIENTED_EDGE('',*,*,#6781,.T.);
#11720=ORIENTED_EDGE('',*,*,#6780,.T.);
#11721=ORIENTED_EDGE('',*,*,#6786,.T.);
#11722=ORIENTED_EDGE('',*,*,#6785,.T.);
#11723=ORIENTED_EDGE('',*,*,#6791,.T.);
#11724=ORIENTED_EDGE('',*,*,#6790,.T.);
#11725=ORIENTED_EDGE('',*,*,#6796,.T.);
#11726=ORIENTED_EDGE('',*,*,#6795,.T.);
#11727=ORIENTED_EDGE('',*,*,#6801,.T.);
#11728=ORIENTED_EDGE('',*,*,#6800,.T.);
#11729=ORIENTED_EDGE('',*,*,#6806,.T.);
#11730=ORIENTED_EDGE('',*,*,#6805,.T.);
#11731=ORIENTED_EDGE('',*,*,#6811,.T.);
#11732=ORIENTED_EDGE('',*,*,#6810,.T.);
#11733=ORIENTED_EDGE('',*,*,#6816,.T.);
#11734=ORIENTED_EDGE('',*,*,#6815,.T.);
#11735=ORIENTED_EDGE('',*,*,#6821,.T.);
#11736=ORIENTED_EDGE('',*,*,#6820,.T.);
#11737=ORIENTED_EDGE('',*,*,#6826,.T.);
#11738=ORIENTED_EDGE('',*,*,#6825,.T.);
#11739=ORIENTED_EDGE('',*,*,#6831,.T.);
#11740=ORIENTED_EDGE('',*,*,#6830,.T.);
#11741=ORIENTED_EDGE('',*,*,#6836,.T.);
#11742=ORIENTED_EDGE('',*,*,#6835,.T.);
#11743=ORIENTED_EDGE('',*,*,#6841,.T.);
#11744=ORIENTED_EDGE('',*,*,#6840,.T.);
#11745=ORIENTED_EDGE('',*,*,#6846,.T.);
#11746=ORIENTED_EDGE('',*,*,#6845,.T.);
#11747=ORIENTED_EDGE('',*,*,#6851,.T.);
#11748=ORIENTED_EDGE('',*,*,#6850,.T.);
#11749=ORIENTED_EDGE('',*,*,#6856,.T.);
#11750=ORIENTED_EDGE('',*,*,#6855,.T.);
#11751=ORIENTED_EDGE('',*,*,#6861,.T.);
#11752=ORIENTED_EDGE('',*,*,#6860,.T.);
#11753=ORIENTED_EDGE('',*,*,#6866,.T.);
#11754=ORIENTED_EDGE('',*,*,#6865,.T.);
#11755=ORIENTED_EDGE('',*,*,#6871,.T.);
#11756=ORIENTED_EDGE('',*,*,#6870,.T.);
#11757=ORIENTED_EDGE('',*,*,#6876,.T.);
#11758=ORIENTED_EDGE('',*,*,#6875,.T.);
#11759=ORIENTED_EDGE('',*,*,#6881,.T.);
#11760=ORIENTED_EDGE('',*,*,#6880,.T.);
#11761=ORIENTED_EDGE('',*,*,#6886,.T.);
#11762=ORIENTED_EDGE('',*,*,#6885,.T.);
#11763=ORIENTED_EDGE('',*,*,#6891,.T.);
#11764=ORIENTED_EDGE('',*,*,#6890,.T.);
#11765=ORIENTED_EDGE('',*,*,#6896,.T.);
#11766=ORIENTED_EDGE('',*,*,#6895,.T.);
#11767=ORIENTED_EDGE('',*,*,#6901,.T.);
#11768=ORIENTED_EDGE('',*,*,#6900,.T.);
#11769=ORIENTED_EDGE('',*,*,#6906,.T.);
#11770=ORIENTED_EDGE('',*,*,#6905,.T.);
#11771=ORIENTED_EDGE('',*,*,#6911,.T.);
#11772=ORIENTED_EDGE('',*,*,#6910,.T.);
#11773=ORIENTED_EDGE('',*,*,#6916,.T.);
#11774=ORIENTED_EDGE('',*,*,#6915,.T.);
#11775=ORIENTED_EDGE('',*,*,#6921,.T.);
#11776=ORIENTED_EDGE('',*,*,#6920,.T.);
#11777=ORIENTED_EDGE('',*,*,#6926,.T.);
#11778=ORIENTED_EDGE('',*,*,#6925,.T.);
#11779=ORIENTED_EDGE('',*,*,#6931,.T.);
#11780=ORIENTED_EDGE('',*,*,#6930,.T.);
#11781=ORIENTED_EDGE('',*,*,#6936,.T.);
#11782=ORIENTED_EDGE('',*,*,#6935,.T.);
#11783=ORIENTED_EDGE('',*,*,#6941,.T.);
#11784=ORIENTED_EDGE('',*,*,#6940,.T.);
#11785=ORIENTED_EDGE('',*,*,#6946,.T.);
#11786=ORIENTED_EDGE('',*,*,#6945,.T.);
#11787=ORIENTED_EDGE('',*,*,#6951,.T.);
#11788=ORIENTED_EDGE('',*,*,#6950,.T.);
#11789=ORIENTED_EDGE('',*,*,#6956,.T.);
#11790=ORIENTED_EDGE('',*,*,#6955,.T.);
#11791=ORIENTED_EDGE('',*,*,#6961,.T.);
#11792=ORIENTED_EDGE('',*,*,#6960,.T.);
#11793=ORIENTED_EDGE('',*,*,#6966,.T.);
#11794=ORIENTED_EDGE('',*,*,#6965,.T.);
#11795=ORIENTED_EDGE('',*,*,#6971,.T.);
#11796=ORIENTED_EDGE('',*,*,#6970,.T.);
#11797=ORIENTED_EDGE('',*,*,#6976,.T.);
#11798=ORIENTED_EDGE('',*,*,#6975,.T.);
#11799=ORIENTED_EDGE('',*,*,#6981,.T.);
#11800=ORIENTED_EDGE('',*,*,#6980,.T.);
#11801=ORIENTED_EDGE('',*,*,#6986,.T.);
#11802=ORIENTED_EDGE('',*,*,#6985,.T.);
#11803=ORIENTED_EDGE('',*,*,#6991,.T.);
#11804=ORIENTED_EDGE('',*,*,#6990,.T.);
#11805=ORIENTED_EDGE('',*,*,#6996,.T.);
#11806=ORIENTED_EDGE('',*,*,#6995,.T.);
#11807=ORIENTED_EDGE('',*,*,#7001,.T.);
#11808=ORIENTED_EDGE('',*,*,#7000,.T.);
#11809=ORIENTED_EDGE('',*,*,#7006,.T.);
#11810=ORIENTED_EDGE('',*,*,#7005,.T.);
#11811=ORIENTED_EDGE('',*,*,#7011,.T.);
#11812=ORIENTED_EDGE('',*,*,#7010,.T.);
#11813=ORIENTED_EDGE('',*,*,#7016,.T.);
#11814=ORIENTED_EDGE('',*,*,#7015,.T.);
#11815=ORIENTED_EDGE('',*,*,#7021,.T.);
#11816=ORIENTED_EDGE('',*,*,#7020,.T.);
#11817=ORIENTED_EDGE('',*,*,#7026,.T.);
#11818=ORIENTED_EDGE('',*,*,#7025,.T.);
#11819=ORIENTED_EDGE('',*,*,#7031,.T.);
#11820=ORIENTED_EDGE('',*,*,#7030,.T.);
#11821=ORIENTED_EDGE('',*,*,#7036,.T.);
#11822=ORIENTED_EDGE('',*,*,#7035,.T.);
#11823=ORIENTED_EDGE('',*,*,#7041,.T.);
#11824=ORIENTED_EDGE('',*,*,#7040,.T.);
#11825=ORIENTED_EDGE('',*,*,#7046,.T.);
#11826=ORIENTED_EDGE('',*,*,#7045,.T.);
#11827=ORIENTED_EDGE('',*,*,#7051,.T.);
#11828=ORIENTED_EDGE('',*,*,#7050,.T.);
#11829=ORIENTED_EDGE('',*,*,#7056,.T.);
#11830=ORIENTED_EDGE('',*,*,#7055,.T.);
#11831=ORIENTED_EDGE('',*,*,#7061,.T.);
#11832=ORIENTED_EDGE('',*,*,#7060,.T.);
#11833=ORIENTED_EDGE('',*,*,#7066,.T.);
#11834=ORIENTED_EDGE('',*,*,#7065,.T.);
#11835=ORIENTED_EDGE('',*,*,#7071,.T.);
#11836=ORIENTED_EDGE('',*,*,#7070,.T.);
#11837=ORIENTED_EDGE('',*,*,#7076,.T.);
#11838=ORIENTED_EDGE('',*,*,#7075,.T.);
#11839=ORIENTED_EDGE('',*,*,#7081,.T.);
#11840=ORIENTED_EDGE('',*,*,#7080,.T.);
#11841=ORIENTED_EDGE('',*,*,#7086,.T.);
#11842=ORIENTED_EDGE('',*,*,#7085,.T.);
#11843=ORIENTED_EDGE('',*,*,#7091,.T.);
#11844=ORIENTED_EDGE('',*,*,#7090,.T.);
#11845=ORIENTED_EDGE('',*,*,#7096,.T.);
#11846=ORIENTED_EDGE('',*,*,#7095,.T.);
#11847=ORIENTED_EDGE('',*,*,#7101,.T.);
#11848=ORIENTED_EDGE('',*,*,#7100,.T.);
#11849=ORIENTED_EDGE('',*,*,#7106,.T.);
#11850=ORIENTED_EDGE('',*,*,#7105,.T.);
#11851=ORIENTED_EDGE('',*,*,#7111,.T.);
#11852=ORIENTED_EDGE('',*,*,#7110,.T.);
#11853=ORIENTED_EDGE('',*,*,#7116,.T.);
#11854=ORIENTED_EDGE('',*,*,#7115,.T.);
#11855=ORIENTED_EDGE('',*,*,#7121,.T.);
#11856=ORIENTED_EDGE('',*,*,#7120,.T.);
#11857=ORIENTED_EDGE('',*,*,#7126,.T.);
#11858=ORIENTED_EDGE('',*,*,#7125,.T.);
#11859=ORIENTED_EDGE('',*,*,#7131,.T.);
#11860=ORIENTED_EDGE('',*,*,#7130,.T.);
#11861=ORIENTED_EDGE('',*,*,#7136,.T.);
#11862=ORIENTED_EDGE('',*,*,#7135,.T.);
#11863=ORIENTED_EDGE('',*,*,#7141,.T.);
#11864=ORIENTED_EDGE('',*,*,#7140,.T.);
#11865=ORIENTED_EDGE('',*,*,#7146,.T.);
#11866=ORIENTED_EDGE('',*,*,#7145,.T.);
#11867=ORIENTED_EDGE('',*,*,#7151,.T.);
#11868=ORIENTED_EDGE('',*,*,#7150,.T.);
#11869=ORIENTED_EDGE('',*,*,#7156,.T.);
#11870=ORIENTED_EDGE('',*,*,#7155,.T.);
#11871=ORIENTED_EDGE('',*,*,#7161,.T.);
#11872=ORIENTED_EDGE('',*,*,#7160,.T.);
#11873=ORIENTED_EDGE('',*,*,#7166,.T.);
#11874=ORIENTED_EDGE('',*,*,#7165,.T.);
#11875=ORIENTED_EDGE('',*,*,#7171,.T.);
#11876=ORIENTED_EDGE('',*,*,#7170,.T.);
#11877=ORIENTED_EDGE('',*,*,#7176,.T.);
#11878=ORIENTED_EDGE('',*,*,#7175,.T.);
#11879=ORIENTED_EDGE('',*,*,#7181,.T.);
#11880=ORIENTED_EDGE('',*,*,#7180,.T.);
#11881=ORIENTED_EDGE('',*,*,#7186,.T.);
#11882=ORIENTED_EDGE('',*,*,#7185,.T.);
#11883=ORIENTED_EDGE('',*,*,#7191,.T.);
#11884=ORIENTED_EDGE('',*,*,#7190,.T.);
#11885=ORIENTED_EDGE('',*,*,#7196,.T.);
#11886=ORIENTED_EDGE('',*,*,#7195,.T.);
#11887=ORIENTED_EDGE('',*,*,#7201,.T.);
#11888=ORIENTED_EDGE('',*,*,#7200,.T.);
#11889=ORIENTED_EDGE('',*,*,#7206,.T.);
#11890=ORIENTED_EDGE('',*,*,#7205,.T.);
#11891=ORIENTED_EDGE('',*,*,#7211,.T.);
#11892=ORIENTED_EDGE('',*,*,#7210,.T.);
#11893=ORIENTED_EDGE('',*,*,#7216,.T.);
#11894=ORIENTED_EDGE('',*,*,#7215,.T.);
#11895=ORIENTED_EDGE('',*,*,#7221,.T.);
#11896=ORIENTED_EDGE('',*,*,#7220,.T.);
#11897=ORIENTED_EDGE('',*,*,#7226,.T.);
#11898=ORIENTED_EDGE('',*,*,#7225,.T.);
#11899=ORIENTED_EDGE('',*,*,#7231,.T.);
#11900=ORIENTED_EDGE('',*,*,#7230,.T.);
#11901=ORIENTED_EDGE('',*,*,#7236,.T.);
#11902=ORIENTED_EDGE('',*,*,#7235,.T.);
#11903=ORIENTED_EDGE('',*,*,#7241,.T.);
#11904=ORIENTED_EDGE('',*,*,#7240,.T.);
#11905=ORIENTED_EDGE('',*,*,#7246,.T.);
#11906=ORIENTED_EDGE('',*,*,#7245,.T.);
#11907=ORIENTED_EDGE('',*,*,#7251,.T.);
#11908=ORIENTED_EDGE('',*,*,#7250,.T.);
#11909=ORIENTED_EDGE('',*,*,#7256,.T.);
#11910=ORIENTED_EDGE('',*,*,#7255,.T.);
#11911=ORIENTED_EDGE('',*,*,#7261,.T.);
#11912=ORIENTED_EDGE('',*,*,#7260,.T.);
#11913=ORIENTED_EDGE('',*,*,#7266,.T.);
#11914=ORIENTED_EDGE('',*,*,#7265,.T.);
#11915=ORIENTED_EDGE('',*,*,#7271,.T.);
#11916=ORIENTED_EDGE('',*,*,#7270,.T.);
#11917=ORIENTED_EDGE('',*,*,#7276,.T.);
#11918=ORIENTED_EDGE('',*,*,#7275,.T.);
#11919=ORIENTED_EDGE('',*,*,#7281,.T.);
#11920=ORIENTED_EDGE('',*,*,#7280,.T.);
#11921=ORIENTED_EDGE('',*,*,#7286,.T.);
#11922=ORIENTED_EDGE('',*,*,#7285,.T.);
#11923=ORIENTED_EDGE('',*,*,#7291,.T.);
#11924=ORIENTED_EDGE('',*,*,#7290,.T.);
#11925=ORIENTED_EDGE('',*,*,#7296,.T.);
#11926=ORIENTED_EDGE('',*,*,#7295,.T.);
#11927=ORIENTED_EDGE('',*,*,#7301,.T.);
#11928=ORIENTED_EDGE('',*,*,#7300,.T.);
#11929=ORIENTED_EDGE('',*,*,#7306,.T.);
#11930=ORIENTED_EDGE('',*,*,#7305,.T.);
#11931=ORIENTED_EDGE('',*,*,#7311,.T.);
#11932=ORIENTED_EDGE('',*,*,#7310,.T.);
#11933=ORIENTED_EDGE('',*,*,#7316,.T.);
#11934=ORIENTED_EDGE('',*,*,#7315,.T.);
#11935=ORIENTED_EDGE('',*,*,#7321,.T.);
#11936=ORIENTED_EDGE('',*,*,#7320,.T.);
#11937=ORIENTED_EDGE('',*,*,#7326,.T.);
#11938=ORIENTED_EDGE('',*,*,#7325,.T.);
#11939=ORIENTED_EDGE('',*,*,#7331,.T.);
#11940=ORIENTED_EDGE('',*,*,#7330,.T.);
#11941=ORIENTED_EDGE('',*,*,#7336,.T.);
#11942=ORIENTED_EDGE('',*,*,#7335,.T.);
#11943=ORIENTED_EDGE('',*,*,#7341,.T.);
#11944=ORIENTED_EDGE('',*,*,#7340,.T.);
#11945=ORIENTED_EDGE('',*,*,#7346,.T.);
#11946=ORIENTED_EDGE('',*,*,#7345,.T.);
#11947=ORIENTED_EDGE('',*,*,#7351,.T.);
#11948=ORIENTED_EDGE('',*,*,#7350,.T.);
#11949=ORIENTED_EDGE('',*,*,#7356,.T.);
#11950=ORIENTED_EDGE('',*,*,#7355,.T.);
#11951=ORIENTED_EDGE('',*,*,#7361,.T.);
#11952=ORIENTED_EDGE('',*,*,#7360,.T.);
#11953=ORIENTED_EDGE('',*,*,#7366,.T.);
#11954=ORIENTED_EDGE('',*,*,#7365,.T.);
#11955=ORIENTED_EDGE('',*,*,#7371,.T.);
#11956=ORIENTED_EDGE('',*,*,#7370,.T.);
#11957=ORIENTED_EDGE('',*,*,#7376,.T.);
#11958=ORIENTED_EDGE('',*,*,#7375,.T.);
#11959=ORIENTED_EDGE('',*,*,#7381,.T.);
#11960=ORIENTED_EDGE('',*,*,#7380,.T.);
#11961=ORIENTED_EDGE('',*,*,#7386,.T.);
#11962=ORIENTED_EDGE('',*,*,#7385,.T.);
#11963=ORIENTED_EDGE('',*,*,#7391,.T.);
#11964=ORIENTED_EDGE('',*,*,#7390,.T.);
#11965=ORIENTED_EDGE('',*,*,#7396,.T.);
#11966=ORIENTED_EDGE('',*,*,#7395,.T.);
#11967=ORIENTED_EDGE('',*,*,#7401,.T.);
#11968=ORIENTED_EDGE('',*,*,#7400,.T.);
#11969=ORIENTED_EDGE('',*,*,#7406,.T.);
#11970=ORIENTED_EDGE('',*,*,#7405,.T.);
#11971=ORIENTED_EDGE('',*,*,#7411,.T.);
#11972=ORIENTED_EDGE('',*,*,#7410,.T.);
#11973=ORIENTED_EDGE('',*,*,#7416,.T.);
#11974=ORIENTED_EDGE('',*,*,#7415,.T.);
#11975=ORIENTED_EDGE('',*,*,#7421,.T.);
#11976=ORIENTED_EDGE('',*,*,#7420,.T.);
#11977=ORIENTED_EDGE('',*,*,#7426,.T.);
#11978=ORIENTED_EDGE('',*,*,#7425,.T.);
#11979=ORIENTED_EDGE('',*,*,#7431,.T.);
#11980=ORIENTED_EDGE('',*,*,#7430,.T.);
#11981=ORIENTED_EDGE('',*,*,#7436,.T.);
#11982=ORIENTED_EDGE('',*,*,#7435,.T.);
#11983=ORIENTED_EDGE('',*,*,#7441,.T.);
#11984=ORIENTED_EDGE('',*,*,#7440,.T.);
#11985=ORIENTED_EDGE('',*,*,#7446,.T.);
#11986=ORIENTED_EDGE('',*,*,#7445,.T.);
#11987=ORIENTED_EDGE('',*,*,#7451,.T.);
#11988=ORIENTED_EDGE('',*,*,#7450,.T.);
#11989=ORIENTED_EDGE('',*,*,#7456,.T.);
#11990=ORIENTED_EDGE('',*,*,#7455,.T.);
#11991=ORIENTED_EDGE('',*,*,#7461,.T.);
#11992=ORIENTED_EDGE('',*,*,#7460,.T.);
#11993=ORIENTED_EDGE('',*,*,#7466,.T.);
#11994=ORIENTED_EDGE('',*,*,#7465,.T.);
#11995=ORIENTED_EDGE('',*,*,#7471,.T.);
#11996=ORIENTED_EDGE('',*,*,#7470,.T.);
#11997=ORIENTED_EDGE('',*,*,#7476,.T.);
#11998=ORIENTED_EDGE('',*,*,#7475,.T.);
#11999=ORIENTED_EDGE('',*,*,#7481,.T.);
#12000=ORIENTED_EDGE('',*,*,#7480,.T.);
#12001=ORIENTED_EDGE('',*,*,#7486,.T.);
#12002=ORIENTED_EDGE('',*,*,#7485,.T.);
#12003=ORIENTED_EDGE('',*,*,#7491,.T.);
#12004=ORIENTED_EDGE('',*,*,#7490,.T.);
#12005=ORIENTED_EDGE('',*,*,#7496,.T.);
#12006=ORIENTED_EDGE('',*,*,#7495,.T.);
#12007=ORIENTED_EDGE('',*,*,#7501,.T.);
#12008=ORIENTED_EDGE('',*,*,#7500,.T.);
#12009=ORIENTED_EDGE('',*,*,#7506,.T.);
#12010=ORIENTED_EDGE('',*,*,#7505,.T.);
#12011=ORIENTED_EDGE('',*,*,#7511,.T.);
#12012=ORIENTED_EDGE('',*,*,#7510,.T.);
#12013=ORIENTED_EDGE('',*,*,#7516,.T.);
#12014=ORIENTED_EDGE('',*,*,#7515,.T.);
#12015=ORIENTED_EDGE('',*,*,#7521,.T.);
#12016=ORIENTED_EDGE('',*,*,#7520,.T.);
#12017=ORIENTED_EDGE('',*,*,#7526,.T.);
#12018=ORIENTED_EDGE('',*,*,#7525,.T.);
#12019=ORIENTED_EDGE('',*,*,#7531,.T.);
#12020=ORIENTED_EDGE('',*,*,#7530,.T.);
#12021=ORIENTED_EDGE('',*,*,#7536,.T.);
#12022=ORIENTED_EDGE('',*,*,#7535,.T.);
#12023=ORIENTED_EDGE('',*,*,#7541,.T.);
#12024=ORIENTED_EDGE('',*,*,#7540,.T.);
#12025=ORIENTED_EDGE('',*,*,#7546,.T.);
#12026=ORIENTED_EDGE('',*,*,#7545,.T.);
#12027=ORIENTED_EDGE('',*,*,#7551,.T.);
#12028=ORIENTED_EDGE('',*,*,#7550,.T.);
#12029=ORIENTED_EDGE('',*,*,#7556,.T.);
#12030=ORIENTED_EDGE('',*,*,#7555,.T.);
#12031=ORIENTED_EDGE('',*,*,#7561,.T.);
#12032=ORIENTED_EDGE('',*,*,#7560,.T.);
#12033=ORIENTED_EDGE('',*,*,#7566,.T.);
#12034=ORIENTED_EDGE('',*,*,#7565,.T.);
#12035=ORIENTED_EDGE('',*,*,#7571,.T.);
#12036=ORIENTED_EDGE('',*,*,#7570,.T.);
#12037=ORIENTED_EDGE('',*,*,#7576,.T.);
#12038=ORIENTED_EDGE('',*,*,#7575,.T.);
#12039=ORIENTED_EDGE('',*,*,#7581,.T.);
#12040=ORIENTED_EDGE('',*,*,#7580,.T.);
#12041=ORIENTED_EDGE('',*,*,#7586,.T.);
#12042=ORIENTED_EDGE('',*,*,#7585,.T.);
#12043=ORIENTED_EDGE('',*,*,#7591,.T.);
#12044=ORIENTED_EDGE('',*,*,#7590,.T.);
#12045=ORIENTED_EDGE('',*,*,#7596,.T.);
#12046=ORIENTED_EDGE('',*,*,#7595,.T.);
#12047=ORIENTED_EDGE('',*,*,#7601,.T.);
#12048=ORIENTED_EDGE('',*,*,#7600,.T.);
#12049=ORIENTED_EDGE('',*,*,#7606,.T.);
#12050=ORIENTED_EDGE('',*,*,#7605,.T.);
#12051=ORIENTED_EDGE('',*,*,#7611,.T.);
#12052=ORIENTED_EDGE('',*,*,#7610,.T.);
#12053=ORIENTED_EDGE('',*,*,#7616,.T.);
#12054=ORIENTED_EDGE('',*,*,#7615,.T.);
#12055=ORIENTED_EDGE('',*,*,#7621,.T.);
#12056=ORIENTED_EDGE('',*,*,#7620,.T.);
#12057=ORIENTED_EDGE('',*,*,#7626,.T.);
#12058=ORIENTED_EDGE('',*,*,#7625,.T.);
#12059=ORIENTED_EDGE('',*,*,#7631,.T.);
#12060=ORIENTED_EDGE('',*,*,#7630,.T.);
#12061=ORIENTED_EDGE('',*,*,#7636,.T.);
#12062=ORIENTED_EDGE('',*,*,#7635,.T.);
#12063=ORIENTED_EDGE('',*,*,#7641,.T.);
#12064=ORIENTED_EDGE('',*,*,#7640,.T.);
#12065=ORIENTED_EDGE('',*,*,#7646,.T.);
#12066=ORIENTED_EDGE('',*,*,#7645,.T.);
#12067=ORIENTED_EDGE('',*,*,#7651,.T.);
#12068=ORIENTED_EDGE('',*,*,#7650,.T.);
#12069=ORIENTED_EDGE('',*,*,#7656,.T.);
#12070=ORIENTED_EDGE('',*,*,#7655,.T.);
#12071=ORIENTED_EDGE('',*,*,#7661,.T.);
#12072=ORIENTED_EDGE('',*,*,#7660,.T.);
#12073=ORIENTED_EDGE('',*,*,#7666,.T.);
#12074=ORIENTED_EDGE('',*,*,#7665,.T.);
#12075=ORIENTED_EDGE('',*,*,#7671,.T.);
#12076=ORIENTED_EDGE('',*,*,#7670,.T.);
#12077=ORIENTED_EDGE('',*,*,#7676,.T.);
#12078=ORIENTED_EDGE('',*,*,#7675,.T.);
#12079=ORIENTED_EDGE('',*,*,#7681,.T.);
#12080=ORIENTED_EDGE('',*,*,#7680,.T.);
#12081=ORIENTED_EDGE('',*,*,#7686,.T.);
#12082=ORIENTED_EDGE('',*,*,#7685,.T.);
#12083=ORIENTED_EDGE('',*,*,#7691,.T.);
#12084=ORIENTED_EDGE('',*,*,#7690,.T.);
#12085=ORIENTED_EDGE('',*,*,#7696,.T.);
#12086=ORIENTED_EDGE('',*,*,#7695,.T.);
#12087=ORIENTED_EDGE('',*,*,#7701,.T.);
#12088=ORIENTED_EDGE('',*,*,#7700,.T.);
#12089=ORIENTED_EDGE('',*,*,#7706,.T.);
#12090=ORIENTED_EDGE('',*,*,#7705,.T.);
#12091=ORIENTED_EDGE('',*,*,#7711,.T.);
#12092=ORIENTED_EDGE('',*,*,#7710,.T.);
#12093=ORIENTED_EDGE('',*,*,#7716,.T.);
#12094=ORIENTED_EDGE('',*,*,#7715,.T.);
#12095=ORIENTED_EDGE('',*,*,#7721,.T.);
#12096=ORIENTED_EDGE('',*,*,#7720,.T.);
#12097=ORIENTED_EDGE('',*,*,#7726,.T.);
#12098=ORIENTED_EDGE('',*,*,#7725,.T.);
#12099=ORIENTED_EDGE('',*,*,#7731,.T.);
#12100=ORIENTED_EDGE('',*,*,#7730,.T.);
#12101=ORIENTED_EDGE('',*,*,#7736,.T.);
#12102=ORIENTED_EDGE('',*,*,#7735,.T.);
#12103=ORIENTED_EDGE('',*,*,#7741,.T.);
#12104=ORIENTED_EDGE('',*,*,#7740,.T.);
#12105=ORIENTED_EDGE('',*,*,#7746,.T.);
#12106=ORIENTED_EDGE('',*,*,#7745,.T.);
#12107=ORIENTED_EDGE('',*,*,#7751,.T.);
#12108=ORIENTED_EDGE('',*,*,#7750,.T.);
#12109=ORIENTED_EDGE('',*,*,#7756,.T.);
#12110=ORIENTED_EDGE('',*,*,#7755,.T.);
#12111=ORIENTED_EDGE('',*,*,#7761,.T.);
#12112=ORIENTED_EDGE('',*,*,#7760,.T.);
#12113=ORIENTED_EDGE('',*,*,#7766,.T.);
#12114=ORIENTED_EDGE('',*,*,#7765,.T.);
#12115=ORIENTED_EDGE('',*,*,#7771,.T.);
#12116=ORIENTED_EDGE('',*,*,#7770,.T.);
#12117=ORIENTED_EDGE('',*,*,#7776,.T.);
#12118=ORIENTED_EDGE('',*,*,#7775,.T.);
#12119=ORIENTED_EDGE('',*,*,#7781,.T.);
#12120=ORIENTED_EDGE('',*,*,#7780,.T.);
#12121=ORIENTED_EDGE('',*,*,#7786,.T.);
#12122=ORIENTED_EDGE('',*,*,#7785,.T.);
#12123=ORIENTED_EDGE('',*,*,#7791,.T.);
#12124=ORIENTED_EDGE('',*,*,#7790,.T.);
#12125=ORIENTED_EDGE('',*,*,#7796,.T.);
#12126=ORIENTED_EDGE('',*,*,#7795,.T.);
#12127=ORIENTED_EDGE('',*,*,#7801,.T.);
#12128=ORIENTED_EDGE('',*,*,#7800,.T.);
#12129=ORIENTED_EDGE('',*,*,#7806,.T.);
#12130=ORIENTED_EDGE('',*,*,#7805,.T.);
#12131=ORIENTED_EDGE('',*,*,#7811,.T.);
#12132=ORIENTED_EDGE('',*,*,#7810,.T.);
#12133=ORIENTED_EDGE('',*,*,#7816,.T.);
#12134=ORIENTED_EDGE('',*,*,#7815,.T.);
#12135=ORIENTED_EDGE('',*,*,#7821,.T.);
#12136=ORIENTED_EDGE('',*,*,#7820,.T.);
#12137=ORIENTED_EDGE('',*,*,#7826,.T.);
#12138=ORIENTED_EDGE('',*,*,#7825,.T.);
#12139=ORIENTED_EDGE('',*,*,#7831,.T.);
#12140=ORIENTED_EDGE('',*,*,#7830,.T.);
#12141=ORIENTED_EDGE('',*,*,#8380,.T.);
#12142=ORIENTED_EDGE('',*,*,#8379,.T.);
#12143=ORIENTED_EDGE('',*,*,#8402,.F.);
#12144=ORIENTED_EDGE('',*,*,#8377,.F.);
#12145=ORIENTED_EDGE('',*,*,#8376,.F.);
#12146=ORIENTED_EDGE('',*,*,#7833,.F.);
#12147=ORIENTED_EDGE('',*,*,#7832,.F.);
#12148=ORIENTED_EDGE('',*,*,#7828,.F.);
#12149=ORIENTED_EDGE('',*,*,#7827,.F.);
#12150=ORIENTED_EDGE('',*,*,#7823,.F.);
#12151=ORIENTED_EDGE('',*,*,#7822,.F.);
#12152=ORIENTED_EDGE('',*,*,#7818,.F.);
#12153=ORIENTED_EDGE('',*,*,#7817,.F.);
#12154=ORIENTED_EDGE('',*,*,#7813,.F.);
#12155=ORIENTED_EDGE('',*,*,#7812,.F.);
#12156=ORIENTED_EDGE('',*,*,#7808,.F.);
#12157=ORIENTED_EDGE('',*,*,#7807,.F.);
#12158=ORIENTED_EDGE('',*,*,#7803,.F.);
#12159=ORIENTED_EDGE('',*,*,#7802,.F.);
#12160=ORIENTED_EDGE('',*,*,#7798,.F.);
#12161=ORIENTED_EDGE('',*,*,#7797,.F.);
#12162=ORIENTED_EDGE('',*,*,#7793,.F.);
#12163=ORIENTED_EDGE('',*,*,#7792,.F.);
#12164=ORIENTED_EDGE('',*,*,#7788,.F.);
#12165=ORIENTED_EDGE('',*,*,#7787,.F.);
#12166=ORIENTED_EDGE('',*,*,#7783,.F.);
#12167=ORIENTED_EDGE('',*,*,#7782,.F.);
#12168=ORIENTED_EDGE('',*,*,#7778,.F.);
#12169=ORIENTED_EDGE('',*,*,#7777,.F.);
#12170=ORIENTED_EDGE('',*,*,#7773,.F.);
#12171=ORIENTED_EDGE('',*,*,#7772,.F.);
#12172=ORIENTED_EDGE('',*,*,#7768,.F.);
#12173=ORIENTED_EDGE('',*,*,#7767,.F.);
#12174=ORIENTED_EDGE('',*,*,#7763,.F.);
#12175=ORIENTED_EDGE('',*,*,#7762,.F.);
#12176=ORIENTED_EDGE('',*,*,#7758,.F.);
#12177=ORIENTED_EDGE('',*,*,#7757,.F.);
#12178=ORIENTED_EDGE('',*,*,#7753,.F.);
#12179=ORIENTED_EDGE('',*,*,#7752,.F.);
#12180=ORIENTED_EDGE('',*,*,#7748,.F.);
#12181=ORIENTED_EDGE('',*,*,#7747,.F.);
#12182=ORIENTED_EDGE('',*,*,#7743,.F.);
#12183=ORIENTED_EDGE('',*,*,#7742,.F.);
#12184=ORIENTED_EDGE('',*,*,#7738,.F.);
#12185=ORIENTED_EDGE('',*,*,#7737,.F.);
#12186=ORIENTED_EDGE('',*,*,#7733,.F.);
#12187=ORIENTED_EDGE('',*,*,#7732,.F.);
#12188=ORIENTED_EDGE('',*,*,#7728,.F.);
#12189=ORIENTED_EDGE('',*,*,#7727,.F.);
#12190=ORIENTED_EDGE('',*,*,#7723,.F.);
#12191=ORIENTED_EDGE('',*,*,#7722,.F.);
#12192=ORIENTED_EDGE('',*,*,#7718,.F.);
#12193=ORIENTED_EDGE('',*,*,#7717,.F.);
#12194=ORIENTED_EDGE('',*,*,#7713,.F.);
#12195=ORIENTED_EDGE('',*,*,#7712,.F.);
#12196=ORIENTED_EDGE('',*,*,#7708,.F.);
#12197=ORIENTED_EDGE('',*,*,#7707,.F.);
#12198=ORIENTED_EDGE('',*,*,#7703,.F.);
#12199=ORIENTED_EDGE('',*,*,#7702,.F.);
#12200=ORIENTED_EDGE('',*,*,#7698,.F.);
#12201=ORIENTED_EDGE('',*,*,#7697,.F.);
#12202=ORIENTED_EDGE('',*,*,#7693,.F.);
#12203=ORIENTED_EDGE('',*,*,#7692,.F.);
#12204=ORIENTED_EDGE('',*,*,#7688,.F.);
#12205=ORIENTED_EDGE('',*,*,#7687,.F.);
#12206=ORIENTED_EDGE('',*,*,#7683,.F.);
#12207=ORIENTED_EDGE('',*,*,#7682,.F.);
#12208=ORIENTED_EDGE('',*,*,#7678,.F.);
#12209=ORIENTED_EDGE('',*,*,#7677,.F.);
#12210=ORIENTED_EDGE('',*,*,#7673,.F.);
#12211=ORIENTED_EDGE('',*,*,#7672,.F.);
#12212=ORIENTED_EDGE('',*,*,#7668,.F.);
#12213=ORIENTED_EDGE('',*,*,#7667,.F.);
#12214=ORIENTED_EDGE('',*,*,#7663,.F.);
#12215=ORIENTED_EDGE('',*,*,#7662,.F.);
#12216=ORIENTED_EDGE('',*,*,#7658,.F.);
#12217=ORIENTED_EDGE('',*,*,#7657,.F.);
#12218=ORIENTED_EDGE('',*,*,#7653,.F.);
#12219=ORIENTED_EDGE('',*,*,#7652,.F.);
#12220=ORIENTED_EDGE('',*,*,#7648,.F.);
#12221=ORIENTED_EDGE('',*,*,#7647,.F.);
#12222=ORIENTED_EDGE('',*,*,#7643,.F.);
#12223=ORIENTED_EDGE('',*,*,#7642,.F.);
#12224=ORIENTED_EDGE('',*,*,#7638,.F.);
#12225=ORIENTED_EDGE('',*,*,#7637,.F.);
#12226=ORIENTED_EDGE('',*,*,#7633,.F.);
#12227=ORIENTED_EDGE('',*,*,#7632,.F.);
#12228=ORIENTED_EDGE('',*,*,#7628,.F.);
#12229=ORIENTED_EDGE('',*,*,#7627,.F.);
#12230=ORIENTED_EDGE('',*,*,#7623,.F.);
#12231=ORIENTED_EDGE('',*,*,#7622,.F.);
#12232=ORIENTED_EDGE('',*,*,#7618,.F.);
#12233=ORIENTED_EDGE('',*,*,#7617,.F.);
#12234=ORIENTED_EDGE('',*,*,#7613,.F.);
#12235=ORIENTED_EDGE('',*,*,#7612,.F.);
#12236=ORIENTED_EDGE('',*,*,#7608,.F.);
#12237=ORIENTED_EDGE('',*,*,#7607,.F.);
#12238=ORIENTED_EDGE('',*,*,#7603,.F.);
#12239=ORIENTED_EDGE('',*,*,#7602,.F.);
#12240=ORIENTED_EDGE('',*,*,#7598,.F.);
#12241=ORIENTED_EDGE('',*,*,#7597,.F.);
#12242=ORIENTED_EDGE('',*,*,#7593,.F.);
#12243=ORIENTED_EDGE('',*,*,#7592,.F.);
#12244=ORIENTED_EDGE('',*,*,#7588,.F.);
#12245=ORIENTED_EDGE('',*,*,#7587,.F.);
#12246=ORIENTED_EDGE('',*,*,#7583,.F.);
#12247=ORIENTED_EDGE('',*,*,#7582,.F.);
#12248=ORIENTED_EDGE('',*,*,#7578,.F.);
#12249=ORIENTED_EDGE('',*,*,#7577,.F.);
#12250=ORIENTED_EDGE('',*,*,#7573,.F.);
#12251=ORIENTED_EDGE('',*,*,#7572,.F.);
#12252=ORIENTED_EDGE('',*,*,#7568,.F.);
#12253=ORIENTED_EDGE('',*,*,#7567,.F.);
#12254=ORIENTED_EDGE('',*,*,#7563,.F.);
#12255=ORIENTED_EDGE('',*,*,#7562,.F.);
#12256=ORIENTED_EDGE('',*,*,#7558,.F.);
#12257=ORIENTED_EDGE('',*,*,#7557,.F.);
#12258=ORIENTED_EDGE('',*,*,#7553,.F.);
#12259=ORIENTED_EDGE('',*,*,#7552,.F.);
#12260=ORIENTED_EDGE('',*,*,#7548,.F.);
#12261=ORIENTED_EDGE('',*,*,#7547,.F.);
#12262=ORIENTED_EDGE('',*,*,#7543,.F.);
#12263=ORIENTED_EDGE('',*,*,#7542,.F.);
#12264=ORIENTED_EDGE('',*,*,#7538,.F.);
#12265=ORIENTED_EDGE('',*,*,#7537,.F.);
#12266=ORIENTED_EDGE('',*,*,#7533,.F.);
#12267=ORIENTED_EDGE('',*,*,#7532,.F.);
#12268=ORIENTED_EDGE('',*,*,#7528,.F.);
#12269=ORIENTED_EDGE('',*,*,#7527,.F.);
#12270=ORIENTED_EDGE('',*,*,#7523,.F.);
#12271=ORIENTED_EDGE('',*,*,#7522,.F.);
#12272=ORIENTED_EDGE('',*,*,#7518,.F.);
#12273=ORIENTED_EDGE('',*,*,#7517,.F.);
#12274=ORIENTED_EDGE('',*,*,#7513,.F.);
#12275=ORIENTED_EDGE('',*,*,#7512,.F.);
#12276=ORIENTED_EDGE('',*,*,#7508,.F.);
#12277=ORIENTED_EDGE('',*,*,#7507,.F.);
#12278=ORIENTED_EDGE('',*,*,#7503,.F.);
#12279=ORIENTED_EDGE('',*,*,#7502,.F.);
#12280=ORIENTED_EDGE('',*,*,#7498,.F.);
#12281=ORIENTED_EDGE('',*,*,#7497,.F.);
#12282=ORIENTED_EDGE('',*,*,#7493,.F.);
#12283=ORIENTED_EDGE('',*,*,#7492,.F.);
#12284=ORIENTED_EDGE('',*,*,#7488,.F.);
#12285=ORIENTED_EDGE('',*,*,#7487,.F.);
#12286=ORIENTED_EDGE('',*,*,#7483,.F.);
#12287=ORIENTED_EDGE('',*,*,#7482,.F.);
#12288=ORIENTED_EDGE('',*,*,#7478,.F.);
#12289=ORIENTED_EDGE('',*,*,#7477,.F.);
#12290=ORIENTED_EDGE('',*,*,#7473,.F.);
#12291=ORIENTED_EDGE('',*,*,#7472,.F.);
#12292=ORIENTED_EDGE('',*,*,#7468,.F.);
#12293=ORIENTED_EDGE('',*,*,#7467,.F.);
#12294=ORIENTED_EDGE('',*,*,#7463,.F.);
#12295=ORIENTED_EDGE('',*,*,#7462,.F.);
#12296=ORIENTED_EDGE('',*,*,#7458,.F.);
#12297=ORIENTED_EDGE('',*,*,#7457,.F.);
#12298=ORIENTED_EDGE('',*,*,#7453,.F.);
#12299=ORIENTED_EDGE('',*,*,#7452,.F.);
#12300=ORIENTED_EDGE('',*,*,#7448,.F.);
#12301=ORIENTED_EDGE('',*,*,#7447,.F.);
#12302=ORIENTED_EDGE('',*,*,#7443,.F.);
#12303=ORIENTED_EDGE('',*,*,#7442,.F.);
#12304=ORIENTED_EDGE('',*,*,#7438,.F.);
#12305=ORIENTED_EDGE('',*,*,#7437,.F.);
#12306=ORIENTED_EDGE('',*,*,#7433,.F.);
#12307=ORIENTED_EDGE('',*,*,#7432,.F.);
#12308=ORIENTED_EDGE('',*,*,#7428,.F.);
#12309=ORIENTED_EDGE('',*,*,#7427,.F.);
#12310=ORIENTED_EDGE('',*,*,#7423,.F.);
#12311=ORIENTED_EDGE('',*,*,#7422,.F.);
#12312=ORIENTED_EDGE('',*,*,#7418,.F.);
#12313=ORIENTED_EDGE('',*,*,#7417,.F.);
#12314=ORIENTED_EDGE('',*,*,#7413,.F.);
#12315=ORIENTED_EDGE('',*,*,#7412,.F.);
#12316=ORIENTED_EDGE('',*,*,#7408,.F.);
#12317=ORIENTED_EDGE('',*,*,#7407,.F.);
#12318=ORIENTED_EDGE('',*,*,#7403,.F.);
#12319=ORIENTED_EDGE('',*,*,#7402,.F.);
#12320=ORIENTED_EDGE('',*,*,#7398,.F.);
#12321=ORIENTED_EDGE('',*,*,#7397,.F.);
#12322=ORIENTED_EDGE('',*,*,#7393,.F.);
#12323=ORIENTED_EDGE('',*,*,#7392,.F.);
#12324=ORIENTED_EDGE('',*,*,#7388,.F.);
#12325=ORIENTED_EDGE('',*,*,#7387,.F.);
#12326=ORIENTED_EDGE('',*,*,#7383,.F.);
#12327=ORIENTED_EDGE('',*,*,#7382,.F.);
#12328=ORIENTED_EDGE('',*,*,#7378,.F.);
#12329=ORIENTED_EDGE('',*,*,#7377,.F.);
#12330=ORIENTED_EDGE('',*,*,#7373,.F.);
#12331=ORIENTED_EDGE('',*,*,#7372,.F.);
#12332=ORIENTED_EDGE('',*,*,#7368,.F.);
#12333=ORIENTED_EDGE('',*,*,#7367,.F.);
#12334=ORIENTED_EDGE('',*,*,#7363,.F.);
#12335=ORIENTED_EDGE('',*,*,#7362,.F.);
#12336=ORIENTED_EDGE('',*,*,#7358,.F.);
#12337=ORIENTED_EDGE('',*,*,#7357,.F.);
#12338=ORIENTED_EDGE('',*,*,#7353,.F.);
#12339=ORIENTED_EDGE('',*,*,#7352,.F.);
#12340=ORIENTED_EDGE('',*,*,#7348,.F.);
#12341=ORIENTED_EDGE('',*,*,#7347,.F.);
#12342=ORIENTED_EDGE('',*,*,#7343,.F.);
#12343=ORIENTED_EDGE('',*,*,#7342,.F.);
#12344=ORIENTED_EDGE('',*,*,#7338,.F.);
#12345=ORIENTED_EDGE('',*,*,#7337,.F.);
#12346=ORIENTED_EDGE('',*,*,#7333,.F.);
#12347=ORIENTED_EDGE('',*,*,#7332,.F.);
#12348=ORIENTED_EDGE('',*,*,#7328,.F.);
#12349=ORIENTED_EDGE('',*,*,#7327,.F.);
#12350=ORIENTED_EDGE('',*,*,#7323,.F.);
#12351=ORIENTED_EDGE('',*,*,#7322,.F.);
#12352=ORIENTED_EDGE('',*,*,#7318,.F.);
#12353=ORIENTED_EDGE('',*,*,#7317,.F.);
#12354=ORIENTED_EDGE('',*,*,#7313,.F.);
#12355=ORIENTED_EDGE('',*,*,#7312,.F.);
#12356=ORIENTED_EDGE('',*,*,#7308,.F.);
#12357=ORIENTED_EDGE('',*,*,#7307,.F.);
#12358=ORIENTED_EDGE('',*,*,#7303,.F.);
#12359=ORIENTED_EDGE('',*,*,#7302,.F.);
#12360=ORIENTED_EDGE('',*,*,#7298,.F.);
#12361=ORIENTED_EDGE('',*,*,#7297,.F.);
#12362=ORIENTED_EDGE('',*,*,#7293,.F.);
#12363=ORIENTED_EDGE('',*,*,#7292,.F.);
#12364=ORIENTED_EDGE('',*,*,#7288,.F.);
#12365=ORIENTED_EDGE('',*,*,#7287,.F.);
#12366=ORIENTED_EDGE('',*,*,#7283,.F.);
#12367=ORIENTED_EDGE('',*,*,#7282,.F.);
#12368=ORIENTED_EDGE('',*,*,#7278,.F.);
#12369=ORIENTED_EDGE('',*,*,#7277,.F.);
#12370=ORIENTED_EDGE('',*,*,#7273,.F.);
#12371=ORIENTED_EDGE('',*,*,#7272,.F.);
#12372=ORIENTED_EDGE('',*,*,#7268,.F.);
#12373=ORIENTED_EDGE('',*,*,#7267,.F.);
#12374=ORIENTED_EDGE('',*,*,#7263,.F.);
#12375=ORIENTED_EDGE('',*,*,#7262,.F.);
#12376=ORIENTED_EDGE('',*,*,#7258,.F.);
#12377=ORIENTED_EDGE('',*,*,#7257,.F.);
#12378=ORIENTED_EDGE('',*,*,#7253,.F.);
#12379=ORIENTED_EDGE('',*,*,#7252,.F.);
#12380=ORIENTED_EDGE('',*,*,#7248,.F.);
#12381=ORIENTED_EDGE('',*,*,#7247,.F.);
#12382=ORIENTED_EDGE('',*,*,#7243,.F.);
#12383=ORIENTED_EDGE('',*,*,#7242,.F.);
#12384=ORIENTED_EDGE('',*,*,#7238,.F.);
#12385=ORIENTED_EDGE('',*,*,#7237,.F.);
#12386=ORIENTED_EDGE('',*,*,#7233,.F.);
#12387=ORIENTED_EDGE('',*,*,#7232,.F.);
#12388=ORIENTED_EDGE('',*,*,#7228,.F.);
#12389=ORIENTED_EDGE('',*,*,#7227,.F.);
#12390=ORIENTED_EDGE('',*,*,#7223,.F.);
#12391=ORIENTED_EDGE('',*,*,#7222,.F.);
#12392=ORIENTED_EDGE('',*,*,#7218,.F.);
#12393=ORIENTED_EDGE('',*,*,#7217,.F.);
#12394=ORIENTED_EDGE('',*,*,#7213,.F.);
#12395=ORIENTED_EDGE('',*,*,#7212,.F.);
#12396=ORIENTED_EDGE('',*,*,#7208,.F.);
#12397=ORIENTED_EDGE('',*,*,#7207,.F.);
#12398=ORIENTED_EDGE('',*,*,#7203,.F.);
#12399=ORIENTED_EDGE('',*,*,#7202,.F.);
#12400=ORIENTED_EDGE('',*,*,#7198,.F.);
#12401=ORIENTED_EDGE('',*,*,#7197,.F.);
#12402=ORIENTED_EDGE('',*,*,#7193,.F.);
#12403=ORIENTED_EDGE('',*,*,#7192,.F.);
#12404=ORIENTED_EDGE('',*,*,#7188,.F.);
#12405=ORIENTED_EDGE('',*,*,#7187,.F.);
#12406=ORIENTED_EDGE('',*,*,#7183,.F.);
#12407=ORIENTED_EDGE('',*,*,#7182,.F.);
#12408=ORIENTED_EDGE('',*,*,#7178,.F.);
#12409=ORIENTED_EDGE('',*,*,#7177,.F.);
#12410=ORIENTED_EDGE('',*,*,#7173,.F.);
#12411=ORIENTED_EDGE('',*,*,#7172,.F.);
#12412=ORIENTED_EDGE('',*,*,#7168,.F.);
#12413=ORIENTED_EDGE('',*,*,#7167,.F.);
#12414=ORIENTED_EDGE('',*,*,#7163,.F.);
#12415=ORIENTED_EDGE('',*,*,#7162,.F.);
#12416=ORIENTED_EDGE('',*,*,#7158,.F.);
#12417=ORIENTED_EDGE('',*,*,#7157,.F.);
#12418=ORIENTED_EDGE('',*,*,#7153,.F.);
#12419=ORIENTED_EDGE('',*,*,#7152,.F.);
#12420=ORIENTED_EDGE('',*,*,#7148,.F.);
#12421=ORIENTED_EDGE('',*,*,#7147,.F.);
#12422=ORIENTED_EDGE('',*,*,#7143,.F.);
#12423=ORIENTED_EDGE('',*,*,#7142,.F.);
#12424=ORIENTED_EDGE('',*,*,#7138,.F.);
#12425=ORIENTED_EDGE('',*,*,#7137,.F.);
#12426=ORIENTED_EDGE('',*,*,#7133,.F.);
#12427=ORIENTED_EDGE('',*,*,#7132,.F.);
#12428=ORIENTED_EDGE('',*,*,#7128,.F.);
#12429=ORIENTED_EDGE('',*,*,#7127,.F.);
#12430=ORIENTED_EDGE('',*,*,#7123,.F.);
#12431=ORIENTED_EDGE('',*,*,#7122,.F.);
#12432=ORIENTED_EDGE('',*,*,#7118,.F.);
#12433=ORIENTED_EDGE('',*,*,#7117,.F.);
#12434=ORIENTED_EDGE('',*,*,#7113,.F.);
#12435=ORIENTED_EDGE('',*,*,#7112,.F.);
#12436=ORIENTED_EDGE('',*,*,#7108,.F.);
#12437=ORIENTED_EDGE('',*,*,#7107,.F.);
#12438=ORIENTED_EDGE('',*,*,#7103,.F.);
#12439=ORIENTED_EDGE('',*,*,#7102,.F.);
#12440=ORIENTED_EDGE('',*,*,#7098,.F.);
#12441=ORIENTED_EDGE('',*,*,#7097,.F.);
#12442=ORIENTED_EDGE('',*,*,#7093,.F.);
#12443=ORIENTED_EDGE('',*,*,#7092,.F.);
#12444=ORIENTED_EDGE('',*,*,#7088,.F.);
#12445=ORIENTED_EDGE('',*,*,#7087,.F.);
#12446=ORIENTED_EDGE('',*,*,#7083,.F.);
#12447=ORIENTED_EDGE('',*,*,#7082,.F.);
#12448=ORIENTED_EDGE('',*,*,#7078,.F.);
#12449=ORIENTED_EDGE('',*,*,#7077,.F.);
#12450=ORIENTED_EDGE('',*,*,#7073,.F.);
#12451=ORIENTED_EDGE('',*,*,#7072,.F.);
#12452=ORIENTED_EDGE('',*,*,#7068,.F.);
#12453=ORIENTED_EDGE('',*,*,#7067,.F.);
#12454=ORIENTED_EDGE('',*,*,#7063,.F.);
#12455=ORIENTED_EDGE('',*,*,#7062,.F.);
#12456=ORIENTED_EDGE('',*,*,#7058,.F.);
#12457=ORIENTED_EDGE('',*,*,#7057,.F.);
#12458=ORIENTED_EDGE('',*,*,#7053,.F.);
#12459=ORIENTED_EDGE('',*,*,#7052,.F.);
#12460=ORIENTED_EDGE('',*,*,#7048,.F.);
#12461=ORIENTED_EDGE('',*,*,#7047,.F.);
#12462=ORIENTED_EDGE('',*,*,#7043,.F.);
#12463=ORIENTED_EDGE('',*,*,#7042,.F.);
#12464=ORIENTED_EDGE('',*,*,#7038,.F.);
#12465=ORIENTED_EDGE('',*,*,#7037,.F.);
#12466=ORIENTED_EDGE('',*,*,#7033,.F.);
#12467=ORIENTED_EDGE('',*,*,#7032,.F.);
#12468=ORIENTED_EDGE('',*,*,#7028,.F.);
#12469=ORIENTED_EDGE('',*,*,#7027,.F.);
#12470=ORIENTED_EDGE('',*,*,#7023,.F.);
#12471=ORIENTED_EDGE('',*,*,#7022,.F.);
#12472=ORIENTED_EDGE('',*,*,#7018,.F.);
#12473=ORIENTED_EDGE('',*,*,#7017,.F.);
#12474=ORIENTED_EDGE('',*,*,#7013,.F.);
#12475=ORIENTED_EDGE('',*,*,#7012,.F.);
#12476=ORIENTED_EDGE('',*,*,#7008,.F.);
#12477=ORIENTED_EDGE('',*,*,#7007,.F.);
#12478=ORIENTED_EDGE('',*,*,#7003,.F.);
#12479=ORIENTED_EDGE('',*,*,#7002,.F.);
#12480=ORIENTED_EDGE('',*,*,#6998,.F.);
#12481=ORIENTED_EDGE('',*,*,#6997,.F.);
#12482=ORIENTED_EDGE('',*,*,#6993,.F.);
#12483=ORIENTED_EDGE('',*,*,#6992,.F.);
#12484=ORIENTED_EDGE('',*,*,#6988,.F.);
#12485=ORIENTED_EDGE('',*,*,#6987,.F.);
#12486=ORIENTED_EDGE('',*,*,#6983,.F.);
#12487=ORIENTED_EDGE('',*,*,#6982,.F.);
#12488=ORIENTED_EDGE('',*,*,#6978,.F.);
#12489=ORIENTED_EDGE('',*,*,#6977,.F.);
#12490=ORIENTED_EDGE('',*,*,#6973,.F.);
#12491=ORIENTED_EDGE('',*,*,#6972,.F.);
#12492=ORIENTED_EDGE('',*,*,#6968,.F.);
#12493=ORIENTED_EDGE('',*,*,#6967,.F.);
#12494=ORIENTED_EDGE('',*,*,#6963,.F.);
#12495=ORIENTED_EDGE('',*,*,#6962,.F.);
#12496=ORIENTED_EDGE('',*,*,#6958,.F.);
#12497=ORIENTED_EDGE('',*,*,#6957,.F.);
#12498=ORIENTED_EDGE('',*,*,#6953,.F.);
#12499=ORIENTED_EDGE('',*,*,#6952,.F.);
#12500=ORIENTED_EDGE('',*,*,#6948,.F.);
#12501=ORIENTED_EDGE('',*,*,#6947,.F.);
#12502=ORIENTED_EDGE('',*,*,#6943,.F.);
#12503=ORIENTED_EDGE('',*,*,#6942,.F.);
#12504=ORIENTED_EDGE('',*,*,#6938,.F.);
#12505=ORIENTED_EDGE('',*,*,#6937,.F.);
#12506=ORIENTED_EDGE('',*,*,#6933,.F.);
#12507=ORIENTED_EDGE('',*,*,#6932,.F.);
#12508=ORIENTED_EDGE('',*,*,#6928,.F.);
#12509=ORIENTED_EDGE('',*,*,#6927,.F.);
#12510=ORIENTED_EDGE('',*,*,#6923,.F.);
#12511=ORIENTED_EDGE('',*,*,#6922,.F.);
#12512=ORIENTED_EDGE('',*,*,#6918,.F.);
#12513=ORIENTED_EDGE('',*,*,#6917,.F.);
#12514=ORIENTED_EDGE('',*,*,#6913,.F.);
#12515=ORIENTED_EDGE('',*,*,#6912,.F.);
#12516=ORIENTED_EDGE('',*,*,#6908,.F.);
#12517=ORIENTED_EDGE('',*,*,#6907,.F.);
#12518=ORIENTED_EDGE('',*,*,#6903,.F.);
#12519=ORIENTED_EDGE('',*,*,#6902,.F.);
#12520=ORIENTED_EDGE('',*,*,#6898,.F.);
#12521=ORIENTED_EDGE('',*,*,#6897,.F.);
#12522=ORIENTED_EDGE('',*,*,#6893,.F.);
#12523=ORIENTED_EDGE('',*,*,#6892,.F.);
#12524=ORIENTED_EDGE('',*,*,#6888,.F.);
#12525=ORIENTED_EDGE('',*,*,#6887,.F.);
#12526=ORIENTED_EDGE('',*,*,#6883,.F.);
#12527=ORIENTED_EDGE('',*,*,#6882,.F.);
#12528=ORIENTED_EDGE('',*,*,#6878,.F.);
#12529=ORIENTED_EDGE('',*,*,#6877,.F.);
#12530=ORIENTED_EDGE('',*,*,#6873,.F.);
#12531=ORIENTED_EDGE('',*,*,#6872,.F.);
#12532=ORIENTED_EDGE('',*,*,#6868,.F.);
#12533=ORIENTED_EDGE('',*,*,#6867,.F.);
#12534=ORIENTED_EDGE('',*,*,#6863,.F.);
#12535=ORIENTED_EDGE('',*,*,#6862,.F.);
#12536=ORIENTED_EDGE('',*,*,#6858,.F.);
#12537=ORIENTED_EDGE('',*,*,#6857,.F.);
#12538=ORIENTED_EDGE('',*,*,#6853,.F.);
#12539=ORIENTED_EDGE('',*,*,#6852,.F.);
#12540=ORIENTED_EDGE('',*,*,#6848,.F.);
#12541=ORIENTED_EDGE('',*,*,#6847,.F.);
#12542=ORIENTED_EDGE('',*,*,#6843,.F.);
#12543=ORIENTED_EDGE('',*,*,#6842,.F.);
#12544=ORIENTED_EDGE('',*,*,#6838,.F.);
#12545=ORIENTED_EDGE('',*,*,#6837,.F.);
#12546=ORIENTED_EDGE('',*,*,#6833,.F.);
#12547=ORIENTED_EDGE('',*,*,#6832,.F.);
#12548=ORIENTED_EDGE('',*,*,#6828,.F.);
#12549=ORIENTED_EDGE('',*,*,#6827,.F.);
#12550=ORIENTED_EDGE('',*,*,#6823,.F.);
#12551=ORIENTED_EDGE('',*,*,#6822,.F.);
#12552=ORIENTED_EDGE('',*,*,#6818,.F.);
#12553=ORIENTED_EDGE('',*,*,#6817,.F.);
#12554=ORIENTED_EDGE('',*,*,#6813,.F.);
#12555=ORIENTED_EDGE('',*,*,#6812,.F.);
#12556=ORIENTED_EDGE('',*,*,#6808,.F.);
#12557=ORIENTED_EDGE('',*,*,#6807,.F.);
#12558=ORIENTED_EDGE('',*,*,#6803,.F.);
#12559=ORIENTED_EDGE('',*,*,#6802,.F.);
#12560=ORIENTED_EDGE('',*,*,#6798,.F.);
#12561=ORIENTED_EDGE('',*,*,#6797,.F.);
#12562=ORIENTED_EDGE('',*,*,#6793,.F.);
#12563=ORIENTED_EDGE('',*,*,#6792,.F.);
#12564=ORIENTED_EDGE('',*,*,#6788,.F.);
#12565=ORIENTED_EDGE('',*,*,#6787,.F.);
#12566=ORIENTED_EDGE('',*,*,#6783,.F.);
#12567=ORIENTED_EDGE('',*,*,#6782,.F.);
#12568=ORIENTED_EDGE('',*,*,#6778,.F.);
#12569=ORIENTED_EDGE('',*,*,#6777,.F.);
#12570=ORIENTED_EDGE('',*,*,#6773,.F.);
#12571=ORIENTED_EDGE('',*,*,#6772,.F.);
#12572=ORIENTED_EDGE('',*,*,#6768,.F.);
#12573=ORIENTED_EDGE('',*,*,#6767,.F.);
#12574=ORIENTED_EDGE('',*,*,#6763,.F.);
#12575=ORIENTED_EDGE('',*,*,#6762,.F.);
#12576=ORIENTED_EDGE('',*,*,#6758,.F.);
#12577=ORIENTED_EDGE('',*,*,#6757,.F.);
#12578=ORIENTED_EDGE('',*,*,#6753,.F.);
#12579=ORIENTED_EDGE('',*,*,#6752,.F.);
#12580=ORIENTED_EDGE('',*,*,#6748,.F.);
#12581=ORIENTED_EDGE('',*,*,#6747,.F.);
#12582=ORIENTED_EDGE('',*,*,#6743,.F.);
#12583=ORIENTED_EDGE('',*,*,#6742,.F.);
#12584=ORIENTED_EDGE('',*,*,#6738,.F.);
#12585=ORIENTED_EDGE('',*,*,#6737,.F.);
#12586=ORIENTED_EDGE('',*,*,#6733,.F.);
#12587=ORIENTED_EDGE('',*,*,#6732,.F.);
#12588=ORIENTED_EDGE('',*,*,#6728,.F.);
#12589=ORIENTED_EDGE('',*,*,#6727,.F.);
#12590=ORIENTED_EDGE('',*,*,#6723,.F.);
#12591=ORIENTED_EDGE('',*,*,#6722,.F.);
#12592=ORIENTED_EDGE('',*,*,#6718,.F.);
#12593=ORIENTED_EDGE('',*,*,#6717,.F.);
#12594=ORIENTED_EDGE('',*,*,#6713,.F.);
#12595=ORIENTED_EDGE('',*,*,#6712,.F.);
#12596=ORIENTED_EDGE('',*,*,#6708,.F.);
#12597=ORIENTED_EDGE('',*,*,#6707,.F.);
#12598=ORIENTED_EDGE('',*,*,#6703,.F.);
#12599=ORIENTED_EDGE('',*,*,#6702,.F.);
#12600=ORIENTED_EDGE('',*,*,#6698,.F.);
#12601=ORIENTED_EDGE('',*,*,#6697,.F.);
#12602=ORIENTED_EDGE('',*,*,#6693,.F.);
#12603=ORIENTED_EDGE('',*,*,#6692,.F.);
#12604=ORIENTED_EDGE('',*,*,#6688,.F.);
#12605=ORIENTED_EDGE('',*,*,#6687,.F.);
#12606=ORIENTED_EDGE('',*,*,#6683,.F.);
#12607=ORIENTED_EDGE('',*,*,#6682,.F.);
#12608=ORIENTED_EDGE('',*,*,#6678,.F.);
#12609=ORIENTED_EDGE('',*,*,#6677,.F.);
#12610=ORIENTED_EDGE('',*,*,#6673,.F.);
#12611=ORIENTED_EDGE('',*,*,#6672,.F.);
#12612=ORIENTED_EDGE('',*,*,#6668,.F.);
#12613=ORIENTED_EDGE('',*,*,#6667,.F.);
#12614=ORIENTED_EDGE('',*,*,#6663,.F.);
#12615=ORIENTED_EDGE('',*,*,#6662,.F.);
#12616=ORIENTED_EDGE('',*,*,#6658,.F.);
#12617=ORIENTED_EDGE('',*,*,#6657,.F.);
#12618=ORIENTED_EDGE('',*,*,#6653,.F.);
#12619=ORIENTED_EDGE('',*,*,#6652,.F.);
#12620=ORIENTED_EDGE('',*,*,#6648,.F.);
#12621=ORIENTED_EDGE('',*,*,#6647,.F.);
#12622=ORIENTED_EDGE('',*,*,#6643,.F.);
#12623=ORIENTED_EDGE('',*,*,#6642,.F.);
#12624=ORIENTED_EDGE('',*,*,#6638,.F.);
#12625=ORIENTED_EDGE('',*,*,#6637,.F.);
#12626=ORIENTED_EDGE('',*,*,#6633,.F.);
#12627=ORIENTED_EDGE('',*,*,#6632,.F.);
#12628=ORIENTED_EDGE('',*,*,#6628,.F.);
#12629=ORIENTED_EDGE('',*,*,#6627,.F.);
#12630=ORIENTED_EDGE('',*,*,#6623,.F.);
#12631=ORIENTED_EDGE('',*,*,#6622,.F.);
#12632=ORIENTED_EDGE('',*,*,#6618,.F.);
#12633=ORIENTED_EDGE('',*,*,#6617,.F.);
#12634=ORIENTED_EDGE('',*,*,#6613,.F.);
#12635=ORIENTED_EDGE('',*,*,#6612,.F.);
#12636=ORIENTED_EDGE('',*,*,#6608,.F.);
#12637=ORIENTED_EDGE('',*,*,#6607,.F.);
#12638=ORIENTED_EDGE('',*,*,#6603,.F.);
#12639=ORIENTED_EDGE('',*,*,#6602,.F.);
#12640=ORIENTED_EDGE('',*,*,#6598,.F.);
#12641=ORIENTED_EDGE('',*,*,#6597,.F.);
#12642=ORIENTED_EDGE('',*,*,#6593,.F.);
#12643=ORIENTED_EDGE('',*,*,#6592,.F.);
#12644=ORIENTED_EDGE('',*,*,#6588,.F.);
#12645=ORIENTED_EDGE('',*,*,#6587,.F.);
#12646=ORIENTED_EDGE('',*,*,#6583,.F.);
#12647=ORIENTED_EDGE('',*,*,#6582,.F.);
#12648=ORIENTED_EDGE('',*,*,#6578,.F.);
#12649=ORIENTED_EDGE('',*,*,#6577,.F.);
#12650=ORIENTED_EDGE('',*,*,#6573,.F.);
#12651=ORIENTED_EDGE('',*,*,#6572,.F.);
#12652=ORIENTED_EDGE('',*,*,#6568,.F.);
#12653=ORIENTED_EDGE('',*,*,#6567,.F.);
#12654=ORIENTED_EDGE('',*,*,#6563,.F.);
#12655=ORIENTED_EDGE('',*,*,#6562,.F.);
#12656=ORIENTED_EDGE('',*,*,#6558,.F.);
#12657=ORIENTED_EDGE('',*,*,#6557,.F.);
#12658=ORIENTED_EDGE('',*,*,#6553,.F.);
#12659=ORIENTED_EDGE('',*,*,#6552,.F.);
#12660=ORIENTED_EDGE('',*,*,#6548,.F.);
#12661=ORIENTED_EDGE('',*,*,#6547,.F.);
#12662=ORIENTED_EDGE('',*,*,#6543,.F.);
#12663=ORIENTED_EDGE('',*,*,#6542,.F.);
#12664=ORIENTED_EDGE('',*,*,#6538,.F.);
#12665=ORIENTED_EDGE('',*,*,#6537,.F.);
#12666=ORIENTED_EDGE('',*,*,#6533,.F.);
#12667=ORIENTED_EDGE('',*,*,#6532,.F.);
#12668=ORIENTED_EDGE('',*,*,#6528,.F.);
#12669=ORIENTED_EDGE('',*,*,#6527,.F.);
#12670=ORIENTED_EDGE('',*,*,#6523,.F.);
#12671=ORIENTED_EDGE('',*,*,#6522,.F.);
#12672=ORIENTED_EDGE('',*,*,#6518,.F.);
#12673=ORIENTED_EDGE('',*,*,#6517,.F.);
#12674=ORIENTED_EDGE('',*,*,#6513,.F.);
#12675=ORIENTED_EDGE('',*,*,#6512,.F.);
#12676=ORIENTED_EDGE('',*,*,#6508,.F.);
#12677=ORIENTED_EDGE('',*,*,#6507,.F.);
#12678=ORIENTED_EDGE('',*,*,#6503,.F.);
#12679=ORIENTED_EDGE('',*,*,#6502,.F.);
#12680=ORIENTED_EDGE('',*,*,#6498,.F.);
#12681=ORIENTED_EDGE('',*,*,#8386,.F.);
#12682=ORIENTED_EDGE('',*,*,#7834,.F.);
#12683=ORIENTED_EDGE('',*,*,#8375,.F.);
#12684=ORIENTED_EDGE('',*,*,#8374,.F.);
#12685=ORIENTED_EDGE('',*,*,#8373,.F.);
#12686=ORIENTED_EDGE('',*,*,#8372,.F.);
#12687=ORIENTED_EDGE('',*,*,#8371,.F.);
#12688=ORIENTED_EDGE('',*,*,#8370,.F.);
#12689=ORIENTED_EDGE('',*,*,#8369,.F.);
#12690=ORIENTED_EDGE('',*,*,#8368,.F.);
#12691=ORIENTED_EDGE('',*,*,#8367,.F.);
#12692=ORIENTED_EDGE('',*,*,#8366,.F.);
#12693=ORIENTED_EDGE('',*,*,#8365,.F.);
#12694=ORIENTED_EDGE('',*,*,#8364,.F.);
#12695=ORIENTED_EDGE('',*,*,#8363,.F.);
#12696=ORIENTED_EDGE('',*,*,#8362,.F.);
#12697=ORIENTED_EDGE('',*,*,#8361,.F.);
#12698=ORIENTED_EDGE('',*,*,#8360,.F.);
#12699=ORIENTED_EDGE('',*,*,#8359,.F.);
#12700=ORIENTED_EDGE('',*,*,#8358,.F.);
#12701=ORIENTED_EDGE('',*,*,#8357,.F.);
#12702=ORIENTED_EDGE('',*,*,#8356,.F.);
#12703=ORIENTED_EDGE('',*,*,#8355,.F.);
#12704=ORIENTED_EDGE('',*,*,#8354,.F.);
#12705=ORIENTED_EDGE('',*,*,#8353,.F.);
#12706=ORIENTED_EDGE('',*,*,#8352,.F.);
#12707=ORIENTED_EDGE('',*,*,#8351,.F.);
#12708=ORIENTED_EDGE('',*,*,#8350,.F.);
#12709=ORIENTED_EDGE('',*,*,#8349,.F.);
#12710=ORIENTED_EDGE('',*,*,#8348,.F.);
#12711=ORIENTED_EDGE('',*,*,#8347,.F.);
#12712=ORIENTED_EDGE('',*,*,#8346,.F.);
#12713=ORIENTED_EDGE('',*,*,#8345,.F.);
#12714=ORIENTED_EDGE('',*,*,#8344,.F.);
#12715=ORIENTED_EDGE('',*,*,#8343,.F.);
#12716=ORIENTED_EDGE('',*,*,#8342,.F.);
#12717=ORIENTED_EDGE('',*,*,#8341,.F.);
#12718=ORIENTED_EDGE('',*,*,#8340,.F.);
#12719=ORIENTED_EDGE('',*,*,#8339,.F.);
#12720=ORIENTED_EDGE('',*,*,#8338,.F.);
#12721=ORIENTED_EDGE('',*,*,#8337,.F.);
#12722=ORIENTED_EDGE('',*,*,#8336,.F.);
#12723=ORIENTED_EDGE('',*,*,#8335,.F.);
#12724=ORIENTED_EDGE('',*,*,#8334,.F.);
#12725=ORIENTED_EDGE('',*,*,#8333,.F.);
#12726=ORIENTED_EDGE('',*,*,#8332,.F.);
#12727=ORIENTED_EDGE('',*,*,#8331,.F.);
#12728=ORIENTED_EDGE('',*,*,#8330,.F.);
#12729=ORIENTED_EDGE('',*,*,#8329,.F.);
#12730=ORIENTED_EDGE('',*,*,#8328,.F.);
#12731=ORIENTED_EDGE('',*,*,#8327,.F.);
#12732=ORIENTED_EDGE('',*,*,#8326,.F.);
#12733=ORIENTED_EDGE('',*,*,#8325,.F.);
#12734=ORIENTED_EDGE('',*,*,#8324,.F.);
#12735=ORIENTED_EDGE('',*,*,#8323,.F.);
#12736=ORIENTED_EDGE('',*,*,#8322,.F.);
#12737=ORIENTED_EDGE('',*,*,#8321,.F.);
#12738=ORIENTED_EDGE('',*,*,#8320,.F.);
#12739=ORIENTED_EDGE('',*,*,#8319,.F.);
#12740=ORIENTED_EDGE('',*,*,#8318,.F.);
#12741=ORIENTED_EDGE('',*,*,#8317,.F.);
#12742=ORIENTED_EDGE('',*,*,#8316,.F.);
#12743=ORIENTED_EDGE('',*,*,#8315,.F.);
#12744=ORIENTED_EDGE('',*,*,#8314,.F.);
#12745=ORIENTED_EDGE('',*,*,#8313,.F.);
#12746=ORIENTED_EDGE('',*,*,#8312,.F.);
#12747=ORIENTED_EDGE('',*,*,#8311,.F.);
#12748=ORIENTED_EDGE('',*,*,#8310,.F.);
#12749=ORIENTED_EDGE('',*,*,#8309,.F.);
#12750=ORIENTED_EDGE('',*,*,#8308,.F.);
#12751=ORIENTED_EDGE('',*,*,#8307,.F.);
#12752=ORIENTED_EDGE('',*,*,#8306,.F.);
#12753=ORIENTED_EDGE('',*,*,#8305,.F.);
#12754=ORIENTED_EDGE('',*,*,#8304,.F.);
#12755=ORIENTED_EDGE('',*,*,#8303,.F.);
#12756=ORIENTED_EDGE('',*,*,#8302,.F.);
#12757=ORIENTED_EDGE('',*,*,#8301,.F.);
#12758=ORIENTED_EDGE('',*,*,#8300,.F.);
#12759=ORIENTED_EDGE('',*,*,#8299,.F.);
#12760=ORIENTED_EDGE('',*,*,#8298,.F.);
#12761=ORIENTED_EDGE('',*,*,#8297,.F.);
#12762=ORIENTED_EDGE('',*,*,#8296,.F.);
#12763=ORIENTED_EDGE('',*,*,#8295,.F.);
#12764=ORIENTED_EDGE('',*,*,#8294,.F.);
#12765=ORIENTED_EDGE('',*,*,#8293,.F.);
#12766=ORIENTED_EDGE('',*,*,#8292,.F.);
#12767=ORIENTED_EDGE('',*,*,#8291,.F.);
#12768=ORIENTED_EDGE('',*,*,#8290,.F.);
#12769=ORIENTED_EDGE('',*,*,#8289,.F.);
#12770=ORIENTED_EDGE('',*,*,#8288,.F.);
#12771=ORIENTED_EDGE('',*,*,#8287,.F.);
#12772=ORIENTED_EDGE('',*,*,#8286,.F.);
#12773=ORIENTED_EDGE('',*,*,#8285,.F.);
#12774=ORIENTED_EDGE('',*,*,#8284,.F.);
#12775=ORIENTED_EDGE('',*,*,#8283,.F.);
#12776=ORIENTED_EDGE('',*,*,#8282,.F.);
#12777=ORIENTED_EDGE('',*,*,#8281,.F.);
#12778=ORIENTED_EDGE('',*,*,#8280,.F.);
#12779=ORIENTED_EDGE('',*,*,#8279,.F.);
#12780=ORIENTED_EDGE('',*,*,#8278,.F.);
#12781=ORIENTED_EDGE('',*,*,#8277,.F.);
#12782=ORIENTED_EDGE('',*,*,#8276,.F.);
#12783=ORIENTED_EDGE('',*,*,#8275,.F.);
#12784=ORIENTED_EDGE('',*,*,#8274,.F.);
#12785=ORIENTED_EDGE('',*,*,#8273,.F.);
#12786=ORIENTED_EDGE('',*,*,#8272,.F.);
#12787=ORIENTED_EDGE('',*,*,#8271,.F.);
#12788=ORIENTED_EDGE('',*,*,#8270,.F.);
#12789=ORIENTED_EDGE('',*,*,#8269,.F.);
#12790=ORIENTED_EDGE('',*,*,#8268,.F.);
#12791=ORIENTED_EDGE('',*,*,#8267,.F.);
#12792=ORIENTED_EDGE('',*,*,#8266,.F.);
#12793=ORIENTED_EDGE('',*,*,#8265,.F.);
#12794=ORIENTED_EDGE('',*,*,#8264,.F.);
#12795=ORIENTED_EDGE('',*,*,#8263,.F.);
#12796=ORIENTED_EDGE('',*,*,#8262,.F.);
#12797=ORIENTED_EDGE('',*,*,#8261,.F.);
#12798=ORIENTED_EDGE('',*,*,#8260,.F.);
#12799=ORIENTED_EDGE('',*,*,#8259,.F.);
#12800=ORIENTED_EDGE('',*,*,#8258,.F.);
#12801=ORIENTED_EDGE('',*,*,#8257,.F.);
#12802=ORIENTED_EDGE('',*,*,#8256,.F.);
#12803=ORIENTED_EDGE('',*,*,#8255,.F.);
#12804=ORIENTED_EDGE('',*,*,#8254,.F.);
#12805=ORIENTED_EDGE('',*,*,#8253,.F.);
#12806=ORIENTED_EDGE('',*,*,#8252,.F.);
#12807=ORIENTED_EDGE('',*,*,#8251,.F.);
#12808=ORIENTED_EDGE('',*,*,#8250,.F.);
#12809=ORIENTED_EDGE('',*,*,#8249,.F.);
#12810=ORIENTED_EDGE('',*,*,#8248,.F.);
#12811=ORIENTED_EDGE('',*,*,#8247,.F.);
#12812=ORIENTED_EDGE('',*,*,#8246,.F.);
#12813=ORIENTED_EDGE('',*,*,#8245,.F.);
#12814=ORIENTED_EDGE('',*,*,#8244,.F.);
#12815=ORIENTED_EDGE('',*,*,#8243,.F.);
#12816=ORIENTED_EDGE('',*,*,#8242,.F.);
#12817=ORIENTED_EDGE('',*,*,#8241,.F.);
#12818=ORIENTED_EDGE('',*,*,#8240,.F.);
#12819=ORIENTED_EDGE('',*,*,#8239,.F.);
#12820=ORIENTED_EDGE('',*,*,#8238,.F.);
#12821=ORIENTED_EDGE('',*,*,#8237,.F.);
#12822=ORIENTED_EDGE('',*,*,#8236,.F.);
#12823=ORIENTED_EDGE('',*,*,#8235,.F.);
#12824=ORIENTED_EDGE('',*,*,#8234,.F.);
#12825=ORIENTED_EDGE('',*,*,#8233,.F.);
#12826=ORIENTED_EDGE('',*,*,#8232,.F.);
#12827=ORIENTED_EDGE('',*,*,#8231,.F.);
#12828=ORIENTED_EDGE('',*,*,#8230,.F.);
#12829=ORIENTED_EDGE('',*,*,#8229,.F.);
#12830=ORIENTED_EDGE('',*,*,#8228,.F.);
#12831=ORIENTED_EDGE('',*,*,#8227,.F.);
#12832=ORIENTED_EDGE('',*,*,#8226,.F.);
#12833=ORIENTED_EDGE('',*,*,#8225,.F.);
#12834=ORIENTED_EDGE('',*,*,#8224,.F.);
#12835=ORIENTED_EDGE('',*,*,#8223,.F.);
#12836=ORIENTED_EDGE('',*,*,#8222,.F.);
#12837=ORIENTED_EDGE('',*,*,#8221,.F.);
#12838=ORIENTED_EDGE('',*,*,#8220,.F.);
#12839=ORIENTED_EDGE('',*,*,#8219,.F.);
#12840=ORIENTED_EDGE('',*,*,#8218,.F.);
#12841=ORIENTED_EDGE('',*,*,#8217,.F.);
#12842=ORIENTED_EDGE('',*,*,#8216,.F.);
#12843=ORIENTED_EDGE('',*,*,#8215,.F.);
#12844=ORIENTED_EDGE('',*,*,#8214,.F.);
#12845=ORIENTED_EDGE('',*,*,#8213,.F.);
#12846=ORIENTED_EDGE('',*,*,#8212,.F.);
#12847=ORIENTED_EDGE('',*,*,#8211,.F.);
#12848=ORIENTED_EDGE('',*,*,#8210,.F.);
#12849=ORIENTED_EDGE('',*,*,#8209,.F.);
#12850=ORIENTED_EDGE('',*,*,#8208,.F.);
#12851=ORIENTED_EDGE('',*,*,#8207,.F.);
#12852=ORIENTED_EDGE('',*,*,#8206,.F.);
#12853=ORIENTED_EDGE('',*,*,#8205,.F.);
#12854=ORIENTED_EDGE('',*,*,#8204,.F.);
#12855=ORIENTED_EDGE('',*,*,#8203,.F.);
#12856=ORIENTED_EDGE('',*,*,#8202,.F.);
#12857=ORIENTED_EDGE('',*,*,#8201,.F.);
#12858=ORIENTED_EDGE('',*,*,#8200,.F.);
#12859=ORIENTED_EDGE('',*,*,#8199,.F.);
#12860=ORIENTED_EDGE('',*,*,#8198,.F.);
#12861=ORIENTED_EDGE('',*,*,#8197,.F.);
#12862=ORIENTED_EDGE('',*,*,#8196,.F.);
#12863=ORIENTED_EDGE('',*,*,#8195,.F.);
#12864=ORIENTED_EDGE('',*,*,#8194,.F.);
#12865=ORIENTED_EDGE('',*,*,#8193,.F.);
#12866=ORIENTED_EDGE('',*,*,#8192,.F.);
#12867=ORIENTED_EDGE('',*,*,#8191,.F.);
#12868=ORIENTED_EDGE('',*,*,#8190,.F.);
#12869=ORIENTED_EDGE('',*,*,#8189,.F.);
#12870=ORIENTED_EDGE('',*,*,#8188,.F.);
#12871=ORIENTED_EDGE('',*,*,#8187,.F.);
#12872=ORIENTED_EDGE('',*,*,#8186,.F.);
#12873=ORIENTED_EDGE('',*,*,#8185,.F.);
#12874=ORIENTED_EDGE('',*,*,#8184,.F.);
#12875=ORIENTED_EDGE('',*,*,#8183,.F.);
#12876=ORIENTED_EDGE('',*,*,#8182,.F.);
#12877=ORIENTED_EDGE('',*,*,#8181,.F.);
#12878=ORIENTED_EDGE('',*,*,#8180,.F.);
#12879=ORIENTED_EDGE('',*,*,#8179,.F.);
#12880=ORIENTED_EDGE('',*,*,#8178,.F.);
#12881=ORIENTED_EDGE('',*,*,#8177,.F.);
#12882=ORIENTED_EDGE('',*,*,#8176,.F.);
#12883=ORIENTED_EDGE('',*,*,#8175,.F.);
#12884=ORIENTED_EDGE('',*,*,#8174,.F.);
#12885=ORIENTED_EDGE('',*,*,#8173,.F.);
#12886=ORIENTED_EDGE('',*,*,#8172,.F.);
#12887=ORIENTED_EDGE('',*,*,#8171,.F.);
#12888=ORIENTED_EDGE('',*,*,#8170,.F.);
#12889=ORIENTED_EDGE('',*,*,#8169,.F.);
#12890=ORIENTED_EDGE('',*,*,#8168,.F.);
#12891=ORIENTED_EDGE('',*,*,#8167,.F.);
#12892=ORIENTED_EDGE('',*,*,#8166,.F.);
#12893=ORIENTED_EDGE('',*,*,#8165,.F.);
#12894=ORIENTED_EDGE('',*,*,#8164,.F.);
#12895=ORIENTED_EDGE('',*,*,#8163,.F.);
#12896=ORIENTED_EDGE('',*,*,#8162,.F.);
#12897=ORIENTED_EDGE('',*,*,#8161,.F.);
#12898=ORIENTED_EDGE('',*,*,#8160,.F.);
#12899=ORIENTED_EDGE('',*,*,#8159,.F.);
#12900=ORIENTED_EDGE('',*,*,#8158,.F.);
#12901=ORIENTED_EDGE('',*,*,#8157,.F.);
#12902=ORIENTED_EDGE('',*,*,#8156,.F.);
#12903=ORIENTED_EDGE('',*,*,#8155,.F.);
#12904=ORIENTED_EDGE('',*,*,#8154,.F.);
#12905=ORIENTED_EDGE('',*,*,#8153,.F.);
#12906=ORIENTED_EDGE('',*,*,#8152,.F.);
#12907=ORIENTED_EDGE('',*,*,#8151,.F.);
#12908=ORIENTED_EDGE('',*,*,#8150,.F.);
#12909=ORIENTED_EDGE('',*,*,#8149,.F.);
#12910=ORIENTED_EDGE('',*,*,#8148,.F.);
#12911=ORIENTED_EDGE('',*,*,#8147,.F.);
#12912=ORIENTED_EDGE('',*,*,#8146,.F.);
#12913=ORIENTED_EDGE('',*,*,#8145,.F.);
#12914=ORIENTED_EDGE('',*,*,#8144,.F.);
#12915=ORIENTED_EDGE('',*,*,#8143,.F.);
#12916=ORIENTED_EDGE('',*,*,#8142,.F.);
#12917=ORIENTED_EDGE('',*,*,#8141,.F.);
#12918=ORIENTED_EDGE('',*,*,#8140,.F.);
#12919=ORIENTED_EDGE('',*,*,#8139,.F.);
#12920=ORIENTED_EDGE('',*,*,#8138,.F.);
#12921=ORIENTED_EDGE('',*,*,#8137,.F.);
#12922=ORIENTED_EDGE('',*,*,#8136,.F.);
#12923=ORIENTED_EDGE('',*,*,#8135,.F.);
#12924=ORIENTED_EDGE('',*,*,#8134,.F.);
#12925=ORIENTED_EDGE('',*,*,#8133,.F.);
#12926=ORIENTED_EDGE('',*,*,#8132,.F.);
#12927=ORIENTED_EDGE('',*,*,#8131,.F.);
#12928=ORIENTED_EDGE('',*,*,#8130,.F.);
#12929=ORIENTED_EDGE('',*,*,#8129,.F.);
#12930=ORIENTED_EDGE('',*,*,#8128,.F.);
#12931=ORIENTED_EDGE('',*,*,#8127,.F.);
#12932=ORIENTED_EDGE('',*,*,#8126,.F.);
#12933=ORIENTED_EDGE('',*,*,#8125,.F.);
#12934=ORIENTED_EDGE('',*,*,#8124,.F.);
#12935=ORIENTED_EDGE('',*,*,#8123,.F.);
#12936=ORIENTED_EDGE('',*,*,#8122,.F.);
#12937=ORIENTED_EDGE('',*,*,#8121,.F.);
#12938=ORIENTED_EDGE('',*,*,#8120,.F.);
#12939=ORIENTED_EDGE('',*,*,#8119,.F.);
#12940=ORIENTED_EDGE('',*,*,#8118,.F.);
#12941=ORIENTED_EDGE('',*,*,#8117,.F.);
#12942=ORIENTED_EDGE('',*,*,#8116,.F.);
#12943=ORIENTED_EDGE('',*,*,#8115,.F.);
#12944=ORIENTED_EDGE('',*,*,#8114,.F.);
#12945=ORIENTED_EDGE('',*,*,#8113,.F.);
#12946=ORIENTED_EDGE('',*,*,#8112,.F.);
#12947=ORIENTED_EDGE('',*,*,#8111,.F.);
#12948=ORIENTED_EDGE('',*,*,#8110,.F.);
#12949=ORIENTED_EDGE('',*,*,#8109,.F.);
#12950=ORIENTED_EDGE('',*,*,#8108,.F.);
#12951=ORIENTED_EDGE('',*,*,#8107,.F.);
#12952=ORIENTED_EDGE('',*,*,#8401,.T.);
#12953=ORIENTED_EDGE('',*,*,#8378,.T.);
#12954=ORIENTED_EDGE('',*,*,#8402,.T.);
#12955=ORIENTED_EDGE('',*,*,#8106,.T.);
#14106=CYLINDRICAL_SURFACE('',#15105,4.91825);
#14107=CYLINDRICAL_SURFACE('',#15107,4.91825);
#14108=CYLINDRICAL_SURFACE('',#15108,4.91825);
#14109=CYLINDRICAL_SURFACE('',#15109,4.91825);
#14110=CYLINDRICAL_SURFACE('',#15110,4.91825);
#14111=CYLINDRICAL_SURFACE('',#15111,4.91825);
#14112=CYLINDRICAL_SURFACE('',#15112,4.91825);
#14113=CYLINDRICAL_SURFACE('',#15113,4.91825);
#14114=CYLINDRICAL_SURFACE('',#15114,4.91825);
#14115=CYLINDRICAL_SURFACE('',#15115,4.91825);
#14116=CYLINDRICAL_SURFACE('',#15116,4.91825);
#14117=CYLINDRICAL_SURFACE('',#15117,4.91825);
#14118=CYLINDRICAL_SURFACE('',#15118,4.91825);
#14119=CYLINDRICAL_SURFACE('',#15119,4.91825);
#14120=CYLINDRICAL_SURFACE('',#15120,4.91825);
#14121=CYLINDRICAL_SURFACE('',#15121,4.91825);
#14122=CYLINDRICAL_SURFACE('',#15122,4.91825);
#14123=CYLINDRICAL_SURFACE('',#15123,4.91825);
#14124=CYLINDRICAL_SURFACE('',#15124,4.91825);
#14125=CYLINDRICAL_SURFACE('',#15125,4.91825);
#14126=CYLINDRICAL_SURFACE('',#15126,4.91825);
#14127=CYLINDRICAL_SURFACE('',#15127,4.91825);
#14128=CYLINDRICAL_SURFACE('',#15128,4.91825);
#14129=CYLINDRICAL_SURFACE('',#15129,4.91825);
#14130=CYLINDRICAL_SURFACE('',#15130,4.91825);
#14131=CYLINDRICAL_SURFACE('',#15131,4.91825);
#14132=CYLINDRICAL_SURFACE('',#15132,4.91825);
#14133=CYLINDRICAL_SURFACE('',#15133,4.91825);
#14134=CYLINDRICAL_SURFACE('',#15134,4.91825);
#14135=CYLINDRICAL_SURFACE('',#15135,4.91825);
#14136=CYLINDRICAL_SURFACE('',#15136,4.91825);
#14137=CYLINDRICAL_SURFACE('',#15137,4.91825);
#14138=CYLINDRICAL_SURFACE('',#15138,4.91825);
#14139=CYLINDRICAL_SURFACE('',#15139,4.91825);
#14140=CYLINDRICAL_SURFACE('',#15140,4.91825);
#14141=CYLINDRICAL_SURFACE('',#15141,4.91825);
#14142=CYLINDRICAL_SURFACE('',#15142,4.91825);
#14143=CYLINDRICAL_SURFACE('',#15143,4.91825);
#14144=CYLINDRICAL_SURFACE('',#15144,4.91825);
#14145=CYLINDRICAL_SURFACE('',#15145,4.91825);
#14146=CYLINDRICAL_SURFACE('',#15146,4.91825);
#14147=CYLINDRICAL_SURFACE('',#15147,4.91825);
#14148=CYLINDRICAL_SURFACE('',#15148,4.91825);
#14149=CYLINDRICAL_SURFACE('',#15149,4.91825);
#14150=CYLINDRICAL_SURFACE('',#15150,4.91825);
#14151=CYLINDRICAL_SURFACE('',#15151,4.91825);
#14152=CYLINDRICAL_SURFACE('',#15152,4.91825);
#14153=CYLINDRICAL_SURFACE('',#15153,4.91825);
#14154=CYLINDRICAL_SURFACE('',#15154,4.91825);
#14155=CYLINDRICAL_SURFACE('',#15155,4.91825);
#14156=CYLINDRICAL_SURFACE('',#15156,4.91825);
#14157=CYLINDRICAL_SURFACE('',#15157,4.91825);
#14158=CYLINDRICAL_SURFACE('',#15158,4.91825);
#14159=CYLINDRICAL_SURFACE('',#15159,4.91825);
#14160=CYLINDRICAL_SURFACE('',#15160,4.91825);
#14161=CYLINDRICAL_SURFACE('',#15161,4.91825);
#14162=CYLINDRICAL_SURFACE('',#15162,4.91825);
#14163=CYLINDRICAL_SURFACE('',#15163,4.91825);
#14164=CYLINDRICAL_SURFACE('',#15164,4.91825);
#14165=CYLINDRICAL_SURFACE('',#15165,4.91825);
#14166=CYLINDRICAL_SURFACE('',#15166,4.91825);
#14167=CYLINDRICAL_SURFACE('',#15167,4.91825);
#14168=CYLINDRICAL_SURFACE('',#15168,4.91825);
#14169=CYLINDRICAL_SURFACE('',#15169,4.91825);
#14170=CYLINDRICAL_SURFACE('',#15170,4.91825);
#14171=CYLINDRICAL_SURFACE('',#15171,4.91825);
#14172=CYLINDRICAL_SURFACE('',#15172,4.91825);
#14173=CYLINDRICAL_SURFACE('',#15173,4.91825);
#14174=CYLINDRICAL_SURFACE('',#15174,4.91825);
#14175=CYLINDRICAL_SURFACE('',#15175,4.91825);
#14176=CYLINDRICAL_SURFACE('',#15176,4.91825);
#14177=CYLINDRICAL_SURFACE('',#15177,4.91825);
#14178=CYLINDRICAL_SURFACE('',#15178,4.91825);
#14179=CYLINDRICAL_SURFACE('',#15179,4.91825);
#14180=CYLINDRICAL_SURFACE('',#15180,4.91825);
#14181=CYLINDRICAL_SURFACE('',#15181,4.91825);
#14182=CYLINDRICAL_SURFACE('',#15182,4.91825);
#14183=CYLINDRICAL_SURFACE('',#15183,4.91825);
#14184=CYLINDRICAL_SURFACE('',#15184,4.91825);
#14185=CYLINDRICAL_SURFACE('',#15185,4.91825);
#14186=CYLINDRICAL_SURFACE('',#15186,4.91825);
#14187=CYLINDRICAL_SURFACE('',#15187,4.91825);
#14188=CYLINDRICAL_SURFACE('',#15188,4.91825);
#14189=CYLINDRICAL_SURFACE('',#15189,4.91825);
#14190=CYLINDRICAL_SURFACE('',#15190,4.91825);
#14191=CYLINDRICAL_SURFACE('',#15191,4.91825);
#14192=CYLINDRICAL_SURFACE('',#15192,4.91825);
#14193=CYLINDRICAL_SURFACE('',#15193,4.91825);
#14194=CYLINDRICAL_SURFACE('',#15194,4.91825);
#14195=CYLINDRICAL_SURFACE('',#15195,4.91825);
#14196=CYLINDRICAL_SURFACE('',#15196,4.91825);
#14197=CYLINDRICAL_SURFACE('',#15197,4.91825);
#14198=CYLINDRICAL_SURFACE('',#15198,4.91825);
#14199=CYLINDRICAL_SURFACE('',#15199,4.91825);
#14200=CYLINDRICAL_SURFACE('',#15200,4.91825);
#14201=CYLINDRICAL_SURFACE('',#15201,4.91825);
#14202=CYLINDRICAL_SURFACE('',#15202,4.91825);
#14203=CYLINDRICAL_SURFACE('',#15203,4.91825);
#14204=CYLINDRICAL_SURFACE('',#15204,4.91825);
#14205=CYLINDRICAL_SURFACE('',#15205,4.91825);
#14206=CYLINDRICAL_SURFACE('',#15206,4.91825);
#14207=CYLINDRICAL_SURFACE('',#15207,4.91825);
#14208=CYLINDRICAL_SURFACE('',#15208,4.91825);
#14209=CYLINDRICAL_SURFACE('',#15209,4.91825);
#14210=CYLINDRICAL_SURFACE('',#15210,4.91825);
#14211=CYLINDRICAL_SURFACE('',#15211,4.91825);
#14212=CYLINDRICAL_SURFACE('',#15212,4.91825);
#14213=CYLINDRICAL_SURFACE('',#15213,4.91825);
#14214=CYLINDRICAL_SURFACE('',#15214,4.91825);
#14215=CYLINDRICAL_SURFACE('',#15215,4.91825);
#14216=CYLINDRICAL_SURFACE('',#15216,4.91825);
#14217=CYLINDRICAL_SURFACE('',#15217,4.91825);
#14218=CYLINDRICAL_SURFACE('',#15218,4.91825);
#14219=CYLINDRICAL_SURFACE('',#15219,4.91825);
#14220=CYLINDRICAL_SURFACE('',#15220,4.91825);
#14221=CYLINDRICAL_SURFACE('',#15221,4.91825);
#14222=CYLINDRICAL_SURFACE('',#15222,4.91825);
#14223=CYLINDRICAL_SURFACE('',#15223,4.91825);
#14224=CYLINDRICAL_SURFACE('',#15224,4.91825);
#14225=CYLINDRICAL_SURFACE('',#15225,4.91825);
#14226=CYLINDRICAL_SURFACE('',#15226,4.91825);
#14227=CYLINDRICAL_SURFACE('',#15227,4.91825);
#14228=CYLINDRICAL_SURFACE('',#15228,4.91825);
#14229=CYLINDRICAL_SURFACE('',#15229,4.91825);
#14230=CYLINDRICAL_SURFACE('',#15230,4.91825);
#14231=CYLINDRICAL_SURFACE('',#15231,4.91825);
#14232=CYLINDRICAL_SURFACE('',#15232,4.91825);
#14233=CYLINDRICAL_SURFACE('',#15233,4.91825);
#14234=CYLINDRICAL_SURFACE('',#15234,4.91825);
#14235=CYLINDRICAL_SURFACE('',#15235,4.91825);
#14236=CYLINDRICAL_SURFACE('',#15236,4.91825);
#14237=CYLINDRICAL_SURFACE('',#15237,4.91825);
#14238=CYLINDRICAL_SURFACE('',#15238,4.91825);
#14239=CYLINDRICAL_SURFACE('',#15239,4.91825);
#14240=CYLINDRICAL_SURFACE('',#15240,4.91825);
#14241=CYLINDRICAL_SURFACE('',#15241,4.91825);
#14242=CYLINDRICAL_SURFACE('',#15242,4.91825);
#14243=CYLINDRICAL_SURFACE('',#15243,4.91825);
#14244=CYLINDRICAL_SURFACE('',#15244,4.91825);
#14245=CYLINDRICAL_SURFACE('',#15245,4.91825);
#14246=CYLINDRICAL_SURFACE('',#15246,4.91825);
#14247=CYLINDRICAL_SURFACE('',#15247,4.91825);
#14248=CYLINDRICAL_SURFACE('',#15248,4.91825);
#14249=CYLINDRICAL_SURFACE('',#15249,4.91825);
#14250=CYLINDRICAL_SURFACE('',#15250,4.91825);
#14251=CYLINDRICAL_SURFACE('',#15251,4.91825);
#14252=CYLINDRICAL_SURFACE('',#15252,4.91825);
#14253=CYLINDRICAL_SURFACE('',#15253,4.91825);
#14254=CYLINDRICAL_SURFACE('',#15254,4.91825);
#14255=CYLINDRICAL_SURFACE('',#15255,4.91825);
#14256=CYLINDRICAL_SURFACE('',#15256,4.91825);
#14257=CYLINDRICAL_SURFACE('',#15257,4.91825);
#14258=CYLINDRICAL_SURFACE('',#15258,4.91825);
#14259=CYLINDRICAL_SURFACE('',#15259,4.91825);
#14260=CYLINDRICAL_SURFACE('',#15260,4.91825);
#14261=CYLINDRICAL_SURFACE('',#15261,4.91825);
#14262=CYLINDRICAL_SURFACE('',#15262,4.91825);
#14263=CYLINDRICAL_SURFACE('',#15263,4.91825);
#14264=CYLINDRICAL_SURFACE('',#15264,4.91825);
#14265=CYLINDRICAL_SURFACE('',#15265,4.91825);
#14266=CYLINDRICAL_SURFACE('',#15266,4.91825);
#14267=CYLINDRICAL_SURFACE('',#15267,4.91825);
#14268=CYLINDRICAL_SURFACE('',#15268,4.91825);
#14269=CYLINDRICAL_SURFACE('',#15269,4.91825);
#14270=CYLINDRICAL_SURFACE('',#15270,4.91825);
#14271=CYLINDRICAL_SURFACE('',#15271,4.91825);
#14272=CYLINDRICAL_SURFACE('',#15272,4.91825);
#14273=CYLINDRICAL_SURFACE('',#15273,4.91825);
#14274=CYLINDRICAL_SURFACE('',#15274,4.91825);
#14275=CYLINDRICAL_SURFACE('',#15275,4.91825);
#14276=CYLINDRICAL_SURFACE('',#15276,4.91825);
#14277=CYLINDRICAL_SURFACE('',#15277,4.91825);
#14278=CYLINDRICAL_SURFACE('',#15278,4.91825);
#14279=CYLINDRICAL_SURFACE('',#15279,4.91825);
#14280=CYLINDRICAL_SURFACE('',#15280,4.91825);
#14281=CYLINDRICAL_SURFACE('',#15281,4.91825);
#14282=CYLINDRICAL_SURFACE('',#15282,4.91825);
#14283=CYLINDRICAL_SURFACE('',#15283,4.91825);
#14284=CYLINDRICAL_SURFACE('',#15284,4.91825);
#14285=CYLINDRICAL_SURFACE('',#15285,4.91825);
#14286=CYLINDRICAL_SURFACE('',#15286,4.91825);
#14287=CYLINDRICAL_SURFACE('',#15287,4.91825);
#14288=CYLINDRICAL_SURFACE('',#15288,4.91825);
#14289=CYLINDRICAL_SURFACE('',#15289,4.91825);
#14290=CYLINDRICAL_SURFACE('',#15290,4.91825);
#14291=CYLINDRICAL_SURFACE('',#15291,4.91825);
#14292=CYLINDRICAL_SURFACE('',#15292,4.91825);
#14293=CYLINDRICAL_SURFACE('',#15293,4.91825);
#14294=CYLINDRICAL_SURFACE('',#15294,4.91825);
#14295=CYLINDRICAL_SURFACE('',#15295,4.91825);
#14296=CYLINDRICAL_SURFACE('',#15296,4.91825);
#14297=CYLINDRICAL_SURFACE('',#15297,4.91825);
#14298=CYLINDRICAL_SURFACE('',#15298,4.91825);
#14299=CYLINDRICAL_SURFACE('',#15299,4.91825);
#14300=CYLINDRICAL_SURFACE('',#15300,4.91825);
#14301=CYLINDRICAL_SURFACE('',#15301,4.91825);
#14302=CYLINDRICAL_SURFACE('',#15302,4.91825);
#14303=CYLINDRICAL_SURFACE('',#15303,4.91825);
#14304=CYLINDRICAL_SURFACE('',#15304,4.91825);
#14305=CYLINDRICAL_SURFACE('',#15305,4.91825);
#14306=CYLINDRICAL_SURFACE('',#15306,4.91825);
#14307=CYLINDRICAL_SURFACE('',#15307,4.91825);
#14308=CYLINDRICAL_SURFACE('',#15308,4.91825);
#14309=CYLINDRICAL_SURFACE('',#15309,4.91825);
#14310=CYLINDRICAL_SURFACE('',#15310,4.91825);
#14311=CYLINDRICAL_SURFACE('',#15311,4.91825);
#14312=CYLINDRICAL_SURFACE('',#15312,4.91825);
#14313=CYLINDRICAL_SURFACE('',#15313,4.91825);
#14314=CYLINDRICAL_SURFACE('',#15314,4.91825);
#14315=CYLINDRICAL_SURFACE('',#15315,4.91825);
#14316=CYLINDRICAL_SURFACE('',#15316,4.91825);
#14317=CYLINDRICAL_SURFACE('',#15317,4.91825);
#14318=CYLINDRICAL_SURFACE('',#15318,4.91825);
#14319=CYLINDRICAL_SURFACE('',#15319,4.91825);
#14320=CYLINDRICAL_SURFACE('',#15320,4.91825);
#14321=CYLINDRICAL_SURFACE('',#15321,4.91825);
#14322=CYLINDRICAL_SURFACE('',#15322,4.91825);
#14323=CYLINDRICAL_SURFACE('',#15323,4.91825);
#14324=CYLINDRICAL_SURFACE('',#15324,4.91825);
#14325=CYLINDRICAL_SURFACE('',#15325,4.91825);
#14326=CYLINDRICAL_SURFACE('',#15326,4.91825);
#14327=CYLINDRICAL_SURFACE('',#15327,4.91825);
#14328=CYLINDRICAL_SURFACE('',#15328,4.91825);
#14329=CYLINDRICAL_SURFACE('',#15329,4.91825);
#14330=CYLINDRICAL_SURFACE('',#15330,4.91825);
#14331=CYLINDRICAL_SURFACE('',#15331,4.91825);
#14332=CYLINDRICAL_SURFACE('',#15332,4.91825);
#14333=CYLINDRICAL_SURFACE('',#15333,4.91825);
#14334=CYLINDRICAL_SURFACE('',#15334,4.91825);
#14335=CYLINDRICAL_SURFACE('',#15335,4.91825);
#14336=CYLINDRICAL_SURFACE('',#15336,4.91825);
#14337=CYLINDRICAL_SURFACE('',#15337,4.91825);
#14338=CYLINDRICAL_SURFACE('',#15338,4.91825);
#14339=CYLINDRICAL_SURFACE('',#15339,4.91825);
#14340=CYLINDRICAL_SURFACE('',#15340,4.91825);
#14341=CYLINDRICAL_SURFACE('',#15341,4.91825);
#14342=CYLINDRICAL_SURFACE('',#15342,4.91825);
#14343=CYLINDRICAL_SURFACE('',#15343,4.91825);
#14344=CYLINDRICAL_SURFACE('',#15344,4.91825);
#14345=CYLINDRICAL_SURFACE('',#15345,4.91825);
#14346=CYLINDRICAL_SURFACE('',#15346,4.91825);
#14347=CYLINDRICAL_SURFACE('',#15347,4.91825);
#14348=CYLINDRICAL_SURFACE('',#15348,4.91825);
#14349=CYLINDRICAL_SURFACE('',#15349,4.91825);
#14350=CYLINDRICAL_SURFACE('',#15350,4.91825);
#14351=CYLINDRICAL_SURFACE('',#15351,4.91825);
#14352=CYLINDRICAL_SURFACE('',#15352,4.91825);
#14353=CYLINDRICAL_SURFACE('',#15353,4.91825);
#14354=CYLINDRICAL_SURFACE('',#15354,4.91825);
#14355=CYLINDRICAL_SURFACE('',#15355,4.91825);
#14356=CYLINDRICAL_SURFACE('',#15356,4.91825);
#14357=CYLINDRICAL_SURFACE('',#15357,4.91825);
#14358=CYLINDRICAL_SURFACE('',#15358,4.91825);
#14359=CYLINDRICAL_SURFACE('',#15359,4.91825);
#14360=CYLINDRICAL_SURFACE('',#15360,4.91825);
#14361=CYLINDRICAL_SURFACE('',#15361,4.91825);
#14362=CYLINDRICAL_SURFACE('',#15362,4.91825);
#14363=CYLINDRICAL_SURFACE('',#15363,4.91825);
#14364=CYLINDRICAL_SURFACE('',#15364,4.91825);
#14365=CYLINDRICAL_SURFACE('',#15365,4.91825);
#14366=CYLINDRICAL_SURFACE('',#15366,4.91825);
#14367=CYLINDRICAL_SURFACE('',#15367,4.91825);
#14368=CYLINDRICAL_SURFACE('',#15368,4.91825);
#14369=CYLINDRICAL_SURFACE('',#15369,4.91825);
#14370=CYLINDRICAL_SURFACE('',#15370,4.91825);
#14371=CYLINDRICAL_SURFACE('',#15371,4.91825);
#14372=CYLINDRICAL_SURFACE('',#15372,4.91825);
#14373=CYLINDRICAL_SURFACE('',#15373,4.91825);
#14374=CYLINDRICAL_SURFACE('',#15374,5.91675);
#14375=CYLINDRICAL_SURFACE('',#15377,4.91825);
#14376=CYLINDRICAL_SURFACE('',#15382,9.);
#14377=CYLINDRICAL_SURFACE('',#15392,7.);
#14499=ADVANCED_FACE('',(#2141),#14106,.T.);
#14500=ADVANCED_FACE('',(#2142),#14107,.T.);
#14501=ADVANCED_FACE('',(#2143),#14108,.T.);
#14502=ADVANCED_FACE('',(#2144),#14109,.T.);
#14503=ADVANCED_FACE('',(#2145),#14110,.T.);
#14504=ADVANCED_FACE('',(#2146),#14111,.T.);
#14505=ADVANCED_FACE('',(#2147),#14112,.T.);
#14506=ADVANCED_FACE('',(#2148),#14113,.T.);
#14507=ADVANCED_FACE('',(#2149),#14114,.T.);
#14508=ADVANCED_FACE('',(#2150),#14115,.T.);
#14509=ADVANCED_FACE('',(#2151),#14116,.T.);
#14510=ADVANCED_FACE('',(#2152),#14117,.T.);
#14511=ADVANCED_FACE('',(#2153),#14118,.T.);
#14512=ADVANCED_FACE('',(#2154),#14119,.T.);
#14513=ADVANCED_FACE('',(#2155),#14120,.T.);
#14514=ADVANCED_FACE('',(#2156),#14121,.T.);
#14515=ADVANCED_FACE('',(#2157),#14122,.T.);
#14516=ADVANCED_FACE('',(#2158),#14123,.T.);
#14517=ADVANCED_FACE('',(#2159),#14124,.T.);
#14518=ADVANCED_FACE('',(#2160),#14125,.T.);
#14519=ADVANCED_FACE('',(#2161),#14126,.T.);
#14520=ADVANCED_FACE('',(#2162),#14127,.T.);
#14521=ADVANCED_FACE('',(#2163),#14128,.T.);
#14522=ADVANCED_FACE('',(#2164),#14129,.T.);
#14523=ADVANCED_FACE('',(#2165),#14130,.T.);
#14524=ADVANCED_FACE('',(#2166),#14131,.T.);
#14525=ADVANCED_FACE('',(#2167),#14132,.T.);
#14526=ADVANCED_FACE('',(#2168),#14133,.T.);
#14527=ADVANCED_FACE('',(#2169),#14134,.T.);
#14528=ADVANCED_FACE('',(#2170),#14135,.T.);
#14529=ADVANCED_FACE('',(#2171),#14136,.T.);
#14530=ADVANCED_FACE('',(#2172),#14137,.T.);
#14531=ADVANCED_FACE('',(#2173),#14138,.T.);
#14532=ADVANCED_FACE('',(#2174),#14139,.T.);
#14533=ADVANCED_FACE('',(#2175),#14140,.T.);
#14534=ADVANCED_FACE('',(#2176),#14141,.T.);
#14535=ADVANCED_FACE('',(#2177),#14142,.T.);
#14536=ADVANCED_FACE('',(#2178),#14143,.T.);
#14537=ADVANCED_FACE('',(#2179),#14144,.T.);
#14538=ADVANCED_FACE('',(#2180),#14145,.T.);
#14539=ADVANCED_FACE('',(#2181),#14146,.T.);
#14540=ADVANCED_FACE('',(#2182),#14147,.T.);
#14541=ADVANCED_FACE('',(#2183),#14148,.T.);
#14542=ADVANCED_FACE('',(#2184),#14149,.T.);
#14543=ADVANCED_FACE('',(#2185),#14150,.T.);
#14544=ADVANCED_FACE('',(#2186),#14151,.T.);
#14545=ADVANCED_FACE('',(#2187),#14152,.T.);
#14546=ADVANCED_FACE('',(#2188),#14153,.T.);
#14547=ADVANCED_FACE('',(#2189),#14154,.T.);
#14548=ADVANCED_FACE('',(#2190),#14155,.T.);
#14549=ADVANCED_FACE('',(#2191),#14156,.T.);
#14550=ADVANCED_FACE('',(#2192),#14157,.T.);
#14551=ADVANCED_FACE('',(#2193),#14158,.T.);
#14552=ADVANCED_FACE('',(#2194),#14159,.T.);
#14553=ADVANCED_FACE('',(#2195),#14160,.T.);
#14554=ADVANCED_FACE('',(#2196),#14161,.T.);
#14555=ADVANCED_FACE('',(#2197),#14162,.T.);
#14556=ADVANCED_FACE('',(#2198),#14163,.T.);
#14557=ADVANCED_FACE('',(#2199),#14164,.T.);
#14558=ADVANCED_FACE('',(#2200),#14165,.T.);
#14559=ADVANCED_FACE('',(#2201),#14166,.T.);
#14560=ADVANCED_FACE('',(#2202),#14167,.T.);
#14561=ADVANCED_FACE('',(#2203),#14168,.T.);
#14562=ADVANCED_FACE('',(#2204),#14169,.T.);
#14563=ADVANCED_FACE('',(#2205),#14170,.T.);
#14564=ADVANCED_FACE('',(#2206),#14171,.T.);
#14565=ADVANCED_FACE('',(#2207),#14172,.T.);
#14566=ADVANCED_FACE('',(#2208),#14173,.T.);
#14567=ADVANCED_FACE('',(#2209),#14174,.T.);
#14568=ADVANCED_FACE('',(#2210),#14175,.T.);
#14569=ADVANCED_FACE('',(#2211),#14176,.T.);
#14570=ADVANCED_FACE('',(#2212),#14177,.T.);
#14571=ADVANCED_FACE('',(#2213),#14178,.T.);
#14572=ADVANCED_FACE('',(#2214),#14179,.T.);
#14573=ADVANCED_FACE('',(#2215),#14180,.T.);
#14574=ADVANCED_FACE('',(#2216),#14181,.T.);
#14575=ADVANCED_FACE('',(#2217),#14182,.T.);
#14576=ADVANCED_FACE('',(#2218),#14183,.T.);
#14577=ADVANCED_FACE('',(#2219),#14184,.T.);
#14578=ADVANCED_FACE('',(#2220),#14185,.T.);
#14579=ADVANCED_FACE('',(#2221),#14186,.T.);
#14580=ADVANCED_FACE('',(#2222),#14187,.T.);
#14581=ADVANCED_FACE('',(#2223),#14188,.T.);
#14582=ADVANCED_FACE('',(#2224),#14189,.T.);
#14583=ADVANCED_FACE('',(#2225),#14190,.T.);
#14584=ADVANCED_FACE('',(#2226),#14191,.T.);
#14585=ADVANCED_FACE('',(#2227),#14192,.T.);
#14586=ADVANCED_FACE('',(#2228),#14193,.T.);
#14587=ADVANCED_FACE('',(#2229),#14194,.T.);
#14588=ADVANCED_FACE('',(#2230),#14195,.T.);
#14589=ADVANCED_FACE('',(#2231),#14196,.T.);
#14590=ADVANCED_FACE('',(#2232),#14197,.T.);
#14591=ADVANCED_FACE('',(#2233),#14198,.T.);
#14592=ADVANCED_FACE('',(#2234),#14199,.T.);
#14593=ADVANCED_FACE('',(#2235),#14200,.T.);
#14594=ADVANCED_FACE('',(#2236),#14201,.T.);
#14595=ADVANCED_FACE('',(#2237),#14202,.T.);
#14596=ADVANCED_FACE('',(#2238),#14203,.T.);
#14597=ADVANCED_FACE('',(#2239),#14204,.T.);
#14598=ADVANCED_FACE('',(#2240),#14205,.T.);
#14599=ADVANCED_FACE('',(#2241),#14206,.T.);
#14600=ADVANCED_FACE('',(#2242),#14207,.T.);
#14601=ADVANCED_FACE('',(#2243),#14208,.T.);
#14602=ADVANCED_FACE('',(#2244),#14209,.T.);
#14603=ADVANCED_FACE('',(#2245),#14210,.T.);
#14604=ADVANCED_FACE('',(#2246),#14211,.T.);
#14605=ADVANCED_FACE('',(#2247),#14212,.T.);
#14606=ADVANCED_FACE('',(#2248),#14213,.T.);
#14607=ADVANCED_FACE('',(#2249),#14214,.T.);
#14608=ADVANCED_FACE('',(#2250),#14215,.T.);
#14609=ADVANCED_FACE('',(#2251),#14216,.T.);
#14610=ADVANCED_FACE('',(#2252),#14217,.T.);
#14611=ADVANCED_FACE('',(#2253),#14218,.T.);
#14612=ADVANCED_FACE('',(#2254),#14219,.T.);
#14613=ADVANCED_FACE('',(#2255),#14220,.T.);
#14614=ADVANCED_FACE('',(#2256),#14221,.T.);
#14615=ADVANCED_FACE('',(#2257),#14222,.T.);
#14616=ADVANCED_FACE('',(#2258),#14223,.T.);
#14617=ADVANCED_FACE('',(#2259),#14224,.T.);
#14618=ADVANCED_FACE('',(#2260),#14225,.T.);
#14619=ADVANCED_FACE('',(#2261),#14226,.T.);
#14620=ADVANCED_FACE('',(#2262),#14227,.T.);
#14621=ADVANCED_FACE('',(#2263),#14228,.T.);
#14622=ADVANCED_FACE('',(#2264),#14229,.T.);
#14623=ADVANCED_FACE('',(#2265),#14230,.T.);
#14624=ADVANCED_FACE('',(#2266),#14231,.T.);
#14625=ADVANCED_FACE('',(#2267),#14232,.T.);
#14626=ADVANCED_FACE('',(#2268),#14233,.T.);
#14627=ADVANCED_FACE('',(#2269),#14234,.T.);
#14628=ADVANCED_FACE('',(#2270),#14235,.T.);
#14629=ADVANCED_FACE('',(#2271),#14236,.T.);
#14630=ADVANCED_FACE('',(#2272),#14237,.T.);
#14631=ADVANCED_FACE('',(#2273),#14238,.T.);
#14632=ADVANCED_FACE('',(#2274),#14239,.T.);
#14633=ADVANCED_FACE('',(#2275),#14240,.T.);
#14634=ADVANCED_FACE('',(#2276),#14241,.T.);
#14635=ADVANCED_FACE('',(#2277),#14242,.T.);
#14636=ADVANCED_FACE('',(#2278),#14243,.T.);
#14637=ADVANCED_FACE('',(#2279),#14244,.T.);
#14638=ADVANCED_FACE('',(#2280),#14245,.T.);
#14639=ADVANCED_FACE('',(#2281),#14246,.T.);
#14640=ADVANCED_FACE('',(#2282),#14247,.T.);
#14641=ADVANCED_FACE('',(#2283),#14248,.T.);
#14642=ADVANCED_FACE('',(#2284),#14249,.T.);
#14643=ADVANCED_FACE('',(#2285),#14250,.T.);
#14644=ADVANCED_FACE('',(#2286),#14251,.T.);
#14645=ADVANCED_FACE('',(#2287),#14252,.T.);
#14646=ADVANCED_FACE('',(#2288),#14253,.T.);
#14647=ADVANCED_FACE('',(#2289),#14254,.T.);
#14648=ADVANCED_FACE('',(#2290),#14255,.T.);
#14649=ADVANCED_FACE('',(#2291),#14256,.T.);
#14650=ADVANCED_FACE('',(#2292),#14257,.T.);
#14651=ADVANCED_FACE('',(#2293),#14258,.T.);
#14652=ADVANCED_FACE('',(#2294),#14259,.T.);
#14653=ADVANCED_FACE('',(#2295),#14260,.T.);
#14654=ADVANCED_FACE('',(#2296),#14261,.T.);
#14655=ADVANCED_FACE('',(#2297),#14262,.T.);
#14656=ADVANCED_FACE('',(#2298),#14263,.T.);
#14657=ADVANCED_FACE('',(#2299),#14264,.T.);
#14658=ADVANCED_FACE('',(#2300),#14265,.T.);
#14659=ADVANCED_FACE('',(#2301),#14266,.T.);
#14660=ADVANCED_FACE('',(#2302),#14267,.T.);
#14661=ADVANCED_FACE('',(#2303),#14268,.T.);
#14662=ADVANCED_FACE('',(#2304),#14269,.T.);
#14663=ADVANCED_FACE('',(#2305),#14270,.T.);
#14664=ADVANCED_FACE('',(#2306),#14271,.T.);
#14665=ADVANCED_FACE('',(#2307),#14272,.T.);
#14666=ADVANCED_FACE('',(#2308),#14273,.T.);
#14667=ADVANCED_FACE('',(#2309),#14274,.T.);
#14668=ADVANCED_FACE('',(#2310),#14275,.T.);
#14669=ADVANCED_FACE('',(#2311),#14276,.T.);
#14670=ADVANCED_FACE('',(#2312),#14277,.T.);
#14671=ADVANCED_FACE('',(#2313),#14278,.T.);
#14672=ADVANCED_FACE('',(#2314),#14279,.T.);
#14673=ADVANCED_FACE('',(#2315),#14280,.T.);
#14674=ADVANCED_FACE('',(#2316),#14281,.T.);
#14675=ADVANCED_FACE('',(#2317),#14282,.T.);
#14676=ADVANCED_FACE('',(#2318),#14283,.T.);
#14677=ADVANCED_FACE('',(#2319),#14284,.T.);
#14678=ADVANCED_FACE('',(#2320),#14285,.T.);
#14679=ADVANCED_FACE('',(#2321),#14286,.T.);
#14680=ADVANCED_FACE('',(#2322),#14287,.T.);
#14681=ADVANCED_FACE('',(#2323),#14288,.T.);
#14682=ADVANCED_FACE('',(#2324),#14289,.T.);
#14683=ADVANCED_FACE('',(#2325),#14290,.T.);
#14684=ADVANCED_FACE('',(#2326),#14291,.T.);
#14685=ADVANCED_FACE('',(#2327),#14292,.T.);
#14686=ADVANCED_FACE('',(#2328),#14293,.T.);
#14687=ADVANCED_FACE('',(#2329),#14294,.T.);
#14688=ADVANCED_FACE('',(#2330),#14295,.T.);
#14689=ADVANCED_FACE('',(#2331),#14296,.T.);
#14690=ADVANCED_FACE('',(#2332),#14297,.T.);
#14691=ADVANCED_FACE('',(#2333),#14298,.T.);
#14692=ADVANCED_FACE('',(#2334),#14299,.T.);
#14693=ADVANCED_FACE('',(#2335),#14300,.T.);
#14694=ADVANCED_FACE('',(#2336),#14301,.T.);
#14695=ADVANCED_FACE('',(#2337),#14302,.T.);
#14696=ADVANCED_FACE('',(#2338),#14303,.T.);
#14697=ADVANCED_FACE('',(#2339),#14304,.T.);
#14698=ADVANCED_FACE('',(#2340),#14305,.T.);
#14699=ADVANCED_FACE('',(#2341),#14306,.T.);
#14700=ADVANCED_FACE('',(#2342),#14307,.T.);
#14701=ADVANCED_FACE('',(#2343),#14308,.T.);
#14702=ADVANCED_FACE('',(#2344),#14309,.T.);
#14703=ADVANCED_FACE('',(#2345),#14310,.T.);
#14704=ADVANCED_FACE('',(#2346),#14311,.T.);
#14705=ADVANCED_FACE('',(#2347),#14312,.T.);
#14706=ADVANCED_FACE('',(#2348),#14313,.T.);
#14707=ADVANCED_FACE('',(#2349),#14314,.T.);
#14708=ADVANCED_FACE('',(#2350),#14315,.T.);
#14709=ADVANCED_FACE('',(#2351),#14316,.T.);
#14710=ADVANCED_FACE('',(#2352),#14317,.T.);
#14711=ADVANCED_FACE('',(#2353),#14318,.T.);
#14712=ADVANCED_FACE('',(#2354),#14319,.T.);
#14713=ADVANCED_FACE('',(#2355),#14320,.T.);
#14714=ADVANCED_FACE('',(#2356),#14321,.T.);
#14715=ADVANCED_FACE('',(#2357),#14322,.T.);
#14716=ADVANCED_FACE('',(#2358),#14323,.T.);
#14717=ADVANCED_FACE('',(#2359),#14324,.T.);
#14718=ADVANCED_FACE('',(#2360),#14325,.T.);
#14719=ADVANCED_FACE('',(#2361),#14326,.T.);
#14720=ADVANCED_FACE('',(#2362),#14327,.T.);
#14721=ADVANCED_FACE('',(#2363),#14328,.T.);
#14722=ADVANCED_FACE('',(#2364),#14329,.T.);
#14723=ADVANCED_FACE('',(#2365),#14330,.T.);
#14724=ADVANCED_FACE('',(#2366),#14331,.T.);
#14725=ADVANCED_FACE('',(#2367),#14332,.T.);
#14726=ADVANCED_FACE('',(#2368),#14333,.T.);
#14727=ADVANCED_FACE('',(#2369),#14334,.T.);
#14728=ADVANCED_FACE('',(#2370),#14335,.T.);
#14729=ADVANCED_FACE('',(#2371),#14336,.T.);
#14730=ADVANCED_FACE('',(#2372),#14337,.T.);
#14731=ADVANCED_FACE('',(#2373),#14338,.T.);
#14732=ADVANCED_FACE('',(#2374),#14339,.T.);
#14733=ADVANCED_FACE('',(#2375),#14340,.T.);
#14734=ADVANCED_FACE('',(#2376),#14341,.T.);
#14735=ADVANCED_FACE('',(#2377),#14342,.T.);
#14736=ADVANCED_FACE('',(#2378),#14343,.T.);
#14737=ADVANCED_FACE('',(#2379),#14344,.T.);
#14738=ADVANCED_FACE('',(#2380),#14345,.T.);
#14739=ADVANCED_FACE('',(#2381),#14346,.T.);
#14740=ADVANCED_FACE('',(#2382),#14347,.T.);
#14741=ADVANCED_FACE('',(#2383),#14348,.T.);
#14742=ADVANCED_FACE('',(#2384),#14349,.T.);
#14743=ADVANCED_FACE('',(#2385),#14350,.T.);
#14744=ADVANCED_FACE('',(#2386),#14351,.T.);
#14745=ADVANCED_FACE('',(#2387),#14352,.T.);
#14746=ADVANCED_FACE('',(#2388),#14353,.T.);
#14747=ADVANCED_FACE('',(#2389),#14354,.T.);
#14748=ADVANCED_FACE('',(#2390),#14355,.T.);
#14749=ADVANCED_FACE('',(#2391),#14356,.T.);
#14750=ADVANCED_FACE('',(#2392),#14357,.T.);
#14751=ADVANCED_FACE('',(#2393),#14358,.T.);
#14752=ADVANCED_FACE('',(#2394),#14359,.T.);
#14753=ADVANCED_FACE('',(#2395),#14360,.T.);
#14754=ADVANCED_FACE('',(#2396),#14361,.T.);
#14755=ADVANCED_FACE('',(#2397),#14362,.T.);
#14756=ADVANCED_FACE('',(#2398),#14363,.T.);
#14757=ADVANCED_FACE('',(#2399),#14364,.T.);
#14758=ADVANCED_FACE('',(#2400),#14365,.T.);
#14759=ADVANCED_FACE('',(#2401),#14366,.T.);
#14760=ADVANCED_FACE('',(#2402),#14367,.T.);
#14761=ADVANCED_FACE('',(#2403),#14368,.T.);
#14762=ADVANCED_FACE('',(#2404),#14369,.T.);
#14763=ADVANCED_FACE('',(#2405),#14370,.T.);
#14764=ADVANCED_FACE('',(#2406),#14371,.T.);
#14765=ADVANCED_FACE('',(#2407),#14372,.T.);
#14766=ADVANCED_FACE('',(#2408),#14373,.T.);
#14767=ADVANCED_FACE('',(#2409),#14374,.T.);
#14768=ADVANCED_FACE('',(#2410),#14375,.T.);
#14769=ADVANCED_FACE('',(#2411,#1987),#2043,.T.);
#14770=ADVANCED_FACE('',(#2412),#14376,.T.);
#14771=ADVANCED_FACE('',(#2413,#1988),#2044,.F.);
#14772=ADVANCED_FACE('',(#2414),#2045,.F.);
#14773=ADVANCED_FACE('',(#2415),#2046,.T.);
#14774=ADVANCED_FACE('',(#2416),#2047,.F.);
#14775=ADVANCED_FACE('',(#2417),#2048,.T.);
#14776=ADVANCED_FACE('',(#2418),#14377,.T.);
#14777=ADVANCED_FACE('',(#2419),#2049,.T.);
#14778=ADVANCED_FACE('',(#2420),#47,.F.);
#14779=ADVANCED_FACE('',(#2421),#48,.F.);
#14780=ADVANCED_FACE('',(#2422),#2050,.F.);
#14939=CLOSED_SHELL('',(#14499,#14500,#14501,#14502,#14503,#14504,#14505,
#14506,#14507,#14508,#14509,#14510,#14511,#14512,#14513,#14514,#14515,#14516,
#14517,#14518,#14519,#14520,#14521,#14522,#14523,#14524,#14525,#14526,#14527,
#14528,#14529,#14530,#14531,#14532,#14533,#14534,#14535,#14536,#14537,#14538,
#14539,#14540,#14541,#14542,#14543,#14544,#14545,#14546,#14547,#14548,#14549,
#14550,#14551,#14552,#14553,#14554,#14555,#14556,#14557,#14558,#14559,#14560,
#14561,#14562,#14563,#14564,#14565,#14566,#14567,#14568,#14569,#14570,#14571,
#14572,#14573,#14574,#14575,#14576,#14577,#14578,#14579,#14580,#14581,#14582,
#14583,#14584,#14585,#14586,#14587,#14588,#14589,#14590,#14591,#14592,#14593,
#14594,#14595,#14596,#14597,#14598,#14599,#14600,#14601,#14602,#14603,#14604,
#14605,#14606,#14607,#14608,#14609,#14610,#14611,#14612,#14613,#14614,#14615,
#14616,#14617,#14618,#14619,#14620,#14621,#14622,#14623,#14624,#14625,#14626,
#14627,#14628,#14629,#14630,#14631,#14632,#14633,#14634,#14635,#14636,#14637,
#14638,#14639,#14640,#14641,#14642,#14643,#14644,#14645,#14646,#14647,#14648,
#14649,#14650,#14651,#14652,#14653,#14654,#14655,#14656,#14657,#14658,#14659,
#14660,#14661,#14662,#14663,#14664,#14665,#14666,#14667,#14668,#14669,#14670,
#14671,#14672,#14673,#14674,#14675,#14676,#14677,#14678,#14679,#14680,#14681,
#14682,#14683,#14684,#14685,#14686,#14687,#14688,#14689,#14690,#14691,#14692,
#14693,#14694,#14695,#14696,#14697,#14698,#14699,#14700,#14701,#14702,#14703,
#14704,#14705,#14706,#14707,#14708,#14709,#14710,#14711,#14712,#14713,#14714,
#14715,#14716,#14717,#14718,#14719,#14720,#14721,#14722,#14723,#14724,#14725,
#14726,#14727,#14728,#14729,#14730,#14731,#14732,#14733,#14734,#14735,#14736,
#14737,#14738,#14739,#14740,#14741,#14742,#14743,#14744,#14745,#14746,#14747,
#14748,#14749,#14750,#14751,#14752,#14753,#14754,#14755,#14756,#14757,#14758,
#14759,#14760,#14761,#14762,#14763,#14764,#14765,#14766,#14767,#14768,#14769,
#14770,#14771,#14772,#14773,#14774,#14775,#14776,#14777,#14778,#14779,#14780));
#15104=AXIS2_PLACEMENT_3D('',#17629,#15848,#15849);
#15105=AXIS2_PLACEMENT_3D('',#17630,#15850,#15851);
#15106=AXIS2_PLACEMENT_3D('',#17823,#15853,#15854);
#15107=AXIS2_PLACEMENT_3D('',#17960,#15855,#15856);
#15108=AXIS2_PLACEMENT_3D('',#18426,#15858,#15859);
#15109=AXIS2_PLACEMENT_3D('',#18892,#15861,#15862);
#15110=AXIS2_PLACEMENT_3D('',#19361,#15864,#15865);
#15111=AXIS2_PLACEMENT_3D('',#19827,#15867,#15868);
#15112=AXIS2_PLACEMENT_3D('',#20293,#15870,#15871);
#15113=AXIS2_PLACEMENT_3D('',#20759,#15873,#15874);
#15114=AXIS2_PLACEMENT_3D('',#21222,#15876,#15877);
#15115=AXIS2_PLACEMENT_3D('',#21688,#15879,#15880);
#15116=AXIS2_PLACEMENT_3D('',#21944,#15882,#15883);
#15117=AXIS2_PLACEMENT_3D('',#22197,#15885,#15886);
#15118=AXIS2_PLACEMENT_3D('',#22657,#15888,#15889);
#15119=AXIS2_PLACEMENT_3D('',#23123,#15891,#15892);
#15120=AXIS2_PLACEMENT_3D('',#23589,#15894,#15895);
#15121=AXIS2_PLACEMENT_3D('',#24052,#15897,#15898);
#15122=AXIS2_PLACEMENT_3D('',#24518,#15900,#15901);
#15123=AXIS2_PLACEMENT_3D('',#24984,#15903,#15904);
#15124=AXIS2_PLACEMENT_3D('',#25450,#15906,#15907);
#15125=AXIS2_PLACEMENT_3D('',#25919,#15909,#15910);
#15126=AXIS2_PLACEMENT_3D('',#26385,#15912,#15913);
#15127=AXIS2_PLACEMENT_3D('',#26851,#15915,#15916);
#15128=AXIS2_PLACEMENT_3D('',#27314,#15918,#15919);
#15129=AXIS2_PLACEMENT_3D('',#27786,#15921,#15922);
#15130=AXIS2_PLACEMENT_3D('',#28252,#15924,#15925);
#15131=AXIS2_PLACEMENT_3D('',#28718,#15927,#15928);
#15132=AXIS2_PLACEMENT_3D('',#29190,#15930,#15931);
#15133=AXIS2_PLACEMENT_3D('',#29656,#15933,#15934);
#15134=AXIS2_PLACEMENT_3D('',#30119,#15936,#15937);
#15135=AXIS2_PLACEMENT_3D('',#30582,#15939,#15940);
#15136=AXIS2_PLACEMENT_3D('',#31054,#15942,#15943);
#15137=AXIS2_PLACEMENT_3D('',#31520,#15945,#15946);
#15138=AXIS2_PLACEMENT_3D('',#31983,#15948,#15949);
#15139=AXIS2_PLACEMENT_3D('',#32452,#15951,#15952);
#15140=AXIS2_PLACEMENT_3D('',#32918,#15954,#15955);
#15141=AXIS2_PLACEMENT_3D('',#33381,#15957,#15958);
#15142=AXIS2_PLACEMENT_3D('',#33844,#15960,#15961);
#15143=AXIS2_PLACEMENT_3D('',#34313,#15963,#15964);
#15144=AXIS2_PLACEMENT_3D('',#34779,#15966,#15967);
#15145=AXIS2_PLACEMENT_3D('',#35242,#15969,#15970);
#15146=AXIS2_PLACEMENT_3D('',#35708,#15972,#15973);
#15147=AXIS2_PLACEMENT_3D('',#36174,#15975,#15976);
#15148=AXIS2_PLACEMENT_3D('',#36637,#15978,#15979);
#15149=AXIS2_PLACEMENT_3D('',#37100,#15981,#15982);
#15150=AXIS2_PLACEMENT_3D('',#37569,#15984,#15985);
#15151=AXIS2_PLACEMENT_3D('',#38035,#15987,#15988);
#15152=AXIS2_PLACEMENT_3D('',#38498,#15990,#15991);
#15153=AXIS2_PLACEMENT_3D('',#38964,#15993,#15994);
#15154=AXIS2_PLACEMENT_3D('',#39430,#15996,#15997);
#15155=AXIS2_PLACEMENT_3D('',#39893,#15999,#16000);
#15156=AXIS2_PLACEMENT_3D('',#40362,#16002,#16003);
#15157=AXIS2_PLACEMENT_3D('',#40831,#16005,#16006);
#15158=AXIS2_PLACEMENT_3D('',#41297,#16008,#16009);
#15159=AXIS2_PLACEMENT_3D('',#41760,#16011,#16012);
#15160=AXIS2_PLACEMENT_3D('',#42226,#16014,#16015);
#15161=AXIS2_PLACEMENT_3D('',#42692,#16017,#16018);
#15162=AXIS2_PLACEMENT_3D('',#43155,#16020,#16021);
#15163=AXIS2_PLACEMENT_3D('',#43627,#16023,#16024);
#15164=AXIS2_PLACEMENT_3D('',#44096,#16026,#16027);
#15165=AXIS2_PLACEMENT_3D('',#44559,#16029,#16030);
#15166=AXIS2_PLACEMENT_3D('',#45022,#16032,#16033);
#15167=AXIS2_PLACEMENT_3D('',#45488,#16035,#16036);
#15168=AXIS2_PLACEMENT_3D('',#45954,#16038,#16039);
#15169=AXIS2_PLACEMENT_3D('',#46414,#16041,#16042);
#15170=AXIS2_PLACEMENT_3D('',#46883,#16044,#16045);
#15171=AXIS2_PLACEMENT_3D('',#47352,#16047,#16048);
#15172=AXIS2_PLACEMENT_3D('',#47815,#16050,#16051);
#15173=AXIS2_PLACEMENT_3D('',#48281,#16053,#16054);
#15174=AXIS2_PLACEMENT_3D('',#48744,#16056,#16057);
#15175=AXIS2_PLACEMENT_3D('',#49210,#16059,#16060);
#15176=AXIS2_PLACEMENT_3D('',#49673,#16062,#16063);
#15177=AXIS2_PLACEMENT_3D('',#49932,#16065,#16066);
#15178=AXIS2_PLACEMENT_3D('',#50185,#16068,#16069);
#15179=AXIS2_PLACEMENT_3D('',#50645,#16071,#16072);
#15180=AXIS2_PLACEMENT_3D('',#51111,#16074,#16075);
#15181=AXIS2_PLACEMENT_3D('',#51574,#16077,#16078);
#15182=AXIS2_PLACEMENT_3D('',#52040,#16080,#16081);
#15183=AXIS2_PLACEMENT_3D('',#52506,#16083,#16084);
#15184=AXIS2_PLACEMENT_3D('',#52975,#16086,#16087);
#15185=AXIS2_PLACEMENT_3D('',#53444,#16089,#16090);
#15186=AXIS2_PLACEMENT_3D('',#53907,#16092,#16093);
#15187=AXIS2_PLACEMENT_3D('',#54373,#16095,#16096);
#15188=AXIS2_PLACEMENT_3D('',#54836,#16098,#16099);
#15189=AXIS2_PLACEMENT_3D('',#55302,#16101,#16102);
#15190=AXIS2_PLACEMENT_3D('',#55768,#16104,#16105);
#15191=AXIS2_PLACEMENT_3D('',#56237,#16107,#16108);
#15192=AXIS2_PLACEMENT_3D('',#56706,#16110,#16111);
#15193=AXIS2_PLACEMENT_3D('',#57169,#16113,#16114);
#15194=AXIS2_PLACEMENT_3D('',#57635,#16116,#16117);
#15195=AXIS2_PLACEMENT_3D('',#58098,#16119,#16120);
#15196=AXIS2_PLACEMENT_3D('',#58567,#16122,#16123);
#15197=AXIS2_PLACEMENT_3D('',#59033,#16125,#16126);
#15198=AXIS2_PLACEMENT_3D('',#59499,#16128,#16129);
#15199=AXIS2_PLACEMENT_3D('',#59968,#16131,#16132);
#15200=AXIS2_PLACEMENT_3D('',#60434,#16134,#16135);
#15201=AXIS2_PLACEMENT_3D('',#60897,#16137,#16138);
#15202=AXIS2_PLACEMENT_3D('',#61360,#16140,#16141);
#15203=AXIS2_PLACEMENT_3D('',#61829,#16143,#16144);
#15204=AXIS2_PLACEMENT_3D('',#62295,#16146,#16147);
#15205=AXIS2_PLACEMENT_3D('',#62761,#16149,#16150);
#15206=AXIS2_PLACEMENT_3D('',#63233,#16152,#16153);
#15207=AXIS2_PLACEMENT_3D('',#63699,#16155,#16156);
#15208=AXIS2_PLACEMENT_3D('',#64162,#16158,#16159);
#15209=AXIS2_PLACEMENT_3D('',#64625,#16161,#16162);
#15210=AXIS2_PLACEMENT_3D('',#65091,#16164,#16165);
#15211=AXIS2_PLACEMENT_3D('',#65557,#16167,#16168);
#15212=AXIS2_PLACEMENT_3D('',#66023,#16170,#16171);
#15213=AXIS2_PLACEMENT_3D('',#66492,#16173,#16174);
#15214=AXIS2_PLACEMENT_3D('',#66958,#16176,#16177);
#15215=AXIS2_PLACEMENT_3D('',#67421,#16179,#16180);
#15216=AXIS2_PLACEMENT_3D('',#67884,#16182,#16183);
#15217=AXIS2_PLACEMENT_3D('',#68350,#16185,#16186);
#15218=AXIS2_PLACEMENT_3D('',#68816,#16188,#16189);
#15219=AXIS2_PLACEMENT_3D('',#69282,#16191,#16192);
#15220=AXIS2_PLACEMENT_3D('',#69751,#16194,#16195);
#15221=AXIS2_PLACEMENT_3D('',#70217,#16197,#16198);
#15222=AXIS2_PLACEMENT_3D('',#70680,#16200,#16201);
#15223=AXIS2_PLACEMENT_3D('',#71149,#16203,#16204);
#15224=AXIS2_PLACEMENT_3D('',#71615,#16206,#16207);
#15225=AXIS2_PLACEMENT_3D('',#72078,#16209,#16210);
#15226=AXIS2_PLACEMENT_3D('',#72544,#16212,#16213);
#15227=AXIS2_PLACEMENT_3D('',#73013,#16215,#16216);
#15228=AXIS2_PLACEMENT_3D('',#73479,#16218,#16219);
#15229=AXIS2_PLACEMENT_3D('',#73942,#16221,#16222);
#15230=AXIS2_PLACEMENT_3D('',#74411,#16224,#16225);
#15231=AXIS2_PLACEMENT_3D('',#74877,#16227,#16228);
#15232=AXIS2_PLACEMENT_3D('',#75340,#16230,#16231);
#15233=AXIS2_PLACEMENT_3D('',#75806,#16233,#16234);
#15234=AXIS2_PLACEMENT_3D('',#76275,#16236,#16237);
#15235=AXIS2_PLACEMENT_3D('',#76741,#16239,#16240);
#15236=AXIS2_PLACEMENT_3D('',#77201,#16242,#16243);
#15237=AXIS2_PLACEMENT_3D('',#77667,#16245,#16246);
#15238=AXIS2_PLACEMENT_3D('',#78133,#16248,#16249);
#15239=AXIS2_PLACEMENT_3D('',#78596,#16251,#16252);
#15240=AXIS2_PLACEMENT_3D('',#79062,#16254,#16255);
#15241=AXIS2_PLACEMENT_3D('',#79531,#16257,#16258);
#15242=AXIS2_PLACEMENT_3D('',#79997,#16260,#16261);
#15243=AXIS2_PLACEMENT_3D('',#80457,#16263,#16264);
#15244=AXIS2_PLACEMENT_3D('',#80923,#16266,#16267);
#15245=AXIS2_PLACEMENT_3D('',#81389,#16269,#16270);
#15246=AXIS2_PLACEMENT_3D('',#81852,#16272,#16273);
#15247=AXIS2_PLACEMENT_3D('',#82111,#16275,#16276);
#15248=AXIS2_PLACEMENT_3D('',#82362,#16278,#16279);
#15249=AXIS2_PLACEMENT_3D('',#82822,#16281,#16282);
#15250=AXIS2_PLACEMENT_3D('',#83282,#16284,#16285);
#15251=AXIS2_PLACEMENT_3D('',#83748,#16287,#16288);
#15252=AXIS2_PLACEMENT_3D('',#84214,#16290,#16291);
#15253=AXIS2_PLACEMENT_3D('',#84677,#16293,#16294);
#15254=AXIS2_PLACEMENT_3D('',#85146,#16296,#16297);
#15255=AXIS2_PLACEMENT_3D('',#85612,#16299,#16300);
#15256=AXIS2_PLACEMENT_3D('',#86081,#16302,#16303);
#15257=AXIS2_PLACEMENT_3D('',#86547,#16305,#16306);
#15258=AXIS2_PLACEMENT_3D('',#87013,#16308,#16309);
#15259=AXIS2_PLACEMENT_3D('',#87479,#16311,#16312);
#15260=AXIS2_PLACEMENT_3D('',#87942,#16314,#16315);
#15261=AXIS2_PLACEMENT_3D('',#88411,#16317,#16318);
#15262=AXIS2_PLACEMENT_3D('',#88877,#16320,#16321);
#15263=AXIS2_PLACEMENT_3D('',#89346,#16323,#16324);
#15264=AXIS2_PLACEMENT_3D('',#89812,#16326,#16327);
#15265=AXIS2_PLACEMENT_3D('',#90275,#16329,#16330);
#15266=AXIS2_PLACEMENT_3D('',#90741,#16332,#16333);
#15267=AXIS2_PLACEMENT_3D('',#91204,#16335,#16336);
#15268=AXIS2_PLACEMENT_3D('',#91673,#16338,#16339);
#15269=AXIS2_PLACEMENT_3D('',#92139,#16341,#16342);
#15270=AXIS2_PLACEMENT_3D('',#92608,#16344,#16345);
#15271=AXIS2_PLACEMENT_3D('',#93074,#16347,#16348);
#15272=AXIS2_PLACEMENT_3D('',#93537,#16350,#16351);
#15273=AXIS2_PLACEMENT_3D('',#94003,#16353,#16354);
#15274=AXIS2_PLACEMENT_3D('',#94469,#16356,#16357);
#15275=AXIS2_PLACEMENT_3D('',#94938,#16359,#16360);
#15276=AXIS2_PLACEMENT_3D('',#95404,#16362,#16363);
#15277=AXIS2_PLACEMENT_3D('',#95867,#16365,#16366);
#15278=AXIS2_PLACEMENT_3D('',#96333,#16368,#16369);
#15279=AXIS2_PLACEMENT_3D('',#96796,#16371,#16372);
#15280=AXIS2_PLACEMENT_3D('',#97262,#16374,#16375);
#15281=AXIS2_PLACEMENT_3D('',#97728,#16377,#16378);
#15282=AXIS2_PLACEMENT_3D('',#97987,#16380,#16381);
#15283=AXIS2_PLACEMENT_3D('',#98447,#16383,#16384);
#15284=AXIS2_PLACEMENT_3D('',#98913,#16386,#16387);
#15285=AXIS2_PLACEMENT_3D('',#99379,#16389,#16390);
#15286=AXIS2_PLACEMENT_3D('',#99842,#16392,#16393);
#15287=AXIS2_PLACEMENT_3D('',#100308,#16395,#16396);
#15288=AXIS2_PLACEMENT_3D('',#100774,#16398,#16399);
#15289=AXIS2_PLACEMENT_3D('',#101240,#16401,#16402);
#15290=AXIS2_PLACEMENT_3D('',#101709,#16404,#16405);
#15291=AXIS2_PLACEMENT_3D('',#102175,#16407,#16408);
#15292=AXIS2_PLACEMENT_3D('',#102638,#16410,#16411);
#15293=AXIS2_PLACEMENT_3D('',#103101,#16413,#16414);
#15294=AXIS2_PLACEMENT_3D('',#103573,#16416,#16417);
#15295=AXIS2_PLACEMENT_3D('',#104039,#16419,#16420);
#15296=AXIS2_PLACEMENT_3D('',#104505,#16422,#16423);
#15297=AXIS2_PLACEMENT_3D('',#104977,#16425,#16426);
#15298=AXIS2_PLACEMENT_3D('',#105443,#16428,#16429);
#15299=AXIS2_PLACEMENT_3D('',#105906,#16431,#16432);
#15300=AXIS2_PLACEMENT_3D('',#106369,#16434,#16435);
#15301=AXIS2_PLACEMENT_3D('',#106841,#16437,#16438);
#15302=AXIS2_PLACEMENT_3D('',#107307,#16440,#16441);
#15303=AXIS2_PLACEMENT_3D('',#107770,#16443,#16444);
#15304=AXIS2_PLACEMENT_3D('',#108239,#16446,#16447);
#15305=AXIS2_PLACEMENT_3D('',#108705,#16449,#16450);
#15306=AXIS2_PLACEMENT_3D('',#109168,#16452,#16453);
#15307=AXIS2_PLACEMENT_3D('',#109631,#16455,#16456);
#15308=AXIS2_PLACEMENT_3D('',#109890,#16458,#16459);
#15309=AXIS2_PLACEMENT_3D('',#110350,#16461,#16462);
#15310=AXIS2_PLACEMENT_3D('',#110813,#16464,#16465);
#15311=AXIS2_PLACEMENT_3D('',#111279,#16467,#16468);
#15312=AXIS2_PLACEMENT_3D('',#111745,#16470,#16471);
#15313=AXIS2_PLACEMENT_3D('',#112208,#16473,#16474);
#15314=AXIS2_PLACEMENT_3D('',#112671,#16476,#16477);
#15315=AXIS2_PLACEMENT_3D('',#113140,#16479,#16480);
#15316=AXIS2_PLACEMENT_3D('',#113606,#16482,#16483);
#15317=AXIS2_PLACEMENT_3D('',#114069,#16485,#16486);
#15318=AXIS2_PLACEMENT_3D('',#114535,#16488,#16489);
#15319=AXIS2_PLACEMENT_3D('',#115001,#16491,#16492);
#15320=AXIS2_PLACEMENT_3D('',#115464,#16494,#16495);
#15321=AXIS2_PLACEMENT_3D('',#115933,#16497,#16498);
#15322=AXIS2_PLACEMENT_3D('',#116402,#16500,#16501);
#15323=AXIS2_PLACEMENT_3D('',#116868,#16503,#16504);
#15324=AXIS2_PLACEMENT_3D('',#117331,#16506,#16507);
#15325=AXIS2_PLACEMENT_3D('',#117797,#16509,#16510);
#15326=AXIS2_PLACEMENT_3D('',#118263,#16512,#16513);
#15327=AXIS2_PLACEMENT_3D('',#118726,#16515,#16516);
#15328=AXIS2_PLACEMENT_3D('',#119198,#16518,#16519);
#15329=AXIS2_PLACEMENT_3D('',#119667,#16521,#16522);
#15330=AXIS2_PLACEMENT_3D('',#120130,#16524,#16525);
#15331=AXIS2_PLACEMENT_3D('',#120593,#16527,#16528);
#15332=AXIS2_PLACEMENT_3D('',#121056,#16530,#16531);
#15333=AXIS2_PLACEMENT_3D('',#121522,#16533,#16534);
#15334=AXIS2_PLACEMENT_3D('',#121982,#16536,#16537);
#15335=AXIS2_PLACEMENT_3D('',#122451,#16539,#16540);
#15336=AXIS2_PLACEMENT_3D('',#122920,#16542,#16543);
#15337=AXIS2_PLACEMENT_3D('',#123383,#16545,#16546);
#15338=AXIS2_PLACEMENT_3D('',#123849,#16548,#16549);
#15339=AXIS2_PLACEMENT_3D('',#124312,#16551,#16552);
#15340=AXIS2_PLACEMENT_3D('',#124778,#16554,#16555);
#15341=AXIS2_PLACEMENT_3D('',#125241,#16557,#16558);
#15342=AXIS2_PLACEMENT_3D('',#125500,#16560,#16561);
#15343=AXIS2_PLACEMENT_3D('',#125753,#16563,#16564);
#15344=AXIS2_PLACEMENT_3D('',#126213,#16566,#16567);
#15345=AXIS2_PLACEMENT_3D('',#126679,#16569,#16570);
#15346=AXIS2_PLACEMENT_3D('',#127142,#16572,#16573);
#15347=AXIS2_PLACEMENT_3D('',#127608,#16575,#16576);
#15348=AXIS2_PLACEMENT_3D('',#128074,#16578,#16579);
#15349=AXIS2_PLACEMENT_3D('',#128543,#16581,#16582);
#15350=AXIS2_PLACEMENT_3D('',#129012,#16584,#16585);
#15351=AXIS2_PLACEMENT_3D('',#129475,#16587,#16588);
#15352=AXIS2_PLACEMENT_3D('',#129941,#16590,#16591);
#15353=AXIS2_PLACEMENT_3D('',#130404,#16593,#16594);
#15354=AXIS2_PLACEMENT_3D('',#130870,#16596,#16597);
#15355=AXIS2_PLACEMENT_3D('',#131336,#16599,#16600);
#15356=AXIS2_PLACEMENT_3D('',#131805,#16602,#16603);
#15357=AXIS2_PLACEMENT_3D('',#132274,#16605,#16606);
#15358=AXIS2_PLACEMENT_3D('',#132737,#16608,#16609);
#15359=AXIS2_PLACEMENT_3D('',#133203,#16611,#16612);
#15360=AXIS2_PLACEMENT_3D('',#133666,#16614,#16615);
#15361=AXIS2_PLACEMENT_3D('',#134135,#16617,#16618);
#15362=AXIS2_PLACEMENT_3D('',#134601,#16620,#16621);
#15363=AXIS2_PLACEMENT_3D('',#135067,#16623,#16624);
#15364=AXIS2_PLACEMENT_3D('',#135536,#16626,#16627);
#15365=AXIS2_PLACEMENT_3D('',#136002,#16629,#16630);
#15366=AXIS2_PLACEMENT_3D('',#136465,#16632,#16633);
#15367=AXIS2_PLACEMENT_3D('',#136928,#16635,#16636);
#15368=AXIS2_PLACEMENT_3D('',#137397,#16638,#16639);
#15369=AXIS2_PLACEMENT_3D('',#137863,#16641,#16642);
#15370=AXIS2_PLACEMENT_3D('',#138329,#16644,#16645);
#15371=AXIS2_PLACEMENT_3D('',#138801,#16647,#16648);
#15372=AXIS2_PLACEMENT_3D('',#139267,#16650,#16651);
#15373=AXIS2_PLACEMENT_3D('',#139730,#16653,#16654);
#15374=AXIS2_PLACEMENT_3D('',#140193,#16656,#16657);
#15375=AXIS2_PLACEMENT_3D('',#140276,#16658,#16659);
#15376=AXIS2_PLACEMENT_3D('',#164173,#16660,#16661);
#15377=AXIS2_PLACEMENT_3D('',#187985,#16662,#16663);
#15378=AXIS2_PLACEMENT_3D('',#188213,#16664,#16665);
#15379=AXIS2_PLACEMENT_3D('',#188388,#16666,#16667);
#15380=AXIS2_PLACEMENT_3D('',#188390,#16668,#16669);
#15381=AXIS2_PLACEMENT_3D('',#188392,#16670,#16671);
#15382=AXIS2_PLACEMENT_3D('',#188393,#16672,#16673);
#15383=AXIS2_PLACEMENT_3D('',#188396,#16675,#16676);
#15384=AXIS2_PLACEMENT_3D('',#188397,#16677,#16678);
#15385=AXIS2_PLACEMENT_3D('',#188613,#16679,#16680);
#15386=AXIS2_PLACEMENT_3D('',#188622,#16685,#16686);
#15387=AXIS2_PLACEMENT_3D('',#188623,#16687,#16688);
#15388=AXIS2_PLACEMENT_3D('',#188624,#16689,#16690);
#15389=AXIS2_PLACEMENT_3D('',#188633,#16695,#16696);
#15390=AXIS2_PLACEMENT_3D('',#188635,#16697,#16698);
#15391=AXIS2_PLACEMENT_3D('',#188636,#16699,#16700);
#15392=AXIS2_PLACEMENT_3D('',#188637,#16701,#16702);
#15393=AXIS2_PLACEMENT_3D('',#188639,#16704,#16705);
#15394=AXIS2_PLACEMENT_3D('',#188640,#16706,#16707);
#15395=AXIS2_PLACEMENT_3D('',#188641,#16708,#16709);
#15396=AXIS2_PLACEMENT_3D('',#202420,#16710,#16711);
#15848=DIRECTION('axis',(0.,0.,1.));
#15849=DIRECTION('refdir',(1.,0.,0.));
#15850=DIRECTION('center_axis',(-1.,0.,0.));
#15851=DIRECTION('ref_axis',(0.,0.968648305440766,0.248436028721142));
#15852=DIRECTION('',(1.,0.,0.));
#15853=DIRECTION('center_axis',(1.,0.,0.));
#15854=DIRECTION('ref_axis',(0.,1.,-2.30250085928462E-11));
#15855=DIRECTION('center_axis',(-1.,0.,0.));
#15856=DIRECTION('ref_axis',(0.,0.968648305440766,0.248436028721142));
#15857=DIRECTION('',(1.,0.,0.));
#15858=DIRECTION('center_axis',(-1.,0.,0.));
#15859=DIRECTION('ref_axis',(0.,0.968648305440766,0.248436028721142));
#15860=DIRECTION('',(1.,0.,0.));
#15861=DIRECTION('center_axis',(-1.,0.,0.));
#15862=DIRECTION('ref_axis',(0.,0.968648305440766,0.248436028721142));
#15863=DIRECTION('',(1.,0.,0.));
#15864=DIRECTION('center_axis',(-1.,0.,0.));
#15865=DIRECTION('ref_axis',(0.,0.968648305440766,0.248436028721142));
#15866=DIRECTION('',(1.,0.,0.));
#15867=DIRECTION('center_axis',(-1.,0.,0.));
#15868=DIRECTION('ref_axis',(0.,0.968648305440766,0.248436028721142));
#15869=DIRECTION('',(1.,0.,0.));
#15870=DIRECTION('center_axis',(-1.,0.,0.));
#15871=DIRECTION('ref_axis',(0.,0.968648305440766,0.248436028721142));
#15872=DIRECTION('',(1.,0.,0.));
#15873=DIRECTION('center_axis',(-1.,0.,0.));
#15874=DIRECTION('ref_axis',(0.,0.968648305440766,0.248436028721142));
#15875=DIRECTION('',(1.,0.,0.));
#15876=DIRECTION('center_axis',(-1.,0.,0.));
#15877=DIRECTION('ref_axis',(0.,0.968648305440766,0.248436028721142));
#15878=DIRECTION('',(1.,0.,0.));
#15879=DIRECTION('center_axis',(-1.,0.,0.));
#15880=DIRECTION('ref_axis',(0.,0.968648305440766,0.248436028721142));
#15881=DIRECTION('',(1.,0.,0.));
#15882=DIRECTION('center_axis',(-1.,0.,0.));
#15883=DIRECTION('ref_axis',(0.,0.968648305440766,0.248436028721142));
#15884=DIRECTION('',(1.,0.,0.));
#15885=DIRECTION('center_axis',(-1.,0.,0.));
#15886=DIRECTION('ref_axis',(0.,0.968648305440766,0.248436028721142));
#15887=DIRECTION('',(1.,0.,0.));
#15888=DIRECTION('center_axis',(-1.,0.,0.));
#15889=DIRECTION('ref_axis',(0.,0.968648305440766,0.248436028721142));
#15890=DIRECTION('',(1.,0.,0.));
#15891=DIRECTION('center_axis',(-1.,0.,0.));
#15892=DIRECTION('ref_axis',(0.,0.968648305440766,0.248436028721142));
#15893=DIRECTION('',(1.,0.,0.));
#15894=DIRECTION('center_axis',(-1.,0.,0.));
#15895=DIRECTION('ref_axis',(0.,0.968648305440766,0.248436028721142));
#15896=DIRECTION('',(1.,0.,0.));
#15897=DIRECTION('center_axis',(-1.,0.,0.));
#15898=DIRECTION('ref_axis',(0.,0.968648305440766,0.248436028721142));
#15899=DIRECTION('',(1.,0.,0.));
#15900=DIRECTION('center_axis',(-1.,0.,0.));
#15901=DIRECTION('ref_axis',(0.,0.968648305440766,0.248436028721142));
#15902=DIRECTION('',(1.,0.,0.));
#15903=DIRECTION('center_axis',(-1.,0.,0.));
#15904=DIRECTION('ref_axis',(0.,0.968648305440766,0.248436028721142));
#15905=DIRECTION('',(1.,0.,0.));
#15906=DIRECTION('center_axis',(-1.,0.,0.));
#15907=DIRECTION('ref_axis',(0.,0.968648305440766,0.248436028721142));
#15908=DIRECTION('',(1.,0.,0.));
#15909=DIRECTION('center_axis',(-1.,0.,0.));
#15910=DIRECTION('ref_axis',(0.,0.968648305440766,0.248436028721142));
#15911=DIRECTION('',(1.,0.,0.));
#15912=DIRECTION('center_axis',(-1.,0.,0.));
#15913=DIRECTION('ref_axis',(0.,0.968648305440766,0.248436028721142));
#15914=DIRECTION('',(1.,0.,0.));
#15915=DIRECTION('center_axis',(-1.,0.,0.));
#15916=DIRECTION('ref_axis',(0.,0.968648305440766,0.248436028721142));
#15917=DIRECTION('',(1.,0.,0.));
#15918=DIRECTION('center_axis',(-1.,0.,0.));
#15919=DIRECTION('ref_axis',(0.,0.968648305440766,0.248436028721142));
#15920=DIRECTION('',(1.,0.,0.));
#15921=DIRECTION('center_axis',(-1.,0.,0.));
#15922=DIRECTION('ref_axis',(0.,0.968648305440766,0.248436028721142));
#15923=DIRECTION('',(1.,0.,0.));
#15924=DIRECTION('center_axis',(-1.,0.,0.));
#15925=DIRECTION('ref_axis',(0.,0.968648305440766,0.248436028721142));
#15926=DIRECTION('',(1.,0.,0.));
#15927=DIRECTION('center_axis',(-1.,0.,0.));
#15928=DIRECTION('ref_axis',(0.,0.968648305440766,0.248436028721142));
#15929=DIRECTION('',(1.,0.,0.));
#15930=DIRECTION('center_axis',(-1.,0.,0.));
#15931=DIRECTION('ref_axis',(0.,0.968648305440766,0.248436028721142));
#15932=DIRECTION('',(1.,0.,0.));
#15933=DIRECTION('center_axis',(-1.,0.,0.));
#15934=DIRECTION('ref_axis',(0.,0.968648305440766,0.248436028721142));
#15935=DIRECTION('',(1.,0.,0.));
#15936=DIRECTION('center_axis',(-1.,0.,0.));
#15937=DIRECTION('ref_axis',(0.,0.968648305440766,0.248436028721142));
#15938=DIRECTION('',(1.,0.,0.));
#15939=DIRECTION('center_axis',(-1.,0.,0.));
#15940=DIRECTION('ref_axis',(0.,0.968648305440766,0.248436028721142));
#15941=DIRECTION('',(1.,0.,0.));
#15942=DIRECTION('center_axis',(-1.,0.,0.));
#15943=DIRECTION('ref_axis',(0.,0.968648305440766,0.248436028721142));
#15944=DIRECTION('',(1.,0.,0.));
#15945=DIRECTION('center_axis',(-1.,0.,0.));
#15946=DIRECTION('ref_axis',(0.,0.968648305440766,0.248436028721142));
#15947=DIRECTION('',(1.,0.,0.));
#15948=DIRECTION('center_axis',(-1.,0.,0.));
#15949=DIRECTION('ref_axis',(0.,0.968648305440766,0.248436028721142));
#15950=DIRECTION('',(1.,0.,0.));
#15951=DIRECTION('center_axis',(-1.,0.,0.));
#15952=DIRECTION('ref_axis',(0.,0.968648305440766,0.248436028721142));
#15953=DIRECTION('',(1.,0.,0.));
#15954=DIRECTION('center_axis',(-1.,0.,0.));
#15955=DIRECTION('ref_axis',(0.,0.968648305440766,0.248436028721142));
#15956=DIRECTION('',(1.,0.,0.));
#15957=DIRECTION('center_axis',(-1.,0.,0.));
#15958=DIRECTION('ref_axis',(0.,0.968648305440766,0.248436028721142));
#15959=DIRECTION('',(1.,0.,0.));
#15960=DIRECTION('center_axis',(-1.,0.,0.));
#15961=DIRECTION('ref_axis',(0.,0.968648305440766,0.248436028721142));
#15962=DIRECTION('',(1.,0.,0.));
#15963=DIRECTION('center_axis',(-1.,0.,0.));
#15964=DIRECTION('ref_axis',(0.,0.968648305440766,0.248436028721142));
#15965=DIRECTION('',(1.,0.,0.));
#15966=DIRECTION('center_axis',(-1.,0.,0.));
#15967=DIRECTION('ref_axis',(0.,0.968648305440766,0.248436028721142));
#15968=DIRECTION('',(1.,0.,0.));
#15969=DIRECTION('center_axis',(-1.,0.,0.));
#15970=DIRECTION('ref_axis',(0.,0.968648305440766,0.248436028721142));
#15971=DIRECTION('',(1.,0.,0.));
#15972=DIRECTION('center_axis',(-1.,0.,0.));
#15973=DIRECTION('ref_axis',(0.,0.968648305440766,0.248436028721142));
#15974=DIRECTION('',(1.,0.,0.));
#15975=DIRECTION('center_axis',(-1.,0.,0.));
#15976=DIRECTION('ref_axis',(0.,0.968648305440766,0.248436028721142));
#15977=DIRECTION('',(1.,0.,0.));
#15978=DIRECTION('center_axis',(-1.,0.,0.));
#15979=DIRECTION('ref_axis',(0.,0.968648305440766,0.248436028721142));
#15980=DIRECTION('',(1.,0.,0.));
#15981=DIRECTION('center_axis',(-1.,0.,0.));
#15982=DIRECTION('ref_axis',(0.,0.968648305440766,0.248436028721142));
#15983=DIRECTION('',(1.,0.,0.));
#15984=DIRECTION('center_axis',(-1.,0.,0.));
#15985=DIRECTION('ref_axis',(0.,0.968648305440766,0.248436028721142));
#15986=DIRECTION('',(1.,0.,0.));
#15987=DIRECTION('center_axis',(-1.,0.,0.));
#15988=DIRECTION('ref_axis',(0.,0.968648305440766,0.248436028721142));
#15989=DIRECTION('',(1.,0.,0.));
#15990=DIRECTION('center_axis',(-1.,0.,0.));
#15991=DIRECTION('ref_axis',(0.,0.968648305440766,0.248436028721142));
#15992=DIRECTION('',(1.,0.,0.));
#15993=DIRECTION('center_axis',(-1.,0.,0.));
#15994=DIRECTION('ref_axis',(0.,0.968648305440766,0.248436028721142));
#15995=DIRECTION('',(1.,0.,0.));
#15996=DIRECTION('center_axis',(-1.,0.,0.));
#15997=DIRECTION('ref_axis',(0.,0.968648305440766,0.248436028721142));
#15998=DIRECTION('',(1.,0.,0.));
#15999=DIRECTION('center_axis',(-1.,0.,0.));
#16000=DIRECTION('ref_axis',(0.,0.968648305440766,0.248436028721142));
#16001=DIRECTION('',(1.,0.,0.));
#16002=DIRECTION('center_axis',(-1.,0.,0.));
#16003=DIRECTION('ref_axis',(0.,0.968648305440766,0.248436028721142));
#16004=DIRECTION('',(1.,0.,0.));
#16005=DIRECTION('center_axis',(-1.,0.,0.));
#16006=DIRECTION('ref_axis',(0.,0.968648305440766,0.248436028721142));
#16007=DIRECTION('',(1.,0.,0.));
#16008=DIRECTION('center_axis',(-1.,0.,0.));
#16009=DIRECTION('ref_axis',(0.,0.968648305440766,0.248436028721142));
#16010=DIRECTION('',(1.,0.,0.));
#16011=DIRECTION('center_axis',(-1.,0.,0.));
#16012=DIRECTION('ref_axis',(0.,0.968648305440766,0.248436028721142));
#16013=DIRECTION('',(1.,0.,0.));
#16014=DIRECTION('center_axis',(-1.,0.,0.));
#16015=DIRECTION('ref_axis',(0.,0.968648305440766,0.248436028721142));
#16016=DIRECTION('',(1.,0.,0.));
#16017=DIRECTION('center_axis',(-1.,0.,0.));
#16018=DIRECTION('ref_axis',(0.,0.968648305440766,0.248436028721142));
#16019=DIRECTION('',(1.,0.,0.));
#16020=DIRECTION('center_axis',(-1.,0.,0.));
#16021=DIRECTION('ref_axis',(0.,0.968648305440766,0.248436028721142));
#16022=DIRECTION('',(1.,0.,0.));
#16023=DIRECTION('center_axis',(-1.,0.,0.));
#16024=DIRECTION('ref_axis',(0.,0.968648305440766,0.248436028721142));
#16025=DIRECTION('',(1.,0.,0.));
#16026=DIRECTION('center_axis',(-1.,0.,0.));
#16027=DIRECTION('ref_axis',(0.,0.968648305440766,0.248436028721142));
#16028=DIRECTION('',(1.,0.,0.));
#16029=DIRECTION('center_axis',(-1.,0.,0.));
#16030=DIRECTION('ref_axis',(0.,0.968648305440766,0.248436028721142));
#16031=DIRECTION('',(1.,0.,0.));
#16032=DIRECTION('center_axis',(-1.,0.,0.));
#16033=DIRECTION('ref_axis',(0.,0.968648305440766,0.248436028721142));
#16034=DIRECTION('',(1.,0.,0.));
#16035=DIRECTION('center_axis',(-1.,0.,0.));
#16036=DIRECTION('ref_axis',(0.,0.968648305440766,0.248436028721142));
#16037=DIRECTION('',(1.,0.,0.));
#16038=DIRECTION('center_axis',(-1.,0.,0.));
#16039=DIRECTION('ref_axis',(0.,0.968648305440766,0.248436028721142));
#16040=DIRECTION('',(1.,0.,0.));
#16041=DIRECTION('center_axis',(-1.,0.,0.));
#16042=DIRECTION('ref_axis',(0.,0.968648305440766,0.248436028721142));
#16043=DIRECTION('',(1.,0.,0.));
#16044=DIRECTION('center_axis',(-1.,0.,0.));
#16045=DIRECTION('ref_axis',(0.,0.968648305440766,0.248436028721142));
#16046=DIRECTION('',(1.,0.,0.));
#16047=DIRECTION('center_axis',(-1.,0.,0.));
#16048=DIRECTION('ref_axis',(0.,0.968648305440766,0.248436028721142));
#16049=DIRECTION('',(1.,0.,0.));
#16050=DIRECTION('center_axis',(-1.,0.,0.));
#16051=DIRECTION('ref_axis',(0.,0.968648305440766,0.248436028721142));
#16052=DIRECTION('',(1.,0.,0.));
#16053=DIRECTION('center_axis',(-1.,0.,0.));
#16054=DIRECTION('ref_axis',(0.,0.968648305440766,0.248436028721142));
#16055=DIRECTION('',(1.,0.,0.));
#16056=DIRECTION('center_axis',(-1.,0.,0.));
#16057=DIRECTION('ref_axis',(0.,0.968648305440766,0.248436028721142));
#16058=DIRECTION('',(1.,0.,0.));
#16059=DIRECTION('center_axis',(-1.,0.,0.));
#16060=DIRECTION('ref_axis',(0.,0.968648305440766,0.248436028721142));
#16061=DIRECTION('',(1.,0.,0.));
#16062=DIRECTION('center_axis',(-1.,0.,0.));
#16063=DIRECTION('ref_axis',(0.,0.968648305440766,0.248436028721142));
#16064=DIRECTION('',(1.,0.,0.));
#16065=DIRECTION('center_axis',(-1.,0.,0.));
#16066=DIRECTION('ref_axis',(0.,0.968648305440766,0.248436028721142));
#16067=DIRECTION('',(1.,0.,0.));
#16068=DIRECTION('center_axis',(-1.,0.,0.));
#16069=DIRECTION('ref_axis',(0.,0.968648305440766,0.248436028721142));
#16070=DIRECTION('',(1.,0.,0.));
#16071=DIRECTION('center_axis',(-1.,0.,0.));
#16072=DIRECTION('ref_axis',(0.,0.968648305440766,0.248436028721142));
#16073=DIRECTION('',(1.,0.,0.));
#16074=DIRECTION('center_axis',(-1.,0.,0.));
#16075=DIRECTION('ref_axis',(0.,0.968648305440766,0.248436028721142));
#16076=DIRECTION('',(1.,0.,0.));
#16077=DIRECTION('center_axis',(-1.,0.,0.));
#16078=DIRECTION('ref_axis',(0.,0.968648305440766,0.248436028721142));
#16079=DIRECTION('',(1.,0.,0.));
#16080=DIRECTION('center_axis',(-1.,0.,0.));
#16081=DIRECTION('ref_axis',(0.,0.968648305440766,0.248436028721142));
#16082=DIRECTION('',(1.,0.,0.));
#16083=DIRECTION('center_axis',(-1.,0.,0.));
#16084=DIRECTION('ref_axis',(0.,0.968648305440766,0.248436028721142));
#16085=DIRECTION('',(1.,0.,0.));
#16086=DIRECTION('center_axis',(-1.,0.,0.));
#16087=DIRECTION('ref_axis',(0.,0.968648305440766,0.248436028721142));
#16088=DIRECTION('',(1.,0.,0.));
#16089=DIRECTION('center_axis',(-1.,0.,0.));
#16090=DIRECTION('ref_axis',(0.,0.968648305440766,0.248436028721142));
#16091=DIRECTION('',(1.,0.,0.));
#16092=DIRECTION('center_axis',(-1.,0.,0.));
#16093=DIRECTION('ref_axis',(0.,0.968648305440766,0.248436028721142));
#16094=DIRECTION('',(1.,0.,0.));
#16095=DIRECTION('center_axis',(-1.,0.,0.));
#16096=DIRECTION('ref_axis',(0.,0.968648305440766,0.248436028721142));
#16097=DIRECTION('',(1.,0.,0.));
#16098=DIRECTION('center_axis',(-1.,0.,0.));
#16099=DIRECTION('ref_axis',(0.,0.968648305440766,0.248436028721142));
#16100=DIRECTION('',(1.,0.,0.));
#16101=DIRECTION('center_axis',(-1.,0.,0.));
#16102=DIRECTION('ref_axis',(0.,0.968648305440766,0.248436028721142));
#16103=DIRECTION('',(1.,0.,0.));
#16104=DIRECTION('center_axis',(-1.,0.,0.));
#16105=DIRECTION('ref_axis',(0.,0.968648305440766,0.248436028721142));
#16106=DIRECTION('',(1.,0.,0.));
#16107=DIRECTION('center_axis',(-1.,0.,0.));
#16108=DIRECTION('ref_axis',(0.,0.968648305440766,0.248436028721142));
#16109=DIRECTION('',(1.,0.,0.));
#16110=DIRECTION('center_axis',(-1.,0.,0.));
#16111=DIRECTION('ref_axis',(0.,0.968648305440766,0.248436028721142));
#16112=DIRECTION('',(1.,0.,0.));
#16113=DIRECTION('center_axis',(-1.,0.,0.));
#16114=DIRECTION('ref_axis',(0.,0.968648305440766,0.248436028721142));
#16115=DIRECTION('',(1.,0.,0.));
#16116=DIRECTION('center_axis',(-1.,0.,0.));
#16117=DIRECTION('ref_axis',(0.,0.968648305440766,0.248436028721142));
#16118=DIRECTION('',(1.,0.,0.));
#16119=DIRECTION('center_axis',(-1.,0.,0.));
#16120=DIRECTION('ref_axis',(0.,0.968648305440766,0.248436028721142));
#16121=DIRECTION('',(1.,0.,0.));
#16122=DIRECTION('center_axis',(-1.,0.,0.));
#16123=DIRECTION('ref_axis',(0.,0.968648305440766,0.248436028721142));
#16124=DIRECTION('',(1.,0.,0.));
#16125=DIRECTION('center_axis',(-1.,0.,0.));
#16126=DIRECTION('ref_axis',(0.,0.968648305440766,0.248436028721142));
#16127=DIRECTION('',(1.,0.,0.));
#16128=DIRECTION('center_axis',(-1.,0.,0.));
#16129=DIRECTION('ref_axis',(0.,0.968648305440766,0.248436028721142));
#16130=DIRECTION('',(1.,0.,0.));
#16131=DIRECTION('center_axis',(-1.,0.,0.));
#16132=DIRECTION('ref_axis',(0.,0.968648305440766,0.248436028721142));
#16133=DIRECTION('',(1.,0.,0.));
#16134=DIRECTION('center_axis',(-1.,0.,0.));
#16135=DIRECTION('ref_axis',(0.,0.968648305440766,0.248436028721142));
#16136=DIRECTION('',(1.,0.,0.));
#16137=DIRECTION('center_axis',(-1.,0.,0.));
#16138=DIRECTION('ref_axis',(0.,0.968648305440766,0.248436028721142));
#16139=DIRECTION('',(1.,0.,0.));
#16140=DIRECTION('center_axis',(-1.,0.,0.));
#16141=DIRECTION('ref_axis',(0.,0.968648305440766,0.248436028721142));
#16142=DIRECTION('',(1.,0.,0.));
#16143=DIRECTION('center_axis',(-1.,0.,0.));
#16144=DIRECTION('ref_axis',(0.,0.968648305440766,0.248436028721142));
#16145=DIRECTION('',(1.,0.,0.));
#16146=DIRECTION('center_axis',(-1.,0.,0.));
#16147=DIRECTION('ref_axis',(0.,0.968648305440766,0.248436028721142));
#16148=DIRECTION('',(1.,0.,0.));
#16149=DIRECTION('center_axis',(-1.,0.,0.));
#16150=DIRECTION('ref_axis',(0.,0.968648305440766,0.248436028721142));
#16151=DIRECTION('',(1.,0.,0.));
#16152=DIRECTION('center_axis',(-1.,0.,0.));
#16153=DIRECTION('ref_axis',(0.,0.968648305440766,0.248436028721142));
#16154=DIRECTION('',(1.,0.,0.));
#16155=DIRECTION('center_axis',(-1.,0.,0.));
#16156=DIRECTION('ref_axis',(0.,0.968648305440766,0.248436028721142));
#16157=DIRECTION('',(1.,0.,0.));
#16158=DIRECTION('center_axis',(-1.,0.,0.));
#16159=DIRECTION('ref_axis',(0.,0.968648305440766,0.248436028721142));
#16160=DIRECTION('',(1.,0.,0.));
#16161=DIRECTION('center_axis',(-1.,0.,0.));
#16162=DIRECTION('ref_axis',(0.,0.968648305440766,0.248436028721142));
#16163=DIRECTION('',(1.,0.,0.));
#16164=DIRECTION('center_axis',(-1.,0.,0.));
#16165=DIRECTION('ref_axis',(0.,0.968648305440766,0.248436028721142));
#16166=DIRECTION('',(1.,0.,0.));
#16167=DIRECTION('center_axis',(-1.,0.,0.));
#16168=DIRECTION('ref_axis',(0.,0.968648305440766,0.248436028721142));
#16169=DIRECTION('',(1.,0.,0.));
#16170=DIRECTION('center_axis',(-1.,0.,0.));
#16171=DIRECTION('ref_axis',(0.,0.968648305440766,0.248436028721142));
#16172=DIRECTION('',(1.,0.,0.));
#16173=DIRECTION('center_axis',(-1.,0.,0.));
#16174=DIRECTION('ref_axis',(0.,0.968648305440766,0.248436028721142));
#16175=DIRECTION('',(1.,0.,0.));
#16176=DIRECTION('center_axis',(-1.,0.,0.));
#16177=DIRECTION('ref_axis',(0.,0.968648305440766,0.248436028721142));
#16178=DIRECTION('',(1.,0.,0.));
#16179=DIRECTION('center_axis',(-1.,0.,0.));
#16180=DIRECTION('ref_axis',(0.,0.968648305440766,0.248436028721142));
#16181=DIRECTION('',(1.,0.,0.));
#16182=DIRECTION('center_axis',(-1.,0.,0.));
#16183=DIRECTION('ref_axis',(0.,0.968648305440766,0.248436028721142));
#16184=DIRECTION('',(1.,0.,0.));
#16185=DIRECTION('center_axis',(-1.,0.,0.));
#16186=DIRECTION('ref_axis',(0.,0.968648305440766,0.248436028721142));
#16187=DIRECTION('',(1.,0.,0.));
#16188=DIRECTION('center_axis',(-1.,0.,0.));
#16189=DIRECTION('ref_axis',(0.,0.968648305440766,0.248436028721142));
#16190=DIRECTION('',(1.,0.,0.));
#16191=DIRECTION('center_axis',(-1.,0.,0.));
#16192=DIRECTION('ref_axis',(0.,0.968648305440766,0.248436028721142));
#16193=DIRECTION('',(1.,0.,0.));
#16194=DIRECTION('center_axis',(-1.,0.,0.));
#16195=DIRECTION('ref_axis',(0.,0.968648305440766,0.248436028721142));
#16196=DIRECTION('',(1.,0.,0.));
#16197=DIRECTION('center_axis',(-1.,0.,0.));
#16198=DIRECTION('ref_axis',(0.,0.968648305440766,0.248436028721142));
#16199=DIRECTION('',(1.,0.,0.));
#16200=DIRECTION('center_axis',(-1.,0.,0.));
#16201=DIRECTION('ref_axis',(0.,0.968648305440766,0.248436028721142));
#16202=DIRECTION('',(1.,0.,0.));
#16203=DIRECTION('center_axis',(-1.,0.,0.));
#16204=DIRECTION('ref_axis',(0.,0.968648305440766,0.248436028721142));
#16205=DIRECTION('',(1.,0.,0.));
#16206=DIRECTION('center_axis',(-1.,0.,0.));
#16207=DIRECTION('ref_axis',(0.,0.968648305440766,0.248436028721142));
#16208=DIRECTION('',(1.,0.,0.));
#16209=DIRECTION('center_axis',(-1.,0.,0.));
#16210=DIRECTION('ref_axis',(0.,0.968648305440766,0.248436028721142));
#16211=DIRECTION('',(1.,0.,0.));
#16212=DIRECTION('center_axis',(-1.,0.,0.));
#16213=DIRECTION('ref_axis',(0.,0.968648305440766,0.248436028721142));
#16214=DIRECTION('',(1.,0.,0.));
#16215=DIRECTION('center_axis',(-1.,0.,0.));
#16216=DIRECTION('ref_axis',(0.,0.968648305440766,0.248436028721142));
#16217=DIRECTION('',(1.,0.,0.));
#16218=DIRECTION('center_axis',(-1.,0.,0.));
#16219=DIRECTION('ref_axis',(0.,0.968648305440766,0.248436028721142));
#16220=DIRECTION('',(1.,0.,0.));
#16221=DIRECTION('center_axis',(-1.,0.,0.));
#16222=DIRECTION('ref_axis',(0.,0.968648305440766,0.248436028721142));
#16223=DIRECTION('',(1.,0.,0.));
#16224=DIRECTION('center_axis',(-1.,0.,0.));
#16225=DIRECTION('ref_axis',(0.,0.968648305440766,0.248436028721142));
#16226=DIRECTION('',(1.,0.,0.));
#16227=DIRECTION('center_axis',(-1.,0.,0.));
#16228=DIRECTION('ref_axis',(0.,0.968648305440766,0.248436028721142));
#16229=DIRECTION('',(1.,0.,0.));
#16230=DIRECTION('center_axis',(-1.,0.,0.));
#16231=DIRECTION('ref_axis',(0.,0.968648305440766,0.248436028721142));
#16232=DIRECTION('',(1.,0.,0.));
#16233=DIRECTION('center_axis',(-1.,0.,0.));
#16234=DIRECTION('ref_axis',(0.,0.968648305440766,0.248436028721142));
#16235=DIRECTION('',(1.,0.,0.));
#16236=DIRECTION('center_axis',(-1.,0.,0.));
#16237=DIRECTION('ref_axis',(0.,0.968648305440766,0.248436028721142));
#16238=DIRECTION('',(1.,0.,0.));
#16239=DIRECTION('center_axis',(-1.,0.,0.));
#16240=DIRECTION('ref_axis',(0.,0.968648305440766,0.248436028721142));
#16241=DIRECTION('',(1.,0.,0.));
#16242=DIRECTION('center_axis',(-1.,0.,0.));
#16243=DIRECTION('ref_axis',(0.,0.968648305440766,0.248436028721142));
#16244=DIRECTION('',(1.,0.,0.));
#16245=DIRECTION('center_axis',(-1.,0.,0.));
#16246=DIRECTION('ref_axis',(0.,0.968648305440766,0.248436028721142));
#16247=DIRECTION('',(1.,0.,0.));
#16248=DIRECTION('center_axis',(-1.,0.,0.));
#16249=DIRECTION('ref_axis',(0.,0.968648305440766,0.248436028721142));
#16250=DIRECTION('',(1.,0.,0.));
#16251=DIRECTION('center_axis',(-1.,0.,0.));
#16252=DIRECTION('ref_axis',(0.,0.968648305440766,0.248436028721142));
#16253=DIRECTION('',(1.,0.,0.));
#16254=DIRECTION('center_axis',(-1.,0.,0.));
#16255=DIRECTION('ref_axis',(0.,0.968648305440766,0.248436028721142));
#16256=DIRECTION('',(1.,0.,0.));
#16257=DIRECTION('center_axis',(-1.,0.,0.));
#16258=DIRECTION('ref_axis',(0.,0.968648305440766,0.248436028721142));
#16259=DIRECTION('',(1.,0.,0.));
#16260=DIRECTION('center_axis',(-1.,0.,0.));
#16261=DIRECTION('ref_axis',(0.,0.968648305440766,0.248436028721142));
#16262=DIRECTION('',(1.,0.,0.));
#16263=DIRECTION('center_axis',(-1.,0.,0.));
#16264=DIRECTION('ref_axis',(0.,0.968648305440766,0.248436028721142));
#16265=DIRECTION('',(1.,0.,0.));
#16266=DIRECTION('center_axis',(-1.,0.,0.));
#16267=DIRECTION('ref_axis',(0.,0.968648305440766,0.248436028721142));
#16268=DIRECTION('',(1.,0.,0.));
#16269=DIRECTION('center_axis',(-1.,0.,0.));
#16270=DIRECTION('ref_axis',(0.,0.968648305440766,0.248436028721142));
#16271=DIRECTION('',(1.,0.,0.));
#16272=DIRECTION('center_axis',(-1.,0.,0.));
#16273=DIRECTION('ref_axis',(0.,0.968648305440766,0.248436028721142));
#16274=DIRECTION('',(1.,0.,0.));
#16275=DIRECTION('center_axis',(-1.,0.,0.));
#16276=DIRECTION('ref_axis',(0.,0.968648305440766,0.248436028721142));
#16277=DIRECTION('',(1.,0.,0.));
#16278=DIRECTION('center_axis',(-1.,0.,0.));
#16279=DIRECTION('ref_axis',(0.,0.968648305440766,0.248436028721142));
#16280=DIRECTION('',(1.,0.,0.));
#16281=DIRECTION('center_axis',(-1.,0.,0.));
#16282=DIRECTION('ref_axis',(0.,0.968648305440766,0.248436028721142));
#16283=DIRECTION('',(1.,0.,0.));
#16284=DIRECTION('center_axis',(-1.,0.,0.));
#16285=DIRECTION('ref_axis',(0.,0.968648305440766,0.248436028721142));
#16286=DIRECTION('',(1.,0.,0.));
#16287=DIRECTION('center_axis',(-1.,0.,0.));
#16288=DIRECTION('ref_axis',(0.,0.968648305440766,0.248436028721142));
#16289=DIRECTION('',(1.,0.,0.));
#16290=DIRECTION('center_axis',(-1.,0.,0.));
#16291=DIRECTION('ref_axis',(0.,0.968648305440766,0.248436028721142));
#16292=DIRECTION('',(1.,0.,0.));
#16293=DIRECTION('center_axis',(-1.,0.,0.));
#16294=DIRECTION('ref_axis',(0.,0.968648305440766,0.248436028721142));
#16295=DIRECTION('',(1.,0.,0.));
#16296=DIRECTION('center_axis',(-1.,0.,0.));
#16297=DIRECTION('ref_axis',(0.,0.968648305440766,0.248436028721142));
#16298=DIRECTION('',(1.,0.,0.));
#16299=DIRECTION('center_axis',(-1.,0.,0.));
#16300=DIRECTION('ref_axis',(0.,0.968648305440766,0.248436028721142));
#16301=DIRECTION('',(1.,0.,0.));
#16302=DIRECTION('center_axis',(-1.,0.,0.));
#16303=DIRECTION('ref_axis',(0.,0.968648305440766,0.248436028721142));
#16304=DIRECTION('',(1.,0.,0.));
#16305=DIRECTION('center_axis',(-1.,0.,0.));
#16306=DIRECTION('ref_axis',(0.,0.968648305440766,0.248436028721142));
#16307=DIRECTION('',(1.,0.,0.));
#16308=DIRECTION('center_axis',(-1.,0.,0.));
#16309=DIRECTION('ref_axis',(0.,0.968648305440766,0.248436028721142));
#16310=DIRECTION('',(1.,0.,0.));
#16311=DIRECTION('center_axis',(-1.,0.,0.));
#16312=DIRECTION('ref_axis',(0.,0.968648305440766,0.248436028721142));
#16313=DIRECTION('',(1.,0.,0.));
#16314=DIRECTION('center_axis',(-1.,0.,0.));
#16315=DIRECTION('ref_axis',(0.,0.968648305440766,0.248436028721142));
#16316=DIRECTION('',(1.,0.,0.));
#16317=DIRECTION('center_axis',(-1.,0.,0.));
#16318=DIRECTION('ref_axis',(0.,0.968648305440766,0.248436028721142));
#16319=DIRECTION('',(1.,0.,0.));
#16320=DIRECTION('center_axis',(-1.,0.,0.));
#16321=DIRECTION('ref_axis',(0.,0.968648305440766,0.248436028721142));
#16322=DIRECTION('',(1.,0.,0.));
#16323=DIRECTION('center_axis',(-1.,0.,0.));
#16324=DIRECTION('ref_axis',(0.,0.968648305440766,0.248436028721142));
#16325=DIRECTION('',(1.,0.,0.));
#16326=DIRECTION('center_axis',(-1.,0.,0.));
#16327=DIRECTION('ref_axis',(0.,0.968648305440766,0.248436028721142));
#16328=DIRECTION('',(1.,0.,0.));
#16329=DIRECTION('center_axis',(-1.,0.,0.));
#16330=DIRECTION('ref_axis',(0.,0.968648305440766,0.248436028721142));
#16331=DIRECTION('',(1.,0.,0.));
#16332=DIRECTION('center_axis',(-1.,0.,0.));
#16333=DIRECTION('ref_axis',(0.,0.968648305440766,0.248436028721142));
#16334=DIRECTION('',(1.,0.,0.));
#16335=DIRECTION('center_axis',(-1.,0.,0.));
#16336=DIRECTION('ref_axis',(0.,0.968648305440766,0.248436028721142));
#16337=DIRECTION('',(1.,0.,0.));
#16338=DIRECTION('center_axis',(-1.,0.,0.));
#16339=DIRECTION('ref_axis',(0.,0.968648305440766,0.248436028721142));
#16340=DIRECTION('',(1.,0.,0.));
#16341=DIRECTION('center_axis',(-1.,0.,0.));
#16342=DIRECTION('ref_axis',(0.,0.968648305440766,0.248436028721142));
#16343=DIRECTION('',(1.,0.,0.));
#16344=DIRECTION('center_axis',(-1.,0.,0.));
#16345=DIRECTION('ref_axis',(0.,0.968648305440766,0.248436028721142));
#16346=DIRECTION('',(1.,0.,0.));
#16347=DIRECTION('center_axis',(-1.,0.,0.));
#16348=DIRECTION('ref_axis',(0.,0.968648305440766,0.248436028721142));
#16349=DIRECTION('',(1.,0.,0.));
#16350=DIRECTION('center_axis',(-1.,0.,0.));
#16351=DIRECTION('ref_axis',(0.,0.968648305440766,0.248436028721142));
#16352=DIRECTION('',(1.,0.,0.));
#16353=DIRECTION('center_axis',(-1.,0.,0.));
#16354=DIRECTION('ref_axis',(0.,0.968648305440766,0.248436028721142));
#16355=DIRECTION('',(1.,0.,0.));
#16356=DIRECTION('center_axis',(-1.,0.,0.));
#16357=DIRECTION('ref_axis',(0.,0.968648305440766,0.248436028721142));
#16358=DIRECTION('',(1.,0.,0.));
#16359=DIRECTION('center_axis',(-1.,0.,0.));
#16360=DIRECTION('ref_axis',(0.,0.968648305440766,0.248436028721142));
#16361=DIRECTION('',(1.,0.,0.));
#16362=DIRECTION('center_axis',(-1.,0.,0.));
#16363=DIRECTION('ref_axis',(0.,0.968648305440766,0.248436028721142));
#16364=DIRECTION('',(1.,0.,0.));
#16365=DIRECTION('center_axis',(-1.,0.,0.));
#16366=DIRECTION('ref_axis',(0.,0.968648305440766,0.248436028721142));
#16367=DIRECTION('',(1.,0.,0.));
#16368=DIRECTION('center_axis',(-1.,0.,0.));
#16369=DIRECTION('ref_axis',(0.,0.968648305440766,0.248436028721142));
#16370=DIRECTION('',(1.,0.,0.));
#16371=DIRECTION('center_axis',(-1.,0.,0.));
#16372=DIRECTION('ref_axis',(0.,0.968648305440766,0.248436028721142));
#16373=DIRECTION('',(1.,0.,0.));
#16374=DIRECTION('center_axis',(-1.,0.,0.));
#16375=DIRECTION('ref_axis',(0.,0.968648305440766,0.248436028721142));
#16376=DIRECTION('',(1.,0.,0.));
#16377=DIRECTION('center_axis',(-1.,0.,0.));
#16378=DIRECTION('ref_axis',(0.,0.968648305440766,0.248436028721142));
#16379=DIRECTION('',(1.,0.,0.));
#16380=DIRECTION('center_axis',(-1.,0.,0.));
#16381=DIRECTION('ref_axis',(0.,0.968648305440766,0.248436028721142));
#16382=DIRECTION('',(1.,0.,0.));
#16383=DIRECTION('center_axis',(-1.,0.,0.));
#16384=DIRECTION('ref_axis',(0.,0.968648305440766,0.248436028721142));
#16385=DIRECTION('',(1.,0.,0.));
#16386=DIRECTION('center_axis',(-1.,0.,0.));
#16387=DIRECTION('ref_axis',(0.,0.968648305440766,0.248436028721142));
#16388=DIRECTION('',(1.,0.,0.));
#16389=DIRECTION('center_axis',(-1.,0.,0.));
#16390=DIRECTION('ref_axis',(0.,0.968648305440766,0.248436028721142));
#16391=DIRECTION('',(1.,0.,0.));
#16392=DIRECTION('center_axis',(-1.,0.,0.));
#16393=DIRECTION('ref_axis',(0.,0.968648305440766,0.248436028721142));
#16394=DIRECTION('',(1.,0.,0.));
#16395=DIRECTION('center_axis',(-1.,0.,0.));
#16396=DIRECTION('ref_axis',(0.,0.968648305440766,0.248436028721142));
#16397=DIRECTION('',(1.,0.,0.));
#16398=DIRECTION('center_axis',(-1.,0.,0.));
#16399=DIRECTION('ref_axis',(0.,0.968648305440766,0.248436028721142));
#16400=DIRECTION('',(1.,0.,0.));
#16401=DIRECTION('center_axis',(-1.,0.,0.));
#16402=DIRECTION('ref_axis',(0.,0.968648305440766,0.248436028721142));
#16403=DIRECTION('',(1.,0.,0.));
#16404=DIRECTION('center_axis',(-1.,0.,0.));
#16405=DIRECTION('ref_axis',(0.,0.968648305440766,0.248436028721142));
#16406=DIRECTION('',(1.,0.,0.));
#16407=DIRECTION('center_axis',(-1.,0.,0.));
#16408=DIRECTION('ref_axis',(0.,0.968648305440766,0.248436028721142));
#16409=DIRECTION('',(1.,0.,0.));
#16410=DIRECTION('center_axis',(-1.,0.,0.));
#16411=DIRECTION('ref_axis',(0.,0.968648305440766,0.248436028721142));
#16412=DIRECTION('',(1.,0.,0.));
#16413=DIRECTION('center_axis',(-1.,0.,0.));
#16414=DIRECTION('ref_axis',(0.,0.968648305440766,0.248436028721142));
#16415=DIRECTION('',(1.,0.,0.));
#16416=DIRECTION('center_axis',(-1.,0.,0.));
#16417=DIRECTION('ref_axis',(0.,0.968648305440766,0.248436028721142));
#16418=DIRECTION('',(1.,0.,0.));
#16419=DIRECTION('center_axis',(-1.,0.,0.));
#16420=DIRECTION('ref_axis',(0.,0.968648305440766,0.248436028721142));
#16421=DIRECTION('',(1.,0.,0.));
#16422=DIRECTION('center_axis',(-1.,0.,0.));
#16423=DIRECTION('ref_axis',(0.,0.968648305440766,0.248436028721142));
#16424=DIRECTION('',(1.,0.,0.));
#16425=DIRECTION('center_axis',(-1.,0.,0.));
#16426=DIRECTION('ref_axis',(0.,0.968648305440766,0.248436028721142));
#16427=DIRECTION('',(1.,0.,0.));
#16428=DIRECTION('center_axis',(-1.,0.,0.));
#16429=DIRECTION('ref_axis',(0.,0.968648305440766,0.248436028721142));
#16430=DIRECTION('',(1.,0.,0.));
#16431=DIRECTION('center_axis',(-1.,0.,0.));
#16432=DIRECTION('ref_axis',(0.,0.968648305440766,0.248436028721142));
#16433=DIRECTION('',(1.,0.,0.));
#16434=DIRECTION('center_axis',(-1.,0.,0.));
#16435=DIRECTION('ref_axis',(0.,0.968648305440766,0.248436028721142));
#16436=DIRECTION('',(1.,0.,0.));
#16437=DIRECTION('center_axis',(-1.,0.,0.));
#16438=DIRECTION('ref_axis',(0.,0.968648305440766,0.248436028721142));
#16439=DIRECTION('',(1.,0.,0.));
#16440=DIRECTION('center_axis',(-1.,0.,0.));
#16441=DIRECTION('ref_axis',(0.,0.968648305440766,0.248436028721142));
#16442=DIRECTION('',(1.,0.,0.));
#16443=DIRECTION('center_axis',(-1.,0.,0.));
#16444=DIRECTION('ref_axis',(0.,0.968648305440766,0.248436028721142));
#16445=DIRECTION('',(1.,0.,0.));
#16446=DIRECTION('center_axis',(-1.,0.,0.));
#16447=DIRECTION('ref_axis',(0.,0.968648305440766,0.248436028721142));
#16448=DIRECTION('',(1.,0.,0.));
#16449=DIRECTION('center_axis',(-1.,0.,0.));
#16450=DIRECTION('ref_axis',(0.,0.968648305440766,0.248436028721142));
#16451=DIRECTION('',(1.,0.,0.));
#16452=DIRECTION('center_axis',(-1.,0.,0.));
#16453=DIRECTION('ref_axis',(0.,0.968648305440766,0.248436028721142));
#16454=DIRECTION('',(1.,0.,0.));
#16455=DIRECTION('center_axis',(-1.,0.,0.));
#16456=DIRECTION('ref_axis',(0.,0.968648305440766,0.248436028721142));
#16457=DIRECTION('',(1.,0.,0.));
#16458=DIRECTION('center_axis',(-1.,0.,0.));
#16459=DIRECTION('ref_axis',(0.,0.968648305440766,0.248436028721142));
#16460=DIRECTION('',(1.,0.,0.));
#16461=DIRECTION('center_axis',(-1.,0.,0.));
#16462=DIRECTION('ref_axis',(0.,0.968648305440766,0.248436028721142));
#16463=DIRECTION('',(1.,0.,0.));
#16464=DIRECTION('center_axis',(-1.,0.,0.));
#16465=DIRECTION('ref_axis',(0.,0.968648305440766,0.248436028721142));
#16466=DIRECTION('',(1.,0.,0.));
#16467=DIRECTION('center_axis',(-1.,0.,0.));
#16468=DIRECTION('ref_axis',(0.,0.968648305440766,0.248436028721142));
#16469=DIRECTION('',(1.,0.,0.));
#16470=DIRECTION('center_axis',(-1.,0.,0.));
#16471=DIRECTION('ref_axis',(0.,0.968648305440766,0.248436028721142));
#16472=DIRECTION('',(1.,0.,0.));
#16473=DIRECTION('center_axis',(-1.,0.,0.));
#16474=DIRECTION('ref_axis',(0.,0.968648305440766,0.248436028721142));
#16475=DIRECTION('',(1.,0.,0.));
#16476=DIRECTION('center_axis',(-1.,0.,0.));
#16477=DIRECTION('ref_axis',(0.,0.968648305440766,0.248436028721142));
#16478=DIRECTION('',(1.,0.,0.));
#16479=DIRECTION('center_axis',(-1.,0.,0.));
#16480=DIRECTION('ref_axis',(0.,0.968648305440766,0.248436028721142));
#16481=DIRECTION('',(1.,0.,0.));
#16482=DIRECTION('center_axis',(-1.,0.,0.));
#16483=DIRECTION('ref_axis',(0.,0.968648305440766,0.248436028721142));
#16484=DIRECTION('',(1.,0.,0.));
#16485=DIRECTION('center_axis',(-1.,0.,0.));
#16486=DIRECTION('ref_axis',(0.,0.968648305440766,0.248436028721142));
#16487=DIRECTION('',(1.,0.,0.));
#16488=DIRECTION('center_axis',(-1.,0.,0.));
#16489=DIRECTION('ref_axis',(0.,0.968648305440766,0.248436028721142));
#16490=DIRECTION('',(1.,0.,0.));
#16491=DIRECTION('center_axis',(-1.,0.,0.));
#16492=DIRECTION('ref_axis',(0.,0.968648305440766,0.248436028721142));
#16493=DIRECTION('',(1.,0.,0.));
#16494=DIRECTION('center_axis',(-1.,0.,0.));
#16495=DIRECTION('ref_axis',(0.,0.968648305440766,0.248436028721142));
#16496=DIRECTION('',(1.,0.,0.));
#16497=DIRECTION('center_axis',(-1.,0.,0.));
#16498=DIRECTION('ref_axis',(0.,0.968648305440766,0.248436028721142));
#16499=DIRECTION('',(1.,0.,0.));
#16500=DIRECTION('center_axis',(-1.,0.,0.));
#16501=DIRECTION('ref_axis',(0.,0.968648305440766,0.248436028721142));
#16502=DIRECTION('',(1.,0.,0.));
#16503=DIRECTION('center_axis',(-1.,0.,0.));
#16504=DIRECTION('ref_axis',(0.,0.968648305440766,0.248436028721142));
#16505=DIRECTION('',(1.,0.,0.));
#16506=DIRECTION('center_axis',(-1.,0.,0.));
#16507=DIRECTION('ref_axis',(0.,0.968648305440766,0.248436028721142));
#16508=DIRECTION('',(1.,0.,0.));
#16509=DIRECTION('center_axis',(-1.,0.,0.));
#16510=DIRECTION('ref_axis',(0.,0.968648305440766,0.248436028721142));
#16511=DIRECTION('',(1.,0.,0.));
#16512=DIRECTION('center_axis',(-1.,0.,0.));
#16513=DIRECTION('ref_axis',(0.,0.968648305440766,0.248436028721142));
#16514=DIRECTION('',(1.,0.,0.));
#16515=DIRECTION('center_axis',(-1.,0.,0.));
#16516=DIRECTION('ref_axis',(0.,0.968648305440766,0.248436028721142));
#16517=DIRECTION('',(1.,0.,0.));
#16518=DIRECTION('center_axis',(-1.,0.,0.));
#16519=DIRECTION('ref_axis',(0.,0.968648305440766,0.248436028721142));
#16520=DIRECTION('',(1.,0.,0.));
#16521=DIRECTION('center_axis',(-1.,0.,0.));
#16522=DIRECTION('ref_axis',(0.,0.968648305440766,0.248436028721142));
#16523=DIRECTION('',(1.,0.,0.));
#16524=DIRECTION('center_axis',(-1.,0.,0.));
#16525=DIRECTION('ref_axis',(0.,0.968648305440766,0.248436028721142));
#16526=DIRECTION('',(1.,0.,0.));
#16527=DIRECTION('center_axis',(-1.,0.,0.));
#16528=DIRECTION('ref_axis',(0.,0.968648305440766,0.248436028721142));
#16529=DIRECTION('',(1.,0.,0.));
#16530=DIRECTION('center_axis',(-1.,0.,0.));
#16531=DIRECTION('ref_axis',(0.,0.968648305440766,0.248436028721142));
#16532=DIRECTION('',(1.,0.,0.));
#16533=DIRECTION('center_axis',(-1.,0.,0.));
#16534=DIRECTION('ref_axis',(0.,0.968648305440766,0.248436028721142));
#16535=DIRECTION('',(1.,0.,0.));
#16536=DIRECTION('center_axis',(-1.,0.,0.));
#16537=DIRECTION('ref_axis',(0.,0.968648305440766,0.248436028721142));
#16538=DIRECTION('',(1.,0.,0.));
#16539=DIRECTION('center_axis',(-1.,0.,0.));
#16540=DIRECTION('ref_axis',(0.,0.968648305440766,0.248436028721142));
#16541=DIRECTION('',(1.,0.,0.));
#16542=DIRECTION('center_axis',(-1.,0.,0.));
#16543=DIRECTION('ref_axis',(0.,0.968648305440766,0.248436028721142));
#16544=DIRECTION('',(1.,0.,0.));
#16545=DIRECTION('center_axis',(-1.,0.,0.));
#16546=DIRECTION('ref_axis',(0.,0.968648305440766,0.248436028721142));
#16547=DIRECTION('',(1.,0.,0.));
#16548=DIRECTION('center_axis',(-1.,0.,0.));
#16549=DIRECTION('ref_axis',(0.,0.968648305440766,0.248436028721142));
#16550=DIRECTION('',(1.,0.,0.));
#16551=DIRECTION('center_axis',(-1.,0.,0.));
#16552=DIRECTION('ref_axis',(0.,0.968648305440766,0.248436028721142));
#16553=DIRECTION('',(1.,0.,0.));
#16554=DIRECTION('center_axis',(-1.,0.,0.));
#16555=DIRECTION('ref_axis',(0.,0.968648305440766,0.248436028721142));
#16556=DIRECTION('',(1.,0.,0.));
#16557=DIRECTION('center_axis',(-1.,0.,0.));
#16558=DIRECTION('ref_axis',(0.,0.968648305440766,0.248436028721142));
#16559=DIRECTION('',(1.,0.,0.));
#16560=DIRECTION('center_axis',(-1.,0.,0.));
#16561=DIRECTION('ref_axis',(0.,0.968648305440766,0.248436028721142));
#16562=DIRECTION('',(1.,0.,0.));
#16563=DIRECTION('center_axis',(-1.,0.,0.));
#16564=DIRECTION('ref_axis',(0.,0.968648305440766,0.248436028721142));
#16565=DIRECTION('',(1.,0.,0.));
#16566=DIRECTION('center_axis',(-1.,0.,0.));
#16567=DIRECTION('ref_axis',(0.,0.968648305440766,0.248436028721142));
#16568=DIRECTION('',(1.,0.,0.));
#16569=DIRECTION('center_axis',(-1.,0.,0.));
#16570=DIRECTION('ref_axis',(0.,0.968648305440766,0.248436028721142));
#16571=DIRECTION('',(1.,0.,0.));
#16572=DIRECTION('center_axis',(-1.,0.,0.));
#16573=DIRECTION('ref_axis',(0.,0.968648305440766,0.248436028721142));
#16574=DIRECTION('',(1.,0.,0.));
#16575=DIRECTION('center_axis',(-1.,0.,0.));
#16576=DIRECTION('ref_axis',(0.,0.968648305440766,0.248436028721142));
#16577=DIRECTION('',(1.,0.,0.));
#16578=DIRECTION('center_axis',(-1.,0.,0.));
#16579=DIRECTION('ref_axis',(0.,0.968648305440766,0.248436028721142));
#16580=DIRECTION('',(1.,0.,0.));
#16581=DIRECTION('center_axis',(-1.,0.,0.));
#16582=DIRECTION('ref_axis',(0.,0.968648305440766,0.248436028721142));
#16583=DIRECTION('',(1.,0.,0.));
#16584=DIRECTION('center_axis',(-1.,0.,0.));
#16585=DIRECTION('ref_axis',(0.,0.968648305440766,0.248436028721142));
#16586=DIRECTION('',(1.,0.,0.));
#16587=DIRECTION('center_axis',(-1.,0.,0.));
#16588=DIRECTION('ref_axis',(0.,0.968648305440766,0.248436028721142));
#16589=DIRECTION('',(1.,0.,0.));
#16590=DIRECTION('center_axis',(-1.,0.,0.));
#16591=DIRECTION('ref_axis',(0.,0.968648305440766,0.248436028721142));
#16592=DIRECTION('',(1.,0.,0.));
#16593=DIRECTION('center_axis',(-1.,0.,0.));
#16594=DIRECTION('ref_axis',(0.,0.968648305440766,0.248436028721142));
#16595=DIRECTION('',(1.,0.,0.));
#16596=DIRECTION('center_axis',(-1.,0.,0.));
#16597=DIRECTION('ref_axis',(0.,0.968648305440766,0.248436028721142));
#16598=DIRECTION('',(1.,0.,0.));
#16599=DIRECTION('center_axis',(-1.,0.,0.));
#16600=DIRECTION('ref_axis',(0.,0.968648305440766,0.248436028721142));
#16601=DIRECTION('',(1.,0.,0.));
#16602=DIRECTION('center_axis',(-1.,0.,0.));
#16603=DIRECTION('ref_axis',(0.,0.968648305440766,0.248436028721142));
#16604=DIRECTION('',(1.,0.,0.));
#16605=DIRECTION('center_axis',(-1.,0.,0.));
#16606=DIRECTION('ref_axis',(0.,0.968648305440766,0.248436028721142));
#16607=DIRECTION('',(1.,0.,0.));
#16608=DIRECTION('center_axis',(-1.,0.,0.));
#16609=DIRECTION('ref_axis',(0.,0.968648305440766,0.248436028721142));
#16610=DIRECTION('',(1.,0.,0.));
#16611=DIRECTION('center_axis',(-1.,0.,0.));
#16612=DIRECTION('ref_axis',(0.,0.968648305440766,0.248436028721142));
#16613=DIRECTION('',(1.,0.,0.));
#16614=DIRECTION('center_axis',(-1.,0.,0.));
#16615=DIRECTION('ref_axis',(0.,0.968648305440766,0.248436028721142));
#16616=DIRECTION('',(1.,0.,0.));
#16617=DIRECTION('center_axis',(-1.,0.,0.));
#16618=DIRECTION('ref_axis',(0.,0.968648305440766,0.248436028721142));
#16619=DIRECTION('',(1.,0.,0.));
#16620=DIRECTION('center_axis',(-1.,0.,0.));
#16621=DIRECTION('ref_axis',(0.,0.968648305440766,0.248436028721142));
#16622=DIRECTION('',(1.,0.,0.));
#16623=DIRECTION('center_axis',(-1.,0.,0.));
#16624=DIRECTION('ref_axis',(0.,0.968648305440766,0.248436028721142));
#16625=DIRECTION('',(1.,0.,0.));
#16626=DIRECTION('center_axis',(-1.,0.,0.));
#16627=DIRECTION('ref_axis',(0.,0.968648305440766,0.248436028721142));
#16628=DIRECTION('',(1.,0.,0.));
#16629=DIRECTION('center_axis',(-1.,0.,0.));
#16630=DIRECTION('ref_axis',(0.,0.968648305440766,0.248436028721142));
#16631=DIRECTION('',(1.,0.,0.));
#16632=DIRECTION('center_axis',(-1.,0.,0.));
#16633=DIRECTION('ref_axis',(0.,0.968648305440766,0.248436028721142));
#16634=DIRECTION('',(1.,0.,0.));
#16635=DIRECTION('center_axis',(-1.,0.,0.));
#16636=DIRECTION('ref_axis',(0.,0.968648305440766,0.248436028721142));
#16637=DIRECTION('',(1.,0.,0.));
#16638=DIRECTION('center_axis',(-1.,0.,0.));
#16639=DIRECTION('ref_axis',(0.,0.968648305440766,0.248436028721142));
#16640=DIRECTION('',(1.,0.,0.));
#16641=DIRECTION('center_axis',(-1.,0.,0.));
#16642=DIRECTION('ref_axis',(0.,0.968648305440766,0.248436028721142));
#16643=DIRECTION('',(1.,0.,0.));
#16644=DIRECTION('center_axis',(-1.,0.,0.));
#16645=DIRECTION('ref_axis',(0.,0.968648305440766,0.248436028721142));
#16646=DIRECTION('',(1.,0.,0.));
#16647=DIRECTION('center_axis',(-1.,0.,0.));
#16648=DIRECTION('ref_axis',(0.,0.968648305440766,0.248436028721142));
#16649=DIRECTION('',(1.,0.,0.));
#16650=DIRECTION('center_axis',(-1.,0.,0.));
#16651=DIRECTION('ref_axis',(0.,0.968648305440766,0.248436028721142));
#16652=DIRECTION('',(1.,0.,0.));
#16653=DIRECTION('center_axis',(-1.,0.,0.));
#16654=DIRECTION('ref_axis',(0.,0.968648305440766,0.248436028721142));
#16655=DIRECTION('',(1.,0.,0.));
#16656=DIRECTION('center_axis',(-1.,0.,0.));
#16657=DIRECTION('ref_axis',(0.,1.,0.));
#16658=DIRECTION('center_axis',(-1.,0.,0.));
#16659=DIRECTION('ref_axis',(0.,1.,0.));
#16660=DIRECTION('center_axis',(-1.,0.,0.));
#16661=DIRECTION('ref_axis',(0.,1.,0.));
#16662=DIRECTION('center_axis',(-1.,0.,0.));
#16663=DIRECTION('ref_axis',(0.,0.968648305440766,0.248436028721142));
#16664=DIRECTION('center_axis',(-1.,0.,0.));
#16665=DIRECTION('ref_axis',(0.,1.,-2.30250085928462E-11));
#16666=DIRECTION('center_axis',(1.,0.,0.));
#16667=DIRECTION('ref_axis',(0.,1.,0.));
#16668=DIRECTION('center_axis',(1.,0.,0.));
#16669=DIRECTION('ref_axis',(0.,1.,0.));
#16670=DIRECTION('center_axis',(1.,0.,0.));
#16671=DIRECTION('ref_axis',(0.,1.,0.));
#16672=DIRECTION('center_axis',(1.,0.,0.));
#16673=DIRECTION('ref_axis',(0.,1.,0.));
#16674=DIRECTION('',(-1.,0.,0.));
#16675=DIRECTION('center_axis',(1.,0.,0.));
#16676=DIRECTION('ref_axis',(0.,1.,0.));
#16677=DIRECTION('center_axis',(1.,0.,0.));
#16678=DIRECTION('ref_axis',(0.,1.,0.));
#16679=DIRECTION('center_axis',(0.,-1.,0.));
#16680=DIRECTION('ref_axis',(0.,0.,1.));
#16681=DIRECTION('',(0.,0.,1.));
#16682=DIRECTION('',(1.,0.,0.));
#16683=DIRECTION('',(0.,0.,1.));
#16684=DIRECTION('',(-1.,0.,0.));
#16685=DIRECTION('center_axis',(1.,0.,0.));
#16686=DIRECTION('ref_axis',(0.,1.,0.));
#16687=DIRECTION('center_axis',(-1.,0.,0.));
#16688=DIRECTION('ref_axis',(0.,1.,0.));
#16689=DIRECTION('center_axis',(0.,1.,0.));
#16690=DIRECTION('ref_axis',(0.,0.,-1.));
#16691=DIRECTION('',(0.,0.,-1.));
#16692=DIRECTION('',(1.,0.,0.));
#16693=DIRECTION('',(0.,0.,-1.));
#16694=DIRECTION('',(-1.,0.,0.));
#16695=DIRECTION('center_axis',(1.,0.,0.));
#16696=DIRECTION('ref_axis',(0.,1.,0.));
#16697=DIRECTION('center_axis',(-1.,0.,0.));
#16698=DIRECTION('ref_axis',(0.,1.,0.));
#16699=DIRECTION('center_axis',(-1.,0.,0.));
#16700=DIRECTION('ref_axis',(0.,1.,0.));
#16701=DIRECTION('center_axis',(1.,0.,0.));
#16702=DIRECTION('ref_axis',(0.,1.,0.));
#16703=DIRECTION('',(-1.,0.,0.));
#16704=DIRECTION('center_axis',(1.,0.,0.));
#16705=DIRECTION('ref_axis',(0.,1.,0.));
#16706=DIRECTION('center_axis',(1.,0.,0.));
#16707=DIRECTION('ref_axis',(0.,1.,0.));
#16708=DIRECTION('center_axis',(1.,0.,0.));
#16709=DIRECTION('ref_axis',(0.,1.,0.));
#16710=DIRECTION('center_axis',(1.,0.,0.));
#16711=DIRECTION('ref_axis',(0.,1.,0.));
#17629=CARTESIAN_POINT('',(0.,0.,0.));
#17630=CARTESIAN_POINT('Origin',(213.235140564004,0.,130.804360617566));
#17631=CARTESIAN_POINT('',(208.584593534951,-4.76405452823405,129.582490119308));
#17632=CARTESIAN_POINT('',(208.930233502018,-4.76405452823405,129.582490119308));
#17633=CARTESIAN_POINT('',(213.235140564004,-4.76405452823405,129.582490119308));
#17634=CARTESIAN_POINT('',(209.999775289582,-2.85698121911692,134.807714383612));
#17635=CARTESIAN_POINT('Ctrl Pts',(209.999775289582,-2.85698121911692,134.807714383612));
#17636=CARTESIAN_POINT('Ctrl Pts',(209.992142339133,-2.74793414685712,134.885535494523));
#17637=CARTESIAN_POINT('Ctrl Pts',(209.984509388684,-2.6354991820663,134.95904446143));
#17638=CARTESIAN_POINT('Ctrl Pts',(209.976876438235,-2.52005924303919,135.027923624563));
#17639=CARTESIAN_POINT('Ctrl Pts',(209.969253020602,-2.40476347730548,135.096716764298));
#17640=CARTESIAN_POINT('Ctrl Pts',(209.961629602968,-2.28647054353313,135.160891390807));
#17641=CARTESIAN_POINT('Ctrl Pts',(209.954006185334,-2.16559535772989,135.220170827378));
#17642=CARTESIAN_POINT('Ctrl Pts',(209.946390314966,-2.04483983966827,135.279391576665));
#17643=CARTESIAN_POINT('Ctrl Pts',(209.938774444599,-1.92150751515212,135.333726595951));
#17644=CARTESIAN_POINT('Ctrl Pts',(209.931158574231,-1.79604065581658,135.38294347967));
#17645=CARTESIAN_POINT('Ctrl Pts',(209.923241190819,-1.66560655139177,135.434108864574));
#17646=CARTESIAN_POINT('Ctrl Pts',(209.915323807407,-1.53286579519913,135.47974227831));
#17647=CARTESIAN_POINT('Ctrl Pts',(209.907406423995,-1.39834203382079,135.519636072823));
#17648=CARTESIAN_POINT('Ctrl Pts',(209.899799007078,-1.26908489356805,135.557968020575));
#17649=CARTESIAN_POINT('Ctrl Pts',(209.892191590161,-1.13818215001209,135.591001152623));
#17650=CARTESIAN_POINT('Ctrl Pts',(209.884584173243,-1.00611629719668,135.618601269945));
#17651=CARTESIAN_POINT('Ctrl Pts',(209.876977848994,-0.874069413258891,
135.646197423007));
#17652=CARTESIAN_POINT('Ctrl Pts',(209.869371524745,-0.740860149380113,
135.668362029476));
#17653=CARTESIAN_POINT('Ctrl Pts',(209.861765200496,-0.606982515147129,
135.685011730769));
#17654=CARTESIAN_POINT('Ctrl Pts',(209.854158190768,-0.473092815912997,
135.701662932526));
#17655=CARTESIAN_POINT('Ctrl Pts',(209.84655118104,-0.338535029477726,135.712798191257));
#17656=CARTESIAN_POINT('Ctrl Pts',(209.838944171311,-0.203809027959443,
135.718385947438));
#17657=CARTESIAN_POINT('Ctrl Pts',(209.831334697465,-0.069039385009203,
135.723975513646));
#17658=CARTESIAN_POINT('Ctrl Pts',(209.823725223619,0.0658981760508359,
135.724013988275));
#17659=CARTESIAN_POINT('Ctrl Pts',(209.816115749772,0.200503645000317,135.718521924528));
#17660=CARTESIAN_POINT('Ctrl Pts',(209.808497878904,0.335257650513392,135.713023800312));
#17661=CARTESIAN_POINT('Ctrl Pts',(209.800880008035,0.469678427016586,135.70198297531));
#17662=CARTESIAN_POINT('Ctrl Pts',(209.793262137167,0.603270740406474,135.68547191278));
#17663=CARTESIAN_POINT('Ctrl Pts',(209.785639287196,0.736950370812096,135.668950058486));
#17664=CARTESIAN_POINT('Ctrl Pts',(209.778016437226,0.86980006175104,135.646950918129));
#17665=CARTESIAN_POINT('Ctrl Pts',(209.770393587255,1.0013360320228,135.619597809385));
#17666=CARTESIAN_POINT('Ctrl Pts',(209.762759835517,1.13306011758494,135.592205581774));
#17667=CARTESIAN_POINT('Ctrl Pts',(209.755126083778,1.26346634291021,135.55944420817));
#17668=CARTESIAN_POINT('Ctrl Pts',(209.74749233204,1.3920871137774,135.521486493579));
#17669=CARTESIAN_POINT('Ctrl Pts',(209.745375345476,1.42775613382599,135.510960087357));
#17670=CARTESIAN_POINT('Ctrl Pts',(209.743258358912,1.4632879682488,135.500034332974));
#17671=CARTESIAN_POINT('Ctrl Pts',(209.741141372347,1.49867295217247,135.488713555265));
#17672=CARTESIAN_POINT('Ctrl Pts',(209.733353704104,1.62884218435411,135.44706829282));
#17673=CARTESIAN_POINT('Ctrl Pts',(209.72556603586,1.75747564403554,135.399928764541));
#17674=CARTESIAN_POINT('Ctrl Pts',(209.717778367616,1.88407583976038,135.347425804478));
#17675=CARTESIAN_POINT('Ctrl Pts',(209.710000228288,2.01052112871054,135.294987086528));
#17676=CARTESIAN_POINT('Ctrl Pts',(209.70222208896,2.13493774786161,135.237198143303));
#17677=CARTESIAN_POINT('Ctrl Pts',(209.694443949632,2.25684297289465,135.174239661452));
#17678=CARTESIAN_POINT('Ctrl Pts',(209.686673485267,2.37862790975512,135.111343302949));
#17679=CARTESIAN_POINT('Ctrl Pts',(209.678903020903,2.49790604053664,135.043287735315));
#17680=CARTESIAN_POINT('Ctrl Pts',(209.671132556538,2.61421457479356,134.970301714058));
#17681=CARTESIAN_POINT('Ctrl Pts',(209.663367919743,2.73043588183068,134.897370429692));
#17682=CARTESIAN_POINT('Ctrl Pts',(209.655603282947,2.84369169700696,134.819516258395));
#17683=CARTESIAN_POINT('Ctrl Pts',(209.647838646152,2.95354411037853,134.737013697937));
#17684=CARTESIAN_POINT('Ctrl Pts',(209.640077319747,3.06334968905691,134.654546311782));
#17685=CARTESIAN_POINT('Ctrl Pts',(209.632315993341,3.16975444150301,134.567434711988));
#17686=CARTESIAN_POINT('Ctrl Pts',(209.624554666936,3.27234990255257,134.475996380787));
#17687=CARTESIAN_POINT('Ctrl Pts',(209.616794973343,3.37492377977697,134.384577286197));
#17688=CARTESIAN_POINT('Ctrl Pts',(209.60903527975,3.47368966925553,134.288833529858));
#17689=CARTESIAN_POINT('Ctrl Pts',(209.601275586157,3.56827293312915,134.189122254254));
#17690=CARTESIAN_POINT('Ctrl Pts',(209.593515860863,3.662856583417,134.089410571287));
#17691=CARTESIAN_POINT('Ctrl Pts',(209.585756135568,3.75325730596229,133.985731619193));
#17692=CARTESIAN_POINT('Ctrl Pts',(209.577996410273,3.83913828939138,133.878478419055));
#17693=CARTESIAN_POINT('Ctrl Pts',(209.570234989105,3.92503804195145,133.771201778926));
#17694=CARTESIAN_POINT('Ctrl Pts',(209.562473567936,4.00641584635018,133.660349640188));
#17695=CARTESIAN_POINT('Ctrl Pts',(209.554712146768,4.08297628367845,133.546346709693));
#17696=CARTESIAN_POINT('Ctrl Pts',(209.546942629375,4.15961658401883,133.432224858542));
#17697=CARTESIAN_POINT('Ctrl Pts',(209.539173111982,4.2314292613647,133.314945973776));
#17698=CARTESIAN_POINT('Ctrl Pts',(209.53140359459,4.29816293429022,133.194962728498));
#17699=CARTESIAN_POINT('Ctrl Pts',(209.523629992291,4.36493169314774,133.074916400764));
#17700=CARTESIAN_POINT('Ctrl Pts',(209.515856389993,4.42661595131892,132.95216322687));
#17701=CARTESIAN_POINT('Ctrl Pts',(209.508082787694,4.48301157575842,132.827178027545));
#17702=CARTESIAN_POINT('Ctrl Pts',(209.50029695563,4.539495924226,132.701996196116));
#17703=CARTESIAN_POINT('Ctrl Pts',(209.492511123565,4.59067486682162,132.574575683597));
#17704=CARTESIAN_POINT('Ctrl Pts',(209.4847252915,4.63639315079776,132.445409554599));
#17705=CARTESIAN_POINT('Ctrl Pts',(209.477381443845,4.67951610924217,132.323575900122));
#17706=CARTESIAN_POINT('Ctrl Pts',(209.470037596189,4.71778115993259,132.200189593167));
#17707=CARTESIAN_POINT('Ctrl Pts',(209.462693748534,4.75109968643114,132.075672865636));
#17708=CARTESIAN_POINT('Ctrl Pts',(209.454909765657,4.78641507584487,131.943693538115));
#17709=CARTESIAN_POINT('Ctrl Pts',(209.447125782781,4.81628128369982,131.810038662946));
#17710=CARTESIAN_POINT('Ctrl Pts',(209.439341799904,4.84053990021811,131.675197305411));
#17711=CARTESIAN_POINT('Ctrl Pts',(209.431567219374,4.86476921452188,131.540518824038));
#17712=CARTESIAN_POINT('Ctrl Pts',(209.423792638845,4.88340434715897,131.404657092206));
#17713=CARTESIAN_POINT('Ctrl Pts',(209.416018058316,4.89633682733635,131.268115656104));
#17714=CARTESIAN_POINT('Ctrl Pts',(209.408251022624,4.90925675719497,131.13170672657));
#17715=CARTESIAN_POINT('Ctrl Pts',(209.400483986932,4.91648501195897,130.994619791219));
#17716=CARTESIAN_POINT('Ctrl Pts',(209.39271695124,4.91796434783536,130.857367559755));
#17717=CARTESIAN_POINT('Ctrl Pts',(209.384955609346,4.91944259925179,130.720215944083));
#17718=CARTESIAN_POINT('Ctrl Pts',(209.377194267452,4.91518031659135,130.582899661805));
#17719=CARTESIAN_POINT('Ctrl Pts',(209.369432925558,4.90517219417271,130.44593516086));
#17720=CARTESIAN_POINT('Ctrl Pts',(209.361674676742,4.89516806022735,130.309025243505));
#17721=CARTESIAN_POINT('Ctrl Pts',(209.353916427926,4.8794226688716,130.172467216696));
#17722=CARTESIAN_POINT('Ctrl Pts',(209.34615817911,4.85798279483743,130.036775946299));
#17723=CARTESIAN_POINT('Ctrl Pts',(209.33840142992,4.83654706500869,129.901110904251));
#17724=CARTESIAN_POINT('Ctrl Pts',(209.330644680729,4.80941910276508,129.766312670191));
#17725=CARTESIAN_POINT('Ctrl Pts',(209.322887931538,4.77669732786597,129.632889021471));
#17726=CARTESIAN_POINT('Ctrl Pts',(209.315131013878,4.74397484227869,129.499462474906));
#17727=CARTESIAN_POINT('Ctrl Pts',(209.307374096217,4.70565839487186,129.367410951764));
#17728=CARTESIAN_POINT('Ctrl Pts',(209.299617178557,4.66189702139654,129.237229728204));
#17729=CARTESIAN_POINT('Ctrl Pts',(209.291858424581,4.61812528817876,129.107017686507));
#17730=CARTESIAN_POINT('Ctrl Pts',(209.284099670606,4.56890618792866,128.978677194934));
#17731=CARTESIAN_POINT('Ctrl Pts',(209.27634091663,4.51443776230667,128.852685759205));
#17732=CARTESIAN_POINT('Ctrl Pts',(209.268573827102,4.45991081898621,128.726558965628));
#17733=CARTESIAN_POINT('Ctrl Pts',(209.260806737574,4.40012343960792,128.602786627605));
#17734=CARTESIAN_POINT('Ctrl Pts',(209.253039648046,4.33532097135991,128.481824258801));
#17735=CARTESIAN_POINT('Ctrl Pts',(209.245268346918,4.27048336484057,128.36079629977));
#17736=CARTESIAN_POINT('Ctrl Pts',(209.237497045789,4.20062544887419,128.242581681554));
#17737=CARTESIAN_POINT('Ctrl Pts',(209.229725744661,4.12603669423767,128.127608058904));
#17738=CARTESIAN_POINT('Ctrl Pts',(209.221941972209,4.05132824014885,128.01244992748));
#17739=CARTESIAN_POINT('Ctrl Pts',(209.214158199757,3.97187400192915,127.900543503149));
#17740=CARTESIAN_POINT('Ctrl Pts',(209.206374427305,3.88800517419154,127.792285115863));
#17741=CARTESIAN_POINT('Ctrl Pts',(209.198998326444,3.80852893868575,127.68969671305));
#17742=CARTESIAN_POINT('Ctrl Pts',(209.191622225582,3.72508894865644,127.590384153448));
#17743=CARTESIAN_POINT('Ctrl Pts',(209.184246124721,3.63799708228773,127.494653637822));
#17744=CARTESIAN_POINT('Ctrl Pts',(209.176480887067,3.54631055945193,127.393872721383));
#17745=CARTESIAN_POINT('Ctrl Pts',(209.168715649414,3.4502845118794,127.296741308387));
#17746=CARTESIAN_POINT('Ctrl Pts',(209.16095041176,3.35024118689397,127.203656929099));
#17747=CARTESIAN_POINT('Ctrl Pts',(209.153194866534,3.25032273416257,127.110688736036));
#17748=CARTESIAN_POINT('Ctrl Pts',(209.145439321308,3.14639726453247,127.021757790806));
#17749=CARTESIAN_POINT('Ctrl Pts',(209.137683776083,3.03882640608876,126.93722768267));
#17750=CARTESIAN_POINT('Ctrl Pts',(209.129936043924,2.9313639163431,126.852782731591));
#17751=CARTESIAN_POINT('Ctrl Pts',(209.122188311766,2.82026365182958,126.772730035885));
#17752=CARTESIAN_POINT('Ctrl Pts',(209.114440579607,2.70592284873513,126.697395241623));
#17753=CARTESIAN_POINT('Ctrl Pts',(209.106698788025,2.59166971649979,126.622118210347));
#17754=CARTESIAN_POINT('Ctrl Pts',(209.098956996444,2.47418131699825,126.551552095381));
#17755=CARTESIAN_POINT('Ctrl Pts',(209.091215204862,2.35388631216353,126.485981026573));
#17756=CARTESIAN_POINT('Ctrl Pts',(209.083476813463,2.23364414070448,126.420438756474));
#17757=CARTESIAN_POINT('Ctrl Pts',(209.075738422064,2.11059815902803,126.359887356409));
#17758=CARTESIAN_POINT('Ctrl Pts',(209.068000030665,1.98520403181973,126.304566398433));
#17759=CARTESIAN_POINT('Ctrl Pts',(209.060263323162,1.85983719073276,126.249257478455));
#17760=CARTESIAN_POINT('Ctrl Pts',(209.052526615659,1.73212357881766,126.19917689495));
#17761=CARTESIAN_POINT('Ctrl Pts',(209.044789908156,1.60254099859459,126.154517027689));
#17762=CARTESIAN_POINT('Ctrl Pts',(209.037053197922,1.47295837263404,126.109857144664));
#17763=CARTESIAN_POINT('Ctrl Pts',(209.029316487689,1.34150714759864,126.070618109647));
#17764=CARTESIAN_POINT('Ctrl Pts',(209.021579777455,1.20868213452804,126.036943018889));
#17765=CARTESIAN_POINT('Ctrl Pts',(209.013841378212,1.07582812427986,126.003260576484));
#17766=CARTESIAN_POINT('Ctrl Pts',(209.006102978968,0.941600109169617,125.975144591564));
#17767=CARTESIAN_POINT('Ctrl Pts',(208.998364579724,0.806504581770787,125.952687357537));
#17768=CARTESIAN_POINT('Ctrl Pts',(208.990617964067,0.67126561374634,125.930206279051));
#17769=CARTESIAN_POINT('Ctrl Pts',(208.982871348409,0.535157680777325,125.913396018048));
#17770=CARTESIAN_POINT('Ctrl Pts',(208.975124732751,0.398694459805113,125.902297195881));
#17771=CARTESIAN_POINT('Ctrl Pts',(208.96737400283,0.262158762602129,125.89119247908));
#17772=CARTESIAN_POINT('Ctrl Pts',(208.95962327291,0.125267792947886,125.885805260436));
#17773=CARTESIAN_POINT('Ctrl Pts',(208.95187254299,-0.0114642699424184,
125.886123978992));
#17774=CARTESIAN_POINT('Ctrl Pts',(208.944109300736,-0.148417065233437,
125.886443212069));
#17775=CARTESIAN_POINT('Ctrl Pts',(208.936346058481,-0.285210049268953,
125.892486772142));
#17776=CARTESIAN_POINT('Ctrl Pts',(208.928582816227,-0.421332761867055,
125.904191052512));
#17777=CARTESIAN_POINT('Ctrl Pts',(208.920988044454,-0.554501469148627,
125.91564133775));
#17778=CARTESIAN_POINT('Ctrl Pts',(208.913393272681,-0.687028371328897,
125.932509047985));
#17779=CARTESIAN_POINT('Ctrl Pts',(208.905798500908,-0.818446588343237,
125.954687613689));
#17780=CARTESIAN_POINT('Ctrl Pts',(208.898021644216,-0.953015561718216,
125.977397911284));
#17781=CARTESIAN_POINT('Ctrl Pts',(208.890244787523,-1.08685066963772,126.005749285875));
#17782=CARTESIAN_POINT('Ctrl Pts',(208.88246793083,-1.21944203414923,126.03968390368));
#17783=CARTESIAN_POINT('Ctrl Pts',(208.874700639736,-1.35187031017909,126.073576781623));
#17784=CARTESIAN_POINT('Ctrl Pts',(208.866933348642,-1.48305751185494,126.113039142483));
#17785=CARTESIAN_POINT('Ctrl Pts',(208.859166057548,-1.61250119783885,126.157961694801));
#17786=CARTESIAN_POINT('Ctrl Pts',(208.851406465771,-1.74181657293481,126.202839717698));
#17787=CARTESIAN_POINT('Ctrl Pts',(208.843646873995,-1.86939150499281,126.253167033694));
#17788=CARTESIAN_POINT('Ctrl Pts',(208.835887282218,-1.99473637499177,126.308783918545));
#17789=CARTESIAN_POINT('Ctrl Pts',(208.828133530137,-2.11998691323083,126.364358947365));
#17790=CARTESIAN_POINT('Ctrl Pts',(208.820379778057,-2.24301037434021,126.425215463548));
#17791=CARTESIAN_POINT('Ctrl Pts',(208.812626025976,-2.36333520675677,126.491144907333));
#17792=CARTESIAN_POINT('Ctrl Pts',(208.804875562439,-2.48360900666527,126.557046388935));
#17793=CARTESIAN_POINT('Ctrl Pts',(208.797125098901,-2.60118611244184,126.62801633147));
#17794=CARTESIAN_POINT('Ctrl Pts',(208.789374635364,-2.71561796378144,126.703799419719));
#17795=CARTESIAN_POINT('Ctrl Pts',(208.7816257893,-2.83002593389613,126.779566692503));
#17796=CARTESIAN_POINT('Ctrl Pts',(208.773876943237,-2.94128962968789,126.860144897434));
#17797=CARTESIAN_POINT('Ctrl Pts',(208.766128097174,-3.04898831266746,126.94523463728));
#17798=CARTESIAN_POINT('Ctrl Pts',(208.758379193181,-3.15668780079374,127.03032501325));
#17799=CARTESIAN_POINT('Ctrl Pts',(208.750630289188,-3.26082191638816,127.119926749237));
#17800=CARTESIAN_POINT('Ctrl Pts',(208.742881385195,-3.36100225403236,127.213699548781));
#17801=CARTESIAN_POINT('Ctrl Pts',(208.735130748187,-3.46120499665153,127.307493320276));
#17802=CARTESIAN_POINT('Ctrl Pts',(208.72738011118,-3.55745191658161,127.405459744678));
#17803=CARTESIAN_POINT('Ctrl Pts',(208.719629474172,-3.64939108013971,127.507221280702));
#17804=CARTESIAN_POINT('Ctrl Pts',(208.711870619809,-3.74142771913452,127.609090706006));
#17805=CARTESIAN_POINT('Ctrl Pts',(208.704111765447,-3.82914721603231,127.714762990261));
#17806=CARTESIAN_POINT('Ctrl Pts',(208.696352911084,-3.91223725814708,127.823826655594));
#17807=CARTESIAN_POINT('Ctrl Pts',(208.68858992237,-3.9953715752872,127.932948436153));
#17808=CARTESIAN_POINT('Ctrl Pts',(208.680826933656,-4.07387129874455,128.045464878446));
#17809=CARTESIAN_POINT('Ctrl Pts',(208.673063944941,-4.14746775971367,128.160935898639));
#17810=CARTESIAN_POINT('Ctrl Pts',(208.665288533692,-4.2211819916358,128.276591698534));
#17811=CARTESIAN_POINT('Ctrl Pts',(208.657513122443,-4.28997708545372,128.39521118624));
#17812=CARTESIAN_POINT('Ctrl Pts',(208.649737711194,-4.35363018030978,128.516329298813));
#17813=CARTESIAN_POINT('Ctrl Pts',(208.642275433161,-4.41471982254941,128.632569713871));
#17814=CARTESIAN_POINT('Ctrl Pts',(208.634813155129,-4.47107348551401,128.751111125156));
#17815=CARTESIAN_POINT('Ctrl Pts',(208.627350877096,-4.52253673740703,128.871527329022));
#17816=CARTESIAN_POINT('Ctrl Pts',(208.618730890364,-4.58198407326541,129.010625078401));
#17817=CARTESIAN_POINT('Ctrl Pts',(208.610110903632,-4.63506623355969,129.152598212464));
#17818=CARTESIAN_POINT('Ctrl Pts',(208.601490916901,-4.68152517477817,129.296877582697));
#17819=CARTESIAN_POINT('Ctrl Pts',(208.595858456251,-4.7118823164303,129.391152423336));
#17820=CARTESIAN_POINT('Ctrl Pts',(208.590225995601,-4.73941254095081,129.486411384885));
#17821=CARTESIAN_POINT('Ctrl Pts',(208.584593534951,-4.76405452823405,129.582490119308));
#17822=CARTESIAN_POINT('',(210.,2.85706463458491,134.807654853105));
#17823=CARTESIAN_POINT('Origin',(210.,0.,130.804360617566));
#17824=CARTESIAN_POINT('Ctrl Pts',(210.000000000001,2.8570646345852,134.807654853105));
#17825=CARTESIAN_POINT('Ctrl Pts',(209.9909009417,2.98784898468668,134.714316887059));
#17826=CARTESIAN_POINT('Ctrl Pts',(209.981801883399,3.11395234888589,134.614641121174));
#17827=CARTESIAN_POINT('Ctrl Pts',(209.972702825097,3.23483545810878,134.509090381187));
#17828=CARTESIAN_POINT('Ctrl Pts',(209.963375605347,3.35874974533411,134.400892926674));
#17829=CARTESIAN_POINT('Ctrl Pts',(209.954048385597,3.47717847121068,134.286522118141));
#17830=CARTESIAN_POINT('Ctrl Pts',(209.944721165847,3.5895811378025,134.166516223369));
#17831=CARTESIAN_POINT('Ctrl Pts',(209.935606290089,3.69942483916691,134.049242389331));
#17832=CARTESIAN_POINT('Ctrl Pts',(209.926491414332,3.80351381339523,133.926587349353));
#17833=CARTESIAN_POINT('Ctrl Pts',(209.917376538574,3.90138231724316,133.799089165732));
#17834=CARTESIAN_POINT('Ctrl Pts',(209.907943146828,4.00267080004885,133.667135604866));
#17835=CARTESIAN_POINT('Ctrl Pts',(209.898509755081,4.09729611895824,133.529994361329));
#17836=CARTESIAN_POINT('Ctrl Pts',(209.889076363335,4.18478649255116,133.388300453216));
#17837=CARTESIAN_POINT('Ctrl Pts',(209.879642971588,4.27227686614407,133.246606545104));
#17838=CARTESIAN_POINT('Ctrl Pts',(209.870209579841,4.35263215794215,133.100360040818));
#17839=CARTESIAN_POINT('Ctrl Pts',(209.860776188095,4.42542767858449,132.95023408171));
#17840=CARTESIAN_POINT('Ctrl Pts',(209.853001533586,4.48542306921053,132.826505787987));
#17841=CARTESIAN_POINT('Ctrl Pts',(209.845226879078,4.54024783943048,132.700213797986));
#17842=CARTESIAN_POINT('Ctrl Pts',(209.837452224569,4.58968782858598,132.571830192588));
#17843=CARTESIAN_POINT('Ctrl Pts',(209.829678554328,4.63912155866696,132.443462840482));
#17844=CARTESIAN_POINT('Ctrl Pts',(209.821904884086,4.68317172608175,132.313004762609));
#17845=CARTESIAN_POINT('Ctrl Pts',(209.814131213844,4.72167262205471,132.180947234034));
#17846=CARTESIAN_POINT('Ctrl Pts',(209.806353640484,4.76019284912417,132.048823400072));
#17847=CARTESIAN_POINT('Ctrl Pts',(209.798576067123,4.79315812506151,131.915098882938));
#17848=CARTESIAN_POINT('Ctrl Pts',(209.790798493763,4.82045280424895,131.780279581675));
#17849=CARTESIAN_POINT('Ctrl Pts',(209.783019152641,4.8477536872307,131.6454296374));
#17850=CARTESIAN_POINT('Ctrl Pts',(209.77523981152,4.86938133801002,131.509484795897));
#17851=CARTESIAN_POINT('Ctrl Pts',(209.767460470399,4.88527157757875,131.372959488301));
#17852=CARTESIAN_POINT('Ctrl Pts',(209.759672670713,4.90117909478188,131.236285735218));
#17853=CARTESIAN_POINT('Ctrl Pts',(209.751884871028,4.91133669930707,131.099030642188));
#17854=CARTESIAN_POINT('Ctrl Pts',(209.744097071342,4.91573223244676,130.961712711241));
#17855=CARTESIAN_POINT('Ctrl Pts',(209.736582172957,4.9199737366231,130.82920669682));
#17856=CARTESIAN_POINT('Ctrl Pts',(209.729067274573,4.91885023632,130.696642495085));
#17857=CARTESIAN_POINT('Ctrl Pts',(209.721552376188,4.91239674626941,130.564483003476));
#17858=CARTESIAN_POINT('Ctrl Pts',(209.713678765481,4.9056352086199,130.426015078175));
#17859=CARTESIAN_POINT('Ctrl Pts',(209.705805154774,4.89300771239889,130.287688864539));
#17860=CARTESIAN_POINT('Ctrl Pts',(209.697931544067,4.87452930506278,130.150031100744));
#17861=CARTESIAN_POINT('Ctrl Pts',(209.690064949113,4.85606736284523,130.012495996406));
#17862=CARTESIAN_POINT('Ctrl Pts',(209.682198354159,4.83176494040784,129.875628528245));
#17863=CARTESIAN_POINT('Ctrl Pts',(209.674331759204,4.80168901966641,129.739952039568));
#17864=CARTESIAN_POINT('Ctrl Pts',(209.666470472472,4.77163339355775,129.604367102686));
#17865=CARTESIAN_POINT('Ctrl Pts',(209.658609185739,4.7358121091933,129.469971912218));
#17866=CARTESIAN_POINT('Ctrl Pts',(209.650747899006,4.69434349581246,129.337281135798));
#17867=CARTESIAN_POINT('Ctrl Pts',(209.642890217533,4.65289390032517,129.204651212609));
#17868=CARTESIAN_POINT('Ctrl Pts',(209.63503253606,4.60580224712704,129.073724506109));
#17869=CARTESIAN_POINT('Ctrl Pts',(209.627174854587,4.5532370807101,128.945001816972));
#17870=CARTESIAN_POINT('Ctrl Pts',(209.619317529717,4.50067429984411,128.816284969622));
#17871=CARTESIAN_POINT('Ctrl Pts',(209.611460204847,4.44263863419322,128.689772293342));
#17872=CARTESIAN_POINT('Ctrl Pts',(209.603602879977,4.37934731209041,128.565945959245));
#17873=CARTESIAN_POINT('Ctrl Pts',(209.595745424998,4.31605494195501,128.442117574724));
#17874=CARTESIAN_POINT('Ctrl Pts',(209.58788797002,4.24750691313248,128.320975957634));
#17875=CARTESIAN_POINT('Ctrl Pts',(209.580030515041,4.17396689693851,128.202979560173));
#17876=CARTESIAN_POINT('Ctrl Pts',(209.572171389685,4.10041124723336,128.084958078438));
#17877=CARTESIAN_POINT('Ctrl Pts',(209.564312264329,4.02186169619298,127.970083468555));
#17878=CARTESIAN_POINT('Ctrl Pts',(209.556453138973,3.93862568001678,127.858785832365));
#17879=CARTESIAN_POINT('Ctrl Pts',(209.548590802169,3.85535565139079,127.747442717001));
#17880=CARTESIAN_POINT('Ctrl Pts',(209.540728465365,3.76739556974505,127.639679788538));
#17881=CARTESIAN_POINT('Ctrl Pts',(209.532866128561,3.67509348629992,127.535894474334));
#17882=CARTESIAN_POINT('Ctrl Pts',(209.524993952985,3.58267589786456,127.431979285253));
#17883=CARTESIAN_POINT('Ctrl Pts',(209.51712177741,3.4859057045839,127.332051936366));
#17884=CARTESIAN_POINT('Ctrl Pts',(209.509249601834,3.38516874447327,127.236473899361));
#17885=CARTESIAN_POINT('Ctrl Pts',(209.501372245105,3.28436548329557,127.140832956688));
#17886=CARTESIAN_POINT('Ctrl Pts',(209.493494888376,3.17959053527948,127.049547279982));
#17887=CARTESIAN_POINT('Ctrl Pts',(209.485617531647,3.07126268549045,126.962937889043));
#17888=CARTESIAN_POINT('Ctrl Pts',(209.477727176986,2.96275609071294,126.876185589382));
#17889=CARTESIAN_POINT('Ctrl Pts',(209.469836822325,2.8506851836161,126.794125217976));
#17890=CARTESIAN_POINT('Ctrl Pts',(209.461946467663,2.73549839812863,126.717034893289));
#17891=CARTESIAN_POINT('Ctrl Pts',(209.455665895901,2.64381191463777,126.655672465717));
#17892=CARTESIAN_POINT('Ctrl Pts',(209.449385324138,2.55015185656929,126.59745814901));
#17893=CARTESIAN_POINT('Ctrl Pts',(209.443104752375,2.45475470409811,126.542510971555));
#17894=CARTESIAN_POINT('Ctrl Pts',(209.435394730144,2.33764527615028,126.47505788357));
#17895=CARTESIAN_POINT('Ctrl Pts',(209.427684707913,2.21753700128125,126.412310841026));
#17896=CARTESIAN_POINT('Ctrl Pts',(209.419974685682,2.09484840718725,126.354552395473));
#17897=CARTESIAN_POINT('Ctrl Pts',(209.412274998352,1.97232427104564,126.296871372241));
#17898=CARTESIAN_POINT('Ctrl Pts',(209.404575311022,1.84722705072554,126.244165814112));
#17899=CARTESIAN_POINT('Ctrl Pts',(209.396875623692,1.72000313242919,126.196674399199));
#17900=CARTESIAN_POINT('Ctrl Pts',(209.389184335902,1.59291800189124,126.149234792365));
#17901=CARTESIAN_POINT('Ctrl Pts',(209.381493048111,1.46371115844236,126.106998152058));
#17902=CARTESIAN_POINT('Ctrl Pts',(209.373801760321,1.33285200466186,126.070156503233));
#17903=CARTESIAN_POINT('Ctrl Pts',(209.366116945084,1.2021029745474,126.033345858257));
#17904=CARTESIAN_POINT('Ctrl Pts',(209.358432129846,1.0697047820666,126.001921279021));
#17905=CARTESIAN_POINT('Ctrl Pts',(209.350747314609,0.936144727381679,125.976025903413));
#17906=CARTESIAN_POINT('Ctrl Pts',(209.342993556857,0.801386470042141,125.949898213526));
#17907=CARTESIAN_POINT('Ctrl Pts',(209.335239799105,0.665445784867029,125.929399571767));
#17908=CARTESIAN_POINT('Ctrl Pts',(209.327486041353,0.528837072948192,125.914624999685));
#17909=CARTESIAN_POINT('Ctrl Pts',(209.319807329801,0.393550554092795,125.899993426072));
#17910=CARTESIAN_POINT('Ctrl Pts',(209.312128618249,0.257609288411705,125.890975634284));
#17911=CARTESIAN_POINT('Ctrl Pts',(209.304449906697,0.121520480433024,125.887612115219));
#17912=CARTESIAN_POINT('Ctrl Pts',(209.29677151016,-0.0145627445721506,
125.88424873414));
#17913=CARTESIAN_POINT('Ctrl Pts',(209.289093113624,-0.150793101684035,
125.886539174479));
#17914=CARTESIAN_POINT('Ctrl Pts',(209.281414717087,-0.286661848309734,
125.894471815646));
#17915=CARTESIAN_POINT('Ctrl Pts',(209.273734902769,-0.422555682476961,
125.902405921538));
#17916=CARTESIAN_POINT('Ctrl Pts',(209.266055088452,-0.558087375780228,
125.915984277149));
#17917=CARTESIAN_POINT('Ctrl Pts',(209.258375274134,-0.692752271574411,
125.935143293116));
#17918=CARTESIAN_POINT('Ctrl Pts',(209.25056542867,-0.82969725255273,125.954626700886));
#17919=CARTESIAN_POINT('Ctrl Pts',(209.242755583206,-0.965745392709727,
125.979881406748));
#17920=CARTESIAN_POINT('Ctrl Pts',(209.234945737741,-1.10037688251651,126.010786400041));
#17921=CARTESIAN_POINT('Ctrl Pts',(209.22725380964,-1.23297563168889,126.041224772666));
#17922=CARTESIAN_POINT('Ctrl Pts',(209.219561881538,-1.36419984247571,126.077143833343));
#17923=CARTESIAN_POINT('Ctrl Pts',(209.211869953437,-1.49356918075577,126.118377885545));
#17924=CARTESIAN_POINT('Ctrl Pts',(209.204001149291,-1.62591336961785,126.160560115622));
#17925=CARTESIAN_POINT('Ctrl Pts',(209.196132345145,-1.75631592647879,126.208304581786));
#17926=CARTESIAN_POINT('Ctrl Pts',(209.188263540999,-1.88428613385585,126.261382648408));
#17927=CARTESIAN_POINT('Ctrl Pts',(209.180394736854,-2.0122563412329,126.314460715029));
#17928=CARTESIAN_POINT('Ctrl Pts',(209.172525932708,-2.1377938314257,126.372872133719));
#17929=CARTESIAN_POINT('Ctrl Pts',(209.164657128562,-2.26043738552501,126.436339797032));
#17930=CARTESIAN_POINT('Ctrl Pts',(209.156868592286,-2.38182988080303,126.499160041239));
#17931=CARTESIAN_POINT('Ctrl Pts',(209.14908005601,-2.500789467108,126.567141780581));
#17932=CARTESIAN_POINT('Ctrl Pts',(209.141291519734,-2.61684735835623,126.64007280744));
#17933=CARTESIAN_POINT('Ctrl Pts',(209.133512703956,-2.73276040333477,126.712912812594));
#17934=CARTESIAN_POINT('Ctrl Pts',(209.125733888177,-2.84577863326455,126.790689607508));
#17935=CARTESIAN_POINT('Ctrl Pts',(209.117955072399,-2.95545619587902,126.873144299842));
#17936=CARTESIAN_POINT('Ctrl Pts',(209.1101333403,-3.06573885798239,126.956053901011));
#17937=CARTESIAN_POINT('Ctrl Pts',(209.1023116082,-3.17264351427431,127.043693011678));
#17938=CARTESIAN_POINT('Ctrl Pts',(209.094489876101,-3.27574388721603,127.135752564385));
#17939=CARTESIAN_POINT('Ctrl Pts',(209.086725556799,-3.37808748650062,127.227136384867));
#17940=CARTESIAN_POINT('Ctrl Pts',(209.078961237497,-3.47668216349184,127.322875713582));
#17941=CARTESIAN_POINT('Ctrl Pts',(209.071196918195,-3.57114231524718,127.422626502241));
#17942=CARTESIAN_POINT('Ctrl Pts',(209.063436157677,-3.66555917109043,127.522331570019));
#17943=CARTESIAN_POINT('Ctrl Pts',(209.055675397159,-3.75584500575455,127.62604415669));
#17944=CARTESIAN_POINT('Ctrl Pts',(209.047914636642,-3.84165048643871,127.733382824982));
#17945=CARTESIAN_POINT('Ctrl Pts',(209.040155768875,-3.92743504024807,127.840695314726));
#17946=CARTESIAN_POINT('Ctrl Pts',(209.032396901109,-4.0087411727101,127.951631821533));
#17947=CARTESIAN_POINT('Ctrl Pts',(209.024638033343,-4.08525957467433,128.065777540493));
#17948=CARTESIAN_POINT('Ctrl Pts',(209.016770989066,-4.16284481963531,128.181514714027));
#17949=CARTESIAN_POINT('Ctrl Pts',(209.008903944789,-4.23550756808287,128.300550941316));
#17950=CARTESIAN_POINT('Ctrl Pts',(209.001036900512,-4.30297085348242,128.422423402486));
#17951=CARTESIAN_POINT('Ctrl Pts',(208.993274395468,-4.36953767002672,128.54267639219));
#17952=CARTESIAN_POINT('Ctrl Pts',(208.985511890425,-4.43104221440763,128.665690330152));
#17953=CARTESIAN_POINT('Ctrl Pts',(208.977749385382,-4.48726508102552,128.79099647884));
#17954=CARTESIAN_POINT('Ctrl Pts',(208.969830071488,-4.54462369481051,128.918833912607));
#17955=CARTESIAN_POINT('Ctrl Pts',(208.961910757594,-4.59648477390531,129.049056774179));
#17956=CARTESIAN_POINT('Ctrl Pts',(208.9539914437,-4.64266756080343,129.181147451539));
#17957=CARTESIAN_POINT('Ctrl Pts',(208.946072129806,-4.68885034770155,129.313238128898));
#17958=CARTESIAN_POINT('Ctrl Pts',(208.938152815912,-4.72935474820577,129.447196203621));
#17959=CARTESIAN_POINT('Ctrl Pts',(208.930233502018,-4.76405452823405,129.582490119308));
#17960=CARTESIAN_POINT('Origin',(213.235140564004,0.,130.804360617566));
#17961=CARTESIAN_POINT('',(206.834782106149,-4.76405452823405,129.582490119308));
#17962=CARTESIAN_POINT('',(207.179891338435,-4.76405452823405,129.582490119308));
#17963=CARTESIAN_POINT('',(213.235140564004,-4.76405452823405,129.582490119308));
#17964=CARTESIAN_POINT('',(208.51485943604,-4.91824939693558,130.801925039035));
#17965=CARTESIAN_POINT('Ctrl Pts',(208.514859435991,-4.91824939693602,130.801925039913));
#17966=CARTESIAN_POINT('Ctrl Pts',(208.5069976833,-4.91831846622271,130.941399130231));
#17967=CARTESIAN_POINT('Ctrl Pts',(208.49913593061,-4.91245027592863,131.080863938173));
#17968=CARTESIAN_POINT('Ctrl Pts',(208.491274177919,-4.90067369759928,131.219788556153));
#17969=CARTESIAN_POINT('Ctrl Pts',(208.483410074226,-4.88889359756652,131.358754718568));
#17970=CARTESIAN_POINT('Ctrl Pts',(208.475545970533,-4.87120162119958,131.497179995886));
#17971=CARTESIAN_POINT('Ctrl Pts',(208.46768186684,-4.84767848973048,131.634539106028));
#17972=CARTESIAN_POINT('Ctrl Pts',(208.459813911939,-4.82414383851507,131.771965483663));
#17973=CARTESIAN_POINT('Ctrl Pts',(208.451945957038,-4.79477240682799,131.908324285026));
#17974=CARTESIAN_POINT('Ctrl Pts',(208.444078002137,-4.75969590309668,132.043101095852));
#17975=CARTESIAN_POINT('Ctrl Pts',(208.436146773066,-4.72433731378016,132.178961783106));
#17976=CARTESIAN_POINT('Ctrl Pts',(208.428215543994,-4.68318159239801,132.313214549761));
#17977=CARTESIAN_POINT('Ctrl Pts',(208.420284314923,-4.6364142414082,132.445349966882));
#17978=CARTESIAN_POINT('Ctrl Pts',(208.41239950935,-4.58992063160245,132.576711961844));
#17979=CARTESIAN_POINT('Ctrl Pts',(208.404514703777,-4.53788111459692,132.705981006347));
#17980=CARTESIAN_POINT('Ctrl Pts',(208.396629898205,-4.48052538922162,132.832678960194));
#17981=CARTESIAN_POINT('Ctrl Pts',(208.388675457384,-4.422663122488,132.960495856452));
#17982=CARTESIAN_POINT('Ctrl Pts',(208.380721016564,-4.35939048241694,133.085695687326));
#17983=CARTESIAN_POINT('Ctrl Pts',(208.372766575744,-4.29098908859084,133.207815569109));
#17984=CARTESIAN_POINT('Ctrl Pts',(208.364812134923,-4.22258769476473,133.329935450891));
#17985=CARTESIAN_POINT('Ctrl Pts',(208.356857694103,-4.14905780241504,133.448975089334));
#17986=CARTESIAN_POINT('Ctrl Pts',(208.348903253283,-4.07072345201489,133.564504389132));
#17987=CARTESIAN_POINT('Ctrl Pts',(208.341130262337,-3.99417599755729,133.677398333739));
#17988=CARTESIAN_POINT('Ctrl Pts',(208.333357271391,-3.91280696466297,133.787284943416));
#17989=CARTESIAN_POINT('Ctrl Pts',(208.325584280444,-3.82688028292267,133.893724688484));
#17990=CARTESIAN_POINT('Ctrl Pts',(208.317820888004,-3.74105970805478,134.000032996049));
#17991=CARTESIAN_POINT('Ctrl Pts',(208.310057495564,-3.65069292565359,134.10290260645));
#17992=CARTESIAN_POINT('Ctrl Pts',(208.302294103124,-3.55608760223375,134.201922100121));
#17993=CARTESIAN_POINT('Ctrl Pts',(208.294538438539,-3.46157645107868,134.300843027563));
#17994=CARTESIAN_POINT('Ctrl Pts',(208.286782773954,-3.36283542354201,134.395921184087));
#17995=CARTESIAN_POINT('Ctrl Pts',(208.279027109369,-3.26021275313167,134.486777740438));
#17996=CARTESIAN_POINT('Ctrl Pts',(208.271277308707,-3.15766767394118,134.577565601723));
#17997=CARTESIAN_POINT('Ctrl Pts',(208.263527508046,-3.05124708510556,134.664137957811));
#17998=CARTESIAN_POINT('Ctrl Pts',(208.255777707384,-2.94133615365521,134.746152683835));
#17999=CARTESIAN_POINT('Ctrl Pts',(208.248031218034,-2.83147218461794,134.828132366852));
#18000=CARTESIAN_POINT('Ctrl Pts',(208.240284728684,-2.71812115194593,134.905558059566));
#18001=CARTESIAN_POINT('Ctrl Pts',(208.232538239334,-2.60170121537788,134.978127962352));
#18002=CARTESIAN_POINT('Ctrl Pts',(208.224793380744,-2.48530578706252,135.050682588017));
#18003=CARTESIAN_POINT('Ctrl Pts',(208.217048522153,-2.3658430715812,135.118383250226));
#18004=CARTESIAN_POINT('Ctrl Pts',(208.209303663563,-2.24375977991022,135.18097176234));
#18005=CARTESIAN_POINT('Ctrl Pts',(208.201558756542,-2.12167572482072,135.243560665835));
#18006=CARTESIAN_POINT('Ctrl Pts',(208.193813849521,-1.99697140887362,135.30103717698));
#18007=CARTESIAN_POINT('Ctrl Pts',(208.186068942499,-1.87011732041024,135.353189507555));
#18008=CARTESIAN_POINT('Ctrl Pts',(208.17832230818,-1.74323494047574,135.405353469337));
#18009=CARTESIAN_POINT('Ctrl Pts',(208.170575673861,-1.61420219565832,135.452190739054));
#18010=CARTESIAN_POINT('Ctrl Pts',(208.162829039542,-1.48350830287314,135.49353817635));
#18011=CARTESIAN_POINT('Ctrl Pts',(208.155074174212,-1.35267554425398,135.534929546429));
#18012=CARTESIAN_POINT('Ctrl Pts',(208.147319308882,-1.22017848536061,135.570819313687));
#18013=CARTESIAN_POINT('Ctrl Pts',(208.139564443553,-1.08652075107271,135.601094477182));
#18014=CARTESIAN_POINT('Ctrl Pts',(208.131805442764,-0.952791740747417,
135.6313857856));
#18015=CARTESIAN_POINT('Ctrl Pts',(208.124046441975,-0.817901206265174,
135.656056453942));
#18016=CARTESIAN_POINT('Ctrl Pts',(208.116287441186,-0.682360651451801,
135.675045066784));
#18017=CARTESIAN_POINT('Ctrl Pts',(208.108515975456,-0.5466023488804,135.694064185092));
#18018=CARTESIAN_POINT('Ctrl Pts',(208.100744509727,-0.410192328696788,
135.707382968629));
#18019=CARTESIAN_POINT('Ctrl Pts',(208.092973043997,-0.273645776384339,
135.714992048611));
#18020=CARTESIAN_POINT('Ctrl Pts',(208.085467239154,-0.141766950797409,
135.722341018723));
#18021=CARTESIAN_POINT('Ctrl Pts',(208.077961434312,-0.00976108821497224,
135.724364294266));
#18022=CARTESIAN_POINT('Ctrl Pts',(208.07045562947,0.121911747919636,135.721099433918));
#18023=CARTESIAN_POINT('Ctrl Pts',(208.062680838016,0.258303362492575,135.717717570297));
#18024=CARTESIAN_POINT('Ctrl Pts',(208.054906046562,0.394769977134225,135.708650746295));
#18025=CARTESIAN_POINT('Ctrl Pts',(208.047131255108,0.530798916088052,135.693883659048));
#18026=CARTESIAN_POINT('Ctrl Pts',(208.03936604126,0.66666028378857,135.679134763071));
#18027=CARTESIAN_POINT('Ctrl Pts',(208.031600827411,0.802084663675805,135.658699617433));
#18028=CARTESIAN_POINT('Ctrl Pts',(208.023835613563,0.936559415699432,135.632614911135));
#18029=CARTESIAN_POINT('Ctrl Pts',(208.016078108725,1.0709006662788,135.606556100746));
#18030=CARTESIAN_POINT('Ctrl Pts',(208.008320603888,1.20429378384447,135.574858965191));
#18031=CARTESIAN_POINT('Ctrl Pts',(208.00056309905,1.33623164391999,135.537611937355));
#18032=CARTESIAN_POINT('Ctrl Pts',(207.992811441313,1.46807005784367,135.500392983899));
#18033=CARTESIAN_POINT('Ctrl Pts',(207.985059783576,1.59845502286451,135.45763257026));
#18034=CARTESIAN_POINT('Ctrl Pts',(207.977308125839,1.72689035222872,135.409470037968));
#18035=CARTESIAN_POINT('Ctrl Pts',(207.969559760361,1.85527113296102,135.36132796111));
#18036=CARTESIAN_POINT('Ctrl Pts',(207.961811394883,1.98170355969654,135.307788465907));
#18037=CARTESIAN_POINT('Ctrl Pts',(207.954063029405,2.10570755579637,135.249040443151));
#18038=CARTESIAN_POINT('Ctrl Pts',(207.946316283345,2.22968563490169,135.190304698807));
#18039=CARTESIAN_POINT('Ctrl Pts',(207.938569537285,2.35123593986109,135.126362759441));
#18040=CARTESIAN_POINT('Ctrl Pts',(207.930822791226,2.46989966875899,135.057451104349));
#18041=CARTESIAN_POINT('Ctrl Pts',(207.923075987157,2.58856428623285,134.988538933234));
#18042=CARTESIAN_POINT('Ctrl Pts',(207.915329183088,2.70434194647162,134.914657168452));
#18043=CARTESIAN_POINT('Ctrl Pts',(207.907582379019,2.8168000428877,134.836087366849));
#18044=CARTESIAN_POINT('Ctrl Pts',(207.899833839831,2.92928332751887,134.757499967287));
#18045=CARTESIAN_POINT('Ctrl Pts',(207.892085300644,3.03844524843345,134.674222665321));
#18046=CARTESIAN_POINT('Ctrl Pts',(207.884336761456,3.14388401280121,134.586579064001));
#18047=CARTESIAN_POINT('Ctrl Pts',(207.876579989602,3.24943480372359,134.498842343127));
#18048=CARTESIAN_POINT('Ctrl Pts',(207.868823217748,3.35125423490542,134.406730306064));
#18049=CARTESIAN_POINT('Ctrl Pts',(207.861066445894,3.44897491534359,134.310605773831));
#18050=CARTESIAN_POINT('Ctrl Pts',(207.853305534651,3.54674774427149,134.21442994489));
#18051=CARTESIAN_POINT('Ctrl Pts',(207.845544623408,3.64041719724162,134.114237639535));
#18052=CARTESIAN_POINT('Ctrl Pts',(207.837783712165,3.72965502772357,134.010426187182));
#18053=CARTESIAN_POINT('Ctrl Pts',(207.830010348593,3.81903603968545,133.906448170074));
#18054=CARTESIAN_POINT('Ctrl Pts',(207.822236985022,3.90397097776096,133.798839708958));
#18055=CARTESIAN_POINT('Ctrl Pts',(207.81446362145,3.98417339609271,133.688029359354));
#18056=CARTESIAN_POINT('Ctrl Pts',(207.806978416186,4.06140271367255,133.581326745409));
#18057=CARTESIAN_POINT('Ctrl Pts',(207.799493210921,4.13424399164836,133.471655678562));
#18058=CARTESIAN_POINT('Ctrl Pts',(207.792008005657,4.20248194836357,133.359420017302));
#18059=CARTESIAN_POINT('Ctrl Pts',(207.784233556478,4.27335676178718,133.242847336433));
#18060=CARTESIAN_POINT('Ctrl Pts',(207.776459107299,4.33948969755912,133.123138859218));
#18061=CARTESIAN_POINT('Ctrl Pts',(207.76868465812,4.40059076633519,133.000717594413));
#18062=CARTESIAN_POINT('Ctrl Pts',(207.76091978728,4.46161655688566,132.87844715603));
#18063=CARTESIAN_POINT('Ctrl Pts',(207.75315491644,4.51762264249707,132.753470926551));
#18064=CARTESIAN_POINT('Ctrl Pts',(207.7453900456,4.56836279360575,132.626239990219));
#18065=CARTESIAN_POINT('Ctrl Pts',(207.737632884128,4.61905256725022,132.499135375386));
#18066=CARTESIAN_POINT('Ctrl Pts',(207.729875722656,4.66448666705683,132.36978086939));
#18067=CARTESIAN_POINT('Ctrl Pts',(207.722118561184,4.70446537714295,132.238650887269));
#18068=CARTESIAN_POINT('Ctrl Pts',(207.714367246798,4.74441395262572,132.107619746505));
#18069=CARTESIAN_POINT('Ctrl Pts',(207.706615932413,4.7789152097074,131.974816165857));
#18070=CARTESIAN_POINT('Ctrl Pts',(207.698864618028,4.80781817473379,131.840732877519));
#18071=CARTESIAN_POINT('Ctrl Pts',(207.691116594631,4.83670886837882,131.706706517151));
#18072=CARTESIAN_POINT('Ctrl Pts',(207.683368571235,4.86000591517799,131.571401911102));
#18073=CARTESIAN_POINT('Ctrl Pts',(207.675620547838,4.87760873613739,131.435325021995));
#18074=CARTESIAN_POINT('Ctrl Pts',(207.667874143036,4.89520787979476,131.299276559912));
#18075=CARTESIAN_POINT('Ctrl Pts',(207.660127738233,4.90711511356422,131.162456523146));
#18076=CARTESIAN_POINT('Ctrl Pts',(207.652381333431,4.91328139537258,131.025378699147));
#18077=CARTESIAN_POINT('Ctrl Pts',(207.644634869463,4.91944772427759,130.888299828178));
#18078=CARTESIAN_POINT('Ctrl Pts',(207.636888405496,4.91987299616475,130.750963556604));
#18079=CARTESIAN_POINT('Ctrl Pts',(207.629141941528,4.9145602531883,130.613885999095));
#18080=CARTESIAN_POINT('Ctrl Pts',(207.621393740952,4.90924631919717,130.476777711437));
#18081=CARTESIAN_POINT('Ctrl Pts',(207.613645540377,4.89819182578494,130.339928643839));
#18082=CARTESIAN_POINT('Ctrl Pts',(207.605897339801,4.88145184537105,130.203851713532));
#18083=CARTESIAN_POINT('Ctrl Pts',(207.598140902255,4.86469406898943,130.067630122324));
#18084=CARTESIAN_POINT('Ctrl Pts',(207.590384464708,4.84223877960226,129.932182696777));
#18085=CARTESIAN_POINT('Ctrl Pts',(207.582628027162,4.81419263987389,129.798014609135));
#18086=CARTESIAN_POINT('Ctrl Pts',(207.574867448415,4.78613152617349,129.663774888491));
#18087=CARTESIAN_POINT('Ctrl Pts',(207.567106869669,4.75247371019375,129.530816245587));
#18088=CARTESIAN_POINT('Ctrl Pts',(207.559346290922,4.71337604578668,129.399629570887));
#18089=CARTESIAN_POINT('Ctrl Pts',(207.55157325334,4.67421561397873,129.268232289064));
#18090=CARTESIAN_POINT('Ctrl Pts',(207.543800215759,4.62959800947895,129.138613029973));
#18091=CARTESIAN_POINT('Ctrl Pts',(207.536027178177,4.57972895160504,129.011244393689));
#18092=CARTESIAN_POINT('Ctrl Pts',(207.528538246066,4.53168261387283,128.888531096581));
#18093=CARTESIAN_POINT('Ctrl Pts',(207.521049313955,4.47876212574444,128.767907055659));
#18094=CARTESIAN_POINT('Ctrl Pts',(207.513560381844,4.42119126588728,128.649772291936));
#18095=CARTESIAN_POINT('Ctrl Pts',(207.505786241846,4.36142788203951,128.527138493384));
#18096=CARTESIAN_POINT('Ctrl Pts',(207.498012101847,4.29646354793691,128.406798788378));
#18097=CARTESIAN_POINT('Ctrl Pts',(207.490237961849,4.22649734688889,128.289225782365));
#18098=CARTESIAN_POINT('Ctrl Pts',(207.482473405643,4.15661739866639,128.171797717822));
#18099=CARTESIAN_POINT('Ctrl Pts',(207.474708849436,4.08174805039643,128.057129898718));
#18100=CARTESIAN_POINT('Ctrl Pts',(207.46694429323,4.00213566156389,127.945673294871));
#18101=CARTESIAN_POINT('Ctrl Pts',(207.459187451483,3.92260237145483,127.834327428501));
#18102=CARTESIAN_POINT('Ctrl Pts',(207.451430609736,3.83833564452231,127.726186744262));
#18103=CARTESIAN_POINT('Ctrl Pts',(207.443673767988,3.74962661345412,127.621675694081));
#18104=CARTESIAN_POINT('Ctrl Pts',(207.435922778062,3.66098450516628,127.517243487847));
#18105=CARTESIAN_POINT('Ctrl Pts',(207.428171788136,3.56790701530164,127.416435762287));
#18106=CARTESIAN_POINT('Ctrl Pts',(207.42042079821,3.47072703641595,127.319645865798));
#18107=CARTESIAN_POINT('Ctrl Pts',(207.412673105353,3.37358839535843,127.222897141206));
#18108=CARTESIAN_POINT('Ctrl Pts',(207.404925412496,3.27235101258055,127.130163121791));
#18109=CARTESIAN_POINT('Ctrl Pts',(207.39717771964,3.16738615389837,127.041801911766));
#18110=CARTESIAN_POINT('Ctrl Pts',(207.389431649034,3.06244327329369,126.953459203261));
#18111=CARTESIAN_POINT('Ctrl Pts',(207.381685578428,2.95377476812009,126.869487734607));
#18112=CARTESIAN_POINT('Ctrl Pts',(207.373939507823,2.84178634723068,126.790206482609));
#18113=CARTESIAN_POINT('Ctrl Pts',(207.366193381404,2.72979711941912,126.710924659357));
#18114=CARTESIAN_POINT('Ctrl Pts',(207.358447254985,2.61448824726982,126.636333346117));
#18115=CARTESIAN_POINT('Ctrl Pts',(207.350701128566,2.49629555308794,126.566708959615));
#18116=CARTESIAN_POINT('Ctrl Pts',(207.342953268587,2.37807640773334,126.497068991383));
#18117=CARTESIAN_POINT('Ctrl Pts',(207.335205408607,2.2569724929127,126.432398360219));
#18118=CARTESIAN_POINT('Ctrl Pts',(207.327457548628,2.13344506692891,126.372927981398));
#18119=CARTESIAN_POINT('Ctrl Pts',(207.319701454607,2.009786362109,126.3133944004));
#18120=CARTESIAN_POINT('Ctrl Pts',(207.311945360586,1.88369935396116,126.259072281538));
#18121=CARTESIAN_POINT('Ctrl Pts',(207.304189266564,1.75566667258516,126.210144950309));
#18122=CARTESIAN_POINT('Ctrl Pts',(207.296429033481,1.62756566619945,126.161191508867));
#18123=CARTESIAN_POINT('Ctrl Pts',(207.288668800398,1.49751728822706,126.117638715693));
#18124=CARTESIAN_POINT('Ctrl Pts',(207.280908567314,1.36601928450809,126.079619949884));
#18125=CARTESIAN_POINT('Ctrl Pts',(207.27313587558,1.23431016757891,126.041540146922));
#18126=CARTESIAN_POINT('Ctrl Pts',(207.265363183846,1.10114715425798,126.009012218405));
#18127=CARTESIAN_POINT('Ctrl Pts',(207.257590492112,0.967039016842553,125.982118545417));
#18128=CARTESIAN_POINT('Ctrl Pts',(207.250097914085,0.837763893371229,125.956194071607));
#18129=CARTESIAN_POINT('Ctrl Pts',(207.242605336058,0.707610899911634,125.935504790949));
#18130=CARTESIAN_POINT('Ctrl Pts',(207.235112758031,0.577038241873283,125.920078691846));
#18131=CARTESIAN_POINT('Ctrl Pts',(207.227338345037,0.441554064636067,125.904072336639));
#18132=CARTESIAN_POINT('Ctrl Pts',(207.219563932042,0.305188826807901,125.893682160164));
#18133=CARTESIAN_POINT('Ctrl Pts',(207.211789519048,0.16844779316213,125.888996093598));
#18134=CARTESIAN_POINT('Ctrl Pts',(207.204024686519,0.0318752664866379,
125.884315801707));
#18135=CARTESIAN_POINT('Ctrl Pts',(207.19625985399,-0.105071747606433,125.885325646935));
#18136=CARTESIAN_POINT('Ctrl Pts',(207.188495021462,-0.241880637176841,
125.892062090414));
#18137=CARTESIAN_POINT('Ctrl Pts',(207.180737900378,-0.378553658495936,
125.898791843767));
#18138=CARTESIAN_POINT('Ctrl Pts',(207.172980779294,-0.515088440319783,
125.911236858428));
#18139=CARTESIAN_POINT('Ctrl Pts',(207.16522365821,-0.650970483668557,125.929381592802));
#18140=CARTESIAN_POINT('Ctrl Pts',(207.157472386242,-0.786750067641371,
125.947512645469));
#18141=CARTESIAN_POINT('Ctrl Pts',(207.149721114274,-0.921877506856219,
125.971334811858));
#18142=CARTESIAN_POINT('Ctrl Pts',(207.141969842306,-1.05584190167843,126.00078060458));
#18143=CARTESIAN_POINT('Ctrl Pts',(207.134221864282,-1.18974936760714,126.030213884153));
#18144=CARTESIAN_POINT('Ctrl Pts',(207.126473886259,-1.32249439111151,126.065265953194));
#18145=CARTESIAN_POINT('Ctrl Pts',(207.118725908236,-1.45357498549394,126.105817989894));
#18146=CARTESIAN_POINT('Ctrl Pts',(207.110979550602,-1.58462816607085,126.146361545663));
#18147=CARTESIAN_POINT('Ctrl Pts',(207.103233192967,-1.71401723664896,126.192402665714));
#18148=CARTESIAN_POINT('Ctrl Pts',(207.095486835333,-1.84125451462641,126.243772401681));
#18149=CARTESIAN_POINT('Ctrl Pts',(207.087740420291,-1.96849273555578,126.295142518348));
#18150=CARTESIAN_POINT('Ctrl Pts',(207.079994005249,-2.09357876953884,126.351841183367));
#18151=CARTESIAN_POINT('Ctrl Pts',(207.072247590207,-2.21604446583207,126.413651109075));
#18152=CARTESIAN_POINT('Ctrl Pts',(207.064499440277,-2.33853758954754,126.475474877736));
#18153=CARTESIAN_POINT('Ctrl Pts',(207.056751290347,-2.45840885885262,126.542412008823));
#18154=CARTESIAN_POINT('Ctrl Pts',(207.049003140418,-2.5752146573241,126.61419922077));
#18155=CARTESIAN_POINT('Ctrl Pts',(207.041246755976,-2.69214459365274,126.686062726109));
#18156=CARTESIAN_POINT('Ctrl Pts',(207.033490371535,-2.80600221754134,126.762786404001));
#18157=CARTESIAN_POINT('Ctrl Pts',(207.025733987093,-2.91637240029103,126.844063269472));
#18158=CARTESIAN_POINT('Ctrl Pts',(207.017973462873,-3.0268014903987,126.925383514462));
#18159=CARTESIAN_POINT('Ctrl Pts',(207.010212938653,-3.13373912581693,127.011261544638));
#18160=CARTESIAN_POINT('Ctrl Pts',(207.002452414433,-3.23680402931943,127.10135066102));
#18161=CARTESIAN_POINT('Ctrl Pts',(206.994679433281,-3.34003436913308,127.191584385416));
#18162=CARTESIAN_POINT('Ctrl Pts',(206.986906452129,-3.43937927123302,127.286042434095));
#18163=CARTESIAN_POINT('Ctrl Pts',(206.979133470977,-3.53449440489227,127.384341266117));
#18164=CARTESIAN_POINT('Ctrl Pts',(206.971644025391,-3.62614001730631,127.47905444491));
#18165=CARTESIAN_POINT('Ctrl Pts',(206.964154579804,-3.71385885862058,127.577332858762));
#18166=CARTESIAN_POINT('Ctrl Pts',(206.956665134218,-3.79738005623955,127.678806623316));
#18167=CARTESIAN_POINT('Ctrl Pts',(206.94892298064,-3.88371941628567,127.783704303698));
#18168=CARTESIAN_POINT('Ctrl Pts',(206.941180827061,-3.96585449861154,127.892359049907));
#18169=CARTESIAN_POINT('Ctrl Pts',(206.933438673483,-4.04343822436208,128.004398048483));
#18170=CARTESIAN_POINT('Ctrl Pts',(206.925706075313,-4.12092619585451,128.116298767914));
#18171=CARTESIAN_POINT('Ctrl Pts',(206.917973477143,-4.19387376171797,128.231575110578));
#18172=CARTESIAN_POINT('Ctrl Pts',(206.910240878973,-4.26197290981049,128.349819931706));
#18173=CARTESIAN_POINT('Ctrl Pts',(206.902517710807,-4.32998901010207,128.46792055173));
#18174=CARTESIAN_POINT('Ctrl Pts',(206.894794542642,-4.39316827069876,128.588982102231));
#18175=CARTESIAN_POINT('Ctrl Pts',(206.887071374476,-4.45124539391763,128.712567724943));
#18176=CARTESIAN_POINT('Ctrl Pts',(206.879353629328,-4.50928173682022,128.836066568895));
#18177=CARTESIAN_POINT('Ctrl Pts',(206.871635884179,-4.56222290117181,128.962085604511));
#18178=CARTESIAN_POINT('Ctrl Pts',(206.863918139031,-4.60984903856988,129.090162582304));
#18179=CARTESIAN_POINT('Ctrl Pts',(206.85620451266,-4.65744975902835,129.218171208453));
#18180=CARTESIAN_POINT('Ctrl Pts',(206.848490886289,-4.69974096176733,129.348235221746));
#18181=CARTESIAN_POINT('Ctrl Pts',(206.840777259918,-4.73655075729518,129.479872042279));
#18182=CARTESIAN_POINT('Ctrl Pts',(206.838778875329,-4.74608714453948,129.513975456281));
#18183=CARTESIAN_POINT('Ctrl Pts',(206.836780490739,-4.75525588437582,129.548184340443));
#18184=CARTESIAN_POINT('Ctrl Pts',(206.834782106149,-4.76405452823405,129.582490119308));
#18185=CARTESIAN_POINT('Ctrl Pts',(208.584593534951,-4.76405452823405,129.582490119308));
#18186=CARTESIAN_POINT('Ctrl Pts',(208.576017307781,-4.80157547937709,129.728783738355));
#18187=CARTESIAN_POINT('Ctrl Pts',(208.567441080611,-4.83239790014226,129.876978832491));
#18188=CARTESIAN_POINT('Ctrl Pts',(208.558864853441,-4.85634444651292,130.026477799062));
#18189=CARTESIAN_POINT('Ctrl Pts',(208.550327451534,-4.88018258496171,130.175299971911));
#18190=CARTESIAN_POINT('Ctrl Pts',(208.541790049627,-4.89720686488144,130.325414009242));
#18191=CARTESIAN_POINT('Ctrl Pts',(208.53325264772,-4.90729068591846,130.476212501012));
#18192=CARTESIAN_POINT('Ctrl Pts',(208.52712157716,-4.91453230567176,130.584507296483));
#18193=CARTESIAN_POINT('Ctrl Pts',(208.5209905066,-4.91819553250619,130.693154702108));
#18194=CARTESIAN_POINT('Ctrl Pts',(208.51485943604,-4.91824939693558,130.801925039035));
#18195=CARTESIAN_POINT('',(208.860140563973,-4.91824943730512,130.802007970582));
#18196=CARTESIAN_POINT('Ctrl Pts',(208.930233502018,-4.76405452823405,129.582490119308));
#18197=CARTESIAN_POINT('Ctrl Pts',(208.922447515776,-4.79817011116022,129.715506259361));
#18198=CARTESIAN_POINT('Ctrl Pts',(208.914661529535,-4.82667498858406,129.849813218037));
#18199=CARTESIAN_POINT('Ctrl Pts',(208.906875543294,-4.84950153322439,129.984898634461));
#18200=CARTESIAN_POINT('Ctrl Pts',(208.899986863779,-4.86969740123493,130.104415945698));
#18201=CARTESIAN_POINT('Ctrl Pts',(208.893098184264,-4.88544907649643,130.224542348731));
#18202=CARTESIAN_POINT('Ctrl Pts',(208.88620950475,-4.89674374081455,130.344922047904));
#18203=CARTESIAN_POINT('Ctrl Pts',(208.877519857836,-4.91099126745915,130.496773658817));
#18204=CARTESIAN_POINT('Ctrl Pts',(208.868830210922,-4.9181763870815,130.64929524746));
#18205=CARTESIAN_POINT('Ctrl Pts',(208.860140564008,-4.91824943730483,130.802007969968));
#18206=CARTESIAN_POINT('Ctrl Pts',(208.860140563973,-4.91824943730512,130.802007970582));
#18207=CARTESIAN_POINT('Ctrl Pts',(208.852452334247,-4.91831406901657,130.93712168745));
#18208=CARTESIAN_POINT('Ctrl Pts',(208.84476410452,-4.91280674963555,131.072453879537));
#18209=CARTESIAN_POINT('Ctrl Pts',(208.837075874794,-4.90169979502435,131.207501017375));
#18210=CARTESIAN_POINT('Ctrl Pts',(208.829396198239,-4.89060519692236,131.342397915002));
#18211=CARTESIAN_POINT('Ctrl Pts',(208.821716521683,-4.87392338696553,131.477009993859));
#18212=CARTESIAN_POINT('Ctrl Pts',(208.814036845128,-4.85167868744603,131.610832549056));
#18213=CARTESIAN_POINT('Ctrl Pts',(208.806363779643,-4.82945313733591,131.744539902748));
#18214=CARTESIAN_POINT('Ctrl Pts',(208.798690714157,-4.80167428999412,131.877458692401));
#18215=CARTESIAN_POINT('Ctrl Pts',(208.791017648672,-4.76841833750263,132.009088645408));
#18216=CARTESIAN_POINT('Ctrl Pts',(208.783348819167,-4.73518074423976,132.140645930992));
#18217=CARTESIAN_POINT('Ctrl Pts',(208.775679989662,-4.69647215728822,132.270915408287));
#18218=CARTESIAN_POINT('Ctrl Pts',(208.768011160158,-4.65241990971906,132.399406712872));
#18219=CARTESIAN_POINT('Ctrl Pts',(208.760344500522,-4.60838012658386,132.527861661278));
#18220=CARTESIAN_POINT('Ctrl Pts',(208.752677840887,-4.55899981853378,132.654539059235));
#18221=CARTESIAN_POINT('Ctrl Pts',(208.745011181251,-4.50445613078236,132.778963876035));
#18222=CARTESIAN_POINT('Ctrl Pts',(208.737344945431,-4.44991545822423,132.90338181459));
#18223=CARTESIAN_POINT('Ctrl Pts',(208.729678709611,-4.39021213419317,133.025547053232));
#18224=CARTESIAN_POINT('Ctrl Pts',(208.722012473791,-4.32557117553024,133.145005201419));
#18225=CARTESIAN_POINT('Ctrl Pts',(208.714344916315,-4.2609190727916,133.264483944144));
#18226=CARTESIAN_POINT('Ctrl Pts',(208.706677358839,-4.19132783308178,133.381254316553));
#18227=CARTESIAN_POINT('Ctrl Pts',(208.699009801363,-4.11706782546444,133.494887625984));
#18228=CARTESIAN_POINT('Ctrl Pts',(208.691334452229,-4.04273235593582,133.608636407888));
#18229=CARTESIAN_POINT('Ctrl Pts',(208.683659103096,-3.96371886154607,133.71924142412));
#18230=CARTESIAN_POINT('Ctrl Pts',(208.675983753962,-3.88034058749315,133.826303699021));
#18231=CARTESIAN_POINT('Ctrl Pts',(208.668304507765,-3.79691997915443,133.933420333466));
#18232=CARTESIAN_POINT('Ctrl Pts',(208.660625261568,-3.70913043605773,134.036990339263));
#18233=CARTESIAN_POINT('Ctrl Pts',(208.652946015371,-3.61732387877702,134.136649773466));
#18234=CARTESIAN_POINT('Ctrl Pts',(208.64525452406,-3.52537092928688,134.236468121861));
#18235=CARTESIAN_POINT('Ctrl Pts',(208.637563032748,-3.42938845130611,134.332363157705));
#18236=CARTESIAN_POINT('Ctrl Pts',(208.629871541437,-3.32976397282271,134.424009073948));
#18237=CARTESIAN_POINT('Ctrl Pts',(208.622501654603,-3.23430509462818,134.511822997684));
#18238=CARTESIAN_POINT('Ctrl Pts',(208.61513176777,-3.13550289223388,134.595735802233));
#18239=CARTESIAN_POINT('Ctrl Pts',(208.607761880937,-3.03372331873832,134.675498161989));
#18240=CARTESIAN_POINT('Ctrl Pts',(208.599996643283,-2.92648387336159,134.759539300387));
#18241=CARTESIAN_POINT('Ctrl Pts',(208.592231405629,-2.81557582884422,134.839257045366));
#18242=CARTESIAN_POINT('Ctrl Pts',(208.584466167976,-2.70138333523345,134.914313310557));
#18243=CARTESIAN_POINT('Ctrl Pts',(208.57671062275,-2.5873333746107,134.989275891887));
#18244=CARTESIAN_POINT('Ctrl Pts',(208.568955077524,-2.4700074457162,135.059588356404));
#18245=CARTESIAN_POINT('Ctrl Pts',(208.561199532298,-2.34982285338321,135.12495266267));
#18246=CARTESIAN_POINT('Ctrl Pts',(208.55345180014,-2.22975933703701,135.190251119831));
#18247=CARTESIAN_POINT('Ctrl Pts',(208.545704067981,-2.10684323005938,135.250611152222));
#18248=CARTESIAN_POINT('Ctrl Pts',(208.537956335823,-1.98152060362814,135.305778078755));
#18249=CARTESIAN_POINT('Ctrl Pts',(208.530214544241,-1.85629406837336,135.360902706024));
#18250=CARTESIAN_POINT('Ctrl Pts',(208.522472752659,-1.7286650435057,135.410841995268));
#18251=CARTESIAN_POINT('Ctrl Pts',(208.514730961078,-1.59910364588964,135.455387449589));
#18252=CARTESIAN_POINT('Ctrl Pts',(208.506992569679,-1.4695991514346,135.499913339618));
#18253=CARTESIAN_POINT('Ctrl Pts',(208.49925417828,-1.33816434213286,135.539049979232));
#18254=CARTESIAN_POINT('Ctrl Pts',(208.491515786881,-1.20528851144165,135.572637315356));
#18255=CARTESIAN_POINT('Ctrl Pts',(208.483779079378,-1.07244159491196,135.606217342779));
#18256=CARTESIAN_POINT('Ctrl Pts',(208.476042371875,-0.938154660477446,
135.634250372453));
#18257=CARTESIAN_POINT('Ctrl Pts',(208.468305664372,-0.802930941415024,
135.656626579549));
#18258=CARTESIAN_POINT('Ctrl Pts',(208.460568954138,-0.667707174624105,
135.679002794542));
#18259=CARTESIAN_POINT('Ctrl Pts',(208.452832243905,-0.531547009266178,
135.695722118751));
#18260=CARTESIAN_POINT('Ctrl Pts',(208.445095533671,-0.394962211773451,
135.706726160217));
#18261=CARTESIAN_POINT('Ctrl Pts',(208.437357134427,-0.258347596300371,
135.717732603987));
#18262=CARTESIAN_POINT('Ctrl Pts',(208.429618735184,-0.121308554920572,
135.723021250898));
#18263=CARTESIAN_POINT('Ctrl Pts',(208.42188033594,0.0156401187563764,135.722585749581));
#18264=CARTESIAN_POINT('Ctrl Pts',(208.414133720282,0.152734200677577,135.722149785862));
#18265=CARTESIAN_POINT('Ctrl Pts',(208.406387104625,0.289737330576747,135.715977534255));
#18266=CARTESIAN_POINT('Ctrl Pts',(208.398640488967,0.426136266850155,135.704114789417));
#18267=CARTESIAN_POINT('Ctrl Pts',(208.390889759046,0.562607645212518,135.692245744223));
#18268=CARTESIAN_POINT('Ctrl Pts',(208.383139029126,0.698473801993175,135.674680234289));
#18269=CARTESIAN_POINT('Ctrl Pts',(208.375388299206,0.833229720990087,135.651515586675));
#18270=CARTESIAN_POINT('Ctrl Pts',(208.367625056951,0.968203182214324,135.628313543383));
#18271=CARTESIAN_POINT('Ctrl Pts',(208.359861814697,1.10206244061413,135.59949438239));
#18272=CARTESIAN_POINT('Ctrl Pts',(208.352098572443,1.23431484450832,135.565206123054));
#18273=CARTESIAN_POINT('Ctrl Pts',(208.34450380067,1.36369723283556,135.531661954829));
#18274=CARTESIAN_POINT('Ctrl Pts',(208.336909028897,1.4915414917313,135.492883804827));
#18275=CARTESIAN_POINT('Ctrl Pts',(208.329314257124,1.61740511662782,135.449054768014));
#18276=CARTESIAN_POINT('Ctrl Pts',(208.321537400431,1.7462863263438,135.404174928507));
#18277=CARTESIAN_POINT('Ctrl Pts',(208.313760543739,1.87350126461924,135.353855985428));
#18278=CARTESIAN_POINT('Ctrl Pts',(208.305983687046,1.99855688905477,135.298240169102));
#18279=CARTESIAN_POINT('Ctrl Pts',(208.298216395952,2.12345869403154,135.242692760692));
#18280=CARTESIAN_POINT('Ctrl Pts',(208.290449104858,2.24620611628277,135.181861599773));
#18281=CARTESIAN_POINT('Ctrl Pts',(208.282681813764,2.36632204495425,135.115938407896));
#18282=CARTESIAN_POINT('Ctrl Pts',(208.274922221987,2.48631890886508,135.050080562298));
#18283=CARTESIAN_POINT('Ctrl Pts',(208.26716263021,2.60368912995268,134.97914091734));
#18284=CARTESIAN_POINT('Ctrl Pts',(208.259403038434,2.71797666759268,134.903358775277));
#18285=CARTESIAN_POINT('Ctrl Pts',(208.251649286353,2.8321781949754,134.827633665168));
#18286=CARTESIAN_POINT('Ctrl Pts',(208.243895534272,2.94330133242635,134.747073526959));
#18287=CARTESIAN_POINT('Ctrl Pts',(208.236141782192,3.05091601399587,134.661962792239));
#18288=CARTESIAN_POINT('Ctrl Pts',(208.228391318654,3.1584850537225,134.576888154925));
#18289=CARTESIAN_POINT('Ctrl Pts',(208.220640855117,3.26254829138391,134.487267001654));
#18290=CARTESIAN_POINT('Ctrl Pts',(208.212890391579,3.36270614264577,134.393426019688));
#18291=CARTESIAN_POINT('Ctrl Pts',(208.205141545516,3.46284309157885,134.29960462176));
#18292=CARTESIAN_POINT('Ctrl Pts',(208.197392699453,3.55907599036995,134.201565413779));
#18293=CARTESIAN_POINT('Ctrl Pts',(208.18964385339,3.65104005214414,134.099673895562));
#18294=CARTESIAN_POINT('Ctrl Pts',(208.181894949397,3.74300480143419,133.997781615613));
#18295=CARTESIAN_POINT('Ctrl Pts',(208.174146045404,3.8307003882748,133.89203725798));
#18296=CARTESIAN_POINT('Ctrl Pts',(208.166397141411,3.91380073916163,133.782841243093));
#18297=CARTESIAN_POINT('Ctrl Pts',(208.158646504403,3.99691967514536,133.673620806907));
#18298=CARTESIAN_POINT('Ctrl Pts',(208.150895867395,4.0754410935826,133.560947488181));
#18299=CARTESIAN_POINT('Ctrl Pts',(208.143145230388,4.14908110408418,133.4452523333));
#18300=CARTESIAN_POINT('Ctrl Pts',(208.135386376025,4.22279918895488,133.329434516483));
#18301=CARTESIAN_POINT('Ctrl Pts',(208.127627521662,4.2916253174381,133.210588793658));
#18302=CARTESIAN_POINT('Ctrl Pts',(208.1198686673,4.3553203343671,133.089173049156));
#18303=CARTESIAN_POINT('Ctrl Pts',(208.112105678585,4.41904929156633,132.967692607549));
#18304=CARTESIAN_POINT('Ctrl Pts',(208.104342689871,4.47764152232339,132.84363976855));
#18305=CARTESIAN_POINT('Ctrl Pts',(208.096579701157,4.53090568215799,132.717493326473));
#18306=CARTESIAN_POINT('Ctrl Pts',(208.088804289908,4.58425507667346,132.591145021609));
#18307=CARTESIAN_POINT('Ctrl Pts',(208.081028878659,4.63225922547976,132.462696784975));
#18308=CARTESIAN_POINT('Ctrl Pts',(208.07325346741,4.67477612230475,132.332644383373));
#18309=CARTESIAN_POINT('Ctrl Pts',(208.065791189377,4.71558076852147,132.207829483103));
#18310=CARTESIAN_POINT('Ctrl Pts',(208.058328911344,4.7513314998731,132.081537413966));
#18311=CARTESIAN_POINT('Ctrl Pts',(208.050866633311,4.78194728272723,131.954214194209));
#18312=CARTESIAN_POINT('Ctrl Pts',(208.043091186579,4.81384791517326,131.821547613227));
#18313=CARTESIAN_POINT('Ctrl Pts',(208.035315739847,4.84027381515582,131.687343110404));
#18314=CARTESIAN_POINT('Ctrl Pts',(208.027540293115,4.861078124341,131.552092208147));
#18315=CARTESIAN_POINT('Ctrl Pts',(208.019774404755,4.88185685874992,131.417007570078));
#18316=CARTESIAN_POINT('Ctrl Pts',(208.012008516394,4.89702769371413,131.280879474633));
#18317=CARTESIAN_POINT('Ctrl Pts',(208.004242628033,4.90649401890281,131.144212798626));
#18318=CARTESIAN_POINT('Ctrl Pts',(207.996484430259,4.91595096955634,131.007681464108));
#18319=CARTESIAN_POINT('Ctrl Pts',(207.988726232485,4.91971462584261,130.870612997836));
#18320=CARTESIAN_POINT('Ctrl Pts',(207.980968034711,4.91773979670522,130.733520273117));
#18321=CARTESIAN_POINT('Ctrl Pts',(207.973215666403,4.91576645144328,130.596530559095));
#18322=CARTESIAN_POINT('Ctrl Pts',(207.965463298095,4.90806320893691,130.45951701213));
#18323=CARTESIAN_POINT('Ctrl Pts',(207.957710929787,4.89463688659452,130.322995048701));
#18324=CARTESIAN_POINT('Ctrl Pts',(207.949961829292,4.88121622377604,130.186530632626));
#18325=CARTESIAN_POINT('Ctrl Pts',(207.942212728797,4.86207731735958,130.050557776108));
#18326=CARTESIAN_POINT('Ctrl Pts',(207.934463628302,4.83727901203156,129.915589093349));
#18327=CARTESIAN_POINT('Ctrl Pts',(207.926716132436,4.81248584176035,129.780648358946));
#18328=CARTESIAN_POINT('Ctrl Pts',(207.91896863657,4.78203567415954,129.646711768862));
#18329=CARTESIAN_POINT('Ctrl Pts',(207.911221140703,4.74603881690609,129.514283638886));
#18330=CARTESIAN_POINT('Ctrl Pts',(207.903473572699,4.71004162447949,129.381854275848));
#18331=CARTESIAN_POINT('Ctrl Pts',(207.895726004694,4.66849774191739,129.25093377808));
#18332=CARTESIAN_POINT('Ctrl Pts',(207.88797843669,4.6215677813401,129.122012762639));
#18333=CARTESIAN_POINT('Ctrl Pts',(207.880229120088,4.57462722884883,128.993062650213));
#18334=CARTESIAN_POINT('Ctrl Pts',(207.872479803487,4.52229831304401,128.866113285295));
#18335=CARTESIAN_POINT('Ctrl Pts',(207.864730486886,4.46479021150502,128.74163634376));
#18336=CARTESIAN_POINT('Ctrl Pts',(207.856972920531,4.40722088809477,128.617026886786));
#18337=CARTESIAN_POINT('Ctrl Pts',(207.849215354176,4.34446152902774,128.494895466436));
#18338=CARTESIAN_POINT('Ctrl Pts',(207.841457787822,4.27676806979314,128.375690623578));
#18339=CARTESIAN_POINT('Ctrl Pts',(207.833696071523,4.20903839765145,128.256422011576));
#18340=CARTESIAN_POINT('Ctrl Pts',(207.825934355225,4.13636957280799,128.140083427958));
#18341=CARTESIAN_POINT('Ctrl Pts',(207.818172638927,4.05906096002361,128.027094482441));
#18342=CARTESIAN_POINT('Ctrl Pts',(207.810398460242,3.98162821878381,127.913924119321));
#18343=CARTESIAN_POINT('Ctrl Pts',(207.802624281556,3.8995410367762,127.804114454981));
#18344=CARTESIAN_POINT('Ctrl Pts',(207.794850102871,3.8131397215582,127.698052756717));
#18345=CARTESIAN_POINT('Ctrl Pts',(207.787373071747,3.73004086967696,127.596044988292));
#18346=CARTESIAN_POINT('Ctrl Pts',(207.779896040622,3.64295184134694,127.49750414666));
#18347=CARTESIAN_POINT('Ctrl Pts',(207.772419009498,3.55220619704574,127.402741268466));
#18348=CARTESIAN_POINT('Ctrl Pts',(207.764646018552,3.45786861039906,127.304227435639));
#18349=CARTESIAN_POINT('Ctrl Pts',(207.756873027606,3.35927983207107,127.209484418543));
#18350=CARTESIAN_POINT('Ctrl Pts',(207.74910003666,3.25677353337066,127.11890145827));
#18351=CARTESIAN_POINT('Ctrl Pts',(207.741336644219,3.15439381494258,127.028430354693));
#18352=CARTESIAN_POINT('Ctrl Pts',(207.733573251779,3.04810649162547,126.942109343302));
#18353=CARTESIAN_POINT('Ctrl Pts',(207.725809859339,2.93828365886333,126.860292641154));
#18354=CARTESIAN_POINT('Ctrl Pts',(207.718054194754,2.82857014621654,126.778557381191));
#18355=CARTESIAN_POINT('Ctrl Pts',(207.710298530169,2.71532843929129,126.701317739946));
#18356=CARTESIAN_POINT('Ctrl Pts',(207.702542865584,2.59896518359309,126.628889023007));
#18357=CARTESIAN_POINT('Ctrl Pts',(207.694793064922,2.48268990813262,126.556515068163));
#18358=CARTESIAN_POINT('Ctrl Pts',(207.687043264261,2.36329811229435,126.488945003391));
#18359=CARTESIAN_POINT('Ctrl Pts',(207.679293463599,2.24122672173557,126.426451773805));
#18360=CARTESIAN_POINT('Ctrl Pts',(207.671546974249,2.11920748947454,126.363985246139));
#18361=CARTESIAN_POINT('Ctrl Pts',(207.663800484899,1.99451128709021,126.306591417108));
#18362=CARTESIAN_POINT('Ctrl Pts',(207.656053995549,1.86760082988694,126.254497960001));
#18363=CARTESIAN_POINT('Ctrl Pts',(207.648309136959,1.74071708935821,126.202415469397));
#18364=CARTESIAN_POINT('Ctrl Pts',(207.640564278368,1.61162038276766,126.155631279747));
#18365=CARTESIAN_POINT('Ctrl Pts',(207.632819419778,1.48079428661614,126.114325293261));
#18366=CARTESIAN_POINT('Ctrl Pts',(207.625074512757,1.34996737237454,126.073019048479));
#18367=CARTESIAN_POINT('Ctrl Pts',(207.617329605736,1.2174114199546,126.037191193011));
#18368=CARTESIAN_POINT('Ctrl Pts',(207.609584698714,1.083625694819,126.006971909526));
#18369=CARTESIAN_POINT('Ctrl Pts',(207.601838064395,0.949810132293465,125.976745886424));
#18370=CARTESIAN_POINT('Ctrl Pts',(207.594091430076,0.814764632732653,125.952131010475));
#18371=CARTESIAN_POINT('Ctrl Pts',(207.586344795757,0.67899879684924,125.933206370739));
#18372=CARTESIAN_POINT('Ctrl Pts',(207.578589930427,0.543088706053562,125.914261623057));
#18373=CARTESIAN_POINT('Ctrl Pts',(207.570835065097,0.40645713800771,125.901019243266));
#18374=CARTESIAN_POINT('Ctrl Pts',(207.563080199768,0.269619519560986,125.893506478297));
#18375=CARTESIAN_POINT('Ctrl Pts',(207.555321198979,0.13270892933102,125.885989706975));
#18376=CARTESIAN_POINT('Ctrl Pts',(207.54756219819,-0.00440753934836094,
125.884208643743));
#18377=CARTESIAN_POINT('Ctrl Pts',(207.539803197401,-0.141215312361107,
125.888138358752));
#18378=CARTESIAN_POINT('Ctrl Pts',(207.532031731671,-0.278242868935376,
125.892074386903));
#18379=CARTESIAN_POINT('Ctrl Pts',(207.524260265942,-0.414960348456821,
125.901739499148));
#18380=CARTESIAN_POINT('Ctrl Pts',(207.516488800212,-0.550858244866477,
125.917056835667));
#18381=CARTESIAN_POINT('Ctrl Pts',(207.508982995369,-0.68211058829548,125.93185056218));
#18382=CARTESIAN_POINT('Ctrl Pts',(207.501477190527,-0.812598161887337,
125.951916317537));
#18383=CARTESIAN_POINT('Ctrl Pts',(207.493971385685,-0.941873648865784,
125.977140186296));
#18384=CARTESIAN_POINT('Ctrl Pts',(207.486196594231,-1.07578200013542,126.003268006481));
#18385=CARTESIAN_POINT('Ctrl Pts',(207.478421802777,-1.20881423660003,126.035013372608));
#18386=CARTESIAN_POINT('Ctrl Pts',(207.470647011323,-1.34046233494028,126.072305694902));
#18387=CARTESIAN_POINT('Ctrl Pts',(207.462881797475,-1.4719482586946,126.109552077552));
#18388=CARTESIAN_POINT('Ctrl Pts',(207.455116583626,-1.60205306444991,126.152331714816));
#18389=CARTESIAN_POINT('Ctrl Pts',(207.447351369778,-1.730277452876,126.200522762193));
#18390=CARTESIAN_POINT('Ctrl Pts',(207.43959386494,-1.85837454498173,126.248665967321));
#18391=CARTESIAN_POINT('Ctrl Pts',(207.431836360103,-1.9845945712413,126.302209754889));
#18392=CARTESIAN_POINT('Ctrl Pts',(207.424078855265,-2.1084523176746,126.360982185945));
#18393=CARTESIAN_POINT('Ctrl Pts',(207.416327197528,-2.23221670822011,126.419710318178));
#18394=CARTESIAN_POINT('Ctrl Pts',(207.408575539791,-2.35362201124919,126.483659082629));
#18395=CARTESIAN_POINT('Ctrl Pts',(207.400823882054,-2.47220230444564,126.552608175526));
#18396=CARTESIAN_POINT('Ctrl Pts',(207.393075516576,-2.59073223460783,126.62152798459));
#18397=CARTESIAN_POINT('Ctrl Pts',(207.385327151098,-2.70643920407983,126.695443702083));
#18398=CARTESIAN_POINT('Ctrl Pts',(207.37757878562,-2.81888145468325,126.774088864081));
#18399=CARTESIAN_POINT('Ctrl Pts',(207.36983203956,-2.93130020471219,126.852717589139));
#18400=CARTESIAN_POINT('Ctrl Pts',(207.3620852935,-3.04045527293811,126.936073568687));
#18401=CARTESIAN_POINT('Ctrl Pts',(207.354338547441,-3.14593382962058,127.023846974931));
#18402=CARTESIAN_POINT('Ctrl Pts',(207.346591743372,-3.25141317614579,127.111621038439));
#18403=CARTESIAN_POINT('Ctrl Pts',(207.338844939303,-3.35321565571256,127.2038123446));
#18404=CARTESIAN_POINT('Ctrl Pts',(207.331098135234,-3.45096179879728,127.30007099972));
#18405=CARTESIAN_POINT('Ctrl Pts',(207.323349596046,-3.54872983493361,127.396351214726));
#18406=CARTESIAN_POINT('Ctrl Pts',(207.315601056858,-3.64243944823346,127.496700317242));
#18407=CARTESIAN_POINT('Ctrl Pts',(207.307852517671,-3.73174857627695,127.600732108211));
#18408=CARTESIAN_POINT('Ctrl Pts',(207.300095745817,-3.82115259346241,127.704874430852));
#18409=CARTESIAN_POINT('Ctrl Pts',(207.292338973963,-3.9061465306836,127.812706961073));
#18410=CARTESIAN_POINT('Ctrl Pts',(207.284582202109,-3.98642879758559,127.923810582541));
#18411=CARTESIAN_POINT('Ctrl Pts',(207.276821290866,-4.06675390699494,128.034973494286));
#18412=CARTESIAN_POINT('Ctrl Pts',(207.269060379623,-4.14236212057786,128.149410649576));
#18413=CARTESIAN_POINT('Ctrl Pts',(207.26129946838,-4.21299620893864,128.266675450732));
#18414=CARTESIAN_POINT('Ctrl Pts',(207.253526104808,-4.28374362920411,128.384128402448));
#18415=CARTESIAN_POINT('Ctrl Pts',(207.245752741237,-4.34950078814551,128.504417723078));
#18416=CARTESIAN_POINT('Ctrl Pts',(207.237979377665,-4.41005688764098,128.627073013626));
#18417=CARTESIAN_POINT('Ctrl Pts',(207.230494172401,-4.46836817471339,128.74518147698));
#18418=CARTESIAN_POINT('Ctrl Pts',(207.223008967137,-4.52185704933858,128.865483326389));
#18419=CARTESIAN_POINT('Ctrl Pts',(207.215523761872,-4.57037874948208,128.987544405402));
#18420=CARTESIAN_POINT('Ctrl Pts',(207.206734347059,-4.6273547888774,129.130873201093));
#18421=CARTESIAN_POINT('Ctrl Pts',(207.197944932245,-4.67763395894565,129.2770080242));
#18422=CARTESIAN_POINT('Ctrl Pts',(207.189155517432,-4.72096468861576,129.425348118949));
#18423=CARTESIAN_POINT('Ctrl Pts',(207.186067457766,-4.73618844143788,129.47746570278));
#18424=CARTESIAN_POINT('Ctrl Pts',(207.1829793981,-4.75055490266602,129.529855284104));
#18425=CARTESIAN_POINT('Ctrl Pts',(207.179891338435,-4.76405452823404,129.582490119308));
#18426=CARTESIAN_POINT('Origin',(213.235140564004,0.,130.804360617566));
#18427=CARTESIAN_POINT('',(205.084976592678,-4.76405452823405,129.582490119308));
#18428=CARTESIAN_POINT('',(205.430026442963,-4.76405452823405,129.582490119308));
#18429=CARTESIAN_POINT('',(213.235140564004,-4.76405452823405,129.582490119308));
#18430=CARTESIAN_POINT('',(206.764859435946,-4.91824826123457,130.808496238813));
#18431=CARTESIAN_POINT('Ctrl Pts',(206.764859435946,-4.91824826123457,130.808496238813));
#18432=CARTESIAN_POINT('Ctrl Pts',(206.755633759936,-4.91811095036783,130.971791882044));
#18433=CARTESIAN_POINT('Ctrl Pts',(206.746408083927,-4.9098372427412,131.134736331661));
#18434=CARTESIAN_POINT('Ctrl Pts',(206.737182407917,-4.89355472835045,131.296605661359));
#18435=CARTESIAN_POINT('Ctrl Pts',(206.727886086852,-4.87714753159103,131.459714495655));
#18436=CARTESIAN_POINT('Ctrl Pts',(206.718589765787,-4.85260850573713,131.621731650502));
#18437=CARTESIAN_POINT('Ctrl Pts',(206.709293444722,-4.82011683649341,131.781937594102));
#18438=CARTESIAN_POINT('Ctrl Pts',(206.699922676766,-4.7873649671415,131.94342650053));
#18439=CARTESIAN_POINT('Ctrl Pts',(206.69055190881,-4.74653262850223,132.103075044456));
#18440=CARTESIAN_POINT('Ctrl Pts',(206.681181140855,-4.69785138332069,132.260168105777));
#18441=CARTESIAN_POINT('Ctrl Pts',(206.680193264038,-4.69271935212153,132.27672903163));
#18442=CARTESIAN_POINT('Ctrl Pts',(206.679205387222,-4.68750013448521,132.293261576894));
#18443=CARTESIAN_POINT('Ctrl Pts',(206.678217510405,-4.68219403218519,132.309764917902));
#18444=CARTESIAN_POINT('Ctrl Pts',(206.670443203729,-4.64043653180415,132.439641469363));
#18445=CARTESIAN_POINT('Ctrl Pts',(206.662668897052,-4.59320493957362,132.567985005214));
#18446=CARTESIAN_POINT('Ctrl Pts',(206.654894590376,-4.54062928664211,132.694299437684));
#18447=CARTESIAN_POINT('Ctrl Pts',(206.647129865258,-4.48811843135327,132.820458192059));
#18448=CARTESIAN_POINT('Ctrl Pts',(206.639365140141,-4.43027676906317,132.944592461411));
#18449=CARTESIAN_POINT('Ctrl Pts',(206.631600415024,-4.36728419816986,133.066220868536));
#18450=CARTESIAN_POINT('Ctrl Pts',(206.623843402325,-4.30435419549641,133.187728466606));
#18451=CARTESIAN_POINT('Ctrl Pts',(206.616086389625,-4.23628364434482,133.306734810711));
#18452=CARTESIAN_POINT('Ctrl Pts',(206.608329376926,-4.16330052534937,133.422778421914));
#18453=CARTESIAN_POINT('Ctrl Pts',(206.600578214196,-4.09037244674563,133.538734518553));
#18454=CARTESIAN_POINT('Ctrl Pts',(206.592827051467,-4.01253938183014,133.651732000017));
#18455=CARTESIAN_POINT('Ctrl Pts',(206.585075888737,-3.93007506123518,133.761334252139));
#18456=CARTESIAN_POINT('Ctrl Pts',(206.577328020864,-3.84764579449751,133.870889914636));
#18457=CARTESIAN_POINT('Ctrl Pts',(206.569580152991,-3.76058942214285,133.977052906525));
#18458=CARTESIAN_POINT('Ctrl Pts',(206.561832285118,-3.66922266005811,134.079416057313));
#18459=CARTESIAN_POINT('Ctrl Pts',(206.554086038175,-3.577875012784,134.181757792739));
#18460=CARTESIAN_POINT('Ctrl Pts',(206.546339791231,-3.48221902964024,134.280300976796));
#18461=CARTESIAN_POINT('Ctrl Pts',(206.538593544287,-3.38261107228556,134.374672284095));
#18462=CARTESIAN_POINT('Ctrl Pts',(206.530847240371,-3.28300238233128,134.469044285479));
#18463=CARTESIAN_POINT('Ctrl Pts',(206.523100936455,-3.17944194398242,134.559244079983));
#18464=CARTESIAN_POINT('Ctrl Pts',(206.515354632539,-3.07232196606475,134.644936199342));
#18465=CARTESIAN_POINT('Ctrl Pts',(206.507606594067,-2.96517800179731,134.730647506916));
#18466=CARTESIAN_POINT('Ctrl Pts',(206.499858555595,-2.85447321715903,134.811848886652));
#18467=CARTESIAN_POINT('Ctrl Pts',(206.492110517123,-2.74063145552457,134.888246302485));
#18468=CARTESIAN_POINT('Ctrl Pts',(206.484354244035,-2.62666870285167,134.964724913502));
#18469=CARTESIAN_POINT('Ctrl Pts',(206.476597970948,-2.50956263835897,135.036389143314));
#18470=CARTESIAN_POINT('Ctrl Pts',(206.46884169786,-2.38976501336611,135.102989031769));
#18471=CARTESIAN_POINT('Ctrl Pts',(206.461081285113,-2.26990345028647,135.169624465748));
#18472=CARTESIAN_POINT('Ctrl Pts',(206.453320872367,-2.14734781348686,135.231189997141));
#18473=CARTESIAN_POINT('Ctrl Pts',(206.44556045962,-2.02257190409865,135.28748296201));
#18474=CARTESIAN_POINT('Ctrl Pts',(206.437787589017,-1.8975956908752,135.343866294457));
#18475=CARTESIAN_POINT('Ctrl Pts',(206.430014718413,-1.77039244561536,135.394960000609));
#18476=CARTESIAN_POINT('Ctrl Pts',(206.422241847809,-1.64145412060007,135.440610333928));
#18477=CARTESIAN_POINT('Ctrl Pts',(206.41475119407,-1.5171972796397,135.484603198007));
#18478=CARTESIAN_POINT('Ctrl Pts',(206.407260540331,-1.39132946298595,135.523541019782));
#18479=CARTESIAN_POINT('Ctrl Pts',(206.399769886592,-1.26429990602564,135.557331142419));
#18480=CARTESIAN_POINT('Ctrl Pts',(206.391995539368,-1.13245935939483,135.592400998174));
#18481=CARTESIAN_POINT('Ctrl Pts',(206.384221192143,-0.998949706372701,
135.622036643276));
#18482=CARTESIAN_POINT('Ctrl Pts',(206.376446844919,-0.864258611065781,
135.646079332619));
#18483=CARTESIAN_POINT('Ctrl Pts',(206.368682078737,-0.72973350798047,135.670092391946));
#18484=CARTESIAN_POINT('Ctrl Pts',(206.360917312556,-0.594030240801939,
135.688526141918));
#18485=CARTESIAN_POINT('Ctrl Pts',(206.353152546374,-0.457651051086741,
135.70127174377));
#18486=CARTESIAN_POINT('Ctrl Pts',(206.345395492141,-0.321407312868765,
135.71400468672));
#18487=CARTESIAN_POINT('Ctrl Pts',(206.337638437907,-0.184489374829276,
135.721060688077));
#18488=CARTESIAN_POINT('Ctrl Pts',(206.329881383673,-0.0474087266159011,
135.722382117635));
#18489=CARTESIAN_POINT('Ctrl Pts',(206.322130178985,0.0895685499512351,
135.723702550711));
#18490=CARTESIAN_POINT('Ctrl Pts',(206.314378974297,0.226707903104169,135.719297015699));
#18491=CARTESIAN_POINT('Ctrl Pts',(206.306627769608,0.363494034138324,135.709159813216));
#18492=CARTESIAN_POINT('Ctrl Pts',(206.298879859279,0.500222029349606,135.699026919171));
#18493=CARTESIAN_POINT('Ctrl Pts',(206.29113194895,0.636596711948773,135.68316723157));
#18494=CARTESIAN_POINT('Ctrl Pts',(206.283384038621,0.772104320862591,135.661627130761));
#18495=CARTESIAN_POINT('Ctrl Pts',(206.275637748924,0.907583585626675,135.640091535498));
#18496=CARTESIAN_POINT('Ctrl Pts',(206.267891459227,1.04219575158091,135.612877951706));
#18497=CARTESIAN_POINT('Ctrl Pts',(206.26014516953,1.17543410337159,135.580084408902));
#18498=CARTESIAN_POINT('Ctrl Pts',(206.252398822603,1.30867343952879,135.547290623819));
#18499=CARTESIAN_POINT('Ctrl Pts',(206.244652475676,1.44053856163545,135.508916890901));
#18500=CARTESIAN_POINT('Ctrl Pts',(206.236906128749,1.57053522864704,135.465111861526));
#18501=CARTESIAN_POINT('Ctrl Pts',(206.229158047049,1.70056100805719,135.421297022135));
#18502=CARTESIAN_POINT('Ctrl Pts',(206.221409965348,1.8287171293106,135.372048590765));
#18503=CARTESIAN_POINT('Ctrl Pts',(206.213661883648,1.95452711044093,135.317564228866));
#18504=CARTESIAN_POINT('Ctrl Pts',(206.20590556723,2.08047080333817,135.263021960589));
#18505=CARTESIAN_POINT('Ctrl Pts',(206.198149250812,2.2040630157501,135.203232801142));
#18506=CARTESIAN_POINT('Ctrl Pts',(206.190392934394,2.32484926327892,135.138441715738));
#18507=CARTESIAN_POINT('Ctrl Pts',(206.182632478194,2.44569997811104,135.073616049356));
#18508=CARTESIAN_POINT('Ctrl Pts',(206.174872021993,2.5637414075819,135.003783336419));
#18509=CARTESIAN_POINT('Ctrl Pts',(206.167111565792,2.67854694058481,134.929232657955));
#18510=CARTESIAN_POINT('Ctrl Pts',(206.159338651962,2.79353676750179,134.8545623055));
#18511=CARTESIAN_POINT('Ctrl Pts',(206.151565738131,2.90527999882711,134.775159079624));
#18512=CARTESIAN_POINT('Ctrl Pts',(206.143792824301,3.01338136800174,134.691353773397));
#18513=CARTESIAN_POINT('Ctrl Pts',(206.136302637127,3.1175507318328,134.61059674412));
#18514=CARTESIAN_POINT('Ctrl Pts',(206.128812449953,3.21833832869957,134.525752506211));
#18515=CARTESIAN_POINT('Ctrl Pts',(206.12132226278,3.31542344251232,134.43714886619));
#18516=CARTESIAN_POINT('Ctrl Pts',(206.113547928467,3.41619156940981,134.345183965593));
#18517=CARTESIAN_POINT('Ctrl Pts',(206.105773594154,3.51328995165438,134.248877485937));
#18518=CARTESIAN_POINT('Ctrl Pts',(206.097999259841,3.60632143845033,134.148553905203));
#18519=CARTESIAN_POINT('Ctrl Pts',(206.090234506665,3.69923827267255,134.048353963863));
#18520=CARTESIAN_POINT('Ctrl Pts',(206.082469753489,3.78809792067824,133.944147055788));
#18521=CARTESIAN_POINT('Ctrl Pts',(206.074705000313,3.87253733969881,133.836296899076));
#18522=CARTESIAN_POINT('Ctrl Pts',(206.066947959165,3.95689289267469,133.72855386018));
#18523=CARTESIAN_POINT('Ctrl Pts',(206.059190918017,4.03683671393217,133.617175079492));
#18524=CARTESIAN_POINT('Ctrl Pts',(206.051433876869,4.11204384499684,133.502559735371));
#18525=CARTESIAN_POINT('Ctrl Pts',(206.043682685331,4.18719426211104,133.388030823066));
#18526=CARTESIAN_POINT('Ctrl Pts',(206.035931493794,4.2576148851709,133.270270530956));
#18527=CARTESIAN_POINT('Ctrl Pts',(206.028180302257,4.32302238761605,133.14970931204));
#18528=CARTESIAN_POINT('Ctrl Pts',(206.020432405131,4.38840209056044,133.029199334061));
#18529=CARTESIAN_POINT('Ctrl Pts',(206.012684508006,4.44877272459587,132.90589113992));
#18530=CARTESIAN_POINT('Ctrl Pts',(206.00493661088,4.50389561038913,132.780242039417));
#18531=CARTESIAN_POINT('Ctrl Pts',(205.997190334417,4.55900696588485,132.654619221492));
#18532=CARTESIAN_POINT('Ctrl Pts',(205.989444057953,4.60887259954457,132.52665682896));
#18533=CARTESIAN_POINT('Ctrl Pts',(205.98169778149,4.65330109429353,132.396834161568));
#18534=CARTESIAN_POINT('Ctrl Pts',(205.973951447814,4.69772991718062,132.267010535338));
#18535=CARTESIAN_POINT('Ctrl Pts',(205.966205114138,4.73672139443581,132.135326976735));
#18536=CARTESIAN_POINT('Ctrl Pts',(205.958458780463,4.77013344123859,132.002279652926));
#18537=CARTESIAN_POINT('Ctrl Pts',(205.950710712019,4.80355297056946,131.869202533566));
#18538=CARTESIAN_POINT('Ctrl Pts',(205.942962643575,4.83139048788632,131.734761420386));
#18539=CARTESIAN_POINT('Ctrl Pts',(205.935214575131,4.85355474113685,131.599464030518));
#18540=CARTESIAN_POINT('Ctrl Pts',(205.927458271901,4.87574255095105,131.464022844171));
#18541=CARTESIAN_POINT('Ctrl Pts',(205.919701968672,4.89224498852538,131.327723949617));
#18542=CARTESIAN_POINT('Ctrl Pts',(205.911945665443,4.90302249002199,131.191082125681));
#18543=CARTESIAN_POINT('Ctrl Pts',(205.904185222415,4.91380574383149,131.054367371435));
#18544=CARTESIAN_POINT('Ctrl Pts',(205.896424779388,4.91885795864703,130.917309713606));
#18545=CARTESIAN_POINT('Ctrl Pts',(205.88866433636,4.91819175271269,130.780424326105));
#18546=CARTESIAN_POINT('Ctrl Pts',(205.880891435541,4.91752447732209,130.643319197341));
#18547=CARTESIAN_POINT('Ctrl Pts',(205.873118534722,4.91112045540052,130.506387282292));
#18548=CARTESIAN_POINT('Ctrl Pts',(205.865345633904,4.89904434121163,130.370139930193));
#18549=CARTESIAN_POINT('Ctrl Pts',(205.857855302258,4.8874072314151,130.238845594031));
#18550=CARTESIAN_POINT('Ctrl Pts',(205.850364970613,4.87050330540731,130.108187218426));
#18551=CARTESIAN_POINT('Ctrl Pts',(205.842874638967,4.84843500802732,129.978611844975));
#18552=CARTESIAN_POINT('Ctrl Pts',(205.835100308635,4.82552998301369,129.844123573455));
#18553=CARTESIAN_POINT('Ctrl Pts',(205.827325978302,4.79698868437903,129.710376028441));
#18554=CARTESIAN_POINT('Ctrl Pts',(205.81955164797,4.76286943415894,129.577878731987));
#18555=CARTESIAN_POINT('Ctrl Pts',(205.811786898866,4.72879223313221,129.445544727644));
#18556=CARTESIAN_POINT('Ctrl Pts',(205.804022149762,4.68915085502848,129.31445828105));
#18557=CARTESIAN_POINT('Ctrl Pts',(205.796257400658,4.64405507193892,129.185121428534));
#18558=CARTESIAN_POINT('Ctrl Pts',(205.788500363668,4.59900407893947,129.055913036128));
#18559=CARTESIAN_POINT('Ctrl Pts',(205.780743326677,4.54850958977095,128.928451146412));
#18560=CARTESIAN_POINT('Ctrl Pts',(205.772986289687,4.49273179575291,128.803224921535));
#18561=CARTESIAN_POINT('Ctrl Pts',(205.765235102389,4.43699606456529,128.67809313154));
#18562=CARTESIAN_POINT('Ctrl Pts',(205.757483915091,4.37598511729972,128.555194006304));
#18563=CARTESIAN_POINT('Ctrl Pts',(205.749732727793,4.30990796060895,128.434998586643));
#18564=CARTESIAN_POINT('Ctrl Pts',(205.741984835016,4.24385888898434,128.314854254173));
#18565=CARTESIAN_POINT('Ctrl Pts',(205.73423694224,4.17274807866374,128.197411683559));
#18566=CARTESIAN_POINT('Ctrl Pts',(205.726489049463,4.09683126462683,128.083118869452));
#18567=CARTESIAN_POINT('Ctrl Pts',(205.718742777414,4.0209303311019,127.968849963467));
#18568=CARTESIAN_POINT('Ctrl Pts',(205.710996505366,3.94022560970842,127.85772982891));
#18569=CARTESIAN_POINT('Ctrl Pts',(205.703250233317,3.85501688262898,127.750178583511));
#18570=CARTESIAN_POINT('Ctrl Pts',(205.695503904118,3.76980752690164,127.642626544626));
#18571=CARTESIAN_POINT('Ctrl Pts',(205.68775757492,3.68009434196701,127.538643753886));
#18572=CARTESIAN_POINT('Ctrl Pts',(205.680011245721,3.58621796636794,127.438617941692));
#18573=CARTESIAN_POINT('Ctrl Pts',(205.672263181812,3.49232056812825,127.338569729755));
#18574=CARTESIAN_POINT('Ctrl Pts',(205.664515117904,3.39425839154965,127.242480544672));
#18575=CARTESIAN_POINT('Ctrl Pts',(205.656767053995,3.29240926887433,127.150701592872));
#18576=CARTESIAN_POINT('Ctrl Pts',(205.649010755368,3.19045189995416,127.058825097503));
#18577=CARTESIAN_POINT('Ctrl Pts',(205.641254456741,3.0846998358618,126.971268248513));
#18578=CARTESIAN_POINT('Ctrl Pts',(205.633498158114,2.97556478881364,126.888342582614));
#18579=CARTESIAN_POINT('Ctrl Pts',(205.625737719733,2.86637149332416,126.805372656956));
#18580=CARTESIAN_POINT('Ctrl Pts',(205.617977281351,2.75379193784736,126.727039062836));
#18581=CARTESIAN_POINT('Ctrl Pts',(205.61021684297,2.63826637271815,126.653609648273));
#18582=CARTESIAN_POINT('Ctrl Pts',(205.602443946826,2.52255535542982,126.580062358127));
#18583=CARTESIAN_POINT('Ctrl Pts',(205.594671050682,2.40388921667307,126.511435175415));
#18584=CARTESIAN_POINT('Ctrl Pts',(205.586898154538,2.2827331157452,126.447950101467));
#18585=CARTESIAN_POINT('Ctrl Pts',(205.579407774743,2.16598059601619,126.386772477791));
#18586=CARTESIAN_POINT('Ctrl Pts',(205.571917394949,2.04691625263489,126.330369789491));
#18587=CARTESIAN_POINT('Ctrl Pts',(205.564427015154,1.92597157701165,126.278897486897));
#18588=CARTESIAN_POINT('Ctrl Pts',(205.556652678921,1.80044195106122,126.225473895836));
#18589=CARTESIAN_POINT('Ctrl Pts',(205.548878342688,1.67248897498338,126.177192652376));
#18590=CARTESIAN_POINT('Ctrl Pts',(205.541104006456,1.54257284960153,126.134280097257));
#18591=CARTESIAN_POINT('Ctrl Pts',(205.533339251373,1.412816833816,126.091420427889));
#18592=CARTESIAN_POINT('Ctrl Pts',(205.525574496289,1.28110285028441,126.053916403621));
#18593=CARTESIAN_POINT('Ctrl Pts',(205.517809741206,1.14791261180821,126.021947032549));
#18594=CARTESIAN_POINT('Ctrl Pts',(205.510052698165,1.01485465937561,125.990009413817));
#18595=CARTESIAN_POINT('Ctrl Pts',(205.502295655124,0.88032374757524,125.963595599504));
#18596=CARTESIAN_POINT('Ctrl Pts',(205.494538612083,0.744818010538801,125.942835219743));
#18597=CARTESIAN_POINT('Ctrl Pts',(205.48678741867,0.609414459097139,125.922090495495));
#18598=CARTESIAN_POINT('Ctrl Pts',(205.479036225256,0.473037930525041,125.906990778956));
#18599=CARTESIAN_POINT('Ctrl Pts',(205.471285031842,0.33619769877146,125.897614835498));
#18600=CARTESIAN_POINT('Ctrl Pts',(205.463537132872,0.199415627413407,125.888242877042));
#18601=CARTESIAN_POINT('Ctrl Pts',(205.455789233902,0.0621706340948198,
125.884589879799));
#18602=CARTESIAN_POINT('Ctrl Pts',(205.448041334933,-0.0750221388880692,
125.88668283825));
#18603=CARTESIAN_POINT('Ctrl Pts',(205.440295056645,-0.212186214308715,
125.888775358903));
#18604=CARTESIAN_POINT('Ctrl Pts',(205.432548778357,-0.349297700448874,
125.896611438603));
#18605=CARTESIAN_POINT('Ctrl Pts',(205.424802500068,-0.485841100123671,
125.910165945515));
#18606=CARTESIAN_POINT('Ctrl Pts',(205.41705616459,-0.622385507893228,125.9237205525));
#18607=CARTESIAN_POINT('Ctrl Pts',(205.409309829111,-0.758361431775545,
125.942993632321));
#18608=CARTESIAN_POINT('Ctrl Pts',(205.401563493633,-0.89325853914859,125.967908173394));
#18609=CARTESIAN_POINT('Ctrl Pts',(205.393815423409,-1.02818585590989,125.992828293927));
#18610=CARTESIAN_POINT('Ctrl Pts',(205.386067353186,-1.16203349102794,126.02339231868));
#18611=CARTESIAN_POINT('Ctrl Pts',(205.378319282963,-1.29430173647038,126.059472201863));
#18612=CARTESIAN_POINT('Ctrl Pts',(205.370562978002,-1.42671055811762,126.095590431159));
#18613=CARTESIAN_POINT('Ctrl Pts',(205.36280667304,-1.55753625913267,126.137236126444));
#18614=CARTESIAN_POINT('Ctrl Pts',(205.355050368079,-1.68629419381508,126.184231295306));
#18615=CARTESIAN_POINT('Ctrl Pts',(205.347289923343,-1.81512085051228,126.231251546915));
#18616=CARTESIAN_POINT('Ctrl Pts',(205.339529478607,-1.94187718064387,126.283626812052));
#18617=CARTESIAN_POINT('Ctrl Pts',(205.331769033871,-2.06609986951013,126.341131473582));
#18618=CARTESIAN_POINT('Ctrl Pts',(205.323996131401,-2.19052197132574,126.398728446543));
#18619=CARTESIAN_POINT('Ctrl Pts',(205.316223228931,-2.31240195646745,126.461471091301));
#18620=CARTESIAN_POINT('Ctrl Pts',(205.308450326461,-2.43130161847012,126.52908805286));
#18621=CARTESIAN_POINT('Ctrl Pts',(205.300960014754,-2.54587857780558,126.594246739811));
#18622=CARTESIAN_POINT('Ctrl Pts',(205.293469703048,-2.65768789450607,126.663931314284));
#18623=CARTESIAN_POINT('Ctrl Pts',(205.285979391341,-2.7663655623862,126.737862783097));
#18624=CARTESIAN_POINT('Ctrl Pts',(205.278237672039,-2.87869092774278,126.814275715097));
#18625=CARTESIAN_POINT('Ctrl Pts',(205.270495952738,-2.98803353029666,126.895472526408));
#18626=CARTESIAN_POINT('Ctrl Pts',(205.262754233436,-3.09395614481765,126.981191979323));
#18627=CARTESIAN_POINT('Ctrl Pts',(205.255024754641,-3.19971128407027,127.066775900384));
#18628=CARTESIAN_POINT('Ctrl Pts',(205.247295275847,-3.30205689954337,127.156867976875));
#18629=CARTESIAN_POINT('Ctrl Pts',(205.239565797052,-3.40058421415425,127.251163456565));
#18630=CARTESIAN_POINT('Ctrl Pts',(205.231843383955,-3.4990214626426,127.345372738552));
#18631=CARTESIAN_POINT('Ctrl Pts',(205.224120970858,-3.59364706915702,127.443777510556));
#18632=CARTESIAN_POINT('Ctrl Pts',(205.216398557761,-3.68408468413249,127.546032349475));
#18633=CARTESIAN_POINT('Ctrl Pts',(205.208681492833,-3.77445966639361,127.648216371643));
#18634=CARTESIAN_POINT('Ctrl Pts',(205.200964427906,-3.86065216668493,127.75424486186));
#18635=CARTESIAN_POINT('Ctrl Pts',(205.193247362978,-3.94232245691661,127.863735393538));
#18636=CARTESIAN_POINT('Ctrl Pts',(205.185533932859,-4.02395427969229,127.97317435417));
#18637=CARTESIAN_POINT('Ctrl Pts',(205.177820502739,-4.1010678957911,128.086071795385));
#18638=CARTESIAN_POINT('Ctrl Pts',(205.17010707262,-4.17336396541682,128.202012394391));
#18639=CARTESIAN_POINT('Ctrl Pts',(205.162394028974,-4.24565641272213,128.317947184313));
#18640=CARTESIAN_POINT('Ctrl Pts',(205.154680985329,-4.31313157631286,128.436924499339));
#18641=CARTESIAN_POINT('Ctrl Pts',(205.146967941683,-4.37553364940197,128.558500349105));
#18642=CARTESIAN_POINT('Ctrl Pts',(205.139255293534,-4.43793252273594,128.680069964896));
#18643=CARTESIAN_POINT('Ctrl Pts',(205.131542645386,-4.49525864776658,128.804237496571));
#18644=CARTESIAN_POINT('Ctrl Pts',(205.123829997237,-4.54730272990832,128.930535400245));
#18645=CARTESIAN_POINT('Ctrl Pts',(205.116113219495,-4.59937467808288,129.056900927775));
#18646=CARTESIAN_POINT('Ctrl Pts',(205.108396441753,-4.64615878721881,129.185398739042));
#18647=CARTESIAN_POINT('Ctrl Pts',(205.100679664011,-4.68749433319855,129.315542314773));
#18648=CARTESIAN_POINT('Ctrl Pts',(205.0954453069,-4.71553259168844,129.403819828246));
#18649=CARTESIAN_POINT('Ctrl Pts',(205.090210949789,-4.74106497151865,129.49285418659));
#18650=CARTESIAN_POINT('Ctrl Pts',(205.084976592678,-4.76405452823405,129.582490119308));
#18651=CARTESIAN_POINT('Ctrl Pts',(206.834782106149,-4.76405452823405,129.582490119308));
#18652=CARTESIAN_POINT('Ctrl Pts',(206.827070043619,-4.79800979989384,129.714881208167));
#18653=CARTESIAN_POINT('Ctrl Pts',(206.819357981088,-4.82644926951694,129.84871625431));
#18654=CARTESIAN_POINT('Ctrl Pts',(206.811645918557,-4.84926402357277,129.983494311653));
#18655=CARTESIAN_POINT('Ctrl Pts',(206.803848171462,-4.8723322600444,130.119769815232));
#18656=CARTESIAN_POINT('Ctrl Pts',(206.796050424368,-4.8896499380063,130.257009012014));
#18657=CARTESIAN_POINT('Ctrl Pts',(206.788252677274,-4.90115795633873,130.394685441948));
#18658=CARTESIAN_POINT('Ctrl Pts',(206.78045493018,-4.91266597467115,130.532361871882));
#18659=CARTESIAN_POINT('Ctrl Pts',(206.772657183085,-4.9183643194193,130.67047511888));
#18660=CARTESIAN_POINT('Ctrl Pts',(206.764859435991,-4.91824826123525,130.80849623801));
#18661=CARTESIAN_POINT('',(207.110140564062,-4.91824906508338,130.801328076312));
#18662=CARTESIAN_POINT('Ctrl Pts',(207.179891338435,-4.76405452823404,129.582490119308));
#18663=CARTESIAN_POINT('Ctrl Pts',(207.171149836886,-4.80226849123941,129.731485781088));
#18664=CARTESIAN_POINT('Ctrl Pts',(207.162408335336,-4.83353292882372,129.882448181632));
#18665=CARTESIAN_POINT('Ctrl Pts',(207.153666833787,-4.85766325863286,130.034756350278));
#18666=CARTESIAN_POINT('Ctrl Pts',(207.14497546476,-4.88165520097116,130.186191031391));
#18667=CARTESIAN_POINT('Ctrl Pts',(207.136284095732,-4.89859453685566,130.338955897152));
#18668=CARTESIAN_POINT('Ctrl Pts',(207.127592726705,-4.90834771356455,130.492421865171));
#18669=CARTESIAN_POINT('Ctrl Pts',(207.121775339157,-4.91487580005554,130.595141127065));
#18670=CARTESIAN_POINT('Ctrl Pts',(207.11595795161,-4.91818546141412,130.698174100575));
#18671=CARTESIAN_POINT('Ctrl Pts',(207.110140564062,-4.91824906508338,130.801328076312));
#18672=CARTESIAN_POINT('Ctrl Pts',(207.110140564008,-4.91824906508397,130.801328077268));
#18673=CARTESIAN_POINT('Ctrl Pts',(207.10232974179,-4.91833446369157,130.939829657053));
#18674=CARTESIAN_POINT('Ctrl Pts',(207.094518919572,-4.91256506400957,131.078351340995));
#18675=CARTESIAN_POINT('Ctrl Pts',(207.086708097354,-4.90096241100966,131.216368515998));
#18676=CARTESIAN_POINT('Ctrl Pts',(207.078896410447,-4.88935847354873,131.354400970065));
#18677=CARTESIAN_POINT('Ctrl Pts',(207.071084723539,-4.87192002824314,131.491928423436));
#18678=CARTESIAN_POINT('Ctrl Pts',(207.063273036631,-4.84872054892325,131.62843106416));
#18679=CARTESIAN_POINT('Ctrl Pts',(207.055458899586,-4.82551379308231,131.764976518963));
#18680=CARTESIAN_POINT('Ctrl Pts',(207.047644762541,-4.79654246897585,131.90049614474));
#18681=CARTESIAN_POINT('Ctrl Pts',(207.039830625497,-4.76193119291241,132.034480276976));
#18682=CARTESIAN_POINT('Ctrl Pts',(207.032012451602,-4.72730203636823,132.168533626559));
#18683=CARTESIAN_POINT('Ctrl Pts',(207.024194277707,-4.68702722138493,132.301049533832));
#18684=CARTESIAN_POINT('Ctrl Pts',(207.016376103812,-4.64128115697165,132.431533713595));
#18685=CARTESIAN_POINT('Ctrl Pts',(207.008547530707,-4.59547424421175,132.562191454661));
#18686=CARTESIAN_POINT('Ctrl Pts',(207.000718957602,-4.54418167570927,132.690811711221));
#18687=CARTESIAN_POINT('Ctrl Pts',(206.992890384497,-4.48762617673331,132.816919774559));
#18688=CARTESIAN_POINT('Ctrl Pts',(206.985055811211,-4.43102733100928,132.943124492946));
#18689=CARTESIAN_POINT('Ctrl Pts',(206.977221237926,-4.36915768710697,133.066812840935));
#18690=CARTESIAN_POINT('Ctrl Pts',(206.96938666464,-4.30228542176686,133.187535645161));
#18691=CARTESIAN_POINT('Ctrl Pts',(206.961539696176,-4.23530735696238,133.308449446476));
#18692=CARTESIAN_POINT('Ctrl Pts',(206.953692727712,-4.16331106348637,133.426388009929));
#18693=CARTESIAN_POINT('Ctrl Pts',(206.945845759248,-4.08660777588555,133.540931455051));
#18694=CARTESIAN_POINT('Ctrl Pts',(206.942922552185,-4.05803373571842,133.583601972889));
#18695=CARTESIAN_POINT('Ctrl Pts',(206.939999345122,-4.02880687363292,133.625801664281));
#18696=CARTESIAN_POINT('Ctrl Pts',(206.937076138059,-3.99894465188146,133.667510060695));
#18697=CARTESIAN_POINT('Ctrl Pts',(206.929301998061,-3.91952739284056,133.77843169773));
#18698=CARTESIAN_POINT('Ctrl Pts',(206.921527858062,-3.83536570986394,133.886222330092));
#18699=CARTESIAN_POINT('Ctrl Pts',(206.913753718064,-3.74673486748187,133.990449269078));
#18700=CARTESIAN_POINT('Ctrl Pts',(206.905989161858,-3.658213287293,134.09454771934));
#18701=CARTESIAN_POINT('Ctrl Pts',(206.898224605652,-3.56523376076694,134.195090922469));
#18702=CARTESIAN_POINT('Ctrl Pts',(206.890460049446,-3.46811454805166,134.291675421838));
#18703=CARTESIAN_POINT('Ctrl Pts',(206.882703207698,-3.37109182792838,134.388163959878));
#18704=CARTESIAN_POINT('Ctrl Pts',(206.874946365951,-3.26993788205166,134.480701347399));
#18705=CARTESIAN_POINT('Ctrl Pts',(206.867189524203,-3.16501068250007,134.568917755153));
#18706=CARTESIAN_POINT('Ctrl Pts',(206.859438534277,-3.0601626408413,134.657067611766));
#18707=CARTESIAN_POINT('Ctrl Pts',(206.851687544352,-2.9515473094897,134.74090272641));
#18708=CARTESIAN_POINT('Ctrl Pts',(206.843936554426,-2.83955863515276,134.820090914788));
#18709=CARTESIAN_POINT('Ctrl Pts',(206.836188861569,-2.72761759787636,134.899245418577));
#18710=CARTESIAN_POINT('Ctrl Pts',(206.828441168712,-2.61230639015696,134.973756702305));
#18711=CARTESIAN_POINT('Ctrl Pts',(206.820693475855,-2.49405090237109,135.043333743086));
#18712=CARTESIAN_POINT('Ctrl Pts',(206.812947405249,-2.37582017552251,135.112896215471));
#18713=CARTESIAN_POINT('Ctrl Pts',(206.805201334644,-2.25464673160865,135.177526301768));
#18714=CARTESIAN_POINT('Ctrl Pts',(206.797455264038,-2.13098388076607,135.236977312298));
#18715=CARTESIAN_POINT('Ctrl Pts',(206.789709137619,-2.00732013888212,135.296428751197));
#18716=CARTESIAN_POINT('Ctrl Pts',(206.7819630112,-1.88116730665591,135.350700870453));
#18717=CARTESIAN_POINT('Ctrl Pts',(206.774216884781,-1.75300127162441,135.399593974446));
#18718=CARTESIAN_POINT('Ctrl Pts',(206.766469024802,-1.62480655341618,135.44849802057));
#18719=CARTESIAN_POINT('Ctrl Pts',(206.758721164823,-1.49459810110302,135.492020516664));
#18720=CARTESIAN_POINT('Ctrl Pts',(206.750973304844,-1.36286927639058,135.530010879485));
#18721=CARTESIAN_POINT('Ctrl Pts',(206.743217210822,-1.23100045680149,135.568041616583));
#18722=CARTESIAN_POINT('Ctrl Pts',(206.735461116801,-1.09760841340135,135.600528367403));
#18723=CARTESIAN_POINT('Ctrl Pts',(206.72770502278,-0.963199626022195,135.627371040832));
#18724=CARTESIAN_POINT('Ctrl Pts',(206.719944789696,-0.828719111006118,
135.654228038931));
#18725=CARTESIAN_POINT('Ctrl Pts',(206.712184556613,-0.693221156955318,
135.675434897598));
#18726=CARTESIAN_POINT('Ctrl Pts',(206.70442432353,-0.557218799917317,135.690943295831));
#18727=CARTESIAN_POINT('Ctrl Pts',(206.696651631796,-0.420998098163723,
135.706476591992));
#18728=CARTESIAN_POINT('Ctrl Pts',(206.688878940061,-0.284271765407574,
135.716293117923));
#18729=CARTESIAN_POINT('Ctrl Pts',(206.681106248327,-0.147555186392696,
135.720396676167));
#18730=CARTESIAN_POINT('Ctrl Pts',(206.6736136703,-0.015765624822631,135.724352349619));
#18731=CARTESIAN_POINT('Ctrl Pts',(206.666121092273,0.11601456527462,135.722999745079));
#18732=CARTESIAN_POINT('Ctrl Pts',(206.658628514246,0.247328944919121,135.716387842196));
#18733=CARTESIAN_POINT('Ctrl Pts',(206.650854101252,0.383582743781857,135.709527231134));
#18734=CARTESIAN_POINT('Ctrl Pts',(206.643079688257,0.519766647294013,135.696982181141));
#18735=CARTESIAN_POINT('Ctrl Pts',(206.635305275263,0.655367801387527,135.678750436549));
#18736=CARTESIAN_POINT('Ctrl Pts',(206.627540442734,0.790801853192383,135.660541159068));
#18737=CARTESIAN_POINT('Ctrl Pts',(206.619775610205,0.925654200685813,135.636659181934));
#18738=CARTESIAN_POINT('Ctrl Pts',(206.612010777677,1.05941334753652,135.607154223538));
#18739=CARTESIAN_POINT('Ctrl Pts',(206.604253656593,1.19303965490963,135.577678567237));
#18740=CARTESIAN_POINT('Ctrl Pts',(206.596496535509,1.32557454289324,135.542591126398));
#18741=CARTESIAN_POINT('Ctrl Pts',(206.588739414425,1.45651334525474,135.501993206179));
#18742=CARTESIAN_POINT('Ctrl Pts',(206.580988142457,1.5873534156012,135.461425898081));
#18743=CARTESIAN_POINT('Ctrl Pts',(206.573236870489,1.71659942391051,135.415356496345));
#18744=CARTESIAN_POINT('Ctrl Pts',(206.565485598521,1.84375893376221,135.363936919885));
#18745=CARTESIAN_POINT('Ctrl Pts',(206.557737620497,1.97086440649336,135.312539194452));
#18746=CARTESIAN_POINT('Ctrl Pts',(206.549989642474,2.09588478259786,135.255795962539));
#18747=CARTESIAN_POINT('Ctrl Pts',(206.542241664451,2.21834499216241,135.193908266043));
#18748=CARTESIAN_POINT('Ctrl Pts',(206.534495306817,2.34077959076295,135.132033512555));
#18749=CARTESIAN_POINT('Ctrl Pts',(206.526748949182,2.46065473910694,135.065016610731));
#18750=CARTESIAN_POINT('Ctrl Pts',(206.519002591548,2.57751784727511,134.993105633615));
#18751=CARTESIAN_POINT('Ctrl Pts',(206.511256176506,2.69438182151258,134.92119412357));
#18752=CARTESIAN_POINT('Ctrl Pts',(206.503509761464,2.80823337806547,134.844388670749));
#18753=CARTESIAN_POINT('Ctrl Pts',(206.495763346422,2.9186472625684,134.762981743565));
#18754=CARTESIAN_POINT('Ctrl Pts',(206.488015196492,3.0290858753689,134.681556584482));
#18755=CARTESIAN_POINT('Ctrl Pts',(206.480267046562,3.13608496949048,134.595528132329));
#18756=CARTESIAN_POINT('Ctrl Pts',(206.472518896633,3.23925116627507,134.505230102469));
#18757=CARTESIAN_POINT('Ctrl Pts',(206.464762512191,3.34252700513922,134.414836106449));
#18758=CARTESIAN_POINT('Ctrl Pts',(206.45700612775,3.44196151476943,134.320163726309));
#18759=CARTESIAN_POINT('Ctrl Pts',(206.449249743308,3.53719670723884,134.221585005399));
#18760=CARTESIAN_POINT('Ctrl Pts',(206.441489219088,3.63248272913906,134.122953670532));
#18761=CARTESIAN_POINT('Ctrl Pts',(206.433728694868,3.7235647084274,134.020412132682));
#18762=CARTESIAN_POINT('Ctrl Pts',(206.425968170648,3.81012466952417,133.914365933507));
#18763=CARTESIAN_POINT('Ctrl Pts',(206.418195189496,3.89682357375458,133.808149512546));
#18764=CARTESIAN_POINT('Ctrl Pts',(206.410422208344,3.9789857203556,133.698417501723));
#18765=CARTESIAN_POINT('Ctrl Pts',(206.402649227192,4.05633571762412,133.58560559211));
#18766=CARTESIAN_POINT('Ctrl Pts',(206.395159781606,4.13086421374525,133.47690873025));
#18767=CARTESIAN_POINT('Ctrl Pts',(206.387670336019,4.20092534590809,133.365353006456));
#18768=CARTESIAN_POINT('Ctrl Pts',(206.380180890433,4.266313865227,133.251348371085));
#18769=CARTESIAN_POINT('Ctrl Pts',(206.372406547022,4.33418975784089,133.133007009811));
#18770=CARTESIAN_POINT('Ctrl Pts',(206.36463220361,4.39724549814214,133.011651903751));
#18771=CARTESIAN_POINT('Ctrl Pts',(206.356857860199,4.45520197698344,132.887713301771));
#18772=CARTESIAN_POINT('Ctrl Pts',(206.349093097628,4.51308703219629,132.763927437583));
#18773=CARTESIAN_POINT('Ctrl Pts',(206.341328335058,4.56588516553323,132.637564763071));
#18774=CARTESIAN_POINT('Ctrl Pts',(206.333563572488,4.61336172857185,132.509082478706));
#18775=CARTESIAN_POINT('Ctrl Pts',(206.32580652166,4.66079113922843,132.380727799318));
#18776=CARTESIAN_POINT('Ctrl Pts',(206.318049470833,4.70290936280457,132.250258063749));
#18777=CARTESIAN_POINT('Ctrl Pts',(206.310292420006,4.73952884382674,132.118152610628));
#18778=CARTESIAN_POINT('Ctrl Pts',(206.302541218515,4.7761207113015,131.986146773889));
#18779=CARTESIAN_POINT('Ctrl Pts',(206.294790017025,4.80722198540851,131.852508049919));
#18780=CARTESIAN_POINT('Ctrl Pts',(206.287038815535,4.83269430378063,131.717732846565));
#18781=CARTESIAN_POINT('Ctrl Pts',(206.279290908073,4.85815579718011,131.583014918637));
#18782=CARTESIAN_POINT('Ctrl Pts',(206.271543000612,4.87799302016867,131.447161855274));
#18783=CARTESIAN_POINT('Ctrl Pts',(206.26379509315,4.89211832584772,131.310682006019));
#18784=CARTESIAN_POINT('Ctrl Pts',(206.256048806118,4.90624067730134,131.17423070073));
#18785=CARTESIAN_POINT('Ctrl Pts',(206.248302519086,4.9146534473754,131.037153258931));
#18786=CARTESIAN_POINT('Ctrl Pts',(206.240556232054,4.91732070875142,130.899964538952));
#18787=CARTESIAN_POINT('Ctrl Pts',(206.232809887587,4.91998798990394,130.762774801783));
#18788=CARTESIAN_POINT('Ctrl Pts',(206.22506354312,4.91690966975381,130.625474175676));
#18789=CARTESIAN_POINT('Ctrl Pts',(206.217317198653,4.90810194759419,130.488578517817));
#18790=CARTESIAN_POINT('Ctrl Pts',(206.209569119204,4.89929225273097,130.351652198845));
#18791=CARTESIAN_POINT('Ctrl Pts',(206.201821039754,4.88475062745858,130.21513141869));
#18792=CARTESIAN_POINT('Ctrl Pts',(206.194072960305,4.86454520291237,130.079527511726));
#18793=CARTESIAN_POINT('Ctrl Pts',(206.186316645792,4.84431830298384,129.943779477834));
#18794=CARTESIAN_POINT('Ctrl Pts',(206.178560331278,4.81841563632905,129.808950651116));
#18795=CARTESIAN_POINT('Ctrl Pts',(206.170804016765,4.78695671008173,129.675543308032));
#18796=CARTESIAN_POINT('Ctrl Pts',(206.163043562283,4.75548099249017,129.542064758175));
#18797=CARTESIAN_POINT('Ctrl Pts',(206.155283107802,4.71844321146889,129.410009580029));
#18798=CARTESIAN_POINT('Ctrl Pts',(206.14752265332,4.6760126848635,129.279864493105));
#18799=CARTESIAN_POINT('Ctrl Pts',(206.139749740871,4.63351404393066,129.149510482424));
#18800=CARTESIAN_POINT('Ctrl Pts',(206.131976828422,4.5856054945835,129.021073056925));
#18801=CARTESIAN_POINT('Ctrl Pts',(206.124203915972,4.53250473784456,128.895019405546));
#18802=CARTESIAN_POINT('Ctrl Pts',(206.116713699522,4.48133522265336,128.773550247191));
#18803=CARTESIAN_POINT('Ctrl Pts',(206.109223483071,4.42534474547032,128.654294760804));
#18804=CARTESIAN_POINT('Ctrl Pts',(206.101733266621,4.36476734543776,128.537647339999));
#18805=CARTESIAN_POINT('Ctrl Pts',(206.093958959944,4.30189235529015,128.416575695624));
#18806=CARTESIAN_POINT('Ctrl Pts',(206.086184653268,4.23387645089009,128.297930328045));
#18807=CARTESIAN_POINT('Ctrl Pts',(206.078410346591,4.16093074001882,128.18217861792));
#18808=CARTESIAN_POINT('Ctrl Pts',(206.070645621474,4.08807493217016,128.066569567707));
#18809=CARTESIAN_POINT('Ctrl Pts',(206.062880896357,4.01030161335004,127.953847406604));
#18810=CARTESIAN_POINT('Ctrl Pts',(206.05511617124,3.92786859889688,127.844456677858));
#18811=CARTESIAN_POINT('Ctrl Pts',(206.04735915854,3.84551746214591,127.735174602927));
#18812=CARTESIAN_POINT('Ctrl Pts',(206.039602145841,3.7585160740671,127.629217685533));
#18813=CARTESIAN_POINT('Ctrl Pts',(206.031845133142,3.66716633068647,127.52700281507));
#18814=CARTESIAN_POINT('Ctrl Pts',(206.024093970412,3.57588547893075,127.424865030194));
#18815=CARTESIAN_POINT('Ctrl Pts',(206.016342807682,3.48026305863852,127.326463965419));
#18816=CARTESIAN_POINT('Ctrl Pts',(206.008591644952,3.38064191709146,127.232184349392));
#18817=CARTESIAN_POINT('Ctrl Pts',(206.000843777079,3.28106312240745,127.137944809658));
#18818=CARTESIAN_POINT('Ctrl Pts',(205.993095909207,3.17748927055705,127.04782350237));
#18819=CARTESIAN_POINT('Ctrl Pts',(205.985348041334,3.070300668997,126.962168942954));
#18820=CARTESIAN_POINT('Ctrl Pts',(205.97760179439,2.96313449232946,126.876532303301));
#18821=CARTESIAN_POINT('Ctrl Pts',(205.969855547446,2.85235537539139,126.79536079669));
#18822=CARTESIAN_POINT('Ctrl Pts',(205.962109300503,2.73837705773569,126.718962943879));
#18823=CARTESIAN_POINT('Ctrl Pts',(205.954362996587,2.62439790178891,126.642564529175));
#18824=CARTESIAN_POINT('Ctrl Pts',(205.94661669267,2.5072198229346,126.570940056014));
#18825=CARTESIAN_POINT('Ctrl Pts',(205.938870388754,2.38728557715688,126.50435472971));
#18826=CARTESIAN_POINT('Ctrl Pts',(205.931122350283,2.26732447565317,126.437754493592));
#18827=CARTESIAN_POINT('Ctrl Pts',(205.923374311811,2.14460632090196,126.376195839389));
#18828=CARTESIAN_POINT('Ctrl Pts',(205.915626273339,2.01959813448211,126.319897836173));
#18829=CARTESIAN_POINT('Ctrl Pts',(205.907870000251,1.8944570893462,126.263539999433));
#18830=CARTESIAN_POINT('Ctrl Pts',(205.900113727163,1.76702150772587,126.212454143145));
#18831=CARTESIAN_POINT('Ctrl Pts',(205.892357454075,1.63777856078686,126.166811216392));
#18832=CARTESIAN_POINT('Ctrl Pts',(205.884597041329,1.5084666346276,126.121143929212));
#18833=CARTESIAN_POINT('Ctrl Pts',(205.876836628582,1.3773457946557,126.08092547459));
#18834=CARTESIAN_POINT('Ctrl Pts',(205.869076215836,1.24491704770284,126.046276485603));
#18835=CARTESIAN_POINT('Ctrl Pts',(205.861303345232,1.11227571174918,126.011571874297));
#18836=CARTESIAN_POINT('Ctrl Pts',(205.853530474629,0.97832265542302,125.982454678108));
#18837=CARTESIAN_POINT('Ctrl Pts',(205.845757604025,0.843568606457823,125.958994267258));
#18838=CARTESIAN_POINT('Ctrl Pts',(205.838266950286,0.713707198462261,125.93638565543));
#18839=CARTESIAN_POINT('Ctrl Pts',(205.830776296547,0.583102259513571,125.919030219509));
#18840=CARTESIAN_POINT('Ctrl Pts',(205.823285642808,0.452212191984598,125.90694423789));
#18841=CARTESIAN_POINT('Ctrl Pts',(205.815511295583,0.316364925691163,125.894400523959));
#18842=CARTESIAN_POINT('Ctrl Pts',(205.807736948359,0.179780181164248,125.887493536688));
#18843=CARTESIAN_POINT('Ctrl Pts',(205.799962601134,0.0429652936190226,
125.886298291198));
#18844=CARTESIAN_POINT('Ctrl Pts',(205.792197834953,-0.0936809843600888,
125.885104518719));
#18845=CARTESIAN_POINT('Ctrl Pts',(205.784433068771,-0.23055645382959,125.889608485683));
#18846=CARTESIAN_POINT('Ctrl Pts',(205.77666830259,-0.367147747384615,125.899833566556));
#18847=CARTESIAN_POINT('Ctrl Pts',(205.768911248356,-0.503603378781414,
125.910048491902));
#18848=CARTESIAN_POINT('Ctrl Pts',(205.761154194123,-0.639775008589745,
125.925973194331));
#18849=CARTESIAN_POINT('Ctrl Pts',(205.753397139889,-0.775148709250783,
125.94757901438));
#18850=CARTESIAN_POINT('Ctrl Pts',(205.745645935201,-0.910420325464687,
125.969168541617));
#18851=CARTESIAN_POINT('Ctrl Pts',(205.737894730512,-1.04489482568991,125.996430597873));
#18852=CARTESIAN_POINT('Ctrl Pts',(205.730143525824,-1.17806320546229,126.029284686606));
#18853=CARTESIAN_POINT('Ctrl Pts',(205.722395615495,-1.31117498700093,126.062124811938));
#18854=CARTESIAN_POINT('Ctrl Pts',(205.714647705166,-1.44298137338557,126.100552149252));
#18855=CARTESIAN_POINT('Ctrl Pts',(205.706899794837,-1.57298357962825,126.144435111646));
#18856=CARTESIAN_POINT('Ctrl Pts',(205.699153505139,-1.70295859328728,126.188308895034));
#18857=CARTESIAN_POINT('Ctrl Pts',(205.691407215442,-1.83112980724108,126.237635908722));
#18858=CARTESIAN_POINT('Ctrl Pts',(205.683660925745,-1.9570140146508,126.292234820454));
#18859=CARTESIAN_POINT('Ctrl Pts',(205.675914578818,-2.08289915209403,126.346834135564));
#18860=CARTESIAN_POINT('Ctrl Pts',(205.668168231891,-2.2064968905978,126.406705270871));
#18861=CARTESIAN_POINT('Ctrl Pts',(205.660421884964,-2.32734478203693,126.471619068844));
#18862=CARTESIAN_POINT('Ctrl Pts',(205.652673803264,-2.44821973703175,126.536547404084));
#18863=CARTESIAN_POINT('Ctrl Pts',(205.644925721563,-2.56634327519558,126.606520464177));
#18864=CARTESIAN_POINT('Ctrl Pts',(205.637177639863,-2.6812786482065,126.68126373862));
#18865=CARTESIAN_POINT('Ctrl Pts',(205.629421323445,-2.79633617537112,126.756086450761));
#18866=CARTESIAN_POINT('Ctrl Pts',(205.621665007027,-2.90819844040077,126.835689291279));
#18867=CARTESIAN_POINT('Ctrl Pts',(205.613908690609,-3.01645828850523,126.919754787342));
#18868=CARTESIAN_POINT('Ctrl Pts',(205.606148234409,-3.12477591819194,127.003865151724));
#18869=CARTESIAN_POINT('Ctrl Pts',(205.598387778208,-3.22948700142695,127.092442665323));
#18870=CARTESIAN_POINT('Ctrl Pts',(205.590627322007,-3.3302192372797,127.185131018031));
#18871=CARTESIAN_POINT('Ctrl Pts',(205.582854408177,-3.43111317560035,127.277968160599));
#18872=CARTESIAN_POINT('Ctrl Pts',(205.575081494346,-3.52801522649826,127.374929052501));
#18873=CARTESIAN_POINT('Ctrl Pts',(205.567308580516,-3.62059096362825,127.475621496428));
#18874=CARTESIAN_POINT('Ctrl Pts',(205.559818393342,-3.70979941414655,127.572651422196));
#18875=CARTESIAN_POINT('Ctrl Pts',(205.552328206168,-3.79499060911529,127.673145922983));
#18876=CARTESIAN_POINT('Ctrl Pts',(205.544838018995,-3.87590312513928,127.776728204766));
#18877=CARTESIAN_POINT('Ctrl Pts',(205.53706126549,-3.95991126511941,127.884273430835));
#18878=CARTESIAN_POINT('Ctrl Pts',(205.529284511985,-4.03957765797006,127.995494127098));
#18879=CARTESIAN_POINT('Ctrl Pts',(205.521507758481,-4.11456321009359,128.110004914871));
#18880=CARTESIAN_POINT('Ctrl Pts',(205.513743508267,-4.18942820212018,128.224331594755));
#18881=CARTESIAN_POINT('Ctrl Pts',(205.505979258053,-4.25962712878069,128.341937508539));
#18882=CARTESIAN_POINT('Ctrl Pts',(205.498215007839,-4.32486122114154,128.462404494927));
#18883=CARTESIAN_POINT('Ctrl Pts',(205.490457952857,-4.39003486021618,128.582759842984));
#18884=CARTESIAN_POINT('Ctrl Pts',(205.482700897876,-4.45025263063646,128.705970650087));
#18885=CARTESIAN_POINT('Ctrl Pts',(205.474943842894,-4.50525896992651,128.831589805638));
#18886=CARTESIAN_POINT('Ctrl Pts',(205.467193142368,-4.5602202488983,128.957106055974));
#18887=CARTESIAN_POINT('Ctrl Pts',(205.459442441842,-4.60997843839768,129.085026371888));
#18888=CARTESIAN_POINT('Ctrl Pts',(205.451691741317,-4.65432411968393,129.214879554002));
#18889=CARTESIAN_POINT('Ctrl Pts',(205.444469975199,-4.69564349946542,129.335871109256));
#18890=CARTESIAN_POINT('Ctrl Pts',(205.437248209081,-4.73226423551571,129.458540250484));
#18891=CARTESIAN_POINT('Ctrl Pts',(205.430026442963,-4.76405452823405,129.582490119308));
#18892=CARTESIAN_POINT('Origin',(213.235140564004,0.,130.804360617566));
#18893=CARTESIAN_POINT('',(203.334773566427,-4.76405452823405,129.582490119308));
#18894=CARTESIAN_POINT('',(203.680274487341,-4.76405452823405,129.582490119308));
#18895=CARTESIAN_POINT('',(213.235140564004,-4.76405452823405,129.582490119308));
#18896=CARTESIAN_POINT('',(205.014859436024,-4.91824993440617,130.805163869501));
#18897=CARTESIAN_POINT('Ctrl Pts',(205.014859435991,-4.91824993440608,130.80516387008));
#18898=CARTESIAN_POINT('Ctrl Pts',(205.012416879836,-4.91824293327168,130.848031247661));
#18899=CARTESIAN_POINT('Ctrl Pts',(205.009974323682,-4.91767549764493,130.890893474637));
#18900=CARTESIAN_POINT('Ctrl Pts',(205.007531767528,-4.91654795620673,130.933740897437));
#18901=CARTESIAN_POINT('Ctrl Pts',(204.999757433917,-4.91295914074164,131.070118584653));
#18902=CARTESIAN_POINT('Ctrl Pts',(204.991983100306,-4.9036859709115,131.206562848942));
#18903=CARTESIAN_POINT('Ctrl Pts',(204.984208766695,-4.88871387579036,131.342561047847));
#18904=CARTESIAN_POINT('Ctrl Pts',(204.976444014264,-4.87376023245488,131.478391640977));
#18905=CARTESIAN_POINT('Ctrl Pts',(204.968679261833,-4.85312168071783,131.613776877648));
#18906=CARTESIAN_POINT('Ctrl Pts',(204.960914509402,-4.82683564131106,131.748204224457));
#18907=CARTESIAN_POINT('Ctrl Pts',(204.95315746904,-4.80057570959591,131.882498055994));
#18908=CARTESIAN_POINT('Ctrl Pts',(204.945400428679,-4.76867952725585,132.015835509765));
#18909=CARTESIAN_POINT('Ctrl Pts',(204.937643388317,-4.73123625092355,132.147709641627));
#18910=CARTESIAN_POINT('Ctrl Pts',(204.929892197607,-4.69382121089179,132.27948432606));
#18911=CARTESIAN_POINT('Ctrl Pts',(204.922141006897,-4.65086750945265,132.409797510464));
#18912=CARTESIAN_POINT('Ctrl Pts',(204.914389816187,-4.60251519606229,132.538153261603));
#18913=CARTESIAN_POINT('Ctrl Pts',(204.906641919949,-4.55418343374924,132.666454457979));
#18914=CARTESIAN_POINT('Ctrl Pts',(204.898894023711,-4.50045776072558,132.792799510701));
#18915=CARTESIAN_POINT('Ctrl Pts',(204.891146127472,-4.44152775223612,132.916708668579));
#18916=CARTESIAN_POINT('Ctrl Pts',(204.883399851932,-4.38261007067356,133.040591907248));
#18917=CARTESIAN_POINT('Ctrl Pts',(204.875653576392,-4.31849038681639,133.162039911728));
#18918=CARTESIAN_POINT('Ctrl Pts',(204.867907300851,-4.2494058332061,133.280594275203));
#18919=CARTESIAN_POINT('Ctrl Pts',(204.860160968134,-4.18032076967024,133.399149513749));
#18920=CARTESIAN_POINT('Ctrl Pts',(204.852414635417,-4.10627096009826,133.514810730874));
#18921=CARTESIAN_POINT('Ctrl Pts',(204.8446683027,-4.02753857581953,133.627145781688));
#18922=CARTESIAN_POINT('Ctrl Pts',(204.83692023525,-3.94878856000942,133.7395059891));
#18923=CARTESIAN_POINT('Ctrl Pts',(204.829172167799,-3.86535410719281,133.848538227898));
#18924=CARTESIAN_POINT('Ctrl Pts',(204.821424100349,-3.77755938889782,133.953841229643));
#18925=CARTESIAN_POINT('Ctrl Pts',(204.813667798163,-3.68967136136312,134.059256148634));
#18926=CARTESIAN_POINT('Ctrl Pts',(204.805911495977,-3.5974140619154,134.160933612335));
#18927=CARTESIAN_POINT('Ctrl Pts',(204.798155193791,-3.50115082848458,134.258506812894));
#18928=CARTESIAN_POINT('Ctrl Pts',(204.790394751835,-3.40483621649768,134.356132091179));
#18929=CARTESIAN_POINT('Ctrl Pts',(204.782634309879,-3.30451169605726,134.449648474981));
#18930=CARTESIAN_POINT('Ctrl Pts',(204.774873867924,-3.20057505400699,134.538728353364));
#18931=CARTESIAN_POINT('Ctrl Pts',(204.767100968216,-3.09647156360682,134.627951230698));
#18932=CARTESIAN_POINT('Ctrl Pts',(204.759328068508,-2.98874467176853,134.712723128926));
#18933=CARTESIAN_POINT('Ctrl Pts',(204.7515551688,-2.87782332804817,134.792758285182));
#18934=CARTESIAN_POINT('Ctrl Pts',(204.744064827105,-2.77093416223283,134.869884028534));
#18935=CARTESIAN_POINT('Ctrl Pts',(204.73657448541,-2.66107901674024,134.942611258251));
#18936=CARTESIAN_POINT('Ctrl Pts',(204.729084143715,-2.54866295096712,135.010724870085));
#18937=CARTESIAN_POINT('Ctrl Pts',(204.721309809264,-2.43198468332284,135.08142097724));
#18938=CARTESIAN_POINT('Ctrl Pts',(204.713535474812,-2.31217786981156,135.147370661178));
#18939=CARTESIAN_POINT('Ctrl Pts',(204.70576114036,-2.18966593526101,135.208284567234));
#18940=CARTESIAN_POINT('Ctrl Pts',(204.697996387077,-2.0673049856553,135.269123402377));
#18941=CARTESIAN_POINT('Ctrl Pts',(204.690231633794,-1.94224589503469,135.324938635623));
#18942=CARTESIAN_POINT('Ctrl Pts',(204.682466880511,-1.8149400992257,135.375484713313));
#18943=CARTESIAN_POINT('Ctrl Pts',(204.674709839286,-1.68776074526766,135.425980587951));
#18944=CARTESIAN_POINT('Ctrl Pts',(204.666952798062,-1.55833948784361,135.471217578389));
#18945=CARTESIAN_POINT('Ctrl Pts',(204.659195756837,-1.42715102488418,135.510996678987));
#18946=CARTESIAN_POINT('Ctrl Pts',(204.651444565255,-1.29606149211033,135.550745781873));
#18947=CARTESIAN_POINT('Ctrl Pts',(204.643693373672,-1.16320777901492,135.585045074249));
#18948=CARTESIAN_POINT('Ctrl Pts',(204.635942182089,-1.02908282854748,135.613744319714));
#18949=CARTESIAN_POINT('Ctrl Pts',(204.628194284967,-0.895014884701764,
135.642431367248));
#18950=CARTESIAN_POINT('Ctrl Pts',(204.620446387844,-0.759677159628549,
135.665523020208));
#18951=CARTESIAN_POINT('Ctrl Pts',(204.612698490721,-0.623575751751765,
135.682919456437));
#18952=CARTESIAN_POINT('Ctrl Pts',(204.604952214289,-0.487502813319543,
135.700312253712));
#18953=CARTESIAN_POINT('Ctrl Pts',(204.597205937857,-0.350666897391173,
135.712012154308));
#18954=CARTESIAN_POINT('Ctrl Pts',(204.589459661425,-0.213581850635355,
135.717970884526));
#18955=CARTESIAN_POINT('Ctrl Pts',(204.58171332781,-0.0764957919198511,
135.723929658732));
#18956=CARTESIAN_POINT('Ctrl Pts',(204.573966994196,0.0608390106965075,
135.724147161014));
#18957=CARTESIAN_POINT('Ctrl Pts',(204.566220660581,0.197906460888714,135.718627205292));
#18958=CARTESIAN_POINT('Ctrl Pts',(204.558472592227,0.335004606408075,135.713106013413));
#18959=CARTESIAN_POINT('Ctrl Pts',(204.550724523873,0.471834889791658,135.701844822528));
#18960=CARTESIAN_POINT('Ctrl Pts',(204.54297645552,0.607884489820787,135.684899471989));
#18961=CARTESIAN_POINT('Ctrl Pts',(204.535220152427,0.744078684979407,135.667936111731));
#18962=CARTESIAN_POINT('Ctrl Pts',(204.527463849334,0.879490150743396,135.645276572288));
#18963=CARTESIAN_POINT('Ctrl Pts',(204.519707546241,1.01361388816882,135.617028271603));
#18964=CARTESIAN_POINT('Ctrl Pts',(204.511947103376,1.14780921147885,135.588764893948));
#18965=CARTESIAN_POINT('Ctrl Pts',(204.50418666051,1.28071505826876,135.554906907859));
#18966=CARTESIAN_POINT('Ctrl Pts',(204.496426217644,1.41184078659271,135.515611901016));
#18967=CARTESIAN_POINT('Ctrl Pts',(204.48865331703,1.54317700952478,135.476253814356));
#18968=CARTESIAN_POINT('Ctrl Pts',(204.480880416416,1.67272703389122,135.431441393526));
#18969=CARTESIAN_POINT('Ctrl Pts',(204.473107515801,1.80001858150718,135.381381064181));
#18970=CARTESIAN_POINT('Ctrl Pts',(204.465617183835,1.9226826930735,135.333140580513));
#18971=CARTESIAN_POINT('Ctrl Pts',(204.458126851868,2.04324940016541,135.280027243014));
#18972=CARTESIAN_POINT('Ctrl Pts',(204.450636519902,2.16131878660124,135.222265569598));
#18973=CARTESIAN_POINT('Ctrl Pts',(204.442862185831,2.28386487105517,135.162313814766));
#18974=CARTESIAN_POINT('Ctrl Pts',(204.435087851759,2.40410871112534,135.097164368467));
#18975=CARTESIAN_POINT('Ctrl Pts',(204.427313517688,2.52157799309945,135.027017066677));
#18976=CARTESIAN_POINT('Ctrl Pts',(204.419548764789,2.63890250468257,134.956956215167));
#18977=CARTESIAN_POINT('Ctrl Pts',(204.411784011889,2.75345892929808,134.881909962079));
#18978=CARTESIAN_POINT('Ctrl Pts',(204.40401925899,2.86479666362884,134.802125385353));
#18979=CARTESIAN_POINT('Ctrl Pts',(204.396262218153,2.9760238157537,134.722420051793));
#18980=CARTESIAN_POINT('Ctrl Pts',(204.388505177315,3.08403832372975,134.637985986342));
#18981=CARTESIAN_POINT('Ctrl Pts',(204.380748136478,3.18841617266462,134.549114998349));
#18982=CARTESIAN_POINT('Ctrl Pts',(204.372996945285,3.29271530945384,134.460311028657));
#18983=CARTESIAN_POINT('Ctrl Pts',(204.365245754092,3.39338294937173,134.3670770487));
#18984=CARTESIAN_POINT('Ctrl Pts',(204.357494562899,3.49002624658722,134.269746578845));
#18985=CARTESIAN_POINT('Ctrl Pts',(204.349746666169,3.58662846782897,134.172457477031));
#18986=CARTESIAN_POINT('Ctrl Pts',(204.341998769439,3.67920947343216,134.07107562512));
#18987=CARTESIAN_POINT('Ctrl Pts',(204.334250872709,3.76741172163867,133.965972861684));
#18988=CARTESIAN_POINT('Ctrl Pts',(204.326504596671,3.85559551983956,133.860892083477));
#18989=CARTESIAN_POINT('Ctrl Pts',(204.318758320634,3.9394021313356,133.752092241188));
#18990=CARTESIAN_POINT('Ctrl Pts',(204.311012044596,4.01851319542896,133.639979555411));
#18991=CARTESIAN_POINT('Ctrl Pts',(204.303265711377,4.09762484350567,133.527866042038));
#18992=CARTESIAN_POINT('Ctrl Pts',(204.295519378158,4.17204064960371,133.412439955821));
#18993=CARTESIAN_POINT('Ctrl Pts',(204.287773044939,4.24148485981986,133.294137564688));
#18994=CARTESIAN_POINT('Ctrl Pts',(204.280024976982,4.31094462158894,133.175808680548));
#18995=CARTESIAN_POINT('Ctrl Pts',(204.272276909025,4.37543037414788,133.054602546852));
#18996=CARTESIAN_POINT('Ctrl Pts',(204.264528841068,4.43471190433788,132.930980797105));
#18997=CARTESIAN_POINT('Ctrl Pts',(204.256772538371,4.49405643965077,132.807227660677));
#18998=CARTESIAN_POINT('Ctrl Pts',(204.249016235674,4.54818553428607,132.681054132738));
#18999=CARTESIAN_POINT('Ctrl Pts',(204.241259932977,4.59691659774419,132.552943145182));
#19000=CARTESIAN_POINT('Ctrl Pts',(204.233499490508,4.64567367044088,132.424763780927));
#19001=CARTESIAN_POINT('Ctrl Pts',(204.225739048038,4.68902684761736,132.2946452673));
#19002=CARTESIAN_POINT('Ctrl Pts',(204.217978605568,4.72684350830149,132.163085575211));
#19003=CARTESIAN_POINT('Ctrl Pts',(204.210205705346,4.76472087565255,132.031314691805));
#19004=CARTESIAN_POINT('Ctrl Pts',(204.202432805124,4.79704387379708,131.898098386972));
#19005=CARTESIAN_POINT('Ctrl Pts',(204.194659904902,4.82373089659542,131.763945579792));
#19006=CARTESIAN_POINT('Ctrl Pts',(204.187169568631,4.849447780786,131.634669555555));
#19007=CARTESIAN_POINT('Ctrl Pts',(204.17967923236,4.86993129066992,131.504524239439));
#19008=CARTESIAN_POINT('Ctrl Pts',(204.172188896089,4.88515415502804,131.373967450489));
#19009=CARTESIAN_POINT('Ctrl Pts',(204.164414562036,4.90095419770749,131.238460571561));
#19010=CARTESIAN_POINT('Ctrl Pts',(204.156640227983,4.91113685606931,131.102081156815));
#19011=CARTESIAN_POINT('Ctrl Pts',(204.14886589393,4.915614960675,130.965334593376));
#19012=CARTESIAN_POINT('Ctrl Pts',(204.141101141049,4.9200875464163,130.828756557876));
#19013=CARTESIAN_POINT('Ctrl Pts',(204.133336388169,4.91886955403614,130.691812660983));
#19014=CARTESIAN_POINT('Ctrl Pts',(204.125571635289,4.9119252950968,130.555015559688));
#19015=CARTESIAN_POINT('Ctrl Pts',(204.117814594472,4.90498793329431,130.418354327222));
#19016=CARTESIAN_POINT('Ctrl Pts',(204.110057553655,4.892335642827,130.281839988143));
#19017=CARTESIAN_POINT('Ctrl Pts',(204.102300512838,4.87398474075138,130.145987008266));
#19018=CARTESIAN_POINT('Ctrl Pts',(204.094549321667,4.85564767723613,130.010236476196));
#19019=CARTESIAN_POINT('Ctrl Pts',(204.086798130496,4.83162060788727,129.875146696503));
#19020=CARTESIAN_POINT('Ctrl Pts',(204.079046939325,4.80197179006196,129.741228457414));
#19021=CARTESIAN_POINT('Ctrl Pts',(204.071299042618,4.77233557377983,129.607367137171));
#19022=CARTESIAN_POINT('Ctrl Pts',(204.063551145911,4.73708244567803,129.474676748098));
#19023=CARTESIAN_POINT('Ctrl Pts',(204.055803249204,4.69633198401899,129.343659088033));
#19024=CARTESIAN_POINT('Ctrl Pts',(204.048056973191,4.65559004648194,129.21266883405));
#19025=CARTESIAN_POINT('Ctrl Pts',(204.040310697177,4.60935317869152,129.083350986195));
#19026=CARTESIAN_POINT('Ctrl Pts',(204.032564421164,4.55779106379823,128.956192962492));
#19027=CARTESIAN_POINT('Ctrl Pts',(204.02481808797,4.50622856828952,128.829034000148));
#19028=CARTESIAN_POINT('Ctrl Pts',(204.017071754777,4.44934089415499,128.704035256081));
#19029=CARTESIAN_POINT('Ctrl Pts',(204.009325421583,4.3873460342304,128.58166454333));
#19030=CARTESIAN_POINT('Ctrl Pts',(204.001577353652,4.3253372909914,128.459266426516));
#19031=CARTESIAN_POINT('Ctrl Pts',(203.993829285721,4.25821926274942,128.339497860818));
#19032=CARTESIAN_POINT('Ctrl Pts',(203.98608121779,4.18625589900541,128.222802055274));
#19033=CARTESIAN_POINT('Ctrl Pts',(203.978324915121,4.1142160517463,128.105982224046));
#19034=CARTESIAN_POINT('Ctrl Pts',(203.970568612452,4.03732078748716,127.992242009999));
#19035=CARTESIAN_POINT('Ctrl Pts',(203.962812309783,3.95587771587694,127.881996068177));
#19036=CARTESIAN_POINT('Ctrl Pts',(203.955051867342,3.87439117565101,127.771691284781));
#19037=CARTESIAN_POINT('Ctrl Pts',(203.9472914249,3.78835223661492,127.664884794093));
#19038=CARTESIAN_POINT('Ctrl Pts',(203.939530982459,3.6981081709207,127.561957339337));
#19039=CARTESIAN_POINT('Ctrl Pts',(203.931758082267,3.60771923743896,127.458864656291));
#19040=CARTESIAN_POINT('Ctrl Pts',(203.923985182075,3.51311195774471,127.359663735743));
#19041=CARTESIAN_POINT('Ctrl Pts',(203.916212281882,3.41467038975604,127.264698318444));
#19042=CARTESIAN_POINT('Ctrl Pts',(203.908721945347,3.3198074100404,127.173185122963));
#19043=CARTESIAN_POINT('Ctrl Pts',(203.901231608812,3.22138430351891,127.085605040283));
#19044=CARTESIAN_POINT('Ctrl Pts',(203.893741272277,3.11977150560056,127.002228476866));
#19045=CARTESIAN_POINT('Ctrl Pts',(203.885966938106,3.01430603775704,126.915690674068));
#19046=CARTESIAN_POINT('Ctrl Pts',(203.878192603936,2.90507014731187,126.83340730906));
#19047=CARTESIAN_POINT('Ctrl Pts',(203.870418269766,2.79244191357776,126.755724894042));
#19048=CARTESIAN_POINT('Ctrl Pts',(203.862653516767,2.67995248406615,126.678138215651));
#19049=CARTESIAN_POINT('Ctrl Pts',(203.854888763768,2.56407934847872,126.605141424973));
#19050=CARTESIAN_POINT('Ctrl Pts',(203.84712401077,2.44523452920922,126.537041651322));
#19051=CARTESIAN_POINT('Ctrl Pts',(203.839366969832,2.32650774828062,126.469009515322));
#19052=CARTESIAN_POINT('Ctrl Pts',(203.831609928895,2.20481549434958,126.405864910317));
#19053=CARTESIAN_POINT('Ctrl Pts',(203.823852887958,2.08059942186419,126.34787218964));
#19054=CARTESIAN_POINT('Ctrl Pts',(203.816101696665,1.95647702167689,126.289923201721));
#19055=CARTESIAN_POINT('Ctrl Pts',(203.808350505372,1.82983494402628,126.237118529847));
#19056=CARTESIAN_POINT('Ctrl Pts',(203.800599314079,1.70113982430083,126.189676840678));
#19057=CARTESIAN_POINT('Ctrl Pts',(203.792851417249,1.57249940342463,126.142255315488));
#19058=CARTESIAN_POINT('Ctrl Pts',(203.785103520418,1.44180804206936,126.100192374375));
#19059=CARTESIAN_POINT('Ctrl Pts',(203.777355623588,1.30955255195562,126.063658646743));
#19060=CARTESIAN_POINT('Ctrl Pts',(203.76960934745,1.17732472683343,126.027132561177));
#19061=CARTESIAN_POINT('Ctrl Pts',(203.761863071312,1.04353380034826,125.996133492601));
#19062=CARTESIAN_POINT('Ctrl Pts',(203.754116795175,0.908681568991501,125.970782143115));
#19063=CARTESIAN_POINT('Ctrl Pts',(203.746370461855,0.77382834218146,125.945430606491));
#19064=CARTESIAN_POINT('Ctrl Pts',(203.738624128536,0.637914179101389,125.925726944381));
#19065=CARTESIAN_POINT('Ctrl Pts',(203.730877795217,0.501450494577304,125.911740617608));
#19066=CARTESIAN_POINT('Ctrl Pts',(203.72312972716,0.364956249953434,125.897751158694));
#19067=CARTESIAN_POINT('Ctrl Pts',(203.715381659102,0.227912627860709,125.889481622733));
#19068=CARTESIAN_POINT('Ctrl Pts',(203.707633591045,0.0908351837803655,
125.88694950684));
#19069=CARTESIAN_POINT('Ctrl Pts',(203.699877288249,-0.0463879478389493,
125.884414699785));
#19070=CARTESIAN_POINT('Ctrl Pts',(203.692120985453,-0.183644581730893,
125.887629501038));
#19071=CARTESIAN_POINT('Ctrl Pts',(203.684364682657,-0.320419586321026,
125.896559241063));
#19072=CARTESIAN_POINT('Ctrl Pts',(203.676604240088,-0.457267591850978,
125.90549374716));
#19073=CARTESIAN_POINT('Ctrl Pts',(203.66884379752,-0.593633067328671,125.920149228124));
#19074=CARTESIAN_POINT('Ctrl Pts',(203.661083354951,-0.729007973603942,
125.940439315065));
#19075=CARTESIAN_POINT('Ctrl Pts',(203.653310454632,-0.864600195689189,
125.960761973454));
#19076=CARTESIAN_POINT('Ctrl Pts',(203.645537554313,-0.999198286843428,
125.986737238823));
#19077=CARTESIAN_POINT('Ctrl Pts',(203.637764653993,-1.13230545553917,126.018227792638));
#19078=CARTESIAN_POINT('Ctrl Pts',(203.630274318817,-1.26057383246008,126.048573582918));
#19079=CARTESIAN_POINT('Ctrl Pts',(203.62278398364,-1.38745750614367,126.084040550359));
#19080=CARTESIAN_POINT('Ctrl Pts',(203.615293648463,-1.51252874683208,126.124463198551));
#19081=CARTESIAN_POINT('Ctrl Pts',(203.607519314355,-1.64234211159146,126.166418486956));
#19082=CARTESIAN_POINT('Ctrl Pts',(203.599744980247,-1.77061410292081,126.213845566141));
#19083=CARTESIAN_POINT('Ctrl Pts',(203.591970646139,-1.89684882919352,126.266613645589));
#19084=CARTESIAN_POINT('Ctrl Pts',(203.584205893202,-2.02292798244727,126.319316693095));
#19085=CARTESIAN_POINT('Ctrl Pts',(203.576441140266,-2.14697450902767,126.377347494701));
#19086=CARTESIAN_POINT('Ctrl Pts',(203.56867638733,-2.2685073041796,126.440525415203));
#19087=CARTESIAN_POINT('Ctrl Pts',(203.560919346456,-2.38991939124546,126.503640586503));
#19088=CARTESIAN_POINT('Ctrl Pts',(203.553162305581,-2.50882237072727,126.571892524047));
#19089=CARTESIAN_POINT('Ctrl Pts',(203.545405264707,-2.62475510966509,126.64505254088));
#19090=CARTESIAN_POINT('Ctrl Pts',(203.537654073478,-2.74060042282238,126.718157387175));
#19091=CARTESIAN_POINT('Ctrl Pts',(203.529902882249,-2.853479624487,126.7961627379));
#19092=CARTESIAN_POINT('Ctrl Pts',(203.52215169102,-2.96295651638203,126.878794194166));
#19093=CARTESIAN_POINT('Ctrl Pts',(203.514403794253,-3.07238687767773,126.961390529858));
#19094=CARTESIAN_POINT('Ctrl Pts',(203.506655897487,-3.17841749393087,127.048608825393));
#19095=CARTESIAN_POINT('Ctrl Pts',(203.498908000721,-3.28064167616848,127.140131741651));
#19096=CARTESIAN_POINT('Ctrl Pts',(203.491161724648,-3.38284447531104,127.231635513289));
#19097=CARTESIAN_POINT('Ctrl Pts',(203.483415448574,-3.48124213307604,127.327441854015));
#19098=CARTESIAN_POINT('Ctrl Pts',(203.475669172501,-3.57546186610856,127.427193830671));
#19099=CARTESIAN_POINT('Ctrl Pts',(203.467922839247,-3.66968229464993,127.526946543675));
#19100=CARTESIAN_POINT('Ctrl Pts',(203.460176505992,-3.75972446845858,127.630644666505));
#19101=CARTESIAN_POINT('Ctrl Pts',(203.452430172738,-3.8452535159746,127.737895476661));
#19102=CARTESIAN_POINT('Ctrl Pts',(203.444682104745,-3.93080171712827,127.845170304894));
#19103=CARTESIAN_POINT('Ctrl Pts',(203.436934036753,-4.01183453713135,127.955999097993));
#19104=CARTESIAN_POINT('Ctrl Pts',(203.429185968761,-4.08805858483793,128.069957562156));
#19105=CARTESIAN_POINT('Ctrl Pts',(203.42142966603,-4.16436364437073,128.184037142734));
#19106=CARTESIAN_POINT('Ctrl Pts',(203.413673363299,-4.23584950448076,128.301252713431));
#19107=CARTESIAN_POINT('Ctrl Pts',(203.405917060567,-4.30226689243356,128.421152139742));
#19108=CARTESIAN_POINT('Ctrl Pts',(203.398156618064,-4.3687197293466,128.541115559989));
#19109=CARTESIAN_POINT('Ctrl Pts',(203.39039617556,-4.4300985288876,128.663765340678));
#19110=CARTESIAN_POINT('Ctrl Pts',(203.382635733057,-4.48620134808193,128.788627369597));
#19111=CARTESIAN_POINT('Ctrl Pts',(203.374862832802,-4.54239422850365,128.913689838133));
#19112=CARTESIAN_POINT('Ctrl Pts',(203.367089932547,-4.59329405862153,129.040971288298));
#19113=CARTESIAN_POINT('Ctrl Pts',(203.359317032292,-4.63874784045621,129.169979531294));
#19114=CARTESIAN_POINT('Ctrl Pts',(203.351826696411,-4.68254926358041,129.294298001835));
#19115=CARTESIAN_POINT('Ctrl Pts',(203.344336360531,-4.72129362844921,129.420219603998));
#19116=CARTESIAN_POINT('Ctrl Pts',(203.336846024651,-4.75488897347145,129.54729502164));
#19117=CARTESIAN_POINT('Ctrl Pts',(203.336155205243,-4.75798740813817,129.55901494531));
#19118=CARTESIAN_POINT('Ctrl Pts',(203.335464385835,-4.76104262034663,129.570746736167));
#19119=CARTESIAN_POINT('Ctrl Pts',(203.334773566427,-4.76405452823405,129.582490119308));
#19120=CARTESIAN_POINT('Ctrl Pts',(205.084976592678,-4.76405452823405,129.582490119308));
#19121=CARTESIAN_POINT('Ctrl Pts',(205.077250789112,-4.79798664166829,129.714790914597));
#19122=CARTESIAN_POINT('Ctrl Pts',(205.069524985546,-4.82637681902747,129.848402380795));
#19123=CARTESIAN_POINT('Ctrl Pts',(205.06179918198,-4.84914957344003,129.982818484193));
#19124=CARTESIAN_POINT('Ctrl Pts',(205.053975890988,-4.87220968401055,130.118930706311));
#19125=CARTESIAN_POINT('Ctrl Pts',(205.046152599995,-4.88950959216643,130.255867593678));
#19126=CARTESIAN_POINT('Ctrl Pts',(205.038329309002,-4.90102524937068,130.393100885121));
#19127=CARTESIAN_POINT('Ctrl Pts',(205.030506018009,-4.91254090657492,130.530334176563));
#19128=CARTESIAN_POINT('Ctrl Pts',(205.022682727017,-4.9182723584033,130.667863456436));
#19129=CARTESIAN_POINT('Ctrl Pts',(205.014859436024,-4.91824993440617,130.805163869501));
#19130=CARTESIAN_POINT('',(205.360140563955,-4.91824853905311,130.808151475242));
#19131=CARTESIAN_POINT('Ctrl Pts',(205.430026442963,-4.76405452823405,129.582490119308));
#19132=CARTESIAN_POINT('Ctrl Pts',(205.422281762578,-4.79814669522109,129.71541496097));
#19133=CARTESIAN_POINT('Ctrl Pts',(205.414537082193,-4.82668292020064,129.849812538585));
#19134=CARTESIAN_POINT('Ctrl Pts',(205.406792401809,-4.8495489326977,129.985179189633));
#19135=CARTESIAN_POINT('Ctrl Pts',(205.399017095509,-4.87250536759203,130.121081140708));
#19136=CARTESIAN_POINT('Ctrl Pts',(205.391241789208,-4.88974655166597,130.257959461279));
#19137=CARTESIAN_POINT('Ctrl Pts',(205.383466482908,-4.90120888938085,130.395295237518));
#19138=CARTESIAN_POINT('Ctrl Pts',(205.375691176608,-4.91267122709574,130.532631013756));
#19139=CARTESIAN_POINT('Ctrl Pts',(205.367915870308,-4.91835469588896,130.670423848268));
#19140=CARTESIAN_POINT('Ctrl Pts',(205.360140564008,-4.91824853905384,130.808151474305));
#19141=CARTESIAN_POINT('Ctrl Pts',(205.360140563955,-4.91824853905311,130.808151475242));
#19142=CARTESIAN_POINT('Ctrl Pts',(205.351139825899,-4.91812565127672,130.967585745387));
#19143=CARTESIAN_POINT('Ctrl Pts',(205.342139087842,-4.91024632687204,131.126698725876));
#19144=CARTESIAN_POINT('Ctrl Pts',(205.333138349785,-4.89472759256679,131.284802973177));
#19145=CARTESIAN_POINT('Ctrl Pts',(205.324085898924,-4.87911969698644,131.443815592));
#19146=CARTESIAN_POINT('Ctrl Pts',(205.315033448062,-4.85578446545969,131.601807746443));
#19147=CARTESIAN_POINT('Ctrl Pts',(205.3059809972,-4.82489013514455,131.758099704678));
#19148=CARTESIAN_POINT('Ctrl Pts',(205.296866878366,-4.79378534351451,131.915456369954));
#19149=CARTESIAN_POINT('Ctrl Pts',(205.287752759532,-4.75501819248919,132.071089491341));
#19150=CARTESIAN_POINT('Ctrl Pts',(205.278638640698,-4.70880867544122,132.224326786385));
#19151=CARTESIAN_POINT('Ctrl Pts',(205.274555892192,-4.68810872187624,132.292970760494));
#19152=CARTESIAN_POINT('Ctrl Pts',(205.270473143687,-4.6659159667685,132.361134266192));
#19153=CARTESIAN_POINT('Ctrl Pts',(205.266390395182,-4.64225323707004,132.42875833531));
#19154=CARTESIAN_POINT('Ctrl Pts',(205.25861606485,-4.59719489536611,132.557527435603));
#19155=CARTESIAN_POINT('Ctrl Pts',(205.250841734518,-4.54670333252088,132.684624302624));
#19156=CARTESIAN_POINT('Ctrl Pts',(205.243067404185,-4.49092120076951,132.809556326463));
#19157=CARTESIAN_POINT('Ctrl Pts',(205.235302655081,-4.43520781594627,132.934334381772));
#19158=CARTESIAN_POINT('Ctrl Pts',(205.227537905977,-4.3742169933291,133.05695254884));
#19159=CARTESIAN_POINT('Ctrl Pts',(205.219773156873,-4.30814086066012,133.176934196448));
#19160=CARTESIAN_POINT('Ctrl Pts',(205.212016119882,-4.24213035621027,133.296796675734));
#19161=CARTESIAN_POINT('Ctrl Pts',(205.204259082892,-4.17104478048607,133.414027506535));
#19162=CARTESIAN_POINT('Ctrl Pts',(205.196502045902,-4.0951238198962,133.528171176731));
#19163=CARTESIAN_POINT('Ctrl Pts',(205.188750858604,-4.0192601123862,133.642228769556));
#19164=CARTESIAN_POINT('Ctrl Pts',(205.180999671306,-3.93856849366088,133.753203511446));
#19165=CARTESIAN_POINT('Ctrl Pts',(205.173248484008,-3.85333375056227,133.860665914698));
#19166=CARTESIAN_POINT('Ctrl Pts',(205.165500591231,-3.76813523516348,133.96808264273));
#19167=CARTESIAN_POINT('Ctrl Pts',(205.157752698454,-3.67839767841762,134.071989695647));
#19168=CARTESIAN_POINT('Ctrl Pts',(205.150004805678,-3.58444808691414,134.171988116966));
#19169=CARTESIAN_POINT('Ctrl Pts',(205.142258533629,-3.49051814807432,134.271965620309));
#19170=CARTESIAN_POINT('Ctrl Pts',(205.134512261581,-3.39237819453857,134.368035833586));
#19171=CARTESIAN_POINT('Ctrl Pts',(205.126765989532,-3.29039400191811,134.459834646285));
#19172=CARTESIAN_POINT('Ctrl Pts',(205.119019660333,-3.18840905688475,134.551634136252));
#19173=CARTESIAN_POINT('Ctrl Pts',(205.111273331135,-3.0825801067567,134.639161901196));
#19174=CARTESIAN_POINT('Ctrl Pts',(205.103527001936,-2.97330779642674,134.722092590303));
#19175=CARTESIAN_POINT('Ctrl Pts',(205.095778938027,-2.86401101569629,134.805041850878));
#19176=CARTESIAN_POINT('Ctrl Pts',(205.088030874119,-2.75126965172672,134.883391750785));
#19177=CARTESIAN_POINT('Ctrl Pts',(205.08028281021,-2.63551491623087,134.956859165287));
#19178=CARTESIAN_POINT('Ctrl Pts',(205.072526511583,-2.51963715546859,135.030404661676));
#19179=CARTESIAN_POINT('Ctrl Pts',(205.064770212956,-2.40073995618037,135.09905709693));
#19180=CARTESIAN_POINT('Ctrl Pts',(205.057013914329,-2.27928130406476,135.162578120105));
#19181=CARTESIAN_POINT('Ctrl Pts',(205.049253475948,-2.15775782605347,135.226133046236));
#19182=CARTESIAN_POINT('Ctrl Pts',(205.041493037566,-2.03367052466753,135.284550936595));
#19183=CARTESIAN_POINT('Ctrl Pts',(205.033732599185,-1.90749822121525,135.337641283768));
#19184=CARTESIAN_POINT('Ctrl Pts',(205.025959703041,-1.78112337448988,135.390816856402));
#19185=CARTESIAN_POINT('Ctrl Pts',(205.018186806897,-1.65265720386027,135.438647659219));
#19186=CARTESIAN_POINT('Ctrl Pts',(205.010413910753,-1.52259542748432,135.480992549491));
#19187=CARTESIAN_POINT('Ctrl Pts',(205.002923530958,-1.39726092104092,135.521798357858));
#19188=CARTESIAN_POINT('Ctrl Pts',(204.995433151164,-1.27044508084342,135.557510033643));
#19189=CARTESIAN_POINT('Ctrl Pts',(204.987942771369,-1.14259930875746,135.588046422688));
#19190=CARTESIAN_POINT('Ctrl Pts',(204.980168435136,-1.00990696933439,135.619740430505));
#19191=CARTESIAN_POINT('Ctrl Pts',(204.972394098903,-0.875684739349071,
135.645959422382));
#19192=CARTESIAN_POINT('Ctrl Pts',(204.964619762671,-0.740424173411585,
135.666557148552));
#19193=CARTESIAN_POINT('Ctrl Pts',(204.956855007588,-0.605330303598526,
135.687129489931));
#19194=CARTESIAN_POINT('Ctrl Pts',(204.949090252504,-0.469201026759951,
135.702094291348));
#19195=CARTESIAN_POINT('Ctrl Pts',(204.941325497421,-0.332541196813679,
135.711355565079));
#19196=CARTESIAN_POINT('Ctrl Pts',(204.93356845438,-0.196017098948459,135.720607640409));
#19197=CARTESIAN_POINT('Ctrl Pts',(204.925811411339,-0.0589638841786129,
135.724167435013));
#19198=CARTESIAN_POINT('Ctrl Pts',(204.918054368298,0.0781056551375337,
135.721990389025));
#19199=CARTESIAN_POINT('Ctrl Pts',(204.910303174885,0.215071829587541,135.719814984758));
#19200=CARTESIAN_POINT('Ctrl Pts',(204.902551981471,0.35205391474676,135.711911357085));
#19201=CARTESIAN_POINT('Ctrl Pts',(204.894800788057,0.488536635525835,135.69828695725));
#19202=CARTESIAN_POINT('Ctrl Pts',(204.887052889087,0.624961347859993,135.684668348112));
#19203=CARTESIAN_POINT('Ctrl Pts',(204.879304990118,0.760886729730015,135.665333841567));
#19204=CARTESIAN_POINT('Ctrl Pts',(204.871557091148,0.895800372082467,135.640342912393));
#19205=CARTESIAN_POINT('Ctrl Pts',(204.86381081286,1.03068579361427,135.615357210744));
#19206=CARTESIAN_POINT('Ctrl Pts',(204.856064534572,1.16455951239554,135.584717511067));
#19207=CARTESIAN_POINT('Ctrl Pts',(204.848318256284,1.29691748072938,135.548534740707));
#19208=CARTESIAN_POINT('Ctrl Pts',(204.840571920805,1.42927642625718,135.512351703211));
#19209=CARTESIAN_POINT('Ctrl Pts',(204.832825585326,1.56011922188006,135.470625616466));
#19210=CARTESIAN_POINT('Ctrl Pts',(204.825079249848,1.68895558188255,135.423517694883));
#19211=CARTESIAN_POINT('Ctrl Pts',(204.817331179624,1.81782079400553,135.376399223767));
#19212=CARTESIAN_POINT('Ctrl Pts',(204.809583109401,1.9446783092763,135.323896653782));
#19213=CARTESIAN_POINT('Ctrl Pts',(204.801835039178,2.06905684589674,135.26621974028));
#19214=CARTESIAN_POINT('Ctrl Pts',(204.794078734217,2.19356757344921,135.208481527095));
#19215=CARTESIAN_POINT('Ctrl Pts',(204.786322429256,2.31559370402974,135.145558149584));
#19216=CARTESIAN_POINT('Ctrl Pts',(204.778566124295,2.43468715333658,135.077706090129));
#19217=CARTESIAN_POINT('Ctrl Pts',(204.770805679558,2.55384416642928,135.009817815973));
#19218=CARTESIAN_POINT('Ctrl Pts',(204.763045234822,2.67006504819365,134.936995825692));
#19219=CARTESIAN_POINT('Ctrl Pts',(204.755284790086,2.78293070430418,134.85953999184));
#19220=CARTESIAN_POINT('Ctrl Pts',(204.747511887616,2.89597754207783,134.78195981922));
#19221=CARTESIAN_POINT('Ctrl Pts',(204.739738985146,3.00565807806422,134.699731172902));
#19222=CARTESIAN_POINT('Ctrl Pts',(204.731966082676,3.11158561669959,134.613194824045));
#19223=CARTESIAN_POINT('Ctrl Pts',(204.724475770969,3.21366206571824,134.529804580902));
#19224=CARTESIAN_POINT('Ctrl Pts',(204.716985459263,3.31225343579821,134.442414621717));
#19225=CARTESIAN_POINT('Ctrl Pts',(204.709495147556,3.40704746464756,134.351360848203));
#19226=CARTESIAN_POINT('Ctrl Pts',(204.701720813585,3.50543595201642,134.256854441481));
#19227=CARTESIAN_POINT('Ctrl Pts',(204.693946479614,3.60004509988113,134.158101516487));
#19228=CARTESIAN_POINT('Ctrl Pts',(204.686172145643,3.69048616693734,134.055436580097));
#19229=CARTESIAN_POINT('Ctrl Pts',(204.678407392841,3.78081577349329,133.952898169028));
#19230=CARTESIAN_POINT('Ctrl Pts',(204.670642640039,3.86698726395705,133.846457629871));
#19231=CARTESIAN_POINT('Ctrl Pts',(204.662877887237,3.94864699528088,133.736487826464));
#19232=CARTESIAN_POINT('Ctrl Pts',(204.655120846494,4.03022562103922,133.626627246574));
#19233=CARTESIAN_POINT('Ctrl Pts',(204.647363805751,4.107301173756,133.513244690025));
#19234=CARTESIAN_POINT('Ctrl Pts',(204.639606765008,4.17955898715758,133.396747497522));
#19235=CARTESIAN_POINT('Ctrl Pts',(204.631855573906,4.25176231040909,133.280338156412));
#19236=CARTESIAN_POINT('Ctrl Pts',(204.624104382805,4.31915492055407,133.160819185333));
#19237=CARTESIAN_POINT('Ctrl Pts',(204.616353191703,4.38146456774871,133.038628127078));
#19238=CARTESIAN_POINT('Ctrl Pts',(204.60860529506,4.44374773172442,132.916489003198));
#19239=CARTESIAN_POINT('Ctrl Pts',(204.600857398416,4.50095205236715,132.79168039854));
#19240=CARTESIAN_POINT('Ctrl Pts',(204.593109501772,4.55285059786026,132.664665564628));
#19241=CARTESIAN_POINT('Ctrl Pts',(204.585363225818,4.60473828731866,132.537677299427));
#19242=CARTESIAN_POINT('Ctrl Pts',(204.577616949864,4.65132226139587,132.4084840846));
#19243=CARTESIAN_POINT('Ctrl Pts',(204.56987067391,4.6924233962874,132.277569948406));
#19244=CARTESIAN_POINT('Ctrl Pts',(204.562124340771,4.73352483459662,132.146654845776));
#19245=CARTESIAN_POINT('Ctrl Pts',(204.554378007632,4.7691432358447,132.014019169442));
#19246=CARTESIAN_POINT('Ctrl Pts',(204.546631674493,4.7991492228434,131.880162550722));
#19247=CARTESIAN_POINT('Ctrl Pts',(204.538883606613,4.82916192948898,131.746275955676));
#19248=CARTESIAN_POINT('Ctrl Pts',(204.531135538733,4.85355963536943,131.611168255589));
#19249=CARTESIAN_POINT('Ctrl Pts',(204.523387470853,4.87226407424628,131.475349330816));
#19250=CARTESIAN_POINT('Ctrl Pts',(204.515631168227,4.89098839243932,131.339386055957));
#19251=CARTESIAN_POINT('Ctrl Pts',(204.507874865602,4.90400730292682,131.202710434351));
#19252=CARTESIAN_POINT('Ctrl Pts',(204.500118562976,4.91129439105524,131.065838086747));
#19253=CARTESIAN_POINT('Ctrl Pts',(204.492358120575,4.91858536852522,130.92889268619));
#19254=CARTESIAN_POINT('Ctrl Pts',(204.484597678174,4.92013842339908,130.791750741167));
#19255=CARTESIAN_POINT('Ctrl Pts',(204.476837235773,4.91597931619433,130.654926935789));
#19256=CARTESIAN_POINT('Ctrl Pts',(204.469064335614,4.91181353241767,130.517883488567));
#19257=CARTESIAN_POINT('Ctrl Pts',(204.461291435454,4.90191729087102,130.381159591714));
#19258=CARTESIAN_POINT('Ctrl Pts',(204.453518535295,4.88636827354715,130.245264778043));
#19259=CARTESIAN_POINT('Ctrl Pts',(204.446028198111,4.87138449911938,130.114310056498));
#19260=CARTESIAN_POINT('Ctrl Pts',(204.438537860927,4.85115184404818,129.984125490812));
#19261=CARTESIAN_POINT('Ctrl Pts',(204.431047523743,4.8257841278719,129.855155363851));
#19262=CARTESIAN_POINT('Ctrl Pts',(204.423273190132,4.79945459374589,129.721295329489));
#19263=CARTESIAN_POINT('Ctrl Pts',(204.415498856521,4.7675095188085,129.588319613196));
#19264=CARTESIAN_POINT('Ctrl Pts',(204.40772452291,4.73002020891244,129.456736083143));
#19265=CARTESIAN_POINT('Ctrl Pts',(204.399959770479,4.69257710128169,129.325314718175));
#19266=CARTESIAN_POINT('Ctrl Pts',(204.392195018048,4.64960345998627,129.195282498014));
#19267=CARTESIAN_POINT('Ctrl Pts',(204.384430265617,4.60122183314642,129.067138494556));
#19268=CARTESIAN_POINT('Ctrl Pts',(204.376673225255,4.55288825966949,128.939121765658));
#19269=CARTESIAN_POINT('Ctrl Pts',(204.368916184894,4.49915752696644,128.812989884719));
#19270=CARTESIAN_POINT('Ctrl Pts',(204.361159144532,4.44020225742291,128.689227766969));
#19271=CARTESIAN_POINT('Ctrl Pts',(204.353407953822,4.38129144656131,128.565558979308));
#19272=CARTESIAN_POINT('Ctrl Pts',(204.345656763112,4.31716410838634,128.444256749339));
#19273=CARTESIAN_POINT('Ctrl Pts',(204.337905572402,4.24804120227294,128.325786631119));
#19274=CARTESIAN_POINT('Ctrl Pts',(204.330157676164,4.17894767531605,128.207366865993));
#19275=CARTESIAN_POINT('Ctrl Pts',(204.322409779926,4.10486300002969,128.091777155478));
#19276=CARTESIAN_POINT('Ctrl Pts',(204.314661883687,4.02605426077588,127.979458822496));
#19277=CARTESIAN_POINT('Ctrl Pts',(204.306915608147,3.94726200666425,127.867163984164));
#19278=CARTESIAN_POINT('Ctrl Pts',(204.299169332607,3.86374787853738,127.758139482086));
#19279=CARTESIAN_POINT('Ctrl Pts',(204.291423057066,3.77582228221695,127.65279764729));
#19280=CARTESIAN_POINT('Ctrl Pts',(204.283676724349,3.68789603690174,127.547455034947));
#19281=CARTESIAN_POINT('Ctrl Pts',(204.275930391632,3.59555850894457,127.445795444277));
#19282=CARTESIAN_POINT('Ctrl Pts',(204.268184058915,3.49916012072415,127.348197786906));
#19283=CARTESIAN_POINT('Ctrl Pts',(204.260435991465,3.40274014480243,127.250578273267));
#19284=CARTESIAN_POINT('Ctrl Pts',(204.252687924014,3.30225777370524,127.15702278111));
#19285=CARTESIAN_POINT('Ctrl Pts',(204.244939856564,3.19809967933992,127.067872760834));
#19286=CARTESIAN_POINT('Ctrl Pts',(204.237183554378,3.09383088454986,126.978627990887));
#19287=CARTESIAN_POINT('Ctrl Pts',(204.229427252191,2.9858788601325,126.893798300623));
#19288=CARTESIAN_POINT('Ctrl Pts',(204.221670950005,2.87466313460505,126.813684619061));
#19289=CARTESIAN_POINT('Ctrl Pts',(204.21391050805,2.76338804993092,126.73352817844));
#19290=CARTESIAN_POINT('Ctrl Pts',(204.206150066094,2.64884611955096,126.658092976936));
#19291=CARTESIAN_POINT('Ctrl Pts',(204.198389624139,2.53148428592039,126.587635540846));
#19292=CARTESIAN_POINT('Ctrl Pts',(204.190616724431,2.41393405262733,126.517065000208));
#19293=CARTESIAN_POINT('Ctrl Pts',(204.182843824723,2.29355521370091,126.451488380188));
#19294=CARTESIAN_POINT('Ctrl Pts',(204.175070925015,2.17081844249119,126.391115739674));
#19295=CARTESIAN_POINT('Ctrl Pts',(204.16758058332,2.05254335990331,126.332937746457));
#19296=CARTESIAN_POINT('Ctrl Pts',(204.160090241625,1.932079080105,126.279592079101));
#19297=CARTESIAN_POINT('Ctrl Pts',(204.15259989993,1.80986091391834,126.231223124032));
#19298=CARTESIAN_POINT('Ctrl Pts',(204.144825565478,1.68300890386598,126.181020282947));
#19299=CARTESIAN_POINT('Ctrl Pts',(204.137051231027,1.55386555861245,126.136019952371));
#19300=CARTESIAN_POINT('Ctrl Pts',(204.129276896576,1.42289670472903,126.096436655757));
#19301=CARTESIAN_POINT('Ctrl Pts',(204.121512143292,1.2920892581833,126.056902141999));
#19302=CARTESIAN_POINT('Ctrl Pts',(204.113747390009,1.15946115004296,126.022771490962));
#19303=CARTESIAN_POINT('Ctrl Pts',(204.105982636726,1.02549850401181,125.994211359927));
#19304=CARTESIAN_POINT('Ctrl Pts',(204.098225595501,0.891668911505565,125.965679595202));
#19305=CARTESIAN_POINT('Ctrl Pts',(204.090468554277,0.756507798773581,125.942707421116));
#19306=CARTESIAN_POINT('Ctrl Pts',(204.082711513052,0.620516445466882,125.925411714021));
#19307=CARTESIAN_POINT('Ctrl Pts',(204.07496032147,0.484627644240924,125.908129049746));
#19308=CARTESIAN_POINT('Ctrl Pts',(204.067209129887,0.347910234907202,125.896514381183));
#19309=CARTESIAN_POINT('Ctrl Pts',(204.059457938304,0.210875335327797,125.890633452221));
#19310=CARTESIAN_POINT('Ctrl Pts',(204.051710041182,0.0738986791749443,
125.884755022807));
#19311=CARTESIAN_POINT('Ctrl Pts',(204.043962144059,-0.0633948090470082,
125.884605502735));
#19312=CARTESIAN_POINT('Ctrl Pts',(204.036214246936,-0.200489466144424,
125.89019873211));
#19313=CARTESIAN_POINT('Ctrl Pts',(204.028467970504,-0.337555446031198,
125.895790791504));
#19314=CARTESIAN_POINT('Ctrl Pts',(204.020721694072,-0.474422287127775,
125.907123195051));
#19315=CARTESIAN_POINT('Ctrl Pts',(204.01297541764,-0.61057530164394,125.924157664458));
#19316=CARTESIAN_POINT('Ctrl Pts',(204.005229084025,-0.746729321239624,
125.941192259614));
#19317=CARTESIAN_POINT('Ctrl Pts',(203.997482750411,-0.882169115799372,
125.963928956088));
#19318=CARTESIAN_POINT('Ctrl Pts',(203.989736416796,-1.0163864843013,125.992277744523));
#19319=CARTESIAN_POINT('Ctrl Pts',(203.981988348442,-1.15063390987372,126.020632881478));
#19320=CARTESIAN_POINT('Ctrl Pts',(203.974240280088,-1.28365798219704,126.054602530483));
#19321=CARTESIAN_POINT('Ctrl Pts',(203.966492211735,-1.41496242369231,126.094045935717));
#19322=CARTESIAN_POINT('Ctrl Pts',(203.958735908642,-1.54640641710633,126.133531261871));
#19323=CARTESIAN_POINT('Ctrl Pts',(203.950979605549,-1.67612675374356,126.178501852826));
#19324=CARTESIAN_POINT('Ctrl Pts',(203.943223302457,-1.80364348801349,126.228767406774));
#19325=CARTESIAN_POINT('Ctrl Pts',(203.935462859591,-1.93122828181124,126.279059788964));
#19326=CARTESIAN_POINT('Ctrl Pts',(203.927702416725,-2.05660677247295,126.334652606956));
#19327=CARTESIAN_POINT('Ctrl Pts',(203.91994197386,-2.17932155377599,126.395308494065));
#19328=CARTESIAN_POINT('Ctrl Pts',(203.912169073245,-2.30223332769157,126.456061751365));
#19329=CARTESIAN_POINT('Ctrl Pts',(203.904396172631,-2.42247250426769,126.521894131622));
#19330=CARTESIAN_POINT('Ctrl Pts',(203.896623272017,-2.53960794450345,126.592523185908));
#19331=CARTESIAN_POINT('Ctrl Pts',(203.88913294005,-2.65248515417354,126.660584658622));
#19332=CARTESIAN_POINT('Ctrl Pts',(203.881642608084,-2.76248011304978,126.733099943225));
#19333=CARTESIAN_POINT('Ctrl Pts',(203.874152276117,-2.86923605004317,126.809780845971));
#19334=CARTESIAN_POINT('Ctrl Pts',(203.866074034918,-2.98437116185463,126.892480361897));
#19335=CARTESIAN_POINT('Ctrl Pts',(203.857995793719,-3.09613368668095,126.980309741443));
#19336=CARTESIAN_POINT('Ctrl Pts',(203.84991755252,-3.20403203740082,127.07295849962));
#19337=CARTESIAN_POINT('Ctrl Pts',(203.842215517175,-3.30690553306662,127.161292580348));
#19338=CARTESIAN_POINT('Ctrl Pts',(203.834513481829,-3.40626624325742,127.25400703648));
#19339=CARTESIAN_POINT('Ctrl Pts',(203.826811446484,-3.50171630356533,127.350787686261));
#19340=CARTESIAN_POINT('Ctrl Pts',(203.819116363939,-3.59708019895571,127.447480969971));
#19341=CARTESIAN_POINT('Ctrl Pts',(203.811421281394,-3.68854018756952,127.548232866472));
#19342=CARTESIAN_POINT('Ctrl Pts',(203.803726198849,-3.77573196917681,127.65268944826));
#19343=CARTESIAN_POINT('Ctrl Pts',(203.796036329942,-3.8628646758669,127.757075257736));
#19344=CARTESIAN_POINT('Ctrl Pts',(203.788346461035,-3.94573467410029,127.86516045547));
#19345=CARTESIAN_POINT('Ctrl Pts',(203.780656592127,-4.02401534417658,127.976555183606));
#19346=CARTESIAN_POINT('Ctrl Pts',(203.772970201974,-4.10226060153588,128.087899518843));
#19347=CARTESIAN_POINT('Ctrl Pts',(203.76528381182,-4.17592043400376,128.202550080349));
#19348=CARTESIAN_POINT('Ctrl Pts',(203.757597421666,-4.24470957225871,128.320085328941));
#19349=CARTESIAN_POINT('Ctrl Pts',(203.749911435145,-4.31349509821327,128.437614405444));
#19350=CARTESIAN_POINT('Ctrl Pts',(203.742225448624,-4.37741023070302,128.558027528844));
#19351=CARTESIAN_POINT('Ctrl Pts',(203.734539462103,-4.4362141058302,128.680875870803));
#19352=CARTESIAN_POINT('Ctrl Pts',(203.726853680479,-4.49501641333659,128.803720937816));
#19353=CARTESIAN_POINT('Ctrl Pts',(203.719167898855,-4.54870756838372,128.929000732856));
#19354=CARTESIAN_POINT('Ctrl Pts',(203.71148211723,-4.59709392678213,129.056244348308));
#19355=CARTESIAN_POINT('Ctrl Pts',(203.703792765134,-4.64550276332794,129.183547075479));
#19356=CARTESIAN_POINT('Ctrl Pts',(203.696103413038,-4.68860174757454,129.312815070517));
#19357=CARTESIAN_POINT('Ctrl Pts',(203.688414060942,-4.72624641962959,129.443560175386));
#19358=CARTESIAN_POINT('Ctrl Pts',(203.685700869741,-4.73952935838289,129.489693641968));
#19359=CARTESIAN_POINT('Ctrl Pts',(203.682987678541,-4.752133674154,129.536010890174));
#19360=CARTESIAN_POINT('Ctrl Pts',(203.680274487341,-4.76405452823405,129.582490119308));
#19361=CARTESIAN_POINT('Origin',(213.235140564004,0.,130.804360617566));
#19362=CARTESIAN_POINT('',(201.584606355351,-4.76405452823405,129.582490119308));
#19363=CARTESIAN_POINT('',(201.930097584127,-4.76405452823404,129.582490119308));
#19364=CARTESIAN_POINT('',(213.235140564004,-4.76405452823405,129.582490119308));
#19365=CARTESIAN_POINT('',(203.264859436027,-4.91824791911963,130.799836396593));
#19366=CARTESIAN_POINT('Ctrl Pts',(203.264859435991,-4.91824791912021,130.799836397221));
#19367=CARTESIAN_POINT('Ctrl Pts',(203.257189383465,-4.91837258488303,130.935359665711));
#19368=CARTESIAN_POINT('Ctrl Pts',(203.249519330939,-4.91289148263668,131.071020543707));
#19369=CARTESIAN_POINT('Ctrl Pts',(203.241849278414,-4.90179734488421,131.206313167236));
#19370=CARTESIAN_POINT('Ctrl Pts',(203.234183418891,-4.89070927198605,131.341531830077));
#19371=CARTESIAN_POINT('Ctrl Pts',(203.226517559368,-4.8740142988451,131.476382241115));
#19372=CARTESIAN_POINT('Ctrl Pts',(203.218851699845,-4.85175723294996,131.610359882465));
#19373=CARTESIAN_POINT('Ctrl Pts',(203.211187985896,-4.82950639651798,131.744300025216));
#19374=CARTESIAN_POINT('Ctrl Pts',(203.203524271947,-4.80169662793145,131.877367489554));
#19375=CARTESIAN_POINT('Ctrl Pts',(203.195860557999,-4.76842439234139,132.009064679576));
#19376=CARTESIAN_POINT('Ctrl Pts',(203.18819724317,-4.73515388954357,132.140755010911));
#19377=CARTESIAN_POINT('Ctrl Pts',(203.180533928342,-4.69642158345535,132.271074821851));
#19378=CARTESIAN_POINT('Ctrl Pts',(203.172870613514,-4.6523745561182,132.399538993825));
#19379=CARTESIAN_POINT('Ctrl Pts',(203.165205951912,-4.60831978783102,132.528025742458));
#19380=CARTESIAN_POINT('Ctrl Pts',(203.157541290311,-4.55894857073882,132.654655825109));
#19381=CARTESIAN_POINT('Ctrl Pts',(203.14987662871,-4.50445695066178,132.778962005729));
#19382=CARTESIAN_POINT('Ctrl Pts',(203.142204113634,-4.44990949660173,132.903395554725));
#19383=CARTESIAN_POINT('Ctrl Pts',(203.134531598558,-4.39023132120439,133.025500078541));
#19384=CARTESIAN_POINT('Ctrl Pts',(203.126859083481,-4.32566565593964,133.144830590782));
#19385=CARTESIAN_POINT('Ctrl Pts',(203.119182649825,-4.26106701508398,133.264222048637));
#19386=CARTESIAN_POINT('Ctrl Pts',(203.111506216169,-4.19157611789148,133.380836329876));
#19387=CARTESIAN_POINT('Ctrl Pts',(203.103829782513,-4.11748010840755,133.494256641461));
#19388=CARTESIAN_POINT('Ctrl Pts',(203.096141011026,-4.04326500925227,133.607859246098));
#19389=CARTESIAN_POINT('Ctrl Pts',(203.08845223954,-3.9644302428689,133.718257299233));
#19390=CARTESIAN_POINT('Ctrl Pts',(203.080763468054,-3.88130435803297,133.825065757565));
#19391=CARTESIAN_POINT('Ctrl Pts',(203.073308445649,-3.80070561283009,133.928627093911));
#19392=CARTESIAN_POINT('Ctrl Pts',(203.065853423243,-3.71607313595503,134.028813718384));
#19393=CARTESIAN_POINT('Ctrl Pts',(203.058398400838,-3.62773852230693,134.125308716569));
#19394=CARTESIAN_POINT('Ctrl Pts',(203.050624066711,-3.53562038179653,134.225936765238));
#19395=CARTESIAN_POINT('Ctrl Pts',(203.042849732584,-3.43916625203493,134.322888467361));
#19396=CARTESIAN_POINT('Ctrl Pts',(203.035075398457,-3.33870121485528,134.415767166326));
#19397=CARTESIAN_POINT('Ctrl Pts',(203.027310645502,-3.23835999185389,134.508531400596));
#19398=CARTESIAN_POINT('Ctrl Pts',(203.019545892547,-3.13401798102474,134.597232356386));
#19399=CARTESIAN_POINT('Ctrl Pts',(203.011781139593,-3.026039452382,134.68150754477));
#19400=CARTESIAN_POINT('Ctrl Pts',(203.0040240987,-2.91816816953492,134.76569902985));
#19401=CARTESIAN_POINT('Ctrl Pts',(202.996267057807,-2.80666786281095,134.845473256243));
#19402=CARTESIAN_POINT('Ctrl Pts',(202.988510016914,-2.69193820449843,134.920505873222));
#19403=CARTESIAN_POINT('Ctrl Pts',(202.980758825666,-2.57729506471272,134.995481907523));
#19404=CARTESIAN_POINT('Ctrl Pts',(202.973007634418,-2.45942774649362,135.065723236469));
#19405=CARTESIAN_POINT('Ctrl Pts',(202.96525644317,-2.33876713339567,135.130947188784));
#19406=CARTESIAN_POINT('Ctrl Pts',(202.957508546385,-2.21815780427522,135.196143419181));
#19407=CARTESIAN_POINT('Ctrl Pts',(202.949760649599,-2.09475788478772,135.256326328838));
#19408=CARTESIAN_POINT('Ctrl Pts',(202.942012752814,-1.96902504732344,135.311257934514));
#19409=CARTESIAN_POINT('Ctrl Pts',(202.934266476722,-1.84331851045724,135.366178049683));
#19410=CARTESIAN_POINT('Ctrl Pts',(202.92652020063,-1.71528038430399,135.415848889344));
#19411=CARTESIAN_POINT('Ctrl Pts',(202.918773924538,-1.58539025926972,135.460079765916));
#19412=CARTESIAN_POINT('Ctrl Pts',(202.911027591264,-1.45549917541524,135.504310968991));
#19413=CARTESIAN_POINT('Ctrl Pts',(202.903281257991,-1.32375643549607,135.54310200282));
#19414=CARTESIAN_POINT('Ctrl Pts',(202.895534924717,-1.19065842226258,135.576311537682));
#19415=CARTESIAN_POINT('Ctrl Pts',(202.887786856706,-1.05753060265117,135.609528509589));
#19416=CARTESIAN_POINT('Ctrl Pts',(202.880038788695,-0.923047285050385,
135.637161400668));
#19417=CARTESIAN_POINT('Ctrl Pts',(202.872290720684,-0.787716324822747,
135.659119731478));
#19418=CARTESIAN_POINT('Ctrl Pts',(202.864534417934,-0.65224153324019,135.681101399863));
#19419=CARTESIAN_POINT('Ctrl Pts',(202.856778115184,-0.515917685950118,
135.697396397709));
#19420=CARTESIAN_POINT('Ctrl Pts',(202.849021812434,-0.379259621354758,
135.707965944477));
#19421=CARTESIAN_POINT('Ctrl Pts',(202.841261369911,-0.242528618235135,
135.71854113253));
#19422=CARTESIAN_POINT('Ctrl Pts',(202.833500927389,-0.105463432899442,
135.723384766673));
#19423=CARTESIAN_POINT('Ctrl Pts',(202.825740484867,0.0314207805563875,
135.722510248987));
#19424=CARTESIAN_POINT('Ctrl Pts',(202.817967584593,0.168524732702548,135.721634327448));
#19425=CARTESIAN_POINT('Ctrl Pts',(202.810194684319,0.305446741698207,135.715021929815));
#19426=CARTESIAN_POINT('Ctrl Pts',(202.802421784046,0.441675557289912,135.70273848831));
#19427=CARTESIAN_POINT('Ctrl Pts',(202.794931448372,0.572952110607848,135.690901580996));
#19428=CARTESIAN_POINT('Ctrl Pts',(202.787441112698,0.703584688784279,135.673798825022));
#19429=CARTESIAN_POINT('Ctrl Pts',(202.779950777025,0.833126405809881,135.651533345502));
#19430=CARTESIAN_POINT('Ctrl Pts',(202.772176442908,0.96757973795983,135.628423663291));
#19431=CARTESIAN_POINT('Ctrl Pts',(202.764402108791,1.10128376375181,135.599678835429));
#19432=CARTESIAN_POINT('Ctrl Pts',(202.756627774674,1.23372905007338,135.565357959878));
#19433=CARTESIAN_POINT('Ctrl Pts',(202.748863021729,1.36601110941638,135.53107938174));
#19434=CARTESIAN_POINT('Ctrl Pts',(202.741098268784,1.49703714105001,135.491238526238));
#19435=CARTESIAN_POINT('Ctrl Pts',(202.733333515839,1.62630527593573,135.445945929931));
#19436=CARTESIAN_POINT('Ctrl Pts',(202.725576474956,1.75544501988741,135.40069831887));
#19437=CARTESIAN_POINT('Ctrl Pts',(202.717819434073,1.88282997506119,135.350009871036));
#19438=CARTESIAN_POINT('Ctrl Pts',(202.710062393191,2.00797122337188,135.294041522554));
#19439=CARTESIAN_POINT('Ctrl Pts',(202.702311201953,2.13301810169324,135.238115380238));
#19440=CARTESIAN_POINT('Ctrl Pts',(202.694560010715,2.25582428551557,135.17691742141));
#19441=CARTESIAN_POINT('Ctrl Pts',(202.686808819477,2.37591905240151,135.110657369874));
#19442=CARTESIAN_POINT('Ctrl Pts',(202.679060922702,2.49596277580801,135.044425480627));
#19443=CARTESIAN_POINT('Ctrl Pts',(202.671313025927,2.61329703275995,134.973135966364));
#19444=CARTESIAN_POINT('Ctrl Pts',(202.663565129152,2.72747421811156,134.897045244072));
#19445=CARTESIAN_POINT('Ctrl Pts',(202.65581885307,2.84162752005722,134.820970438319));
#19446=CARTESIAN_POINT('Ctrl Pts',(202.648072576988,2.95262473882447,134.740096638841));
#19447=CARTESIAN_POINT('Ctrl Pts',(202.640326300906,3.06004621322242,134.654724267332));
#19448=CARTESIAN_POINT('Ctrl Pts',(202.632579967643,3.1674684805811,134.569351265625));
#19449=CARTESIAN_POINT('Ctrl Pts',(202.62483363438,3.27131464482454,134.479479868875));
#19450=CARTESIAN_POINT('Ctrl Pts',(202.617087301116,3.37119749425472,134.385451305782));
#19451=CARTESIAN_POINT('Ctrl Pts',(202.609339233116,3.47110271175664,134.291401685645));
#19452=CARTESIAN_POINT('Ctrl Pts',(202.601591165115,3.56704256369362,134.193193314579));
#19453=CARTESIAN_POINT('Ctrl Pts',(202.593843097114,3.65866641892285,134.091204559335));
#19454=CARTESIAN_POINT('Ctrl Pts',(202.586086794374,3.75038765307602,133.989107409229));
#19455=CARTESIAN_POINT('Ctrl Pts',(202.578330491635,3.83778346561284,133.883222140185));
#19456=CARTESIAN_POINT('Ctrl Pts',(202.570574188895,3.92054294663494,133.7739609385));
#19457=CARTESIAN_POINT('Ctrl Pts',(202.562813746383,4.00334659888406,133.664641420822));
#19458=CARTESIAN_POINT('Ctrl Pts',(202.555053303871,4.08150876616667,133.551942701296));
#19459=CARTESIAN_POINT('Ctrl Pts',(202.547292861359,4.15476227066247,133.436305437804));
#19460=CARTESIAN_POINT('Ctrl Pts',(202.539519961095,4.22813336818707,133.320482543111));
#19461=CARTESIAN_POINT('Ctrl Pts',(202.531747060832,4.29657986120505,133.201712016897));
#19462=CARTESIAN_POINT('Ctrl Pts',(202.523974160569,4.35988045644892,133.080459356192));
#19463=CARTESIAN_POINT('Ctrl Pts',(202.516483824783,4.42087991581972,132.963614534721));
#19464=CARTESIAN_POINT('Ctrl Pts',(202.508993488998,4.47710098314102,132.844465187877));
#19465=CARTESIAN_POINT('Ctrl Pts',(202.501503153212,4.52838886767896,132.723443035176));
#19466=CARTESIAN_POINT('Ctrl Pts',(202.493728819094,4.58162134777368,132.597832291183));
#19467=CARTESIAN_POINT('Ctrl Pts',(202.485954484976,4.62970780184522,132.46980602598));
#19468=CARTESIAN_POINT('Ctrl Pts',(202.478180150858,4.67242258964327,132.339824783964));
#19469=CARTESIAN_POINT('Ctrl Pts',(202.470415397911,4.7150847352829,132.210003732212));
#19470=CARTESIAN_POINT('Ctrl Pts',(202.462650644965,4.75238826578558,132.078232865362));
#19471=CARTESIAN_POINT('Ctrl Pts',(202.454885892019,4.78415490621555,131.944994167762));
#19472=CARTESIAN_POINT('Ctrl Pts',(202.447128851135,4.81588999557021,131.811887804716));
#19473=CARTESIAN_POINT('Ctrl Pts',(202.439371810251,4.8420990486564,131.677316889991));
#19474=CARTESIAN_POINT('Ctrl Pts',(202.431614769367,4.86265319342588,131.541779754126));
#19475=CARTESIAN_POINT('Ctrl Pts',(202.423863578128,4.88319183815493,131.406344827869));
#19476=CARTESIAN_POINT('Ctrl Pts',(202.416112386889,4.89808400423516,131.269945515757));
#19477=CARTESIAN_POINT('Ctrl Pts',(202.40836119565,4.90725170126882,131.133091210749));
#19478=CARTESIAN_POINT('Ctrl Pts',(202.400613298874,4.91641550178662,130.996295072471));
#19479=CARTESIAN_POINT('Ctrl Pts',(202.392865402097,4.91985964633597,130.859044715197));
#19480=CARTESIAN_POINT('Ctrl Pts',(202.385117505321,4.91755792427646,130.721855321458));
#19481=CARTESIAN_POINT('Ctrl Pts',(202.377371229238,4.91525668368759,130.584694624784));
#19482=CARTESIAN_POINT('Ctrl Pts',(202.369624953155,4.907211973712,130.447595256941));
#19483=CARTESIAN_POINT('Ctrl Pts',(202.361878677072,4.89344971050554,130.311072676042));
#19484=CARTESIAN_POINT('Ctrl Pts',(202.354132343808,4.8796873457092,130.174549087364));
#19485=CARTESIAN_POINT('Ctrl Pts',(202.346386010544,4.86020738267642,130.038602683118));
#19486=CARTESIAN_POINT('Ctrl Pts',(202.338639677279,4.83508760939448,129.903743677918));
#19487=CARTESIAN_POINT('Ctrl Pts',(202.330891609277,4.80996221071351,129.76885447198));
#19488=CARTESIAN_POINT('Ctrl Pts',(202.323143541275,4.77919456014558,129.635053533938));
#19489=CARTESIAN_POINT('Ctrl Pts',(202.315395473273,4.74291346365742,129.502840376172));
#19490=CARTESIAN_POINT('Ctrl Pts',(202.307639170533,4.70659380718827,129.37048670069));
#19491=CARTESIAN_POINT('Ctrl Pts',(202.299882867792,4.66474910293164,129.239724554101));
#19492=CARTESIAN_POINT('Ctrl Pts',(202.292126565051,4.6175580804997,129.111038310469));
#19493=CARTESIAN_POINT('Ctrl Pts',(202.284366122538,4.57034187079823,128.982283383115));
#19494=CARTESIAN_POINT('Ctrl Pts',(202.276605680025,4.51777380687754,128.855606927377));
#19495=CARTESIAN_POINT('Ctrl Pts',(202.268845237512,4.46008021055639,128.731471913872));
#19496=CARTESIAN_POINT('Ctrl Pts',(202.261072337248,4.40229399935262,128.607137627823));
#19497=CARTESIAN_POINT('Ctrl Pts',(202.253299436983,4.33936599324112,128.485353284181));
#19498=CARTESIAN_POINT('Ctrl Pts',(202.245526536719,4.27156821364134,128.366556675755));
#19499=CARTESIAN_POINT('Ctrl Pts',(202.238036200946,4.20623505399508,128.252078623088));
#19500=CARTESIAN_POINT('Ctrl Pts',(202.230545865172,4.13638019427766,128.140375114719));
#19501=CARTESIAN_POINT('Ctrl Pts',(202.223055529399,4.06228318417237,128.03180973542));
#19502=CARTESIAN_POINT('Ctrl Pts',(202.215281195279,3.98537676351187,127.919128066919));
#19503=CARTESIAN_POINT('Ctrl Pts',(202.207506861159,3.90365654367928,127.80947024764));
#19504=CARTESIAN_POINT('Ctrl Pts',(202.199732527038,3.81738802965387,127.703275050614));
#19505=CARTESIAN_POINT('Ctrl Pts',(202.19196777409,3.73122583386185,127.597210729678));
#19506=CARTESIAN_POINT('Ctrl Pts',(202.184203021142,3.64052674103213,127.494600840736));
#19507=CARTESIAN_POINT('Ctrl Pts',(202.176438268194,3.54559989628898,127.395855895854));
#19508=CARTESIAN_POINT('Ctrl Pts',(202.168681227307,3.45076733422572,127.297209025842));
#19509=CARTESIAN_POINT('Ctrl Pts',(202.160924186421,3.35171564577153,127.202419740696));
#19510=CARTESIAN_POINT('Ctrl Pts',(202.153167145535,3.24879443203218,127.111865823948));
#19511=CARTESIAN_POINT('Ctrl Pts',(202.145415954294,3.14595083198053,127.021380194613));
#19512=CARTESIAN_POINT('Ctrl Pts',(202.137664763052,3.03924380716249,126.935123833573));
#19513=CARTESIAN_POINT('Ctrl Pts',(202.129913571811,2.92905976858584,126.853437695697));
#19514=CARTESIAN_POINT('Ctrl Pts',(202.122165675033,2.818922561165,126.771786276608));
#19515=CARTESIAN_POINT('Ctrl Pts',(202.114417778254,2.70531159267622,126.694701449615));
#19516=CARTESIAN_POINT('Ctrl Pts',(202.106669881476,2.58864613328299,126.622483735215));
#19517=CARTESIAN_POINT('Ctrl Pts',(202.098923605391,2.47200507778859,126.550281127204));
#19518=CARTESIAN_POINT('Ctrl Pts',(202.091177329306,2.35231113448206,126.482943812387));
#19519=CARTESIAN_POINT('Ctrl Pts',(202.08343105322,2.23001198118519,126.420728604467));
#19520=CARTESIAN_POINT('Ctrl Pts',(202.075684719954,2.10771192510372,126.358512937288));
#19521=CARTESIAN_POINT('Ctrl Pts',(202.067938386687,1.98280696912467,126.301419629723));
#19522=CARTESIAN_POINT('Ctrl Pts',(202.060192053421,1.85576841756085,126.249659019999));
#19523=CARTESIAN_POINT('Ctrl Pts',(202.052443985416,1.7287014165942,126.197886818844));
#19524=CARTESIAN_POINT('Ctrl Pts',(202.044695917412,1.5995002312647,126.151449839382));
#19525=CARTESIAN_POINT('Ctrl Pts',(202.036947849408,1.46865473825808,126.110509712148));
#19526=CARTESIAN_POINT('Ctrl Pts',(202.029191546665,1.33767018110433,126.06952607326));
#19527=CARTESIAN_POINT('Ctrl Pts',(202.021435243922,1.20503819899675,126.034051073798));
#19528=CARTESIAN_POINT('Ctrl Pts',(202.013678941179,1.07126291727623,126.004196159491));
#19529=CARTESIAN_POINT('Ctrl Pts',(202.005918498663,0.937416235660115,125.974325310717));
#19530=CARTESIAN_POINT('Ctrl Pts',(201.998158056148,0.802425423148925,125.950080593152));
#19531=CARTESIAN_POINT('Ctrl Pts',(201.990397613633,0.666802322505834,125.931521842765));
#19532=CARTESIAN_POINT('Ctrl Pts',(201.982624713366,0.530961507621308,125.912933300225));
#19533=CARTESIAN_POINT('Ctrl Pts',(201.974851813099,0.394486765759838,125.900049001524));
#19534=CARTESIAN_POINT('Ctrl Pts',(201.967078912833,0.257893458632686,125.892876725045));
#19535=CARTESIAN_POINT('Ctrl Pts',(201.959588577084,0.126265662529295,125.885965178895));
#19536=CARTESIAN_POINT('Ctrl Pts',(201.952098241335,-0.00547192021256673,
125.884357576005));
#19537=CARTESIAN_POINT('Ctrl Pts',(201.944607905586,-0.136862291999976,
125.888015249762));
#19538=CARTESIAN_POINT('Ctrl Pts',(201.936833571467,-0.273234369901628,
125.891811605337));
#19539=CARTESIAN_POINT('Ctrl Pts',(201.929059237349,-0.409664373849437,
125.901292410854));
#19540=CARTESIAN_POINT('Ctrl Pts',(201.92128490323,-0.545639639740232,125.916471456993));
#19541=CARTESIAN_POINT('Ctrl Pts',(201.913520150283,-0.681447328268266,
125.931631796315));
#19542=CARTESIAN_POINT('Ctrl Pts',(201.905755397337,-0.816801008994345,
125.952476360477));
#19543=CARTESIAN_POINT('Ctrl Pts',(201.89799064439,-0.951188206001152,125.978966948728));
#19544=CARTESIAN_POINT('Ctrl Pts',(201.890233603505,-1.08544192774853,126.005431226153));
#19545=CARTESIAN_POINT('Ctrl Pts',(201.882476562621,-1.21873069496959,126.037530292947));
#19546=CARTESIAN_POINT('Ctrl Pts',(201.874719521736,-1.35054769974211,126.075174221026));
#19547=CARTESIAN_POINT('Ctrl Pts',(201.866968330497,-1.48226530028765,126.112789761526));
#19548=CARTESIAN_POINT('Ctrl Pts',(201.859217139257,-1.6125129730937,126.155941733518));
#19549=CARTESIAN_POINT('Ctrl Pts',(201.851465948017,-1.74079499858619,126.204489332911));
#19550=CARTESIAN_POINT('Ctrl Pts',(201.84371805124,-1.86902250079471,126.253016298278));
#19551=CARTESIAN_POINT('Ctrl Pts',(201.835970154464,-1.99528565245025,126.306934191786));
#19552=CARTESIAN_POINT('Ctrl Pts',(201.828222257687,-2.11910499138351,126.366052708239));
#19553=CARTESIAN_POINT('Ctrl Pts',(201.820475981603,-2.24289842998043,126.425158858373));
#19554=CARTESIAN_POINT('Ctrl Pts',(201.81272970552,-2.36424872005608,126.489463299298));
#19555=CARTESIAN_POINT('Ctrl Pts',(201.804983429436,-2.48269781617095,126.558728201061));
#19556=CARTESIAN_POINT('Ctrl Pts',(201.797237096171,-2.60114778665004,126.627993614122));
#19557=CARTESIAN_POINT('Ctrl Pts',(201.789490762906,-2.71669618293738,126.702219363732));
#19558=CARTESIAN_POINT('Ctrl Pts',(201.781744429641,-2.82891129003388,126.781122621173));
#19559=CARTESIAN_POINT('Ctrl Pts',(201.773996361638,-2.94115152692565,126.860043548452));
#19560=CARTESIAN_POINT('Ctrl Pts',(201.766248293636,-3.05005666948663,126.943643843122));
#19561=CARTESIAN_POINT('Ctrl Pts',(201.758500225633,-3.15522594305475,127.031598723307));
#19562=CARTESIAN_POINT('Ctrl Pts',(201.750743922892,-3.26050699177834,127.119647082985));
#19563=CARTESIAN_POINT('Ctrl Pts',(201.74298762015,-3.36204393957021,127.212059022098));
#19564=CARTESIAN_POINT('Ctrl Pts',(201.735231317409,-3.45947053192138,127.30847064486));
#19565=CARTESIAN_POINT('Ctrl Pts',(201.727470874895,-3.55694912377835,127.404933725407));
#19566=CARTESIAN_POINT('Ctrl Pts',(201.719710432381,-3.65031272280732,127.505400457023));
#19567=CARTESIAN_POINT('Ctrl Pts',(201.711949989868,-3.73923432379541,127.609472554699));
#19568=CARTESIAN_POINT('Ctrl Pts',(201.704177089603,-3.82829866963167,127.713711718145));
#19569=CARTESIAN_POINT('Ctrl Pts',(201.696404189338,-3.9129065265913,127.821567505439));
#19570=CARTESIAN_POINT('Ctrl Pts',(201.688631289073,-3.99277278490735,127.932610532582));
#19571=CARTESIAN_POINT('Ctrl Pts',(201.681140953306,-4.06973570361064,128.039616866056));
#19572=CARTESIAN_POINT('Ctrl Pts',(201.67365061754,-4.14229560697238,128.14958247704));
#19573=CARTESIAN_POINT('Ctrl Pts',(201.666160281774,-4.21023800794793,128.262101980265));
#19574=CARTESIAN_POINT('Ctrl Pts',(201.658128312424,-4.28309339110042,128.382757879996));
#19575=CARTESIAN_POINT('Ctrl Pts',(201.650096343074,-4.35085732043947,128.506711456361));
#19576=CARTESIAN_POINT('Ctrl Pts',(201.642064373724,-4.41322893384724,128.633509761345));
#19577=CARTESIAN_POINT('Ctrl Pts',(201.634043232433,-4.47551646283025,128.760137126988));
#19578=CARTESIAN_POINT('Ctrl Pts',(201.626022091142,-4.53242599296163,128.889601270105));
#19579=CARTESIAN_POINT('Ctrl Pts',(201.618000949852,-4.58370062266684,129.021421565253));
#19580=CARTESIAN_POINT('Ctrl Pts',(201.609992618133,-4.63489336800769,129.153031346524));
#19581=CARTESIAN_POINT('Ctrl Pts',(201.601984286414,-4.68046901878164,129.286989451782));
#19582=CARTESIAN_POINT('Ctrl Pts',(201.593975954695,-4.72021745497381,129.422792580783));
#19583=CARTESIAN_POINT('Ctrl Pts',(201.590852754914,-4.73571909895888,129.475754960174));
#19584=CARTESIAN_POINT('Ctrl Pts',(201.587729555133,-4.75033495592387,129.528997715094));
#19585=CARTESIAN_POINT('Ctrl Pts',(201.584606355351,-4.76405452823405,129.582490119308));
#19586=CARTESIAN_POINT('Ctrl Pts',(203.334773566427,-4.76405452823405,129.582490119308));
#19587=CARTESIAN_POINT('Ctrl Pts',(203.32473014209,-4.80784291725373,129.753220383514));
#19588=CARTESIAN_POINT('Ctrl Pts',(203.314686717754,-4.84247434312161,129.926402595191));
#19589=CARTESIAN_POINT('Ctrl Pts',(203.304643293417,-4.86772242676584,130.101181096774));
#19590=CARTESIAN_POINT('Ctrl Pts',(203.294796401501,-4.89247644913987,130.272539485777));
#19591=CARTESIAN_POINT('Ctrl Pts',(203.284949509584,-4.90821079695266,130.445432509572));
#19592=CARTESIAN_POINT('Ctrl Pts',(203.275102617668,-4.91475699054651,130.619031757498));
#19593=CARTESIAN_POINT('Ctrl Pts',(203.271688223788,-4.9170268726106,130.679227016553));
#19594=CARTESIAN_POINT('Ctrl Pts',(203.268273829907,-4.91819242300989,130.739506976807));
#19595=CARTESIAN_POINT('Ctrl Pts',(203.264859436027,-4.91824791911963,130.799836396593));
#19596=CARTESIAN_POINT('',(203.610140564065,-4.91824975435206,130.805915067923));
#19597=CARTESIAN_POINT('Ctrl Pts',(203.680274487341,-4.76405452823405,129.582490119308));
#19598=CARTESIAN_POINT('Ctrl Pts',(203.672576598541,-4.7978764752882,129.714361377553));
#19599=CARTESIAN_POINT('Ctrl Pts',(203.664878709741,-4.82619293906168,129.847536976704));
#19600=CARTESIAN_POINT('Ctrl Pts',(203.65718082094,-4.84892836211919,129.981513850825));
#19601=CARTESIAN_POINT('Ctrl Pts',(203.649340778128,-4.87208363166798,130.1179648254));
#19602=CARTESIAN_POINT('Ctrl Pts',(203.641500735315,-4.88944965601479,130.255246526921));
#19603=CARTESIAN_POINT('Ctrl Pts',(203.633660692502,-4.90100205051574,130.392824515455));
#19604=CARTESIAN_POINT('Ctrl Pts',(203.62582064969,-4.9125544450167,130.530402503989));
#19605=CARTESIAN_POINT('Ctrl Pts',(203.617980606877,-4.91829325611943,130.668276348449));
#19606=CARTESIAN_POINT('Ctrl Pts',(203.610140564065,-4.91824975435206,130.805915067923));
#19607=CARTESIAN_POINT('Ctrl Pts',(203.610140564008,-4.91824975435174,130.80591506892));
#19608=CARTESIAN_POINT('Ctrl Pts',(203.60532859344,-4.91822305432427,130.890393366163));
#19609=CARTESIAN_POINT('Ctrl Pts',(203.600516622872,-4.91601993127815,130.974834611061));
#19610=CARTESIAN_POINT('Ctrl Pts',(203.595704652304,-4.91164526425146,131.059162227954));
#19611=CARTESIAN_POINT('Ctrl Pts',(203.587930318251,-4.90457744819619,131.195403930679));
#19612=CARTESIAN_POINT('Ctrl Pts',(203.580155984198,-4.89182542922343,131.331567131691));
#19613=CARTESIAN_POINT('Ctrl Pts',(203.572381650145,-4.87338772313762,131.467138983592));
#19614=CARTESIAN_POINT('Ctrl Pts',(203.564616897265,-4.85497273987956,131.60254375528));
#19615=CARTESIAN_POINT('Ctrl Pts',(203.556852144384,-4.83088606373339,131.737358244241));
#19616=CARTESIAN_POINT('Ctrl Pts',(203.549087391504,-4.80117818244719,131.871071038858));
#19617=CARTESIAN_POINT('Ctrl Pts',(203.541330350687,-4.77149980745165,132.004651028024));
#19618=CARTESIAN_POINT('Ctrl Pts',(203.53357330987,-4.73621142210639,132.1371311212));
#19619=CARTESIAN_POINT('Ctrl Pts',(203.525816269053,-4.69541509058143,132.268006814446));
#19620=CARTESIAN_POINT('Ctrl Pts',(203.518065077882,-4.65464952389258,132.398783813296));
#19621=CARTESIAN_POINT('Ctrl Pts',(203.510313886711,-4.60838439436307,132.527958448688));
#19622=CARTESIAN_POINT('Ctrl Pts',(203.50256269554,-4.55677236142872,132.655038522718));
#19623=CARTESIAN_POINT('Ctrl Pts',(203.494814798833,-4.50518226499348,132.782064584306));
#19624=CARTESIAN_POINT('Ctrl Pts',(203.487066902126,-4.44824993194415,132.906997493689));
#19625=CARTESIAN_POINT('Ctrl Pts',(203.479319005419,-4.38617711843204,133.029362493575));
#19626=CARTESIAN_POINT('Ctrl Pts',(203.471572729406,-4.32411728922029,133.151701897329));
#19627=CARTESIAN_POINT('Ctrl Pts',(203.463826453393,-4.25691929509247,133.271474111561));
#19628=CARTESIAN_POINT('Ctrl Pts',(203.456080177379,-4.18483188932866,133.388226930005));
#19629=CARTESIAN_POINT('Ctrl Pts',(203.448333844186,-4.11274395143813,133.504980610282));
#19630=CARTESIAN_POINT('Ctrl Pts',(203.440587510992,-4.03576673529106,133.618714517632));
#19631=CARTESIAN_POINT('Ctrl Pts',(203.432841177798,-3.95419334811849,133.729003848491));
#19632=CARTESIAN_POINT('Ctrl Pts',(203.425093109867,-3.87260169315755,133.839317877873));
#19633=CARTESIAN_POINT('Ctrl Pts',(203.417345041936,-3.78641205146594,133.946185481521));
#19634=CARTESIAN_POINT('Ctrl Pts',(203.409596974005,-3.69595872886982,134.049213794058));
#19635=CARTESIAN_POINT('Ctrl Pts',(203.401840671336,-3.60540927141139,134.152351606306));
#19636=CARTESIAN_POINT('Ctrl Pts',(203.394084368667,-3.51058733926155,134.251641682045));
#19637=CARTESIAN_POINT('Ctrl Pts',(203.386328065998,-3.41186551250551,134.346726604738));
#19638=CARTESIAN_POINT('Ctrl Pts',(203.378567623557,-3.3130909949427,134.441862277113));
#19639=CARTESIAN_POINT('Ctrl Pts',(203.370807181116,-3.21041272778059,134.532788065183));
#19640=CARTESIAN_POINT('Ctrl Pts',(203.363046738675,-3.10423672854745,134.619186615647));
#19641=CARTESIAN_POINT('Ctrl Pts',(203.355273838482,-2.99789028617232,134.705723860737));
#19642=CARTESIAN_POINT('Ctrl Pts',(203.34750093829,-2.8880352049204,134.787719111404));
#19643=CARTESIAN_POINT('Ctrl Pts',(203.339728038097,-2.77510758697802,134.864897644019));
#19644=CARTESIAN_POINT('Ctrl Pts',(203.332237701562,-2.66628516014054,134.939270550948));
#19645=CARTESIAN_POINT('Ctrl Pts',(203.324747365027,-2.55460996759745,135.009170695082));
#19646=CARTESIAN_POINT('Ctrl Pts',(203.317257028492,-2.44049242510876,135.074393379207));
#19647=CARTESIAN_POINT('Ctrl Pts',(203.309482694322,-2.32204809275828,135.142088994682));
#19648=CARTESIAN_POINT('Ctrl Pts',(203.301708360151,-2.20059735556435,135.204959896962));
#19649=CARTESIAN_POINT('Ctrl Pts',(203.293934025981,-2.0765708843453,135.262727630811));
#19650=CARTESIAN_POINT('Ctrl Pts',(203.286169272982,-1.95269726465683,135.320424171095));
#19651=CARTESIAN_POINT('Ctrl Pts',(203.278404519984,-1.82625457798257,135.373029893092));
#19652=CARTESIAN_POINT('Ctrl Pts',(203.270639766985,-1.69770037928056,135.420310843109));
#19653=CARTESIAN_POINT('Ctrl Pts',(203.262882726048,-1.56927386241116,135.467544833023));
#19654=CARTESIAN_POINT('Ctrl Pts',(203.25512568511,-1.43874037156367,135.509464441505));
#19655=CARTESIAN_POINT('Ctrl Pts',(203.247368644173,-1.30657952838765,135.545882841335));
#19656=CARTESIAN_POINT('Ctrl Pts',(203.23961745288,-1.1745183487227,135.582273777769));
#19657=CARTESIAN_POINT('Ctrl Pts',(203.231866261587,-1.04083263478582,135.613171659453));
#19658=CARTESIAN_POINT('Ctrl Pts',(203.224115070294,-0.906019002783906,
135.638438878113));
#19659=CARTESIAN_POINT('Ctrl Pts',(203.216367173464,-0.771262670161606,
135.663695357533));
#19660=CARTESIAN_POINT('Ctrl Pts',(203.208619276634,-0.635379756424377,
135.683325861913));
#19661=CARTESIAN_POINT('Ctrl Pts',(203.200871379803,-0.498878742470774,
135.697243516513));
#19662=CARTESIAN_POINT('Ctrl Pts',(203.193125103666,-0.362406281580614,
135.711158259841));
#19663=CARTESIAN_POINT('Ctrl Pts',(203.185378827528,-0.22531636634765,135.719362490687));
#19664=CARTESIAN_POINT('Ctrl Pts',(203.17763255139,-0.0881239079495214,
135.721821063706));
#19665=CARTESIAN_POINT('Ctrl Pts',(203.169886218071,0.0490695631770811,
135.724279654873));
#19666=CARTESIAN_POINT('Ctrl Pts',(203.162139884752,0.186365188076857,135.720992496577));
#19667=CARTESIAN_POINT('Ctrl Pts',(203.154393551432,0.323247135849997,135.711976571536));
#19668=CARTESIAN_POINT('Ctrl Pts',(203.146645483375,0.4601597373901,135.702958627442));
#19669=CARTESIAN_POINT('Ctrl Pts',(203.138897415318,0.596658087415218,135.688209389437));
#19670=CARTESIAN_POINT('Ctrl Pts',(203.131149347261,0.73223095668038,135.667797765158));
#19671=CARTESIAN_POINT('Ctrl Pts',(203.123393044465,0.867947914404447,135.647364447162));
#19672=CARTESIAN_POINT('Ctrl Pts',(203.115636741669,1.00273703927327,135.621256779485));
#19673=CARTESIAN_POINT('Ctrl Pts',(203.107880438873,1.13609623798184,135.589595031944));
#19674=CARTESIAN_POINT('Ctrl Pts',(203.100119996304,1.26952661451173,135.557916385574));
#19675=CARTESIAN_POINT('Ctrl Pts',(203.092359553736,1.40152516805726,135.520677858664));
#19676=CARTESIAN_POINT('Ctrl Pts',(203.084599111167,1.53160543789726,135.478049508057));
#19677=CARTESIAN_POINT('Ctrl Pts',(203.076826210848,1.66189452412713,135.435352726641));
#19678=CARTESIAN_POINT('Ctrl Pts',(203.069053310528,1.79025880671704,135.387248968902));
#19679=CARTESIAN_POINT('Ctrl Pts',(203.061280410209,1.9162314290031,135.333956645139));
#19680=CARTESIAN_POINT('Ctrl Pts',(203.053790075032,2.03762461883292,135.282601635949));
#19681=CARTESIAN_POINT('Ctrl Pts',(203.046299739856,2.15679673695984,135.226428878422));
#19682=CARTESIAN_POINT('Ctrl Pts',(203.038809404679,2.27335372629928,135.16567302298));
#19683=CARTESIAN_POINT('Ctrl Pts',(203.031035070571,2.39433001860291,135.102613585972));
#19684=CARTESIAN_POINT('Ctrl Pts',(203.023260736462,2.51287217837938,135.034416900165));
#19685=CARTESIAN_POINT('Ctrl Pts',(203.015486402354,2.62851314525934,134.961294789248));
#19686=CARTESIAN_POINT('Ctrl Pts',(203.007721649418,2.74401159498189,134.888262794799));
#19687=CARTESIAN_POINT('Ctrl Pts',(202.999956896482,2.85661563863572,134.810317659964));
#19688=CARTESIAN_POINT('Ctrl Pts',(202.992192143545,2.96588112472585,134.727717880994));
#19689=CARTESIAN_POINT('Ctrl Pts',(202.984435102671,3.07503808679438,134.64520014129));
#19690=CARTESIAN_POINT('Ctrl Pts',(202.976678061797,3.18086278023441,134.558037191785));
#19691=CARTESIAN_POINT('Ctrl Pts',(202.968921020923,3.28293877480054,134.466531567073));
#19692=CARTESIAN_POINT('Ctrl Pts',(202.961169829694,3.38493779306489,134.375094947464));
#19693=CARTESIAN_POINT('Ctrl Pts',(202.953418638464,3.483193449336,134.279322430943));
#19694=CARTESIAN_POINT('Ctrl Pts',(202.945667447235,3.57732153668663,134.179557454146));
#19695=CARTESIAN_POINT('Ctrl Pts',(202.937919550469,3.67140961708933,134.079834880125));
#19696=CARTESIAN_POINT('Ctrl Pts',(202.930171653703,3.76137335005203,133.976123504614));
#19697=CARTESIAN_POINT('Ctrl Pts',(202.922423756936,3.84686479905085,133.868804169065));
#19698=CARTESIAN_POINT('Ctrl Pts',(202.914677480863,3.93233836508166,133.761507282408));
#19699=CARTESIAN_POINT('Ctrl Pts',(202.90693120479,4.01334126447339,133.650604242471));
#19700=CARTESIAN_POINT('Ctrl Pts',(202.899184928717,4.08956560638427,133.536509261688));
#19701=CARTESIAN_POINT('Ctrl Pts',(202.891438595462,4.16579051096613,133.422413438681));
#19702=CARTESIAN_POINT('Ctrl Pts',(202.883692262207,4.23723657049395,133.305125952902));
#19703=CARTESIAN_POINT('Ctrl Pts',(202.875945928953,4.30363925381155,133.185089967062));
#19704=CARTESIAN_POINT('Ctrl Pts',(202.868197860961,4.37005680754998,133.065027099995));
#19705=CARTESIAN_POINT('Ctrl Pts',(202.860449792968,4.43142854843043,132.942214850122));
#19706=CARTESIAN_POINT('Ctrl Pts',(202.852701724976,4.48753611850486,132.817120575339));
#19707=CARTESIAN_POINT('Ctrl Pts',(202.844945422245,4.54370332037339,132.69189334887));
#19708=CARTESIAN_POINT('Ctrl Pts',(202.837189119514,4.59459501491842,132.564379609861));
#19709=CARTESIAN_POINT('Ctrl Pts',(202.829432816783,4.64004099484783,132.435066792397));
#19710=CARTESIAN_POINT('Ctrl Pts',(202.821672374279,4.68551123066541,132.305684956788));
#19711=CARTESIAN_POINT('Ctrl Pts',(202.813911931776,4.72552984631434,132.174502503168));
#19712=CARTESIAN_POINT('Ctrl Pts',(202.806151489272,4.75997697153195,132.04202062459));
#19713=CARTESIAN_POINT('Ctrl Pts',(202.798378589017,4.79447939433392,131.909326074335));
#19714=CARTESIAN_POINT('Ctrl Pts',(202.790605688762,4.82339237153089,131.775328313116));
#19715=CARTESIAN_POINT('Ctrl Pts',(202.782832788507,4.84664731046149,131.640538176758));
#19716=CARTESIAN_POINT('Ctrl Pts',(202.775342452627,4.86905687417027,131.510647999147));
#19717=CARTESIAN_POINT('Ctrl Pts',(202.767852116746,4.8862125852588,131.380022361244));
#19718=CARTESIAN_POINT('Ctrl Pts',(202.760361780866,4.89809886429187,131.249119628855));
#19719=CARTESIAN_POINT('Ctrl Pts',(202.752587446755,4.91043581499945,131.113253681868));
#19720=CARTESIAN_POINT('Ctrl Pts',(202.744813112644,4.91713494470752,130.976658831053));
#19721=CARTESIAN_POINT('Ctrl Pts',(202.737038778533,4.91812200914719,130.839842523405));
#19722=CARTESIAN_POINT('Ctrl Pts',(202.729274025594,4.91910785711814,130.703194829631));
#19723=CARTESIAN_POINT('Ctrl Pts',(202.721509272656,4.91439564375304,130.566326609267));
#19724=CARTESIAN_POINT('Ctrl Pts',(202.713744519717,4.90396277453586,130.429751263082));
#19725=CARTESIAN_POINT('Ctrl Pts',(202.70598747884,4.89354026739166,130.293311565459));
#19726=CARTESIAN_POINT('Ctrl Pts',(202.698230437964,4.87740844109174,130.157164550445));
#19727=CARTESIAN_POINT('Ctrl Pts',(202.690473397087,4.8555967358373,130.021824099935));
#19728=CARTESIAN_POINT('Ctrl Pts',(202.682722205856,4.83380147895985,129.886585710714));
#19729=CARTESIAN_POINT('Ctrl Pts',(202.674971014624,4.80633493061361,129.752153059763));
#19730=CARTESIAN_POINT('Ctrl Pts',(202.667219823393,4.77327836053893,129.619035027143));
#19731=CARTESIAN_POINT('Ctrl Pts',(202.659471926624,4.74023584038906,129.485973573241));
#19732=CARTESIAN_POINT('Ctrl Pts',(202.651724029856,4.70160811803909,129.35422600501));
#19733=CARTESIAN_POINT('Ctrl Pts',(202.643976133088,4.6575275379995,129.224290905409));
#19734=CARTESIAN_POINT('Ctrl Pts',(202.636229857012,4.61345617866757,129.094382985432));
#19735=CARTESIAN_POINT('Ctrl Pts',(202.628483580937,4.56393435592693,128.966287149981));
#19736=CARTESIAN_POINT('Ctrl Pts',(202.620737304862,4.50914413590637,128.840486328279));
#19737=CARTESIAN_POINT('Ctrl Pts',(202.612990971605,4.45435351143753,128.714684577946));
#19738=CARTESIAN_POINT('Ctrl Pts',(202.605244638349,4.39429456820026,128.591178233612));
#19739=CARTESIAN_POINT('Ctrl Pts',(202.597498305092,4.3291971659843,128.470429393101));
#19740=CARTESIAN_POINT('Ctrl Pts',(202.589750237099,4.26408518565718,128.349653511726));
#19741=CARTESIAN_POINT('Ctrl Pts',(202.582002169105,4.19393268660458,128.231636707049));
#19742=CARTESIAN_POINT('Ctrl Pts',(202.574254101111,4.11901484245543,128.116815308156));
#19743=CARTESIAN_POINT('Ctrl Pts',(202.566497798378,4.04401737473066,128.001871875715));
#19744=CARTESIAN_POINT('Ctrl Pts',(202.558741495645,3.9642446586756,127.890130961117));
#19745=CARTESIAN_POINT('Ctrl Pts',(202.550985192912,3.88001478519079,127.781999234607));
#19746=CARTESIAN_POINT('Ctrl Pts',(202.543224750407,3.79573995568691,127.67380979494));
#19747=CARTESIAN_POINT('Ctrl Pts',(202.535464307902,3.70700348138614,127.569233679702));
#19748=CARTESIAN_POINT('Ctrl Pts',(202.527703865397,3.61416223739328,127.468642646229));
#19749=CARTESIAN_POINT('Ctrl Pts',(202.519930965141,3.52117195639349,127.367890135099));
#19750=CARTESIAN_POINT('Ctrl Pts',(202.512158064885,3.42406401521649,127.2711357655));
#19751=CARTESIAN_POINT('Ctrl Pts',(202.504385164629,3.32323111850202,127.178713365623));
#19752=CARTESIAN_POINT('Ctrl Pts',(202.49689482877,3.22606375019959,127.089650751528));
#19753=CARTESIAN_POINT('Ctrl Pts',(202.489404492912,3.12543778266822,127.004610818164));
#19754=CARTESIAN_POINT('Ctrl Pts',(202.481914157053,3.02173043097238,126.923854430864));
#19755=CARTESIAN_POINT('Ctrl Pts',(202.474139822926,2.91409098479571,126.84003614159));
#19756=CARTESIAN_POINT('Ctrl Pts',(202.466365488799,2.80279091121412,126.760567120498));
#19757=CARTESIAN_POINT('Ctrl Pts',(202.458591154673,2.68821700891863,126.685784118888));
#19758=CARTESIAN_POINT('Ctrl Pts',(202.450826401718,2.57378430871652,126.611093280644));
#19759=CARTESIAN_POINT('Ctrl Pts',(202.443061648763,2.45608613190742,126.541077182797));
#19760=CARTESIAN_POINT('Ctrl Pts',(202.435296895808,2.33554220421387,126.476032340409));
#19761=CARTESIAN_POINT('Ctrl Pts',(202.427539854915,2.21511800244725,126.411052101475));
#19762=CARTESIAN_POINT('Ctrl Pts',(202.419782814022,2.09185401638329,126.351033476568));
#19763=CARTESIAN_POINT('Ctrl Pts',(202.412025773129,1.96619850256614,126.29622946253));
#19764=CARTESIAN_POINT('Ctrl Pts',(202.404274581881,1.8406377465481,126.241466776625));
#19765=CARTESIAN_POINT('Ctrl Pts',(202.396523390633,1.71268940938756,126.191911030093));
#19766=CARTESIAN_POINT('Ctrl Pts',(202.388772199385,1.58282555457417,126.147768910503));
#19767=CARTESIAN_POINT('Ctrl Pts',(202.3810243026,1.45301689536158,126.103645552491));
#19768=CARTESIAN_POINT('Ctrl Pts',(202.373276405815,1.3212947071609,126.064931370595));
#19769=CARTESIAN_POINT('Ctrl Pts',(202.36552850903,1.18814999737997,126.031784515897));
#19770=CARTESIAN_POINT('Ctrl Pts',(202.357782232937,1.05503313860108,125.998644594806));
#19771=CARTESIAN_POINT('Ctrl Pts',(202.350035956845,0.92049472925159,125.97106977892));
#19772=CARTESIAN_POINT('Ctrl Pts',(202.342289680753,0.785039482555496,125.949167925887));
#19773=CARTESIAN_POINT('Ctrl Pts',(202.33454334748,0.649583235958816,125.927265911181));
#19774=CARTESIAN_POINT('Ctrl Pts',(202.326797014206,0.513210524463309,125.911037005295));
#19775=CARTESIAN_POINT('Ctrl Pts',(202.319050680933,0.376434368889621,125.900537595839));
#19776=CARTESIAN_POINT('Ctrl Pts',(202.311302612921,0.239627583243728,125.890035835114));
#19777=CARTESIAN_POINT('Ctrl Pts',(202.30355454491,0.102417563480344,125.885266153919));
#19778=CARTESIAN_POINT('Ctrl Pts',(202.295806476899,-0.0346798563142518,
125.886232887416));
#19779=CARTESIAN_POINT('Ctrl Pts',(202.288050174149,-0.17192298487841,125.887200648369));
#19780=CARTESIAN_POINT('Ctrl Pts',(202.280293871399,-0.309052882836018,
125.893917000127));
#19781=CARTESIAN_POINT('Ctrl Pts',(202.272537568649,-0.445555471089543,
125.906334139005));
#19782=CARTESIAN_POINT('Ctrl Pts',(202.264777126127,-0.58213091488482,125.918757905285));
#19783=CARTESIAN_POINT('Ctrl Pts',(202.257016683604,-0.718077994486212,
125.936888469828));
#19784=CARTESIAN_POINT('Ctrl Pts',(202.249256241082,-0.852891040206172,
125.960626527421));
#19785=CARTESIAN_POINT('Ctrl Pts',(202.241483340808,-0.987920499794184,
125.984402691451));
#19786=CARTESIAN_POINT('Ctrl Pts',(202.233710440535,-1.12181190557149,126.013804252784));
#19787=CARTESIAN_POINT('Ctrl Pts',(202.225937540261,-1.25407213197427,126.048681260176));
#19788=CARTESIAN_POINT('Ctrl Pts',(202.218447204587,-1.38152436436558,126.082290400067));
#19789=CARTESIAN_POINT('Ctrl Pts',(202.210956868914,-1.50746165896199,126.120983714381));
#19790=CARTESIAN_POINT('Ctrl Pts',(202.20346653324,-1.63146064844767,126.164584845498));
#19791=CARTESIAN_POINT('Ctrl Pts',(202.195692103635,-1.76016267956143,126.209839683114));
#19792=CARTESIAN_POINT('Ctrl Pts',(202.187917674029,-1.88718416540828,126.260525329425));
#19793=CARTESIAN_POINT('Ctrl Pts',(202.180143244423,-2.01203269537097,126.316498376447));
#19794=CARTESIAN_POINT('Ctrl Pts',(202.172378418318,-2.1367270040091,126.372402281787));
#19795=CARTESIAN_POINT('Ctrl Pts',(202.164613592212,-2.2592533441934,126.433580433836));
#19796=CARTESIAN_POINT('Ctrl Pts',(202.156848766106,-2.37913536422814,126.499839972804));
#19797=CARTESIAN_POINT('Ctrl Pts',(202.149091674296,-2.49889797360211,126.566033512757));
#19798=CARTESIAN_POINT('Ctrl Pts',(202.141334582486,-2.61602116454483,126.637298179153));
#19799=CARTESIAN_POINT('Ctrl Pts',(202.133577490676,-2.73004978163739,126.713393586132));
#19800=CARTESIAN_POINT('Ctrl Pts',(202.125826270674,-2.84399208364077,126.78943139194));
#19801=CARTESIAN_POINT('Ctrl Pts',(202.118075050671,-2.95484415052419,126.870292443658));
#19802=CARTESIAN_POINT('Ctrl Pts',(202.110323830669,-3.06217692439492,126.955691296073));
#19803=CARTESIAN_POINT('Ctrl Pts',(202.102576019855,-3.16946249051467,127.041052587846));
#19804=CARTESIAN_POINT('Ctrl Pts',(202.094828209041,-3.27323153754679,127.130947467042));
#19805=CARTESIAN_POINT('Ctrl Pts',(202.087080398227,-3.37308562112851,127.225048329565));
#19806=CARTESIAN_POINT('Ctrl Pts',(202.079334239672,-3.47291841033375,127.319129124614));
#19807=CARTESIAN_POINT('Ctrl Pts',(202.071588081117,-3.568837612584,127.417413850761));
#19808=CARTESIAN_POINT('Ctrl Pts',(202.063841922562,-3.66047969139515,127.519536194346));
#19809=CARTESIAN_POINT('Ctrl Pts',(202.056095738413,-3.75212207299657,127.621658875349));
#19810=CARTESIAN_POINT('Ctrl Pts',(202.048349554264,-3.83948704196994,127.727618908041));
#19811=CARTESIAN_POINT('Ctrl Pts',(202.040603370115,-3.92224987613099,127.837015175645));
#19812=CARTESIAN_POINT('Ctrl Pts',(202.032855482865,-4.0050309067957,127.946435495465));
#19813=CARTESIAN_POINT('Ctrl Pts',(202.025107595616,-4.08320755361812,128.059293241692));
#19814=CARTESIAN_POINT('Ctrl Pts',(202.017359708366,-4.1564973670384,128.175156802663));
#19815=CARTESIAN_POINT('Ctrl Pts',(202.00960402534,-4.22986092326722,128.291136943332));
#19816=CARTESIAN_POINT('Ctrl Pts',(202.001848342314,-4.29832761616902,128.410128608468));
#19817=CARTESIAN_POINT('Ctrl Pts',(201.994092659288,-4.36165984536912,128.531673561283));
#19818=CARTESIAN_POINT('Ctrl Pts',(201.986332849536,-4.42502577306113,128.653283187041));
#19819=CARTESIAN_POINT('Ctrl Pts',(201.978573039783,-4.48325162754233,128.777448453866));
#19820=CARTESIAN_POINT('Ctrl Pts',(201.97081323003,-4.5361476689452,128.903690370516));
#19821=CARTESIAN_POINT('Ctrl Pts',(201.9630419948,-4.58912159402284,129.030118164673));
#19822=CARTESIAN_POINT('Ctrl Pts',(201.955270759571,-4.63674989270561,129.158628350682));
#19823=CARTESIAN_POINT('Ctrl Pts',(201.947499524341,-4.67889225145815,129.28872531785));
#19824=CARTESIAN_POINT('Ctrl Pts',(201.941698877603,-4.71034837504711,129.385832988111));
#19825=CARTESIAN_POINT('Ctrl Pts',(201.935898230865,-4.73874903929908,129.483824402015));
#19826=CARTESIAN_POINT('Ctrl Pts',(201.930097584127,-4.76405452823404,129.582490119308));
#19827=CARTESIAN_POINT('Origin',(213.235140564004,0.,130.804360617566));
#19828=CARTESIAN_POINT('',(199.834960626423,-4.76405452823405,129.582490119308));
#19829=CARTESIAN_POINT('',(200.179870531952,-4.76405452823405,129.582490119308));
#19830=CARTESIAN_POINT('',(213.235140564004,-4.76405452823405,129.582490119308));
#19831=CARTESIAN_POINT('',(201.51485943594,-4.91824986053202,130.805531888988));
#19832=CARTESIAN_POINT('Ctrl Pts',(201.51485943594,-4.91824986053202,130.805531888988));
#19833=CARTESIAN_POINT('Ctrl Pts',(201.506582193965,-4.9182148650919,130.952480167015));
#19834=CARTESIAN_POINT('Ctrl Pts',(201.49830495199,-4.91158982122124,131.099253060515));
#19835=CARTESIAN_POINT('Ctrl Pts',(201.490027710014,-4.89844708438231,131.245267891272));
#19836=CARTESIAN_POINT('Ctrl Pts',(201.481501455677,-4.88490896174189,131.395675428935));
#19837=CARTESIAN_POINT('Ctrl Pts',(201.472975201339,-4.86445493793769,131.545278220582));
#19838=CARTESIAN_POINT('Ctrl Pts',(201.464448947001,-4.83721994611014,131.693453557283));
#19839=CARTESIAN_POINT('Ctrl Pts',(201.456128501245,-4.81064235843921,131.838052205476));
#19840=CARTESIAN_POINT('Ctrl Pts',(201.447808055489,-4.77760755788874,131.981291262248));
#19841=CARTESIAN_POINT('Ctrl Pts',(201.439487609733,-4.73829111258486,132.122609605769));
#19842=CARTESIAN_POINT('Ctrl Pts',(201.430858451104,-4.69751591217013,132.269171273154));
#19843=CARTESIAN_POINT('Ctrl Pts',(201.422229292475,-4.6499841405859,132.413666610456));
#19844=CARTESIAN_POINT('Ctrl Pts',(201.413600133847,-4.59594544262833,132.555494122152));
#19845=CARTESIAN_POINT('Ctrl Pts',(201.404970975218,-4.54190674467076,132.697321633848));
#19846=CARTESIAN_POINT('Ctrl Pts',(201.396341816589,-4.48136133127772,132.836481025787));
#19847=CARTESIAN_POINT('Ctrl Pts',(201.38771265796,-4.41461067614117,132.972400202214));
#19848=CARTESIAN_POINT('Ctrl Pts',(201.379938323841,-4.3544724960429,133.094854909123));
#19849=CARTESIAN_POINT('Ctrl Pts',(201.372163989722,-4.28914013406402,133.21499946427));
#19850=CARTESIAN_POINT('Ctrl Pts',(201.364389655603,-4.21881414473507,133.332361858603));
#19851=CARTESIAN_POINT('Ctrl Pts',(201.356624902656,-4.14857482590277,133.449579614273));
#19852=CARTESIAN_POINT('Ctrl Pts',(201.348860149708,-4.07335432377154,133.564021699203));
#19853=CARTESIAN_POINT('Ctrl Pts',(201.341095396761,-3.9934004017413,133.675237886603));
#19854=CARTESIAN_POINT('Ctrl Pts',(201.333338355876,-3.91352589107348,133.786343612518));
#19855=CARTESIAN_POINT('Ctrl Pts',(201.325581314991,-3.8289275430417,133.89422950163));
#19856=CARTESIAN_POINT('Ctrl Pts',(201.317824274106,-3.73989781193985,133.998471983619));
#19857=CARTESIAN_POINT('Ctrl Pts',(201.310073082865,-3.65093521885079,134.102635855541));
#19858=CARTESIAN_POINT('Ctrl Pts',(201.302321891625,-3.55754814710466,134.203161493023));
#19859=CARTESIAN_POINT('Ctrl Pts',(201.294570700385,-3.46007071453197,134.299656558247));
#19860=CARTESIAN_POINT('Ctrl Pts',(201.286822803607,-3.36263471246837,134.396110610494));
#19861=CARTESIAN_POINT('Ctrl Pts',(201.27907490683,-3.26111208461592,134.488537223235));
#19862=CARTESIAN_POINT('Ctrl Pts',(201.271327010053,-3.15587521323921,134.576579420998));
#19863=CARTESIAN_POINT('Ctrl Pts',(201.263580733969,-3.05066035514734,134.664603202231));
#19864=CARTESIAN_POINT('Ctrl Pts',(201.255834457884,-2.94173309858087,134.748244141987));
#19865=CARTESIAN_POINT('Ctrl Pts',(201.2480881818,-2.82950014815832,134.827184498134));
#19866=CARTESIAN_POINT('Ctrl Pts',(201.240341848535,-2.71726636925778,134.906125437001));
#19867=CARTESIAN_POINT('Ctrl Pts',(201.232595515269,-2.60172716759431,134.980365498095));
#19868=CARTESIAN_POINT('Ctrl Pts',(201.224849182004,-2.48331923024386,135.049629591754));
#19869=CARTESIAN_POINT('Ctrl Pts',(201.217101114,-2.36488477625662,135.118909196626));
#19870=CARTESIAN_POINT('Ctrl Pts',(201.209353045997,-2.24358064561767,135.183210419302));
#19871=CARTESIAN_POINT('Ctrl Pts',(201.201604977994,-2.11986882164754,135.242303749413));
#19872=CARTESIAN_POINT('Ctrl Pts',(201.193848675252,-1.99602551527869,135.301459884618));
#19873=CARTESIAN_POINT('Ctrl Pts',(201.18609237251,-1.8697697571969,135.355396901697));
#19874=CARTESIAN_POINT('Ctrl Pts',(201.178336069768,-1.74158475661268,135.403932945298));
#19875=CARTESIAN_POINT('Ctrl Pts',(201.170575627254,-1.61333133983404,135.452494894046));
#19876=CARTESIAN_POINT('Ctrl Pts',(201.162815184739,-1.4831469997239,135.49565000241));
#19877=CARTESIAN_POINT('Ctrl Pts',(201.155054742225,-1.35152990844939,135.533266407394));
#19878=CARTESIAN_POINT('Ctrl Pts',(201.147281841959,-1.21970153373557,135.57094319757));
#19879=CARTESIAN_POINT('Ctrl Pts',(201.139508941694,-1.08643619206553,135.603063425218));
#19880=CARTESIAN_POINT('Ctrl Pts',(201.131736041428,-0.952242926124562,
135.629546258777));
#19881=CARTESIAN_POINT('Ctrl Pts',(201.124245705668,-0.822927923447469,
135.655066374622));
#19882=CARTESIAN_POINT('Ctrl Pts',(201.116755369908,-0.692751594327094,
135.675351800014));
#19883=CARTESIAN_POINT('Ctrl Pts',(201.109265034147,-0.562171798684125,
135.690375960488));
#19884=CARTESIAN_POINT('Ctrl Pts',(201.101490700028,-0.426641030368497,
135.705969766576));
#19885=CARTESIAN_POINT('Ctrl Pts',(201.093716365909,-0.290246275975597,
135.715944866885));
#19886=CARTESIAN_POINT('Ctrl Pts',(201.08594203179,-0.153493054712102,135.7202148612));
#19887=CARTESIAN_POINT('Ctrl Pts',(201.078177278843,-0.0169083695718419,
135.724479593129));
#19888=CARTESIAN_POINT('Ctrl Pts',(201.070412525896,0.12003351640835,135.723053196639));
#19889=CARTESIAN_POINT('Ctrl Pts',(201.062647772949,0.256819892510846,135.715900763519));
#19890=CARTESIAN_POINT('Ctrl Pts',(201.054890732064,0.39347041045627,135.708755434297));
#19891=CARTESIAN_POINT('Ctrl Pts',(201.047133691179,0.52996533799027,135.695895406474));
#19892=CARTESIAN_POINT('Ctrl Pts',(201.039376650294,0.665790234716704,135.677337780026));
#19893=CARTESIAN_POINT('Ctrl Pts',(201.031625459054,0.801512704831837,135.658794148028));
#19894=CARTESIAN_POINT('Ctrl Pts',(201.023874267814,0.936565764060569,135.634561522245));
#19895=CARTESIAN_POINT('Ctrl Pts',(201.016123076574,1.07043872863637,135.604708937296));
#19896=CARTESIAN_POINT('Ctrl Pts',(201.008375179797,1.20425479363109,135.574869040492));
#19897=CARTESIAN_POINT('Ctrl Pts',(201.00062728302,1.33689138076679,135.539414020244));
#19898=CARTESIAN_POINT('Ctrl Pts',(200.992879386243,1.46784687475884,135.498464218336));
#19899=CARTESIAN_POINT('Ctrl Pts',(200.985133110159,1.59877497568463,135.457522982243));
#19900=CARTESIAN_POINT('Ctrl Pts',(200.977386834075,1.72802231000401,135.411089367299));
#19901=CARTESIAN_POINT('Ctrl Pts',(200.969640557991,1.85510171848053,135.359333798232));
#19902=CARTESIAN_POINT('Ctrl Pts',(200.961894224726,1.98218206502826,135.307577847118));
#19903=CARTESIAN_POINT('Ctrl Pts',(200.954147891461,2.10709409171268,135.250500010957));
#19904=CARTESIAN_POINT('Ctrl Pts',(200.946401558195,2.22937031777955,135.188318994273));
#19905=CARTESIAN_POINT('Ctrl Pts',(200.938653490193,2.35167392675948,135.126124052582));
#19906=CARTESIAN_POINT('Ctrl Pts',(200.93090542219,2.47134021212813,135.058823833469));
#19907=CARTESIAN_POINT('Ctrl Pts',(200.923157354187,2.58792636704384,134.986682960626));
#19908=CARTESIAN_POINT('Ctrl Pts',(200.915401051445,2.70463643111238,134.914465415605));
#19909=CARTESIAN_POINT('Ctrl Pts',(200.907644748703,2.81825949236634,134.837397145802));
#19910=CARTESIAN_POINT('Ctrl Pts',(200.899888445961,2.92838136436711,134.755786391553));
#19911=CARTESIAN_POINT('Ctrl Pts',(200.892128003447,3.03856201172679,134.674132079186));
#19912=CARTESIAN_POINT('Ctrl Pts',(200.884367560933,3.14523744236723,134.587930697037));
#19913=CARTESIAN_POINT('Ctrl Pts',(200.876607118419,3.24802744199153,134.497530096289));
#19914=CARTESIAN_POINT('Ctrl Pts',(200.868834218154,3.35098244924848,134.406984376471));
#19915=CARTESIAN_POINT('Ctrl Pts',(200.861061317888,3.45003927881987,134.312226237882));
#19916=CARTESIAN_POINT('Ctrl Pts',(200.853288417623,3.54485477481942,134.213640261118));
#19917=CARTESIAN_POINT('Ctrl Pts',(200.84579808186,3.63622348872338,134.118638132923));
#19918=CARTESIAN_POINT('Ctrl Pts',(200.838307746098,3.723653677273,134.020081868339));
#19919=CARTESIAN_POINT('Ctrl Pts',(200.830817410335,3.80687549814816,133.918342313739));
#19920=CARTESIAN_POINT('Ctrl Pts',(200.823043076216,3.8932526996479,133.812745273014));
#19921=CARTESIAN_POINT('Ctrl Pts',(200.815268742097,3.97536973042481,133.703384288615));
#19922=CARTESIAN_POINT('Ctrl Pts',(200.807494407978,4.052880654051,133.59063796674));
#19923=CARTESIAN_POINT('Ctrl Pts',(200.799729655031,4.13029605239111,133.47803059463));
#19924=CARTESIAN_POINT('Ctrl Pts',(200.791964902084,4.20311641899065,133.362046505414));
#19925=CARTESIAN_POINT('Ctrl Pts',(200.784200149136,4.27103525191642,133.243098188398));
#19926=CARTESIAN_POINT('Ctrl Pts',(200.776443108251,4.33888662689985,133.124268012527));
#19927=CARTESIAN_POINT('Ctrl Pts',(200.768686067366,4.40184596368367,133.002479805092));
#19928=CARTESIAN_POINT('Ctrl Pts',(200.760929026481,4.45964958136172,132.878175622324));
#19929=CARTESIAN_POINT('Ctrl Pts',(200.753177835241,4.51740960888204,132.753965178307));
#19930=CARTESIAN_POINT('Ctrl Pts',(200.745426644001,4.57002149187464,132.627242888525));
#19931=CARTESIAN_POINT('Ctrl Pts',(200.737675452761,4.61726727407009,132.498475720592));
#19932=CARTESIAN_POINT('Ctrl Pts',(200.729927555984,4.66449297554781,132.369763282141));
#19933=CARTESIAN_POINT('Ctrl Pts',(200.722179659207,4.70635697805043,132.239008060438));
#19934=CARTESIAN_POINT('Ctrl Pts',(200.71443176243,4.74268939321458,132.106697126303));
#19935=CARTESIAN_POINT('Ctrl Pts',(200.706685486346,4.77901420842072,131.974413868764));
#19936=CARTESIAN_POINT('Ctrl Pts',(200.698939210262,4.80980963434076,131.840575922843));
#19937=CARTESIAN_POINT('Ctrl Pts',(200.691192934178,4.83495573265951,131.705685268135));
#19938=CARTESIAN_POINT('Ctrl Pts',(200.683446600912,4.86010201660105,131.570793617694));
#19939=CARTESIAN_POINT('Ctrl Pts',(200.675700267647,4.8795988180791,131.434849627302));
#19940=CARTESIAN_POINT('Ctrl Pts',(200.667953934382,4.89337745463654,131.298364816895));
#19941=CARTESIAN_POINT('Ctrl Pts',(200.660205866379,4.90715917682409,131.161849441661));
#19942=CARTESIAN_POINT('Ctrl Pts',(200.652457798376,4.91522014669572,131.024793394324));
#19943=CARTESIAN_POINT('Ctrl Pts',(200.644709730373,4.91754365174374,130.887712256391));
#19944=CARTESIAN_POINT('Ctrl Pts',(200.636953427631,4.91986962624059,130.750485426993));
#19945=CARTESIAN_POINT('Ctrl Pts',(200.629197124889,4.91644594817341,130.613233845261));
#19946=CARTESIAN_POINT('Ctrl Pts',(200.621440822147,4.90730807097843,130.476472589407));
#19947=CARTESIAN_POINT('Ctrl Pts',(200.613680379633,4.89816531662325,130.339638339953));
#19948=CARTESIAN_POINT('Ctrl Pts',(200.605919937119,4.88330232842366,130.203295326312));
#19949=CARTESIAN_POINT('Ctrl Pts',(200.598159494605,4.86280624831729,130.067951455601));
#19950=CARTESIAN_POINT('Ctrl Pts',(200.590386594339,4.84227726608359,129.932390318894));
#19951=CARTESIAN_POINT('Ctrl Pts',(200.582613694074,4.81609719637891,129.797831914236));
#19952=CARTESIAN_POINT('Ctrl Pts',(200.574840793809,4.78440411361137,129.664772823599));
#19953=CARTESIAN_POINT('Ctrl Pts',(200.567350458046,4.75386315423193,129.53655076606));
#19954=CARTESIAN_POINT('Ctrl Pts',(200.559860122284,4.71820313009367,129.409721203914));
#19955=CARTESIAN_POINT('Ctrl Pts',(200.552369786522,4.67759018838714,129.284711614669));
#19956=CARTESIAN_POINT('Ctrl Pts',(200.544595452403,4.63543739465235,129.154962248855));
#19957=CARTESIAN_POINT('Ctrl Pts',(200.536821118284,4.58781516216797,129.026762581828));
#19958=CARTESIAN_POINT('Ctrl Pts',(200.529046784165,4.53485503596222,128.900608305602));
#19959=CARTESIAN_POINT('Ctrl Pts',(200.521282031218,4.48196017837884,128.774609503247));
#19960=CARTESIAN_POINT('Ctrl Pts',(200.51351727827,4.42374066616417,128.650651433156));
#19961=CARTESIAN_POINT('Ctrl Pts',(200.505752525323,4.36037786647262,128.529214924632));
#19962=CARTESIAN_POINT('Ctrl Pts',(200.497995484438,4.29707799960699,128.407899028561));
#19963=CARTESIAN_POINT('Ctrl Pts',(200.490238443553,4.22864519086966,128.289100054462));
#19964=CARTESIAN_POINT('Ctrl Pts',(200.482481402668,4.15530882871568,128.173278786741));
#19965=CARTESIAN_POINT('Ctrl Pts',(200.474730211428,4.08202777008282,128.057544860739));
#19966=CARTESIAN_POINT('Ctrl Pts',(200.466979020188,4.00385072660107,127.944784500539));
#19967=CARTESIAN_POINT('Ctrl Pts',(200.459227828948,3.92105276066194,127.835433486327));
#19968=CARTESIAN_POINT('Ctrl Pts',(200.451479932171,3.83828998606706,127.726128949213));
#19969=CARTESIAN_POINT('Ctrl Pts',(200.443732035394,3.75091043080558,127.620231187053));
#19970=CARTESIAN_POINT('Ctrl Pts',(200.435984138616,3.65923205254183,127.518146405414));
#19971=CARTESIAN_POINT('Ctrl Pts',(200.428237862532,3.56757285141844,127.41608297771));
#19972=CARTESIAN_POINT('Ctrl Pts',(200.420491586448,3.47161687695752,127.317831234768));
#19973=CARTESIAN_POINT('Ctrl Pts',(200.412745310364,3.37172162921752,127.223763416321));
#19974=CARTESIAN_POINT('Ctrl Pts',(200.404998977099,3.27182564407353,127.129694903486));
#19975=CARTESIAN_POINT('Ctrl Pts',(200.397252643833,3.16799061225729,127.039810644801));
#19976=CARTESIAN_POINT('Ctrl Pts',(200.389506310568,3.06060976543159,126.954444913782));
#19977=CARTESIAN_POINT('Ctrl Pts',(200.381758242565,2.95320487140979,126.869060065699));
#19978=CARTESIAN_POINT('Ctrl Pts',(200.374010174562,2.84225288827149,126.788196002082));
#19979=CARTESIAN_POINT('Ctrl Pts',(200.366262106559,2.72817855582115,126.712145468034));
#19980=CARTESIAN_POINT('Ctrl Pts',(200.358505803817,2.61398298381271,126.636014106574));
#19981=CARTESIAN_POINT('Ctrl Pts',(200.350749501075,2.49665875931106,126.564706711413));
#19982=CARTESIAN_POINT('Ctrl Pts',(200.342993198333,2.37665839565136,126.498471866927));
#19983=CARTESIAN_POINT('Ctrl Pts',(200.335232755819,2.25659398418439,126.43220167091));
#19984=CARTESIAN_POINT('Ctrl Pts',(200.327472313305,2.13385093720195,126.371009594588));
#19985=CARTESIAN_POINT('Ctrl Pts',(200.319711870791,2.00890367369267,126.315096859184));
#19986=CARTESIAN_POINT('Ctrl Pts',(200.311938970525,1.8837558337437,126.259094367693));
#19987=CARTESIAN_POINT('Ctrl Pts',(200.30416607026,1.75639706985327,126.208388297305));
#19988=CARTESIAN_POINT('Ctrl Pts',(200.296393169994,1.62731980308813,126.163130896794));
#19989=CARTESIAN_POINT('Ctrl Pts',(200.288902834233,1.50293482010056,126.11951871679));
#19990=CARTESIAN_POINT('Ctrl Pts',(200.281412498471,1.37695440338238,126.08096602872));
#19991=CARTESIAN_POINT('Ctrl Pts',(200.273922162709,1.24982800848328,126.047564110282));
#19992=CARTESIAN_POINT('Ctrl Pts',(200.26614782859,1.11788157767805,126.012895747953));
#19993=CARTESIAN_POINT('Ctrl Pts',(200.258373494471,0.984282587110447,125.983666629395));
#19994=CARTESIAN_POINT('Ctrl Pts',(200.250599160352,0.849519179810192,125.960034015691));
#19995=CARTESIAN_POINT('Ctrl Pts',(200.242834407405,0.714921856365283,125.936430527071));
#19996=CARTESIAN_POINT('Ctrl Pts',(200.235069654458,0.579163352880725,125.918409886831));
#19997=CARTESIAN_POINT('Ctrl Pts',(200.227304901511,0.442746238043899,125.906079405631));
#19998=CARTESIAN_POINT('Ctrl Pts',(200.219547860626,0.306464614608663,125.893761171238));
#19999=CARTESIAN_POINT('Ctrl Pts',(200.211790819741,0.1695260684516,125.88712188402));
#20000=CARTESIAN_POINT('Ctrl Pts',(200.204033778856,0.0324422606050424,
125.886217618199));
#20001=CARTESIAN_POINT('Ctrl Pts',(200.196282587615,-0.104538171275545,
125.885314034291));
#20002=CARTESIAN_POINT('Ctrl Pts',(200.188531396375,-0.241663257432193,
125.890136866048));
#20003=CARTESIAN_POINT('Ctrl Pts',(200.180780205135,-0.378417685712695,
125.900690245524));
#20004=CARTESIAN_POINT('Ctrl Pts',(200.173032308358,-0.515113989713261,
125.911239139532));
#20005=CARTESIAN_POINT('Ctrl Pts',(200.165284411581,-0.651439560181567,
125.927513706947));
#20006=CARTESIAN_POINT('Ctrl Pts',(200.157536514804,-0.78688078098602,125.949466005011));
#20007=CARTESIAN_POINT('Ctrl Pts',(200.14979023872,-0.922293670406798,125.971413711128));
#20008=CARTESIAN_POINT('Ctrl Pts',(200.142043962636,-1.05682219242837,125.999036723063));
#20009=CARTESIAN_POINT('Ctrl Pts',(200.134297686552,-1.18995993370752,126.032235470562));
#20010=CARTESIAN_POINT('Ctrl Pts',(200.126551353286,-1.3230986577791,126.065434463126));
#20011=CARTESIAN_POINT('Ctrl Pts',(200.118805020021,-1.454846201273,126.104209178789));
#20012=CARTESIAN_POINT('Ctrl Pts',(200.111058686756,-1.58470877909421,126.148409463617));
#20013=CARTESIAN_POINT('Ctrl Pts',(200.103310618753,-1.71460043873933,126.192619646792));
#20014=CARTESIAN_POINT('Ctrl Pts',(200.09556255075,-1.84260592268838,126.242257690929));
#20015=CARTESIAN_POINT('Ctrl Pts',(200.087814482747,-1.96824935395539,126.297124486282));
#20016=CARTESIAN_POINT('Ctrl Pts',(200.080058180005,-2.09402632055645,126.352049594717));
#20017=CARTESIAN_POINT('Ctrl Pts',(200.072301877263,-2.21743586078181,126.41221439872));
#20018=CARTESIAN_POINT('Ctrl Pts',(200.064545574521,-2.33802423904589,126.477372551933));
#20019=CARTESIAN_POINT('Ctrl Pts',(200.056785132007,-2.45867697895829,126.542565482013));
#20020=CARTESIAN_POINT('Ctrl Pts',(200.049024689493,-2.57650522087711,126.612756871751));
#20021=CARTESIAN_POINT('Ctrl Pts',(200.041264246979,-2.69108323663666,126.687656344));
#20022=CARTESIAN_POINT('Ctrl Pts',(200.033491346713,-2.80584518319893,126.762676051532));
#20023=CARTESIAN_POINT('Ctrl Pts',(200.025718446448,-2.91734615908058,126.842418716971));
#20024=CARTESIAN_POINT('Ctrl Pts',(200.017945546182,-3.02519190746045,126.926552346708));
#20025=CARTESIAN_POINT('Ctrl Pts',(200.01045521042,-3.12911719124147,127.007627507086));
#20026=CARTESIAN_POINT('Ctrl Pts',(200.002964874658,-3.22964815206794,127.092779730022));
#20027=CARTESIAN_POINT('Ctrl Pts',(199.995474538896,-3.32646505372397,127.181680213659));
#20028=CARTESIAN_POINT('Ctrl Pts',(199.987817885007,-3.42543171291799,127.272554675822));
#20029=CARTESIAN_POINT('Ctrl Pts',(199.980161231117,-3.52085100355156,127.367652463917));
#20030=CARTESIAN_POINT('Ctrl Pts',(199.972504577228,-3.61233263415092,127.466661409616));
#20031=CARTESIAN_POINT('Ctrl Pts',(199.964856779005,-3.7037084573244,127.565555841815));
#20032=CARTESIAN_POINT('Ctrl Pts',(199.957208980783,-3.79115540274886,127.668352146295));
#20033=CARTESIAN_POINT('Ctrl Pts',(199.94956118256,-3.87431677020004,127.774698486792));
#20034=CARTESIAN_POINT('Ctrl Pts',(199.941920455469,-3.95740124690412,127.880946499786));
#20035=CARTESIAN_POINT('Ctrl Pts',(199.934279728377,-4.03620777736056,127.990737706671));
#20036=CARTESIAN_POINT('Ctrl Pts',(199.926639001285,-4.11041742727574,128.10368447333));
#20037=CARTESIAN_POINT('Ctrl Pts',(199.918999136713,-4.18461870007081,128.216618490047));
#20038=CARTESIAN_POINT('Ctrl Pts',(199.911359272141,-4.2542238720399,128.332707043142));
#20039=CARTESIAN_POINT('Ctrl Pts',(199.90371940757,-4.31895501961334,128.451530279217));
#20040=CARTESIAN_POINT('Ctrl Pts',(199.896087179009,-4.38362146868872,128.570234751988));
#20041=CARTESIAN_POINT('Ctrl Pts',(199.888454950448,-4.44342342148269,128.69166809915));
#20042=CARTESIAN_POINT('Ctrl Pts',(199.880822721887,-4.49812811338532,128.815384363793));
#20043=CARTESIAN_POINT('Ctrl Pts',(199.87317903931,-4.55291490299365,128.939286294805));
#20044=CARTESIAN_POINT('Ctrl Pts',(199.865535356733,-4.60258893508908,129.065477639417));
#20045=CARTESIAN_POINT('Ctrl Pts',(199.857891674155,-4.64696388063631,129.19348825932));
#20046=CARTESIAN_POINT('Ctrl Pts',(199.850247991578,-4.69133882618354,129.321498879223));
#20047=CARTESIAN_POINT('Ctrl Pts',(199.842604309,-4.73041455848543,129.451328387816));
#20048=CARTESIAN_POINT('Ctrl Pts',(199.834960626423,-4.76405452823405,129.582490119308));
#20049=CARTESIAN_POINT('Ctrl Pts',(201.584606355351,-4.76405452823405,129.582490119308));
#20050=CARTESIAN_POINT('Ctrl Pts',(201.576612163084,-4.79917136563237,129.719410135352));
#20051=CARTESIAN_POINT('Ctrl Pts',(201.568617970816,-4.82841256673479,129.857966876512));
#20052=CARTESIAN_POINT('Ctrl Pts',(201.560623778548,-4.85163618075089,129.997633010422));
#20053=CARTESIAN_POINT('Ctrl Pts',(201.55263857145,-4.87483369230245,130.137142164875));
#20054=CARTESIAN_POINT('Ctrl Pts',(201.544653364352,-4.89202704125614,130.277757877198));
#20055=CARTESIAN_POINT('Ctrl Pts',(201.536668157254,-4.90312503397178,130.418941412363));
#20056=CARTESIAN_POINT('Ctrl Pts',(201.5293985835,-4.91322842585438,130.547472095315));
#20057=CARTESIAN_POINT('Ctrl Pts',(201.522129009746,-4.9182805956174,130.676473036305));
#20058=CARTESIAN_POINT('Ctrl Pts',(201.514859435991,-4.91824986053224,130.805531888085));
#20059=CARTESIAN_POINT('',(201.860140564039,-4.91824790150174,130.799817284683));
#20060=CARTESIAN_POINT('Ctrl Pts',(201.930097584127,-4.76405452823404,129.582490119308));
#20061=CARTESIAN_POINT('Ctrl Pts',(201.928404692561,-4.77143981658942,129.611285246518));
#20062=CARTESIAN_POINT('Ctrl Pts',(201.926711800994,-4.77856158153426,129.640137793894));
#20063=CARTESIAN_POINT('Ctrl Pts',(201.925018909427,-4.78541909345683,129.669042528888));
#20064=CARTESIAN_POINT('Ctrl Pts',(201.914205851863,-4.82922028700719,129.853666617963));
#20065=CARTESIAN_POINT('Ctrl Pts',(201.903392794298,-4.86235268751459,130.040911499407));
#20066=CARTESIAN_POINT('Ctrl Pts',(201.892579736733,-4.88456555156559,130.22972818291));
#20067=CARTESIAN_POINT('Ctrl Pts',(201.882347687665,-4.90558487136082,130.408399345895));
#20068=CARTESIAN_POINT('Ctrl Pts',(201.872115638597,-4.91682686629452,130.58847825068));
#20069=CARTESIAN_POINT('Ctrl Pts',(201.861883589529,-4.91812325643309,130.769052020427));
#20070=CARTESIAN_POINT('Ctrl Pts',(201.861302581032,-4.91819686961459,130.779305577046));
#20071=CARTESIAN_POINT('Ctrl Pts',(201.860721572536,-4.91823842679033,130.789560721775));
#20072=CARTESIAN_POINT('Ctrl Pts',(201.860140564039,-4.91824790150174,130.799817284683));
#20073=CARTESIAN_POINT('Ctrl Pts',(201.860140564008,-4.91824790150225,130.799817285234));
#20074=CARTESIAN_POINT('Ctrl Pts',(201.852483585455,-4.91837276654937,130.934986190149));
#20075=CARTESIAN_POINT('Ctrl Pts',(201.844826606902,-4.91292114291673,131.07031288466));
#20076=CARTESIAN_POINT('Ctrl Pts',(201.83716962835,-4.90188083750575,131.205293676061));
#20077=CARTESIAN_POINT('Ctrl Pts',(201.829228030736,-4.89043015072319,131.345291865101));
#20078=CARTESIAN_POINT('Ctrl Pts',(201.821286433122,-4.8729672167622,131.484917501621));
#20079=CARTESIAN_POINT('Ctrl Pts',(201.813344835508,-4.84953772420023,131.62360839697));
#20080=CARTESIAN_POINT('Ctrl Pts',(201.80569610997,-4.82697226989009,131.757184617366));
#20081=CARTESIAN_POINT('Ctrl Pts',(201.798047384431,-4.79887259272399,131.889893384014));
#20082=CARTESIAN_POINT('Ctrl Pts',(201.790398658893,-4.76533224076631,132.021238465837));
#20083=CARTESIAN_POINT('Ctrl Pts',(201.782750978392,-4.73179647139039,132.152565602125));
#20084=CARTESIAN_POINT('Ctrl Pts',(201.775103297891,-4.69282160461944,132.282529034708));
#20085=CARTESIAN_POINT('Ctrl Pts',(201.767455617389,-4.64855188812975,132.410644654051));
#20086=CARTESIAN_POINT('Ctrl Pts',(201.759807225106,-4.60427805138161,132.538772197334));
#20087=CARTESIAN_POINT('Ctrl Pts',(201.752158832822,-4.5547085165048,132.665051205577));
#20088=CARTESIAN_POINT('Ctrl Pts',(201.744510440538,-4.50003661315956,132.789015132267));
#20089=CARTESIAN_POINT('Ctrl Pts',(201.736859579318,-4.44534706147838,132.913019075069));
#20090=CARTESIAN_POINT('Ctrl Pts',(201.729208718099,-4.38555202834284,133.034706082836));
#20091=CARTESIAN_POINT('Ctrl Pts',(201.72155785688,-4.32089170944105,133.153632397881));
#20092=CARTESIAN_POINT('Ctrl Pts',(201.713898683524,-4.25616114153522,133.272687918215));
#20093=CARTESIAN_POINT('Ctrl Pts',(201.706239510168,-4.18655493051007,133.388976406699));
#20094=CARTESIAN_POINT('Ctrl Pts',(201.698580336813,-4.11235781880762,133.502081179928));
#20095=CARTESIAN_POINT('Ctrl Pts',(201.690916213761,-4.03811275765906,133.615259046451));
#20096=CARTESIAN_POINT('Ctrl Pts',(201.68325209071,-3.95927112365503,133.725248776863));
#20097=CARTESIAN_POINT('Ctrl Pts',(201.675587967659,-3.87615836955861,133.831666244126));
#20098=CARTESIAN_POINT('Ctrl Pts',(201.667913108811,-3.79292919227884,133.938232779488));
#20099=CARTESIAN_POINT('Ctrl Pts',(201.660238249964,-3.70541721587963,134.041216762563));
#20100=CARTESIAN_POINT('Ctrl Pts',(201.652563391116,-3.61398532778852,134.140270255585));
#20101=CARTESIAN_POINT('Ctrl Pts',(201.650566022616,-3.59019033991468,134.166048752722));
#20102=CARTESIAN_POINT('Ctrl Pts',(201.648568654115,-3.56613003589684,134.191561251679));
#20103=CARTESIAN_POINT('Ctrl Pts',(201.646571285615,-3.54181117222063,134.216802072424));
#20104=CARTESIAN_POINT('Ctrl Pts',(201.638796951494,-3.44715514275093,134.315046624639));
#20105=CARTESIAN_POINT('Ctrl Pts',(201.631022617374,-3.34825835130227,134.409505379128));
#20106=CARTESIAN_POINT('Ctrl Pts',(201.623248283254,-3.24545589596689,134.499790104085));
#20107=CARTESIAN_POINT('Ctrl Pts',(201.615483530306,-3.14278013546986,134.589963561187));
#20108=CARTESIAN_POINT('Ctrl Pts',(201.607718777357,-3.03620857922076,134.675972968507));
#20109=CARTESIAN_POINT('Ctrl Pts',(201.599954024409,-2.92611462881938,134.757465250827));
#20110=CARTESIAN_POINT('Ctrl Pts',(201.592196983523,-2.8161300252812,134.838876593864));
#20111=CARTESIAN_POINT('Ctrl Pts',(201.584439942637,-2.70263030195642,134.915779509083));
#20112=CARTESIAN_POINT('Ctrl Pts',(201.576682901751,-2.58602327795652,134.987859950465));
#20113=CARTESIAN_POINT('Ctrl Pts',(201.568931710509,-2.46950418822028,135.059886035426));
#20114=CARTESIAN_POINT('Ctrl Pts',(201.561180519268,-2.3498827930975,135.127096680372));
#20115=CARTESIAN_POINT('Ctrl Pts',(201.553429328027,-2.22759704920044,135.189220301626));
#20116=CARTESIAN_POINT('Ctrl Pts',(201.545681431248,-2.10536328000659,135.251317518684));
#20117=CARTESIAN_POINT('Ctrl Pts',(201.53793353447,-1.98046776216892,135.308331835635));
#20118=CARTESIAN_POINT('Ctrl Pts',(201.530185637692,-1.85337409203519,135.360037025902));
#20119=CARTESIAN_POINT('Ctrl Pts',(201.522439361606,-1.72630700715721,135.411731400558));
#20120=CARTESIAN_POINT('Ctrl Pts',(201.514693085521,-1.59704304647646,135.458118710247));
#20121=CARTESIAN_POINT('Ctrl Pts',(201.506946809436,-1.46606651029953,135.499020567965));
#20122=CARTESIAN_POINT('Ctrl Pts',(201.499200476169,-1.33508900728361,135.539922727611));
#20123=CARTESIAN_POINT('Ctrl Pts',(201.491454142903,-1.20239927673706,135.575339237944));
#20124=CARTESIAN_POINT('Ctrl Pts',(201.483707809636,-1.0684971462986,135.605141482264));
#20125=CARTESIAN_POINT('Ctrl Pts',(201.475959741632,-0.934565029406161,
135.63495040059));
#20126=CARTESIAN_POINT('Ctrl Pts',(201.468211673628,-0.799420353905459,
135.659142466148));
#20127=CARTESIAN_POINT('Ctrl Pts',(201.460463605623,-0.663573118682993,
135.677640188724));
#20128=CARTESIAN_POINT('Ctrl Pts',(201.45270730288,-0.527581503402445,135.696157570899));
#20129=CARTESIAN_POINT('Ctrl Pts',(201.444951000137,-0.390886224816852,
135.708968467706));
#20130=CARTESIAN_POINT('Ctrl Pts',(201.437194697394,-0.254002943294543,
135.716047249192));
#20131=CARTESIAN_POINT('Ctrl Pts',(201.429434254879,-0.117046603043397,
135.723129808838));
#20132=CARTESIAN_POINT('Ctrl Pts',(201.421673812363,0.0200975493309183,
135.724474153213));
#20133=CARTESIAN_POINT('Ctrl Pts',(201.413913369848,0.156914869496959,135.720106826051));
#20134=CARTESIAN_POINT('Ctrl Pts',(201.406140469581,0.293951820971461,135.715732488067));
#20135=CARTESIAN_POINT('Ctrl Pts',(201.398367569315,0.430660501673616,135.705628185033));
#20136=CARTESIAN_POINT('Ctrl Pts',(201.390594669048,0.566531497579824,135.689872374255));
#20137=CARTESIAN_POINT('Ctrl Pts',(201.383104333299,0.697463240297336,135.674689326915));
#20138=CARTESIAN_POINT('Ctrl Pts',(201.37561399755,0.827616840453072,135.654258578995));
#20139=CARTESIAN_POINT('Ctrl Pts',(201.368123661801,0.956548189162586,135.628694625935));
#20140=CARTESIAN_POINT('Ctrl Pts',(201.360349327683,1.09036800937337,135.60216140778));
#20141=CARTESIAN_POINT('Ctrl Pts',(201.352574993564,1.22329496617451,135.570014000326));
#20142=CARTESIAN_POINT('Ctrl Pts',(201.344800659445,1.35482130044931,135.532324482313));
#20143=CARTESIAN_POINT('Ctrl Pts',(201.337035906498,1.48618554027203,135.494681413262));
#20144=CARTESIAN_POINT('Ctrl Pts',(201.329271153552,1.61615221984584,135.451509930292));
#20145=CARTESIAN_POINT('Ctrl Pts',(201.321506400605,1.74422245430599,135.402933340966));
#20146=CARTESIAN_POINT('Ctrl Pts',(201.31374935972,1.87216548760419,135.354404998592));
#20147=CARTESIAN_POINT('Ctrl Pts',(201.305992318836,1.99821546100229,135.300482371031));
#20148=CARTESIAN_POINT('Ctrl Pts',(201.298235277951,2.12188772249806,135.241338818505));
#20149=CARTESIAN_POINT('Ctrl Pts',(201.290484086711,2.24546672177877,135.182239866593));
#20150=CARTESIAN_POINT('Ctrl Pts',(201.282732895472,2.36667122683608,135.117927994348));
#20151=CARTESIAN_POINT('Ctrl Pts',(201.274981704232,2.48503602038379,135.048624869459));
#20152=CARTESIAN_POINT('Ctrl Pts',(201.267233807455,2.60335050573666,134.979351200247));
#20153=CARTESIAN_POINT('Ctrl Pts',(201.259485910679,2.71882734343585,134.905090694853));
#20154=CARTESIAN_POINT('Ctrl Pts',(201.251738013902,2.83102561750346,134.826111109024));
#20155=CARTESIAN_POINT('Ctrl Pts',(201.243991737818,2.94320042211094,134.747148044021));
#20156=CARTESIAN_POINT('Ctrl Pts',(201.236245461735,3.0520977076928,134.663468086941));
#20157=CARTESIAN_POINT('Ctrl Pts',(201.228499185651,3.15730561606483,134.575382270814));
#20158=CARTESIAN_POINT('Ctrl Pts',(201.220752852386,3.26251430105758,134.487295804458));
#20159=CARTESIAN_POINT('Ctrl Pts',(201.213006519121,3.36403325472788,134.394803665141));
#20160=CARTESIAN_POINT('Ctrl Pts',(201.205260185856,3.46148409915498,134.298256851543));
#20161=CARTESIAN_POINT('Ctrl Pts',(201.197512117854,3.55895676702291,134.201688416955));
#20162=CARTESIAN_POINT('Ctrl Pts',(201.189764049851,3.6523592351274,134.101063776349));
#20163=CARTESIAN_POINT('Ctrl Pts',(201.182015981848,3.74135064190172,133.996770120879));
#20164=CARTESIAN_POINT('Ctrl Pts',(201.174259679107,3.8304366298024,133.89236562087));
#20165=CARTESIAN_POINT('Ctrl Pts',(201.166503376366,3.91510193715322,133.784284614265));
#20166=CARTESIAN_POINT('Ctrl Pts',(201.158747073624,3.99504627372427,133.672947087119));
#20167=CARTESIAN_POINT('Ctrl Pts',(201.15098663111,4.07503327899471,133.561550135783));
#20168=CARTESIAN_POINT('Ctrl Pts',(201.143226188597,4.1502940782862,133.446893527272));
#20169=CARTESIAN_POINT('Ctrl Pts',(201.135465746083,4.22057282576062,133.329424593974));
#20170=CARTESIAN_POINT('Ctrl Pts',(201.127692845818,4.2909643909197,133.211767089115));
#20171=CARTESIAN_POINT('Ctrl Pts',(201.119919945553,4.35635773583158,133.091288581682));
#20172=CARTESIAN_POINT('Ctrl Pts',(201.112147045288,4.41654351812895,132.968460064212));
#20173=CARTESIAN_POINT('Ctrl Pts',(201.104656709521,4.47454139567703,132.850096672665));
#20174=CARTESIAN_POINT('Ctrl Pts',(201.097166373755,4.5277036290204,132.729551444137));
#20175=CARTESIAN_POINT('Ctrl Pts',(201.089676037989,4.57588649471474,132.607259907595));
#20176=CARTESIAN_POINT('Ctrl Pts',(201.08190170387,4.62589622837748,132.48033165035));
#20177=CARTESIAN_POINT('Ctrl Pts',(201.074127369751,4.67069997109745,132.351119977928));
#20178=CARTESIAN_POINT('Ctrl Pts',(201.066353035632,4.71008390855603,132.220091042775));
#20179=CARTESIAN_POINT('Ctrl Pts',(201.058588282685,4.74941930883149,132.089223589074));
#20180=CARTESIAN_POINT('Ctrl Pts',(201.050823529738,4.78334808245175,131.956543699629));
#20181=CARTESIAN_POINT('Ctrl Pts',(201.043058776791,4.81170431210567,131.822537751155));
#20182=CARTESIAN_POINT('Ctrl Pts',(201.035301735906,4.84003237795253,131.688664899279));
#20183=CARTESIAN_POINT('Ctrl Pts',(201.027544695021,4.86279883378002,131.553468989404));
#20184=CARTESIAN_POINT('Ctrl Pts',(201.019787654136,4.87988756620843,131.417451478421));
#20185=CARTESIAN_POINT('Ctrl Pts',(201.012036462896,4.89696341189084,131.281536539302));
#20186=CARTESIAN_POINT('Ctrl Pts',(201.004285271656,4.90837000793079,131.144801618648));
#20187=CARTESIAN_POINT('Ctrl Pts',(200.996534080416,4.91404238832683,131.007757933741));
#20188=CARTESIAN_POINT('Ctrl Pts',(200.988786183639,4.91971235780988,130.870772496056));
#20189=CARTESIAN_POINT('Ctrl Pts',(200.981038286862,4.91965294290856,130.733478944942));
#20190=CARTESIAN_POINT('Ctrl Pts',(200.973290390085,4.91385108825839,130.596392964019));
#20191=CARTESIAN_POINT('Ctrl Pts',(200.965544114001,4.90805044723114,130.459335658529));
#20192=CARTESIAN_POINT('Ctrl Pts',(200.957797837917,4.89650977221841,130.322486227234));
#20193=CARTESIAN_POINT('Ctrl Pts',(200.950051561833,4.87926812470907,130.186359299041));
#20194=CARTESIAN_POINT('Ctrl Pts',(200.942305228568,4.86202634992579,130.050231365991));
#20195=CARTESIAN_POINT('Ctrl Pts',(200.934558895303,4.83908356779839,129.91482633455));
#20196=CARTESIAN_POINT('Ctrl Pts',(200.926812562038,4.81053056094829,129.780652268141));
#20197=CARTESIAN_POINT('Ctrl Pts',(200.919064494035,4.78197115985042,129.646448154381));
#20198=CARTESIAN_POINT('Ctrl Pts',(200.911316426032,4.74779911535903,129.513475936524));
#20199=CARTESIAN_POINT('Ctrl Pts',(200.903568358029,4.70815593835484,129.382231677338));
#20200=CARTESIAN_POINT('Ctrl Pts',(200.895812055287,4.66847062811032,129.250847930191));
#20201=CARTESIAN_POINT('Ctrl Pts',(200.888055752546,4.62330268292331,129.121196185172));
#20202=CARTESIAN_POINT('Ctrl Pts',(200.880299449804,4.57284313475343,128.993756097678));
#20203=CARTESIAN_POINT('Ctrl Pts',(200.87253900729,4.52235665480324,128.866247991572));
#20204=CARTESIAN_POINT('Ctrl Pts',(200.864778564776,4.46657310317764,128.740954252085));
#20205=CARTESIAN_POINT('Ctrl Pts',(200.857018122262,4.40573054235811,128.618331923648));
#20206=CARTESIAN_POINT('Ctrl Pts',(200.849245221996,4.34479031165874,128.495512750964));
#20207=CARTESIAN_POINT('Ctrl Pts',(200.841472321731,4.27877503146672,128.375373901733));
#20208=CARTESIAN_POINT('Ctrl Pts',(200.833699421466,4.20796780647951,128.258346084589));
#20209=CARTESIAN_POINT('Ctrl Pts',(200.826209085702,4.13973460246116,128.145572523353));
#20210=CARTESIAN_POINT('Ctrl Pts',(200.818718749939,4.06705197339164,128.035687990354));
#20211=CARTESIAN_POINT('Ctrl Pts',(200.811228414176,3.99020865609362,127.929048818241));
#20212=CARTESIAN_POINT('Ctrl Pts',(200.803454080057,3.91045180107535,127.818366389521));
#20213=CARTESIAN_POINT('Ctrl Pts',(200.795679745938,3.82595987893068,127.710829666744));
#20214=CARTESIAN_POINT('Ctrl Pts',(200.787905411818,3.73700950505258,127.606870504736));
#20215=CARTESIAN_POINT('Ctrl Pts',(200.780140658871,3.64816875456051,127.503039463103));
#20216=CARTESIAN_POINT('Ctrl Pts',(200.772375905924,3.55488073677464,127.402777503809));
#20217=CARTESIAN_POINT('Ctrl Pts',(200.764611152976,3.45746497184096,127.306487116281));
#20218=CARTESIAN_POINT('Ctrl Pts',(200.756854112091,3.36014596161846,127.210292365723));
#20219=CARTESIAN_POINT('Ctrl Pts',(200.749097071206,3.25870763916541,127.118061610023));
#20220=CARTESIAN_POINT('Ctrl Pts',(200.741340030321,3.15350913224816,127.030163588352));
#20221=CARTESIAN_POINT('Ctrl Pts',(200.733588839081,3.04838995634344,126.942331851264));
#20222=CARTESIAN_POINT('Ctrl Pts',(200.72583764784,2.93951653884054,126.858826594413));
#20223=CARTESIAN_POINT('Ctrl Pts',(200.7180864566,2.82728386560443,126.779978800964));
#20224=CARTESIAN_POINT('Ctrl Pts',(200.710338559823,2.71509889424786,126.701164519931));
#20225=CARTESIAN_POINT('Ctrl Pts',(200.702590663046,2.59955782612968,126.627003989411));
#20226=CARTESIAN_POINT('Ctrl Pts',(200.694842766268,2.48108746374105,126.557786932845));
#20227=CARTESIAN_POINT('Ctrl Pts',(200.687096490184,2.36264188279868,126.488584354995));
#20228=CARTESIAN_POINT('Ctrl Pts',(200.6793502141,2.24126856372764,126.424323391385));
#20229=CARTESIAN_POINT('Ctrl Pts',(200.671603938015,2.11742159208994,126.36524934797));
#20230=CARTESIAN_POINT('Ctrl Pts',(200.66385760475,1.99357370624226,126.306174868485));
#20231=CARTESIAN_POINT('Ctrl Pts',(200.656111271484,1.86725248426869,126.252287553918));
#20232=CARTESIAN_POINT('Ctrl Pts',(200.648364938219,1.7389344445388,126.203785646968));
#20233=CARTESIAN_POINT('Ctrl Pts',(200.640616870216,1.61058766887319,126.155272878351));
#20234=CARTESIAN_POINT('Ctrl Pts',(200.632868802213,1.48024355127012,126.112148055408));
#20235=CARTESIAN_POINT('Ctrl Pts',(200.625120734209,1.34839593347158,126.074560255067));
#20236=CARTESIAN_POINT('Ctrl Pts',(200.617364431467,1.21640818645573,126.036932505965));
#20237=CARTESIAN_POINT('Ctrl Pts',(200.609608128725,1.08291412377568,126.004853642373));
#20238=CARTESIAN_POINT('Ctrl Pts',(200.601851825983,0.948420550542189,125.978422209152));
#20239=CARTESIAN_POINT('Ctrl Pts',(200.594091383469,0.813855194038882,125.951976668679));
#20240=CARTESIAN_POINT('Ctrl Pts',(200.586330940955,0.678289650257551,125.931184623874));
#20241=CARTESIAN_POINT('Ctrl Pts',(200.57857049844,0.54223712220886,125.916092829709));
#20242=CARTESIAN_POINT('Ctrl Pts',(200.570797598175,0.405966190564276,125.900976808856));
#20243=CARTESIAN_POINT('Ctrl Pts',(200.563024697909,0.269207102735885,125.891579351172));
#20244=CARTESIAN_POINT('Ctrl Pts',(200.555251797643,0.132475251099434,125.887895081193));
#20245=CARTESIAN_POINT('Ctrl Pts',(200.547761461883,0.000713946712914748,
125.884344743708));
#20246=CARTESIAN_POINT('Ctrl Pts',(200.540271126123,-0.131021759319523,
125.88609942386));
#20247=CARTESIAN_POINT('Ctrl Pts',(200.532780790363,-0.262276004943429,
125.893108805682));
#20248=CARTESIAN_POINT('Ctrl Pts',(200.525006456244,-0.398506795217166,
125.900383950348));
#20249=CARTESIAN_POINT('Ctrl Pts',(200.517232122125,-0.534650433432306,
125.913343171992));
#20250=CARTESIAN_POINT('Ctrl Pts',(200.509457788006,-0.670194070517084,
125.931987174331));
#20251=CARTESIAN_POINT('Ctrl Pts',(200.501693035059,-0.805570662182922,
125.950608199603));
#20252=CARTESIAN_POINT('Ctrl Pts',(200.493928282112,-0.940348340398937,
125.974900012985));
#20253=CARTESIAN_POINT('Ctrl Pts',(200.486163529165,-1.07401577096679,126.004811348498));
#20254=CARTESIAN_POINT('Ctrl Pts',(200.47840648828,-1.20755044115865,126.03469297565));
#20255=CARTESIAN_POINT('Ctrl Pts',(200.470649447395,-1.33997667909172,126.070182932893));
#20256=CARTESIAN_POINT('Ctrl Pts',(200.46289240651,-1.47079013672649,126.111178388395));
#20257=CARTESIAN_POINT('Ctrl Pts',(200.45514121527,-1.60150494691511,126.152142928905));
#20258=CARTESIAN_POINT('Ctrl Pts',(200.44739002403,-1.73060902603362,126.198604587446));
#20259=CARTESIAN_POINT('Ctrl Pts',(200.43963883279,-1.85761040906449,126.250409955708));
#20260=CARTESIAN_POINT('Ctrl Pts',(200.431890936013,-1.9845578131194,126.302193305306));
#20261=CARTESIAN_POINT('Ctrl Pts',(200.424143039236,-2.10940393734354,126.359315699986));
#20262=CARTESIAN_POINT('Ctrl Pts',(200.416395142459,-2.23167433202904,126.421574661321));
#20263=CARTESIAN_POINT('Ctrl Pts',(200.408648866375,-2.35391915038416,126.483820599422));
#20264=CARTESIAN_POINT('Ctrl Pts',(200.400902590291,-2.47358896269875,126.551200789732));
#20265=CARTESIAN_POINT('Ctrl Pts',(200.393156314207,-2.59023194178586,126.623465791066));
#20266=CARTESIAN_POINT('Ctrl Pts',(200.385409980941,-2.70687578190523,126.695731325845));
#20267=CARTESIAN_POINT('Ctrl Pts',(200.377663647676,-2.82049241186166,126.772881537696));
#20268=CARTESIAN_POINT('Ctrl Pts',(200.369917314411,-2.93065747463995,126.854622673241));
#20269=CARTESIAN_POINT('Ctrl Pts',(200.362169246408,-3.04084720811968,126.936382114147));
#20270=CARTESIAN_POINT('Ctrl Pts',(200.354421178405,-3.14758352241582,127.022734291636));
#20271=CARTESIAN_POINT('Ctrl Pts',(200.346673110402,-3.25047406136048,127.113344302386));
#20272=CARTESIAN_POINT('Ctrl Pts',(200.33891680766,-3.3534739535945,127.204050614535));
#20273=CARTESIAN_POINT('Ctrl Pts',(200.331160504918,-3.45261961170661,127.29902354087));
#20274=CARTESIAN_POINT('Ctrl Pts',(200.323404202176,-3.54755418657293,127.397889957803));
#20275=CARTESIAN_POINT('Ctrl Pts',(200.315643759662,-3.64253943088031,127.496809142719));
#20276=CARTESIAN_POINT('Ctrl Pts',(200.307883317148,-3.73330885482172,127.599625666022));
#20277=CARTESIAN_POINT('Ctrl Pts',(200.300122874634,-3.8195457233528,127.705933027688));
#20278=CARTESIAN_POINT('Ctrl Pts',(200.292349974369,-3.90592102696098,127.812411043368));
#20279=CARTESIAN_POINT('Ctrl Pts',(200.284577074103,-3.98774900175901,127.922390781748));
#20280=CARTESIAN_POINT('Ctrl Pts',(200.276804173838,-4.06475558810789,128.035435723054));
#20281=CARTESIAN_POINT('Ctrl Pts',(200.269313838075,-4.13896279108229,128.144371196012));
#20282=CARTESIAN_POINT('Ctrl Pts',(200.261823502312,-4.20869289593499,128.256152623966));
#20283=CARTESIAN_POINT('Ctrl Pts',(200.25433316655,-4.27374183033709,128.37036928025));
#20284=CARTESIAN_POINT('Ctrl Pts',(200.246220788594,-4.34419281654029,128.494071169452));
#20285=CARTESIAN_POINT('Ctrl Pts',(200.238108410639,-4.40935986504164,128.620992964794));
#20286=CARTESIAN_POINT('Ctrl Pts',(200.229996032683,-4.46895007272139,128.750664362025));
#20287=CARTESIAN_POINT('Ctrl Pts',(200.221641782561,-4.53031697432501,128.88420193782));
#20288=CARTESIAN_POINT('Ctrl Pts',(200.213287532439,-4.58576906133034,129.02065536604));
#20289=CARTESIAN_POINT('Ctrl Pts',(200.204933282317,-4.6350349423211,129.159479422475));
#20290=CARTESIAN_POINT('Ctrl Pts',(200.196579032196,-4.68430082331187,129.298303478911));
#20291=CARTESIAN_POINT('Ctrl Pts',(200.188224782074,-4.7273802889641,129.439497817004));
#20292=CARTESIAN_POINT('Ctrl Pts',(200.179870531952,-4.76405452823405,129.582490119308));
#20293=CARTESIAN_POINT('Origin',(213.235140564004,0.,130.804360617566));
#20294=CARTESIAN_POINT('',(198.084936573762,-4.76405452823404,129.582490119308));
#20295=CARTESIAN_POINT('',(198.430216174721,-4.76405452823404,129.582490119308));
#20296=CARTESIAN_POINT('',(213.235140564004,-4.76405452823405,129.582490119308));
#20297=CARTESIAN_POINT('',(199.76485943604,-4.91824827604694,130.808478585671));
#20298=CARTESIAN_POINT('Ctrl Pts',(199.764859435991,-4.91824827604621,130.808478586542));
#20299=CARTESIAN_POINT('Ctrl Pts',(199.752723897668,-4.91806930075772,131.022235637443));
#20300=CARTESIAN_POINT('Ctrl Pts',(199.740588359346,-4.90395198746022,131.235429274479));
#20301=CARTESIAN_POINT('Ctrl Pts',(199.728452821023,-4.87613221702235,131.446635998237));
#20302=CARTESIAN_POINT('Ctrl Pts',(199.72464418571,-4.86740121908247,131.512921429102));
#20303=CARTESIAN_POINT('Ctrl Pts',(199.720835550396,-4.85732086664738,131.57901143828));
#20304=CARTESIAN_POINT('Ctrl Pts',(199.717026915083,-4.84589923841166,131.64486263045));
#20305=CARTESIAN_POINT('Ctrl Pts',(199.709252580964,-4.82258496786947,131.779280637941));
#20306=CARTESIAN_POINT('Ctrl Pts',(199.701478246845,-4.79363669851475,131.912940764209));
#20307=CARTESIAN_POINT('Ctrl Pts',(199.693703912726,-4.75911430351347,132.045333666666));
#20308=CARTESIAN_POINT('Ctrl Pts',(199.685939159779,-4.7246344542787,132.177563406704));
#20309=CARTESIAN_POINT('Ctrl Pts',(199.678174406832,-4.68459424557846,132.308528655646));
#20310=CARTESIAN_POINT('Ctrl Pts',(199.670409653885,-4.63910497760412,132.437727713252));
#20311=CARTESIAN_POINT('Ctrl Pts',(199.662652613,-4.59366089021201,132.566798448532));
#20312=CARTESIAN_POINT('Ctrl Pts',(199.654895572115,-4.54277864283484,132.694106117038));
#20313=CARTESIAN_POINT('Ctrl Pts',(199.64713853123,-4.48661991546082,132.819162046166));
#20314=CARTESIAN_POINT('Ctrl Pts',(199.63938733999,-4.43050353782002,132.944123669646));
#20315=CARTESIAN_POINT('Ctrl Pts',(199.631636148749,-4.36911875972351,133.066836578412));
#20316=CARTESIAN_POINT('Ctrl Pts',(199.623884957509,-4.30267602109411,133.186830369735));
#20317=CARTESIAN_POINT('Ctrl Pts',(199.616137060732,-4.23626152240097,133.306773160497));
#20318=CARTESIAN_POINT('Ctrl Pts',(199.608389163955,-4.16479352789244,133.423998791095));
#20319=CARTESIAN_POINT('Ctrl Pts',(199.600641267178,-4.08852913543883,133.538060047124));
#20320=CARTESIAN_POINT('Ctrl Pts',(199.592894991094,-4.01228069585204,133.652097443998));
#20321=CARTESIAN_POINT('Ctrl Pts',(199.58514871501,-3.93123807111655,133.762971458094));
#20322=CARTESIAN_POINT('Ctrl Pts',(199.577402438926,-3.84570232123248,133.870262885899));
#20323=CARTESIAN_POINT('Ctrl Pts',(199.56965610566,-3.76016593994299,133.977555105704));
#20324=CARTESIAN_POINT('Ctrl Pts',(199.561909772395,-3.67013661103911,134.081264380741));
#20325=CARTESIAN_POINT('Ctrl Pts',(199.554163439129,-3.57595615209479,134.181004019051));
#20326=CARTESIAN_POINT('Ctrl Pts',(199.546415371126,-3.48175460208978,134.280765993363));
#20327=CARTESIAN_POINT('Ctrl Pts',(199.538667303124,-3.38340034058184,134.376556277787));
#20328=CARTESIAN_POINT('Ctrl Pts',(199.530919235121,-3.28127226748557,134.468024817398));
#20329=CARTESIAN_POINT('Ctrl Pts',(199.523162932379,-3.17903565145775,134.559590570861));
#20330=CARTESIAN_POINT('Ctrl Pts',(199.515406629637,-3.07301750343207,134.646825142842));
#20331=CARTESIAN_POINT('Ctrl Pts',(199.507650326895,-2.96363048238186,134.729418251079));
#20332=CARTESIAN_POINT('Ctrl Pts',(199.499889884381,-2.85418507818486,134.812055441745));
#20333=CARTESIAN_POINT('Ctrl Pts',(199.492129441867,-2.7413675396017,134.890046010246));
#20334=CARTESIAN_POINT('Ctrl Pts',(199.484368999352,-2.62561893060417,134.963123449678));
#20335=CARTESIAN_POINT('Ctrl Pts',(199.476596099087,-2.50968451166382,135.036318199503));
#20336=CARTESIAN_POINT('Ctrl Pts',(199.468823198821,-2.3908099590241,135.104583864727));
#20337=CARTESIAN_POINT('Ctrl Pts',(199.461050298556,-2.26946110594807,135.167699860748));
#20338=CARTESIAN_POINT('Ctrl Pts',(199.453559962794,-2.15252358934225,135.228521431332));
#20339=CARTESIAN_POINT('Ctrl Pts',(199.446069627032,-2.03328882194573,135.284561108335));
#20340=CARTESIAN_POINT('Ctrl Pts',(199.43857929127,-1.91218875833745,135.335664758207));
#20341=CARTESIAN_POINT('Ctrl Pts',(199.430804957151,-1.78649714900839,135.388706018497));
#20342=CARTESIAN_POINT('Ctrl Pts',(199.423030623032,-1.65839785264128,135.436597582708));
#20343=CARTESIAN_POINT('Ctrl Pts',(199.415256288913,-1.52835175648752,135.479114511724));
#20344=CARTESIAN_POINT('Ctrl Pts',(199.407491535966,-1.39846593052474,135.521579042424));
#20345=CARTESIAN_POINT('Ctrl Pts',(199.399726783019,-1.26663844662274,135.558681996903));
#20346=CARTESIAN_POINT('Ctrl Pts',(199.391962030072,-1.13335155987423,135.590245833932));
#20347=CARTESIAN_POINT('Ctrl Pts',(199.384204989187,-1.00019705554075,135.621778321313));
#20348=CARTESIAN_POINT('Ctrl Pts',(199.376447948302,-0.865586410911478,
135.647782550024));
#20349=CARTESIAN_POINT('Ctrl Pts',(199.368690907417,-0.730018152069129,
135.668130406541));
#20350=CARTESIAN_POINT('Ctrl Pts',(199.360939716176,-0.594552126305398,
135.688462918582));
#20351=CARTESIAN_POINT('Ctrl Pts',(199.353188524936,-0.458130308783093,
135.703147490879));
#20352=CARTESIAN_POINT('Ctrl Pts',(199.345437333696,-0.321262210558749,
135.712106908336));
#20353=CARTESIAN_POINT('Ctrl Pts',(199.337689436919,-0.184452284927075,
135.721062517801));
#20354=CARTESIAN_POINT('Ctrl Pts',(199.329941540142,-0.0471968451682756,
135.724297786676));
#20355=CARTESIAN_POINT('Ctrl Pts',(199.322193643365,0.0899888868944208,
135.72178728837));
#20356=CARTESIAN_POINT('Ctrl Pts',(199.314447367281,0.227145922659364,135.719277315206));
#20357=CARTESIAN_POINT('Ctrl Pts',(199.306701091197,0.3642328890792,135.711023972638));
#20358=CARTESIAN_POINT('Ctrl Pts',(199.298954815113,0.500734368080969,135.697053961229));
#20359=CARTESIAN_POINT('Ctrl Pts',(199.291208481847,0.637236854705554,135.683083846697));
#20360=CARTESIAN_POINT('Ctrl Pts',(199.283462148582,0.773153456354327,135.663397018924));
#20361=CARTESIAN_POINT('Ctrl Pts',(199.275715815317,0.907974077383442,135.638072042269));
#20362=CARTESIAN_POINT('Ctrl Pts',(199.267967747314,1.04282489055591,135.61274139426));
#20363=CARTESIAN_POINT('Ctrl Pts',(199.260219679311,1.17657885054553,135.581770157055));
#20364=CARTESIAN_POINT('Ctrl Pts',(199.252471611308,1.30873664156906,135.545287896645));
#20365=CARTESIAN_POINT('Ctrl Pts',(199.244715308566,1.4410348914656,135.508766862454));
#20366=CARTESIAN_POINT('Ctrl Pts',(199.236959005824,1.57173320612938,135.466723208909));
#20367=CARTESIAN_POINT('Ctrl Pts',(199.229202703082,1.70034748405164,135.419336402549));
#20368=CARTESIAN_POINT('Ctrl Pts',(199.221442260568,1.82903040728659,135.371924304424));
#20369=CARTESIAN_POINT('Ctrl Pts',(199.213681818054,1.95562671669996,135.319163521356));
#20370=CARTESIAN_POINT('Ctrl Pts',(199.20592137554,2.0796737866346,135.261281079464));
#20371=CARTESIAN_POINT('Ctrl Pts',(199.198148475274,2.2039199879383,135.203305719538));
#20372=CARTESIAN_POINT('Ctrl Pts',(199.190375575009,2.32560842485003,135.140192451236));
#20373=CARTESIAN_POINT('Ctrl Pts',(199.182602674743,2.44430171903778,135.072213961908));
#20374=CARTESIAN_POINT('Ctrl Pts',(199.175112338981,2.55868021301209,135.006706661894));
#20375=CARTESIAN_POINT('Ctrl Pts',(199.167622003219,2.67027728465172,134.936681889443));
#20376=CARTESIAN_POINT('Ctrl Pts',(199.160131667457,2.7787297750351,134.862419747228));
#20377=CARTESIAN_POINT('Ctrl Pts',(199.152357333338,2.89129427455412,134.78534193332));
#20378=CARTESIAN_POINT('Ctrl Pts',(199.144582999219,3.00082760257082,134.703454927598));
#20379=CARTESIAN_POINT('Ctrl Pts',(199.1368086651,3.10689139061681,134.617024902474));
#20380=CARTESIAN_POINT('Ctrl Pts',(199.129043912153,3.21282446452324,134.530701394631));
#20381=CARTESIAN_POINT('Ctrl Pts',(199.121279159206,3.31529620605177,134.439846252062));
#20382=CARTESIAN_POINT('Ctrl Pts',(199.113514406258,3.41389657407908,134.344769244263));
#20383=CARTESIAN_POINT('Ctrl Pts',(199.105757365373,3.51239901083084,134.249786668289));
#20384=CARTESIAN_POINT('Ctrl Pts',(199.098000324488,3.60703744639372,134.150590841398));
#20385=CARTESIAN_POINT('Ctrl Pts',(199.090243283603,3.69743462970616,134.047531939212));
#20386=CARTESIAN_POINT('Ctrl Pts',(199.082492092363,3.78776364379947,133.944550754547));
#20387=CARTESIAN_POINT('Ctrl Pts',(199.074740901123,3.87385751502113,133.837712585816));
#20388=CARTESIAN_POINT('Ctrl Pts',(199.066989709883,3.95537587695083,133.727404362455));
#20389=CARTESIAN_POINT('Ctrl Pts',(199.059241813106,4.03685959140212,133.617143023032));
#20390=CARTESIAN_POINT('Ctrl Pts',(199.051493916329,4.11377143257403,133.503414876139));
#20391=CARTESIAN_POINT('Ctrl Pts',(199.043746019552,4.18581151837598,133.386639648796));
#20392=CARTESIAN_POINT('Ctrl Pts',(199.035999743468,4.25783653494499,133.269888848313));
#20393=CARTESIAN_POINT('Ctrl Pts',(199.028253467384,4.32499161798016,133.150092567702));
#20394=CARTESIAN_POINT('Ctrl Pts',(199.020507191299,4.38702063536518,133.027698875092));
#20395=CARTESIAN_POINT('Ctrl Pts',(199.012760858034,4.44905011063427,132.905304279));
#20396=CARTESIAN_POINT('Ctrl Pts',(199.005014524769,4.50595326800805,132.780312581386));
#20397=CARTESIAN_POINT('Ctrl Pts',(198.997268191503,4.55752048674992,132.653195406117));
#20398=CARTESIAN_POINT('Ctrl Pts',(198.9895201235,4.60909925361287,132.526049763837));
#20399=CARTESIAN_POINT('Ctrl Pts',(198.981772055497,4.65533955709796,132.396778058965));
#20400=CARTESIAN_POINT('Ctrl Pts',(198.974023987494,4.6960805123652,132.265870413593));
#20401=CARTESIAN_POINT('Ctrl Pts',(198.966267684753,4.73686476760453,132.134823638018));
#20402=CARTESIAN_POINT('Ctrl Pts',(198.958511382011,4.77213788269821,132.002137822608));
#20403=CARTESIAN_POINT('Ctrl Pts',(198.950755079269,4.80178917923892,131.868317261722));
#20404=CARTESIAN_POINT('Ctrl Pts',(198.942994636755,4.8314563015694,131.734425276773));
#20405=CARTESIAN_POINT('Ctrl Pts',(198.935234194241,4.85549555803585,131.599397724268));
#20406=CARTESIAN_POINT('Ctrl Pts',(198.927473751726,4.87384789167415,131.463746537436));
#20407=CARTESIAN_POINT('Ctrl Pts',(198.919700851461,4.89222968610765,131.327877591277));
#20408=CARTESIAN_POINT('Ctrl Pts',(198.911927951196,4.90490627858033,131.191383399763));
#20409=CARTESIAN_POINT('Ctrl Pts',(198.90415505093,4.91187067501122,131.054779335846));
#20410=CARTESIAN_POINT('Ctrl Pts',(198.896664715168,4.91858189808959,130.923141173736));
#20411=CARTESIAN_POINT('Ctrl Pts',(198.889174379406,4.91998901695341,130.791401296814));
#20412=CARTESIAN_POINT('Ctrl Pts',(198.881684043644,4.91613139364612,130.660016643299));
#20413=CARTESIAN_POINT('Ctrl Pts',(198.873909709525,4.91212750737863,130.523650500714));
#20414=CARTESIAN_POINT('Ctrl Pts',(198.866135375406,4.90243908959812,130.387235082915));
#20415=CARTESIAN_POINT('Ctrl Pts',(198.858361041287,4.88705312982617,130.251283074398));
#20416=CARTESIAN_POINT('Ctrl Pts',(198.85059628834,4.87168613187456,130.115498614582));
#20417=CARTESIAN_POINT('Ctrl Pts',(198.842831535393,4.85063560658772,129.980176812465));
#20418=CARTESIAN_POINT('Ctrl Pts',(198.835066782445,4.82394053457245,129.845830085236));
#20419=CARTESIAN_POINT('Ctrl Pts',(198.82730974156,4.79727197647905,129.71161679307));
#20420=CARTESIAN_POINT('Ctrl Pts',(198.819552700675,4.7649701040377,129.578377029504));
#20421=CARTESIAN_POINT('Ctrl Pts',(198.81179565979,4.72712561650387,129.446617465017));
#20422=CARTESIAN_POINT('Ctrl Pts',(198.80404446855,4.68930966779249,129.314957261443));
#20423=CARTESIAN_POINT('Ctrl Pts',(198.79629327731,4.64595953098006,129.184775409413));
#20424=CARTESIAN_POINT('Ctrl Pts',(198.78854208607,4.59721676439492,129.056567413647));
#20425=CARTESIAN_POINT('Ctrl Pts',(198.780794189293,4.54849471478581,128.928413909699));
#20426=CARTESIAN_POINT('Ctrl Pts',(198.773046292516,4.49438473268614,128.802232958104));
#20427=CARTESIAN_POINT('Ctrl Pts',(198.765298395739,4.43507785272916,128.678503730866));
#20428=CARTESIAN_POINT('Ctrl Pts',(198.757552119655,4.37578337849294,128.554800385114));
#20429=CARTESIAN_POINT('Ctrl Pts',(198.749805843571,4.31129433754229,128.433548095968));
#20430=CARTESIAN_POINT('Ctrl Pts',(198.742059567486,4.24184925661964,128.315204546401));
#20431=CARTESIAN_POINT('Ctrl Pts',(198.734313234221,4.1724036630692,128.196860123249));
#20432=CARTESIAN_POINT('Ctrl Pts',(198.726566900956,4.0980021544152,128.081424819717));
#20433=CARTESIAN_POINT('Ctrl Pts',(198.71882056769,4.01892821604465,127.969329919887));
#20434=CARTESIAN_POINT('Ctrl Pts',(198.711072499687,3.93983656961388,127.857209917182));
#20435=CARTESIAN_POINT('Ctrl Pts',(198.703324431684,3.85607063665606,127.748432126146));
#20436=CARTESIAN_POINT('Ctrl Pts',(198.695576363682,3.76795580858273,127.643396826716));
#20437=CARTESIAN_POINT('Ctrl Pts',(198.68782006094,3.67974733102151,127.538249894519));
#20438=CARTESIAN_POINT('Ctrl Pts',(198.680063758198,3.58718097696145,127.436853699544));
#20439=CARTESIAN_POINT('Ctrl Pts',(198.672307455456,3.49062119914604,127.339573942088));
#20440=CARTESIAN_POINT('Ctrl Pts',(198.664547012942,3.39400988446978,127.242242263496));
#20441=CARTESIAN_POINT('Ctrl Pts',(198.656786570428,3.29340118567955,127.149031665843));
#20442=CARTESIAN_POINT('Ctrl Pts',(198.649026127913,3.1891938849692,127.060268547841));
#20443=CARTESIAN_POINT('Ctrl Pts',(198.641253227648,3.08481930144869,126.971362939403));
#20444=CARTESIAN_POINT('Ctrl Pts',(198.633480327383,2.97683488028589,126.886919318566));
#20445=CARTESIAN_POINT('Ctrl Pts',(198.625707427117,2.86567043886961,126.80722214132));
#20446=CARTESIAN_POINT('Ctrl Pts',(198.618217091355,2.7585471049054,126.730422157211));
#20447=CARTESIAN_POINT('Ctrl Pts',(198.610726755593,2.64847119750003,126.658029686858));
#20448=CARTESIAN_POINT('Ctrl Pts',(198.603236419831,2.53584842786697,126.590258600127));
#20449=CARTESIAN_POINT('Ctrl Pts',(198.595462085712,2.4189555316921,126.519917952044));
#20450=CARTESIAN_POINT('Ctrl Pts',(198.587687751593,2.29894855074917,126.454333226861));
#20451=CARTESIAN_POINT('Ctrl Pts',(198.579913417474,2.1762517885438,126.393792489154));
#20452=CARTESIAN_POINT('Ctrl Pts',(198.572148664527,2.05370623913212,126.333326362497));
#20453=CARTESIAN_POINT('Ctrl Pts',(198.56438391158,1.92847785139323,126.277892026139));
#20454=CARTESIAN_POINT('Ctrl Pts',(198.556619158633,1.80101880639067,126.227733658601));
#20455=CARTESIAN_POINT('Ctrl Pts',(198.548862117748,1.6736863555085,126.17762510906));
#20456=CARTESIAN_POINT('Ctrl Pts',(198.541105076863,1.54412801780239,126.132782242412));
#20457=CARTESIAN_POINT('Ctrl Pts',(198.533348035978,1.41281909465994,126.093402618574));
#20458=CARTESIAN_POINT('Ctrl Pts',(198.525596844738,1.2816091925979,126.054052691217));
#20459=CARTESIAN_POINT('Ctrl Pts',(198.517845653498,1.14865170571014,126.020157918166));
#20460=CARTESIAN_POINT('Ctrl Pts',(198.510094462257,1.01444003188544,125.991867034795));
#20461=CARTESIAN_POINT('Ctrl Pts',(198.50234656548,0.880285401602321,125.963588175804));
#20462=CARTESIAN_POINT('Ctrl Pts',(198.494598668703,0.744878026361152,125.940908549741));
#20463=CARTESIAN_POINT('Ctrl Pts',(198.486850771926,0.608724306023622,125.92392643793));
#20464=CARTESIAN_POINT('Ctrl Pts',(198.479104495842,0.472599066109263,125.906947878411));
#20465=CARTESIAN_POINT('Ctrl Pts',(198.471358219758,0.335728179341729,125.895664510952));
#20466=CARTESIAN_POINT('Ctrl Pts',(198.463611943674,0.198625636898631,125.890123045077));
#20467=CARTESIAN_POINT('Ctrl Pts',(198.455865610409,0.061522082395698,125.884581538295));
#20468=CARTESIAN_POINT('Ctrl Pts',(198.448119277143,-0.0758127405487922,
125.884782033463));
#20469=CARTESIAN_POINT('Ctrl Pts',(198.440372943878,-0.212862749645825,
125.890719145876));
#20470=CARTESIAN_POINT('Ctrl Pts',(198.432624875875,-0.349943450142099,
125.896657587864));
#20471=CARTESIAN_POINT('Ctrl Pts',(198.424876807872,-0.486738819347844,
125.908335186536));
#20472=CARTESIAN_POINT('Ctrl Pts',(198.417128739869,-0.622736208410933,
125.925694541964));
#20473=CARTESIAN_POINT('Ctrl Pts',(198.409372437127,-0.75887813711759,125.943072347121));
#20474=CARTESIAN_POINT('Ctrl Pts',(198.401616134385,-0.894220003067948,
125.966143922283));
#20475=CARTESIAN_POINT('Ctrl Pts',(198.393859831644,-1.02825713663446,125.994800312979));
#20476=CARTESIAN_POINT('Ctrl Pts',(198.386099389129,-1.16236580985501,126.023471998453));
#20477=CARTESIAN_POINT('Ctrl Pts',(198.378338946615,-1.2951679847218,126.057734341305));
#20478=CARTESIAN_POINT('Ctrl Pts',(198.370578504101,-1.42617350123758,126.097428261257));
#20479=CARTESIAN_POINT('Ctrl Pts',(198.362805603836,-1.55738931943859,126.137185901413));
#20480=CARTESIAN_POINT('Ctrl Pts',(198.35503270357,-1.68680234652046,126.182392413503));
#20481=CARTESIAN_POINT('Ctrl Pts',(198.347259803305,-1.81394093480719,126.232839935394));
#20482=CARTESIAN_POINT('Ctrl Pts',(198.339769467543,-1.93645771516747,126.281453562794));
#20483=CARTESIAN_POINT('Ctrl Pts',(198.332279131781,-2.05686226744433,126.334933642695));
#20484=CARTESIAN_POINT('Ctrl Pts',(198.324788796019,-2.17475536003933,126.393054440652));
#20485=CARTESIAN_POINT('Ctrl Pts',(198.317013701679,-2.29713037045767,126.453384805213));
#20486=CARTESIAN_POINT('Ctrl Pts',(198.309238607339,-2.41718687346733,126.518906845975));
#20487=CARTESIAN_POINT('Ctrl Pts',(198.301463513,-2.53445302826001,126.589419228882));
#20488=CARTESIAN_POINT('Ctrl Pts',(198.293698169544,-2.65157211748876,126.659843180958));
#20489=CARTESIAN_POINT('Ctrl Pts',(198.285932826088,-2.76590748987507,126.735244822049));
#20490=CARTESIAN_POINT('Ctrl Pts',(198.278167482632,-2.87700919668973,126.815375640825));
#20491=CARTESIAN_POINT('Ctrl Pts',(198.270116194762,-2.99220201841537,126.89845712883));
#20492=CARTESIAN_POINT('Ctrl Pts',(198.262064906893,-3.10391807437486,126.986622596305));
#20493=CARTESIAN_POINT('Ctrl Pts',(198.254013619023,-3.21168484940525,127.079543374989));
#20494=CARTESIAN_POINT('Ctrl Pts',(198.246262861591,-3.31542901381586,127.168995699587));
#20495=CARTESIAN_POINT('Ctrl Pts',(198.23851210416,-3.4155130831933,127.262854447875));
#20496=CARTESIAN_POINT('Ctrl Pts',(198.230761346728,-3.51154654453313,127.360783418188));
#20497=CARTESIAN_POINT('Ctrl Pts',(198.223014065701,-3.60753693251182,127.458668464957));
#20498=CARTESIAN_POINT('Ctrl Pts',(198.215266784674,-3.69948005432967,127.560619822749));
#20499=CARTESIAN_POINT('Ctrl Pts',(198.207519503647,-3.78702100058199,127.666263263491));
#20500=CARTESIAN_POINT('Ctrl Pts',(198.199774019722,-3.8745416403494,127.771882198593));
#20501=CARTESIAN_POINT('Ctrl Pts',(198.192028535798,-3.95766188812499,127.881191211036));
#20502=CARTESIAN_POINT('Ctrl Pts',(198.184283051873,-4.036066276408,127.993782016114));
#20503=CARTESIAN_POINT('Ctrl Pts',(198.176537687326,-4.1144694562842,128.106371085887));
#20504=CARTESIAN_POINT('Ctrl Pts',(198.168792322778,-4.18815669953273,128.222241525939));
#20505=CARTESIAN_POINT('Ctrl Pts',(198.161046958231,-4.25685536445191,128.340955358857));
#20506=CARTESIAN_POINT('Ctrl Pts',(198.153297277113,-4.32559231583465,128.459735352199));
#20507=CARTESIAN_POINT('Ctrl Pts',(198.145547595995,-4.38933494059853,128.581361564616));
#20508=CARTESIAN_POINT('Ctrl Pts',(198.137797914878,-4.44785607756905,128.705370532851));
#20509=CARTESIAN_POINT('Ctrl Pts',(198.130045641782,-4.50639678766299,128.82942097743));
#20510=CARTESIAN_POINT('Ctrl Pts',(198.122293368687,-4.55971237526599,128.955855407105));
#20511=CARTESIAN_POINT('Ctrl Pts',(198.114541095592,-4.60762386482984,129.084190456579));
#20512=CARTESIAN_POINT('Ctrl Pts',(198.106781573825,-4.65558015346834,129.212645504231));
#20513=CARTESIAN_POINT('Ctrl Pts',(198.099022052058,-4.69812213230576,129.343004349367));
#20514=CARTESIAN_POINT('Ctrl Pts',(198.091262530291,-4.73512064756484,129.474768381012));
#20515=CARTESIAN_POINT('Ctrl Pts',(198.089153878115,-4.74517500427239,129.510575292887));
#20516=CARTESIAN_POINT('Ctrl Pts',(198.087045225939,-4.75482027712228,129.546485914373));
#20517=CARTESIAN_POINT('Ctrl Pts',(198.084936573762,-4.76405452823404,129.582490119308));
#20518=CARTESIAN_POINT('Ctrl Pts',(199.834960626423,-4.76405452823405,129.582490119308));
#20519=CARTESIAN_POINT('Ctrl Pts',(199.827324041593,-4.79766326068053,129.713530057033));
#20520=CARTESIAN_POINT('Ctrl Pts',(199.819687456764,-4.82584625215587,129.845899345302));
#20521=CARTESIAN_POINT('Ctrl Pts',(199.812050871934,-4.84851847510395,129.979102076819));
#20522=CARTESIAN_POINT('Ctrl Pts',(199.804185632618,-4.87186954934494,130.116293162135));
#20523=CARTESIAN_POINT('Ctrl Pts',(199.796320393303,-4.88937460082088,130.254367925497));
#20524=CARTESIAN_POINT('Ctrl Pts',(199.788455153987,-4.90099827408403,130.392779544234));
#20525=CARTESIAN_POINT('Ctrl Pts',(199.780589914672,-4.91262194734719,130.53119116297));
#20526=CARTESIAN_POINT('Ctrl Pts',(199.772724675356,-4.91836427281118,130.669939172252));
#20527=CARTESIAN_POINT('Ctrl Pts',(199.76485943604,-4.91824827604694,130.808478585671));
#20528=CARTESIAN_POINT('',(200.110140563961,-4.91824997595732,130.804846925942));
#20529=CARTESIAN_POINT('Ctrl Pts',(200.179870531952,-4.76405452823405,129.582490119308));
#20530=CARTESIAN_POINT('Ctrl Pts',(200.171798423708,-4.79949019568666,129.720653248895));
#20531=CARTESIAN_POINT('Ctrl Pts',(200.163726315465,-4.8289461026174,129.860494510444));
#20532=CARTESIAN_POINT('Ctrl Pts',(200.155654207222,-4.85227401211597,130.001478326166));
#20533=CARTESIAN_POINT('Ctrl Pts',(200.147594415967,-4.87556632625476,130.142247018897));
#20534=CARTESIAN_POINT('Ctrl Pts',(200.139534624712,-4.89274923115088,130.284154452949));
#20535=CARTESIAN_POINT('Ctrl Pts',(200.131474833457,-4.90372514985256,130.426653433092));
#20536=CARTESIAN_POINT('Ctrl Pts',(200.124363410307,-4.91340956969396,130.552385045013));
#20537=CARTESIAN_POINT('Ctrl Pts',(200.117251987158,-4.91826246131281,130.678576831645));
#20538=CARTESIAN_POINT('Ctrl Pts',(200.110140564008,-4.9182499759574,130.804846925109));
#20539=CARTESIAN_POINT('Ctrl Pts',(200.110140563961,-4.91824997595732,130.804846925942));
#20540=CARTESIAN_POINT('Ctrl Pts',(200.101963209632,-4.91823561914748,130.95004364306));
#20541=CARTESIAN_POINT('Ctrl Pts',(200.093785855304,-4.91178722962492,131.095096221673));
#20542=CARTESIAN_POINT('Ctrl Pts',(200.085608500975,-4.8989686251045,131.239434717854));
#20543=CARTESIAN_POINT('Ctrl Pts',(200.077418065999,-4.88612951570811,131.384004100554));
#20544=CARTESIAN_POINT('Ctrl Pts',(200.069227631024,-4.86689987818642,131.527856800843));
#20545=CARTESIAN_POINT('Ctrl Pts',(200.061037196048,-4.84139484664338,131.670431631626));
#20546=CARTESIAN_POINT('Ctrl Pts',(200.052825216095,-4.81582272399528,131.81338150617));
#20547=CARTESIAN_POINT('Ctrl Pts',(200.044613236142,-4.78394225338721,131.955046471638));
#20548=CARTESIAN_POINT('Ctrl Pts',(200.036401256189,-4.74591932059585,132.094877128462));
#20549=CARTESIAN_POINT('Ctrl Pts',(200.028177613076,-4.70784238529188,132.234906381402));
#20550=CARTESIAN_POINT('Ctrl Pts',(200.019953969963,-4.66360567060591,132.373095819458));
#20551=CARTESIAN_POINT('Ctrl Pts',(200.01173032685,-4.61342381118858,132.508914459737));
#20552=CARTESIAN_POINT('Ctrl Pts',(200.003487519808,-4.56312501070649,132.645049604358));
#20553=CARTESIAN_POINT('Ctrl Pts',(199.995244712766,-4.50685348823889,132.778802607651));
#20554=CARTESIAN_POINT('Ctrl Pts',(199.987001905724,-4.4448713186341,132.90966392666));
#20555=CARTESIAN_POINT('Ctrl Pts',(199.983296451395,-4.41700798305935,132.96849105176));
#20556=CARTESIAN_POINT('Ctrl Pts',(199.979590997066,-4.38799121645204,133.026734176052));
#20557=CARTESIAN_POINT('Ctrl Pts',(199.975885542737,-4.35784769754507,133.084348886725));
#20558=CARTESIAN_POINT('Ctrl Pts',(199.968111208618,-4.29460422813576,133.205229073381));
#20559=CARTESIAN_POINT('Ctrl Pts',(199.960336874499,-4.22622722019875,133.3236673123));
#20560=CARTESIAN_POINT('Ctrl Pts',(199.95256254038,-4.15292920796671,133.43919686601));
#20561=CARTESIAN_POINT('Ctrl Pts',(199.944797787433,-4.07972152898389,133.554584039872));
#20562=CARTESIAN_POINT('Ctrl Pts',(199.937033034486,-4.00160512008709,133.667069334041));
#20563=CARTESIAN_POINT('Ctrl Pts',(199.929268281538,-3.91883915315159,133.776208990923));
#20564=CARTESIAN_POINT('Ctrl Pts',(199.921511240653,-3.83615539054131,133.88524024876));
#20565=CARTESIAN_POINT('Ctrl Pts',(199.913754199768,-3.74883149464554,133.990932172596));
#20566=CARTESIAN_POINT('Ctrl Pts',(199.905997158883,-3.65717063344393,134.092868793073));
#20567=CARTESIAN_POINT('Ctrl Pts',(199.898245967643,-3.56557889441098,134.194728542351));
#20568=CARTESIAN_POINT('Ctrl Pts',(199.890494776403,-3.46965696023711,134.292838335461));
#20569=CARTESIAN_POINT('Ctrl Pts',(199.882743585163,-3.36974885186079,134.386814488572));
#20570=CARTESIAN_POINT('Ctrl Pts',(199.874995688386,-3.26988320709536,134.48075069931));
#20571=CARTESIAN_POINT('Ctrl Pts',(199.867247791609,-3.16603504200538,134.570556497095));
#20572=CARTESIAN_POINT('Ctrl Pts',(199.859499894832,-3.05858572710474,134.655884525378));
#20573=CARTESIAN_POINT('Ctrl Pts',(199.851753618747,-2.95115888828444,134.741194704878));
#20574=CARTESIAN_POINT('Ctrl Pts',(199.844007342663,-2.84013270394872,134.822028734951));
#20575=CARTESIAN_POINT('Ctrl Pts',(199.836261066579,-2.72592185460808,134.89807935547));
#20576=CARTESIAN_POINT('Ctrl Pts',(199.828514733314,-2.61171016218902,134.974130537379));
#20577=CARTESIAN_POINT('Ctrl Pts',(199.820768400049,-2.49431408327654,135.045398022584));
#20578=CARTESIAN_POINT('Ctrl Pts',(199.813022066783,-2.37417718264307,135.111617954656));
#20579=CARTESIAN_POINT('Ctrl Pts',(199.80527399878,-2.25401337818375,135.177852716222));
#20580=CARTESIAN_POINT('Ctrl Pts',(199.797525930777,-2.13110787296654,135.239037486666));
#20581=CARTESIAN_POINT('Ctrl Pts',(199.789777862774,-2.00592835665058,135.294954619531));
#20582=CARTESIAN_POINT('Ctrl Pts',(199.782021560032,-1.88061579805486,135.35093118179));
#20583=CARTESIAN_POINT('Ctrl Pts',(199.77426525729,-1.75302475798892,135.401628763137));
#20584=CARTESIAN_POINT('Ctrl Pts',(199.766508954549,-1.623642929,135.446877898267));
#20585=CARTESIAN_POINT('Ctrl Pts',(199.758748512034,-1.49419204503319,135.492151184223));
#20586=CARTESIAN_POINT('Ctrl Pts',(199.75098806952,-1.362948841577,135.531970116074));
#20587=CARTESIAN_POINT('Ctrl Pts',(199.743227627006,-1.23041469352731,135.566215586426));
#20588=CARTESIAN_POINT('Ctrl Pts',(199.73545472674,-1.09766778989741,135.600516030646));
#20589=CARTESIAN_POINT('Ctrl Pts',(199.727681826475,-0.96362618299564,135.629225052453));
#20590=CARTESIAN_POINT('Ctrl Pts',(199.71990892621,-0.828800812444949,135.65227483667));
#20591=CARTESIAN_POINT('Ctrl Pts',(199.712418590448,-0.698876683722678,
135.674486703171));
#20592=CARTESIAN_POINT('Ctrl Pts',(199.704928254686,-0.568225091055471,
135.691443604055));
#20593=CARTESIAN_POINT('Ctrl Pts',(199.697437918924,-0.437304423404299,
135.703130657461));
#20594=CARTESIAN_POINT('Ctrl Pts',(199.689663584805,-0.301419858842875,
135.715260829049));
#20595=CARTESIAN_POINT('Ctrl Pts',(199.681889250686,-0.164814971104963,
135.721752076884));
#20596=CARTESIAN_POINT('Ctrl Pts',(199.674114916567,-0.0279973195866715,
135.722530929033));
#20597=CARTESIAN_POINT('Ctrl Pts',(199.66635016362,0.10865171640381,135.723308821316));
#20598=CARTESIAN_POINT('Ctrl Pts',(199.658585410673,0.245512607244556,135.718388323244));
#20599=CARTESIAN_POINT('Ctrl Pts',(199.650820657726,0.382071918374638,135.707747621637));
#20600=CARTESIAN_POINT('Ctrl Pts',(199.643063616841,0.518495596871722,135.697117488524));
#20601=CARTESIAN_POINT('Ctrl Pts',(199.635306575956,0.654617904481336,135.680778488268));
#20602=CARTESIAN_POINT('Ctrl Pts',(199.627549535071,0.789925004703764,135.658760843077));
#20603=CARTESIAN_POINT('Ctrl Pts',(199.619798343831,0.925130068789412,135.636759801564));
#20604=CARTESIAN_POINT('Ctrl Pts',(199.612047152591,1.05952076479068,135.609088701334));
#20605=CARTESIAN_POINT('Ctrl Pts',(199.604295961351,1.19258833691385,135.575829586464));
#20606=CARTESIAN_POINT('Ctrl Pts',(199.596548064574,1.32559935176917,135.542584607605));
#20607=CARTESIAN_POINT('Ctrl Pts',(199.588800167797,1.45728798274033,135.503756432513));
#20608=CARTESIAN_POINT('Ctrl Pts',(199.581052271019,1.58715584884965,135.459478164306));
#20609=CARTESIAN_POINT('Ctrl Pts',(199.573305994935,1.71699654940101,135.415209158157));
#20610=CARTESIAN_POINT('Ctrl Pts',(199.565559718851,1.84501687283777,135.365492452586));
#20611=CARTESIAN_POINT('Ctrl Pts',(199.557813442767,1.97073416756975,135.310510848447));
#20612=CARTESIAN_POINT('Ctrl Pts',(199.550067109502,2.09645239031821,135.255528838447));
#20613=CARTESIAN_POINT('Ctrl Pts',(199.542320776237,2.21986719223249,135.195282008988));
#20614=CARTESIAN_POINT('Ctrl Pts',(199.534574442971,2.34051682582934,135.130000922828));
#20615=CARTESIAN_POINT('Ctrl Pts',(199.526826374968,2.46119347807506,135.064705217422));
#20616=CARTESIAN_POINT('Ctrl Pts',(199.519078306965,2.57910338599568,134.994373197965));
#20617=CARTESIAN_POINT('Ctrl Pts',(199.511330238962,2.6938106397786,134.919280701786));
#20618=CARTESIAN_POINT('Ctrl Pts',(199.503573936221,2.80863980579594,134.844108396408));
#20619=CARTESIAN_POINT('Ctrl Pts',(199.495817633479,2.92025919055272,134.764165721911));
#20620=CARTESIAN_POINT('Ctrl Pts',(199.488061330737,3.02826260835506,134.679771387709));
#20621=CARTESIAN_POINT('Ctrl Pts',(199.480300888223,3.13632367083349,134.595332009709));
#20622=CARTESIAN_POINT('Ctrl Pts',(199.472540445709,3.24076462319159,134.506436490939));
#20623=CARTESIAN_POINT('Ctrl Pts',(199.464780003195,3.34121425162771,134.41344227184));
#20624=CARTESIAN_POINT('Ctrl Pts',(199.457007102929,3.44182513072487,134.320298770166));
#20625=CARTESIAN_POINT('Ctrl Pts',(199.449234202664,3.53843160653162,134.223043697568));
#20626=CARTESIAN_POINT('Ctrl Pts',(199.441461302398,3.63070044887218,134.122070266263));
#20627=CARTESIAN_POINT('Ctrl Pts',(199.433970966636,3.71961508638472,134.024767473521));
#20628=CARTESIAN_POINT('Ctrl Pts',(199.426480630874,3.8045017845271,133.924012207482));
#20629=CARTESIAN_POINT('Ctrl Pts',(199.418990295112,3.88510025233675,133.820182079754));
#20630=CARTESIAN_POINT('Ctrl Pts',(199.411215960993,3.96875463554883,133.712415201177));
#20631=CARTESIAN_POINT('Ctrl Pts',(199.403441626874,4.04805418477677,133.600994318284));
#20632=CARTESIAN_POINT('Ctrl Pts',(199.395667292754,4.12266273775037,133.486306741795));
#20633=CARTESIAN_POINT('Ctrl Pts',(199.387902539807,4.19717934235037,133.371760507494));
#20634=CARTESIAN_POINT('Ctrl Pts',(199.38013778686,4.26701624247923,133.253955914529));
#20635=CARTESIAN_POINT('Ctrl Pts',(199.372373033913,4.33187756216918,133.133313139382));
#20636=CARTESIAN_POINT('Ctrl Pts',(199.364615993028,4.39667446068206,133.01279018834));
#20637=CARTESIAN_POINT('Ctrl Pts',(199.356858952143,4.45650542925731,132.889435007023));
#20638=CARTESIAN_POINT('Ctrl Pts',(199.349101911258,4.51111815351607,132.763696236473));
#20639=CARTESIAN_POINT('Ctrl Pts',(199.341350720018,4.56568969389464,132.638052286508));
#20640=CARTESIAN_POINT('Ctrl Pts',(199.333599528778,4.61505066744896,132.510028682241));
#20641=CARTESIAN_POINT('Ctrl Pts',(199.325848337538,4.65899510525039,132.380097801158));
#20642=CARTESIAN_POINT('Ctrl Pts',(199.318100440761,4.7029208654935,132.250222144165));
#20643=CARTESIAN_POINT('Ctrl Pts',(199.310352543983,4.74143454383123,132.118441192244));
#20644=CARTESIAN_POINT('Ctrl Pts',(199.302604647206,4.77437873659335,131.985246192914));
#20645=CARTESIAN_POINT('Ctrl Pts',(199.294858371122,4.80731603814052,131.852079055106));
#20646=CARTESIAN_POINT('Ctrl Pts',(199.287112095038,4.83468607758103,131.717498837516));
#20647=CARTESIAN_POINT('Ctrl Pts',(199.279365818954,4.85638176547755,131.582010416921));
#20648=CARTESIAN_POINT('Ctrl Pts',(199.271619485689,4.8780776135267,131.446520996182));
#20649=CARTESIAN_POINT('Ctrl Pts',(199.263873152423,4.89409896463232,131.310123745109));
#20650=CARTESIAN_POINT('Ctrl Pts',(199.256126819158,4.9043902119798,131.17333176974));
#20651=CARTESIAN_POINT('Ctrl Pts',(199.248378751155,4.91468376398078,131.036509160757));
#20652=CARTESIAN_POINT('Ctrl Pts',(199.240630683152,4.91924462944542,130.899292041369));
#20653=CARTESIAN_POINT('Ctrl Pts',(199.232882615149,4.91806925823009,130.762196251662));
#20654=CARTESIAN_POINT('Ctrl Pts',(199.225126312407,4.91689263781624,130.624954754918));
#20655=CARTESIAN_POINT('Ctrl Pts',(199.217370009665,4.90996760558296,130.487835237022));
#20656=CARTESIAN_POINT('Ctrl Pts',(199.209613706923,4.8973427474991,130.351351703727));
#20657=CARTESIAN_POINT('Ctrl Pts',(199.201853264409,4.88471115114836,130.21479532506));
#20658=CARTESIAN_POINT('Ctrl Pts',(199.194092821895,4.86637371941593,130.07887599463));
#20659=CARTESIAN_POINT('Ctrl Pts',(199.186332379381,4.8424305269433,129.944099230412));
#20660=CARTESIAN_POINT('Ctrl Pts',(199.178559479115,4.81844889873255,129.809106110568));
#20661=CARTESIAN_POINT('Ctrl Pts',(199.17078657885,4.788843611667,129.675259604108));
#20662=CARTESIAN_POINT('Ctrl Pts',(199.163013678584,4.75376536727037,129.543052607823));
#20663=CARTESIAN_POINT('Ctrl Pts',(199.155523342822,4.71996230541452,129.415651668864));
#20664=CARTESIAN_POINT('Ctrl Pts',(199.14803300706,4.68107738037903,129.289773403227));
#20665=CARTESIAN_POINT('Ctrl Pts',(199.140542671298,4.63728759387846,129.165840909366));
#20666=CARTESIAN_POINT('Ctrl Pts',(199.132768337179,4.59183750431285,129.037209477331));
#20667=CARTESIAN_POINT('Ctrl Pts',(199.12499400306,4.54095930328843,128.910266811875));
#20668=CARTESIAN_POINT('Ctrl Pts',(199.117219668941,4.48479714236479,128.785505086742));
#20669=CARTESIAN_POINT('Ctrl Pts',(199.109454915994,4.42870419628514,128.660897119286));
#20670=CARTESIAN_POINT('Ctrl Pts',(199.101690163047,4.36734040620565,128.538465097289));
#20671=CARTESIAN_POINT('Ctrl Pts',(199.0939254101,4.30089935031177,128.418685065235));
#20672=CARTESIAN_POINT('Ctrl Pts',(199.086168369215,4.23452428461125,128.299024000398));
#20673=CARTESIAN_POINT('Ctrl Pts',(199.07841132833,4.16308217693648,128.182010023415));
#20674=CARTESIAN_POINT('Ctrl Pts',(199.070654287445,4.08681409961739,128.068097914961));
#20675=CARTESIAN_POINT('Ctrl Pts',(199.062903096205,4.01060353664873,127.954271708514));
#20676=CARTESIAN_POINT('Ctrl Pts',(199.055151904965,3.92957446447712,127.84354303823));
#20677=CARTESIAN_POINT('Ctrl Pts',(199.047400713724,3.84401297642226,127.736340523173));
#20678=CARTESIAN_POINT('Ctrl Pts',(199.039652816947,3.75848785428223,127.629183572045));
#20679=CARTESIAN_POINT('Ctrl Pts',(199.03190492017,3.66843439109177,127.525550100254));
#20680=CARTESIAN_POINT('Ctrl Pts',(199.024157023393,3.57418080677142,127.425838067248));
#20681=CARTESIAN_POINT('Ctrl Pts',(199.016410747309,3.47994693826904,127.32614689185));
#20682=CARTESIAN_POINT('Ctrl Pts',(199.008664471225,3.38151496456809,127.230375807597));
#20683=CARTESIAN_POINT('Ctrl Pts',(199.000918195141,3.27925176834539,127.138887810096));
#20684=CARTESIAN_POINT('Ctrl Pts',(198.993171861876,3.17698781723904,127.047399137251));
#20685=CARTESIAN_POINT('Ctrl Pts',(198.98542552861,3.07089287855635,126.960193874925));
#20686=CARTESIAN_POINT('Ctrl Pts',(198.977679195345,2.96136858609743,126.877596153051));
#20687=CARTESIAN_POINT('Ctrl Pts',(198.969931127342,2.85181976643257,126.794979933991));
#20688=CARTESIAN_POINT('Ctrl Pts',(198.962183059339,2.73884037688976,126.716973543961));
#20689=CARTESIAN_POINT('Ctrl Pts',(198.954434991336,2.62286248940288,126.643858793965));
#20690=CARTESIAN_POINT('Ctrl Pts',(198.946678688594,2.50676133923701,126.570666336743));
#20691=CARTESIAN_POINT('Ctrl Pts',(198.938922385852,2.38765565632938,126.502376113735));
#20692=CARTESIAN_POINT('Ctrl Pts',(198.931166083111,2.26600415017978,126.439225080854));
#20693=CARTESIAN_POINT('Ctrl Pts',(198.923405640596,2.14428771495838,126.376040342365));
#20694=CARTESIAN_POINT('Ctrl Pts',(198.915645198082,2.02002310306419,126.318000424913));
#20695=CARTESIAN_POINT('Ctrl Pts',(198.907884755568,1.8936897138752,126.265294377681));
#20696=CARTESIAN_POINT('Ctrl Pts',(198.900111855303,1.76715352311459,126.212503722024));
#20697=CARTESIAN_POINT('Ctrl Pts',(198.892338955037,1.63854228569136,126.165064182373));
#20698=CARTESIAN_POINT('Ctrl Pts',(198.884566054772,1.50835214749063,126.123115392024));
#20699=CARTESIAN_POINT('Ctrl Pts',(198.87707571901,1.38289474874265,126.082691545867));
#20700=CARTESIAN_POINT('Ctrl Pts',(198.869585383248,1.25597154700458,126.047366257253));
#20701=CARTESIAN_POINT('Ctrl Pts',(198.862095047486,1.12803418073941,126.017219304675));
#20702=CARTESIAN_POINT('Ctrl Pts',(198.854320713367,0.995246030346574,125.985929321228));
#20703=CARTESIAN_POINT('Ctrl Pts',(198.846546379248,0.860944660272916,125.96011898127));
#20704=CARTESIAN_POINT('Ctrl Pts',(198.838772045129,0.72562206766675,125.939933037941));
#20705=CARTESIAN_POINT('Ctrl Pts',(198.831007292181,0.590466248061855,125.919771971984));
#20706=CARTESIAN_POINT('Ctrl Pts',(198.823242539234,0.454292093069238,125.905221568033));
#20707=CARTESIAN_POINT('Ctrl Pts',(198.815477786287,0.317604746131932,125.89637627695));
#20708=CARTESIAN_POINT('Ctrl Pts',(198.807720745402,0.181053158994685,125.887539771135));
#20709=CARTESIAN_POINT('Ctrl Pts',(198.799963704517,0.0439897818821281,
125.884397126882));
#20710=CARTESIAN_POINT('Ctrl Pts',(198.792206663632,-0.0930724598611862,
125.886991343278));
#20711=CARTESIAN_POINT('Ctrl Pts',(198.784455472392,-0.230031341901755,
125.889583603354));
#20712=CARTESIAN_POINT('Ctrl Pts',(198.776704281152,-0.366988700963738,
125.897904105649));
#20713=CARTESIAN_POINT('Ctrl Pts',(198.768953089912,-0.503429287263447,
125.911943830821));
#20714=CARTESIAN_POINT('Ctrl Pts',(198.761205193135,-0.639811882674504,
125.925977588736));
#20715=CARTESIAN_POINT('Ctrl Pts',(198.753457296358,-0.775677754077462,
125.945725694873));
#20716=CARTESIAN_POINT('Ctrl Pts',(198.745709399581,-0.910514676033535,
125.971127115321));
#20717=CARTESIAN_POINT('Ctrl Pts',(198.737963123496,-1.04532339301227,125.996523222339));
#20718=CARTESIAN_POINT('Ctrl Pts',(198.730216847412,-1.17910320469284,126.027570219174));
#20719=CARTESIAN_POINT('Ctrl Pts',(198.722470571328,-1.31135040354105,126.064155645032));
#20720=CARTESIAN_POINT('Ctrl Pts',(198.714724238063,-1.44359857860805,126.100741340956));
#20721=CARTESIAN_POINT('Ctrl Pts',(198.706977904797,-1.57431374145571,126.14286544324));
#20722=CARTESIAN_POINT('Ctrl Pts',(198.699231571532,-1.70300609951057,126.190365246141));
#20723=CARTESIAN_POINT('Ctrl Pts',(198.691483503529,-1.83172727732661,126.237875686293));
#20724=CARTESIAN_POINT('Ctrl Pts',(198.683735435526,-1.95842438223704,126.290764087235));
#20725=CARTESIAN_POINT('Ctrl Pts',(198.675987367523,-2.08262677322981,126.348819260343));
#20726=CARTESIAN_POINT('Ctrl Pts',(198.668231064781,-2.20696116800184,126.406936135179));
#20727=CARTESIAN_POINT('Ctrl Pts',(198.660474762039,-2.32879519762787,126.47023058584));
#20728=CARTESIAN_POINT('Ctrl Pts',(198.652718459298,-2.44768156069828,126.538444767491));
#20729=CARTESIAN_POINT('Ctrl Pts',(198.644958016783,-2.56663137700036,126.606695357105));
#20730=CARTESIAN_POINT('Ctrl Pts',(198.637197574269,-2.68263006138942,126.679870701362));
#20731=CARTESIAN_POINT('Ctrl Pts',(198.629437131755,-2.79525943435933,126.757669653689));
#20732=CARTESIAN_POINT('Ctrl Pts',(198.62166423149,-2.90806960999747,126.835593495801));
#20733=CARTESIAN_POINT('Ctrl Pts',(198.613891331224,-3.01749935359477,126.918155542348));
#20734=CARTESIAN_POINT('Ctrl Pts',(198.606118430959,-3.12316300873507,127.005013846953));
#20735=CARTESIAN_POINT('Ctrl Pts',(198.598628095197,-3.22498552385993,127.088714633402));
#20736=CARTESIAN_POINT('Ctrl Pts',(198.591137759435,-3.32331078044587,127.176404536312));
#20737=CARTESIAN_POINT('Ctrl Pts',(198.583647423673,-3.41782753696518,127.267746701677));
#20738=CARTESIAN_POINT('Ctrl Pts',(198.575987342496,-3.51448622497807,127.361158856193));
#20739=CARTESIAN_POINT('Ctrl Pts',(198.568327261318,-3.60748705227816,127.458705550652));
#20740=CARTESIAN_POINT('Ctrl Pts',(198.560667180141,-3.69644762254403,127.560064386287));
#20741=CARTESIAN_POINT('Ctrl Pts',(198.553016015211,-3.78530464372584,127.6613052414));
#20742=CARTESIAN_POINT('Ctrl Pts',(198.545364850281,-3.87013049362145,127.766349116946));
#20743=CARTESIAN_POINT('Ctrl Pts',(198.53771368535,-3.95057739062617,127.874834829461));
#20744=CARTESIAN_POINT('Ctrl Pts',(198.530069653823,-4.03094928465215,127.983219397595));
#20745=CARTESIAN_POINT('Ctrl Pts',(198.522425622296,-4.10695010528644,128.095039100229));
#20746=CARTESIAN_POINT('Ctrl Pts',(198.514781590769,-4.17827075473654,128.209897944369));
#20747=CARTESIAN_POINT('Ctrl Pts',(198.507143088631,-4.24953981365601,128.324673704173));
#20748=CARTESIAN_POINT('Ctrl Pts',(198.499504586494,-4.31613522474468,128.442483890537));
#20749=CARTESIAN_POINT('Ctrl Pts',(198.491866084356,-4.37779019060595,128.562902139357));
#20750=CARTESIAN_POINT('Ctrl Pts',(198.484230874548,-4.43941858208351,128.683268485777));
#20751=CARTESIAN_POINT('Ctrl Pts',(198.47659566474,-4.49611058101027,128.806240300078));
#20752=CARTESIAN_POINT('Ctrl Pts',(198.468960454932,-4.54764472612785,128.931365554192));
#20753=CARTESIAN_POINT('Ctrl Pts',(198.461325447542,-4.5991775050181,129.056487491098));
#20754=CARTESIAN_POINT('Ctrl Pts',(198.453690440153,-4.64555254017037,129.183762384902));
#20755=CARTESIAN_POINT('Ctrl Pts',(198.446055432763,-4.68659615849717,129.312717392911));
#20756=CARTESIAN_POINT('Ctrl Pts',(198.440775680082,-4.71497860042732,129.401892231183));
#20757=CARTESIAN_POINT('Ctrl Pts',(198.435495927401,-4.74081256549775,129.491870059345));
#20758=CARTESIAN_POINT('Ctrl Pts',(198.430216174721,-4.76405452823404,129.582490119308));
#20759=CARTESIAN_POINT('Origin',(213.235140564004,0.,130.804360617566));
#20760=CARTESIAN_POINT('',(196.33459504632,-4.76405452823405,129.582490119308));
#20761=CARTESIAN_POINT('',(196.680227908624,-4.76405452823405,129.582490119308));
#20762=CARTESIAN_POINT('',(213.235140564004,-4.76405452823405,129.582490119308));
#20763=CARTESIAN_POINT('',(198.014859435953,-4.91824901604543,130.801249561772));
#20764=CARTESIAN_POINT('Ctrl Pts',(198.014859435953,-4.91824901604543,130.801249561772));
#20765=CARTESIAN_POINT('Ctrl Pts',(198.007194602125,-4.91833425441149,130.936002371663));
#20766=CARTESIAN_POINT('Ctrl Pts',(197.999529768297,-4.9128772797748,131.070975950461));
#20767=CARTESIAN_POINT('Ctrl Pts',(197.991864934469,-4.90185011753594,131.205669087091));
#20768=CARTESIAN_POINT('Ctrl Pts',(197.984208471378,-4.89083499802213,131.340215125821));
#20769=CARTESIAN_POINT('Ctrl Pts',(197.976552008288,-4.87426182187178,131.47448093386));
#20770=CARTESIAN_POINT('Ctrl Pts',(197.968895545198,-4.85215462495801,131.607964100634));
#20771=CARTESIAN_POINT('Ctrl Pts',(197.961245495214,-4.83006594518477,131.741335460987));
#20772=CARTESIAN_POINT('Ctrl Pts',(197.95359544523,-4.80245253092967,131.873925089211));
#20773=CARTESIAN_POINT('Ctrl Pts',(197.945945395246,-4.76939029060855,132.005235014974));
#20774=CARTESIAN_POINT('Ctrl Pts',(197.938299305357,-4.73634516515454,132.136476967365));
#20775=CARTESIAN_POINT('Ctrl Pts',(197.930653215467,-4.69785692034788,132.266440145392));
#20776=CARTESIAN_POINT('Ctrl Pts',(197.923007125577,-4.65405260327977,132.394636514511));
#20777=CARTESIAN_POINT('Ctrl Pts',(197.915363000358,-4.61025954177498,132.522799943444));
#20778=CARTESIAN_POINT('Ctrl Pts',(197.907718875139,-4.56115325357192,132.649197085549));
#20779=CARTESIAN_POINT('Ctrl Pts',(197.90007474992,-4.50691057686776,132.773355314008));
#20780=CARTESIAN_POINT('Ctrl Pts',(197.892430829445,-4.45266935302643,132.897510216952));
#20781=CARTESIAN_POINT('Ctrl Pts',(197.88478690897,-4.3932921754651,133.019425956816));
#20782=CARTESIAN_POINT('Ctrl Pts',(197.877142988494,-4.32900370978916,133.138650647346));
#20783=CARTESIAN_POINT('Ctrl Pts',(197.869497513223,-4.26470216764921,133.257899588531));
#20784=CARTESIAN_POINT('Ctrl Pts',(197.861852037952,-4.19548754221391,133.374456038018));
#20785=CARTESIAN_POINT('Ctrl Pts',(197.854206562681,-4.12162977785966,133.487893929593));
#20786=CARTESIAN_POINT('Ctrl Pts',(197.846553256078,-4.04769636030815,133.60144801666));
#20787=CARTESIAN_POINT('Ctrl Pts',(197.838899949475,-3.9691105266443,133.711876829538));
#20788=CARTESIAN_POINT('Ctrl Pts',(197.831246642873,-3.8861849641364,133.818784192152));
#20789=CARTESIAN_POINT('Ctrl Pts',(197.823589202619,-3.80321461244542,133.925749296834));
#20790=CARTESIAN_POINT('Ctrl Pts',(197.815931762365,-3.71590012432521,134.029188857436));
#20791=CARTESIAN_POINT('Ctrl Pts',(197.808274322111,-3.62459270805556,134.128741877772));
#20792=CARTESIAN_POINT('Ctrl Pts',(197.800605170645,-3.53314564714557,134.228447153492));
#20793=CARTESIAN_POINT('Ctrl Pts',(197.792936019179,-3.43769374582733,134.324253733522));
#20794=CARTESIAN_POINT('Ctrl Pts',(197.785266867713,-3.33862350365245,134.415839007832));
#20795=CARTESIAN_POINT('Ctrl Pts',(197.779475761273,-3.26381388226844,134.484996602939));
#20796=CARTESIAN_POINT('Ctrl Pts',(197.773684654833,-3.18694180385115,134.55174800559));
#20797=CARTESIAN_POINT('Ctrl Pts',(197.767893548393,-3.10818467377065,134.615970657462));
#20798=CARTESIAN_POINT('Ctrl Pts',(197.760119214274,-3.00245630392844,134.702187058218));
#20799=CARTESIAN_POINT('Ctrl Pts',(197.752344880155,-2.89297047802538,134.784137565104));
#20800=CARTESIAN_POINT('Ctrl Pts',(197.744570546035,-2.78010632827789,134.861476818264));
#20801=CARTESIAN_POINT('Ctrl Pts',(197.736805793088,-2.66738127350782,134.938720757708));
#20802=CARTESIAN_POINT('Ctrl Pts',(197.729041040141,-2.55128649839717,135.011364531943));
#20803=CARTESIAN_POINT('Ctrl Pts',(197.721276287194,-2.43223495821874,135.07910226713));
#20804=CARTESIAN_POINT('Ctrl Pts',(197.713519246309,-2.31330166170844,135.146772724244));
#20805=CARTESIAN_POINT('Ctrl Pts',(197.705762205424,-2.19141778190944,135.209546647202));
#20806=CARTESIAN_POINT('Ctrl Pts',(197.698005164539,-2.06702577581684,135.267161028139));
#20807=CARTESIAN_POINT('Ctrl Pts',(197.690253973299,-1.94272757470384,135.324731961623));
#20808=CARTESIAN_POINT('Ctrl Pts',(197.682502782059,-1.8159253653342,135.377150933938));
#20809=CARTESIAN_POINT('Ctrl Pts',(197.674751590819,-1.68708644647367,135.424200699714));
#20810=CARTESIAN_POINT('Ctrl Pts',(197.667003694042,-1.55830228759047,135.471230468085));
#20811=CARTESIAN_POINT('Ctrl Pts',(197.659255797265,-1.42748350741483,135.512895434921));
#20812=CARTESIAN_POINT('Ctrl Pts',(197.651507900488,-1.29511743474276,135.549026453294));
#20813=CARTESIAN_POINT('Ctrl Pts',(197.643761624403,-1.16277905019961,135.585149913837));
#20814=CARTESIAN_POINT('Ctrl Pts',(197.636015348319,-1.02889439386554,135.615741625526));
#20815=CARTESIAN_POINT('Ctrl Pts',(197.628269072235,-0.89396562727687,135.640682414112));
#20816=CARTESIAN_POINT('Ctrl Pts',(197.62052273897,-0.759035864674597,135.665623386805));
#20817=CARTESIAN_POINT('Ctrl Pts',(197.612776405705,-0.623062360890706,
135.684913282095));
#20818=CARTESIAN_POINT('Ctrl Pts',(197.605030072439,-0.486556739791109,
135.698484196049));
#20819=CARTESIAN_POINT('Ctrl Pts',(197.597282004436,-0.350020549204351,
135.712058149115));
#20820=CARTESIAN_POINT('Ctrl Pts',(197.589533936433,-0.212952393152231,
135.71991053368));
#20821=CARTESIAN_POINT('Ctrl Pts',(197.58178586843,-0.0758678779773515,
135.72202542188));
#20822=CARTESIAN_POINT('Ctrl Pts',(197.574029565689,0.061362332251699,135.724142557809));
#20823=CARTESIAN_POINT('Ctrl Pts',(197.566273262947,0.198608544793241,135.720510010164));
#20824=CARTESIAN_POINT('Ctrl Pts',(197.558516960205,0.335355735986595,135.711164016199));
#20825=CARTESIAN_POINT('Ctrl Pts',(197.550756517691,0.472175913273558,135.701813033997));
#20826=CARTESIAN_POINT('Ctrl Pts',(197.542996075176,0.608496150094301,135.686742572151));
#20827=CARTESIAN_POINT('Ctrl Pts',(197.535235632662,0.743808672534506,135.666040545447));
#20828=CARTESIAN_POINT('Ctrl Pts',(197.527462732397,0.879338410648007,135.645305286012));
#20829=CARTESIAN_POINT('Ctrl Pts',(197.519689832131,1.01385681788001,135.618920471637));
#20830=CARTESIAN_POINT('Ctrl Pts',(197.511916931866,1.14686752295984,135.587024932284));
#20831=CARTESIAN_POINT('Ctrl Pts',(197.504426596104,1.27504295387604,135.556288876127));
#20832=CARTESIAN_POINT('Ctrl Pts',(197.496936260342,1.40181810066686,135.52043588028));
#20833=CARTESIAN_POINT('Ctrl Pts',(197.48944592458,1.52676573916633,135.479632742289));
#20834=CARTESIAN_POINT('Ctrl Pts',(197.481671590461,1.65645080535675,135.437282540919));
#20835=CARTESIAN_POINT('Ctrl Pts',(197.473897256342,1.78457785099881,135.38946526551));
#20836=CARTESIAN_POINT('Ctrl Pts',(197.466122922223,1.91065138484321,135.336313215299));
#20837=CARTESIAN_POINT('Ctrl Pts',(197.458358169276,2.03656954432468,135.283226670239));
#20838=CARTESIAN_POINT('Ctrl Pts',(197.450593416329,2.16043887068706,135.22481858236));
#20839=CARTESIAN_POINT('Ctrl Pts',(197.442828663381,2.28177881119425,135.161271050348));
#20840=CARTESIAN_POINT('Ctrl Pts',(197.435071622496,2.40299823516199,135.097786634641));
#20841=CARTESIAN_POINT('Ctrl Pts',(197.427314581611,2.52169292860744,135.029173113332));
#20842=CARTESIAN_POINT('Ctrl Pts',(197.419557540726,2.63740245675027,134.955660575847));
#20843=CARTESIAN_POINT('Ctrl Pts',(197.411806349486,2.7530247274378,134.882203474739));
#20844=CARTESIAN_POINT('Ctrl Pts',(197.404055158246,2.86566598491015,134.803854919712));
#20845=CARTESIAN_POINT('Ctrl Pts',(197.396303967006,2.97489086808598,134.720890636023));
#20846=CARTESIAN_POINT('Ctrl Pts',(197.388556070229,3.08406932777271,134.637961614368));
#20847=CARTESIAN_POINT('Ctrl Pts',(197.380808173452,3.18983399049617,134.550421001924));
#20848=CARTESIAN_POINT('Ctrl Pts',(197.373060276675,3.2917791350376,134.458587374163));
#20849=CARTESIAN_POINT('Ctrl Pts',(197.365314000591,3.39370295485246,134.366772956017));
#20850=CARTESIAN_POINT('Ctrl Pts',(197.357567724507,3.49180855536177,134.270667570245));
#20851=CARTESIAN_POINT('Ctrl Pts',(197.349821448422,3.58572424131846,134.170629282976));
#20852=CARTESIAN_POINT('Ctrl Pts',(197.342075115157,3.67964062053938,134.070590257247));
#20853=CARTESIAN_POINT('Ctrl Pts',(197.334328781892,3.76936675589715,133.96661855713));
#20854=CARTESIAN_POINT('Ctrl Pts',(197.326582448626,3.85456897269458,133.859107922539));
#20855=CARTESIAN_POINT('Ctrl Pts',(197.318834380623,3.93979026993763,133.751573211687));
#20856=CARTESIAN_POINT('Ctrl Pts',(197.31108631262,4.02048538988445,133.640498295691));
#20857=CARTESIAN_POINT('Ctrl Pts',(197.303338244617,4.09636223415192,133.52630835937));
#20858=CARTESIAN_POINT('Ctrl Pts',(197.295581941876,4.17231972123249,133.411997060627));
#20859=CARTESIAN_POINT('Ctrl Pts',(197.287825639134,4.24344848632279,133.294564454268));
#20860=CARTESIAN_POINT('Ctrl Pts',(197.280069336392,4.3095006339843,133.17446343141));
#20861=CARTESIAN_POINT('Ctrl Pts',(197.272308893878,4.37558803566593,133.054298307018));
#20862=CARTESIAN_POINT('Ctrl Pts',(197.264548451364,4.43659324710592,132.931462278247));
#20863=CARTESIAN_POINT('Ctrl Pts',(197.256788008849,4.49231576929894,132.80643006976));
#20864=CARTESIAN_POINT('Ctrl Pts',(197.249015108584,4.54812774223136,132.681197148472));
#20865=CARTESIAN_POINT('Ctrl Pts',(197.241242208318,4.59863993554477,132.553761366054));
#20866=CARTESIAN_POINT('Ctrl Pts',(197.233469308053,4.64370085002127,132.424615374699));
#20867=CARTESIAN_POINT('Ctrl Pts',(197.225978972291,4.68712368675483,132.300164165429));
#20868=CARTESIAN_POINT('Ctrl Pts',(197.218488636529,4.72548460943441,132.174125223962));
#20869=CARTESIAN_POINT('Ctrl Pts',(197.210998300767,4.75869302446231,132.046948144235));
#20870=CARTESIAN_POINT('Ctrl Pts',(197.203223966648,4.79316054663953,131.914949106876));
#20871=CARTESIAN_POINT('Ctrl Pts',(197.195449632529,4.82218631642961,131.781305789271));
#20872=CARTESIAN_POINT('Ctrl Pts',(197.18767529841,4.84561381580234,131.646506573209));
#20873=CARTESIAN_POINT('Ctrl Pts',(197.179910545463,4.86901244287585,131.511873485134));
#20874=CARTESIAN_POINT('Ctrl Pts',(197.172145792516,4.88682646091603,131.376087714508));
#20875=CARTESIAN_POINT('Ctrl Pts',(197.164381039568,4.8989493242116,131.239651992747));
#20876=CARTESIAN_POINT('Ctrl Pts',(197.156623998683,4.91106014690847,131.103351780867));
#20877=CARTESIAN_POINT('Ctrl Pts',(197.148866957798,4.91749102928209,130.966403289417));
#20878=CARTESIAN_POINT('Ctrl Pts',(197.141109916913,4.91818667583652,130.829318264172));
#20879=CARTESIAN_POINT('Ctrl Pts',(197.133358725673,4.91888179779847,130.692336615812));
#20880=CARTESIAN_POINT('Ctrl Pts',(197.125607534433,4.91385029058759,130.555219027973));
#20881=CARTESIAN_POINT('Ctrl Pts',(197.117856343193,4.90308880637215,130.418480818499));
#20882=CARTESIAN_POINT('Ctrl Pts',(197.110108446416,4.89233189607456,130.281800726411));
#20883=CARTESIAN_POINT('Ctrl Pts',(197.102360549639,4.87584988319397,130.145500080927));
#20884=CARTESIAN_POINT('Ctrl Pts',(197.094612652862,4.85369149206835,130.010092424621));
#20885=CARTESIAN_POINT('Ctrl Pts',(197.086866376778,4.83153773600045,129.874713092679));
#20886=CARTESIAN_POINT('Ctrl Pts',(197.079120100694,4.80371002654195,129.740226763961));
#20887=CARTESIAN_POINT('Ctrl Pts',(197.071373824609,4.77030870450874,129.607139699695));
#20888=CARTESIAN_POINT('Ctrl Pts',(197.063627491344,4.7369071359146,129.474051653011));
#20889=CARTESIAN_POINT('Ctrl Pts',(197.055881158079,4.69793196781799,129.342363270595));
#20890=CARTESIAN_POINT('Ctrl Pts',(197.048134824813,4.65353410543624,129.212568108461));
#20891=CARTESIAN_POINT('Ctrl Pts',(197.04038675681,4.60912630046099,129.082743879601));
#20892=CARTESIAN_POINT('Ctrl Pts',(197.032638688807,4.55929351124709,128.954814084533));
#20893=CARTESIAN_POINT('Ctrl Pts',(197.024890620804,4.50423557151517,128.829254296682));
#20894=CARTESIAN_POINT('Ctrl Pts',(197.017134318063,4.44911911554975,128.703561062393));
#20895=CARTESIAN_POINT('Ctrl Pts',(197.009378015321,4.3887665729042,128.580243225664));
#20896=CARTESIAN_POINT('Ctrl Pts',(197.001621712579,4.32342498015975,128.459754146657));
#20897=CARTESIAN_POINT('Ctrl Pts',(196.993861270065,4.25804851263973,128.339200759));
#20898=CARTESIAN_POINT('Ctrl Pts',(196.986100827551,4.18767788965592,128.22147947287));
#20899=CARTESIAN_POINT('Ctrl Pts',(196.978340385036,4.11260413590295,128.107015574036));
#20900=CARTESIAN_POINT('Ctrl Pts',(196.970567484771,4.03740986709589,127.992367927591));
#20901=CARTESIAN_POINT('Ctrl Pts',(196.962794584506,3.95749760849355,127.880988435588));
#20902=CARTESIAN_POINT('Ctrl Pts',(196.95502168424,3.87319995331092,127.773270849154));
#20903=CARTESIAN_POINT('Ctrl Pts',(196.947531348478,3.79196673022726,127.669469068311));
#20904=CARTESIAN_POINT('Ctrl Pts',(196.940041012716,3.70666161488837,127.569067811088));
#20905=CARTESIAN_POINT('Ctrl Pts',(196.932550676954,3.61761389535537,127.472386312948));
#20906=CARTESIAN_POINT('Ctrl Pts',(196.924776342835,3.52518990447059,127.372039106421));
#20907=CARTESIAN_POINT('Ctrl Pts',(196.917002008716,3.42844113395928,127.275381426659));
#20908=CARTESIAN_POINT('Ctrl Pts',(196.909227674597,3.32769387143375,127.182808939));
#20909=CARTESIAN_POINT('Ctrl Pts',(196.90146292165,3.22707077090526,127.090350538659));
#20910=CARTESIAN_POINT('Ctrl Pts',(196.893698168703,3.12245926830746,127.001967574988));
#20911=CARTESIAN_POINT('Ctrl Pts',(196.885933415755,3.01422473525758,126.91802142652));
#20912=CARTESIAN_POINT('Ctrl Pts',(196.87817637487,2.90609770227194,126.83415865455));
#20913=CARTESIAN_POINT('Ctrl Pts',(196.870419333985,2.79435510683866,126.754724166296));
#20914=CARTESIAN_POINT('Ctrl Pts',(196.8626622931,2.67939760660565,126.680041094515));
#20915=CARTESIAN_POINT('Ctrl Pts',(196.85491110186,2.56452679671837,126.605414341821));
#20916=CARTESIAN_POINT('Ctrl Pts',(196.84715991062,2.44644623414905,126.535532085827));
#20917=CARTESIAN_POINT('Ctrl Pts',(196.83940871938,2.32558766080939,126.470675685041));
#20918=CARTESIAN_POINT('Ctrl Pts',(196.831660822603,2.20478045558657,126.405846849956));
#20919=CARTESIAN_POINT('Ctrl Pts',(196.823912925826,2.08119793174799,126.346039805974));
#20920=CARTESIAN_POINT('Ctrl Pts',(196.816165029049,1.95529848390204,126.291491142238));
#20921=CARTESIAN_POINT('Ctrl Pts',(196.808418752965,1.82942537150677,126.236953888906));
#20922=CARTESIAN_POINT('Ctrl Pts',(196.800672476881,1.70123665761377,126.187672983311));
#20923=CARTESIAN_POINT('Ctrl Pts',(196.792926200797,1.57121251079405,126.143837652445));
#20924=CARTESIAN_POINT('Ctrl Pts',(196.785179867531,1.44118740416556,126.100001997995));
#20925=CARTESIAN_POINT('Ctrl Pts',(196.777433534266,1.30932720805258,126.061612123386));
#20926=CARTESIAN_POINT('Ctrl Pts',(196.769687201001,1.17612873306436,126.028807846864));
#20927=CARTESIAN_POINT('Ctrl Pts',(196.761939132998,1.04290042920136,125.995996224052));
#20928=CARTESIAN_POINT('Ctrl Pts',(196.754191064995,0.908333629647398,125.968772781862));
#20929=CARTESIAN_POINT('Ctrl Pts',(196.746442996992,0.772936462800047,125.947226453579));
#20930=CARTESIAN_POINT('Ctrl Pts',(196.73868669425,0.63739539423235,125.925657225601));
#20931=CARTESIAN_POINT('Ctrl Pts',(196.730930391508,0.501022582156627,125.909777226043));
#20932=CARTESIAN_POINT('Ctrl Pts',(196.723174088766,0.364332980624142,125.899623668276));
#20933=CARTESIAN_POINT('Ctrl Pts',(196.715413646252,0.227570423735663,125.88946469125));
#20934=CARTESIAN_POINT('Ctrl Pts',(196.707653203738,0.0904911310544043,
125.88503825871));
#20935=CARTESIAN_POINT('Ctrl Pts',(196.699892761224,-0.0463897865020519,
125.886329400686));
#20936=CARTESIAN_POINT('Ctrl Pts',(196.692119860958,-0.183490437459122,
125.887622615317));
#20937=CARTESIAN_POINT('Ctrl Pts',(196.684346960693,-0.320391686252509,
125.894651725689));
#20938=CARTESIAN_POINT('Ctrl Pts',(196.676574060427,-0.456582484150821,
125.907349743812));
#20939=CARTESIAN_POINT('Ctrl Pts',(196.669083724665,-0.587822403502649,
125.919586156992));
#20940=CARTESIAN_POINT('Ctrl Pts',(196.661593388903,-0.718402323251377,
125.937086434526));
#20941=CARTESIAN_POINT('Ctrl Pts',(196.654103053141,-0.847875673318612,
125.959746091611));
#20942=CARTESIAN_POINT('Ctrl Pts',(196.646328719022,-0.982258044805317,
125.983264896481));
#20943=CARTESIAN_POINT('Ctrl Pts',(196.638554384903,-1.11587396195838,126.012416540273));
#20944=CARTESIAN_POINT('Ctrl Pts',(196.630780050784,-1.24821417389864,126.047140374758));
#20945=CARTESIAN_POINT('Ctrl Pts',(196.623015297837,-1.38039128835494,126.081821415221));
#20946=CARTESIAN_POINT('Ctrl Pts',(196.61525054489,-1.51129545125909,126.12206088437));
#20947=CARTESIAN_POINT('Ctrl Pts',(196.607485791943,-1.64042513233221,126.16774671864));
#20948=CARTESIAN_POINT('Ctrl Pts',(196.599728751058,-1.76942655998645,126.213387177096));
#20949=CARTESIAN_POINT('Ctrl Pts',(196.591971710173,-1.89665664695338,126.264463106153));
#20950=CARTESIAN_POINT('Ctrl Pts',(196.584214669288,-2.02162696724649,126.320812082332));
#20951=CARTESIAN_POINT('Ctrl Pts',(196.576463478048,-2.14650304644767,126.377118565309));
#20952=CARTESIAN_POINT('Ctrl Pts',(196.568712286808,-2.26912239593048,126.43869002048));
#20953=CARTESIAN_POINT('Ctrl Pts',(196.560961095568,-2.38901493376489,126.505315292293));
#20954=CARTESIAN_POINT('Ctrl Pts',(196.55321319879,-2.50885651407307,126.571912246589));
#20955=CARTESIAN_POINT('Ctrl Pts',(196.545465302013,-2.62597324680375,126.643558555793));
#20956=CARTESIAN_POINT('Ctrl Pts',(196.537717405236,-2.73991830932937,126.719996441748));
#20957=CARTESIAN_POINT('Ctrl Pts',(196.529971129152,-2.85383953700426,126.796418338546));
#20958=CARTESIAN_POINT('Ctrl Pts',(196.522224853068,-2.96459008963101,126.87762960081));
#20959=CARTESIAN_POINT('Ctrl Pts',(196.514478576984,-3.07175122234275,126.963328530934));
#20960=CARTESIAN_POINT('Ctrl Pts',(196.506732243719,-3.17891314609344,127.049028093668));
#20961=CARTESIAN_POINT('Ctrl Pts',(196.498985910453,-3.28248529172354,127.139215146181));
#20962=CARTESIAN_POINT('Ctrl Pts',(196.491239577188,-3.38208148791119,127.233547282816));
#20963=CARTESIAN_POINT('Ctrl Pts',(196.483491509185,-3.48169998797647,127.327900544479));
#20964=CARTESIAN_POINT('Ctrl Pts',(196.475743441182,-3.57734048303421,127.426400468601));
#20965=CARTESIAN_POINT('Ctrl Pts',(196.467995373179,-3.6686534951838,127.528667622981));
#20966=CARTESIAN_POINT('Ctrl Pts',(196.460239070437,-3.76006355588962,127.631043468109));
#20967=CARTESIAN_POINT('Ctrl Pts',(196.452482767696,-3.8471366852804,127.737194249536));
#20968=CARTESIAN_POINT('Ctrl Pts',(196.444726464954,-3.92956322945105,127.846706836569));
#20969=CARTESIAN_POINT('Ctrl Pts',(196.43696602244,-4.01203376715042,127.956277873767));
#20970=CARTESIAN_POINT('Ctrl Pts',(196.429205579925,-4.08985255625137,128.069213970078));
#20971=CARTESIAN_POINT('Ctrl Pts',(196.421445137411,-4.16275376138207,128.185073656464));
#20972=CARTESIAN_POINT('Ctrl Pts',(196.413672237146,-4.23577199399886,128.301119331103));
#20973=CARTESIAN_POINT('Ctrl Pts',(196.40589933688,-4.30385667334007,128.42009763481));
#20974=CARTESIAN_POINT('Ctrl Pts',(196.398126436615,-4.36678792397595,128.541542399167));
#20975=CARTESIAN_POINT('Ctrl Pts',(196.390636100853,-4.42743146513705,128.65857234044));
#20976=CARTESIAN_POINT('Ctrl Pts',(196.383145765091,-4.48328962222919,128.777892252615));
#20977=CARTESIAN_POINT('Ctrl Pts',(196.375655429329,-4.53420891924256,128.899069947048));
#20978=CARTESIAN_POINT('Ctrl Pts',(196.366995286457,-4.59308056412885,129.03917263136));
#20979=CARTESIAN_POINT('Ctrl Pts',(196.358335143585,-4.64550922581911,129.182135375472));
#20980=CARTESIAN_POINT('Ctrl Pts',(196.349675000714,-4.69123825435021,129.327381706606));
#20981=CARTESIAN_POINT('Ctrl Pts',(196.344648349249,-4.71778099061184,129.411687784913));
#20982=CARTESIAN_POINT('Ctrl Pts',(196.339621697785,-4.74206742463025,129.496762736058));
#20983=CARTESIAN_POINT('Ctrl Pts',(196.33459504632,-4.76405452823405,129.582490119308));
#20984=CARTESIAN_POINT('Ctrl Pts',(198.084936573762,-4.76405452823404,129.582490119308));
#20985=CARTESIAN_POINT('Ctrl Pts',(198.077162780964,-4.79809767465422,129.715223830524));
#20986=CARTESIAN_POINT('Ctrl Pts',(198.069388988166,-4.82655054116148,129.849229756449));
#20987=CARTESIAN_POINT('Ctrl Pts',(198.061615195367,-4.84934911569474,129.983997151406));
#20988=CARTESIAN_POINT('Ctrl Pts',(198.056523854313,-4.8642807354981,130.072261244428));
#20989=CARTESIAN_POINT('Ctrl Pts',(198.051432513259,-4.87678805849738,130.160851841391));
#20990=CARTESIAN_POINT('Ctrl Pts',(198.046341172205,-4.88686521477497,130.249625153473));
#20991=CARTESIAN_POINT('Ctrl Pts',(198.035847260134,-4.90763553654045,130.43259842543));
#20992=CARTESIAN_POINT('Ctrl Pts',(198.025353348062,-4.91813231630581,130.616759698695));
#20993=CARTESIAN_POINT('Ctrl Pts',(198.014859435991,-4.91824901604501,130.80124956111));
#20994=CARTESIAN_POINT('',(198.360140564038,-4.91824805313947,130.80873672198));
#20995=CARTESIAN_POINT('Ctrl Pts',(198.430216174721,-4.76405452823404,129.582490119308));
#20996=CARTESIAN_POINT('Ctrl Pts',(198.422577902284,-4.7976789144689,129.713591090917));
#20997=CARTESIAN_POINT('Ctrl Pts',(198.414939629846,-4.82587604532326,129.846036456349));
#20998=CARTESIAN_POINT('Ctrl Pts',(198.407301357409,-4.84855734705283,129.97933048791));
#20999=CARTESIAN_POINT('Ctrl Pts',(198.399441225181,-4.87189744550764,130.116496152261));
#21000=CARTESIAN_POINT('Ctrl Pts',(198.391581092952,-4.88939633379473,130.254560081246));
#21001=CARTESIAN_POINT('Ctrl Pts',(198.383720960724,-4.90101480488931,130.392976436106));
#21002=CARTESIAN_POINT('Ctrl Pts',(198.375860828495,-4.91263327598389,130.531392790965));
#21003=CARTESIAN_POINT('Ctrl Pts',(198.368000696266,-4.91837135341764,130.670161108681));
#21004=CARTESIAN_POINT('Ctrl Pts',(198.360140564038,-4.91824805313947,130.80873672198));
#21005=CARTESIAN_POINT('Ctrl Pts',(198.360140564008,-4.918248053139,130.808736722507));
#21006=CARTESIAN_POINT('Ctrl Pts',(198.348902089221,-4.91807175747449,131.006873152139));
#21007=CARTESIAN_POINT('Ctrl Pts',(198.337663614434,-4.90591901972274,131.20449843287));
#21008=CARTESIAN_POINT('Ctrl Pts',(198.326425139647,-4.8819937463978,131.400447962368));
#21009=CARTESIAN_POINT('Ctrl Pts',(198.319350026384,-4.86693173648915,131.523806793625));
#21010=CARTESIAN_POINT('Ctrl Pts',(198.312274913122,-4.84720485499847,131.646502289585));
#21011=CARTESIAN_POINT('Ctrl Pts',(198.30519979986,-4.82287271835716,131.768249514185));
#21012=CARTESIAN_POINT('Ctrl Pts',(198.297425465741,-4.79613587993932,131.902028800401));
#21013=CARTESIAN_POINT('Ctrl Pts',(198.289651131622,-4.76378621750837,132.0349066804));
#21014=CARTESIAN_POINT('Ctrl Pts',(198.281876797503,-4.7258965824454,132.166375505345));
#21015=CARTESIAN_POINT('Ctrl Pts',(198.274112044556,-4.68805364297136,132.297682306713));
#21016=CARTESIAN_POINT('Ctrl Pts',(198.266347291608,-4.64468442282832,132.427583136145));
#21017=CARTESIAN_POINT('Ctrl Pts',(198.258582538661,-4.59591298865343,132.555579297008));
#21018=CARTESIAN_POINT('Ctrl Pts',(198.250825497776,-4.54718999495454,132.683448330279));
#21019=CARTESIAN_POINT('Ctrl Pts',(198.243068456891,-4.49307560322901,132.809416096658));
#21020=CARTESIAN_POINT('Ctrl Pts',(198.235311416006,-4.43374391105737,132.932998208529));
#21021=CARTESIAN_POINT('Ctrl Pts',(198.227560224766,-4.37445696137642,133.056487126168));
#21022=CARTESIAN_POINT('Ctrl Pts',(198.219809033526,-4.30996071097418,133.177593619155));
#21023=CARTESIAN_POINT('Ctrl Pts',(198.212057842286,-4.24047753526522,133.295852808084));
#21024=CARTESIAN_POINT('Ctrl Pts',(198.204309945509,-4.17102389175934,133.414061733703));
#21025=CARTESIAN_POINT('Ctrl Pts',(198.196562048732,-4.09658773626326,133.529425425838));
#21026=CARTESIAN_POINT('Ctrl Pts',(198.188814151955,-4.01743749521107,133.6415033765));
#21027=CARTESIAN_POINT('Ctrl Pts',(198.181067875871,-3.93830381068304,133.753557882871));
#21028=CARTESIAN_POINT('Ctrl Pts',(198.173321599787,-3.85445822736556,133.862327695705));
#21029=CARTESIAN_POINT('Ctrl Pts',(198.165575323702,-3.76621240470724,133.967401430633));
#21030=CARTESIAN_POINT('Ctrl Pts',(198.157828990437,-3.67796593063832,134.072475941192));
#21031=CARTESIAN_POINT('Ctrl Pts',(198.150082657172,-3.58531940385276,134.173854020016));
#21032=CARTESIAN_POINT('Ctrl Pts',(198.142336323906,-3.48862439845058,134.271157823783));
#21033=CARTESIAN_POINT('Ctrl Pts',(198.134588255903,-3.3919077388725,134.368483418062));
#21034=CARTESIAN_POINT('Ctrl Pts',(198.126840187901,-3.29114107212411,134.461732644436));
#21035=CARTESIAN_POINT('Ctrl Pts',(198.119092119898,-3.18671210764418,134.550565230971));
#21036=CARTESIAN_POINT('Ctrl Pts',(198.111335817156,-3.08217215481793,134.639492229836));
#21037=CARTESIAN_POINT('Ctrl Pts',(198.103579514414,-2.97396242717541,134.723992958252));
#21038=CARTESIAN_POINT('Ctrl Pts',(198.095823211672,-2.86250336727734,134.803767765485));
#21039=CARTESIAN_POINT('Ctrl Pts',(198.088062769158,-2.75098481832297,134.883585150935));
#21040=CARTESIAN_POINT('Ctrl Pts',(198.080302326644,-2.63621380844923,134.958671375235));
#21041=CARTESIAN_POINT('Ctrl Pts',(198.07254188413,-2.51863805887903,135.028771273606));
#21042=CARTESIAN_POINT('Ctrl Pts',(198.064768983864,-2.40087356627779,135.098983702558));
#21043=CARTESIAN_POINT('Ctrl Pts',(198.056996083599,-2.2802956808095,135.164193623964));
#21044=CARTESIAN_POINT('Ctrl Pts',(198.049223183333,-2.15737571304909,135.22419241247));
#21045=CARTESIAN_POINT('Ctrl Pts',(198.041732847571,-2.03892419573207,135.282010093887));
#21046=CARTESIAN_POINT('Ctrl Pts',(198.034242511809,-1.91829820299034,135.33498881632));
#21047=CARTESIAN_POINT('Ctrl Pts',(198.026752176047,-1.79593348200914,135.382985519291));
#21048=CARTESIAN_POINT('Ctrl Pts',(198.018977841928,-1.66892926544145,135.432802031844));
#21049=CARTESIAN_POINT('Ctrl Pts',(198.011203507809,-1.53964955897284,135.477409084513));
#21050=CARTESIAN_POINT('Ctrl Pts',(198.00342917369,-1.40856083989839,135.516593572631));
#21051=CARTESIAN_POINT('Ctrl Pts',(197.995664420743,-1.27763367595456,135.555729769371));
#21052=CARTESIAN_POINT('Ctrl Pts',(197.987899667796,-1.14490230633097,135.589456587496));
#21053=CARTESIAN_POINT('Ctrl Pts',(197.980134914848,-1.01085335967749,135.617608850073));
#21054=CARTESIAN_POINT('Ctrl Pts',(197.972377873963,-0.876937552327542,
135.645733151425));
#21055=CARTESIAN_POINT('Ctrl Pts',(197.964620833078,-0.741707152334974,
135.668293835729));
#21056=CARTESIAN_POINT('Ctrl Pts',(197.956863792193,-0.605663792714778,
135.685175552871));
#21057=CARTESIAN_POINT('Ctrl Pts',(197.949112600953,-0.469723024450324,
135.702044539379));
#21058=CARTESIAN_POINT('Ctrl Pts',(197.941361409713,-0.332970903234851,
135.713243034937));
#21059=CARTESIAN_POINT('Ctrl Pts',(197.933610218473,-0.195918744622959,
135.718706851604));
#21060=CARTESIAN_POINT('Ctrl Pts',(197.925862321696,-0.0589248368344638,
135.724168346004));
#21061=CARTESIAN_POINT('Ctrl Pts',(197.918114424919,0.0783684648781298,
135.723899993757));
#21062=CARTESIAN_POINT('Ctrl Pts',(197.910366528142,0.215445457623812,135.717889524298));
#21063=CARTESIAN_POINT('Ctrl Pts',(197.902620252058,0.352493776817673,135.711880312099));
#21064=CARTESIAN_POINT('Ctrl Pts',(197.894873975974,0.489325486701273,135.700131388911));
#21065=CARTESIAN_POINT('Ctrl Pts',(197.88712769989,0.625426018410143,135.682682599354));
#21066=CARTESIAN_POINT('Ctrl Pts',(197.879381366624,0.761527554782069,135.665233680994));
#21067=CARTESIAN_POINT('Ctrl Pts',(197.871635033359,0.896897514417944,135.642084862025));
#21068=CARTESIAN_POINT('Ctrl Pts',(197.863888700093,1.03102797264083,135.613327698149));
#21069=CARTESIAN_POINT('Ctrl Pts',(197.856140632091,1.16518846844996,135.584564094306));
#21070=CARTESIAN_POINT('Ctrl Pts',(197.848392564088,1.29810852829368,135.550189728304));
#21071=CARTESIAN_POINT('Ctrl Pts',(197.840644496085,1.42929230533578,135.510346865783));
#21072=CARTESIAN_POINT('Ctrl Pts',(197.832888193343,1.56061550605723,135.470461657794));
#21073=CARTESIAN_POINT('Ctrl Pts',(197.825131890601,1.69019836301931,135.425096457024));
#21074=CARTESIAN_POINT('Ctrl Pts',(197.817375587859,1.81756151209824,135.374443025164));
#21075=CARTESIAN_POINT('Ctrl Pts',(197.809615145345,1.94499263872476,135.323762558043));
#21076=CARTESIAN_POINT('Ctrl Pts',(197.801854702831,2.0702013400551,135.267788395269));
#21077=CARTESIAN_POINT('Ctrl Pts',(197.794094260316,2.19273093447755,135.206759294593));
#21078=CARTESIAN_POINT('Ctrl Pts',(197.786321360051,2.3154572242826,135.145632224586));
#21079=CARTESIAN_POINT('Ctrl Pts',(197.778548459786,2.43549547037675,135.079434189959));
#21080=CARTESIAN_POINT('Ctrl Pts',(197.77077555952,2.55241539546258,135.008448950547));
#21081=CARTESIAN_POINT('Ctrl Pts',(197.763285223758,2.66508498676848,134.940044203388));
#21082=CARTESIAN_POINT('Ctrl Pts',(197.755794887996,2.77485878191613,134.867194432942));
#21083=CARTESIAN_POINT('Ctrl Pts',(197.748304552234,2.88138088807747,134.790188917973));
#21084=CARTESIAN_POINT('Ctrl Pts',(197.740530218115,2.99194181227019,134.710263715498));
#21085=CARTESIAN_POINT('Ctrl Pts',(197.732755883996,3.09934982819655,134.62560823861));
#21086=CARTESIAN_POINT('Ctrl Pts',(197.724981549877,3.20317350249298,134.53649975959));
#21087=CARTESIAN_POINT('Ctrl Pts',(197.71721679693,3.3068692233898,134.447501098806));
#21088=CARTESIAN_POINT('Ctrl Pts',(197.709452043983,3.40698909809778,134.354060607414));
#21089=CARTESIAN_POINT('Ctrl Pts',(197.701687291035,3.50313112391044,134.256498417711));
#21090=CARTESIAN_POINT('Ctrl Pts',(197.69393025015,3.5991776601077,134.15903312815));
#21091=CARTESIAN_POINT('Ctrl Pts',(197.686173209265,3.6912539371464,134.057454563654));
#21092=CARTESIAN_POINT('Ctrl Pts',(197.67841616838,3.77899176281173,133.952122412731));
#21093=CARTESIAN_POINT('Ctrl Pts',(197.67066497714,3.86666342470019,133.846869693603));
#21094=CARTESIAN_POINT('Ctrl Pts',(197.6629137859,3.95000289804419,133.737869321391));
#21095=CARTESIAN_POINT('Ctrl Pts',(197.65516259466,4.02867980116461,133.625516785202));
#21096=CARTESIAN_POINT('Ctrl Pts',(197.647414697883,4.10732326450247,133.513212001837));
#21097=CARTESIAN_POINT('Ctrl Pts',(197.639666801106,4.18130787530829,133.397558207814));
#21098=CARTESIAN_POINT('Ctrl Pts',(197.631918904329,4.25034455999749,133.278982646038));
#21099=CARTESIAN_POINT('Ctrl Pts',(197.624172628245,4.31936680370051,133.160431887714));
#21100=CARTESIAN_POINT('Ctrl Pts',(197.616426352161,4.38344298336774,133.038960914946));
#21101=CARTESIAN_POINT('Ctrl Pts',(197.608680076076,4.4423284843672,132.915024186087));
#21102=CARTESIAN_POINT('Ctrl Pts',(197.600933742811,4.50121442004603,132.791086542354));
#21103=CARTESIAN_POINT('Ctrl Pts',(197.593187409546,4.55490943281703,132.664683459342));
#21104=CARTESIAN_POINT('Ctrl Pts',(197.58544107628,4.60321600539095,132.536291756559));
#21105=CARTESIAN_POINT('Ctrl Pts',(197.577693008277,4.65153339588684,132.407871301344));
#21106=CARTESIAN_POINT('Ctrl Pts',(197.569944940274,4.69445980733516,132.277461706041));
#21107=CARTESIAN_POINT('Ctrl Pts',(197.562196872271,4.73184691452124,132.14555703869));
#21108=CARTESIAN_POINT('Ctrl Pts',(197.55444056953,4.76927375716978,132.013512181488));
#21109=CARTESIAN_POINT('Ctrl Pts',(197.546684266788,4.80114942837765,131.879969454826));
#21110=CARTESIAN_POINT('Ctrl Pts',(197.538927964046,4.82737615466953,131.745435813195));
#21111=CARTESIAN_POINT('Ctrl Pts',(197.531167521532,4.85361687895492,131.610830366909));
#21112=CARTESIAN_POINT('Ctrl Pts',(197.523407079018,4.87420259200423,131.475233338161));
#21113=CARTESIAN_POINT('Ctrl Pts',(197.515646636503,4.88908731990802,131.33915800052));
#21114=CARTESIAN_POINT('Ctrl Pts',(197.507873736238,4.90399594209845,131.202864222668));
#21115=CARTESIAN_POINT('Ctrl Pts',(197.500100835973,4.91318526485212,131.066090991876));
#21116=CARTESIAN_POINT('Ctrl Pts',(197.492327935707,4.91666144796523,130.929353691744));
#21117=CARTESIAN_POINT('Ctrl Pts',(197.484837599945,4.9200112630662,130.797587136892));
#21118=CARTESIAN_POINT('Ctrl Pts',(197.477347264183,4.91805610562799,130.665854253699));
#21119=CARTESIAN_POINT('Ctrl Pts',(197.469856928421,4.91084698530234,130.534610827118));
#21120=CARTESIAN_POINT('Ctrl Pts',(197.462082594302,4.90336452898838,130.398391266127));
#21121=CARTESIAN_POINT('Ctrl Pts',(197.454308260183,4.89019813490943,130.262267507292));
#21122=CARTESIAN_POINT('Ctrl Pts',(197.446533926064,4.87134787981786,130.126752400162));
#21123=CARTESIAN_POINT('Ctrl Pts',(197.438769173117,4.852520855981,129.991404303289));
#21124=CARTESIAN_POINT('Ctrl Pts',(197.43100442017,4.82802396204446,129.856663749147));
#21125=CARTESIAN_POINT('Ctrl Pts',(197.423239667222,4.79790924209346,129.723041993323));
#21126=CARTESIAN_POINT('Ctrl Pts',(197.415482626337,4.76782443250686,129.589552952511));
#21127=CARTESIAN_POINT('Ctrl Pts',(197.407725585452,4.73213298616931,129.457180877599));
#21128=CARTESIAN_POINT('Ctrl Pts',(197.399968544567,4.69093850232438,129.326429959548));
#21129=CARTESIAN_POINT('Ctrl Pts',(197.392217353327,4.64977508356018,129.195777641781));
#21130=CARTESIAN_POINT('Ctrl Pts',(197.384466162087,4.60311700438922,129.066744418897));
#21131=CARTESIAN_POINT('Ctrl Pts',(197.376714970847,4.55111842163095,128.939822021883));
#21132=CARTESIAN_POINT('Ctrl Pts',(197.36896707407,4.49914193965744,128.812953570273));
#21133=CARTESIAN_POINT('Ctrl Pts',(197.361219177293,4.44182961657508,128.688194521179));
#21134=CARTESIAN_POINT('Ctrl Pts',(197.353471280516,4.37938465260795,128.56601901562));
#21135=CARTESIAN_POINT('Ctrl Pts',(197.345725004432,4.3169527507811,128.443869066543));
#21136=CARTESIAN_POINT('Ctrl Pts',(197.337978728348,4.24939052141315,128.324301933984));
#21137=CARTESIAN_POINT('Ctrl Pts',(197.330232452263,4.17694809300133,128.207769064997));
#21138=CARTESIAN_POINT('Ctrl Pts',(197.322486118998,4.10450512983598,128.091235335791));
#21139=CARTESIAN_POINT('Ctrl Pts',(197.314739785733,4.02718210215263,127.97773624689));
#21140=CARTESIAN_POINT('Ctrl Pts',(197.306993452467,3.9452734087893,127.867695707775));
#21141=CARTESIAN_POINT('Ctrl Pts',(197.299245384464,3.86334637254203,127.757630525843));
#21142=CARTESIAN_POINT('Ctrl Pts',(197.291497316461,3.77683186054576,127.65102574846));
#21143=CARTESIAN_POINT('Ctrl Pts',(197.283749248458,3.68606537283357,127.548273221672));
#21144=CARTESIAN_POINT('Ctrl Pts',(197.275992945717,3.59520241741809,127.445411488276));
#21145=CARTESIAN_POINT('Ctrl Pts',(197.268236642975,3.50007871824481,127.3464104776));
#21146=CARTESIAN_POINT('Ctrl Pts',(197.260480340233,3.4010679415342,127.251626470523));
#21147=CARTESIAN_POINT('Ctrl Pts',(197.252719897719,3.30200431979083,127.156791874367));
#21148=CARTESIAN_POINT('Ctrl Pts',(197.244959455205,3.19904977993481,127.066179024781));
#21149=CARTESIAN_POINT('Ctrl Pts',(197.23719901269,3.09261130353576,126.980104037818));
#21150=CARTESIAN_POINT('Ctrl Pts',(197.229426112425,2.98600196264525,126.893890875646));
#21151=CARTESIAN_POINT('Ctrl Pts',(197.22165321216,2.87589782337121,126.812230366043));
#21152=CARTESIAN_POINT('Ctrl Pts',(197.213880311894,2.76273582205164,126.735395904024));
#21153=CARTESIAN_POINT('Ctrl Pts',(197.206389976132,2.65368754451797,126.661354568233));
#21154=CARTESIAN_POINT('Ctrl Pts',(197.19889964037,2.54180012866534,126.591794656438));
#21155=CARTESIAN_POINT('Ctrl Pts',(197.191409304608,2.4274846112473,126.526919615675));
#21156=CARTESIAN_POINT('Ctrl Pts',(197.183634970489,2.30883478624092,126.459584818023));
#21157=CARTESIAN_POINT('Ctrl Pts',(197.17586063637,2.18719325510115,126.397083861596));
#21158=CARTESIAN_POINT('Ctrl Pts',(197.168086302251,2.06299153416462,126.339693889526));
#21159=CARTESIAN_POINT('Ctrl Pts',(197.160321549304,1.93894288074894,126.282374645468));
#21160=CARTESIAN_POINT('Ctrl Pts',(197.152556796357,1.81234066695579,126.230154015391));
#21161=CARTESIAN_POINT('Ctrl Pts',(197.144792043409,1.68364315769026,126.183264559263));
#21162=CARTESIAN_POINT('Ctrl Pts',(197.137035002524,1.55507347260519,126.136421674404));
#21163=CARTESIAN_POINT('Ctrl Pts',(197.129277961639,1.42441299845145,126.094899559184));
#21164=CARTESIAN_POINT('Ctrl Pts',(197.121520920754,1.29214192328729,126.058883580156));
#21165=CARTESIAN_POINT('Ctrl Pts',(197.113769729514,1.15997059476984,126.022894761058));
#21166=CARTESIAN_POINT('Ctrl Pts',(197.106018538274,1.02619145846807,125.99240391571));
#21167=CARTESIAN_POINT('Ctrl Pts',(197.098267347034,0.891301547113867,125.967547140222));
#21168=CARTESIAN_POINT('Ctrl Pts',(197.090519450257,0.756468967570347,125.942700929528));
#21169=CARTESIAN_POINT('Ctrl Pts',(197.08277155348,0.620526935649892,125.923484096662));
#21170=CARTESIAN_POINT('Ctrl Pts',(197.075023656703,0.483984194306158,125.909981968323));
#21171=CARTESIAN_POINT('Ctrl Pts',(197.067277380619,0.347470014760427,125.896482664339));
#21172=CARTESIAN_POINT('Ctrl Pts',(197.059531104535,0.210355764548132,125.88869572563));
#21173=CARTESIAN_POINT('Ctrl Pts',(197.051784828451,0.0731564594262019,
125.886654730168));
#21174=CARTESIAN_POINT('Ctrl Pts',(197.044038495185,-0.0640438584697734,
125.884613719641));
#21175=CARTESIAN_POINT('Ctrl Pts',(197.03629216192,-0.201328841606274,125.888318742812));
#21176=CARTESIAN_POINT('Ctrl Pts',(197.028545828654,-0.338182713167988,
125.897751247032));
#21177=CARTESIAN_POINT('Ctrl Pts',(197.020797760651,-0.475067232205337,
125.907185863595));
#21178=CARTESIAN_POINT('Ctrl Pts',(197.013049692649,-0.611520057590418,
125.922350486614));
#21179=CARTESIAN_POINT('Ctrl Pts',(197.005301624646,-0.747030172182732,
125.943174652768));
#21180=CARTESIAN_POINT('Ctrl Pts',(196.997545321904,-0.882684308537553,
125.964020951094));
#21181=CARTESIAN_POINT('Ctrl Pts',(196.989789019162,-1.01739334560279,125.990538748746));
#21182=CARTESIAN_POINT('Ctrl Pts',(196.98203271642,-1.15065555846418,126.022606248271));
#21183=CARTESIAN_POINT('Ctrl Pts',(196.974272273906,-1.28398889738112,126.054690863185));
#21184=CARTESIAN_POINT('Ctrl Pts',(196.966511831392,-1.41587349762368,126.092330974847));
#21185=CARTESIAN_POINT('Ctrl Pts',(196.958751388877,-1.5458234183235,126.135355046584));
#21186=CARTESIAN_POINT('Ctrl Pts',(196.950978488612,-1.67598194617242,126.17844818438));
#21187=CARTESIAN_POINT('Ctrl Pts',(196.943205588347,-1.80419922236758,126.226942414954));
#21188=CARTESIAN_POINT('Ctrl Pts',(196.935432688081,-1.93000905717825,126.280617908071));
#21189=CARTESIAN_POINT('Ctrl Pts',(196.927942352319,-2.05124538759802,126.332342161813));
#21190=CARTESIAN_POINT('Ctrl Pts',(196.920452016557,-2.17024599270099,126.388877382166));
#21191=CARTESIAN_POINT('Ctrl Pts',(196.912961680795,-2.28661753132807,126.44998772036));
#21192=CARTESIAN_POINT('Ctrl Pts',(196.905186437551,-2.40741545658494,126.513422492751));
#21193=CARTESIAN_POINT('Ctrl Pts',(196.897411194306,-2.52576305120591,126.581988282265));
#21194=CARTESIAN_POINT('Ctrl Pts',(196.889635951062,-2.6411937391818,126.655471766969));
#21195=CARTESIAN_POINT('Ctrl Pts',(196.881870490011,-2.75647920144334,126.728862800595));
#21196=CARTESIAN_POINT('Ctrl Pts',(196.874105028959,-2.86885473277439,126.807159009799));
#21197=CARTESIAN_POINT('Ctrl Pts',(196.866339567908,-2.97787685313513,126.890100469075));
#21198=CARTESIAN_POINT('Ctrl Pts',(196.858583393819,-3.08676859046736,126.972942736017));
#21199=CARTESIAN_POINT('Ctrl Pts',(196.85082721973,-3.19231459493436,127.060418953556));
#21200=CARTESIAN_POINT('Ctrl Pts',(196.843071045641,-3.294099502712,127.152225416244));
#21201=CARTESIAN_POINT('Ctrl Pts',(196.835320138421,-3.39581529293819,127.243969537295));
#21202=CARTESIAN_POINT('Ctrl Pts',(196.827569231201,-3.49377477829833,127.340037793094));
#21203=CARTESIAN_POINT('Ctrl Pts',(196.819818323981,-3.58759484370538,127.440085613955));
#21204=CARTESIAN_POINT('Ctrl Pts',(196.812071001449,-3.6813715186174,127.54008716407));
#21205=CARTESIAN_POINT('Ctrl Pts',(196.804323678917,-3.77101231623895,127.644064332384));
#21206=CARTESIAN_POINT('Ctrl Pts',(196.796576356385,-3.85617053877141,127.751635304274));
#21207=CARTESIAN_POINT('Ctrl Pts',(196.788830939126,-3.94130781864133,127.859179821613));
#21208=CARTESIAN_POINT('Ctrl Pts',(196.781085521866,-4.02196447570508,127.970316076795));
#21209=CARTESIAN_POINT('Ctrl Pts',(196.773340104606,-4.09783398032599,128.084629062396));
#21210=CARTESIAN_POINT('Ctrl Pts',(196.765580754941,-4.17383995850953,128.19914767344));
#21211=CARTESIAN_POINT('Ctrl Pts',(196.757821405275,-4.24504131628586,128.316854134644));
#21212=CARTESIAN_POINT('Ctrl Pts',(196.75006205561,-4.31117357625514,128.437302219913));
#21213=CARTESIAN_POINT('Ctrl Pts',(196.742313049751,-4.37721767686617,128.557589738676));
#21214=CARTESIAN_POINT('Ctrl Pts',(196.734564043892,-4.43820602078034,128.680611220613));
#21215=CARTESIAN_POINT('Ctrl Pts',(196.726815038034,-4.49392167184312,128.805898441332));
#21216=CARTESIAN_POINT('Ctrl Pts',(196.719050516465,-4.54974888145534,128.931436522632));
#21217=CARTESIAN_POINT('Ctrl Pts',(196.711285994897,-4.60028211429378,129.059249060427));
#21218=CARTESIAN_POINT('Ctrl Pts',(196.703521473329,-4.64535222085451,129.188846517751));
#21219=CARTESIAN_POINT('Ctrl Pts',(196.69575695176,-4.69042232741525,129.318443975074));
#21220=CARTESIAN_POINT('Ctrl Pts',(196.687992430192,-4.73002922227267,129.449825967771));
#21221=CARTESIAN_POINT('Ctrl Pts',(196.680227908624,-4.76405452823405,129.582490119308));
#21222=CARTESIAN_POINT('Origin',(213.235140564004,0.,130.804360617566));
#21223=CARTESIAN_POINT('',(194.584773235637,-4.76405452823404,129.582490119308));
#21224=CARTESIAN_POINT('',(194.92989654745,-4.76405452823404,129.582490119308));
#21225=CARTESIAN_POINT('',(213.235140564004,-4.76405452823405,129.582490119308));
#21226=CARTESIAN_POINT('',(196.264859436042,-4.91824930178245,130.801739927489));
#21227=CARTESIAN_POINT('Ctrl Pts',(196.264859435991,-4.91824930178293,130.801739928394));
#21228=CARTESIAN_POINT('Ctrl Pts',(196.257012721372,-4.9183234709409,130.940933241881));
#21229=CARTESIAN_POINT('Ctrl Pts',(196.249166006753,-4.91248424618416,131.080125087051));
#21230=CARTESIAN_POINT('Ctrl Pts',(196.241319292134,-4.90075854751751,131.218786390696));
#21231=CARTESIAN_POINT('Ctrl Pts',(196.233470637992,-4.88902995053467,131.357481968145));
#21232=CARTESIAN_POINT('Ctrl Pts',(196.22562198385,-4.87141201293207,131.495646367384));
#21233=CARTESIAN_POINT('Ctrl Pts',(196.217773329708,-4.84798352666506,131.632755926392));
#21234=CARTESIAN_POINT('Ctrl Pts',(196.209921209237,-4.82454469329633,131.769926039314));
#21235=CARTESIAN_POINT('Ctrl Pts',(196.202069088767,-4.79529026322915,131.906040012911));
#21236=CARTESIAN_POINT('Ctrl Pts',(196.194216968297,-4.76035005680923,132.040584868718));
#21237=CARTESIAN_POINT('Ctrl Pts',(196.186132871399,-4.72437760638351,132.179104604331));
#21238=CARTESIAN_POINT('Ctrl Pts',(196.1780487745,-4.68237835041523,132.315960659695));
#21239=CARTESIAN_POINT('Ctrl Pts',(196.169964677602,-4.63454850944733,132.450611866944));
#21240=CARTESIAN_POINT('Ctrl Pts',(196.162096228248,-4.58799455469389,132.581671182278));
#21241=CARTESIAN_POINT('Ctrl Pts',(196.154227778895,-4.53591733384053,132.710641463661));
#21242=CARTESIAN_POINT('Ctrl Pts',(196.146359329542,-4.47854577483177,132.837046231535));
#21243=CARTESIAN_POINT('Ctrl Pts',(196.138167408871,-4.41881567566367,132.968647489212));
#21244=CARTESIAN_POINT('Ctrl Pts',(196.1299754882,-4.35334689846171,133.097467395895));
#21245=CARTESIAN_POINT('Ctrl Pts',(196.121783567529,-4.2824489092148,133.222999574183));
#21246=CARTESIAN_POINT('Ctrl Pts',(196.113591646858,-4.21155091996789,133.348531752471));
#21247=CARTESIAN_POINT('Ctrl Pts',(196.105399726187,-4.13522401973526,133.470775856601));
#21248=CARTESIAN_POINT('Ctrl Pts',(196.097207805515,-4.05382567680301,133.589262850068));
#21249=CARTESIAN_POINT('Ctrl Pts',(196.089433471396,-3.97657664814305,133.701709919927));
#21250=CARTESIAN_POINT('Ctrl Pts',(196.081659137277,-3.89452304616624,133.811118503023));
#21251=CARTESIAN_POINT('Ctrl Pts',(196.073884803158,-3.80793171009603,133.917050636464));
#21252=CARTESIAN_POINT('Ctrl Pts',(196.066120050211,-3.72144709010858,134.022852218017));
#21253=CARTESIAN_POINT('Ctrl Pts',(196.058355297264,-3.63043610820173,134.125185574825));
#21254=CARTESIAN_POINT('Ctrl Pts',(196.050590544317,-3.53520915752512,134.223641137654));
#21255=CARTESIAN_POINT('Ctrl Pts',(196.042833503432,-3.44007678759841,134.32199891303));
#21256=CARTESIAN_POINT('Ctrl Pts',(196.035076462547,-3.34073705198568,134.41648627984));
#21257=CARTESIAN_POINT('Ctrl Pts',(196.027319421662,-3.2375407000163,134.506726520369));
#21258=CARTESIAN_POINT('Ctrl Pts',(196.019568230422,-3.13442216921906,134.59689871003));
#21259=CARTESIAN_POINT('Ctrl Pts',(196.011817039182,-3.02745310398911,134.68282989205));
#21260=CARTESIAN_POINT('Ctrl Pts',(196.004065847942,-2.91702095129357,134.764180289245));
#21261=CARTESIAN_POINT('Ctrl Pts',(195.996317951164,-2.8066357352085,134.845496110351));
#21262=CARTESIAN_POINT('Ctrl Pts',(195.988570054387,-2.69279067328169,134.92223478758));
#21263=CARTESIAN_POINT('Ctrl Pts',(195.98082215761,-2.57590594841546,134.994097077944));
#21264=CARTESIAN_POINT('Ctrl Pts',(195.973075881526,-2.45904567331386,135.065944336265));
#21265=CARTESIAN_POINT('Ctrl Pts',(195.965329605442,-2.3391473328201,135.13291703199));
#21266=CARTESIAN_POINT('Ctrl Pts',(195.957583329358,-2.2166593843348,135.194759715181));
#21267=CARTESIAN_POINT('Ctrl Pts',(195.949836996093,-2.09417053167117,135.256602854881));
#21268=CARTESIAN_POINT('Ctrl Pts',(195.942090662827,-1.96909238187651,135.313315730276));
#21269=CARTESIAN_POINT('Ctrl Pts',(195.934344329562,-1.84189687727761,135.364689438602));
#21270=CARTESIAN_POINT('Ctrl Pts',(195.926596261559,-1.7146728881277,135.416074651714));
#21271=CARTESIAN_POINT('Ctrl Pts',(195.918848193556,-1.58533096307996,135.462118172125));
#21272=CARTESIAN_POINT('Ctrl Pts',(195.911100125553,-1.45436146849866,135.502659861063));
#21273=CARTESIAN_POINT('Ctrl Pts',(195.903343822811,-1.32325277797986,135.543244638191));
#21274=CARTESIAN_POINT('Ctrl Pts',(195.895587520069,-1.19051343654138,135.578315787215));
#21275=CARTESIAN_POINT('Ctrl Pts',(195.887831217328,-1.0566479063914,135.607763397306));
#21276=CARTESIAN_POINT('Ctrl Pts',(195.880070774813,-0.922710928177224,
135.637226724474));
#21277=CARTESIAN_POINT('Ctrl Pts',(195.872310332299,-0.787646948375374,
135.661060464155));
#21278=CARTESIAN_POINT('Ctrl Pts',(195.864549889785,-0.651967989498143,
135.679206338527));
#21279=CARTESIAN_POINT('Ctrl Pts',(195.85677698952,-0.516071226711214,135.697381342267));
#21280=CARTESIAN_POINT('Ctrl Pts',(195.849004089254,-0.379557901639337,
135.709850199137));
#21281=CARTESIAN_POINT('Ctrl Pts',(195.841231188989,-0.242943397281255,
135.716606699372));
#21282=CARTESIAN_POINT('Ctrl Pts',(195.833740853227,-0.111295174267542,
135.723117583805));
#21283=CARTESIAN_POINT('Ctrl Pts',(195.826250517465,0.0204466914981448,
135.724324215373));
#21284=CARTESIAN_POINT('Ctrl Pts',(195.818760181703,0.151825322225019,135.720266651456));
#21285=CARTESIAN_POINT('Ctrl Pts',(195.810985847584,0.288185213667395,135.716055243769));
#21286=CARTESIAN_POINT('Ctrl Pts',(195.803211513465,0.424585729377166,135.706159236164));
#21287=CARTESIAN_POINT('Ctrl Pts',(195.795437179345,0.560514165651644,135.690566398395));
#21288=CARTESIAN_POINT('Ctrl Pts',(195.787672426398,0.69627508227663,135.674992777405));
#21289=CARTESIAN_POINT('Ctrl Pts',(195.779907673451,0.831564692377237,135.653736339747));
#21290=CARTESIAN_POINT('Ctrl Pts',(195.772142920504,0.96587063867978,135.626836845795));
#21291=CARTESIAN_POINT('Ctrl Pts',(195.764385879619,1.10004319042296,135.5999640688));
#21292=CARTESIAN_POINT('Ctrl Pts',(195.756628838734,1.23323364174855,135.567459465525));
#21293=CARTESIAN_POINT('Ctrl Pts',(195.748871797849,1.36493546079199,135.529414506187));
#21294=CARTESIAN_POINT('Ctrl Pts',(195.741120606609,1.496537962469,135.491398236849));
#21295=CARTESIAN_POINT('Ctrl Pts',(195.733369415369,1.62665369222182,135.447850035617));
#21296=CARTESIAN_POINT('Ctrl Pts',(195.725618224129,1.75478736133172,135.398912214731));
#21297=CARTESIAN_POINT('Ctrl Pts',(195.717870327352,1.88286657021454,135.349995193724));
#21298=CARTESIAN_POINT('Ctrl Pts',(195.710122430575,2.00896502951187,135.295693248354));
#21299=CARTESIAN_POINT('Ctrl Pts',(195.702374533797,2.13260385849881,135.236198142252));
#21300=CARTESIAN_POINT('Ctrl Pts',(195.694628257713,2.25621682490795,135.176715481244));
#21301=CARTESIAN_POINT('Ctrl Pts',(195.686881981629,2.37737083230292,135.112041989627));
#21302=CARTESIAN_POINT('Ctrl Pts',(195.679135705545,2.49560856123834,135.042416890384));
#21303=CARTESIAN_POINT('Ctrl Pts',(195.67138937228,2.61384716297782,134.972791277185));
#21304=CARTESIAN_POINT('Ctrl Pts',(195.663643039014,2.72916910640684,134.898214181805));
#21305=CARTESIAN_POINT('Ctrl Pts',(195.655896705749,2.84114353935931,134.818969745645));
#21306=CARTESIAN_POINT('Ctrl Pts',(195.648148637746,2.95314304820954,134.739707563244));
#21307=CARTESIAN_POINT('Ctrl Pts',(195.640400569743,3.06179323579177,134.655776186005));
#21308=CARTESIAN_POINT('Ctrl Pts',(195.63265250174,3.16669431782458,134.567501614122));
#21309=CARTESIAN_POINT('Ctrl Pts',(195.624896198998,3.27170688997588,134.479133222973));
#21310=CARTESIAN_POINT('Ctrl Pts',(195.617139896256,3.37296209730263,134.386412668355));
#21311=CARTESIAN_POINT('Ctrl Pts',(195.609383593514,3.47009479456587,134.289704959123));
#21312=CARTESIAN_POINT('Ctrl Pts',(195.601623151,3.56727933447434,134.192945634076));
#21313=CARTESIAN_POINT('Ctrl Pts',(195.593862708486,3.660336714878,134.092195201126));
#21314=CARTESIAN_POINT('Ctrl Pts',(195.586102265972,3.74894114432121,133.987852938731));
#21315=CARTESIAN_POINT('Ctrl Pts',(195.578329365706,3.83768780946045,133.883343176873));
#21316=CARTESIAN_POINT('Ctrl Pts',(195.570556465441,3.92196699860579,133.775230371938));
#21317=CARTESIAN_POINT('Ctrl Pts',(195.562783565176,4.00149491020802,133.663944773712));
#21318=CARTESIAN_POINT('Ctrl Pts',(195.555293229414,4.07813178190516,133.556704687292));
#21319=CARTESIAN_POINT('Ctrl Pts',(195.547802893651,4.15035665163739,133.446518738335));
#21320=CARTESIAN_POINT('Ctrl Pts',(195.540312557889,4.21795626720724,133.333792963059));
#21321=CARTESIAN_POINT('Ctrl Pts',(195.53253822377,4.28811894274751,133.216793155752));
#21322=CARTESIAN_POINT('Ctrl Pts',(195.524763889651,4.35352096178859,133.096686504988));
#21323=CARTESIAN_POINT('Ctrl Pts',(195.516989555532,4.41387490580435,132.973897752167));
#21324=CARTESIAN_POINT('Ctrl Pts',(195.509224802585,4.47415446897807,132.851260325509));
#21325=CARTESIAN_POINT('Ctrl Pts',(195.501460049638,4.52939816485493,132.725947721159));
#21326=CARTESIAN_POINT('Ctrl Pts',(195.493695296691,4.57936250334169,132.598412491255));
#21327=CARTESIAN_POINT('Ctrl Pts',(195.485938255806,4.62927721654309,132.47100393114));
#21328=CARTESIAN_POINT('Ctrl Pts',(195.478181214921,4.67392286552881,132.341377500251));
#21329=CARTESIAN_POINT('Ctrl Pts',(195.470424174036,4.71310261393714,132.210008800078));
#21330=CARTESIAN_POINT('Ctrl Pts',(195.462672982796,4.75225281659245,132.078739166064));
#21331=CARTESIAN_POINT('Ctrl Pts',(195.454921791556,4.78594521173213,131.945730251064));
#21332=CARTESIAN_POINT('Ctrl Pts',(195.447170600316,4.81403181502214,131.811475678746));
#21333=CARTESIAN_POINT('Ctrl Pts',(195.439422703538,4.84210648075651,131.677278168202));
#21334=CARTESIAN_POINT('Ctrl Pts',(195.431674806761,4.86458001358226,131.54183643523));
#21335=CARTESIAN_POINT('Ctrl Pts',(195.423926909984,4.88135490294342,131.405657028673));
#21336=CARTESIAN_POINT('Ctrl Pts',(195.4161806339,4.89812628335934,131.269506107912));
#21337=CARTESIAN_POINT('Ctrl Pts',(195.408434357816,4.90920134356196,131.132618208275));
#21338=CARTESIAN_POINT('Ctrl Pts',(195.400688081732,4.91453415629017,130.995507391426));
#21339=CARTESIAN_POINT('Ctrl Pts',(195.392941748467,4.919867008384,130.858395562457));
#21340=CARTESIAN_POINT('Ctrl Pts',(195.385195415201,4.91945751322652,130.721061203664));
#21341=CARTESIAN_POINT('Ctrl Pts',(195.377449081936,4.91331184090468,130.584020388543));
#21342=CARTESIAN_POINT('Ctrl Pts',(195.369701013933,4.90716479230216,130.446948884082));
#21343=CARTESIAN_POINT('Ctrl Pts',(195.36195294593,4.8952790278877,130.310171444601));
#21344=CARTESIAN_POINT('Ctrl Pts',(195.354204877927,4.8777127276868,130.174200631005));
#21345=CARTESIAN_POINT('Ctrl Pts',(195.346448575185,4.86012775781292,130.03808530601));
#21346=CARTESIAN_POINT('Ctrl Pts',(195.338692272444,4.83685024208653,129.902778707793));
#21347=CARTESIAN_POINT('Ctrl Pts',(195.330935969702,4.80798990287418,129.768785339588));
#21348=CARTESIAN_POINT('Ctrl Pts',(195.323175527188,4.77911416002987,129.634720455087));
#21349=CARTESIAN_POINT('Ctrl Pts',(195.315415084674,4.74464975455025,129.501970575457));
#21350=CARTESIAN_POINT('Ctrl Pts',(195.307654642159,4.70475651246827,129.371025618033));
#21351=CARTESIAN_POINT('Ctrl Pts',(195.299881741894,4.66479923021246,129.239870456138));
#21352=CARTESIAN_POINT('Ctrl Pts',(195.292108841629,4.61939582587396,129.11052637553));
#21353=CARTESIAN_POINT('Ctrl Pts',(195.284335941363,4.56875487911233,128.983464707008));
#21354=CARTESIAN_POINT('Ctrl Pts',(195.276845605601,4.5199548583218,128.861022050185));
#21355=CARTESIAN_POINT('Ctrl Pts',(195.269355269839,4.46629160511688,128.740699024911));
#21356=CARTESIAN_POINT('Ctrl Pts',(195.261864934077,4.40799146124495,128.622894518794));
#21357=CARTESIAN_POINT('Ctrl Pts',(195.254090599958,4.3474808496989,128.500623419023));
#21358=CARTESIAN_POINT('Ctrl Pts',(195.246316265839,4.28178311163883,128.380678269616));
#21359=CARTESIAN_POINT('Ctrl Pts',(195.23854193172,4.21110023729952,128.263530467021));
#21360=CARTESIAN_POINT('Ctrl Pts',(195.230777178773,4.14050447328558,128.146527038623));
#21361=CARTESIAN_POINT('Ctrl Pts',(195.223012425825,4.06493599723231,128.032314429117));
#21362=CARTESIAN_POINT('Ctrl Pts',(195.215247672878,3.98464394172745,127.9213421091));
#21363=CARTESIAN_POINT('Ctrl Pts',(195.207490631993,3.90443163342391,127.810480008356));
#21364=CARTESIAN_POINT('Ctrl Pts',(195.199733591108,3.81950530971266,127.702852107236));
#21365=CARTESIAN_POINT('Ctrl Pts',(195.191976550223,3.73015871273531,127.59888108397));
#21366=CARTESIAN_POINT('Ctrl Pts',(195.184225358983,3.64087949272173,127.49498846606));
#21367=CARTESIAN_POINT('Ctrl Pts',(195.176474167743,3.5471868880792,127.39474753233));
#21368=CARTESIAN_POINT('Ctrl Pts',(195.168722976503,3.44941620923195,127.29854960184));
#21369=CARTESIAN_POINT('Ctrl Pts',(195.160975079726,3.35168708553179,127.202392558036));
#21370=CARTESIAN_POINT('Ctrl Pts',(195.153227182949,3.24988361311233,127.110275373367));
#21371=CARTESIAN_POINT('Ctrl Pts',(195.145479286172,3.14437925902386,127.022553888247));
#21372=CARTESIAN_POINT('Ctrl Pts',(195.137733010088,3.03889697417174,126.934850752571));
#21373=CARTESIAN_POINT('Ctrl Pts',(195.129986734003,2.92971564790252,126.851541737333));
#21374=CARTESIAN_POINT('Ctrl Pts',(195.122240457919,2.8172429500486,126.772943345328));
#21375=CARTESIAN_POINT('Ctrl Pts',(195.114494124654,2.70476942194696,126.694344373127));
#21376=CARTESIAN_POINT('Ctrl Pts',(195.106747791389,2.58900479424786,126.620456317494));
#21377=CARTESIAN_POINT('Ctrl Pts',(195.099001458123,2.47038658928282,126.551552937692));
#21378=CARTESIAN_POINT('Ctrl Pts',(195.09125339012,2.35174182059327,126.482634127456));
#21379=CARTESIAN_POINT('Ctrl Pts',(195.083505322117,2.23024254102713,126.418702410666));
#21380=CARTESIAN_POINT('Ctrl Pts',(195.075757254114,2.10635143031566,126.359985890509));
#21381=CARTESIAN_POINT('Ctrl Pts',(195.068000951373,1.98232864665704,126.301206965734));
#21382=CARTESIAN_POINT('Ctrl Pts',(195.060244648631,1.8559093076601,126.247654477585));
#21383=CARTESIAN_POINT('Ctrl Pts',(195.052488345889,1.72757717380225,126.199508809847));
#21384=CARTESIAN_POINT('Ctrl Pts',(195.044727903375,1.59917654522038,126.151337445316));
#21385=CARTESIAN_POINT('Ctrl Pts',(195.036967460861,1.46886145881318,126.108578773192));
#21386=CARTESIAN_POINT('Ctrl Pts',(195.029207018346,1.33713048578585,126.071363139595));
#21387=CARTESIAN_POINT('Ctrl Pts',(195.021434118081,1.2051880465063,126.034087764159));
#21388=CARTESIAN_POINT('Ctrl Pts',(195.013661217816,1.0718255591914,126.002373299147));
#21389=CARTESIAN_POINT('Ctrl Pts',(195.00588831755,0.937552310192054,125.976299026394));
#21390=CARTESIAN_POINT('Ctrl Pts',(194.998397981788,0.808160232008243,125.951172619133));
#21391=CARTESIAN_POINT('Ctrl Pts',(194.990907646026,0.677922763967373,125.931283499663));
#21392=CARTESIAN_POINT('Ctrl Pts',(194.983417310264,0.547297844753216,125.916656848757));
#21393=CARTESIAN_POINT('Ctrl Pts',(194.975642976145,0.411720242024034,125.901475623937));
#21394=CARTESIAN_POINT('Ctrl Pts',(194.967868642026,0.27529575862716,125.891915708546));
#21395=CARTESIAN_POINT('Ctrl Pts',(194.960094307907,0.138530174400293,125.888061963774));
#21396=CARTESIAN_POINT('Ctrl Pts',(194.95232955496,0.00193314153252316,
125.884212968398));
#21397=CARTESIAN_POINT('Ctrl Pts',(194.944564802013,-0.135003768683377,
125.886056162276));
#21398=CARTESIAN_POINT('Ctrl Pts',(194.936800049066,-0.271767741656031,
125.893624892942));
#21399=CARTESIAN_POINT('Ctrl Pts',(194.929043008181,-0.408395878722369,
125.901186106239));
#21400=CARTESIAN_POINT('Ctrl Pts',(194.921285967296,-0.544851032521165,
125.914461518103));
#21401=CARTESIAN_POINT('Ctrl Pts',(194.913528926411,-0.680618817085562,
125.933432462858));
#21402=CARTESIAN_POINT('Ctrl Pts',(194.90577773517,-0.816284218107408,125.952389101476));
#21403=CARTESIAN_POINT('Ctrl Pts',(194.89802654393,-0.951262896003321,125.977032670072));
#21404=CARTESIAN_POINT('Ctrl Pts',(194.89027535269,-1.08504437948985,126.00729258));
#21405=CARTESIAN_POINT('Ctrl Pts',(194.882527455913,-1.21876900227714,126.037539628659));
#21406=CARTESIAN_POINT('Ctrl Pts',(194.874779559136,-1.35129706216439,126.073398184829));
#21407=CARTESIAN_POINT('Ctrl Pts',(194.867031662359,-1.48212731246938,126.114746380538));
#21408=CARTESIAN_POINT('Ctrl Pts',(194.859285386275,-1.61293019590674,126.156085927097));
#21409=CARTESIAN_POINT('Ctrl Pts',(194.851539110191,-1.74203560361091,126.202912711391));
#21410=CARTESIAN_POINT('Ctrl Pts',(194.843792834107,-1.86895689731614,126.255054826737));
#21411=CARTESIAN_POINT('Ctrl Pts',(194.836046500841,-1.9958791279254,126.307197326983));
#21412=CARTESIAN_POINT('Ctrl Pts',(194.828300167576,-2.12061685072737,126.364655088006));
#21413=CARTESIAN_POINT('Ctrl Pts',(194.820553834311,-2.24270325279445,126.427207983444));
#21414=CARTESIAN_POINT('Ctrl Pts',(194.812805766308,-2.3648169952645,126.489774887168));
#21415=CARTESIAN_POINT('Ctrl Pts',(194.805057698305,-2.48427788763078,126.557439017562));
#21416=CARTESIAN_POINT('Ctrl Pts',(194.797309630302,-2.60064393052617,126.629934404406));
#21417=CARTESIAN_POINT('Ctrl Pts',(194.78955332756,-2.71713364863695,126.70250684021));
#21418=CARTESIAN_POINT('Ctrl Pts',(194.781797024818,-2.83052161429419,126.779920582553));
#21419=CARTESIAN_POINT('Ctrl Pts',(194.774040722076,-2.94039458115534,126.861866131887));
#21420=CARTESIAN_POINT('Ctrl Pts',(194.766280279562,-3.050326190527,126.943855418027));
#21421=CARTESIAN_POINT('Ctrl Pts',(194.758519837048,-3.15673875969899,127.030381084215));
#21422=CARTESIAN_POINT('Ctrl Pts',(194.750759394534,-3.25925313487488,127.121094123636));
#21423=CARTESIAN_POINT('Ctrl Pts',(194.742986494268,-3.36193207522668,127.211952783681));
#21424=CARTESIAN_POINT('Ctrl Pts',(194.735213594003,-3.46070003479519,127.307011978273));
#21425=CARTESIAN_POINT('Ctrl Pts',(194.727440693737,-3.55521502981467,127.40588608415));
#21426=CARTESIAN_POINT('Ctrl Pts',(194.719950357975,-3.6462941666962,127.501165867229));
#21427=CARTESIAN_POINT('Ctrl Pts',(194.712460022213,-3.73342397889856,127.599987782716));
#21428=CARTESIAN_POINT('Ctrl Pts',(194.704969686451,-3.81633575408038,127.701980164651));
#21429=CARTESIAN_POINT('Ctrl Pts',(194.697219842191,-3.90212007209462,127.807506151856));
#21430=CARTESIAN_POINT('Ctrl Pts',(194.68946999793,-3.98366789287206,127.916769679002));
#21431=CARTESIAN_POINT('Ctrl Pts',(194.681720153669,-4.06063403806943,128.029394983297));
#21432=CARTESIAN_POINT('Ctrl Pts',(194.673641243833,-4.14086823717748,128.146802462472));
#21433=CARTESIAN_POINT('Ctrl Pts',(194.665562333997,-4.21612278806056,128.26786322798));
#21434=CARTESIAN_POINT('Ctrl Pts',(194.657483424161,-4.28605088173785,128.39211044363));
#21435=CARTESIAN_POINT('Ctrl Pts',(194.649752999485,-4.35296261511464,128.510998234348));
#21436=CARTESIAN_POINT('Ctrl Pts',(194.642022574809,-4.41499755592588,128.632802943297));
#21437=CARTESIAN_POINT('Ctrl Pts',(194.634292150133,-4.47189467077365,128.757084105708));
#21438=CARTESIAN_POINT('Ctrl Pts',(194.626567138405,-4.52875194548538,128.881278244753));
#21439=CARTESIAN_POINT('Ctrl Pts',(194.618842126678,-4.58047838715712,129.007945031798));
#21440=CARTESIAN_POINT('Ctrl Pts',(194.61111711495,-4.62685868724639,129.136619105595));
#21441=CARTESIAN_POINT('Ctrl Pts',(194.603396293483,-4.67321382938121,129.265223383023));
#21442=CARTESIAN_POINT('Ctrl Pts',(194.595675472015,-4.71422847016418,129.395832410166));
#21443=CARTESIAN_POINT('Ctrl Pts',(194.587954650547,-4.74973548014277,129.527961020585));
#21444=CARTESIAN_POINT('Ctrl Pts',(194.58689417891,-4.75461244526093,129.546109172866));
#21445=CARTESIAN_POINT('Ctrl Pts',(194.585833707274,-4.75938558135185,129.564285966276));
#21446=CARTESIAN_POINT('Ctrl Pts',(194.584773235637,-4.76405452823405,129.582490119308));
#21447=CARTESIAN_POINT('Ctrl Pts',(196.33459504632,-4.76405452823405,129.582490119308));
#21448=CARTESIAN_POINT('Ctrl Pts',(196.325979820702,-4.80173843363128,129.729419094519));
#21449=CARTESIAN_POINT('Ctrl Pts',(196.317364595083,-4.83266542359164,129.878265641535));
#21450=CARTESIAN_POINT('Ctrl Pts',(196.308749369464,-4.85665623691895,130.028426819555));
#21451=CARTESIAN_POINT('Ctrl Pts',(196.300175614881,-4.88053156587922,130.177865168033));
#21452=CARTESIAN_POINT('Ctrl Pts',(196.291601860298,-4.89753723731489,130.328605301003));
#21453=CARTESIAN_POINT('Ctrl Pts',(196.283028105715,-4.90754478717536,130.48003481784));
#21454=CARTESIAN_POINT('Ctrl Pts',(196.276971882491,-4.91461379705869,130.586999735934));
#21455=CARTESIAN_POINT('Ctrl Pts',(196.270915659266,-4.91819205678833,130.694308241907));
#21456=CARTESIAN_POINT('Ctrl Pts',(196.264859436042,-4.91824930178245,130.801739927489));
#21457=CARTESIAN_POINT('',(196.610140563971,-4.91824935727201,130.801846220335));
#21458=CARTESIAN_POINT('Ctrl Pts',(196.680227908624,-4.76405452823405,129.582490119308));
#21459=CARTESIAN_POINT('Ctrl Pts',(196.672454999871,-4.79811658810201,129.71529757377));
#21460=CARTESIAN_POINT('Ctrl Pts',(196.664682091119,-4.82658494688575,129.849389568182));
#21461=CARTESIAN_POINT('Ctrl Pts',(196.656909182367,-4.84939273648973,129.984255045228));
#21462=CARTESIAN_POINT('Ctrl Pts',(196.649444140572,-4.87129716224193,130.113778812316));
#21463=CARTESIAN_POINT('Ctrl Pts',(196.641979098777,-4.88798086211456,130.244015655847));
#21464=CARTESIAN_POINT('Ctrl Pts',(196.634514056982,-4.89942987008945,130.374511794635));
#21465=CARTESIAN_POINT('Ctrl Pts',(196.626389559324,-4.91189027433556,130.516535858678));
#21466=CARTESIAN_POINT('Ctrl Pts',(196.618265061666,-4.91817638477932,130.659109497139));
#21467=CARTESIAN_POINT('Ctrl Pts',(196.610140564008,-4.91824935727168,130.801846219679));
#21468=CARTESIAN_POINT('Ctrl Pts',(196.610140563971,-4.91824935727201,130.801846220335));
#21469=CARTESIAN_POINT('Ctrl Pts',(196.602459708905,-4.91831834504391,130.936788726876));
#21470=CARTESIAN_POINT('Ctrl Pts',(196.59477885384,-4.91282949710972,131.071957218089));
#21471=CARTESIAN_POINT('Ctrl Pts',(196.587097998774,-4.90175335462761,131.206849266967));
#21472=CARTESIAN_POINT('Ctrl Pts',(196.579425945198,-4.89068990429389,131.341586743087));
#21473=CARTESIAN_POINT('Ctrl Pts',(196.571753891622,-4.87405192579336,131.476048011019));
#21474=CARTESIAN_POINT('Ctrl Pts',(196.564081838046,-4.85186195546942,131.60972924594));
#21475=CARTESIAN_POINT('Ctrl Pts',(196.556416637028,-4.82969180487755,131.743291078887));
#21476=CARTESIAN_POINT('Ctrl Pts',(196.548751436009,-4.80197959258732,131.8760738716));
#21477=CARTESIAN_POINT('Ctrl Pts',(196.541086234991,-4.76879973819775,132.007578020808));
#21478=CARTESIAN_POINT('Ctrl Pts',(196.533377076582,-4.73542960832549,132.139836302786));
#21479=CARTESIAN_POINT('Ctrl Pts',(196.525667918172,-4.69652895673484,132.270800820309));
#21480=CARTESIAN_POINT('Ctrl Pts',(196.517958759763,-4.65222593936672,132.399972372218));
#21481=CARTESIAN_POINT('Ctrl Pts',(196.51030050335,-4.60821544575988,132.528291030792));
#21482=CARTESIAN_POINT('Ctrl Pts',(196.502642246937,-4.55887385694772,132.654839949545));
#21483=CARTESIAN_POINT('Ctrl Pts',(196.494983990524,-4.50437694002413,132.779144515788));
#21484=CARTESIAN_POINT('Ctrl Pts',(196.487326349773,-4.44988440421434,132.903439088945));
#21485=CARTESIAN_POINT('Ctrl Pts',(196.479668709022,-4.39023752537237,133.025489301258));
#21486=CARTESIAN_POINT('Ctrl Pts',(196.472011068271,-4.32565999840557,133.144841047028));
#21487=CARTESIAN_POINT('Ctrl Pts',(196.464352292712,-4.26107290151344,133.264210479868));
#21488=CARTESIAN_POINT('Ctrl Pts',(196.456693517154,-4.19155389441899,133.380880298477));
#21489=CARTESIAN_POINT('Ctrl Pts',(196.449034741596,-4.11737209033022,133.494421979742));
#21490=CARTESIAN_POINT('Ctrl Pts',(196.44128738256,-4.04233227935724,133.609276914914));
#21491=CARTESIAN_POINT('Ctrl Pts',(196.433540023525,-3.96252135406451,133.720930539313));
#21492=CARTESIAN_POINT('Ctrl Pts',(196.425792664489,-3.87826158539609,133.82897135909));
#21493=CARTESIAN_POINT('Ctrl Pts',(196.418122442924,-3.79484075880011,133.935936458026));
#21494=CARTESIAN_POINT('Ctrl Pts',(196.41045222136,-3.70705958893727,134.03936010492));
#21495=CARTESIAN_POINT('Ctrl Pts',(196.402781999795,-3.61526928634412,134.138878731135));
#21496=CARTESIAN_POINT('Ctrl Pts',(196.394996072024,-3.52209431609966,134.239898607683));
#21497=CARTESIAN_POINT('Ctrl Pts',(196.387210144253,-3.4247885873534,134.336894393959));
#21498=CARTESIAN_POINT('Ctrl Pts',(196.379424216482,-3.32375503379505,134.429527584455));
#21499=CARTESIAN_POINT('Ctrl Pts',(196.371638288711,-3.2227214802367,134.52216077495));
#21500=CARTESIAN_POINT('Ctrl Pts',(196.36385236094,-3.1179604696731,134.610431147627));
#21501=CARTESIAN_POINT('Ctrl Pts',(196.356066433169,-3.00990550869428,134.694045937901));
#21502=CARTESIAN_POINT('Ctrl Pts',(196.34829209905,-2.90201144717865,134.777536221399));
#21503=CARTESIAN_POINT('Ctrl Pts',(196.340517764931,-2.79047001289452,134.856666115183));
#21504=CARTESIAN_POINT('Ctrl Pts',(196.332743430812,-2.67566902769502,134.931100046793));
#21505=CARTESIAN_POINT('Ctrl Pts',(196.324978677865,-2.56100952444973,135.005442245234));
#21506=CARTESIAN_POINT('Ctrl Pts',(196.317213924918,-2.44309878802772,135.075099785956));
#21507=CARTESIAN_POINT('Ctrl Pts',(196.309449171971,-2.32235744469594,135.139777432771));
#21508=CARTESIAN_POINT('Ctrl Pts',(196.301692131086,-2.20173602336822,135.204390840836));
#21509=CARTESIAN_POINT('Ctrl Pts',(196.293935090201,-2.07828993234506,135.264034014541));
#21510=CARTESIAN_POINT('Ctrl Pts',(196.286178049316,-1.95246819612849,135.318455322555));
#21511=CARTESIAN_POINT('Ctrl Pts',(196.278426858075,-1.82674134306254,135.372835591037));
#21512=CARTESIAN_POINT('Ctrl Pts',(196.270675666835,-1.69864276804628,135.4220016773));
#21513=CARTESIAN_POINT('Ctrl Pts',(196.262924475595,-1.56864516146753,135.465748331531));
#21514=CARTESIAN_POINT('Ctrl Pts',(196.255176578818,-1.43870280733915,135.509476392268));
#21515=CARTESIAN_POINT('Ctrl Pts',(196.247428682041,-1.30686339675709,135.547789477832));
#21516=CARTESIAN_POINT('Ctrl Pts',(196.239680785264,-1.17361841621132,135.58053093233));
#21517=CARTESIAN_POINT('Ctrl Pts',(196.23193450918,-1.04040130764291,135.613265538021));
#21518=CARTESIAN_POINT('Ctrl Pts',(196.224188233096,-0.90577959335298,135.640430737586));
#21519=CARTESIAN_POINT('Ctrl Pts',(196.216441957012,-0.770258312508345,
135.661920210048));
#21520=CARTESIAN_POINT('Ctrl Pts',(196.208695623746,-0.634736031276551,
135.68340984114));
#21521=CARTESIAN_POINT('Ctrl Pts',(196.200949290481,-0.49831455638039,135.699223600296));
#21522=CARTESIAN_POINT('Ctrl Pts',(196.193202957216,-0.361507077887804,
135.709306661626));
#21523=CARTESIAN_POINT('Ctrl Pts',(196.185454889213,-0.224668962309024,
135.719391980987));
#21524=CARTESIAN_POINT('Ctrl Pts',(196.17770682121,-0.0874450609556074,
135.723744020074));
#21525=CARTESIAN_POINT('Ctrl Pts',(196.169958753207,0.0496487812816021,
135.722360013765));
#21526=CARTESIAN_POINT('Ctrl Pts',(196.162202450465,0.186888328485989,135.720974536519));
#21527=CARTESIAN_POINT('Ctrl Pts',(196.154446147723,0.323997148879435,135.71384083974));
#21528=CARTESIAN_POINT('Ctrl Pts',(196.146689844981,0.460461311244389,135.701008291572));
#21529=CARTESIAN_POINT('Ctrl Pts',(196.138929402467,0.596998308641748,135.688168894286));
#21530=CARTESIAN_POINT('Ctrl Pts',(196.131168959953,0.732889575229854,135.669624637705));
#21531=CARTESIAN_POINT('Ctrl Pts',(196.123408517439,0.8676297459151,135.645476365666));
#21532=CARTESIAN_POINT('Ctrl Pts',(196.115635617173,1.00258621348393,135.621289328677));
#21533=CARTESIAN_POINT('Ctrl Pts',(196.107862716908,1.13638751074486,135.591480384296));
#21534=CARTESIAN_POINT('Ctrl Pts',(196.100089816642,1.268540970819,135.556200983977));
#21535=CARTESIAN_POINT('Ctrl Pts',(196.09259948088,1.39589031974556,135.522204078723));
#21536=CARTESIAN_POINT('Ctrl Pts',(196.085109145118,1.52170926338293,135.483127633423));
#21537=CARTESIAN_POINT('Ctrl Pts',(196.077618809356,1.64557497313272,135.439149293471));
#21538=CARTESIAN_POINT('Ctrl Pts',(196.069844475237,1.77413708891525,135.393503501393));
#21539=CARTESIAN_POINT('Ctrl Pts',(196.062070141118,1.90100217941226,135.342432174158));
#21540=CARTESIAN_POINT('Ctrl Pts',(196.054295806999,2.02567829082461,135.286080212162));
#21541=CARTESIAN_POINT('Ctrl Pts',(196.046531054052,2.15020075007207,135.229797698922));
#21542=CARTESIAN_POINT('Ctrl Pts',(196.038766301105,2.27253924505167,135.168247659205));
#21543=CARTESIAN_POINT('Ctrl Pts',(196.031001548158,2.3922180264252,135.101624395431));
#21544=CARTESIAN_POINT('Ctrl Pts',(196.023244507273,2.51177794114601,135.03506730282));
#21545=CARTESIAN_POINT('Ctrl Pts',(196.015487466388,2.62868305990259,134.963447202521));
#21546=CARTESIAN_POINT('Ctrl Pts',(196.007730425503,2.7424789694179,134.887005858681));
#21547=CARTESIAN_POINT('Ctrl Pts',(195.999979234263,2.85618906455235,134.810622159854));
#21548=CARTESIAN_POINT('Ctrl Pts',(195.992228043023,2.96679429415914,134.729424671326));
#21549=CARTESIAN_POINT('Ctrl Pts',(195.984476851783,3.0738664750577,134.643700138371));
#21550=CARTESIAN_POINT('Ctrl Pts',(195.976728955005,3.18089314742335,134.55801204063));
#21551=CARTESIAN_POINT('Ctrl Pts',(195.968981058228,3.28438945316746,134.467800969217));
#21552=CARTESIAN_POINT('Ctrl Pts',(195.961233161451,3.38395793279755,134.373395749301));
#21553=CARTESIAN_POINT('Ctrl Pts',(195.953486885367,3.4835055848481,134.279010276921));
#21554=CARTESIAN_POINT('Ctrl Pts',(195.945740609283,3.57912676149234,134.180432669916));
#21555=CARTESIAN_POINT('Ctrl Pts',(195.937994333199,3.67045902587537,134.078030362954));
#21556=CARTESIAN_POINT('Ctrl Pts',(195.930247999934,3.76179196445257,133.975627300082));
#21557=CARTESIAN_POINT('Ctrl Pts',(195.922501666668,3.84883566736076,133.869399772691));
#21558=CARTESIAN_POINT('Ctrl Pts',(195.914755333403,3.93126661625871,133.759749907387));
#21559=CARTESIAN_POINT('Ctrl Pts',(195.9070072654,4.01371602499605,133.650075486756));
#21560=CARTESIAN_POINT('Ctrl Pts',(195.899259197397,4.09155038929708,133.536977515595));
#21561=CARTESIAN_POINT('Ctrl Pts',(195.891511129394,4.16448855602539,133.420888494206));
#21562=CARTESIAN_POINT('Ctrl Pts',(195.883754826652,4.23750424230527,133.304676092023));
#21563=CARTESIAN_POINT('Ctrl Pts',(195.875998523911,4.3056131276605,133.185466620943));
#21564=CARTESIAN_POINT('Ctrl Pts',(195.868242221169,4.36857895453045,133.063719150542));
#21565=CARTESIAN_POINT('Ctrl Pts',(195.860481778655,4.43157838815802,132.941906699851));
#21566=CARTESIAN_POINT('Ctrl Pts',(195.85272133614,4.48942912881509,132.817553904979));
#21567=CARTESIAN_POINT('Ctrl Pts',(195.844960893626,4.5419428571012,132.691140452451));
#21568=CARTESIAN_POINT('Ctrl Pts',(195.837187993361,4.59454088508596,132.564524069826));
#21569=CARTESIAN_POINT('Ctrl Pts',(195.829415093095,4.64178464539287,132.435840786428));
#21570=CARTESIAN_POINT('Ctrl Pts',(195.82164219283,4.68353525993757,132.305586960068));
#21571=CARTESIAN_POINT('Ctrl Pts',(195.814151857068,4.72376813448038,132.180068188384));
#21572=CARTESIAN_POINT('Ctrl Pts',(195.806661521306,4.75890022668183,132.053091374545));
#21573=CARTESIAN_POINT('Ctrl Pts',(195.799171185544,4.78885244545705,131.925108277898));
#21574=CARTESIAN_POINT('Ctrl Pts',(195.791396851425,4.81994031171073,131.792272663244));
#21575=CARTESIAN_POINT('Ctrl Pts',(195.783622517306,4.84554623795796,131.657932169745));
#21576=CARTESIAN_POINT('Ctrl Pts',(195.775848183187,4.86552621996172,131.522579014271));
#21577=CARTESIAN_POINT('Ctrl Pts',(195.76808343024,4.88548157842337,131.387392669463));
#21578=CARTESIAN_POINT('Ctrl Pts',(195.760318677292,4.89982473164211,131.25119652892));
#21579=CARTESIAN_POINT('Ctrl Pts',(195.752553924345,4.90846199760866,131.114495879237));
#21580=CARTESIAN_POINT('Ctrl Pts',(195.74479688346,4.91709068492086,130.977931002566));
#21581=CARTESIAN_POINT('Ctrl Pts',(195.737039842575,4.92002473840631,130.840863001602));
#21582=CARTESIAN_POINT('Ctrl Pts',(195.72928280169,4.91722193961525,130.70380486653));
#21583=CARTESIAN_POINT('Ctrl Pts',(195.72153161045,4.91442125443657,130.566850088065));
#21584=CARTESIAN_POINT('Ctrl Pts',(195.71378041921,4.90589233599108,130.429905549986));
#21585=CARTESIAN_POINT('Ctrl Pts',(195.70602922797,4.89164498773053,130.293486487754));
#21586=CARTESIAN_POINT('Ctrl Pts',(195.698281331193,4.87740369497295,130.157125407263));
#21587=CARTESIAN_POINT('Ctrl Pts',(195.690533434416,4.85744884697578,130.021289746446));
#21588=CARTESIAN_POINT('Ctrl Pts',(195.682785537639,4.83184225710067,129.886491637266));
#21589=CARTESIAN_POINT('Ctrl Pts',(195.675039261555,4.80624102357217,129.751721724946));
#21590=CARTESIAN_POINT('Ctrl Pts',(195.667292985471,4.77499047258891,129.617989316424));
#21591=CARTESIAN_POINT('Ctrl Pts',(195.659546709387,4.73820383137157,129.485797947506));
#21592=CARTESIAN_POINT('Ctrl Pts',(195.651800376121,4.70141691860354,129.353605602781));
#21593=CARTESIAN_POINT('Ctrl Pts',(195.644054042856,4.65909393887212,129.222954697012));
#21594=CARTESIAN_POINT('Ctrl Pts',(195.63630770959,4.61139834311363,129.094334774595));
#21595=CARTESIAN_POINT('Ctrl Pts',(195.628559641587,4.5636920662572,128.965686048638));
#21596=CARTESIAN_POINT('Ctrl Pts',(195.620811573584,4.51061091513302,128.839069577583));
#21597=CARTESIAN_POINT('Ctrl Pts',(195.613063505581,4.45236679435636,128.714955680505));
#21598=CARTESIAN_POINT('Ctrl Pts',(195.60530720284,4.3940607710351,128.590709873701));
#21599=CARTESIAN_POINT('Ctrl Pts',(195.597550900098,4.33058098301466,128.468972308536));
#21600=CARTESIAN_POINT('Ctrl Pts',(195.589794597356,4.26218595554776,128.350189893506));
#21601=CARTESIAN_POINT('Ctrl Pts',(195.582034154842,4.19375442359537,128.231344080725));
#21602=CARTESIAN_POINT('Ctrl Pts',(195.574273712328,4.12040263382347,128.115456891078));
#21603=CARTESIAN_POINT('Ctrl Pts',(195.566513269813,4.04243236885387,128.002946045293));
#21604=CARTESIAN_POINT('Ctrl Pts',(195.558740369548,3.96433693909305,127.89025458711));
#21605=CARTESIAN_POINT('Ctrl Pts',(195.550967469282,3.88160845470985,127.780950615611));
#21606=CARTESIAN_POINT('Ctrl Pts',(195.543194569017,3.79458944858941,127.675419266381));
#21607=CARTESIAN_POINT('Ctrl Pts',(195.535704233255,3.71073380252928,127.573724247514));
#21608=CARTESIAN_POINT('Ctrl Pts',(195.528213897493,3.62289436686037,127.475532553891));
#21609=CARTESIAN_POINT('Ctrl Pts',(195.520723561731,3.53140846885445,127.381154914047));
#21610=CARTESIAN_POINT('Ctrl Pts',(195.512949227612,3.43645385521897,127.283198917303));
#21611=CARTESIAN_POINT('Ctrl Pts',(195.505174893493,3.33727002191439,127.189041608169));
#21612=CARTESIAN_POINT('Ctrl Pts',(195.497400559374,3.23419324712464,127.099070196728));
#21613=CARTESIAN_POINT('Ctrl Pts',(195.489635806427,3.1312435052475,127.009209667011));
#21614=CARTESIAN_POINT('Ctrl Pts',(195.48187105348,3.02441065959921,126.92352502525));
#21615=CARTESIAN_POINT('Ctrl Pts',(195.474106300532,2.91406918468932,126.842368208519));
#21616=CARTESIAN_POINT('Ctrl Pts',(195.466349259647,2.80383730248746,126.761291997883));
#21617=CARTESIAN_POINT('Ctrl Pts',(195.458592218762,2.69010403888476,126.684734892995));
#21618=CARTESIAN_POINT('Ctrl Pts',(195.450835177877,2.57327816695157,126.61300969716));
#21619=CARTESIAN_POINT('Ctrl Pts',(195.443083986637,2.45654039431791,126.541338589853));
#21620=CARTESIAN_POINT('Ctrl Pts',(195.435332795397,2.33671498721072,126.474492342605));
#21621=CARTESIAN_POINT('Ctrl Pts',(195.427581604157,2.2142407268208,126.412741204845));
#21622=CARTESIAN_POINT('Ctrl Pts',(195.41983370738,2.09181852125829,126.351016312966));
#21623=CARTESIAN_POINT('Ctrl Pts',(195.412085810603,1.96675004998067,126.294382399095));
#21624=CARTESIAN_POINT('Ctrl Pts',(195.404337913826,1.83949959574408,126.243064277735));
#21625=CARTESIAN_POINT('Ctrl Pts',(195.396591637742,1.71227575955951,126.19175689102));
#21626=CARTESIAN_POINT('Ctrl Pts',(195.388845361658,1.5828712106282,126.145763231222));
#21627=CARTESIAN_POINT('Ctrl Pts',(195.381099085574,1.45177078996202,126.105260210476));
#21628=CARTESIAN_POINT('Ctrl Pts',(195.373352752308,1.32066940154283,126.064756890746));
#21629=CARTESIAN_POINT('Ctrl Pts',(195.365606419043,1.18787248995334,126.02974440635));
#21630=CARTESIAN_POINT('Ctrl Pts',(195.357860085778,1.05388027198198,126.000349852088));
#21631=CARTESIAN_POINT('Ctrl Pts',(195.350112017775,0.919858047382009,125.97094871512));
#21632=CARTESIAN_POINT('Ctrl Pts',(195.342363949772,0.784640365557708,125.947168095513));
#21633=CARTESIAN_POINT('Ctrl Pts',(195.334615881769,0.648737458886747,125.92908393086));
#21634=CARTESIAN_POINT('Ctrl Pts',(195.326859579027,0.512690112989033,125.910980546142));
#21635=CARTESIAN_POINT('Ctrl Pts',(195.319103276285,0.375956475623729,125.898585762068));
#21636=CARTESIAN_POINT('Ctrl Pts',(195.311346973543,0.239052282779265,125.891923638978));
#21637=CARTESIAN_POINT('Ctrl Pts',(195.303586531029,0.102075020045067,125.885257960113));
#21638=CARTESIAN_POINT('Ctrl Pts',(195.295826088515,-0.0350725887894774,
125.884331041572));
#21639=CARTESIAN_POINT('Ctrl Pts',(195.288065646001,-0.17187598256682,125.889114773347));
#21640=CARTESIAN_POINT('Ctrl Pts',(195.280292745735,-0.308898985296921,
125.893906184392));
#21641=CARTESIAN_POINT('Ctrl Pts',(195.27251984547,-0.445576278733256,125.904426534803));
#21642=CARTESIAN_POINT('Ctrl Pts',(195.264746945204,-0.58139869000898,125.920595817153));
#21643=CARTESIAN_POINT('Ctrl Pts',(195.257256609442,-0.712283614519818,
125.936177305362));
#21644=CARTESIAN_POINT('Ctrl Pts',(195.24976627368,-0.842374427875423,125.957004101464));
#21645=CARTESIAN_POINT('Ctrl Pts',(195.242275937918,-0.971227371730748,
125.982960358834));
#21646=CARTESIAN_POINT('Ctrl Pts',(195.234501603799,-1.10496581411534,126.009900755591));
#21647=CARTESIAN_POINT('Ctrl Pts',(195.22672726968,-1.23779430956464,126.042452598076));
#21648=CARTESIAN_POINT('Ctrl Pts',(195.218952935561,-1.36920532069673,126.080542262435));
#21649=CARTESIAN_POINT('Ctrl Pts',(195.211188182614,-1.50045437950196,126.118584984687));
#21650=CARTESIAN_POINT('Ctrl Pts',(195.203423429667,-1.63028905794107,126.162151841558));
#21651=CARTESIAN_POINT('Ctrl Pts',(195.19565867672,-1.7582108487659,126.211118007625));
#21652=CARTESIAN_POINT('Ctrl Pts',(195.187901635835,-1.88600558586439,126.260035539804));
#21653=CARTESIAN_POINT('Ctrl Pts',(195.18014459495,-2.01189085348242,126.314341570363));
#21654=CARTESIAN_POINT('Ctrl Pts',(195.172387554065,-2.13538252951149,126.373861264766));
#21655=CARTESIAN_POINT('Ctrl Pts',(195.164636362824,-2.25878107950726,126.433336074905));
#21656=CARTESIAN_POINT('Ctrl Pts',(195.156885171584,-2.37978927994142,126.498016554088));
#21657=CARTESIAN_POINT('Ctrl Pts',(195.149133980344,-2.49794259036277,126.567679619691));
#21658=CARTESIAN_POINT('Ctrl Pts',(195.141386083567,-2.61604568247549,126.637313076633));
#21659=CARTESIAN_POINT('Ctrl Pts',(195.13363818679,-2.73129596186393,126.711924709835));
#21660=CARTESIAN_POINT('Ctrl Pts',(195.125890290013,-2.84325332954889,126.791245422794));
#21661=CARTESIAN_POINT('Ctrl Pts',(195.118144013929,-2.95518727816587,126.87054954357));
#21662=CARTESIAN_POINT('Ctrl Pts',(195.110397737845,-3.06382936634111,126.954560558935));
#21663=CARTESIAN_POINT('Ctrl Pts',(195.102651461761,-3.16876868447561,127.042966183744));
#21664=CARTESIAN_POINT('Ctrl Pts',(195.094905128495,-3.27370877724855,127.131372461143));
#21665=CARTESIAN_POINT('Ctrl Pts',(195.08715879523,-3.37494574643612,127.224173160824));
#21666=CARTESIAN_POINT('Ctrl Pts',(195.079412461965,-3.47210228418942,127.321016134081));
#21667=CARTESIAN_POINT('Ctrl Pts',(195.071664393962,-3.56928057947593,127.41788079465));
#21668=CARTESIAN_POINT('Ctrl Pts',(195.063916325959,-3.6623763481555,127.518789254161));
#21669=CARTESIAN_POINT('Ctrl Pts',(195.056168257956,-3.75104990871693,127.62335328579));
#21670=CARTESIAN_POINT('Ctrl Pts',(195.048411955214,-3.83981771259343,127.728028449315));
#21671=CARTESIAN_POINT('Ctrl Pts',(195.040655652472,-3.92415366637445,127.836366647376));
#21672=CARTESIAN_POINT('Ctrl Pts',(195.03289934973,-4.00375875951405,127.947946981883));
#21673=CARTESIAN_POINT('Ctrl Pts',(195.025138907216,-4.08340634028877,128.059586870174));
#21674=CARTESIAN_POINT('Ctrl Pts',(195.017378464702,-4.15831781570031,128.174472015597));
#21675=CARTESIAN_POINT('Ctrl Pts',(195.009618022188,-4.22823870262148,128.292154309128));
#21676=CARTESIAN_POINT('Ctrl Pts',(195.001845121922,-4.29827183275764,128.410025516725));
#21677=CARTESIAN_POINT('Ctrl Pts',(194.994072221657,-4.36329817963602,128.530702500966));
#21678=CARTESIAN_POINT('Ctrl Pts',(194.986299321391,-4.42310983539823,128.65371363433));
#21679=CARTESIAN_POINT('Ctrl Pts',(194.978808985629,-4.48074718681689,128.772253003149));
#21680=CARTESIAN_POINT('Ctrl Pts',(194.971318649867,-4.53354227567348,128.892959480803));
#21681=CARTESIAN_POINT('Ctrl Pts',(194.963828314105,-4.58135270478999,129.015397102898));
#21682=CARTESIAN_POINT('Ctrl Pts',(194.954994481147,-4.63773860762726,129.159795636662));
#21683=CARTESIAN_POINT('Ctrl Pts',(194.946160648188,-4.68734145347547,129.306984074171));
#21684=CARTESIAN_POINT('Ctrl Pts',(194.937326815229,-4.72991114124837,129.456353325896));
#21685=CARTESIAN_POINT('Ctrl Pts',(194.934850059303,-4.74184647294076,129.498232222765));
#21686=CARTESIAN_POINT('Ctrl Pts',(194.932373303377,-4.75322921960265,129.540282405251));
#21687=CARTESIAN_POINT('Ctrl Pts',(194.92989654745,-4.76405452823406,129.582490119308));
#21688=CARTESIAN_POINT('Origin',(213.235140564004,0.,130.804360617566));
#21689=CARTESIAN_POINT('',(192.834981455508,-4.76405452823404,129.582490119308));
#21690=CARTESIAN_POINT('',(193.179932595466,-4.75726252818781,129.584191622251));
#21691=CARTESIAN_POINT('',(213.235140564004,-4.76405452823405,129.582490119308));
#21692=CARTESIAN_POINT('',(194.514859435944,-4.91824832267119,130.808422518846));
#21693=CARTESIAN_POINT('Ctrl Pts',(194.514859435944,-4.91824832267119,130.808422518846));
#21694=CARTESIAN_POINT('Ctrl Pts',(194.505690899192,-4.91811426966856,130.970737137015));
#21695=CARTESIAN_POINT('Ctrl Pts',(194.49652236244,-4.90994121534633,131.132707678005));
#21696=CARTESIAN_POINT('Ctrl Pts',(194.487353825688,-4.89385416878415,131.293619687154));
#21697=CARTESIAN_POINT('Ctrl Pts',(194.478119857513,-4.87765231673291,131.45568004767));
#21698=CARTESIAN_POINT('Ctrl Pts',(194.468885889339,-4.85342321642564,131.616666662758));
#21699=CARTESIAN_POINT('Ctrl Pts',(194.459651921164,-4.82134334935995,131.775870458012));
#21700=CARTESIAN_POINT('Ctrl Pts',(194.450346899683,-4.78901663493732,131.936299290638));
#21701=CARTESIAN_POINT('Ctrl Pts',(194.441041878201,-4.74871793267665,132.094917714119));
#21702=CARTESIAN_POINT('Ctrl Pts',(194.43173685672,-4.70067592055807,132.251021929825));
#21703=CARTESIAN_POINT('Ctrl Pts',(194.429998592026,-4.69170122515761,132.280183651511));
#21704=CARTESIAN_POINT('Ctrl Pts',(194.428260327332,-4.68245643851761,132.309257694875));
#21705=CARTESIAN_POINT('Ctrl Pts',(194.426522062638,-4.67294323328106,132.338239557063));
#21706=CARTESIAN_POINT('Ctrl Pts',(194.418747728519,-4.63039572235757,132.467860023283));
#21707=CARTESIAN_POINT('Ctrl Pts',(194.4109733944,-4.58238351476863,132.595914150803));
#21708=CARTESIAN_POINT('Ctrl Pts',(194.403199060281,-4.5290396636491,132.721906650284));
#21709=CARTESIAN_POINT('Ctrl Pts',(194.395434307334,-4.47576155405861,132.84774387527));
#21710=CARTESIAN_POINT('Ctrl Pts',(194.387669554386,-4.41716502578731,132.971524171027));
#21711=CARTESIAN_POINT('Ctrl Pts',(194.379904801439,-4.35343290862853,133.092767262498));
#21712=CARTESIAN_POINT('Ctrl Pts',(194.372147760554,-4.28976409110701,133.213889933622));
#21713=CARTESIAN_POINT('Ctrl Pts',(194.364390719669,-4.22097001613394,133.332480071522));
#21714=CARTESIAN_POINT('Ctrl Pts',(194.356633678784,-4.14728147357108,133.448077592107));
#21715=CARTESIAN_POINT('Ctrl Pts',(194.348882487544,-4.07364850011134,133.563587939702));
#21716=CARTESIAN_POINT('Ctrl Pts',(194.341131296304,-3.99512861499202,133.676109833574));
#21717=CARTESIAN_POINT('Ctrl Pts',(194.333380105064,-3.91199820569556,133.785208332753));
#21718=CARTESIAN_POINT('Ctrl Pts',(194.325632208287,-3.82890312904064,133.894260462159));
#21719=CARTESIAN_POINT('Ctrl Pts',(194.31788431151,-3.74120166215483,133.999891780499));
#21720=CARTESIAN_POINT('Ctrl Pts',(194.310136414733,-3.64921299757971,134.101697051841));
#21721=CARTESIAN_POINT('Ctrl Pts',(194.302390138649,-3.55724357505019,134.203481027715));
#21722=CARTESIAN_POINT('Ctrl Pts',(194.294643862565,-3.46098900054278,134.301440258582));
#21723=CARTESIAN_POINT('Ctrl Pts',(194.286897586481,-3.3608079054297,134.395203594542));
#21724=CARTESIAN_POINT('Ctrl Pts',(194.279151253215,-3.26062607080245,134.488967622642));
#21725=CARTESIAN_POINT('Ctrl Pts',(194.27140491995,-3.15651794317866,134.578535426871));
#21726=CARTESIAN_POINT('Ctrl Pts',(194.263658586685,-3.04887776981329,134.663573932121));
#21727=CARTESIAN_POINT('Ctrl Pts',(194.255910518682,-2.94121349117735,134.748631481155));
#21728=CARTESIAN_POINT('Ctrl Pts',(194.248162450679,-2.83001589956761,134.829157470545));
#21729=CARTESIAN_POINT('Ctrl Pts',(194.240414382676,-2.71571062383656,134.904860449304));
#21730=CARTESIAN_POINT('Ctrl Pts',(194.232658079934,-2.60128386309834,134.980643886089));
#21731=CARTESIAN_POINT('Ctrl Pts',(194.224901777192,-2.48374314685267,135.051593856377));
#21732=CARTESIAN_POINT('Ctrl Pts',(194.21714547445,-2.36354174294401,135.11746315424));
#21733=CARTESIAN_POINT('Ctrl Pts',(194.209385031936,-2.24327618392683,135.18336760853));
#21734=CARTESIAN_POINT('Ctrl Pts',(194.201624589422,-2.12034745785099,135.244185813801));
#21735=CARTESIAN_POINT('Ctrl Pts',(194.193864146908,-1.99523059395582,135.299717993731));
#21736=CARTESIAN_POINT('Ctrl Pts',(194.186091246642,-1.86991288136339,135.355339318846));
#21737=CARTESIAN_POINT('Ctrl Pts',(194.178318346377,-1.74240037555429,135.4056575181));
#21738=CARTESIAN_POINT('Ctrl Pts',(194.170545446111,-1.61318595870733,135.450521842182));
#21739=CARTESIAN_POINT('Ctrl Pts',(194.16305511035,-1.48866881138538,135.493755235078));
#21740=CARTESIAN_POINT('Ctrl Pts',(194.155564774588,-1.36257163707573,135.531924303522));
#21741=CARTESIAN_POINT('Ctrl Pts',(194.148074438826,-1.23534416706417,135.564939138229));
#21742=CARTESIAN_POINT('Ctrl Pts',(194.140300104707,-1.10329282885606,135.599205740429));
#21743=CARTESIAN_POINT('Ctrl Pts',(194.132525770587,-0.969605493727146,
135.628028094229));
#21744=CARTESIAN_POINT('Ctrl Pts',(194.124751436468,-0.834770781094737,
135.651250425013));
#21745=CARTESIAN_POINT('Ctrl Pts',(194.116986683521,-0.700102240195215,
135.67444413635));
#21746=CARTESIAN_POINT('Ctrl Pts',(194.109221930574,-0.564289516904608,
135.692051490933));
#21747=CARTESIAN_POINT('Ctrl Pts',(194.101457177627,-0.427835504199164,
135.703966708248));
#21748=CARTESIAN_POINT('Ctrl Pts',(194.093700136742,-0.29151701954285,135.715870091201));
#21749=CARTESIAN_POINT('Ctrl Pts',(194.085943095857,-0.154558899969262,
135.722092553836));
#21750=CARTESIAN_POINT('Ctrl Pts',(194.078186054972,-0.0174729748113956,
135.722579579513));
#21751=CARTESIAN_POINT('Ctrl Pts',(194.070434863732,0.119509572784076,135.723066237919));
#21752=CARTESIAN_POINT('Ctrl Pts',(194.062683672492,0.256619344746097,135.717826066908));
#21753=CARTESIAN_POINT('Ctrl Pts',(194.054932481252,0.393341018732792,135.706856502876));
#21754=CARTESIAN_POINT('Ctrl Pts',(194.047184584475,0.530004582360826,135.695891601202));
#21755=CARTESIAN_POINT('Ctrl Pts',(194.039436687697,0.666279987193505,135.679202181027));
#21756=CARTESIAN_POINT('Ctrl Pts',(194.03168879092,0.801653765399529,135.656837748158));
#21757=CARTESIAN_POINT('Ctrl Pts',(194.023942514836,0.936999226329496,135.634477993447));
#21758=CARTESIAN_POINT('Ctrl Pts',(194.016196238752,1.07144305027789,135.606445650913));
#21759=CARTESIAN_POINT('Ctrl Pts',(194.008449962668,1.20447912930477,135.572841831702));
#21760=CARTESIAN_POINT('Ctrl Pts',(194.000703629403,1.33751619037367,135.539237764435));
#21761=CARTESIAN_POINT('Ctrl Pts',(193.992957296137,1.46914510672559,135.50006223417));
#21762=CARTESIAN_POINT('Ctrl Pts',(193.985210962872,1.59887255256962,135.455466897059));
#21763=CARTESIAN_POINT('Ctrl Pts',(193.977462894869,1.72862904997563,135.410861573131));
#21764=CARTESIAN_POINT('Ctrl Pts',(193.969714826866,1.85648285988052,135.360834154252));
#21765=CARTESIAN_POINT('Ctrl Pts',(193.961966758863,1.98195871352415,135.305585197654));
#21766=CARTESIAN_POINT('Ctrl Pts',(193.954210456121,2.10756792439832,135.250277521806));
#21767=CARTESIAN_POINT('Ctrl Pts',(193.946454153379,2.2307937720316,135.189737380293));
#21768=CARTESIAN_POINT('Ctrl Pts',(193.938697850637,2.35118327273367,135.124212499346));
#21769=CARTESIAN_POINT('Ctrl Pts',(193.930937408123,2.47163702893723,135.058652645797));
#21770=CARTESIAN_POINT('Ctrl Pts',(193.923176965609,2.58925108663829,134.988102952543));
#21771=CARTESIAN_POINT('Ctrl Pts',(193.915416523095,2.70360060345122,134.912855091156));
#21772=CARTESIAN_POINT('Ctrl Pts',(193.907643622829,2.81813368425998,134.837486435221));
#21773=CARTESIAN_POINT('Ctrl Pts',(193.899870722564,2.92939143443346,134.757404768529));
#21774=CARTESIAN_POINT('Ctrl Pts',(193.892097822299,3.03698060945102,134.672943283132));
#21775=CARTESIAN_POINT('Ctrl Pts',(193.884607486536,3.14065864695626,134.591552185475));
#21776=CARTESIAN_POINT('Ctrl Pts',(193.877117150774,3.24092996805332,134.506094375295));
#21777=CARTESIAN_POINT('Ctrl Pts',(193.869626815012,3.33747583876709,134.416899626095));
#21778=CARTESIAN_POINT('Ctrl Pts',(193.861852480893,3.43768227551313,134.32432303087));
#21779=CARTESIAN_POINT('Ctrl Pts',(193.854078146774,3.53419260818798,134.227427275858));
#21780=CARTESIAN_POINT('Ctrl Pts',(193.846303812655,3.62661166846604,134.126539250428));
#21781=CARTESIAN_POINT('Ctrl Pts',(193.838539059708,3.71891683051201,134.025775560474));
#21782=CARTESIAN_POINT('Ctrl Pts',(193.830774306761,3.80714049093836,133.921029675189));
#21783=CARTESIAN_POINT('Ctrl Pts',(193.823009553814,3.8909218276634,133.812667515725));
#21784=CARTESIAN_POINT('Ctrl Pts',(193.815252512929,3.97461995158371,133.704412983086));
#21785=CARTESIAN_POINT('Ctrl Pts',(193.807495472044,4.05388429464595,133.59254963128));
#21786=CARTESIAN_POINT('Ctrl Pts',(193.799738431159,4.12839233419866,133.477478609243));
#21787=CARTESIAN_POINT('Ctrl Pts',(193.791987239919,4.20284418665918,133.36249436316));
#21788=CARTESIAN_POINT('Ctrl Pts',(193.784236048679,4.27254666321562,133.244307588428));
#21789=CARTESIAN_POINT('Ctrl Pts',(193.776484857438,4.33721906272395,133.123350454638));
#21790=CARTESIAN_POINT('Ctrl Pts',(193.768736960661,4.40186397473727,133.002444730857));
#21791=CARTESIAN_POINT('Ctrl Pts',(193.760989063884,4.46148287789932,132.878771333985));
#21792=CARTESIAN_POINT('Ctrl Pts',(193.753241167107,4.51583988094174,132.752789018148));
#21793=CARTESIAN_POINT('Ctrl Pts',(193.745494891023,4.57018551367091,132.626833055096));
#21794=CARTESIAN_POINT('Ctrl Pts',(193.737748614939,4.61927128079769,132.498569492494));
#21795=CARTESIAN_POINT('Ctrl Pts',(193.730002338855,4.66290868628648,132.368478786329));
#21796=CARTESIAN_POINT('Ctrl Pts',(193.72225600559,4.70654641389667,132.238387119863));
#21797=CARTESIAN_POINT('Ctrl Pts',(193.714509672324,4.74473557527959,132.106468653588));
#21798=CARTESIAN_POINT('Ctrl Pts',(193.706763339059,4.77733710840989,131.973220410317));
#21799=CARTESIAN_POINT('Ctrl Pts',(193.699015271056,4.80994594242749,131.839942327026));
#21800=CARTESIAN_POINT('Ctrl Pts',(193.691267203053,4.83696456533113,131.705334253853));
#21801=CARTESIAN_POINT('Ctrl Pts',(193.68351913505,4.85830481722543,131.569904453949));
#21802=CARTESIAN_POINT('Ctrl Pts',(193.675762832308,4.87966774979339,131.434330717642));
#21803=CARTESIAN_POINT('Ctrl Pts',(193.668006529566,4.89534019475674,131.297933896828));
#21804=CARTESIAN_POINT('Ctrl Pts',(193.660250226825,4.9052857224612,131.161229001593));
#21805=CARTESIAN_POINT('Ctrl Pts',(193.65248978431,4.91523655839326,131.02445114284));
#21806=CARTESIAN_POINT('Ctrl Pts',(193.644729341796,4.91945437445847,130.887365272617));
#21807=CARTESIAN_POINT('Ctrl Pts',(193.636968899282,4.9179549245226,130.750486478465));
#21808=CARTESIAN_POINT('Ctrl Pts',(193.629195999017,4.91645306753658,130.613387954321));
#21809=CARTESIAN_POINT('Ctrl Pts',(193.621423098751,4.90921562490836,130.476497561166));
#21810=CARTESIAN_POINT('Ctrl Pts',(193.613650198486,4.89631036227887,130.340326245196));
#21811=CARTESIAN_POINT('Ctrl Pts',(193.606159862724,4.88387423845236,130.209105099557));
#21812=CARTESIAN_POINT('Ctrl Pts',(193.598669526962,4.86617526077355,130.078551963462));
#21813=CARTESIAN_POINT('Ctrl Pts',(193.5911791912,4.84331859353017,129.949113247465));
#21814=CARTESIAN_POINT('Ctrl Pts',(193.583404857081,4.81959530880109,129.814766823208));
#21815=CARTESIAN_POINT('Ctrl Pts',(193.575630522962,4.79024035808555,129.68119542462));
#21816=CARTESIAN_POINT('Ctrl Pts',(193.567856188842,4.75531516453582,129.548908209692));
#21817=CARTESIAN_POINT('Ctrl Pts',(193.560091435895,4.7204330131658,129.416784026935));
#21818=CARTESIAN_POINT('Ctrl Pts',(193.552326682948,4.67999437676145,129.285941253237));
#21819=CARTESIAN_POINT('Ctrl Pts',(193.544561930001,4.63411208200157,129.156881247757));
#21820=CARTESIAN_POINT('Ctrl Pts',(193.536804889116,4.5882753581837,129.027949426493));
#21821=CARTESIAN_POINT('Ctrl Pts',(193.529047848231,4.53700586573875,128.900797215727));
#21822=CARTESIAN_POINT('Ctrl Pts',(193.521290807346,4.48046677125739,128.775912793697));
#21823=CARTESIAN_POINT('Ctrl Pts',(193.513539616106,4.42397031334695,128.651122547982));
#21824=CARTESIAN_POINT('Ctrl Pts',(193.505788424866,4.36221232369776,128.528597041763));
#21825=CARTESIAN_POINT('Ctrl Pts',(193.498037233626,4.29540467300197,128.408806035084));
#21826=CARTESIAN_POINT('Ctrl Pts',(193.490289336849,4.22862541733986,128.289065942777));
#21827=CARTESIAN_POINT('Ctrl Pts',(193.482541440072,4.1568009593707,128.172058379152));
#21828=CARTESIAN_POINT('Ctrl Pts',(193.474793543294,4.08018975694076,128.058229774023));
#21829=CARTESIAN_POINT('Ctrl Pts',(193.46704726721,4.00359457992282,127.944424979385));
#21830=CARTESIAN_POINT('Ctrl Pts',(193.459300991126,3.92221486821154,127.833798144722));
#21831=CARTESIAN_POINT('Ctrl Pts',(193.451554715042,3.83635295632385,127.726767555284));
#21832=CARTESIAN_POINT('Ctrl Pts',(193.443808381777,3.75049041062306,127.619736175771));
#21833=CARTESIAN_POINT('Ctrl Pts',(193.436062048511,3.66014584337031,127.516301399417));
#21834=CARTESIAN_POINT('Ctrl Pts',(193.428315715246,3.56566224751357,127.416848876013));
#21835=CARTESIAN_POINT('Ctrl Pts',(193.420567647243,3.47115749271066,127.317374080907));
#21836=CARTESIAN_POINT('Ctrl Pts',(193.41281957924,3.3725121340977,127.221883596716));
#21837=CARTESIAN_POINT('Ctrl Pts',(193.405071511237,3.27010613528105,127.130726323506));
#21838=CARTESIAN_POINT('Ctrl Pts',(193.397315208495,3.16759129815017,127.03947216726));
#21839=CARTESIAN_POINT('Ctrl Pts',(193.389558905753,3.06130812916382,126.952560682118));
#21840=CARTESIAN_POINT('Ctrl Pts',(193.381802603011,2.95167022977636,126.870300892911));
#21841=CARTESIAN_POINT('Ctrl Pts',(193.374042160497,2.8419738133408,126.787997199178));
#21842=CARTESIAN_POINT('Ctrl Pts',(193.366281717983,2.72891942085808,126.710350369704));
#21843=CARTESIAN_POINT('Ctrl Pts',(193.358521275469,2.61294892541234,126.637625567711));
#21844=CARTESIAN_POINT('Ctrl Pts',(193.350748375203,2.49679226383197,126.564784021411));
#21845=CARTESIAN_POINT('Ctrl Pts',(193.342975474938,2.37771048460871,126.496880485635));
#21846=CARTESIAN_POINT('Ctrl Pts',(193.335202574673,2.25617009023159,126.434134126131));
#21847=CARTESIAN_POINT('Ctrl Pts',(193.32771223891,2.13904799533144,126.373668754842));
#21848=CARTESIAN_POINT('Ctrl Pts',(193.320221903148,2.01964321472039,126.317992247027));
#21849=CARTESIAN_POINT('Ctrl Pts',(193.312731567386,1.89838817010611,126.2672574208));
#21850=CARTESIAN_POINT('Ctrl Pts',(193.304957233267,1.77253570362098,126.214598968217));
#21851=CARTESIAN_POINT('Ctrl Pts',(193.297182899148,1.64429123515347,126.167097516029));
#21852=CARTESIAN_POINT('Ctrl Pts',(193.289408565029,1.51411633445749,126.124976599532));
#21853=CARTESIAN_POINT('Ctrl Pts',(193.281643812082,1.38410186269265,126.082907593301));
#21854=CARTESIAN_POINT('Ctrl Pts',(193.273879059135,1.25216206077593,126.046206048193));
#21855=CARTESIAN_POINT('Ctrl Pts',(193.266114306188,1.11877972194069,126.015048036801));
#21856=CARTESIAN_POINT('Ctrl Pts',(193.258357265303,0.985529860324888,125.983920971985));
#21857=CARTESIAN_POINT('Ctrl Pts',(193.250600224418,0.850840691275775,125.958326572221));
#21858=CARTESIAN_POINT('Ctrl Pts',(193.242843183533,0.715211128500449,125.9383914331));
#21859=CARTESIAN_POINT('Ctrl Pts',(193.235091992293,0.579683845033364,125.918471327223));
#21860=CARTESIAN_POINT('Ctrl Pts',(193.227340801053,0.443217964620638,125.904202044029));
#21861=CARTESIAN_POINT('Ctrl Pts',(193.219589609812,0.306323230974984,125.895659247482));
#21862=CARTESIAN_POINT('Ctrl Pts',(193.211841713035,0.169486681242845,125.887120081852));
#21863=CARTESIAN_POINT('Ctrl Pts',(193.204093816258,0.0322220301962203,
125.884302586307));
#21864=CARTESIAN_POINT('Ctrl Pts',(193.196345919481,-0.10495542533834,125.887230619163));
#21865=CARTESIAN_POINT('Ctrl Pts',(193.188599643397,-0.24210418630643,125.890158039538));
#21866=CARTESIAN_POINT('Ctrl Pts',(193.180853367313,-0.379165397413132,
125.898828589448));
#21867=CARTESIAN_POINT('Ctrl Pts',(193.173107091229,-0.515623724240199,
125.913213999696));
#21868=CARTESIAN_POINT('Ctrl Pts',(193.165360757964,-0.65208305837159,125.927599516134));
#21869=CARTESIAN_POINT('Ctrl Pts',(193.157614424698,-0.787939110532302,
125.947699936101));
#21870=CARTESIAN_POINT('Ctrl Pts',(193.149868091433,-0.922682026564098,
125.973435143047));
#21871=CARTESIAN_POINT('Ctrl Pts',(193.14212002343,-1.05745511733767,125.999176113215));
#21872=CARTESIAN_POINT('Ctrl Pts',(193.134371955427,-1.19111419199571,126.030554308008));
#21873=CARTESIAN_POINT('Ctrl Pts',(193.126623887424,-1.32316033142207,126.06743864229));
#21874=CARTESIAN_POINT('Ctrl Pts',(193.118867584682,-1.45534681105682,126.104362177682));
#21875=CARTESIAN_POINT('Ctrl Pts',(193.11111128194,-1.58591655391597,126.146803437196));
#21876=CARTESIAN_POINT('Ctrl Pts',(193.103354979199,-1.71438600696752,126.194581481684));
#21877=CARTESIAN_POINT('Ctrl Pts',(193.095594536684,-1.84292402803436,126.242385026753));
#21878=CARTESIAN_POINT('Ctrl Pts',(193.08783409417,-1.96935916538758,126.295530881055));
#21879=CARTESIAN_POINT('Ctrl Pts',(193.080073651656,-2.09322948650229,126.35379061145));
#21880=CARTESIAN_POINT('Ctrl Pts',(193.072300751391,-2.21729865525309,126.412143865536));
#21881=CARTESIAN_POINT('Ctrl Pts',(193.064527851125,-2.33879443343359,126.475627219245));
#21882=CARTESIAN_POINT('Ctrl Pts',(193.05675495086,-2.45728027470416,126.54396665526));
#21883=CARTESIAN_POINT('Ctrl Pts',(193.049264615098,-2.57145885719628,126.609821780639));
#21884=CARTESIAN_POINT('Ctrl Pts',(193.041774279336,-2.68284228060499,126.680185891838));
#21885=CARTESIAN_POINT('Ctrl Pts',(193.034283943574,-2.791068240227,126.75477778215));
#21886=CARTESIAN_POINT('Ctrl Pts',(193.026549215124,-2.90282536774334,126.831803436867));
#21887=CARTESIAN_POINT('Ctrl Pts',(193.018814486674,-3.01157783489076,126.913587324279));
#21888=CARTESIAN_POINT('Ctrl Pts',(193.011079758224,-3.11689046048007,126.99986631216));
#21889=CARTESIAN_POINT('Ctrl Pts',(193.003357254067,-3.22203664554232,127.086008941079));
#21890=CARTESIAN_POINT('Ctrl Pts',(192.995634749909,-3.32375351182408,127.176632275114));
#21891=CARTESIAN_POINT('Ctrl Pts',(192.987912245751,-3.42163455168092,127.271429814784));
#21892=CARTESIAN_POINT('Ctrl Pts',(192.980196799127,-3.51942613885007,127.366140719753));
#21893=CARTESIAN_POINT('Ctrl Pts',(192.972481352503,-3.613388589409,127.465017970231));
#21894=CARTESIAN_POINT('Ctrl Pts',(192.964765905879,-3.70314804461637,127.567714572328));
#21895=CARTESIAN_POINT('Ctrl Pts',(192.957055793399,-3.79284544381304,127.670340174201));
#21896=CARTESIAN_POINT('Ctrl Pts',(192.949345680918,-3.87834536897914,127.776779578253));
#21897=CARTESIAN_POINT('Ctrl Pts',(192.941635568438,-3.95931079161108,127.886648994062));
#21898=CARTESIAN_POINT('Ctrl Pts',(192.933929070916,-4.04023825284938,127.99646689657));
#21899=CARTESIAN_POINT('Ctrl Pts',(192.926222573394,-4.11663520834471,128.109711292731));
#21900=CARTESIAN_POINT('Ctrl Pts',(192.918516075872,-4.18820520986374,128.225965732648));
#21901=CARTESIAN_POINT('Ctrl Pts',(192.910809982444,-4.25977145856918,128.342214076698));
#21902=CARTESIAN_POINT('Ctrl Pts',(192.903103889017,-4.32651104118669,128.461471819057));
#21903=CARTESIAN_POINT('Ctrl Pts',(192.895397795589,-4.3881712193687,128.583294114283));
#21904=CARTESIAN_POINT('Ctrl Pts',(192.887692066741,-4.44982848037876,128.705110646039));
#21905=CARTESIAN_POINT('Ctrl Pts',(192.879986337892,-4.50640664147058,128.829491133795));
#21906=CARTESIAN_POINT('Ctrl Pts',(192.872280609043,-4.55769962141508,128.955967471222));
#21907=CARTESIAN_POINT('Ctrl Pts',(192.864570878078,-4.60901924134692,129.082509496546));
#21908=CARTESIAN_POINT('Ctrl Pts',(192.856861147112,-4.65504805292081,129.211149177261));
#21909=CARTESIAN_POINT('Ctrl Pts',(192.849151416146,-4.69562867427047,129.341399778764));
#21910=CARTESIAN_POINT('Ctrl Pts',(192.844428095933,-4.72049014737659,129.421197024804));
#21911=CARTESIAN_POINT('Ctrl Pts',(192.839704775721,-4.74330770610149,129.50159857469));
#21912=CARTESIAN_POINT('Ctrl Pts',(192.834981455508,-4.76405452823404,129.582490119308));
#21913=CARTESIAN_POINT('Ctrl Pts',(194.584773235637,-4.76405452823405,129.582490119308));
#21914=CARTESIAN_POINT('Ctrl Pts',(194.577053952228,-4.79804027850044,129.715000043791));
#21915=CARTESIAN_POINT('Ctrl Pts',(194.569334668819,-4.82650137584579,129.848960603857));
#21916=CARTESIAN_POINT('Ctrl Pts',(194.56161538541,-4.84932764823365,129.983870262609));
#21917=CARTESIAN_POINT('Ctrl Pts',(194.553822727173,-4.87237089332568,130.120062290773));
#21918=CARTESIAN_POINT('Ctrl Pts',(194.546030068937,-4.88967153265256,130.257221158943));
#21919=CARTESIAN_POINT('Ctrl Pts',(194.5382374107,-4.90116937806975,130.394822109033));
#21920=CARTESIAN_POINT('Ctrl Pts',(194.530444752464,-4.91266722348695,130.532423059123));
#21921=CARTESIAN_POINT('Ctrl Pts',(194.522652094227,-4.91836225895716,130.670465679262));
#21922=CARTESIAN_POINT('Ctrl Pts',(194.514859435991,-4.91824832267189,130.808422518005));
#21923=CARTESIAN_POINT('',(194.860140564008,-4.91266024513891,130.801203006911));
#21924=CARTESIAN_POINT('Ctrl Pts',(194.92989654745,-4.76405452823406,129.582490119308));
#21925=CARTESIAN_POINT('Ctrl Pts',(194.921111692065,-4.80245103303602,129.732197508783));
#21926=CARTESIAN_POINT('Ctrl Pts',(194.912326836681,-4.83383095715299,129.883888334153));
#21927=CARTESIAN_POINT('Ctrl Pts',(194.903541981296,-4.85800796205853,130.036935244597));
#21928=CARTESIAN_POINT('Ctrl Pts',(194.894810448159,-4.88203821756628,130.189053192086));
#21929=CARTESIAN_POINT('Ctrl Pts',(194.886078915021,-4.89895263873311,130.342510630792));
#21930=CARTESIAN_POINT('Ctrl Pts',(194.877347381884,-4.90861601348531,130.496672634935));
#21931=CARTESIAN_POINT('Ctrl Pts',(194.871611775925,-4.9149637314563,130.597939216148));
#21932=CARTESIAN_POINT('Ctrl Pts',(194.865876169967,-4.91818362286876,130.699509432803));
#21933=CARTESIAN_POINT('Ctrl Pts',(194.860140564008,-4.9182489840691,130.801199414751));
#21934=CARTESIAN_POINT('Ctrl Pts',(194.860140564008,-4.91221266644762,130.801203294592));
#21935=CARTESIAN_POINT('Ctrl Pts',(194.80188727277,-4.90617542648731,131.832747380102));
#21936=CARTESIAN_POINT('Ctrl Pts',(194.650818106927,-4.08404315233992,134.516670434198));
#21937=CARTESIAN_POINT('Ctrl Pts',(194.406933066479,0.327902356760881,136.612472175972));
#21938=CARTESIAN_POINT('Ctrl Pts',(194.128485442666,5.06376798164403,133.667913246476));
#21939=CARTESIAN_POINT('Ctrl Pts',(193.850037818853,5.14627821021483,128.091889343334));
#21940=CARTESIAN_POINT('Ctrl Pts',(193.57159019504,0.499610173265479,125.008494029623));
#21941=CARTESIAN_POINT('Ctrl Pts',(193.348221787245,-3.59620912304385,126.807588037525));
#21942=CARTESIAN_POINT('Ctrl Pts',(193.217669254053,-4.59434972149962,128.935771315469));
#21943=CARTESIAN_POINT('Ctrl Pts',(193.179932595466,-4.75726252818781,129.584191622251));
#21944=CARTESIAN_POINT('Origin',(213.235140564004,0.,130.804360617566));
#21945=CARTESIAN_POINT('',(191.084784152919,-4.76405452823405,129.582490119308));
#21946=CARTESIAN_POINT('',(191.430300680169,-4.76051597898721,129.583432241588));
#21947=CARTESIAN_POINT('',(213.235140564004,-4.76405452823405,129.582490119308));
#21948=CARTESIAN_POINT('',(192.764859436031,-4.9182499011834,130.805346522958));
#21949=CARTESIAN_POINT('Ctrl Pts',(192.764859435991,-4.91824990118326,130.805346523653));
#21950=CARTESIAN_POINT('Ctrl Pts',(192.761851730581,-4.91823931916517,130.85813553689));
#21951=CARTESIAN_POINT('Ctrl Pts',(192.758844025171,-4.91737886410589,130.910915070119));
#21952=CARTESIAN_POINT('Ctrl Pts',(192.755836319761,-4.91566928905583,130.963666936127));
#21953=CARTESIAN_POINT('Ctrl Pts',(192.748061985642,-4.91125036970399,131.100020260621));
#21954=CARTESIAN_POINT('Ctrl Pts',(192.740287651523,-4.90114679519269,131.236405558342));
#21955=CARTESIAN_POINT('Ctrl Pts',(192.732513317404,-4.88534711553905,131.372310107569));
#21956=CARTESIAN_POINT('Ctrl Pts',(192.724748564456,-4.86956690757853,131.508047166585));
#21957=CARTESIAN_POINT('Ctrl Pts',(192.716983811509,-4.84810460677939,131.643304271342));
#21958=CARTESIAN_POINT('Ctrl Pts',(192.709219058562,-4.82100075318953,131.77756912567));
#21959=CARTESIAN_POINT('Ctrl Pts',(192.701462017677,-4.79392381952918,131.911700626251));
#21960=CARTESIAN_POINT('Ctrl Pts',(192.693704976792,-4.76121656070021,132.044841456872));
#21961=CARTESIAN_POINT('Ctrl Pts',(192.685947935907,-4.72297121766863,132.176485225455));
#21962=CARTESIAN_POINT('Ctrl Pts',(192.678196744667,-4.68475471574775,132.308029720448));
#21963=CARTESIAN_POINT('Ctrl Pts',(192.670445553427,-4.6410085509534,132.43807902658));
#21964=CARTESIAN_POINT('Ctrl Pts',(192.662694362187,-4.59187578910414,132.56613807228));
#21965=CARTESIAN_POINT('Ctrl Pts',(192.65494646541,-4.54276390998926,132.69414268947));
#21966=CARTESIAN_POINT('Ctrl Pts',(192.647198568633,-4.48827012711119,132.820158364431));
#21967=CARTESIAN_POINT('Ctrl Pts',(192.639450671856,-4.42858693265309,132.943706508822));
#21968=CARTESIAN_POINT('Ctrl Pts',(192.631704395771,-4.36891622263265,133.067228809605));
#21969=CARTESIAN_POINT('Ctrl Pts',(192.623958119687,-4.30405843013184,133.188284254661));
#21970=CARTESIAN_POINT('Ctrl Pts',(192.616211843603,-4.23425347381781,133.30641588913));
#21971=CARTESIAN_POINT('Ctrl Pts',(192.608465510338,-4.16444800221951,133.42454839562));
#21972=CARTESIAN_POINT('Ctrl Pts',(192.600719177073,-4.08969549283255,133.539756711864));
#21973=CARTESIAN_POINT('Ctrl Pts',(192.592972843807,-4.01028074241126,133.65161041861));
#21974=CARTESIAN_POINT('Ctrl Pts',(192.585224775804,-3.93084820760729,133.763489174218));
#21975=CARTESIAN_POINT('Ctrl Pts',(192.577476707801,-3.84675158046991,133.872011506716));
#21976=CARTESIAN_POINT('Ctrl Pts',(192.569728639798,-3.7583174692179,133.976778128404));
#21977=CARTESIAN_POINT('Ctrl Pts',(192.561972337057,-3.66978936913993,134.081656097304));
#21978=CARTESIAN_POINT('Ctrl Pts',(192.554216034315,-3.57691482870239,134.182770082479));
#21979=CARTESIAN_POINT('Ctrl Pts',(192.546459731573,-3.4800594120266,134.279755494593));
#21980=CARTESIAN_POINT('Ctrl Pts',(192.538699289059,-3.38315230069857,134.376792670742));
#21981=CARTESIAN_POINT('Ctrl Pts',(192.530938846545,-3.28226036692496,134.469696618379));
#21982=CARTESIAN_POINT('Ctrl Pts',(192.523178404031,-3.17778338449789,134.558142154058));
#21983=CARTESIAN_POINT('Ctrl Pts',(192.515405503765,-3.07313868634362,134.646729670363));
#21984=CARTESIAN_POINT('Ctrl Pts',(192.5076326035,-2.96489774802298,134.73084423263));
#21985=CARTESIAN_POINT('Ctrl Pts',(192.499859703234,-2.85349125072007,134.810202694404));
#21986=CARTESIAN_POINT('Ctrl Pts',(192.492369367472,-2.74613466020842,134.886676276202));
#21987=CARTESIAN_POINT('Ctrl Pts',(192.48487903171,-2.63583892488735,134.958733378042));
#21988=CARTESIAN_POINT('Ctrl Pts',(192.477388695948,-2.52301040503746,135.026161365893));
#21989=CARTESIAN_POINT('Ctrl Pts',(192.469614361829,-2.40590395756583,135.096145906396));
#21990=CARTESIAN_POINT('Ctrl Pts',(192.46184002771,-2.28569791514371,135.161365067826));
#21991=CARTESIAN_POINT('Ctrl Pts',(192.454065693591,-2.16281745608086,135.221532078373));
#21992=CARTESIAN_POINT('Ctrl Pts',(192.446300940644,-2.04008843620172,135.281624938458));
#21993=CARTESIAN_POINT('Ctrl Pts',(192.438536187696,-1.91469190546091,135.336677865911));
#21994=CARTESIAN_POINT('Ctrl Pts',(192.430771434749,-1.78708078602292,135.386448059631));
#21995=CARTESIAN_POINT('Ctrl Pts',(192.423014393864,-1.65959641174775,135.436168820892));
#21996=CARTESIAN_POINT('Ctrl Pts',(192.415257352979,-1.52990218788621,135.480617148817));
#21997=CARTESIAN_POINT('Ctrl Pts',(192.407500312094,-1.39847401492876,135.519596931058));
#21998=CARTESIAN_POINT('Ctrl Pts',(192.399749120854,-1.26714495297885,135.558547318341));
#21999=CARTESIAN_POINT('Ctrl Pts',(192.391997929614,-1.13408491791114,135.592037257539));
#22000=CARTESIAN_POINT('Ctrl Pts',(192.384246738374,-0.999787758028332,
135.6199195157));
#22001=CARTESIAN_POINT('Ctrl Pts',(192.376498841597,-0.865547678020963,
135.647789923158));
#22002=CARTESIAN_POINT('Ctrl Pts',(192.36875094482,-0.730071900997154,135.670057310698));
#22003=CARTESIAN_POINT('Ctrl Pts',(192.361003048043,-0.593867123607528,
135.686624938759));
#22004=CARTESIAN_POINT('Ctrl Pts',(192.353256771959,-0.457690837321097,
135.70318910123));
#22005=CARTESIAN_POINT('Ctrl Pts',(192.345510495875,-0.320786241840849,
135.714055828527));
#22006=CARTESIAN_POINT('Ctrl Pts',(192.337764219791,-0.18366746813134,135.719179975757));
#22007=CARTESIAN_POINT('Ctrl Pts',(192.330017886525,-0.0465476822422854,
135.724304160812));
#22008=CARTESIAN_POINT('Ctrl Pts',(192.32227155326,0.0907858943383346,135.723685666614));
#22009=CARTESIAN_POINT('Ctrl Pts',(192.314525219994,0.227817198101151,135.717331448616));
#22010=CARTESIAN_POINT('Ctrl Pts',(192.306777151991,0.364879189074196,135.710975807636));
#22011=CARTESIAN_POINT('Ctrl Pts',(192.299029083989,0.501638382059588,135.698881905005));
#22012=CARTESIAN_POINT('Ctrl Pts',(192.291281015986,0.637582305285388,135.681108700714));
#22013=CARTESIAN_POINT('Ctrl Pts',(192.283524713244,0.773670711330755,135.663316606849));
#22014=CARTESIAN_POINT('Ctrl Pts',(192.275768410502,0.908941728448333,135.639833204469));
#22015=CARTESIAN_POINT('Ctrl Pts',(192.26801210776,1.04289102096811,135.610768983579));
#22016=CARTESIAN_POINT('Ctrl Pts',(192.260251665246,1.17691180625858,135.58168925024));
#22017=CARTESIAN_POINT('Ctrl Pts',(192.252491222732,1.30960908320894,135.547022861951));
#22018=CARTESIAN_POINT('Ctrl Pts',(192.244730780217,1.44049317827798,135.50693039013));
#22019=CARTESIAN_POINT('Ctrl Pts',(192.236957879952,1.5715873801157,135.466773558314));
#22020=CARTESIAN_POINT('Ctrl Pts',(192.229184979687,1.70086221469286,135.42117336688));
#22021=CARTESIAN_POINT('Ctrl Pts',(192.221412079421,1.82784666917891,135.37033911253));
#22022=CARTESIAN_POINT('Ctrl Pts',(192.213921743659,1.95021491889024,135.321352811369));
#22023=CARTESIAN_POINT('Ctrl Pts',(192.206431407897,2.07045613849443,135.267506509144));
#22024=CARTESIAN_POINT('Ctrl Pts',(192.198941072135,2.18817178530026,135.209027154379));
#22025=CARTESIAN_POINT('Ctrl Pts',(192.191166738016,2.31035065663324,135.148330537103));
#22026=CARTESIAN_POINT('Ctrl Pts',(192.183392403897,2.43019568637188,135.082450339021));
#22027=CARTESIAN_POINT('Ctrl Pts',(192.175618069778,2.5472357860093,135.011589267518));
#22028=CARTESIAN_POINT('Ctrl Pts',(192.167853316831,2.66413164418405,134.940815525952));
#22029=CARTESIAN_POINT('Ctrl Pts',(192.160088563884,2.7782291190768,134.865073325257));
#22030=CARTESIAN_POINT('Ctrl Pts',(192.152323810936,2.88907911974915,134.784612481749));
#22031=CARTESIAN_POINT('Ctrl Pts',(192.144566770051,2.99981902263817,134.704231553085));
#22032=CARTESIAN_POINT('Ctrl Pts',(192.136809729166,3.10731755571858,134.619141536373));
#22033=CARTESIAN_POINT('Ctrl Pts',(192.129052688281,3.21115248827715,134.529636816659));
#22034=CARTESIAN_POINT('Ctrl Pts',(192.121301497041,3.3149091181053,134.440199593151));
#22035=CARTESIAN_POINT('Ctrl Pts',(192.113550305801,3.41500735156303,134.346354547366));
#22036=CARTESIAN_POINT('Ctrl Pts',(192.105799114561,3.51105638032787,134.248437584862));
#22037=CARTESIAN_POINT('Ctrl Pts',(192.098051217784,3.60706458569329,134.150562239679));
#22038=CARTESIAN_POINT('Ctrl Pts',(192.090303321007,3.69902673613745,134.048618698472));
#22039=CARTESIAN_POINT('Ctrl Pts',(192.08255542423,3.78658756001065,133.942980969388));
#22040=CARTESIAN_POINT('Ctrl Pts',(192.074809148146,3.87413006804709,133.83736533744));
#22041=CARTESIAN_POINT('Ctrl Pts',(192.067062872062,3.95727283142153,133.728057355462));
#22042=CARTESIAN_POINT('Ctrl Pts',(192.059316595977,4.03569996811177,133.615465174476));
#22043=CARTESIAN_POINT('Ctrl Pts',(192.051570262712,4.1141276837333,133.502872162361));
#22044=CARTESIAN_POINT('Ctrl Pts',(192.043823929447,4.18783947974799,133.386995223673));
#22045=CARTESIAN_POINT('Ctrl Pts',(192.036077596181,4.25656226304545,133.268272296851));
#22046=CARTESIAN_POINT('Ctrl Pts',(192.028329528178,4.32530043633368,133.149522782853));
#22047=CARTESIAN_POINT('Ctrl Pts',(192.020581460175,4.38904717787134,133.027926350791));
#22048=CARTESIAN_POINT('Ctrl Pts',(192.012833392173,4.4475750888561,132.903946026995));
#22049=CARTESIAN_POINT('Ctrl Pts',(192.005077089431,4.50616520400119,132.779833935435));
#22050=CARTESIAN_POINT('Ctrl Pts',(191.997320786689,4.55952524142413,132.653333245059));
#22051=CARTESIAN_POINT('Ctrl Pts',(191.989564483947,4.60747555374874,132.524927990297));
#22052=CARTESIAN_POINT('Ctrl Pts',(191.981804041433,4.65545145859881,132.396454201785));
#22053=CARTESIAN_POINT('Ctrl Pts',(191.974043598919,4.69801176383069,132.266074194861));
#22054=CARTESIAN_POINT('Ctrl Pts',(191.966283156404,4.73502688221655,132.134286738517));
#22055=CARTESIAN_POINT('Ctrl Pts',(191.958510256139,4.77210142055647,132.002287725248));
#22056=CARTESIAN_POINT('Ctrl Pts',(191.950737355874,4.80361289384034,131.868877128348));
#22057=CARTESIAN_POINT('Ctrl Pts',(191.942964455608,4.82948279537217,131.73456435423));
#22058=CARTESIAN_POINT('Ctrl Pts',(191.935474119846,4.85441226082101,131.605134187765));
#22059=CARTESIAN_POINT('Ctrl Pts',(191.927983784084,4.87410315800352,131.474866602682));
#22060=CARTESIAN_POINT('Ctrl Pts',(191.920493448322,4.88853100308117,131.344219575456));
#22061=CARTESIAN_POINT('Ctrl Pts',(191.912719114203,4.90350588429017,131.208619026484));
#22062=CARTESIAN_POINT('Ctrl Pts',(191.904944780084,4.91285817377069,131.0721801525));
#22063=CARTESIAN_POINT('Ctrl Pts',(191.897170445965,4.9165037801426,130.935408861902));
#22064=CARTESIAN_POINT('Ctrl Pts',(191.889405693018,4.92014489363048,130.798806129696));
#22065=CARTESIAN_POINT('Ctrl Pts',(191.881640940071,4.91809330722021,130.661872183078));
#22066=CARTESIAN_POINT('Ctrl Pts',(191.873876187123,4.91031645383257,130.525119886796));
#22067=CARTESIAN_POINT('Ctrl Pts',(191.866119146238,4.90254732452534,130.388503414822));
#22068=CARTESIAN_POINT('Ctrl Pts',(191.858362105353,4.88906426651891,130.252068621953));
#22069=CARTESIAN_POINT('Ctrl Pts',(191.850605064468,4.86988672827563,130.116329865154));
#22070=CARTESIAN_POINT('Ctrl Pts',(191.842853873228,4.85072365196311,129.980693470007));
#22071=CARTESIAN_POINT('Ctrl Pts',(191.835102681988,4.82587469733376,129.84575245173));
#22072=CARTESIAN_POINT('Ctrl Pts',(191.827351490748,4.79541122980165,129.712017173592));
#22073=CARTESIAN_POINT('Ctrl Pts',(191.819603593971,4.76496071005587,129.578338736515));
#22074=CARTESIAN_POINT('Ctrl Pts',(191.811855697194,4.72890051026299,129.445865400711));
#22075=CARTESIAN_POINT('Ctrl Pts',(191.804107800417,4.68735326106434,129.31509822682));
#22076=CARTESIAN_POINT('Ctrl Pts',(191.796361524333,4.64581470265456,129.184358406603));
#22077=CARTESIAN_POINT('Ctrl Pts',(191.788615248249,4.59879149613188,129.055324410796));
#22078=CARTESIAN_POINT('Ctrl Pts',(191.780868972164,4.54645628856314,128.928482615487));
#22079=CARTESIAN_POINT('Ctrl Pts',(191.773122638899,4.49412069466779,128.801639883861));
#22080=CARTESIAN_POINT('Ctrl Pts',(191.765376305634,4.43647317060039,128.676989746434));
#22081=CARTESIAN_POINT('Ctrl Pts',(191.757629972368,4.37373455287664,128.5549986806));
#22082=CARTESIAN_POINT('Ctrl Pts',(191.749881904365,4.31098188527447,128.432980295712));
#22083=CARTESIAN_POINT('Ctrl Pts',(191.742133836362,4.24313603409257,128.313622514967));
#22084=CARTESIAN_POINT('Ctrl Pts',(191.734385768359,4.17046364188854,128.197366932459));
#22085=CARTESIAN_POINT('Ctrl Pts',(191.726629465618,4.09771401260122,128.080987792135));
#22086=CARTESIAN_POINT('Ctrl Pts',(191.718873162876,4.02012780272054,127.967717768317));
#22087=CARTESIAN_POINT('Ctrl Pts',(191.711116860134,3.93801514032661,127.857969635863));
#22088=CARTESIAN_POINT('Ctrl Pts',(191.70335641762,3.85585865193233,127.748162927527));
#22089=CARTESIAN_POINT('Ctrl Pts',(191.695595975106,3.76917114412413,127.641882158914));
#22090=CARTESIAN_POINT('Ctrl Pts',(191.687835532591,3.67830220031926,127.539505952251));
#22091=CARTESIAN_POINT('Ctrl Pts',(191.680062632326,3.58728738561886,127.436965402214));
#22092=CARTESIAN_POINT('Ctrl Pts',(191.67228973206,3.49207799308258,127.338342220929));
#22093=CARTESIAN_POINT('Ctrl Pts',(191.664516831795,3.39306016596735,127.243977804914));
#22094=CARTESIAN_POINT('Ctrl Pts',(191.657026496033,3.29764188627902,127.153043773112));
#22095=CARTESIAN_POINT('Ctrl Pts',(191.649536160271,3.19868748848367,127.066064451937));
#22096=CARTESIAN_POINT('Ctrl Pts',(191.642045824509,3.09656904704697,126.983307987809));
#22097=CARTESIAN_POINT('Ctrl Pts',(191.63427149039,2.99057875386455,126.89741378719));
#22098=CARTESIAN_POINT('Ctrl Pts',(191.626497156271,2.88084400593911,126.815796897087));
#22099=CARTESIAN_POINT('Ctrl Pts',(191.618722822152,2.76774498488753,126.738801521804));
#22100=CARTESIAN_POINT('Ctrl Pts',(191.610958069205,2.65478534827152,126.661901036441));
#22101=CARTESIAN_POINT('Ctrl Pts',(191.603193316258,2.53847000824377,126.589610951247));
#22102=CARTESIAN_POINT('Ctrl Pts',(191.59542856331,2.41921284913904,126.522235881753));
#22103=CARTESIAN_POINT('Ctrl Pts',(191.587671522425,2.30007413792603,126.454927730128));
#22104=CARTESIAN_POINT('Ctrl Pts',(191.57991448154,2.17799976045686,126.392525070538));
#22105=CARTESIAN_POINT('Ctrl Pts',(191.572157440656,2.05343297218267,126.335289562945));
#22106=CARTESIAN_POINT('Ctrl Pts',(191.564406249415,1.92896012069234,126.278097217093));
#22107=CARTESIAN_POINT('Ctrl Pts',(191.556655058175,1.80199895334133,126.226064429886));
#22108=CARTESIAN_POINT('Ctrl Pts',(191.548903866935,1.67301742795112,126.179407023391));
#22109=CARTESIAN_POINT('Ctrl Pts',(191.541155970158,1.54409072314994,126.132769447539));
#22110=CARTESIAN_POINT('Ctrl Pts',(191.533408073381,1.41314573509101,126.09150284106));
#22111=CARTESIAN_POINT('Ctrl Pts',(191.525660176604,1.28067030513812,126.055774866836));
#22112=CARTESIAN_POINT('Ctrl Pts',(191.51791390052,1.14822258618934,126.020054366134));
#22113=CARTESIAN_POINT('Ctrl Pts',(191.510167624436,1.01424543935255,125.989870294983));
#22114=CARTESIAN_POINT('Ctrl Pts',(191.502421348352,0.879241386563487,125.965340298674));
#22115=CARTESIAN_POINT('Ctrl Pts',(191.494675015086,0.744236337205225,125.940810121289));
#22116=CARTESIAN_POINT('Ctrl Pts',(191.486928681821,0.608204751435609,125.921934171922));
#22117=CARTESIAN_POINT('Ctrl Pts',(191.479182348555,0.471658457426965,125.908778796981));
#22118=CARTESIAN_POINT('Ctrl Pts',(191.471434280553,0.335081584822615,125.895620475986));
#22119=CARTESIAN_POINT('Ctrl Pts',(191.46368621255,0.197990163703318,125.888185316112));
#22120=CARTESIAN_POINT('Ctrl Pts',(191.455938144547,0.0608998465023526,
125.886487675816));
#22121=CARTESIAN_POINT('Ctrl Pts',(191.448181841805,-0.0763361719192702,
125.884788231248));
#22122=CARTESIAN_POINT('Ctrl Pts',(191.440425539063,-0.21357069252026,125.888838492329));
#22123=CARTESIAN_POINT('Ctrl Pts',(191.432669236321,-0.350288804319249,
125.898600654414));
#22124=CARTESIAN_POINT('Ctrl Pts',(191.424908793807,-0.487079886691054,
125.908368026859));
#22125=CARTESIAN_POINT('Ctrl Pts',(191.417148351293,-0.623353622783719,
125.923853330808));
#22126=CARTESIAN_POINT('Ctrl Pts',(191.409387908778,-0.758602508617255,
125.944967106394));
#22127=CARTESIAN_POINT('Ctrl Pts',(191.401615008513,-0.894068507969185,
125.966114775688));
#22128=CARTESIAN_POINT('Ctrl Pts',(191.393842108248,-1.02850598582216,125.992908895609));
#22129=CARTESIAN_POINT('Ctrl Pts',(191.386069207982,-1.16141899575531,126.025209126056));
#22130=CARTESIAN_POINT('Ctrl Pts',(191.37857887222,-1.28950028298996,126.056335161768));
#22131=CARTESIAN_POINT('Ctrl Pts',(191.371088536458,-1.41616571838099,126.092573851485));
#22132=CARTESIAN_POINT('Ctrl Pts',(191.363598200696,-1.54098858741563,126.13375709811));
#22133=CARTESIAN_POINT('Ctrl Pts',(191.355823866577,-1.67054415346853,126.176501820048));
#22134=CARTESIAN_POINT('Ctrl Pts',(191.348049532458,-1.79852506629693,126.224708848623));
#22135=CARTESIAN_POINT('Ctrl Pts',(191.340275198339,-1.92443623961998,126.278244377108));
#22136=CARTESIAN_POINT('Ctrl Pts',(191.332510445392,-2.05019223867488,126.331713927838));
#22137=CARTESIAN_POINT('Ctrl Pts',(191.324745692445,-2.17388321715495,126.390498760795));
#22138=CARTESIAN_POINT('Ctrl Pts',(191.316980939498,-2.29502917879571,126.454415315499));
#22139=CARTESIAN_POINT('Ctrl Pts',(191.309223898613,-2.41605481655935,126.51826838738));
#22140=CARTESIAN_POINT('Ctrl Pts',(191.301466857728,-2.53454012426197,126.587242856692));
#22141=CARTESIAN_POINT('Ctrl Pts',(191.293709816843,-2.65002536956902,126.661107233673));
#22142=CARTESIAN_POINT('Ctrl Pts',(191.285958625602,-2.76542352655441,126.734915908953));
#22143=CARTESIAN_POINT('Ctrl Pts',(191.278207434362,-2.87782579622934,126.813606942315));
#22144=CARTESIAN_POINT('Ctrl Pts',(191.270456243122,-2.98679765874186,126.896903284692));
#22145=CARTESIAN_POINT('Ctrl Pts',(191.262708346345,-3.09572320530585,126.980164223901));
#22146=CARTESIAN_POINT('Ctrl Pts',(191.254960449568,-3.20122093462301,127.068026342114));
#22147=CARTESIAN_POINT('Ctrl Pts',(191.247212552791,-3.302886096988,127.160169830461));
#22148=CARTESIAN_POINT('Ctrl Pts',(191.239466276707,-3.40452999319271,127.252294044376));
#22149=CARTESIAN_POINT('Ctrl Pts',(191.231720000623,-3.50234262754816,127.348697584696));
#22150=CARTESIAN_POINT('Ctrl Pts',(191.223973724539,-3.59595339635909,127.449021255636));
#22151=CARTESIAN_POINT('Ctrl Pts',(191.216227391273,-3.68956485618348,127.549345667144));
#22152=CARTESIAN_POINT('Ctrl Pts',(191.208481058008,-3.77897412184559,127.653589981163));
#22153=CARTESIAN_POINT('Ctrl Pts',(191.200734724743,-3.86384871860262,127.761359444012));
#22154=CARTESIAN_POINT('Ctrl Pts',(191.19298665674,-3.94874232243708,127.869153041084));
#22155=CARTESIAN_POINT('Ctrl Pts',(191.185238588737,-4.02909899477355,127.980473050777));
#22156=CARTESIAN_POINT('Ctrl Pts',(191.177490520734,-4.10462793269824,128.094893401191));
#22157=CARTESIAN_POINT('Ctrl Pts',(191.169734217992,-4.18023714367694,128.209435358914));
#22158=CARTESIAN_POINT('Ctrl Pts',(191.16197791525,-4.251008154845,128.327083912827));
#22159=CARTESIAN_POINT('Ctrl Pts',(191.154221612508,-4.31669445035687,128.447385419402));
#22160=CARTESIAN_POINT('Ctrl Pts',(191.146461169994,-4.38241580462248,128.567751134514));
#22161=CARTESIAN_POINT('Ctrl Pts',(191.13870072748,-4.44304686287264,128.690772273196));
#22162=CARTESIAN_POINT('Ctrl Pts',(191.130940284966,-4.49838857192929,128.815973502732));
#22163=CARTESIAN_POINT('Ctrl Pts',(191.1231673847,-4.5538191204103,128.941375716397));
#22164=CARTESIAN_POINT('Ctrl Pts',(191.115394484435,-4.603943209069,129.068964650282));
#22165=CARTESIAN_POINT('Ctrl Pts',(191.107621584169,-4.64861083885302,129.198247193365));
#22166=CARTESIAN_POINT('Ctrl Pts',(191.100131248407,-4.69165468778338,129.322829990364));
#22167=CARTESIAN_POINT('Ctrl Pts',(191.092640912645,-4.72963181359555,129.44898510548));
#22168=CARTESIAN_POINT('Ctrl Pts',(191.085150576883,-4.76245299152071,129.576262671124));
#22169=CARTESIAN_POINT('Ctrl Pts',(191.085028435562,-4.76298819076576,129.578338125491));
#22170=CARTESIAN_POINT('Ctrl Pts',(191.08490629424,-4.76352203648398,129.580413942056));
#22171=CARTESIAN_POINT('Ctrl Pts',(191.084784152919,-4.76405452823405,129.582490119308));
#22172=CARTESIAN_POINT('Ctrl Pts',(192.834981455508,-4.76405452823404,129.582490119308));
#22173=CARTESIAN_POINT('Ctrl Pts',(192.827262795634,-4.79795815032377,129.714679827277));
#22174=CARTESIAN_POINT('Ctrl Pts',(192.819544135761,-4.82632919785479,129.848178265195));
#22175=CARTESIAN_POINT('Ctrl Pts',(192.811825475887,-4.84909224210237,129.982480157838));
#22176=CARTESIAN_POINT('Ctrl Pts',(192.803997802578,-4.87217677708874,130.118678844873));
#22177=CARTESIAN_POINT('Ctrl Pts',(192.796170129268,-4.88949364919261,130.255703433094));
#22178=CARTESIAN_POINT('Ctrl Pts',(192.788342455959,-4.90101880375934,130.393024079319));
#22179=CARTESIAN_POINT('Ctrl Pts',(192.78051478265,-4.91254395832607,130.530344725543));
#22180=CARTESIAN_POINT('Ctrl Pts',(192.77268710934,-4.91827744128822,130.667961010208));
#22181=CARTESIAN_POINT('Ctrl Pts',(192.764859436031,-4.9182499011834,130.805346522958));
#22182=CARTESIAN_POINT('',(193.110140564008,-4.91324924050575,130.80805185308));
#22183=CARTESIAN_POINT('Ctrl Pts',(193.179932595466,-4.75726252818781,129.584191622251));
#22184=CARTESIAN_POINT('Ctrl Pts',(193.15666858498,-4.85769551258501,129.983931752434));
#22185=CARTESIAN_POINT('Ctrl Pts',(193.133404574494,-4.9103928439719,130.396313003733));
#22186=CARTESIAN_POINT('Ctrl Pts',(193.110140564008,-4.91324924050575,130.80805185308));
#22187=CARTESIAN_POINT('Ctrl Pts',(193.110140564008,-4.91324924050575,130.80805185308));
#22188=CARTESIAN_POINT('Ctrl Pts',(193.078325358477,-4.91715556795767,131.371134307201));
#22189=CARTESIAN_POINT('Ctrl Pts',(192.953694278342,-4.56730227853154,133.572215041493));
#22190=CARTESIAN_POINT('Ctrl Pts',(192.736247323602,-1.31701101669081,136.470678805982));
#22191=CARTESIAN_POINT('Ctrl Pts',(192.457799699789,4.05535734608101,134.975182673953));
#22192=CARTESIAN_POINT('Ctrl Pts',(192.179352075976,5.70105042302464,129.646904828089));
#22193=CARTESIAN_POINT('Ctrl Pts',(191.900904452163,2.10775667300519,125.382272307895));
#22194=CARTESIAN_POINT('Ctrl Pts',(191.651220653561,-2.85118716275981,126.026104000732));
#22195=CARTESIAN_POINT('Ctrl Pts',(191.494352729563,-4.4694424636812,128.488577529337));
#22196=CARTESIAN_POINT('Ctrl Pts',(191.430300680169,-4.76051597898714,129.583432241587));
#22197=CARTESIAN_POINT('Origin',(213.235140564004,0.,130.804360617566));
#22198=CARTESIAN_POINT('',(189.334601801321,-4.76405452823404,129.582490119308));
#22199=CARTESIAN_POINT('',(189.680106903305,-4.76405452823404,129.582490119308));
#22200=CARTESIAN_POINT('',(213.235140564004,-4.76405452823405,129.582490119308));
#22201=CARTESIAN_POINT('',(191.014859436046,-4.91824790535574,130.799821458629));
#22202=CARTESIAN_POINT('Ctrl Pts',(191.014859435991,-4.91824790535664,130.799821459599));
#22203=CARTESIAN_POINT('Ctrl Pts',(191.007192991401,-4.9183728969955,130.93525183469));
#22204=CARTESIAN_POINT('Ctrl Pts',(190.999526546812,-4.91289980315623,131.070824814365));
#22205=CARTESIAN_POINT('Ctrl Pts',(190.991860102222,-4.90182013838234,131.206035104495));
#22206=CARTESIAN_POINT('Ctrl Pts',(190.984145221007,-4.8906704722459,131.342099653731));
#22207=CARTESIAN_POINT('Ctrl Pts',(190.976430339793,-4.87384310420628,131.477796505531));
#22208=CARTESIAN_POINT('Ctrl Pts',(190.968715458578,-4.85138271638349,131.612611074835));
#22209=CARTESIAN_POINT('Ctrl Pts',(190.961055815356,-4.82908314331645,131.746460381553));
#22210=CARTESIAN_POINT('Ctrl Pts',(190.953396172134,-4.80123103213926,131.879439600074));
#22211=CARTESIAN_POINT('Ctrl Pts',(190.945736528912,-4.76792200125562,132.011051486199));
#22212=CARTESIAN_POINT('Ctrl Pts',(190.938077448338,-4.7346154171254,132.142653704621));
#22213=CARTESIAN_POINT('Ctrl Pts',(190.930418367764,-4.69585280864405,132.27288840198));
#22214=CARTESIAN_POINT('Ctrl Pts',(190.92275928719,-4.65178043486449,132.401270711564));
#22215=CARTESIAN_POINT('Ctrl Pts',(190.91509902035,-4.60770123499393,132.529672905471));
#22216=CARTESIAN_POINT('Ctrl Pts',(190.907438753509,-4.55831076464351,132.65622176218));
#22217=CARTESIAN_POINT('Ctrl Pts',(190.899778486669,-4.50380428023245,132.780450207605));
#22218=CARTESIAN_POINT('Ctrl Pts',(190.892022192202,-4.44861451305745,132.906235956834));
#22219=CARTESIAN_POINT('Ctrl Pts',(190.884265897736,-4.38817975595761,133.029642333155));
#22220=CARTESIAN_POINT('Ctrl Pts',(190.876509603269,-4.32275123572271,133.150209039045));
#22221=CARTESIAN_POINT('Ctrl Pts',(190.868837761032,-4.25803511551729,133.269462988289));
#22222=CARTESIAN_POINT('Ctrl Pts',(190.861165918795,-4.18843370140229,133.385938486624));
#22223=CARTESIAN_POINT('Ctrl Pts',(190.853494076558,-4.11423393107197,133.499219096766));
#22224=CARTESIAN_POINT('Ctrl Pts',(190.845695555977,-4.03880896557229,133.614370209414));
#22225=CARTESIAN_POINT('Ctrl Pts',(190.837897035395,-3.95863270394605,133.726219643716));
#22226=CARTESIAN_POINT('Ctrl Pts',(190.830098514814,-3.87404868695243,133.834365540602));
#22227=CARTESIAN_POINT('Ctrl Pts',(190.822299994233,-3.78946466995879,133.942511437488));
#22228=CARTESIAN_POINT('Ctrl Pts',(190.814501473652,-3.70047322628425,134.046953515992));
#22229=CARTESIAN_POINT('Ctrl Pts',(190.80670295307,-3.60745575518182,134.147330260998));
#22230=CARTESIAN_POINT('Ctrl Pts',(190.798928618951,-3.51472677001999,134.247395695888));
#22231=CARTESIAN_POINT('Ctrl Pts',(190.791154284832,-3.41768425491403,134.343758457961));
#22232=CARTESIAN_POINT('Ctrl Pts',(190.783379950713,-3.31665570023412,134.436023876818));
#22233=CARTESIAN_POINT('Ctrl Pts',(190.775615197766,-3.21575165421878,134.528175586793));
#22234=CARTESIAN_POINT('Ctrl Pts',(190.767850444819,-3.11087162883549,134.616239739652));
#22235=CARTESIAN_POINT('Ctrl Pts',(190.760085691872,-3.00238209392103,134.699856070599));
#22236=CARTESIAN_POINT('Ctrl Pts',(190.752328650987,-2.89400031234197,134.783389352628));
#22237=CARTESIAN_POINT('Ctrl Pts',(190.744571610102,-2.78201646323467,134.862483366925));
#22238=CARTESIAN_POINT('Ctrl Pts',(190.736814569217,-2.66683218589617,134.936816201691));
#22239=CARTESIAN_POINT('Ctrl Pts',(190.729063377977,-2.55173476991692,135.011092981489));
#22240=CARTESIAN_POINT('Ctrl Pts',(190.721312186737,-2.43344205673886,135.080615517179));
#22241=CARTESIAN_POINT('Ctrl Pts',(190.713560995496,-2.3123866426324,135.145103765631));
#22242=CARTESIAN_POINT('Ctrl Pts',(190.705813098719,-2.19138268030653,135.209564604857));
#22243=CARTESIAN_POINT('Ctrl Pts',(190.698065201942,-2.06761869682469,135.268995229124));
#22244=CARTESIAN_POINT('Ctrl Pts',(190.690317305165,-1.94155380476799,135.323160445584));
#22245=CARTESIAN_POINT('Ctrl Pts',(190.682571029081,-1.81551528276903,135.377314331847));
#22246=CARTESIAN_POINT('Ctrl Pts',(190.674824752997,-1.68717716851246,135.426204846825));
#22247=CARTESIAN_POINT('Ctrl Pts',(190.667078476913,-1.55702020428703,135.469644225873));
#22248=CARTESIAN_POINT('Ctrl Pts',(190.659332143647,-1.42686227927271,135.513083925581));
#22249=CARTESIAN_POINT('Ctrl Pts',(190.651585810382,-1.29488584835446,135.551072285292));
#22250=CARTESIAN_POINT('Ctrl Pts',(190.643839477117,-1.16158814539901,135.583470999527));
#22251=CARTESIAN_POINT('Ctrl Pts',(190.636091409114,-1.02826059134723,135.615876969229));
#22252=CARTESIAN_POINT('Ctrl Pts',(190.628343341111,-0.893611556303883,
135.642690710273));
#22253=CARTESIAN_POINT('Ctrl Pts',(190.620595273108,-0.758149436995237,
135.663824836354));
#22254=CARTESIAN_POINT('Ctrl Pts',(190.612838970366,-0.622543346934008,
135.684981424036));
#22255=CARTESIAN_POINT('Ctrl Pts',(190.605082667624,-0.486122833271634,
135.700446278109));
#22256=CARTESIAN_POINT('Ctrl Pts',(190.597326364882,-0.349402960938852,
135.710183752717));
#22257=CARTESIAN_POINT('Ctrl Pts',(190.589565922368,-0.21261011709358,135.719926424509));
#22258=CARTESIAN_POINT('Ctrl Pts',(190.581805479854,-0.0755179868161497,
135.723935614332));
#22259=CARTESIAN_POINT('Ctrl Pts',(190.57404503734,0.0613583669252786,135.722227859909));
#22260=CARTESIAN_POINT('Ctrl Pts',(190.566272137074,0.198454446740975,135.720517364047));
#22261=CARTESIAN_POINT('Ctrl Pts',(190.558499236809,0.335333667223026,135.713071605924));
#22262=CARTESIAN_POINT('Ctrl Pts',(190.550726336543,0.471485185895587,135.699959128676));
#22263=CARTESIAN_POINT('Ctrl Pts',(190.543236000781,0.602687253919808,135.687323323004));
#22264=CARTESIAN_POINT('Ctrl Pts',(190.535745665019,0.7332133040056,135.669425686172));
#22265=CARTESIAN_POINT('Ctrl Pts',(190.528255329257,0.862617086158864,135.646372061704));
#22266=CARTESIAN_POINT('Ctrl Pts',(190.520480995138,0.996927252043568,135.622444352059));
#22267=CARTESIAN_POINT('Ctrl Pts',(190.512706661019,1.13045382272073,135.592886162405));
#22268=CARTESIAN_POINT('Ctrl Pts',(190.5049323269,1.26268773426236,135.557759690676));
#22269=CARTESIAN_POINT('Ctrl Pts',(190.497167573953,1.3947586793262,135.522676509184));
#22270=CARTESIAN_POINT('Ctrl Pts',(190.489402821006,1.5255397607892,135.482038799179));
#22271=CARTESIAN_POINT('Ctrl Pts',(190.481638068059,1.65452979177848,135.435960150192));
#22272=CARTESIAN_POINT('Ctrl Pts',(190.473881027174,1.78339170804989,135.389927267168));
#22273=CARTESIAN_POINT('Ctrl Pts',(190.466123986289,1.91046574813598,135.338464330073));
#22274=CARTESIAN_POINT('Ctrl Pts',(190.458366945404,2.03526398267376,135.281735248232));
#22275=CARTESIAN_POINT('Ctrl Pts',(190.450615754164,2.15996810589255,135.225048946233));
#22276=CARTESIAN_POINT('Ctrl Pts',(190.442864562924,2.28239948508168,135.163104565135));
#22277=CARTESIAN_POINT('Ctrl Pts',(190.435113371684,2.40208868317336,135.096114690282));
#22278=CARTESIAN_POINT('Ctrl Pts',(190.427365474906,2.52172701016312,135.029153287912));
#22279=CARTESIAN_POINT('Ctrl Pts',(190.419617578129,2.63862513369723,134.95715084752));
#22280=CARTESIAN_POINT('Ctrl Pts',(190.411869681352,2.75233701780585,134.880366506045));
#22281=CARTESIAN_POINT('Ctrl Pts',(190.404123405268,2.86602511583959,134.803598226199));
#22282=CARTESIAN_POINT('Ctrl Pts',(190.396377129184,2.97652797633052,134.722050253513));
#22283=CARTESIAN_POINT('Ctrl Pts',(190.3886308531,3.08342777461511,134.636025558715));
#22284=CARTESIAN_POINT('Ctrl Pts',(190.380884519835,3.1903283620097,134.550000228902));
#22285=CARTESIAN_POINT('Ctrl Pts',(190.373138186569,3.29362552953602,134.459498356145));
#22286=CARTESIAN_POINT('Ctrl Pts',(190.365391853304,3.39293414982598,134.364863519888));
#22287=CARTESIAN_POINT('Ctrl Pts',(190.357643785301,3.49226500959297,134.270207490816));
#22288=CARTESIAN_POINT('Ctrl Pts',(190.349895717298,3.58760526176411,134.171416926171));
#22289=CARTESIAN_POINT('Ctrl Pts',(190.342147649295,3.67860658491866,134.068872320086));
#22290=CARTESIAN_POINT('Ctrl Pts',(190.334391346553,3.76970462536241,133.966218728374));
#22291=CARTESIAN_POINT('Ctrl Pts',(190.326635043811,3.85645426497193,133.859803417977));
#22292=CARTESIAN_POINT('Ctrl Pts',(190.31887874107,3.93854710870415,133.750040460152));
#22293=CARTESIAN_POINT('Ctrl Pts',(190.311118298555,4.02068376785884,133.640218918532));
#22294=CARTESIAN_POINT('Ctrl Pts',(190.303357856041,4.09815845787932,133.527046491708));
#22295=CARTESIAN_POINT('Ctrl Pts',(190.295597413527,4.17070668830499,133.410965455785));
#22296=CARTESIAN_POINT('Ctrl Pts',(190.287824513262,4.24337137959067,133.294698076279));
#22297=CARTESIAN_POINT('Ctrl Pts',(190.280051612996,4.31109361453856,133.175513097328));
#22298=CARTESIAN_POINT('Ctrl Pts',(190.272278712731,4.37365493759366,133.053877354415));
#22299=CARTESIAN_POINT('Ctrl Pts',(190.264788376969,4.43394199897344,132.936663377138));
#22300=CARTESIAN_POINT('Ctrl Pts',(190.257298041207,4.4894367285661,132.817174004629));
#22301=CARTESIAN_POINT('Ctrl Pts',(190.249807705445,4.53998696650629,132.695841890657));
#22302=CARTESIAN_POINT('Ctrl Pts',(190.242033371326,4.59245383208216,132.569909432706));
#22303=CARTESIAN_POINT('Ctrl Pts',(190.234259037206,4.63976006301382,132.44159282362));
#22304=CARTESIAN_POINT('Ctrl Pts',(190.226484703087,4.68168282669612,132.3113539728));
#22305=CARTESIAN_POINT('Ctrl Pts',(190.21871995014,4.72355392431904,132.181275629723));
#22306=CARTESIAN_POINT('Ctrl Pts',(190.210955197193,4.76005463700814,132.049280127086));
#22307=CARTESIAN_POINT('Ctrl Pts',(190.203190444246,4.79100962710627,131.915850525516));
#22308=CARTESIAN_POINT('Ctrl Pts',(190.195433403361,4.82193387227178,131.782553448108));
#22309=CARTESIAN_POINT('Ctrl Pts',(190.187676362476,4.84732326841009,131.647825484707));
#22310=CARTESIAN_POINT('Ctrl Pts',(190.179919321591,4.8670519793402,131.5121657411));
#22311=CARTESIAN_POINT('Ctrl Pts',(190.172168130351,4.8867658126959,131.376608299561));
#22312=CARTESIAN_POINT('Ctrl Pts',(190.164416939111,4.90082740152704,131.240120861754));
#22313=CARTESIAN_POINT('Ctrl Pts',(190.156665747871,4.90916185770046,131.103213285948));
#22314=CARTESIAN_POINT('Ctrl Pts',(190.148917851094,4.91749277150769,130.966363899514));
#22315=CARTESIAN_POINT('Ctrl Pts',(190.141169954316,4.92010137035702,130.829095119669));
#22316=CARTESIAN_POINT('Ctrl Pts',(190.133422057539,4.91696458015609,130.691922278951));
#22317=CARTESIAN_POINT('Ctrl Pts',(190.125675781455,4.91382844610404,130.554778131835));
#22318=CARTESIAN_POINT('Ctrl Pts',(190.117929505371,4.90494932240312,130.417730274544));
#22319=CARTESIAN_POINT('Ctrl Pts',(190.110183229287,4.8903562624689,130.281293997879));
#22320=CARTESIAN_POINT('Ctrl Pts',(190.102436896022,4.87576309481204,130.144856714072));
#22321=CARTESIAN_POINT('Ctrl Pts',(190.094690562756,4.85545594833678,130.009031408648));
#22322=CARTESIAN_POINT('Ctrl Pts',(190.086944229491,4.82951571541046,129.87432781325));
#22323=CARTESIAN_POINT('Ctrl Pts',(190.079196161488,4.80356967334887,129.739594051917));
#22324=CARTESIAN_POINT('Ctrl Pts',(190.071448093485,4.77198810853258,129.605982884305));
#22325=CARTESIAN_POINT('Ctrl Pts',(190.063700025482,4.73490286521561,129.473993029464));
#22326=CARTESIAN_POINT('Ctrl Pts',(190.05594372274,4.69777820726065,129.341862894234));
#22327=CARTESIAN_POINT('Ctrl Pts',(190.048187419998,4.65513829197155,129.211357890945));
#22328=CARTESIAN_POINT('Ctrl Pts',(190.040431117256,4.60716479417153,129.082961296709));
#22329=CARTESIAN_POINT('Ctrl Pts',(190.032670674742,4.55916569147128,128.954496173345));
#22330=CARTESIAN_POINT('Ctrl Pts',(190.024910232228,4.50582748595494,128.828142061345));
#22331=CARTESIAN_POINT('Ctrl Pts',(190.017149789714,4.44737931348167,128.704360545062));
#22332=CARTESIAN_POINT('Ctrl Pts',(190.009376889448,4.38883731481318,128.580380323701));
#22333=CARTESIAN_POINT('Ctrl Pts',(190.001603989183,4.32516913872479,128.458981297068));
#22334=CARTESIAN_POINT('Ctrl Pts',(189.993831088917,4.25664946656522,128.34059959399));
#22335=CARTESIAN_POINT('Ctrl Pts',(189.986340753155,4.19062065707926,128.226521364005));
#22336=CARTESIAN_POINT('Ctrl Pts',(189.978850417393,4.12008712075145,128.115245151775));
#22337=CARTESIAN_POINT('Ctrl Pts',(189.971360081631,4.04533061532805,128.007132833636));
#22338=CARTESIAN_POINT('Ctrl Pts',(189.963585747512,3.96773969427981,127.894921404095));
#22339=CARTESIAN_POINT('Ctrl Pts',(189.955811413393,3.88535347027769,127.785763070711));
#22340=CARTESIAN_POINT('Ctrl Pts',(189.948037079274,3.79844011431754,127.680094982182));
#22341=CARTESIAN_POINT('Ctrl Pts',(189.940272326327,3.71163387130119,127.574557120128));
#22342=CARTESIAN_POINT('Ctrl Pts',(189.93250757338,3.62031184341438,127.472501243445));
#22343=CARTESIAN_POINT('Ctrl Pts',(189.924742820433,3.52478566895689,127.374335974737));
#22344=CARTESIAN_POINT('Ctrl Pts',(189.916985779548,3.42935437244241,127.276268205157));
#22345=CARTESIAN_POINT('Ctrl Pts',(189.909228738663,3.32972750992248,127.18208363199));
#22346=CARTESIAN_POINT('Ctrl Pts',(189.901471697778,3.22625697570096,127.092157903645));
#22347=CARTESIAN_POINT('Ctrl Pts',(189.893720506538,3.12286446941407,127.002299988992));
#22348=CARTESIAN_POINT('Ctrl Pts',(189.885969315298,3.01563435469827,126.916694782037));
#22349=CARTESIAN_POINT('Ctrl Pts',(189.878218124058,2.90495511089095,126.835680879138));
#22350=CARTESIAN_POINT('Ctrl Pts',(189.87047022728,2.79432290871461,126.754701409308));
#22351=CARTESIAN_POINT('Ctrl Pts',(189.862722330503,2.68024480797378,126.678309592735));
#22352=CARTESIAN_POINT('Ctrl Pts',(189.854974433726,2.56314190041725,126.606803392128));
#22353=CARTESIAN_POINT('Ctrl Pts',(189.847228157642,2.44606348826436,126.535312149077));
#22354=CARTESIAN_POINT('Ctrl Pts',(189.839481881558,2.32596186128318,126.468704692871));
#22355=CARTESIAN_POINT('Ctrl Pts',(189.831735605474,2.20328625229884,126.407235107311));
#22356=CARTESIAN_POINT('Ctrl Pts',(189.823989272209,2.0806097377515,126.345765067998));
#22357=CARTESIAN_POINT('Ctrl Pts',(189.816242938943,1.9553595528264,126.289433150157));
#22358=CARTESIAN_POINT('Ctrl Pts',(189.808496605678,1.82800827349247,126.238446819152));
#22359=CARTESIAN_POINT('Ctrl Pts',(189.800748537675,1.70062847472297,126.187449070113));
#22360=CARTESIAN_POINT('Ctrl Pts',(189.793000469672,1.57114700814089,126.141799435301));
#22361=CARTESIAN_POINT('Ctrl Pts',(189.785252401669,1.44005472524652,126.10165656024));
#22362=CARTESIAN_POINT('Ctrl Pts',(189.777496098927,1.30882311591319,126.061471020852));
#22363=CARTESIAN_POINT('Ctrl Pts',(189.769739796186,1.17597764480057,126.02680404717));
#22364=CARTESIAN_POINT('Ctrl Pts',(189.761983493444,1.04202310631098,125.997764014104));
#22365=CARTESIAN_POINT('Ctrl Pts',(189.75422305093,0.907997072250902,125.968708481497));
#22366=CARTESIAN_POINT('Ctrl Pts',(189.746462608415,0.772861176351149,125.945285940508));
#22367=CARTESIAN_POINT('Ctrl Pts',(189.738702165901,0.637127616130016,125.927553110265));
#22368=CARTESIAN_POINT('Ctrl Pts',(189.730929265636,0.501176164348156,125.909791813709));
#22369=CARTESIAN_POINT('Ctrl Pts',(189.723156365371,0.36462552068547,125.897738514198));
#22370=CARTESIAN_POINT('Ctrl Pts',(189.715383465105,0.227991084653854,125.891397852816));
#22371=CARTESIAN_POINT('Ctrl Pts',(189.707893129343,0.0963236545319259,
125.885287690447));
#22372=CARTESIAN_POINT('Ctrl Pts',(189.700402793581,-0.035421273587108,
125.88448204139));
#22373=CARTESIAN_POINT('Ctrl Pts',(189.692912457819,-0.166786945949541,
125.888939457873));
#22374=CARTESIAN_POINT('Ctrl Pts',(189.6851381237,-0.303133387705632,125.893565878656));
#22375=CARTESIAN_POINT('Ctrl Pts',(189.677363789581,-0.439503151574217,
125.903876996674));
#22376=CARTESIAN_POINT('Ctrl Pts',(189.669589455462,-0.575383499002755,
125.91988348162));
#22377=CARTESIAN_POINT('Ctrl Pts',(189.661824702515,-0.711096386047016,
125.935870240005));
#22378=CARTESIAN_POINT('Ctrl Pts',(189.654059949567,-0.846320672210825,
125.95753835424));
#22379=CARTESIAN_POINT('Ctrl Pts',(189.64629519662,-0.980544123610611,125.984846504696));
#22380=CARTESIAN_POINT('Ctrl Pts',(189.638538155735,-1.11463426238657,126.012127532312));
#22381=CARTESIAN_POINT('Ctrl Pts',(189.63078111485,-1.24772516395203,126.045037370947));
#22382=CARTESIAN_POINT('Ctrl Pts',(189.623024073965,-1.37931057719251,126.083483009097));
#22383=CARTESIAN_POINT('Ctrl Pts',(189.615272882725,-1.51079676084857,126.121899655092));
#22384=CARTESIAN_POINT('Ctrl Pts',(189.607521691485,-1.64077934216929,126.165843682135));
#22385=CARTESIAN_POINT('Ctrl Pts',(189.599770500245,-1.76876346787959,126.215171271157));
#22386=CARTESIAN_POINT('Ctrl Pts',(189.592022603468,-1.89669319692298,126.264477894638));
#22387=CARTESIAN_POINT('Ctrl Pts',(189.584274706691,-2.02262579569819,126.319163388819));
#22388=CARTESIAN_POINT('Ctrl Pts',(189.576526809914,-2.14608296936092,126.379034533409));
#22389=CARTESIAN_POINT('Ctrl Pts',(189.56878053383,-2.26951431844442,126.438893154247));
#22390=CARTESIAN_POINT('Ctrl Pts',(189.561034257746,-2.39047092080065,126.503935097423));
#22391=CARTESIAN_POINT('Ctrl Pts',(189.553287981662,-2.50849618721501,126.573919749143));
#22392=CARTESIAN_POINT('Ctrl Pts',(189.545541648396,-2.62652232486488,126.643904917472));
#22393=CARTESIAN_POINT('Ctrl Pts',(189.537795315131,-2.74161674710555,126.718832667743));
#22394=CARTESIAN_POINT('Ctrl Pts',(189.530048981866,-2.85334946859526,126.798417548504));
#22395=CARTESIAN_POINT('Ctrl Pts',(189.522300913863,-2.96510721185335,126.878020251747));
#22396=CARTESIAN_POINT('Ctrl Pts',(189.51455284586,-3.0735014379343,126.962281934019));
#22397=CARTESIAN_POINT('Ctrl Pts',(189.506804777857,-3.17813335664093,127.050875379829));
#22398=CARTESIAN_POINT('Ctrl Pts',(189.499048475115,-3.28287647939589,127.139562983809));
#22399=CARTESIAN_POINT('Ctrl Pts',(189.491292172373,-3.38384900824164,127.232591294972));
#22400=CARTESIAN_POINT('Ctrl Pts',(189.483535869631,-3.48068691059195,127.329594194778));
#22401=CARTESIAN_POINT('Ctrl Pts',(189.475775427117,-3.5775764982465,127.426648867953));
#22402=CARTESIAN_POINT('Ctrl Pts',(189.468014984603,-3.67032679795341,127.527682068888));
#22403=CARTESIAN_POINT('Ctrl Pts',(189.460254542089,-3.75861323503234,127.632293529382));
#22404=CARTESIAN_POINT('Ctrl Pts',(189.452481641823,-3.84704139733793,127.737072921479));
#22405=CARTESIAN_POINT('Ctrl Pts',(189.444708741558,-3.93099113791891,127.845441742504));
#22406=CARTESIAN_POINT('Ctrl Pts',(189.436935841292,-4.01017996607299,127.95696888087));
#22407=CARTESIAN_POINT('Ctrl Pts',(189.42944550553,-4.08649008085959,128.064441726837));
#22408=CARTESIAN_POINT('Ctrl Pts',(189.421955169768,-4.15837924792512,128.174846993079));
#22409=CARTESIAN_POINT('Ctrl Pts',(189.414464834006,-4.22563545189443,128.287777996194));
#22410=CARTESIAN_POINT('Ctrl Pts',(189.406414631678,-4.29791873357895,128.409150048544));
#22411=CARTESIAN_POINT('Ctrl Pts',(189.398364429349,-4.36506593948658,128.533801166826));
#22412=CARTESIAN_POINT('Ctrl Pts',(189.39031422702,-4.42677811181953,128.661274382433));
#22413=CARTESIAN_POINT('Ctrl Pts',(189.382275040237,-4.48840583991566,128.788573169269));
#22414=CARTESIAN_POINT('Ctrl Pts',(189.374235853453,-4.54461318938345,128.918686050171));
#22415=CARTESIAN_POINT('Ctrl Pts',(189.366196666669,-4.59514535868655,129.051128689086));
#22416=CARTESIAN_POINT('Ctrl Pts',(189.358170521655,-4.64559555092435,129.183356469644));
#22417=CARTESIAN_POINT('Ctrl Pts',(189.350144376642,-4.69038878678416,129.317906148175));
#22418=CARTESIAN_POINT('Ctrl Pts',(189.342118231628,-4.72931719504994,129.454271016427));
#22419=CARTESIAN_POINT('Ctrl Pts',(189.339612754859,-4.74146925838755,129.496839274155));
#22420=CARTESIAN_POINT('Ctrl Pts',(189.33710727809,-4.7530501596044,129.539584253036));
#22421=CARTESIAN_POINT('Ctrl Pts',(189.334601801321,-4.76405452823404,129.582490119308));
#22422=CARTESIAN_POINT('Ctrl Pts',(191.084784152919,-4.76405452823405,129.582490119308));
#22423=CARTESIAN_POINT('Ctrl Pts',(191.074632403862,-4.8083124628535,129.755051134682));
#22424=CARTESIAN_POINT('Ctrl Pts',(191.064480654806,-4.84321315731302,129.930105519379));
#22425=CARTESIAN_POINT('Ctrl Pts',(191.054328905749,-4.86852710622365,130.106774150907));
#22426=CARTESIAN_POINT('Ctrl Pts',(191.04439137085,-4.89330690026231,130.279714861098));
#22427=CARTESIAN_POINT('Ctrl Pts',(191.03445383595,-4.90890030782398,130.45420266127));
#22428=CARTESIAN_POINT('Ctrl Pts',(191.02451630105,-4.91513668305779,130.629390764849));
#22429=CARTESIAN_POINT('Ctrl Pts',(191.021297346049,-4.91715676263013,130.686137496098));
#22430=CARTESIAN_POINT('Ctrl Pts',(191.018078391047,-4.91819542437289,130.74295751366));
#22431=CARTESIAN_POINT('Ctrl Pts',(191.014859436046,-4.91824790535574,130.799821458629));
#22432=CARTESIAN_POINT('',(191.360141518956,-4.92180512007539,130.806071931916));
#22433=CARTESIAN_POINT('Ctrl Pts',(191.430300680169,-4.76051597898714,129.583432241587));
#22434=CARTESIAN_POINT('Ctrl Pts',(191.406914637273,-4.86678982625872,129.983174630901));
#22435=CARTESIAN_POINT('Ctrl Pts',(191.383528594377,-4.92378206388031,130.394832064542));
#22436=CARTESIAN_POINT('Ctrl Pts',(191.360142551482,-4.9256493795537,130.806055125649));
#22437=CARTESIAN_POINT('Ctrl Pts',(191.360140564008,-4.9182496968395,130.806087475454));
#22438=CARTESIAN_POINT('Ctrl Pts',(191.354763444185,-4.91821654842555,130.90049719961));
#22439=CARTESIAN_POINT('Ctrl Pts',(191.349386324361,-4.91546519350092,130.994855987655));
#22440=CARTESIAN_POINT('Ctrl Pts',(191.344009204538,-4.91000321302235,131.089056087516));
#22441=CARTESIAN_POINT('Ctrl Pts',(191.336234870419,-4.90210618588047,131.225252243524));
#22442=CARTESIAN_POINT('Ctrl Pts',(191.3284605363,-4.88852553889003,131.361335297868));
#22443=CARTESIAN_POINT('Ctrl Pts',(191.32068620218,-4.86926290974064,131.49679240361));
#22444=CARTESIAN_POINT('Ctrl Pts',(191.312921449233,-4.85002402006014,131.632082570575));
#22445=CARTESIAN_POINT('Ctrl Pts',(191.305156696286,-4.82511713569348,131.76674794049));
#22446=CARTESIAN_POINT('Ctrl Pts',(191.297391943339,-4.79459585657098,131.900277418538));
#22447=CARTESIAN_POINT('Ctrl Pts',(191.289634902454,-4.76410489161315,132.033674273226));
#22448=CARTESIAN_POINT('Ctrl Pts',(191.281877861569,-4.72801071553388,132.165937102515));
#22449=CARTESIAN_POINT('Ctrl Pts',(191.274120820684,-4.68641846168075,132.296562033099));
#22450=CARTESIAN_POINT('Ctrl Pts',(191.266369629444,-4.64485757286983,132.427088458406));
#22451=CARTESIAN_POINT('Ctrl Pts',(191.258618438204,-4.59780697707092,132.555979072473));
#22452=CARTESIAN_POINT('Ctrl Pts',(191.250867246964,-4.5454223270494,132.682742615792));
#22453=CARTESIAN_POINT('Ctrl Pts',(191.243119350187,-4.49305994190156,132.809452281224));
#22454=CARTESIAN_POINT('Ctrl Pts',(191.235371453409,-4.4353681606558,132.934036313446));
#22455=CARTESIAN_POINT('Ctrl Pts',(191.227623556632,-4.37255162571712,133.056021192106));
#22456=CARTESIAN_POINT('Ctrl Pts',(191.219877280548,-4.3097482306434,133.177980554159));
#22457=CARTESIAN_POINT('Ctrl Pts',(191.212131004464,-4.24182239299693,133.297341496706));
#22458=CARTESIAN_POINT('Ctrl Pts',(191.20438472838,-4.16902561416592,133.413653336087));
#22459=CARTESIAN_POINT('Ctrl Pts',(191.196638395115,-4.09622829796563,133.529966034056));
#22460=CARTESIAN_POINT('Ctrl Pts',(191.188892061849,-4.01856017625269,133.643229252539));
#22461=CARTESIAN_POINT('Ctrl Pts',(191.181145728584,-3.93631693673612,133.753019980067));
#22462=CARTESIAN_POINT('Ctrl Pts',(191.173397660581,-3.85405527941647,133.862835294467));
#22463=CARTESIAN_POINT('Ctrl Pts',(191.165649592578,-3.76721669987783,133.969176257649));
#22464=CARTESIAN_POINT('Ctrl Pts',(191.157901524575,-3.67613788924386,134.071652046528));
#22465=CARTESIAN_POINT('Ctrl Pts',(191.150145221833,-3.58496227896587,134.174236747894));
#22466=CARTESIAN_POINT('Ctrl Pts',(191.142388919091,-3.48953769537748,134.272947776186));
#22467=CARTESIAN_POINT('Ctrl Pts',(191.134632616349,-3.3902388873648,134.367429989484));
#22468=CARTESIAN_POINT('Ctrl Pts',(191.126872173835,-3.29088708058837,134.461962630784));
#22469=CARTESIAN_POINT('Ctrl Pts',(191.119111731321,-3.18765722326609,134.552261702453));
#22470=CARTESIAN_POINT('Ctrl Pts',(191.111351288807,-3.08095725723101,134.638012328613));
#22471=CARTESIAN_POINT('Ctrl Pts',(191.103578388541,-2.97408600693812,134.723900609291));
#22472=CARTESIAN_POINT('Ctrl Pts',(191.095805488276,-2.86373383115774,134.805225621522));
#22473=CARTESIAN_POINT('Ctrl Pts',(191.088032588011,-2.7503384963244,134.881715301443));
#22474=CARTESIAN_POINT('Ctrl Pts',(191.080542252248,-2.64106536753748,134.955424388834));
#22475=CARTESIAN_POINT('Ctrl Pts',(191.073051916486,-2.52896675349539,135.024643431626));
#22476=CARTESIAN_POINT('Ctrl Pts',(191.065561580724,-2.41445430827056,135.08917023478));
#22477=CARTESIAN_POINT('Ctrl Pts',(191.057787246605,-2.29560008888017,135.156143591289));
#22478=CARTESIAN_POINT('Ctrl Pts',(191.050012912486,-2.17376888976368,135.218274023238));
#22479=CARTESIAN_POINT('Ctrl Pts',(191.042238578367,-2.04939306878735,135.275285702166));
#22480=CARTESIAN_POINT('Ctrl Pts',(191.03447382542,-1.92517052989461,135.332227119295));
#22481=CARTESIAN_POINT('Ctrl Pts',(191.026709072473,-1.79840996087941,135.384062173901));
#22482=CARTESIAN_POINT('Ctrl Pts',(191.018944319526,-1.66957033235678,135.430559701891));
#22483=CARTESIAN_POINT('Ctrl Pts',(191.011187278641,-1.54085866916962,135.477011047882));
#22484=CARTESIAN_POINT('Ctrl Pts',(191.003430237756,-1.41007242119069,135.518135285236));
#22485=CARTESIAN_POINT('Ctrl Pts',(190.995673196871,-1.27769233844608,135.553748509787));
#22486=CARTESIAN_POINT('Ctrl Pts',(190.987922005631,-1.14541208455148,135.589334878129));
#22487=CARTESIAN_POINT('Ctrl Pts',(190.980170814391,-1.01154076426068,135.619418404572));
#22488=CARTESIAN_POINT('Ctrl Pts',(190.972419623151,-0.876575822233106,
135.643864506435));
#22489=CARTESIAN_POINT('Ctrl Pts',(190.964671726373,-0.741668243906204,
135.668300218052));
#22490=CARTESIAN_POINT('Ctrl Pts',(190.956923829596,-0.605668352230964,
135.687103201124));
#22491=CARTESIAN_POINT('Ctrl Pts',(190.949175932819,-0.469085147509697,
135.700189677785));
#22492=CARTESIAN_POINT('Ctrl Pts',(190.941429656735,-0.332530513050464,
135.713273417038));
#22493=CARTESIAN_POINT('Ctrl Pts',(190.933683380651,-0.195393197179081,
135.720642991066));
#22494=CARTESIAN_POINT('Ctrl Pts',(190.925937104567,-0.0581883154667574,
135.722266389584));
#22495=CARTESIAN_POINT('Ctrl Pts',(190.918190771302,0.0790175790607411,
135.723889800085));
#22496=CARTESIAN_POINT('Ctrl Pts',(190.910444438036,0.216290649486569,135.71976694581));
#22497=CARTESIAN_POINT('Ctrl Pts',(190.902698104771,0.353115177852348,135.709917949172));
#22498=CARTESIAN_POINT('Ctrl Pts',(190.894950036768,0.489970347122603,135.700066746919));
#22499=CARTESIAN_POINT('Ctrl Pts',(190.887201968765,0.626376384571554,135.684486878679));
#22500=CARTESIAN_POINT('Ctrl Pts',(190.879453900762,0.7618224898918,135.663250362806));
#22501=CARTESIAN_POINT('Ctrl Pts',(190.87169759802,0.897412548944634,135.641991276511));
#22502=CARTESIAN_POINT('Ctrl Pts',(190.863941295278,1.03204025099248,135.615063593716));
#22503=CARTESIAN_POINT('Ctrl Pts',(190.856184992537,1.16520424415458,135.58259063839));
#22504=CARTESIAN_POINT('Ctrl Pts',(190.848424550022,1.29843931094942,135.550100351271));
#22505=CARTESIAN_POINT('Ctrl Pts',(190.840664107508,1.43020873675926,135.512059002598));
#22506=CARTESIAN_POINT('Ctrl Pts',(190.832903664994,1.56002710506518,135.468639607288));
#22507=CARTESIAN_POINT('Ctrl Pts',(190.825130764729,1.69005386934062,135.42515051131));
#22508=CARTESIAN_POINT('Ctrl Pts',(190.817357864463,1.81812295188554,135.376266256074));
#22509=CARTESIAN_POINT('Ctrl Pts',(190.809584964198,1.94376883421616,135.322208089718));
#22510=CARTESIAN_POINT('Ctrl Pts',(190.802094628436,2.06484717224159,135.270115073873));
#22511=CARTESIAN_POINT('Ctrl Pts',(190.794604292674,2.1836751523785,135.21321791848));
#22512=CARTESIAN_POINT('Ctrl Pts',(190.787113956912,2.29986015313222,135.151753668411));
#22513=CARTESIAN_POINT('Ctrl Pts',(190.779339622793,2.42045034350282,135.087958982619));
#22514=CARTESIAN_POINT('Ctrl Pts',(190.771565288673,2.5385751745423,135.019041960452));
#22515=CARTESIAN_POINT('Ctrl Pts',(190.763790954554,2.65376888396502,134.945217264807));
#22516=CARTESIAN_POINT('Ctrl Pts',(190.756026201607,2.768820627436,134.871483551501));
#22517=CARTESIAN_POINT('Ctrl Pts',(190.74826144866,2.88094811077286,134.792854407899));
#22518=CARTESIAN_POINT('Ctrl Pts',(190.740496695713,2.98970876424912,134.709591029139));
#22519=CARTESIAN_POINT('Ctrl Pts',(190.732739654828,3.09836139511106,134.62641034874));
#22520=CARTESIAN_POINT('Ctrl Pts',(190.724982613943,3.20365354236057,134.538604829062));
#22521=CARTESIAN_POINT('Ctrl Pts',(190.717225573058,3.3051706250811,134.446479534021));
#22522=CARTESIAN_POINT('Ctrl Pts',(190.709474381818,3.40661115297993,134.354423711382));
#22523=CARTESIAN_POINT('Ctrl Pts',(190.701723190578,3.50428199439297,134.258054859062));
#22524=CARTESIAN_POINT('Ctrl Pts',(190.693971999338,3.59780104010722,134.157718746115));
#22525=CARTESIAN_POINT('Ctrl Pts',(190.68622410256,3.69128033773231,134.057425278691));
#22526=CARTESIAN_POINT('Ctrl Pts',(190.678476205783,3.78061108335151,133.953168189747));
#22527=CARTESIAN_POINT('Ctrl Pts',(190.670728309006,3.86544766517695,133.845330431668));
#22528=CARTESIAN_POINT('Ctrl Pts',(190.662982032922,3.95026650101836,133.737515230923));
#22529=CARTESIAN_POINT('Ctrl Pts',(190.655235756838,4.03059280135912,133.626121157924));
#22530=CARTESIAN_POINT('Ctrl Pts',(190.647489480754,4.10612120249017,133.511564291648));
#22531=CARTESIAN_POINT('Ctrl Pts',(190.639743147489,4.18165016115467,133.397006579739));
#22532=CARTESIAN_POINT('Ctrl Pts',(190.631996814223,4.25238093473435,133.279286354372));
#22533=CARTESIAN_POINT('Ctrl Pts',(190.624250480958,4.31805169463097,133.158848380328));
#22534=CARTESIAN_POINT('Ctrl Pts',(190.616502412955,4.38373716103891,133.038383435034));
#22535=CARTESIAN_POINT('Ctrl Pts',(190.608754344952,4.44436017178771,132.915199873166));
#22536=CARTESIAN_POINT('Ctrl Pts',(190.601006276949,4.49970521791473,132.789766373166));
#22537=CARTESIAN_POINT('Ctrl Pts',(190.593249974207,4.55510908541542,132.664199560951));
#22538=CARTESIAN_POINT('Ctrl Pts',(190.585493671465,4.60522362466958,132.536378392067));
#22539=CARTESIAN_POINT('Ctrl Pts',(190.577737368723,4.64988159868781,132.40679132767));
#22540=CARTESIAN_POINT('Ctrl Pts',(190.569976926209,4.69456340801143,132.277135098755));
#22541=CARTESIAN_POINT('Ctrl Pts',(190.562216483695,4.73378273728387,132.145711470748));
#22542=CARTESIAN_POINT('Ctrl Pts',(190.554456041181,4.76742276936732,132.013022357102));
#22543=CARTESIAN_POINT('Ctrl Pts',(190.546683140915,4.80111680341668,131.880120239111));
#22544=CARTESIAN_POINT('Ctrl Pts',(190.53891024065,4.82921356238978,131.745948958842));
#22545=CARTESIAN_POINT('Ctrl Pts',(190.531137340384,4.85164756449836,131.611019760201));
#22546=CARTESIAN_POINT('Ctrl Pts',(190.523647004622,4.8732660341224,131.480995577798));
#22547=CARTESIAN_POINT('Ctrl Pts',(190.51615666886,4.88962627167772,131.350267930446));
#22548=CARTESIAN_POINT('Ctrl Pts',(190.508666333098,4.90071548822044,131.219295270272));
#22549=CARTESIAN_POINT('Ctrl Pts',(190.500891998979,4.91222515577889,131.083356741879));
#22550=CARTESIAN_POINT('Ctrl Pts',(190.49311766486,4.91809266973481,130.946723642184));
#22551=CARTESIAN_POINT('Ctrl Pts',(190.485343330741,4.91824687616993,130.809903860727));
#22552=CARTESIAN_POINT('Ctrl Pts',(190.477578577794,4.91840089255939,130.673252697422));
#22553=CARTESIAN_POINT('Ctrl Pts',(190.469813824847,4.91285561076338,130.536415697335));
#22554=CARTESIAN_POINT('Ctrl Pts',(190.4620490719,4.90159156190185,130.399906389262));
#22555=CARTESIAN_POINT('Ctrl Pts',(190.454292031015,4.89033870065244,130.26353266416));
#22556=CARTESIAN_POINT('Ctrl Pts',(190.44653499013,4.8733784076575,130.127486370495));
#22557=CARTESIAN_POINT('Ctrl Pts',(190.438777949245,4.85074325071888,129.992281201434));
#22558=CARTESIAN_POINT('Ctrl Pts',(190.431026758005,4.82812516312819,129.857177991643));
#22559=CARTESIAN_POINT('Ctrl Pts',(190.423275566765,4.79984079389075,129.722915027962));
#22560=CARTESIAN_POINT('Ctrl Pts',(190.415524375525,4.76597450893968,129.590000686311));
#22561=CARTESIAN_POINT('Ctrl Pts',(190.407776478747,4.73212261806311,129.457142836802));
#22562=CARTESIAN_POINT('Ctrl Pts',(190.40002858197,4.6926936264518,129.325632847339));
#22563=CARTESIAN_POINT('Ctrl Pts',(190.392280685193,4.64782291118133,129.195968486027));
#22564=CARTESIAN_POINT('Ctrl Pts',(190.384534409109,4.60296158189719,129.066331247704));
#22565=CARTESIAN_POINT('Ctrl Pts',(190.376788133025,4.55266092085215,128.938539238861));
#22566=CARTESIAN_POINT('Ctrl Pts',(190.369041856941,4.49710593053007,128.813074271484));
#22567=CARTESIAN_POINT('Ctrl Pts',(190.361295523676,4.44155053011368,128.687608377954));
#22568=CARTESIAN_POINT('Ctrl Pts',(190.35354919041,4.38074088131789,128.564469917655));
#22569=CARTESIAN_POINT('Ctrl Pts',(190.345802857145,4.31490965259537,128.444119580629));
#22570=CARTESIAN_POINT('Ctrl Pts',(190.338054789142,4.24906368142562,128.32374229198));
#22571=CARTESIAN_POINT('Ctrl Pts',(190.330306721139,4.17819408019494,128.206154711989));
#22572=CARTESIAN_POINT('Ctrl Pts',(190.322558653136,4.10257867349393,128.091791486596));
#22573=CARTESIAN_POINT('Ctrl Pts',(190.314802350394,4.02688290183881,127.977306714606));
#22574=CARTESIAN_POINT('Ctrl Pts',(190.307046047653,3.94643146495612,127.866053469427));
#22575=CARTESIAN_POINT('Ctrl Pts',(190.299289744911,3.86154492337111,127.758436477459));
#22576=CARTESIAN_POINT('Ctrl Pts',(190.291529302397,3.77661307528294,127.650762047062));
#22577=CARTESIAN_POINT('Ctrl Pts',(190.283768859882,3.68724166038745,127.546728033458));
#22578=CARTESIAN_POINT('Ctrl Pts',(190.276008417368,3.59378981017076,127.446704014694));
#22579=CARTESIAN_POINT('Ctrl Pts',(190.268235517103,3.50018794274785,127.346519428494));
#22580=CARTESIAN_POINT('Ctrl Pts',(190.260462616837,3.40249282925593,127.250357975128));
#22581=CARTESIAN_POINT('Ctrl Pts',(190.252689716572,3.30109919916671,127.158551086096));
#22582=CARTESIAN_POINT('Ctrl Pts',(190.24519938081,3.2033914829259,127.070081608727));
#22583=CARTESIAN_POINT('Ctrl Pts',(190.237709045048,3.10224971882835,126.985655790931));
#22584=CARTESIAN_POINT('Ctrl Pts',(190.230218709286,2.99805270289559,126.905532196981));
#22585=CARTESIAN_POINT('Ctrl Pts',(190.222444375167,2.88990502543422,126.822370692614));
#22586=CARTESIAN_POINT('Ctrl Pts',(190.214670041048,2.7781232636251,126.743580659112));
#22587=CARTESIAN_POINT('Ctrl Pts',(190.206895706929,2.66309625889214,126.669496486984));
#22588=CARTESIAN_POINT('Ctrl Pts',(190.199130953982,2.54821101466232,126.595503616977));
#22589=CARTESIAN_POINT('Ctrl Pts',(190.191366201034,2.43008881080192,126.526205278626));
#22590=CARTESIAN_POINT('Ctrl Pts',(190.183601448087,2.30915117022697,126.461895426509));
#22591=CARTESIAN_POINT('Ctrl Pts',(190.175844407202,2.18833364662157,126.397649447844));
#22592=CARTESIAN_POINT('Ctrl Pts',(190.168087366317,2.06470659408811,126.33838227784));
#22593=CARTESIAN_POINT('Ctrl Pts',(190.160330325432,1.938719800928,126.284344179986));
#22594=CARTESIAN_POINT('Ctrl Pts',(190.152579134192,1.81282801538859,126.230346832682));
#22595=CARTESIAN_POINT('Ctrl Pts',(190.144827942952,1.68458038906157,126.181570862152));
#22596=CARTESIAN_POINT('Ctrl Pts',(190.137076751712,1.55445023485514,126.138220078549));
#22597=CARTESIAN_POINT('Ctrl Pts',(190.129328854935,1.42437538943564,126.094887720185));
#22598=CARTESIAN_POINT('Ctrl Pts',(190.121580958158,1.29241997767127,126.0569760859));
#22599=CARTESIAN_POINT('Ctrl Pts',(190.113833061381,1.1590759605821,126.024640334945));
#22600=CARTESIAN_POINT('Ctrl Pts',(190.106086785297,1.02575983618676,125.992311347931));
#22601=CARTESIAN_POINT('Ctrl Pts',(190.098340509213,0.891056063932395,125.965556016384));
#22602=CARTESIAN_POINT('Ctrl Pts',(190.090594233128,0.755470004251004,125.944479123622));
#22603=CARTESIAN_POINT('Ctrl Pts',(190.082847899863,0.619882943704145,125.923402075275));
#22604=CARTESIAN_POINT('Ctrl Pts',(190.075101566598,0.483413969059678,125.90800360941));
#22605=CARTESIAN_POINT('Ctrl Pts',(190.067355233332,0.346576434879642,125.898336989689));
#22606=CARTESIAN_POINT('Ctrl Pts',(190.059607165329,0.20970825688259,125.888668205195));
#22607=CARTESIAN_POINT('Ctrl Pts',(190.051859097326,0.0724717450308378,
125.884733848621));
#22608=CARTESIAN_POINT('Ctrl Pts',(190.044111029323,-0.0646172497580651,
125.886535115016));
#22609=CARTESIAN_POINT('Ctrl Pts',(190.036354726582,-0.201851944362056,
125.888338295818));
#22610=CARTESIAN_POINT('Ctrl Pts',(190.02859842384,-0.33893841715767,125.89588927164));
#22611=CARTESIAN_POINT('Ctrl Pts',(190.020842121098,-0.475362889567487,
125.909137110338));
#22612=CARTESIAN_POINT('Ctrl Pts',(190.013081678584,-0.611860175825985,
125.922392019806));
#22613=CARTESIAN_POINT('Ctrl Pts',(190.00532123607,-0.747694370636893,125.941349796762));
#22614=CARTESIAN_POINT('Ctrl Pts',(189.997560793555,-0.882360418181386,
125.965908059679));
#22615=CARTESIAN_POINT('Ctrl Pts',(189.98978789329,-1.01724264362044,125.990505745699));
#22616=CARTESIAN_POINT('Ctrl Pts',(189.982014993024,-1.15095259295001,126.02072179713));
#22617=CARTESIAN_POINT('Ctrl Pts',(189.974242092759,-1.28299806253933,126.056403263712));
#22618=CARTESIAN_POINT('Ctrl Pts',(189.966751756997,-1.4102433467065,126.090787619106));
#22619=CARTESIAN_POINT('Ctrl Pts',(189.959261421235,-1.53594277230061,126.130246832991));
#22620=CARTESIAN_POINT('Ctrl Pts',(189.951771085473,-1.65967405337326,126.17460197385));
#22621=CARTESIAN_POINT('Ctrl Pts',(189.943996623503,-1.78809875550871,126.220639610442));
#22622=CARTESIAN_POINT('Ctrl Pts',(189.936222161534,-1.91480987036354,126.272097770317));
#22623=CARTESIAN_POINT('Ctrl Pts',(189.928447699565,-2.03931586329617,126.328830048772));
#22624=CARTESIAN_POINT('Ctrl Pts',(189.92068284859,-2.16366793863765,126.385492193289));
#22625=CARTESIAN_POINT('Ctrl Pts',(189.912917997615,-2.28581996373698,126.447415322767));
#22626=CARTESIAN_POINT('Ctrl Pts',(189.905153146641,-2.40529676525213,126.514403679138));
#22627=CARTESIAN_POINT('Ctrl Pts',(189.897396037425,-2.5246544452745,126.581325246367));
#22628=CARTESIAN_POINT('Ctrl Pts',(189.88963892821,-2.6413418709589,126.653301800276));
#22629=CARTESIAN_POINT('Ctrl Pts',(189.881881818995,-2.75490535575686,126.730090186762));
#22630=CARTESIAN_POINT('Ctrl Pts',(189.874130589026,-2.86838276883409,126.806820374008));
#22631=CARTESIAN_POINT('Ctrl Pts',(189.866379359057,-2.97874063130287,126.888354916463));
#22632=CARTESIAN_POINT('Ctrl Pts',(189.858628129089,-3.08555162944487,126.974405760844));
#22633=CARTESIAN_POINT('Ctrl Pts',(189.850880345889,-3.19231513152848,127.060418340663));
#22634=CARTESIAN_POINT('Ctrl Pts',(189.84313256269,-3.29553460322023,127.150942982288));
#22635=CARTESIAN_POINT('Ctrl Pts',(189.835384779491,-3.39481360629566,127.245649665408));
#22636=CARTESIAN_POINT('Ctrl Pts',(189.827638659146,-3.49407130178288,127.340336022266));
#22637=CARTESIAN_POINT('Ctrl Pts',(189.819892538802,-3.58938992840192,127.439202365372));
#22638=CARTESIAN_POINT('Ctrl Pts',(189.812146418457,-3.68040819178631,127.541880180179));
#22639=CARTESIAN_POINT('Ctrl Pts',(189.804400283122,-3.77142663131764,127.644558193698));
#22640=CARTESIAN_POINT('Ctrl Pts',(189.796654147786,-3.85814443183768,127.751047400979));
#22641=CARTESIAN_POINT('Ctrl Pts',(189.788908012451,-3.94023932495192,127.860944723642));
#22642=CARTESIAN_POINT('Ctrl Pts',(189.781160184633,-4.02235215528922,127.970866058186));
#22643=CARTESIAN_POINT('Ctrl Pts',(189.773412356815,-4.0998398346877,128.084196676547));
#22644=CARTESIAN_POINT('Ctrl Pts',(189.765664528998,-4.17242255225989,128.200503265887));
#22645=CARTESIAN_POINT('Ctrl Pts',(189.757909049044,-4.24507695609062,128.31692472533));
#22646=CARTESIAN_POINT('Ctrl Pts',(189.750153569091,-4.31281651589305,128.436327693783));
#22647=CARTESIAN_POINT('Ctrl Pts',(189.742398089138,-4.37540644239081,128.55825253326));
#22648=CARTESIAN_POINT('Ctrl Pts',(189.734638486836,-4.43802963794533,128.68024218068));
#22649=CARTESIAN_POINT('Ctrl Pts',(189.726878884534,-4.49549758245539,128.804756015469));
#22650=CARTESIAN_POINT('Ctrl Pts',(189.719119282232,-4.54762346778534,128.931313939624));
#22651=CARTESIAN_POINT('Ctrl Pts',(189.711348586192,-4.59982387637704,129.058052800933));
#22652=CARTESIAN_POINT('Ctrl Pts',(189.703577890153,-4.64666683607839,129.186841222174));
#22653=CARTESIAN_POINT('Ctrl Pts',(189.695807194114,-4.68801507639694,129.317182852141));
#22654=CARTESIAN_POINT('Ctrl Pts',(189.690573763844,-4.71586240582347,129.404965700449));
#22655=CARTESIAN_POINT('Ctrl Pts',(189.685340333575,-4.74121849260404,129.493452762972));
#22656=CARTESIAN_POINT('Ctrl Pts',(189.680106903305,-4.76405452823404,129.582490119308));
#22657=CARTESIAN_POINT('Origin',(213.235140564004,0.,130.804360617566));
#22658=CARTESIAN_POINT('',(187.584954980304,-4.76405452823404,129.582490119308));
#22659=CARTESIAN_POINT('',(187.929867347344,-4.76405452823404,129.582490119308));
#22660=CARTESIAN_POINT('',(213.235140564004,-4.76405452823405,129.582490119308));
#22661=CARTESIAN_POINT('',(189.264859435947,-4.91824989634823,130.805370355446));
#22662=CARTESIAN_POINT('Ctrl Pts',(189.264859435947,-4.91824989634823,130.805370355446));
#22663=CARTESIAN_POINT('Ctrl Pts',(189.256607171556,-4.91821981685867,130.951882088204));
#22664=CARTESIAN_POINT('Ctrl Pts',(189.248354907165,-4.91163874752937,131.098225889341));
#22665=CARTESIAN_POINT('Ctrl Pts',(189.240102642774,-4.89857698727829,131.243822290761));
#22666=CARTESIAN_POINT('Ctrl Pts',(189.231428856725,-4.88484803865739,131.396855685653));
#22667=CARTESIAN_POINT('Ctrl Pts',(189.222755070677,-4.86395906746465,131.549062909309));
#22668=CARTESIAN_POINT('Ctrl Pts',(189.214081284629,-4.83605175230801,131.699785941922));
#22669=CARTESIAN_POINT('Ctrl Pts',(189.205787676123,-4.80936763247221,131.843902688434));
#22670=CARTESIAN_POINT('Ctrl Pts',(189.197494067618,-4.77626745182874,131.986662328151));
#22671=CARTESIAN_POINT('Ctrl Pts',(189.189200459113,-4.73692581437122,132.127507204926));
#22672=CARTESIAN_POINT('Ctrl Pts',(189.180893279678,-4.69751980172804,132.268582547836));
#22673=CARTESIAN_POINT('Ctrl Pts',(189.172586100243,-4.65185203318383,132.407736580464));
#22674=CARTESIAN_POINT('Ctrl Pts',(189.164278920808,-4.60014566525104,132.544430421043));
#22675=CARTESIAN_POINT('Ctrl Pts',(189.155952232729,-4.54831786968213,132.681445274498));
#22676=CARTESIAN_POINT('Ctrl Pts',(189.147625544649,-4.49042324122083,132.815988102357));
#22677=CARTESIAN_POINT('Ctrl Pts',(189.139298856569,-4.42673210121107,132.947541890022));
#22678=CARTESIAN_POINT('Ctrl Pts',(189.138204974444,-4.41836495704328,132.964824191878));
#22679=CARTESIAN_POINT('Ctrl Pts',(189.137111092319,-4.40989783749088,132.982054947649));
#22680=CARTESIAN_POINT('Ctrl Pts',(189.136017210193,-4.40133141131699,132.99923302166));
#22681=CARTESIAN_POINT('Ctrl Pts',(189.128242876074,-4.34044892888366,133.121319381593));
#22682=CARTESIAN_POINT('Ctrl Pts',(189.120468541955,-4.27438642335554,133.241064014106));
#22683=CARTESIAN_POINT('Ctrl Pts',(189.112694207836,-4.20334731880043,133.357996139725));
#22684=CARTESIAN_POINT('Ctrl Pts',(189.104929454889,-4.13239576359281,133.47478415695));
#22685=CARTESIAN_POINT('Ctrl Pts',(189.097164701942,-4.05648001367186,133.588766232983));
#22686=CARTESIAN_POINT('Ctrl Pts',(189.089399948995,-3.97585056850522,133.699493657586));
#22687=CARTESIAN_POINT('Ctrl Pts',(189.08164290811,-3.8953012056402,133.81011110615));
#22688=CARTESIAN_POINT('Ctrl Pts',(189.073885867225,-3.81004769299365,133.917480022228));
#22689=CARTESIAN_POINT('Ctrl Pts',(189.06612882634,-3.7203850578337,134.0211786236));
#22690=CARTESIAN_POINT('Ctrl Pts',(189.0583776351,-3.63079003796426,134.124799025051));
#22691=CARTESIAN_POINT('Ctrl Pts',(189.050626443859,-3.53679276837891,134.224754326412));
#22692=CARTESIAN_POINT('Ctrl Pts',(189.042875252619,-3.43872974898933,134.320654231006));
#22693=CARTESIAN_POINT('Ctrl Pts',(189.035127355842,-3.34070840899898,134.416513375581));
#22694=CARTESIAN_POINT('Ctrl Pts',(189.027379459065,-3.23862503510299,134.508320278819));
#22695=CARTESIAN_POINT('Ctrl Pts',(189.019631562288,-3.13285417567755,134.595720238657));
#22696=CARTESIAN_POINT('Ctrl Pts',(189.011885286204,-3.02710544123581,134.683101916308));
#22697=CARTESIAN_POINT('Ctrl Pts',(189.00413901012,-2.91767105670176,134.766078235263));
#22698=CARTESIAN_POINT('Ctrl Pts',(188.996392734036,-2.80495965334516,134.844333935003));
#22699=CARTESIAN_POINT('Ctrl Pts',(188.98864640077,-2.69224741797864,134.922590212409));
#22700=CARTESIAN_POINT('Ctrl Pts',(188.980900067505,-2.57625843666835,134.996125578092));
#22701=CARTESIAN_POINT('Ctrl Pts',(188.97315373424,-2.45743106294825,135.064667605725));
#22702=CARTESIAN_POINT('Ctrl Pts',(188.965405666237,-2.33857707866192,135.13322498287));
#22703=CARTESIAN_POINT('Ctrl Pts',(188.957657598234,-2.21688377571787,135.19678660152));
#22704=CARTESIAN_POINT('Ctrl Pts',(188.949909530231,-2.09281452597186,135.255125767782));
#22705=CARTESIAN_POINT('Ctrl Pts',(188.942153227489,-1.96861341395046,135.313526937605));
#22706=CARTESIAN_POINT('Ctrl Pts',(188.934396924747,-1.84203166516669,135.366694400722));
#22707=CARTESIAN_POINT('Ctrl Pts',(188.926640622005,-1.71355358688341,135.414449246582));
#22708=CARTESIAN_POINT('Ctrl Pts',(188.918880179491,-1.5850069359812,135.46222958064));
#22709=CARTESIAN_POINT('Ctrl Pts',(188.911119736977,-1.45456231049509,135.504591420412));
#22710=CARTESIAN_POINT('Ctrl Pts',(188.903359294463,-1.3227186760497,135.541405937861));
#22711=CARTESIAN_POINT('Ctrl Pts',(188.895586394197,-1.19066339449785,135.578279553241));
#22712=CARTESIAN_POINT('Ctrl Pts',(188.887813493932,-1.05720499698669,135.609587961818));
#22713=CARTESIAN_POINT('Ctrl Pts',(188.880040593666,-0.922853008814749,
135.635253432214));
#22714=CARTESIAN_POINT('Ctrl Pts',(188.872550257904,-0.793385053824595,
135.659985898115));
#22715=CARTESIAN_POINT('Ctrl Pts',(188.865059922142,-0.663087653395633,
135.679478527407));
#22716=CARTESIAN_POINT('Ctrl Pts',(188.85756958638,-0.532418820732127,135.693707533242));
#22717=CARTESIAN_POINT('Ctrl Pts',(188.849795252261,-0.396795639562776,
135.708476036158));
#22718=CARTESIAN_POINT('Ctrl Pts',(188.842020918142,-0.260342690980689,
135.717620678069));
#22719=CARTESIAN_POINT('Ctrl Pts',(188.834246584023,-0.123566010769087,
135.721058137597));
#22720=CARTESIAN_POINT('Ctrl Pts',(188.826481831076,0.0130421044082147,
135.724491360764));
#22721=CARTESIAN_POINT('Ctrl Pts',(188.818717078129,0.149972770293301,135.722231386573));
#22722=CARTESIAN_POINT('Ctrl Pts',(188.810952325181,0.28671307317168,135.714246428476));
#22723=CARTESIAN_POINT('Ctrl Pts',(188.803195284296,0.423317563653494,135.706269401151));
#22724=CARTESIAN_POINT('Ctrl Pts',(188.795438243411,0.559731679614168,135.692578728228));
#22725=CARTESIAN_POINT('Ctrl Pts',(188.787681202526,0.695441094281352,135.673194640911));
#22726=CARTESIAN_POINT('Ctrl Pts',(188.779930011286,0.8310481694232,135.653825171285));
#22727=CARTESIAN_POINT('Ctrl Pts',(188.772178820046,0.965951215561337,135.628770888172));
#22728=CARTESIAN_POINT('Ctrl Pts',(188.764427628806,1.09963997862434,135.598103933589));
#22729=CARTESIAN_POINT('Ctrl Pts',(188.756679732029,1.23327192039691,135.567450013279));
#22730=CARTESIAN_POINT('Ctrl Pts',(188.748931835252,1.36569022531323,135.531188253377));
#22731=CARTESIAN_POINT('Ctrl Pts',(188.741183938475,1.49639401993704,135.489442046911));
#22732=CARTESIAN_POINT('Ctrl Pts',(188.733437662391,1.62707047414466,135.447704572852));
#22733=CARTESIAN_POINT('Ctrl Pts',(188.725691386307,1.75603275921754,135.400485053005));
#22734=CARTESIAN_POINT('Ctrl Pts',(188.717945110223,1.88279476236884,135.34795687442));
#22735=CARTESIAN_POINT('Ctrl Pts',(188.710198776957,2.00955770124844,135.295428308083));
#22736=CARTESIAN_POINT('Ctrl Pts',(188.702452443692,2.13411996461381,135.237591154481));
#22737=CARTESIAN_POINT('Ctrl Pts',(188.694706110426,2.25601541168853,135.174666959772));
#22738=CARTESIAN_POINT('Ctrl Pts',(188.686958042423,2.3779381564034,135.111728673626));
#22739=CARTESIAN_POINT('Ctrl Pts',(188.679209974421,2.4971925490977,135.043701258784));
#22740=CARTESIAN_POINT('Ctrl Pts',(188.671461906418,2.61333740197348,134.970852029527));
#22741=CARTESIAN_POINT('Ctrl Pts',(188.663705603676,2.72960569498105,134.897925375242));
#22742=CARTESIAN_POINT('Ctrl Pts',(188.655949300934,2.84275751463042,134.820166877511));
#22743=CARTESIAN_POINT('Ctrl Pts',(188.648192998192,2.95238055850332,134.737887292227));
#22744=CARTESIAN_POINT('Ctrl Pts',(188.640432555678,3.06206211149548,134.655563791851));
#22745=CARTESIAN_POINT('Ctrl Pts',(188.632672113164,3.1682108334075,134.568714643188));
#22746=CARTESIAN_POINT('Ctrl Pts',(188.62491167065,3.27044863445584,134.477690005449));
#22747=CARTESIAN_POINT('Ctrl Pts',(188.617138770384,3.37285055669868,134.386519246881));
#22748=CARTESIAN_POINT('Ctrl Pts',(188.609365870119,3.47132873129138,134.291159876902));
#22749=CARTESIAN_POINT('Ctrl Pts',(188.601592969853,3.5655423497568,134.191998557871));
#22750=CARTESIAN_POINT('Ctrl Pts',(188.594102634091,3.65633106588129,134.096442002558));
#22751=CARTESIAN_POINT('Ctrl Pts',(188.586612298329,3.74315969458697,133.997355351629));
#22752=CARTESIAN_POINT('Ctrl Pts',(188.579121962567,3.82576065600049,133.895111087193));
#22753=CARTESIAN_POINT('Ctrl Pts',(188.571347628448,3.91149345797192,133.788990200394));
#22754=CARTESIAN_POINT('Ctrl Pts',(188.563573294329,3.99294325595813,133.679131372527));
#22755=CARTESIAN_POINT('Ctrl Pts',(188.55579896021,4.06976642462402,133.565915308588));
#22756=CARTESIAN_POINT('Ctrl Pts',(188.548034207263,4.14649491560041,133.452838773329));
#22757=CARTESIAN_POINT('Ctrl Pts',(188.540269454316,4.21860790493604,133.336413554789));
#22758=CARTESIAN_POINT('Ctrl Pts',(188.532504701369,4.28580140731598,133.217054000395));
#22759=CARTESIAN_POINT('Ctrl Pts',(188.524747660484,4.35292817216208,133.097812995594));
#22760=CARTESIAN_POINT('Ctrl Pts',(188.516990619599,4.41514498306898,132.97564379326));
#22761=CARTESIAN_POINT('Ctrl Pts',(188.509233578714,4.47219085493765,132.850990046533));
#22762=CARTESIAN_POINT('Ctrl Pts',(188.501482387474,4.52919370807062,132.726430302165));
#22763=CARTESIAN_POINT('Ctrl Pts',(188.493731196234,4.58103322174094,132.599390096789));
#22764=CARTESIAN_POINT('Ctrl Pts',(188.485980004993,4.6274942862818,132.470337716127));
#22765=CARTESIAN_POINT('Ctrl Pts',(188.478232108216,4.67393560363083,132.341340186169));
#22766=CARTESIAN_POINT('Ctrl Pts',(188.470484211439,4.71500288634316,132.210332548992));
#22767=CARTESIAN_POINT('Ctrl Pts',(188.462736314662,4.75052921414137,132.077802900549));
#22768=CARTESIAN_POINT('Ctrl Pts',(188.454990038578,4.78604811059766,131.945300974451));
#22769=CARTESIAN_POINT('Ctrl Pts',(188.447243762494,4.81602825638518,131.81127804774));
#22770=CARTESIAN_POINT('Ctrl Pts',(188.43949748641,4.84035277110316,131.676236820805));
#22771=CARTESIAN_POINT('Ctrl Pts',(188.431751153145,4.86467746537918,131.541194597026));
#22772=CARTESIAN_POINT('Ctrl Pts',(188.424004819879,4.88334637597157,131.405134442797));
#22773=CARTESIAN_POINT('Ctrl Pts',(188.416258486614,4.89629393546274,131.268568286666));
#22774=CARTESIAN_POINT('Ctrl Pts',(188.408510418611,4.90924439447009,131.13197154749));
#22775=CARTESIAN_POINT('Ctrl Pts',(188.400762350608,4.91647091592922,130.994868970073));
#22776=CARTESIAN_POINT('Ctrl Pts',(188.393014282605,4.91795992613311,130.857776228101));
#22777=CARTESIAN_POINT('Ctrl Pts',(188.385257979863,4.91945051887476,130.720537782331));
#22778=CARTESIAN_POINT('Ctrl Pts',(188.377501677121,4.91519141490565,130.583309584453));
#22779=CARTESIAN_POINT('Ctrl Pts',(188.36974537438,4.90522120243238,130.44660648732));
#22780=CARTESIAN_POINT('Ctrl Pts',(188.361984931865,4.89524566855652,130.309830427629));
#22781=CARTESIAN_POINT('Ctrl Pts',(188.354224489351,4.87955299711073,130.173580415335));
#22782=CARTESIAN_POINT('Ctrl Pts',(188.346464046837,4.85823342019293,130.03836381769));
#22783=CARTESIAN_POINT('Ctrl Pts',(188.338691146572,4.8368796191976,129.902930158358));
#22784=CARTESIAN_POINT('Ctrl Pts',(188.330918246306,4.80988093934744,129.768533612271));
#22785=CARTESIAN_POINT('Ctrl Pts',(188.323145346041,4.77737847532777,129.635669911701));
#22786=CARTESIAN_POINT('Ctrl Pts',(188.315655010279,4.74605755774389,129.50763614131));
#22787=CARTESIAN_POINT('Ctrl Pts',(188.308164674517,4.70962614676043,129.381026001712));
#22788=CARTESIAN_POINT('Ctrl Pts',(188.300674338755,4.66825298866656,129.256265951111));
#22789=CARTESIAN_POINT('Ctrl Pts',(188.292900004636,4.62531115470858,129.126775585272));
#22790=CARTESIAN_POINT('Ctrl Pts',(188.285125670517,4.57690941679345,128.998868183534));
#22791=CARTESIAN_POINT('Ctrl Pts',(188.277351336398,4.52318233493014,128.873038627975));
#22792=CARTESIAN_POINT('Ctrl Pts',(188.269586583451,4.46952146689349,128.747364146098));
#22793=CARTESIAN_POINT('Ctrl Pts',(188.261821830503,4.41054846539562,128.623762771359));
#22794=CARTESIAN_POINT('Ctrl Pts',(188.254057077556,4.34644762117504,128.502714220119));
#22795=CARTESIAN_POINT('Ctrl Pts',(188.246300036671,4.28241044281667,128.381785896006));
#22796=CARTESIAN_POINT('Ctrl Pts',(188.238542995786,4.21325573890659,128.263405692909));
#22797=CARTESIAN_POINT('Ctrl Pts',(188.230785954901,4.13921569857526,128.148032990339));
#22798=CARTESIAN_POINT('Ctrl Pts',(188.223034763661,4.06523149241429,128.032747291222));
#22799=CARTESIAN_POINT('Ctrl Pts',(188.215283572421,3.98636949305475,127.920464906065));
#22800=CARTESIAN_POINT('Ctrl Pts',(188.207532381181,3.90290741050956,127.811619932594));
#22801=CARTESIAN_POINT('Ctrl Pts',(188.199784484404,3.81948080157582,127.702821221139));
#22802=CARTESIAN_POINT('Ctrl Pts',(188.192036587627,3.73145823551986,127.597457325174));
#22803=CARTESIAN_POINT('Ctrl Pts',(188.18428869085,3.63916013680356,127.495932507239));
#22804=CARTESIAN_POINT('Ctrl Pts',(188.176542414766,3.54688134485975,127.394428926108));
#22805=CARTESIAN_POINT('Ctrl Pts',(188.168796138682,3.45032906199472,127.296763114795));
#22806=CARTESIAN_POINT('Ctrl Pts',(188.161049862597,3.34986304757216,127.203305129933));
#22807=CARTESIAN_POINT('Ctrl Pts',(188.153303529332,3.24939629153235,127.109846455185));
#22808=CARTESIAN_POINT('Ctrl Pts',(188.145557196067,3.14501603254435,127.020595935158));
#22809=CARTESIAN_POINT('Ctrl Pts',(188.137810862801,3.03711752980305,126.935885443461));
#22810=CARTESIAN_POINT('Ctrl Pts',(188.130062794798,2.92919486394014,126.851155981437));
#22811=CARTESIAN_POINT('Ctrl Pts',(188.122314726795,2.81775269397828,126.770968812257));
#22812=CARTESIAN_POINT('Ctrl Pts',(188.114566658792,2.703217533875,126.695614090089));
#22813=CARTESIAN_POINT('Ctrl Pts',(188.106810356051,2.58856064444062,126.620179280026));
#22814=CARTESIAN_POINT('Ctrl Pts',(188.099054053309,2.47080452533179,126.549587391881));
#22815=CARTESIAN_POINT('Ctrl Pts',(188.091297750567,2.35040319470329,126.484084250847));
#22816=CARTESIAN_POINT('Ctrl Pts',(188.083537308053,2.22993760225931,126.418546148814));
#22817=CARTESIAN_POINT('Ctrl Pts',(188.075776865539,2.10682433588469,126.358102378005));
#22818=CARTESIAN_POINT('Ctrl Pts',(188.068016423024,1.98153903066888,126.302951267992));
#22819=CARTESIAN_POINT('Ctrl Pts',(188.060243522759,1.85605260635887,126.24771162452));
#22820=CARTESIAN_POINT('Ctrl Pts',(188.052470622493,1.72838753988925,126.197781762542));
#22821=CARTESIAN_POINT('Ctrl Pts',(188.044697722228,1.59903716998487,126.153310930505));
#22822=CARTESIAN_POINT('Ctrl Pts',(188.037207386466,1.47438901184074,126.110456725228));
#22823=CARTESIAN_POINT('Ctrl Pts',(188.029717050704,1.34817624808902,126.072671630003));
#22824=CARTESIAN_POINT('Ctrl Pts',(188.022226714942,1.22084888158536,126.040044184873));
#22825=CARTESIAN_POINT('Ctrl Pts',(188.014452380823,1.08869385928014,126.006179660243));
#22826=CARTESIAN_POINT('Ctrl Pts',(188.006678046704,0.954919418051348,125.977764338209));
#22827=CARTESIAN_POINT('Ctrl Pts',(187.998903712585,0.820014649177363,125.954952505473));
#22828=CARTESIAN_POINT('Ctrl Pts',(187.991138959638,0.685276138374253,125.932168786282));
#22829=CARTESIAN_POINT('Ctrl Pts',(187.98337420669,0.54941045342816,125.914974880467));
#22830=CARTESIAN_POINT('Ctrl Pts',(187.975609453743,0.412920806945482,125.903475037419));
#22831=CARTESIAN_POINT('Ctrl Pts',(187.967852412858,0.276566723903787,125.891986616178));
#22832=CARTESIAN_POINT('Ctrl Pts',(187.960095371973,0.139590299674858,125.886181035769));
#22833=CARTESIAN_POINT('Ctrl Pts',(187.952338331088,0.00250352715083474,
125.886111254749));
#22834=CARTESIAN_POINT('Ctrl Pts',(187.944587139848,-0.134479867171555,
125.886041526351));
#22835=CARTESIAN_POINT('Ctrl Pts',(187.936835948608,-0.271573054772387,
125.891698988073));
#22836=CARTESIAN_POINT('Ctrl Pts',(187.929084757368,-0.408260707894014,
125.90308463504));
#22837=CARTESIAN_POINT('Ctrl Pts',(187.921336860591,-0.544890265116803,
125.914465442803));
#22838=CARTESIAN_POINT('Ctrl Pts',(187.913588963814,-0.681114241876996,
125.931569561129));
#22839=CARTESIAN_POINT('Ctrl Pts',(187.905841067037,-0.816419323400283,
125.954345921621));
#22840=CARTESIAN_POINT('Ctrl Pts',(187.898094790952,-0.951696102017355,
125.977117517791));
#22841=CARTESIAN_POINT('Ctrl Pts',(187.890348514868,-1.08605398242313,126.005558931233));
#22842=CARTESIAN_POINT('Ctrl Pts',(187.882602238784,-1.21898716676947,126.039567510856));
#22843=CARTESIAN_POINT('Ctrl Pts',(187.874855905519,-1.35192133239828,126.073576341522));
#22844=CARTESIAN_POINT('Ctrl Pts',(187.867109572253,-1.48343040221569,126.113152323472));
#22845=CARTESIAN_POINT('Ctrl Pts',(187.859363238988,-1.61302151430496,126.158142299741));
#22846=CARTESIAN_POINT('Ctrl Pts',(187.851615170985,-1.74264164742518,126.203142351204));
#22847=CARTESIAN_POINT('Ctrl Pts',(187.843867102982,-1.87034259886549,126.253558681377));
#22848=CARTESIAN_POINT('Ctrl Pts',(187.836119034979,-1.99564971249439,126.309189287403));
#22849=CARTESIAN_POINT('Ctrl Pts',(187.828362732237,-2.12109000401499,126.364879018299));
#22850=CARTESIAN_POINT('Ctrl Pts',(187.820606429495,-2.24413101750869,126.425793936487));
#22851=CARTESIAN_POINT('Ctrl Pts',(187.812850126754,-2.36432052537678,126.491684938155));
#22852=CARTESIAN_POINT('Ctrl Pts',(187.805089684239,-2.48457418200409,126.557611107835));
#22853=CARTESIAN_POINT('Ctrl Pts',(187.797329241725,-2.60197296592657,126.628518451041));
#22854=CARTESIAN_POINT('Ctrl Pts',(187.789568799211,-2.71609292447437,126.70411400448));
#22855=CARTESIAN_POINT('Ctrl Pts',(187.781795898946,-2.83039607851072,126.779830910613));
#22856=CARTESIAN_POINT('Ctrl Pts',(187.77402299868,-2.94140957229936,126.860250836692));
#22857=CARTESIAN_POINT('Ctrl Pts',(187.766250098415,-3.04874117726313,126.945039395309));
#22858=CARTESIAN_POINT('Ctrl Pts',(187.758759762653,-3.15217100803496,127.026745676251));
#22859=CARTESIAN_POINT('Ctrl Pts',(187.751269426891,-3.25218176050425,127.112508282006));
#22860=CARTESIAN_POINT('Ctrl Pts',(187.743779091128,-3.34845570588935,127.201996470482));
#22861=CARTESIAN_POINT('Ctrl Pts',(187.736122099101,-3.44687169893981,127.293475726888));
#22862=CARTESIAN_POINT('Ctrl Pts',(187.728465107073,-3.54171430929935,127.389156956171));
#22863=CARTESIAN_POINT('Ctrl Pts',(187.720808115045,-3.63259513007057,127.488725582842));
#22864=CARTESIAN_POINT('Ctrl Pts',(187.713159991201,-3.72337069438334,127.588178891002));
#22865=CARTESIAN_POINT('Ctrl Pts',(187.705511867358,-3.81019332122524,127.691510351903));
#22866=CARTESIAN_POINT('Ctrl Pts',(187.697863743514,-3.8927084393723,127.798365928858));
#22867=CARTESIAN_POINT('Ctrl Pts',(187.690222703422,-3.97514713137943,127.905122535353));
#22868=CARTESIAN_POINT('Ctrl Pts',(187.68258166333,-4.05328600255709,128.015396450587));
#22869=CARTESIAN_POINT('Ctrl Pts',(187.674940623237,-4.12680846773921,128.1287980724));
#22870=CARTESIAN_POINT('Ctrl Pts',(187.667304890307,-4.2002798671441,128.242120929961));
#22871=CARTESIAN_POINT('Ctrl Pts',(187.659669157377,-4.26914101941565,128.358566835824));
#22872=CARTESIAN_POINT('Ctrl Pts',(187.652033424447,-4.33311701410075,128.47771496242));
#22873=CARTESIAN_POINT('Ctrl Pts',(187.6444009553,-4.39706566317769,128.596812160883));
#22874=CARTESIAN_POINT('Ctrl Pts',(187.636768486153,-4.45613311784616,128.718608927462));
#22875=CARTESIAN_POINT('Ctrl Pts',(187.629136017006,-4.5100892971886,128.842657889351));
#22876=CARTESIAN_POINT('Ctrl Pts',(187.621503159863,-4.56404821939219,128.966713157266));
#22877=CARTESIAN_POINT('Ctrl Pts',(187.613870302719,-4.61289517533641,129.093020483825));
#22878=CARTESIAN_POINT('Ctrl Pts',(187.606237445576,-4.65644742360532,129.221110651926));
#22879=CARTESIAN_POINT('Ctrl Pts',(187.599143290485,-4.69692589686468,129.340160635574));
#22880=CARTESIAN_POINT('Ctrl Pts',(187.592049135395,-4.73283104437265,129.460750229615));
#22881=CARTESIAN_POINT('Ctrl Pts',(187.584954980304,-4.76405452823404,129.582490119308));
#22882=CARTESIAN_POINT('Ctrl Pts',(189.334601801321,-4.76405452823404,129.582490119308));
#22883=CARTESIAN_POINT('Ctrl Pts',(189.326589951379,-4.79924357938049,129.71969169566));
#22884=CARTESIAN_POINT('Ctrl Pts',(189.318578101437,-4.82853357011572,129.858539643826));
#22885=CARTESIAN_POINT('Ctrl Pts',(189.310566251495,-4.85178106031378,129.99850479592));
#22886=CARTESIAN_POINT('Ctrl Pts',(189.302564129565,-4.8750003233392,130.138300001905));
#22887=CARTESIAN_POINT('Ctrl Pts',(189.294562007635,-4.89219165463957,130.279209361064));
#22888=CARTESIAN_POINT('Ctrl Pts',(189.286559885705,-4.90326234654455,130.420692240633));
#22889=CARTESIAN_POINT('Ctrl Pts',(189.279326402467,-4.91326965023596,130.548585072909));
#22890=CARTESIAN_POINT('Ctrl Pts',(189.272092919229,-4.91827626236202,130.676946189752));
#22891=CARTESIAN_POINT('Ctrl Pts',(189.264859435991,-4.91824989634839,130.805370354665));
#22892=CARTESIAN_POINT('',(189.610140563969,-4.91824791299378,130.799829742121));
#22893=CARTESIAN_POINT('Ctrl Pts',(189.680106903305,-4.76405452823404,129.582490119308));
#22894=CARTESIAN_POINT('Ctrl Pts',(189.67784575609,-4.77392102796961,129.620959452032));
#22895=CARTESIAN_POINT('Ctrl Pts',(189.675584608875,-4.78331723303707,129.659531493429));
#22896=CARTESIAN_POINT('Ctrl Pts',(189.67332346166,-4.79224143417708,129.69819376801));
#22897=CARTESIAN_POINT('Ctrl Pts',(189.662792978718,-4.83380270327263,129.87824945843));
#22898=CARTESIAN_POINT('Ctrl Pts',(189.652262495776,-4.86523011335524,130.060725185327));
#22899=CARTESIAN_POINT('Ctrl Pts',(189.641732012834,-4.88629864809003,130.244656602775));
#22900=CARTESIAN_POINT('Ctrl Pts',(189.631201529892,-4.90736718282481,130.428588020222));
#22901=CARTESIAN_POINT('Ctrl Pts',(189.62067104695,-4.91807669726267,130.613975751142));
#22902=CARTESIAN_POINT('Ctrl Pts',(189.610140564008,-4.91824791299315,130.799829741432));
#22903=CARTESIAN_POINT('Ctrl Pts',(189.610140563969,-4.91824791299378,130.799829742121));
#22904=CARTESIAN_POINT('Ctrl Pts',(189.602485915437,-4.91837237034752,130.934927722133));
#22905=CARTESIAN_POINT('Ctrl Pts',(189.594831266904,-4.91292619023357,131.070187999666));
#22906=CARTESIAN_POINT('Ctrl Pts',(189.587176618372,-4.90189607666226,131.205107315747));
#22907=CARTESIAN_POINT('Ctrl Pts',(189.57916408585,-4.89035026324752,131.346334624011));
#22908=CARTESIAN_POINT('Ctrl Pts',(189.571151553328,-4.87268569848204,131.487187873076));
#22909=CARTESIAN_POINT('Ctrl Pts',(189.563139020806,-4.84894837207892,131.627089459538));
#22910=CARTESIAN_POINT('Ctrl Pts',(189.555493068658,-4.82629704912697,131.760590426017));
#22911=CARTESIAN_POINT('Ctrl Pts',(189.547847116509,-4.79811638583712,131.893224434576));
#22912=CARTESIAN_POINT('Ctrl Pts',(189.54020116436,-4.76449933419752,132.02449551049));
#22913=CARTESIAN_POINT('Ctrl Pts',(189.532556401308,-4.73088751067271,132.155746171162));
#22914=CARTESIAN_POINT('Ctrl Pts',(189.524911638256,-4.69184107950793,132.285633931062));
#22915=CARTESIAN_POINT('Ctrl Pts',(189.517266875204,-4.64750370934258,132.413674861009));
#22916=CARTESIAN_POINT('Ctrl Pts',(189.509621542448,-4.60316303506545,132.541725332827));
#22917=CARTESIAN_POINT('Ctrl Pts',(189.501976209692,-4.55353076963928,132.667928320977));
#22918=CARTESIAN_POINT('Ctrl Pts',(189.494330876936,-4.49879968865441,132.791817390395));
#22919=CARTESIAN_POINT('Ctrl Pts',(189.486683215447,-4.44405193682891,132.915744195865));
#22920=CARTESIAN_POINT('Ctrl Pts',(189.479035553957,-4.38420244384357,133.037355313473));
#22921=CARTESIAN_POINT('Ctrl Pts',(189.471387892468,-4.31949088284538,133.156207035918));
#22922=CARTESIAN_POINT('Ctrl Pts',(189.46373199972,-4.25470967211568,133.275186679718));
#22923=CARTESIAN_POINT('Ctrl Pts',(189.456076106972,-4.18505614095032,133.39140064717));
#22924=CARTESIAN_POINT('Ctrl Pts',(189.448420214224,-4.11081455193053,133.504432242937));
#22925=CARTESIAN_POINT('Ctrl Pts',(189.440759493914,-4.0365261485234,133.617535112838));
#22926=CARTESIAN_POINT('Ctrl Pts',(189.433098773603,-3.95764416228724,133.727451290957));
#22927=CARTESIAN_POINT('Ctrl Pts',(189.425438053292,-3.87449360985302,133.833796593075));
#22928=CARTESIAN_POINT('Ctrl Pts',(189.417766480026,-3.79122525788974,133.940292554763));
#22929=CARTESIAN_POINT('Ctrl Pts',(189.41009490676,-3.70367653135893,134.043207240323));
#22930=CARTESIAN_POINT('Ctrl Pts',(189.402423333494,-3.61220996172295,134.142192586813));
#22931=CARTESIAN_POINT('Ctrl Pts',(189.399907501612,-3.58221422237703,134.174654049665));
#22932=CARTESIAN_POINT('Ctrl Pts',(189.397391669729,-3.55179740394281,134.206693246693));
#22933=CARTESIAN_POINT('Ctrl Pts',(189.394875837847,-3.52097305098158,134.238298857657));
#22934=CARTESIAN_POINT('Ctrl Pts',(189.387101503728,-3.42572073281059,134.335965391495));
#22935=CARTESIAN_POINT('Ctrl Pts',(189.379327169609,-3.32625077645834,134.429820383029));
#22936=CARTESIAN_POINT('Ctrl Pts',(189.37155283549,-3.22290063708545,134.519477647482));
#22937=CARTESIAN_POINT('Ctrl Pts',(189.363788082543,-3.11967786752259,134.609024417371));
#22938=CARTESIAN_POINT('Ctrl Pts',(189.356023329596,-3.01258472214135,134.694383499813));
#22939=CARTESIAN_POINT('Ctrl Pts',(189.348258576648,-2.90199674489212,134.775204099137));
#22940=CARTESIAN_POINT('Ctrl Pts',(189.340501535763,-2.79151860518099,134.855944426302));
#22941=CARTESIAN_POINT('Ctrl Pts',(189.332744494878,-2.67755285489058,134.932155011651));
#22942=CARTESIAN_POINT('Ctrl Pts',(189.324987453993,-2.56050921726351,135.003524297492));
#22943=CARTESIAN_POINT('Ctrl Pts',(189.317236262753,-2.44355384315431,135.074839763199));
#22944=CARTESIAN_POINT('Ctrl Pts',(189.309485071513,-2.32352553408762,135.141320993499));
#22945=CARTESIAN_POINT('Ctrl Pts',(189.301733880273,-2.20086389176815,135.202699075713));
#22946=CARTESIAN_POINT('Ctrl Pts',(189.293985983496,-2.07825438391844,135.264051070604));
#22947=CARTESIAN_POINT('Ctrl Pts',(189.286238086719,-1.95301411779677,135.320304056746));
#22948=CARTESIAN_POINT('Ctrl Pts',(189.278490189942,-1.82560805826677,135.371234633793));
#22949=CARTESIAN_POINT('Ctrl Pts',(189.270743913858,-1.69822864933794,135.422154557262));
#22950=CARTESIAN_POINT('Ctrl Pts',(189.262997637774,-1.56868471092015,135.467754141087));
#22951=CARTESIAN_POINT('Ctrl Pts',(189.255251361689,-1.43746162023923,135.507857949641));
#22952=CARTESIAN_POINT('Ctrl Pts',(189.247505028424,-1.3062375608992,135.547962054233));
#22953=CARTESIAN_POINT('Ctrl Pts',(189.239758695159,-1.1733346984564,135.582570188336));
#22954=CARTESIAN_POINT('Ctrl Pts',(189.232012361893,-1.03925363421513,135.611556780224));
#22955=CARTESIAN_POINT('Ctrl Pts',(189.22426429389,-0.905142543449059,135.640549863458));
#22956=CARTESIAN_POINT('Ctrl Pts',(189.216516225887,-0.76985310791742,135.663918816804));
#22957=CARTESIAN_POINT('Ctrl Pts',(189.208768157884,-0.633895788762408,
135.681589255993));
#22958=CARTESIAN_POINT('Ctrl Pts',(189.201011855143,-0.497793972550918,
135.699278475534));
#22959=CARTESIAN_POINT('Ctrl Pts',(189.193255552401,-0.361023243067375,
135.711257032039));
#22960=CARTESIAN_POINT('Ctrl Pts',(189.185499249659,-0.224099407142775,
135.717502435));
#22961=CARTESIAN_POINT('Ctrl Pts',(189.177738807145,-0.0871024908441983,
135.723751171321));
#22962=CARTESIAN_POINT('Ctrl Pts',(189.16997836463,0.0500473039532961,135.724260655423));
#22963=CARTESIAN_POINT('Ctrl Pts',(189.162217922116,0.186835504032796,135.719060563334));
#22964=CARTESIAN_POINT('Ctrl Pts',(189.154445021851,0.323843288674548,135.713852123596));
#22965=CARTESIAN_POINT('Ctrl Pts',(189.146672121585,0.46048792870308,135.702915823248));
#22966=CARTESIAN_POINT('Ctrl Pts',(189.13889922132,0.596260497125072,135.686333219094));
#22967=CARTESIAN_POINT('Ctrl Pts',(189.131408885558,0.727097390693978,135.67035343437));
#22968=CARTESIAN_POINT('Ctrl Pts',(189.123918549796,0.857124211873021,135.649130783049));
#22969=CARTESIAN_POINT('Ctrl Pts',(189.116428214034,0.985897556969896,135.622782461869));
#22970=CARTESIAN_POINT('Ctrl Pts',(189.108653879915,1.11955338258629,135.595435136084));
#22971=CARTESIAN_POINT('Ctrl Pts',(189.100879545796,1.25228218617169,135.562479160128));
#22972=CARTESIAN_POINT('Ctrl Pts',(189.093105211677,1.38357665678069,135.523989702284));
#22973=CARTESIAN_POINT('Ctrl Pts',(189.08534045873,1.51470931868909,135.485547679256));
#22974=CARTESIAN_POINT('Ctrl Pts',(189.077575705783,1.64441079321712,135.441585852083));
#22975=CARTESIAN_POINT('Ctrl Pts',(189.069810952835,1.7721829553513,135.392230562896));
#22976=CARTESIAN_POINT('Ctrl Pts',(189.06205391195,1.89982821237275,135.342924294078));
#22977=CARTESIAN_POINT('Ctrl Pts',(189.054296871065,2.02554760802274,135.288235363609));
#22978=CARTESIAN_POINT('Ctrl Pts',(189.04653983018,2.14885755457138,135.228340078714));
#22979=CARTESIAN_POINT('Ctrl Pts',(189.03878863894,2.2720745121302,135.16848996132));
#22980=CARTESIAN_POINT('Ctrl Pts',(189.0310374477,2.39288528693343,135.103441474395));
#22981=CARTESIAN_POINT('Ctrl Pts',(189.02328625646,2.51082601966835,135.033419113432));
#22982=CARTESIAN_POINT('Ctrl Pts',(189.015538359683,2.62871662444556,134.963426513841));
#22983=CARTESIAN_POINT('Ctrl Pts',(189.007790462906,2.7437392778564,134.888464444029));
#22984=CARTESIAN_POINT('Ctrl Pts',(189.000042566129,2.85545470199736,134.808803338762));
#22985=CARTESIAN_POINT('Ctrl Pts',(188.992296290045,2.96714675767976,134.729158896881));
#22986=CARTESIAN_POINT('Ctrl Pts',(188.984550013961,3.07553264200004,134.644817601504));
#22987=CARTESIAN_POINT('Ctrl Pts',(188.976803737876,3.18020239775109,134.556092986997));
#22988=CARTESIAN_POINT('Ctrl Pts',(188.969057404611,3.28487292615045,134.467367717545));
#22989=CARTESIAN_POINT('Ctrl Pts',(188.961311071346,3.38582697300727,134.374259317201));
#22990=CARTESIAN_POINT('Ctrl Pts',(188.95356473808,3.48268830403982,134.277121081434));
#22991=CARTESIAN_POINT('Ctrl Pts',(188.945816670077,3.57957132649582,134.179961092233));
#22992=CARTESIAN_POINT('Ctrl Pts',(188.938068602074,3.67235953332192,134.078769748627));
#22993=CARTESIAN_POINT('Ctrl Pts',(188.930320534071,3.76071442620922,133.973936309516));
#22994=CARTESIAN_POINT('Ctrl Pts',(188.92256423133,3.8491632237282,133.868991452179));
#22995=CARTESIAN_POINT('Ctrl Pts',(188.914807928588,3.93316904266262,133.7603970663));
#22996=CARTESIAN_POINT('Ctrl Pts',(188.907051625846,4.01243415492057,133.648574958105));
#22997=CARTESIAN_POINT('Ctrl Pts',(188.899291183332,4.09174157335567,133.536693167084));
#22998=CARTESIAN_POINT('Ctrl Pts',(188.891530740818,4.16630303091852,133.421580549039));
#22999=CARTESIAN_POINT('Ctrl Pts',(188.883770298303,4.23586540955038,133.303685985475));
#23000=CARTESIAN_POINT('Ctrl Pts',(188.875997398038,4.30553945588784,133.185602167092));
#23001=CARTESIAN_POINT('Ctrl Pts',(188.868224497773,4.37019820233963,133.064727823987));
#23002=CARTESIAN_POINT('Ctrl Pts',(188.860451597507,4.42963517748233,132.941535214297));
#23003=CARTESIAN_POINT('Ctrl Pts',(188.852961261745,4.48691146886592,132.822820966272));
#23004=CARTESIAN_POINT('Ctrl Pts',(188.845470925983,4.53933892418261,132.701954357632));
#23005=CARTESIAN_POINT('Ctrl Pts',(188.837980590221,4.58677647383961,132.579371784159));
#23006=CARTESIAN_POINT('Ctrl Pts',(188.830206256102,4.63601263261018,132.452141455156));
#23007=CARTESIAN_POINT('Ctrl Pts',(188.822431921983,4.68002899709644,132.322659443626));
#23008=CARTESIAN_POINT('Ctrl Pts',(188.814657587864,4.7186145945435,132.191393194927));
#23009=CARTESIAN_POINT('Ctrl Pts',(188.806892834917,4.75715263869014,132.060288720149));
#23010=CARTESIAN_POINT('Ctrl Pts',(188.79912808197,4.79027312354286,131.927404754878));
#23011=CARTESIAN_POINT('Ctrl Pts',(188.791363329022,4.8178130955777,131.793228676803));
#23012=CARTESIAN_POINT('Ctrl Pts',(188.783606288137,4.84532571452407,131.659185864302));
#23013=CARTESIAN_POINT('Ctrl Pts',(188.775849247252,4.86726877266508,131.523853873413));
#23014=CARTESIAN_POINT('Ctrl Pts',(188.768092206367,4.88352921128275,131.387734858554));
#23015=CARTESIAN_POINT('Ctrl Pts',(188.760341015127,4.89977738777712,131.251718492103));
#23016=CARTESIAN_POINT('Ctrl Pts',(188.752589823887,4.91035142820668,131.114916669642));
#23017=CARTESIAN_POINT('Ctrl Pts',(188.744838632647,4.91518947969835,130.977840994447));
#23018=CARTESIAN_POINT('Ctrl Pts',(188.73709073587,4.9200254748891,130.840823580069));
#23019=CARTESIAN_POINT('Ctrl Pts',(188.729342839093,4.91913031627366,130.70353293436));
#23020=CARTESIAN_POINT('Ctrl Pts',(188.721594942316,4.91249408784202,130.566484810858));
#23021=CARTESIAN_POINT('Ctrl Pts',(188.713848666232,4.90585924756631,130.429465354868));
#23022=CARTESIAN_POINT('Ctrl Pts',(188.706102390148,4.89348574504375,130.29268871044));
#23023=CARTESIAN_POINT('Ctrl Pts',(188.698356114064,4.87541577373173,130.156669259165));
#23024=CARTESIAN_POINT('Ctrl Pts',(188.690609780798,4.85734566903134,130.020648803825));
#23025=CARTESIAN_POINT('Ctrl Pts',(188.682863447533,4.8335790631205,129.885385940352));
#23026=CARTESIAN_POINT('Ctrl Pts',(188.675117114268,4.8042098296649,129.751388170134));
#23027=CARTESIAN_POINT('Ctrl Pts',(188.667369046265,4.77483401917306,129.617360392044));
#23028=CARTESIAN_POINT('Ctrl Pts',(188.659620978262,4.73985316817686,129.484598652787));
#23029=CARTESIAN_POINT('Ctrl Pts',(188.651872910259,4.69941180461004,129.353598144522));
#23030=CARTESIAN_POINT('Ctrl Pts',(188.644116607517,4.65892745948071,129.222458407358));
#23031=CARTESIAN_POINT('Ctrl Pts',(188.636360304775,4.61297112417784,129.093084014587));
#23032=CARTESIAN_POINT('Ctrl Pts',(188.628604002033,4.56173674692024,128.965953449853));
#23033=CARTESIAN_POINT('Ctrl Pts',(188.620843559519,4.51047502433273,128.838755031709));
#23034=CARTESIAN_POINT('Ctrl Pts',(188.613083117005,4.4539298076903,128.713803183936));
#23035=CARTESIAN_POINT('Ctrl Pts',(188.605322674491,4.39234193722288,128.591553493343));
#23036=CARTESIAN_POINT('Ctrl Pts',(188.597549774225,4.33065520043842,128.469107556694));
#23037=CARTESIAN_POINT('Ctrl Pts',(188.58977687396,4.26390982407976,128.349372787105));
#23038=CARTESIAN_POINT('Ctrl Pts',(188.582003973694,4.1923915294448,128.23277816189));
#23039=CARTESIAN_POINT('Ctrl Pts',(188.574513637932,4.12347310496294,128.120422044985));
#23040=CARTESIAN_POINT('Ctrl Pts',(188.56702330217,4.05012292420374,128.010981987703));
#23041=CARTESIAN_POINT('Ctrl Pts',(188.559532966408,3.9726318877381,127.904812558467));
#23042=CARTESIAN_POINT('Ctrl Pts',(188.551758632289,3.89220275507264,127.794617683053));
#23043=CARTESIAN_POINT('Ctrl Pts',(188.54398429817,3.80705779181573,127.687597278996));
#23044=CARTESIAN_POINT('Ctrl Pts',(188.536209964051,3.71747623705813,127.584181509285));
#23045=CARTESIAN_POINT('Ctrl Pts',(188.528445211104,3.62800508356063,127.480893190268));
#23046=CARTESIAN_POINT('Ctrl Pts',(188.520680458157,3.53410847118426,127.38120095924));
#23047=CARTESIAN_POINT('Ctrl Pts',(188.512915705209,3.4361083642224,127.285505353162));
#23048=CARTESIAN_POINT('Ctrl Pts',(188.505158664324,3.33820559234877,127.18990479331));
#23049=CARTESIAN_POINT('Ctrl Pts',(188.49740162344,3.23620771452785,127.098293230294));
#23050=CARTESIAN_POINT('Ctrl Pts',(188.489644582555,3.13047609649216,127.011037210342));
#23051=CARTESIAN_POINT('Ctrl Pts',(188.481893391314,3.02482421149156,126.923846990833));
#23052=CARTESIAN_POINT('Ctrl Pts',(188.474142200074,2.91544449096346,126.841006024537));
#23053=CARTESIAN_POINT('Ctrl Pts',(188.466391008834,2.80273392824307,126.762842884093));
#23054=CARTESIAN_POINT('Ctrl Pts',(188.458643112057,2.69007127051854,126.684712965069));
#23055=CARTESIAN_POINT('Ctrl Pts',(188.45089521528,2.57408090691345,126.611257139848));
#23056=CARTESIAN_POINT('Ctrl Pts',(188.443147318503,2.45519139564007,126.542762528436));
#23057=CARTESIAN_POINT('Ctrl Pts',(188.435401042419,2.33632675348964,126.47428224462));
#23058=CARTESIAN_POINT('Ctrl Pts',(188.427654766335,2.21456450846326,126.410761305459));
#23059=CARTESIAN_POINT('Ctrl Pts',(188.419908490251,2.09036023095675,126.352442248218));
#23060=CARTESIAN_POINT('Ctrl Pts',(188.412162156985,1.96615503660239,126.294122760479));
#23061=CARTESIAN_POINT('Ctrl Pts',(188.40441582372,1.83950812769249,126.241005397451));
#23062=CARTESIAN_POINT('Ctrl Pts',(188.396669490455,1.71089722052739,126.193285497457));
#23063=CARTESIAN_POINT('Ctrl Pts',(188.388921422452,1.58225751184136,126.145554910922));
#23064=CARTESIAN_POINT('Ctrl Pts',(188.381173354449,1.45165329617858,126.10322432862));
#23065=CARTESIAN_POINT('Ctrl Pts',(188.373425286446,1.31957931360486,126.066439818565));
#23066=CARTESIAN_POINT('Ctrl Pts',(188.365668983704,1.18736496123061,126.029616213495));
#23067=CARTESIAN_POINT('Ctrl Pts',(188.357912680962,1.05367809874174,125.998350560498));
#23068=CARTESIAN_POINT('Ctrl Pts',(188.35015637822,0.919026121729599,125.972738317543));
#23069=CARTESIAN_POINT('Ctrl Pts',(188.342395935706,0.78430227690315,125.947112404563));
#23070=CARTESIAN_POINT('Ctrl Pts',(188.334635493192,0.648612677762575,125.927145970928));
#23071=CARTESIAN_POINT('Ctrl Pts',(188.326875050678,0.512470802420838,125.912882646731));
#23072=CARTESIAN_POINT('Ctrl Pts',(188.319102150412,0.376110380054625,125.89859642578));
#23073=CARTESIAN_POINT('Ctrl Pts',(188.311329250147,0.239296621066078,125.89003163359));
#23074=CARTESIAN_POINT('Ctrl Pts',(188.303556349881,0.102544875559919,125.88717975746));
#23075=CARTESIAN_POINT('Ctrl Pts',(188.296066014119,-0.0292355995406955,
125.88443155421));
#23076=CARTESIAN_POINT('Ctrl Pts',(188.288575678357,-0.160958183613458,
125.886988114484));
#23077=CARTESIAN_POINT('Ctrl Pts',(188.281085342595,-0.292167329337183,
125.894796348288));
#23078=CARTESIAN_POINT('Ctrl Pts',(188.273311008476,-0.428351309700771,
125.90290063365));
#23079=CARTESIAN_POINT('Ctrl Pts',(188.265536674357,-0.564413539030559,
125.916688360158));
#23080=CARTESIAN_POINT('Ctrl Pts',(188.257762340238,-0.699841173472941,
125.936157109658));
#23081=CARTESIAN_POINT('Ctrl Pts',(188.249997587291,-0.835101905459319,
125.955601865663));
#23082=CARTESIAN_POINT('Ctrl Pts',(188.242232834344,-0.9697292153955,125.980713658957));
#23083=CARTESIAN_POINT('Ctrl Pts',(188.234468081397,-1.10321209062758,126.011438111871));
#23084=CARTESIAN_POINT('Ctrl Pts',(188.226711040512,-1.23656238878648,126.042132048826));
#23085=CARTESIAN_POINT('Ctrl Pts',(188.218953999627,-1.36877013572612,126.07842746462));
#23086=CARTESIAN_POINT('Ctrl Pts',(188.211196958742,-1.49933161871793,126.120218459218));
#23087=CARTESIAN_POINT('Ctrl Pts',(188.203445767502,-1.62979464427913,126.161977938902));
#23088=CARTESIAN_POINT('Ctrl Pts',(188.195694576262,-1.75861350609556,126.20922462979));
#23089=CARTESIAN_POINT('Ctrl Pts',(188.187943385022,-1.88529718210462,126.261802131685));
#23090=CARTESIAN_POINT('Ctrl Pts',(188.180195488244,-2.01192701417225,126.314357286739));
#23091=CARTESIAN_POINT('Ctrl Pts',(188.172447591467,-2.13642310505805,126.372238596868));
#23092=CARTESIAN_POINT('Ctrl Pts',(188.16469969469,-2.25831224638831,126.435240699286));
#23093=CARTESIAN_POINT('Ctrl Pts',(188.156953418606,-2.38017589113758,126.498229623022));
#23094=CARTESIAN_POINT('Ctrl Pts',(188.149207142522,-2.49943332390471,126.566337029047));
#23095=CARTESIAN_POINT('Ctrl Pts',(188.141460866438,-2.61563424429333,126.6393107304));
#23096=CARTESIAN_POINT('Ctrl Pts',(188.133714533173,-2.73183602245093,126.712284970429));
#23097=CARTESIAN_POINT('Ctrl Pts',(188.125968199908,-2.84498091211698,126.790125369541));
#23098=CARTESIAN_POINT('Ctrl Pts',(188.118221866642,-2.95464635229878,126.872535596619));
#23099=CARTESIAN_POINT('Ctrl Pts',(188.110473798639,-3.06433635129529,126.954964278895));
#23100=CARTESIAN_POINT('Ctrl Pts',(188.102725730636,-3.17054503780084,127.04196459072));
#23101=CARTESIAN_POINT('Ctrl Pts',(188.094977662633,-3.27288210156859,127.133199246592));
#23102=CARTESIAN_POINT('Ctrl Pts',(188.087221359892,-3.37532793038579,127.224530867742));
#23103=CARTESIAN_POINT('Ctrl Pts',(188.07946505715,-3.47389362439947,127.320105562212));
#23104=CARTESIAN_POINT('Ctrl Pts',(188.071708754408,-3.56822461240654,127.419548041083));
#23105=CARTESIAN_POINT('Ctrl Pts',(188.063948311894,-3.66260594770211,127.519043595399));
#23106=CARTESIAN_POINT('Ctrl Pts',(188.05618786938,-3.75274781653608,127.622410752998));
#23107=CARTESIAN_POINT('Ctrl Pts',(188.048427426866,-3.83833596421348,127.729241093332));
#23108=CARTESIAN_POINT('Ctrl Pts',(188.0406545266,-3.92406150558378,127.836242927212));
#23109=CARTESIAN_POINT('Ctrl Pts',(188.032881626335,-4.00521848641537,127.946718738031));
#23110=CARTESIAN_POINT('Ctrl Pts',(188.025108726069,-4.08153550936666,128.060230345826));
#23111=CARTESIAN_POINT('Ctrl Pts',(188.017618390307,-4.15507821630353,128.169615520761));
#23112=CARTESIAN_POINT('Ctrl Pts',(188.010128054545,-4.22412658393381,128.281819344595));
#23113=CARTESIAN_POINT('Ctrl Pts',(188.002637718783,-4.28847904391944,128.396429856027));
#23114=CARTESIAN_POINT('Ctrl Pts',(187.994504561361,-4.35835424099316,128.52087625753));
#23115=CARTESIAN_POINT('Ctrl Pts',(187.98637140394,-4.42289737344505,128.648524117943));
#23116=CARTESIAN_POINT('Ctrl Pts',(187.978238246518,-4.48181742515692,128.778898786264));
#23117=CARTESIAN_POINT('Ctrl Pts',(187.970122616113,-4.54061050370865,128.908992496183));
#23118=CARTESIAN_POINT('Ctrl Pts',(187.962006985708,-4.59380452073732,129.041800991969));
#23119=CARTESIAN_POINT('Ctrl Pts',(187.953891355302,-4.6411539136234,129.176824623322));
#23120=CARTESIAN_POINT('Ctrl Pts',(187.94588335265,-4.68787536899956,129.310057600188));
#23121=CARTESIAN_POINT('Ctrl Pts',(187.937875349997,-4.72890612235297,129.445447018229));
#23122=CARTESIAN_POINT('Ctrl Pts',(187.929867347344,-4.76405452823405,129.582490119308));
#23123=CARTESIAN_POINT('Origin',(213.235140564004,0.,130.804360617566));
#23124=CARTESIAN_POINT('',(185.834939443695,-4.76405452823405,129.582490119308));
#23125=CARTESIAN_POINT('',(186.18020938313,-4.76405452823405,129.582490119308));
#23126=CARTESIAN_POINT('',(213.235140564004,-4.76405452823405,129.582490119308));
#23127=CARTESIAN_POINT('',(187.514859436036,-4.91824821531416,130.808550493347));
#23128=CARTESIAN_POINT('Ctrl Pts',(187.514859435991,-4.91824821531348,130.808550494141));
#23129=CARTESIAN_POINT('Ctrl Pts',(187.50296817185,-4.91806974195455,131.018049810722));
#23130=CARTESIAN_POINT('Ctrl Pts',(187.49107690771,-4.90450242768287,131.226999653672));
#23131=CARTESIAN_POINT('Ctrl Pts',(187.47918564357,-4.87777335736303,131.434051126228));
#23132=CARTESIAN_POINT('Ctrl Pts',(187.474567584818,-4.86739292886978,131.514461068646));
#23133=CARTESIAN_POINT('Ctrl Pts',(187.469949526067,-4.85502785952663,131.594585104556));
#23134=CARTESIAN_POINT('Ctrl Pts',(187.465331467316,-4.84069308080701,131.674345421989));
#23135=CARTESIAN_POINT('Ctrl Pts',(187.457557133197,-4.8165610016603,131.808619018444));
#23136=CARTESIAN_POINT('Ctrl Pts',(187.449782799078,-4.78679964152417,131.942100451967));
#23137=CARTESIAN_POINT('Ctrl Pts',(187.442008464958,-4.75147197296815,132.074280753873));
#23138=CARTESIAN_POINT('Ctrl Pts',(187.434243712011,-4.71618784260629,132.206298155371));
#23139=CARTESIAN_POINT('Ctrl Pts',(187.426478959064,-4.67535115311574,132.337017241715));
#23140=CARTESIAN_POINT('Ctrl Pts',(187.418714206117,-4.62907625661752,132.465936999476));
#23141=CARTESIAN_POINT('Ctrl Pts',(187.410957165232,-4.58284732099878,132.594728712316));
#23142=CARTESIAN_POINT('Ctrl Pts',(187.403200124347,-4.53119105843935,132.721724287424));
#23143=CARTESIAN_POINT('Ctrl Pts',(187.395443083462,-4.47427212062073,132.846436045442));
#23144=CARTESIAN_POINT('Ctrl Pts',(187.387691892222,-4.41739610581604,132.971053757354));
#23145=CARTESIAN_POINT('Ctrl Pts',(187.379940700982,-4.35526547673165,133.093390725966));
#23146=CARTESIAN_POINT('Ctrl Pts',(187.372189509742,-4.28809353286631,133.212977838274));
#23147=CARTESIAN_POINT('Ctrl Pts',(187.364441612965,-4.22095013886891,133.332514122869));
#23148=CARTESIAN_POINT('Ctrl Pts',(187.356693716188,-4.14876988281084,133.44930253558));
#23149=CARTESIAN_POINT('Ctrl Pts',(187.348945819411,-4.07181258012,133.562897435315));
#23150=CARTESIAN_POINT('Ctrl Pts',(187.341199543326,-3.99487137523789,133.676468573446));
#23151=CARTESIAN_POINT('Ctrl Pts',(187.333453267242,-3.91315533044107,133.786847203844));
#23152=CARTESIAN_POINT('Ctrl Pts',(187.325706991158,-3.82696805196249,133.893615963399));
#23153=CARTESIAN_POINT('Ctrl Pts',(187.317960657893,-3.74078013726901,134.000385511097));
#23154=CARTESIAN_POINT('Ctrl Pts',(187.310214324628,-3.65012116860682,134.103544830563));
#23155=CARTESIAN_POINT('Ctrl Pts',(187.302467991362,-3.55533531112048,134.202709317744));
#23156=CARTESIAN_POINT('Ctrl Pts',(187.294719923359,-3.46052822699846,134.301896012124));
#23157=CARTESIAN_POINT('Ctrl Pts',(187.286971855356,-3.36159268511726,134.397085811471));
#23158=CARTESIAN_POINT('Ctrl Pts',(187.279223787353,-3.25890970925504,134.487930973813));
#23159=CARTESIAN_POINT('Ctrl Pts',(187.271467484611,-3.15611760070424,134.578872687475));
#23160=CARTESIAN_POINT('Ctrl Pts',(187.263711181869,-3.04957039534964,134.665460280642));
#23161=CARTESIAN_POINT('Ctrl Pts',(187.255954879128,-2.93968263329513,134.747385988776));
#23162=CARTESIAN_POINT('Ctrl Pts',(187.248194436613,-2.82973622083337,134.829355423126));
#23163=CARTESIAN_POINT('Ctrl Pts',(187.240433994099,-2.71644602177129,134.906657794264));
#23164=CARTESIAN_POINT('Ctrl Pts',(187.232673551585,-2.60025471421194,134.979029285103));
#23165=CARTESIAN_POINT('Ctrl Pts',(187.22490065132,-2.48387688605068,135.051516953085));
#23166=CARTESIAN_POINT('Ctrl Pts',(187.217127751054,-2.36458898340092,135.119057730363));
#23167=CARTESIAN_POINT('Ctrl Pts',(187.209354850789,-2.24285817365602,135.181433872078));
#23168=CARTESIAN_POINT('Ctrl Pts',(187.201864515027,-2.12555258546736,135.241542483926));
#23169=CARTESIAN_POINT('Ctrl Pts',(187.194374179265,-2.0059788977942,135.296855306772));
#23170=CARTESIAN_POINT('Ctrl Pts',(187.186883843503,-1.88456999546703,135.347220839352));
#23171=CARTESIAN_POINT('Ctrl Pts',(187.179109509384,-1.75855783770604,135.399495996409));
#23172=CARTESIAN_POINT('Ctrl Pts',(187.171335175265,-1.63016938517756,135.446606896525));
#23173=CARTESIAN_POINT('Ctrl Pts',(187.163560841146,-1.49986688586205,135.488331410301));
#23174=CARTESIAN_POINT('Ctrl Pts',(187.155796088199,-1.36972497273157,135.530004502343));
#23175=CARTESIAN_POINT('Ctrl Pts',(187.148031335251,-1.23767407507255,135.566304298079));
#23176=CARTESIAN_POINT('Ctrl Pts',(187.140266582304,-1.10419751978648,135.597056195192));
#23177=CARTESIAN_POINT('Ctrl Pts',(187.132509541419,-0.970853535296745,
135.627777549087));
#23178=CARTESIAN_POINT('Ctrl Pts',(187.124752500534,-0.836087089569735,
135.6529618828));
#23179=CARTESIAN_POINT('Ctrl Pts',(187.116995459649,-0.700397479315045,
135.672484119848));
#23180=CARTESIAN_POINT('Ctrl Pts',(187.109244268409,-0.564810193650936,
135.691991635025));
#23181=CARTESIAN_POINT('Ctrl Pts',(187.101493077169,-0.42830151454915,135.705845496927));
#23182=CARTESIAN_POINT('Ctrl Pts',(187.093741885929,-0.291381413656383,
135.713971593425));
#23183=CARTESIAN_POINT('Ctrl Pts',(187.085993989152,-0.154519507459005,
135.722094236115));
#23184=CARTESIAN_POINT('Ctrl Pts',(187.078246092375,-0.017246916725652,
135.724493932228));
#23185=CARTESIAN_POINT('Ctrl Pts',(187.070498195598,0.119920991487449,135.721148391947));
#23186=CARTESIAN_POINT('Ctrl Pts',(187.062751919514,0.257060207131151,135.717803551481));
#23187=CARTESIAN_POINT('Ctrl Pts',(187.05500564343,0.394094393208233,135.708715874552));
#23188=CARTESIAN_POINT('Ctrl Pts',(187.047259367345,0.53050830372916,135.693915198729));
#23189=CARTESIAN_POINT('Ctrl Pts',(187.03951303408,0.66692322122647,135.679114413651));
#23190=CARTESIAN_POINT('Ctrl Pts',(187.031766700815,0.802717465346965,135.658600587698));
#23191=CARTESIAN_POINT('Ctrl Pts',(187.024020367549,0.937381428141232,135.632455388868));
#23192=CARTESIAN_POINT('Ctrl Pts',(187.016272299546,1.07207554799625,135.606304335003));
#23193=CARTESIAN_POINT('Ctrl Pts',(187.008524231543,1.20563849912314,135.574519473305));
#23194=CARTESIAN_POINT('Ctrl Pts',(187.000776163541,1.33757176369478,135.537233406842));
#23195=CARTESIAN_POINT('Ctrl Pts',(186.993019860799,1.46964524851015,135.499907712303));
#23196=CARTESIAN_POINT('Ctrl Pts',(186.985263558057,1.60008520998432,135.457069239991));
#23197=CARTESIAN_POINT('Ctrl Pts',(186.977507255315,1.7284086480416,135.408900399985));
#23198=CARTESIAN_POINT('Ctrl Pts',(186.969746812801,1.85680057618161,135.360705850817));
#23199=CARTESIAN_POINT('Ctrl Pts',(186.961986370287,1.98307337019677,135.307175417617));
#23200=CARTESIAN_POINT('Ctrl Pts',(186.954225927772,2.10676579497374,135.248538938429));
#23201=CARTESIAN_POINT('Ctrl Pts',(186.946453027507,2.23065678181183,135.189808330759));
#23202=CARTESIAN_POINT('Ctrl Pts',(186.938680127242,2.3519587757408,135.125955479745));
#23203=CARTESIAN_POINT('Ctrl Pts',(186.930907226976,2.47023606645755,135.05725573013));
#23204=CARTESIAN_POINT('Ctrl Pts',(186.923416891214,2.58421367973449,134.991053389458));
#23205=CARTESIAN_POINT('Ctrl Pts',(186.915926555452,2.69538242307315,134.920350591354));
#23206=CARTESIAN_POINT('Ctrl Pts',(186.90843621969,2.80338084934492,134.845429643953));
#23207=CARTESIAN_POINT('Ctrl Pts',(186.900661885571,2.91547406877391,134.76766804606));
#23208=CARTESIAN_POINT('Ctrl Pts',(186.892887551452,3.02450689794558,134.685115797058));
#23209=CARTESIAN_POINT('Ctrl Pts',(186.885113217333,3.13004259678052,134.5980417329));
#23210=CARTESIAN_POINT('Ctrl Pts',(186.877348464386,3.23544823229863,134.511074979743));
#23211=CARTESIAN_POINT('Ctrl Pts',(186.869583711439,3.3373650142225,134.419597745934));
#23212=CARTESIAN_POINT('Ctrl Pts',(186.861818958491,3.43538479468078,134.323922291266));
#23213=CARTESIAN_POINT('Ctrl Pts',(186.854061917606,3.53330722051126,134.228341862808));
#23214=CARTESIAN_POINT('Ctrl Pts',(186.846304876721,3.62734006948965,134.128571782767));
#23215=CARTESIAN_POINT('Ctrl Pts',(186.838547835836,3.7171082291624,134.024964516712));
#23216=CARTESIAN_POINT('Ctrl Pts',(186.830796644596,3.8068086939677,133.921435381702));
#23217=CARTESIAN_POINT('Ctrl Pts',(186.823045453356,3.89225061581199,133.814075114605));
#23218=CARTESIAN_POINT('Ctrl Pts',(186.815294262116,3.97309598993045,133.703272709593));
#23219=CARTESIAN_POINT('Ctrl Pts',(186.807546365339,4.05390700260826,133.592517398559));
#23220=CARTESIAN_POINT('Ctrl Pts',(186.799798468562,4.13012512327185,133.478323174578));
#23221=CARTESIAN_POINT('Ctrl Pts',(186.792050571785,4.20145303038427,133.36111158236));
#23222=CARTESIAN_POINT('Ctrl Pts',(186.784304295701,4.27276601723617,133.24392450828));
#23223=CARTESIAN_POINT('Ctrl Pts',(186.776558019617,4.33919062208088,133.123721655165));
#23224=CARTESIAN_POINT('Ctrl Pts',(186.768811743533,4.40047344506548,133.000952641992));
#23225=CARTESIAN_POINT('Ctrl Pts',(186.761065410267,4.46175672042594,132.878182722566));
#23226=CARTESIAN_POINT('Ctrl Pts',(186.753319077002,4.51789796357578,132.752846955089));
#23227=CARTESIAN_POINT('Ctrl Pts',(186.745572743736,4.56869042857052,132.62541823071));
#23228=CARTESIAN_POINT('Ctrl Pts',(186.737824675734,4.61949426818561,132.497960969551));
#23229=CARTESIAN_POINT('Ctrl Pts',(186.730076607731,4.66494680138576,132.368410181932));
#23230=CARTESIAN_POINT('Ctrl Pts',(186.722328539728,4.70489012982407,132.237256960218));
#23231=CARTESIAN_POINT('Ctrl Pts',(186.714572236986,4.74487591050721,132.105964347298));
#23232=CARTESIAN_POINT('Ctrl Pts',(186.706815934244,4.77934067585266,131.973066272786));
#23233=CARTESIAN_POINT('Ctrl Pts',(186.699059631502,4.80817681928663,131.839067695427));
#23234=CARTESIAN_POINT('Ctrl Pts',(186.691299188988,4.83702835343861,131.704997598992));
#23235=CARTESIAN_POINT('Ctrl Pts',(186.683538746474,4.86024521347585,131.569826214457));
#23236=CARTESIAN_POINT('Ctrl Pts',(186.675778303959,4.8777714598113,131.434065825064));
#23237=CARTESIAN_POINT('Ctrl Pts',(186.668005403694,4.89532584083327,131.298087501042));
#23238=CARTESIAN_POINT('Ctrl Pts',(186.660232503429,4.90717131955267,131.161518672433));
#23239=CARTESIAN_POINT('Ctrl Pts',(186.652459603163,4.91330403923953,131.024874745214));
#23240=CARTESIAN_POINT('Ctrl Pts',(186.644969267401,4.91921381911843,130.893198168935));
#23241=CARTESIAN_POINT('Ctrl Pts',(186.637478931639,4.91981897388855,130.761452167314));
#23242=CARTESIAN_POINT('Ctrl Pts',(186.629988595877,4.91516164637668,130.630093430501));
#23243=CARTESIAN_POINT('Ctrl Pts',(186.622214261758,4.91032773487667,130.493754187256));
#23244=CARTESIAN_POINT('Ctrl Pts',(186.614439927639,4.89980909723262,130.357400273068));
#23245=CARTESIAN_POINT('Ctrl Pts',(186.60666559352,4.88359584406322,130.221544442131));
#23246=CARTESIAN_POINT('Ctrl Pts',(186.598900840573,4.86740257227934,130.085856041365));
#23247=CARTESIAN_POINT('Ctrl Pts',(186.591136087626,4.84552869479156,129.95066488697));
#23248=CARTESIAN_POINT('Ctrl Pts',(186.583371334678,4.81801631071333,129.816483149354));
#23249=CARTESIAN_POINT('Ctrl Pts',(186.575614293793,4.79053125232284,129.682434682933));
#23250=CARTESIAN_POINT('Ctrl Pts',(186.567857252908,4.75741891010157,129.549394018657));
#23251=CARTESIAN_POINT('Ctrl Pts',(186.560100212023,4.71877306587156,129.417867265507));
#23252=CARTESIAN_POINT('Ctrl Pts',(186.552349020783,4.68015636477332,129.286439697704));
#23253=CARTESIAN_POINT('Ctrl Pts',(186.544597829543,4.63601457725516,129.156524142229));
#23254=CARTESIAN_POINT('Ctrl Pts',(186.536846638303,4.58649227530057,129.028615232915));
#23255=CARTESIAN_POINT('Ctrl Pts',(186.529098741526,4.53699102164532,128.9007606883));
#23256=CARTESIAN_POINT('Ctrl Pts',(186.521350844749,4.48211394281148,128.774911457366));
#23257=CARTESIAN_POINT('Ctrl Pts',(186.513602947972,4.42205498674884,128.651545540354));
#23258=CARTESIAN_POINT('Ctrl Pts',(186.505856671888,4.3620085937251,128.528205428834));
#23259=CARTESIAN_POINT('Ctrl Pts',(186.498110395804,4.29678265050747,128.407347949309));
#23260=CARTESIAN_POINT('Ctrl Pts',(186.490364119719,4.2266184654652,128.289429324292));
#23261=CARTESIAN_POINT('Ctrl Pts',(186.482617786454,4.15645376248687,128.171509828827));
#23262=CARTESIAN_POINT('Ctrl Pts',(186.474871453189,4.08135094486343,128.056529567145));
#23263=CARTESIAN_POINT('Ctrl Pts',(186.467125119923,4.00159611807821,127.94491808968));
#23264=CARTESIAN_POINT('Ctrl Pts',(186.45937705192,3.92182343075255,127.833281617599));
#23265=CARTESIAN_POINT('Ctrl Pts',(186.451628983917,3.83739688849461,127.725015748974));
#23266=CARTESIAN_POINT('Ctrl Pts',(186.443880915914,3.74864431330477,127.620518775573));
#23267=CARTESIAN_POINT('Ctrl Pts',(186.436124613173,3.65979741082176,127.515910741544));
#23268=CARTESIAN_POINT('Ctrl Pts',(186.428368310431,3.56661554438332,127.415079902877));
#23269=CARTESIAN_POINT('Ctrl Pts',(186.420612007689,3.46946538610199,127.318389734564));
#23270=CARTESIAN_POINT('Ctrl Pts',(186.412851565175,3.37226337585601,127.221647959797));
#23271=CARTESIAN_POINT('Ctrl Pts',(186.405091122661,3.2710891417477,127.129051522826));
#23272=CARTESIAN_POINT('Ctrl Pts',(186.397330680146,3.166343445464,127.040924388816));
#23273=CARTESIAN_POINT('Ctrl Pts',(186.389557779881,3.06142960208977,126.952655785307));
#23274=CARTESIAN_POINT('Ctrl Pts',(186.381784879615,2.95293314934019,126.868871060837));
#23275=CARTESIAN_POINT('Ctrl Pts',(186.37401197935,2.84128562820487,126.789852049702));
#23276=CARTESIAN_POINT('Ctrl Pts',(186.366521643588,2.73369677568628,126.713705578658));
#23277=CARTESIAN_POINT('Ctrl Pts',(186.359031307826,2.6231822342181,126.641984512861));
#23278=CARTESIAN_POINT('Ctrl Pts',(186.351540972064,2.51014900938351,126.574900248537));
#23279=CARTESIAN_POINT('Ctrl Pts',(186.343766637945,2.39283009547328,126.50527246394));
#23280=CARTESIAN_POINT('Ctrl Pts',(186.335992303826,2.27242610514435,126.440419470445));
#23281=CARTESIAN_POINT('Ctrl Pts',(186.328217969707,2.14936308757183,126.380626744435));
#23282=CARTESIAN_POINT('Ctrl Pts',(186.32045321676,2.02645173417003,126.320907707617));
#23283=CARTESIAN_POINT('Ctrl Pts',(186.312688463813,1.90088822208354,126.266236699069));
#23284=CARTESIAN_POINT('Ctrl Pts',(186.304923710865,1.773126210382,126.216855140233));
#23285=CARTESIAN_POINT('Ctrl Pts',(186.29716666998,1.64549109371175,126.167522627858));
#23286=CARTESIAN_POINT('Ctrl Pts',(186.289409629095,1.51566218516442,126.123469250419));
#23287=CARTESIAN_POINT('Ctrl Pts',(186.28165258821,1.38411597992469,126.08488967088));
#23288=CARTESIAN_POINT('Ctrl Pts',(186.27390139697,1.25266897470157,126.046339184501));
#23289=CARTESIAN_POINT('Ctrl Pts',(186.26615020573,1.11950762410406,126.013254389403));
#23290=CARTESIAN_POINT('Ctrl Pts',(186.25839901449,0.985126222273834,125.985781014749));
#23291=CARTESIAN_POINT('Ctrl Pts',(186.250651117713,0.850801936124037,125.958319317012));
#23292=CARTESIAN_POINT('Ctrl Pts',(186.242903220936,0.715259012346737,125.936464374276));
#23293=CARTESIAN_POINT('Ctrl Pts',(186.235155324159,0.579004439687522,125.920311383445));
#23294=CARTESIAN_POINT('Ctrl Pts',(186.227409048075,0.442778368547621,125.904161771471));
#23295=CARTESIAN_POINT('Ctrl Pts',(186.219662771991,0.305841332620214,125.893711785003));
#23296=CARTESIAN_POINT('Ctrl Pts',(186.211916495907,0.168707597893969,125.889005003888));
#23297=CARTESIAN_POINT('Ctrl Pts',(186.204170162641,0.0315728508776698,
125.884298188029));
#23298=CARTESIAN_POINT('Ctrl Pts',(186.196423829376,-0.10575820709968,125.885334675529));
#23299=CARTESIAN_POINT('Ctrl Pts',(186.18867749611,-0.242769536089092,125.892105940247));
#23300=CARTESIAN_POINT('Ctrl Pts',(186.180929428107,-0.379811547815777,
125.898878721341));
#23301=CARTESIAN_POINT('Ctrl Pts',(186.173181360104,-0.516533297662758,
125.911388815894));
#23302=CARTESIAN_POINT('Ctrl Pts',(186.165433292102,-0.652422495685759,
125.929575704401));
#23303=CARTESIAN_POINT('Ctrl Pts',(186.15767698936,-0.788456118365381,125.947781922149));
#23304=CARTESIAN_POINT('Ctrl Pts',(186.149920686618,-0.923655033517907,
125.971676934201));
#23305=CARTESIAN_POINT('Ctrl Pts',(186.142164383876,-1.05751524410295,126.001148716037));
#23306=CARTESIAN_POINT('Ctrl Pts',(186.134403941362,-1.19144689991294,126.03063622785));
#23307=CARTESIAN_POINT('Ctrl Pts',(186.126643498848,-1.3240380496573,126.065706340432));
#23308=CARTESIAN_POINT('Ctrl Pts',(186.118883056333,-1.45479951078708,126.106196992711));
#23309=CARTESIAN_POINT('Ctrl Pts',(186.111110156068,-1.5857708818227,126.146752644179));
#23310=CARTESIAN_POINT('Ctrl Pts',(186.103337255803,-1.7149063263107,126.192746092524));
#23311=CARTESIAN_POINT('Ctrl Pts',(186.095564355537,-1.8417354706294,126.243966608412));
#23312=CARTESIAN_POINT('Ctrl Pts',(186.088074019775,-1.96395405608863,126.293325129531));
#23313=CARTESIAN_POINT('Ctrl Pts',(186.080583684013,-2.08403082912152,126.347537155255));
#23314=CARTESIAN_POINT('Ctrl Pts',(186.073093348251,-2.20156793963613,126.406374525084));
#23315=CARTESIAN_POINT('Ctrl Pts',(186.065318218632,-2.32357398828093,126.467448980412));
#23316=CARTESIAN_POINT('Ctrl Pts',(186.057543089012,-2.44322994792608,126.533700949362));
#23317=CARTESIAN_POINT('Ctrl Pts',(186.049767959393,-2.56006520571822,126.604926226488));
#23318=CARTESIAN_POINT('Ctrl Pts',(186.042002588127,-2.67675382676365,126.67606211071));
#23319=CARTESIAN_POINT('Ctrl Pts',(186.03423721686,-2.79062845967751,126.75215868097));
#23320=CARTESIAN_POINT('Ctrl Pts',(186.026471845594,-2.90124067215559,126.832964688585));
#23321=CARTESIAN_POINT('Ctrl Pts',(186.018491328848,-3.01491747957512,126.916009487709));
#23322=CARTESIAN_POINT('Ctrl Pts',(186.010510812103,-3.12514807592882,127.004028321582));
#23323=CARTESIAN_POINT('Ctrl Pts',(186.002530295357,-3.2314741111118,127.096698533218));
#23324=CARTESIAN_POINT('Ctrl Pts',(185.994779503498,-3.33473947526146,127.186701166476));
#23325=CARTESIAN_POINT('Ctrl Pts',(185.987028711639,-3.43432165183175,127.28109080366));
#23326=CARTESIAN_POINT('Ctrl Pts',(185.979277919781,-3.52983187439647,127.37952923471));
#23327=CARTESIAN_POINT('Ctrl Pts',(185.971530630239,-3.62529893917089,127.477923184813));
#23328=CARTESIAN_POINT('Ctrl Pts',(185.963783340697,-3.71669743948121,127.580362008493));
#23329=CARTESIAN_POINT('Ctrl Pts',(185.956036051155,-3.80367440789667,127.686469653916));
#23330=CARTESIAN_POINT('Ctrl Pts',(185.948290584601,-3.89063091006273,127.792552331516));
#23331=CARTESIAN_POINT('Ctrl Pts',(185.940545118047,-3.97316770391064,127.902301810235));
#23332=CARTESIAN_POINT('Ctrl Pts',(185.932799651493,-4.05097143863642,128.015308186031));
#23333=CARTESIAN_POINT('Ctrl Pts',(185.925054330194,-4.12877371426179,128.12831244255));
#23334=CARTESIAN_POINT('Ctrl Pts',(185.917309008896,-4.20184288741614,128.244573151684));
#23335=CARTESIAN_POINT('Ctrl Pts',(185.909563687597,-4.26990858509716,128.363650938515));
#23336=CARTESIAN_POINT('Ctrl Pts',(185.901814172698,-4.33801113604076,128.482793198423));
#23337=CARTESIAN_POINT('Ctrl Pts',(185.894064657798,-4.40110460739271,128.604755242451));
#23338=CARTESIAN_POINT('Ctrl Pts',(185.886315142899,-4.45896424491958,128.729072462868));
#23339=CARTESIAN_POINT('Ctrl Pts',(185.878563054062,-4.51684310004943,128.853430974228));
#23340=CARTESIAN_POINT('Ctrl Pts',(185.870810965225,-4.56948450454414,128.980145861196));
#23341=CARTESIAN_POINT('Ctrl Pts',(185.863058876388,-4.61671198790392,129.108732862649));
#23342=CARTESIAN_POINT('Ctrl Pts',(185.855299774332,-4.66398219738179,129.237436195167));
#23343=CARTESIAN_POINT('Ctrl Pts',(185.847540672277,-4.70582858667214,129.368014652284));
#23344=CARTESIAN_POINT('Ctrl Pts',(185.839781570221,-4.74212459112503,129.49996902577));
#23345=CARTESIAN_POINT('Ctrl Pts',(185.838167528046,-4.74967485680883,129.527418068522));
#23346=CARTESIAN_POINT('Ctrl Pts',(185.83655348587,-4.75698512267265,129.554926614318));
#23347=CARTESIAN_POINT('Ctrl Pts',(185.834939443695,-4.76405452823405,129.582490119308));
#23348=CARTESIAN_POINT('Ctrl Pts',(187.584954980304,-4.76405452823404,129.582490119308));
#23349=CARTESIAN_POINT('Ctrl Pts',(187.577318467045,-4.79766509150003,129.713537195371));
#23350=CARTESIAN_POINT('Ctrl Pts',(187.569681953786,-4.82585013568644,129.845916938469));
#23351=CARTESIAN_POINT('Ctrl Pts',(187.562045440527,-4.84852382797168,129.979133526341));
#23352=CARTESIAN_POINT('Ctrl Pts',(187.554181106445,-4.87187394666516,130.116324377291));
#23353=CARTESIAN_POINT('Ctrl Pts',(187.546316772363,-4.88937865955207,130.254402327779));
#23354=CARTESIAN_POINT('Ctrl Pts',(187.538452438282,-4.90100172800805,130.392820674715));
#23355=CARTESIAN_POINT('Ctrl Pts',(187.5305881042,-4.91262479646404,130.53123902165));
#23356=CARTESIAN_POINT('Ctrl Pts',(187.522723770118,-4.91836624934627,130.669997300341));
#23357=CARTESIAN_POINT('Ctrl Pts',(187.514859436036,-4.91824821531416,130.808550493347));
#23358=CARTESIAN_POINT('',(187.860140563976,-4.91824998954374,130.80468132454));
#23359=CARTESIAN_POINT('Ctrl Pts',(187.929867347344,-4.76405452823405,129.582490119308));
#23360=CARTESIAN_POINT('Ctrl Pts',(187.921775086847,-4.79957275528882,129.72097514753));
#23361=CARTESIAN_POINT('Ctrl Pts',(187.913682826349,-4.82908397265096,129.861148571076));
#23362=CARTESIAN_POINT('Ctrl Pts',(187.905590565851,-4.85243842824599,130.00247261879));
#23363=CARTESIAN_POINT('Ctrl Pts',(187.897511509163,-4.87575477733303,130.143566073847));
#23364=CARTESIAN_POINT('Ctrl Pts',(187.889432452475,-4.8929343404035,130.285806076163));
#23365=CARTESIAN_POINT('Ctrl Pts',(187.881353395787,-4.90387800511191,130.428643205833));
#23366=CARTESIAN_POINT('Ctrl Pts',(187.87428245186,-4.91345610840887,130.553656975815));
#23367=CARTESIAN_POINT('Ctrl Pts',(187.867211507934,-4.91825817656564,130.679127798048));
#23368=CARTESIAN_POINT('Ctrl Pts',(187.860140564008,-4.91824998954378,130.804681323973));
#23369=CARTESIAN_POINT('Ctrl Pts',(187.860140563976,-4.91824998954374,130.80468132454));
#23370=CARTESIAN_POINT('Ctrl Pts',(187.851985238763,-4.91824054696515,130.949489407629));
#23371=CARTESIAN_POINT('Ctrl Pts',(187.84382991355,-4.91183143561811,131.094160796668));
#23372=CARTESIAN_POINT('Ctrl Pts',(187.835674588336,-4.89908446976143,131.238128321115));
#23373=CARTESIAN_POINT('Ctrl Pts',(187.827507043422,-4.8863184042239,131.382311562291));
#23374=CARTESIAN_POINT('Ctrl Pts',(187.819339498508,-4.86719555824919,131.525788509872));
#23375=CARTESIAN_POINT('Ctrl Pts',(187.811171953594,-4.84182909625093,131.668000626596));
#23376=CARTESIAN_POINT('Ctrl Pts',(187.802983701521,-4.81639832271632,131.810573293393));
#23377=CARTESIAN_POINT('Ctrl Pts',(187.794795449448,-4.78469233773483,131.951874395443));
#23378=CARTESIAN_POINT('Ctrl Pts',(187.786607197375,-4.74687508460216,132.091357118604));
#23379=CARTESIAN_POINT('Ctrl Pts',(187.778407825462,-4.70900647474592,132.2310292626));
#23380=CARTESIAN_POINT('Ctrl Pts',(187.770208453549,-4.66501012991102,132.368877788919));
#23381=CARTESIAN_POINT('Ctrl Pts',(187.762009081637,-4.61509878206581,132.504374233475));
#23382=CARTESIAN_POINT('Ctrl Pts',(187.7537907155,-4.56507181227561,132.640184561809));
#23383=CARTESIAN_POINT('Ctrl Pts',(187.745572349363,-4.5091025670614,132.773631612781));
#23384=CARTESIAN_POINT('Ctrl Pts',(187.737353983226,-4.44745127249184,132.904208288544));
#23385=CARTESIAN_POINT('Ctrl Pts',(187.732966020474,-4.4145343179928,132.973925989116));
#23386=CARTESIAN_POINT('Ctrl Pts',(187.728578057722,-4.37999833546582,133.042825876845));
#23387=CARTESIAN_POINT('Ctrl Pts',(187.724190094969,-4.34388802098799,133.110834099663));
#23388=CARTESIAN_POINT('Ctrl Pts',(187.71641576085,-4.27990989132784,133.23132706574));
#23389=CARTESIAN_POINT('Ctrl Pts',(187.708641426731,-4.21081318308159,133.349346880017));
#23390=CARTESIAN_POINT('Ctrl Pts',(187.700867092612,-4.13681326770758,133.464428107428));
#23391=CARTESIAN_POINT('Ctrl Pts',(187.693102339665,-4.06290455061579,133.57936750751));
#23392=CARTESIAN_POINT('Ctrl Pts',(187.685337586718,-3.98410485912279,133.691375200834));
#23393=CARTESIAN_POINT('Ctrl Pts',(187.677572833771,-3.90067606158043,133.800009015678));
#23394=CARTESIAN_POINT('Ctrl Pts',(187.669815792886,-3.81733012669587,133.908534933887));
#23395=CARTESIAN_POINT('Ctrl Pts',(187.662058752001,-3.72936447197065,134.013693334156));
#23396=CARTESIAN_POINT('Ctrl Pts',(187.654301711116,-3.63708479189096,134.115070100305));
#23397=CARTESIAN_POINT('Ctrl Pts',(187.646550519876,-3.54487470063586,134.216370417446));
#23398=CARTESIAN_POINT('Ctrl Pts',(187.638799328636,-3.44835732151588,134.313894488769));
#23399=CARTESIAN_POINT('Ctrl Pts',(187.631048137396,-3.34787900468798,134.407260731706));
#23400=CARTESIAN_POINT('Ctrl Pts',(187.623300240619,-3.24744339382506,134.500587291499));
#23401=CARTESIAN_POINT('Ctrl Pts',(187.615552343842,-3.14305047942049,134.589759272133));
#23402=CARTESIAN_POINT('Ctrl Pts',(187.607804447065,-3.03508373938013,134.674431645009));
#23403=CARTESIAN_POINT('Ctrl Pts',(187.60005817098,-2.92713958365424,134.759086306249));
#23404=CARTESIAN_POINT('Ctrl Pts',(187.592311894896,-2.81562339669253,134.839242990757));
#23405=CARTESIAN_POINT('Ctrl Pts',(187.584565618812,-2.70095172170201,134.914596968378));
#23406=CARTESIAN_POINT('Ctrl Pts',(187.576819285547,-2.58627920023135,134.989951502245));
#23407=CARTESIAN_POINT('Ctrl Pts',(187.569072952282,-2.4684514709862,135.060503043776));
#23408=CARTESIAN_POINT('Ctrl Pts',(187.561326619016,-2.34791369668973,135.125990441533));
#23409=CARTESIAN_POINT('Ctrl Pts',(187.553578551013,-2.22734892879446,135.191492504738));
#23410=CARTESIAN_POINT('Ctrl Pts',(187.54583048301,-2.10407325166797,135.251927980875));
#23411=CARTESIAN_POINT('Ctrl Pts',(187.538082415007,-1.97855567117998,135.307082074479));
#23412=CARTESIAN_POINT('Ctrl Pts',(187.530326112265,-1.8529046891137,135.36229478651));
#23413=CARTESIAN_POINT('Ctrl Pts',(187.522569809524,-1.72500740244735,135.412214745672));
#23414=CARTESIAN_POINT('Ctrl Pts',(187.514813506782,-1.59535252627577,135.456675458525));
#23415=CARTESIAN_POINT('Ctrl Pts',(187.507053064268,-1.46562844939287,135.501159901399));
#23416=CARTESIAN_POINT('Ctrl Pts',(187.499292621754,-1.33414528842969,135.540179180866));
#23417=CARTESIAN_POINT('Ctrl Pts',(187.491532179239,-1.20140513403331,135.573617243752));
#23418=CARTESIAN_POINT('Ctrl Pts',(187.483759278974,-1.06845189335697,135.607108984385));
#23419=CARTESIAN_POINT('Ctrl Pts',(187.475986378709,-0.934238009971892,
135.635001524974));
#23420=CARTESIAN_POINT('Ctrl Pts',(187.468213478443,-0.799274826844706,
135.657230161833));
#23421=CARTESIAN_POINT('Ctrl Pts',(187.460723142681,-0.669217895375251,
135.678650731752));
#23422=CARTESIAN_POINT('Ctrl Pts',(187.453232806919,-0.538465501906267,
135.694812005137));
#23423=CARTESIAN_POINT('Ctrl Pts',(187.445742471157,-0.40747611749601,135.705701890745));
#23424=CARTESIAN_POINT('Ctrl Pts',(187.437968137038,-0.271520230763168,
135.717004669676));
#23425=CARTESIAN_POINT('Ctrl Pts',(187.430193802919,-0.134878359929164,
135.722664244519));
#23426=CARTESIAN_POINT('Ctrl Pts',(187.4224194688,0.0019414977692763,135.722610234359));
#23427=CARTESIAN_POINT('Ctrl Pts',(187.414654715853,0.138592737221022,135.722556290762));
#23428=CARTESIAN_POINT('Ctrl Pts',(187.406889962905,0.275421139878357,135.716802772767));
#23429=CARTESIAN_POINT('Ctrl Pts',(187.399125209958,0.411913147910088,135.70533099302));
#23430=CARTESIAN_POINT('Ctrl Pts',(187.391368169073,0.548269590155265,135.693870607207));
#23431=CARTESIAN_POINT('Ctrl Pts',(187.383611128188,0.684289915601994,135.676703294552));
#23432=CARTESIAN_POINT('Ctrl Pts',(187.375854087303,0.819460481241922,135.653862404573));
#23433=CARTESIAN_POINT('Ctrl Pts',(187.368102896063,0.954529113706643,135.631038739087));
#23434=CARTESIAN_POINT('Ctrl Pts',(187.360351704823,1.08874887791857,135.602550077227));
#23435=CARTESIAN_POINT('Ctrl Pts',(187.352600513583,1.22161152693562,135.568481558491));
#23436=CARTESIAN_POINT('Ctrl Pts',(187.344852616806,1.35441770578278,135.534427519784));
#23437=CARTESIAN_POINT('Ctrl Pts',(187.337104720029,1.4858675387463,135.494798438013));
#23438=CARTESIAN_POINT('Ctrl Pts',(187.329356823252,1.6154634643188,135.449730447617));
#23439=CARTESIAN_POINT('Ctrl Pts',(187.321610547168,1.74503228121749,135.404671884473));
#23440=CARTESIAN_POINT('Ctrl Pts',(187.313864271084,1.87274759303631,135.354176803992));
#23441=CARTESIAN_POINT('Ctrl Pts',(187.306117994999,1.99812786988819,135.298430941679));
#23442=CARTESIAN_POINT('Ctrl Pts',(187.298371661734,2.12350907226879,135.242684667863));
#23443=CARTESIAN_POINT('Ctrl Pts',(187.290625328469,2.24655484804188,135.181687693709));
#23444=CARTESIAN_POINT('Ctrl Pts',(187.282878995203,2.36680486178025,135.115673388492));
#23445=CARTESIAN_POINT('Ctrl Pts',(187.2751309272,2.48708180467538,135.04964429983));
#23446=CARTESIAN_POINT('Ctrl Pts',(187.267382859197,2.60456139703364,134.978595832385));
#23447=CARTESIAN_POINT('Ctrl Pts',(187.259634791194,2.71880941621897,134.902806471884));
#23448=CARTESIAN_POINT('Ctrl Pts',(187.251878488453,2.83317885955863,134.826936561549));
#23449=CARTESIAN_POINT('Ctrl Pts',(187.244122185711,2.9443095425167,134.746315909328));
#23450=CARTESIAN_POINT('Ctrl Pts',(187.236365882969,3.05179722699965,134.661265691298));
#23451=CARTESIAN_POINT('Ctrl Pts',(187.228605440455,3.15934228089629,134.576170079406));
#23452=CARTESIAN_POINT('Ctrl Pts',(187.220844997941,3.26324016595116,134.486640445942));
#23453=CARTESIAN_POINT('Ctrl Pts',(187.213084555426,3.36312185108178,134.393036484411));
#23454=CARTESIAN_POINT('Ctrl Pts',(187.205311655161,3.46316387516043,134.299282261492));
#23455=CARTESIAN_POINT('Ctrl Pts',(187.197538754896,3.55917654184175,134.201440919767));
#23456=CARTESIAN_POINT('Ctrl Pts',(187.18976585463,3.65082902071832,134.099907692633));
#23457=CARTESIAN_POINT('Ctrl Pts',(187.182275518868,3.73914970112908,134.002065454052));
#23458=CARTESIAN_POINT('Ctrl Pts',(187.174785183106,3.82342150061338,133.900795325352));
#23459=CARTESIAN_POINT('Ctrl Pts',(187.167294847344,3.90338643166027,133.796476495608));
#23460=CARTESIAN_POINT('Ctrl Pts',(187.159520513225,3.98638325737254,133.688202385727));
#23461=CARTESIAN_POINT('Ctrl Pts',(187.151746179106,4.06500308682427,133.576300848341));
#23462=CARTESIAN_POINT('Ctrl Pts',(187.143971844987,4.13891212164383,133.461161233309));
#23463=CARTESIAN_POINT('Ctrl Pts',(187.13620709204,4.2127300701834,133.346163517562));
#23464=CARTESIAN_POINT('Ctrl Pts',(187.128442339093,4.28184856640189,133.227935990211));
#23465=CARTESIAN_POINT('Ctrl Pts',(187.120677586145,4.34597429754696,133.106900621032));
#23466=CARTESIAN_POINT('Ctrl Pts',(187.11292054526,4.41003633811182,132.985985465888));
#23467=CARTESIAN_POINT('Ctrl Pts',(187.105163504375,4.46911530015668,132.862268361969));
#23468=CARTESIAN_POINT('Ctrl Pts',(187.09740646349,4.52296160498285,132.736199477914));
#23469=CARTESIAN_POINT('Ctrl Pts',(187.08965527225,4.5767673038917,132.610225663385));
#23470=CARTESIAN_POINT('Ctrl Pts',(187.08190408101,4.62534804688488,132.481903956843));
#23471=CARTESIAN_POINT('Ctrl Pts',(187.07415288977,4.6685007443457,132.351707980812));
#23472=CARTESIAN_POINT('Ctrl Pts',(187.066404992993,4.71163510075898,132.221567341544));
#23473=CARTESIAN_POINT('Ctrl Pts',(187.058657096216,4.74934587746924,132.089554387528));
#23474=CARTESIAN_POINT('Ctrl Pts',(187.050909199439,4.7814786640856,131.956161315341));
#23475=CARTESIAN_POINT('Ctrl Pts',(187.043162923355,4.8136047292157,131.822796146108));
#23476=CARTESIAN_POINT('Ctrl Pts',(187.035416647271,4.84015503356989,131.688051812779));
#23477=CARTESIAN_POINT('Ctrl Pts',(187.027670371187,4.86102556302323,131.552433834661));
#23478=CARTESIAN_POINT('Ctrl Pts',(187.019924037921,4.88189624653807,131.416814855442));
#23479=CARTESIAN_POINT('Ctrl Pts',(187.012177704656,4.89708701202375,131.280322604983));
#23480=CARTESIAN_POINT('Ctrl Pts',(187.00443137139,4.90654537711804,131.143470518309));
#23481=CARTESIAN_POINT('Ctrl Pts',(186.996683303387,4.9160058603476,131.006587784559));
#23482=CARTESIAN_POINT('Ctrl Pts',(186.988935235385,4.91973136175744,130.869345444204));
#23483=CARTESIAN_POINT('Ctrl Pts',(186.981187167382,4.9177214713347,130.732259349382));
#23484=CARTESIAN_POINT('Ctrl Pts',(186.97343086464,4.91570944477649,130.595027557828));
#23485=CARTESIAN_POINT('Ctrl Pts',(186.965674561898,4.90794985542348,130.457952735076));
#23486=CARTESIAN_POINT('Ctrl Pts',(186.957918259156,4.89449441724326,130.321548581599));
#23487=CARTESIAN_POINT('Ctrl Pts',(186.950157816642,4.88103179749054,130.185071625118));
#23488=CARTESIAN_POINT('Ctrl Pts',(186.942397374128,4.8618673259655,130.04926643811));
#23489=CARTESIAN_POINT('Ctrl Pts',(186.934636931613,4.83710415268687,129.914637920003));
#23490=CARTESIAN_POINT('Ctrl Pts',(186.926864031348,4.81230122736411,129.779793284246));
#23491=CARTESIAN_POINT('Ctrl Pts',(186.919091131083,4.78188172714106,129.646129473437));
#23492=CARTESIAN_POINT('Ctrl Pts',(186.911318230817,4.74599935115195,129.514138457872));
#23493=CARTESIAN_POINT('Ctrl Pts',(186.903827895055,4.71142138991215,129.386945648188));
#23494=CARTESIAN_POINT('Ctrl Pts',(186.896337559293,4.67177092859245,129.261306418357));
#23495=CARTESIAN_POINT('Ctrl Pts',(186.888847223531,4.62722754114839,129.137642781537));
#23496=CARTESIAN_POINT('Ctrl Pts',(186.881072889412,4.58099527763089,129.00929040034));
#23497=CARTESIAN_POINT('Ctrl Pts',(186.873298555293,4.52934528322642,128.882659796889));
#23498=CARTESIAN_POINT('Ctrl Pts',(186.865524221174,4.47242470282503,128.758242258316));
#23499=CARTESIAN_POINT('Ctrl Pts',(186.857759468227,4.41557427195186,128.63397805324));
#23500=CARTESIAN_POINT('Ctrl Pts',(186.84999471528,4.35346634033301,128.511921838433));
#23501=CARTESIAN_POINT('Ctrl Pts',(186.842229962332,4.28629738038526,128.392548471191));
#23502=CARTESIAN_POINT('Ctrl Pts',(186.834472921447,4.21919513359548,128.27329366726));
#23503=CARTESIAN_POINT('Ctrl Pts',(186.826715880562,4.14704205228711,128.156716746663));
#23504=CARTESIAN_POINT('Ctrl Pts',(186.818958839677,4.07008197270261,128.04327101417));
#23505=CARTESIAN_POINT('Ctrl Pts',(186.811207648437,3.99317992931273,127.929910831987));
#23506=CARTESIAN_POINT('Ctrl Pts',(186.803456457197,3.91147832157752,127.81967746021));
#23507=CARTESIAN_POINT('Ctrl Pts',(186.795705265957,3.82526584664194,127.712997768431));
#23508=CARTESIAN_POINT('Ctrl Pts',(186.78795736918,3.739090014308,127.606363418365));
#23509=CARTESIAN_POINT('Ctrl Pts',(186.780209472403,3.64840737324212,127.503280047653));
#23510=CARTESIAN_POINT('Ctrl Pts',(186.772461575626,3.55354855977579,127.404143610401));
#23511=CARTESIAN_POINT('Ctrl Pts',(186.764715299542,3.45870958872832,127.305027910354));
#23512=CARTESIAN_POINT('Ctrl Pts',(186.756969023458,3.35969645297088,127.209857783879));
#23513=CARTESIAN_POINT('Ctrl Pts',(186.749222747373,3.25687823804013,127.11899398654));
#23514=CARTESIAN_POINT('Ctrl Pts',(186.741476414108,3.15405926412871,127.028129518465));
#23515=CARTESIAN_POINT('Ctrl Pts',(186.733730080843,3.04743544795587,126.941571701855));
#23516=CARTESIAN_POINT('Ctrl Pts',(186.725983747577,2.9374103889513,126.859642215781));
#23517=CARTESIAN_POINT('Ctrl Pts',(186.718235679574,2.82736069059759,126.777694382167));
#23518=CARTESIAN_POINT('Ctrl Pts',(186.710487611571,2.71390854726417,126.700377175026));
#23519=CARTESIAN_POINT('Ctrl Pts',(186.702739543568,2.5974877383432,126.627969769997));
#23520=CARTESIAN_POINT('Ctrl Pts',(186.694983240827,2.48094319600109,126.555485409516));
#23521=CARTESIAN_POINT('Ctrl Pts',(186.687226938085,2.36142401787533,126.487921481866));
#23522=CARTESIAN_POINT('Ctrl Pts',(186.679470635343,2.23939034738478,126.425512146274));
#23523=CARTESIAN_POINT('Ctrl Pts',(186.671710192829,2.11729154384987,126.36306950094));
#23524=CARTESIAN_POINT('Ctrl Pts',(186.663949750315,1.99267592883989,126.305787092796));
#23525=CARTESIAN_POINT('Ctrl Pts',(186.6561893078,1.86602404364675,126.253851049283));
#23526=CARTESIAN_POINT('Ctrl Pts',(186.648416407535,1.73916884560389,126.201831633423));
#23527=CARTESIAN_POINT('Ctrl Pts',(186.64064350727,1.6102712131062,126.155175865823));
#23528=CARTESIAN_POINT('Ctrl Pts',(186.632870607004,1.47982813283383,126.114020357012));
#23529=CARTESIAN_POINT('Ctrl Pts',(186.625380271242,1.35412698709598,126.074360954611));
#23530=CARTESIAN_POINT('Ctrl Pts',(186.61788993548,1.22699110189288,126.039808938046));
#23531=CARTESIAN_POINT('Ctrl Pts',(186.610399599718,1.09887259295406,126.010441335084));
#23532=CARTESIAN_POINT('Ctrl Pts',(186.602625265599,0.965896431807742,125.979960250529));
#23533=CARTESIAN_POINT('Ctrl Pts',(186.59485093148,0.831440435162286,125.954967919335));
#23534=CARTESIAN_POINT('Ctrl Pts',(186.587076597361,0.695997472203889,125.935606097036));
#23535=CARTESIAN_POINT('Ctrl Pts',(186.579311844414,0.560721430592498,125.916268136452));
#23536=CARTESIAN_POINT('Ctrl Pts',(186.571547091467,0.424461226152909,125.902546932818));
#23537=CARTESIAN_POINT('Ctrl Pts',(186.56378233852,0.287722567918223,125.894533860295));
#23538=CARTESIAN_POINT('Ctrl Pts',(186.556025297635,0.151119720446433,125.886528746469));
#23539=CARTESIAN_POINT('Ctrl Pts',(186.54826825675,0.014039752633058,125.884220504122));
#23540=CARTESIAN_POINT('Ctrl Pts',(186.540511215865,-0.123004157933034,
125.887649009221));
#23541=CARTESIAN_POINT('Ctrl Pts',(186.532760024625,-0.259944722620193,
125.891074928858));
#23542=CARTESIAN_POINT('Ctrl Pts',(186.525008833384,-0.396848894920734,
125.90022897531));
#23543=CARTESIAN_POINT('Ctrl Pts',(186.517257642144,-0.533201489500632,
125.915098992935));
#23544=CARTESIAN_POINT('Ctrl Pts',(186.509509745367,-0.669496130590324,
125.929962690404));
#23545=CARTESIAN_POINT('Ctrl Pts',(186.50176184859,-0.805239272386058,125.950537484778));
#23546=CARTESIAN_POINT('Ctrl Pts',(186.494013951813,-0.939919070470149,
125.976759225211));
#23547=CARTESIAN_POINT('Ctrl Pts',(186.486267675729,-1.07457069644382,126.002975480622));
#23548=CARTESIAN_POINT('Ctrl Pts',(186.478521399645,-1.20815903761232,126.034836257913));
#23549=CARTESIAN_POINT('Ctrl Pts',(186.470775123561,-1.34018108035477,126.072226032164));
#23550=CARTESIAN_POINT('Ctrl Pts',(186.463028790295,-1.47220409765393,126.109616082418));
#23551=CARTESIAN_POINT('Ctrl Pts',(186.45528245703,-1.60266041728542,126.152535104537));
#23552=CARTESIAN_POINT('Ctrl Pts',(186.447536123765,-1.73106124618654,126.200817414288));
#23553=CARTESIAN_POINT('Ctrl Pts',(186.439788055762,-1.85949082956307,126.249110536526));
#23554=CARTESIAN_POINT('Ctrl Pts',(186.432039987759,-1.98586364036161,126.302769198807));
#23555=CARTESIAN_POINT('Ctrl Pts',(186.424291919756,-2.10971033185508,126.361579351494));
#23556=CARTESIAN_POINT('Ctrl Pts',(186.416535617014,-2.23368864908604,126.42045200831));
#23557=CARTESIAN_POINT('Ctrl Pts',(186.408779314272,-2.35513513012335,126.484486924591));
#23558=CARTESIAN_POINT('Ctrl Pts',(186.40102301153,-2.47360405141956,126.553423537427));
#23559=CARTESIAN_POINT('Ctrl Pts',(186.393262569016,-2.59213620314615,126.622396943809));
#23560=CARTESIAN_POINT('Ctrl Pts',(186.385502126502,-2.70768729925805,126.696277049213));
#23561=CARTESIAN_POINT('Ctrl Pts',(186.377741683988,-2.81984100116167,126.774760167066));
#23562=CARTESIAN_POINT('Ctrl Pts',(186.369968783722,-2.93217474214415,126.853369272988));
#23563=CARTESIAN_POINT('Ctrl Pts',(186.362195883457,-3.04109987965048,126.936595919761));
#23564=CARTESIAN_POINT('Ctrl Pts',(186.354422983192,-3.14623284593448,127.024095819743));
#23565=CARTESIAN_POINT('Ctrl Pts',(186.346932647429,-3.24754396407987,127.108414877961));
#23566=CARTESIAN_POINT('Ctrl Pts',(186.339442311667,-3.34533360559828,127.196701689925));
#23567=CARTESIAN_POINT('Ctrl Pts',(186.331951975905,-3.43929258525454,127.288617513255));
#23568=CARTESIAN_POINT('Ctrl Pts',(186.324290294265,-3.53540093236302,127.382635965623));
#23569=CARTESIAN_POINT('Ctrl Pts',(186.316628612625,-3.62782449528663,127.480768053431));
#23570=CARTESIAN_POINT('Ctrl Pts',(186.308966930984,-3.7161827594279,127.582688883663));
#23571=CARTESIAN_POINT('Ctrl Pts',(186.301314183386,-3.80443799181967,127.68449086727));
#23572=CARTESIAN_POINT('Ctrl Pts',(186.293661435788,-3.88863708801042,127.790072509402));
#23573=CARTESIAN_POINT('Ctrl Pts',(186.28600868819,-3.96843439155349,127.899070349377));
#23574=CARTESIAN_POINT('Ctrl Pts',(186.278363092695,-4.04815711815039,128.007966322175));
#23575=CARTESIAN_POINT('Ctrl Pts',(186.2707174972,-4.12348599584845,128.120271821147));
#23576=CARTESIAN_POINT('Ctrl Pts',(186.263071901705,-4.19411426884116,128.235588817191));
#23577=CARTESIAN_POINT('Ctrl Pts',(186.255431906839,-4.26469080449765,128.350821340064));
#23578=CARTESIAN_POINT('Ctrl Pts',(186.247791911973,-4.33057337660585,128.469060628456));
#23579=CARTESIAN_POINT('Ctrl Pts',(186.240151917107,-4.39149772261774,128.589878552896));
#23580=CARTESIAN_POINT('Ctrl Pts',(186.232515226792,-4.45239571683195,128.710644219582));
#23581=CARTESIAN_POINT('Ctrl Pts',(186.224878536477,-4.50833957015994,128.833985944203));
#23582=CARTESIAN_POINT('Ctrl Pts',(186.217241846161,-4.5591105114303,128.959450211322));
#23583=CARTESIAN_POINT('Ctrl Pts',(186.209605532488,-4.60987894867488,129.084908290537));
#23584=CARTESIAN_POINT('Ctrl Pts',(186.201969218815,-4.65547482316395,129.212488333294));
#23585=CARTESIAN_POINT('Ctrl Pts',(186.194332905142,-4.695727286753,129.341716330344));
#23586=CARTESIAN_POINT('Ctrl Pts',(186.189625064471,-4.72054321146236,129.421386292359));
#23587=CARTESIAN_POINT('Ctrl Pts',(186.184917223801,-4.74332916114695,129.501682227587));
#23588=CARTESIAN_POINT('Ctrl Pts',(186.18020938313,-4.76405452823405,129.582490119308));
#23589=CARTESIAN_POINT('Origin',(213.235140564004,0.,130.804360617566));
#23590=CARTESIAN_POINT('',(184.084599308536,-4.76405452823405,129.582490119308));
#23591=CARTESIAN_POINT('',(184.430229652623,-4.76405452823406,129.582490119308));
#23592=CARTESIAN_POINT('',(213.235140564004,-4.76405452823405,129.582490119308));
#23593=CARTESIAN_POINT('',(185.764859435953,-4.91824909926408,130.801384027568));
#23594=CARTESIAN_POINT('Ctrl Pts',(185.764859435953,-4.91824909926409,130.801384027568));
#23595=CARTESIAN_POINT('Ctrl Pts',(185.757191235898,-4.9183306751947,130.936172744721));
#23596=CARTESIAN_POINT('Ctrl Pts',(185.749523035843,-4.91286708241096,131.071183771682));
#23597=CARTESIAN_POINT('Ctrl Pts',(185.741854835789,-4.901829924088,131.205915667111));
#23598=CARTESIAN_POINT('Ctrl Pts',(185.734195115826,-4.89080497151269,131.340498565537));
#23599=CARTESIAN_POINT('Ctrl Pts',(185.726535395862,-4.87421874451201,131.474802549089));
#23600=CARTESIAN_POINT('Ctrl Pts',(185.718875675899,-4.85209485286721,131.608324921052));
#23601=CARTESIAN_POINT('Ctrl Pts',(185.711222480037,-4.82998980505673,131.741733566484));
#23602=CARTESIAN_POINT('Ctrl Pts',(185.703569284174,-4.80235654064527,131.874361530089));
#23603=CARTESIAN_POINT('Ctrl Pts',(185.695916088312,-4.76927054522506,132.00571049539));
#23604=CARTESIAN_POINT('Ctrl Pts',(185.688267001704,-4.73620231477376,132.136988935073));
#23605=CARTESIAN_POINT('Ctrl Pts',(185.680617915096,-4.69768727340913,132.266989353296));
#23606=CARTESIAN_POINT('Ctrl Pts',(185.672968828489,-4.65385205465889,132.395223313039));
#23607=CARTESIAN_POINT('Ctrl Pts',(185.665321809995,-4.61002868781017,132.523422601658));
#23608=CARTESIAN_POINT('Ctrl Pts',(185.657674791501,-4.56088813315632,132.649856001177));
#23609=CARTESIAN_POINT('Ctrl Pts',(185.650027773007,-4.50660683515309,132.774050414425));
#23610=CARTESIAN_POINT('Ctrl Pts',(185.642381064432,-4.4523277370657,132.898239794315));
#23611=CARTESIAN_POINT('Ctrl Pts',(185.634734355857,-4.39290847102935,133.020189999991));
#23612=CARTESIAN_POINT('Ctrl Pts',(185.627087647282,-4.3285733387234,133.139448606014));
#23613=CARTESIAN_POINT('Ctrl Pts',(185.619439490905,-4.26422602542105,133.258729792058));
#23614=CARTESIAN_POINT('Ctrl Pts',(185.611791334528,-4.19496118620005,133.37531801141));
#23615=CARTESIAN_POINT('Ctrl Pts',(185.604143178151,-4.12104844176228,133.488786590311));
#23616=CARTESIAN_POINT('Ctrl Pts',(185.596487235631,-4.04706045105567,133.602370684977));
#23617=CARTESIAN_POINT('Ctrl Pts',(185.58883129311,-3.96841532550673,133.71282845947));
#23618=CARTESIAN_POINT('Ctrl Pts',(185.58117535059,-3.88542548694373,133.819763053048));
#23619=CARTESIAN_POINT('Ctrl Pts',(185.573515374056,-3.80239191997511,133.926753991828));
#23620=CARTESIAN_POINT('Ctrl Pts',(185.565855397521,-3.71500934088863,134.03021774658));
#23621=CARTESIAN_POINT('Ctrl Pts',(185.558195420987,-3.62362875719401,134.129792573348));
#23622=CARTESIAN_POINT('Ctrl Pts',(185.550523572136,-3.5321065413066,134.229521732694));
#23623=CARTESIAN_POINT('Ctrl Pts',(185.542851723284,-3.43657422762343,134.325349640552));
#23624=CARTESIAN_POINT('Ctrl Pts',(185.535179874433,-3.33741822988249,134.416952847717));
#23625=CARTESIAN_POINT('Ctrl Pts',(185.528852616497,-3.25564060551483,134.492501405919));
#23626=CARTESIAN_POINT('Ctrl Pts',(185.522525358561,-3.17139888835135,134.56517703643));
#23627=CARTESIAN_POINT('Ctrl Pts',(185.516198100626,-3.08492473413098,134.634820439473));
#23628=CARTESIAN_POINT('Ctrl Pts',(185.508423766507,-2.97867349948799,134.720391644243));
#23629=CARTESIAN_POINT('Ctrl Pts',(185.500649432388,-2.86869084610792,134.801674161477));
#23630=CARTESIAN_POINT('Ctrl Pts',(185.492875098269,-2.75535800148616,134.878324945606));
#23631=CARTESIAN_POINT('Ctrl Pts',(185.485110345321,-2.64216482946666,134.954881264495));
#23632=CARTESIAN_POINT('Ctrl Pts',(185.477345592374,-2.52563000205102,135.026816990961));
#23633=CARTESIAN_POINT('Ctrl Pts',(185.469580839427,-2.4061683288018,135.093828770609));
#23634=CARTESIAN_POINT('Ctrl Pts',(185.461823798542,-2.28682530657056,135.160773993213));
#23635=CARTESIAN_POINT('Ctrl Pts',(185.454066757657,-2.16456156231129,135.222804811345));
#23636=CARTESIAN_POINT('Ctrl Pts',(185.446309716772,-2.03982114582494,135.279660915372));
#23637=CARTESIAN_POINT('Ctrl Pts',(185.438558525532,-1.91517479705691,135.33647414377));
#23638=CARTESIAN_POINT('Ctrl Pts',(185.430807334292,-1.78805584787562,135.388120263844));
#23639=CARTESIAN_POINT('Ctrl Pts',(185.423056143052,-1.65893291082312,135.434384878829));
#23640=CARTESIAN_POINT('Ctrl Pts',(185.415308246275,-1.52986485446345,135.480629830119));
#23641=CARTESIAN_POINT('Ctrl Pts',(185.407560349498,-1.39879487157781,135.521497693954));
#23642=CARTESIAN_POINT('Ctrl Pts',(185.399812452721,-1.2662113115785,135.556822293049));
#23643=CARTESIAN_POINT('Ctrl Pts',(185.392066176637,-1.13365548520171,135.592139502999));
#23644=CARTESIAN_POINT('Ctrl Pts',(185.384319900553,-0.999587089008202,
135.62191565399));
#23645=CARTESIAN_POINT('Ctrl Pts',(185.376573624468,-0.864509000677892,
135.646034630782));
#23646=CARTESIAN_POINT('Ctrl Pts',(185.368827291203,-0.729429915231751,
135.670153785614));
#23647=CARTESIAN_POINT('Ctrl Pts',(185.361080957938,-0.593341507654216,
135.688615614195));
#23648=CARTESIAN_POINT('Ctrl Pts',(185.353334624672,-0.456755805682509,
135.701355328251));
#23649=CARTESIAN_POINT('Ctrl Pts',(185.345586556669,-0.320139516289562,
135.714097895278));
#23650=CARTESIAN_POINT('Ctrl Pts',(185.337838488666,-0.183026100098795,
135.721115761585));
#23651=CARTESIAN_POINT('Ctrl Pts',(185.330090420663,-0.0459312508572161,
135.722396138248));
#23652=CARTESIAN_POINT('Ctrl Pts',(185.322334117922,0.0913093044211189,
135.723677875712));
#23653=CARTESIAN_POINT('Ctrl Pts',(185.31457781518,0.228530861759579,135.719209938718));
#23654=CARTESIAN_POINT('Ctrl Pts',(185.306821512438,0.365218627626155,135.709031698947));
#23655=CARTESIAN_POINT('Ctrl Pts',(185.299061069924,0.501979347869056,135.698848026743));
#23656=CARTESIAN_POINT('Ctrl Pts',(185.29130062741,0.638205320812515,135.682948024144));
#23657=CARTESIAN_POINT('Ctrl Pts',(185.283540184895,0.773389317112324,135.661422695271));
#23658=CARTESIAN_POINT('Ctrl Pts',(185.27576728463,0.908790322764111,135.639862812028));
#23659=CARTESIAN_POINT('Ctrl Pts',(185.267994384365,1.04314562582757,135.612659634777));
#23660=CARTESIAN_POINT('Ctrl Pts',(185.260221484099,1.175959709326,135.57995501246));
#23661=CARTESIAN_POINT('Ctrl Pts',(185.252731148337,1.30394566635063,135.548439285542));
#23662=CARTESIAN_POINT('Ctrl Pts',(185.245240812575,1.43050021692963,135.511815237666));
#23663=CARTESIAN_POINT('Ctrl Pts',(185.237750476813,1.55519716015653,135.470252263923));
#23664=CARTESIAN_POINT('Ctrl Pts',(185.229976142694,1.68462202588672,135.427113417397));
#23665=CARTESIAN_POINT('Ctrl Pts',(185.222201808575,1.81245562030366,135.378517082239));
#23666=CARTESIAN_POINT('Ctrl Pts',(185.214427474456,1.93820326668134,135.324598571427));
#23667=CARTESIAN_POINT('Ctrl Pts',(185.206662721509,2.06379594032369,135.270746510361));
#23668=CARTESIAN_POINT('Ctrl Pts',(185.198897968562,2.18730742506553,135.211585476901));
#23669=CARTESIAN_POINT('Ctrl Pts',(185.191133215614,2.30825828556062,135.147300491619));
#23670=CARTESIAN_POINT('Ctrl Pts',(185.183376174729,2.42908901595603,135.083079355091));
#23671=CARTESIAN_POINT('Ctrl Pts',(185.175619133844,2.54736384028493,135.013744576743));
#23672=CARTESIAN_POINT('Ctrl Pts',(185.167862092959,2.66262373291742,134.939529044535));
#23673=CARTESIAN_POINT('Ctrl Pts',(185.160110901719,2.77779670716764,134.865369478838));
#23674=CARTESIAN_POINT('Ctrl Pts',(185.152359710479,2.8899589477656,134.786336696123));
#23675=CARTESIAN_POINT('Ctrl Pts',(185.144608519239,2.99867678011411,134.702709066705));
#23676=CARTESIAN_POINT('Ctrl Pts',(185.136860622462,3.107348404484,134.61911698126));
#23677=CARTESIAN_POINT('Ctrl Pts',(185.129112725685,3.21257822307831,134.530934171219));
#23678=CARTESIAN_POINT('Ctrl Pts',(185.121364828908,3.31396246145469,134.438481675892));
#23679=CARTESIAN_POINT('Ctrl Pts',(185.113618552824,3.41532549243393,134.346048519634));
#23680=CARTESIAN_POINT('Ctrl Pts',(185.10587227674,3.51284425451252,134.249347717836));
#23681=CARTESIAN_POINT('Ctrl Pts',(185.098126000655,3.60614923898019,134.148739592608));
#23682=CARTESIAN_POINT('Ctrl Pts',(185.09037966739,3.69945491220408,134.048130724714));
#23683=CARTESIAN_POINT('Ctrl Pts',(185.082633334125,3.78854647989511,133.943614762498));
#23684=CARTESIAN_POINT('Ctrl Pts',(185.074887000859,3.87309267034491,133.835587469753));
#23685=CARTESIAN_POINT('Ctrl Pts',(185.067138932856,3.95765779432756,133.727535985046));
#23686=CARTESIAN_POINT('Ctrl Pts',(185.059390864854,4.03767527464004,133.615971912911));
#23687=CARTESIAN_POINT('Ctrl Pts',(185.051642796851,4.11285560653182,133.501322208379));
#23688=CARTESIAN_POINT('Ctrl Pts',(185.043886494109,4.18811584097532,133.386550652776));
#23689=CARTESIAN_POINT('Ctrl Pts',(185.036130191367,4.2585284426082,133.268687241189));
#23690=CARTESIAN_POINT('Ctrl Pts',(185.028373888625,4.32384827746161,133.148186365354));
#23691=CARTESIAN_POINT('Ctrl Pts',(185.020613446111,4.38920297547765,133.027621174572));
#23692=CARTESIAN_POINT('Ctrl Pts',(185.012853003597,4.44945931886022,132.904416065631));
#23693=CARTESIAN_POINT('Ctrl Pts',(185.005092561082,4.50441970210254,132.779046974892));
#23694=CARTESIAN_POINT('Ctrl Pts',(184.997319660817,4.55946831263118,132.65347663056));
#23695=CARTESIAN_POINT('Ctrl Pts',(184.989546760552,4.6092038322925,132.525735727174));
#23696=CARTESIAN_POINT('Ctrl Pts',(184.981773860286,4.65347776358927,132.396317830019));
#23697=CARTESIAN_POINT('Ctrl Pts',(184.974283524524,4.69614222596426,132.271604599409));
#23698=CARTESIAN_POINT('Ctrl Pts',(184.966793188762,4.7337352030942,132.145334479326));
#23699=CARTESIAN_POINT('Ctrl Pts',(184.959302853,4.7661688398658,132.017957606847));
#23700=CARTESIAN_POINT('Ctrl Pts',(184.951528518881,4.79983220783342,131.885751201534));
#23701=CARTESIAN_POINT('Ctrl Pts',(184.943754184762,4.8280439150364,131.751933671931));
#23702=CARTESIAN_POINT('Ctrl Pts',(184.935979850643,4.85065041926304,131.616994343548));
#23703=CARTESIAN_POINT('Ctrl Pts',(184.928215097696,4.87322906299363,131.482221315828));
#23704=CARTESIAN_POINT('Ctrl Pts',(184.920450344748,4.8902161844549,131.346329622014));
#23705=CARTESIAN_POINT('Ctrl Pts',(184.912685591801,4.90150830017843,131.209822632781));
#23706=CARTESIAN_POINT('Ctrl Pts',(184.904928550916,4.91278920041345,131.073451224213));
#23707=CARTESIAN_POINT('Ctrl Pts',(184.897171510031,4.91838631929962,130.936466123495));
#23708=CARTESIAN_POINT('Ctrl Pts',(184.889414469146,4.91824747750727,130.799379403521));
#23709=CARTESIAN_POINT('Ctrl Pts',(184.881663277906,4.9181087404166,130.662396061707));
#23710=CARTESIAN_POINT('Ctrl Pts',(184.873912086666,4.91224265275202,130.525311642551));
#23711=CARTESIAN_POINT('Ctrl Pts',(184.866160895426,4.9006490036298,130.388641474728));
#23712=CARTESIAN_POINT('Ctrl Pts',(184.858412998649,4.88906028211778,130.252029395372));
#23713=CARTESIAN_POINT('Ctrl Pts',(184.850665101872,4.87174887389483,130.115831605913));
#23714=CARTESIAN_POINT('Ctrl Pts',(184.842917205095,4.84876662847558,129.980561342814));
#23715=CARTESIAN_POINT('Ctrl Pts',(184.835170929011,4.82578919044663,129.845319375338));
#23716=CARTESIAN_POINT('Ctrl Pts',(184.827424652926,4.7971433401164,129.711004933506));
#23717=CARTESIAN_POINT('Ctrl Pts',(184.819678376842,4.76293249819749,129.578123658363));
#23718=CARTESIAN_POINT('Ctrl Pts',(184.811932043577,4.72872140374189,129.445241402321));
#23719=CARTESIAN_POINT('Ctrl Pts',(184.804185710312,4.68894533320337,129.313792712696));
#23720=CARTESIAN_POINT('Ctrl Pts',(184.796439377046,4.64375819341888,129.184270217756));
#23721=CARTESIAN_POINT('Ctrl Pts',(184.788691309043,4.59856093428778,129.054718717152));
#23722=CARTESIAN_POINT('Ctrl Pts',(184.78094324104,4.54795032338664,128.927094638659));
#23723=CARTESIAN_POINT('Ctrl Pts',(184.773195173037,4.49212908568403,128.801872330446));
#23724=CARTESIAN_POINT('Ctrl Pts',(184.765438870295,4.43624852050568,128.676516934474));
#23725=CARTESIAN_POINT('Ctrl Pts',(184.757682567554,4.37514642537891,128.553568765596));
#23726=CARTESIAN_POINT('Ctrl Pts',(184.749926264812,4.30907259203993,128.433479671793));
#23727=CARTESIAN_POINT('Ctrl Pts',(184.742165822298,4.24296349310673,128.313326482825));
#23728=CARTESIAN_POINT('Ctrl Pts',(184.734405379783,4.17187757104574,128.196035743754));
#23729=CARTESIAN_POINT('Ctrl Pts',(184.726644937269,4.09610843399477,128.08203096092));
#23730=CARTESIAN_POINT('Ctrl Pts',(184.718872037004,4.02021766559842,127.967843167486));
#23731=CARTESIAN_POINT('Ctrl Pts',(184.711099136738,3.93962888900392,127.856952187687));
#23732=CARTESIAN_POINT('Ctrl Pts',(184.703326236473,3.85467708813893,127.749749740764));
#23733=CARTESIAN_POINT('Ctrl Pts',(184.695835900711,3.77281349921669,127.646444372814));
#23734=CARTESIAN_POINT('Ctrl Pts',(184.688345564949,3.68689879343445,127.546564252244));
#23735=CARTESIAN_POINT('Ctrl Pts',(184.680855229187,3.59726419602927,127.450426604133));
#23736=CARTESIAN_POINT('Ctrl Pts',(184.673080895068,3.50423107561896,127.350643867872));
#23737=CARTESIAN_POINT('Ctrl Pts',(184.665306560949,3.4068957149069,127.25457691618));
#23738=CARTESIAN_POINT('Ctrl Pts',(184.65753222683,3.30558680398728,127.162619420857));
#23739=CARTESIAN_POINT('Ctrl Pts',(184.649767473883,3.20440274724626,127.070775254929));
#23740=CARTESIAN_POINT('Ctrl Pts',(184.642002720936,3.09925517067157,126.983030728698));
#23741=CARTESIAN_POINT('Ctrl Pts',(184.634237967988,2.99051163892463,126.899744989882));
#23742=CARTESIAN_POINT('Ctrl Pts',(184.626480927103,2.88187611278586,126.816541971634));
#23743=CARTESIAN_POINT('Ctrl Pts',(184.618723886218,2.7696520474073,126.737789164012));
#23744=CARTESIAN_POINT('Ctrl Pts',(184.610966845333,2.65424206001439,126.663807254868));
#23745=CARTESIAN_POINT('Ctrl Pts',(184.603215654093,2.53891910419166,126.589881136058));
#23746=CARTESIAN_POINT('Ctrl Pts',(184.595464462853,2.42041533625422,126.52071896472));
#23747=CARTESIAN_POINT('Ctrl Pts',(184.587713271613,2.29916420282371,126.456599466013));
#23748=CARTESIAN_POINT('Ctrl Pts',(184.579965374836,2.17796460435902,126.392507219803));
#23749=CARTESIAN_POINT('Ctrl Pts',(184.572217478059,2.0540203077666,126.333453565807));
#23750=CARTESIAN_POINT('Ctrl Pts',(184.564469581282,1.92779113934713,126.279672298405));
#23751=CARTESIAN_POINT('Ctrl Pts',(184.556723305198,1.80158837534844,126.225902280884));
#23752=CARTESIAN_POINT('Ctrl Pts',(184.548977029114,1.67310204963539,126.177402609436));
#23753=CARTESIAN_POINT('Ctrl Pts',(184.54123075303,1.54281347376092,126.134359584624));
#23754=CARTESIAN_POINT('Ctrl Pts',(184.533484419764,1.41252393612583,126.091316242077));
#23755=CARTESIAN_POINT('Ctrl Pts',(184.525738086499,1.28043249301377,126.053729749183));
#23756=CARTESIAN_POINT('Ctrl Pts',(184.517991753233,1.14703679694263,126.021736897372));
#23757=CARTESIAN_POINT('Ctrl Pts',(184.51024368523,1.01361122783021,125.989736880984));
#23758=CARTESIAN_POINT('Ctrl Pts',(184.502495617228,0.878881204667642,125.963333089485));
#23759=CARTESIAN_POINT('Ctrl Pts',(184.494747549225,0.743355387800147,125.94261136139));
#23760=CARTESIAN_POINT('Ctrl Pts',(184.486991246483,0.607685532481822,125.921867609995));
#23761=CARTESIAN_POINT('Ctrl Pts',(184.479234943741,0.471218581013933,125.906818044672));
#23762=CARTESIAN_POINT('Ctrl Pts',(184.471478640999,0.334469704435209,125.897496743429));
#23763=CARTESIAN_POINT('Ctrl Pts',(184.463718198485,0.197647840863254,125.888170467126));
#23764=CARTESIAN_POINT('Ctrl Pts',(184.455957755971,0.0605441429922865,
125.88457855716));
#23765=CARTESIAN_POINT('Ctrl Pts',(184.448197313456,-0.0763263789303934,
125.886702908211));
#23766=CARTESIAN_POINT('Ctrl Pts',(184.440424413191,-0.213416617565448,
125.888830669458));
#23767=CARTESIAN_POINT('Ctrl Pts',(184.432651512926,-0.350272541705855,
125.896693006356));
#23768=CARTESIAN_POINT('Ctrl Pts',(184.42487861266,-0.486383519863692,125.910219821256));
#23769=CARTESIAN_POINT('Ctrl Pts',(184.417388276898,-0.617546521122763,
125.923254902363));
#23770=CARTESIAN_POINT('Ctrl Pts',(184.409897941136,-0.748017492370623,
125.941549732693));
#23771=CARTESIAN_POINT('Ctrl Pts',(184.402407605374,-0.877350507831442,
125.964997110977));
#23772=CARTESIAN_POINT('Ctrl Pts',(184.394633271255,-1.01158722388324,125.989333503735));
#23773=CARTESIAN_POINT('Ctrl Pts',(184.386858937136,-1.14502321111271,126.019297965427));
#23774=CARTESIAN_POINT('Ctrl Pts',(184.379084603017,-1.27714959725893,126.054826748993));
#23775=CARTESIAN_POINT('Ctrl Pts',(184.37131985007,-1.40911314944234,126.090311746508));
#23776=CARTESIAN_POINT('Ctrl Pts',(184.363555097123,-1.53976993792535,126.131347320907));
#23777=CARTESIAN_POINT('Ctrl Pts',(184.355790344176,-1.66861912388403,126.177818357745));
#23778=CARTESIAN_POINT('Ctrl Pts',(184.348033303291,-1.79734033501496,126.224243238894));
#23779=CARTESIAN_POINT('Ctrl Pts',(184.340276262406,-1.92425715102514,126.276092707283));
#23780=CARTESIAN_POINT('Ctrl Pts',(184.332519221521,-2.04888214369525,126.333201369256));
#23781=CARTESIAN_POINT('Ctrl Pts',(184.32476803028,-2.17341315568864,126.390266965143));
#23782=CARTESIAN_POINT('Ctrl Pts',(184.31701683904,-2.29565543039551,126.452583698322));
#23783=CARTESIAN_POINT('Ctrl Pts',(184.3092656478,-2.41514017995914,126.51993755563));
#23784=CARTESIAN_POINT('Ctrl Pts',(184.301517751023,-2.5345741453172,126.587262785753));
#23785=CARTESIAN_POINT('Ctrl Pts',(184.293769854246,-2.65125257672636,126.659620690311));
#23786=CARTESIAN_POINT('Ctrl Pts',(184.286021957469,-2.76473022900649,126.736750775986));
#23787=CARTESIAN_POINT('Ctrl Pts',(184.278275681385,-2.87818414420808,126.81386472771));
#23788=CARTESIAN_POINT('Ctrl Pts',(184.270529405301,-2.98843828887982,126.895748655367));
#23789=CARTESIAN_POINT('Ctrl Pts',(184.262783129217,-3.09507576243218,126.982098317919));
#23790=CARTESIAN_POINT('Ctrl Pts',(184.255036795951,-3.20171402315806,127.068448617884));
#23791=CARTESIAN_POINT('Ctrl Pts',(184.247290462686,-3.30473525564962,127.159264472488));
#23792=CARTESIAN_POINT('Ctrl Pts',(184.239544129421,-3.40375538006029,127.254201131682));
#23793=CARTESIAN_POINT('Ctrl Pts',(184.231796061418,-3.50279767934135,127.349159051283));
#23794=CARTESIAN_POINT('Ctrl Pts',(184.224047993415,-3.59783680540671,127.448239341269));
#23795=CARTESIAN_POINT('Ctrl Pts',(184.216299925412,-3.6885255965423,127.551060449098));
#23796=CARTESIAN_POINT('Ctrl Pts',(184.20854362267,-3.77931077280425,127.653990836424));
#23797=CARTESIAN_POINT('Ctrl Pts',(184.200787319928,-3.86573611899577,127.760669689976));
#23798=CARTESIAN_POINT('Ctrl Pts',(184.193031017186,-3.94749450179272,127.870682001764));
#23799=CARTESIAN_POINT('Ctrl Pts',(184.185270574672,-4.02929652150032,127.980753030435));
#23800=CARTESIAN_POINT('Ctrl Pts',(184.177510132158,-4.10642639472572,128.094160739358));
#23801=CARTESIAN_POINT('Ctrl Pts',(184.169749689644,-4.17862097836977,128.210462049459));
#23802=CARTESIAN_POINT('Ctrl Pts',(184.161976789378,-4.25093145516856,128.326950056747));
#23803=CARTESIAN_POINT('Ctrl Pts',(184.154203889113,-4.31829061835359,128.446340606829));
#23804=CARTESIAN_POINT('Ctrl Pts',(184.146430988847,-4.38048143426836,128.568166201481));
#23805=CARTESIAN_POINT('Ctrl Pts',(184.138940653085,-4.44041145737599,128.685563128908));
#23806=CARTESIAN_POINT('Ctrl Pts',(184.131450317323,-4.49554224537381,128.805220854819));
#23807=CARTESIAN_POINT('Ctrl Pts',(184.123959981561,-4.54572295595053,128.926706264325));
#23808=CARTESIAN_POINT('Ctrl Pts',(184.115260747627,-4.60400255170544,129.067798737404));
#23809=CARTESIAN_POINT('Ctrl Pts',(184.106561513693,-4.65576212734771,129.211734291794));
#23810=CARTESIAN_POINT('Ctrl Pts',(184.097862279759,-4.70074664434197,129.357929130005));
#23811=CARTESIAN_POINT('Ctrl Pts',(184.093441289351,-4.72360798128571,129.432226014336));
#23812=CARTESIAN_POINT('Ctrl Pts',(184.089020298944,-4.74472023587179,129.507106006827));
#23813=CARTESIAN_POINT('Ctrl Pts',(184.084599308536,-4.76405452823405,129.582490119308));
#23814=CARTESIAN_POINT('Ctrl Pts',(185.834939443695,-4.76405452823405,129.582490119308));
#23815=CARTESIAN_POINT('Ctrl Pts',(185.82716587756,-4.79810227029313,129.71524174885));
#23816=CARTESIAN_POINT('Ctrl Pts',(185.819392311426,-4.82655888961819,129.849268541578));
#23817=CARTESIAN_POINT('Ctrl Pts',(185.811618745292,-4.84935969226982,129.984059674321));
#23818=CARTESIAN_POINT('Ctrl Pts',(185.805961071674,-4.8659543281669,130.082161912396));
#23819=CARTESIAN_POINT('Ctrl Pts',(185.800303398056,-4.87955412703471,130.180668865511));
#23820=CARTESIAN_POINT('Ctrl Pts',(185.794645724439,-4.8901515047038,130.279383167057));
#23821=CARTESIAN_POINT('Ctrl Pts',(185.784716961623,-4.90874905140923,130.45261883826));
#23822=CARTESIAN_POINT('Ctrl Pts',(185.774788198807,-4.91814347496568,130.626859993452));
#23823=CARTESIAN_POINT('Ctrl Pts',(185.764859435991,-4.91824909926368,130.801384026903));
#23824=CARTESIAN_POINT('',(186.110140564058,-4.91824801325411,130.808781321355));
#23825=CARTESIAN_POINT('Ctrl Pts',(186.18020938313,-4.76405452823405,129.582490119308));
#23826=CARTESIAN_POINT('Ctrl Pts',(186.17256993295,-4.79768574483935,129.713617722427));
#23827=CARTESIAN_POINT('Ctrl Pts',(186.164930482769,-4.82588839263014,129.846093738758));
#23828=CARTESIAN_POINT('Ctrl Pts',(186.157291032589,-4.84857298836732,129.979422414441));
#23829=CARTESIAN_POINT('Ctrl Pts',(186.149432621167,-4.87190776796963,130.116572544767));
#23830=CARTESIAN_POINT('Ctrl Pts',(186.141574209745,-4.88940334476083,130.254624496003));
#23831=CARTESIAN_POINT('Ctrl Pts',(186.133715798323,-4.90101953991361,130.393032850591));
#23832=CARTESIAN_POINT('Ctrl Pts',(186.125857386902,-4.9126357350664,130.531441205178));
#23833=CARTESIAN_POINT('Ctrl Pts',(186.11799897548,-4.91837257034282,130.67020550101));
#23834=CARTESIAN_POINT('Ctrl Pts',(186.110140564058,-4.91824801325411,130.808781321355));
#23835=CARTESIAN_POINT('Ctrl Pts',(186.110140564008,-4.91824801325332,130.808781322232));
#23836=CARTESIAN_POINT('Ctrl Pts',(186.099074116598,-4.91807260824191,131.003927891408));
#23837=CARTESIAN_POINT('Ctrl Pts',(186.088007669188,-4.90627932088814,131.198573828951));
#23838=CARTESIAN_POINT('Ctrl Pts',(186.076941221778,-4.88306599966,131.391599500359));
#23839=CARTESIAN_POINT('Ctrl Pts',(186.069128931883,-4.86667869954997,131.527864775596));
#23840=CARTESIAN_POINT('Ctrl Pts',(186.061316641987,-4.84460109965971,131.663323468629));
#23841=CARTESIAN_POINT('Ctrl Pts',(186.053504352092,-4.81691589639799,131.797589850688));
#23842=CARTESIAN_POINT('Ctrl Pts',(186.045730017973,-4.78936520086549,131.931203903559));
#23843=CARTESIAN_POINT('Ctrl Pts',(186.037955683854,-4.75620727242799,132.063882400062));
#23844=CARTESIAN_POINT('Ctrl Pts',(186.030181349735,-4.71751805131938,132.195118144231));
#23845=CARTESIAN_POINT('Ctrl Pts',(186.022416596788,-4.67887651121803,132.326192152075));
#23846=CARTESIAN_POINT('Ctrl Pts',(186.014651843841,-4.63471735138709,132.455826573993));
#23847=CARTESIAN_POINT('Ctrl Pts',(186.006887090894,-4.58516767187299,132.583523477821));
#23848=CARTESIAN_POINT('Ctrl Pts',(185.999130050009,-4.53566720579912,132.711093551284));
#23849=CARTESIAN_POINT('Ctrl Pts',(185.991373009124,-4.48078701513992,132.83672957411));
#23850=CARTESIAN_POINT('Ctrl Pts',(185.983615968239,-4.42070414285521,132.95994822744));
#23851=CARTESIAN_POINT('Ctrl Pts',(185.975864776998,-4.36066657953178,133.083073960625));
#23852=CARTESIAN_POINT('Ctrl Pts',(185.968113585758,-4.29543431449837,133.203785602808));
#23853=CARTESIAN_POINT('Ctrl Pts',(185.960362394518,-4.22523254890233,133.321619636856));
#23854=CARTESIAN_POINT('Ctrl Pts',(185.952614497741,-4.15506062092945,133.439403588296));
#23855=CARTESIAN_POINT('Ctrl Pts',(185.944866600964,-4.07992359302457,133.554312029003));
#23856=CARTESIAN_POINT('Ctrl Pts',(185.937118704187,-4.0000925681456,133.665906093138));
#23857=CARTESIAN_POINT('Ctrl Pts',(185.929372428103,-3.92027824219608,133.7774768142));
#23858=CARTESIAN_POINT('Ctrl Pts',(185.921626152019,-3.83577209961954,133.885734219918));
#23859=CARTESIAN_POINT('Ctrl Pts',(185.913879875934,-3.74688829830369,133.990268830703));
#23860=CARTESIAN_POINT('Ctrl Pts',(185.906133542669,-3.65800384086778,134.09480421314));
#23861=CARTESIAN_POINT('Ctrl Pts',(185.898387209404,-3.56474191346714,134.195616447958));
#23862=CARTESIAN_POINT('Ctrl Pts',(185.890640876138,-3.4674563837275,134.292329838968));
#23863=CARTESIAN_POINT('Ctrl Pts',(185.882892808135,-3.37014906756808,134.389064888271));
#23864=CARTESIAN_POINT('Ctrl Pts',(185.875144740132,-3.26881663328405,134.481698991651));
#23865=CARTESIAN_POINT('Ctrl Pts',(185.867396672129,-3.16384885446265,134.569894243576));
#23866=CARTESIAN_POINT('Ctrl Pts',(185.859640369388,-3.05876951463674,134.658183230465));
#23867=CARTESIAN_POINT('Ctrl Pts',(185.851884066646,-2.95004741195152,134.742023689953));
#23868=CARTESIAN_POINT('Ctrl Pts',(185.844127763904,-2.83810480523698,134.82111853621));
#23869=CARTESIAN_POINT('Ctrl Pts',(185.83636732139,-2.72610245138265,134.900255597768));
#23870=CARTESIAN_POINT('Ctrl Pts',(185.828606878875,-2.6108764967903,134.974641787181));
#23871=CARTESIAN_POINT('Ctrl Pts',(185.820846436361,-2.49287620764804,135.044024669804));
#23872=CARTESIAN_POINT('Ctrl Pts',(185.813073536096,-2.3746864939661,135.11351893199));
#23873=CARTESIAN_POINT('Ctrl Pts',(185.80530063583,-2.25371389122609,135.177993653395));
#23874=CARTESIAN_POINT('Ctrl Pts',(185.797527735565,-2.13043097123238,135.237243081529));
#23875=CARTESIAN_POINT('Ctrl Pts',(185.790037399803,-2.01162969591266,135.294338643711));
#23876=CARTESIAN_POINT('Ctrl Pts',(185.782547064041,-1.89068344157314,135.346582099913));
#23877=CARTESIAN_POINT('Ctrl Pts',(185.775056728279,-1.76802881817535,135.393833044828));
#23878=CARTESIAN_POINT('Ctrl Pts',(185.76728239416,-1.64072370745012,135.442875523682));
#23879=CARTESIAN_POINT('Ctrl Pts',(185.759508060041,-1.51117486044447,135.486694787618));
#23880=CARTESIAN_POINT('Ctrl Pts',(185.751733725922,-1.37985004303931,135.525080575499));
#23881=CARTESIAN_POINT('Ctrl Pts',(185.743968972975,-1.24868707173481,135.563419056326));
#23882=CARTESIAN_POINT('Ctrl Pts',(185.736204220028,-1.11575285660129,135.596337276052));
#23883=CARTESIAN_POINT('Ctrl Pts',(185.728439467081,-0.981535022751411,
135.623673023046));
#23884=CARTESIAN_POINT('Ctrl Pts',(185.720682426196,-0.847450495946294,
135.650981619791));
#23885=CARTESIAN_POINT('Ctrl Pts',(185.712925385311,-0.712085268171024,
135.672718700269));
#23886=CARTESIAN_POINT('Ctrl Pts',(185.705168344426,-0.575941665315386,
135.688771970089));
#23887=CARTESIAN_POINT('Ctrl Pts',(185.697417153186,-0.439900729409612,
135.704813134013));
#23888=CARTESIAN_POINT('Ctrl Pts',(185.689665961946,-0.303082973473198,
135.715178973112));
#23889=CARTESIAN_POINT('Ctrl Pts',(185.681914770705,-0.166000094317469,
135.719808413158));
#23890=CARTESIAN_POINT('Ctrl Pts',(185.674166873928,-0.0289754790421877,
135.724435885568));
#23891=CARTESIAN_POINT('Ctrl Pts',(185.666418977151,0.108313645407252,135.723331794998));
#23892=CARTESIAN_POINT('Ctrl Pts',(185.658671080374,0.245351511000205,135.716487010336));
#23893=CARTESIAN_POINT('Ctrl Pts',(185.65092480429,0.382360711225824,135.709643657456));
#23894=CARTESIAN_POINT('Ctrl Pts',(185.643178528206,0.519118366904536,135.697062018493));
#23895=CARTESIAN_POINT('Ctrl Pts',(185.635432252122,0.655110161251152,135.678785069655));
#23896=CARTESIAN_POINT('Ctrl Pts',(185.627685918857,0.791102959458301,135.660507985901));
#23897=CARTESIAN_POINT('Ctrl Pts',(185.619939585591,0.926329497570983,135.636535560459));
#23898=CARTESIAN_POINT('Ctrl Pts',(185.612193252326,1.06028241764848,135.606962439217));
#23899=CARTESIAN_POINT('Ctrl Pts',(185.604445184323,1.19426533555364,135.577382695279));
#23900=CARTESIAN_POINT('Ctrl Pts',(185.59669711632,1.32697368617402,135.542199844023));
#23901=CARTESIAN_POINT('Ctrl Pts',(185.588949048317,1.45791249787162,135.501559166813));
#23902=CARTESIAN_POINT('Ctrl Pts',(185.581192745575,1.58899047289653,135.460875296208));
#23903=CARTESIAN_POINT('Ctrl Pts',(185.573436442833,1.71829477813514,135.414722128319));
#23904=CARTESIAN_POINT('Ctrl Pts',(185.565680140092,1.84534722565303,135.363294339312));
#23905=CARTESIAN_POINT('Ctrl Pts',(185.557919697577,1.97246748488773,135.311839101746));
#23906=CARTESIAN_POINT('Ctrl Pts',(185.550159255063,2.09733313577467,135.25510379514));
#23907=CARTESIAN_POINT('Ctrl Pts',(185.542398812549,2.21948895854959,135.193329952772));
#23908=CARTESIAN_POINT('Ctrl Pts',(185.534625912284,2.34184087669565,135.131456945548));
#23909=CARTESIAN_POINT('Ctrl Pts',(185.526853012018,2.46147393253308,135.064529430542));
#23910=CARTESIAN_POINT('Ctrl Pts',(185.519080111753,2.57795958406316,134.992833781553));
#23911=CARTESIAN_POINT('Ctrl Pts',(185.511589775991,2.69021068875094,134.923744449994));
#23912=CARTESIAN_POINT('Ctrl Pts',(185.504099440229,2.79953899281448,134.850227805036));
#23913=CARTESIAN_POINT('Ctrl Pts',(185.496609104467,2.90559037094153,134.772575286506));
#23914=CARTESIAN_POINT('Ctrl Pts',(185.488834770348,3.01566271930338,134.691978549134));
#23915=CARTESIAN_POINT('Ctrl Pts',(185.481060436228,3.12255342329199,134.606670817637));
#23916=CARTESIAN_POINT('Ctrl Pts',(185.473286102109,3.22583274537233,134.516931985417));
#23917=CARTESIAN_POINT('Ctrl Pts',(185.465521349162,3.32898478491854,134.427303748286));
#23918=CARTESIAN_POINT('Ctrl Pts',(185.457756596215,3.42853400584439,134.333255530036));
#23919=CARTESIAN_POINT('Ctrl Pts',(185.449991843268,3.52408036162776,134.235109904134));
#23920=CARTESIAN_POINT('Ctrl Pts',(185.442234802383,3.61953181942352,134.137061757852));
#23921=CARTESIAN_POINT('Ctrl Pts',(185.434477761498,3.71098805294843,134.034924580939));
#23922=CARTESIAN_POINT('Ctrl Pts',(185.426720720613,3.79808306633545,133.92906029653));
#23923=CARTESIAN_POINT('Ctrl Pts',(185.418969529373,3.88511240069542,133.823275845201));
#23924=CARTESIAN_POINT('Ctrl Pts',(185.411218338133,3.96778681374832,133.713770181484));
#23925=CARTESIAN_POINT('Ctrl Pts',(185.403467146893,4.0457783373907,133.600940798287));
#23926=CARTESIAN_POINT('Ctrl Pts',(185.395719250116,4.12373671255506,133.488159370587));
#23927=CARTESIAN_POINT('Ctrl Pts',(185.387971353338,4.19701593512668,133.372057354035));
#23928=CARTESIAN_POINT('Ctrl Pts',(185.380223456561,4.2653295376257,133.253063743296));
#23929=CARTESIAN_POINT('Ctrl Pts',(185.372477180477,4.33362885039174,133.134095023454));
#23930=CARTESIAN_POINT('Ctrl Pts',(185.364730904393,4.39696441458693,133.01223625137));
#23931=CARTESIAN_POINT('Ctrl Pts',(185.356984628309,4.45509438652842,132.887943366012));
#23932=CARTESIAN_POINT('Ctrl Pts',(185.349238295044,4.51322478757213,132.763649563153));
#23933=CARTESIAN_POINT('Ctrl Pts',(185.341491961778,4.56614935405513,132.636921965314));
#23934=CARTESIAN_POINT('Ctrl Pts',(185.333745628513,4.61367347488339,132.508238585514));
#23935=CARTESIAN_POINT('Ctrl Pts',(185.32599756051,4.661208238409,132.379526387963));
#23936=CARTESIAN_POINT('Ctrl Pts',(185.318249492507,4.70334001430907,132.248857903597));
#23937=CARTESIAN_POINT('Ctrl Pts',(185.310501424504,4.73992348764949,132.116728094201));
#23938=CARTESIAN_POINT('Ctrl Pts',(185.302745121762,4.77654584234074,131.98445785567));
#23939=CARTESIAN_POINT('Ctrl Pts',(185.29498881902,4.80760801048513,131.850723566987));
#23940=CARTESIAN_POINT('Ctrl Pts',(185.287232516278,4.83301530639473,131.716032768426));
#23941=CARTESIAN_POINT('Ctrl Pts',(185.279472073764,4.85843616294317,131.581270081331));
#23942=CARTESIAN_POINT('Ctrl Pts',(185.27171163125,4.87819607698591,131.445550253803));
#23943=CARTESIAN_POINT('Ctrl Pts',(185.263951188736,4.8922521999072,131.30938682976));
#23944=CARTESIAN_POINT('Ctrl Pts',(185.25617828847,4.90633088696485,131.173004824101));
#23945=CARTESIAN_POINT('Ctrl Pts',(185.248405388205,4.91468746198499,131.036178189385));
#23946=CARTESIAN_POINT('Ctrl Pts',(185.24063248794,4.91733122193595,130.899422262165));
#23947=CARTESIAN_POINT('Ctrl Pts',(185.233142152178,4.91987887455347,130.767637757367));
#23948=CARTESIAN_POINT('Ctrl Pts',(185.225651816415,4.91712185788959,130.635919216476));
#23949=CARTESIAN_POINT('Ctrl Pts',(185.218161480653,4.90911395514333,130.504722105494));
#23950=CARTESIAN_POINT('Ctrl Pts',(185.210387146534,4.90080243033051,130.368550616171));
#23951=CARTESIAN_POINT('Ctrl Pts',(185.202612812415,4.8868076562378,130.232509526972));
#23952=CARTESIAN_POINT('Ctrl Pts',(185.194838478296,4.86713283147692,130.097111677475));
#23953=CARTESIAN_POINT('Ctrl Pts',(185.187073725349,4.84748225417918,129.961880693727));
#23954=CARTESIAN_POINT('Ctrl Pts',(185.179308972402,4.82216561011635,129.827291755562));
#23955=CARTESIAN_POINT('Ctrl Pts',(185.171544219455,4.79123805456728,129.693855792288));
#23956=CARTESIAN_POINT('Ctrl Pts',(185.16378717857,4.76034121670238,129.560552359494));
#23957=CARTESIAN_POINT('Ctrl Pts',(185.156030137685,4.72384464525298,129.428400001093));
#23958=CARTESIAN_POINT('Ctrl Pts',(185.1482730968,4.68185500669668,129.297902268069));
#23959=CARTESIAN_POINT('Ctrl Pts',(185.14052190556,4.63989703285347,129.167502944401));
#23960=CARTESIAN_POINT('Ctrl Pts',(185.13277071432,4.59245435629693,129.038756133175));
#23961=CARTESIAN_POINT('Ctrl Pts',(185.12501952308,4.53968412429643,128.912152617871));
#23962=CARTESIAN_POINT('Ctrl Pts',(185.117271626302,4.48693632105218,128.785602912438));
#23963=CARTESIAN_POINT('Ctrl Pts',(185.109523729525,4.42886561609171,128.661195051217));
#23964=CARTESIAN_POINT('Ctrl Pts',(185.101775832748,4.36567809210519,128.539401929507));
#23965=CARTESIAN_POINT('Ctrl Pts',(185.094029556664,4.30250378558652,128.417634284293));
#23966=CARTESIAN_POINT('Ctrl Pts',(185.08628328058,4.23421496891706,128.298480637502));
#23967=CARTESIAN_POINT('Ctrl Pts',(185.078537004496,4.16106451404611,128.182390905223));
#23968=CARTESIAN_POINT('Ctrl Pts',(185.070790671231,4.08791351919513,128.066300315995));
#23969=CARTESIAN_POINT('Ctrl Pts',(185.063044337965,4.00990102295931,127.953274017186));
#23970=CARTESIAN_POINT('Ctrl Pts',(185.0552980047,3.92732399917947,127.843734118332));
#23971=CARTESIAN_POINT('Ctrl Pts',(185.047549936697,3.84472848284773,127.734169688777));
#23972=CARTESIAN_POINT('Ctrl Pts',(185.039801868694,3.75756664022695,127.628093524923));
#23973=CARTESIAN_POINT('Ctrl Pts',(185.032053800691,3.66617635041229,127.525895423275));
#23974=CARTESIAN_POINT('Ctrl Pts',(185.024297497949,3.57468892991002,127.423588704268));
#23975=CARTESIAN_POINT('Ctrl Pts',(185.016541195207,3.47896434590667,127.325168572807));
#23976=CARTESIAN_POINT('Ctrl Pts',(185.008784892466,3.37937842648236,127.230989028559));
#23977=CARTESIAN_POINT('Ctrl Pts',(185.001024449951,3.27973935505435,127.136759217851));
#23978=CARTESIAN_POINT('Ctrl Pts',(184.993264007437,3.17623513657302,127.046774760618));
#23979=CARTESIAN_POINT('Ctrl Pts',(184.985503564923,3.06927466935573,126.961349289642));
#23980=CARTESIAN_POINT('Ctrl Pts',(184.977730664658,2.96214249970095,126.875786686117));
#23981=CARTESIAN_POINT('Ctrl Pts',(184.969957764392,2.85154330970152,126.794797924641));
#23982=CARTESIAN_POINT('Ctrl Pts',(184.962184864127,2.73791569183312,126.718653735408));
#23983=CARTESIAN_POINT('Ctrl Pts',(184.954694528365,2.62841872408481,126.645277579249));
#23984=CARTESIAN_POINT('Ctrl Pts',(184.947204192603,2.51610995032003,126.576400046695));
#23985=CARTESIAN_POINT('Ctrl Pts',(184.939713856841,2.40140163811663,126.512222078918));
#23986=CARTESIAN_POINT('Ctrl Pts',(184.931939522722,2.28234412539138,126.445610783985));
#23987=CARTESIAN_POINT('Ctrl Pts',(184.924165188603,2.16032438692566,126.383851452082));
#23988=CARTESIAN_POINT('Ctrl Pts',(184.916390854484,2.03577561811003,126.327218594444));
#23989=CARTESIAN_POINT('Ctrl Pts',(184.908626101536,1.91138034452076,126.270655531741));
#23990=CARTESIAN_POINT('Ctrl Pts',(184.900861348589,1.78446259457604,126.2192065328));
#23991=CARTESIAN_POINT('Ctrl Pts',(184.893096595642,1.65548204034892,126.173101363693));
#23992=CARTESIAN_POINT('Ctrl Pts',(184.885339554757,1.5266295914267,126.12704198689));
#23993=CARTESIAN_POINT('Ctrl Pts',(184.877582513872,1.3957187812083,126.086316008371));
#23994=CARTESIAN_POINT('Ctrl Pts',(184.869825472987,1.26323091723401,126.051105868213));
#23995=CARTESIAN_POINT('Ctrl Pts',(184.862074281747,1.13084296338832,126.015922280296));
#23996=CARTESIAN_POINT('Ctrl Pts',(184.854323090507,0.996880699273993,125.986246351446));
#23997=CARTESIAN_POINT('Ctrl Pts',(184.846571899267,0.861841976869711,125.962211149674));
#23998=CARTESIAN_POINT('Ctrl Pts',(184.83882400249,0.726860649524842,125.938186163504));
#23999=CARTESIAN_POINT('Ctrl Pts',(184.831076105713,0.590804157979271,125.919797204415));
#24000=CARTESIAN_POINT('Ctrl Pts',(184.823328208936,0.454181755168668,125.907126500662));
#24001=CARTESIAN_POINT('Ctrl Pts',(184.815581932852,0.317587930819519,125.894458447347));
#24002=CARTESIAN_POINT('Ctrl Pts',(184.807835656767,0.180428819710515,125.88750630627));
#24003=CARTESIAN_POINT('Ctrl Pts',(184.800089380683,0.0432196324551924,
125.886300519736));
#24004=CARTESIAN_POINT('Ctrl Pts',(184.792343047418,-0.0939905676472747,
125.8850947243));
#24005=CARTESIAN_POINT('Ctrl Pts',(184.784596714153,-0.231250453683563,
125.889635371485));
#24006=CARTESIAN_POINT('Ctrl Pts',(184.776850380887,-0.368044371329767,
125.899900769302));
#24007=CARTESIAN_POINT('Ctrl Pts',(184.769102312884,-0.504868923025204,
125.910168465984));
#24008=CARTESIAN_POINT('Ctrl Pts',(184.761354244881,-0.641226908890993,
125.926163435116));
#24009=CARTESIAN_POINT('Ctrl Pts',(184.753606176878,-0.77660775018482,125.947812103976));
#24010=CARTESIAN_POINT('Ctrl Pts',(184.745849874136,-0.912132475847942,
125.969483781299));
#24011=CARTESIAN_POINT('Ctrl Pts',(184.738093571395,-1.04667759570581,125.996821099783));
#24012=CARTESIAN_POINT('Ctrl Pts',(184.730337268653,-1.17974213555564,126.029699210084));
#24013=CARTESIAN_POINT('Ctrl Pts',(184.722576826139,-1.312877695957,126.062594868424));
#24014=CARTESIAN_POINT('Ctrl Pts',(184.714816383624,-1.44453072664021,126.101037101697));
#24015=CARTESIAN_POINT('Ctrl Pts',(184.70705594111,-1.57421633993268,126.144851418349));
#24016=CARTESIAN_POINT('Ctrl Pts',(184.699283040845,-1.70411013608448,126.188736069632));
#24017=CARTESIAN_POINT('Ctrl Pts',(184.691510140579,-1.83202983856468,126.238009896672));
#24018=CARTESIAN_POINT('Ctrl Pts',(184.683737240314,-1.95751060444897,126.292450235481));
#24019=CARTESIAN_POINT('Ctrl Pts',(184.676246904552,-2.07842982842536,126.344911530846));
#24020=CARTESIAN_POINT('Ctrl Pts',(184.66875656879,-2.19708408278854,126.402170094191));
#24021=CARTESIAN_POINT('Ctrl Pts',(184.661266233028,-2.31308146934551,126.463987686737));
#24022=CARTESIAN_POINT('Ctrl Pts',(184.653490953882,-2.43349156701393,126.528156911382));
#24023=CARTESIAN_POINT('Ctrl Pts',(184.645715674736,-2.55142012255629,126.597442189508));
#24024=CARTESIAN_POINT('Ctrl Pts',(184.63794039559,-2.66640186075916,126.671627359849));
#24025=CARTESIAN_POINT('Ctrl Pts',(184.630174906103,-2.78123882835338,126.745719125512));
#24026=CARTESIAN_POINT('Ctrl Pts',(184.622409416615,-2.89313603609128,126.824698297011));
#24027=CARTESIAN_POINT('Ctrl Pts',(184.614643927127,-3.00165158969343,126.908302250884));
#24028=CARTESIAN_POINT('Ctrl Pts',(184.606887744613,-3.11003708692624,126.99180600505));
#24029=CARTESIAN_POINT('Ctrl Pts',(184.599131562098,-3.21504869422354,127.079923265202));
#24030=CARTESIAN_POINT('Ctrl Pts',(184.591375379584,-3.31627290310998,127.172347801702));
#24031=CARTESIAN_POINT('Ctrl Pts',(184.583624474521,-3.41742823714848,127.264709450816));
#24032=CARTESIAN_POINT('Ctrl Pts',(184.575873569458,-3.51480101205282,127.361372283403));
#24033=CARTESIAN_POINT('Ctrl Pts',(184.568122664396,-3.60801021796009,127.461989403952));
#24034=CARTESIAN_POINT('Ctrl Pts',(184.560375354587,-3.70117618882434,127.562559853301));
#24035=CARTESIAN_POINT('Ctrl Pts',(184.552628044778,-3.79018216867158,127.66708065461));
#24036=CARTESIAN_POINT('Ctrl Pts',(184.544880734968,-3.87468379235378,127.77516789148));
#24037=CARTESIAN_POINT('Ctrl Pts',(184.537135340988,-3.9591645196716,127.883228399511));
#24038=CARTESIAN_POINT('Ctrl Pts',(184.529389947007,-4.03914286792834,127.994853279576));
#24039=CARTESIAN_POINT('Ctrl Pts',(184.521644553026,-4.11431484242556,128.10962566958));
#24040=CARTESIAN_POINT('Ctrl Pts',(184.513896696704,-4.18951071487447,128.22443454692));
#24041=CARTESIAN_POINT('Ctrl Pts',(184.506148840382,-4.25989694066962,128.342392609911));
#24042=CARTESIAN_POINT('Ctrl Pts',(184.49840098406,-4.32521289149947,128.463054036679));
#24043=CARTESIAN_POINT('Ctrl Pts',(184.49065211975,-4.39053733987044,128.583731161379));
#24044=CARTESIAN_POINT('Ctrl Pts',(184.482903255439,-4.45079002018339,128.707112002701));
#24045=CARTESIAN_POINT('Ctrl Pts',(184.475154391129,-4.50575679107406,128.832727081082));
#24046=CARTESIAN_POINT('Ctrl Pts',(184.467398393862,-4.56077415977317,128.958457790189));
#24047=CARTESIAN_POINT('Ctrl Pts',(184.459642396596,-4.61049574662458,129.086426484169));
#24048=CARTESIAN_POINT('Ctrl Pts',(184.451886399329,-4.65475582965104,129.216144250433));
#24049=CARTESIAN_POINT('Ctrl Pts',(184.44466748376,-4.6959510224118,129.336879414498));
#24050=CARTESIAN_POINT('Ctrl Pts',(184.437448568192,-4.73241533402233,129.459129381269));
#24051=CARTESIAN_POINT('Ctrl Pts',(184.430229652623,-4.76405452823406,129.582490119308));
#24052=CARTESIAN_POINT('Origin',(213.235140564004,0.,130.804360617566));
#24053=CARTESIAN_POINT('',(182.334764431275,-4.76405452823405,129.582490119308));
#24054=CARTESIAN_POINT('',(182.679902359578,-4.76405452823405,129.582490119308));
#24055=CARTESIAN_POINT('',(213.235140564004,-4.76405452823405,129.582490119308));
#24056=CARTESIAN_POINT('',(184.014859436043,-4.9182492280365,130.801605001777));
#24057=CARTESIAN_POINT('Ctrl Pts',(184.014859435991,-4.91824922803702,130.801605002707));
#24058=CARTESIAN_POINT('Ctrl Pts',(184.0070245266,-4.91832708928895,130.94057255142));
#24059=CARTESIAN_POINT('Ctrl Pts',(183.999189617208,-4.91251071226177,131.079545490942));
#24060=CARTESIAN_POINT('Ctrl Pts',(183.991354707817,-4.90082530395939,131.217996209085));
#24061=CARTESIAN_POINT('Ctrl Pts',(183.983518210813,-4.88913752780615,131.356474981931));
#24062=CARTESIAN_POINT('Ctrl Pts',(183.97568171381,-4.87157838318562,131.494430945472));
#24063=CARTESIAN_POINT('Ctrl Pts',(183.967845216806,-4.84822496807564,131.631341706484));
#24064=CARTESIAN_POINT('Ctrl Pts',(183.960005585196,-4.82486221157711,131.768307231932));
#24065=CARTESIAN_POINT('Ctrl Pts',(183.952165953587,-4.79570063209204,131.904226349297));
#24066=CARTESIAN_POINT('Ctrl Pts',(183.944326321977,-4.76086839271114,132.038587180959));
#24067=CARTESIAN_POINT('Ctrl Pts',(183.936091824958,-4.72428172823233,132.179715479181));
#24068=CARTESIAN_POINT('Ctrl Pts',(183.927857327939,-4.68143846664776,132.319123983606));
#24069=CARTESIAN_POINT('Ctrl Pts',(183.91962283092,-4.63254572439523,132.456239297702));
#24070=CARTESIAN_POINT('Ctrl Pts',(183.911767314248,-4.58590319711227,132.58704408557));
#24071=CARTESIAN_POINT('Ctrl Pts',(183.903911797577,-4.53375578798978,132.71576172528));
#24072=CARTESIAN_POINT('Ctrl Pts',(183.896056280906,-4.47633184758892,132.84191705918));
#24073=CARTESIAN_POINT('Ctrl Pts',(183.888194193542,-4.41885987532938,132.968177914837));
#24074=CARTESIAN_POINT('Ctrl Pts',(183.880332106178,-4.35610274681267,133.09187185747));
#24075=CARTESIAN_POINT('Ctrl Pts',(183.872470018814,-4.28833398097888,133.212549715225));
#24076=CARTESIAN_POINT('Ctrl Pts',(183.864595817316,-4.2204607950577,133.333413516936));
#24077=CARTESIAN_POINT('Ctrl Pts',(183.856721615819,-4.14756075301982,133.451251635519));
#24078=CARTESIAN_POINT('Ctrl Pts',(183.848847414322,-4.06995003088787,133.565644704468));
#24079=CARTESIAN_POINT('Ctrl Pts',(183.847735728798,-4.05899289239229,133.58179480158));
#24080=CARTESIAN_POINT('Ctrl Pts',(183.846624043273,-4.04794192437879,133.597876287981));
#24081=CARTESIAN_POINT('Ctrl Pts',(183.845512357748,-4.03679807846351,133.613888039787));
#24082=CARTESIAN_POINT('Ctrl Pts',(183.837738023629,-3.95886598381865,133.7258627895));
#24083=CARTESIAN_POINT('Ctrl Pts',(183.82996368951,-3.87614790100592,133.834769861943));
#24084=CARTESIAN_POINT('Ctrl Pts',(183.822189355391,-3.78891333030926,133.940172926666));
#24085=CARTESIAN_POINT('Ctrl Pts',(183.814424602444,-3.70178626842471,134.045446091532));
#24086=CARTESIAN_POINT('Ctrl Pts',(183.806659849497,-3.61015404055219,134.147223542661));
#24087=CARTESIAN_POINT('Ctrl Pts',(183.79889509655,-3.51432952725466,134.245097607858));
#24088=CARTESIAN_POINT('Ctrl Pts',(183.791138055665,-3.41860018821441,134.342874463155));
#24089=CARTESIAN_POINT('Ctrl Pts',(183.78338101478,-3.31868712171636,134.436755370167));
#24090=CARTESIAN_POINT('Ctrl Pts',(183.775623973895,-3.21494336377899,134.526365753268));
#24091=CARTESIAN_POINT('Ctrl Pts',(183.767872782655,-3.11127783981671,134.615908560482));
#24092=CARTESIAN_POINT('Ctrl Pts',(183.760121591415,-3.00378766898042,134.701186999335));
#24093=CARTESIAN_POINT('Ctrl Pts',(183.752370400174,-2.89286235937896,134.781863657438));
#24094=CARTESIAN_POINT('Ctrl Pts',(183.744622503397,-2.7819841959931,134.862506025808));
#24095=CARTESIAN_POINT('Ctrl Pts',(183.73687460662,-2.66767411324236,134.938550274043));
#24096=CARTESIAN_POINT('Ctrl Pts',(183.729126709843,-2.55035410782106,135.009699722468));
#24097=CARTESIAN_POINT('Ctrl Pts',(183.721380433759,-2.43305864321574,135.080834287963));
#24098=CARTESIAN_POINT('Ctrl Pts',(183.713634157675,-2.31275484235268,135.147075887609));
#24099=CARTESIAN_POINT('Ctrl Pts',(183.705887881591,-2.18989270931988,135.20817180609));
#24100=CARTESIAN_POINT('Ctrl Pts',(183.698141548325,-2.06702966934689,135.269268175567));
#24101=CARTESIAN_POINT('Ctrl Pts',(183.69039521506,-1.94160860959151,135.325218614004));
#24102=CARTESIAN_POINT('Ctrl Pts',(183.682648881795,-1.81410273528698,135.375817095356));
#24103=CARTESIAN_POINT('Ctrl Pts',(183.674900813792,-1.68656830692579,135.426426907886));
#24104=CARTESIAN_POINT('Ctrl Pts',(183.667152745789,-1.55694849830684,135.471682234208));
#24105=CARTESIAN_POINT('Ctrl Pts',(183.659404677786,-1.4257346415192,135.511425923515));
#24106=CARTESIAN_POINT('Ctrl Pts',(183.651648375044,-1.29438132908304,135.551211852889));
#24107=CARTESIAN_POINT('Ctrl Pts',(183.643892072302,-1.1614309589586,135.585474330078));
#24108=CARTESIAN_POINT('Ctrl Pts',(183.63613576956,-1.02738865306596,135.614106517097));
#24109=CARTESIAN_POINT('Ctrl Pts',(183.628375327046,-0.893274804758753,
135.642753985975));
#24110=CARTESIAN_POINT('Ctrl Pts',(183.620614884532,-0.758068244641496,
135.665765111291));
#24111=CARTESIAN_POINT('Ctrl Pts',(183.612854442018,-0.622281340493539,
135.683084733129));
#24112=CARTESIAN_POINT('Ctrl Pts',(183.605081541752,-0.486276459152402,
135.700432157962));
#24113=CARTESIAN_POINT('Ctrl Pts',(183.597308641487,-0.349689761885385,
135.712069788455));
#24114=CARTESIAN_POINT('Ctrl Pts',(183.589535741221,-0.213036659942975,
135.717994552244));
#24115=CARTESIAN_POINT('Ctrl Pts',(183.582045405459,-0.0813512424637309,
135.723703935946));
#24116=CARTESIAN_POINT('Ctrl Pts',(183.574555069697,0.0503955275397817,
135.724108595028));
#24117=CARTESIAN_POINT('Ctrl Pts',(183.567064733935,0.181747024582314,135.719251367273));
#24118=CARTESIAN_POINT('Ctrl Pts',(183.559290399816,0.318078753557754,135.714209976251));
#24119=CARTESIAN_POINT('Ctrl Pts',(183.551516065697,0.45441650227473,135.703483843342));
#24120=CARTESIAN_POINT('Ctrl Pts',(183.543741731578,0.590247502080792,135.687063859499));
#24121=CARTESIAN_POINT('Ctrl Pts',(183.535976978631,0.725911102318697,135.67066411182));
#24122=CARTESIAN_POINT('Ctrl Pts',(183.528212225684,0.861068811846414,135.648584521738));
#24123=CARTESIAN_POINT('Ctrl Pts',(183.520447472737,0.995208524915738,135.620867967756));
#24124=CARTESIAN_POINT('Ctrl Pts',(183.512690431852,1.12921500853146,135.593178942246));
#24125=CARTESIAN_POINT('Ctrl Pts',(183.504933390967,1.26220512740057,135.559864173125));
#24126=CARTESIAN_POINT('Ctrl Pts',(183.497176350082,1.39367291584853,135.521018212318));
#24127=CARTESIAN_POINT('Ctrl Pts',(183.489425158842,1.52504156341419,135.482201545552));
#24128=CARTESIAN_POINT('Ctrl Pts',(183.481673967602,1.65488979216254,135.43786209979));
#24129=CARTESIAN_POINT('Ctrl Pts',(183.473922776362,1.78272318884635,135.388145199595));
#24130=CARTESIAN_POINT('Ctrl Pts',(183.466174879585,1.91050225292687,135.33844943041));
#24131=CARTESIAN_POINT('Ctrl Pts',(183.458426982807,2.0362678245576,135.283380894017));
#24132=CARTESIAN_POINT('Ctrl Pts',(183.45067908603,2.15954219920582,135.223134265576));
#24133=CARTESIAN_POINT('Ctrl Pts',(183.442932809946,2.28279078751236,135.162900239432));
#24134=CARTESIAN_POINT('Ctrl Pts',(183.435186533862,2.40354886430429,135.097490447235));
#24135=CARTESIAN_POINT('Ctrl Pts',(183.427440257778,2.52136057482751,135.027146891367));
#24136=CARTESIAN_POINT('Ctrl Pts',(183.419693924513,2.63917315501009,134.95680281624));
#24137=CARTESIAN_POINT('Ctrl Pts',(183.411947591247,2.7540389898437,134.881525105199));
#24138=CARTESIAN_POINT('Ctrl Pts',(183.404201257982,2.86552896479428,134.8016005171));
#24139=CARTESIAN_POINT('Ctrl Pts',(183.396453189979,2.97704390715139,134.721658030443));
#24140=CARTESIAN_POINT('Ctrl Pts',(183.388705121976,3.08518116758142,134.637066823728));
#24141=CARTESIAN_POINT('Ctrl Pts',(183.380957053973,3.18954295366573,134.548155324708));
#24142=CARTESIAN_POINT('Ctrl Pts',(183.373200751231,3.29401565669837,134.459149329488));
#24143=CARTESIAN_POINT('Ctrl Pts',(183.36544444849,3.3947045716674,134.36581412358));
#24144=CARTESIAN_POINT('Ctrl Pts',(183.357688145748,3.49124678201167,134.268516931821));
#24145=CARTESIAN_POINT('Ctrl Pts',(183.349927703234,3.58784051984049,134.171167809621));
#24146=CARTESIAN_POINT('Ctrl Pts',(183.342167260719,3.68028287962462,134.069852776656));
#24147=CARTESIAN_POINT('Ctrl Pts',(183.334406818205,3.76825050646584,133.964973087171));
#24148=CARTESIAN_POINT('Ctrl Pts',(183.32663391794,3.85635934675105,133.859925035496));
#24149=CARTESIAN_POINT('Ctrl Pts',(183.318861017674,3.93997886106847,133.751301202296));
#24150=CARTESIAN_POINT('Ctrl Pts',(183.311088117409,4.01882787217965,133.639533556964));
#24151=CARTESIAN_POINT('Ctrl Pts',(183.303597781647,4.094810523129,133.531828947063));
#24152=CARTESIAN_POINT('Ctrl Pts',(183.296107445885,4.16636332155617,133.421205386315));
#24153=CARTESIAN_POINT('Ctrl Pts',(183.288617110123,4.23327549087247,133.308070201539));
#24154=CARTESIAN_POINT('Ctrl Pts',(183.280842776004,4.3027246554253,133.190645461847));
#24155=CARTESIAN_POINT('Ctrl Pts',(183.273068441885,4.36739433944492,133.070142915728));
#24156=CARTESIAN_POINT('Ctrl Pts',(183.265294107765,4.42699971525186,132.94698904631));
#24157=CARTESIAN_POINT('Ctrl Pts',(183.257529354818,4.48653163276008,132.823986953029));
#24158=CARTESIAN_POINT('Ctrl Pts',(183.249764601871,4.5410114917085,132.698340386375));
#24159=CARTESIAN_POINT('Ctrl Pts',(183.241999848924,4.59019856132849,132.570503372294));
#24160=CARTESIAN_POINT('Ctrl Pts',(183.234242808039,4.63933677765773,132.442793327737));
#24161=CARTESIAN_POINT('Ctrl Pts',(183.226485767154,4.6831925265859,132.312897527787));
#24162=CARTESIAN_POINT('Ctrl Pts',(183.218728726269,4.72157187051949,132.181292763323));
#24163=CARTESIAN_POINT('Ctrl Pts',(183.210977535029,4.75992227229126,132.049787243035));
#24164=CARTESIAN_POINT('Ctrl Pts',(183.203226343789,4.79280438017088,131.91657569721));
#24165=CARTESIAN_POINT('Ctrl Pts',(183.195475152549,4.82007321739351,131.782152641192));
#24166=CARTESIAN_POINT('Ctrl Pts',(183.187727255772,4.84733046463286,131.647786718558));
#24167=CARTESIAN_POINT('Ctrl Pts',(183.179979358994,4.86897910880454,131.512210692235));
#24168=CARTESIAN_POINT('Ctrl Pts',(183.172231462217,4.88492472466578,131.375931695254));
#24169=CARTESIAN_POINT('Ctrl Pts',(183.164485186133,4.90086700504792,131.239681204901));
#24170=CARTESIAN_POINT('Ctrl Pts',(183.156738910049,4.91110858455677,131.102728424444));
#24171=CARTESIAN_POINT('Ctrl Pts',(183.148992633965,4.91560666602142,130.965587685597));
#24172=CARTESIAN_POINT('Ctrl Pts',(183.1412463007,4.92010478068989,130.828445934408));
#24173=CARTESIAN_POINT('Ctrl Pts',(183.133499967434,4.91885929989721,130.691116612814));
#24174=CARTESIAN_POINT('Ctrl Pts',(183.125753634169,4.91187953510186,130.554115747194));
#24175=CARTESIAN_POINT('Ctrl Pts',(183.118005566166,4.90489820723658,130.417084201179));
#24176=CARTESIAN_POINT('Ctrl Pts',(183.110257498163,4.89218005994142,130.280381647888));
#24177=CARTESIAN_POINT('Ctrl Pts',(183.10250943016,4.87378639226766,130.144520284571));
#24178=CARTESIAN_POINT('Ctrl Pts',(183.094753127418,4.85537317558499,130.00851452618));
#24179=CARTESIAN_POINT('Ctrl Pts',(183.086996824676,4.83127244146896,129.873352131727));
#24180=CARTESIAN_POINT('Ctrl Pts',(183.079240521934,4.80159698130756,129.739536927184));
#24181=CARTESIAN_POINT('Ctrl Pts',(183.07148007942,4.77190568245958,129.605650301438));
#24182=CARTESIAN_POINT('Ctrl Pts',(183.063719636906,4.73663382932912,129.473112675974));
#24183=CARTESIAN_POINT('Ctrl Pts',(183.055959194392,4.69594422725383,129.342412986144));
#24184=CARTESIAN_POINT('Ctrl Pts',(183.048186294126,4.65518930661703,129.211503485568));
#24185=CARTESIAN_POINT('Ctrl Pts',(183.040413393861,4.6089993893674,129.082438184816));
#24186=CARTESIAN_POINT('Ctrl Pts',(183.032640493595,4.55758592042437,128.955687136269));
#24187=CARTESIAN_POINT('Ctrl Pts',(183.025150157833,4.50804146058063,128.833543807605));
#24188=CARTESIAN_POINT('Ctrl Pts',(183.017659822071,4.453646761226,128.713549675095));
#24189=CARTESIAN_POINT('Ctrl Pts',(183.010169486309,4.39463058805635,128.596102241148));
#24190=CARTESIAN_POINT('Ctrl Pts',(183.00239515219,4.33337679874275,128.474201752045));
#24191=CARTESIAN_POINT('Ctrl Pts',(182.994620818071,4.26695013774061,128.354658745723));
#24192=CARTESIAN_POINT('Ctrl Pts',(182.986846483952,4.19555546106626,128.237943380323));
#24193=CARTESIAN_POINT('Ctrl Pts',(182.979081731005,4.1242487719503,128.121371856181));
#24194=CARTESIAN_POINT('Ctrl Pts',(182.971316978058,4.0479864514346,128.007621369533));
#24195=CARTESIAN_POINT('Ctrl Pts',(182.963552225111,3.96702036354612,127.897139866108));
#24196=CARTESIAN_POINT('Ctrl Pts',(182.955795184226,3.88613469231738,127.786768094469));
#24197=CARTESIAN_POINT('Ctrl Pts',(182.948038143341,3.80055478051184,127.679659158082));
#24198=CARTESIAN_POINT('Ctrl Pts',(182.940281102456,3.71057693779105,127.576233939253));
#24199=CARTESIAN_POINT('Ctrl Pts',(182.932529911216,3.62066694806208,127.472886714187));
#24200=CARTESIAN_POINT('Ctrl Pts',(182.924778719976,3.52636588431209,127.373217971168));
#24201=CARTESIAN_POINT('Ctrl Pts',(182.917027528736,3.42801143282299,127.277616980876));
#24202=CARTESIAN_POINT('Ctrl Pts',(182.909279631959,3.3296987845988,127.182056623554));
#24203=CARTESIAN_POINT('Ctrl Pts',(182.901531735182,3.22733645491275,127.090560852235));
#24204=CARTESIAN_POINT('Ctrl Pts',(182.893783838404,3.12130006999723,127.003483227339));
#24205=CARTESIAN_POINT('Ctrl Pts',(182.88603756232,3.01528586560767,126.916423817206));
#24206=CARTESIAN_POINT('Ctrl Pts',(182.878291286236,2.90559943659399,126.833780963214));
#24207=CARTESIAN_POINT('Ctrl Pts',(182.870545010152,2.79265037187774,126.75586868069));
#24208=CARTESIAN_POINT('Ctrl Pts',(182.862798676887,2.67970047339745,126.677955823035));
#24209=CARTESIAN_POINT('Ctrl Pts',(182.855052343622,2.5634882129824,126.604773828524));
#24210=CARTESIAN_POINT('Ctrl Pts',(182.847306010356,2.4444527713082,126.536593788023));
#24211=CARTESIAN_POINT('Ctrl Pts',(182.839557942353,2.32539067247181,126.468398479076));
#24212=CARTESIAN_POINT('Ctrl Pts',(182.83180987435,2.2035044734996,126.405207547392));
#24213=CARTESIAN_POINT('Ctrl Pts',(182.824061806347,2.07925823407926,126.34724627547));
#24214=CARTESIAN_POINT('Ctrl Pts',(182.816305503605,1.9548799442771,126.289223401619));
#24215=CARTESIAN_POINT('Ctrl Pts',(182.808549200864,1.82813695834241,126.236441456072));
#24216=CARTESIAN_POINT('Ctrl Pts',(182.800792898122,1.69951412583694,126.189077874485));
#24217=CARTESIAN_POINT('Ctrl Pts',(182.793032455608,1.57082264345299,126.141689013529));
#24218=CARTESIAN_POINT('Ctrl Pts',(182.785272013093,1.44024968730915,126.099724398543));
#24219=CARTESIAN_POINT('Ctrl Pts',(182.777511570579,1.3082946128271,126.063311338287));
#24220=CARTESIAN_POINT('Ctrl Pts',(182.769738670314,1.17612771234498,126.026839824555));
#24221=CARTESIAN_POINT('Ctrl Pts',(182.761965770048,1.04257464097785,125.995937762452));
#24222=CARTESIAN_POINT('Ctrl Pts',(182.754192869783,0.908145158251714,125.970681332172));
#24223=CARTESIAN_POINT('Ctrl Pts',(182.746702534021,0.778602525828482,125.94634303675));
#24224=CARTESIAN_POINT('Ctrl Pts',(182.739212198259,0.64824640006857,125.927247078214));
#24225=CARTESIAN_POINT('Ctrl Pts',(182.731721862497,0.517534864453755,125.913415849265));
#24226=CARTESIAN_POINT('Ctrl Pts',(182.723947528378,0.381867361238935,125.899060205066));
#24227=CARTESIAN_POINT('Ctrl Pts',(182.716173194259,0.245387211553195,125.890330921351));
#24228=CARTESIAN_POINT('Ctrl Pts',(182.708398860139,0.108600702437423,125.88730977891));
#24229=CARTESIAN_POINT('Ctrl Pts',(182.700634107192,-0.0280172295310573,
125.884292359757));
#24230=CARTESIAN_POINT('Ctrl Pts',(182.692869354245,-0.164940382578901,
125.886969093325));
#24231=CARTESIAN_POINT('Ctrl Pts',(182.685104601298,-0.301655748620083,
125.895370204882));
#24232=CARTESIAN_POINT('Ctrl Pts',(182.677347560413,-0.438235327031179,
125.903762972337));
#24233=CARTESIAN_POINT('Ctrl Pts',(182.669590519528,-0.57460714143116,125.91786877949));
#24234=CARTESIAN_POINT('Ctrl Pts',(182.661833478643,-0.710256929006805,
125.937665829797));
#24235=CARTESIAN_POINT('Ctrl Pts',(182.654082287403,-0.845804422024122,
125.957447950995));
#24236=CARTESIAN_POINT('Ctrl Pts',(182.646331096163,-0.980630586681961,
125.982912716527));
#24237=CARTESIAN_POINT('Ctrl Pts',(182.638579904923,-1.11422539084784,126.013986431671));
#24238=CARTESIAN_POINT('Ctrl Pts',(182.630832008146,-1.24776341365743,126.045046939657));
#24239=CARTESIAN_POINT('Ctrl Pts',(182.623084111369,-1.38007073689753,126.081711567367));
#24240=CARTESIAN_POINT('Ctrl Pts',(182.615336214591,-1.51064686501784,126.123855397858));
#24241=CARTESIAN_POINT('Ctrl Pts',(182.607589938507,-1.64119567942685,126.165990412768));
#24242=CARTESIAN_POINT('Ctrl Pts',(182.599843662423,-1.7700136471794,126.213602230732));
#24243=CARTESIAN_POINT('Ctrl Pts',(182.592097386339,-1.89661518547082,126.266515985944));
#24244=CARTESIAN_POINT('Ctrl Pts',(182.584351053074,-2.02321765830595,126.319430131753));
#24245=CARTESIAN_POINT('Ctrl Pts',(182.576604719809,-2.14760330830669,126.37764614214));
#24246=CARTESIAN_POINT('Ctrl Pts',(182.568858386543,-2.26930667116602,126.440941053199));
#24247=CARTESIAN_POINT('Ctrl Pts',(182.56111031854,-2.39103728865015,126.504250138715));
#24248=CARTESIAN_POINT('Ctrl Pts',(182.553362250537,-2.51008407691616,126.572640207808));
#24249=CARTESIAN_POINT('Ctrl Pts',(182.545614182534,-2.62600666382235,126.645842604612));
#24250=CARTESIAN_POINT('Ctrl Pts',(182.537857879792,-2.74205245463323,126.719122801795));
#24251=CARTESIAN_POINT('Ctrl Pts',(182.53010157705,-2.85496708005182,126.797225334571));
#24252=CARTESIAN_POINT('Ctrl Pts',(182.522345274309,-2.96433918540366,126.879838193579));
#24253=CARTESIAN_POINT('Ctrl Pts',(182.514584831794,-3.07376966594129,126.962495145556));
#24254=CARTESIAN_POINT('Ctrl Pts',(182.50682438928,-3.17965355724597,127.049666972136));
#24255=CARTESIAN_POINT('Ctrl Pts',(182.499063946766,-3.28161383704965,127.141002364953));
#24256=CARTESIAN_POINT('Ctrl Pts',(182.491291046501,-3.38373779254603,127.232484377452));
#24257=CARTESIAN_POINT('Ctrl Pts',(182.483518146235,-3.4819252698745,127.328143039421));
#24258=CARTESIAN_POINT('Ctrl Pts',(182.47574524597,-3.57583663900372,127.427590652991));
#24259=CARTESIAN_POINT('Ctrl Pts',(182.468254910208,-3.66633409331571,127.523423095313));
#24260=CARTESIAN_POINT('Ctrl Pts',(182.460764574446,-3.75286073415508,127.622773563756));
#24261=CARTESIAN_POINT('Ctrl Pts',(182.453274238684,-3.83515011659531,127.725268763516));
#24262=CARTESIAN_POINT('Ctrl Pts',(182.445516365561,-3.92037868426403,127.831424853274));
#24263=CARTESIAN_POINT('Ctrl Pts',(182.437758492438,-4.00133819468862,127.941298988973));
#24264=CARTESIAN_POINT('Ctrl Pts',(182.430000619315,-4.07768537362654,128.054512429718));
#24265=CARTESIAN_POINT('Ctrl Pts',(182.422064270311,-4.15578897855251,128.170330433359));
#24266=CARTESIAN_POINT('Ctrl Pts',(182.414127921308,-4.22906513008165,128.289642999518));
#24267=CARTESIAN_POINT('Ctrl Pts',(182.406191572305,-4.29718794017761,128.4120063651));
#24268=CARTESIAN_POINT('Ctrl Pts',(182.398453166183,-4.36361167865667,128.53131782896));
#24269=CARTESIAN_POINT('Ctrl Pts',(182.390714760061,-4.42513586114829,128.653529356966));
#24270=CARTESIAN_POINT('Ctrl Pts',(182.382976353939,-4.48150092218885,128.778198593709));
#24271=CARTESIAN_POINT('Ctrl Pts',(182.374941033495,-4.54002865001674,128.907651255019));
#24272=CARTESIAN_POINT('Ctrl Pts',(182.366905713051,-4.5929932099943,129.039753638606));
#24273=CARTESIAN_POINT('Ctrl Pts',(182.358870392607,-4.64015582391395,129.173981216231));
#24274=CARTESIAN_POINT('Ctrl Pts',(182.350835072163,-4.68731843783359,129.308208793856));
#24275=CARTESIAN_POINT('Ctrl Pts',(182.342799751719,-4.72867891245574,129.444561130289));
#24276=CARTESIAN_POINT('Ctrl Pts',(182.334764431275,-4.76405452823405,129.582490119308));
#24277=CARTESIAN_POINT('Ctrl Pts',(184.084599308536,-4.76405452823405,129.582490119308));
#24278=CARTESIAN_POINT('Ctrl Pts',(184.075945911235,-4.8018983817438,129.730042729782));
#24279=CARTESIAN_POINT('Ctrl Pts',(184.067292513934,-4.83292755031847,129.879527941908));
#24280=CARTESIAN_POINT('Ctrl Pts',(184.058639116632,-4.85696110866322,130.030337458072));
#24281=CARTESIAN_POINT('Ctrl Pts',(184.050029728944,-4.88087243667851,130.180379984322));
#24282=CARTESIAN_POINT('Ctrl Pts',(184.041420341256,-4.89785903432467,130.331733166547));
#24283=CARTESIAN_POINT('Ctrl Pts',(184.032810953568,-4.90779083573385,130.483779621269));
#24284=CARTESIAN_POINT('Ctrl Pts',(184.026827114393,-4.91469380078797,130.589457465631));
#24285=CARTESIAN_POINT('Ctrl Pts',(184.020843275218,-4.91818976220946,130.69546982899));
#24286=CARTESIAN_POINT('Ctrl Pts',(184.014859436043,-4.9182492280365,130.801605001777));
#24287=CARTESIAN_POINT('',(184.360140563971,-4.91824943376093,130.802000573005));
#24288=CARTESIAN_POINT('Ctrl Pts',(184.430229652623,-4.76405452823406,129.582490119308));
#24289=CARTESIAN_POINT('Ctrl Pts',(184.422327812055,-4.7986868585295,129.717521049511));
#24290=CARTESIAN_POINT('Ctrl Pts',(184.414425971487,-4.82753715525285,129.853882584735));
#24291=CARTESIAN_POINT('Ctrl Pts',(184.406524130919,-4.85053490297993,129.991037669732));
#24292=CARTESIAN_POINT('Ctrl Pts',(184.398622290351,-4.873532650707,130.128192754729));
#24293=CARTESIAN_POINT('Ctrl Pts',(184.390720449783,-4.89067785997628,130.266140963835));
#24294=CARTESIAN_POINT('Ctrl Pts',(184.382818609216,-4.90195570679255,130.404343978982));
#24295=CARTESIAN_POINT('Ctrl Pts',(184.375259260813,-4.91274473405513,130.536556813798));
#24296=CARTESIAN_POINT('Ctrl Pts',(184.367699912411,-4.91818571452675,130.669211977639));
#24297=CARTESIAN_POINT('Ctrl Pts',(184.360140564008,-4.91824943376062,130.802000572364));
#24298=CARTESIAN_POINT('Ctrl Pts',(184.360140563971,-4.91824943376093,130.802000573005));
#24299=CARTESIAN_POINT('Ctrl Pts',(184.352455145915,-4.9183142156431,130.937003725306));
#24300=CARTESIAN_POINT('Ctrl Pts',(184.344769727858,-4.9128161630471,131.072233610613));
#24301=CARTESIAN_POINT('Ctrl Pts',(184.337084309801,-4.90172557734377,131.207187412745));
#24302=CARTESIAN_POINT('Ctrl Pts',(184.329407784764,-4.89064782487823,131.341985055925));
#24303=CARTESIAN_POINT('Ctrl Pts',(184.321731259727,-4.87399044269163,131.476506855924));
#24304=CARTESIAN_POINT('Ctrl Pts',(184.314054734689,-4.85177572413915,131.610248565828));
#24305=CARTESIAN_POINT('Ctrl Pts',(184.306385156566,-4.82958110892026,131.743869245425));
#24306=CARTESIAN_POINT('Ctrl Pts',(184.298715578444,-4.80183922716559,131.876710846574));
#24307=CARTESIAN_POINT('Ctrl Pts',(184.291046000321,-4.76862425691908,132.008273304941));
#24308=CARTESIAN_POINT('Ctrl Pts',(184.283267874699,-4.73493919537421,132.141697766086));
#24309=CARTESIAN_POINT('Ctrl Pts',(184.275489749077,-4.69562496363401,132.273806182506));
#24310=CARTESIAN_POINT('Ctrl Pts',(184.267711623456,-4.65081294627124,132.404086219441));
#24311=CARTESIAN_POINT('Ctrl Pts',(184.260049224998,-4.606667666365,132.532427879451));
#24312=CARTESIAN_POINT('Ctrl Pts',(184.252386826541,-4.55718721851533,132.658994805512));
#24313=CARTESIAN_POINT('Ctrl Pts',(184.244724428084,-4.50254756195381,132.783311985044));
#24314=CARTESIAN_POINT('Ctrl Pts',(184.237062723623,-4.44791285419833,132.90761790496));
#24315=CARTESIAN_POINT('Ctrl Pts',(184.229401019162,-4.38812002801154,133.029674116977));
#24316=CARTESIAN_POINT('Ctrl Pts',(184.221739314701,-4.32339297491415,133.149026104787));
#24317=CARTESIAN_POINT('Ctrl Pts',(184.214076556531,-4.25865701995485,133.268394506983));
#24318=CARTESIAN_POINT('Ctrl Pts',(184.206413798362,-4.18898567966582,133.385057593469));
#24319=CARTESIAN_POINT('Ctrl Pts',(184.198751040193,-4.11464827331411,133.498586415344));
#24320=CARTESIAN_POINT('Ctrl Pts',(184.190886035627,-4.0383488485568,133.615111651125));
#24321=CARTESIAN_POINT('Ctrl Pts',(184.183021031061,-3.95713386805491,133.728334497134));
#24322=CARTESIAN_POINT('Ctrl Pts',(184.175156026495,-3.87134055205237,133.837824873583));
#24323=CARTESIAN_POINT('Ctrl Pts',(184.167481864777,-3.78762899462731,133.944658486767));
#24324=CARTESIAN_POINT('Ctrl Pts',(184.159807703058,-3.69955904336469,134.047938419428));
#24325=CARTESIAN_POINT('Ctrl Pts',(184.15213354134,-3.60748270613891,134.147301177523));
#24326=CARTESIAN_POINT('Ctrl Pts',(184.14417311535,-3.51197170509786,134.25037040006));
#24327=CARTESIAN_POINT('Ctrl Pts',(184.136212689361,-3.41214997576047,134.34922420526));
#24328=CARTESIAN_POINT('Ctrl Pts',(184.128252263371,-3.30844873692504,134.443502002239));
#24329=CARTESIAN_POINT('Ctrl Pts',(184.120291837381,-3.2047474980896,134.537779799218));
#24330=CARTESIAN_POINT('Ctrl Pts',(184.112331411392,-3.09716715988707,134.627481342045));
#24331=CARTESIAN_POINT('Ctrl Pts',(184.104370985402,-2.98617212354664,134.712296020186));
#24332=CARTESIAN_POINT('Ctrl Pts',(184.096596651283,-2.87777183200501,134.795127975026));
#24333=CARTESIAN_POINT('Ctrl Pts',(184.088822317164,-2.76575077820207,134.873577418346));
#24334=CARTESIAN_POINT('Ctrl Pts',(184.081047983045,-2.65049881953031,134.947311144687));
#24335=CARTESIAN_POINT('Ctrl Pts',(184.073283230098,-2.53538889859732,135.020954000799));
#24336=CARTESIAN_POINT('Ctrl Pts',(184.065518477151,-2.41705632156664,135.089892494809));
#24337=CARTESIAN_POINT('Ctrl Pts',(184.057753724204,-2.29592350409848,135.153833956469));
#24338=CARTESIAN_POINT('Ctrl Pts',(184.049996683319,-2.17491099745172,135.217711910569));
#24339=CARTESIAN_POINT('Ctrl Pts',(184.042239642434,-2.05110412867136,135.27660252783));
#24340=CARTESIAN_POINT('Ctrl Pts',(184.034482601549,-1.92495344569139,135.330256914922));
#24341=CARTESIAN_POINT('Ctrl Pts',(184.026731410308,-1.79889789392326,135.383870840824));
#24342=CARTESIAN_POINT('Ctrl Pts',(184.018980219068,-1.67050240435444,135.432256243768));
#24343=CARTESIAN_POINT('Ctrl Pts',(184.011229027828,-1.54024090802878,135.475210755146));
#24344=CARTESIAN_POINT('Ctrl Pts',(184.003481131051,-1.41003477631391,135.518147009712));
#24345=CARTESIAN_POINT('Ctrl Pts',(183.995733234274,-1.27796458578426,135.55565684151));
#24346=CARTESIAN_POINT('Ctrl Pts',(183.987985337497,-1.14452276743259,135.587586589369));
#24347=CARTESIAN_POINT('Ctrl Pts',(183.980239061413,-1.01110886223263,135.619509658213));
#24348=CARTESIAN_POINT('Ctrl Pts',(183.972492785329,-0.876324279891128,
135.645854873884));
#24349=CARTESIAN_POINT('Ctrl Pts',(183.964746509245,-0.740674697423658,
135.666518991693));
#24350=CARTESIAN_POINT('Ctrl Pts',(183.957000175979,-0.605024113621508,
135.68718326204));
#24351=CARTESIAN_POINT('Ctrl Pts',(183.949253842714,-0.468508903458449,
135.702166291965));
#24352=CARTESIAN_POINT('Ctrl Pts',(183.941507509448,-0.331642581234947,
135.711416380527));
#24353=CARTESIAN_POINT('Ctrl Pts',(183.933759441445,-0.194745608747665,
135.720668540583));
#24354=CARTESIAN_POINT('Ctrl Pts',(183.926011373442,-0.0574977577378105,
135.724185178199));
#24355=CARTESIAN_POINT('Ctrl Pts',(183.918263305439,0.0795851196291304,
135.721966668403));
#24356=CARTESIAN_POINT('Ctrl Pts',(183.910507002698,0.216813690309234,135.719745800749));
#24357=CARTESIAN_POINT('Ctrl Pts',(183.902750699956,0.353876545556638,135.711777615836));
#24358=CARTESIAN_POINT('Ctrl Pts',(183.894994397214,0.490260064193617,135.698114609335));
#24359=CARTESIAN_POINT('Ctrl Pts',(183.8872339547,0.626716374821129,135.684444310477));
#24360=CARTESIAN_POINT('Ctrl Pts',(183.879473512186,0.762492239505508,135.665073188767));
#24361=CARTESIAN_POINT('Ctrl Pts',(183.871713069671,0.89708291638147,135.640105162477));
#24362=CARTESIAN_POINT('Ctrl Pts',(183.863940169406,1.03188965016026,135.615097055295));
#24363=CARTESIAN_POINT('Ctrl Pts',(183.856167269141,1.16550701288779,135.58447417673));
#24364=CARTESIAN_POINT('Ctrl Pts',(183.848394368875,1.29744326874112,135.548390974435));
#24365=CARTESIAN_POINT('Ctrl Pts',(183.840904033113,1.42458330936598,135.513619487432));
#24366=CARTESIAN_POINT('Ctrl Pts',(183.833413697351,1.55016205245454,135.473777870507));
#24367=CARTESIAN_POINT('Ctrl Pts',(183.825923361589,1.67375775862039,135.42904633964));
#24368=CARTESIAN_POINT('Ctrl Pts',(183.81814902747,1.80203963355247,135.382618799184));
#24369=CARTESIAN_POINT('Ctrl Pts',(183.810374693351,1.92859148786851,135.330776154368));
#24370=CARTESIAN_POINT('Ctrl Pts',(183.802600359232,2.05292225893399,135.273666297565));
#24371=CARTESIAN_POINT('Ctrl Pts',(183.794835606285,2.17709980343563,135.216626823557));
#24372=CARTESIAN_POINT('Ctrl Pts',(183.787070853338,2.29906135920444,135.154333215077));
#24373=CARTESIAN_POINT('Ctrl Pts',(183.779306100391,2.41833236849072,135.086982666966));
#24374=CARTESIAN_POINT('Ctrl Pts',(183.771549059506,2.53748491612928,135.019699012369));
#24375=CARTESIAN_POINT('Ctrl Pts',(183.763792018621,2.65395189702597,134.947368604385));
#24376=CARTESIAN_POINT('Ctrl Pts',(183.756034977736,2.76728037800997,134.870235968826));
#24377=CARTESIAN_POINT('Ctrl Pts',(183.748283786496,2.88052339710438,134.793161499588));
#24378=CARTESIAN_POINT('Ctrl Pts',(183.740532595256,2.99063230529288,134.711292230035));
#24379=CARTESIAN_POINT('Ctrl Pts',(183.732781404016,3.09718067282804,134.624917506602));
#24380=CARTESIAN_POINT('Ctrl Pts',(183.725033507239,3.20368375446525,134.53857949473));
#24381=CARTESIAN_POINT('Ctrl Pts',(183.717285610461,3.30662900226592,134.447740083331));
#24382=CARTESIAN_POINT('Ctrl Pts',(183.709537713684,3.4056209657537,134.352730510928));
#24383=CARTESIAN_POINT('Ctrl Pts',(183.7017914376,3.50459222225675,134.25774081248));
#24384=CARTESIAN_POINT('Ctrl Pts',(183.694045161516,3.59961155738863,134.158582958646));
#24385=CARTESIAN_POINT('Ctrl Pts',(183.686298885432,3.6903187776887,134.055626583546));
#24386=CARTESIAN_POINT('Ctrl Pts',(183.678552552167,3.78102666756886,133.952669448445));
#24387=CARTESIAN_POINT('Ctrl Pts',(183.670806218901,3.86742212064859,133.845914029478));
#24388=CARTESIAN_POINT('Ctrl Pts',(183.663059885636,3.94918407243948,133.73576441515));
#24389=CARTESIAN_POINT('Ctrl Pts',(183.655311817633,4.03096433425261,133.625590133579));
#24390=CARTESIAN_POINT('Ctrl Pts',(183.64756374963,4.10810879701171,133.512020457994));
#24391=CARTESIAN_POINT('Ctrl Pts',(183.639815681627,4.18033894554159,133.395489592142));
#24392=CARTESIAN_POINT('Ctrl Pts',(183.632059378885,4.25264586113286,133.278834875899));
#24393=CARTESIAN_POINT('Ctrl Pts',(183.624303076144,4.32002782270208,133.159213015378));
#24394=CARTESIAN_POINT('Ctrl Pts',(183.616546773402,4.38225137155276,133.037084509816));
#24395=CARTESIAN_POINT('Ctrl Pts',(183.608786330888,4.444508130985,132.914890820593));
#24396=CARTESIAN_POINT('Ctrl Pts',(183.601025888373,4.50160082904401,132.790188175812));
#24397=CARTESIAN_POINT('Ctrl Pts',(183.593265445859,4.55334406980649,132.663457399463));
#24398=CARTESIAN_POINT('Ctrl Pts',(183.585492545594,4.60517037341259,132.53652318362));
#24399=CARTESIAN_POINT('Ctrl Pts',(183.577719645328,4.65162992673136,132.407554698248));
#24400=CARTESIAN_POINT('Ctrl Pts',(183.569946745063,4.69258687572239,132.277049137348));
#24401=CARTESIAN_POINT('Ctrl Pts',(183.562456409301,4.73205493645361,132.15128778231));
#24402=CARTESIAN_POINT('Ctrl Pts',(183.554966073539,4.7664134338327,132.024099462039));
#24403=CARTESIAN_POINT('Ctrl Pts',(183.547475737777,4.79558602822751,131.895936408965));
#24404=CARTESIAN_POINT('Ctrl Pts',(183.539701403658,4.82586471040535,131.762914014781));
#24405=CARTESIAN_POINT('Ctrl Pts',(183.531927069538,4.85065239351974,131.62842013976));
#24406=CARTESIAN_POINT('Ctrl Pts',(183.524152735419,4.86980807226552,131.492947868245));
#24407=CARTESIAN_POINT('Ctrl Pts',(183.516387982472,4.88894014334924,131.357642554197));
#24408=CARTESIAN_POINT('Ctrl Pts',(183.508623229525,4.90245396625799,131.221361626208));
#24409=CARTESIAN_POINT('Ctrl Pts',(183.500858476578,4.91025893654111,131.084610931782));
#24410=CARTESIAN_POINT('Ctrl Pts',(183.493101435693,4.91805615481771,130.947996060074));
#24411=CARTESIAN_POINT('Ctrl Pts',(183.485344394808,4.92015578211555,130.810912738245));
#24412=CARTESIAN_POINT('Ctrl Pts',(183.477587353923,4.91651872348393,130.673874203975));
#24413=CARTESIAN_POINT('Ctrl Pts',(183.469836162683,4.9128844075865,130.536939011528));
#24414=CARTESIAN_POINT('Ctrl Pts',(183.462084971443,4.90352202688916,130.40004892866));
#24415=CARTESIAN_POINT('Ctrl Pts',(183.454333780202,4.88844452104653,130.263719121609));
#24416=CARTESIAN_POINT('Ctrl Pts',(183.446585883425,4.87337342354616,130.127447258364));
#24417=CARTESIAN_POINT('Ctrl Pts',(183.438837986648,4.85259207504386,129.991735585091));
#24418=CARTESIAN_POINT('Ctrl Pts',(183.431090089871,4.82616540524861,129.857095847989));
#24419=CARTESIAN_POINT('Ctrl Pts',(183.423343813787,4.79974426334297,129.722484274618));
#24420=CARTESIAN_POINT('Ctrl Pts',(183.415597537703,4.76768022423145,129.588944574821));
#24421=CARTESIAN_POINT('Ctrl Pts',(183.407851261619,4.73008957820223,129.45697958583));
#24422=CARTESIAN_POINT('Ctrl Pts',(183.400104928353,4.69249865468751,129.325013622703));
#24423=CARTESIAN_POINT('Ctrl Pts',(183.392358595088,4.64938114995637,129.194622769583));
#24424=CARTESIAN_POINT('Ctrl Pts',(183.384612261823,4.60090349191246,129.066295566825));
#24425=CARTESIAN_POINT('Ctrl Pts',(183.37686419382,4.55241497763291,128.937939626078));
#24426=CARTESIAN_POINT('Ctrl Pts',(183.369116125817,4.49856405958199,128.811648620967));
#24427=CARTESIAN_POINT('Ctrl Pts',(183.361368057814,4.43956550141456,128.687891571927));
#24428=CARTESIAN_POINT('Ctrl Pts',(183.353611755072,4.38050423887763,128.564002992422));
#24429=CARTESIAN_POINT('Ctrl Pts',(183.34585545233,4.31628457587822,128.44265410226));
#24430=CARTESIAN_POINT('Ctrl Pts',(183.338099149588,4.24716775333799,128.324290227939));
#24431=CARTESIAN_POINT('Ctrl Pts',(183.330338707074,4.17801404106853,128.205863179254));
#24432=CARTESIAN_POINT('Ctrl Pts',(183.32257826456,4.10395817211934,128.090424649892));
#24433=CARTESIAN_POINT('Ctrl Pts',(183.314817822046,4.02530446630552,127.978390515806));
#24434=CARTESIAN_POINT('Ctrl Pts',(183.30704492178,3.94652449858048,127.866176534582));
#24435=CARTESIAN_POINT('Ctrl Pts',(183.299272021515,3.86313218266577,127.757378179998));
#24436=CARTESIAN_POINT('Ctrl Pts',(183.291499121249,3.77547238952982,127.652378495409));
#24437=CARTESIAN_POINT('Ctrl Pts',(183.284008785487,3.69099925067666,127.551195813834));
#24438=CARTESIAN_POINT('Ctrl Pts',(183.276518449725,3.60256372176028,127.453540643053));
#24439=CARTESIAN_POINT('Ctrl Pts',(183.269028113963,3.51050501529534,127.359721652437));
#24440=CARTESIAN_POINT('Ctrl Pts',(183.261253779844,3.41495587499346,127.262345486275));
#24441=CARTESIAN_POINT('Ctrl Pts',(183.253479445725,3.31520071706981,127.168793681802));
#24442=CARTESIAN_POINT('Ctrl Pts',(183.245705111606,3.21157817053554,127.079451394908));
#24443=CARTESIAN_POINT('Ctrl Pts',(183.237940358659,3.10808332952903,126.990219214398));
#24444=CARTESIAN_POINT('Ctrl Pts',(183.230175605712,3.00073087651156,126.905186482029));
#24445=CARTESIAN_POINT('Ctrl Pts',(183.222410852765,2.88989742139538,126.824702848824));
#24446=CARTESIAN_POINT('Ctrl Pts',(183.21465381188,2.77917404762878,126.744299153096));
#24447=CARTESIAN_POINT('Ctrl Pts',(183.206896770995,2.66497686641319,126.668435793291));
#24448=CARTESIAN_POINT('Ctrl Pts',(183.19913973011,2.54771654736785,126.597423078599));
#24449=CARTESIAN_POINT('Ctrl Pts',(183.19138853887,2.43054465524129,126.526463915148));
#24450=CARTESIAN_POINT('Ctrl Pts',(183.18363734763,2.31031455614051,126.460348317669));
#24451=CARTESIAN_POINT('Ctrl Pts',(183.175886156389,2.18746666821171,126.3993438596));
#24452=CARTESIAN_POINT('Ctrl Pts',(183.168138259612,2.0646709939127,126.338365330053));
#24453=CARTESIAN_POINT('Ctrl Pts',(183.160390362835,1.93926009315588,126.282493792761));
#24454=CARTESIAN_POINT('Ctrl Pts',(183.152642466058,1.811699608605,126.231951231839));
#24455=CARTESIAN_POINT('Ctrl Pts',(183.144896189974,1.68416580695755,126.181419243332));
#24456=CARTESIAN_POINT('Ctrl Pts',(183.13714991389,1.55448367913088,126.136214157909));
#24457=CARTESIAN_POINT('Ctrl Pts',(183.129403637806,1.42313913406825,126.096509933062));
#24458=CARTESIAN_POINT('Ctrl Pts',(183.121657304541,1.29179361945,126.056805415127));
#24459=CARTESIAN_POINT('Ctrl Pts',(183.113910971275,1.15878603734873,126.022601951924));
#24460=CARTESIAN_POINT('Ctrl Pts',(183.10616463801,1.02461736894711,125.994023590938));
#24461=CARTESIAN_POINT('Ctrl Pts',(183.098416570007,0.890418654402585,125.965438830026));
#24462=CARTESIAN_POINT('Ctrl Pts',(183.090668502004,0.755058718467256,125.942481759427));
#24463=CARTESIAN_POINT('Ctrl Pts',(183.082920434001,0.619048246319054,125.925225209399));
#24464=CARTESIAN_POINT('Ctrl Pts',(183.075164131259,0.482893220622485,125.907950318904));
#24465=CARTESIAN_POINT('Ctrl Pts',(183.067407828517,0.346086666046123,125.896388100937));
#24466=CARTESIAN_POINT('Ctrl Pts',(183.059651525776,0.209144455485154,125.890559475961));
#24467=CARTESIAN_POINT('Ctrl Pts',(183.051891083261,0.0721291547430187,
125.884727740072));
#24468=CARTESIAN_POINT('Ctrl Pts',(183.044130640747,-0.065021555480375,
125.884635695128));
#24469=CARTESIAN_POINT('Ctrl Pts',(183.036370198233,-0.201793294674736,
125.890252099358));
#24470=CARTESIAN_POINT('Ctrl Pts',(183.028597297968,-0.338784592006899,
125.895877519539));
#24471=CARTESIAN_POINT('Ctrl Pts',(183.020824397702,-0.475395312770501,
125.907229668511));
#24472=CARTESIAN_POINT('Ctrl Pts',(183.013051497437,-0.611116780560397,
125.92422544085));
#24473=CARTESIAN_POINT('Ctrl Pts',(183.005561161675,-0.74190443113344,125.940603374055));
#24474=CARTESIAN_POINT('Ctrl Pts',(182.998070825913,-0.87186605558637,125.96222168399));
#24475=CARTESIAN_POINT('Ctrl Pts',(182.990580490151,-1.00055860898726,125.988961824892));
#24476=CARTESIAN_POINT('Ctrl Pts',(182.982806156032,-1.13413057966649,126.016715826365));
#24477=CARTESIAN_POINT('Ctrl Pts',(182.975031821913,-1.26675846180681,126.050075630492));
#24478=CARTESIAN_POINT('Ctrl Pts',(182.967257487794,-1.39793517559902,126.088964525261));
#24479=CARTESIAN_POINT('Ctrl Pts',(182.959492734846,-1.52895022581513,126.127805492943));
#24480=CARTESIAN_POINT('Ctrl Pts',(182.951727981899,-1.65851729489495,126.172161883161));
#24481=CARTESIAN_POINT('Ctrl Pts',(182.943963228952,-1.78613864467428,126.221905838247));
#24482=CARTESIAN_POINT('Ctrl Pts',(182.936206188067,-1.91363323913031,126.271600386936));
#24483=CARTESIAN_POINT('Ctrl Pts',(182.928449147182,-2.03918559816484,126.326671710685));
#24484=CARTESIAN_POINT('Ctrl Pts',(182.920692106297,-2.16231267290643,126.386942031209));
#24485=CARTESIAN_POINT('Ctrl Pts',(182.912940915057,-2.28534689656263,126.447166901416));
#24486=CARTESIAN_POINT('Ctrl Pts',(182.905189723817,-2.40595912655983,126.512582793482));
#24487=CARTESIAN_POINT('Ctrl Pts',(182.897438532577,-2.52368618902095,126.582963801127));
#24488=CARTESIAN_POINT('Ctrl Pts',(182.8896906358,-2.64136321434017,126.653314894965));
#24489=CARTESIAN_POINT('Ctrl Pts',(182.881942739023,-2.75615717621927,126.728626706948));
#24490=CARTESIAN_POINT('Ctrl Pts',(182.874194842245,-2.86762962189981,126.808627466553));
#24491=CARTESIAN_POINT('Ctrl Pts',(182.866448566161,-2.97907874994782,126.888611491724));
#24492=CARTESIAN_POINT('Ctrl Pts',(182.858702290077,-3.08720742634127,126.973282285786));
#24493=CARTESIAN_POINT('Ctrl Pts',(182.850956013993,-3.1916066500627,127.062325068059));
#24494=CARTESIAN_POINT('Ctrl Pts',(182.843209680728,-3.29600664443559,127.151368507625));
#24495=CARTESIAN_POINT('Ctrl Pts',(182.835463347462,-3.39667683373769,127.24478374609));
#24496=CARTESIAN_POINT('Ctrl Pts',(182.827717014197,-3.49324206073987,127.342216344492));
#24497=CARTESIAN_POINT('Ctrl Pts',(182.819968946194,-3.58982891285543,127.43967076225));
#24498=CARTESIAN_POINT('Ctrl Pts',(182.812220878191,-3.68230869825185,127.541144052529));
#24499=CARTESIAN_POINT('Ctrl Pts',(182.804472810188,-3.77034410495834,127.64624592796));
#24500=CARTESIAN_POINT('Ctrl Pts',(182.796716507446,-3.85847307674226,127.751459506914));
#24501=CARTESIAN_POINT('Ctrl Pts',(182.788960204704,-3.94214798261169,127.860309074608));
#24502=CARTESIAN_POINT('Ctrl Pts',(182.781203901962,-4.02107237968682,127.972371920586));
#24503=CARTESIAN_POINT('Ctrl Pts',(182.773443459448,-4.10003890108901,128.08449457788));
#24504=CARTESIAN_POINT('Ctrl Pts',(182.765683016934,-4.17424965007582,128.19983360216));
#24505=CARTESIAN_POINT('Ctrl Pts',(182.75792257442,-4.24345287600184,128.317939343596));
#24506=CARTESIAN_POINT('Ctrl Pts',(182.750149674154,-4.31276719308979,128.436234678853));
#24507=CARTESIAN_POINT('Ctrl Pts',(182.742376773889,-4.37705774012523,128.557305261059));
#24508=CARTESIAN_POINT('Ctrl Pts',(182.734603873624,-4.43611948403242,128.680678205837));
#24509=CARTESIAN_POINT('Ctrl Pts',(182.727113537862,-4.49303418478051,128.799566233313));
#24510=CARTESIAN_POINT('Ctrl Pts',(182.7196232021,-4.54509352087592,128.920591853246));
#24511=CARTESIAN_POINT('Ctrl Pts',(182.712132866338,-4.59215775161795,129.043318242507));
#24512=CARTESIAN_POINT('Ctrl Pts',(182.703253522123,-4.64794957700628,129.188803023033));
#24513=CARTESIAN_POINT('Ctrl Pts',(182.694374177909,-4.69687000701748,129.337061417581));
#24514=CARTESIAN_POINT('Ctrl Pts',(182.685494833695,-4.73867041310273,129.487475740865));
#24515=CARTESIAN_POINT('Ctrl Pts',(182.683630675656,-4.74744612459306,129.519054206932));
#24516=CARTESIAN_POINT('Ctrl Pts',(182.681766517617,-4.75590817585868,129.550727615035));
#24517=CARTESIAN_POINT('Ctrl Pts',(182.679902359578,-4.76405452823405,129.582490119308));
#24518=CARTESIAN_POINT('Origin',(213.235140564004,0.,130.804360617566));
#24519=CARTESIAN_POINT('',(180.584985772263,-4.76405452823404,129.582490119308));
#24520=CARTESIAN_POINT('',(180.930009319727,-4.76405452823406,129.582490119308));
#24521=CARTESIAN_POINT('',(213.235140564004,-4.76405452823405,129.582490119308));
#24522=CARTESIAN_POINT('',(182.264859435942,-4.91824838731473,130.808343477848));
#24523=CARTESIAN_POINT('Ctrl Pts',(182.264859435942,-4.91824838731473,130.808343477848));
#24524=CARTESIAN_POINT('Ctrl Pts',(182.255745689485,-4.91811770455124,130.969717526973));
#24525=CARTESIAN_POINT('Ctrl Pts',(182.246631943028,-4.91004084791699,131.130754613443));
#24526=CARTESIAN_POINT('Ctrl Pts',(182.237518196571,-4.89414028983605,131.290749233699));
#24527=CARTESIAN_POINT('Ctrl Pts',(182.228343751195,-4.87813383165355,131.451809442121));
#24528=CARTESIAN_POINT('Ctrl Pts',(182.21916930582,-4.85419921674639,131.611813182237));
#24529=CARTESIAN_POINT('Ctrl Pts',(182.209994860445,-4.82251028849471,131.770061181852));
#24530=CARTESIAN_POINT('Ctrl Pts',(182.200752520834,-4.79058685063821,131.929480274271));
#24531=CARTESIAN_POINT('Ctrl Pts',(182.191510181223,-4.75079397460461,132.087117477438));
#24532=CARTESIAN_POINT('Ctrl Pts',(182.182267841612,-4.70335754186608,132.242279563777));
#24533=CARTESIAN_POINT('Ctrl Pts',(182.179787432699,-4.69062680965446,132.28392112189));
#24534=CARTESIAN_POINT('Ctrl Pts',(182.177307023785,-4.67734581439877,132.325384532998));
#24535=CARTESIAN_POINT('Ctrl Pts',(182.174826614871,-4.66351949799474,132.366656669639));
#24536=CARTESIAN_POINT('Ctrl Pts',(182.167052280752,-4.62018373880961,132.496015735516));
#24537=CARTESIAN_POINT('Ctrl Pts',(182.159277946633,-4.57139291895546,132.623775226555));
#24538=CARTESIAN_POINT('Ctrl Pts',(182.151503612514,-4.51728310406877,132.749440672524));
#24539=CARTESIAN_POINT('Ctrl Pts',(182.143738859567,-4.46323997469291,132.874951247062));
#24540=CARTESIAN_POINT('Ctrl Pts',(182.13597410662,-4.40389104628627,132.998372555757));
#24541=CARTESIAN_POINT('Ctrl Pts',(182.128209353673,-4.33942206882534,133.119225445389));
#24542=CARTESIAN_POINT('Ctrl Pts',(182.120452312788,-4.27501712286173,133.239958302227));
#24543=CARTESIAN_POINT('Ctrl Pts',(182.112695271903,-4.20550243065429,133.358127473865));
#24544=CARTESIAN_POINT('Ctrl Pts',(182.104938231018,-4.13111157845121,133.473274289622));
#24545=CARTESIAN_POINT('Ctrl Pts',(182.097187039777,-4.05677682496856,133.588334272269));
#24546=CARTESIAN_POINT('Ctrl Pts',(182.089435848537,-3.97757344193555,133.700376108544));
#24547=CARTESIAN_POINT('Ctrl Pts',(182.081684657297,-3.89378045932293,133.808966547983));
#24548=CARTESIAN_POINT('Ctrl Pts',(182.07393676052,-3.81002309096304,133.917510833588));
#24549=CARTESIAN_POINT('Ctrl Pts',(182.066188863743,-3.72168024116592,134.022606331103));
#24550=CARTESIAN_POINT('Ctrl Pts',(182.058440966966,-3.62907356334536,134.123849755118));
#24551=CARTESIAN_POINT('Ctrl Pts',(182.050694690882,-3.53648625684542,134.225072001192));
#24552=CARTESIAN_POINT('Ctrl Pts',(182.042948414798,-3.43963716006998,134.322443488187));
#24553=CARTESIAN_POINT('Ctrl Pts',(182.035202138714,-3.33888715704143,134.415595256169));
#24554=CARTESIAN_POINT('Ctrl Pts',(182.027455805448,-3.23813641029925,134.508747711776));
#24555=CARTESIAN_POINT('Ctrl Pts',(182.019709472183,-3.1334849869114,134.597680120798));
#24556=CARTESIAN_POINT('Ctrl Pts',(182.011963138918,-3.02532915435104,134.682061814194));
#24557=CARTESIAN_POINT('Ctrl Pts',(182.004215070915,-2.91714910104202,134.766462404286));
#24558=CARTESIAN_POINT('Ctrl Pts',(181.996467002912,-2.8054633851131,134.846310010414));
#24559=CARTESIAN_POINT('Ctrl Pts',(181.988718934909,-2.69069940167571,134.921315777915));
#24560=CARTESIAN_POINT('Ctrl Pts',(181.980962632167,-2.5758134457109,134.996401262438));
#24561=CARTESIAN_POINT('Ctrl Pts',(181.973206329425,-2.45784301461549,135.066634414486));
#24562=CARTESIAN_POINT('Ctrl Pts',(181.965450026683,-2.33724287264859,135.13177079188));
#24563=CARTESIAN_POINT('Ctrl Pts',(181.957689584169,-2.21657836275474,135.196941934519));
#24564=CARTESIAN_POINT('Ctrl Pts',(181.949929141655,-2.09328169658598,135.257010710924));
#24565=CARTESIAN_POINT('Ctrl Pts',(181.942168699141,-1.96782911067562,135.311780240108));
#24566=CARTESIAN_POINT('Ctrl Pts',(181.934395798875,-1.8421751371371,135.366637690203));
#24567=CARTESIAN_POINT('Ctrl Pts',(181.92662289861,-1.71435869267866,135.416178752362));
#24568=CARTESIAN_POINT('Ctrl Pts',(181.918849998344,-1.58487356800099,135.460255680382));
#24569=CARTESIAN_POINT('Ctrl Pts',(181.911359662582,-1.46009555375806,135.502730301045));
#24570=CARTESIAN_POINT('Ctrl Pts',(181.90386932682,-1.33376836978196,135.540131073015));
#24571=CARTESIAN_POINT('Ctrl Pts',(181.896378991058,-1.20634228632941,135.572370826313));
#24572=CARTESIAN_POINT('Ctrl Pts',(181.888604656939,-1.07408480419308,135.605832959655));
#24573=CARTESIAN_POINT('Ctrl Pts',(181.88083032282,-0.940224496132468,135.63384098669));
#24574=CARTESIAN_POINT('Ctrl Pts',(181.873055988701,-0.805250920756176,
135.656242110051));
#24575=CARTESIAN_POINT('Ctrl Pts',(181.865291235754,-0.670443688248645,
135.67861562603));
#24576=CARTESIAN_POINT('Ctrl Pts',(181.857526482807,-0.534526300288229,
135.695395923796));
#24577=CARTESIAN_POINT('Ctrl Pts',(181.849761729859,-0.398002284449767,
135.706480286043));
#24578=CARTESIAN_POINT('Ctrl Pts',(181.842004688974,-0.261613866188487,
135.717553639146));
#24579=CARTESIAN_POINT('Ctrl Pts',(181.834247648089,-0.124620406235299,
135.722942283547));
#24580=CARTESIAN_POINT('Ctrl Pts',(181.826490607204,0.0124659437015487,
135.722594819264));
#24581=CARTESIAN_POINT('Ctrl Pts',(181.818739415964,0.149448915755369,135.722247617006));
#24582=CARTESIAN_POINT('Ctrl Pts',(181.810988224724,0.286524248982427,135.716172916984));
#24583=CARTESIAN_POINT('Ctrl Pts',(181.803237033484,0.423176614983207,135.704371292558));
#24584=CARTESIAN_POINT('Ctrl Pts',(181.795489136707,0.559770900083301,135.692574684136));
#24585=CARTESIAN_POINT('Ctrl Pts',(181.78774123993,0.695942186810799,135.675056026109));
#24586=CARTESIAN_POINT('Ctrl Pts',(181.779993343153,0.831177318203662,135.651867948989));
#24587=CARTESIAN_POINT('Ctrl Pts',(181.772247067069,0.966384161322348,135.628684722316));
#24588=CARTESIAN_POINT('Ctrl Pts',(181.764500790985,1.10065485351256,135.599834501441));
#24589=CARTESIAN_POINT('Ctrl Pts',(181.756754514901,1.2334839117036,135.565421476457));
#24590=CARTESIAN_POINT('Ctrl Pts',(181.749008181635,1.36631395040857,135.531008197445));
#24591=CARTESIAN_POINT('Ctrl Pts',(181.74126184837,1.49770195540958,135.491032130437));
#24592=CARTESIAN_POINT('Ctrl Pts',(181.733515515104,1.62715553322994,135.44564793179));
#24593=CARTESIAN_POINT('Ctrl Pts',(181.725767447101,1.75663810128136,135.400253569667));
#24594=CARTESIAN_POINT('Ctrl Pts',(181.718019379098,1.88418501125313,135.34944879525));
#24595=CARTESIAN_POINT('Ctrl Pts',(181.710271311096,2.00932222403949,135.293437055151));
#24596=CARTESIAN_POINT('Ctrl Pts',(181.702515008354,2.13459243414487,135.237365785108));
#24597=CARTESIAN_POINT('Ctrl Pts',(181.694758705612,2.2574474736639,135.176076654553));
#24598=CARTESIAN_POINT('Ctrl Pts',(181.68700240287,2.37743587527888,135.109820142569));
#24599=CARTESIAN_POINT('Ctrl Pts',(181.679241960356,2.49748831831668,135.043528267489));
#24600=CARTESIAN_POINT('Ctrl Pts',(181.671481517842,2.61467074089446,134.972263931206));
#24601=CARTESIAN_POINT('Ctrl Pts',(181.663721075327,2.72856008398556,134.896321386022));
#24602=CARTESIAN_POINT('Ctrl Pts',(181.655948175062,2.84263225236077,134.820256931122));
#24603=CARTESIAN_POINT('Ctrl Pts',(181.648175274797,2.9534004613508,134.739499490654));
#24604=CARTESIAN_POINT('Ctrl Pts',(181.640402374531,3.06047350195551,134.654384644287));
#24605=CARTESIAN_POINT('Ctrl Pts',(181.632912038769,3.16365416783352,134.572363936976));
#24606=CARTESIAN_POINT('Ctrl Pts',(181.625421703007,3.26340342518855,134.486297330141));
#24607=CARTESIAN_POINT('Ctrl Pts',(181.617931367245,3.35940455337579,134.396516531395));
#24608=CARTESIAN_POINT('Ctrl Pts',(181.610157033126,3.45904559351708,134.303331666377));
#24609=CARTESIAN_POINT('Ctrl Pts',(181.602382699007,3.5549643061159,134.205850220831));
#24610=CARTESIAN_POINT('Ctrl Pts',(181.594608364888,3.64676752003656,134.104401483572));
#24611=CARTESIAN_POINT('Ctrl Pts',(181.586843611941,3.73845759470076,134.003077772814));
#24612=CARTESIAN_POINT('Ctrl Pts',(181.579078858994,3.82604200261285,133.897796785766));
#24613=CARTESIAN_POINT('Ctrl Pts',(181.571314106046,3.90916215584225,133.788926633226));
#24614=CARTESIAN_POINT('Ctrl Pts',(181.563557065161,3.99219975296364,133.680164612056));
#24615=CARTESIAN_POINT('Ctrl Pts',(181.555800024276,4.07078168346808,133.567820828264));
#24616=CARTESIAN_POINT('Ctrl Pts',(181.548042983391,4.14458787258715,133.452298386643));
#24617=CARTESIAN_POINT('Ctrl Pts',(181.540291792151,4.21833840388486,133.336863061394));
#24618=CARTESIAN_POINT('Ctrl Pts',(181.532540600911,4.28732015257257,133.21825417763));
#24619=CARTESIAN_POINT('Ctrl Pts',(181.524789409671,4.35125505344596,133.096905605644));
#24620=CARTESIAN_POINT('Ctrl Pts',(181.517041512894,4.41516278028099,132.975608610038));
#24621=CARTESIAN_POINT('Ctrl Pts',(181.509293616117,4.47402774377339,132.851574587362));
#24622=CARTESIAN_POINT('Ctrl Pts',(181.50154571934,4.52761684959189,132.72526371918));
#24623=CARTESIAN_POINT('Ctrl Pts',(181.493799443256,4.5811947457247,132.598979272509));
#24624=CARTESIAN_POINT('Ctrl Pts',(181.486053167172,4.62949882669481,132.470419287337));
#24625=CARTESIAN_POINT('Ctrl Pts',(181.478306891088,4.67234352463098,132.340065358178));
#24626=CARTESIAN_POINT('Ctrl Pts',(181.470560557822,4.71518853883696,132.209710466776));
#24627=CARTESIAN_POINT('Ctrl Pts',(181.462814224557,4.75257396751604,132.07756197638));
#24628=CARTESIAN_POINT('Ctrl Pts',(181.455067891292,4.78436377673831,131.944117747105));
#24629=CARTESIAN_POINT('Ctrl Pts',(181.447319823289,4.81616070506794,131.810643633919));
#24630=CARTESIAN_POINT('Ctrl Pts',(181.439571755286,4.84235942983139,131.675873584696));
#24631=CARTESIAN_POINT('Ctrl Pts',(181.431823687283,4.86287488670871,131.540316389823));
#24632=CARTESIAN_POINT('Ctrl Pts',(181.424067384541,4.88341214765773,131.404615123149));
#24633=CARTESIAN_POINT('Ctrl Pts',(181.416311081799,4.89825401608467,131.268125426831));
#24634=CARTESIAN_POINT('Ctrl Pts',(181.408554779057,4.90736719802281,131.131362523172));
#24635=CARTESIAN_POINT('Ctrl Pts',(181.400794336543,4.91648524394055,130.994526625032));
#24636=CARTESIAN_POINT('Ctrl Pts',(181.393033894029,4.91986850125779,130.85741761965));
#24637=CARTESIAN_POINT('Ctrl Pts',(181.385273451515,4.91753585903247,130.720550489122));
#24638=CARTESIAN_POINT('Ctrl Pts',(181.377500551249,4.91519947224276,130.583463647326));
#24639=CARTESIAN_POINT('Ctrl Pts',(181.369727650984,4.90712887303039,130.4466198468));
#24640=CARTESIAN_POINT('Ctrl Pts',(181.361954750718,4.89339493605524,130.310529611767));
#24641=CARTESIAN_POINT('Ctrl Pts',(181.354464414956,4.88016026228275,130.179386599566));
#24642=CARTESIAN_POINT('Ctrl Pts',(181.346974079194,4.86166689853009,130.048943621018));
#24643=CARTESIAN_POINT('Ctrl Pts',(181.339483743432,4.83802272456425,129.91964643824));
#24644=CARTESIAN_POINT('Ctrl Pts',(181.331709409313,4.81348207455615,129.785446913479));
#24645=CARTESIAN_POINT('Ctrl Pts',(181.323935075194,4.78331458070452,129.652056681576));
#24646=CARTESIAN_POINT('Ctrl Pts',(181.316160741075,4.74758476441283,129.519984517191));
#24647=CARTESIAN_POINT('Ctrl Pts',(181.308395988128,4.71189898192648,129.388075119944));
#24648=CARTESIAN_POINT('Ctrl Pts',(181.300631235181,4.67066461765525,129.257480931918));
#24649=CARTESIAN_POINT('Ctrl Pts',(181.292866482234,4.62399754810301,129.128702616172));
#24650=CARTESIAN_POINT('Ctrl Pts',(181.285109441349,4.57737682894217,129.000052204864));
#24651=CARTESIAN_POINT('Ctrl Pts',(181.277352400464,4.52533427480508,128.873214441886));
#24652=CARTESIAN_POINT('Ctrl Pts',(181.269595359579,4.46803602093881,128.748676503191));
#24653=CARTESIAN_POINT('Ctrl Pts',(181.261844168339,4.41078097613147,128.624232479525));
#24654=CARTESIAN_POINT('Ctrl Pts',(181.254092977099,4.3482782831815,128.502085181832));
#24655=CARTESIAN_POINT('Ctrl Pts',(181.246341785858,4.28074266841829,128.382703071734));
#24656=CARTESIAN_POINT('Ctrl Pts',(181.238593889081,4.2132357580929,128.263371702218));
#24657=CARTESIAN_POINT('Ctrl Pts',(181.230845992304,4.14070037261404,128.146803522334));
#24658=CARTESIAN_POINT('Ctrl Pts',(181.223098095527,4.06339768258434,128.03344338032));
#24659=CARTESIAN_POINT('Ctrl Pts',(181.215351819443,3.98611116261093,127.920106950803));
#24660=CARTESIAN_POINT('Ctrl Pts',(181.207605543359,3.90405954173491,127.809977547203));
#24661=CARTESIAN_POINT('Ctrl Pts',(181.199859267275,3.81754769509268,127.703471606622));
#24662=CARTESIAN_POINT('Ctrl Pts',(181.19211293401,3.7310352098397,127.596964879839));
#24663=CARTESIAN_POINT('Ctrl Pts',(181.184366600744,3.64006267962051,127.494081972915));
#24664=CARTESIAN_POINT('Ctrl Pts',(181.176620267479,3.54497543858795,127.395206440602));
#24665=CARTESIAN_POINT('Ctrl Pts',(181.168872199476,3.44986690342704,127.2963087658));
#24666=CARTESIAN_POINT('Ctrl Pts',(181.161124131473,3.35064209480331,127.201420533123));
#24667=CARTESIAN_POINT('Ctrl Pts',(181.15337606347,3.24768309313699,127.110888323227));
#24668=CARTESIAN_POINT('Ctrl Pts',(181.145619760728,3.14461466541844,127.02025989462));
#24669=CARTESIAN_POINT('Ctrl Pts',(181.137863457986,3.03780441073446,126.933996995563));
#24670=CARTESIAN_POINT('Ctrl Pts',(181.130107155245,2.92766780399824,126.852406127452));
#24671=CARTESIAN_POINT('Ctrl Pts',(181.12234671273,2.81747241403878,126.770771711838));
#24672=CARTESIAN_POINT('Ctrl Pts',(181.114586270216,2.7039474579022,126.693814515155));
#24673=CARTESIAN_POINT('Ctrl Pts',(181.106825827702,2.58753641460957,126.621797005908));
#24674=CARTESIAN_POINT('Ctrl Pts',(181.099052927437,2.4709384979758,126.54966388776));
#24675=CARTESIAN_POINT('Ctrl Pts',(181.091280027171,2.35144557696644,126.48248649467));
#24676=CARTESIAN_POINT('Ctrl Pts',(181.083507126906,2.22952547955141,126.420481148588));
#24677=CARTESIAN_POINT('Ctrl Pts',(181.076016791144,2.11203748477606,126.360729853018));
#24678=CARTESIAN_POINT('Ctrl Pts',(181.068526455382,1.99229599775392,126.305781227551));
#24679=CARTESIAN_POINT('Ctrl Pts',(181.06103611962,1.87073436242814,126.255785455196));
#24680=CARTESIAN_POINT('Ctrl Pts',(181.053261785501,1.74456368075061,126.203894077936));
#24681=CARTESIAN_POINT('Ctrl Pts',(181.045487451382,1.61603243353411,126.15717416632));
#24682=CARTESIAN_POINT('Ctrl Pts',(181.037713117262,1.48560354270351,126.115846441795));
#24683=CARTESIAN_POINT('Ctrl Pts',(181.029948364315,1.35533539382416,126.074569649997));
#24684=CARTESIAN_POINT('Ctrl Pts',(181.022183611368,1.22317462372418,126.038671939907));
#24685=CARTESIAN_POINT('Ctrl Pts',(181.014418858421,1.08960508849571,126.008326441955));
#24686=CARTESIAN_POINT('Ctrl Pts',(181.006661817536,0.956168216412676,125.97801108358));
#24687=CARTESIAN_POINT('Ctrl Pts',(180.998904776651,0.821325742465903,125.953237049223));
#24688=CARTESIAN_POINT('Ctrl Pts',(180.991147735766,0.685577341742052,125.934127895099));
#24689=CARTESIAN_POINT('Ctrl Pts',(180.983396544526,0.549931309943087,125.915033151336));
#24690=CARTESIAN_POINT('Ctrl Pts',(180.975645353286,0.413381096750075,125.901594839067));
#24691=CARTESIAN_POINT('Ctrl Pts',(180.967894162046,0.276436897019386,125.893885517897));
#24692=CARTESIAN_POINT('Ctrl Pts',(180.960146265269,0.139550902226688,125.886179473395));
#24693=CARTESIAN_POINT('Ctrl Pts',(180.952398368492,0.00227164348105247,
125.884197598944));
#24694=CARTESIAN_POINT('Ctrl Pts',(180.944650471714,-0.134885446705906,
125.887960615657));
#24695=CARTESIAN_POINT('Ctrl Pts',(180.93690419563,-0.272013846586339,125.891722845229));
#24696=CARTESIAN_POINT('Ctrl Pts',(180.929157919546,-0.409019738167906,
125.901227564989));
#24697=CARTESIAN_POINT('Ctrl Pts',(180.921411643462,-0.545387968662936,
125.916443369275));
#24698=CARTESIAN_POINT('Ctrl Pts',(180.913665310197,-0.681757205797242,
125.931659285882));
#24699=CARTESIAN_POINT('Ctrl Pts',(180.905918976931,-0.817488383898427,
125.952586327784));
#24700=CARTESIAN_POINT('Ctrl Pts',(180.898172643666,-0.95207214594684,125.979141276291));
#24701=CARTESIAN_POINT('Ctrl Pts',(180.890424575663,-1.08668604709579,126.005702171595));
#24702=CARTESIAN_POINT('Ctrl Pts',(180.88267650766,-1.22015163738299,126.037893405747));
#24703=CARTESIAN_POINT('Ctrl Pts',(180.874928439657,-1.35197080488857,126.075580858978));
#24704=CARTESIAN_POINT('Ctrl Pts',(180.867172136915,-1.48393007137391,126.113308366883));
#24705=CARTESIAN_POINT('Ctrl Pts',(180.859415834173,-1.61423904308519,126.156543655144));
#24706=CARTESIAN_POINT('Ctrl Pts',(180.851659531431,-1.74241527737747,126.20510284444));
#24707=CARTESIAN_POINT('Ctrl Pts',(180.843899088917,-1.87065992318532,126.253687951238));
#24708=CARTESIAN_POINT('Ctrl Pts',(180.836138646403,-1.99676920408849,126.307602467438));
#24709=CARTESIAN_POINT('Ctrl Pts',(180.828378203889,-2.12028258665798,126.366615152218));
#24710=CARTESIAN_POINT('Ctrl Pts',(180.820605303623,-2.24399424387421,126.425722569399));
#24711=CARTESIAN_POINT('Ctrl Pts',(180.812832403358,-2.3651013298266,126.489944326195));
#24712=CARTESIAN_POINT('Ctrl Pts',(180.805059503092,-2.48316897428491,126.559003752985));
#24713=CARTESIAN_POINT('Ctrl Pts',(180.79756916733,-2.59694456247199,126.62555269566));
#24714=CARTESIAN_POINT('Ctrl Pts',(180.790078831568,-2.707897595887,126.696593525687));
#24715=CARTESIAN_POINT('Ctrl Pts',(180.782588495806,-2.81566748832438,126.771842836118));
#24716=CARTESIAN_POINT('Ctrl Pts',(180.774860431703,-2.92685778253992,126.849480409815));
#24717=CARTESIAN_POINT('Ctrl Pts',(180.7671323676,-3.03502137085671,126.931850825884));
#24718=CARTESIAN_POINT('Ctrl Pts',(180.759404303497,-3.13972510257354,127.018689033452));
#24719=CARTESIAN_POINT('Ctrl Pts',(180.751688447729,-3.24426342957341,127.105390059193));
#24720=CARTESIAN_POINT('Ctrl Pts',(180.743972591961,-3.3453524815515,127.196544571404));
#24721=CARTESIAN_POINT('Ctrl Pts',(180.736256736193,-3.44258800822052,127.291844301852));
#24722=CARTESIAN_POINT('Ctrl Pts',(180.728547930298,-3.53973469210992,127.387056958232));
#24723=CARTESIAN_POINT('Ctrl Pts',(180.720839124402,-3.63303457198762,127.486407025166));
#24724=CARTESIAN_POINT('Ctrl Pts',(180.713130318507,-3.72211626851405,127.589545918993));
#24725=CARTESIAN_POINT('Ctrl Pts',(180.705426833656,-3.81113647592418,127.692613620647));
#24726=CARTESIAN_POINT('Ctrl Pts',(180.697723348805,-3.89594403403888,127.799464648121));
#24727=CARTESIAN_POINT('Ctrl Pts',(180.690019863954,-3.97620460244335,127.909713830476));
#24728=CARTESIAN_POINT('Ctrl Pts',(180.682319975564,-4.05642770026874,128.01991154172));
#24729=CARTESIAN_POINT('Ctrl Pts',(180.674620087175,-4.13210780008793,128.133503931074));
#24730=CARTESIAN_POINT('Ctrl Pts',(180.666920198785,-4.20295133298381,128.250073406803));
#24731=CARTESIAN_POINT('Ctrl Pts',(180.659220735343,-4.27379095611665,128.366636449212));
#24732=CARTESIAN_POINT('Ctrl Pts',(180.6515212719,-4.33979432957215,128.486175917609));
#24733=CARTESIAN_POINT('Ctrl Pts',(180.643821808457,-4.40071176989382,128.608246098508));
#24734=CARTESIAN_POINT('Ctrl Pts',(180.636122680545,-4.46162655553023,128.730310959782));
#24735=CARTESIAN_POINT('Ctrl Pts',(180.628423552633,-4.51745567719539,128.854905956993));
#24736=CARTESIAN_POINT('Ctrl Pts',(180.620724424721,-4.56799625155725,128.981562409245));
#24737=CARTESIAN_POINT('Ctrl Pts',(180.61302142386,-4.61856224971331,129.108282574417));
#24738=CARTESIAN_POINT('Ctrl Pts',(180.605318422999,-4.66383424513525,129.237065895624));
#24739=CARTESIAN_POINT('Ctrl Pts',(180.597615422138,-4.70365818002023,129.367425410944));
#24740=CARTESIAN_POINT('Ctrl Pts',(180.593405538846,-4.72542295989178,129.438670157685));
#24741=CARTESIAN_POINT('Ctrl Pts',(180.589195655555,-4.74556133082426,129.510385423281));
#24742=CARTESIAN_POINT('Ctrl Pts',(180.584985772263,-4.76405452823404,129.582490119308));
#24743=CARTESIAN_POINT('Ctrl Pts',(182.334764431275,-4.76405452823405,129.582490119308));
#24744=CARTESIAN_POINT('Ctrl Pts',(182.327037589112,-4.79807206386625,129.71512397445));
#24745=CARTESIAN_POINT('Ctrl Pts',(182.319310746949,-4.82655566072364,129.849215252561));
#24746=CARTESIAN_POINT('Ctrl Pts',(182.311583904787,-4.84939387740225,129.984261791623));
#24747=CARTESIAN_POINT('Ctrl Pts',(182.303796493321,-4.87241111868681,130.120366935819));
#24748=CARTESIAN_POINT('Ctrl Pts',(182.296009081855,-4.88969399094239,130.257441989725));
#24749=CARTESIAN_POINT('Ctrl Pts',(182.288221670389,-4.90118122870282,130.394963956721));
#24750=CARTESIAN_POINT('Ctrl Pts',(182.280434258923,-4.91266846646326,130.532485923717));
#24751=CARTESIAN_POINT('Ctrl Pts',(182.272646847457,-4.91836005162741,130.670454396298));
#24752=CARTESIAN_POINT('Ctrl Pts',(182.264859435991,-4.91824838731544,130.808343476974));
#24753=CARTESIAN_POINT('',(182.610140564063,-4.91824890646276,130.801080895348));
#24754=CARTESIAN_POINT('Ctrl Pts',(182.679902359578,-4.76405452823405,129.582490119308));
#24755=CARTESIAN_POINT('Ctrl Pts',(182.671073039678,-4.80263856972609,129.732928711491));
#24756=CARTESIAN_POINT('Ctrl Pts',(182.662243719779,-4.83413672793406,129.885367666505));
#24757=CARTESIAN_POINT('Ctrl Pts',(182.65341439988,-4.85836093134102,130.039172978278));
#24758=CARTESIAN_POINT('Ctrl Pts',(182.644641758985,-4.88242962971196,130.19199095106));
#24759=CARTESIAN_POINT('Ctrl Pts',(182.635869118089,-4.89931737459966,130.346157623678));
#24760=CARTESIAN_POINT('Ctrl Pts',(182.627096477193,-4.90888732968651,130.501032005425));
#24761=CARTESIAN_POINT('Ctrl Pts',(182.62144450615,-4.91505298831555,130.600813306337));
#24762=CARTESIAN_POINT('Ctrl Pts',(182.615792535106,-4.91818209306794,130.700887987475));
#24763=CARTESIAN_POINT('Ctrl Pts',(182.610140564063,-4.91824890646276,130.801080895348));
#24764=CARTESIAN_POINT('Ctrl Pts',(182.610140564008,-4.91824890646341,130.80108089632));
#24765=CARTESIAN_POINT('Ctrl Pts',(182.602350736543,-4.91834099197833,130.939171742779));
#24766=CARTESIAN_POINT('Ctrl Pts',(182.594560909078,-4.91261293631802,131.077296116385));
#24767=CARTESIAN_POINT('Ctrl Pts',(182.586771081613,-4.90108295938559,131.214932033668));
#24768=CARTESIAN_POINT('Ctrl Pts',(182.578981013679,-4.88955262652708,131.352572199721));
#24769=CARTESIAN_POINT('Ctrl Pts',(182.571190945745,-4.87222004712722,131.48972349604));
#24770=CARTESIAN_POINT('Ctrl Pts',(182.563400877811,-4.84915540080159,131.625868354217));
#24771=CARTESIAN_POINT('Ctrl Pts',(182.555608953444,-4.82608525799307,131.762045656762));
#24772=CARTESIAN_POINT('Ctrl Pts',(182.547817029077,-4.79728039275426,131.897215664416));
#24773=CARTESIAN_POINT('Ctrl Pts',(182.54002510471,-4.76286219548405,132.030870613175));
#24774=CARTESIAN_POINT('Ctrl Pts',(182.532229707094,-4.72842865631017,132.164585138597));
#24775=CARTESIAN_POINT('Ctrl Pts',(182.524434309478,-4.68837689938111,132.296782888428));
#24776=CARTESIAN_POINT('Ctrl Pts',(182.516638911862,-4.64287820456094,132.42697118086));
#24777=CARTESIAN_POINT('Ctrl Pts',(182.508833566481,-4.59732144851264,132.557325607555));
#24778=CARTESIAN_POINT('Ctrl Pts',(182.501028221099,-4.54630400030386,132.685665092519));
#24779=CARTESIAN_POINT('Ctrl Pts',(182.493222875718,-4.49004557517999,132.811516265568));
#24780=CARTESIAN_POINT('Ctrl Pts',(182.48541197276,-4.43374709282834,132.937457047402));
#24781=CARTESIAN_POINT('Ctrl Pts',(182.477601069802,-4.37220036926214,133.060905643736));
#24782=CARTESIAN_POINT('Ctrl Pts',(182.469790166844,-4.30567070775944,133.181414007552));
#24783=CARTESIAN_POINT('Ctrl Pts',(182.461966709995,-4.23903411801708,133.302116055611));
#24784=CARTESIAN_POINT('Ctrl Pts',(182.454143253146,-4.16739879386563,133.419868104856));
#24785=CARTESIAN_POINT('Ctrl Pts',(182.446319796298,-4.09107330250262,133.534251145783));
#24786=CARTESIAN_POINT('Ctrl Pts',(182.442108278373,-4.04998581634815,133.595825745913));
#24787=CARTESIAN_POINT('Ctrl Pts',(182.437896760449,-4.00753987680767,133.656424612155));
#24788=CARTESIAN_POINT('Ctrl Pts',(182.433685242525,-3.96378825988816,133.715986571097));
#24789=CARTESIAN_POINT('Ctrl Pts',(182.425910908406,-3.88302410446949,133.825936137482));
#24790=CARTESIAN_POINT('Ctrl Pts',(182.418136574287,-3.7975538023016,133.932696893848));
#24791=CARTESIAN_POINT('Ctrl Pts',(182.410362240168,-3.70765790045001,134.035839529106));
#24792=CARTESIAN_POINT('Ctrl Pts',(182.402597487221,-3.61787278726326,134.138855050285));
#24793=CARTESIAN_POINT('Ctrl Pts',(182.394832734273,-3.52367318095091,134.238261030556));
#24794=CARTESIAN_POINT('Ctrl Pts',(182.387067981326,-3.42538226341174,134.333657914763));
#24795=CARTESIAN_POINT('Ctrl Pts',(182.379310940441,-3.32718896979766,134.42896004944));
#24796=CARTESIAN_POINT('Ctrl Pts',(182.371553899556,-3.22491273033872,134.520260741664));
#24797=CARTESIAN_POINT('Ctrl Pts',(182.363796858671,-3.11891602473428,134.607194546777));
#24798=CARTESIAN_POINT('Ctrl Pts',(182.356045667431,-3.01299925206974,134.694062794431));
#24799=CARTESIAN_POINT('Ctrl Pts',(182.348294476191,-2.90336789877549,134.77657046277));
#24800=CARTESIAN_POINT('Ctrl Pts',(182.340543284951,-2.79041995640996,134.854390188985));
#24801=CARTESIAN_POINT('Ctrl Pts',(182.332795388174,-2.67752001993321,134.932176839741));
#24802=CARTESIAN_POINT('Ctrl Pts',(182.325047491397,-2.56130661932331,135.005279289951));
#24803=CARTESIAN_POINT('Ctrl Pts',(182.31729959462,-2.44220918470204,135.073411725325));
#24804=CARTESIAN_POINT('Ctrl Pts',(182.309553318536,-2.32313666269663,135.141529908862));
#24805=CARTESIAN_POINT('Ctrl Pts',(182.301807042451,-2.20118164577595,135.204679951408));
#24806=CARTESIAN_POINT('Ctrl Pts',(182.294060766367,-2.07680044042566,135.262620703423));
#24807=CARTESIAN_POINT('Ctrl Pts',(182.286314433102,-1.95241831692144,135.320561883144));
#24808=CARTESIAN_POINT('Ctrl Pts',(182.278568099837,-1.82561032364971,135.37329353051));
#24809=CARTESIAN_POINT('Ctrl Pts',(182.270821766571,-1.6968547692407,135.420621762108));
#24810=CARTESIAN_POINT('Ctrl Pts',(182.263073698568,-1.56807038091839,135.467960592535));
#24811=CARTESIAN_POINT('Ctrl Pts',(182.255325630565,-1.43733793047416,135.509893464457));
#24812=CARTESIAN_POINT('Ctrl Pts',(182.247577562562,-1.30515260026303,135.546275816357));
#24813=CARTESIAN_POINT('Ctrl Pts',(182.239821259821,-1.17282678190962,135.582696835854));
#24814=CARTESIAN_POINT('Ctrl Pts',(182.232064957079,-1.03904537675643,135.613555447207));
#24815=CARTESIAN_POINT('Ctrl Pts',(182.224308654337,-0.904316068585796,
135.638757737228));
#24816=CARTESIAN_POINT('Ctrl Pts',(182.216548211823,-0.769514851326632,
135.663973478471));
#24817=CARTESIAN_POINT('Ctrl Pts',(182.208787769308,-0.633765109735002,
135.683526827158));
#24818=CARTESIAN_POINT('Ctrl Pts',(182.201027326794,-0.497580452340472,
135.69737571625));
#24819=CARTESIAN_POINT('Ctrl Pts',(182.193254426529,-0.361177179244034,
135.711246836808));
#24820=CARTESIAN_POINT('Ctrl Pts',(182.185481526263,-0.224337985686155,
135.719395175306));
#24821=CARTESIAN_POINT('Ctrl Pts',(182.177708625998,-0.0875781934747493,
135.721830812954));
#24822=CARTESIAN_POINT('Ctrl Pts',(182.170218290236,0.0442100358122264,
135.724177909039));
#24823=CARTESIAN_POINT('Ctrl Pts',(182.162727954474,0.175924228464083,135.72122044237));
#24824=CARTESIAN_POINT('Ctrl Pts',(182.155237618712,0.307109000857396,135.713012889228));
#24825=CARTESIAN_POINT('Ctrl Pts',(182.147463284593,0.443267683768998,135.704494144214));
#24826=CARTESIAN_POINT('Ctrl Pts',(182.139688950474,0.579287317770908,135.690292354947));
#24827=CARTESIAN_POINT('Ctrl Pts',(182.131914616355,0.714655068745021,135.670411500491));
#24828=CARTESIAN_POINT('Ctrl Pts',(182.124149863408,0.849855991064199,135.650555147412));
#24829=CARTESIAN_POINT('Ctrl Pts',(182.116385110461,0.984406245755034,135.625033711212));
#24830=CARTESIAN_POINT('Ctrl Pts',(182.108620357513,1.11779498803749,135.593903124656));
#24831=CARTESIAN_POINT('Ctrl Pts',(182.100863316628,1.25105124674114,135.562803457436));
#24832=CARTESIAN_POINT('Ctrl Pts',(182.093106275743,1.38314791054298,135.526105814856));
#24833=CARTESIAN_POINT('Ctrl Pts',(182.085349234858,1.5135815913709,135.483917629588));
#24834=CARTESIAN_POINT('Ctrl Pts',(182.077598043618,1.64391691114509,135.441761258759));
#24835=CARTESIAN_POINT('Ctrl Pts',(182.069846852378,1.77259137360677,135.39412270641));
#24836=CARTESIAN_POINT('Ctrl Pts',(182.062095661138,1.8991144349961,135.341159866518));
#24837=CARTESIAN_POINT('Ctrl Pts',(182.054347764361,2.02558372070912,135.288219537246));
#24838=CARTESIAN_POINT('Ctrl Pts',(182.046599867584,2.14990306413975,135.229959571943));
#24839=CARTESIAN_POINT('Ctrl Pts',(182.038851970807,2.27159988415978,135.166586772729));
#24840=CARTESIAN_POINT('Ctrl Pts',(182.031105694723,2.39327124782866,135.103227229737));
#24841=CARTESIAN_POINT('Ctrl Pts',(182.023359418639,2.51232083268777,135.034757160578));
#24842=CARTESIAN_POINT('Ctrl Pts',(182.015613142554,2.62829910799688,134.961430121604));
#24843=CARTESIAN_POINT('Ctrl Pts',(182.007866809289,2.74427823943102,134.888102541346));
#24844=CARTESIAN_POINT('Ctrl Pts',(182.000120476024,2.85718568561855,134.809918128662));
#24845=CARTESIAN_POINT('Ctrl Pts',(181.992374142758,2.96659978945404,134.727174499426));
#24846=CARTESIAN_POINT('Ctrl Pts',(181.984626074756,3.07603839581934,134.644412340328));
#24847=CARTESIAN_POINT('Ctrl Pts',(181.976878006753,3.18198179135113,134.557089168775));
#24848=CARTESIAN_POINT('Ctrl Pts',(181.96912993875,3.28404069419147,134.465543456676));
#24849=CARTESIAN_POINT('Ctrl Pts',(181.961373636008,3.3862080664486,134.373900448704));
#24850=CARTESIAN_POINT('Ctrl Pts',(181.953617333266,3.48448240741909,134.278026196862));
#24851=CARTESIAN_POINT('Ctrl Pts',(181.945861030524,3.57851028979258,134.178297067523));
#24852=CARTESIAN_POINT('Ctrl Pts',(181.93810058801,3.67258835767799,134.078514709744));
#24853=CARTESIAN_POINT('Ctrl Pts',(181.930340145496,3.76241519491009,133.974873670094));
#24854=CARTESIAN_POINT('Ctrl Pts',(181.922579702982,3.84767779134117,133.86778332371));
#24855=CARTESIAN_POINT('Ctrl Pts',(181.914806802716,3.93307725886131,133.760521066396));
#24856=CARTESIAN_POINT('Ctrl Pts',(181.907033902451,4.01389761341318,133.64979875336));
#24857=CARTESIAN_POINT('Ctrl Pts',(181.899261002185,4.08986879258137,133.536055388577));
#24858=CARTESIAN_POINT('Ctrl Pts',(181.891770666423,4.16307822802756,133.426446881605));
#24859=CARTESIAN_POINT('Ctrl Pts',(181.884280330661,4.23178476598698,133.314033418012));
#24860=CARTESIAN_POINT('Ctrl Pts',(181.876789994899,4.29578809292371,133.199227570696));
#24861=CARTESIAN_POINT('Ctrl Pts',(181.86901566078,4.36221812545415,133.080068824786));
#24862=CARTESIAN_POINT('Ctrl Pts',(181.861241326661,4.42379169257108,132.957955240427));
#24863=CARTESIAN_POINT('Ctrl Pts',(181.853466992542,4.480234942605,132.833320430268));
#24864=CARTESIAN_POINT('Ctrl Pts',(181.845702239595,4.53660863137767,132.708839221374));
#24865=CARTESIAN_POINT('Ctrl Pts',(181.837937486648,4.5878644235316,132.58184332178));
#24866=CARTESIAN_POINT('Ctrl Pts',(181.8301727337,4.63377325280224,132.452792752692));
#24867=CARTESIAN_POINT('Ctrl Pts',(181.822415692815,4.67963648477647,132.323870358447));
#24868=CARTESIAN_POINT('Ctrl Pts',(181.81465865193,4.72016319216763,132.192897721815));
#24869=CARTESIAN_POINT('Ctrl Pts',(181.806901611045,4.75517166757724,132.06035642742));
#24870=CARTESIAN_POINT('Ctrl Pts',(181.799150419805,4.7901537428232,131.927915083446));
#24871=CARTESIAN_POINT('Ctrl Pts',(181.791399228565,4.81962576954726,131.793907812746));
#24872=CARTESIAN_POINT('Ctrl Pts',(181.783648037325,4.84345543753907,131.658832669229));
#24873=CARTESIAN_POINT('Ctrl Pts',(181.775900140548,4.86727497728632,131.523814936251));
#24874=CARTESIAN_POINT('Ctrl Pts',(181.768152243771,4.88545686026262,131.387730617391));
#24875=CARTESIAN_POINT('Ctrl Pts',(181.760404346994,4.8979196333033,131.251089090133));
#24876=CARTESIAN_POINT('Ctrl Pts',(181.75265807091,4.91037979940052,131.114476145337));
#24877=CARTESIAN_POINT('Ctrl Pts',(181.744911794826,4.91712319960808,130.97730661308));
#24878=CARTESIAN_POINT('Ctrl Pts',(181.737165518741,4.91812017572067,130.840095749709));
#24879=CARTESIAN_POINT('Ctrl Pts',(181.729419185476,4.91911715919271,130.702883873479));
#24880=CARTESIAN_POINT('Ctrl Pts',(181.721672852211,4.91436763108547,130.565631056479));
#24881=CARTESIAN_POINT('Ctrl Pts',(181.713926518945,4.90389406809912,130.428852919426));
#24882=CARTESIAN_POINT('Ctrl Pts',(181.706178450942,4.89341815963096,130.292044151858));
#24883=CARTESIAN_POINT('Ctrl Pts',(181.698430382939,4.87721569537927,130.155710665513));
#24884=CARTESIAN_POINT('Ctrl Pts',(181.690682314937,4.85536102499316,130.020362926576));
#24885=CARTESIAN_POINT('Ctrl Pts',(181.682926012195,4.83348312720327,129.884871338452));
#24886=CARTESIAN_POINT('Ctrl Pts',(181.675169709453,4.80594108560759,129.75036797714));
#24887=CARTESIAN_POINT('Ctrl Pts',(181.667413406711,4.77286051180006,129.617353626264));
#24888=CARTESIAN_POINT('Ctrl Pts',(181.659652964197,4.73976228189421,129.484268281624));
#24889=CARTESIAN_POINT('Ctrl Pts',(181.651892521683,4.70111973963549,129.352673905927));
#24890=CARTESIAN_POINT('Ctrl Pts',(181.644132079168,4.65710811429238,129.22305512074));
#24891=CARTESIAN_POINT('Ctrl Pts',(181.636359178903,4.61302583758112,129.093228259972));
#24892=CARTESIAN_POINT('Ctrl Pts',(181.628586278637,4.5635573955876,128.965383691997));
#24893=CARTESIAN_POINT('Ctrl Pts',(181.620813378372,4.5089261594554,128.839985920346));
#24894=CARTESIAN_POINT('Ctrl Pts',(181.61332304261,4.45628090636462,128.719146673552));
#24895=CARTESIAN_POINT('Ctrl Pts',(181.605832706848,4.39884183774708,128.600579694375));
#24896=CARTESIAN_POINT('Ctrl Pts',(181.598342371086,4.33684778850805,128.484676517993));
#24897=CARTESIAN_POINT('Ctrl Pts',(181.590568036967,4.27250321604925,128.36437883745));
#24898=CARTESIAN_POINT('Ctrl Pts',(181.582793702848,4.20304761613661,128.246569876445));
#24899=CARTESIAN_POINT('Ctrl Pts',(181.575019368729,4.12869777585513,128.13171441237));
#24900=CARTESIAN_POINT('Ctrl Pts',(181.567254615782,4.05443956510713,128.01700049739));
#24901=CARTESIAN_POINT('Ctrl Pts',(181.559489862835,3.97529932571951,127.905233162034));
#24902=CARTESIAN_POINT('Ctrl Pts',(181.551725109888,3.89154027064978,127.796853778935));
#24903=CARTESIAN_POINT('Ctrl Pts',(181.543968069003,3.80786440625398,127.688582039767));
#24904=CARTESIAN_POINT('Ctrl Pts',(181.536211028118,3.71957909298195,127.583691863779));
#24905=CARTESIAN_POINT('Ctrl Pts',(181.528453987233,3.62699128433114,127.482596434803));
#24906=CARTESIAN_POINT('Ctrl Pts',(181.520702795992,3.5344732968673,127.381577242677));
#24907=CARTESIAN_POINT('Ctrl Pts',(181.512951604752,3.43765953508295,127.28434738878));
#24908=CARTESIAN_POINT('Ctrl Pts',(181.505200413512,3.33689750893684,127.191287399743));
#24909=CARTESIAN_POINT('Ctrl Pts',(181.497452516735,3.23617830933978,127.098266963683));
#24910=CARTESIAN_POINT('Ctrl Pts',(181.489704619958,3.13151446964089,127.00941313221));
#24911=CARTESIAN_POINT('Ctrl Pts',(181.481956723181,3.02329051611814,126.925069765149));
#24912=CARTESIAN_POINT('Ctrl Pts',(181.474210447097,2.91508920071343,126.840744040902));
#24913=CARTESIAN_POINT('Ctrl Pts',(181.466464171013,2.80332956091226,126.760927144587));
#24914=CARTESIAN_POINT('Ctrl Pts',(181.458717894929,2.688429065486,126.685922537134));
#24915=CARTESIAN_POINT('Ctrl Pts',(181.450971561663,2.57352772189059,126.610917376014));
#24916=CARTESIAN_POINT('Ctrl Pts',(181.443225228398,2.45548580379192,126.54072478835));
#24917=CARTESIAN_POINT('Ctrl Pts',(181.435478895133,2.33474926670635,126.475604569448));
#24918=CARTESIAN_POINT('Ctrl Pts',(181.42773082713,2.21398569151045,126.410469767325));
#24919=CARTESIAN_POINT('Ctrl Pts',(181.419982759127,2.0905266405883,126.350409779878));
#24920=CARTESIAN_POINT('Ctrl Pts',(181.412234691124,1.96484177140072,126.295637974083));
#24921=CARTESIAN_POINT('Ctrl Pts',(181.404478388382,1.83902332283823,126.240807956161));
#24922=CARTESIAN_POINT('Ctrl Pts',(181.39672208564,1.71097468939951,126.19127750357));
#24923=CARTESIAN_POINT('Ctrl Pts',(181.388965782898,1.58118509066446,126.1472116215));
#24924=CARTESIAN_POINT('Ctrl Pts',(181.381205340384,1.45132621931234,126.103122220142));
#24925=CARTESIAN_POINT('Ctrl Pts',(181.37344489787,1.31972490610537,126.064503310922));
#24926=CARTESIAN_POINT('Ctrl Pts',(181.365684455356,1.18688359259093,126.031469418289));
#24927=CARTESIAN_POINT('Ctrl Pts',(181.35791155509,1.05382903040709,125.998382496718));
#24928=CARTESIAN_POINT('Ctrl Pts',(181.350138654825,0.919530873392618,125.970898586219));
#24929=CARTESIAN_POINT('Ctrl Pts',(181.342365754559,0.784500659081397,125.949080833825));
#24930=CARTESIAN_POINT('Ctrl Pts',(181.334875418797,0.65437913317976,125.928056211687));
#24931=CARTESIAN_POINT('Ctrl Pts',(181.327385083035,0.523578155989451,125.912292978468));
#24932=CARTESIAN_POINT('Ctrl Pts',(181.319894747273,0.39255623324671,125.901801829929));
#24933=CARTESIAN_POINT('Ctrl Pts',(181.312120413154,0.256566574481517,125.890912906304));
#24934=CARTESIAN_POINT('Ctrl Pts',(181.304346079035,0.119908110764656,125.885669248528));
#24935=CARTESIAN_POINT('Ctrl Pts',(181.296571744916,-0.0169109488048534,
125.88613969102));
#24936=CARTESIAN_POINT('Ctrl Pts',(181.288806991969,-0.153561391111778,
125.886609553735));
#24937=CARTESIAN_POINT('Ctrl Pts',(181.281042239022,-0.290371648259795,
125.892779503671));
#24938=CARTESIAN_POINT('Ctrl Pts',(181.273277486075,-0.426828107918584,
125.904666665002));
#24939=CARTESIAN_POINT('Ctrl Pts',(181.26552044519,-0.563149037097825,125.916542019838));
#24940=CARTESIAN_POINT('Ctrl Pts',(181.257763404305,-0.699116481113278,
125.934123252056));
#24941=CARTESIAN_POINT('Ctrl Pts',(181.25000636342,-0.834216900840216,125.957375448943));
#24942=CARTESIAN_POINT('Ctrl Pts',(181.242255172179,-0.969215440289043,
125.980610111167));
#24943=CARTESIAN_POINT('Ctrl Pts',(181.234503980939,-1.1033478731167,126.009507159861));
#24944=CARTESIAN_POINT('Ctrl Pts',(181.226752789699,-1.23610621387061,126.043979908995));
#24945=CARTESIAN_POINT('Ctrl Pts',(181.219004892922,-1.36880812878891,126.078438006292));
#24946=CARTESIAN_POINT('Ctrl Pts',(181.211256996145,-1.50013673559273,126.118466992577));
#24947=CARTESIAN_POINT('Ctrl Pts',(181.203509099368,-1.62959488942576,126.16392921964));
#24948=CARTESIAN_POINT('Ctrl Pts',(181.195762823284,-1.75902596340384,126.209381936985));
#24949=CARTESIAN_POINT('Ctrl Pts',(181.1880165472,-1.88658699399867,126.260265505053));
#24950=CARTESIAN_POINT('Ctrl Pts',(181.180270271116,-2.01179701886858,126.316392723589));
#24951=CARTESIAN_POINT('Ctrl Pts',(181.17252393785,-2.13700796800998,126.372520356442));
#24952=CARTESIAN_POINT('Ctrl Pts',(181.164777604585,-2.25986752003577,126.433891557078));
#24953=CARTESIAN_POINT('Ctrl Pts',(181.15703127132,-2.37991605194676,126.500271556198));
#24954=CARTESIAN_POINT('Ctrl Pts',(181.149283203317,-2.49999146789432,126.566666420659));
#24955=CARTESIAN_POINT('Ctrl Pts',(181.141535135314,-2.61725426899975,126.63807212648));
#24956=CARTESIAN_POINT('Ctrl Pts',(181.133787067311,-2.73127108225299,126.7142088676));
#24957=CARTESIAN_POINT('Ctrl Pts',(181.126030764569,-2.8454090739322,126.790426527755));
#24958=CARTESIAN_POINT('Ctrl Pts',(181.118274461827,-2.95629386060742,126.871385050119));
#24959=CARTESIAN_POINT('Ctrl Pts',(181.110518159085,-3.06352218360704,126.956762029739));
#24960=CARTESIAN_POINT('Ctrl Pts',(181.102757716571,-3.17080773759117,127.042184577624));
#24961=CARTESIAN_POINT('Ctrl Pts',(181.094997274057,-3.27443264399057,127.132030025815));
#24962=CARTESIAN_POINT('Ctrl Pts',(181.087236831543,-3.37402896821536,127.22593755927));
#24963=CARTESIAN_POINT('Ctrl Pts',(181.079463931278,-3.4737851733016,127.319995841434));
#24964=CARTESIAN_POINT('Ctrl Pts',(181.071691031012,-3.56949959987051,127.418128959495));
#24965=CARTESIAN_POINT('Ctrl Pts',(181.063918130747,-3.66084262200152,127.519940674953));
#24966=CARTESIAN_POINT('Ctrl Pts',(181.056427794985,-3.7488650952,127.618051278106));
#24967=CARTESIAN_POINT('Ctrl Pts',(181.048937459222,-3.83282827290767,127.7195774321));
#24968=CARTESIAN_POINT('Ctrl Pts',(181.04144712346,-3.9124753229297,127.824139164391));
#24969=CARTESIAN_POINT('Ctrl Pts',(181.033651562904,-3.99536792231622,127.932961698101));
#24970=CARTESIAN_POINT('Ctrl Pts',(181.025856002347,-4.07385081342254,128.045421065337));
#24971=CARTESIAN_POINT('Ctrl Pts',(181.018060441791,-4.14758872176929,128.161125694682));
#24972=CARTESIAN_POINT('Ctrl Pts',(181.01027762814,-4.22120605762,128.276641129674));
#24973=CARTESIAN_POINT('Ctrl Pts',(181.00249481449,-4.29009365664689,128.395390934063));
#24974=CARTESIAN_POINT('Ctrl Pts',(180.994712000839,-4.35395702277294,128.516951317431));
#24975=CARTESIAN_POINT('Ctrl Pts',(180.986936519403,-4.41776022301778,128.638397178372));
#24976=CARTESIAN_POINT('Ctrl Pts',(180.979161037966,-4.47654842553653,128.762648010892));
#24977=CARTESIAN_POINT('Ctrl Pts',(180.971385556529,-4.53007071000093,128.889251632445));
#24978=CARTESIAN_POINT('Ctrl Pts',(180.963616832862,-4.58354647756522,129.015745221175));
#24979=CARTESIAN_POINT('Ctrl Pts',(180.955848109195,-4.63176528846851,129.144587172));
#24980=CARTESIAN_POINT('Ctrl Pts',(180.948079385529,-4.67452267920003,129.275301827282));
#24981=CARTESIAN_POINT('Ctrl Pts',(180.942056030262,-4.70767393617805,129.376649338295));
#24982=CARTESIAN_POINT('Ctrl Pts',(180.936032674994,-4.73754299834085,129.479122066623));
#24983=CARTESIAN_POINT('Ctrl Pts',(180.930009319727,-4.76405452823405,129.582490119308));
#24984=CARTESIAN_POINT('Origin',(213.235140564004,0.,130.804360617566));
#24985=CARTESIAN_POINT('',(178.834794689177,-4.76405452823405,129.582490119308));
#24986=CARTESIAN_POINT('',(179.180279212536,-4.76405452823405,129.582490119308));
#24987=CARTESIAN_POINT('',(213.235140564004,-4.76405452823405,129.582490119308));
#24988=CARTESIAN_POINT('',(180.514859436037,-4.91824986164052,130.805527225028));
#24989=CARTESIAN_POINT('Ctrl Pts',(180.514859435991,-4.91824986164033,130.805527225829));
#24990=CARTESIAN_POINT('Ctrl Pts',(180.511286581325,-4.91823498623681,130.86823975205));
#24991=CARTESIAN_POINT('Ctrl Pts',(180.507713726659,-4.91702069103772,130.930936615505));
#24992=CARTESIAN_POINT('Ctrl Pts',(180.504140871993,-4.9146084703115,130.993587058748));
#24993=CARTESIAN_POINT('Ctrl Pts',(180.496366537874,-4.90935961144405,131.129910957714));
#24994=CARTESIAN_POINT('Ctrl Pts',(180.488592203755,-4.89842600811054,131.266232225206));
#24995=CARTESIAN_POINT('Ctrl Pts',(180.480817869636,-4.88179933162287,131.402038079301));
#24996=CARTESIAN_POINT('Ctrl Pts',(180.473053116689,-4.86519314602801,131.537676564819));
#24997=CARTESIAN_POINT('Ctrl Pts',(180.465288363742,-4.84290789448837,131.672800516459));
#24998=CARTESIAN_POINT('Ctrl Pts',(180.457523610795,-4.81498723479294,131.80689789432));
#24999=CARTESIAN_POINT('Ctrl Pts',(180.44976656991,-4.78709430629035,131.940862084775));
#25000=CARTESIAN_POINT('Ctrl Pts',(180.442009529025,-4.75357718742527,132.073801350235));
#25001=CARTESIAN_POINT('Ctrl Pts',(180.43425248814,-4.714531200007,132.205209869506));
#25002=CARTESIAN_POINT('Ctrl Pts',(180.4265012969,-4.67551465747153,132.33651929259));
#25003=CARTESIAN_POINT('Ctrl Pts',(180.41875010566,-4.63097765615341,132.466299893888));
#25004=CARTESIAN_POINT('Ctrl Pts',(180.41099891442,-4.58106627286169,132.594057481884));
#25005=CARTESIAN_POINT('Ctrl Pts',(180.403251017643,-4.53117610323931,132.721760769497));
#25006=CARTESIAN_POINT('Ctrl Pts',(180.395503120866,-4.47591623682387,132.847442390555));
#25007=CARTESIAN_POINT('Ctrl Pts',(180.387755224089,-4.41548207553511,132.970624937341));
#25008=CARTESIAN_POINT('Ctrl Pts',(180.380008948005,-4.35506055577006,133.093781716993));
#25009=CARTESIAN_POINT('Ctrl Pts',(180.37226267192,-4.28946706608026,133.21444011138));
#25010=CARTESIAN_POINT('Ctrl Pts',(180.364516395836,-4.21894430230164,133.332144634561));
#25011=CARTESIAN_POINT('Ctrl Pts',(180.356770062571,-4.14842101794008,133.449850026611));
#25012=CARTESIAN_POINT('Ctrl Pts',(180.349023729306,-4.07296858782303,133.56460116857));
#25013=CARTESIAN_POINT('Ctrl Pts',(180.34127739604,-3.99287442351235,133.675969382799));
#25014=CARTESIAN_POINT('Ctrl Pts',(180.333529328037,-3.91276232266898,133.787362537167));
#25015=CARTESIAN_POINT('Ctrl Pts',(180.325781260035,-3.82800664740718,133.895370938959));
#25016=CARTESIAN_POINT('Ctrl Pts',(180.318033192032,-3.73893643047199,133.999597296028));
#25017=CARTESIAN_POINT('Ctrl Pts',(180.31027688929,-3.64977154865013,134.10393442611));
#25018=CARTESIAN_POINT('Ctrl Pts',(180.302520586548,-3.55628321943548,134.204481184188));
#25019=CARTESIAN_POINT('Ctrl Pts',(180.294764283806,-3.45883921953503,134.300875212975));
#25020=CARTESIAN_POINT('Ctrl Pts',(180.287003841292,-3.36134321083779,134.397320690157));
#25021=CARTESIAN_POINT('Ctrl Pts',(180.279243398778,-3.25988761365962,134.489608758661));
#25022=CARTESIAN_POINT('Ctrl Pts',(180.271482956264,-3.15487417386967,134.577416674604));
#25023=CARTESIAN_POINT('Ctrl Pts',(180.263710055998,-3.04969215718354,134.665365547608));
#25024=CARTESIAN_POINT('Ctrl Pts',(180.255937155733,-2.94094119510187,134.748819658113));
#25025=CARTESIAN_POINT('Ctrl Pts',(180.248164255467,-2.82905368442206,134.827498486588));
#25026=CARTESIAN_POINT('Ctrl Pts',(180.240673919705,-2.72123356658074,134.90331714147));
#25027=CARTESIAN_POINT('Ctrl Pts',(180.233183583943,-2.61050124275258,134.974701506813));
#25028=CARTESIAN_POINT('Ctrl Pts',(180.225693248181,-2.49726436005296,135.041441426155));
#25029=CARTESIAN_POINT('Ctrl Pts',(180.217918914062,-2.37973406653057,135.110711809822));
#25030=CARTESIAN_POINT('Ctrl Pts',(180.210144579943,-2.259133243701,135.175198034593));
#25031=CARTESIAN_POINT('Ctrl Pts',(180.202370245824,-2.13588880765785,135.234615922153));
#25032=CARTESIAN_POINT('Ctrl Pts',(180.194605492877,-2.01279625936746,135.293960582477));
#25033=CARTESIAN_POINT('Ctrl Pts',(180.186840739929,-1.88706692913862,135.348249165653));
#25034=CARTESIAN_POINT('Ctrl Pts',(180.179075986982,-1.75915520874346,135.397241632142));
#25035=CARTESIAN_POINT('Ctrl Pts',(180.171318946097,-1.63137053207232,135.446185438622));
#25036=CARTESIAN_POINT('Ctrl Pts',(180.163561905212,-1.5014081415564,135.48984345747));
#25037=CARTESIAN_POINT('Ctrl Pts',(180.155804864327,-1.36974512266039,135.528022476913));
#25038=CARTESIAN_POINT('Ctrl Pts',(180.148053673087,-1.23818139187112,135.56617270526));
#25039=CARTESIAN_POINT('Ctrl Pts',(180.140302481847,-1.10491995933232,135.598852049766));
#25040=CARTESIAN_POINT('Ctrl Pts',(180.132551290607,-0.970455560445589,
135.625916286404));
#25041=CARTESIAN_POINT('Ctrl Pts',(180.12480339383,-0.836048312515253,135.652969020018));
#25042=CARTESIAN_POINT('Ctrl Pts',(180.117055497053,-0.700439497635642,
135.674411315488));
#25043=CARTESIAN_POINT('Ctrl Pts',(180.109307600276,-0.564136391950636,
135.69014951945));
#25044=CARTESIAN_POINT('Ctrl Pts',(180.101561324192,-0.427861797936961,
135.705884431319));
#25045=CARTESIAN_POINT('Ctrl Pts',(180.093815048108,-0.290893590128375,
135.71591758015));
#25046=CARTESIAN_POINT('Ctrl Pts',(180.086068772024,-0.153746164773559,
135.720206951547));
#25047=CARTESIAN_POINT('Ctrl Pts',(180.078322438758,-0.0165977270276053,
135.724496354607));
#25048=CARTESIAN_POINT('Ctrl Pts',(180.070576105493,0.120729540130282,135.723041883407));
#25049=CARTESIAN_POINT('Ctrl Pts',(180.062829772227,0.257719625092028,135.715853634699));
#25050=CARTESIAN_POINT('Ctrl Pts',(180.055081704225,0.394740388033409,135.708663776232));
#25051=CARTESIAN_POINT('Ctrl Pts',(180.047333636222,0.531423428169907,135.695737605649));
#25052=CARTESIAN_POINT('Ctrl Pts',(180.039585568219,0.667256642130682,135.677137201407));
#25053=CARTESIAN_POINT('Ctrl Pts',(180.031829265477,0.803234221247715,135.658517028435));
#25054=CARTESIAN_POINT('Ctrl Pts',(180.024072962735,0.93835978197096,135.634210628072));
#25055=CARTESIAN_POINT('Ctrl Pts',(180.016316659993,1.07212967055861,135.604331558312));
#25056=CARTESIAN_POINT('Ctrl Pts',(180.008556217479,1.20597095616365,135.574436541194));
#25057=CARTESIAN_POINT('Ctrl Pts',(180.000795774965,1.33845475039577,135.538963029203));
#25058=CARTESIAN_POINT('Ctrl Pts',(179.99303533245,1.46909236623006,135.498074571567));
#25059=CARTESIAN_POINT('Ctrl Pts',(179.985262432185,1.59993969316269,135.457120476149));
#25060=CARTESIAN_POINT('Ctrl Pts',(179.97748953192,1.72893455126841,135.41073419697));
#25061=CARTESIAN_POINT('Ctrl Pts',(179.969716631654,1.85560721049188,135.359127894044));
#25062=CARTESIAN_POINT('Ctrl Pts',(179.962226295892,1.97767499948376,135.309397610217));
#25063=CARTESIAN_POINT('Ctrl Pts',(179.95473596013,2.09758621357152,135.254820363207));
#25064=CARTESIAN_POINT('Ctrl Pts',(179.947245624368,2.21494369894812,135.195625523375));
#25065=CARTESIAN_POINT('Ctrl Pts',(179.939471290249,2.33675082905244,135.134186293199));
#25066=CARTESIAN_POINT('Ctrl Pts',(179.93169695613,2.45619260687545,135.067577785012));
#25067=CARTESIAN_POINT('Ctrl Pts',(179.923922622011,2.57279918657586,134.996005570094));
#25068=CARTESIAN_POINT('Ctrl Pts',(179.916157869064,2.68926205908817,134.924521561534));
#25069=CARTESIAN_POINT('Ctrl Pts',(179.908393116117,2.8028963557451,134.848086220452));
#25070=CARTESIAN_POINT('Ctrl Pts',(179.900628363169,2.9132545146317,134.76695209228));
#25071=CARTESIAN_POINT('Ctrl Pts',(179.892871322284,3.02350306423898,134.685898547668));
#25072=CARTESIAN_POINT('Ctrl Pts',(179.8851142814,3.1304816385372,134.600155733395));
#25073=CARTESIAN_POINT('Ctrl Pts',(179.877357240515,3.2337698066414,134.51002059929));
#25074=CARTESIAN_POINT('Ctrl Pts',(179.869606049274,3.33698008433468,134.419953436792));
#25075=CARTESIAN_POINT('Ctrl Pts',(179.861854858034,3.43650520177386,134.32550080338));
#25076=CARTESIAN_POINT('Ctrl Pts',(179.854103666794,3.53195640262972,134.22700097735));
#25077=CARTESIAN_POINT('Ctrl Pts',(179.846355770017,3.627367034179,134.128543016374));
#25078=CARTESIAN_POINT('Ctrl Pts',(179.83860787324,3.71870692150715,134.026041564233));
#25079=CARTESIAN_POINT('Ctrl Pts',(179.830859976463,3.8056230762406,133.919872784784));
#25080=CARTESIAN_POINT('Ctrl Pts',(179.823113700379,3.89252104998818,133.813726213555));
#25081=CARTESIAN_POINT('Ctrl Pts',(179.815367424295,3.97499688420821,133.703914143201));
#25082=CARTESIAN_POINT('Ctrl Pts',(179.807621148211,4.05273718726214,133.590846640047));
#25083=CARTESIAN_POINT('Ctrl Pts',(179.799874814945,4.13047806417734,133.477778302254));
#25084=CARTESIAN_POINT('Ctrl Pts',(179.79212848168,4.20348311866762,133.361454805873));
#25085=CARTESIAN_POINT('Ctrl Pts',(179.784382148415,4.27148192853796,133.242315743624));
#25086=CARTESIAN_POINT('Ctrl Pts',(179.776634080412,4.33949596627027,133.123150001009));
#25087=CARTESIAN_POINT('Ctrl Pts',(179.768886012409,4.40250133473337,133.001167777338));
#25088=CARTESIAN_POINT('Ctrl Pts',(179.761137944406,4.4602734579108,132.876833474603));
#25089=CARTESIAN_POINT('Ctrl Pts',(179.753381641664,4.51810698198826,132.752367027892));
#25090=CARTESIAN_POINT('Ctrl Pts',(179.745625338922,4.57069598516582,132.625543863588));
#25091=CARTESIAN_POINT('Ctrl Pts',(179.73786903618,4.61786376985074,132.496849100717));
#25092=CARTESIAN_POINT('Ctrl Pts',(179.730108593666,4.66505672940257,132.368085649577));
#25093=CARTESIAN_POINT('Ctrl Pts',(179.722348151152,4.7068225859822,132.237448981634));
#25094=CARTESIAN_POINT('Ctrl Pts',(179.714587708638,4.74303479091117,132.105438645474));
#25095=CARTESIAN_POINT('Ctrl Pts',(179.706814808372,4.77930512688626,131.973216394604));
#25096=CARTESIAN_POINT('Ctrl Pts',(179.699041908107,4.81000390816578,131.839616450211));
#25097=CARTESIAN_POINT('Ctrl Pts',(179.691269007841,4.83505573040974,131.705148687165));
#25098=CARTESIAN_POINT('Ctrl Pts',(179.683778672079,4.85919685581355,131.575569166008));
#25099=CARTESIAN_POINT('Ctrl Pts',(179.676288336317,4.8780944124047,131.445184130401));
#25100=CARTESIAN_POINT('Ctrl Pts',(179.668798000555,4.89172670463108,131.314451697373));
#25101=CARTESIAN_POINT('Ctrl Pts',(179.661023666436,4.90587586936059,131.178762504413));
#25102=CARTESIAN_POINT('Ctrl Pts',(179.653249332317,4.91439744341293,131.042269228285));
#25103=CARTESIAN_POINT('Ctrl Pts',(179.645474998198,4.917210416574,130.905478279901));
#25104=CARTESIAN_POINT('Ctrl Pts',(179.637710245251,4.92001992299706,130.768855914136));
#25105=CARTESIAN_POINT('Ctrl Pts',(179.629945492304,4.91713481879837,130.631936993176));
#25106=CARTESIAN_POINT('Ctrl Pts',(179.622180739356,4.9085256594554,130.495234570511));
#25107=CARTESIAN_POINT('Ctrl Pts',(179.614423698471,4.89992505085085,130.358667922619));
#25108=CARTESIAN_POINT('Ctrl Pts',(179.606666657586,4.88561172534523,130.222317732772));
#25109=CARTESIAN_POINT('Ctrl Pts',(179.598909616701,4.86560826207741,130.086698230016));
#25110=CARTESIAN_POINT('Ctrl Pts',(179.591158425461,4.84561988357684,129.951180998982));
#25111=CARTESIAN_POINT('Ctrl Pts',(179.583407234221,4.81994996506197,129.81639374349));
#25112=CARTESIAN_POINT('Ctrl Pts',(179.575656042981,4.78867297735071,129.68284638293));
#25113=CARTESIAN_POINT('Ctrl Pts',(179.567908146204,4.75740928319356,129.549355783561));
#25114=CARTESIAN_POINT('Ctrl Pts',(179.560160249427,4.7205433487172,129.417104410853));
#25115=CARTESIAN_POINT('Ctrl Pts',(179.55241235265,4.67820085238921,129.286592569673));
#25116=CARTESIAN_POINT('Ctrl Pts',(179.544666076566,4.63586721319865,129.156108028757));
#25117=CARTESIAN_POINT('Ctrl Pts',(179.536919800482,4.58805941135035,129.027362667255));
#25118=CARTESIAN_POINT('Ctrl Pts',(179.529173524397,4.53495305142171,128.900841801294));
#25119=CARTESIAN_POINT('Ctrl Pts',(179.521427191132,4.48184629947401,128.774320001385));
#25120=CARTESIAN_POINT('Ctrl Pts',(179.513680857867,4.42344106271525,128.650023090278));
#25121=CARTESIAN_POINT('Ctrl Pts',(179.505934524601,4.35996101314982,128.528416192429));
#25122=CARTESIAN_POINT('Ctrl Pts',(179.498186456598,4.29646674766747,128.406782061558));
#25123=CARTESIAN_POINT('Ctrl Pts',(179.490438388595,4.22789558882288,128.28783948919));
#25124=CARTESIAN_POINT('Ctrl Pts',(179.482690320592,4.15451686234194,128.172028438107));
#25125=CARTESIAN_POINT('Ctrl Pts',(179.474934017851,4.08106014807724,128.056094301661));
#25126=CARTESIAN_POINT('Ctrl Pts',(179.467177715109,4.00278586890444,127.943298665755));
#25127=CARTESIAN_POINT('Ctrl Pts',(179.459421412367,3.92000665983544,127.834052409762));
#25128=CARTESIAN_POINT('Ctrl Pts',(179.451660969853,3.83718326901008,127.724747845754));
#25129=CARTESIAN_POINT('Ctrl Pts',(179.443900527339,3.74985040611597,127.618996737741));
#25130=CARTESIAN_POINT('Ctrl Pts',(179.436140084824,3.65835995287435,127.517175572926));
#25131=CARTESIAN_POINT('Ctrl Pts',(179.428367184559,3.56672263103505,127.415190955737));
#25132=CARTESIAN_POINT('Ctrl Pts',(179.420594284294,3.47091465521116,127.317149168308));
#25133=CARTESIAN_POINT('Ctrl Pts',(179.412821384028,3.37132423968277,127.223389250265));
#25134=CARTESIAN_POINT('Ctrl Pts',(179.405331048266,3.27535418661257,127.133037741411));
#25135=CARTESIAN_POINT('Ctrl Pts',(179.397840712504,3.17587215439751,127.046662395268));
#25136=CARTESIAN_POINT('Ctrl Pts',(179.390350376742,3.07325184289293,126.964529088364));
#25137=CARTESIAN_POINT('Ctrl Pts',(179.382576042623,2.96674065108638,126.879281672164));
#25138=CARTESIAN_POINT('Ctrl Pts',(179.374801708504,2.85651111111605,126.798334280789));
#25139=CARTESIAN_POINT('Ctrl Pts',(179.367027374385,2.74294549282422,126.722028797895));
#25140=CARTESIAN_POINT('Ctrl Pts',(179.359262621438,2.62951983400729,126.645817354689));
#25141=CARTESIAN_POINT('Ctrl Pts',(179.351497868491,2.51276659876644,126.574236653353));
#25142=CARTESIAN_POINT('Ctrl Pts',(179.343733115544,2.39310151804933,126.507588784339));
#25143=CARTESIAN_POINT('Ctrl Pts',(179.335976074659,2.27355529037732,126.441007110929));
#25144=CARTESIAN_POINT('Ctrl Pts',(179.328219033774,2.15110331196261,126.3793487089));
#25145=CARTESIAN_POINT('Ctrl Pts',(179.320461992889,2.0261904228423,126.322872535145));
#25146=CARTESIAN_POINT('Ctrl Pts',(179.312710801649,1.90137173150333,126.266438950512));
#25147=CARTESIAN_POINT('Ctrl Pts',(179.304959610409,1.77409617810434,126.215179976013));
#25148=CARTESIAN_POINT('Ctrl Pts',(179.297208419168,1.64483302556683,126.169308581126));
#25149=CARTESIAN_POINT('Ctrl Pts',(179.289460522391,1.51562481331742,126.123456682806));
#25150=CARTESIAN_POINT('Ctrl Pts',(179.281712625614,1.3844310498194,126.08298794021));
#25151=CARTESIAN_POINT('Ctrl Pts',(179.273964728837,1.25174058800957,126.048067043487));
#25152=CARTESIAN_POINT('Ctrl Pts',(179.266218452753,1.11907788218387,126.013153451461));
#25153=CARTESIAN_POINT('Ctrl Pts',(179.258472176669,0.984919478625015,125.983785496472));
#25154=CARTESIAN_POINT('Ctrl Pts',(179.250725900585,0.849768606098465,125.960077762634));
#25155=CARTESIAN_POINT('Ctrl Pts',(179.24297956732,0.714616735918967,125.936369853791));
#25156=CARTESIAN_POINT('Ctrl Pts',(179.235233234054,0.578472767238265,125.918322317024));
#25157=CARTESIAN_POINT('Ctrl Pts',(179.227486900789,0.441848922615117,125.905998381871));
#25158=CARTESIAN_POINT('Ctrl Pts',(179.219738832786,0.305194482029227,125.893671686858));
#25159=CARTESIAN_POINT('Ctrl Pts',(179.211990764783,0.168060340967948,125.887071179131));
#25160=CARTESIAN_POINT('Ctrl Pts',(179.20424269678,0.0309622297147287,125.88620807796));
#25161=CARTESIAN_POINT('Ctrl Pts',(179.196486394038,-0.10628159104269,125.885344059475));
#25162=CARTESIAN_POINT('Ctrl Pts',(179.188730091296,-0.243488913916986,
125.890229630992));
#25163=CARTESIAN_POINT('Ctrl Pts',(179.180973788555,-0.38014506759449,125.900823854159));
#25164=CARTESIAN_POINT('Ctrl Pts',(179.17321334604,-0.51687415877599,125.911423731781));
#25165=CARTESIAN_POINT('Ctrl Pts',(179.165452903526,-0.653051106591565,
125.927738285734));
#25166=CARTESIAN_POINT('Ctrl Pts',(179.157692461012,-0.788168961031706,
125.949674968488));
#25167=CARTESIAN_POINT('Ctrl Pts',(179.149919560747,-0.923503718646903,
125.971646865952));
#25168=CARTESIAN_POINT('Ctrl Pts',(179.142146660481,-1.05777560227164,125.999258848526));
#25169=CARTESIAN_POINT('Ctrl Pts',(179.134373760216,-1.19048952896382,126.032367559741));
#25170=CARTESIAN_POINT('Ctrl Pts',(179.126883424454,-1.3183789701352,126.064272685909));
#25171=CARTESIAN_POINT('Ctrl Pts',(179.119393088692,-1.44482146351932,126.101281752664));
#25172=CARTESIAN_POINT('Ctrl Pts',(179.11190275293,-1.56939132576419,126.143224068492));
#25173=CARTESIAN_POINT('Ctrl Pts',(179.104128393758,-1.69868470883825,126.186756780254));
#25174=CARTESIAN_POINT('Ctrl Pts',(179.096354034586,-1.82637020688291,126.235742147257));
#25175=CARTESIAN_POINT('Ctrl Pts',(179.088579675415,-1.95195355254964,126.290043350117));
#25176=CARTESIAN_POINT('Ctrl Pts',(179.080814903304,-2.07738203333556,126.34427759068));
#25177=CARTESIAN_POINT('Ctrl Pts',(179.073050131194,-2.2007131642445,126.403814470295));
#25178=CARTESIAN_POINT('Ctrl Pts',(179.065285359084,-2.32146807181828,126.46846750841));
#25179=CARTESIAN_POINT('Ctrl Pts',(179.0575283049,-2.44210295301114,126.533056283545));
#25180=CARTESIAN_POINT('Ctrl Pts',(179.049771250716,-2.56016636431176,126.602750913835));
#25181=CARTESIAN_POINT('Ctrl Pts',(179.042014196532,-2.6751999888338,126.677317113768));
#25182=CARTESIAN_POINT('Ctrl Pts',(179.034262997838,-2.79014677906578,126.751827026654));
#25183=CARTESIAN_POINT('Ctrl Pts',(179.026511799144,-2.9020680080604,126.831200977799));
#25184=CARTESIAN_POINT('Ctrl Pts',(179.018760600451,-3.01053084945795,126.915159277064));
#25185=CARTESIAN_POINT('Ctrl Pts',(179.011012726883,-3.11894716223425,126.999081559718));
#25186=CARTESIAN_POINT('Ctrl Pts',(179.003264853315,-3.22390772980016,127.087584040042));
#25187=CARTESIAN_POINT('Ctrl Pts',(178.995516979748,-3.32500976055551,127.180344453873));
#25188=CARTESIAN_POINT('Ctrl Pts',(178.987770735199,-3.42609053423857,127.273085364487));
#25189=CARTESIAN_POINT('Ctrl Pts',(178.98002449065,-3.5233140969294,127.370082163717));
#25190=CARTESIAN_POINT('Ctrl Pts',(178.972278246101,-3.61631204294623,127.470973410753));
#25191=CARTESIAN_POINT('Ctrl Pts',(178.964531952702,-3.70931057542868,127.571865294032));
#25192=CARTESIAN_POINT('Ctrl Pts',(178.956785659304,-3.79808317311763,127.676651386634));
#25193=CARTESIAN_POINT('Ctrl Pts',(178.949039365905,-3.8822997754526,127.784934924488));
#25194=CARTESIAN_POINT('Ctrl Pts',(178.941291346114,-3.96653514688435,127.893242595163));
#25195=CARTESIAN_POINT('Ctrl Pts',(178.933543326323,-4.04621226256158,128.005048953545));
#25196=CARTESIAN_POINT('Ctrl Pts',(178.925795306531,-4.12104292365446,128.11992617361));
#25197=CARTESIAN_POINT('Ctrl Pts',(178.918039169389,-4.19595198242991,128.234923746853));
#25198=CARTESIAN_POINT('Ctrl Pts',(178.910283032246,-4.26600423054555,128.352998280208));
#25199=CARTESIAN_POINT('Ctrl Pts',(178.902526895103,-4.33095593282109,128.473694667572));
#25200=CARTESIAN_POINT('Ctrl Pts',(178.894766621628,-4.39594227369947,128.594455422059));
#25201=CARTESIAN_POINT('Ctrl Pts',(178.887006348154,-4.4558224781109,128.717840465114));
#25202=CARTESIAN_POINT('Ctrl Pts',(178.87924607468,-4.51040040079451,128.843373293024));
#25203=CARTESIAN_POINT('Ctrl Pts',(178.871473622124,-4.56506397883664,128.969103133919));
#25204=CARTESIAN_POINT('Ctrl Pts',(178.863701169567,-4.61440850661788,129.096987130188));
#25205=CARTESIAN_POINT('Ctrl Pts',(178.855928717011,-4.658287010806,129.226531353211));
#25206=CARTESIAN_POINT('Ctrl Pts',(178.848884041066,-4.69805693422395,129.343945652631));
#25207=CARTESIAN_POINT('Ctrl Pts',(178.841839365122,-4.73333712484633,129.462723429701));
#25208=CARTESIAN_POINT('Ctrl Pts',(178.834794689177,-4.76405452823405,129.582490119308));
#25209=CARTESIAN_POINT('Ctrl Pts',(180.584985772263,-4.76405452823404,129.582490119308));
#25210=CARTESIAN_POINT('Ctrl Pts',(180.57727395094,-4.79793105739994,129.714574192378));
#25211=CARTESIAN_POINT('Ctrl Pts',(180.569562129616,-4.82628395215226,129.847965328554));
#25212=CARTESIAN_POINT('Ctrl Pts',(180.561850308293,-4.84903779404517,129.982158979024));
#25213=CARTESIAN_POINT('Ctrl Pts',(180.55401849625,-4.8721456703155,130.118440591857));
#25214=CARTESIAN_POINT('Ctrl Pts',(180.546186684208,-4.889478756331,130.255549475578));
#25215=CARTESIAN_POINT('Ctrl Pts',(180.538354872165,-4.90101294444811,130.392954272389));
#25216=CARTESIAN_POINT('Ctrl Pts',(180.530523060122,-4.91254713256523,130.5303590692));
#25217=CARTESIAN_POINT('Ctrl Pts',(180.522691248079,-4.91828246897984,130.668059355764));
#25218=CARTESIAN_POINT('Ctrl Pts',(180.514859436037,-4.91824986164052,130.805527225028));
#25219=CARTESIAN_POINT('',(180.860140563953,-4.91824868670176,130.80795481517));
#25220=CARTESIAN_POINT('Ctrl Pts',(180.930009319727,-4.76405452823405,129.582490119308));
#25221=CARTESIAN_POINT('Ctrl Pts',(180.922246799312,-4.79822091605315,129.715704346868));
#25222=CARTESIAN_POINT('Ctrl Pts',(180.914484278898,-4.82680923366528,129.850405798733));
#25223=CARTESIAN_POINT('Ctrl Pts',(180.906721758483,-4.84970257641179,129.986089279412));
#25224=CARTESIAN_POINT('Ctrl Pts',(180.89895822607,-4.87259890375656,130.121790449105));
#25225=CARTESIAN_POINT('Ctrl Pts',(180.891194693658,-4.88979869697442,130.258473522519));
#25226=CARTESIAN_POINT('Ctrl Pts',(180.883431161245,-4.9012362819718,130.395623574));
#25227=CARTESIAN_POINT('Ctrl Pts',(180.875667628833,-4.91267386696918,130.532773625481));
#25228=CARTESIAN_POINT('Ctrl Pts',(180.86790409642,-4.9183492172088,130.670390267495));
#25229=CARTESIAN_POINT('Ctrl Pts',(180.860140564008,-4.91824868670247,130.8079548142));
#25230=CARTESIAN_POINT('Ctrl Pts',(180.860140563953,-4.91824868670176,130.80795481517));
#25231=CARTESIAN_POINT('Ctrl Pts',(180.851235208711,-4.91813337062327,130.96575169062));
#25232=CARTESIAN_POINT('Ctrl Pts',(180.842329853469,-4.91041999025756,131.123241678084));
#25233=CARTESIAN_POINT('Ctrl Pts',(180.833424498227,-4.89522072462637,131.279752161126));
#25234=CARTESIAN_POINT('Ctrl Pts',(180.824474260165,-4.87994485498848,131.437051453996));
#25235=CARTESIAN_POINT('Ctrl Pts',(180.815524022103,-4.85710756303225,131.593361207987));
#25236=CARTESIAN_POINT('Ctrl Pts',(180.806573784042,-4.82687215032326,131.74801749744));
#25237=CARTESIAN_POINT('Ctrl Pts',(180.79756682713,-4.79644513177894,131.903653864388));
#25238=CARTESIAN_POINT('Ctrl Pts',(180.788559870219,-4.75852601683665,132.057615609648));
#25239=CARTESIAN_POINT('Ctrl Pts',(180.779552913307,-4.71332967202739,132.209247255443));
#25240=CARTESIAN_POINT('Ctrl Pts',(180.774035108754,-4.68564167489048,132.302139204833));
#25241=CARTESIAN_POINT('Ctrl Pts',(180.768517304201,-4.65522348627133,132.394157094063));
#25242=CARTESIAN_POINT('Ctrl Pts',(180.762999499647,-4.6221331923805,132.485154422408));
#25243=CARTESIAN_POINT('Ctrl Pts',(180.755225165528,-4.57551048251068,132.613365493978));
#25244=CARTESIAN_POINT('Ctrl Pts',(180.747450831409,-4.52347530734763,132.739838306069));
#25245=CARTESIAN_POINT('Ctrl Pts',(180.73967649729,-4.46617630640889,132.864082021682));
#25246=CARTESIAN_POINT('Ctrl Pts',(180.731911744343,-4.4089479213679,132.988172618018));
#25247=CARTESIAN_POINT('Ctrl Pts',(180.724146991396,-4.34646878029648,133.11003923229));
#25248=CARTESIAN_POINT('Ctrl Pts',(180.716382238449,-4.27893680000363,133.229207607393));
#25249=CARTESIAN_POINT('Ctrl Pts',(180.708625197564,-4.21147189342562,133.348257622787));
#25250=CARTESIAN_POINT('Ctrl Pts',(180.700868156679,-4.13896432627984,133.464614394248));
#25251=CARTESIAN_POINT('Ctrl Pts',(180.693111115794,-4.06165931338313,133.577825361259));
#25252=CARTESIAN_POINT('Ctrl Pts',(180.685359924554,-3.9844125967981,133.690950954998));
#25253=CARTESIAN_POINT('Ctrl Pts',(180.677608733314,-3.90237585503431,133.800935144591));
#25254=CARTESIAN_POINT('Ctrl Pts',(180.669857542074,-3.81583908314369,133.90735194112));
#25255=CARTESIAN_POINT('Ctrl Pts',(180.662109645297,-3.72933909168942,134.013723507672));
#25256=CARTESIAN_POINT('Ctrl Pts',(180.65436174852,-3.6383431203381,134.116530394143));
#25257=CARTESIAN_POINT('Ctrl Pts',(180.646613851742,-3.54318300903784,134.215377654604));
#25258=CARTESIAN_POINT('Ctrl Pts',(180.638867575658,-3.44804280318141,134.314204238349));
#25259=CARTESIAN_POINT('Ctrl Pts',(180.631121299574,-3.34874046091821,134.409072562077));
#25260=CARTESIAN_POINT('Ctrl Pts',(180.62337502349,-3.24564616409112,134.499622995263));
#25261=CARTESIAN_POINT('Ctrl Pts',(180.615628690225,-3.14255110624534,134.590174096871));
#25262=CARTESIAN_POINT('Ctrl Pts',(180.60788235696,-3.03566433172752,134.676406986332));
#25263=CARTESIAN_POINT('Ctrl Pts',(180.600136023694,-2.92539041717838,134.758001214482));
#25264=CARTESIAN_POINT('Ctrl Pts',(180.592387955691,-2.81509180755061,134.839613715093));
#25265=CARTESIAN_POINT('Ctrl Pts',(180.584639887688,-2.70140486273715,134.916585254807));
#25266=CARTESIAN_POINT('Ctrl Pts',(180.576891819685,-2.58476420983551,134.988637979555));
#25267=CARTESIAN_POINT('Ctrl Pts',(180.569135516943,-2.46799958986003,135.060767282796));
#25268=CARTESIAN_POINT('Ctrl Pts',(180.561379214202,-2.34827532398418,135.12796712223));
#25269=CARTESIAN_POINT('Ctrl Pts',(180.55362291146,-2.22605226619562,135.190004740231));
#25270=CARTESIAN_POINT('Ctrl Pts',(180.545862468946,-2.10376397428102,135.252075469577));
#25271=CARTESIAN_POINT('Ctrl Pts',(180.538102026431,-1.97897458853601,135.308978325326));
#25272=CARTESIAN_POINT('Ctrl Pts',(180.530341583917,-1.85216521453456,135.360528643503));
#25273=CARTESIAN_POINT('Ctrl Pts',(180.522568683652,-1.72515227486836,135.412161714826));
#25274=CARTESIAN_POINT('Ctrl Pts',(180.514795783386,-1.59611323530802,135.458424946265));
#25275=CARTESIAN_POINT('Ctrl Pts',(180.507022883121,-1.46554549602716,135.499183240581));
#25276=CARTESIAN_POINT('Ctrl Pts',(180.499532547359,-1.33972422294845,135.538459868235));
#25277=CARTESIAN_POINT('Ctrl Pts',(180.492042211597,-1.21248376217569,135.572624766855));
#25278=CARTESIAN_POINT('Ctrl Pts',(180.484551875835,-1.08427646179028,135.601602285119));
#25279=CARTESIAN_POINT('Ctrl Pts',(180.476777541716,-0.951208142644003,
135.631678494795));
#25280=CARTESIAN_POINT('Ctrl Pts',(180.469003207597,-0.81667670073027,135.656261472423));
#25281=CARTESIAN_POINT('Ctrl Pts',(180.461228873478,-0.68117543440742,135.675210963251));
#25282=CARTESIAN_POINT('Ctrl Pts',(180.45346412053,-0.545841161285354,135.694137100525));
#25283=CARTESIAN_POINT('Ctrl Pts',(180.445699367583,-0.409539825369746,
135.707443511412));
#25284=CARTESIAN_POINT('Ctrl Pts',(180.437934614636,-0.272777411462797,
135.715040361379));
#25285=CARTESIAN_POINT('Ctrl Pts',(180.430177573751,-0.13615083191333,135.722629666048));
#25286=CARTESIAN_POINT('Ctrl Pts',(180.422420532866,0.000935526450582369,
135.724520673434));
#25287=CARTESIAN_POINT('Ctrl Pts',(180.414663491981,0.137968367048358,135.720675069693));
#25288=CARTESIAN_POINT('Ctrl Pts',(180.406912300741,0.274897870115078,135.716832365952));
#25289=CARTESIAN_POINT('Ctrl Pts',(180.399161109501,0.411773546516112,135.707261672693));
#25290=CARTESIAN_POINT('Ctrl Pts',(180.391409918261,0.548080250301332,135.691976713551));
#25291=CARTESIAN_POINT('Ctrl Pts',(180.383662021484,0.684329020101435,135.676698250924));
#25292=CARTESIAN_POINT('Ctrl Pts',(180.375914124707,0.820008910547644,135.655710396422));
#25293=CARTESIAN_POINT('Ctrl Pts',(180.36816622793,0.9546082748462,135.629078858468));
#25294=CARTESIAN_POINT('Ctrl Pts',(180.360419951846,1.08917948385937,135.602452891258));
#25295=CARTESIAN_POINT('Ctrl Pts',(180.352673675761,1.22267023300946,135.570185664586));
#25296=CARTESIAN_POINT('Ctrl Pts',(180.344927399677,1.35457786262363,135.532394233837));
#25297=CARTESIAN_POINT('Ctrl Pts',(180.337181066412,1.4864864659498,135.494602524121));
#25298=CARTESIAN_POINT('Ctrl Pts',(180.329434733147,1.61681155057666,135.451286636637));
#25299=CARTESIAN_POINT('Ctrl Pts',(180.321688399881,1.74506482999139,135.402613742572));
#25300=CARTESIAN_POINT('Ctrl Pts',(180.313940331878,1.87334683083893,135.35392994855));
#25301=CARTESIAN_POINT('Ctrl Pts',(180.306192263875,1.99955573777708,135.299886899446));
#25302=CARTESIAN_POINT('Ctrl Pts',(180.298444195872,2.12322285774621,135.240700072437));
#25303=CARTESIAN_POINT('Ctrl Pts',(180.29068789313,2.24702141260209,135.181450340963));
#25304=CARTESIAN_POINT('Ctrl Pts',(180.282931590389,2.36827243084956,135.117046079976));
#25305=CARTESIAN_POINT('Ctrl Pts',(180.275175287647,2.48653098406956,135.047749207804));
#25306=CARTESIAN_POINT('Ctrl Pts',(180.267414845133,2.60485265544017,134.978415349805));
#25307=CARTESIAN_POINT('Ctrl Pts',(180.259654402618,2.72017835070013,134.904183888821));
#25308=CARTESIAN_POINT('Ctrl Pts',(180.251893960104,2.83209265750178,134.825359777206));
#25309=CARTESIAN_POINT('Ctrl Pts',(180.244121059839,2.94418661908395,134.746409130129));
#25310=CARTESIAN_POINT('Ctrl Pts',(180.236348159573,3.05285793877241,134.662851338207));
#25311=CARTESIAN_POINT('Ctrl Pts',(180.228575259308,3.15772409849079,134.575031854934));
#25312=CARTESIAN_POINT('Ctrl Pts',(180.221084923546,3.25877810916079,134.490404831082));
#25313=CARTESIAN_POINT('Ctrl Pts',(180.213594587784,3.35629858303754,134.401820790026));
#25314=CARTESIAN_POINT('Ctrl Pts',(180.206104252022,3.44997736733326,134.309619413631));
#25315=CARTESIAN_POINT('Ctrl Pts',(180.198329917903,3.54720801120912,134.213922194025));
#25316=CARTESIAN_POINT('Ctrl Pts',(180.190555583784,3.6406078969809,134.114024781695));
#25317=CARTESIAN_POINT('Ctrl Pts',(180.182781249665,3.72979238454181,134.010266391402));
#25318=CARTESIAN_POINT('Ctrl Pts',(180.175016496718,3.81886696019247,133.906635874052));
#25319=CARTESIAN_POINT('Ctrl Pts',(180.167251743771,3.90373622193616,133.799154140003));
#25320=CARTESIAN_POINT('Ctrl Pts',(180.159486990823,3.98405109229198,133.688198330841));
#25321=CARTESIAN_POINT('Ctrl Pts',(180.151729949938,4.06428619278623,133.577352724553));
#25322=CARTESIAN_POINT('Ctrl Pts',(180.143972909054,4.1399756760726,133.463040224457));
#25323=CARTESIAN_POINT('Ctrl Pts',(180.136215868169,4.21080985828836,133.345671971934));
#25324=CARTESIAN_POINT('Ctrl Pts',(180.128464676928,4.28159062389636,133.228392227724));
#25325=CARTESIAN_POINT('Ctrl Pts',(180.120713485688,4.3475231750704,133.108061651164));
#25326=CARTESIAN_POINT('Ctrl Pts',(180.112962294448,4.40834060892407,132.985121067091));
#25327=CARTESIAN_POINT('Ctrl Pts',(180.105214397671,4.46913219374597,132.862232736046));
#25328=CARTESIAN_POINT('Ctrl Pts',(180.097466500894,4.52481281229799,132.736736953544));
#25329=CARTESIAN_POINT('Ctrl Pts',(180.089718604117,4.57516118934884,132.609099699532));
#25330=CARTESIAN_POINT('Ctrl Pts',(180.081972328033,4.62549903460459,132.481489144482));
#25331=CARTESIAN_POINT('Ctrl Pts',(180.074226051949,4.6705067135582,132.351738372381));
#25332=CARTESIAN_POINT('Ctrl Pts',(180.066479775865,4.71001100838992,132.220333556342));
#25333=CARTESIAN_POINT('Ctrl Pts',(180.058733442599,4.74951559483336,132.088927770302));
#25334=CARTESIAN_POINT('Ctrl Pts',(180.050987109334,4.78351660353165,131.955868290373));
#25335=CARTESIAN_POINT('Ctrl Pts',(180.043240776069,4.811890749551,131.821656285937));
#25336=CARTESIAN_POINT('Ctrl Pts',(180.035492708066,4.84027124976361,131.687414225652));
#25337=CARTESIAN_POINT('Ctrl Pts',(180.027744640063,4.86302229899824,131.552019509708));
#25338=CARTESIAN_POINT('Ctrl Pts',(180.01999657206,4.880071844258,131.415982933526));
#25339=CARTESIAN_POINT('Ctrl Pts',(180.012240269318,4.89713950997736,131.279801776052));
#25340=CARTESIAN_POINT('Ctrl Pts',(180.004483966576,4.90849351826859,131.142977784168));
#25341=CARTESIAN_POINT('Ctrl Pts',(179.996727663834,4.9141137337624,131.006026862009));
#25342=CARTESIAN_POINT('Ctrl Pts',(179.98896722132,4.91973694893445,130.869002845019));
#25343=CARTESIAN_POINT('Ctrl Pts',(179.981206778806,4.91962027373891,130.731852153537));
#25344=CARTESIAN_POINT('Ctrl Pts',(179.973446336292,4.91379573270794,130.595089119934));
#25345=CARTESIAN_POINT('Ctrl Pts',(179.965673436026,4.90796184160662,130.458106542167));
#25346=CARTESIAN_POINT('Ctrl Pts',(179.957900535761,4.89640180751873,130.321513255635));
#25347=CARTESIAN_POINT('Ctrl Pts',(179.950127635495,4.87919950989027,130.185817809681));
#25348=CARTESIAN_POINT('Ctrl Pts',(179.942637299733,4.8626225591104,130.055055234982));
#25349=CARTESIAN_POINT('Ctrl Pts',(179.935146963971,4.84080649473996,129.925126660408));
#25350=CARTESIAN_POINT('Ctrl Pts',(179.927656628209,4.81387053664267,129.796474949971));
#25351=CARTESIAN_POINT('Ctrl Pts',(179.91988229409,4.7859132935074,129.662945370831));
#25352=CARTESIAN_POINT('Ctrl Pts',(179.912107959971,4.75235169095122,129.530368410215));
#25353=CARTESIAN_POINT('Ctrl Pts',(179.904333625852,4.71326321258631,129.399251030601));
#25354=CARTESIAN_POINT('Ctrl Pts',(179.896568872905,4.67422290727756,129.268295241439));
#25355=CARTESIAN_POINT('Ctrl Pts',(179.888804119958,4.62966938940084,129.138795825271));
#25356=CARTESIAN_POINT('Ctrl Pts',(179.88103936701,4.57973127394808,129.011250325107));
#25357=CARTESIAN_POINT('Ctrl Pts',(179.873282326125,4.52984275773558,128.883831504932));
#25358=CARTESIAN_POINT('Ctrl Pts',(179.86552528524,4.47458042844114,128.758363100465));
#25359=CARTESIAN_POINT('Ctrl Pts',(179.857768244355,4.41412279926086,128.635327889471));
#25360=CARTESIAN_POINT('Ctrl Pts',(179.850017053115,4.35371076164904,128.512385460287));
#25361=CARTESIAN_POINT('Ctrl Pts',(179.842265861875,4.28811139405136,128.391872921809));
#25362=CARTESIAN_POINT('Ctrl Pts',(179.834514670635,4.21755130735877,128.274253103586));
#25363=CARTESIAN_POINT('Ctrl Pts',(179.826766773858,4.14702121058527,128.156683276924));
#25364=CARTESIAN_POINT('Ctrl Pts',(179.819018877081,4.07153478894331,128.042004059732));
#25365=CARTESIAN_POINT('Ctrl Pts',(179.811270980304,3.99136447989174,127.930653490672));
#25366=CARTESIAN_POINT('Ctrl Pts',(179.80352470422,3.91121094074054,127.819326213751));
#25367=CARTESIAN_POINT('Ctrl Pts',(179.795778428136,3.82637569128667,127.711326517104));
#25368=CARTESIAN_POINT('Ctrl Pts',(179.788032152051,3.7371741342777,127.607062922232));
#25369=CARTESIAN_POINT('Ctrl Pts',(179.780285818786,3.64797191880316,127.50279855771));
#25370=CARTESIAN_POINT('Ctrl Pts',(179.772539485521,3.5544035856207,127.402270647074));
#25371=CARTESIAN_POINT('Ctrl Pts',(179.764793152255,3.4568241442069,127.305853807722));
#25372=CARTESIAN_POINT('Ctrl Pts',(179.757045084252,3.35922285055371,127.209415376487));
#25373=CARTESIAN_POINT('Ctrl Pts',(179.749297016249,3.25760893928871,127.117090123255));
#25374=CARTESIAN_POINT('Ctrl Pts',(179.741548948246,3.15237321066194,127.029214765655));
#25375=CARTESIAN_POINT('Ctrl Pts',(179.733792645505,3.04702563625045,126.94124601308));
#25376=CARTESIAN_POINT('Ctrl Pts',(179.726036342763,2.93804885563987,126.857736854617));
#25377=CARTESIAN_POINT('Ctrl Pts',(179.718280040021,2.82586602993138,126.77898308951));
#25378=CARTESIAN_POINT('Ctrl Pts',(179.710519597507,2.71362332887097,126.700187291147));
#25379=CARTESIAN_POINT('Ctrl Pts',(179.702759154993,2.59817150202462,126.626152154456));
#25380=CARTESIAN_POINT('Ctrl Pts',(179.694998712478,2.4799605818237,126.557128745499));
#25381=CARTESIAN_POINT('Ctrl Pts',(179.687225812213,2.36155989895946,126.487994534039));
#25382=CARTESIAN_POINT('Ctrl Pts',(179.679452911947,2.2403916176828,126.423888310267));
#25383=CARTESIAN_POINT('Ctrl Pts',(179.671680011682,2.11692893384896,126.365014387373));
#25384=CARTESIAN_POINT('Ctrl Pts',(179.66418967592,1.99795442955653,126.30828067987));
#25385=CARTESIAN_POINT('Ctrl Pts',(179.656699340158,1.87684972432121,126.256405584449));
#25386=CARTESIAN_POINT('Ctrl Pts',(179.649209004396,1.75405185342764,126.209528176879));
#25387=CARTESIAN_POINT('Ctrl Pts',(179.641434670277,1.6265980639352,126.160873398153));
#25388=CARTESIAN_POINT('Ctrl Pts',(179.633660336158,1.49691644622467,126.117448639312));
#25389=CARTESIAN_POINT('Ctrl Pts',(179.625886002039,1.36547540397288,126.079462736802));
#25390=CARTESIAN_POINT('Ctrl Pts',(179.618121249092,1.23419635105852,126.041523648523));
#25391=CARTESIAN_POINT('Ctrl Pts',(179.610356496145,1.10116255992973,126.009010187295));
#25392=CARTESIAN_POINT('Ctrl Pts',(179.602591743197,0.966862147156906,125.982083079836));
#25393=CARTESIAN_POINT('Ctrl Pts',(179.594834702312,0.832695123447448,125.955182716759));
#25394=CARTESIAN_POINT('Ctrl Pts',(179.587077661427,0.697264362478954,125.933857742155));
#25395=CARTESIAN_POINT('Ctrl Pts',(179.579320620542,0.561072529599974,125.918218920989));
#25396=CARTESIAN_POINT('Ctrl Pts',(179.571569429302,0.424983400041494,125.90259189318));
#25397=CARTESIAN_POINT('Ctrl Pts',(179.563818238062,0.288134727787094,125.89264252828));
#25398=CARTESIAN_POINT('Ctrl Pts',(179.556067046822,0.151038393166892,125.888430342807));
#25399=CARTESIAN_POINT('Ctrl Pts',(179.548319150045,0.0140003281460682,
125.884219947625));
#25400=CARTESIAN_POINT('Ctrl Pts',(179.540571253268,-0.123284799917584,
125.885741893951));
#25401=CARTESIAN_POINT('Ctrl Pts',(179.532823356491,-0.260301197590463,
125.893003743032));
#25402=CARTESIAN_POINT('Ctrl Pts',(179.525077080407,-0.39728893438668,125.90026407309));
#25403=CARTESIAN_POINT('Ctrl Pts',(179.517330804322,-0.534007662432173,
125.913261897038));
#25404=CARTESIAN_POINT('Ctrl Pts',(179.509584528238,-0.669943198128833,
125.931952673461));
#25405=CARTESIAN_POINT('Ctrl Pts',(179.501838194973,-0.805879737270736,
125.950643587855));
#25406=CARTESIAN_POINT('Ctrl Pts',(179.494091861708,-0.941032685206453,
125.975027485324));
#25407=CARTESIAN_POINT('Ctrl Pts',(179.486345528442,-1.07489497441483,126.005008176197));
#25408=CARTESIAN_POINT('Ctrl Pts',(179.478597460439,-1.20878724115488,126.034995581037));
#25409=CARTESIAN_POINT('Ctrl Pts',(179.470849392436,-1.34138789258256,126.070582187898));
#25410=CARTESIAN_POINT('Ctrl Pts',(179.463101324433,-1.47220240153905,126.111621209565));
#25411=CARTESIAN_POINT('Ctrl Pts',(179.455345021691,-1.60315594171228,126.152703847993));
#25412=CARTESIAN_POINT('Ctrl Pts',(179.44758871895,-1.73231917365516,126.199250359929));
#25413=CARTESIAN_POINT('Ctrl Pts',(179.439832416208,-1.85921450417547,126.251064614673));
#25414=CARTESIAN_POINT('Ctrl Pts',(179.432071973694,-1.98617756255448,126.302906524244));
#25415=CARTESIAN_POINT('Ctrl Pts',(179.424311531179,-2.11086995231502,126.360021616145));
#25416=CARTESIAN_POINT('Ctrl Pts',(179.416551088665,-2.23283719094561,126.422166972686));
#25417=CARTESIAN_POINT('Ctrl Pts',(179.4087781884,-2.35500022221536,126.48441209047));
#25418=CARTESIAN_POINT('Ctrl Pts',(179.401005288134,-2.47442901958706,126.551703417341));
#25419=CARTESIAN_POINT('Ctrl Pts',(179.393232387869,-2.59069591467029,126.623753276496));
#25420=CARTESIAN_POINT('Ctrl Pts',(179.385742052107,-2.70273621525825,126.693183941787));
#25421=CARTESIAN_POINT('Ctrl Pts',(179.378251716345,-2.81184025354116,126.76703300397));
#25422=CARTESIAN_POINT('Ctrl Pts',(179.370761380583,-2.91765479288965,126.845007946734));
#25423=CARTESIAN_POINT('Ctrl Pts',(179.362824623581,-3.02977583963157,126.927630167234));
#25424=CARTESIAN_POINT('Ctrl Pts',(179.354887866579,-3.13858421238573,127.015166053473));
#25425=CARTESIAN_POINT('Ctrl Pts',(179.346951109577,-3.24361582879236,127.107315930562));
#25426=CARTESIAN_POINT('Ctrl Pts',(179.339259878588,-3.34539825992441,127.196615122934));
#25427=CARTESIAN_POINT('Ctrl Pts',(179.331568647598,-3.44363378017725,127.290246806879));
#25428=CARTESIAN_POINT('Ctrl Pts',(179.323877416609,-3.53792844756241,127.387893822406));
#25429=CARTESIAN_POINT('Ctrl Pts',(179.316193156561,-3.63213765104985,127.485452335638));
#25430=CARTESIAN_POINT('Ctrl Pts',(179.308508896513,-3.72241282922045,127.587018658588));
#25431=CARTESIAN_POINT('Ctrl Pts',(179.300824636464,-3.80839397804645,127.692236203202));
#25432=CARTESIAN_POINT('Ctrl Pts',(179.293145599922,-3.89431667973043,127.797382224409));
#25433=CARTESIAN_POINT('Ctrl Pts',(179.28546656338,-3.97595090671817,127.906174222729));
#25434=CARTESIAN_POINT('Ctrl Pts',(179.277787526838,-4.05297468425983,128.018220048383));
#25435=CARTESIAN_POINT('Ctrl Pts',(179.270111970762,-4.12996355134694,128.130215090099));
#25436=CARTESIAN_POINT('Ctrl Pts',(179.262436414686,-4.20234590173357,128.245460696354));
#25437=CARTESIAN_POINT('Ctrl Pts',(179.25476085861,-4.26984142786074,128.363533453791));
#25438=CARTESIAN_POINT('Ctrl Pts',(179.247085795211,-4.33733262159974,128.481598632399));
#25439=CARTESIAN_POINT('Ctrl Pts',(179.239410731811,-4.39993741066976,128.60249025877));
#25440=CARTESIAN_POINT('Ctrl Pts',(179.231735668412,-4.45742018209201,128.725758110404));
#25441=CARTESIAN_POINT('Ctrl Pts',(179.224060790413,-4.51490156495416,128.849022984367));
#25442=CARTESIAN_POINT('Ctrl Pts',(179.216385912414,-4.56726101346593,128.974663605236));
#25443=CARTESIAN_POINT('Ctrl Pts',(179.208711034414,-4.61431036413111,129.102208178455));
#25444=CARTESIAN_POINT('Ctrl Pts',(179.201032838487,-4.66138005470733,129.229807890485));
#25445=CARTESIAN_POINT('Ctrl Pts',(179.19335464256,-4.70313493368093,129.359312821299));
#25446=CARTESIAN_POINT('Ctrl Pts',(179.185676446633,-4.73943621873225,129.490234523514));
#25447=CARTESIAN_POINT('Ctrl Pts',(179.183877368601,-4.74794197257219,129.520910786621));
#25448=CARTESIAN_POINT('Ctrl Pts',(179.182078290568,-4.75614853636364,129.551664776996));
#25449=CARTESIAN_POINT('Ctrl Pts',(179.180279212536,-4.76405452823405,129.582490119308));
#25450=CARTESIAN_POINT('Origin',(213.235140564004,0.,130.804360617566));
#25451=CARTESIAN_POINT('',(177.084597561451,-4.76405452823403,129.582490119308));
#25452=CARTESIAN_POINT('',(177.430115848357,-4.76405452823405,129.582490119308));
#25453=CARTESIAN_POINT('',(213.235140564004,-4.76405452823405,129.582490119308));
#25454=CARTESIAN_POINT('',(178.764859436029,-4.91824789753406,130.799812991619));
#25455=CARTESIAN_POINT('Ctrl Pts',(178.764859435991,-4.91824789753469,130.799812992297));
#25456=CARTESIAN_POINT('Ctrl Pts',(178.757196290994,-4.9183730412926,130.935155723463));
#25457=CARTESIAN_POINT('Ctrl Pts',(178.749533145997,-4.91290734326878,131.070645942394));
#25458=CARTESIAN_POINT('Ctrl Pts',(178.741870001,-4.90184112669081,131.205778892166));
#25459=CARTESIAN_POINT('Ctrl Pts',(178.734084063679,-4.89059758781915,131.343077178612));
#25460=CARTESIAN_POINT('Ctrl Pts',(178.726298126358,-4.87357245610437,131.480006229492));
#25461=CARTESIAN_POINT('Ctrl Pts',(178.718512189038,-4.85081073812513,131.61603681248));
#25462=CARTESIAN_POINT('Ctrl Pts',(178.710856306159,-4.82842922645917,131.749795173024));
#25463=CARTESIAN_POINT('Ctrl Pts',(178.70320042328,-4.80050136400255,131.882684439534));
#25464=CARTESIAN_POINT('Ctrl Pts',(178.695544540401,-4.76712209381898,132.01420771746));
#25465=CARTESIAN_POINT('Ctrl Pts',(178.687889375061,-4.73374595206982,132.145718668516));
#25466=CARTESIAN_POINT('Ctrl Pts',(178.680234209721,-4.69491951717209,132.27586349683));
#25467=CARTESIAN_POINT('Ctrl Pts',(178.672579044381,-4.65078839204757,132.404157603091));
#25468=CARTESIAN_POINT('Ctrl Pts',(178.664922844915,-4.60665130530803,132.532469040433));
#25469=CARTESIAN_POINT('Ctrl Pts',(178.657266645449,-4.55720823398827,132.65892887934));
#25470=CARTESIAN_POINT('Ctrl Pts',(178.649610445982,-4.50265380566106,132.783070239735));
#25471=CARTESIAN_POINT('Ctrl Pts',(178.641726867593,-4.44647918349511,132.910898433141));
#25472=CARTESIAN_POINT('Ctrl Pts',(178.633843289203,-4.3848850536798,133.036267873534));
#25473=CARTESIAN_POINT('Ctrl Pts',(178.625959710813,-4.31813542196403,133.158694820707));
#25474=CARTESIAN_POINT('Ctrl Pts',(178.618292097771,-4.25321435168799,133.277767963686));
#25475=CARTESIAN_POINT('Ctrl Pts',(178.610624484729,-4.18341682154212,133.394057413434));
#25476=CARTESIAN_POINT('Ctrl Pts',(178.602956871687,-4.10902994539855,133.507147322121));
#25477=CARTESIAN_POINT('Ctrl Pts',(178.594965310623,-4.03150030744991,133.625015152183));
#25478=CARTESIAN_POINT('Ctrl Pts',(178.586973749559,-3.94898534362607,133.739406770363));
#25479=CARTESIAN_POINT('Ctrl Pts',(178.578982188495,-3.861856090724,133.849890226195));
#25480=CARTESIAN_POINT('Ctrl Pts',(178.570990627431,-3.77472683782194,133.960373682027));
#25481=CARTESIAN_POINT('Ctrl Pts',(178.562999066367,-3.68298366963375,134.066948657916));
#25482=CARTESIAN_POINT('Ctrl Pts',(178.555007505303,-3.58703931231371,134.169227930614));
#25483=CARTESIAN_POINT('Ctrl Pts',(178.547233171184,-3.493702918501,134.268727043871));
#25484=CARTESIAN_POINT('Ctrl Pts',(178.539458837065,-3.39607561388428,134.364497295231));
#25485=CARTESIAN_POINT('Ctrl Pts',(178.531684502946,-3.2944872852368,134.456146015137));
#25486=CARTESIAN_POINT('Ctrl Pts',(178.523919749999,-3.19302415512523,134.547681786186));
#25487=CARTESIAN_POINT('Ctrl Pts',(178.516154997052,-3.08761000143176,134.635105872937));
#25488=CARTESIAN_POINT('Ctrl Pts',(178.508390244105,-2.97861348023738,134.718060248075));
#25489=CARTESIAN_POINT('Ctrl Pts',(178.50063320322,-2.86972521592481,134.800932231759));
#25490=CARTESIAN_POINT('Ctrl Pts',(178.492876162335,-2.75726197390471,134.879343103152));
#25491=CARTESIAN_POINT('Ctrl Pts',(178.48511912145,-2.64162734560113,134.952973401313));
#25492=CARTESIAN_POINT('Ctrl Pts',(178.47736793021,-2.52607991827016,135.026548174295));
#25493=CARTESIAN_POINT('Ctrl Pts',(178.46961673897,-2.40736619337517,135.095349340572));
#25494=CARTESIAN_POINT('Ctrl Pts',(178.46186554773,-2.28592046387358,135.159099495541));
#25495=CARTESIAN_POINT('Ctrl Pts',(178.454117650953,-2.16452635204637,135.222822554993));
#25496=CARTESIAN_POINT('Ctrl Pts',(178.446369754175,-2.04040289054619,135.281498691652));
#25497=CARTESIAN_POINT('Ctrl Pts',(178.438621857398,-1.91401061513348,135.334895511776));
#25498=CARTESIAN_POINT('Ctrl Pts',(178.430875581314,-1.78764477826022,135.388281162436));
#25499=CARTESIAN_POINT('Ctrl Pts',(178.42312930523,-1.6590114313704,135.436389541058));
#25500=CARTESIAN_POINT('Ctrl Pts',(178.415383029146,-1.52859245082243,135.479035812891));
#25501=CARTESIAN_POINT('Ctrl Pts',(178.407636695881,-1.39817250755127,135.521682399529));
#25502=CARTESIAN_POINT('Ctrl Pts',(178.399890362615,-1.26596727592271,135.55886667741));
#25503=CARTESIAN_POINT('Ctrl Pts',(178.39214402935,-1.1324748224956,135.590453370419));
#25504=CARTESIAN_POINT('Ctrl Pts',(178.384395961347,-0.998952474358899,
135.62204713705));
#25505=CARTESIAN_POINT('Ctrl Pts',(178.376647893344,-0.864142711197707,
135.648040734402));
#25506=CARTESIAN_POINT('Ctrl Pts',(178.368899825341,-0.728554452264122,
135.668349872549));
#25507=CARTESIAN_POINT('Ctrl Pts',(178.361143522599,-0.592822088515468,
135.688680595488));
#25508=CARTESIAN_POINT('Ctrl Pts',(178.353387219857,-0.456309963453038,
135.703314732646));
#25509=CARTESIAN_POINT('Ctrl Pts',(178.345630917115,-0.319533349451039,
135.712219774173));
#25510=CARTESIAN_POINT('Ctrl Pts',(178.337870474601,-0.182683733651767,
135.721129568589));
#25511=CARTESIAN_POINT('Ctrl Pts',(178.330110032087,-0.045569738297517,
135.724304165422));
#25512=CARTESIAN_POINT('Ctrl Pts',(178.322349589573,0.0912936838562829,
135.721763237424));
#25513=CARTESIAN_POINT('Ctrl Pts',(178.314576689307,0.228376811325325,135.719218230503));
#25514=CARTESIAN_POINT('Ctrl Pts',(178.306803789042,0.365208171309374,135.710939387667));
#25515=CARTESIAN_POINT('Ctrl Pts',(178.299030888776,0.501277348038855,135.696998360424));
#25516=CARTESIAN_POINT('Ctrl Pts',(178.291540553014,0.632400067457702,135.683564124637));
#25517=CARTESIAN_POINT('Ctrl Pts',(178.284050217252,0.762814751203412,135.664872270292));
#25518=CARTESIAN_POINT('Ctrl Pts',(178.27655988149,0.89207580184942,135.641031355404));
#25519=CARTESIAN_POINT('Ctrl Pts',(178.268785547371,1.02623782451768,135.616286504981));
#25520=CARTESIAN_POINT('Ctrl Pts',(178.261011213252,1.15958199216667,135.585916048837));
#25521=CARTESIAN_POINT('Ctrl Pts',(178.253236879133,1.29159962891666,135.549985282569));
#25522=CARTESIAN_POINT('Ctrl Pts',(178.245472126186,1.4234545657279,135.514098797758));
#25523=CARTESIAN_POINT('Ctrl Pts',(178.237707373239,1.55398585084488,135.472665739113));
#25524=CARTESIAN_POINT('Ctrl Pts',(178.229942620292,1.68269299813225,135.425802744926));
#25525=CARTESIAN_POINT('Ctrl Pts',(178.222185579407,1.8112723116667,135.378986295725));
#25526=CARTESIAN_POINT('Ctrl Pts',(178.214428538522,1.93803072786065,135.326750776369));
#25527=CARTESIAN_POINT('Ctrl Pts',(178.206671497637,2.0624813241539,135.269263063311));
#25528=CARTESIAN_POINT('Ctrl Pts',(178.198920306396,2.18683807128475,135.211818702184));
#25529=CARTESIAN_POINT('Ctrl Pts',(178.191169115156,2.30889010907471,135.149130194217));
#25530=CARTESIAN_POINT('Ctrl Pts',(178.183417923916,2.4281693032209,135.081412978409));
#25531=CARTESIAN_POINT('Ctrl Pts',(178.175670027139,2.54739780052733,135.013724544225));
#25532=CARTESIAN_POINT('Ctrl Pts',(178.167922130362,2.66385545891849,134.941011845815));
#25533=CARTESIAN_POINT('Ctrl Pts',(178.160174233585,2.77709782812862,134.863536730462));
#25534=CARTESIAN_POINT('Ctrl Pts',(178.152427957501,2.89031650947648,134.786077821232));
#25535=CARTESIAN_POINT('Ctrl Pts',(178.144681681417,3.00032091694965,134.703858697166));
#25536=CARTESIAN_POINT('Ctrl Pts',(178.136935405333,3.10669507789473,134.617184866792));
#25537=CARTESIAN_POINT('Ctrl Pts',(178.129189072067,3.21307002406978,134.530510396611));
#25538=CARTESIAN_POINT('Ctrl Pts',(178.121442738802,3.31581436715207,134.439381401466));
#25539=CARTESIAN_POINT('Ctrl Pts',(178.113696405536,3.41454507837464,134.344143798814));
#25540=CARTESIAN_POINT('Ctrl Pts',(178.105948337533,3.51329789965507,134.248884868362));
#25541=CARTESIAN_POINT('Ctrl Pts',(178.098200269531,3.60803501918481,134.149515770902));
#25542=CARTESIAN_POINT('Ctrl Pts',(178.090452201528,3.69841043817253,134.046419113848));
#25543=CARTESIAN_POINT('Ctrl Pts',(178.082695898786,3.78888190923118,133.943212884441));
#25544=CARTESIAN_POINT('Ctrl Pts',(178.074939596044,3.87498216137205,133.836271475994));
#25545=CARTESIAN_POINT('Ctrl Pts',(178.067183293302,3.95640532583519,133.726010829382));
#25546=CARTESIAN_POINT('Ctrl Pts',(178.059422850788,4.03787194829286,133.615691333343));
#25547=CARTESIAN_POINT('Ctrl Pts',(178.051662408274,4.11465629020247,133.502049392914));
#25548=CARTESIAN_POINT('Ctrl Pts',(178.04390196576,4.18649655826401,133.385528886034));
#25549=CARTESIAN_POINT('Ctrl Pts',(178.036129065494,4.25845215070156,133.268821330092));
#25550=CARTESIAN_POINT('Ctrl Pts',(178.028356165229,4.32544761811766,133.149226314896));
#25551=CARTESIAN_POINT('Ctrl Pts',(178.020583264963,4.38726735076485,133.027211997081));
#25552=CARTESIAN_POINT('Ctrl Pts',(178.013092929201,4.44683978041567,132.909633207054));
#25553=CARTESIAN_POINT('Ctrl Pts',(178.005602593439,4.50160611609361,132.789808236237));
#25554=CARTESIAN_POINT('Ctrl Pts',(177.998112257677,4.5514168344388,132.668170656622));
#25555=CARTESIAN_POINT('Ctrl Pts',(177.990337923558,4.60311614130971,132.541921151206));
#25556=CARTESIAN_POINT('Ctrl Pts',(177.982563589439,4.64964039614636,132.413318953074));
#25557=CARTESIAN_POINT('Ctrl Pts',(177.97478925532,4.69076958224579,132.282827319517));
#25558=CARTESIAN_POINT('Ctrl Pts',(177.967024502373,4.73184808029915,132.152496505236));
#25559=CARTESIAN_POINT('Ctrl Pts',(177.959259749426,4.76754462262512,132.020281257972));
#25560=CARTESIAN_POINT('Ctrl Pts',(177.951494996479,4.79768681534231,131.886665696733));
#25561=CARTESIAN_POINT('Ctrl Pts',(177.943737955594,4.82779907040887,131.753182844352));
#25562=CARTESIAN_POINT('Ctrl Pts',(177.935980914709,4.85236786878697,131.618302824688));
#25563=CARTESIAN_POINT('Ctrl Pts',(177.928223873824,4.87127041482564,131.482525500279));
#25564=CARTESIAN_POINT('Ctrl Pts',(177.920472682584,4.89015870630732,131.346850566606));
#25565=CARTESIAN_POINT('Ctrl Pts',(177.912721491344,4.90338919683614,131.210280060711));
#25566=CARTESIAN_POINT('Ctrl Pts',(177.904970300103,4.91089010331847,131.073324287285));
#25567=CARTESIAN_POINT('Ctrl Pts',(177.897222403326,4.91838782171541,130.936426723716));
#25568=CARTESIAN_POINT('Ctrl Pts',(177.889474506549,4.92016077820899,130.799144607863));
#25569=CARTESIAN_POINT('Ctrl Pts',(177.881726609772,4.91618903610976,130.661993403172));
#25570=CARTESIAN_POINT('Ctrl Pts',(177.873980333688,4.91221812481335,130.524870887557));
#25571=CARTESIAN_POINT('Ctrl Pts',(177.866234057604,4.90250491641586,130.387879619192));
#25572=CARTESIAN_POINT('Ctrl Pts',(177.85848778152,4.88708160051593,130.251534702473));
#25573=CARTESIAN_POINT('Ctrl Pts',(177.850741448255,4.87165817076464,130.115188779287));
#25574=CARTESIAN_POINT('Ctrl Pts',(177.842995114989,4.85052459334789,129.979489605756));
#25575=CARTESIAN_POINT('Ctrl Pts',(177.835248781724,4.82376486201545,129.844946411665));
#25576=CARTESIAN_POINT('Ctrl Pts',(177.827500713721,4.79699913802668,129.710373087558));
#25577=CARTESIAN_POINT('Ctrl Pts',(177.819752645718,4.76460482924301,129.5769566414));
#25578=CARTESIAN_POINT('Ctrl Pts',(177.812004577715,4.72671681332008,129.445194980428));
#25579=CARTESIAN_POINT('Ctrl Pts',(177.804248274973,4.68878852956294,129.313293281594));
#25580=CARTESIAN_POINT('Ctrl Pts',(177.796491972232,4.64535498329599,129.183050257527));
#25581=CARTESIAN_POINT('Ctrl Pts',(177.78873566949,4.59660078782142,129.054948070481));
#25582=CARTESIAN_POINT('Ctrl Pts',(177.780975226976,4.54782057076469,128.92677751144));
#25583=CARTESIAN_POINT('Ctrl Pts',(177.773214784461,4.49371420013841,128.800750425285));
#25584=CARTESIAN_POINT('Ctrl Pts',(177.765454341947,4.43451361735137,128.677326993002));
#25585=CARTESIAN_POINT('Ctrl Pts',(177.757681441682,4.37521800053336,128.553705430469));
#25586=CARTESIAN_POINT('Ctrl Pts',(177.749908541416,4.31081201373659,128.432696219338));
#25587=CARTESIAN_POINT('Ctrl Pts',(177.742135641151,4.24157298806052,128.314733808292));
#25588=CARTESIAN_POINT('Ctrl Pts',(177.734645305389,4.17485097537009,128.201059628016));
#25589=CARTESIAN_POINT('Ctrl Pts',(177.727154969627,4.10364137597732,128.090214835132));
#25590=CARTESIAN_POINT('Ctrl Pts',(177.719664633865,4.02822814525213,127.98255958413));
#25591=CARTESIAN_POINT('Ctrl Pts',(177.711890299746,3.94995559896276,127.870822551566));
#25592=CARTESIAN_POINT('Ctrl Pts',(177.704115965627,3.86690642362824,127.762167748963));
#25593=CARTESIAN_POINT('Ctrl Pts',(177.696341631508,3.77935144632403,127.657030684485));
#25594=CARTESIAN_POINT('Ctrl Pts',(177.68857687856,3.69190437270419,127.552023192042));
#25595=CARTESIAN_POINT('Ctrl Pts',(177.680812125613,3.59996279371412,127.450525109322));
#25596=CARTESIAN_POINT('Ctrl Pts',(177.673047372666,3.50384082928145,127.352943154326));
#25597=CARTESIAN_POINT('Ctrl Pts',(177.665290331781,3.40781433453969,127.255458119104));
#25598=CARTESIAN_POINT('Ctrl Pts',(177.657533290896,3.30761598964536,127.161881747948));
#25599=CARTESIAN_POINT('Ctrl Pts',(177.649776250011,3.20359996906105,127.07258754023));
#25600=CARTESIAN_POINT('Ctrl Pts',(177.642025058771,3.09966238776662,126.983360669968));
#25601=CARTESIAN_POINT('Ctrl Pts',(177.634273867531,2.99191315658411,126.898409789223));
#25602=CARTESIAN_POINT('Ctrl Pts',(177.626522676291,2.88074280878541,126.818071123296));
#25603=CARTESIAN_POINT('Ctrl Pts',(177.618774779514,2.76961971135003,126.737766603444));
#25604=CARTESIAN_POINT('Ctrl Pts',(177.611026882737,2.6550787055422,126.662070628012));
#25605=CARTESIAN_POINT('Ctrl Pts',(177.60327898596,2.53754268909244,126.591278590886));
#25606=CARTESIAN_POINT('Ctrl Pts',(177.595532709876,2.42003125864345,126.520501361928));
#25607=CARTESIAN_POINT('Ctrl Pts',(177.587786433792,2.29952639837607,126.454626232496));
#25608=CARTESIAN_POINT('Ctrl Pts',(177.580040157707,2.17647887947239,126.393904547077));
#25609=CARTESIAN_POINT('Ctrl Pts',(177.572293824442,2.05343045225994,126.333182413425));
#25610=CARTESIAN_POINT('Ctrl Pts',(177.564547491177,1.92783967955764,126.277613972709));
#25611=CARTESIAN_POINT('Ctrl Pts',(177.556801157911,1.80018039147927,126.227403809748));
#25612=CARTESIAN_POINT('Ctrl Pts',(177.549053089908,1.67249251498833,126.177182402568));
#25613=CARTESIAN_POINT('Ctrl Pts',(177.541305021905,1.54273556511313,126.132321803976));
#25614=CARTESIAN_POINT('Ctrl Pts',(177.533556953902,1.41140134997992,126.092977668603));
#25615=CARTESIAN_POINT('Ctrl Pts',(177.525800651161,1.27992755128002,126.053591717815));
#25616=CARTESIAN_POINT('Ctrl Pts',(177.518044348419,1.14687351377778,126.019734054521));
#25617=CARTESIAN_POINT('Ctrl Pts',(177.510288045677,1.01274468223166,125.991509978796));
#25618=CARTESIAN_POINT('Ctrl Pts',(177.502527603163,0.878544262089551,125.963270839032));
#25619=CARTESIAN_POINT('Ctrl Pts',(177.494767160649,0.743268290289755,125.940671342562));
#25620=CARTESIAN_POINT('Ctrl Pts',(177.487006718134,0.607429300126163,125.923765089575));
#25621=CARTESIAN_POINT('Ctrl Pts',(177.479233817869,0.471372249156296,125.906831697169));
#25622=CARTESIAN_POINT('Ctrl Pts',(177.471460917604,0.334750763605367,125.895609843503));
#25623=CARTESIAN_POINT('Ctrl Pts',(177.463688017338,0.198080261687735,125.890101032193));
#25624=CARTESIAN_POINT('Ctrl Pts',(177.456197681576,0.0663780767674675,
125.88479248005));
#25625=CARTESIAN_POINT('Ctrl Pts',(177.448707345814,-0.065369314635894,
125.884788814691));
#25626=CARTESIAN_POINT('Ctrl Pts',(177.441217010052,-0.196705419535636,
125.890045808722));
#25627=CARTESIAN_POINT('Ctrl Pts',(177.433442675933,-0.333021172771505,
125.895502123279));
#25628=CARTESIAN_POINT('Ctrl Pts',(177.425668341814,-0.469325643322197,
125.906643171715));
#25629=CARTESIAN_POINT('Ctrl Pts',(177.417894007695,-0.605106037185557,
125.92347650234));
#25630=CARTESIAN_POINT('Ctrl Pts',(177.410129254748,-0.740719093848522,
125.940289087391));
#25631=CARTESIAN_POINT('Ctrl Pts',(177.402364501801,-0.875808974658048,
125.962779948777));
#25632=CARTESIAN_POINT('Ctrl Pts',(177.394599748854,-1.0098637067454,125.990904649522));
#25633=CARTESIAN_POINT('Ctrl Pts',(177.386842707969,-1.14378529378262,126.019001416418));
#25634=CARTESIAN_POINT('Ctrl Pts',(177.379085667084,-1.27667339795259,126.052720807403));
#25635=CARTESIAN_POINT('Ctrl Pts',(177.371328626199,-1.40802234370792,126.091966731003));
#25636=CARTESIAN_POINT('Ctrl Pts',(177.363577434959,-1.53927223820197,126.131183058947));
#25637=CARTESIAN_POINT('Ctrl Pts',(177.355826243718,-1.66898491148166,126.175917512674));
#25638=CARTESIAN_POINT('Ctrl Pts',(177.348075052478,-1.79666639490785,126.22602326347));
#25639=CARTESIAN_POINT('Ctrl Pts',(177.340327155701,-1.92429361029779,126.276107717985));
#25640=CARTESIAN_POINT('Ctrl Pts',(177.332579258924,-2.04989098970907,126.331558786443));
#25641=CARTESIAN_POINT('Ctrl Pts',(177.324831362147,-2.17298142334587,126.392180340617));
#25642=CARTESIAN_POINT('Ctrl Pts',(177.317085086063,-2.29604610911759,126.452789214069));
#25643=CARTESIAN_POINT('Ctrl Pts',(177.309338809979,-2.41660454165909,126.51856624934));
#25644=CARTESIAN_POINT('Ctrl Pts',(177.301592533895,-2.53420160489976,126.589268057702));
#25645=CARTESIAN_POINT('Ctrl Pts',(177.293846200629,-2.65179953621539,126.659970387969));
#25646=CARTESIAN_POINT('Ctrl Pts',(177.286099867364,-2.76643571954052,126.735597362417));
#25647=CARTESIAN_POINT('Ctrl Pts',(177.278353534098,-2.87768191512406,126.815860917445));
#25648=CARTESIAN_POINT('Ctrl Pts',(177.270605466096,-2.98895302352125,126.896142446938));
#25649=CARTESIAN_POINT('Ctrl Pts',(177.262857398093,-3.09683231653177,126.981062394456));
#25650=CARTESIAN_POINT('Ctrl Pts',(177.25510933009,-3.20092300320065,127.070291123022));
#25651=CARTESIAN_POINT('Ctrl Pts',(177.247353027348,-3.30512431869023,127.159614684944));
#25652=CARTESIAN_POINT('Ctrl Pts',(177.239596724606,-3.40552868701428,127.25325592095));
#25653=CARTESIAN_POINT('Ctrl Pts',(177.231840421864,-3.50177431099875,127.350846503315));
#25654=CARTESIAN_POINT('Ctrl Pts',(177.22407997935,-3.5980713041704,127.448489172712));
#25655=CARTESIAN_POINT('Ctrl Pts',(177.216319536836,-3.69020486765812,127.550085099136));
#25656=CARTESIAN_POINT('Ctrl Pts',(177.208559094322,-3.77785286934135,127.655232046023));
#25657=CARTESIAN_POINT('Ctrl Pts',(177.200786194056,-3.86564157137814,127.760547784123));
#25658=CARTESIAN_POINT('Ctrl Pts',(177.193013293791,-3.94893008479244,127.869425623223));
#25659=CARTESIAN_POINT('Ctrl Pts',(177.185240393525,-4.02743854841442,127.981432740123));
#25660=CARTESIAN_POINT('Ctrl Pts',(177.177750057763,-4.10309303163337,128.089368116195));
#25661=CARTESIAN_POINT('Ctrl Pts',(177.170259722001,-4.17430879856663,128.200208946648));
#25662=CARTESIAN_POINT('Ctrl Pts',(177.162769386239,-4.24087631336455,128.313547265016));
#25663=CARTESIAN_POINT('Ctrl Pts',(177.154700370286,-4.31258662861912,128.435641751572));
#25664=CARTESIAN_POINT('Ctrl Pts',(177.146631354333,-4.37911546164311,128.560996731004));
#25665=CARTESIAN_POINT('Ctrl Pts',(177.13856233838,-4.44016575555388,128.689151141957));
#25666=CARTESIAN_POINT('Ctrl Pts',(177.130504536925,-4.50113120040202,128.817127441046));
#25667=CARTESIAN_POINT('Ctrl Pts',(177.122446735471,-4.55663311807126,128.947895111476));
#25668=CARTESIAN_POINT('Ctrl Pts',(177.114388934016,-4.60641880221569,129.080966036777));
#25669=CARTESIAN_POINT('Ctrl Pts',(177.106344406022,-4.65612247536795,129.213817756923));
#25670=CARTESIAN_POINT('Ctrl Pts',(177.098299878028,-4.7001285599589,129.348964844431));
#25671=CARTESIAN_POINT('Ctrl Pts',(177.090255350033,-4.73823142587321,129.485897111295));
#25672=CARTESIAN_POINT('Ctrl Pts',(177.088369420506,-4.74716412148423,129.517999007829));
#25673=CARTESIAN_POINT('Ctrl Pts',(177.086483490979,-4.75577257872343,129.550198923862));
#25674=CARTESIAN_POINT('Ctrl Pts',(177.084597561451,-4.76405452823403,129.582490119308));
#25675=CARTESIAN_POINT('Ctrl Pts',(178.834794689177,-4.76405452823405,129.582490119308));
#25676=CARTESIAN_POINT('Ctrl Pts',(178.834348169157,-4.76600152135323,129.59008141593));
#25677=CARTESIAN_POINT('Ctrl Pts',(178.833901649136,-4.76793019492675,129.597676684138));
#25678=CARTESIAN_POINT('Ctrl Pts',(178.833455129116,-4.76984053507245,129.605275828037));
#25679=CARTESIAN_POINT('Ctrl Pts',(178.823192962182,-4.81374501544364,129.779923502642));
#25680=CARTESIAN_POINT('Ctrl Pts',(178.812930795248,-4.84807446073973,129.95706774057));
#25681=CARTESIAN_POINT('Ctrl Pts',(178.802668628314,-4.87259841686327,130.13580416484));
#25682=CARTESIAN_POINT('Ctrl Pts',(178.792640946099,-4.89656201443736,130.310456562743));
#25683=CARTESIAN_POINT('Ctrl Pts',(178.782613263885,-4.91116315740482,130.486629512172));
#25684=CARTESIAN_POINT('Ctrl Pts',(178.772585581671,-4.9162311945412,130.663456734298));
#25685=CARTESIAN_POINT('Ctrl Pts',(178.77001019979,-4.91753280449775,130.708870780548));
#25686=CARTESIAN_POINT('Ctrl Pts',(178.76743481791,-4.91820583999571,130.754327852339));
#25687=CARTESIAN_POINT('Ctrl Pts',(178.764859436029,-4.91824789753406,130.799812991619));
#25688=CARTESIAN_POINT('',(179.11014056404,-4.9182496345238,130.80625666781));
#25689=CARTESIAN_POINT('Ctrl Pts',(179.180279212536,-4.76405452823405,129.582490119308));
#25690=CARTESIAN_POINT('Ctrl Pts',(179.172592770908,-4.79783235438911,129.714189350837));
#25691=CARTESIAN_POINT('Ctrl Pts',(179.16490632928,-4.82611955095255,129.847191517955));
#25692=CARTESIAN_POINT('Ctrl Pts',(179.157219887652,-4.84884024883698,129.980994779218));
#25693=CARTESIAN_POINT('Ctrl Pts',(179.149373333716,-4.87203422987842,130.117585227311));
#25694=CARTESIAN_POINT('Ctrl Pts',(179.141526779781,-4.88942719215613,130.255010073371));
#25695=CARTESIAN_POINT('Ctrl Pts',(179.133680225846,-4.90099431101235,130.392732355751));
#25696=CARTESIAN_POINT('Ctrl Pts',(179.125833671911,-4.91256142986858,130.530454638131));
#25697=CARTESIAN_POINT('Ctrl Pts',(179.117987117976,-4.91830275159455,130.668473919319));
#25698=CARTESIAN_POINT('Ctrl Pts',(179.11014056404,-4.9182496345238,130.80625666781));
#25699=CARTESIAN_POINT('Ctrl Pts',(179.110140564008,-4.91824963452358,130.806256668381));
#25700=CARTESIAN_POINT('Ctrl Pts',(179.104198294929,-4.9182094084543,130.910600839437));
#25701=CARTESIAN_POINT('Ctrl Pts',(179.09825602585,-4.91484884784317,131.014877292883));
#25702=CARTESIAN_POINT('Ctrl Pts',(179.09231375677,-4.90817921990328,131.11893939595));
#25703=CARTESIAN_POINT('Ctrl Pts',(179.084539422651,-4.89945327441634,131.255084957113));
#25704=CARTESIAN_POINT('Ctrl Pts',(179.076765088532,-4.88504450286705,131.391082820901));
#25705=CARTESIAN_POINT('Ctrl Pts',(179.068990754413,-4.86495766475957,131.526420159846));
#25706=CARTESIAN_POINT('Ctrl Pts',(179.061226001466,-4.84489558188487,131.661590707615));
#25707=CARTESIAN_POINT('Ctrl Pts',(179.053461248519,-4.81916941265581,131.796101967218));
#25708=CARTESIAN_POINT('Ctrl Pts',(179.045696495572,-4.78783586718883,131.929443179585));
#25709=CARTESIAN_POINT('Ctrl Pts',(179.037939454687,-4.75653344264092,132.062651955581));
#25710=CARTESIAN_POINT('Ctrl Pts',(179.030182413802,-4.71963481392058,132.194692618852));
#25711=CARTESIAN_POINT('Ctrl Pts',(179.022425372917,-4.67724817964733,132.325061945403));
#25712=CARTESIAN_POINT('Ctrl Pts',(179.014674181676,-4.63489350946472,132.455332959431));
#25713=CARTESIAN_POINT('Ctrl Pts',(179.006922990436,-4.58705919165299,132.583934775123));
#25714=CARTESIAN_POINT('Ctrl Pts',(178.999171799196,-4.53390386652968,132.710377089574));
#25715=CARTESIAN_POINT('Ctrl Pts',(178.991423902419,-4.48077113383746,132.836765662669));
#25716=CARTESIAN_POINT('Ctrl Pts',(178.983676005642,-4.42232204312134,132.960996200391));
#25717=CARTESIAN_POINT('Ctrl Pts',(178.975928108865,-4.35876411544756,133.082596436876));
#25718=CARTESIAN_POINT('Ctrl Pts',(178.968181832781,-4.29521948272209,133.204171237213));
#25719=CARTESIAN_POINT('Ctrl Pts',(178.960435556697,-4.22656831964791,133.323116484425));
#25720=CARTESIAN_POINT('Ctrl Pts',(178.952689280612,-4.15306486639283,133.438983034163));
#25721=CARTESIAN_POINT('Ctrl Pts',(178.944942947347,-4.07956087055197,133.554850439201));
#25722=CARTESIAN_POINT('Ctrl Pts',(178.937196614082,-4.00120472249036,133.667638771277));
#25723=CARTESIAN_POINT('Ctrl Pts',(178.929450280816,-3.91829467942949,133.776926826695));
#25724=CARTESIAN_POINT('Ctrl Pts',(178.921702212813,-3.83536606923948,133.886239356415));
#25725=CARTESIAN_POINT('Ctrl Pts',(178.91395414481,-3.74788177099222,133.992049738264));
#25726=CARTESIAN_POINT('Ctrl Pts',(178.906206076807,-3.65618084862433,134.093969205932));
#25727=CARTESIAN_POINT('Ctrl Pts',(178.898449774065,-3.56438246542475,134.195996994824));
#25728=CARTESIAN_POINT('Ctrl Pts',(178.890693471324,-3.4683587677859,134.294125317703));
#25729=CARTESIAN_POINT('Ctrl Pts',(178.882937168582,-3.3684866595003,134.388001320436));
#25730=CARTESIAN_POINT('Ctrl Pts',(178.875176726068,-3.2685612464633,134.481927427618));
#25731=CARTESIAN_POINT('Ctrl Pts',(178.867416283553,-3.1647836256717,134.571596436813));
#25732=CARTESIAN_POINT('Ctrl Pts',(178.859655841039,-3.0575636481392,134.656695961235));
#25733=CARTESIAN_POINT('Ctrl Pts',(178.851882940774,-2.95017155158026,134.741932094967));
#25734=CARTESIAN_POINT('Ctrl Pts',(178.844110040508,-2.83932637193757,134.822583855418));
#25735=CARTESIAN_POINT('Ctrl Pts',(178.836337140243,-2.7254675236648,134.898381848575));
#25736=CARTESIAN_POINT('Ctrl Pts',(178.828846804481,-2.61574773132176,134.971424393755));
#25737=CARTESIAN_POINT('Ctrl Pts',(178.821356468719,-2.50322983824925,135.039959777996));
#25738=CARTESIAN_POINT('Ctrl Pts',(178.813866132957,-2.38832672171129,135.10378831586));
#25739=CARTESIAN_POINT('Ctrl Pts',(178.806091798838,-2.26906701858384,135.170036932139));
#25740=CARTESIAN_POINT('Ctrl Pts',(178.798317464719,-2.1468598711432,135.231424591867));
#25741=CARTESIAN_POINT('Ctrl Pts',(178.7905431306,-2.02213930829118,135.287678103576));
#25742=CARTESIAN_POINT('Ctrl Pts',(178.782778377653,-1.8975724523863,135.34386228786));
#25743=CARTESIAN_POINT('Ctrl Pts',(178.775013624706,-1.77049869726083,135.39492475452));
#25744=CARTESIAN_POINT('Ctrl Pts',(178.767248871759,-1.64137841218754,135.440637137631));
#25745=CARTESIAN_POINT('Ctrl Pts',(178.759491830874,-1.51238637120182,135.486304118559));
#25746=CARTESIAN_POINT('Ctrl Pts',(178.751734789989,-1.38135221148386,135.526631460963));
#25747=CARTESIAN_POINT('Ctrl Pts',(178.743977749104,-1.24875779362943,135.561438190546));
#25748=CARTESIAN_POINT('Ctrl Pts',(178.736226557863,-1.11626336625679,135.596218672103));
#25749=CARTESIAN_POINT('Ctrl Pts',(178.728475366623,-0.982211399327259,
135.625486728446));
#25750=CARTESIAN_POINT('Ctrl Pts',(178.720724175383,-0.847100147526754,
135.649110807468));
#25751=CARTESIAN_POINT('Ctrl Pts',(178.712976278606,-0.712046321612475,
135.672724845628));
#25752=CARTESIAN_POINT('Ctrl Pts',(178.705228381829,-0.575934490605304,
135.690699610382));
#25753=CARTESIAN_POINT('Ctrl Pts',(178.697480485052,-0.439274155356607,
135.702954423847));
#25754=CARTESIAN_POINT('Ctrl Pts',(178.689734208968,-0.302642406504035,
135.715206673869));
#25755=CARTESIAN_POINT('Ctrl Pts',(178.681987932884,-0.165462770780643,
135.721741317591));
#25756=CARTESIAN_POINT('Ctrl Pts',(178.6742416568,-0.0282505490694401,135.722529480972));
#25757=CARTESIAN_POINT('Ctrl Pts',(178.666495323534,0.10896268551119,135.723317650172));
#25758=CARTESIAN_POINT('Ctrl Pts',(178.658748990269,0.246208115600862,135.718359252141));
#25759=CARTESIAN_POINT('Ctrl Pts',(178.651002657004,0.382970155287087,135.707677548243));
#25760=CARTESIAN_POINT('Ctrl Pts',(178.643254589001,0.519762821883836,135.69699345225));
#25761=CARTESIAN_POINT('Ctrl Pts',(178.635506520998,0.6560714929648,135.680583530403));
#25762=CARTESIAN_POINT('Ctrl Pts',(178.627758452995,0.791385816082687,135.658522909105));
#25763=CARTESIAN_POINT('Ctrl Pts',(178.620002150253,0.926843952873513,135.636438841517));
#25764=CARTESIAN_POINT('Ctrl Pts',(178.612245847511,1.06130524413376,135.608692140596));
#25765=CARTESIAN_POINT('Ctrl Pts',(178.604489544769,1.19426909797958,135.575409179896));
#25766=CARTESIAN_POINT('Ctrl Pts',(178.596729102255,1.32730391863779,135.542108455078));
#25767=CARTESIAN_POINT('Ctrl Pts',(178.588968659741,1.45883933457868,135.503265693328));
#25768=CARTESIAN_POINT('Ctrl Pts',(178.581208217227,1.58839099146788,135.459056861224));
#25769=CARTESIAN_POINT('Ctrl Pts',(178.573435316961,1.71815061617768,135.414777061178));
#25770=CARTESIAN_POINT('Ctrl Pts',(178.565662416696,1.84591975356253,135.365114118798));
#25771=CARTESIAN_POINT('Ctrl Pts',(178.55788951643,1.97123424056386,135.310292111866));
#25772=CARTESIAN_POINT('Ctrl Pts',(178.550399180668,2.09199323031518,135.257463022974));
#25773=CARTESIAN_POINT('Ctrl Pts',(178.542908844906,2.21047265971088,135.199843582111));
#25774=CARTESIAN_POINT('Ctrl Pts',(178.535418509144,2.32628135749008,135.137673219755));
#25775=CARTESIAN_POINT('Ctrl Pts',(178.527644175025,2.44648097724423,135.073145649215));
#25776=CARTESIAN_POINT('Ctrl Pts',(178.519869840906,2.56418410222925,135.003510844547));
#25777=CARTESIAN_POINT('Ctrl Pts',(178.512095506787,2.67892628550298,134.928986299897));
#25778=CARTESIAN_POINT('Ctrl Pts',(178.50433075384,2.7935270592906,134.854553600087));
#25779=CARTESIAN_POINT('Ctrl Pts',(178.496566000893,2.90517382725016,134.775243361484));
#25780=CARTESIAN_POINT('Ctrl Pts',(178.488801247946,3.01342561782393,134.691319468434));
#25781=CARTESIAN_POINT('Ctrl Pts',(178.481044207061,3.12156989119321,134.607478929778));
#25782=CARTESIAN_POINT('Ctrl Pts',(178.473287166176,3.22632559050266,134.519034093746));
#25783=CARTESIAN_POINT('Ctrl Pts',(178.465530125291,3.32727999952759,134.426292542277));
#25784=CARTESIAN_POINT('Ctrl Pts',(178.457778934051,3.42815827804732,134.333620927934));
#25785=CARTESIAN_POINT('Ctrl Pts',(178.45002774281,3.52524068528896,134.236659310972));
#25786=CARTESIAN_POINT('Ctrl Pts',(178.44227655157,3.61814722391349,134.135755780045));
#25787=CARTESIAN_POINT('Ctrl Pts',(178.434528654793,3.7110142747808,134.03489513581));
#25788=CARTESIAN_POINT('Ctrl Pts',(178.426780758016,3.79970872281605,133.930096196904));
#25789=CARTESIAN_POINT('Ctrl Pts',(178.419032861239,3.88388729377466,133.821744012456));
#25790=CARTESIAN_POINT('Ctrl Pts',(178.411286585155,3.9680482563909,133.713414492949));
#25791=CARTESIAN_POINT('Ctrl Pts',(178.403540309071,4.04769498113156,133.601533514834));
#25792=CARTESIAN_POINT('Ctrl Pts',(178.395794032987,4.12252464273607,133.486519008216));
#25793=CARTESIAN_POINT('Ctrl Pts',(178.388047699721,4.19735485671613,133.371503652587));
#25794=CARTESIAN_POINT('Ctrl Pts',(178.380301366456,4.26736772339357,133.253355050009));
#25795=CARTESIAN_POINT('Ctrl Pts',(178.372555033191,4.33230412643069,133.132519550846));
#25796=CARTESIAN_POINT('Ctrl Pts',(178.364806965188,4.39725507152502,133.011656991411));
#25797=CARTESIAN_POINT('Ctrl Pts',(178.357058897185,4.45712710576504,132.888106682375));
#25798=CARTESIAN_POINT('Ctrl Pts',(178.349310829182,4.51170757715973,132.762338605363));
#25799=CARTESIAN_POINT('Ctrl Pts',(178.34155452644,4.56634605732897,132.636436860543));
#25800=CARTESIAN_POINT('Ctrl Pts',(178.333798223698,4.61568158434175,132.508312998465));
#25801=CARTESIAN_POINT('Ctrl Pts',(178.326041920956,4.65954989770892,132.378456489253));
#25802=CARTESIAN_POINT('Ctrl Pts',(178.318281478442,4.70344162491581,132.248530671711));
#25803=CARTESIAN_POINT('Ctrl Pts',(178.310521035928,4.74186021461869,132.116870739491));
#25804=CARTESIAN_POINT('Ctrl Pts',(178.302760593414,4.77469190713376,131.983979307843));
#25805=CARTESIAN_POINT('Ctrl Pts',(178.294987693148,4.80757630399631,131.850874547072));
#25806=CARTESIAN_POINT('Ctrl Pts',(178.287214792883,4.83485580373611,131.716534719739));
#25807=CARTESIAN_POINT('Ctrl Pts',(178.279441892618,4.85646803786491,131.581471458886));
#25808=CARTESIAN_POINT('Ctrl Pts',(178.271951556856,4.87729461284502,131.451318087769));
#25809=CARTESIAN_POINT('Ctrl Pts',(178.264461221094,4.89285877098853,131.320493273089));
#25810=CARTESIAN_POINT('Ctrl Pts',(178.256970885332,4.90315051431672,131.189455536327));
#25811=CARTESIAN_POINT('Ctrl Pts',(178.249196551213,4.91383247222137,131.053449463947));
#25812=CARTESIAN_POINT('Ctrl Pts',(178.241422217093,4.91886815300688,130.916783178524));
#25813=CARTESIAN_POINT('Ctrl Pts',(178.233647882974,4.91818949574107,130.779964993322));
#25814=CARTESIAN_POINT('Ctrl Pts',(178.225883130027,4.91751167485968,130.643315424305));
#25815=CARTESIAN_POINT('Ctrl Pts',(178.21811837708,4.91113353014638,130.506514715195));
#25816=CARTESIAN_POINT('Ctrl Pts',(178.210353624133,4.89903871907738,130.370076503787));
#25817=CARTESIAN_POINT('Ctrl Pts',(178.202596583248,4.88695592074523,130.233773804734));
#25818=CARTESIAN_POINT('Ctrl Pts',(178.194839542363,4.86916778958114,130.097833273809));
#25819=CARTESIAN_POINT('Ctrl Pts',(178.187082501478,4.84571001977967,129.962768396412));
#25820=CARTESIAN_POINT('Ctrl Pts',(178.179331310238,4.82226993966489,129.827805372489));
#25821=CARTESIAN_POINT('Ctrl Pts',(178.171580118998,4.793168797703,129.693717071373));
#25822=CARTESIAN_POINT('Ctrl Pts',(178.163828927758,4.75849405289253,129.561011346007));
#25823=CARTESIAN_POINT('Ctrl Pts',(178.156081030981,4.72383404577358,129.428362024114));
#25824=CARTESIAN_POINT('Ctrl Pts',(178.148333134204,4.68360524605732,129.297094486689));
#25825=CARTESIAN_POINT('Ctrl Pts',(178.140585237426,4.63794605836684,129.167705668538));
#25826=CARTESIAN_POINT('Ctrl Pts',(178.132838961342,4.59229642159413,129.038343915737));
#25827=CARTESIAN_POINT('Ctrl Pts',(178.125092685258,4.54121878627432,128.910860468985));
#25828=CARTESIAN_POINT('Ctrl Pts',(178.117346409174,4.48490108438993,128.785736005178));
#25829=CARTESIAN_POINT('Ctrl Pts',(178.109600075909,4.42858296678106,128.660610617731));
#25830=CARTESIAN_POINT('Ctrl Pts',(178.101853742643,4.36702486588853,128.537844604495));
#25831=CARTESIAN_POINT('Ctrl Pts',(178.094107409378,4.30046225020525,128.417897230657));
#25832=CARTESIAN_POINT('Ctrl Pts',(178.086359341375,4.23388472828575,128.297922995436));
#25833=CARTESIAN_POINT('Ctrl Pts',(178.078611273372,4.16230065112997,128.180768997448));
#25834=CARTESIAN_POINT('Ctrl Pts',(178.070863205369,4.08599048399426,128.066868183383));
#25835=CARTESIAN_POINT('Ctrl Pts',(178.063106902627,4.00959921350474,127.952846314178));
#25836=CARTESIAN_POINT('Ctrl Pts',(178.055350599885,3.92847203712003,127.842084860995));
#25837=CARTESIAN_POINT('Ctrl Pts',(178.047594297143,3.84293197311061,127.734986591393));
#25838=CARTESIAN_POINT('Ctrl Pts',(178.039833854629,3.75734625379343,127.62783116022));
#25839=CARTESIAN_POINT('Ctrl Pts',(178.032073412115,3.66734321017411,127.524343103294));
#25840=CARTESIAN_POINT('Ctrl Pts',(178.024312969601,3.57328421681137,127.42488980568));
#25841=CARTESIAN_POINT('Ctrl Pts',(178.016540069336,3.47907423160235,127.325276856804));
#25842=CARTESIAN_POINT('Ctrl Pts',(178.00876716907,3.38079556611414,127.229711882971));
#25843=CARTESIAN_POINT('Ctrl Pts',(178.000994268805,3.27884496002266,127.138523906713));
#25844=CARTESIAN_POINT('Ctrl Pts',(177.993503933043,3.18060051525979,127.05065084308));
#25845=CARTESIAN_POINT('Ctrl Pts',(177.98601359728,3.07894670116865,126.966842268125));
#25846=CARTESIAN_POINT('Ctrl Pts',(177.978523261518,2.97426388070669,126.88735443549));
#25847=CARTESIAN_POINT('Ctrl Pts',(177.970748927399,2.86561197929017,126.804852797521));
#25848=CARTESIAN_POINT('Ctrl Pts',(177.96297459328,2.75335267124101,126.726744671128));
#25849=CARTESIAN_POINT('Ctrl Pts',(177.955200259161,2.63787682630871,126.653362073634));
#25850=CARTESIAN_POINT('Ctrl Pts',(177.947435506214,2.52254329503498,126.580069913634));
#25851=CARTESIAN_POINT('Ctrl Pts',(177.939670753267,2.40400144105069,126.511491902602));
#25852=CARTESIAN_POINT('Ctrl Pts',(177.93190600032,2.28267456884699,126.447919423743));
#25853=CARTESIAN_POINT('Ctrl Pts',(177.924148959435,2.16146820020326,126.384410085966));
#25854=CARTESIAN_POINT('Ctrl Pts',(177.91639191855,2.03748266210701,126.325896567003));
#25855=CARTESIAN_POINT('Ctrl Pts',(177.908634877665,1.91116925795102,126.272626387719));
#25856=CARTESIAN_POINT('Ctrl Pts',(177.900883686425,1.78495110771554,126.219396379892));
#25857=CARTESIAN_POINT('Ctrl Pts',(177.893132495185,1.65640894434316,126.17140199277));
#25858=CARTESIAN_POINT('Ctrl Pts',(177.885381303944,1.52601731262292,126.128844151541));
#25859=CARTESIAN_POINT('Ctrl Pts',(177.877633407167,1.3956811008245,126.086304398529));
#25860=CARTESIAN_POINT('Ctrl Pts',(177.86988551039,1.26349735500979,126.049196716703));
#25861=CARTESIAN_POINT('Ctrl Pts',(177.862137613613,1.12995897158237,126.017673267734));
#25862=CARTESIAN_POINT('Ctrl Pts',(177.854391337529,0.996448521506018,125.986156412791));
#25863=CARTESIAN_POINT('Ctrl Pts',(177.846645061445,0.861584377703353,125.960221557053));
#25864=CARTESIAN_POINT('Ctrl Pts',(177.838898785361,0.72587252908902,125.939970405626));
#25865=CARTESIAN_POINT('Ctrl Pts',(177.831152452096,0.590159678680649,125.91971910471));
#25866=CARTESIAN_POINT('Ctrl Pts',(177.82340611883,0.453599497657837,125.905151649526));
#25867=CARTESIAN_POINT('Ctrl Pts',(177.815659785565,0.316705655302379,125.896318177815));
#25868=CARTESIAN_POINT('Ctrl Pts',(177.807911717562,0.179781156520127,125.887482727909));
#25869=CARTESIAN_POINT('Ctrl Pts',(177.800163649559,0.042523237797915,125.884383841828));
#25870=CARTESIAN_POINT('Ctrl Pts',(177.792415581556,-0.0945522522296156,
125.887019574472));
#25871=CARTESIAN_POINT('Ctrl Pts',(177.784659278814,-0.231773427719213,
125.889658108404));
#25872=CARTESIAN_POINT('Ctrl Pts',(177.776902976072,-0.368811395686946,
125.898043428593));
#25873=CARTESIAN_POINT('Ctrl Pts',(177.769146673331,-0.505152697112924,
125.912121476324));
#25874=CARTESIAN_POINT('Ctrl Pts',(177.761386230816,-0.641566767996746,
125.926207037933));
#25875=CARTESIAN_POINT('Ctrl Pts',(177.753625788302,-0.777283044745458,
125.945991324944));
#25876=CARTESIAN_POINT('Ctrl Pts',(177.745865345788,-0.911797104123172,
125.971368883307));
#25877=CARTESIAN_POINT('Ctrl Pts',(177.738092445523,-1.04652709741053,125.99678717998));
#25878=CARTESIAN_POINT('Ctrl Pts',(177.730319545257,-1.18005063572303,126.027816601991));
#25879=CARTESIAN_POINT('Ctrl Pts',(177.722546644992,-1.31187645560094,126.064301205729));
#25880=CARTESIAN_POINT('Ctrl Pts',(177.71505630923,-1.43891007487704,126.099459502223));
#25881=CARTESIAN_POINT('Ctrl Pts',(177.707565973468,-1.5643669721172,126.139683153101));
#25882=CARTESIAN_POINT('Ctrl Pts',(177.700075637706,-1.68782595840395,126.18479065959));
#25883=CARTESIAN_POINT('Ctrl Pts',(177.692301143226,-1.81596857280812,126.231609396601));
#25884=CARTESIAN_POINT('Ctrl Pts',(177.684526648747,-1.94236462080105,126.283838170655));
#25885=CARTESIAN_POINT('Ctrl Pts',(177.676752154268,-2.06652346192655,126.341327585669));
#25886=CARTESIAN_POINT('Ctrl Pts',(177.668987278277,-2.19052869558818,126.398745875637));
#25887=CARTESIAN_POINT('Ctrl Pts',(177.661222402286,-2.3123018782479,126.461411693872));
#25888=CARTESIAN_POINT('Ctrl Pts',(177.653457526295,-2.43136903252473,126.529126391213));
#25889=CARTESIAN_POINT('Ctrl Pts',(177.645700399525,-2.55031735970011,126.596773510377));
#25890=CARTESIAN_POINT('Ctrl Pts',(177.637943272756,-2.66656469520047,126.669459289141));
#25891=CARTESIAN_POINT('Ctrl Pts',(177.630186145986,-2.77965883815893,126.746937814117));
#25892=CARTESIAN_POINT('Ctrl Pts',(177.6224349059,-2.89266715687538,126.82435754263));
#25893=CARTESIAN_POINT('Ctrl Pts',(177.614683665815,-3.00252672482441,126.906562557649));
#25894=CARTESIAN_POINT('Ctrl Pts',(177.60693242573,-3.10881198829223,126.993262208452));
#25895=CARTESIAN_POINT('Ctrl Pts',(177.599184669519,-3.21504948075091,127.079922891202));
#25896=CARTESIAN_POINT('Ctrl Pts',(177.591436913309,-3.31771556266314,127.171073943901));
#25897=CARTESIAN_POINT('Ctrl Pts',(177.583689157098,-3.41641581650257,127.266382942219));
#25898=CARTESIAN_POINT('Ctrl Pts',(177.575943074336,-3.51509475193759,127.361671354615));
#25899=CARTESIAN_POINT('Ctrl Pts',(177.568196991574,-3.60980928238566,127.461115654579));
#25900=CARTESIAN_POINT('Ctrl Pts',(177.560450908813,-3.70020036884153,127.5643451403));
#25901=CARTESIAN_POINT('Ctrl Pts',(177.55270482166,-3.79059150653467,127.667574684535));
#25902=CARTESIAN_POINT('Ctrl Pts',(177.544958734507,-3.87665893800549,127.774589124554));
#25903=CARTESIAN_POINT('Ctrl Pts',(177.537212647354,-3.95808286043119,127.884983435279));
#25904=CARTESIAN_POINT('Ctrl Pts',(177.529464878335,-4.03952446199705,127.995401715328));
#25905=CARTESIAN_POINT('Ctrl Pts',(177.521717109316,-4.11632031667493,128.109201011568));
#25906=CARTESIAN_POINT('Ctrl Pts',(177.513969340297,-4.18819326244221,128.225946326004));
#25907=CARTESIAN_POINT('Ctrl Pts',(177.506214060889,-4.26013587907757,128.342804808855));
#25908=CARTESIAN_POINT('Ctrl Pts',(177.498458781481,-4.32714585161612,128.462614679699));
#25909=CARTESIAN_POINT('Ctrl Pts',(177.490703502072,-4.38899120993295,128.584914916128));
#25910=CARTESIAN_POINT('Ctrl Pts',(177.482944104692,-4.4508694074842,128.707280092696));
#25911=CARTESIAN_POINT('Ctrl Pts',(177.475184707312,-4.50757736508188,128.832137914138));
#25912=CARTESIAN_POINT('Ctrl Pts',(177.467425309932,-4.55893121262907,128.959007193147));
#25913=CARTESIAN_POINT('Ctrl Pts',(177.459655143061,-4.61035633565865,129.086052557677));
#25914=CARTESIAN_POINT('Ctrl Pts',(177.45188497619,-4.65641237482056,129.21511458816));
#25915=CARTESIAN_POINT('Ctrl Pts',(177.444114809319,-4.69696510604612,129.345696209594));
#25916=CARTESIAN_POINT('Ctrl Pts',(177.439448488999,-4.72131877012145,129.424116105041));
#25917=CARTESIAN_POINT('Ctrl Pts',(177.434782168678,-4.74368863307899,129.503083803194));
#25918=CARTESIAN_POINT('Ctrl Pts',(177.430115848357,-4.76405452823405,129.582490119308));
#25919=CARTESIAN_POINT('Origin',(213.235140564004,0.,130.804360617566));
#25920=CARTESIAN_POINT('',(175.334949039109,-4.76405452823403,129.582490119308));
#25921=CARTESIAN_POINT('',(175.679864508177,-4.76405452823404,129.582490119308));
#25922=CARTESIAN_POINT('',(213.235140564004,-4.76405452823405,129.582490119308));
#25923=CARTESIAN_POINT('',(177.014859435954,-4.91824992708477,130.805207512282));
#25924=CARTESIAN_POINT('Ctrl Pts',(177.014859435954,-4.91824992708477,130.805207512282));
#25925=CARTESIAN_POINT('Ctrl Pts',(177.006631410613,-4.9182247716926,130.951294745208));
#25926=CARTESIAN_POINT('Ctrl Pts',(176.998403385273,-4.91168649620771,131.097221500934));
#25927=CARTESIAN_POINT('Ctrl Pts',(176.990175359932,-4.89870335558759,131.242411409661));
#25928=CARTESIAN_POINT('Ctrl Pts',(176.981932190048,-4.88569631813616,131.387868555634));
#25929=CARTESIAN_POINT('Ctrl Pts',(176.973689020164,-4.86622075556974,131.532585836547));
#25930=CARTESIAN_POINT('Ctrl Pts',(176.96544585028,-4.84039616539851,131.67599587643));
#25931=CARTESIAN_POINT('Ctrl Pts',(176.957179149515,-4.81449785657614,131.81981529337));
#25932=CARTESIAN_POINT('Ctrl Pts',(176.94891244875,-4.78221432656776,131.962319697986));
#25933=CARTESIAN_POINT('Ctrl Pts',(176.940645747984,-4.7437157708782,132.102953605234));
#25934=CARTESIAN_POINT('Ctrl Pts',(176.932366109354,-4.70515696271938,132.243807612692));
#25935=CARTESIAN_POINT('Ctrl Pts',(176.924086470723,-4.6603638026299,132.382784981659));
#25936=CARTESIAN_POINT('Ctrl Pts',(176.915806832093,-4.60955515649318,132.519348757976));
#25937=CARTESIAN_POINT('Ctrl Pts',(176.907507626756,-4.55862643774319,132.656235266166));
#25938=CARTESIAN_POINT('Ctrl Pts',(176.899208421419,-4.50165392909692,132.790696489665));
#25939=CARTESIAN_POINT('Ctrl Pts',(176.890909216082,-4.43890382996342,132.922217045853));
#25940=CARTESIAN_POINT('Ctrl Pts',(176.888713398197,-4.42230130184235,132.957014978649));
#25941=CARTESIAN_POINT('Ctrl Pts',(176.886517580312,-4.40529456252688,132.991607204195));
#25942=CARTESIAN_POINT('Ctrl Pts',(176.884321762426,-4.38788905353696,133.025984509306));
#25943=CARTESIAN_POINT('Ctrl Pts',(176.876547428307,-4.32626452478983,133.14769799831));
#25944=CARTESIAN_POINT('Ctrl Pts',(176.868773094188,-4.2594743236812,133.267038271011));
#25945=CARTESIAN_POINT('Ctrl Pts',(176.860998760069,-4.18772473627818,133.383535794956));
#25946=CARTESIAN_POINT('Ctrl Pts',(176.853234007122,-4.11606357382926,133.499889746114));
#25947=CARTESIAN_POINT('Ctrl Pts',(176.845469254175,-4.03945538920248,133.613407589607));
#25948=CARTESIAN_POINT('Ctrl Pts',(176.837704501228,-3.95815340865091,133.723642148369));
#25949=CARTESIAN_POINT('Ctrl Pts',(176.829947460343,-3.87693217837241,133.833767220613));
#25950=CARTESIAN_POINT('Ctrl Pts',(176.822190419458,-3.79102666020864,133.940615185065));
#25951=CARTESIAN_POINT('Ctrl Pts',(176.814433378573,-3.70073444346966,134.043766063233));
#25952=CARTESIAN_POINT('Ctrl Pts',(176.806682187332,-3.61051031679379,134.146839154521));
#25953=CARTESIAN_POINT('Ctrl Pts',(176.798930996092,-3.51590633247001,134.246220415883));
#25954=CARTESIAN_POINT('Ctrl Pts',(176.791179804852,-3.41726136002214,134.34152160624));
#25955=CARTESIAN_POINT('Ctrl Pts',(176.783431908075,-3.31865831431899,134.43678229105));
#25956=CARTESIAN_POINT('Ctrl Pts',(176.775684011298,-3.21601797711347,134.527966082846));
#25957=CARTESIAN_POINT('Ctrl Pts',(176.767936114521,-3.10971704901438,134.614720566123));
#25958=CARTESIAN_POINT('Ctrl Pts',(176.760189838437,-3.00343835677783,134.701456902232));
#25959=CARTESIAN_POINT('Ctrl Pts',(176.752443562353,-2.8935008994043,134.783765525669));
#25960=CARTESIAN_POINT('Ctrl Pts',(176.744697286269,-2.78031521967282,134.861333669209));
#25961=CARTESIAN_POINT('Ctrl Pts',(176.736950953003,-2.6671287044304,134.938902385339));
#25962=CARTESIAN_POINT('Ctrl Pts',(176.729204619738,-2.55069424148432,135.011730330731));
#25963=CARTESIAN_POINT('Ctrl Pts',(176.721458286473,-2.43145183458326,135.079547752488));
#25964=CARTESIAN_POINT('Ctrl Pts',(176.71371021847,-2.31218272417198,135.147380361486));
#25965=CARTESIAN_POINT('Ctrl Pts',(176.705962150467,-2.19010475830888,135.210200020811));
#25966=CARTESIAN_POINT('Ctrl Pts',(176.698214082464,-2.06568268021461,135.267782861446));
#25967=CARTESIAN_POINT('Ctrl Pts',(176.690457779722,-1.94112836485505,135.325426901809));
#25968=CARTESIAN_POINT('Ctrl Pts',(176.68270147698,-1.81422531589903,135.377822840822));
#25969=CARTESIAN_POINT('Ctrl Pts',(176.674945174238,-1.68545892071563,135.424794719366));
#25970=CARTESIAN_POINT('Ctrl Pts',(176.667184731724,-1.55662379902994,135.471791668216));
#25971=CARTESIAN_POINT('Ctrl Pts',(176.65942428921,-1.42592372183812,135.513358669661));
#25972=CARTESIAN_POINT('Ctrl Pts',(176.651663846695,-1.2938584297329,135.549369935398));
#25973=CARTESIAN_POINT('Ctrl Pts',(176.64389094643,-1.16158113469664,135.585439009615));
#25974=CARTESIAN_POINT('Ctrl Pts',(176.636118046164,-1.02793462669097,135.615934438973));
#25975=CARTESIAN_POINT('Ctrl Pts',(176.628345145899,-0.893428894747038,
135.640781595162));
#25976=CARTESIAN_POINT('Ctrl Pts',(176.620854810137,-0.763812784960541,
135.664725494637));
#25977=CARTESIAN_POINT('Ctrl Pts',(176.613364474375,-0.633399141475654,
135.683424605516));
#25978=CARTESIAN_POINT('Ctrl Pts',(176.605874138613,-0.502646113807985,
135.696857929448));
#25979=CARTESIAN_POINT('Ctrl Pts',(176.598099804494,-0.366935545353002,
135.71080058194));
#25980=CARTESIAN_POINT('Ctrl Pts',(176.590325470375,-0.230429458897136,
135.719114426593));
#25981=CARTESIAN_POINT('Ctrl Pts',(176.582551136256,-0.0936343880487996,
135.72171922396));
#25982=CARTESIAN_POINT('Ctrl Pts',(176.574786383309,0.0429920951004432,
135.724320811146));
#25983=CARTESIAN_POINT('Ctrl Pts',(176.567021630362,0.179906466873114,135.721227342998));
#25984=CARTESIAN_POINT('Ctrl Pts',(176.559256877415,0.316595629564081,135.712410155808));
#25985=CARTESIAN_POINT('Ctrl Pts',(176.55149983653,0.453149030651684,135.703601725973));
#25986=CARTESIAN_POINT('Ctrl Pts',(176.543742795645,0.589477280162869,135.689080915264));
#25987=CARTESIAN_POINT('Ctrl Pts',(176.53598575476,0.725066184007642,135.668871085363));
#25988=CARTESIAN_POINT('Ctrl Pts',(176.528234563519,0.86055283920516,135.648676495852));
#25989=CARTESIAN_POINT('Ctrl Pts',(176.520483372279,0.995300873369753,135.622801483805));
#25990=CARTESIAN_POINT('Ctrl Pts',(176.512732181039,1.12880048103276,135.591321295963));
#25991=CARTESIAN_POINT('Ctrl Pts',(176.504984284262,1.26224334780143,135.559854488041));
#25992=CARTESIAN_POINT('Ctrl Pts',(176.497236387485,1.39443846368844,135.522787332179));
#25993=CARTESIAN_POINT('Ctrl Pts',(176.489488490708,1.52488571566593,135.480246268077));
#25994=CARTESIAN_POINT('Ctrl Pts',(176.481742214624,1.65530568089043,135.43771410265));
#25995=CARTESIAN_POINT('Ctrl Pts',(176.47399593854,1.78397813797108,135.389710427638));
#25996=CARTESIAN_POINT('Ctrl Pts',(176.466249662456,1.91041803858375,135.336411585986));
#25997=CARTESIAN_POINT('Ctrl Pts',(176.45850332919,2.036858872547,135.283112350893));
#25998=CARTESIAN_POINT('Ctrl Pts',(176.450756995925,2.16106675689199,135.224518023027));
#25999=CARTESIAN_POINT('Ctrl Pts',(176.44301066266,2.28257690809317,135.160852981973));
#26000=CARTESIAN_POINT('Ctrl Pts',(176.435262594657,2.40411427065022,135.097173683575));
#26001=CARTESIAN_POINT('Ctrl Pts',(176.427514526654,2.52295235165426,135.028421593787));
#26002=CARTESIAN_POINT('Ctrl Pts',(176.419766458651,2.6386515986994,134.954866707573));
#26003=CARTESIAN_POINT('Ctrl Pts',(176.412010155909,2.75447381228113,134.881233646349));
#26004=CARTESIAN_POINT('Ctrl Pts',(176.404253853167,2.8671501974432,134.80278780206));
#26005=CARTESIAN_POINT('Ctrl Pts',(176.396497550425,2.97627035106568,134.719842434644));
#26006=CARTESIAN_POINT('Ctrl Pts',(176.388737107911,3.08544874539976,134.636852796787));
#26007=CARTESIAN_POINT('Ctrl Pts',(176.380976665397,3.19106682520322,134.549359099839));
#26008=CARTESIAN_POINT('Ctrl Pts',(176.373216222883,3.29274863921616,134.457713798062));
#26009=CARTESIAN_POINT('Ctrl Pts',(176.365443322617,3.39459368190384,134.365921379111));
#26010=CARTESIAN_POINT('Ctrl Pts',(176.357670422352,3.49248955237282,134.26996431132));
#26011=CARTESIAN_POINT('Ctrl Pts',(176.349897522086,3.58609780218386,134.170231324482));
#26012=CARTESIAN_POINT('Ctrl Pts',(176.342407186324,3.67630315632983,134.074123882926));
#26013=CARTESIAN_POINT('Ctrl Pts',(176.334916850562,3.76252700773423,133.974510517335));
#26014=CARTESIAN_POINT('Ctrl Pts',(176.3274265148,3.84450404888564,133.871765331751));
#26015=CARTESIAN_POINT('Ctrl Pts',(176.319652180681,3.92958927446819,133.765124531226));
#26016=CARTESIAN_POINT('Ctrl Pts',(176.311877846562,4.01036882151141,133.65477193075));
#26017=CARTESIAN_POINT('Ctrl Pts',(176.304103512443,4.08650138850617,133.54109032001));
#26018=CARTESIAN_POINT('Ctrl Pts',(176.296338759496,4.16254012891625,133.427548811695));
#26019=CARTESIAN_POINT('Ctrl Pts',(176.288574006549,4.23394306881452,133.31068677801));
#26020=CARTESIAN_POINT('Ctrl Pts',(176.280809253602,4.30040875076859,133.190920409152));
#26021=CARTESIAN_POINT('Ctrl Pts',(176.273052212717,4.36680841807035,133.071272993939));
#26022=CARTESIAN_POINT('Ctrl Pts',(176.265295171832,4.42828039763348,132.94872732373));
#26023=CARTESIAN_POINT('Ctrl Pts',(176.257538130947,4.48456640983697,132.823728632134));
#26024=CARTESIAN_POINT('Ctrl Pts',(176.249786939707,4.5408099763208,132.698824203024));
#26025=CARTESIAN_POINT('Ctrl Pts',(176.242035748466,4.5918751997365,132.571470789575));
#26026=CARTESIAN_POINT('Ctrl Pts',(176.234284557226,4.63754982499086,132.442137978268));
#26027=CARTESIAN_POINT('Ctrl Pts',(176.226536660449,4.68320503731109,132.312860136855));
#26028=CARTESIAN_POINT('Ctrl Pts',(176.218788763672,4.72347407846985,132.18160493874));
#26029=CARTESIAN_POINT('Ctrl Pts',(176.211040866895,4.75819300246096,132.048861486923));
#26030=CARTESIAN_POINT('Ctrl Pts',(176.203294590811,4.79290466400163,131.916145802175));
#26031=CARTESIAN_POINT('Ctrl Pts',(176.195548314727,4.8220684187313,131.781942860941));
#26032=CARTESIAN_POINT('Ctrl Pts',(176.187802038643,4.84557044849468,131.646756065782));
#26033=CARTESIAN_POINT('Ctrl Pts',(176.180055705377,4.8690726517447,131.511568272705));
#26034=CARTESIAN_POINT('Ctrl Pts',(176.172309372112,4.88691297966808,131.375396996397));
#26035=CARTESIAN_POINT('Ctrl Pts',(176.164563038847,4.89902898231643,131.238754555051));
#26036=CARTESIAN_POINT('Ctrl Pts',(176.156814970844,4.91114769825956,131.102081513577));
#26037=CARTESIAN_POINT('Ctrl Pts',(176.149066902841,4.91753950352483,130.964937486466));
#26038=CARTESIAN_POINT('Ctrl Pts',(176.141318834838,4.91819396370879,130.827838220477));
#26039=CARTESIAN_POINT('Ctrl Pts',(176.133562532096,4.91884911946082,130.690593243756));
#26040=CARTESIAN_POINT('Ctrl Pts',(176.125806229354,4.91375474741247,130.553393514774));
#26041=CARTESIAN_POINT('Ctrl Pts',(176.118049926612,4.90295256911087,130.416753641946));
#26042=CARTESIAN_POINT('Ctrl Pts',(176.110289484098,4.89214462536145,130.280040840304));
#26043=CARTESIAN_POINT('Ctrl Pts',(176.102529041584,4.87562285216725,130.143888878153));
#26044=CARTESIAN_POINT('Ctrl Pts',(176.09476859907,4.85348056844284,130.008804564074));
#26045=CARTESIAN_POINT('Ctrl Pts',(176.086995698805,4.83130273995889,129.873503400662));
#26046=CARTESIAN_POINT('Ctrl Pts',(176.079222798539,4.80348645040933,129.739273693259));
#26047=CARTESIAN_POINT('Ctrl Pts',(176.071449898274,4.77017580952837,129.606610306069));
#26048=CARTESIAN_POINT('Ctrl Pts',(176.063959562512,4.73807609434798,129.478769567164));
#26049=CARTESIAN_POINT('Ctrl Pts',(176.05646922675,4.7008746464984,129.352383541698));
#26050=CARTESIAN_POINT('Ctrl Pts',(176.048978890988,4.65874280511444,129.227877652769));
#26051=CARTESIAN_POINT('Ctrl Pts',(176.041204556869,4.6150135221586,129.098651085218));
#26052=CARTESIAN_POINT('Ctrl Pts',(176.03343022275,4.56583407235678,128.971040688426));
#26053=CARTESIAN_POINT('Ctrl Pts',(176.02565588863,4.51134202571253,128.845540516194));
#26054=CARTESIAN_POINT('Ctrl Pts',(176.017891135683,4.45691713564568,128.720195011708));
#26055=CARTESIAN_POINT('Ctrl Pts',(176.010126382736,4.39719283013072,128.596954912415));
#26056=CARTESIAN_POINT('Ctrl Pts',(176.002361629789,4.33235631666133,128.476298803957));
#26057=CARTESIAN_POINT('Ctrl Pts',(175.994604588904,4.26758419973116,128.355762532847));
#26058=CARTESIAN_POINT('Ctrl Pts',(175.986847548019,4.19771016320102,128.237805487371));
#26059=CARTESIAN_POINT('Ctrl Pts',(175.979090507134,4.12296918827295,128.122885625131));
#26060=CARTESIAN_POINT('Ctrl Pts',(175.971339315894,4.04828457609545,128.008052424854));
#26061=CARTESIAN_POINT('Ctrl Pts',(175.963588124654,3.9687405431181,127.896252175402));
#26062=CARTESIAN_POINT('Ctrl Pts',(175.955836933414,3.88461743668457,127.787917275962));
#26063=CARTESIAN_POINT('Ctrl Pts',(175.948089036637,3.80053008481534,127.679628421744));
#26064=CARTESIAN_POINT('Ctrl Pts',(175.940341139859,3.71186776967313,127.574802296271));
#26065=CARTESIAN_POINT('Ctrl Pts',(175.932593243082,3.61895337064391,127.47384120408));
#26066=CARTESIAN_POINT('Ctrl Pts',(175.924846966998,3.52605840730398,127.372901230774));
#26067=CARTESIAN_POINT('Ctrl Pts',(175.917100690914,3.42891339381489,127.275824970133));
#26068=CARTESIAN_POINT('Ctrl Pts',(175.90935441483,3.32788033551458,127.182980281976));
#26069=CARTESIAN_POINT('Ctrl Pts',(175.901608081565,3.22684653141127,127.090134908461));
#26070=CARTESIAN_POINT('Ctrl Pts',(175.893861748299,3.12192491310012,127.001521434303));
#26071=CARTESIAN_POINT('Ctrl Pts',(175.886115415034,3.01351275266165,126.917469320907));
#26072=CARTESIAN_POINT('Ctrl Pts',(175.878367347031,2.90507631407145,126.833398384623));
#26073=CARTESIAN_POINT('Ctrl Pts',(175.870619279028,2.79314808681636,126.753891081245));
#26074=CARTESIAN_POINT('Ctrl Pts',(175.862871211025,2.67815634320237,126.679234963254));
#26075=CARTESIAN_POINT('Ctrl Pts',(175.855114908283,2.56304238499486,126.604499499852));
#26076=CARTESIAN_POINT('Ctrl Pts',(175.847358605541,2.44485873477475,126.534625734532));
#26077=CARTESIAN_POINT('Ctrl Pts',(175.839602302799,2.32406089869263,126.469856724193));
#26078=CARTESIAN_POINT('Ctrl Pts',(175.831841860285,2.20319858916816,126.405053144683));
#26079=CARTESIAN_POINT('Ctrl Pts',(175.824081417771,2.07971966540841,126.345359919152));
#26080=CARTESIAN_POINT('Ctrl Pts',(175.816320975257,1.95410096097882,126.290972478174));
#26081=CARTESIAN_POINT('Ctrl Pts',(175.808548074991,1.82828060225302,126.236497729648));
#26082=CARTESIAN_POINT('Ctrl Pts',(175.800775174726,1.70031396387985,126.18734592625));
#26083=CARTESIAN_POINT('Ctrl Pts',(175.79300227446,1.57069528396139,126.14366331057));
#26084=CARTESIAN_POINT('Ctrl Pts',(175.785511938698,1.44578856954715,126.101568668));
#26085=CARTESIAN_POINT('Ctrl Pts',(175.778021602936,1.3193481356255,126.064552565761));
#26086=CARTESIAN_POINT('Ctrl Pts',(175.770531267174,1.19182451568294,126.032700802961));
#26087=CARTESIAN_POINT('Ctrl Pts',(175.762756933055,1.05946579893085,125.999641370894));
#26088=CARTESIAN_POINT('Ctrl Pts',(175.754982598936,0.925520864102131,125.972040898323));
#26089=CARTESIAN_POINT('Ctrl Pts',(175.747208264817,0.790479732600394,125.950050691856));
#26090=CARTESIAN_POINT('Ctrl Pts',(175.73944351187,0.655605027224353,125.928087586353));
#26091=CARTESIAN_POINT('Ctrl Pts',(175.731678758923,0.51963719536985,125.911721052089));
#26092=CARTESIAN_POINT('Ctrl Pts',(175.723914005976,0.383080074915559,125.901052273325));
#26093=CARTESIAN_POINT('Ctrl Pts',(175.716156965091,0.246658584918514,125.890394090943));
#26094=CARTESIAN_POINT('Ctrl Pts',(175.708399924206,0.109649358329901,125.885422432471));
#26095=CARTESIAN_POINT('Ctrl Pts',(175.700642883321,-0.0274352990704107,
125.886187138838));
#26096=CARTESIAN_POINT('Ctrl Pts',(175.692891692081,-0.1644165798644,125.886951268534));
#26097=CARTESIAN_POINT('Ctrl Pts',(175.68514050084,-0.301472788870795,125.893443150581));
#26098=CARTESIAN_POINT('Ctrl Pts',(175.6773893096,-0.438088601822157,125.905660643139));
#26099=CARTESIAN_POINT('Ctrl Pts',(175.669641412823,-0.574646349408622,
125.917872942937));
#26100=CARTESIAN_POINT('Ctrl Pts',(175.661893516046,-0.710763684631094,
125.935805978375));
#26101=CARTESIAN_POINT('Ctrl Pts',(175.654145619269,-0.845927613093618,
125.959405557309));
#26102=CARTESIAN_POINT('Ctrl Pts',(175.646399343185,-0.98106326817615,125.983000199721));
#26103=CARTESIAN_POINT('Ctrl Pts',(175.638653067101,-1.11524552828541,126.012258960764));
#26104=CARTESIAN_POINT('Ctrl Pts',(175.630906791017,-1.24796922981086,126.04707611231));
#26105=CARTESIAN_POINT('Ctrl Pts',(175.623160457752,-1.38069391107248,126.081893520869));
#26106=CARTESIAN_POINT('Ctrl Pts',(175.615414124486,-1.51195963409641,126.122269302602));
#26107=CARTESIAN_POINT('Ctrl Pts',(175.607667791221,-1.64127447840742,126.168047303193));
#26108=CARTESIAN_POINT('Ctrl Pts',(175.599919723218,-1.77061828188111,126.213835555451));
#26109=CARTESIAN_POINT('Ctrl Pts',(175.592171655215,-1.89800996880706,126.265028303463));
#26110=CARTESIAN_POINT('Ctrl Pts',(175.584423587212,-2.02297612149675,126.321420658749));
#26111=CARTESIAN_POINT('Ctrl Pts',(175.57666728447,-2.14807508970072,126.377872948502));
#26112=CARTESIAN_POINT('Ctrl Pts',(175.568910981728,-2.27074301713271,126.43953572365));
#26113=CARTESIAN_POINT('Ctrl Pts',(175.561154678986,-2.39052920093837,126.506157132159));
#26114=CARTESIAN_POINT('Ctrl Pts',(175.553394236472,-2.51037931823709,126.57281409852));
#26115=CARTESIAN_POINT('Ctrl Pts',(175.545633793958,-2.62734429390807,126.644434767697));
#26116=CARTESIAN_POINT('Ctrl Pts',(175.537873351444,-2.74100196648704,126.720723601105));
#26117=CARTESIAN_POINT('Ctrl Pts',(175.530100451179,-2.85484209245202,126.79713490012));
#26118=CARTESIAN_POINT('Ctrl Pts',(175.522327550913,-2.96536399050178,126.878229106851));
#26119=CARTESIAN_POINT('Ctrl Pts',(175.514554650648,-3.07217747483731,126.963669452476));
#26120=CARTESIAN_POINT('Ctrl Pts',(175.507064314886,-3.17510801997039,127.046003826326));
#26121=CARTESIAN_POINT('Ctrl Pts',(175.499573979124,-3.27459485814811,127.132373636935));
#26122=CARTESIAN_POINT('Ctrl Pts',(175.492083643362,-3.37032227979657,127.222446214233));
#26123=CARTESIAN_POINT('Ctrl Pts',(175.484426013505,-3.46818774075487,127.314530531821));
#26124=CARTESIAN_POINT('Ctrl Pts',(175.476768383649,-3.56245359475089,127.410795582262));
#26125=CARTESIAN_POINT('Ctrl Pts',(175.469110753793,-3.65273331836966,127.510924362319));
#26126=CARTESIAN_POINT('Ctrl Pts',(175.461462005809,-3.74290832904258,127.610937005784));
#26127=CARTESIAN_POINT('Ctrl Pts',(175.453813257825,-3.82910613282586,127.714804174024));
#26128=CARTESIAN_POINT('Ctrl Pts',(175.446164509841,-3.91097428624597,127.822169611808));
#26129=CARTESIAN_POINT('Ctrl Pts',(175.438522859586,-3.99276646932869,127.929435418805));
#26130=CARTESIAN_POINT('Ctrl Pts',(175.430881209331,-4.07023674784178,128.040192721918));
#26131=CARTESIAN_POINT('Ctrl Pts',(175.423239559076,-4.1430708837805,128.154049934935));
#26132=CARTESIAN_POINT('Ctrl Pts',(175.415603284732,-4.21585378080787,128.267827049251));
#26133=CARTESIAN_POINT('Ctrl Pts',(175.407967010388,-4.28400680640056,128.384699396879));
#26134=CARTESIAN_POINT('Ctrl Pts',(175.400330736044,-4.3472575948339,128.504244432096));
#26135=CARTESIAN_POINT('Ctrl Pts',(175.392697732783,-4.41048128909551,128.623738258882));
#26136=CARTESIAN_POINT('Ctrl Pts',(175.385064729521,-4.46880673517313,128.745902139713));
#26137=CARTESIAN_POINT('Ctrl Pts',(175.377431726259,-4.52200655733599,128.870287258588));
#26138=CARTESIAN_POINT('Ctrl Pts',(175.369798525334,-4.5752077571597,128.994675598536));
#26139=CARTESIAN_POINT('Ctrl Pts',(175.362165324408,-4.62328289879717,129.121284924899));
#26140=CARTESIAN_POINT('Ctrl Pts',(175.354532123482,-4.66605208952326,129.249644900673));
#26141=CARTESIAN_POINT('Ctrl Pts',(175.348004428691,-4.70262707637903,129.359414675293));
#26142=CARTESIAN_POINT('Ctrl Pts',(175.3414767339,-4.73532246569085,129.470464243522));
#26143=CARTESIAN_POINT('Ctrl Pts',(175.334949039109,-4.76405452823403,129.582490119308));
#26144=CARTESIAN_POINT('Ctrl Pts',(177.084597561451,-4.76405452823403,129.582490119308));
#26145=CARTESIAN_POINT('Ctrl Pts',(177.076567484955,-4.79931814076276,129.719982409358));
#26146=CARTESIAN_POINT('Ctrl Pts',(177.068537408458,-4.82865840725863,129.859130859221));
#26147=CARTESIAN_POINT('Ctrl Pts',(177.060507331961,-4.85193039187213,129.999404385882));
#26148=CARTESIAN_POINT('Ctrl Pts',(177.05248775733,-4.87517194100357,130.13949446053));
#26149=CARTESIAN_POINT('Ctrl Pts',(177.044468182699,-4.89236097345581,130.280706334928));
#26150=CARTESIAN_POINT('Ctrl Pts',(177.036448608067,-4.90340326199463,130.422497405459));
#26151=CARTESIAN_POINT('Ctrl Pts',(177.029252217375,-4.91331209458416,130.549734071631));
#26152=CARTESIAN_POINT('Ctrl Pts',(177.022055826683,-4.91827192846218,130.677436781746));
#26153=CARTESIAN_POINT('Ctrl Pts',(177.014859435991,-4.91824992708488,130.805207511627));
#26154=CARTESIAN_POINT('',(177.360140563968,-4.91824793051881,130.799848805581));
#26155=CARTESIAN_POINT('Ctrl Pts',(177.430115848357,-4.76405452823405,129.582490119308));
#26156=CARTESIAN_POINT('Ctrl Pts',(177.427286570202,-4.77640275516735,129.630635668711));
#26157=CARTESIAN_POINT('Ctrl Pts',(177.424457292047,-4.78801440829828,129.678942445579));
#26158=CARTESIAN_POINT('Ctrl Pts',(177.421628013893,-4.79888619662381,129.727385996531));
#26159=CARTESIAN_POINT('Ctrl Pts',(177.410989040785,-4.83976753005932,129.909548939735));
#26160=CARTESIAN_POINT('Ctrl Pts',(177.400350067677,-4.87028956772032,130.094115230531));
#26161=CARTESIAN_POINT('Ctrl Pts',(177.389711094569,-4.89022784483775,130.280094761274));
#26162=CARTESIAN_POINT('Ctrl Pts',(177.379854251049,-4.90870034924447,130.452401911033));
#26163=CARTESIAN_POINT('Ctrl Pts',(177.369997407528,-4.91808837710366,130.625922424611));
#26164=CARTESIAN_POINT('Ctrl Pts',(177.360140564008,-4.91824793051816,130.79984880487));
#26165=CARTESIAN_POINT('Ctrl Pts',(177.360140563968,-4.91824793051882,130.799848805581));
#26166=CARTESIAN_POINT('Ctrl Pts',(177.352487945942,-4.91837180396175,130.934881095582));
#26167=CARTESIAN_POINT('Ctrl Pts',(177.344835327916,-4.91293045659475,131.070080067784));
#26168=CARTESIAN_POINT('Ctrl Pts',(177.33718270989,-4.90190951832219,131.204942864654));
#26169=CARTESIAN_POINT('Ctrl Pts',(177.329535914745,-4.89089696588737,131.339703044352));
#26170=CARTESIAN_POINT('Ctrl Pts',(177.321889119601,-4.87431330117688,131.474127158148));
#26171=CARTESIAN_POINT('Ctrl Pts',(177.314242324456,-4.85219622232653,131.607712895549));
#26172=CARTESIAN_POINT('Ctrl Pts',(177.306598711799,-4.83008834829065,131.74124303646));
#26173=CARTESIAN_POINT('Ctrl Pts',(177.298955099142,-4.80245170335256,131.87393509822));
#26174=CARTESIAN_POINT('Ctrl Pts',(177.291311486484,-4.76937573609459,132.005292818172));
#26175=CARTESIAN_POINT('Ctrl Pts',(177.283669304355,-4.73630595911592,132.136625954081));
#26176=CARTESIAN_POINT('Ctrl Pts',(177.276027122226,-4.69779898193594,132.266624854489));
#26177=CARTESIAN_POINT('Ctrl Pts',(177.268384940097,-4.65399505901825,132.394804911823));
#26178=CARTESIAN_POINT('Ctrl Pts',(177.260742427898,-4.61018924418316,132.522990505329));
#26179=CARTESIAN_POINT('Ctrl Pts',(177.253099915698,-4.56108615912356,132.649356718698));
#26180=CARTESIAN_POINT('Ctrl Pts',(177.245457403499,-4.50687529735599,132.773436064719));
#26181=CARTESIAN_POINT('Ctrl Pts',(177.237812800583,-4.45264960545219,132.897549354373));
#26182=CARTESIAN_POINT('Ctrl Pts',(177.230168197668,-4.39331351973143,133.019374164111));
#26183=CARTESIAN_POINT('Ctrl Pts',(177.222523594753,-4.32910360359455,133.138465382105));
#26184=CARTESIAN_POINT('Ctrl Pts',(177.21487088778,-4.26482561840363,133.257682848926));
#26185=CARTESIAN_POINT('Ctrl Pts',(177.207218180807,-4.19566368022283,133.374160584805));
#26186=CARTESIAN_POINT('Ctrl Pts',(177.199565473833,-4.12189915921267,133.487480142258));
#26187=CARTESIAN_POINT('Ctrl Pts',(177.19190814988,-4.04809013508669,133.600868066906));
#26188=CARTESIAN_POINT('Ctrl Pts',(177.184250825927,-3.96967323333913,133.711093693201));
#26189=CARTESIAN_POINT('Ctrl Pts',(177.176593501974,-3.88697082811644,133.817770786108));
#26190=CARTESIAN_POINT('Ctrl Pts',(177.168925089948,-3.8041486669113,133.924602351185));
#26191=CARTESIAN_POINT('Ctrl Pts',(177.161256677921,-3.71702887440284,134.02787482013));
#26192=CARTESIAN_POINT('Ctrl Pts',(177.153588265894,-3.62597167935547,134.127237750867));
#26193=CARTESIAN_POINT('Ctrl Pts',(177.150118973956,-3.58477618912948,134.172190866761));
#26194=CARTESIAN_POINT('Ctrl Pts',(177.146649682018,-3.54277526702529,134.216344320271));
#26195=CARTESIAN_POINT('Ctrl Pts',(177.14318039008,-3.50000445877035,134.259668397068));
#26196=CARTESIAN_POINT('Ctrl Pts',(177.135406055961,-3.4041593814917,134.356753293475));
#26197=CARTESIAN_POINT('Ctrl Pts',(177.127631721842,-3.30411994611471,134.450001044235));
#26198=CARTESIAN_POINT('Ctrl Pts',(177.119857387723,-3.20022595236407,134.539027525915));
#26199=CARTESIAN_POINT('Ctrl Pts',(177.112092634776,-3.0964599986757,134.627944290412));
#26200=CARTESIAN_POINT('Ctrl Pts',(177.104327881829,-2.98884923252015,134.712649884976));
#26201=CARTESIAN_POINT('Ctrl Pts',(177.096563128882,-2.8777713262827,134.792795806475));
#26202=CARTESIAN_POINT('Ctrl Pts',(177.088806087997,-2.76680374418746,134.872862125915));
#26203=CARTESIAN_POINT('Ctrl Pts',(177.081049047112,-2.65237618995443,134.948377557388));
#26204=CARTESIAN_POINT('Ctrl Pts',(177.073292006227,-2.53490027577508,135.019033043079));
#26205=CARTESIAN_POINT('Ctrl Pts',(177.065540814986,-2.41751295109669,135.089635246917));
#26206=CARTESIAN_POINT('Ctrl Pts',(177.057789623746,-2.2970821757582,135.155384599089));
#26207=CARTESIAN_POINT('Ctrl Pts',(177.050038432506,-2.17404918026736,135.216014867876));
#26208=CARTESIAN_POINT('Ctrl Pts',(177.042290535729,-2.05106847708128,135.276619367182));
#26209=CARTESIAN_POINT('Ctrl Pts',(177.034542638952,-1.92548810347863,135.332108938039));
#26210=CARTESIAN_POINT('Ctrl Pts',(177.026794742175,-1.79777437560963,135.382263014614));
#26211=CARTESIAN_POINT('Ctrl Pts',(177.019048466091,-1.67008736269943,135.432406600038));
#26212=CARTESIAN_POINT('Ctrl Pts',(177.011302190007,-1.54026824682151,135.477216768286));
#26213=CARTESIAN_POINT('Ctrl Pts',(177.003555913923,-1.40880346413521,135.516521041611));
#26214=CARTESIAN_POINT('Ctrl Pts',(176.995809580657,-1.27733771100549,135.555825605072));
#26215=CARTESIAN_POINT('Ctrl Pts',(176.988063247392,-1.14422664140964,135.58962408052));
#26216=CARTESIAN_POINT('Ctrl Pts',(176.980316914127,-1.00997161176771,135.617793945859));
#26217=CARTESIAN_POINT('Ctrl Pts',(176.972568846124,-0.875686516643258,
135.645970119644));
#26218=CARTESIAN_POINT('Ctrl Pts',(176.964820778121,-0.740257334260181,
135.668515094824));
#26219=CARTESIAN_POINT('Ctrl Pts',(176.957072710118,-0.604194969101184,
135.685357595829));
#26220=CARTESIAN_POINT('Ctrl Pts',(176.949316407376,-0.467987995241147,
135.702217997245));
#26221=CARTESIAN_POINT('Ctrl Pts',(176.941560104634,-0.331146882929249,
135.713363769564));
#26222=CARTESIAN_POINT('Ctrl Pts',(176.933803801892,-0.194187566345887,
135.71877556256));
#26223=CARTESIAN_POINT('Ctrl Pts',(176.926043359378,-0.0571551504514058,
135.724190243992));
#26224=CARTESIAN_POINT('Ctrl Pts',(176.918282916864,0.0799952046522575,
135.723864848926));
#26225=CARTESIAN_POINT('Ctrl Pts',(176.91052247435,0.216749215926602,135.717832184584));
#26226=CARTESIAN_POINT('Ctrl Pts',(176.902749574084,0.353722756880248,135.711789836074));
#26227=CARTESIAN_POINT('Ctrl Pts',(176.894976673819,0.490298292835616,135.700021943642));
#26228=CARTESIAN_POINT('Ctrl Pts',(176.887203773553,0.625967402688034,135.682613160565));
#26229=CARTESIAN_POINT('Ctrl Pts',(176.879713437791,0.756704598669194,135.665837230602));
#26230=CARTESIAN_POINT('Ctrl Pts',(176.872223102029,0.886599822452162,135.643823462321));
#26231=CARTESIAN_POINT('Ctrl Pts',(176.864732766267,1.01521039196965,135.616691749412));
#26232=CARTESIAN_POINT('Ctrl Pts',(176.856958432148,1.14869727031917,135.588531329362));
#26233=CARTESIAN_POINT('Ctrl Pts',(176.849184098029,1.28122300236775,135.554768006105));
#26234=CARTESIAN_POINT('Ctrl Pts',(176.84140976391,1.41228074413996,135.515480034672));
#26235=CARTESIAN_POINT('Ctrl Pts',(176.833645010963,1.54317696895822,135.476240482153));
#26236=CARTESIAN_POINT('Ctrl Pts',(176.825880258016,1.67260843229818,135.431489939802));
#26237=CARTESIAN_POINT('Ctrl Pts',(176.818115505069,1.80007778745586,135.381357779637));
#26238=CARTESIAN_POINT('Ctrl Pts',(176.810358464184,1.92742053825299,135.331275411441));
#26239=CARTESIAN_POINT('Ctrl Pts',(176.802601423299,2.05280469757118,135.275822204587));
#26240=CARTESIAN_POINT('Ctrl Pts',(176.794844382414,2.1757477598724,135.215177406768));
#26241=CARTESIAN_POINT('Ctrl Pts',(176.787093191173,2.29859810985412,135.154578341664));
#26242=CARTESIAN_POINT('Ctrl Pts',(176.779341999933,2.41901067771043,135.088795650461));
#26243=CARTESIAN_POINT('Ctrl Pts',(176.771590808693,2.53652297929066,135.018056648135));
#26244=CARTESIAN_POINT('Ctrl Pts',(176.763842911916,2.65398533500795,134.947347711772));
#26245=CARTESIAN_POINT('Ctrl Pts',(176.756095015139,2.76854954191965,134.871686855295));
#26246=CARTESIAN_POINT('Ctrl Pts',(176.748347118362,2.87977797647419,134.791347182469));
#26247=CARTESIAN_POINT('Ctrl Pts',(176.740600842278,2.99098314443811,134.71102431497));
#26248=CARTESIAN_POINT('Ctrl Pts',(176.732854566194,3.09885361121525,134.6260248066));
#26249=CARTESIAN_POINT('Ctrl Pts',(176.72510829011,3.20298133576673,134.536664681443));
#26250=CARTESIAN_POINT('Ctrl Pts',(176.717361956844,3.30710982896542,134.447303896649));
#26251=CARTESIAN_POINT('Ctrl Pts',(176.709615623579,3.40749522811752,134.35358268545));
#26252=CARTESIAN_POINT('Ctrl Pts',(176.701869290313,3.50376345652187,134.255856627015));
#26253=CARTESIAN_POINT('Ctrl Pts',(176.69412122231,3.60005324352857,134.158108683507));
#26254=CARTESIAN_POINT('Ctrl Pts',(176.686373154307,3.69222375077429,134.05635438659));
#26255=CARTESIAN_POINT('Ctrl Pts',(176.678625086304,3.77993885575116,133.950985048489));
#26256=CARTESIAN_POINT('Ctrl Pts',(176.670868783563,3.86774718538536,133.845503722602));
#26257=CARTESIAN_POINT('Ctrl Pts',(176.663112480821,3.95109040303699,133.736399981461));
#26258=CARTESIAN_POINT('Ctrl Pts',(176.655356178079,4.02967335378458,133.624097435834));
#26259=CARTESIAN_POINT('Ctrl Pts',(176.647595735565,4.10829824661905,133.511734950958));
#26260=CARTESIAN_POINT('Ctrl Pts',(176.639835293051,4.18215759955181,133.396170588928));
#26261=CARTESIAN_POINT('Ctrl Pts',(176.632074850536,4.25100103168297,133.277854763735));
#26262=CARTESIAN_POINT('Ctrl Pts',(176.624301950271,4.31995497740302,133.159349007475));
#26263=CARTESIAN_POINT('Ctrl Pts',(176.616529050006,4.38387672944328,133.03808330775));
#26264=CARTESIAN_POINT('Ctrl Pts',(176.60875614974,4.44256269497506,132.914531170795));
#26265=CARTESIAN_POINT('Ctrl Pts',(176.601265813978,4.49911527783851,132.795470465229));
#26266=CARTESIAN_POINT('Ctrl Pts',(176.593775478216,4.55080601244283,132.674286955166));
#26267=CARTESIAN_POINT('Ctrl Pts',(176.586285142454,4.59749648827391,132.551417887036));
#26268=CARTESIAN_POINT('Ctrl Pts',(176.578510808335,4.64595724768758,132.423890200843));
#26269=CARTESIAN_POINT('Ctrl Pts',(176.570736474216,4.689184602897,132.294142648211));
#26270=CARTESIAN_POINT('Ctrl Pts',(176.562962140097,4.7269704305287,132.162643950088));
#26271=CARTESIAN_POINT('Ctrl Pts',(176.55519738715,4.76470969050479,132.031307312359));
#26272=CARTESIAN_POINT('Ctrl Pts',(176.547432634203,4.79702065929808,131.898224195328));
#26273=CARTESIAN_POINT('Ctrl Pts',(176.539667881256,4.82374335321012,131.763882959599));
#26274=CARTESIAN_POINT('Ctrl Pts',(176.531910840371,4.85043950576582,131.62967515348));
#26275=CARTESIAN_POINT('Ctrl Pts',(176.524153799486,4.8715583531125,131.494212096357));
#26276=CARTESIAN_POINT('Ctrl Pts',(176.516396758601,4.88698989538333,131.357996621562));
#26277=CARTESIAN_POINT('Ctrl Pts',(176.508645567361,4.90240980060812,131.221883867917));
#26278=CARTESIAN_POINT('Ctrl Pts',(176.50089437612,4.91215089360298,131.085020212891));
#26279=CARTESIAN_POINT('Ctrl Pts',(176.49314318488,4.91615443691515,130.947917626797));
#26280=CARTESIAN_POINT('Ctrl Pts',(176.485395288103,4.92015627861463,130.810873312959));
#26281=CARTESIAN_POINT('Ctrl Pts',(176.477647391326,4.91842540945625,130.673590660013));
#26282=CARTESIAN_POINT('Ctrl Pts',(176.469899494549,4.91095505315188,130.5365854723));
#26283=CARTESIAN_POINT('Ctrl Pts',(176.462153218465,4.90348625948502,130.39960894312));
#26284=CARTESIAN_POINT('Ctrl Pts',(176.454406942381,4.89028038795833,130.262910153868));
#26285=CARTESIAN_POINT('Ctrl Pts',(176.446660666297,4.87138276243421,130.127003219763));
#26286=CARTESIAN_POINT('Ctrl Pts',(176.438914333031,4.85248499741213,129.991095282423));
#26287=CARTESIAN_POINT('Ctrl Pts',(176.431167999766,4.82789544839928,129.855979599134));
#26288=CARTESIAN_POINT('Ctrl Pts',(176.423421666501,4.79771107662709,129.722163090444));
#26289=CARTESIAN_POINT('Ctrl Pts',(176.415673598498,4.76751994527414,129.588316614474));
#26290=CARTESIAN_POINT('Ctrl Pts',(176.407925530495,4.73173158400299,129.455770273354));
#26291=CARTESIAN_POINT('Ctrl Pts',(176.400177462492,4.6904935324448,129.325018370284));
#26292=CARTESIAN_POINT('Ctrl Pts',(176.39242115975,4.64921165259457,129.194127502535));
#26293=CARTESIAN_POINT('Ctrl Pts',(176.384664857008,4.60246863010648,129.065035256028));
#26294=CARTESIAN_POINT('Ctrl Pts',(176.376908554266,4.55046132227167,128.938218924926));
#26295=CARTESIAN_POINT('Ctrl Pts',(176.369148111752,4.49842625657074,128.811334908129));
#26296=CARTESIAN_POINT('Ctrl Pts',(176.361387669238,4.44112147021729,128.686729582207));
#26297=CARTESIAN_POINT('Ctrl Pts',(176.353627226724,4.37879057226528,128.564857059466));
#26298=CARTESIAN_POINT('Ctrl Pts',(176.345854326458,4.31635961522244,128.442788896133));
#26299=CARTESIAN_POINT('Ctrl Pts',(176.338081426193,4.24888661597369,128.323462643002));
#26300=CARTESIAN_POINT('Ctrl Pts',(176.330308525927,4.17665990182982,128.207305530174));
#26301=CARTESIAN_POINT('Ctrl Pts',(176.322818190165,4.10705881067231,128.095371020979));
#26302=CARTESIAN_POINT('Ctrl Pts',(176.315327854403,4.03304379623021,127.986379494736));
#26303=CARTESIAN_POINT('Ctrl Pts',(176.307837518641,3.95490791204331,127.880683742507));
#26304=CARTESIAN_POINT('Ctrl Pts',(176.300063184522,3.87380948205952,127.770980503707));
#26305=CARTESIAN_POINT('Ctrl Pts',(176.292288850403,3.78801463276585,127.664480384049));
#26306=CARTESIAN_POINT('Ctrl Pts',(176.284514516284,3.69780521660363,127.561611838743));
#26307=CARTESIAN_POINT('Ctrl Pts',(176.276749763336,3.60770697548464,127.458870069725));
#26308=CARTESIAN_POINT('Ctrl Pts',(176.268985010389,3.51320524788856,127.359751261094));
#26309=CARTESIAN_POINT('Ctrl Pts',(176.261220257442,3.41462443032569,127.264653982501));
#26310=CARTESIAN_POINT('Ctrl Pts',(176.253463216557,3.31614152462077,127.169651155866));
#26311=CARTESIAN_POINT('Ctrl Pts',(176.245706175672,3.21358787099731,127.078662180232));
#26312=CARTESIAN_POINT('Ctrl Pts',(176.237949134787,3.10732705976352,126.992051395302));
#26313=CARTESIAN_POINT('Ctrl Pts',(176.230197943547,3.00114638063378,126.905505924237));
#26314=CARTESIAN_POINT('Ctrl Pts',(176.222446752307,2.89126441018347,126.823332318197));
#26315=CARTESIAN_POINT('Ctrl Pts',(176.214695561067,2.77808013450735,126.745856727121));
#26316=CARTESIAN_POINT('Ctrl Pts',(176.20694766429,2.66494396516788,126.668414065239));
#26317=CARTESIAN_POINT('Ctrl Pts',(176.199199767513,2.54850860413817,126.59566566725));
#26318=CARTESIAN_POINT('Ctrl Pts',(176.191451870736,2.42920434947129,126.527896039084));
#26319=CARTESIAN_POINT('Ctrl Pts',(176.183705594652,2.30992505068262,126.460140586864));
#26320=CARTESIAN_POINT('Ctrl Pts',(176.175959318567,2.18777839164242,126.397362025945));
#26321=CARTESIAN_POINT('Ctrl Pts',(176.168213042483,2.06322141069901,126.339800115912));
#26322=CARTESIAN_POINT('Ctrl Pts',(176.160466709218,1.9386635103043,126.282237780969));
#26323=CARTESIAN_POINT('Ctrl Pts',(176.152720375953,1.81169560740304,126.229892337764));
#26324=CARTESIAN_POINT('Ctrl Pts',(176.144974042687,1.68279659852437,126.182956213005));
#26325=CARTESIAN_POINT('Ctrl Pts',(176.137225974684,1.55386872360639,126.136009577226));
#26326=CARTESIAN_POINT('Ctrl Pts',(176.129477906681,1.42300924946788,126.094474804143));
#26327=CARTESIAN_POINT('Ctrl Pts',(176.121729838678,1.29071379616576,126.058494947439));
#26328=CARTESIAN_POINT('Ctrl Pts',(176.113973535936,1.15827773768127,126.022476850915));
#26329=CARTESIAN_POINT('Ctrl Pts',(176.106217233195,1.02440302919617,125.992025567076));
#26330=CARTESIAN_POINT('Ctrl Pts',(176.098460930453,0.889597637980695,125.967233463459));
#26331=CARTESIAN_POINT('Ctrl Pts',(176.090700487939,0.75472029706883,125.94242812755));
#26332=CARTESIAN_POINT('Ctrl Pts',(176.082940045424,0.618911670593171,125.92328804495));
#26333=CARTESIAN_POINT('Ctrl Pts',(176.07517960291,0.482685492741861,125.909853719257));
#26334=CARTESIAN_POINT('Ctrl Pts',(176.067406702645,0.346240632536643,125.896397827591));
#26335=CARTESIAN_POINT('Ctrl Pts',(176.059633802379,0.209377272069173,125.888666018271));
#26336=CARTESIAN_POINT('Ctrl Pts',(176.051860902114,0.0726107000767102,
125.886646641669));
#26337=CARTESIAN_POINT('Ctrl Pts',(176.044370566352,-0.0591840625283202,
125.884700674493));
#26338=CARTESIAN_POINT('Ctrl Pts',(176.03688023059,-0.190888643576832,125.888059020157));
#26339=CARTESIAN_POINT('Ctrl Pts',(176.029389894828,-0.322047827361773,
125.896665816604));
#26340=CARTESIAN_POINT('Ctrl Pts',(176.021615560709,-0.458179951466051,
125.905598942354));
#26341=CARTESIAN_POINT('Ctrl Pts',(176.01384122659,-0.594155730072887,125.920214662816));
#26342=CARTESIAN_POINT('Ctrl Pts',(176.006066892471,-0.729462343550482,
125.940507438055));
#26343=CARTESIAN_POINT('Ctrl Pts',(175.998302139524,-0.864602203719436,
125.960775204261));
#26344=CARTESIAN_POINT('Ctrl Pts',(175.990537386577,-0.99907415670959,125.986706046939));
#26345=CARTESIAN_POINT('Ctrl Pts',(175.98277263363,-1.1323675303472,126.018242478749));
#26346=CARTESIAN_POINT('Ctrl Pts',(175.975015592745,-1.265528515127,126.04974758813));
#26347=CARTESIAN_POINT('Ctrl Pts',(175.96725855186,-1.39751287206479,126.086847117534));
#26348=CARTESIAN_POINT('Ctrl Pts',(175.959501510975,-1.52781754240825,126.129432102646));
#26349=CARTESIAN_POINT('Ctrl Pts',(175.951750319735,-1.65802394898635,126.17198497409));
#26350=CARTESIAN_POINT('Ctrl Pts',(175.943999128495,-1.78655282007018,126.220014946582));
#26351=CARTESIAN_POINT('Ctrl Pts',(175.936247937254,-1.912914094747,126.27336263383));
#26352=CARTESIAN_POINT('Ctrl Pts',(175.928500040477,-2.03922166251126,126.326687646888));
#26353=CARTESIAN_POINT('Ctrl Pts',(175.9207521437,-2.16336310680931,126.385325727652));
#26354=CARTESIAN_POINT('Ctrl Pts',(175.913004246923,-2.28486647813643,126.449068636586));
#26355=CARTESIAN_POINT('Ctrl Pts',(175.905257970839,-2.40634443357779,126.512798211878));
#26356=CARTESIAN_POINT('Ctrl Pts',(175.897511694755,-2.52518506766956,126.581630309873));
#26357=CARTESIAN_POINT('Ctrl Pts',(175.889765418671,-2.64093962349206,126.655310007177));
#26358=CARTESIAN_POINT('Ctrl Pts',(175.882019085406,-2.75669503378842,126.728990248368));
#26359=CARTESIAN_POINT('Ctrl Pts',(175.87427275214,-2.86936399053878,126.807517950335));
#26360=CARTESIAN_POINT('Ctrl Pts',(175.866526418875,-2.97852574443112,126.890594215204));
#26361=CARTESIAN_POINT('Ctrl Pts',(175.858778350872,-3.08771194434152,126.973689084426));
#26362=CARTESIAN_POINT('Ctrl Pts',(175.851030282869,-3.19338906745496,127.061334306757));
#26363=CARTESIAN_POINT('Ctrl Pts',(175.843282214866,-3.29516886390869,127.153190227016));
#26364=CARTESIAN_POINT('Ctrl Pts',(175.835525912124,-3.39705683314104,127.245143772841));
#26365=CARTESIAN_POINT('Ctrl Pts',(175.827769609382,-3.49503891066816,127.341316693889));
#26366=CARTESIAN_POINT('Ctrl Pts',(175.82001330664,-3.58876281634651,127.441331549819));
#26367=CARTESIAN_POINT('Ctrl Pts',(175.812252864126,-3.68253674529536,127.54139978669));
#26368=CARTESIAN_POINT('Ctrl Pts',(175.804492421612,-3.77204771878202,127.645313748276));
#26369=CARTESIAN_POINT('Ctrl Pts',(175.796731979098,-3.85698397410572,127.752663108639));
#26370=CARTESIAN_POINT('Ctrl Pts',(175.788959078833,-3.94205657664672,127.860184795725));
#26371=CARTESIAN_POINT('Ctrl Pts',(175.781186178567,-4.02253955621019,127.97115258526));
#26372=CARTESIAN_POINT('Ctrl Pts',(175.773413278302,-4.09816418780871,128.085126653329));
#26373=CARTESIAN_POINT('Ctrl Pts',(175.76592294254,-4.17103967356237,128.19495747694));
#26374=CARTESIAN_POINT('Ctrl Pts',(175.758432606778,-4.23940374536326,128.30757953891));
#26375=CARTESIAN_POINT('Ctrl Pts',(175.750942271015,-4.30305734633331,128.422579658563));
#26376=CARTESIAN_POINT('Ctrl Pts',(175.742787679911,-4.37235585373531,128.547778178704));
#26377=CARTESIAN_POINT('Ctrl Pts',(175.734633088806,-4.4362732431258,128.67615975229));
#26378=CARTESIAN_POINT('Ctrl Pts',(175.726478497701,-4.49452037997105,128.807245293774));
#26379=CARTESIAN_POINT('Ctrl Pts',(175.718341777153,-4.55263986985782,128.938043564989));
#26380=CARTESIAN_POINT('Ctrl Pts',(175.710205056605,-4.60511374545798,129.071533685418));
#26381=CARTESIAN_POINT('Ctrl Pts',(175.702068336057,-4.65169851612172,129.207211915156));
#26382=CARTESIAN_POINT('Ctrl Pts',(175.694667060097,-4.69407268163103,129.330626749682));
#26383=CARTESIAN_POINT('Ctrl Pts',(175.687265784137,-4.73157464057992,129.455851530296));
#26384=CARTESIAN_POINT('Ctrl Pts',(175.679864508177,-4.76405452823404,129.582490119308));
#26385=CARTESIAN_POINT('Origin',(213.235140564004,0.,130.804360617566));
#26386=CARTESIAN_POINT('',(173.584942037299,-4.76405452823404,129.582490119308));
#26387=CARTESIAN_POINT('',(173.930202354372,-4.76405452823406,129.582490119308));
#26388=CARTESIAN_POINT('',(213.235140564004,-4.76405452823405,129.582490119308));
#26389=CARTESIAN_POINT('',(175.264859436032,-4.91824815910515,130.808615962297));
#26390=CARTESIAN_POINT('Ctrl Pts',(175.264859435991,-4.91824815910454,130.808615963011));
#26391=CARTESIAN_POINT('Ctrl Pts',(175.25319186359,-4.91807026830515,131.014218800192));
#26392=CARTESIAN_POINT('Ctrl Pts',(175.241524291189,-4.90499673116812,131.219285084506));
#26393=CARTESIAN_POINT('Ctrl Pts',(175.229856718788,-4.8792466415552,131.422531527082));
#26394=CARTESIAN_POINT('Ctrl Pts',(175.224449819042,-4.86731372627334,131.516718483985));
#26395=CARTESIAN_POINT('Ctrl Pts',(175.219042919295,-4.85265909434396,131.610515169461));
#26396=CARTESIAN_POINT('Ctrl Pts',(175.213636019548,-4.83530754954034,131.70379597592));
#26397=CARTESIAN_POINT('Ctrl Pts',(175.205861685429,-4.81035855601216,131.837920185781));
#26398=CARTESIAN_POINT('Ctrl Pts',(175.19808735131,-4.77978520791269,131.971217980356));
#26399=CARTESIAN_POINT('Ctrl Pts',(175.190313017191,-4.74365357488158,132.103180783722));
#26400=CARTESIAN_POINT('Ctrl Pts',(175.182548264244,-4.70756647085903,132.234980954727));
#26401=CARTESIAN_POINT('Ctrl Pts',(175.174783511297,-4.6659348137967,132.365449034629));
#26402=CARTESIAN_POINT('Ctrl Pts',(175.16701875835,-4.61887600350787,132.494084715376));
#26403=CARTESIAN_POINT('Ctrl Pts',(175.159261717465,-4.57186393269282,132.622592633351));
#26404=CARTESIAN_POINT('Ctrl Pts',(175.15150467658,-4.51943556909307,132.749271409193));
#26405=CARTESIAN_POINT('Ctrl Pts',(175.143747635695,-4.46175852998218,132.873634374861));
#26406=CARTESIAN_POINT('Ctrl Pts',(175.135996444455,-4.40412498557524,132.99790355745));
#26407=CARTESIAN_POINT('Ctrl Pts',(175.128245253215,-4.34125080777626,133.119860052667));
#26408=CARTESIAN_POINT('Ctrl Pts',(175.120494061975,-4.27335214775605,133.239036054615));
#26409=CARTESIAN_POINT('Ctrl Pts',(175.112746165198,-4.20548234647749,133.358161403582));
#26410=CARTESIAN_POINT('Ctrl Pts',(175.104998268421,-4.13259250353576,133.474508270769));
#26411=CARTESIAN_POINT('Ctrl Pts',(175.097250371644,-4.05494514228876,133.587632604909));
#26412=CARTESIAN_POINT('Ctrl Pts',(175.08950409556,-3.97731402319586,133.700733275878));
#26413=CARTESIAN_POINT('Ctrl Pts',(175.081757819476,-3.89492758635569,133.810612432457));
#26414=CARTESIAN_POINT('Ctrl Pts',(175.074011543391,-3.80809197298378,133.916854567407));
#26415=CARTESIAN_POINT('Ctrl Pts',(175.066265210126,-3.72125571861122,134.023097486612));
#26416=CARTESIAN_POINT('Ctrl Pts',(175.058518876861,-3.62997046959219,134.1257030279));
#26417=CARTESIAN_POINT('Ctrl Pts',(175.050772543595,-3.53458272588869,134.224288689375));
#26418=CARTESIAN_POINT('Ctrl Pts',(175.043024475592,-3.43917362076133,134.322896428426));
#26419=CARTESIAN_POINT('Ctrl Pts',(175.035276407589,-3.33966046460008,134.417482215401));
#26420=CARTESIAN_POINT('Ctrl Pts',(175.027528339586,-3.23642639092771,134.507700634174));
#26421=CARTESIAN_POINT('Ctrl Pts',(175.019772036845,-3.13308259885326,134.598014938155));
#26422=CARTESIAN_POINT('Ctrl Pts',(175.012015734103,-3.02601028431556,134.683952343975));
#26423=CARTESIAN_POINT('Ctrl Pts',(175.004259431361,-2.91562585318813,134.765207616217));
#26424=CARTESIAN_POINT('Ctrl Pts',(174.996498988847,-2.80518250656608,134.846506256844));
#26425=CARTESIAN_POINT('Ctrl Pts',(174.988738546333,-2.69142384503477,134.923117566151));
#26426=CARTESIAN_POINT('Ctrl Pts',(174.980978103818,-2.57479414442493,134.994780426647));
#26427=CARTESIAN_POINT('Ctrl Pts',(174.973205203553,-2.45797721946581,135.066558326728));
#26428=CARTESIAN_POINT('Ctrl Pts',(174.965432303288,-2.33828038706294,135.13337171331));
#26429=CARTESIAN_POINT('Ctrl Pts',(174.957659403022,-2.21617213142889,135.19500568935));
#26430=CARTESIAN_POINT('Ctrl Pts',(174.95016906726,-2.09850281845932,135.254399115114));
#26431=CARTESIAN_POINT('Ctrl Pts',(174.942678731498,-1.9785946413567,135.308983034166));
#26432=CARTESIAN_POINT('Ctrl Pts',(174.935188395736,-1.8568813991624,135.358608583141));
#26433=CARTESIAN_POINT('Ctrl Pts',(174.927414061617,-1.73055336239648,135.410115699889));
#26434=CARTESIAN_POINT('Ctrl Pts',(174.919639727498,-1.60188051118809,135.456444190198));
#26435=CARTESIAN_POINT('Ctrl Pts',(174.911865393379,-1.47132643711803,135.497374742618));
#26436=CARTESIAN_POINT('Ctrl Pts',(174.904100640432,-1.34093325927635,135.53825485179));
#26437=CARTESIAN_POINT('Ctrl Pts',(174.896335887485,-1.20866384105492,135.573750143681));
#26438=CARTESIAN_POINT('Ctrl Pts',(174.888571134538,-1.07500256325419,135.603688961355));
#26439=CARTESIAN_POINT('Ctrl Pts',(174.880814093653,-0.94147403971895,135.633598043374));
#26440=CARTESIAN_POINT('Ctrl Pts',(174.873057052768,-0.806556786714803,
135.657961548872));
#26441=CARTESIAN_POINT('Ctrl Pts',(174.865300011883,-0.670750853076566,
135.676657443048));
#26442=CARTESIAN_POINT('Ctrl Pts',(174.857548820642,-0.535047331749209,
135.695339238504));
#26443=CARTESIAN_POINT('Ctrl Pts',(174.849797629402,-0.398456849447651,
135.70836187665));
#26444=CARTESIAN_POINT('Ctrl Pts',(174.842046438162,-0.26148981951155,135.715654351074));
#26445=CARTESIAN_POINT('Ctrl Pts',(174.834298541385,-0.124581004216886,
135.722943726001));
#26446=CARTESIAN_POINT('Ctrl Pts',(174.826550644608,0.0127036508045441,
135.724507760431));
#26447=CARTESIAN_POINT('Ctrl Pts',(174.818802747831,0.149848652360622,135.720327302145));
#26448=CARTESIAN_POINT('Ctrl Pts',(174.811056471747,0.286964966138925,135.71614771832));
#26449=CARTESIAN_POINT('Ctrl Pts',(174.803310195663,0.423941294021012,135.70622604378));
#26450=CARTESIAN_POINT('Ctrl Pts',(174.795563919579,0.560262581193397,135.690595251987));
#26451=CARTESIAN_POINT('Ctrl Pts',(174.787817586313,0.696584874658464,135.674964344811));
#26452=CARTESIAN_POINT('Ctrl Pts',(174.780071253048,0.832251729344999,135.653624280825));
#26453=CARTESIAN_POINT('Ctrl Pts',(174.772324919783,0.966754043881733,135.626659828641));
#26454=CARTESIAN_POINT('Ctrl Pts',(174.76457685178,1.10128647927914,135.599689337956));
#26455=CARTESIAN_POINT('Ctrl Pts',(174.756828783777,1.23465347231902,135.567092029565));
#26456=CARTESIAN_POINT('Ctrl Pts',(174.749080715774,1.36635732160314,135.529003538698));
#26457=CARTESIAN_POINT('Ctrl Pts',(174.741324413032,1.49820114730575,135.490874566929));
#26458=CARTESIAN_POINT('Ctrl Pts',(174.73356811029,1.62837792208956,135.447242863246));
#26459=CARTESIAN_POINT('Ctrl Pts',(174.725811807548,1.75640576520965,135.398293774507));
#26460=CARTESIAN_POINT('Ctrl Pts',(174.718051365034,1.88450194064447,135.349318560164));
#26461=CARTESIAN_POINT('Ctrl Pts',(174.71029092252,2.01044654017648,135.295020460421));
#26462=CARTESIAN_POINT('Ctrl Pts',(174.702530480006,2.13377973632738,135.235632116734));
#26463=CARTESIAN_POINT('Ctrl Pts',(174.69475757974,2.2573109178738,135.176148437605));
#26464=CARTESIAN_POINT('Ctrl Pts',(174.686984679475,2.37822197393003,135.11155836997));
#26465=CARTESIAN_POINT('Ctrl Pts',(174.679211779209,2.49607887836731,135.042139905763));
#26466=CARTESIAN_POINT('Ctrl Pts',(174.671721443447,2.60965138746606,134.975244977583));
#26467=CARTESIAN_POINT('Ctrl Pts',(174.664231107685,2.72038768310657,134.903866773744));
#26468=CARTESIAN_POINT('Ctrl Pts',(174.656740771923,2.82792804334672,134.828289797379));
#26469=CARTESIAN_POINT('Ctrl Pts',(174.648966437804,2.93954582903031,134.749847296986));
#26470=CARTESIAN_POINT('Ctrl Pts',(174.641192103685,3.04807411910548,134.666632863708));
#26471=CARTESIAN_POINT('Ctrl Pts',(174.633417769566,3.15307781806533,134.578917987076));
#26472=CARTESIAN_POINT('Ctrl Pts',(174.625653016619,3.25795210935062,134.491311211191));
#26473=CARTESIAN_POINT('Ctrl Pts',(174.617888263672,3.35931015510609,134.399215275864));
#26474=CARTESIAN_POINT('Ctrl Pts',(174.610123510724,3.4567457158364,134.302944919615));
#26475=CARTESIAN_POINT('Ctrl Pts',(174.602366469839,3.5540845021942,134.206770180442));
#26476=CARTESIAN_POINT('Ctrl Pts',(174.594609428954,3.64750828016641,134.106429544268));
#26477=CARTESIAN_POINT('Ctrl Pts',(174.586852388069,3.73664408980739,134.002277753548));
#26478=CARTESIAN_POINT('Ctrl Pts',(174.579101196829,3.82571268144092,133.898204504504));
#26479=CARTESIAN_POINT('Ctrl Pts',(174.571350005589,3.91049948782595,133.790326117314));
#26480=CARTESIAN_POINT('Ctrl Pts',(174.563598814349,3.99066887837805,133.679033636475));
#26481=CARTESIAN_POINT('Ctrl Pts',(174.555850917572,4.07080419480064,133.56778845791));
#26482=CARTESIAN_POINT('Ctrl Pts',(174.548103020795,4.14632577066547,133.453132388349));
#26483=CARTESIAN_POINT('Ctrl Pts',(174.540355124018,4.21693885600655,133.335488774575));
#26484=CARTESIAN_POINT('Ctrl Pts',(174.532608847934,4.28753717061244,133.217869769308));
#26485=CARTESIAN_POINT('Ctrl Pts',(174.52486257185,4.35322883587855,133.09726479785));
#26486=CARTESIAN_POINT('Ctrl Pts',(174.517116295765,4.41376319360522,132.974125013365));
#26487=CARTESIAN_POINT('Ctrl Pts',(174.5093699625,4.47429799818273,132.85098431989));
#26488=CARTESIAN_POINT('Ctrl Pts',(174.501623629235,4.52967524677419,132.725309126912));
#26489=CARTESIAN_POINT('Ctrl Pts',(174.493877295969,4.57969107588829,132.59757357534));
#26490=CARTESIAN_POINT('Ctrl Pts',(174.486129227966,4.62971810570053,132.469809418277));
#26491=CARTESIAN_POINT('Ctrl Pts',(174.478381159963,4.67438118435536,132.339984348464));
#26492=CARTESIAN_POINT('Ctrl Pts',(174.47063309196,4.71352540584998,132.208590410337));
#26493=CARTESIAN_POINT('Ctrl Pts',(174.462876789219,4.75271123028905,132.07705682517));
#26494=CARTESIAN_POINT('Ctrl Pts',(174.455120486477,4.78636636878165,131.943951416142));
#26495=CARTESIAN_POINT('Ctrl Pts',(174.447364183735,4.8143862905749,131.809779787676));
#26496=CARTESIAN_POINT('Ctrl Pts',(174.439603741221,4.84242116744409,131.675536547772));
#26497=CARTESIAN_POINT('Ctrl Pts',(174.431843298707,4.86481477074275,131.540226340033));
#26498=CARTESIAN_POINT('Ctrl Pts',(174.424082856192,4.88151428033375,131.40436177873));
#26499=CARTESIAN_POINT('Ctrl Pts',(174.416309955927,4.89824059746005,131.268279115571));
#26500=CARTESIAN_POINT('Ctrl Pts',(174.408537055661,4.90925452348748,131.131640710474));
#26501=CARTESIAN_POINT('Ctrl Pts',(174.400764155396,4.91455533918001,130.994961983346));
#26502=CARTESIAN_POINT('Ctrl Pts',(174.393273819634,4.91966345687014,130.863251872223));
#26503=CARTESIAN_POINT('Ctrl Pts',(174.385783483872,4.91946662512228,130.731504627803));
#26504=CARTESIAN_POINT('Ctrl Pts',(174.37829314811,4.91400976598499,130.600176675239));
#26505=CARTESIAN_POINT('Ctrl Pts',(174.370518813991,4.90834600837489,130.463869383436));
#26506=CARTESIAN_POINT('Ctrl Pts',(174.362744479872,4.89699754063936,130.327582025503));
#26507=CARTESIAN_POINT('Ctrl Pts',(174.354970145753,4.87995759486065,130.191827406334));
#26508=CARTESIAN_POINT('Ctrl Pts',(174.347205392806,4.86293864929222,130.056240092601));
#26509=CARTESIAN_POINT('Ctrl Pts',(174.339440639859,4.84024223014815,129.921184595486));
#26510=CARTESIAN_POINT('Ctrl Pts',(174.331675886912,4.81191355348855,129.787172819638));
#26511=CARTESIAN_POINT('Ctrl Pts',(174.323918846027,4.78361301326998,129.653294146176));
#26512=CARTESIAN_POINT('Ctrl Pts',(174.316161805142,4.74969142825887,129.52045751106));
#26513=CARTESIAN_POINT('Ctrl Pts',(174.308404764257,4.71024565936873,129.389168443019));
#26514=CARTESIAN_POINT('Ctrl Pts',(174.300653573016,4.67082963683975,129.257978381086));
#26515=CARTESIAN_POINT('Ctrl Pts',(174.292902381776,4.6258978343061,129.128333936235));
#26516=CARTESIAN_POINT('Ctrl Pts',(174.285151190536,4.57559783204922,129.000728853085));
#26517=CARTESIAN_POINT('Ctrl Pts',(174.277403293759,4.52531920863508,128.873178005499));
#26518=CARTESIAN_POINT('Ctrl Pts',(174.269655396982,4.46967706655748,128.747665158614));
#26519=CARTESIAN_POINT('Ctrl Pts',(174.261907500205,4.40886825989597,128.6246671232));
#26520=CARTESIAN_POINT('Ctrl Pts',(174.254161224121,4.34807217312593,128.501694816323));
#26521=CARTESIAN_POINT('Ctrl Pts',(174.246414948037,4.28211174461267,128.381236624837));
#26522=CARTESIAN_POINT('Ctrl Pts',(174.238668671953,4.2112310554105,128.263747293889));
#26523=CARTESIAN_POINT('Ctrl Pts',(174.230922338687,4.14034984298321,128.146257095661));
#26524=CARTESIAN_POINT('Ctrl Pts',(174.223176005422,4.06454849935292,128.031736136464));
#26525=CARTESIAN_POINT('Ctrl Pts',(174.215429672157,3.98411573949752,127.92061221717));
#26526=CARTESIAN_POINT('Ctrl Pts',(174.207681604154,3.90366496728322,127.809463412444));
#26527=CARTESIAN_POINT('Ctrl Pts',(174.199933536151,3.81858094418172,127.70171347806));
#26528=CARTESIAN_POINT('Ctrl Pts',(174.192185468148,3.72919391063464,127.597758702862));
#26529=CARTESIAN_POINT('Ctrl Pts',(174.184429165406,3.63971187548456,127.493693443291));
#26530=CARTESIAN_POINT('Ctrl Pts',(174.176672862664,3.54591794955613,127.393431697254));
#26531=CARTESIAN_POINT('Ctrl Pts',(174.168916559922,3.44818101074379,127.297334700974));
#26532=CARTESIAN_POINT('Ctrl Pts',(174.161156117408,3.35039190678437,127.201186414834));
#26533=CARTESIAN_POINT('Ctrl Pts',(174.153395674894,3.24865588640648,127.10920756974));
#26534=CARTESIAN_POINT('Ctrl Pts',(174.145635232379,3.14337567593979,127.021719685306));
#26535=CARTESIAN_POINT('Ctrl Pts',(174.137862332114,3.03792646033292,126.934091357552));
#26536=CARTESIAN_POINT('Ctrl Pts',(174.130089431849,2.92892199637252,126.850968634122));
#26537=CARTESIAN_POINT('Ctrl Pts',(174.122316531583,2.81679553265813,126.772630717176));
#26538=CARTESIAN_POINT('Ctrl Pts',(174.114826195821,2.70874514832878,126.697140580833));
#26539=CARTESIAN_POINT('Ctrl Pts',(174.107335860059,2.59779606795384,126.626093577242));
#26540=CARTESIAN_POINT('Ctrl Pts',(174.099845524297,2.48435657640448,126.559698621155));
#26541=CARTESIAN_POINT('Ctrl Pts',(174.092071190178,2.36661599205441,126.490786280128));
#26542=CARTESIAN_POINT('Ctrl Pts',(174.084296856059,2.24581945395365,126.426667421473));
#26543=CARTESIAN_POINT('Ctrl Pts',(174.07652252194,2.12239474115937,126.367624922801));
#26544=CARTESIAN_POINT('Ctrl Pts',(174.068757768993,1.99912213829291,126.308655188733));
#26545=CARTESIAN_POINT('Ctrl Pts',(174.060993016045,1.87322815466102,126.25474953385));
#26546=CARTESIAN_POINT('Ctrl Pts',(174.053228263098,1.7451679105289,126.206146613568));
#26547=CARTESIAN_POINT('Ctrl Pts',(174.045471222213,1.61723485763655,126.157591966392));
#26548=CARTESIAN_POINT('Ctrl Pts',(174.037714181328,1.48714018910576,126.114329710576));
#26549=CARTESIAN_POINT('Ctrl Pts',(174.029957140443,1.35536157626157,126.076551604916));
#26550=CARTESIAN_POINT('Ctrl Pts',(174.022205949203,1.22368233869441,126.038801988019));
#26551=CARTESIAN_POINT('Ctrl Pts',(174.014454757963,1.09032205872987,126.006528396842));
#26552=CARTESIAN_POINT('Ctrl Pts',(174.006703566723,0.955775908446305,125.979873548941));
#26553=CARTESIAN_POINT('Ctrl Pts',(173.998955669946,0.821286943865748,125.953230030061));
#26554=CARTESIAN_POINT('Ctrl Pts',(173.991207773169,0.6856134941453,125.932200580495));
#26555=CARTESIAN_POINT('Ctrl Pts',(173.983459876392,0.549263118127799,125.916877309199));
#26556=CARTESIAN_POINT('Ctrl Pts',(173.975713600308,0.412941263669539,125.901557243201));
#26557=CARTESIAN_POINT('Ctrl Pts',(173.967967324224,0.275943152834509,125.891941024953));
#26558=CARTESIAN_POINT('Ctrl Pts',(173.960221048139,0.138783307366114,125.88806910301));
#26559=CARTESIAN_POINT('Ctrl Pts',(173.952474714874,0.00162244941485037,
125.884197152486));
#26560=CARTESIAN_POINT('Ctrl Pts',(173.944728381609,-0.135699754742573,
125.886069593912));
#26561=CARTESIAN_POINT('Ctrl Pts',(173.936982048343,-0.272667326619256,
125.893674760021));
#26562=CARTESIAN_POINT('Ctrl Pts',(173.92923398034,-0.409665571433761,125.901281629254));
#26563=CARTESIAN_POINT('Ctrl Pts',(173.921485912337,-0.546308635646817,
125.914623756121));
#26564=CARTESIAN_POINT('Ctrl Pts',(173.913737844334,-0.682084607205077,
125.933637503786));
#26565=CARTESIAN_POINT('Ctrl Pts',(173.905981541593,-0.818004883081849,
125.952671459487));
#26566=CARTESIAN_POINT('Ctrl Pts',(173.898225238851,-0.953055837591119,
125.977389022991));
#26567=CARTESIAN_POINT('Ctrl Pts',(173.890468936109,-1.08673416495545,126.007675103879));
#26568=CARTESIAN_POINT('Ctrl Pts',(173.882708493595,-1.22048384046815,126.03797734936));
#26569=CARTESIAN_POINT('Ctrl Pts',(173.874948051081,-1.35285905187628,126.073853932136));
#26570=CARTESIAN_POINT('Ctrl Pts',(173.867187608566,-1.48337161220605,126.115139816345));
#26571=CARTESIAN_POINT('Ctrl Pts',(173.859414708301,-1.61409368288399,126.156491976321));
#26572=CARTESIAN_POINT('Ctrl Pts',(173.851641808036,-1.74294675961674,126.203270656618));
#26573=CARTESIAN_POINT('Ctrl Pts',(173.84386890777,-1.86946176026684,126.255262268508));
#26574=CARTESIAN_POINT('Ctrl Pts',(173.836378572008,-1.99137762197043,126.305363854347));
#26575=CARTESIAN_POINT('Ctrl Pts',(173.828888236246,-2.11112216627042,126.360305817047));
#26576=CARTESIAN_POINT('Ctrl Pts',(173.821397900484,-2.22829893932381,126.419857578508));
#26577=CARTESIAN_POINT('Ctrl Pts',(173.813622735437,-2.34993150416124,126.481673869385));
#26578=CARTESIAN_POINT('Ctrl Pts',(173.805847570389,-2.469182484828,126.548653319388));
#26579=CARTESIAN_POINT('Ctrl Pts',(173.798072405342,-2.58558251387288,126.620588859158));
#26580=CARTESIAN_POINT('Ctrl Pts',(173.790307006116,-2.70183634127263,126.692434045906));
#26581=CARTESIAN_POINT('Ctrl Pts',(173.78254160689,-2.81524601298638,126.769222731812));
#26582=CARTESIAN_POINT('Ctrl Pts',(173.774776207664,-2.92536462976308,126.850700940073));
#26583=CARTESIAN_POINT('Ctrl Pts',(173.766866450566,-3.03753033887832,126.933693818794));
#26584=CARTESIAN_POINT('Ctrl Pts',(173.758956693467,-3.14628104028566,127.021552147574));
#26585=CARTESIAN_POINT('Ctrl Pts',(173.751046936369,-3.25117224834878,127.113959274342));
#26586=CARTESIAN_POINT('Ctrl Pts',(173.743296109138,-3.35395588905281,127.204509675007));
#26587=CARTESIAN_POINT('Ctrl Pts',(173.735545281908,-3.45303335142762,127.299427539009));
#26588=CARTESIAN_POINT('Ctrl Pts',(173.727794454678,-3.54801762590248,127.398372656814));
#26589=CARTESIAN_POINT('Ctrl Pts',(173.720047155673,-3.64295866294001,127.497272734182));
#26590=CARTESIAN_POINT('Ctrl Pts',(173.712299856667,-3.7338099494695,127.600196136174));
#26591=CARTESIAN_POINT('Ctrl Pts',(173.704552557662,-3.82022046937444,127.706764997109));
#26592=CARTESIAN_POINT('Ctrl Pts',(173.696807107526,-3.90661036767271,127.813308425711));
#26593=CARTESIAN_POINT('Ctrl Pts',(173.689061657391,-3.98856136312799,127.923495277988));
#26594=CARTESIAN_POINT('Ctrl Pts',(173.681316207255,-4.06576222993557,128.036914041364));
#26595=CARTESIAN_POINT('Ctrl Pts',(173.673285026425,-4.14581104706803,128.154516838126));
#26596=CARTESIAN_POINT('Ctrl Pts',(173.665253845595,-4.22075226631428,128.275594224663));
#26597=CARTESIAN_POINT('Ctrl Pts',(173.657222664766,-4.29028791897018,128.399654266504));
#26598=CARTESIAN_POINT('Ctrl Pts',(173.649473245828,-4.35738401790963,128.519361848497));
#26599=CARTESIAN_POINT('Ctrl Pts',(173.64172382689,-4.41944728697983,128.641845955821));
#26600=CARTESIAN_POINT('Ctrl Pts',(173.633974407952,-4.47625713219153,128.766640040793));
#26601=CARTESIAN_POINT('Ctrl Pts',(173.626222377563,-4.53308612156845,128.891476179719));
#26602=CARTESIAN_POINT('Ctrl Pts',(173.618470347174,-4.58465800978425,129.018623486625));
#26603=CARTESIAN_POINT('Ctrl Pts',(173.610718316784,-4.63080065760616,129.147596200995));
#26604=CARTESIAN_POINT('Ctrl Pts',(173.60295954152,-4.67698345315476,129.276681131754));
#26605=CARTESIAN_POINT('Ctrl Pts',(173.595200766255,-4.71772746156828,129.407594268184));
#26606=CARTESIAN_POINT('Ctrl Pts',(173.587441990991,-4.75291059024451,129.539835416694));
#26607=CARTESIAN_POINT('Ctrl Pts',(173.586608673094,-4.75668937359732,129.55403854954));
#26608=CARTESIAN_POINT('Ctrl Pts',(173.585775355196,-4.76040405828026,129.568256992362));
#26609=CARTESIAN_POINT('Ctrl Pts',(173.584942037299,-4.76405452823404,129.582490119308));
#26610=CARTESIAN_POINT('Ctrl Pts',(175.334949039109,-4.76405452823403,129.582490119308));
#26611=CARTESIAN_POINT('Ctrl Pts',(175.327312301175,-4.79766811449444,129.71354898198));
#26612=CARTESIAN_POINT('Ctrl Pts',(175.319675563241,-4.82585603888722,129.845944000492));
#26613=CARTESIAN_POINT('Ctrl Pts',(175.312038825307,-4.84853163743738,129.979179411243));
#26614=CARTESIAN_POINT('Ctrl Pts',(175.304175593761,-4.87187975850474,130.116366374303));
#26615=CARTESIAN_POINT('Ctrl Pts',(175.296312362215,-4.8893834241265,130.254443897876));
#26616=CARTESIAN_POINT('Ctrl Pts',(175.288449130669,-4.90100548934506,130.392865470681));
#26617=CARTESIAN_POINT('Ctrl Pts',(175.280585899123,-4.91262755456361,130.531287043487));
#26618=CARTESIAN_POINT('Ctrl Pts',(175.272722667577,-4.9183680466244,130.670052201154));
#26619=CARTESIAN_POINT('Ctrl Pts',(175.264859436032,-4.91824815910515,130.808615962297));
#26620=CARTESIAN_POINT('',(175.610140563974,-4.9182499975673,130.80451530825));
#26621=CARTESIAN_POINT('Ctrl Pts',(175.679864508177,-4.76405452823404,129.582490119308));
#26622=CARTESIAN_POINT('Ctrl Pts',(175.671751454559,-4.79965799329642,129.721307489228));
#26623=CARTESIAN_POINT('Ctrl Pts',(175.66363840094,-4.82922619760711,129.861823675682));
#26624=CARTESIAN_POINT('Ctrl Pts',(175.655525347322,-4.85260786805939,130.003498618625));
#26625=CARTESIAN_POINT('Ctrl Pts',(175.647426424684,-4.87594881328887,130.144926798034));
#26626=CARTESIAN_POINT('Ctrl Pts',(175.639327502045,-4.89312465678322,130.287509379538));
#26627=CARTESIAN_POINT('Ctrl Pts',(175.631228579407,-4.90403474638115,130.430694631977));
#26628=CARTESIAN_POINT('Ctrl Pts',(175.624199240941,-4.9135039950584,130.554970124867));
#26629=CARTESIAN_POINT('Ctrl Pts',(175.617169902474,-4.91825392331427,130.679699262973));
#26630=CARTESIAN_POINT('Ctrl Pts',(175.610140564008,-4.91824999756732,130.804515307654));
#26631=CARTESIAN_POINT('Ctrl Pts',(175.610140563974,-4.9182499975673,130.80451530825));
#26632=CARTESIAN_POINT('Ctrl Pts',(175.602006617861,-4.91824545490126,130.948945255158));
#26633=CARTESIAN_POINT('Ctrl Pts',(175.593872671748,-4.91187459119385,131.093245944634));
#26634=CARTESIAN_POINT('Ctrl Pts',(175.585738725635,-4.89919723011719,131.236852886759));
#26635=CARTESIAN_POINT('Ctrl Pts',(175.577593375339,-4.8865020947703,131.380661172728));
#26636=CARTESIAN_POINT('Ctrl Pts',(175.569448025042,-4.86748284501924,131.52377344223));
#26637=CARTESIAN_POINT('Ctrl Pts',(175.561302674745,-4.84225068832209,131.665633706629));
#26638=CARTESIAN_POINT('Ctrl Pts',(175.553137416072,-4.81695686070191,131.807840697373));
#26639=CARTESIAN_POINT('Ctrl Pts',(175.544972157399,-4.78541982124724,131.948789238779));
#26640=CARTESIAN_POINT('Ctrl Pts',(175.536806898725,-4.74780158491423,132.087934991253));
#26641=CARTESIAN_POINT('Ctrl Pts',(175.52863104151,-4.7101345199425,132.227261355535));
#26642=CARTESIAN_POINT('Ctrl Pts',(175.520455184294,-4.66637060377285,132.364779946843));
#26643=CARTESIAN_POINT('Ctrl Pts',(175.512279327079,-4.61672068197947,132.499964700801));
#26644=CARTESIAN_POINT('Ctrl Pts',(175.5040846359,-4.56695638626696,132.635460867336));
#26645=CARTESIAN_POINT('Ctrl Pts',(175.49588994472,-4.51127910012212,132.768612141795));
#26646=CARTESIAN_POINT('Ctrl Pts',(175.487695253541,-4.44994722009171,132.898913744345));
#26647=CARTESIAN_POINT('Ctrl Pts',(175.482628384762,-4.41202503592258,132.979480675718));
#26648=CARTESIAN_POINT('Ctrl Pts',(175.477561515982,-4.37194195059445,133.058958661978));
#26649=CARTESIAN_POINT('Ctrl Pts',(175.472494647203,-4.32976738006333,133.137233845377));
#26650=CARTESIAN_POINT('Ctrl Pts',(175.464720313084,-4.26505696088523,133.257335125965));
#26651=CARTESIAN_POINT('Ctrl Pts',(175.456945978965,-4.19524311273341,133.374932142333));
#26652=CARTESIAN_POINT('Ctrl Pts',(175.449171644846,-4.12054403631122,133.489560779066));
#26653=CARTESIAN_POINT('Ctrl Pts',(175.441406891898,-4.04593701982468,133.604048146249));
#26654=CARTESIAN_POINT('Ctrl Pts',(175.433642138951,-3.9664569656865,133.715574088242));
#26655=CARTESIAN_POINT('Ctrl Pts',(175.425877386004,-3.88236842902149,133.823698035583));
#26656=CARTESIAN_POINT('Ctrl Pts',(175.418120345119,-3.79836341027648,133.931714592695));
#26657=CARTESIAN_POINT('Ctrl Pts',(175.410363304234,-3.70975925632101,134.036335572715));
#26658=CARTESIAN_POINT('Ctrl Pts',(175.402606263349,-3.61686417682021,134.137148727983));
#26659=CARTESIAN_POINT('Ctrl Pts',(175.394855072109,-3.52403915022179,134.237885859265));
#26660=CARTESIAN_POINT('Ctrl Pts',(175.387103880869,-3.4269299026427,134.334820595012));
#26661=CARTESIAN_POINT('Ctrl Pts',(175.379352689629,-3.32588510062422,134.427573468055));
#26662=CARTESIAN_POINT('Ctrl Pts',(175.371604792852,-3.22488324534181,134.520286918652));
#26663=CARTESIAN_POINT('Ctrl Pts',(175.363856896075,-3.11994944993998,134.608821777836));
#26664=CARTESIAN_POINT('Ctrl Pts',(175.356108999298,-3.01146928550664,134.692835357737));
#26665=CARTESIAN_POINT('Ctrl Pts',(175.348362723214,-2.90301181278509,134.776831363809));
#26666=CARTESIAN_POINT('Ctrl Pts',(175.340616447129,-2.79100975547024,134.856307732517));
#26667=CARTESIAN_POINT('Ctrl Pts',(175.332870171045,-2.67588150403046,134.93096227497));
#26668=CARTESIAN_POINT('Ctrl Pts',(175.32512383778,-2.56075240274012,135.005617368506));
#26669=CARTESIAN_POINT('Ctrl Pts',(175.317377504515,-2.44249738931157,135.075450352049));
#26670=CARTESIAN_POINT('Ctrl Pts',(175.309631171249,-2.3215632079231,135.140202788831));
#26671=CARTESIAN_POINT('Ctrl Pts',(175.301883103246,-2.20060194416336,135.204969726472));
#26672=CARTESIAN_POINT('Ctrl Pts',(175.294135035243,-2.07696066315284,135.264653668843));
#26673=CARTESIAN_POINT('Ctrl Pts',(175.28638696724,-1.95110966959261,135.319042679431));
#26674=CARTESIAN_POINT('Ctrl Pts',(175.278630664499,-1.82512492009864,135.373489495306));
#26675=CARTESIAN_POINT('Ctrl Pts',(175.270874361757,-1.69692612611241,135.422629982482));
#26676=CARTESIAN_POINT('Ctrl Pts',(175.263118059015,-1.5670030071668,135.466300625549));
#26677=CARTESIAN_POINT('Ctrl Pts',(175.255357616501,-1.43701054434061,135.509994576953));
#26678=CARTESIAN_POINT('Ctrl Pts',(175.247597173987,-1.30529229802676,135.548212758163));
#26679=CARTESIAN_POINT('Ctrl Pts',(175.239836731472,-1.17235105601835,135.580842174523));
#26680=CARTESIAN_POINT('Ctrl Pts',(175.232063831207,-1.03919640492635,135.613523970519));
#26681=CARTESIAN_POINT('Ctrl Pts',(175.224290930941,-0.904815218402296,
135.640598996321));
#26682=CARTESIAN_POINT('Ctrl Pts',(175.216518030676,-0.769719223808543,
135.662005662132));
#26683=CARTESIAN_POINT('Ctrl Pts',(175.209027694914,-0.639534308903681,
135.682634141721));
#26684=CARTESIAN_POINT('Ctrl Pts',(175.201537359152,-0.508685959715356,
135.697999188744));
#26685=CARTESIAN_POINT('Ctrl Pts',(175.19404702339,-0.377632712410248,135.708091503026));
#26686=CARTESIAN_POINT('Ctrl Pts',(175.186272689271,-0.241610541401607,
135.718566470472));
#26687=CARTESIAN_POINT('Ctrl Pts',(175.178498355152,-0.104936750786517,
135.723394162604));
#26688=CARTESIAN_POINT('Ctrl Pts',(175.170724021032,0.0318802431817009,
135.722507292137));
#26689=CARTESIAN_POINT('Ctrl Pts',(175.162959268085,0.168528622432492,135.721621514658));
#26690=CARTESIAN_POINT('Ctrl Pts',(175.155194515138,0.305319466679357,135.715035189939));
#26691=CARTESIAN_POINT('Ctrl Pts',(175.147429762191,0.44173911385091,135.702732757144));
#26692=CARTESIAN_POINT('Ctrl Pts',(175.139672721306,0.578023267105712,135.690442543298));
#26693=CARTESIAN_POINT('Ctrl Pts',(175.131915680421,0.713936570106025,135.672447554386));
#26694=CARTESIAN_POINT('Ctrl Pts',(175.124158639536,0.848965592368096,135.648784265997));
#26695=CARTESIAN_POINT('Ctrl Pts',(175.116407448296,0.98389278819383,135.625138822278));
#26696=CARTESIAN_POINT('Ctrl Pts',(175.108656257056,1.11793664705349,135.595833654446));
#26697=CARTESIAN_POINT('Ctrl Pts',(175.100905065816,1.25058944968992,135.560956994265));
#26698=CARTESIAN_POINT('Ctrl Pts',(175.093157169039,1.38318587134687,135.526095157595));
#26699=CARTESIAN_POINT('Ctrl Pts',(175.085409272261,1.51439203538062,135.485666637616));
#26700=CARTESIAN_POINT('Ctrl Pts',(175.077661375484,1.64371121819141,135.439810595043));
#26701=CARTESIAN_POINT('Ctrl Pts',(175.0699150994,1.77300335021696,135.393964144565));
#26702=CARTESIAN_POINT('Ctrl Pts',(175.062168823316,1.90040891787971,135.342692560288));
#26703=CARTESIAN_POINT('Ctrl Pts',(175.054422547232,2.02544753083894,135.286184505485));
#26704=CARTESIAN_POINT('Ctrl Pts',(175.046676213967,2.15048706680477,135.229676033552));
#26705=CARTESIAN_POINT('Ctrl Pts',(175.038929880701,2.27315925692985,135.167931174969));
#26706=CARTESIAN_POINT('Ctrl Pts',(175.031183547436,2.39300519490094,135.101186096879));
#26707=CARTESIAN_POINT('Ctrl Pts',(175.023435479433,2.51287797153889,135.034426071693));
#26708=CARTESIAN_POINT('Ctrl Pts',(175.01568741143,2.62992289508509,134.962663788988));
#26709=CARTESIAN_POINT('Ctrl Pts',(175.007939343427,2.74370744617025,134.886180372569));
#26710=CARTESIAN_POINT('Ctrl Pts',(175.000183040685,2.85761292883036,134.809615668664));
#26711=CARTESIAN_POINT('Ctrl Pts',(174.992426737943,2.96825079200132,134.728320026146));
#26712=CARTESIAN_POINT('Ctrl Pts',(174.984670435201,3.07521876016915,134.642617075856));
#26713=CARTESIAN_POINT('Ctrl Pts',(174.976909992687,3.18224382036244,134.55686838332));
#26714=CARTESIAN_POINT('Ctrl Pts',(174.969149550173,3.28559478813973,134.466707952717));
#26715=CARTESIAN_POINT('Ctrl Pts',(174.961389107659,3.38490482881226,134.372497717284));
#26716=CARTESIAN_POINT('Ctrl Pts',(174.953616207393,3.48437429077838,134.278136247217));
#26717=CARTESIAN_POINT('Ctrl Pts',(174.945843307128,3.5797895905496,134.179712261912));
#26718=CARTESIAN_POINT('Ctrl Pts',(174.938070406862,3.67082230974587,134.077623001301));
#26719=CARTESIAN_POINT('Ctrl Pts',(174.9305800711,3.75854576030193,133.97924494246));
#26720=CARTESIAN_POINT('Ctrl Pts',(174.923089735338,3.84219953840779,133.877463703698));
#26721=CARTESIAN_POINT('Ctrl Pts',(174.915599399576,3.92152796956395,133.772660037508));
#26722=CARTESIAN_POINT('Ctrl Pts',(174.907825065457,4.0038641622986,133.66388270846));
#26723=CARTESIAN_POINT('Ctrl Pts',(174.900050731338,4.08180135868748,133.551504663133));
#26724=CARTESIAN_POINT('Ctrl Pts',(174.892276397219,4.15500813662662,133.435917276098));
#26725=CARTESIAN_POINT('Ctrl Pts',(174.884511644272,4.22812469375459,133.320472340188));
#26726=CARTESIAN_POINT('Ctrl Pts',(174.876746891325,4.29652222485149,133.201826259415));
#26727=CARTESIAN_POINT('Ctrl Pts',(174.868982138378,4.35990999124917,133.080402781214));
#26728=CARTESIAN_POINT('Ctrl Pts',(174.861225097493,4.42323480002363,132.959099902525));
#26729=CARTESIAN_POINT('Ctrl Pts',(174.853468056608,4.4815595663455,132.835025460387));
#26730=CARTESIAN_POINT('Ctrl Pts',(174.845711015723,4.53463745644448,132.708631134355));
#26731=CARTESIAN_POINT('Ctrl Pts',(174.837959824483,4.58767532009363,132.582332123267));
#26732=CARTESIAN_POINT('Ctrl Pts',(174.830208633243,4.63547403234835,132.453717069458));
#26733=CARTESIAN_POINT('Ctrl Pts',(174.822457442003,4.67783339042948,132.323260822939));
#26734=CARTESIAN_POINT('Ctrl Pts',(174.814709545225,4.72017474465348,132.192860023806));
#26735=CARTESIAN_POINT('Ctrl Pts',(174.806961648448,4.75708122234953,132.060619959483));
#26736=CARTESIAN_POINT('Ctrl Pts',(174.799213751671,4.78840141212789,131.927033757367));
#26737=CARTESIAN_POINT('Ctrl Pts',(174.791467475587,4.81971505039774,131.793475498606));
#26738=CARTESIAN_POINT('Ctrl Pts',(174.783721199503,4.84544463583429,131.658572042538));
#26739=CARTESIAN_POINT('Ctrl Pts',(174.775974923419,4.86548923347927,131.522829532271));
#26740=CARTESIAN_POINT('Ctrl Pts',(174.768228590154,4.88553397908892,131.387086019983));
#26741=CARTESIAN_POINT('Ctrl Pts',(174.760482256888,4.89989359605523,131.250503827908));
#26742=CARTESIAN_POINT('Ctrl Pts',(174.752735923623,4.90851872841307,131.113596701033));
#26743=CARTESIAN_POINT('Ctrl Pts',(174.74498785562,4.9171457923095,130.976658914757));
#26744=CARTESIAN_POINT('Ctrl Pts',(174.737239787617,4.92003579161466,130.839396439));
#26745=CARTESIAN_POINT('Ctrl Pts',(174.729491719614,4.91719145646168,130.70232511884));
#26746=CARTESIAN_POINT('Ctrl Pts',(174.721735416872,4.91434409831544,130.56510811765));
#26747=CARTESIAN_POINT('Ctrl Pts',(174.71397911413,4.90575023937708,130.4280830694));
#26748=CARTESIAN_POINT('Ctrl Pts',(174.706222811389,4.89146471969663,130.291763350247));
#26749=CARTESIAN_POINT('Ctrl Pts',(174.698462368875,4.87717157540419,130.155370873155));
#26750=CARTESIAN_POINT('Ctrl Pts',(174.69070192636,4.85718077423298,130.019684861881));
#26751=CARTESIAN_POINT('Ctrl Pts',(174.682941483846,4.83159853775673,129.885209578592));
#26752=CARTESIAN_POINT('Ctrl Pts',(174.675168583581,4.8059752344034,129.75051842364));
#26753=CARTESIAN_POINT('Ctrl Pts',(174.667395683315,4.77474264822851,129.617042261444));
#26754=CARTESIAN_POINT('Ctrl Pts',(174.65962278305,4.73805747028144,129.485272117574));
#26755=CARTESIAN_POINT('Ctrl Pts',(174.652132447288,4.70270589095705,129.358292150343));
#26756=CARTESIAN_POINT('Ctrl Pts',(174.644642111526,4.66229136261598,129.232896611929));
#26757=CARTESIAN_POINT('Ctrl Pts',(174.637151775764,4.61699602480054,129.109506414551));
#26758=CARTESIAN_POINT('Ctrl Pts',(174.629377441645,4.56998330048471,128.981437840337));
#26759=CARTESIAN_POINT('Ctrl Pts',(174.621603107526,4.51756342660974,128.855123991234));
#26760=CARTESIAN_POINT('Ctrl Pts',(174.613828773407,4.45988653594367,128.731055249559));
#26761=CARTESIAN_POINT('Ctrl Pts',(174.60606402046,4.40228072689065,128.607139411519));
#26762=CARTESIAN_POINT('Ctrl Pts',(174.598299267512,4.33943095516473,128.485463526739));
#26763=CARTESIAN_POINT('Ctrl Pts',(174.590534514565,4.27153658013364,128.366501247733));
#26764=CARTESIAN_POINT('Ctrl Pts',(174.58277747368,4.20370963875299,128.24765712374));
#26765=CARTESIAN_POINT('Ctrl Pts',(174.575020432795,4.13084825746991,128.131521579328));
#26766=CARTESIAN_POINT('Ctrl Pts',(174.56726339191,4.05319902740399,128.018546426571));
#26767=CARTESIAN_POINT('Ctrl Pts',(174.55951220067,3.97560835322643,127.905656469254));
#26768=CARTESIAN_POINT('Ctrl Pts',(174.55176100943,3.89323723741079,127.795922480723));
#26769=CARTESIAN_POINT('Ctrl Pts',(174.54400981819,3.80637697022949,127.689769565276));
#26770=CARTESIAN_POINT('Ctrl Pts',(174.536261921413,3.71955362097885,127.583661767649));
#26771=CARTESIAN_POINT('Ctrl Pts',(174.528514024636,3.6282451623162,127.481132317808));
#26772=CARTESIAN_POINT('Ctrl Pts',(174.520766127859,3.53278463473215,127.382575149846));
#26773=CARTESIAN_POINT('Ctrl Pts',(174.513019851775,3.43734407543255,127.284038597919));
#26774=CARTESIAN_POINT('Ctrl Pts',(174.505273575691,3.33775344658681,127.189472955786));
#26775=CARTESIAN_POINT('Ctrl Pts',(174.497527299606,3.23438402291478,127.099236725601));
#26776=CARTESIAN_POINT('Ctrl Pts',(174.489780966341,3.13101383619319,127.008999829311));
#26777=CARTESIAN_POINT('Ctrl Pts',(174.482034633076,3.02386509351492,126.92309266585));
#26778=CARTESIAN_POINT('Ctrl Pts',(174.47428829981,2.91334334498373,126.841834451502));
#26779=CARTESIAN_POINT('Ctrl Pts',(174.466540231807,2.8027968458733,126.760558039941));
#26780=CARTESIAN_POINT('Ctrl Pts',(174.458792163804,2.68887615276026,126.683932880708));
#26781=CARTESIAN_POINT('Ctrl Pts',(174.451044095801,2.57201673642119,126.612235503728));
#26782=CARTESIAN_POINT('Ctrl Pts',(174.44328779306,2.45503312050375,126.540461925923));
#26783=CARTESIAN_POINT('Ctrl Pts',(174.435531490318,2.335104875987,126.473626797237));
#26784=CARTESIAN_POINT('Ctrl Pts',(174.427775187576,2.21269356315809,126.411961471534));
#26785=CARTESIAN_POINT('Ctrl Pts',(174.420014745062,2.09021691572571,126.350263233191));
#26786=CARTESIAN_POINT('Ctrl Pts',(174.412254302548,1.96525491527737,126.293740456976));
#26787=CARTESIAN_POINT('Ctrl Pts',(174.404493860033,1.83828922721223,126.242576341692));
#26788=CARTESIAN_POINT('Ctrl Pts',(174.396720959768,1.71111972255312,126.191330093227));
#26789=CARTESIAN_POINT('Ctrl Pts',(174.388948059502,1.5819404713301,126.145459826525));
#26790=CARTESIAN_POINT('Ctrl Pts',(174.381175159237,1.45124928260237,126.105099124284));
#26791=CARTESIAN_POINT('Ctrl Pts',(174.373684823475,1.32530904777689,126.066205635232));
#26792=CARTESIAN_POINT('Ctrl Pts',(174.366194487713,1.1979651901758,126.032428171055));
#26793=CARTESIAN_POINT('Ctrl Pts',(174.358704151951,1.06967028604185,126.003841005934));
#26794=CARTESIAN_POINT('Ctrl Pts',(174.350929817832,0.936511041622508,125.974169949759));
#26795=CARTESIAN_POINT('Ctrl Pts',(174.343155483713,0.801905400721561,125.94999655343));
#26796=CARTESIAN_POINT('Ctrl Pts',(174.335381149594,0.666347086299638,125.931459569619));
#26797=CARTESIAN_POINT('Ctrl Pts',(174.327616396647,0.530955835385183,125.912945430984));
#26798=CARTESIAN_POINT('Ctrl Pts',(174.3198516437,0.394614630670574,125.900053936113));
#26799=CARTESIAN_POINT('Ctrl Pts',(174.312086890753,0.257829728039735,125.892873379077));
#26800=CARTESIAN_POINT('Ctrl Pts',(174.304329849868,0.121180682102519,125.885699953872));
#26801=CARTESIAN_POINT('Ctrl Pts',(174.296572808983,-0.0159107968626869,
125.884226198964));
#26802=CARTESIAN_POINT('Ctrl Pts',(174.288815768098,-0.152931298038684,
125.888488865722));
#26803=CARTESIAN_POINT('Ctrl Pts',(174.281064576857,-0.289848470988973,
125.89274831797));
#26804=CARTESIAN_POINT('Ctrl Pts',(174.273313385617,-0.426694383493149,
125.902735569373));
#26805=CARTESIAN_POINT('Ctrl Pts',(174.265562194377,-0.562953933757235,
125.918435328435));
#26806=CARTESIAN_POINT('Ctrl Pts',(174.2578142976,-0.699155570077616,125.934128414681));
#26807=CARTESIAN_POINT('Ctrl Pts',(174.250066400823,-0.834770952254194,
125.955529134883));
#26808=CARTESIAN_POINT('Ctrl Pts',(174.242318504046,-0.969288635856963,
125.982570223646));
#26809=CARTESIAN_POINT('Ctrl Pts',(174.234572227962,-1.10377818126019,126.009605655996));
#26810=CARTESIAN_POINT('Ctrl Pts',(174.226825951878,-1.23717010175166,126.04227903313));
#26811=CARTESIAN_POINT('Ctrl Pts',(174.219079675794,-1.36896209626315,126.080471770282));
#26812=CARTESIAN_POINT('Ctrl Pts',(174.211333342528,-1.50075506363308,126.118664789363));
#26813=CARTESIAN_POINT('Ctrl Pts',(174.203587009263,-1.63094770594155,126.162377140939));
#26814=CARTESIAN_POINT('Ctrl Pts',(174.195840675997,-1.75905224774906,126.211440168419));
#26815=CARTESIAN_POINT('Ctrl Pts',(174.188092607994,-1.8871854776808,126.260514183225));
#26816=CARTESIAN_POINT('Ctrl Pts',(174.180344539991,-2.01322931157661,126.314941118504));
#26817=CARTESIAN_POINT('Ctrl Pts',(174.172596471988,-2.13671571438622,126.374504071537));
#26818=CARTESIAN_POINT('Ctrl Pts',(174.164840169247,-2.26033336001404,126.434130328786));
#26819=CARTESIAN_POINT('Ctrl Pts',(174.157083866505,-2.38138779221869,126.498903337848));
#26820=CARTESIAN_POINT('Ctrl Pts',(174.149327563763,-2.49943488183132,126.568559827398));
#26821=CARTESIAN_POINT('Ctrl Pts',(174.141567121249,-2.61754497673016,126.638253494714));
#26822=CARTESIAN_POINT('Ctrl Pts',(174.133806678735,-2.73264420277672,126.71283562361));
#26823=CARTESIAN_POINT('Ctrl Pts',(174.12604623622,-2.84431807771759,126.79199999877));
#26824=CARTESIAN_POINT('Ctrl Pts',(174.118273335955,-2.95617122147637,126.871291455612));
#26825=CARTESIAN_POINT('Ctrl Pts',(174.110500435689,-3.06458771663076,126.955179618617));
#26826=CARTESIAN_POINT('Ctrl Pts',(174.102727535424,-3.16918609831779,127.043317871634));
#26827=CARTESIAN_POINT('Ctrl Pts',(174.095237199662,-3.26998206536386,127.128252077148));
#26828=CARTESIAN_POINT('Ctrl Pts',(174.0877468639,-3.36723246818446,127.217132526666));
#26829=CARTESIAN_POINT('Ctrl Pts',(174.080256528138,-3.46063018929389,127.309618601988));
#26830=CARTESIAN_POINT('Ctrl Pts',(174.072592942127,-3.55618818451548,127.404243865203));
#26831=CARTESIAN_POINT('Ctrl Pts',(174.064929356116,-3.64803424359307,127.502961956952));
#26832=CARTESIAN_POINT('Ctrl Pts',(174.057265770104,-3.73578973359036,127.605445468816));
#26833=CARTESIAN_POINT('Ctrl Pts',(174.049611137343,-3.82344270020136,127.707809250773));
#26834=CARTESIAN_POINT('Ctrl Pts',(174.041956504581,-3.9070143390471,127.813929404798));
#26835=CARTESIAN_POINT('Ctrl Pts',(174.034301871819,-3.98616111841343,127.923440174279));
#26836=CARTESIAN_POINT('Ctrl Pts',(174.026654411474,-4.06523373698538,128.032848331806));
#26837=CARTESIAN_POINT('Ctrl Pts',(174.019006951128,-4.13988950626791,128.145640462903));
#26838=CARTESIAN_POINT('Ctrl Pts',(174.011359490783,-4.20982401111621,128.261416485673));
#26839=CARTESIAN_POINT('Ctrl Pts',(174.003717703085,-4.27970664072984,128.3771066294));
#26840=CARTESIAN_POINT('Ctrl Pts',(173.996075915387,-4.3448747666291,128.495775917224));
#26841=CARTESIAN_POINT('Ctrl Pts',(173.988434127689,-4.40506665823473,128.616994439029));
#26842=CARTESIAN_POINT('Ctrl Pts',(173.980795658444,-4.46523241146658,128.7381603216));
#26843=CARTESIAN_POINT('Ctrl Pts',(173.973157189198,-4.52042605048181,128.861872875672));
#26844=CARTESIAN_POINT('Ctrl Pts',(173.965518719952,-4.57043148963561,128.987677084023));
#26845=CARTESIAN_POINT('Ctrl Pts',(173.957880796175,-4.6204333578595,129.113472308591));
#26846=CARTESIAN_POINT('Ctrl Pts',(173.950242872399,-4.66524760870487,129.241358518312));
#26847=CARTESIAN_POINT('Ctrl Pts',(173.942604948623,-4.70470621169906,129.370860521961));
#26848=CARTESIAN_POINT('Ctrl Pts',(173.938470750539,-4.72606406831749,129.440956394999));
#26849=CARTESIAN_POINT('Ctrl Pts',(173.934336552455,-4.74585369313538,129.511525339495));
#26850=CARTESIAN_POINT('Ctrl Pts',(173.930202354372,-4.76405452823406,129.582490119308));
#26851=CARTESIAN_POINT('Origin',(213.235140564004,0.,130.804360617566));
#26852=CARTESIAN_POINT('',(171.834603948179,-4.76405452823406,129.582490119308));
#26853=CARTESIAN_POINT('',(172.180231140679,-4.76405452823404,129.582490119308));
#26854=CARTESIAN_POINT('',(213.235140564004,-4.76405452823405,129.582490119308));
#26855=CARTESIAN_POINT('',(173.514859435953,-4.91824918172569,130.801523549609));
#26856=CARTESIAN_POINT('Ctrl Pts',(173.514859435953,-4.91824918172569,130.801523549609));
#26857=CARTESIAN_POINT('Ctrl Pts',(173.507187584774,-4.91832695800124,130.936353983495));
#26858=CARTESIAN_POINT('Ctrl Pts',(173.499515733596,-4.91285613080631,131.071408084697));
#26859=CARTESIAN_POINT('Ctrl Pts',(173.491843882417,-4.90180792317066,131.206184144554));
#26860=CARTESIAN_POINT('Ctrl Pts',(173.484180616626,-4.89077207932404,131.340809379696));
#26861=CARTESIAN_POINT('Ctrl Pts',(173.476517350836,-4.87417130102263,131.475156795457));
#26862=CARTESIAN_POINT('Ctrl Pts',(173.468854085045,-4.85202881415562,131.608723377211));
#26863=CARTESIAN_POINT('Ctrl Pts',(173.461197450555,-4.82990548798381,131.742174378968));
#26864=CARTESIAN_POINT('Ctrl Pts',(173.453540816066,-4.8022500580158,131.874845496675));
#26865=CARTESIAN_POINT('Ctrl Pts',(173.445884181576,-4.7691376287652,132.006238040765));
#26866=CARTESIAN_POINT('Ctrl Pts',(173.438231801396,-4.73604359800506,132.137557578298));
#26867=CARTESIAN_POINT('Ctrl Pts',(173.430579421216,-4.69749869592266,132.267599566633));
#26868=CARTESIAN_POINT('Ctrl Pts',(173.422927041036,-4.65362918335053,132.395875143534));
#26869=CARTESIAN_POINT('Ctrl Pts',(173.415276829414,-4.60977210267183,132.524114369261));
#26870=CARTESIAN_POINT('Ctrl Pts',(173.407626617791,-4.56059354113234,132.650587798968));
#26871=CARTESIAN_POINT('Ctrl Pts',(173.399976406169,-4.50626958902363,132.774821846198));
#26872=CARTESIAN_POINT('Ctrl Pts',(173.392326606852,-4.45194856468911,132.899049197869));
#26873=CARTESIAN_POINT('Ctrl Pts',(173.384676807536,-4.39248286221509,133.021037039006));
#26874=CARTESIAN_POINT('Ctrl Pts',(173.37702700822,-4.32809645737784,133.140332389256));
#26875=CARTESIAN_POINT('Ctrl Pts',(173.369375865516,-4.26369874559336,133.259648689057));
#26876=CARTESIAN_POINT('Ctrl Pts',(173.361724722813,-4.19437880415203,133.376271204381));
#26877=CARTESIAN_POINT('Ctrl Pts',(173.354073580109,-4.12040596640364,133.489772640799));
#26878=CARTESIAN_POINT('Ctrl Pts',(173.346414694795,-4.04635827148544,133.603388935543));
#26879=CARTESIAN_POINT('Ctrl Pts',(173.33875580948,-3.96764849618805,133.713877506441));
#26880=CARTESIAN_POINT('Ctrl Pts',(173.331096924166,-3.8845888314214,133.820840797063));
#26881=CARTESIAN_POINT('Ctrl Pts',(173.323434102541,-3.80148647785632,133.927859061833));
#26882=CARTESIAN_POINT('Ctrl Pts',(173.315771280917,-3.71403004215883,134.031348131974));
#26883=CARTESIAN_POINT('Ctrl Pts',(173.308108459292,-3.62257036387388,134.130945506199));
#26884=CARTESIAN_POINT('Ctrl Pts',(173.300433602329,-3.53096703769839,134.230699309497));
#26885=CARTESIAN_POINT('Ctrl Pts',(173.292758745366,-3.43534819248633,134.326548922592));
#26886=CARTESIAN_POINT('Ctrl Pts',(173.285083888404,-3.33610018744934,134.418170048319));
#26887=CARTESIAN_POINT('Ctrl Pts',(173.278223476555,-3.24738424225639,134.500068467995));
#26888=CARTESIAN_POINT('Ctrl Pts',(173.271363064707,-3.1557691341598,134.578588662547));
#26889=CARTESIAN_POINT('Ctrl Pts',(173.264502652858,-3.06155048147109,134.653528282387));
#26890=CARTESIAN_POINT('Ctrl Pts',(173.256728318739,-2.95478031920592,134.738451120297));
#26891=CARTESIAN_POINT('Ctrl Pts',(173.24895398462,-2.84430491379653,134.819062635927));
#26892=CARTESIAN_POINT('Ctrl Pts',(173.241179650501,-2.73050757389078,134.895022110702));
#26893=CARTESIAN_POINT('Ctrl Pts',(173.233414897554,-2.61685047903623,134.970887972213));
#26894=CARTESIAN_POINT('Ctrl Pts',(173.225650144607,-2.49987991755621,135.042112985306));
#26895=CARTESIAN_POINT('Ctrl Pts',(173.21788539166,-2.38001253793216,135.108396326268));
#26896=CARTESIAN_POINT('Ctrl Pts',(173.210128350775,-2.26026421227955,135.174613833682));
#26897=CARTESIAN_POINT('Ctrl Pts',(173.20237130989,-2.13762513408804,135.235899248413));
#26898=CARTESIAN_POINT('Ctrl Pts',(173.194614269005,-2.01254092950996,135.291994968708));
#26899=CARTESIAN_POINT('Ctrl Pts',(173.186863077765,-1.88755105190373,135.348048386784));
#26900=CARTESIAN_POINT('Ctrl Pts',(173.179111886525,-1.76012007335078,135.398919740851));
#26901=CARTESIAN_POINT('Ctrl Pts',(173.171360695285,-1.63071790280482,135.444397490692));
#26902=CARTESIAN_POINT('Ctrl Pts',(173.163612798508,-1.50137073163291,135.489855911277));
#26903=CARTESIAN_POINT('Ctrl Pts',(173.155864901731,-1.37005440288363,135.529925157737));
#26904=CARTESIAN_POINT('Ctrl Pts',(173.148117004954,-1.23725826848959,135.564442028588));
#26905=CARTESIAN_POINT('Ctrl Pts',(173.140370728869,-1.10448991218415,135.598951679253));
#26906=CARTESIAN_POINT('Ctrl Pts',(173.132624452785,-0.97024274408504,135.62791116618));
#26907=CARTESIAN_POINT('Ctrl Pts',(173.124878176701,-0.835020339381439,
135.65120743744));
#26908=CARTESIAN_POINT('Ctrl Pts',(173.117131843436,-0.69979693649658,135.674503880667));
#26909=CARTESIAN_POINT('Ctrl Pts',(173.109385510171,-0.563598667931364,
135.692136958429));
#26910=CARTESIAN_POINT('Ctrl Pts',(173.101639176905,-0.426937946320922,
135.704045000513));
#26911=CARTESIAN_POINT('Ctrl Pts',(173.093891108902,-0.290246620489972,
135.715955709319));
#26912=CARTESIAN_POINT('Ctrl Pts',(173.086143040899,-0.153093024949944,
135.72213879732));
#26913=CARTESIAN_POINT('Ctrl Pts',(173.078394972896,-0.0159929217430619,
135.722584615002));
#26914=CARTESIAN_POINT('Ctrl Pts',(173.070638670155,0.121252893085441,135.723030906504));
#26915=CARTESIAN_POINT('Ctrl Pts',(173.062882367413,0.258444710425685,135.717727745723));
#26916=CARTESIAN_POINT('Ctrl Pts',(173.055126064671,0.395067985950195,135.706717637304));
#26917=CARTESIAN_POINT('Ctrl Pts',(173.047365622157,0.5317641814305,135.695701652459));
#26918=CARTESIAN_POINT('Ctrl Pts',(173.039605179643,0.667890842593393,135.678972698288));
#26919=CARTESIAN_POINT('Ctrl Pts',(173.031844737128,0.802941303460366,135.656624864873));
#26920=CARTESIAN_POINT('Ctrl Pts',(173.024071836863,0.938208559316431,135.634241156733));
#26921=CARTESIAN_POINT('Ctrl Pts',(173.016298936598,1.07239577962624,135.60622062463));
#26922=CARTESIAN_POINT('Ctrl Pts',(173.008526036332,1.20500832006864,135.57270813123));
#26923=CARTESIAN_POINT('Ctrl Pts',(173.00103570057,1.33280006063679,135.540413901378));
#26924=CARTESIAN_POINT('Ctrl Pts',(172.993545364808,1.45912932548036,135.50302015859));
#26925=CARTESIAN_POINT('Ctrl Pts',(172.986055029046,1.58357095274533,135.460698889226));
#26926=CARTESIAN_POINT('Ctrl Pts',(172.978280694927,1.71273082212963,135.41677299607));
#26927=CARTESIAN_POINT('Ctrl Pts',(172.970506360808,1.84026622840091,135.367399401916));
#26928=CARTESIAN_POINT('Ctrl Pts',(172.962732026688,1.9656833276869,135.312716428475));
#26929=CARTESIAN_POINT('Ctrl Pts',(172.954967273741,2.09094586160686,135.258100846911));
#26930=CARTESIAN_POINT('Ctrl Pts',(172.947202520794,2.2140949279641,135.198189060103));
#26931=CARTESIAN_POINT('Ctrl Pts',(172.939437767847,2.33465222656795,135.133169003656));
#26932=CARTESIAN_POINT('Ctrl Pts',(172.931680726962,2.45508978596318,135.068213526045));
#26933=CARTESIAN_POINT('Ctrl Pts',(172.923923686077,2.57294035845778,134.998160059884));
#26934=CARTESIAN_POINT('Ctrl Pts',(172.916166645192,2.68774634458161,134.923244283038));
#26935=CARTESIAN_POINT('Ctrl Pts',(172.908415453952,2.80246575461867,134.848385000761));
#26936=CARTESIAN_POINT('Ctrl Pts',(172.900664262712,2.91414482213019,134.768670918946));
#26937=CARTESIAN_POINT('Ctrl Pts',(172.892913071472,3.02235157507306,134.68438304265));
#26938=CARTESIAN_POINT('Ctrl Pts',(172.885165174694,3.13051233725909,134.60013099095));
#26939=CARTESIAN_POINT('Ctrl Pts',(172.877417277917,3.23520341239461,134.511309250959));
#26940=CARTESIAN_POINT('Ctrl Pts',(172.86966938114,3.33602298777566,134.418241313927));
#26941=CARTESIAN_POINT('Ctrl Pts',(172.861923105056,3.43682147387489,134.325192844702));
#26942=CARTESIAN_POINT('Ctrl Pts',(172.854176828972,3.53374978392915,134.227900210162));
#26943=CARTESIAN_POINT('Ctrl Pts',(172.846430552888,3.62644060945729,134.126725975045));
#26944=CARTESIAN_POINT('Ctrl Pts',(172.838684219623,3.71913211920805,134.025550993084));
#26945=CARTESIAN_POINT('Ctrl Pts',(172.830937886357,3.80758581791146,133.920494641647));
#26946=CARTESIAN_POINT('Ctrl Pts',(172.823191553092,3.89147284912339,133.81195469374));
#26947=CARTESIAN_POINT('Ctrl Pts',(172.815443485089,3.97537866625415,133.703390439064));
#26948=CARTESIAN_POINT('Ctrl Pts',(172.807695417086,4.05471554185538,133.591341344839));
#26949=CARTESIAN_POINT('Ctrl Pts',(172.799947349083,4.12919657553683,133.476236120481));
#26950=CARTESIAN_POINT('Ctrl Pts',(172.792191046341,4.20375676854742,133.36100856092));
#26951=CARTESIAN_POINT('Ctrl Pts',(172.784434743599,4.27345059755786,133.242718711578));
#26952=CARTESIAN_POINT('Ctrl Pts',(172.776678440857,4.33803569915251,133.12182244797));
#26953=CARTESIAN_POINT('Ctrl Pts',(172.768917998343,4.4026552717605,133.000861658385));
#26954=CARTESIAN_POINT('Ctrl Pts',(172.761157555829,4.46216051426459,132.877292034684));
#26955=CARTESIAN_POINT('Ctrl Pts',(172.753397113315,4.5163567219789,132.751590707292));
#26956=CARTESIAN_POINT('Ctrl Pts',(172.745624213049,4.57063993025715,132.62568759297));
#26957=CARTESIAN_POINT('Ctrl Pts',(172.737851312784,4.61959693329831,132.497646302103));
#26958=CARTESIAN_POINT('Ctrl Pts',(172.730078412518,4.66308224082845,132.367961294776));
#26959=CARTESIAN_POINT('Ctrl Pts',(172.722588076756,4.7049867478969,132.242990664122));
#26960=CARTESIAN_POINT('Ctrl Pts',(172.715097740994,4.74181038645512,132.116494044411));
#26961=CARTESIAN_POINT('Ctrl Pts',(172.707607405232,4.77346804312973,131.988922099178));
#26962=CARTESIAN_POINT('Ctrl Pts',(172.699833071113,4.80632600947932,131.856513224868));
#26963=CARTESIAN_POINT('Ctrl Pts',(172.692058736994,4.83372260870009,131.722526441924));
#26964=CARTESIAN_POINT('Ctrl Pts',(172.684284402875,4.85550728008837,131.587452001447));
#26965=CARTESIAN_POINT('Ctrl Pts',(172.676519649928,4.8772651038161,131.452544028146));
#26966=CARTESIAN_POINT('Ctrl Pts',(172.668754896981,4.89342469923445,131.316551446661));
#26967=CARTESIAN_POINT('Ctrl Pts',(172.660990144034,4.90388564895249,131.179978248273));
#26968=CARTESIAN_POINT('Ctrl Pts',(172.653233103149,4.91433620870783,131.04354069631));
#26969=CARTESIAN_POINT('Ctrl Pts',(172.645476062264,4.9190993567033,130.906524062358));
#26970=CARTESIAN_POINT('Ctrl Pts',(172.637719021379,4.91812603170907,130.769440727451));
#26971=CARTESIAN_POINT('Ctrl Pts',(172.629967830139,4.91715344070678,130.632460768155));
#26972=CARTESIAN_POINT('Ctrl Pts',(172.622216638899,4.91045298995868,130.495414597396));
#26973=CARTESIAN_POINT('Ctrl Pts',(172.614465447658,4.89802760553687,130.358817535588));
#26974=CARTESIAN_POINT('Ctrl Pts',(172.606717550881,4.88560750223493,130.222278531174));
#26975=CARTESIAN_POINT('Ctrl Pts',(172.598969654104,4.8674673401504,130.086188644601));
#26976=CARTESIAN_POINT('Ctrl Pts',(172.591221757327,4.84366209205329,129.951060787198));
#26977=CARTESIAN_POINT('Ctrl Pts',(172.583475481243,4.81986182350088,129.81596119563));
#26978=CARTESIAN_POINT('Ctrl Pts',(172.575729205159,4.79039889378159,129.681823617755));
#26979=CARTESIAN_POINT('Ctrl Pts',(172.567982929075,4.75537979967245,129.549153055699));
#26980=CARTESIAN_POINT('Ctrl Pts',(172.56023659581,4.72036044706037,129.4164815143));
#26981=CARTESIAN_POINT('Ctrl Pts',(172.552490262544,4.6797849479972,129.285277388346));
#26982=CARTESIAN_POINT('Ctrl Pts',(172.544743929279,4.63381020523644,129.156032360104));
#26983=CARTESIAN_POINT('Ctrl Pts',(172.536995861276,4.58782516675081,129.026758388334));
#26984=CARTESIAN_POINT('Ctrl Pts',(172.529247793273,4.53643860955747,128.899444755574));
#26985=CARTESIAN_POINT('Ctrl Pts',(172.52149972527,4.47985614236095,128.774564567158));
#26986=CARTESIAN_POINT('Ctrl Pts',(172.513743422528,4.42321353864481,128.649551654592));
#26987=CARTESIAN_POINT('Ctrl Pts',(172.505987119787,4.36136415519768,128.526977709454));
#26988=CARTESIAN_POINT('Ctrl Pts',(172.498230817045,4.29456052965462,128.407293050802));
#26989=CARTESIAN_POINT('Ctrl Pts',(172.490470374531,4.22772124900527,128.287544512844));
#26990=CARTESIAN_POINT('Ctrl Pts',(172.482709932016,4.15592266198212,128.170688667083));
#26991=CARTESIAN_POINT('Ctrl Pts',(172.474949489502,4.07946094928639,128.057147224735));
#26992=CARTESIAN_POINT('Ctrl Pts',(172.467176589237,4.00287649346144,127.943423515585));
#26993=CARTESIAN_POINT('Ctrl Pts',(172.459403688972,3.92161418512189,127.833025157096));
#26994=CARTESIAN_POINT('Ctrl Pts',(172.451630788706,3.83601138649515,127.72634182211));
#26995=CARTESIAN_POINT('Ctrl Pts',(172.444140452944,3.75352046521824,127.623536695069));
#26996=CARTESIAN_POINT('Ctrl Pts',(172.436650117182,3.66699935259202,127.524181412244));
#26997=CARTESIAN_POINT('Ctrl Pts',(172.42915978142,3.57678119875583,127.428591176575));
#26998=CARTESIAN_POINT('Ctrl Pts',(172.421385447301,3.48314239619632,127.329376608068));
#26999=CARTESIAN_POINT('Ctrl Pts',(172.413611113182,3.38522405208093,127.233903944241));
#27000=CARTESIAN_POINT('Ctrl Pts',(172.405836779063,3.28335724680598,127.142564848774));
#27001=CARTESIAN_POINT('Ctrl Pts',(172.398072026115,3.18161598326433,127.051338320578));
#27002=CARTESIAN_POINT('Ctrl Pts',(172.390307273168,3.07593622899429,126.964235483192));
#27003=CARTESIAN_POINT('Ctrl Pts',(172.382542520221,2.96668772808122,126.88161324021));
#27004=CARTESIAN_POINT('Ctrl Pts',(172.374785479336,2.85754773432011,126.799073058805));
#27005=CARTESIAN_POINT('Ctrl Pts',(172.367028438451,2.74484635750175,126.721004850029));
#27006=CARTESIAN_POINT('Ctrl Pts',(172.359271397566,2.62898815951006,126.64772684495));
#27007=CARTESIAN_POINT('Ctrl Pts',(172.351520206326,2.51321733108573,126.574504099383));
#27008=CARTESIAN_POINT('Ctrl Pts',(172.343769015086,2.39429474898018,126.50606457553));
#27009=CARTESIAN_POINT('Ctrl Pts',(172.336017823846,2.2726555484634,126.442684354873));
#27010=CARTESIAN_POINT('Ctrl Pts',(172.328269927069,2.15106804785209,126.379331072501));
#27011=CARTESIAN_POINT('Ctrl Pts',(172.320522030292,2.02676657130688,126.321032996745));
#27012=CARTESIAN_POINT('Ctrl Pts',(172.312774133515,1.90021235978166,126.268021118561));
#27013=CARTESIAN_POINT('Ctrl Pts',(172.305027857431,1.77368462066922,126.215020329319));
#27014=CARTESIAN_POINT('Ctrl Pts',(172.297281581346,1.64490544424396,126.167303689192));
#27015=CARTESIAN_POINT('Ctrl Pts',(172.289535305262,1.51435726720566,126.125054565408));
#27016=CARTESIAN_POINT('Ctrl Pts',(172.281788971997,1.38380812649077,126.082805129751));
#27017=CARTESIAN_POINT('Ctrl Pts',(172.274042638732,1.25149033107672,126.046023411354));
#27018=CARTESIAN_POINT('Ctrl Pts',(172.266296305466,1.11790235694933,126.014843169761));
#27019=CARTESIAN_POINT('Ctrl Pts',(172.258548237463,0.984284466720592,125.983655945569));
#27020=CARTESIAN_POINT('Ctrl Pts',(172.25080016946,0.849396212419496,125.958072783163));
#27021=CARTESIAN_POINT('Ctrl Pts',(172.243052101457,0.713746767490395,125.938176423108));
#27022=CARTESIAN_POINT('Ctrl Pts',(172.235295798715,0.577953152717437,125.918258916964));
#27023=CARTESIAN_POINT('Ctrl Pts',(172.227539495974,0.441397118690106,125.904040343542));
#27024=CARTESIAN_POINT('Ctrl Pts',(172.219783193232,0.30459403434467,125.895551644226));
#27025=CARTESIAN_POINT('Ctrl Pts',(172.212022750718,0.167717934074336,125.887058414236));
#27026=CARTESIAN_POINT('Ctrl Pts',(172.204262308203,0.0305949114422294,
125.884301159944));
#27027=CARTESIAN_POINT('Ctrl Pts',(172.196501865689,-0.10626014305852,125.887258641351));
#27028=CARTESIAN_POINT('Ctrl Pts',(172.188728965424,-0.243334889442407,
125.890220870369));
#27029=CARTESIAN_POINT('Ctrl Pts',(172.180956065158,-0.380140417683305,
125.898916142451));
#27030=CARTESIAN_POINT('Ctrl Pts',(172.173183164893,-0.516166532458371,
125.913271252888));
#27031=CARTESIAN_POINT('Ctrl Pts',(172.165692829131,-0.647247755330227,
125.927104518902));
#27032=CARTESIAN_POINT('Ctrl Pts',(172.158202493369,-0.777604943426181,
125.946193224104));
#27033=CARTESIAN_POINT('Ctrl Pts',(172.150712157607,-0.906792831796963,
125.970427454737));
#27034=CARTESIAN_POINT('Ctrl Pts',(172.142937823488,-1.0408789182228,125.99558053359));
#27035=CARTESIAN_POINT('Ctrl Pts',(172.135163489369,-1.17413003100894,126.026356702838));
#27036=CARTESIAN_POINT('Ctrl Pts',(172.12738915525,-1.30603769536912,126.062689118951));
#27037=CARTESIAN_POINT('Ctrl Pts',(172.119624402303,-1.43778279532265,126.09897675861));
#27038=CARTESIAN_POINT('Ctrl Pts',(172.111859649356,-1.56818736785014,126.140806917671));
#27039=CARTESIAN_POINT('Ctrl Pts',(172.104094896409,-1.69675128414133,126.188061435075));
#27040=CARTESIAN_POINT('Ctrl Pts',(172.096337855524,-1.82518750893799,126.235269018626));
#27041=CARTESIAN_POINT('Ctrl Pts',(172.088580814639,-1.95178635104295,126.287890105047));
#27042=CARTESIAN_POINT('Ctrl Pts',(172.080823773754,-2.07606139806592,126.345756336632));
#27043=CARTESIAN_POINT('Ctrl Pts',(172.073072582514,-2.20024272830921,126.403578930842));
#27044=CARTESIAN_POINT('Ctrl Pts',(172.065321391273,-2.32210339850782,126.466638632859));
#27045=CARTESIAN_POINT('Ctrl Pts',(172.057570200033,-2.44117593224942,126.534718579841));
#27046=CARTESIAN_POINT('Ctrl Pts',(172.049822303256,-2.56019785698778,126.60276959103));
#27047=CARTESIAN_POINT('Ctrl Pts',(172.042074406479,-2.67643366351317,126.675836409693));
#27048=CARTESIAN_POINT('Ctrl Pts',(172.034326509702,-2.78943970059156,126.753655837005));
#27049=CARTESIAN_POINT('Ctrl Pts',(172.026580233618,-2.90242209924305,126.83145898617));
#27050=CARTESIAN_POINT('Ctrl Pts',(172.018833957534,-3.01217575045164,126.914012544979));
#27051=CARTESIAN_POINT('Ctrl Pts',(172.01108768145,-3.11828561335356,127.001009740241));
#27052=CARTESIAN_POINT('Ctrl Pts',(172.003341348184,-3.22439625953463,127.088007577696));
#27053=CARTESIAN_POINT('Ctrl Pts',(171.995595014919,-3.32686276139793,127.179448869175));
#27054=CARTESIAN_POINT('Ctrl Pts',(171.987848681654,-3.42530314480444,127.274986533016));
#27055=CARTESIAN_POINT('Ctrl Pts',(171.980100613651,-3.52376557325187,127.370545591854));
#27056=CARTESIAN_POINT('Ctrl Pts',(171.972352545648,-3.61819980861456,127.470202576247));
#27057=CARTESIAN_POINT('Ctrl Pts',(171.964604477645,-3.70826101822914,127.573573827451));
#27058=CARTESIAN_POINT('Ctrl Pts',(171.956848174903,-3.79841794596916,127.677054942851));
#27059=CARTESIAN_POINT('Ctrl Pts',(171.949091872161,-3.88419230643845,127.784257915503));
#27060=CARTESIAN_POINT('Ctrl Pts',(171.941335569419,-3.96527949827477,127.894765875499));
#27061=CARTESIAN_POINT('Ctrl Pts',(171.933575126905,-4.04640996878683,128.005332816921));
#27062=CARTESIAN_POINT('Ctrl Pts',(171.925814684391,-4.12284806806102,128.119207936093));
#27063=CARTESIAN_POINT('Ctrl Pts',(171.918054241877,-4.19433335502167,128.235946560321));
#27064=CARTESIAN_POINT('Ctrl Pts',(171.910281341612,-4.26593339651131,128.352872583753));
#27065=CARTESIAN_POINT('Ctrl Pts',(171.902508441346,-4.33256454752172,128.47267095615));
#27066=CARTESIAN_POINT('Ctrl Pts',(171.894735541081,-4.39401262421191,128.594872866804));
#27067=CARTESIAN_POINT('Ctrl Pts',(171.887245205319,-4.45322690853672,128.712632430199));
#27068=CARTESIAN_POINT('Ctrl Pts',(171.879754869556,-4.50762828454832,128.832623535885));
#27069=CARTESIAN_POINT('Ctrl Pts',(171.872264533794,-4.55706854922347,128.954412158776));
#27070=CARTESIAN_POINT('Ctrl Pts',(171.863524797849,-4.61475553043118,129.096515321982));
#27071=CARTESIAN_POINT('Ctrl Pts',(171.854785061903,-4.66584301224399,129.241444733054));
#27072=CARTESIAN_POINT('Ctrl Pts',(171.846045325957,-4.71007753832181,129.388608998991));
#27073=CARTESIAN_POINT('Ctrl Pts',(171.842231533364,-4.72938033064195,129.452827642531));
#27074=CARTESIAN_POINT('Ctrl Pts',(171.838417740772,-4.74737875562519,129.517471534996));
#27075=CARTESIAN_POINT('Ctrl Pts',(171.834603948179,-4.76405452823406,129.582490119308));
#27076=CARTESIAN_POINT('Ctrl Pts',(173.584942037299,-4.76405452823404,129.582490119308));
#27077=CARTESIAN_POINT('Ctrl Pts',(173.577168687926,-4.79810681298591,129.71525946074));
#27078=CARTESIAN_POINT('Ctrl Pts',(173.569395338553,-4.82656714898436,129.849306908375));
#27079=CARTESIAN_POINT('Ctrl Pts',(173.56162198918,-4.84937016082865,129.984121563531));
#27080=CARTESIAN_POINT('Ctrl Pts',(173.55539808501,-4.86762789680362,130.092063900104));
#27081=CARTESIAN_POINT('Ctrl Pts',(173.549174180841,-4.88225986259371,130.200497867035));
#27082=CARTESIAN_POINT('Ctrl Pts',(173.542950276672,-4.89325658827015,130.309160633872));
#27083=CARTESIAN_POINT('Ctrl Pts',(173.533586663111,-4.90980071987285,130.472639397256));
#27084=CARTESIAN_POINT('Ctrl Pts',(173.524223049551,-4.91815425455034,130.636960909544));
#27085=CARTESIAN_POINT('Ctrl Pts',(173.514859435991,-4.91824918172531,130.801523548944));
#27086=CARTESIAN_POINT('',(173.860140564047,-4.91824797895214,130.808819320649));
#27087=CARTESIAN_POINT('Ctrl Pts',(173.930202354372,-4.76405452823406,129.582490119308));
#27088=CARTESIAN_POINT('Ctrl Pts',(173.922561425174,-4.7976937708428,129.713649015693));
#27089=CARTESIAN_POINT('Ctrl Pts',(173.914920495977,-4.82590276153612,129.846160505067));
#27090=CARTESIAN_POINT('Ctrl Pts',(173.907279566779,-4.84859108433937,129.979528780544));
#27091=CARTESIAN_POINT('Ctrl Pts',(173.899423066324,-4.8719195060305,130.116659735421));
#27092=CARTESIAN_POINT('Ctrl Pts',(173.891566565869,-4.88941106084076,130.254696087604));
#27093=CARTESIAN_POINT('Ctrl Pts',(173.883710065413,-4.90102458032567,130.393092912119));
#27094=CARTESIAN_POINT('Ctrl Pts',(173.875853564958,-4.91263809981058,130.531489736635));
#27095=CARTESIAN_POINT('Ctrl Pts',(173.867997064503,-4.91837360391904,130.670246572473));
#27096=CARTESIAN_POINT('Ctrl Pts',(173.860140564047,-4.91824797895214,130.808819320649));
#27097=CARTESIAN_POINT('Ctrl Pts',(173.860140564008,-4.91824797895151,130.808819321346));
#27098=CARTESIAN_POINT('Ctrl Pts',(173.849233599194,-4.91807357721686,131.001196079562));
#27099=CARTESIAN_POINT('Ctrl Pts',(173.83832663438,-4.90660860059347,131.193082194159));
#27100=CARTESIAN_POINT('Ctrl Pts',(173.827419669566,-4.88404528139263,131.38339839855));
#27101=CARTESIAN_POINT('Ctrl Pts',(173.818882747819,-4.86638488790488,131.532359596444));
#27102=CARTESIAN_POINT('Ctrl Pts',(173.810345826072,-4.8419263040771,131.68035995043));
#27103=CARTESIAN_POINT('Ctrl Pts',(173.801808904325,-4.81078058184838,131.826893382719));
#27104=CARTESIAN_POINT('Ctrl Pts',(173.794034570206,-4.7824170501024,131.960337251127));
#27105=CARTESIAN_POINT('Ctrl Pts',(173.786260236087,-4.74845208433762,132.092811447682));
#27106=CARTESIAN_POINT('Ctrl Pts',(173.778485901968,-4.70896471082672,132.223809248087));
#27107=CARTESIAN_POINT('Ctrl Pts',(173.770721149021,-4.66952600197456,132.354645605411));
#27108=CARTESIAN_POINT('Ctrl Pts',(173.762956396074,-4.62457853878966,132.484008816164));
#27109=CARTESIAN_POINT('Ctrl Pts',(173.755191643127,-4.57425245001799,132.611401731101));
#27110=CARTESIAN_POINT('Ctrl Pts',(173.747434602242,-4.52397634582726,132.738668117598));
#27111=CARTESIAN_POINT('Ctrl Pts',(173.739677561357,-4.46833238984024,132.863967741382));
#27112=CARTESIAN_POINT('Ctrl Pts',(173.731920520472,-4.40750056383562,132.986818370259));
#27113=CARTESIAN_POINT('Ctrl Pts',(173.724169329232,-4.34671461158427,133.10957635652));
#27114=CARTESIAN_POINT('Ctrl Pts',(173.716418137991,-4.2807487491259,133.229888674883));
#27115=CARTESIAN_POINT('Ctrl Pts',(173.708666946751,-4.20983099499577,133.347293187666));
#27116=CARTESIAN_POINT('Ctrl Pts',(173.700919049974,-4.13894338280274,133.464647800399));
#27117=CARTESIAN_POINT('Ctrl Pts',(173.693171153197,-4.06310826671952,133.579096731704));
#27118=CARTESIAN_POINT('Ctrl Pts',(173.68542325642,-3.98259941618203,133.690202774152));
#27119=CARTESIAN_POINT('Ctrl Pts',(173.677676980336,-3.90210740636054,133.801285575611));
#27120=CARTESIAN_POINT('Ctrl Pts',(173.669930704252,-3.81694383593146,133.909026562693));
#27121=CARTESIAN_POINT('Ctrl Pts',(173.662184428168,-3.72742534958035,134.013018175768));
#27122=CARTESIAN_POINT('Ctrl Pts',(173.654438094903,-3.63790620242411,134.117010556485));
#27123=CARTESIAN_POINT('Ctrl Pts',(173.646691761637,-3.54403233026384,134.217253211663));
#27124=CARTESIAN_POINT('Ctrl Pts',(173.638945428372,-3.44615988113825,134.313372606165));
#27125=CARTESIAN_POINT('Ctrl Pts',(173.631197360369,-3.34826551415631,134.409513525939));
#27126=CARTESIAN_POINT('Ctrl Pts',(173.623449292366,-3.24637106724771,134.501529073735));
#27127=CARTESIAN_POINT('Ctrl Pts',(173.615701224363,-3.14086836370495,134.589083722943));
#27128=CARTESIAN_POINT('Ctrl Pts',(173.607944921621,-3.03525353063332,134.676731426275));
#27129=CARTESIAN_POINT('Ctrl Pts',(173.600188618879,-2.92602308164329,134.759908510095));
#27130=CARTESIAN_POINT('Ctrl Pts',(173.592432316137,-2.81360107618712,134.838320464488));
#27131=CARTESIAN_POINT('Ctrl Pts',(173.584671873623,-2.70111906772156,134.916774269702));
#27132=CARTESIAN_POINT('Ctrl Pts',(173.576911431109,-2.58544243815103,134.99045766782));
#27133=CARTESIAN_POINT('Ctrl Pts',(173.569150988595,-2.46702198198113,135.059120963687));
#27134=CARTESIAN_POINT('Ctrl Pts',(173.56137808833,-2.34841142678219,135.127894483972));
#27135=CARTESIAN_POINT('Ctrl Pts',(173.553605188064,-2.22704858945512,135.19163161624));
#27136=CARTESIAN_POINT('Ctrl Pts',(173.545832287799,-2.10340728552242,135.250129488494));
#27137=CARTESIAN_POINT('Ctrl Pts',(173.538341952037,-1.98426065442175,135.306500815744));
#27138=CARTESIAN_POINT('Ctrl Pts',(173.530851616275,-1.86299862018901,135.358007069818));
#27139=CARTESIAN_POINT('Ctrl Pts',(173.523361280513,-1.74005863938335,135.404510505777));
#27140=CARTESIAN_POINT('Ctrl Pts',(173.515586946394,-1.61245735183837,135.452777133645));
#27141=CARTESIAN_POINT('Ctrl Pts',(173.507812612275,-1.48264416477591,135.495806985109));
#27142=CARTESIAN_POINT('Ctrl Pts',(173.500038278155,-1.35108811532953,135.533392650352));
#27143=CARTESIAN_POINT('Ctrl Pts',(173.492273525208,-1.21969419695664,135.570931994621));
#27144=CARTESIAN_POINT('Ctrl Pts',(173.484508772261,-1.08656206223956,135.60304039615));
#27145=CARTESIAN_POINT('Ctrl Pts',(173.476744019314,-0.9521803146846,135.629558614626));
#27146=CARTESIAN_POINT('Ctrl Pts',(173.468986978429,-0.817932036975901,
135.656050494833));
#27147=CARTESIAN_POINT('Ctrl Pts',(173.461229937544,-0.682436997426369,
135.676963166011));
#27148=CARTESIAN_POINT('Ctrl Pts',(173.453472896659,-0.546198196186696,
135.692187393648));
#27149=CARTESIAN_POINT('Ctrl Pts',(173.445721705419,-0.410062133686591,
135.707400140576));
#27150=CARTESIAN_POINT('Ctrl Pts',(173.437970514179,-0.273183812861581,
135.716932939106));
#27151=CARTESIAN_POINT('Ctrl Pts',(173.430219322939,-0.136075292818587,
135.720727830985));
#27152=CARTESIAN_POINT('Ctrl Pts',(173.422471426162,0.000974952445806226,
135.724521109934));
#27153=CARTESIAN_POINT('Ctrl Pts',(173.414723529385,0.138254812332943,135.722581321952));
#27154=CARTESIAN_POINT('Ctrl Pts',(173.406975632607,0.275248472784505,135.714902475725));
#27155=CARTESIAN_POINT('Ctrl Pts',(173.399229356523,0.412213477115542,135.707225235747));
#27156=CARTESIAN_POINT('Ctrl Pts',(173.391483080439,0.548892010984102,135.693811347225));
#27157=CARTESIAN_POINT('Ctrl Pts',(173.383736804355,0.684770028742482,135.674706916366));
#27158=CARTESIAN_POINT('Ctrl Pts',(173.37599047109,0.820649049521523,135.655602344482));
#27159=CARTESIAN_POINT('Ctrl Pts',(173.368244137824,0.955727155241739,135.630807200875));
#27160=CARTESIAN_POINT('Ctrl Pts',(173.360497804559,1.08949757349896,135.600419218109));
#27161=CARTESIAN_POINT('Ctrl Pts',(173.352749736556,1.22329794871381,135.570024430165));
#27162=CARTESIAN_POINT('Ctrl Pts',(173.345001668553,1.35578967255406,135.534034397368));
#27163=CARTESIAN_POINT('Ctrl Pts',(173.33725360055,1.4864786669213,135.492597411424));
#27164=CARTESIAN_POINT('Ctrl Pts',(173.329497297808,1.61730655910707,135.451116385759));
#27165=CARTESIAN_POINT('Ctrl Pts',(173.321740995066,1.7463275212036,135.404176960975));
#27166=CARTESIAN_POINT('Ctrl Pts',(173.313984692324,1.87306455918525,135.351976720496));
#27167=CARTESIAN_POINT('Ctrl Pts',(173.30622424981,1.99986924054009,135.299748619176));
#27168=CARTESIAN_POINT('Ctrl Pts',(173.298463807296,2.12438721404093,135.242254271087));
#27169=CARTESIAN_POINT('Ctrl Pts',(173.290703364782,2.24616473863931,135.17973797608));
#27170=CARTESIAN_POINT('Ctrl Pts',(173.282930464517,2.36813775133103,135.117121324366));
#27171=CARTESIAN_POINT('Ctrl Pts',(173.275157564251,2.48736118386485,135.049466809006));
#27172=CARTESIAN_POINT('Ctrl Pts',(173.267384663986,2.60340824542052,134.977063407147));
#27173=CARTESIAN_POINT('Ctrl Pts',(173.259894328224,2.71523670398502,134.907292051318));
#27174=CARTESIAN_POINT('Ctrl Pts',(173.252403992461,2.82411546576469,134.833111256035));
#27175=CARTESIAN_POINT('Ctrl Pts',(173.244913656699,2.92969218608533,134.754814611386));
#27176=CARTESIAN_POINT('Ctrl Pts',(173.23713932258,3.03927187984508,134.673549325659));
#27177=CARTESIAN_POINT('Ctrl Pts',(173.229364988461,3.14564131102171,134.587592500662));
#27178=CARTESIAN_POINT('Ctrl Pts',(173.221590654342,3.24837245383282,134.497226640546));
#27179=CARTESIAN_POINT('Ctrl Pts',(173.213825901395,3.35097698969172,134.406972148277));
#27180=CARTESIAN_POINT('Ctrl Pts',(173.206061148448,3.44995186800253,134.312319688159));
#27181=CARTESIAN_POINT('Ctrl Pts',(173.198296395501,3.54489901325132,134.213594262881));
#27182=CARTESIAN_POINT('Ctrl Pts',(173.190539354616,3.63975185565693,134.114966893088));
#27183=CARTESIAN_POINT('Ctrl Pts',(173.182782313731,3.73058465672387,134.012274888488));
#27184=CARTESIAN_POINT('Ctrl Pts',(173.175025272846,3.81703363049503,133.905882393432));
#27185=CARTESIAN_POINT('Ctrl Pts',(173.167274081606,3.90341741242252,133.799570129784));
#27186=CARTESIAN_POINT('Ctrl Pts',(173.159522890366,3.98542370165354,133.689563232335));
#27187=CARTESIAN_POINT('Ctrl Pts',(173.151771699126,4.06272695581327,133.576261183064));
#27188=CARTESIAN_POINT('Ctrl Pts',(173.144023802348,4.13999735402793,133.463007290186));
#27189=CARTESIAN_POINT('Ctrl Pts',(173.136275905571,4.21256847297687,133.346461353309));
#27190=CARTESIAN_POINT('Ctrl Pts',(173.128528008794,4.28015646190007,133.227054102957));
#27191=CARTESIAN_POINT('Ctrl Pts',(173.12078173271,4.34773031287302,133.107671830027));
#27192=CARTESIAN_POINT('Ctrl Pts',(173.113035456626,4.41032291467358,132.985429774148));
#27193=CARTESIAN_POINT('Ctrl Pts',(173.105289180542,4.46769520352962,132.860785338011));
#27194=CARTESIAN_POINT('Ctrl Pts',(173.097542847277,4.52506791589482,132.736139981778));
#27195=CARTESIAN_POINT('Ctrl Pts',(173.089796514011,4.57722007495053,132.609092565049));
#27196=CARTESIAN_POINT('Ctrl Pts',(173.082050180746,4.62395998300934,132.480122276642));
#27197=CARTESIAN_POINT('Ctrl Pts',(173.074302112743,4.67071035814649,132.351123106232));
#27198=CARTESIAN_POINT('Ctrl Pts',(173.06655404474,4.71204593728985,132.220200574773));
#27199=CARTESIAN_POINT('Ctrl Pts',(173.058805976737,4.74782442117051,132.08785051945));
#27200=CARTESIAN_POINT('Ctrl Pts',(173.051049673995,4.78364093084961,131.955359800913));
#27201=CARTESIAN_POINT('Ctrl Pts',(173.043293371254,4.8138884449104,131.821438905782));
#27202=CARTESIAN_POINT('Ctrl Pts',(173.035537068512,4.83847536896097,131.686595941308));
#27203=CARTESIAN_POINT('Ctrl Pts',(173.027776625998,4.86307541579321,131.551681007084));
#27204=CARTESIAN_POINT('Ctrl Pts',(173.020016183483,4.88200879861843,131.415843409925));
#27205=CARTESIAN_POINT('Ctrl Pts',(173.012255740969,4.89523579570234,131.279596945065));
#27206=CARTESIAN_POINT('Ctrl Pts',(173.004482840704,4.9084840259362,131.143131765284));
#27207=CARTESIAN_POINT('Ctrl Pts',(172.996709940438,4.91600754356677,131.006256796804));
#27208=CARTESIAN_POINT('Ctrl Pts',(172.988937040173,4.91781878238998,130.869487310038));
#27209=CARTESIAN_POINT('Ctrl Pts',(172.981446704411,4.91956417811974,130.737689738616));
#27210=CARTESIAN_POINT('Ctrl Pts',(172.973956368649,4.91600540439234,130.605990420908));
#27211=CARTESIAN_POINT('Ctrl Pts',(172.966466032887,4.90719901596116,130.474844487081));
#27212=CARTESIAN_POINT('Ctrl Pts',(172.958691698768,4.898058730636,130.338726115312));
#27213=CARTESIAN_POINT('Ctrl Pts',(172.950917364649,4.88323609511096,130.202772736801));
#27214=CARTESIAN_POINT('Ctrl Pts',(172.94314303053,4.8627374297386,130.067497162156));
#27215=CARTESIAN_POINT('Ctrl Pts',(172.935378277583,4.84226402713931,129.932388302566));
#27216=CARTESIAN_POINT('Ctrl Pts',(172.927613524635,4.81612857106773,129.79795596762));
#27217=CARTESIAN_POINT('Ctrl Pts',(172.919848771688,4.78438932595254,129.664710741415));
#27218=CARTESIAN_POINT('Ctrl Pts',(172.912091730803,4.75268160470302,129.531597856246));
#27219=CARTESIAN_POINT('Ctrl Pts',(172.904334689918,4.71538126053565,129.399670111312));
#27220=CARTESIAN_POINT('Ctrl Pts',(172.896577649033,4.67259802320951,129.269430398957));
#27221=CARTESIAN_POINT('Ctrl Pts',(172.888826457793,4.62984704905545,129.139288901382));
#27222=CARTESIAN_POINT('Ctrl Pts',(172.881075266553,4.58162153311918,129.010833272575));
#27223=CARTESIAN_POINT('Ctrl Pts',(172.873324075313,4.52808160729683,128.884553330321));
#27224=CARTESIAN_POINT('Ctrl Pts',(172.865576178536,4.47456443737116,128.758327060411));
#27225=CARTESIAN_POINT('Ctrl Pts',(172.857828281759,4.41573750236395,128.634274997043));
#27226=CARTESIAN_POINT('Ctrl Pts',(172.850080384982,4.35180975979507,128.512868772271));
#27227=CARTESIAN_POINT('Ctrl Pts',(172.842334108898,4.28789538953182,128.391487943064));
#27228=CARTESIAN_POINT('Ctrl Pts',(172.834587832814,4.21888251602815,128.272752197324));
#27229=CARTESIAN_POINT('Ctrl Pts',(172.82684155673,4.14502674531517,128.1571099035));
#27230=CARTESIAN_POINT('Ctrl Pts',(172.819095223464,4.07117042941569,128.041466756031));
#27231=CARTESIAN_POINT('Ctrl Pts',(172.811348890199,3.99247135540927,127.928917435545));
#27232=CARTESIAN_POINT('Ctrl Pts',(172.803602556933,3.90922906113504,127.819882235993));
#27233=CARTESIAN_POINT('Ctrl Pts',(172.795854488931,3.8259681253262,127.710822618764));
#27234=CARTESIAN_POINT('Ctrl Pts',(172.788106420928,3.73816218189519,127.605278999132));
#27235=CARTESIAN_POINT('Ctrl Pts',(172.780358352925,3.64615147647902,127.503639109612));
#27236=CARTESIAN_POINT('Ctrl Pts',(172.772602050183,3.55404298099015,127.401891196008));
#27237=CARTESIAN_POINT('Ctrl Pts',(172.764845747441,3.45772105926657,127.304055590757));
#27238=CARTESIAN_POINT('Ctrl Pts',(172.757089444699,3.35756368732163,127.210483999194));
#27239=CARTESIAN_POINT('Ctrl Pts',(172.749329002185,3.25735285837149,127.116862465656));
#27240=CARTESIAN_POINT('Ctrl Pts',(172.741568559671,3.15330279665184,127.027509735182));
#27241=CARTESIAN_POINT('Ctrl Pts',(172.733808117156,3.04582430207586,126.942736945665));
#27242=CARTESIAN_POINT('Ctrl Pts',(172.726035216891,2.93817327347894,126.857828071341));
#27243=CARTESIAN_POINT('Ctrl Pts',(172.718262316626,2.82708313104801,126.777514059061));
#27244=CARTESIAN_POINT('Ctrl Pts',(172.71048941636,2.71299410714415,126.702062964165));
#27245=CARTESIAN_POINT('Ctrl Pts',(172.702999080598,2.60305250663191,126.629354706617));
#27246=CARTESIAN_POINT('Ctrl Pts',(172.695508744836,2.49032653659821,126.561162105588));
#27247=CARTESIAN_POINT('Ctrl Pts',(172.688018409074,2.37522968016847,126.497683588934));
#27248=CARTESIAN_POINT('Ctrl Pts',(172.680244074955,2.25576889144443,126.431798265027));
#27249=CARTESIAN_POINT('Ctrl Pts',(172.672469740836,2.13337546713922,126.370782846162));
#27250=CARTESIAN_POINT('Ctrl Pts',(172.664695406717,2.00848426564509,126.314909201507));
#27251=CARTESIAN_POINT('Ctrl Pts',(172.65693065377,1.883746981395,126.259104416125));
#27252=CARTESIAN_POINT('Ctrl Pts',(172.649165900823,1.75651839828276,126.208428954782));
#27253=CARTESIAN_POINT('Ctrl Pts',(172.641401147875,1.62725957851607,126.16310978114));
#27254=CARTESIAN_POINT('Ctrl Pts',(172.63364410699,1.49812914043149,126.11783561914));
#27255=CARTESIAN_POINT('Ctrl Pts',(172.625887066105,1.36697284509654,126.077907286437));
#27256=CARTESIAN_POINT('Ctrl Pts',(172.61813002522,1.23427310169855,126.043504289874));
#27257=CARTESIAN_POINT('Ctrl Pts',(172.61037883398,1.10167342820917,126.009127236878));
#27258=CARTESIAN_POINT('Ctrl Pts',(172.60262764274,0.967533000303468,125.98026732418));
#27259=CARTESIAN_POINT('Ctrl Pts',(172.5948764515,0.832350470758849,125.957054586756));
#27260=CARTESIAN_POINT('Ctrl Pts',(172.587128554723,0.697225397395445,125.933851715365));
#27261=CARTESIAN_POINT('Ctrl Pts',(172.579380657946,0.561059487848173,125.916291311462));
#27262=CARTESIAN_POINT('Ctrl Pts',(172.571632761169,0.424362486164162,125.904452501812));
#27263=CARTESIAN_POINT('Ctrl Pts',(172.563886485085,0.287694078546057,125.892616168585));
#27264=CARTESIAN_POINT('Ctrl Pts',(172.556140209001,0.150495189021715,125.886499082755));
#27265=CARTESIAN_POINT('Ctrl Pts',(172.548393932916,0.0132812039699516,
125.886128549829));
#27266=CARTESIAN_POINT('Ctrl Pts',(172.540647599651,-0.123933793964279,
125.885758014166));
#27267=CARTESIAN_POINT('Ctrl Pts',(172.532901266386,-0.261163496684503,
125.891134117109));
#27268=CARTESIAN_POINT('Ctrl Pts',(172.52515493312,-0.397892391465982,125.902232028135));
#27269=CARTESIAN_POINT('Ctrl Pts',(172.517406865117,-0.534651905735297,
125.913332424462));
#27270=CARTESIAN_POINT('Ctrl Pts',(172.509658797114,-0.670909999286356,
125.930157147007));
#27271=CARTESIAN_POINT('Ctrl Pts',(172.501910729112,-0.806156550694722,
125.952629516374));
#27272=CARTESIAN_POINT('Ctrl Pts',(172.49415442637,-0.941546843747564,125.975125769643));
#27273=CARTESIAN_POINT('Ctrl Pts',(172.486398123628,-1.07592306077914,126.003281595962));
#27274=CARTESIAN_POINT('Ctrl Pts',(172.478641820886,-1.20878499686194,126.036969098731));
#27275=CARTESIAN_POINT('Ctrl Pts',(172.470881378372,-1.34171784536042,126.070674581534));
#27276=CARTESIAN_POINT('Ctrl Pts',(172.463120935858,-1.47313442803267,126.109917511927));
#27277=CARTESIAN_POINT('Ctrl Pts',(172.455360493343,-1.60255092836956,126.154520449939));
#27278=CARTESIAN_POINT('Ctrl Pts',(172.447587593078,-1.73217517956185,126.199194988546));
#27279=CARTESIAN_POINT('Ctrl Pts',(172.439814692813,-1.85979256821545,126.249246586193));
#27280=CARTESIAN_POINT('Ctrl Pts',(172.432041792547,-1.98493961543744,126.304449753386));
#27281=CARTESIAN_POINT('Ctrl Pts',(172.424551456785,-2.10553725226601,126.357646146402));
#27282=CARTESIAN_POINT('Ctrl Pts',(172.417061121023,-2.22384075911418,126.415625931003));
#27283=CARTESIAN_POINT('Ctrl Pts',(172.409570785261,-2.33945969527697,126.478148487229));
#27284=CARTESIAN_POINT('Ctrl Pts',(172.401795470065,-2.45947750219968,126.54304979432));
#27285=CARTESIAN_POINT('Ctrl Pts',(172.39402015487,-2.5769826467889,126.61305200159));
#27286=CARTESIAN_POINT('Ctrl Pts',(172.386244839674,-2.69151117187928,126.687936116358));
#27287=CARTESIAN_POINT('Ctrl Pts',(172.3784793216,-2.80589538771341,126.762725874973));
#27288=CARTESIAN_POINT('Ctrl Pts',(172.370713803526,-2.9173101231536,126.842385088473));
#27289=CARTESIAN_POINT('Ctrl Pts',(172.362948285453,-3.02531508606934,126.926648445099));
#27290=CARTESIAN_POINT('Ctrl Pts',(172.355192093898,-3.13319033319682,127.010810600007));
#27291=CARTESIAN_POINT('Ctrl Pts',(172.347435902343,-3.23766365768947,127.099565645918));
#27292=CARTESIAN_POINT('Ctrl Pts',(172.339679710788,-3.33832342166466,127.192604840265));
#27293=CARTESIAN_POINT('Ctrl Pts',(172.331928807266,-3.43891455760079,127.285580602142));
#27294=CARTESIAN_POINT('Ctrl Pts',(172.324177903745,-3.5356970197125,127.382834437454));
#27295=CARTESIAN_POINT('Ctrl Pts',(172.316427000224,-3.62829191739539,127.484017137644));
#27296=CARTESIAN_POINT('Ctrl Pts',(172.308679702519,-3.72084373877824,127.58515276638));
#27297=CARTESIAN_POINT('Ctrl Pts',(172.300932404815,-3.80921160902707,127.690213335137));
#27298=CARTESIAN_POINT('Ctrl Pts',(172.29318510711,-3.89305350831285,127.798812839887));
#27299=CARTESIAN_POINT('Ctrl Pts',(172.285439735789,-3.97687456011947,127.907385341122));
#27300=CARTESIAN_POINT('Ctrl Pts',(172.277694364468,-4.05617164293115,128.019494717258));
#27301=CARTESIAN_POINT('Ctrl Pts',(172.269948993146,-4.13064330814986,128.134722266902));
#27302=CARTESIAN_POINT('Ctrl Pts',(172.262201269052,-4.20513759526255,128.249984818656));
#27303=CARTESIAN_POINT('Ctrl Pts',(172.254453544957,-4.27480331843837,128.368367111375));
#27304=CARTESIAN_POINT('Ctrl Pts',(172.246705820862,-4.33938258107259,128.489421767924));
#27305=CARTESIAN_POINT('Ctrl Pts',(172.238957093025,-4.40397021015532,128.610492107487));
#27306=CARTESIAN_POINT('Ctrl Pts',(172.231208365187,-4.46346988910171,128.734235151717));
#27307=CARTESIAN_POINT('Ctrl Pts',(172.22345963735,-4.51767034852206,128.860180151512));
#27308=CARTESIAN_POINT('Ctrl Pts',(172.215704049381,-4.57191879289411,128.986236653402));
#27309=CARTESIAN_POINT('Ctrl Pts',(172.207948461411,-4.62085849667513,129.114498643236));
#27310=CARTESIAN_POINT('Ctrl Pts',(172.200192873442,-4.66432674005495,129.244476287076));
#27311=CARTESIAN_POINT('Ctrl Pts',(172.193538962521,-4.70162034312863,129.355990677374));
#27312=CARTESIAN_POINT('Ctrl Pts',(172.1868850516,-4.73488728942838,129.46876749788));
#27313=CARTESIAN_POINT('Ctrl Pts',(172.180231140679,-4.76405452823404,129.582490119308));
#27314=CARTESIAN_POINT('Origin',(213.235140564004,0.,130.804360617566));
#27315=CARTESIAN_POINT('',(170.084755673967,-4.76405452823406,129.582490119308));
#27316=CARTESIAN_POINT('',(170.429908526381,-4.76405452823404,129.582490119308));
#27317=CARTESIAN_POINT('',(213.235140564004,-4.76405452823405,129.582490119308));
#27318=CARTESIAN_POINT('',(171.764859436045,-4.91824915272082,130.801473705555));
#27319=CARTESIAN_POINT('Ctrl Pts',(171.764859435991,-4.91824915272138,130.801473706505));
#27320=CARTESIAN_POINT('Ctrl Pts',(171.757035919054,-4.91833059512529,130.940222017634));
#27321=CARTESIAN_POINT('Ctrl Pts',(171.749212402117,-4.91253637186168,131.078982524251));
#27322=CARTESIAN_POINT('Ctrl Pts',(171.74138888518,-4.90088999446994,131.217229028327));
#27323=CARTESIAN_POINT('Ctrl Pts',(171.733564120028,-4.88924175893856,131.355497589159));
#27324=CARTESIAN_POINT('Ctrl Pts',(171.725739354875,-4.87173954124688,131.493251605358));
#27325=CARTESIAN_POINT('Ctrl Pts',(171.717914589723,-4.84845876191544,131.629969905611));
#27326=CARTESIAN_POINT('Ctrl Pts',(171.710087010741,-4.82516961068537,131.766737370529));
#27327=CARTESIAN_POINT('Ctrl Pts',(171.70225943176,-4.79609782325277,131.902468003263));
#27328=CARTESIAN_POINT('Ctrl Pts',(171.694431852778,-4.76136992124217,132.036650979287));
#27329=CARTESIAN_POINT('Ctrl Pts',(171.68659989282,-4.72662258255471,132.170909055475));
#27330=CARTESIAN_POINT('Ctrl Pts',(171.678767932861,-4.68621292006633,132.30361738256));
#27331=CARTESIAN_POINT('Ctrl Pts',(171.670935972903,-4.64031719067666,132.434280686898));
#27332=CARTESIAN_POINT('Ctrl Pts',(171.663093341267,-4.59435892464868,132.565122030542));
#27333=CARTESIAN_POINT('Ctrl Pts',(171.655250709631,-4.54289979057624,132.6939124286));
#27334=CARTESIAN_POINT('Ctrl Pts',(171.647408077995,-4.4861642914408,132.8201763365));
#27335=CARTESIAN_POINT('Ctrl Pts',(171.639559178351,-4.42938344802311,132.946541157344));
#27336=CARTESIAN_POINT('Ctrl Pts',(171.631710278708,-4.36731800569649,133.070375125644));
#27337=CARTESIAN_POINT('Ctrl Pts',(171.623861379065,-4.3002378395814,133.191228352807));
#27338=CARTESIAN_POINT('Ctrl Pts',(171.616000175001,-4.23305251444804,133.312271036964));
#27339=CARTESIAN_POINT('Ctrl Pts',(171.608138970937,-4.16083696557177,133.430323326701));
#27340=CARTESIAN_POINT('Ctrl Pts',(171.600277766874,-4.08390400590978,133.544964772313));
#27341=CARTESIAN_POINT('Ctrl Pts',(171.598124147909,-4.06282780949502,133.576371410451));
#27342=CARTESIAN_POINT('Ctrl Pts',(171.595970528945,-4.04139779314482,133.60752225611));
#27343=CARTESIAN_POINT('Ctrl Pts',(171.593816909981,-4.01962089508612,133.638409121436));
#27344=CARTESIAN_POINT('Ctrl Pts',(171.586042575862,-3.94100862225861,133.749907401736));
#27345=CARTESIAN_POINT('Ctrl Pts',(171.578268241743,-3.85762912375874,133.858308927935));
#27346=CARTESIAN_POINT('Ctrl Pts',(171.570493907623,-3.76975455094454,133.963179018192));
#27347=CARTESIAN_POINT('Ctrl Pts',(171.562729154676,-3.68198827568764,134.067919865435));
#27348=CARTESIAN_POINT('Ctrl Pts',(171.554964401729,-3.58973819731478,134.169137639484));
#27349=CARTESIAN_POINT('Ctrl Pts',(171.547199648782,-3.49331967220828,134.266426580292));
#27350=CARTESIAN_POINT('Ctrl Pts',(171.539442607897,-3.39699691134051,134.363618892351));
#27351=CARTESIAN_POINT('Ctrl Pts',(171.531685567012,-3.29651421627276,134.456889860773));
#27352=CARTESIAN_POINT('Ctrl Pts',(171.523928526127,-3.19222689663071,134.5458670659));
#27353=CARTESIAN_POINT('Ctrl Pts',(171.516177334887,-3.08801822086768,134.634777172625));
#27354=CARTESIAN_POINT('Ctrl Pts',(171.508426143647,-2.98001092751311,134.719399708287));
#27355=CARTESIAN_POINT('Ctrl Pts',(171.500674952407,-2.86859657138408,134.799399637794));
#27356=CARTESIAN_POINT('Ctrl Pts',(171.49292705563,-2.7572295693284,134.879365565197));
#27357=CARTESIAN_POINT('Ctrl Pts',(171.485179158853,-2.64245870155574,134.954712566589));
#27358=CARTESIAN_POINT('Ctrl Pts',(171.477431262076,-2.52470776291514,135.025146536607));
#27359=CARTESIAN_POINT('Ctrl Pts',(171.469684985991,-2.40698145523242,135.095565773358));
#27360=CARTESIAN_POINT('Ctrl Pts',(171.461938709907,-2.28627665190136,135.161073822318));
#27361=CARTESIAN_POINT('Ctrl Pts',(171.454192433823,-2.1630448870223,135.221420712157));
#27362=CARTESIAN_POINT('Ctrl Pts',(171.446446100558,-2.03981221247431,135.281768047463));
#27363=CARTESIAN_POINT('Ctrl Pts',(171.438699767293,-1.91405289028095,135.336953975678));
#27364=CARTESIAN_POINT('Ctrl Pts',(171.430953434027,-1.78624137104705,135.38677535511));
#27365=CARTESIAN_POINT('Ctrl Pts',(171.423205366024,-1.65840122930977,135.436607891694));
#27366=CARTESIAN_POINT('Ctrl Pts',(171.415457298021,-1.52850834022933,135.481073346974));
#27367=CARTESIAN_POINT('Ctrl Pts',(171.407709230018,-1.39705498341314,135.520017563933));
#27368=CARTESIAN_POINT('Ctrl Pts',(171.399952927276,-1.26546191640478,135.55900317127));
#27369=CARTESIAN_POINT('Ctrl Pts',(171.392196624535,-1.13230544411911,135.592455707017));
#27370=CARTESIAN_POINT('Ctrl Pts',(171.384440321793,-0.998091329470628,
135.620271409985));
#27371=CARTESIAN_POINT('Ctrl Pts',(171.376679879279,-0.863805580708047,
135.648101959031));
#27372=CARTESIAN_POINT('Ctrl Pts',(171.368919436764,-0.72846145040388,135.670289617296));
#27373=CARTESIAN_POINT('Ctrl Pts',(171.36115899425,-0.592571632618561,135.686782344815));
#27374=CARTESIAN_POINT('Ctrl Pts',(171.353386093985,-0.456463672433956,
135.703301547925));
#27375=CARTESIAN_POINT('Ctrl Pts',(171.345613193719,-0.319808664241963,
135.714107520806));
#27376=CARTESIAN_POINT('Ctrl Pts',(171.337840293454,-0.18312202844603,135.719200328604));
#27377=CARTESIAN_POINT('Ctrl Pts',(171.330349957692,-0.0514042961550611,
135.724108000011));
#27378=CARTESIAN_POINT('Ctrl Pts',(171.32285962193,0.0803424961590377,135.723710671613));
#27379=CARTESIAN_POINT('Ctrl Pts',(171.315369286168,0.211661992236977,135.718053960006));
#27380=CARTESIAN_POINT('Ctrl Pts',(171.307594952049,0.347960506923273,135.71218277246));
#27381=CARTESIAN_POINT('Ctrl Pts',(171.29982061793,0.484230436602179,135.700626911707));
#27382=CARTESIAN_POINT('Ctrl Pts',(171.292046283811,0.619958966672321,135.68338039024));
#27383=CARTESIAN_POINT('Ctrl Pts',(171.284281530864,0.755520223459236,135.666155123569));
#27384=CARTESIAN_POINT('Ctrl Pts',(171.276516777917,0.89054102409612,135.643253199231));
#27385=CARTESIAN_POINT('Ctrl Pts',(171.268752024969,1.0245095333365,135.614720612265));
#27386=CARTESIAN_POINT('Ctrl Pts',(171.260994984084,1.1583449831651,135.586216364267));
#27387=CARTESIAN_POINT('Ctrl Pts',(171.253237943199,1.29112984157983,135.552092663791));
#27388=CARTESIAN_POINT('Ctrl Pts',(171.245480902314,1.42235872784494,135.512447140966));
#27389=CARTESIAN_POINT('Ctrl Pts',(171.237729711074,1.55348865338571,135.472831515139));
#27390=CARTESIAN_POINT('Ctrl Pts',(171.229978519834,1.6830645695557,135.42770246786));
#27391=CARTESIAN_POINT('Ctrl Pts',(171.222227328594,1.8105929568999,135.377208330635));
#27392=CARTESIAN_POINT('Ctrl Pts',(171.214479431817,1.93806714127793,135.326735654766));
#27393=CARTESIAN_POINT('Ctrl Pts',(171.20673153504,2.06349516495256,135.270902567934));
#27394=CARTESIAN_POINT('Ctrl Pts',(171.198983638263,2.18640051728477,135.209906649617));
#27395=CARTESIAN_POINT('Ctrl Pts',(171.191237362179,2.30928016046664,135.14892349033));
#27396=CARTESIAN_POINT('Ctrl Pts',(171.183491086095,2.42963783192029,135.082779821336));
#27397=CARTESIAN_POINT('Ctrl Pts',(171.175744810011,2.54701915847475,135.011720415451));
#27398=CARTESIAN_POINT('Ctrl Pts',(171.167998476745,2.66440135151142,134.940660485022));
#27399=CARTESIAN_POINT('Ctrl Pts',(171.16025214348,2.77880682135337,134.864684947764));
#27400=CARTESIAN_POINT('Ctrl Pts',(171.152505810215,2.88980820699957,134.78408316936));
#27401=CARTESIAN_POINT('Ctrl Pts',(171.144757742212,3.00083445063688,134.703463340746));
#27402=CARTESIAN_POINT('Ctrl Pts',(171.137009674209,3.10845477684925,134.618215439113));
#27403=CARTESIAN_POINT('Ctrl Pts',(171.129261606206,3.21227339982114,134.528670307603));
#27404=CARTESIAN_POINT('Ctrl Pts',(171.121505303464,3.31620236246078,134.439030006461));
#27405=CARTESIAN_POINT('Ctrl Pts',(171.113749000722,3.4163212540074,134.345083607835));
#27406=CARTESIAN_POINT('Ctrl Pts',(171.10599269798,3.51226940002566,134.247200538931));
#27407=CARTESIAN_POINT('Ctrl Pts',(171.098232255466,3.6082687564584,134.149265226886));
#27408=CARTESIAN_POINT('Ctrl Pts',(171.090471812952,3.70009267013737,134.047389348172));
#27409=CARTESIAN_POINT('Ctrl Pts',(171.082711370438,3.78742023470387,133.941976117951));
#27410=CARTESIAN_POINT('Ctrl Pts',(171.074938470172,3.87488798522955,133.836393669055));
#27411=CARTESIAN_POINT('Ctrl Pts',(171.067165569907,3.95784472616718,133.727262832685));
#27412=CARTESIAN_POINT('Ctrl Pts',(171.059392669641,4.03601191500818,133.615017281837));
#27413=CARTESIAN_POINT('Ctrl Pts',(171.051902333879,4.11133752964417,133.506852139491));
#27414=CARTESIAN_POINT('Ctrl Pts',(171.044411998117,4.18221560535061,133.395795066148));
#27415=CARTESIAN_POINT('Ctrl Pts',(171.036921662355,4.24843784895795,133.282254664139));
#27416=CARTESIAN_POINT('Ctrl Pts',(171.029147328236,4.31717092905886,133.164409343279));
#27417=CARTESIAN_POINT('Ctrl Pts',(171.021372994117,4.38110588169799,133.043515367071));
#27418=CARTESIAN_POINT('Ctrl Pts',(171.013598659998,4.4399604805969,132.920000944568));
#27419=CARTESIAN_POINT('Ctrl Pts',(171.005833907051,4.49874254646279,132.796638742552));
#27420=CARTESIAN_POINT('Ctrl Pts',(170.998069154104,4.55245654971177,132.670662869473));
#27421=CARTESIAN_POINT('Ctrl Pts',(170.990304401156,4.60086452782022,132.542528808261));
#27422=CARTESIAN_POINT('Ctrl Pts',(170.982547360271,4.64922442644237,132.414522011606));
#27423=CARTESIAN_POINT('Ctrl Pts',(170.974790319386,4.69228865022188,132.284361655934));
#27424=CARTESIAN_POINT('Ctrl Pts',(170.967033278501,4.72986616751987,132.152525703841));
#27425=CARTESIAN_POINT('Ctrl Pts',(170.959282087261,4.76741534731984,132.020789170265));
#27426=CARTESIAN_POINT('Ctrl Pts',(170.951530896021,4.79948594948081,131.887379929817));
#27427=CARTESIAN_POINT('Ctrl Pts',(170.943779704781,4.82593601017924,131.752793371194));
#27428=CARTESIAN_POINT('Ctrl Pts',(170.936031808004,4.85237482889622,131.61826401545));
#27429=CARTESIAN_POINT('Ctrl Pts',(170.928283911227,4.87319778221532,131.482558719594));
#27430=CARTESIAN_POINT('Ctrl Pts',(170.92053601445,4.88831353370598,131.346185182058));
#27431=CARTESIAN_POINT('Ctrl Pts',(170.912789738366,4.90342612330728,131.209840170926));
#27432=CARTESIAN_POINT('Ctrl Pts',(170.905043462282,4.91283384261687,131.072827584485));
#27433=CARTESIAN_POINT('Ctrl Pts',(170.897297186197,4.9164970261399,130.93566200544));
#27434=CARTESIAN_POINT('Ctrl Pts',(170.889550852932,4.92016023670372,130.798495413869));
#27435=CARTESIAN_POINT('Ctrl Pts',(170.881804519667,4.91807881642764,130.661176218265));
#27436=CARTESIAN_POINT('Ctrl Pts',(170.874058186401,4.91026521779664,130.524220378763));
#27437=CARTESIAN_POINT('Ctrl Pts',(170.866310118398,4.90244986936441,130.38723386895));
#27438=CARTESIAN_POINT('Ctrl Pts',(170.858562050395,4.88889981046437,130.250611267413));
#27439=CARTESIAN_POINT('Ctrl Pts',(170.850813982392,4.8696794569021,130.114864388769));
#27440=CARTESIAN_POINT('Ctrl Pts',(170.843057679651,4.85043867571933,129.978973236726));
#27441=CARTESIAN_POINT('Ctrl Pts',(170.835301376909,4.82551561627538,129.843960054527));
#27442=CARTESIAN_POINT('Ctrl Pts',(170.827545074167,4.79502613480021,129.71032797222));
#27443=CARTESIAN_POINT('Ctrl Pts',(170.819784631653,4.76452038017076,129.576624566447));
#27444=CARTESIAN_POINT('Ctrl Pts',(170.812024189139,4.72844238640119,129.444304106379));
#27445=CARTESIAN_POINT('Ctrl Pts',(170.804263746624,4.68695793210101,129.313854527268));
#27446=CARTESIAN_POINT('Ctrl Pts',(170.796490846359,4.64540688327195,129.183195538912));
#27447=CARTESIAN_POINT('Ctrl Pts',(170.788717946094,4.59843216469574,129.054413800578));
#27448=CARTESIAN_POINT('Ctrl Pts',(170.780945045828,4.54624807871649,128.927978068813));
#27449=CARTESIAN_POINT('Ctrl Pts',(170.773454710066,4.49596101570655,128.80613859437));
#27450=CARTESIAN_POINT('Ctrl Pts',(170.765964374304,4.44083688581637,128.686477801046));
#27451=CARTESIAN_POINT('Ctrl Pts',(170.758474038542,4.38110687021332,128.569391791325));
#27452=CARTESIAN_POINT('Ctrl Pts',(170.750699704423,4.31911217291391,128.447866429957));
#27453=CARTESIAN_POINT('Ctrl Pts',(170.742925370304,4.25195905043413,128.328729996429));
#27454=CARTESIAN_POINT('Ctrl Pts',(170.735151036185,4.17985521698085,128.212451393157));
#27455=CARTESIAN_POINT('Ctrl Pts',(170.727386283238,4.10784024505831,128.096316092871));
#27456=CARTESIAN_POINT('Ctrl Pts',(170.719621530291,4.03088690600835,127.983031944147));
#27457=CARTESIAN_POINT('Ctrl Pts',(170.711856777344,3.94924978596426,127.873045351246));
#27458=CARTESIAN_POINT('Ctrl Pts',(170.704099736459,3.86769374905841,127.763167998579));
#27459=CARTESIAN_POINT('Ctrl Pts',(170.696342695574,3.78146342035344,127.656581995887));
#27460=CARTESIAN_POINT('Ctrl Pts',(170.688585654689,3.69085766605104,127.553706413955));
#27461=CARTESIAN_POINT('Ctrl Pts',(170.680834463449,3.60032023825277,127.4509084113));
#27462=CARTESIAN_POINT('Ctrl Pts',(170.673083272209,3.50541420975416,127.351815552252));
#27463=CARTESIAN_POINT('Ctrl Pts',(170.665332080968,3.40647963018167,127.256815044686));
#27464=CARTESIAN_POINT('Ctrl Pts',(170.657584184191,3.3075871004449,127.161854914871));
#27465=CARTESIAN_POINT('Ctrl Pts',(170.649836287414,3.20466970656614,127.070983947312));
#27466=CARTESIAN_POINT('Ctrl Pts',(170.642088390637,3.09810522004097,126.984553409335));
#27467=CARTESIAN_POINT('Ctrl Pts',(170.634342114553,2.99156302450901,126.898140950763));
#27468=CARTESIAN_POINT('Ctrl Pts',(170.626595838469,2.88137555722152,126.816167320378));
#27469=CARTESIAN_POINT('Ctrl Pts',(170.618849562385,2.76795431101178,126.738944034404));
#27470=CARTESIAN_POINT('Ctrl Pts',(170.61110322912,2.65453222755217,126.661720178385));
#27471=CARTESIAN_POINT('Ctrl Pts',(170.603356895854,2.53787664070854,126.58924695678));
#27472=CARTESIAN_POINT('Ctrl Pts',(170.595610562589,2.41842837322653,126.521792782018));
#27473=CARTESIAN_POINT('Ctrl Pts',(170.587862494586,2.29895335613314,126.45432350136));
#27474=CARTESIAN_POINT('Ctrl Pts',(170.580114426583,2.17668475429278,126.391875696347));
#27475=CARTESIAN_POINT('Ctrl Pts',(170.57236635858,2.0520879901537,126.334671820439));
#27476=CARTESIAN_POINT('Ctrl Pts',(170.564610055838,1.9273588030912,126.27740714757));
#27477=CARTESIAN_POINT('Ctrl Pts',(170.556853753096,1.80029686672665,126.225397700479));
#27478=CARTESIAN_POINT('Ctrl Pts',(170.549097450355,1.67138810173988,126.178817960119));
#27479=CARTESIAN_POINT('Ctrl Pts',(170.54133700784,1.54241053426362,126.132213358749));
#27480=CARTESIAN_POINT('Ctrl Pts',(170.533576565326,1.41158454681163,126.091044355915));
#27481=CARTESIAN_POINT('Ctrl Pts',(170.525816122812,1.27941026051825,126.055435218301));
#27482=CARTESIAN_POINT('Ctrl Pts',(170.518043222547,1.14702379632676,126.019768917739));
#27483=CARTESIAN_POINT('Ctrl Pts',(170.510270322281,1.01328508976567,125.989680403631));
#27484=CARTESIAN_POINT('Ctrl Pts',(170.502497422016,0.878704354646793,125.965242751712));
#27485=CARTESIAN_POINT('Ctrl Pts',(170.495007086254,0.749015968238953,125.941693469995));
#27486=CARTESIAN_POINT('Ctrl Pts',(170.487516750492,0.61854601515919,125.92339138));
#27487=CARTESIAN_POINT('Ctrl Pts',(170.48002641473,0.487752706712771,125.910356085529));
#27488=CARTESIAN_POINT('Ctrl Pts',(170.472252080611,0.352000330221832,125.896826553907));
#27489=CARTESIAN_POINT('Ctrl Pts',(170.464477746492,0.21546957156963,125.888928225334));
#27490=CARTESIAN_POINT('Ctrl Pts',(170.456703412373,0.0786672062396304,
125.886739797173));
#27491=CARTESIAN_POINT('Ctrl Pts',(170.448938659426,-0.0579665624011073,
125.884554066054));
#27492=CARTESIAN_POINT('Ctrl Pts',(170.441173906479,-0.194870884542369,
125.888064240124));
#27493=CARTESIAN_POINT('Ctrl Pts',(170.433409153531,-0.331532577613189,
125.897297421266));
#27494=CARTESIAN_POINT('Ctrl Pts',(170.425652112646,-0.468058536364183,
125.906521431882));
#27495=CARTESIAN_POINT('Ctrl Pts',(170.417895071762,-0.604341958059236,
125.921457111628));
#27496=CARTESIAN_POINT('Ctrl Pts',(170.410138030877,-0.739868722095001,
125.942079533901));
#27497=CARTESIAN_POINT('Ctrl Pts',(170.402386839636,-0.875293284343255,
125.962686404645));
#27498=CARTESIAN_POINT('Ctrl Pts',(170.394635648396,-1.00996193972761,125.988971423506));
#27499=CARTESIAN_POINT('Ctrl Pts',(170.386884457156,-1.143365114166,126.020857792417));
#27500=CARTESIAN_POINT('Ctrl Pts',(170.379136560379,-1.27671158869719,126.052730608771));
#27501=CARTESIAN_POINT('Ctrl Pts',(170.371388663602,-1.40879327259354,126.090199949401));
#27502=CARTESIAN_POINT('Ctrl Pts',(170.363640766825,-1.53911043998262,126.133137853017));
#27503=CARTESIAN_POINT('Ctrl Pts',(170.355894490741,-1.66940034782977,126.176066774951));
#27504=CARTESIAN_POINT('Ctrl Pts',(170.348148214657,-1.79792610223434,126.22446186231));
#27505=CARTESIAN_POINT('Ctrl Pts',(170.340401938573,-1.92420319384619,126.27814529665));
#27506=CARTESIAN_POINT('Ctrl Pts',(170.332655605307,-2.0504812176065,126.331829127269));
#27507=CARTESIAN_POINT('Ctrl Pts',(170.324909272042,-2.17451018565046,126.390801229804));
#27508=CARTESIAN_POINT('Ctrl Pts',(170.317162938777,-2.29582599953964,126.454835811068));
#27509=CARTESIAN_POINT('Ctrl Pts',(170.309414870774,-2.4171689812639,126.518884732433));
#27510=CARTESIAN_POINT('Ctrl Pts',(170.301666802771,-2.53579725410604,126.587998206005));
#27511=CARTESIAN_POINT('Ctrl Pts',(170.293918734768,-2.65127208946793,126.661904900228));
#27512=CARTESIAN_POINT('Ctrl Pts',(170.286162432026,-2.76686965285929,126.735890143364));
#27513=CARTESIAN_POINT('Ctrl Pts',(170.278406129284,-2.87930675394613,126.814678572455));
#27514=CARTESIAN_POINT('Ctrl Pts',(170.270649826542,-2.98817394496498,126.897955679886));
#27515=CARTESIAN_POINT('Ctrl Pts',(170.262889384028,-3.097099241682,126.981277234817));
#27516=CARTESIAN_POINT('Ctrl Pts',(170.255128941514,-3.20245053155298,127.069091991604));
#27517=CARTESIAN_POINT('Ctrl Pts',(170.247368499,-3.30385293780894,127.161046353351));
#27518=CARTESIAN_POINT('Ctrl Pts',(170.239595598734,-3.40541812420926,127.253148328403));
#27519=CARTESIAN_POINT('Ctrl Pts',(170.231822698469,-3.5030214809247,127.349402913082));
#27520=CARTESIAN_POINT('Ctrl Pts',(170.224049798203,-3.59632574424345,127.449420349276));
#27521=CARTESIAN_POINT('Ctrl Pts',(170.216559462441,-3.686238162572,127.545801899737));
#27522=CARTESIAN_POINT('Ctrl Pts',(170.209069126679,-3.77215842577424,127.64567723967));
#27523=CARTESIAN_POINT('Ctrl Pts',(170.201578790917,-3.85382236621166,127.74867145926));
#27524=CARTESIAN_POINT('Ctrl Pts',(170.193812524806,-3.938494657719,127.855459798618));
#27525=CARTESIAN_POINT('Ctrl Pts',(170.186046258694,-4.01886496298055,127.965946739028));
#27526=CARTESIAN_POINT('Ctrl Pts',(170.178279992583,-4.09459191344809,128.079750530815));
#27527=CARTESIAN_POINT('Ctrl Pts',(170.170486299365,-4.17058629888614,128.193956228575));
#27528=CARTESIAN_POINT('Ctrl Pts',(170.162692606147,-4.24190416979371,128.31150198608));
#27529=CARTESIAN_POINT('Ctrl Pts',(170.154898912929,-4.30823965276746,128.431966435137));
#27530=CARTESIAN_POINT('Ctrl Pts',(170.147152164206,-4.37417557090397,128.551705279197));
#27531=CARTESIAN_POINT('Ctrl Pts',(170.139405415483,-4.43518874164617,128.674327418701));
#27532=CARTESIAN_POINT('Ctrl Pts',(170.131658666761,-4.49102105971179,128.799388571944));
#27533=CARTESIAN_POINT('Ctrl Pts',(170.123841501295,-4.54736088487774,128.925586511648));
#27534=CARTESIAN_POINT('Ctrl Pts',(170.116024335829,-4.59842496368119,129.054267699693));
#27535=CARTESIAN_POINT('Ctrl Pts',(170.108207170364,-4.64399504249936,129.184949271508));
#27536=CARTESIAN_POINT('Ctrl Pts',(170.100390004898,-4.68956512131752,129.315630843323));
#27537=CARTESIAN_POINT('Ctrl Pts',(170.092572839433,-4.72964103274668,129.448312422701));
#27538=CARTESIAN_POINT('Ctrl Pts',(170.084755673967,-4.76405452823406,129.582490119308));
#27539=CARTESIAN_POINT('Ctrl Pts',(171.834603948179,-4.76405452823406,129.582490119308));
#27540=CARTESIAN_POINT('Ctrl Pts',(171.825910999201,-4.80206436672034,129.730689902686));
#27541=CARTESIAN_POINT('Ctrl Pts',(171.817218050222,-4.83319925274758,129.880837722785));
#27542=CARTESIAN_POINT('Ctrl Pts',(171.808525101244,-4.85727658297744,130.032319647825));
#27543=CARTESIAN_POINT('Ctrl Pts',(171.799878869647,-4.88122451755313,130.182987483321));
#27544=CARTESIAN_POINT('Ctrl Pts',(171.79123263805,-4.8981904550706,130.334974919894));
#27545=CARTESIAN_POINT('Ctrl Pts',(171.782586406452,-4.90804272339544,130.487659357977));
#27546=CARTESIAN_POINT('Ctrl Pts',(171.776677416316,-4.9147759407161,130.592006648287));
#27547=CARTESIAN_POINT('Ctrl Pts',(171.770768426181,-4.91818764042097,130.696679096119));
#27548=CARTESIAN_POINT('Ctrl Pts',(171.764859436045,-4.91824915272082,130.801473705556));
#27549=CARTESIAN_POINT('',(172.110140563973,-4.91824950728406,130.802159118055));
#27550=CARTESIAN_POINT('Ctrl Pts',(172.180231140679,-4.76405452823404,129.582490119308));
#27551=CARTESIAN_POINT('Ctrl Pts',(172.172465945589,-4.79809305117586,129.715205803652));
#27552=CARTESIAN_POINT('Ctrl Pts',(172.1647007505,-4.82654693481475,129.849209433246));
#27553=CARTESIAN_POINT('Ctrl Pts',(172.156935555411,-4.84934811999046,129.9839912656));
#27554=CARTESIAN_POINT('Ctrl Pts',(172.149159740024,-4.87218048987978,130.118957436304));
#27555=CARTESIAN_POINT('Ctrl Pts',(172.141383924637,-4.88934468447975,130.254703547973));
#27556=CARTESIAN_POINT('Ctrl Pts',(172.133608109249,-4.90082457327812,130.390716368901));
#27557=CARTESIAN_POINT('Ctrl Pts',(172.132779793315,-4.90204746429799,130.405205085667));
#27558=CARTESIAN_POINT('Ctrl Pts',(172.131951477382,-4.90320590135478,130.41969683088));
#27559=CARTESIAN_POINT('Ctrl Pts',(172.131123161448,-4.90429989972426,130.434190986093));
#27560=CARTESIAN_POINT('Ctrl Pts',(172.124128962302,-4.91353748909132,130.556577872414));
#27561=CARTESIAN_POINT('Ctrl Pts',(172.117134763155,-4.91819451989084,130.679314828552));
#27562=CARTESIAN_POINT('Ctrl Pts',(172.110140564008,-4.91824950728378,130.802159117434));
#27563=CARTESIAN_POINT('Ctrl Pts',(172.110140563973,-4.91824950728406,130.802159118055));
#27564=CARTESIAN_POINT('Ctrl Pts',(172.102450296272,-4.91830996705132,130.937228973409));
#27565=CARTESIAN_POINT('Ctrl Pts',(172.094760028571,-4.91280209186903,131.072526111654));
#27566=CARTESIAN_POINT('Ctrl Pts',(172.087069760869,-4.90169598927124,131.207547288058));
#27567=CARTESIAN_POINT('Ctrl Pts',(172.0793884731,-4.89060285527838,131.342410800125));
#27568=CARTESIAN_POINT('Ctrl Pts',(172.071707185331,-4.87392452826556,131.476998596401));
#27569=CARTESIAN_POINT('Ctrl Pts',(172.064025897562,-4.8516831047687,131.610805974303));
#27570=CARTESIAN_POINT('Ctrl Pts',(172.056351646764,-4.82946205705517,131.744490768767));
#27571=CARTESIAN_POINT('Ctrl Pts',(172.048677395965,-4.80168811669321,131.877396174964));
#27572=CARTESIAN_POINT('Ctrl Pts',(172.041003145167,-4.76843526592711,132.009021639249));
#27573=CARTESIAN_POINT('Ctrl Pts',(172.03315616152,-4.734433956477,132.143609743414));
#27574=CARTESIAN_POINT('Ctrl Pts',(172.025309177873,-4.69470417974674,132.276859175735));
#27575=CARTESIAN_POINT('Ctrl Pts',(172.017462194226,-4.64938062361568,132.408244303887));
#27576=CARTESIAN_POINT('Ctrl Pts',(172.009795351173,-4.60509754529266,132.536613267338));
#27577=CARTESIAN_POINT('Ctrl Pts',(172.00212850812,-4.55547487742502,132.663202199823));
#27578=CARTESIAN_POINT('Ctrl Pts',(171.994461665067,-4.50068881193671,132.787535667986));
#27579=CARTESIAN_POINT('Ctrl Pts',(171.986795591432,-4.44590824458666,132.911856658476));
#27580=CARTESIAN_POINT('Ctrl Pts',(171.979129517797,-4.38596547125795,133.033922268786));
#27581=CARTESIAN_POINT('Ctrl Pts',(171.971463444162,-4.3210846192262,133.153277554366));
#27582=CARTESIAN_POINT('Ctrl Pts',(171.963796395263,-4.25619551317209,133.272648024106));
#27583=CARTESIAN_POINT('Ctrl Pts',(171.956129346364,-4.18636727026433,133.389307132091));
#27584=CARTESIAN_POINT('Ctrl Pts',(171.948462297465,-4.11186945341913,133.502825488662));
#27585=CARTESIAN_POINT('Ctrl Pts',(171.94048006748,-4.03430914105516,133.621010417665));
#27586=CARTESIAN_POINT('Ctrl Pts',(171.932497837494,-3.95168740455701,133.73579046403));
#27587=CARTESIAN_POINT('Ctrl Pts',(171.924515607508,-3.86435680919402,133.846716532599));
#27588=CARTESIAN_POINT('Ctrl Pts',(171.916837196073,-3.78035017906484,133.953420548245));
#27589=CARTESIAN_POINT('Ctrl Pts',(171.909158784638,-3.6919868793546,134.056558317157));
#27590=CARTESIAN_POINT('Ctrl Pts',(171.901480373204,-3.59961974551205,134.155766404728));
#27591=CARTESIAN_POINT('Ctrl Pts',(171.893796744521,-3.50718985100099,134.255041901187));
#27592=CARTESIAN_POINT('Ctrl Pts',(171.886113115839,-3.4107509900769,134.350382121039));
#27593=CARTESIAN_POINT('Ctrl Pts',(171.878429487156,-3.31069053982214,134.441462652433));
#27594=CARTESIAN_POINT('Ctrl Pts',(171.870735374791,-3.21049356527748,134.532667455753));
#27595=CARTESIAN_POINT('Ctrl Pts',(171.863041262427,-3.10666544848945,134.619600721057));
#27596=CARTESIAN_POINT('Ctrl Pts',(171.855347150062,-2.99962419783545,134.701980113394));
#27597=CARTESIAN_POINT('Ctrl Pts',(171.854456612586,-2.98723495257262,134.711514928151));
#27598=CARTESIAN_POINT('Ctrl Pts',(171.85356607511,-2.97480269154766,134.720988787297));
#27599=CARTESIAN_POINT('Ctrl Pts',(171.852675537635,-2.96232808469272,134.730401292488));
#27600=CARTESIAN_POINT('Ctrl Pts',(171.844901203515,-2.8534255799377,134.812571849301));
#27601=CARTESIAN_POINT('Ctrl Pts',(171.837126869396,-2.74092905759722,134.890337935185));
#27602=CARTESIAN_POINT('Ctrl Pts',(171.829352535277,-2.62523039615684,134.963368724025));
#27603=CARTESIAN_POINT('Ctrl Pts',(171.82158778233,-2.50967432297672,135.036309508945));
#27604=CARTESIAN_POINT('Ctrl Pts',(171.813823029383,-2.39092429019464,135.104526401701));
#27605=CARTESIAN_POINT('Ctrl Pts',(171.806058276436,-2.26940448721128,135.167729308833));
#27606=CARTESIAN_POINT('Ctrl Pts',(171.798301235551,-2.14800537940892,135.230869441946));
#27607=CARTESIAN_POINT('Ctrl Pts',(171.790544194666,-2.02384232058094,135.289005320549));
#27608=CARTESIAN_POINT('Ctrl Pts',(171.782787153781,-1.89736736539807,135.341890798537));
#27609=CARTESIAN_POINT('Ctrl Pts',(171.775035962541,-1.77098778596248,135.394736395174));
#27610=CARTESIAN_POINT('Ctrl Pts',(171.767284771301,-1.64230013958309,135.442339321861));
#27611=CARTESIAN_POINT('Ctrl Pts',(171.759533580061,-1.51177958039806,135.484500098692));
#27612=CARTESIAN_POINT('Ctrl Pts',(171.751785683284,-1.38131449593287,135.526642956067));
#27613=CARTESIAN_POINT('Ctrl Pts',(171.744037786506,-1.24901841936518,135.563348144159));
#27614=CARTESIAN_POINT('Ctrl Pts',(171.736289889729,-1.1153847079433,135.59446500221));
#27615=CARTESIAN_POINT('Ctrl Pts',(171.728543613645,-0.981778949813042,
135.625575351285));
#27616=CARTESIAN_POINT('Ctrl Pts',(171.720797337561,-0.846836493912149,
135.651099606832));
#27617=CARTESIAN_POINT('Ctrl Pts',(171.713051061477,-0.711063636366915,
135.670937604272));
#27618=CARTESIAN_POINT('Ctrl Pts',(171.705304728212,-0.575289776577245,
135.690775748152));
#27619=CARTESIAN_POINT('Ctrl Pts',(171.697558394946,-0.438685889769167,
135.704927493644));
#27620=CARTESIAN_POINT('Ctrl Pts',(171.689812061681,-0.301765795447225,
135.713344266673));
#27621=CARTESIAN_POINT('Ctrl Pts',(171.682063993678,-0.164815038819777,
135.721762924579));
#27622=CARTESIAN_POINT('Ctrl Pts',(171.674315925675,-0.0275483239237374,
135.724444030416));
#27623=CARTESIAN_POINT('Ctrl Pts',(171.666567857672,0.109518508915834,135.721391099341));
#27624=CARTESIAN_POINT('Ctrl Pts',(171.65881155493,0.246731018016651,135.718334923575));
#27625=CARTESIAN_POINT('Ctrl Pts',(171.651055252188,0.383742829203628,135.70953254579));
#27626=CARTESIAN_POINT('Ctrl Pts',(171.643298949447,0.520040650371349,135.695039587245));
#27627=CARTESIAN_POINT('Ctrl Pts',(171.635538506932,0.656411217790121,135.680538893372));
#27628=CARTESIAN_POINT('Ctrl Pts',(171.627778064418,0.792066649346082,135.660341624338));
#27629=CARTESIAN_POINT('Ctrl Pts',(171.620017621904,0.926502845105625,135.634554768996));
#27630=CARTESIAN_POINT('Ctrl Pts',(171.612244721639,1.06115484978138,135.608726518305));
#27631=CARTESIAN_POINT('Ctrl Pts',(171.604471821373,1.19458332673509,135.5772908403));
#27632=CARTESIAN_POINT('Ctrl Pts',(171.596698921108,1.32629748942126,135.540405173105));
#27633=CARTESIAN_POINT('Ctrl Pts',(171.589208585346,1.45322351052502,135.504860392824));
#27634=CARTESIAN_POINT('Ctrl Pts',(171.581718249584,1.57855739969979,135.464255080619));
#27635=CARTESIAN_POINT('Ctrl Pts',(171.574227913822,1.70187852239886,135.418772016379));
#27636=CARTESIAN_POINT('Ctrl Pts',(171.566453579703,1.82987540294846,135.371564447935));
#27637=CARTESIAN_POINT('Ctrl Pts',(171.558679245584,1.95610933165808,135.318952406585));
#27638=CARTESIAN_POINT('Ctrl Pts',(171.550904911465,2.08009015525429,135.261086771203));
#27639=CARTESIAN_POINT('Ctrl Pts',(171.543140158518,2.20391818356556,135.203292450046));
#27640=CARTESIAN_POINT('Ctrl Pts',(171.535375405571,2.3254982807933,135.140257581115));
#27641=CARTESIAN_POINT('Ctrl Pts',(171.527610652623,2.44435709836126,135.072182244367));
#27642=CARTESIAN_POINT('Ctrl Pts',(171.519853611738,2.56309786367635,135.004174521003));
#27643=CARTESIAN_POINT('Ctrl Pts',(171.512096570853,2.67912239098659,134.931136485563));
#27644=CARTESIAN_POINT('Ctrl Pts',(171.504339529968,2.79197924401099,134.853315416463));
#27645=CARTESIAN_POINT('Ctrl Pts',(171.496588338728,2.90475099080486,134.775553032836));
#27646=CARTESIAN_POINT('Ctrl Pts',(171.488837147488,3.01435949745014,134.693015015954));
#27647=CARTESIAN_POINT('Ctrl Pts',(171.481085956248,3.12038010343401,134.605993302689));
#27648=CARTESIAN_POINT('Ctrl Pts',(171.473338059471,3.22635564783182,134.519008575973));
#27649=CARTESIAN_POINT('Ctrl Pts',(171.465590162694,3.32874602301495,134.427544190675));
#27650=CARTESIAN_POINT('Ctrl Pts',(171.457842265917,3.42715780217672,134.3319337864));
#27651=CARTESIAN_POINT('Ctrl Pts',(171.450095989833,3.52554899571583,134.236343381761));
#27652=CARTESIAN_POINT('Ctrl Pts',(171.442349713749,3.61996296835883,134.13660895543));
#27653=CARTESIAN_POINT('Ctrl Pts',(171.434603437664,3.71004178338641,134.033102327277));
#27654=CARTESIAN_POINT('Ctrl Pts',(171.426857104399,3.80012126335536,133.929594935061));
#27655=CARTESIAN_POINT('Ctrl Pts',(171.419110771134,3.88586526519137,133.82231558038));
#27656=CARTESIAN_POINT('Ctrl Pts',(171.411364437868,3.96695519015602,133.711670298662));
#27657=CARTESIAN_POINT('Ctrl Pts',(171.403616369865,4.04806327464702,133.6010002387));
#27658=CARTESIAN_POINT('Ctrl Pts',(171.395868301862,4.12451497724753,133.486963067057));
#27659=CARTESIAN_POINT('Ctrl Pts',(171.388120233859,4.19603443106404,133.369994674836));
#27660=CARTESIAN_POINT('Ctrl Pts',(171.380363931118,4.2676298966072,133.252901967217));
#27661=CARTESIAN_POINT('Ctrl Pts',(171.372607628376,4.3342824375269,133.132872149886));
#27662=CARTESIAN_POINT('Ctrl Pts',(171.364851325634,4.39576140264166,133.010367134679));
#27663=CARTESIAN_POINT('Ctrl Pts',(171.35709088312,4.45727318093121,132.887796734857));
#27664=CARTESIAN_POINT('Ctrl Pts',(171.349330440606,4.51360572080102,132.762748861069));
#27665=CARTESIAN_POINT('Ctrl Pts',(171.341569998091,4.56457655667485,132.635705456954));
#27666=CARTESIAN_POINT('Ctrl Pts',(171.333797097826,4.61562921545938,132.508458111489));
#27667=CARTESIAN_POINT('Ctrl Pts',(171.326024197561,4.661302840214,132.379209203116));
#27668=CARTESIAN_POINT('Ctrl Pts',(171.318251297295,4.7014646059764,132.248456743609));
#27669=CARTESIAN_POINT('Ctrl Pts',(171.310760961533,4.74016639039183,132.12245746535));
#27670=CARTESIAN_POINT('Ctrl Pts',(171.303270625771,4.77375001978124,131.99506235166));
#27671=CARTESIAN_POINT('Ctrl Pts',(171.295780290009,4.80214190879403,131.866724091291));
#27672=CARTESIAN_POINT('Ctrl Pts',(171.28800595589,4.83161028490836,131.733519846771));
#27673=CARTESIAN_POINT('Ctrl Pts',(171.280231621771,4.85557880637322,131.598877573947));
#27674=CARTESIAN_POINT('Ctrl Pts',(171.272457287652,4.8739094720403,131.463291206366));
#27675=CARTESIAN_POINT('Ctrl Pts',(171.264692534705,4.89221754680019,131.327871936865));
#27676=CARTESIAN_POINT('Ctrl Pts',(171.256927781758,4.90490153863927,131.19151127137));
#27677=CARTESIAN_POINT('Ctrl Pts',(171.249163028811,4.91187392402293,131.054715599549));
#27678=CARTESIAN_POINT('Ctrl Pts',(171.241405987926,4.91883938433513,130.918055795117));
#27679=CARTESIAN_POINT('Ctrl Pts',(171.233648947041,4.92010450764289,130.780962232097));
#27680=CARTESIAN_POINT('Ctrl Pts',(171.225891906156,4.91563332394328,130.643948376642));
#27681=CARTESIAN_POINT('Ctrl Pts',(171.218140714916,4.91116551199808,130.507037844401));
#27682=CARTESIAN_POINT('Ctrl Pts',(171.210389523676,4.90097001597565,130.370207289259));
#27683=CARTESIAN_POINT('Ctrl Pts',(171.202638332436,4.88506291125395,130.233971789142));
#27684=CARTESIAN_POINT('Ctrl Pts',(171.194890435658,4.86916256747607,130.097794192747));
#27685=CARTESIAN_POINT('Ctrl Pts',(171.187142538881,4.84755548852937,129.962211535864));
#27686=CARTESIAN_POINT('Ctrl Pts',(171.179394642104,4.82030971806418,129.827735159964));
#27687=CARTESIAN_POINT('Ctrl Pts',(171.17164836602,4.79306964682682,129.693286913623));
#27688=CARTESIAN_POINT('Ctrl Pts',(171.163902089936,4.76019330773209,129.559944870916));
#27689=CARTESIAN_POINT('Ctrl Pts',(171.156155813852,4.72180004982653,129.428211151862));
#27690=CARTESIAN_POINT('Ctrl Pts',(171.148409480587,4.68340650851073,129.29647646038));
#27691=CARTESIAN_POINT('Ctrl Pts',(171.140663147321,4.63949607651496,129.16635049159));
#27692=CARTESIAN_POINT('Ctrl Pts',(171.132916814056,4.59023815254312,129.038320763702));
#27693=CARTESIAN_POINT('Ctrl Pts',(171.125168746053,4.54096919760087,128.910262364443));
#27694=CARTESIAN_POINT('Ctrl Pts',(171.11742067805,4.48635050808955,128.784301505036));
#27695=CARTESIAN_POINT('Ctrl Pts',(171.109672610047,4.42659969874548,128.660905889897));
#27696=CARTESIAN_POINT('Ctrl Pts',(171.101916307306,4.36678538552995,128.53737912843));
#27697=CARTESIAN_POINT('Ctrl Pts',(171.094160004564,4.30182822723501,128.416423409898));
#27698=CARTESIAN_POINT('Ctrl Pts',(171.086403701822,4.23199217077095,128.298482462301));
#27699=CARTESIAN_POINT('Ctrl Pts',(171.078643259308,4.16211884070077,128.18047856607));
#27700=CARTESIAN_POINT('Ctrl Pts',(171.070882816793,4.0873616367418,128.06549297461));
#27701=CARTESIAN_POINT('Ctrl Pts',(171.063122374279,4.00802740462579,127.953939703689));
#27702=CARTESIAN_POINT('Ctrl Pts',(171.055349474014,3.92856581815739,127.842207357554));
#27703=CARTESIAN_POINT('Ctrl Pts',(171.047576573749,3.84451276084427,127.733918651447));
#27704=CARTESIAN_POINT('Ctrl Pts',(171.039803673483,3.75621542895881,127.629454522301));
#27705=CARTESIAN_POINT('Ctrl Pts',(171.032313337721,3.67112792749383,127.528787927377));
#27706=CARTESIAN_POINT('Ctrl Pts',(171.024823001959,3.58209958233881,127.431672898084));
#27707=CARTESIAN_POINT('Ctrl Pts',(171.017332666197,3.48947147868166,127.33841603319));
#27708=CARTESIAN_POINT('Ctrl Pts',(171.009558332078,3.39333135232187,127.241623305919));
#27709=CARTESIAN_POINT('Ctrl Pts',(171.001783997958,3.29300856624316,127.148680472706));
#27710=CARTESIAN_POINT('Ctrl Pts',(170.994009663839,3.18884408773586,127.059970620969));
#27711=CARTESIAN_POINT('Ctrl Pts',(170.986244910892,3.08480798263913,126.971370096198));
#27712=CARTESIAN_POINT('Ctrl Pts',(170.978480157945,2.97693990023683,126.88699242414));
#27713=CARTESIAN_POINT('Ctrl Pts',(170.970715404998,2.86561857188853,126.807184956809));
#27714=CARTESIAN_POINT('Ctrl Pts',(170.962958364113,2.75440780945225,126.727456755379));
#27715=CARTESIAN_POINT('Ctrl Pts',(170.955201323228,2.63975094224204,126.652289951801));
#27716=CARTESIAN_POINT('Ctrl Pts',(170.947444282343,2.5220605212085,126.581992349655));
#27717=CARTESIAN_POINT('Ctrl Pts',(170.939693091103,2.40445885143709,126.511747759477));
#27718=CARTESIAN_POINT('Ctrl Pts',(170.931941899863,2.28382851551378,126.446365261706));
#27719=CARTESIAN_POINT('Ctrl Pts',(170.924190708623,2.16061155222033,126.38610974387));
#27720=CARTESIAN_POINT('Ctrl Pts',(170.916442811845,2.03744695942353,126.325879836238));
#27721=CARTESIAN_POINT('Ctrl Pts',(170.908694915068,1.91169827633441,126.270772745864));
#27722=CARTESIAN_POINT('Ctrl Pts',(170.900947018291,1.78383248826975,126.221007618255));
#27723=CARTESIAN_POINT('Ctrl Pts',(170.893200742207,1.65599344697153,126.171252900438));
#27724=CARTESIAN_POINT('Ctrl Pts',(170.885454466123,1.52603854566862,126.126838064481));
#27725=CARTESIAN_POINT('Ctrl Pts',(170.877708190039,1.39445474323015,126.087934106787));
#27726=CARTESIAN_POINT('Ctrl Pts',(170.869961856774,1.26286996947003,126.049029861912));
#27727=CARTESIAN_POINT('Ctrl Pts',(170.862215523508,1.12965664550267,126.015636687324));
#27728=CARTESIAN_POINT('Ctrl Pts',(170.854469190243,0.995316498341022,125.987875578595));
#27729=CARTESIAN_POINT('Ctrl Pts',(170.84672112224,0.860946266634589,125.960108252958));
#27730=CARTESIAN_POINT('Ctrl Pts',(170.838973054237,0.725449092400377,125.937975582051));
#27731=CARTESIAN_POINT('Ctrl Pts',(170.831224986234,0.589336094692924,125.921547286095));
#27732=CARTESIAN_POINT('Ctrl Pts',(170.823468683492,0.453078434471974,125.905101529951));
#27733=CARTESIAN_POINT('Ctrl Pts',(170.81571238075,0.316204032101677,125.894372306533));
#27734=CARTESIAN_POINT('Ctrl Pts',(170.807956078008,0.179228878268098,125.889377395652));
#27735=CARTESIAN_POINT('Ctrl Pts',(170.800195635494,0.0421806166707686,
125.884379818837));
#27736=CARTESIAN_POINT('Ctrl Pts',(170.79243519298,-0.0949681127710925,
125.885122650899));
#27737=CARTESIAN_POINT('Ctrl Pts',(170.784674750466,-0.231703129255,125.891571519468));
#27738=CARTESIAN_POINT('Ctrl Pts',(170.7769018502,-0.368657644926318,125.898030740332));
#27739=CARTESIAN_POINT('Ctrl Pts',(170.769128949935,-0.505196730856685,
125.910214267207));
#27740=CARTESIAN_POINT('Ctrl Pts',(170.761356049669,-0.640812225951854,
125.928035899751));
#27741=CARTESIAN_POINT('Ctrl Pts',(170.753865713907,-0.771497756204666,
125.945209671062));
#27742=CARTESIAN_POINT('Ctrl Pts',(170.746375378145,-0.901325375981167,
125.967618693755));
#27743=CARTESIAN_POINT('Ctrl Pts',(170.738885042383,-1.02985277017972,125.995141727325));
#27744=CARTESIAN_POINT('Ctrl Pts',(170.731110708264,-1.16325331959507,126.023708305078));
#27745=CARTESIAN_POINT('Ctrl Pts',(170.723336374145,-1.2956756738514,126.057874834688));
#27746=CARTESIAN_POINT('Ctrl Pts',(170.715562040026,-1.42661322950235,126.097561518825));
#27747=CARTESIAN_POINT('Ctrl Pts',(170.707797287079,-1.55738941631831,126.137199292671));
#27748=CARTESIAN_POINT('Ctrl Pts',(170.700032534132,-1.68668407488329,126.182343572593));
#27749=CARTESIAN_POINT('Ctrl Pts',(170.692267781185,-1.81400025456092,126.232863473418));
#27750=CARTESIAN_POINT('Ctrl Pts',(170.6845107403,-1.94118998201404,126.283333197166));
#27751=CARTESIAN_POINT('Ctrl Pts',(170.676753699415,-2.06640478007488,126.339167773415));
#27752=CARTESIAN_POINT('Ctrl Pts',(170.66899665853,-2.1891626910087,126.400186486722));
#27753=CARTESIAN_POINT('Ctrl Pts',(170.66124546729,-2.31182802924725,126.461159185342));
#27754=CARTESIAN_POINT('Ctrl Pts',(170.65349427605,-2.43203981947728,126.527308066281));
#27755=CARTESIAN_POINT('Ctrl Pts',(170.645743084809,-2.54933627155889,126.598404407973));
#27756=CARTESIAN_POINT('Ctrl Pts',(170.637995188032,-2.66658286951899,126.669470531822));
#27757=CARTESIAN_POINT('Ctrl Pts',(170.630247291255,-2.78091626015609,126.745479731881));
#27758=CARTESIAN_POINT('Ctrl Pts',(170.622499394478,-2.89189965317959,126.826157573673));
#27759=CARTESIAN_POINT('Ctrl Pts',(170.614753118394,-3.0028598308699,126.9068185394));
#27760=CARTESIAN_POINT('Ctrl Pts',(170.60700684231,-3.11047108873344,126.992145974653));
#27761=CARTESIAN_POINT('Ctrl Pts',(170.599260566226,-3.21432634948992,127.081822614876));
#27762=CARTESIAN_POINT('Ctrl Pts',(170.591514232961,-3.31818237688276,127.171499917071));
#27763=CARTESIAN_POINT('Ctrl Pts',(170.583767899695,-3.41828205592868,127.265526232784));
#27764=CARTESIAN_POINT('Ctrl Pts',(170.57602156643,-3.51425239391991,127.363544845932));
#27765=CARTESIAN_POINT('Ctrl Pts',(170.568273498427,-3.6102442238021,127.461585409667));
#27766=CARTESIAN_POINT('Ctrl Pts',(170.560525430424,-3.70210459904195,127.563619770583));
#27767=CARTESIAN_POINT('Ctrl Pts',(170.552777362421,-3.78949858970825,127.669255595226));
#27768=CARTESIAN_POINT('Ctrl Pts',(170.545021059679,-3.87698546374816,127.775003690882));
#27769=CARTESIAN_POINT('Ctrl Pts',(170.537264756937,-3.95999622110164,127.884360594747));
#27770=CARTESIAN_POINT('Ctrl Pts',(170.529508454195,-4.0382369975398,127.996901799667));
#27771=CARTESIAN_POINT('Ctrl Pts',(170.521748011681,-4.11651953343623,128.109503071216));
#27772=CARTESIAN_POINT('Ctrl Pts',(170.513987569167,-4.19002680609195,128.225291700424));
#27773=CARTESIAN_POINT('Ctrl Pts',(170.506227126653,-4.25850980667207,128.343816513312));
#27774=CARTESIAN_POINT('Ctrl Pts',(170.498454226387,-4.32710274224426,128.462531592752));
#27775=CARTESIAN_POINT('Ctrl Pts',(170.490681326122,-4.39065510712692,128.583991286608));
#27776=CARTESIAN_POINT('Ctrl Pts',(170.482908425857,-4.44896475062447,128.70772147117));
#27777=CARTESIAN_POINT('Ctrl Pts',(170.475418090095,-4.50515469170763,128.826953751865));
#27778=CARTESIAN_POINT('Ctrl Pts',(170.467927754333,-4.55647634596472,128.948294029428));
#27779=CARTESIAN_POINT('Ctrl Pts',(170.460437418571,-4.60279263435049,129.071304638185));
#27780=CARTESIAN_POINT('Ctrl Pts',(170.45151081296,-4.65799005846015,129.217902497775));
#27781=CARTESIAN_POINT('Ctrl Pts',(170.442584207349,-4.70622458911788,129.367257882038));
#27782=CARTESIAN_POINT('Ctrl Pts',(170.433657601738,-4.74724902999245,129.518744146866));
#27783=CARTESIAN_POINT('Ctrl Pts',(170.432407909952,-4.75299230005541,129.539951663926));
#27784=CARTESIAN_POINT('Ctrl Pts',(170.431158218167,-4.75859433443983,129.561200906575));
#27785=CARTESIAN_POINT('Ctrl Pts',(170.429908526381,-4.76405452823404,129.582490119308));
#27786=CARTESIAN_POINT('Origin',(213.235140564004,0.,130.804360617566));
#27787=CARTESIAN_POINT('',(168.33498954974,-4.76405452823405,129.582490119308));
#27788=CARTESIAN_POINT('',(168.68000091015,-4.76405452823405,129.582490119308));
#27789=CARTESIAN_POINT('',(213.235140564004,-4.76405452823405,129.582490119308));
#27790=CARTESIAN_POINT('',(170.01485943594,-4.91824845497615,130.808259030672));
#27791=CARTESIAN_POINT('Ctrl Pts',(170.01485943594,-4.91824845497615,130.808259030672));
#27792=CARTESIAN_POINT('Ctrl Pts',(170.005798405087,-4.91812126027409,130.968728208735));
#27793=CARTESIAN_POINT('Ctrl Pts',(169.996737374234,-4.91013668640864,131.128867560345));
#27794=CARTESIAN_POINT('Ctrl Pts',(169.987676343381,-4.89441470293228,131.287980073565));
#27795=CARTESIAN_POINT('Ctrl Pts',(169.978558931458,-4.87859489148667,131.448082643419));
#27796=CARTESIAN_POINT('Ctrl Pts',(169.969441519536,-4.85494118831579,131.607145469039));
#27797=CARTESIAN_POINT('Ctrl Pts',(169.960324107613,-4.82362485110961,131.764478505254));
#27798=CARTESIAN_POINT('Ctrl Pts',(169.951141754702,-4.79208545566063,131.922932184357));
#27799=CARTESIAN_POINT('Ctrl Pts',(169.941959401791,-4.75277395392615,132.079631260207));
#27800=CARTESIAN_POINT('Ctrl Pts',(169.93277704888,-4.70591350270164,132.233892417699));
#27801=CARTESIAN_POINT('Ctrl Pts',(169.929561754955,-4.689504840823,132.287908525272));
#27802=CARTESIAN_POINT('Ctrl Pts',(169.926346461029,-4.67217101099181,132.34162591278));
#27803=CARTESIAN_POINT('Ctrl Pts',(169.923131167104,-4.65392295427785,132.395015890762));
#27804=CARTESIAN_POINT('Ctrl Pts',(169.915356832985,-4.60980055265348,132.524108762849));
#27805=CARTESIAN_POINT('Ctrl Pts',(169.907582498866,-4.56023292849578,132.651568883231));
#27806=CARTESIAN_POINT('Ctrl Pts',(169.899808164747,-4.50535915490091,132.776902619109));
#27807=CARTESIAN_POINT('Ctrl Pts',(169.8920434118,-4.45055300832781,132.902081892359));
#27808=CARTESIAN_POINT('Ctrl Pts',(169.884278658853,-4.39045387898229,133.02513964057));
#27809=CARTESIAN_POINT('Ctrl Pts',(169.876513905906,-4.325250430141,133.145597850113));
#27810=CARTESIAN_POINT('Ctrl Pts',(169.868756865021,-4.26011174228435,133.265936418864));
#27811=CARTESIAN_POINT('Ctrl Pts',(169.860999824136,-4.1898790087351,133.383680245439));
#27812=CARTESIAN_POINT('Ctrl Pts',(169.853242783251,-4.11478860347228,133.49837208956));
#27813=CARTESIAN_POINT('Ctrl Pts',(169.84549159201,-4.03975482446804,133.612977443669));
#27814=CARTESIAN_POINT('Ctrl Pts',(169.83774040077,-3.95987087843147,133.724535070595));
#27815=CARTESIAN_POINT('Ctrl Pts',(169.82998920953,-3.87541842748207,133.832613426437));
#27816=CARTESIAN_POINT('Ctrl Pts',(169.822241312753,-3.79100187107726,133.940645846094));
#27817=CARTESIAN_POINT('Ctrl Pts',(169.814493415976,-3.70202091194556,134.04520162843));
#27818=CARTESIAN_POINT('Ctrl Pts',(169.806745519199,-3.60879965245402,134.145879453507));
#27819=CARTESIAN_POINT('Ctrl Pts',(169.798999243115,-3.51559789284029,134.246536218953));
#27820=CARTESIAN_POINT('Ctrl Pts',(169.791252967031,-3.41815786257564,134.343316353938));
#27821=CARTESIAN_POINT('Ctrl Pts',(169.783506690946,-3.31684268495997,134.435853102169));
#27822=CARTESIAN_POINT('Ctrl Pts',(169.775760357681,-3.21552675945878,134.528390533485));
#27823=CARTESIAN_POINT('Ctrl Pts',(169.768014024416,-3.11033591820378,134.616684251877));
#27824=CARTESIAN_POINT('Ctrl Pts',(169.76026769115,-3.00166843420253,134.700406006626));
#27825=CARTESIAN_POINT('Ctrl Pts',(169.752519623147,-2.89297661487175,134.78414651028));
#27826=CARTESIAN_POINT('Ctrl Pts',(169.744771555144,-2.78080691317856,134.863312774364));
#27827=CARTESIAN_POINT('Ctrl Pts',(169.737023487141,-2.66558847465607,134.93761855124));
#27828=CARTESIAN_POINT('Ctrl Pts',(169.729267184399,-2.55024758060592,135.012003301181));
#27829=CARTESIAN_POINT('Ctrl Pts',(169.721510881658,-2.43185180609838,135.081517032473));
#27830=CARTESIAN_POINT('Ctrl Pts',(169.713754578916,-2.31085739495577,135.145918075746));
#27831=CARTESIAN_POINT('Ctrl Pts',(169.705994136401,-2.18979840545274,135.210353491795));
#27832=CARTESIAN_POINT('Ctrl Pts',(169.698233693887,-2.06613836799405,135.269670613461));
#27833=CARTESIAN_POINT('Ctrl Pts',(169.690473251373,-1.94035470875989,135.323675462395));
#27834=CARTESIAN_POINT('Ctrl Pts',(169.682700351108,-1.81436913042947,135.377767004707));
#27835=CARTESIAN_POINT('Ctrl Pts',(169.674927450842,-1.68625348360705,135.426529094009));
#27836=CARTESIAN_POINT('Ctrl Pts',(169.667154550577,-1.55650244921759,135.469816992679));
#27837=CARTESIAN_POINT('Ctrl Pts',(169.659664214815,-1.43146819175013,135.511531267197));
#27838=CARTESIAN_POINT('Ctrl Pts',(169.652173879053,-1.30491567920915,135.548162356793));
#27839=CARTESIAN_POINT('Ctrl Pts',(169.64468354329,-1.1772957041373,135.579625834025));
#27840=CARTESIAN_POINT('Ctrl Pts',(169.636909209171,-1.04483697892247,135.612282258559));
#27841=CARTESIAN_POINT('Ctrl Pts',(169.629134875052,-0.910808658173165,
135.63947492098));
#27842=CARTESIAN_POINT('Ctrl Pts',(169.621360540933,-0.775701221548527,
135.661054006837));
#27843=CARTESIAN_POINT('Ctrl Pts',(169.613595787986,-0.640760292764631,
135.6826064984));
#27844=CARTESIAN_POINT('Ctrl Pts',(169.605831035039,-0.504743276603272,
135.698559117546));
#27845=CARTESIAN_POINT('Ctrl Pts',(169.598066282092,-0.36815431657947,135.708812213992));
#27846=CARTESIAN_POINT('Ctrl Pts',(169.590309241207,-0.23170101863633,135.719055126917));
#27847=CARTESIAN_POINT('Ctrl Pts',(169.582552200322,-0.0946772946466856,
135.723609753405));
#27848=CARTESIAN_POINT('Ctrl Pts',(169.574795159437,0.0424044002839236,
135.722427812037));
#27849=CARTESIAN_POINT('Ctrl Pts',(169.567043968197,0.179382720841906,135.721246761982));
#27850=CARTESIAN_POINT('Ctrl Pts',(169.559292776957,0.316418535957338,135.71433775805));
#27851=CARTESIAN_POINT('Ctrl Pts',(169.551541585717,0.452996530268747,135.701704510542));
#27852=CARTESIAN_POINT('Ctrl Pts',(169.543793688939,0.589516475289328,135.6890766325));
#27853=CARTESIAN_POINT('Ctrl Pts',(169.536045792162,0.725578598034433,135.670729385781));
#27854=CARTESIAN_POINT('Ctrl Pts',(169.528297895385,0.860670071426506,135.646718523654));
#27855=CARTESIAN_POINT('Ctrl Pts',(169.520551619301,0.995733286594627,135.622712684081));
#27856=CARTESIAN_POINT('Ctrl Pts',(169.512805343217,1.1298258715768,135.59304565392));
#27857=CARTESIAN_POINT('Ctrl Pts',(169.505059067133,1.26244298690241,135.557824698352));
#27858=CARTESIAN_POINT('Ctrl Pts',(169.497312733868,1.39506108117734,135.52260348279));
#27859=CARTESIAN_POINT('Ctrl Pts',(169.489566400602,1.52620330619644,135.481828360368));
#27860=CARTESIAN_POINT('Ctrl Pts',(169.481820067337,1.65537821904303,135.435656981913));
#27861=CARTESIAN_POINT('Ctrl Pts',(169.474071999334,1.78458205971567,135.389475263699));
#27862=CARTESIAN_POINT('Ctrl Pts',(169.466323931331,1.91181734345662,135.337895016334));
#27863=CARTESIAN_POINT('Ctrl Pts',(169.458575863328,2.03661127838026,135.28112256827));
#27864=CARTESIAN_POINT('Ctrl Pts',(169.450819560586,2.1615378457831,135.224289781773));
#27865=CARTESIAN_POINT('Ctrl Pts',(169.443063257844,2.28401752474915,135.162253933268));
#27866=CARTESIAN_POINT('Ctrl Pts',(169.435306955103,2.40360038106265,135.095268245406));
#27867=CARTESIAN_POINT('Ctrl Pts',(169.427546512588,2.52324706234722,135.028246805265));
#27868=CARTESIAN_POINT('Ctrl Pts',(169.419786070074,2.63999350756389,134.956270466679));
#27869=CARTESIAN_POINT('Ctrl Pts',(169.41202562756,2.75341845672161,134.879636051777));
#27870=CARTESIAN_POINT('Ctrl Pts',(169.404252727295,2.86702548567707,134.80287861651));
#27871=CARTESIAN_POINT('Ctrl Pts',(169.396479827029,2.97730004892688,134.721448394762));
#27872=CARTESIAN_POINT('Ctrl Pts',(169.388706926764,3.0838529874878,134.635683341386));
#27873=CARTESIAN_POINT('Ctrl Pts',(169.381216591002,3.1865324583413,134.55303606373));
#27874=CARTESIAN_POINT('Ctrl Pts',(169.37372625524,3.2857559557091,134.466363849468));
#27875=CARTESIAN_POINT('Ctrl Pts',(169.366235919478,3.38120878401291,134.376000328037));
#27876=CARTESIAN_POINT('Ctrl Pts',(169.358461585359,3.48028073531418,134.282210646226));
#27877=CARTESIAN_POINT('Ctrl Pts',(169.35068725124,3.5756042735339,134.184147122356));
#27878=CARTESIAN_POINT('Ctrl Pts',(169.342912917121,3.66678823929541,134.082141432487));
#27879=CARTESIAN_POINT('Ctrl Pts',(169.335148164174,3.75785982896842,133.980261455514));
#27880=CARTESIAN_POINT('Ctrl Pts',(169.327383411226,3.84480173889385,133.874449267929));
#27881=CARTESIAN_POINT('Ctrl Pts',(169.319618658279,3.9272576285798,133.765075156535));
#27882=CARTESIAN_POINT('Ctrl Pts',(169.311861617394,4.00963162191369,133.65580967705));
#27883=CARTESIAN_POINT('Ctrl Pts',(169.304104576509,4.08752822797811,133.542989624214));
#27884=CARTESIAN_POINT('Ctrl Pts',(169.296347535624,4.16062983174815,133.427020043734));
#27885=CARTESIAN_POINT('Ctrl Pts',(169.288596344384,4.23367630903015,133.311137916817));
#27886=CARTESIAN_POINT('Ctrl Pts',(169.280845153144,4.30193477370519,133.192111319117));
#27887=CARTESIAN_POINT('Ctrl Pts',(169.273093961904,4.36512980681248,133.070375805551));
#27888=CARTESIAN_POINT('Ctrl Pts',(169.265346065127,4.42829798034491,132.948692032825));
#27889=CARTESIAN_POINT('Ctrl Pts',(169.25759816835,4.4864068229048,132.824301980472));
#27890=CARTESIAN_POINT('Ctrl Pts',(169.249850271573,4.53922604573536,132.69766724044));
#27891=CARTESIAN_POINT('Ctrl Pts',(169.242103995489,4.59203421992316,132.571058989666));
#27892=CARTESIAN_POINT('Ctrl Pts',(169.234357719405,4.63955482481111,132.442207345761));
#27893=CARTESIAN_POINT('Ctrl Pts',(169.22661144332,4.6816052275686,132.311595023922));
#27894=CARTESIAN_POINT('Ctrl Pts',(169.218865110055,4.72365594073262,132.180981737931));
#27895=CARTESIAN_POINT('Ctrl Pts',(169.21111877679,4.76023625137703,132.048608120225));
#27896=CARTESIAN_POINT('Ctrl Pts',(169.203372443524,4.79121315870816,131.91497284977));
#27897=CARTESIAN_POINT('Ctrl Pts',(169.195624375521,4.8221970031029,131.781307652623));
#27898=CARTESIAN_POINT('Ctrl Pts',(169.187876307518,4.84757485892271,131.646380621303));
#27899=CARTESIAN_POINT('Ctrl Pts',(169.180128239515,4.86726476057517,131.510701054581));
#27900=CARTESIAN_POINT('Ctrl Pts',(169.172371936774,4.88697558888943,131.374877286002));
#27901=CARTESIAN_POINT('Ctrl Pts',(169.164615634032,4.90098633080901,131.238299771856));
#27902=CARTESIAN_POINT('Ctrl Pts',(169.15685933129,4.90926682928844,131.101483927571));
#27903=CARTESIAN_POINT('Ctrl Pts',(169.149098888776,4.91755174731924,130.96459506055));
#27904=CARTESIAN_POINT('Ctrl Pts',(169.141338446262,4.92010032052056,130.827468000632));
#27905=CARTESIAN_POINT('Ctrl Pts',(169.133578003747,4.9169345724426,130.690617605391));
#27906=CARTESIAN_POINT('Ctrl Pts',(169.125805103482,4.91376374242477,130.553547525745));
#27907=CARTESIAN_POINT('Ctrl Pts',(169.118032203217,4.90486028568715,130.416755388647));
#27908=CARTESIAN_POINT('Ctrl Pts',(169.110259302951,4.8902981832823,130.280751277422));
#27909=CARTESIAN_POINT('Ctrl Pts',(169.102768967189,4.87626544997962,130.149691258215));
#27910=CARTESIAN_POINT('Ctrl Pts',(169.095278631427,4.85697838543172,130.019363270828));
#27911=CARTESIAN_POINT('Ctrl Pts',(169.087788295665,4.83254758088737,129.890212412427));
#27912=CARTESIAN_POINT('Ctrl Pts',(169.080013961546,4.80719047496313,129.756164759974));
#27913=CARTESIAN_POINT('Ctrl Pts',(169.072239627427,4.77621155584309,129.622960637581));
#27914=CARTESIAN_POINT('Ctrl Pts',(169.064465293308,4.73967844079104,129.49110841772));
#27915=CARTESIAN_POINT('Ctrl Pts',(169.056700540361,4.70319034953823,129.359418693936));
#27916=CARTESIAN_POINT('Ctrl Pts',(169.048935787414,4.66116178535475,129.229077930797));
#27917=CARTESIAN_POINT('Ctrl Pts',(169.041171034466,4.61371167027568,129.100586076712));
#27918=CARTESIAN_POINT('Ctrl Pts',(169.033413993581,4.56630868331985,128.972221842549));
#27919=CARTESIAN_POINT('Ctrl Pts',(169.025656952696,4.5134949959467,128.845703227379));
#27920=CARTESIAN_POINT('Ctrl Pts',(169.017899911811,4.45543970590349,128.721516386818));
#27921=CARTESIAN_POINT('Ctrl Pts',(169.010148720571,4.3974281958061,128.59742319652));
#27922=CARTESIAN_POINT('Ctrl Pts',(169.002397529331,4.33418311561574,128.475658633566));
#27923=CARTESIAN_POINT('Ctrl Pts',(168.994646338091,4.26592203934227,128.356689843799));
#27924=CARTESIAN_POINT('Ctrl Pts',(168.986898441314,4.19768997584712,128.237771618941));
#27925=CARTESIAN_POINT('Ctrl Pts',(168.979150544537,4.12444635068408,128.121647142274));
#27926=CARTESIAN_POINT('Ctrl Pts',(168.97140264776,4.04645503753438,128.008759663976));
#27927=CARTESIAN_POINT('Ctrl Pts',(168.963656371676,3.96848003848606,127.895895799305));
#27928=CARTESIAN_POINT('Ctrl Pts',(168.955910095592,3.88575954889843,127.786267907652));
#27929=CARTESIAN_POINT('Ctrl Pts',(168.948163819508,3.79860097323011,127.680290562546));
#27930=CARTESIAN_POINT('Ctrl Pts',(168.940417486242,3.71144175417708,127.574312435138));
#27931=CARTESIAN_POINT('Ctrl Pts',(168.932671152977,3.61984463201219,127.471985210009));
#27932=CARTESIAN_POINT('Ctrl Pts',(168.924924819712,3.52415726929668,127.373690332656));
#27933=CARTESIAN_POINT('Ctrl Pts',(168.917176751709,3.42844847805977,127.275373442847));
#27934=CARTESIAN_POINT('Ctrl Pts',(168.909428683706,3.3286478962373,127.181090977803));
#27935=CARTESIAN_POINT('Ctrl Pts',(168.901680615703,3.22513970690524,127.091187185925));
#27936=CARTESIAN_POINT('Ctrl Pts',(168.893924312961,3.12152150783768,127.001187843227));
#27937=CARTESIAN_POINT('Ctrl Pts',(168.886168010219,3.01418812534955,126.915576726758));
#27938=CARTESIAN_POINT('Ctrl Pts',(168.878411707477,2.90355689241722,126.834657803123));
#27939=CARTESIAN_POINT('Ctrl Pts',(168.870651264963,2.79286661226476,126.753695690622));
#27940=CARTESIAN_POINT('Ctrl Pts',(168.862890822449,2.67887529918352,126.677430978408));
#27941=CARTESIAN_POINT('Ctrl Pts',(168.855130379935,2.5620280216982,126.606123430539));
#27942=CARTESIAN_POINT('Ctrl Pts',(168.847357479669,2.44499317058989,126.534701413465));
#27943=CARTESIAN_POINT('Ctrl Pts',(168.839584579404,2.32509353564874,126.468252652342));
#27944=CARTESIAN_POINT('Ctrl Pts',(168.831811679138,2.20279825299001,126.406990617313));
#27945=CARTESIAN_POINT('Ctrl Pts',(168.824321343376,2.08494871189854,126.347955611567));
#27946=CARTESIAN_POINT('Ctrl Pts',(168.816831007614,1.9648749555283,126.293736904589));
#27947=CARTESIAN_POINT('Ctrl Pts',(168.809340671852,1.84301123400021,126.244482038717));
#27948=CARTESIAN_POINT('Ctrl Pts',(168.801566337733,1.71652701243132,126.193359659635));
#27949=CARTESIAN_POINT('Ctrl Pts',(168.793792003614,1.58771374923849,126.147423019814));
#27950=CARTESIAN_POINT('Ctrl Pts',(168.786017669495,1.4570357013638,126.106890018674));
#27951=CARTESIAN_POINT('Ctrl Pts',(168.778252916548,1.32651870250418,126.066406970836));
#27952=CARTESIAN_POINT('Ctrl Pts',(168.770488163601,1.19414186148694,126.031314425968));
#27953=CARTESIAN_POINT('Ctrl Pts',(168.762723410654,1.06039007933355,126.00178256592));
#27954=CARTESIAN_POINT('Ctrl Pts',(168.754966369769,0.926771141335774,125.972280037332));
#27955=CARTESIAN_POINT('Ctrl Pts',(168.747209328884,0.791780359128918,125.948327286392));
#27956=CARTESIAN_POINT('Ctrl Pts',(168.739452287999,0.65591815066357,125.930044825362));
#27957=CARTESIAN_POINT('Ctrl Pts',(168.731701096759,0.520158396946435,125.911776151277));
#27958=CARTESIAN_POINT('Ctrl Pts',(168.723949905518,0.383528910891622,125.899169307894));
#27959=CARTESIAN_POINT('Ctrl Pts',(168.716198714278,0.246540319593697,125.892293747773));
#27960=CARTESIAN_POINT('Ctrl Pts',(168.708450817501,0.109609952101364,125.885421109949));
#27961=CARTESIAN_POINT('Ctrl Pts',(168.700702920724,-0.0276788274098269,
125.88427493003));
#27962=CARTESIAN_POINT('Ctrl Pts',(168.692955023947,-0.164810469842722,
125.888872791162));
#27963=CARTESIAN_POINT('Ctrl Pts',(168.685208747863,-0.301913427292237,
125.89346969052));
#27964=CARTESIAN_POINT('Ctrl Pts',(168.677462471779,-0.438858922544996,
125.903808227928));
#27965=CARTESIAN_POINT('Ctrl Pts',(168.669716195695,-0.575132003533086,
125.919853862426));
#27966=CARTESIAN_POINT('Ctrl Pts',(168.661969862429,-0.711406090458104,
125.935899615369));
#27967=CARTESIAN_POINT('Ctrl Pts',(168.654223529164,-0.84700736493107,125.957652503748));
#27968=CARTESIAN_POINT('Ctrl Pts',(168.646477195899,-0.981426985945333,
125.985026209812));
#27969=CARTESIAN_POINT('Ctrl Pts',(168.638729127896,-1.11587670930163,126.012406046028));
#27970=CARTESIAN_POINT('Ctrl Pts',(168.630981059893,-1.24914386960109,126.045409126682));
#27971=CARTESIAN_POINT('Ctrl Pts',(168.62323299189,-1.38073118057777,126.083898302339));
#27972=CARTESIAN_POINT('Ctrl Pts',(168.615476689148,-1.51245834411457,126.12242838475));
#27973=CARTESIAN_POINT('Ctrl Pts',(168.607720386406,-1.64250171603113,126.166456099657));
#27974=CARTESIAN_POINT('Ctrl Pts',(168.599964083664,-1.77037998194666,126.215794634383));
#27975=CARTESIAN_POINT('Ctrl Pts',(168.59220364115,-1.89832650034323,126.265159502571));
#27976=CARTESIAN_POINT('Ctrl Pts',(168.584443198636,-2.02410525177077,126.319840682847));
#27977=CARTESIAN_POINT('Ctrl Pts',(168.576682756122,-2.14725711896144,126.379604135276));
#27978=CARTESIAN_POINT('Ctrl Pts',(168.568909855856,-2.27060668046215,126.439463525304));
#27979=CARTESIAN_POINT('Ctrl Pts',(168.561136955591,-2.39132058651883,126.504421305426));
#27980=CARTESIAN_POINT('Ctrl Pts',(168.553364055326,-2.50896565912489,126.574198163968));
#27981=CARTESIAN_POINT('Ctrl Pts',(168.545873719564,-2.6223340370115,126.641438457944));
#27982=CARTESIAN_POINT('Ctrl Pts',(168.538383383802,-2.73285256902816,126.713153374356));
#27983=CARTESIAN_POINT('Ctrl Pts',(168.53089304804,-2.84016240082866,126.789057316516));
#27984=CARTESIAN_POINT('Ctrl Pts',(168.52317132459,-2.95078719402167,126.86730604511));
#27985=CARTESIAN_POINT('Ctrl Pts',(168.51544960114,-3.05836308616123,126.950262473689));
#27986=CARTESIAN_POINT('Ctrl Pts',(168.50772787769,-3.16245894428162,127.03765960896));
#27987=CARTESIAN_POINT('Ctrl Pts',(168.500018346955,-3.26639043351439,127.124918742872));
#27988=CARTESIAN_POINT('Ctrl Pts',(168.492308816219,-3.36685252945368,127.216604368201));
#27989=CARTESIAN_POINT('Ctrl Pts',(168.484599285484,-3.46344322780615,127.312406426821));
#27990=CARTESIAN_POINT('Ctrl Pts',(168.476896797498,-3.5599456893932,127.408120969107));
#27991=CARTESIAN_POINT('Ctrl Pts',(168.469194309512,-3.65258350677029,127.507944188805));
#27992=CARTESIAN_POINT('Ctrl Pts',(168.461491821526,-3.7409877692236,127.611525893842));
#27993=CARTESIAN_POINT('Ctrl Pts',(168.453794642419,-3.82933109973314,127.715036206002));
#27994=CARTESIAN_POINT('Ctrl Pts',(168.446097463312,-3.91344642311149,127.822299549752));
#27995=CARTESIAN_POINT('Ctrl Pts',(168.438400284205,-3.99300207612229,127.932929357274));
#27996=CARTESIAN_POINT('Ctrl Pts',(168.430706684397,-4.07252073461947,128.043507720357));
#27997=CARTESIAN_POINT('Ctrl Pts',(168.423013084588,-4.14748371086074,128.15744911039));
#27998=CARTESIAN_POINT('Ctrl Pts',(168.415319484779,-4.2176003035411,128.274334779344));
#27999=CARTESIAN_POINT('Ctrl Pts',(168.407626333773,-4.28771280600053,128.391213629824));
#28000=CARTESIAN_POINT('Ctrl Pts',(168.399933182767,-4.35297927547694,128.511036081975));
#28001=CARTESIAN_POINT('Ctrl Pts',(168.392240031762,-4.41315307034798,128.633355541529));
#28002=CARTESIAN_POINT('Ctrl Pts',(168.384547189035,-4.47332445394333,128.755670099515));
#28003=CARTESIAN_POINT('Ctrl Pts',(168.376854346307,-4.52840339898507,128.88048110705));
#28004=CARTESIAN_POINT('Ctrl Pts',(168.36916150358,-4.57819020506195,129.007319296735));
#28005=CARTESIAN_POINT('Ctrl Pts',(168.361464918195,-4.62800123300544,129.13421919469));
#28006=CARTESIAN_POINT('Ctrl Pts',(168.353768332809,-4.67251484040017,129.263147872706));
#28007=CARTESIAN_POINT('Ctrl Pts',(168.346071747424,-4.71158027578738,129.393618129615));
#28008=CARTESIAN_POINT('Ctrl Pts',(168.342377681529,-4.73033018698689,129.456238850643));
#28009=CARTESIAN_POINT('Ctrl Pts',(168.338683615635,-4.74782577970215,129.519214475088));
#28010=CARTESIAN_POINT('Ctrl Pts',(168.33498954974,-4.76405452823405,129.582490119308));
#28011=CARTESIAN_POINT('Ctrl Pts',(170.084755673967,-4.76405452823406,129.582490119308));
#28012=CARTESIAN_POINT('Ctrl Pts',(170.077020912222,-4.79810525795013,129.715253397679));
#28013=CARTESIAN_POINT('Ctrl Pts',(170.069286150477,-4.82661229531109,129.849481010834));
#28014=CARTESIAN_POINT('Ctrl Pts',(170.061551388732,-4.84946291612859,129.984670134766));
#28015=CARTESIAN_POINT('Ctrl Pts',(170.053769396608,-4.872453068518,130.120684757099));
#28016=CARTESIAN_POINT('Ctrl Pts',(170.045987404485,-4.88971739268245,130.25767228365));
#28017=CARTESIAN_POINT('Ctrl Pts',(170.038205412361,-4.90119355435987,130.395111542795));
#28018=CARTESIAN_POINT('Ctrl Pts',(170.030423420238,-4.91266971603728,130.532550801939));
#28019=CARTESIAN_POINT('Ctrl Pts',(170.022641428114,-4.9183576950795,130.670441390693));
#28020=CARTESIAN_POINT('Ctrl Pts',(170.014859435991,-4.91824845497686,130.808259029769));
#28021=CARTESIAN_POINT('',(170.360140564063,-4.91824882901199,130.800966737464));
#28022=CARTESIAN_POINT('Ctrl Pts',(170.429908526381,-4.76405452823404,129.582490119308));
#28023=CARTESIAN_POINT('Ctrl Pts',(170.421033020534,-4.80283367562411,129.733689426426));
#28024=CARTESIAN_POINT('Ctrl Pts',(170.412157514688,-4.83445442237841,129.886906563728));
#28025=CARTESIAN_POINT('Ctrl Pts',(170.403282008841,-4.85872694272219,130.041500500267));
#28026=CARTESIAN_POINT('Ctrl Pts',(170.39446678309,-4.8828346105065,130.195044475543));
#28027=CARTESIAN_POINT('Ctrl Pts',(170.385651557339,-4.89969344204067,130.349946452333));
#28028=CARTESIAN_POINT('Ctrl Pts',(170.376836331588,-4.90916496957448,130.505559071381));
#28029=CARTESIAN_POINT('Ctrl Pts',(170.371271075747,-4.91514456390694,130.603800915855));
#28030=CARTESIAN_POINT('Ctrl Pts',(170.365705819905,-4.91818076085781,130.702325621825));
#28031=CARTESIAN_POINT('Ctrl Pts',(170.360140564063,-4.91824882901199,130.800966737464));
#28032=CARTESIAN_POINT('Ctrl Pts',(170.360140564008,-4.91824882901267,130.800966738437));
#28033=CARTESIAN_POINT('Ctrl Pts',(170.352360472836,-4.91834398659548,130.938864598804));
#28034=CARTESIAN_POINT('Ctrl Pts',(170.344580381664,-4.91263525214567,131.076802536184));
#28035=CARTESIAN_POINT('Ctrl Pts',(170.336800290492,-4.90113922727987,131.214259797022));
#28036=CARTESIAN_POINT('Ctrl Pts',(170.329020253002,-4.88964328173574,131.351716109415));
#28037=CARTESIAN_POINT('Ctrl Pts',(170.321240215512,-4.87236015654906,131.488691367181));
#28038=CARTESIAN_POINT('Ctrl Pts',(170.313460178022,-4.84935842684873,131.624669041545));
#28039=CARTESIAN_POINT('Ctrl Pts',(170.305678564943,-4.82635203890897,131.760674253689));
#28040=CARTESIAN_POINT('Ctrl Pts',(170.297896951864,-4.79762480510897,131.895681099668));
#28041=CARTESIAN_POINT('Ctrl Pts',(170.290115338785,-4.76329654399539,132.029182684832));
#28042=CARTESIAN_POINT('Ctrl Pts',(170.282330520181,-4.72895414184579,132.162739264064));
#28043=CARTESIAN_POINT('Ctrl Pts',(170.274545701578,-4.68900621523641,132.294788974566));
#28044=CARTESIAN_POINT('Ctrl Pts',(170.266760882975,-4.64362251945257,132.424839855117));
#28045=CARTESIAN_POINT('Ctrl Pts',(170.258966330822,-4.59818207932088,132.555053341473));
#28046=CARTESIAN_POINT('Ctrl Pts',(170.251171778669,-4.54729242388263,132.683262641997));
#28047=CARTESIAN_POINT('Ctrl Pts',(170.243377226516,-4.49117180285544,132.808994973187));
#28048=CARTESIAN_POINT('Ctrl Pts',(170.23557732948,-4.43501269877819,132.934813521591));
#28049=CARTESIAN_POINT('Ctrl Pts',(170.227777432445,-4.37361565378318,133.058151371684));
#28050=CARTESIAN_POINT('Ctrl Pts',(170.219977535409,-4.30724457420593,133.178560954621));
#28051=CARTESIAN_POINT('Ctrl Pts',(170.212164997682,-4.24076593214009,133.29916567608));
#28052=CARTESIAN_POINT('Ctrl Pts',(170.204352459955,-4.16929735363983,133.416832321866));
#28053=CARTESIAN_POINT('Ctrl Pts',(170.196539922227,-4.09314611327394,133.531142229263));
#28054=CARTESIAN_POINT('Ctrl Pts',(170.191689879738,-4.04587123738561,133.602106098782));
#28055=CARTESIAN_POINT('Ctrl Pts',(170.186839837248,-3.99679250347402,133.671776929543));
#28056=CARTESIAN_POINT('Ctrl Pts',(170.181989794758,-3.94599092647641,133.740061329605));
#28057=CARTESIAN_POINT('Ctrl Pts',(170.174215460639,-3.86455897321264,133.849517224542));
#28058=CARTESIAN_POINT('Ctrl Pts',(170.16644112652,-3.77844037158533,133.95575572089));
#28059=CARTESIAN_POINT('Ctrl Pts',(170.158666792401,-3.68791827680057,134.058349223284));
#28060=CARTESIAN_POINT('Ctrl Pts',(170.150902039454,-3.59750774240747,134.160816288355));
#28061=CARTESIAN_POINT('Ctrl Pts',(170.143137286507,-3.50270476897911,134.259647007123));
#28062=CARTESIAN_POINT('Ctrl Pts',(170.13537253356,-3.40383496463212,134.354443799133));
#28063=CARTESIAN_POINT('Ctrl Pts',(170.127615492675,-3.30506335916833,134.449146437634));
#28064=CARTESIAN_POINT('Ctrl Pts',(170.11985845179,-3.20223324142314,134.539822853769));
#28065=CARTESIAN_POINT('Ctrl Pts',(170.112101410905,-3.09570930894535,134.626109816167));
#28066=CARTESIAN_POINT('Ctrl Pts',(170.104350219664,-2.98926570699406,134.712331708896));
#28067=CARTESIAN_POINT('Ctrl Pts',(170.096599028424,-2.87913413731964,134.794170491394));
#28068=CARTESIAN_POINT('Ctrl Pts',(170.088847837184,-2.76571457685697,134.871301229606));
#28069=CARTESIAN_POINT('Ctrl Pts',(170.081099940407,-2.65234322273291,134.948399185197));
#28070=CARTESIAN_POINT('Ctrl Pts',(170.07335204363,-2.53568697992477,135.020792857034));
#28071=CARTESIAN_POINT('Ctrl Pts',(170.065604146853,-2.41617701043069,135.088199050183));
#28072=CARTESIAN_POINT('Ctrl Pts',(170.057857870769,-2.29669203984581,135.15559114341));
#28073=CARTESIAN_POINT('Ctrl Pts',(170.050111594685,-2.17435487023594,135.217997641129));
#28074=CARTESIAN_POINT('Ctrl Pts',(170.042365318601,-2.04962326757815,135.275180175936));
#28075=CARTESIAN_POINT('Ctrl Pts',(170.034618985335,-1.92489074418012,135.332363132851));
#28076=CARTESIAN_POINT('Ctrl Pts',(170.02687265207,-1.79776410786242,135.384321886974));
#28077=CARTESIAN_POINT('Ctrl Pts',(170.019126318805,-1.66872283861668,135.430865470085));
#28078=CARTESIAN_POINT('Ctrl Pts',(170.011378250802,-1.53965267147335,135.477419476308));
#28079=CARTESIAN_POINT('Ctrl Pts',(170.003630182799,-1.40866738590499,135.51855576578));
#28080=CARTESIAN_POINT('Ctrl Pts',(169.995882114796,-1.276263035079,135.554132793975));
#28081=CARTESIAN_POINT('Ctrl Pts',(169.988125812054,-1.14371796333346,135.58974763386));
#28082=CARTESIAN_POINT('Ctrl Pts',(169.980369509312,-1.00975119171394,135.619791308089));
#28083=CARTESIAN_POINT('Ctrl Pts',(169.97261320657,-0.874870966272833,135.644172995631));
#28084=CARTESIAN_POINT('Ctrl Pts',(169.964852764056,-0.739918751194152,
135.668567696414));
#28085=CARTESIAN_POINT('Ctrl Pts',(169.957092321542,-0.604052497947626,
135.687294335615));
#28086=CARTESIAN_POINT('Ctrl Pts',(169.949331879027,-0.467786061620851,
135.700313973456));
#28087=CARTESIAN_POINT('Ctrl Pts',(169.941558978762,-0.331300878313273,
135.713354511576));
#28088=CARTESIAN_POINT('Ctrl Pts',(169.933786078497,-0.194414618819575,
135.720669720093));
#28089=CARTESIAN_POINT('Ctrl Pts',(169.926013178231,-0.0576425340327472,
135.722272816942));
#28090=CARTESIAN_POINT('Ctrl Pts',(169.918522842469,0.0741575409652403,
135.723817637183));
#28091=CARTESIAN_POINT('Ctrl Pts',(169.911032506707,0.205851290320753,135.720058443634));
#28092=CARTESIAN_POINT('Ctrl Pts',(169.903542170945,0.33698367046011,135.711052483614));
#28093=CARTESIAN_POINT('Ctrl Pts',(169.895767836826,0.473087974648075,135.701705059883));
#28094=CARTESIAN_POINT('Ctrl Pts',(169.887993502707,0.6090186381992,135.686675543623));
#28095=CARTESIAN_POINT('Ctrl Pts',(169.880219168587,0.744262860718677,135.665971035592));
#28096=CARTESIAN_POINT('Ctrl Pts',(169.87245441564,0.879340406820976,135.645292044015));
#28097=CARTESIAN_POINT('Ctrl Pts',(169.864689662693,1.01373281238139,135.618952035079));
#28098=CARTESIAN_POINT('Ctrl Pts',(169.856924909746,1.14692958256326,135.587010050165));
#28099=CARTESIAN_POINT('Ctrl Pts',(169.849167868861,1.27999405983516,135.555099790481));
#28100=CARTESIAN_POINT('Ctrl Pts',(169.841410827976,1.41186488722495,135.517598717937));
#28101=CARTESIAN_POINT('Ctrl Pts',(169.833653787091,1.54203933996029,135.474617327482));
#28102=CARTESIAN_POINT('Ctrl Pts',(169.825902595851,1.67211562712836,135.431668349627));
#28103=CARTESIAN_POINT('Ctrl Pts',(169.818151404611,1.80049771616081,135.383247401935));
#28104=CARTESIAN_POINT('Ctrl Pts',(169.810400213371,1.9266960335319,135.329515361536));
#28105=CARTESIAN_POINT('Ctrl Pts',(169.802652316593,2.05284071325161,135.275806158687));
#28106=CARTESIAN_POINT('Ctrl Pts',(169.794904419816,2.17680310838795,135.216790505677));
#28107=CARTESIAN_POINT('Ctrl Pts',(169.787156523039,2.29811190543176,135.152678077528));
#28108=CARTESIAN_POINT('Ctrl Pts',(169.779410246955,2.41939532729038,135.088579060317));
#28109=CARTESIAN_POINT('Ctrl Pts',(169.771663970871,2.53802590969138,135.019385571137));
#28110=CARTESIAN_POINT('Ctrl Pts',(169.763917694787,2.65355567369279,134.945353898062));
#28111=CARTESIAN_POINT('Ctrl Pts',(169.756171361521,2.76908629050859,134.871321678502));
#28112=CARTESIAN_POINT('Ctrl Pts',(169.748425028256,2.88151571407146,134.792451414722));
#28113=CARTESIAN_POINT('Ctrl Pts',(169.740678694991,2.99042410676061,134.709043283828));
#28114=CARTESIAN_POINT('Ctrl Pts',(169.732930626988,3.09935688872904,134.625616474262));
#28115=CARTESIAN_POINT('Ctrl Pts',(169.725182558985,3.20476676044471,134.537650013086));
#28116=CARTESIAN_POINT('Ctrl Pts',(169.717434490982,3.30626650763675,134.445484735607));
#28117=CARTESIAN_POINT('Ctrl Pts',(169.70967818824,3.40787412996818,134.353221503774));
#28118=CARTESIAN_POINT('Ctrl Pts',(169.701921885498,3.50556303635941,134.256750804453));
#28119=CARTESIAN_POINT('Ctrl Pts',(169.694165582756,3.5989820970972,134.156451148455));
#28120=CARTESIAN_POINT('Ctrl Pts',(169.686405140242,3.69245101840044,134.05609795951));
#28121=CARTESIAN_POINT('Ctrl Pts',(169.678644697728,3.78164529892404,133.951912038634));
#28122=CARTESIAN_POINT('Ctrl Pts',(169.670884255214,3.86625442630231,133.844304658761));
#28123=CARTESIAN_POINT('Ctrl Pts',(169.663111354948,3.95099937576314,133.73652453797));
#28124=CARTESIAN_POINT('Ctrl Pts',(169.655338454683,4.03114423475479,133.625312299924));
#28125=CARTESIAN_POINT('Ctrl Pts',(169.647565554417,4.10642161820729,133.511108584411));
#28126=CARTESIAN_POINT('Ctrl Pts',(169.640075218655,4.17896247915849,133.401056461619));
#28127=CARTESIAN_POINT('Ctrl Pts',(169.632584882893,4.24698345148421,133.288226844591));
#28128=CARTESIAN_POINT('Ctrl Pts',(169.625094547131,4.31028673680823,133.173033517946));
#28129=CARTESIAN_POINT('Ctrl Pts',(169.617320213012,4.37599018543632,133.053472601308));
#28130=CARTESIAN_POINT('Ctrl Pts',(169.609545878893,4.43681927168965,132.930986463652));
#28131=CARTESIAN_POINT('Ctrl Pts',(169.601771544774,4.49250278849581,132.806010376604));
#28132=CARTESIAN_POINT('Ctrl Pts',(169.594006791827,4.54811768034397,132.681188311414));
#28133=CARTESIAN_POINT('Ctrl Pts',(169.58624203888,4.59859946276015,132.553882756205));
#28134=CARTESIAN_POINT('Ctrl Pts',(169.578477285933,4.64372187400349,132.424555118051));
#28135=CARTESIAN_POINT('Ctrl Pts',(169.570720245048,4.68879946903203,132.295355929929));
#28136=CARTESIAN_POINT('Ctrl Pts',(169.562963204163,4.72852815794359,132.164139022346));
#28137=CARTESIAN_POINT('Ctrl Pts',(169.555206163278,4.76272916824859,132.031387077107));
#28138=CARTESIAN_POINT('Ctrl Pts',(169.547454972038,4.79690438730564,131.898735241143));
#28139=CARTESIAN_POINT('Ctrl Pts',(169.539703780798,4.82556012768876,131.764551048696));
#28140=CARTESIAN_POINT('Ctrl Pts',(169.531952589557,4.84856711343453,131.629333349855));
#28141=CARTESIAN_POINT('Ctrl Pts',(169.52420469278,4.87156432059757,131.494173122145));
#28142=CARTESIAN_POINT('Ctrl Pts',(169.516456796003,4.88891748283141,131.35798064633));
#28143=CARTESIAN_POINT('Ctrl Pts',(169.508708899226,4.90054824920584,131.221265786286));
#28144=CARTESIAN_POINT('Ctrl Pts',(169.500962623142,4.91217658267468,131.084579524044));
#28145=CARTESIAN_POINT('Ctrl Pts',(169.493216347058,4.91808486806646,130.94737148423));
#28146=CARTESIAN_POINT('Ctrl Pts',(169.485470070974,4.91824658423699,130.810157094182));
#28147=CARTESIAN_POINT('Ctrl Pts',(169.477723737709,4.91840830160127,130.672941691249));
#28148=CARTESIAN_POINT('Ctrl Pts',(169.469977404443,4.91282336463777,130.535720328952));
#28149=CARTESIAN_POINT('Ctrl Pts',(169.462231071178,4.90151738835985,130.399008481632));
#28150=CARTESIAN_POINT('Ctrl Pts',(169.454483003175,4.89020888018696,130.262266018642));
#28151=CARTESIAN_POINT('Ctrl Pts',(169.446734935172,4.87317681550208,130.12603368724));
#28152=CARTESIAN_POINT('Ctrl Pts',(169.438986867169,4.85049864992938,129.990821491566));
#28153=CARTESIAN_POINT('Ctrl Pts',(169.431230564428,4.82779638173237,129.855465590761));
#28154=CARTESIAN_POINT('Ctrl Pts',(169.423474261686,4.79943609029013,129.721132377709));
#28155=CARTESIAN_POINT('Ctrl Pts',(169.415717958944,4.76554643328138,129.588321862123));
#28156=CARTESIAN_POINT('Ctrl Pts',(169.40795751643,4.73163868834225,129.455440461566));
#28157=CARTESIAN_POINT('Ctrl Pts',(169.400197073916,4.69219580972468,129.324083752131));
#28158=CARTESIAN_POINT('Ctrl Pts',(169.392436631401,4.64739597347956,129.194735279736));
#28159=CARTESIAN_POINT('Ctrl Pts',(169.384663731136,4.60252422056019,129.065179165689));
#28160=CARTESIAN_POINT('Ctrl Pts',(169.376890830871,4.55227846893061,128.937638094825));
#28161=CARTESIAN_POINT('Ctrl Pts',(169.369117930605,4.49688491316069,128.812575202345));
#28162=CARTESIAN_POINT('Ctrl Pts',(169.361627594843,4.44350505267042,128.692058661019));
#28163=CARTESIAN_POINT('Ctrl Pts',(169.354137259081,4.3853452974095,128.573843526525));
#28164=CARTESIAN_POINT('Ctrl Pts',(169.346646923319,4.32264686124391,128.458319872933));
#28165=CARTESIAN_POINT('Ctrl Pts',(169.3388725892,4.25757119481492,128.338416104903));
#28166=CARTESIAN_POINT('Ctrl Pts',(169.331098255081,4.18739974516979,128.221032122576));
#28167=CARTESIAN_POINT('Ctrl Pts',(169.323323920962,4.11235212460887,128.106631375087));
#28168=CARTESIAN_POINT('Ctrl Pts',(169.315559168015,4.03739699353317,127.992371616296));
#28169=CARTESIAN_POINT('Ctrl Pts',(169.307794415067,3.95757786093702,127.881088100829));
#28170=CARTESIAN_POINT('Ctrl Pts',(169.30002966212,3.8731606216617,127.773220590891));
#28171=CARTESIAN_POINT('Ctrl Pts',(169.292272621235,3.78882722677847,127.665460216485));
#28172=CARTESIAN_POINT('Ctrl Pts',(169.28451558035,3.69990505295632,127.561109401629));
#28173=CARTESIAN_POINT('Ctrl Pts',(169.276758539465,3.60670356317283,127.460579453988));
#28174=CARTESIAN_POINT('Ctrl Pts',(169.269007348225,3.51357235735718,127.360125316763));
#28175=CARTESIAN_POINT('Ctrl Pts',(169.261256156985,3.41616852358905,127.263486597156));
#28176=CARTESIAN_POINT('Ctrl Pts',(169.253504965745,3.31484188176225,127.171041699357));
#28177=CARTESIAN_POINT('Ctrl Pts',(169.245757068968,3.21355830646176,127.078636093106));
#28178=CARTESIAN_POINT('Ctrl Pts',(169.238009172191,3.10835552744922,126.990421026387));
#28179=CARTESIAN_POINT('Ctrl Pts',(169.230261275414,2.99962015705057,126.906738011936));
#28180=CARTESIAN_POINT('Ctrl Pts',(169.22251499933,2.89090753174728,126.823072502168));
#28181=CARTESIAN_POINT('Ctrl Pts',(169.214768723245,2.77866409449039,126.743937397324));
#28182=CARTESIAN_POINT('Ctrl Pts',(169.207022447161,2.66330915356937,126.669633611461));
#28183=CARTESIAN_POINT('Ctrl Pts',(169.199276113896,2.54795336112462,126.595329277104));
#28184=CARTESIAN_POINT('Ctrl Pts',(169.191529780631,2.42948634786476,126.525856544606));
#28185=CARTESIAN_POINT('Ctrl Pts',(169.183783447365,2.30835564249141,126.461472489801));
#28186=CARTESIAN_POINT('Ctrl Pts',(169.176035379362,2.18719781073601,126.397074016634));
#28187=CARTESIAN_POINT('Ctrl Pts',(169.168287311359,2.06337544503259,126.337766672244));
#28188=CARTESIAN_POINT('Ctrl Pts',(169.160539243356,1.93735949296564,126.283760960716));
#28189=CARTESIAN_POINT('Ctrl Pts',(169.152782940614,1.81120960964558,126.229697851275));
#28190=CARTESIAN_POINT('Ctrl Pts',(169.145026637872,1.68286184272782,126.180947784745));
#28191=CARTESIAN_POINT('Ctrl Pts',(169.137270335131,1.55280640716156,126.13767278524));
#28192=CARTESIAN_POINT('Ctrl Pts',(169.129509892616,1.42268155709341,126.094374688565));
#28193=CARTESIAN_POINT('Ctrl Pts',(169.121749450102,1.29084759789218,126.056557589411));
#28194=CARTESIAN_POINT('Ctrl Pts',(169.113989007588,1.15780765893901,126.0243329516));
#28195=CARTESIAN_POINT('Ctrl Pts',(169.106216107323,1.02455415246505,125.992056583939));
#28196=CARTESIAN_POINT('Ctrl Pts',(169.098443207057,0.890091181320103,125.965390693653));
#28197=CARTESIAN_POINT('Ctrl Pts',(169.090670306792,0.754930657954383,125.944395312733));
#28198=CARTESIAN_POINT('Ctrl Pts',(169.08317997103,0.624683560064065,125.924163166794));
#28199=CARTESIAN_POINT('Ctrl Pts',(169.075689635268,0.493789051041498,125.909196448306));
#28200=CARTESIAN_POINT('Ctrl Pts',(169.068199299506,0.362705693235946,125.899503061776));
#28201=CARTESIAN_POINT('Ctrl Pts',(169.060424965387,0.226652270075251,125.889442147549));
#28202=CARTESIAN_POINT('Ctrl Pts',(169.052650631268,0.0899644186898381,
125.885030465782));
#28203=CARTESIAN_POINT('Ctrl Pts',(169.044876297149,-0.0468492422225645,
125.886333756008));
#28204=CARTESIAN_POINT('Ctrl Pts',(169.037111544202,-0.18349429252528,125.887635440045));
#28205=CARTESIAN_POINT('Ctrl Pts',(169.029346791255,-0.320264456659288,
125.894638078533));
#28206=CARTESIAN_POINT('Ctrl Pts',(169.021582038308,-0.456646027570617,
125.907355668824));
#28207=CARTESIAN_POINT('Ctrl Pts',(169.013824997423,-0.592892142383768,
125.920060627825));
#28208=CARTESIAN_POINT('Ctrl Pts',(169.006067956538,-0.728750045287246,
125.938469206728));
#28209=CARTESIAN_POINT('Ctrl Pts',(168.998310915652,-0.863706419194596,
125.962543367407));
#28210=CARTESIAN_POINT('Ctrl Pts',(168.990559724412,-0.998561021450345,
125.986599373573));
#28211=CARTESIAN_POINT('Ctrl Pts',(168.982808533172,-1.13251506457823,126.016312389062));
#28212=CARTESIAN_POINT('Ctrl Pts',(168.975057341932,-1.26506110021994,126.051592637198));
#28213=CARTESIAN_POINT('Ctrl Pts',(168.967309445155,-1.39755080026042,126.086857890287));
#28214=CARTESIAN_POINT('Ctrl Pts',(168.959561548378,-1.52863330604812,126.127685569434));
#28215=CARTESIAN_POINT('Ctrl Pts',(168.951813651601,-1.65781231984146,126.173935002714));
#28216=CARTESIAN_POINT('Ctrl Pts',(168.944067375517,-1.78696431216984,126.220174761609));
#28217=CARTESIAN_POINT('Ctrl Pts',(168.936321099433,-1.91421323663274,126.271833887122));
#28218=CARTESIAN_POINT('Ctrl Pts',(168.928574823349,-2.03907927934068,126.328722254711));
#28219=CARTESIAN_POINT('Ctrl Pts',(168.920828490083,-2.1639462437813,126.385611042236));
#28220=CARTESIAN_POINT('Ctrl Pts',(168.913082156818,-2.28642993558682,126.44772898677));
#28221=CARTESIAN_POINT('Ctrl Pts',(168.905335823553,-2.4060721693812,126.514838525511));
#28222=CARTESIAN_POINT('Ctrl Pts',(168.89758775555,-2.52574119622397,126.581963092967));
#28223=CARTESIAN_POINT('Ctrl Pts',(168.889839687547,-2.64256715792227,126.654081287759));
#28224=CARTESIAN_POINT('Ctrl Pts',(168.882091619544,-2.75611839275433,126.730910670946));
#28225=CARTESIAN_POINT('Ctrl Pts',(168.874335316802,-2.86979031119055,126.807821709315));
#28226=CARTESIAN_POINT('Ctrl Pts',(168.86657901406,-2.98018022592325,126.889453718875));
#28227=CARTESIAN_POINT('Ctrl Pts',(168.858822711318,-3.08688684832269,126.975481845895));
#28228=CARTESIAN_POINT('Ctrl Pts',(168.851062268804,-3.19365042325931,127.061555888717));
#28229=CARTESIAN_POINT('Ctrl Pts',(168.84330182629,-3.29672649498496,127.152030466498));
#28230=CARTESIAN_POINT('Ctrl Pts',(168.835541383776,-3.39574933211034,127.246542531158));
#28231=CARTESIAN_POINT('Ctrl Pts',(168.82776848351,-3.4949311294847,127.341206314975));
#28232=CARTESIAN_POINT('Ctrl Pts',(168.819995583245,-3.59004641854384,127.439920255738));
#28233=CARTESIAN_POINT('Ctrl Pts',(168.812222682979,-3.68076799149061,127.542286115762));
#28234=CARTESIAN_POINT('Ctrl Pts',(168.804732347217,-3.76819160674695,127.640930718931));
#28235=CARTESIAN_POINT('Ctrl Pts',(168.797242011455,-3.8515352102945,127.742966099573));
#28236=CARTESIAN_POINT('Ctrl Pts',(168.789751675693,-3.93054428769766,127.848010728776));
#28237=CARTESIAN_POINT('Ctrl Pts',(168.781946135203,-4.0128781873223,127.957475795844));
#28238=CARTESIAN_POINT('Ctrl Pts',(168.774140594712,-4.09076778232355,128.070558441467));
#28239=CARTESIAN_POINT('Ctrl Pts',(168.766335054222,-4.16387970994941,128.186863946399));
#28240=CARTESIAN_POINT('Ctrl Pts',(168.758542386704,-4.23687106068391,128.302977639177));
#28241=CARTESIAN_POINT('Ctrl Pts',(168.750749719185,-4.30510023353292,128.422303280493));
#28242=CARTESIAN_POINT('Ctrl Pts',(168.742957051667,-4.36827486879498,128.544414217061));
#28243=CARTESIAN_POINT('Ctrl Pts',(168.735171791586,-4.43138945245822,128.666409079244));
#28244=CARTESIAN_POINT('Ctrl Pts',(168.727386531505,-4.48945887876381,128.791183629434));
#28245=CARTESIAN_POINT('Ctrl Pts',(168.719601271423,-4.54223454595667,128.918283102717));
#28246=CARTESIAN_POINT('Ctrl Pts',(168.711822962697,-4.59496309046274,129.045269090583));
#28247=CARTESIAN_POINT('Ctrl Pts',(168.70404465397,-4.64240713964826,129.174575512534));
#28248=CARTESIAN_POINT('Ctrl Pts',(168.696266345244,-4.68436470074569,129.305724433261));
#28249=CARTESIAN_POINT('Ctrl Pts',(168.690844533546,-4.71361090368806,129.397140803778));
#28250=CARTESIAN_POINT('Ctrl Pts',(168.685422721848,-4.74019235577851,129.489451871063));
#28251=CARTESIAN_POINT('Ctrl Pts',(168.68000091015,-4.76405452823405,129.582490119308));
#28252=CARTESIAN_POINT('Origin',(213.235140564004,0.,130.804360617566));
#28253=CARTESIAN_POINT('',(166.584804846393,-4.76405452823406,129.582490119308));
#28254=CARTESIAN_POINT('',(166.930280810341,-4.76405452823404,129.582490119308));
#28255=CARTESIAN_POINT('',(213.235140564004,-4.76405452823405,129.582490119308));
#28256=CARTESIAN_POINT('',(168.264859436042,-4.91824981607796,130.805705663694));
#28257=CARTESIAN_POINT('Ctrl Pts',(168.264859435991,-4.91824981607772,130.805705664594));
#28258=CARTESIAN_POINT('Ctrl Pts',(168.260721432069,-4.91822995091836,130.878343880455));
#28259=CARTESIAN_POINT('Ctrl Pts',(168.256583428148,-4.91660096545378,130.950958115917));
#28260=CARTESIAN_POINT('Ctrl Pts',(168.252445424226,-4.91336553894317,131.023500169509));
#28261=CARTESIAN_POINT('Ctrl Pts',(168.244671090107,-4.90728693505862,131.159789591416));
#28262=CARTESIAN_POINT('Ctrl Pts',(168.236896755988,-4.89552370805166,131.296041777244));
#28263=CARTESIAN_POINT('Ctrl Pts',(168.229122421869,-4.87807065083757,131.431743903873));
#28264=CARTESIAN_POINT('Ctrl Pts',(168.221357668922,-4.8606391029567,131.567278789759));
#28265=CARTESIAN_POINT('Ctrl Pts',(168.213592915975,-4.8375317264647,131.702264581214));
#28266=CARTESIAN_POINT('Ctrl Pts',(168.205828163028,-4.8087952952739,131.836189513581));
#28267=CARTESIAN_POINT('Ctrl Pts',(168.198071122143,-4.78008740551166,131.969981429817));
#28268=CARTESIAN_POINT('Ctrl Pts',(168.190314081258,-4.74576166859946,132.102714204006));
#28269=CARTESIAN_POINT('Ctrl Pts',(168.182557040373,-4.70591648365769,132.233882604574));
#28270=CARTESIAN_POINT('Ctrl Pts',(168.174805849133,-4.6661013462798,132.36495209003));
#28271=CARTESIAN_POINT('Ctrl Pts',(168.167054657893,-4.62077515877267,132.494459177426));
#28272=CARTESIAN_POINT('Ctrl Pts',(168.159303466652,-4.57008700352293,132.621910573614));
#28273=CARTESIAN_POINT('Ctrl Pts',(168.151555569875,-4.51942039209137,132.749307799559));
#28274=CARTESIAN_POINT('Ctrl Pts',(168.143807673098,-4.46339648981288,132.874650709536));
#28275=CARTESIAN_POINT('Ctrl Pts',(168.136059776321,-4.40221360110317,132.997463094142));
#28276=CARTESIAN_POINT('Ctrl Pts',(168.128313500237,-4.34104351053483,133.120249789044));
#28277=CARTESIAN_POINT('Ctrl Pts',(168.120567224153,-4.27471675424657,133.240506661721));
#28278=CARTESIAN_POINT('Ctrl Pts',(168.112820948069,-4.20347879624994,133.357779712031));
#28279=CARTESIAN_POINT('Ctrl Pts',(168.105074614803,-4.13224031239089,133.475053628023));
#28280=CARTESIAN_POINT('Ctrl Pts',(168.097328281538,-4.05609075746079,133.589343343552));
#28281=CARTESIAN_POINT('Ctrl Pts',(168.089581948273,-3.97532014717889,133.700221938474));
#28282=CARTESIAN_POINT('Ctrl Pts',(168.08183388027,-3.8945314488789,133.81112536389));
#28283=CARTESIAN_POINT('Ctrl Pts',(168.074085812267,-3.80911986614477,133.918615832685));
#28284=CARTESIAN_POINT('Ctrl Pts',(168.066337744264,-3.71941684405539,134.022298062989));
#28285=CARTESIAN_POINT('Ctrl Pts',(168.058581441522,-3.62961848452657,134.126090488002));
#28286=CARTESIAN_POINT('Ctrl Pts',(168.05082513878,-3.53551983077862,134.226066293187));
#28287=CARTESIAN_POINT('Ctrl Pts',(168.043068836038,-3.43749085847617,134.32186536673));
#28288=CARTESIAN_POINT('Ctrl Pts',(168.035308393524,-3.33940956515953,134.417715571124));
#28289=CARTESIAN_POINT('Ctrl Pts',(168.02754795101,-3.2373940640506,134.509384340727));
#28290=CARTESIAN_POINT('Ctrl Pts',(168.019787508496,-3.13184805820872,134.596551383178));
#28291=CARTESIAN_POINT('Ctrl Pts',(168.01201460823,-3.02613262054841,134.683858353904));
#28292=CARTESIAN_POINT('Ctrl Pts',(168.004241707965,-2.91687566451193,134.766648920223));
#28293=CARTESIAN_POINT('Ctrl Pts',(167.996468807699,-2.80451128648739,134.844645199927));
#28294=CARTESIAN_POINT('Ctrl Pts',(167.988978471937,-2.69623163663488,134.919806118402));
#28295=CARTESIAN_POINT('Ctrl Pts',(167.981488136175,-2.58506682753121,134.99051510207));
#28296=CARTESIAN_POINT('Ctrl Pts',(167.973997800413,-2.471425778021,135.056564479828));
#28297=CARTESIAN_POINT('Ctrl Pts',(167.966223466294,-2.35347599357613,135.125118139819));
#28298=CARTESIAN_POINT('Ctrl Pts',(167.958449132175,-2.23248485924698,135.188869038371));
#28299=CARTESIAN_POINT('Ctrl Pts',(167.950674798056,-2.10888101309144,135.247535601192));
#28300=CARTESIAN_POINT('Ctrl Pts',(167.942910045109,-1.98542949762945,135.306129862718));
#28301=CARTESIAN_POINT('Ctrl Pts',(167.935145292162,-1.85937202685914,135.359652089933));
#28302=CARTESIAN_POINT('Ctrl Pts',(167.927380539215,-1.73116444532265,135.407865013757));
#28303=CARTESIAN_POINT('Ctrl Pts',(167.91962349833,-1.60308420136363,135.456030051825));
#28304=CARTESIAN_POINT('Ctrl Pts',(167.911866457445,-1.47285845999743,135.498896143833));
#28305=CARTESIAN_POINT('Ctrl Pts',(167.90410941656,-1.34096547398435,135.53627298574));
#28306=CARTESIAN_POINT('Ctrl Pts',(167.89635822532,-1.20917194949804,135.57362164148));
#28307=CARTESIAN_POINT('Ctrl Pts',(167.88860703408,-1.07571405753944,135.60548918035));
#28308=CARTESIAN_POINT('Ctrl Pts',(167.88085584284,-0.941087402276455,135.631734392589));
#28309=CARTESIAN_POINT('Ctrl Pts',(167.873107946063,-0.806517966933102,
135.657968449912));
#28310=CARTESIAN_POINT('Ctrl Pts',(167.865360049285,-0.670781139232144,
135.678584858759));
#28311=CARTESIAN_POINT('Ctrl Pts',(167.857612152508,-0.534384756013413,
135.693493055437));
#28312=CARTESIAN_POINT('Ctrl Pts',(167.849865876424,-0.398016903977686,
135.708398133641));
#28313=CARTESIAN_POINT('Ctrl Pts',(167.84211960034,-0.260990159248068,135.717597332224));
#28314=CARTESIAN_POINT('Ctrl Pts',(167.834373324256,-0.123819164296225,
135.721051768844));
#28315=CARTESIAN_POINT('Ctrl Pts',(167.826626990991,0.0133528432206947,
135.724506230963));
#28316=CARTESIAN_POINT('Ctrl Pts',(167.818880657725,0.150668712243327,135.722215836658));
#28317=CARTESIAN_POINT('Ctrl Pts',(167.81113432446,0.287612502185891,135.714193823601));
#28318=CARTESIAN_POINT('Ctrl Pts',(167.803386256457,0.424586959740618,135.706170014071));
#28319=CARTESIAN_POINT('Ctrl Pts',(167.795638188454,0.561188782187678,135.692412054519));
#28320=CARTESIAN_POINT('Ctrl Pts',(167.787890120451,0.69690625353351,135.672985139573));
#28321=CARTESIAN_POINT('Ctrl Pts',(167.780133817709,0.832767967023085,135.65353757747));
#28322=CARTESIAN_POINT('Ctrl Pts',(167.772377514968,0.967743064224729,135.628409079807));
#28323=CARTESIAN_POINT('Ctrl Pts',(167.764621212226,1.10132859198792,135.597716268357));
#28324=CARTESIAN_POINT('Ctrl Pts',(167.756860769712,1.23498541836955,135.56700707523));
#28325=CARTESIAN_POINT('Ctrl Pts',(167.749100327197,1.36725082064779,135.530727754023));
#28326=CARTESIAN_POINT('Ctrl Pts',(167.741339884683,1.49763711642252,135.489044825708));
#28327=CARTESIAN_POINT('Ctrl Pts',(167.733566984418,1.62823271985433,135.447294984256));
#28328=CARTESIAN_POINT('Ctrl Pts',(167.725794084152,1.7569428215368,135.400124336193));
#28329=CARTESIAN_POINT('Ctrl Pts',(167.718021183887,1.88329899159583,135.347747896981));
#28330=CARTESIAN_POINT('Ctrl Pts',(167.710530848125,2.00506179660252,135.297275473263));
#28331=CARTESIAN_POINT('Ctrl Pts',(167.703040512363,2.12463856182078,135.241969303848));
#28332=CARTESIAN_POINT('Ctrl Pts',(167.695550176601,2.24163353704436,135.182061172435));
#28333=CARTESIAN_POINT('Ctrl Pts',(167.687775842482,2.36306441231212,135.119881606011));
#28334=CARTESIAN_POINT('Ctrl Pts',(167.680001508363,2.48209851226058,135.052547255923));
#28335=CARTESIAN_POINT('Ctrl Pts',(167.672227174243,2.59826725112435,134.980266549724));
#28336=CARTESIAN_POINT('Ctrl Pts',(167.664462421296,2.71429282239976,134.908074923036));
#28337=CARTESIAN_POINT('Ctrl Pts',(167.656697668349,2.82745973006033,134.830949273907));
#28338=CARTESIAN_POINT('Ctrl Pts',(167.648932915402,2.93732195779911,134.749144867526));
#28339=CARTESIAN_POINT('Ctrl Pts',(167.641175874517,3.04707506882444,134.667421710434));
#28340=CARTESIAN_POINT('Ctrl Pts',(167.633418833632,3.15352972021036,134.581029275831));
#28341=CARTESIAN_POINT('Ctrl Pts',(167.625661792747,3.25626729647943,134.490267067325));
#28342=CARTESIAN_POINT('Ctrl Pts',(167.617910601507,3.35892739754301,134.399573303308));
#28343=CARTESIAN_POINT('Ctrl Pts',(167.610159410267,3.45787571102379,134.304516582246));
#28344=CARTESIAN_POINT('Ctrl Pts',(167.602408219027,3.5527255469913,134.205437542638));
#28345=CARTESIAN_POINT('Ctrl Pts',(167.59466032225,3.64753506924837,134.106400614264));
#28346=CARTESIAN_POINT('Ctrl Pts',(167.586912425473,3.73824930882739,134.003345049419));
#28347=CARTESIAN_POINT('Ctrl Pts',(167.579164528696,3.82451757371098,133.896649153728));
#28348=CARTESIAN_POINT('Ctrl Pts',(167.571418252612,3.91076779313329,133.789975576518));
#28349=CARTESIAN_POINT('Ctrl Pts',(167.563671976527,3.99257364202647,133.679663486915));
#28350=CARTESIAN_POINT('Ctrl Pts',(167.555925700443,4.06962423074853,133.566124851349));
#28351=CARTESIAN_POINT('Ctrl Pts',(167.548179367178,4.14667538824053,133.452585377668));
#28352=CARTESIAN_POINT('Ctrl Pts',(167.540433033913,4.21897099597718,133.335819634003));
#28353=CARTESIAN_POINT('Ctrl Pts',(167.532686700647,4.2862433126994,133.216268851069));
#28354=CARTESIAN_POINT('Ctrl Pts',(167.524938632644,4.35353069459053,133.096691295566));
#28355=CARTESIAN_POINT('Ctrl Pts',(167.517190564641,4.41579235529187,132.974327800382));
#28356=CARTESIAN_POINT('Ctrl Pts',(167.509442496638,4.47280654989458,132.849644125963));
#28357=CARTESIAN_POINT('Ctrl Pts',(167.501686193897,4.52988133986178,132.724827936251));
#28358=CARTESIAN_POINT('Ctrl Pts',(167.493929891155,4.58169736008899,132.597686997497));
#28359=CARTESIAN_POINT('Ctrl Pts',(167.486173588413,4.62808086931449,132.468707495349));
#28360=CARTESIAN_POINT('Ctrl Pts',(167.478413145899,4.67448913481547,132.339659152957));
#28361=CARTESIAN_POINT('Ctrl Pts',(167.470652703385,4.71545899509354,132.208770664785));
#28362=CARTESIAN_POINT('Ctrl Pts',(167.46289226087,4.75086694470893,132.076542340502));
#28363=CARTESIAN_POINT('Ctrl Pts',(167.455119360605,4.7863317343084,131.944101751574));
#28364=CARTESIAN_POINT('Ctrl Pts',(167.447346460339,4.81621668602879,131.810317410283));
#28365=CARTESIAN_POINT('Ctrl Pts',(167.439573560074,4.84044950068023,131.675699641061));
#28366=CARTESIAN_POINT('Ctrl Pts',(167.432083224312,4.86380139148021,131.545975566831));
#28367=CARTESIAN_POINT('Ctrl Pts',(167.42459288855,4.88190490722373,131.415477912168));
#28368=CARTESIAN_POINT('Ctrl Pts',(167.417102552788,4.89474114144904,131.284664917678));
#28369=CARTESIAN_POINT('Ctrl Pts',(167.409328218669,4.90806406539654,131.148892108742));
#28370=CARTESIAN_POINT('Ctrl Pts',(167.40155388455,4.91575460825063,131.012349488279));
#28371=CARTESIAN_POINT('Ctrl Pts',(167.393779550431,4.91773484396511,130.875543950949));
#28372=CARTESIAN_POINT('Ctrl Pts',(167.386014797484,4.91971263921605,130.738907014216));
#28373=CARTESIAN_POINT('Ctrl Pts',(167.378250044537,4.91599412413756,130.602008192495));
#28374=CARTESIAN_POINT('Ctrl Pts',(167.370485291589,4.90655297785485,130.465360709006));
#28375=CARTESIAN_POINT('Ctrl Pts',(167.362728250704,4.89712120865172,130.328848945724));
#28376=CARTESIAN_POINT('Ctrl Pts',(167.354971209819,4.8819781460325,130.192588411405));
#28377=CARTESIAN_POINT('Ctrl Pts',(167.347214168934,4.86114949897587,130.057093188123));
#28378=CARTESIAN_POINT('Ctrl Pts',(167.339462977694,4.84033655896402,129.921700142843));
#28379=CARTESIAN_POINT('Ctrl Pts',(167.331711786454,4.81384662777197,129.787071644726));
#28380=CARTESIAN_POINT('Ctrl Pts',(167.323960595214,4.78175727886192,129.653717150392));
#28381=CARTESIAN_POINT('Ctrl Pts',(167.316212698437,4.74968156878115,129.520419335274));
#28382=CARTESIAN_POINT('Ctrl Pts',(167.30846480166,4.71201126570212,129.388394826284));
#28383=CARTESIAN_POINT('Ctrl Pts',(167.300716904883,4.66887509126163,129.258143153981));
#28384=CARTESIAN_POINT('Ctrl Pts',(167.292970628799,4.62574793997892,129.127918727519));
#28385=CARTESIAN_POINT('Ctrl Pts',(167.285224352715,4.57715731434078,128.99946677103));
#28386=CARTESIAN_POINT('Ctrl Pts',(167.277478076631,4.52328176992806,128.873271522693));
#28387=CARTESIAN_POINT('Ctrl Pts',(167.269731743365,4.46940582781833,128.747075342812));
#28388=CARTESIAN_POINT('Ctrl Pts',(167.2619854101,4.41024504259584,128.623136263893));
#28389=CARTESIAN_POINT('Ctrl Pts',(167.254239076834,4.34602591346543,128.501918040218));
#28390=CARTESIAN_POINT('Ctrl Pts',(167.246491008831,4.28179240290631,128.380672670561));
#28391=CARTESIAN_POINT('Ctrl Pts',(167.238742940829,4.21249847732859,128.26214971403));
#28392=CARTESIAN_POINT('Ctrl Pts',(167.230994872826,4.13841613564653,128.146787485793));
#28393=CARTESIAN_POINT('Ctrl Pts',(167.223238570084,4.06425505837013,128.031302649207));
#28394=CARTESIAN_POINT('Ctrl Pts',(167.215482267342,3.98529561038756,127.918985580898));
#28395=CARTESIAN_POINT('Ctrl Pts',(167.2077259646,3.90185292205769,127.810245249527));
#28396=CARTESIAN_POINT('Ctrl Pts',(167.199965522086,3.81836569785261,127.701446880166));
#28397=CARTESIAN_POINT('Ctrl Pts',(167.192205079572,3.7303907160241,127.596229351402));
#28398=CARTESIAN_POINT('Ctrl Pts',(167.184444637057,3.6382821435583,127.494967001454));
#28399=CARTESIAN_POINT('Ctrl Pts',(167.176671736792,3.54602571023496,127.393542096192));
#28400=CARTESIAN_POINT('Ctrl Pts',(167.168898836527,3.44962270132345,127.296085335592));
#28401=CARTESIAN_POINT('Ctrl Pts',(167.161125936261,3.3494633877416,127.20293338983));
#28402=CARTESIAN_POINT('Ctrl Pts',(167.153635600499,3.25294511749426,127.113167751932));
#28403=CARTESIAN_POINT('Ctrl Pts',(167.146145264737,3.15293913720184,127.02739958149));
#28404=CARTESIAN_POINT('Ctrl Pts',(167.138654928975,3.04982075826178,126.945892475288));
#28405=CARTESIAN_POINT('Ctrl Pts',(167.130880594856,2.94279261464236,126.861295002381));
#28406=CARTESIAN_POINT('Ctrl Pts',(167.123106260737,2.83207236722314,126.781020109271));
#28407=CARTESIAN_POINT('Ctrl Pts',(167.115331926618,2.71804435990667,126.705407346293));
#28408=CARTESIAN_POINT('Ctrl Pts',(167.107567173671,2.60415688191836,126.629887769288));
#28409=CARTESIAN_POINT('Ctrl Pts',(167.099802420724,2.48697007779855,126.559019104257));
#28410=CARTESIAN_POINT('Ctrl Pts',(167.092037667776,2.36690150970268,126.493100905386));
#28411=CARTESIAN_POINT('Ctrl Pts',(167.084280626891,2.24695219540119,126.427248177399));
#28412=CARTESIAN_POINT('Ctrl Pts',(167.076523586006,2.12412715354412,126.366336317706));
#28413=CARTESIAN_POINT('Ctrl Pts',(167.068766545121,1.99887279227081,126.310621570534));
#28414=CARTESIAN_POINT('Ctrl Pts',(167.061015353881,1.87371288628576,126.254948838286));
#28415=CARTESIAN_POINT('Ctrl Pts',(167.053264162641,1.74612766308127,126.204465575916));
#28416=CARTESIAN_POINT('Ctrl Pts',(167.045512971401,1.61658767329015,126.159381892419));
#28417=CARTESIAN_POINT('Ctrl Pts',(167.037765074624,1.48710274145019,126.11431737069));
#28418=CARTESIAN_POINT('Ctrl Pts',(167.030017177847,1.35566506394611,126.074647991562));
#28419=CARTESIAN_POINT('Ctrl Pts',(167.02226928107,1.22276448717305,126.040535466345));
#28420=CARTESIAN_POINT('Ctrl Pts',(167.014523004986,1.08989171033569,126.006430076732));
#28421=CARTESIAN_POINT('Ctrl Pts',(167.006776728902,0.955557021343663,125.977879326144));
#28422=CARTESIAN_POINT('Ctrl Pts',(166.999030452818,0.820264337144804,125.954994733277));
#28423=CARTESIAN_POINT('Ctrl Pts',(166.991284119552,0.684970654246222,125.932109971481));
#28424=CARTESIAN_POINT('Ctrl Pts',(166.983537786287,0.548719347519155,125.914891516073));
#28425=CARTESIAN_POINT('Ctrl Pts',(166.975791453021,0.412023014928205,125.903399477374));
#28426=CARTESIAN_POINT('Ctrl Pts',(166.968043385019,0.275296070141404,125.891904865113));
#28427=CARTESIAN_POINT('Ctrl Pts',(166.960295317016,0.13812429069425,125.886139254118));
#28428=CARTESIAN_POINT('Ctrl Pts',(166.952547249013,0.00102346560978314,
125.886110724055));
#28429=CARTESIAN_POINT('Ctrl Pts',(166.944790946271,-0.136223071863291,
125.88608216367));
#28430=CARTESIAN_POINT('Ctrl Pts',(166.937034643529,-0.273398112743194,
125.891802864587));
#28431=CARTESIAN_POINT('Ctrl Pts',(166.929278340787,-0.409987244455299,
125.903228756263));
#28432=CARTESIAN_POINT('Ctrl Pts',(166.921517898273,-0.54664927789971,125.91466074628));
#28433=CARTESIAN_POINT('Ctrl Pts',(166.913757455759,-0.682724391351298,
125.931803945695));
#28434=CARTESIAN_POINT('Ctrl Pts',(166.905997013244,-0.81770620755624,125.954562722744));
#28435=CARTESIAN_POINT('Ctrl Pts',(166.898224112979,-0.952904708555676,
125.977358034201));
#28436=CARTESIAN_POINT('Ctrl Pts',(166.890451212714,-1.08700602245833,126.005786856256));
#28437=CARTESIAN_POINT('Ctrl Pts',(166.882678312448,-1.21951594814637,126.039702821384));
#28438=CARTESIAN_POINT('Ctrl Pts',(166.875187976686,-1.34720880426391,126.072385855751));
#28439=CARTESIAN_POINT('Ctrl Pts',(166.867697640924,-1.47342367026775,126.11016392816));
#28440=CARTESIAN_POINT('Ctrl Pts',(166.860207305162,-1.59773590974054,126.152863759003));
#28441=CARTESIAN_POINT('Ctrl Pts',(166.852432913953,-1.72676243303172,126.197182892357));
#28442=CARTESIAN_POINT('Ctrl Pts',(166.844658522745,-1.85414789569075,126.246944837167));
#28443=CARTESIAN_POINT('Ctrl Pts',(166.836884131537,-1.97939886630912,126.302009766005));
#28444=CARTESIAN_POINT('Ctrl Pts',(166.829119334888,-2.10449526175076,126.357006737916));
#28445=CARTESIAN_POINT('Ctrl Pts',(166.821354538239,-2.22746205203118,126.417293516249));
#28446=CARTESIAN_POINT('Ctrl Pts',(166.81358974159,-2.34782150329167,126.482680706793));
#28447=CARTESIAN_POINT('Ctrl Pts',(166.805832670334,-2.46806120587771,126.54800284196));
#28448=CARTESIAN_POINT('Ctrl Pts',(166.798075599079,-2.58569839054954,126.61841510528));
#28449=CARTESIAN_POINT('Ctrl Pts',(166.790318527823,-2.70027617224483,126.693680423716));
#28450=CARTESIAN_POINT('Ctrl Pts',(166.782567319501,-2.81476735399967,126.768888855277));
#28451=CARTESIAN_POINT('Ctrl Pts',(166.774816111179,-2.92620340997121,126.848942827103));
#28452=CARTESIAN_POINT('Ctrl Pts',(166.767064902857,-3.03415322304247,126.933560018));
#28453=CARTESIAN_POINT('Ctrl Pts',(166.759317058284,-3.14205618971799,127.018140488033));
#28454=CARTESIAN_POINT('Ctrl Pts',(166.751569213712,-3.24647561586085,127.107279997354));
#28455=CARTESIAN_POINT('Ctrl Pts',(166.74382136914,-3.34701068383153,127.200653839148));
#28456=CARTESIAN_POINT('Ctrl Pts',(166.736075164187,-3.44752447629983,127.294007920917));
#28457=CARTESIAN_POINT('Ctrl Pts',(166.728328959235,-3.54415525947485,127.391594286795));
#28458=CARTESIAN_POINT('Ctrl Pts',(166.720582754283,-3.63653684047063,127.493049265488));
#28459=CARTESIAN_POINT('Ctrl Pts',(166.712836511089,-3.72891887753324,127.594504745042));
#28460=CARTESIAN_POINT('Ctrl Pts',(166.705090267895,-3.81705140741029,127.6998285864));
#28461=CARTESIAN_POINT('Ctrl Pts',(166.697344024701,-3.90060679718677,127.808622031467));
#28462=CARTESIAN_POINT('Ctrl Pts',(166.68959606574,-3.98418069421321,127.917439573933));
#28463=CARTESIAN_POINT('Ctrl Pts',(166.681848106778,-4.06317519580791,128.029727939255));
#28464=CARTESIAN_POINT('Ctrl Pts',(166.674100147817,-4.13730471913056,128.145057565343));
#28465=CARTESIAN_POINT('Ctrl Pts',(166.666344219302,-4.21151049209885,128.260505819514));
#28466=CARTESIAN_POINT('Ctrl Pts',(166.658588290788,-4.28084107984005,128.379001253493));
#28467=CARTESIAN_POINT('Ctrl Pts',(166.650832362274,-4.34505554027724,128.500087323357));
#28468=CARTESIAN_POINT('Ctrl Pts',(166.64307230181,-4.40930421079557,128.621237901499));
#28469=CARTESIAN_POINT('Ctrl Pts',(166.635312241346,-4.4684311546285,128.744981513072));
#28470=CARTESIAN_POINT('Ctrl Pts',(166.627552180882,-4.52224314406754,128.870840509464));
#28471=CARTESIAN_POINT('Ctrl Pts',(166.619780289522,-4.57613717462138,128.996891388975));
#28472=CARTESIAN_POINT('Ctrl Pts',(166.612008398163,-4.62469992236801,129.125063731427));
#28473=CARTESIAN_POINT('Ctrl Pts',(166.604236506803,-4.66778744933132,129.254862831067));
#28474=CARTESIAN_POINT('Ctrl Pts',(166.597759286667,-4.70369729217216,129.363039503006));
#28475=CARTESIAN_POINT('Ctrl Pts',(166.59128206653,-4.73580502071292,129.472345718229));
#28476=CARTESIAN_POINT('Ctrl Pts',(166.584804846393,-4.76405452823406,129.582490119308));
#28477=CARTESIAN_POINT('Ctrl Pts',(168.33498954974,-4.76405452823405,129.582490119308));
#28478=CARTESIAN_POINT('Ctrl Pts',(168.32728426315,-4.79790534790346,129.714473951441));
#28479=CARTESIAN_POINT('Ctrl Pts',(168.31957897656,-4.82624105686554,129.847763448461));
#28480=CARTESIAN_POINT('Ctrl Pts',(168.311873689969,-4.84898620031437,129.981854756395));
#28481=CARTESIAN_POINT('Ctrl Pts',(168.304037980981,-4.87211633608039,130.118215741083));
#28482=CARTESIAN_POINT('Ctrl Pts',(168.296202271994,-4.88946488867095,130.255405497073));
#28483=CARTESIAN_POINT('Ctrl Pts',(168.288366563006,-4.90100765122071,130.392891219948));
#28484=CARTESIAN_POINT('Ctrl Pts',(168.280530854018,-4.91255041377047,130.530376942823));
#28485=CARTESIAN_POINT('Ctrl Pts',(168.27269514503,-4.91828743264541,130.668158205622));
#28486=CARTESIAN_POINT('Ctrl Pts',(168.264859436042,-4.91824981607796,130.805705663694));
#28487=CARTESIAN_POINT('',(168.610140563953,-4.91824876274648,130.807849205066));
#28488=CARTESIAN_POINT('Ctrl Pts',(168.68000091015,-4.76405452823405,129.582490119308));
#28489=CARTESIAN_POINT('Ctrl Pts',(168.672228899302,-4.79826026490074,129.715857767427));
#28490=CARTESIAN_POINT('Ctrl Pts',(168.664456888454,-4.82687611153899,129.850720065033));
#28491=CARTESIAN_POINT('Ctrl Pts',(168.656684877605,-4.84978382879872,129.986570989103));
#28492=CARTESIAN_POINT('Ctrl Pts',(168.648912706895,-4.87269201724581,130.122424707481));
#28493=CARTESIAN_POINT('Ctrl Pts',(168.641140536184,-4.88989176638913,130.259266713356));
#28494=CARTESIAN_POINT('Ctrl Pts',(168.633368365474,-4.90131605062345,130.396581223284));
#28495=CARTESIAN_POINT('Ctrl Pts',(168.625625764985,-4.91269686970111,130.533373302523));
#28496=CARTESIAN_POINT('Ctrl Pts',(168.617883164497,-4.91834609158011,130.670633913812));
#28497=CARTESIAN_POINT('Ctrl Pts',(168.610140564008,-4.91824876274717,130.807849204087));
#28498=CARTESIAN_POINT('Ctrl Pts',(168.610140563953,-4.91824876274648,130.807849205066));
#28499=CARTESIAN_POINT('Ctrl Pts',(168.601280367312,-4.91813738507152,130.964870667785));
#28500=CARTESIAN_POINT('Ctrl Pts',(168.592420170671,-4.91050237173166,131.121592477866));
#28501=CARTESIAN_POINT('Ctrl Pts',(168.58355997403,-4.8954535172796,131.277348907754));
#28502=CARTESIAN_POINT('Ctrl Pts',(168.574657903986,-4.88033354174772,131.433841444534));
#28503=CARTESIAN_POINT('Ctrl Pts',(168.565755833942,-4.85772959459143,131.589359305109));
#28504=CARTESIAN_POINT('Ctrl Pts',(168.556853763897,-4.82780256547689,131.743245834871));
#28505=CARTESIAN_POINT('Ctrl Pts',(168.547897218697,-4.79769240147487,131.89807405491));
#28506=CARTESIAN_POINT('Ctrl Pts',(168.538940673496,-4.7601693460731,132.05125076968));
#28507=CARTESIAN_POINT('Ctrl Pts',(168.529984128295,-4.71544577824053,132.20212818586));
#28508=CARTESIAN_POINT('Ctrl Pts',(168.523757436157,-4.68435344498441,132.307019882386));
#28509=CARTESIAN_POINT('Ctrl Pts',(168.517530744019,-4.64978198049473,132.410800722358));
#28510=CARTESIAN_POINT('Ctrl Pts',(168.511304051881,-4.61181608600089,132.513259517853));
#28511=CARTESIAN_POINT('Ctrl Pts',(168.503529717762,-4.56441378275859,132.641184408302));
#28512=CARTESIAN_POINT('Ctrl Pts',(168.495755383642,-4.51160969578233,132.767338124264));
#28513=CARTESIAN_POINT('Ctrl Pts',(168.487981049523,-4.45355544969984,132.891230742645));
#28514=CARTESIAN_POINT('Ctrl Pts',(168.480216296576,-4.39557275028721,133.014970674448));
#28515=CARTESIAN_POINT('Ctrl Pts',(168.472451543629,-4.33235293013857,133.136454702548));
#28516=CARTESIAN_POINT('Ctrl Pts',(168.464686790682,-4.26409678933356,133.255209783405));
#28517=CARTESIAN_POINT('Ctrl Pts',(168.456929749797,-4.19590844148999,133.373846915042));
#28518=CARTESIAN_POINT('Ctrl Pts',(168.449172708912,-4.12269392104773,133.489760156541));
#28519=CARTESIAN_POINT('Ctrl Pts',(168.441415668027,-4.0447011931447,133.602498448459));
#28520=CARTESIAN_POINT('Ctrl Pts',(168.433664476787,-3.96676728016439,133.715151723554));
#28521=CARTESIAN_POINT('Ctrl Pts',(168.425913285547,-3.88406255337208,133.824634494463));
#28522=CARTESIAN_POINT('Ctrl Pts',(168.418162094307,-3.7968795955622,133.930522545442));
#28523=CARTESIAN_POINT('Ctrl Pts',(168.41041419753,-3.70973369283501,134.036365591176));
#28524=CARTESIAN_POINT('Ctrl Pts',(168.402666300752,-3.6181135927303,134.138616654568));
#28525=CARTESIAN_POINT('Ctrl Pts',(168.394918403975,-3.52235353319592,134.236882817011));
#28526=CARTESIAN_POINT('Ctrl Pts',(168.387172127891,-3.42661350460165,134.335128424291));
#28527=CARTESIAN_POINT('Ctrl Pts',(168.379425851807,-3.32673551176757,134.429390508785));
#28528=CARTESIAN_POINT('Ctrl Pts',(168.371679575723,-3.22309191885105,134.519311700035));
#28529=CARTESIAN_POINT('Ctrl Pts',(168.363933242458,-3.11944756086106,134.609233555062));
#28530=CARTESIAN_POINT('Ctrl Pts',(168.356186909192,-3.01203784263378,134.694814196693));
#28531=CARTESIAN_POINT('Ctrl Pts',(168.348440575927,-2.90126928397905,134.775735644473));
#28532=CARTESIAN_POINT('Ctrl Pts',(168.340692507924,-2.79047591947359,134.85667521405));
#28533=CARTESIAN_POINT('Ctrl Pts',(168.332944439921,-2.67632253340668,134.932953282958));
#28534=CARTESIAN_POINT('Ctrl Pts',(168.325196371918,-2.5592454361998,135.004294647975));
#28535=CARTESIAN_POINT('Ctrl Pts',(168.317440069176,-2.44204390806084,135.075711835444));
#28536=CARTESIAN_POINT('Ctrl Pts',(168.309683766434,-2.32191279590227,135.142181634232));
#28537=CARTESIAN_POINT('Ctrl Pts',(168.301927463692,-2.19931436203489,135.203474096376));
#28538=CARTESIAN_POINT('Ctrl Pts',(168.294167021178,-2.0766504936919,135.264799272153));
#28539=CARTESIAN_POINT('Ctrl Pts',(168.286406578664,-1.95151703617139,135.320941445213));
#28540=CARTESIAN_POINT('Ctrl Pts',(168.27864613615,-1.82439621023559,135.371718883629));
#28541=CARTESIAN_POINT('Ctrl Pts',(168.270873235884,-1.69707131866469,135.422577834498));
#28542=CARTESIAN_POINT('Ctrl Pts',(168.263100335619,-1.56775305247812,135.468054711526));
#28543=CARTESIAN_POINT('Ctrl Pts',(168.255327435354,-1.43693962500906,135.508017447797));
#28544=CARTESIAN_POINT('Ctrl Pts',(168.247837099591,-1.31088159512657,135.546527437944));
#28545=CARTESIAN_POINT('Ctrl Pts',(168.240346763829,-1.1834355203898,135.579917154768));
#28546=CARTESIAN_POINT('Ctrl Pts',(168.232856428067,-1.05505420101026,135.608113701919));
#28547=CARTESIAN_POINT('Ctrl Pts',(168.225082093948,-0.921805264886874,
135.637379329725));
#28548=CARTESIAN_POINT('Ctrl Pts',(168.217307759829,-0.78712667196695,135.661142920815));
#28549=CARTESIAN_POINT('Ctrl Pts',(168.20953342571,-0.651512565239633,135.679267225885));
#28550=CARTESIAN_POINT('Ctrl Pts',(168.201768672763,-0.516065590778632,
135.697369194369));
#28551=CARTESIAN_POINT('Ctrl Pts',(168.194003919816,-0.37968578031111,135.7098456538));
#28552=CARTESIAN_POINT('Ctrl Pts',(168.186239166869,-0.242879656112835,
135.716609851384));
#28553=CARTESIAN_POINT('Ctrl Pts',(168.178482125984,-0.106209409685695,
135.723367330672));
#28554=CARTESIAN_POINT('Ctrl Pts',(168.170725085099,0.0308859198843273,
135.724423819449));
#28555=CARTESIAN_POINT('Ctrl Pts',(168.162968044214,0.167892812299595,135.719744129163));
#28556=CARTESIAN_POINT('Ctrl Pts',(168.155216852974,0.304796386751348,135.715067967868));
#28557=CARTESIAN_POINT('Ctrl Pts',(168.147465661734,0.441611267636705,135.704664250839));
#28558=CARTESIAN_POINT('Ctrl Pts',(168.139714470493,0.577822402089663,135.688549837298));
#28559=CARTESIAN_POINT('Ctrl Pts',(168.131966573716,0.713975643177067,135.672442272812));
#28560=CARTESIAN_POINT('Ctrl Pts',(168.124218676939,0.849525260761727,135.650628885162));
#28561=CARTESIAN_POINT('Ctrl Pts',(168.116470780162,0.983960017515345,135.623178496095));
#28562=CARTESIAN_POINT('Ctrl Pts',(168.108724504078,1.11836665341593,135.595733849057));
#28563=CARTESIAN_POINT('Ctrl Pts',(168.100978227994,1.25165850952432,135.562654624143));
#28564=CARTESIAN_POINT('Ctrl Pts',(168.09323195191,1.38333364803016,135.5240609344));
#28565=CARTESIAN_POINT('Ctrl Pts',(168.085485618645,1.51500975853188,135.485466959768));
#28566=CARTESIAN_POINT('Ctrl Pts',(168.077739285379,1.64506875243519,135.441358549047));
#28567=CARTESIAN_POINT('Ctrl Pts',(168.069992952114,1.77302336989257,135.391905842664));
#28568=CARTESIAN_POINT('Ctrl Pts',(168.062244884111,1.90100664189935,135.342442061689));
#28569=CARTESIAN_POINT('Ctrl Pts',(168.054496816108,2.02688423509956,135.28763174444));
#28570=CARTESIAN_POINT('Ctrl Pts',(168.046748748105,2.15018877678808,135.227693217165));
#28571=CARTESIAN_POINT('Ctrl Pts',(168.038992445363,2.27362436801094,135.16769098651));
#28572=CARTESIAN_POINT('Ctrl Pts',(168.031236142621,2.39448109274114,135.102549829421));
#28573=CARTESIAN_POINT('Ctrl Pts',(168.02347983988,2.51231562517436,135.032534367781));
#28574=CARTESIAN_POINT('Ctrl Pts',(168.015719397365,2.6302130494455,134.96248153678));
#28575=CARTESIAN_POINT('Ctrl Pts',(168.007958954851,2.74508474001502,134.887549430893));
#28576=CARTESIAN_POINT('Ctrl Pts',(168.000198512337,2.85651714856342,134.808045525556));
#28577=CARTESIAN_POINT('Ctrl Pts',(167.992425612072,2.96812843830649,134.728413993492));
#28578=CARTESIAN_POINT('Ctrl Pts',(167.984652711806,3.07628910457113,134.644196236534));
#28579=CARTESIAN_POINT('Ctrl Pts',(167.976879811541,3.18061873924162,134.555740030273));
#28580=CARTESIAN_POINT('Ctrl Pts',(167.969389475779,3.28115572890079,134.470499429919));
#28581=CARTESIAN_POINT('Ctrl Pts',(167.961899140017,3.37813515974809,134.381323395316));
#28582=CARTESIAN_POINT('Ctrl Pts',(167.954408804255,3.47125095244502,134.288553477849));
#28583=CARTESIAN_POINT('Ctrl Pts',(167.946634470136,3.56789725872451,134.192266160764));
#28584=CARTESIAN_POINT('Ctrl Pts',(167.938860136017,3.66068731010971,134.091802047688));
#28585=CARTESIAN_POINT('Ctrl Pts',(167.931085801898,3.74923853851688,133.987502688508));
#28586=CARTESIAN_POINT('Ctrl Pts',(167.923321048951,3.83768063544908,133.883331868967));
#28587=CARTESIAN_POINT('Ctrl Pts',(167.915556296004,3.92189405293988,133.775335503021));
#28588=CARTESIAN_POINT('Ctrl Pts',(167.907791543056,4.00153201574385,133.663892850201));
#28589=CARTESIAN_POINT('Ctrl Pts',(167.900034502171,4.08109088100043,133.552560883795));
#28590=CARTESIAN_POINT('Ctrl Pts',(167.892277461286,4.15608310930224,133.437789758276));
#28591=CARTESIAN_POINT('Ctrl Pts',(167.884520420401,4.22620152525857,133.319992492543));
#28592=CARTESIAN_POINT('Ctrl Pts',(167.876769229161,4.29626706437197,133.202284058645));
#28593=CARTESIAN_POINT('Ctrl Pts',(167.869018037921,4.36146590759516,133.081554361378));
#28594=CARTESIAN_POINT('Ctrl Pts',(167.861266846681,4.4215338404127,132.958245842128));
#28595=CARTESIAN_POINT('Ctrl Pts',(167.853518949904,4.48157624275646,132.834989732287));
#28596=CARTESIAN_POINT('Ctrl Pts',(167.845771053127,4.5364919012276,132.709157331202));
#28597=CARTESIAN_POINT('Ctrl Pts',(167.83802315635,4.58606238124673,132.581215957152));
#28598=CARTESIAN_POINT('Ctrl Pts',(167.830276880266,4.63562249219005,132.453301345678));
#28599=CARTESIAN_POINT('Ctrl Pts',(167.822530604182,4.67983950747819,132.323279003041));
#28600=CARTESIAN_POINT('Ctrl Pts',(167.814784328098,4.71854317197448,132.191636147774));
#28601=CARTESIAN_POINT('Ctrl Pts',(167.807037994832,4.75724712217241,132.059992320749));
#28602=CARTESIAN_POINT('Ctrl Pts',(167.799291661567,4.79043753008965,131.926728332313));
#28603=CARTESIAN_POINT('Ctrl Pts',(167.791545328302,4.81799416383687,131.792346093033));
#28604=CARTESIAN_POINT('Ctrl Pts',(167.783797260299,4.84555696870114,131.657933759783));
#28605=CARTESIAN_POINT('Ctrl Pts',(167.776049192296,4.86748341034595,131.522403060295));
#28606=CARTESIAN_POINT('Ctrl Pts',(167.768301124293,4.8837045464661,131.386265219134));
#28607=CARTESIAN_POINT('Ctrl Pts',(167.760544821551,4.89994292260276,131.249982689056));
#28608=CARTESIAN_POINT('Ctrl Pts',(167.752788518809,4.9104638340566,131.113092117132));
#28609=CARTESIAN_POINT('Ctrl Pts',(167.745032216067,4.91525028628631,130.97610952051));
#28610=CARTESIAN_POINT('Ctrl Pts',(167.737271773553,4.92003929318968,130.839053812151));
#28611=CARTESIAN_POINT('Ctrl Pts',(167.729511331039,4.91908774496876,130.701906371988));
#28612=CARTESIAN_POINT('Ctrl Pts',(167.721750888525,4.91243079644946,130.565181327921));
#28613=CARTESIAN_POINT('Ctrl Pts',(167.713977988259,4.90576316160543,130.428236800676));
#28614=CARTESIAN_POINT('Ctrl Pts',(167.706205087994,4.8933718595932,130.291716414109));
#28615=CARTESIAN_POINT('Ctrl Pts',(167.698432187728,4.87534386398892,130.156128197546));
#28616=CARTESIAN_POINT('Ctrl Pts',(167.690941851966,4.85797123143446,130.025468954179));
#28617=CARTESIAN_POINT('Ctrl Pts',(167.683451516204,4.83536465915356,129.895675587456));
#28618=CARTESIAN_POINT('Ctrl Pts',(167.675961180442,4.80764606064002,129.76719022746));
#28619=CARTESIAN_POINT('Ctrl Pts',(167.668186846323,4.77887650303921,129.633833305989));
#28620=CARTESIAN_POINT('Ctrl Pts',(167.660412512204,4.74450848871262,129.501463100717));
#28621=CARTESIAN_POINT('Ctrl Pts',(167.652638178085,4.70462258586134,129.370586093067));
#28622=CARTESIAN_POINT('Ctrl Pts',(167.644873425138,4.66478583882064,129.239870379632));
#28623=CARTESIAN_POINT('Ctrl Pts',(167.63710867219,4.6194448467148,129.110644572697));
#28624=CARTESIAN_POINT('Ctrl Pts',(167.629343919243,4.56873125083833,128.983405423138));
#28625=CARTESIAN_POINT('Ctrl Pts',(167.621586878358,4.51806802442023,128.856292649297));
#28626=CARTESIAN_POINT('Ctrl Pts',(167.613829837473,4.46204295721851,128.731162966953));
#28627=CARTESIAN_POINT('Ctrl Pts',(167.606072796588,4.40083749792711,128.608498058265));
#28628=CARTESIAN_POINT('Ctrl Pts',(167.598321605348,4.33967819414871,128.485925652139));
#28629=CARTESIAN_POINT('Ctrl Pts',(167.590570414108,4.27334644792807,128.365814668449));
#28630=CARTESIAN_POINT('Ctrl Pts',(167.582819222868,4.20207168333242,128.248626548725));
#28631=CARTESIAN_POINT('Ctrl Pts',(167.575071326091,4.13082721241299,128.131488237077));
#28632=CARTESIAN_POINT('Ctrl Pts',(167.567323429314,4.05464410441463,128.017270651899));
#28633=CARTESIAN_POINT('Ctrl Pts',(167.559575532537,3.9737974582142,127.906410165334));
#28634=CARTESIAN_POINT('Ctrl Pts',(167.551829256453,3.8929677233893,127.795572868393));
#28635=CARTESIAN_POINT('Ctrl Pts',(167.544082980368,3.8074766209286,127.688091588973));
#28636=CARTESIAN_POINT('Ctrl Pts',(167.536336704284,3.71764203452229,127.58437292106));
#28637=CARTESIAN_POINT('Ctrl Pts',(167.528590371019,3.62780678497748,127.480653487519));
#28638=CARTESIAN_POINT('Ctrl Pts',(167.520844037754,3.53362824347411,127.380697016434));
#28639=CARTESIAN_POINT('Ctrl Pts',(167.513097704488,3.43546369331372,127.284875957218));
#28640=CARTESIAN_POINT('Ctrl Pts',(167.505349636485,3.33727715988305,127.189033439541));
#28641=CARTESIAN_POINT('Ctrl Pts',(167.497601568482,3.23510312126705,127.097328449602));
#28642=CARTESIAN_POINT('Ctrl Pts',(167.489853500479,3.12933442017091,127.010095319879));
#28643=CARTESIAN_POINT('Ctrl Pts',(167.482097197737,3.02345330684048,126.922769477747));
#28644=CARTESIAN_POINT('Ctrl Pts',(167.474340894996,2.91397020136689,126.839925239111));
#28645=CARTESIAN_POINT('Ctrl Pts',(167.466584592254,2.80131005762509,126.76185582183));
#28646=CARTESIAN_POINT('Ctrl Pts',(167.45882414974,2.68858978377239,126.683744736551));
#28647=CARTESIAN_POINT('Ctrl Pts',(167.451063707225,2.57268942309025,126.610413759598));
#28648=CARTESIAN_POINT('Ctrl Pts',(167.443303264711,2.45406052798238,126.542111212909));
#28649=CARTESIAN_POINT('Ctrl Pts',(167.435530364446,2.3352411992407,126.473699020908));
#28650=CARTESIAN_POINT('Ctrl Pts',(167.42775746418,2.21368493015196,126.410331570596));
#28651=CARTESIAN_POINT('Ctrl Pts',(167.419984563915,2.08986615151655,126.352210290899));
#28652=CARTESIAN_POINT('Ctrl Pts',(167.412494228153,1.97054849736614,126.296201866117));
#28653=CARTESIAN_POINT('Ctrl Pts',(167.405003892391,1.84913025749133,126.245064930536));
#28654=CARTESIAN_POINT('Ctrl Pts',(167.397513556629,1.72604930567319,126.198935896991));
#28655=CARTESIAN_POINT('Ctrl Pts',(167.38973922251,1.59830170215628,126.151057867117));
#28656=CARTESIAN_POINT('Ctrl Pts',(167.381964888391,1.46835814831326,126.108423321652));
#28657=CARTESIAN_POINT('Ctrl Pts',(167.374190554272,1.33668831038928,126.071238241864));
#28658=CARTESIAN_POINT('Ctrl Pts',(167.366425801325,1.20518074377299,126.034098989364));
#28659=CARTESIAN_POINT('Ctrl Pts',(167.358661048377,1.07195149878536,126.002395944983));
#28660=CARTESIAN_POINT('Ctrl Pts',(167.35089629543,0.937489661342259,125.976286861152));
#28661=CARTESIAN_POINT('Ctrl Pts',(167.343139254545,0.80316137329168,125.950203709231));
#28662=CARTESIAN_POINT('Ctrl Pts',(167.33538221366,0.667603310368305,125.929703535211));
#28663=CARTESIAN_POINT('Ctrl Pts',(167.327625172775,0.531318802865246,125.914894042139));
#28664=CARTESIAN_POINT('Ctrl Pts',(167.319873981535,0.395137068569294,125.90009571702));
#28665=CARTESIAN_POINT('Ctrl Pts',(167.312122790295,0.258230367195635,125.89097957317));
#28666=CARTESIAN_POINT('Ctrl Pts',(167.304371599055,0.121110931884357,125.88760201004));
#28667=CARTESIAN_POINT('Ctrl Pts',(167.296623702278,-0.0159502240090409,
125.884225882465));
#28668=CARTESIAN_POINT('Ctrl Pts',(167.288875805501,-0.153223543977972,
125.886583494134));
#28669=CARTESIAN_POINT('Ctrl Pts',(167.281127908724,-0.290193198117832,
125.894679266372));
#28670=CARTESIAN_POINT('Ctrl Pts',(167.27338163264,-0.427134201158817,125.902773345148));
#28671=CARTESIAN_POINT('Ctrl Pts',(167.265635356555,-0.563771274679385,
125.91660317398));
#28672=CARTESIAN_POINT('Ctrl Pts',(167.257889080471,-0.699590515744292,
125.936121082294));
#28673=CARTESIAN_POINT('Ctrl Pts',(167.250142747206,-0.835410759395936,
125.955639134686));
#28674=CARTESIAN_POINT('Ctrl Pts',(167.242396413941,-0.970412771555679,
125.980845294734));
#28675=CARTESIAN_POINT('Ctrl Pts',(167.234650080675,-1.104090079631,126.011640287883));
#28676=CARTESIAN_POINT('Ctrl Pts',(167.226902012672,-1.23779732381261,126.042442177357));
#28677=CARTESIAN_POINT('Ctrl Pts',(167.219153944669,-1.37017889268054,126.078835302682));
#28678=CARTESIAN_POINT('Ctrl Pts',(167.211405876666,-1.50074116177388,126.120669869037));
#28679=CARTESIAN_POINT('Ctrl Pts',(167.203649573924,-1.63144219400052,126.162548897666));
#28680=CARTESIAN_POINT('Ctrl Pts',(167.195893271183,-1.76031969101819,126.209880800458));
#28681=CARTESIAN_POINT('Ctrl Pts',(167.188136968441,-1.88689726238662,126.262466543097));
#28682=CARTESIAN_POINT('Ctrl Pts',(167.180376525927,-2.01354239201624,126.31508035233));
#28683=CARTESIAN_POINT('Ctrl Pts',(167.172616083412,-2.13788479574006,126.372953423989));
#28684=CARTESIAN_POINT('Ctrl Pts',(167.164855640898,-2.25947147817604,126.435840078321));
#28685=CARTESIAN_POINT('Ctrl Pts',(167.157082740633,-2.38125334234854,126.498827683892));
#28686=CARTESIAN_POINT('Ctrl Pts',(167.149309840367,-2.50027030557501,126.566844760999));
#28687=CARTESIAN_POINT('Ctrl Pts',(167.141536940102,-2.61609645855909,126.639601034827));
#28688=CARTESIAN_POINT('Ctrl Pts',(167.13404660434,-2.72771203913334,126.709712434839));
#28689=CARTESIAN_POINT('Ctrl Pts',(167.126556268578,-2.8363645157687,126.784224276019));
#28690=CARTESIAN_POINT('Ctrl Pts',(167.119065932816,-2.94170243901029,126.862841897222));
#28691=CARTESIAN_POINT('Ctrl Pts',(167.111199886046,-3.05232405293764,126.945402933865));
#28692=CARTESIAN_POINT('Ctrl Pts',(167.103333839276,-3.15966371172855,127.032771436361));
#28693=CARTESIAN_POINT('Ctrl Pts',(167.095467792506,-3.26327073246246,127.124653130665));
#28694=CARTESIAN_POINT('Ctrl Pts',(167.087781493189,-3.36451022366116,127.214435231491));
#28695=CARTESIAN_POINT('Ctrl Pts',(167.080095193872,-3.46218547176523,127.30852623909));
#28696=CARTESIAN_POINT('Ctrl Pts',(167.072408894555,-3.55590447501027,127.406607473634));
#28697=CARTESIAN_POINT('Ctrl Pts',(167.064729576481,-3.64953835600144,127.504599623836));
#28698=CARTESIAN_POINT('Ctrl Pts',(167.057050258406,-3.73922286352088,127.60657450746));
#28699=CARTESIAN_POINT('Ctrl Pts',(167.049370940332,-3.82460012110788,127.712174178148));
#28700=CARTESIAN_POINT('Ctrl Pts',(167.041696852393,-3.90991923100195,127.81770192831));
#28701=CARTESIAN_POINT('Ctrl Pts',(167.034022764454,-3.99093667579042,127.926849245719));
#28702=CARTESIAN_POINT('Ctrl Pts',(167.026348676516,-4.06733278223542,128.039222808875));
#28703=CARTESIAN_POINT('Ctrl Pts',(167.018343021001,-4.14702966813711,128.156451597853));
#28704=CARTESIAN_POINT('Ctrl Pts',(167.010337365487,-4.22169662929612,128.277191330639));
#28705=CARTESIAN_POINT('Ctrl Pts',(167.002331709972,-4.29101887596182,128.400958847441));
#28706=CARTESIAN_POINT('Ctrl Pts',(166.994661686735,-4.35743482925626,128.519537485767));
#28707=CARTESIAN_POINT('Ctrl Pts',(166.986991663498,-4.41894493693751,128.640894790965));
#28708=CARTESIAN_POINT('Ctrl Pts',(166.979321640262,-4.47531821493297,128.764578781783));
#28709=CARTESIAN_POINT('Ctrl Pts',(166.971651727104,-4.53169068387077,128.888260997515));
#28710=CARTESIAN_POINT('Ctrl Pts',(166.963981813945,-4.58292631008536,129.014269466317));
#28711=CARTESIAN_POINT('Ctrl Pts',(166.956311900787,-4.62884177147018,129.142131115604));
#28712=CARTESIAN_POINT('Ctrl Pts',(166.948638803841,-4.67477629240354,129.270045840375));
#28713=CARTESIAN_POINT('Ctrl Pts',(166.940965706896,-4.71538611344544,129.399814902524));
#28714=CARTESIAN_POINT('Ctrl Pts',(166.93329260995,-4.75053746781127,129.530949124991));
#28715=CARTESIAN_POINT('Ctrl Pts',(166.932288676747,-4.75513660320975,129.548106473702));
#28716=CARTESIAN_POINT('Ctrl Pts',(166.931284743544,-4.75964236840377,129.565287175094));
#28717=CARTESIAN_POINT('Ctrl Pts',(166.930280810341,-4.76405452823404,129.582490119308));
#28718=CARTESIAN_POINT('Origin',(213.235140564004,0.,130.804360617566));
#28719=CARTESIAN_POINT('',(164.834593643846,-4.76405452823404,129.582490119308));
#28720=CARTESIAN_POINT('',(165.180124424339,-4.76405452823406,129.582490119308));
#28721=CARTESIAN_POINT('',(213.235140564004,-4.76405452823405,129.582490119308));
#28722=CARTESIAN_POINT('',(166.514859436034,-4.91824789572956,130.799811040474));
#28723=CARTESIAN_POINT('Ctrl Pts',(166.514859435991,-4.91824789573026,130.799811041232));
#28724=CARTESIAN_POINT('Ctrl Pts',(166.50719928455,-4.91837301695292,130.935071369845));
#28725=CARTESIAN_POINT('Ctrl Pts',(166.499539133109,-4.91291410273851,131.070483954823));
#28726=CARTESIAN_POINT('Ctrl Pts',(166.491878981668,-4.9018603121385,131.205544543941));
#28727=CARTESIAN_POINT('Ctrl Pts',(166.484022026496,-4.89052252881979,131.344075094204));
#28728=CARTESIAN_POINT('Ctrl Pts',(166.476165071324,-4.87329844142217,131.48223488994));
#28729=CARTESIAN_POINT('Ctrl Pts',(166.468308116152,-4.85023337199573,131.619479811107));
#28730=CARTESIAN_POINT('Ctrl Pts',(166.460655682011,-4.82776869950276,131.753152168573));
#28731=CARTESIAN_POINT('Ctrl Pts',(166.45300324787,-4.79976345135041,131.885956273128));
#28732=CARTESIAN_POINT('Ctrl Pts',(166.44535081373,-4.76631191956373,132.017395550255));
#28733=CARTESIAN_POINT('Ctrl Pts',(166.43769924852,-4.73286418618494,132.148819902506));
#28734=CARTESIAN_POINT('Ctrl Pts',(166.43004768331,-4.69397149780892,132.278879346447));
#28735=CARTESIAN_POINT('Ctrl Pts',(166.4223961181,-4.64977882485534,132.407089522411));
#28736=CARTESIAN_POINT('Ctrl Pts',(166.414743667661,-4.60558103913832,132.535314531339));
#28737=CARTESIAN_POINT('Ctrl Pts',(166.407091217222,-4.55608218060183,132.661689467338));
#28738=CARTESIAN_POINT('Ctrl Pts',(166.399438766784,-4.50147627089817,132.785747617887));
#28739=CARTESIAN_POINT('Ctrl Pts',(166.39142820768,-4.44431499026091,132.915611268128));
#28740=CARTESIAN_POINT('Ctrl Pts',(166.383417648576,-4.38155730016116,133.042935601766));
#28741=CARTESIAN_POINT('Ctrl Pts',(166.375407089472,-4.31348037665624,133.167212729464));
#28742=CARTESIAN_POINT('Ctrl Pts',(166.367743386369,-4.24835117367229,133.286108676275));
#28743=CARTESIAN_POINT('Ctrl Pts',(166.360079683266,-4.17835399115401,133.402215459577));
#28744=CARTESIAN_POINT('Ctrl Pts',(166.352415980163,-4.10377613867891,133.515117793358));
#28745=CARTESIAN_POINT('Ctrl Pts',(166.344747105723,-4.02914796232981,133.628096311726));
#28746=CARTESIAN_POINT('Ctrl Pts',(166.337078231283,-3.94993319759305,133.737865752398));
#28747=CARTESIAN_POINT('Ctrl Pts',(166.329409356843,-3.86645964211029,133.844043643546));
#28748=CARTESIAN_POINT('Ctrl Pts',(166.321729972862,-3.78287169321013,133.950367042475));
#28749=CARTESIAN_POINT('Ctrl Pts',(166.314050588881,-3.69501357024591,134.05308877026));
#28750=CARTESIAN_POINT('Ctrl Pts',(166.3063712049,-3.60325019743161,134.151862832234));
#28751=CARTESIAN_POINT('Ctrl Pts',(166.305351489112,-3.59106529298784,134.164978659059));
#28752=CARTESIAN_POINT('Ctrl Pts',(166.304331773324,-3.57881157822753,134.178024938227));
#28753=CARTESIAN_POINT('Ctrl Pts',(166.303312057536,-3.56648995038607,134.191000913832));
#28754=CARTESIAN_POINT('Ctrl Pts',(166.295537723417,-3.47254960653709,134.28993001848));
#28755=CARTESIAN_POINT('Ctrl Pts',(166.287763389298,-3.37434113002548,134.385104210327));
#28756=CARTESIAN_POINT('Ctrl Pts',(166.279989055179,-3.27219679180351,134.476132835203));
#28757=CARTESIAN_POINT('Ctrl Pts',(166.272224302232,-3.17017833734954,134.567049275435));
#28758=CARTESIAN_POINT('Ctrl Pts',(166.264459549285,-3.06423396150634,134.653830056546));
#28759=CARTESIAN_POINT('Ctrl Pts',(166.256694796338,-2.95473449293845,134.73611940197));
#28760=CARTESIAN_POINT('Ctrl Pts',(166.248937755453,-2.84534378078619,134.818327016457));
#28761=CARTESIAN_POINT('Ctrl Pts',(166.241180714568,-2.73240531321915,134.896051839404));
#28762=CARTESIAN_POINT('Ctrl Pts',(166.233423673683,-2.61632461883319,134.968976872563));
#28763=CARTESIAN_POINT('Ctrl Pts',(166.225672482442,-2.50033146180196,135.041846912388));
#28764=CARTESIAN_POINT('Ctrl Pts',(166.217921291202,-2.38120112416977,135.109924159801));
#28765=CARTESIAN_POINT('Ctrl Pts',(166.210170099962,-2.25936957948818,135.172933859001));
#28766=CARTESIAN_POINT('Ctrl Pts',(166.202422203185,-2.13758981646312,135.235916777398));
#28767=CARTESIAN_POINT('Ctrl Pts',(166.194674306408,-2.01311147638515,135.293836252184));
#28768=CARTESIAN_POINT('Ctrl Pts',(166.186926409631,-1.88639650112873,135.346462697334));
#28769=CARTESIAN_POINT('Ctrl Pts',(166.179180133547,-1.75970803191326,135.399078134165));
#28770=CARTESIAN_POINT('Ctrl Pts',(166.171433857463,-1.63078421894571,135.446402593758));
#28771=CARTESIAN_POINT('Ctrl Pts',(166.163687581379,-1.50010805479801,135.488254178102));
#28772=CARTESIAN_POINT('Ctrl Pts',(166.155941248113,-1.3694309260286,135.530106071385));
#28773=CARTESIAN_POINT('Ctrl Pts',(166.148194914848,-1.23700179260285,135.566484889558));
#28774=CARTESIAN_POINT('Ctrl Pts',(166.140448581583,-1.10331953531569,135.597258390885));
#28775=CARTESIAN_POINT('Ctrl Pts',(166.13270051358,-0.969607340813889,135.628038783725));
#28776=CARTESIAN_POINT('Ctrl Pts',(166.124952445577,-0.834641844960347,
135.653211274185));
#28777=CARTESIAN_POINT('Ctrl Pts',(166.117204377574,-0.698932470674764,
135.672694671833));
#28778=CARTESIAN_POINT('Ctrl Pts',(166.109448074832,-0.56307886285132,135.692198776668));
#28779=CARTESIAN_POINT('Ctrl Pts',(166.10169177209,-0.426480184895817,135.706001654637));
#28780=CARTESIAN_POINT('Ctrl Pts',(166.093935469348,-0.289651897532332,
135.714073933102));
#28781=CARTESIAN_POINT('Ctrl Pts',(166.086175026834,-0.152750580792108,
135.722150519986));
#28782=CARTESIAN_POINT('Ctrl Pts',(166.07841458432,-0.0156198011707654,
135.724490406195));
#28783=CARTESIAN_POINT('Ctrl Pts',(166.070654141806,0.121225617870744,135.721116398777));
#28784=CARTESIAN_POINT('Ctrl Pts',(166.06288124154,0.258290713327604,135.717736975103));
#28785=CARTESIAN_POINT('Ctrl Pts',(166.055108341275,0.395069142477458,135.708625354329));
#28786=CARTESIAN_POINT('Ctrl Pts',(166.047335441009,0.531050935170631,135.693856293682));
#28787=CARTESIAN_POINT('Ctrl Pts',(166.039845105247,0.66208944718171,135.67962412559));
#28788=CARTESIAN_POINT('Ctrl Pts',(166.032354769485,0.792387932021461,135.660138746365));
#28789=CARTESIAN_POINT('Ctrl Pts',(166.024864433723,0.921501461342684,135.63551142449));
#28790=CARTESIAN_POINT('Ctrl Pts',(166.017090099604,1.05551036937161,135.609950350221));
#28791=CARTESIAN_POINT('Ctrl Pts',(166.009315765485,1.18866719287546,135.578768752975));
#28792=CARTESIAN_POINT('Ctrl Pts',(166.001541431366,1.3204636628719,135.542035023594));
#28793=CARTESIAN_POINT('Ctrl Pts',(165.993776678419,1.45209770549798,135.505346565252));
#28794=CARTESIAN_POINT('Ctrl Pts',(165.986011925472,1.58237435738474,135.463119693283));
#28795=CARTESIAN_POINT('Ctrl Pts',(165.978247172525,1.71079385168009,135.415474090422));
#28796=CARTESIAN_POINT('Ctrl Pts',(165.97049013164,1.83908579792323,135.367875809845));
#28797=CARTESIAN_POINT('Ctrl Pts',(165.962733090755,1.96552389314472,135.314869643834));
#28798=CARTESIAN_POINT('Ctrl Pts',(165.95497604987,2.08962223963026,135.256625429787));
#28799=CARTESIAN_POINT('Ctrl Pts',(165.94722485863,2.21362700258758,135.198425138155));
#28800=CARTESIAN_POINT('Ctrl Pts',(165.93947366739,2.33529517629466,135.134994826264));
#28801=CARTESIAN_POINT('Ctrl Pts',(165.931722476149,2.4541599465604,135.06655277879));
#28802=CARTESIAN_POINT('Ctrl Pts',(165.923974579372,2.57297419612779,134.998139821012));
#28803=CARTESIAN_POINT('Ctrl Pts',(165.916226682595,2.68898707399475,134.924719558978));
#28804=CARTESIAN_POINT('Ctrl Pts',(165.908478785818,2.80175573206886,134.846556540616));
#28805=CARTESIAN_POINT('Ctrl Pts',(165.900732509734,2.91450080137084,134.768409872272));
#28806=CARTESIAN_POINT('Ctrl Pts',(165.89298623365,3.02400267957236,134.685522643484));
#28807=CARTESIAN_POINT('Ctrl Pts',(165.885239957566,3.12984726144414,134.598202889265));
#28808=CARTESIAN_POINT('Ctrl Pts',(165.877493624301,3.23569262463666,134.510882490471));
#28809=CARTESIAN_POINT('Ctrl Pts',(165.869747291035,3.33788033604528,134.419129749757));
#28810=CARTESIAN_POINT('Ctrl Pts',(165.86200095777,3.43602947969742,134.323292909775));
#28811=CARTESIAN_POINT('Ctrl Pts',(165.854252889767,3.53420060316946,134.227434607797));
#28812=CARTESIAN_POINT('Ctrl Pts',(165.846504821764,3.62833107953929,134.12749065968));
#28813=CARTESIAN_POINT('Ctrl Pts',(165.838756753761,3.71807724546604,134.023845771942));
#28814=CARTESIAN_POINT('Ctrl Pts',(165.831000451019,3.80791879468609,133.920090729184));
#28815=CARTESIAN_POINT('Ctrl Pts',(165.823244148277,3.89336646888192,133.81262718544));
#28816=CARTESIAN_POINT('Ctrl Pts',(165.815487845536,3.9741169369108,133.70187293579));
#28817=CARTESIAN_POINT('Ctrl Pts',(165.807727403021,4.05491050389588,133.591059573262));
#28818=CARTESIAN_POINT('Ctrl Pts',(165.799966960507,4.13100165242269,133.476952330271));
#28819=CARTESIAN_POINT('Ctrl Pts',(165.792206517993,4.20213129605263,133.359996670144));
#28820=CARTESIAN_POINT('Ctrl Pts',(165.784433617728,4.27337512330112,133.242853262408));
#28821=CARTESIAN_POINT('Ctrl Pts',(165.776660717462,4.33964134064374,133.122852642606));
#28822=CARTESIAN_POINT('Ctrl Pts',(165.768887817197,4.40071719213011,133.000464271174));
#28823=CARTESIAN_POINT('Ctrl Pts',(165.761397481435,4.45957278257376,132.882525025322));
#28824=CARTESIAN_POINT('Ctrl Pts',(165.753907145673,4.51360869495033,132.762368896355));
#28825=CARTESIAN_POINT('Ctrl Pts',(165.746416809911,4.5626780479461,132.640430358423));
#28826=CARTESIAN_POINT('Ctrl Pts',(165.738642475792,4.61360788037535,132.513868483762));
#28827=CARTESIAN_POINT('Ctrl Pts',(165.730868141673,4.65934843514372,132.384985461987));
#28828=CARTESIAN_POINT('Ctrl Pts',(165.723093807554,4.69968251960326,132.254245881108));
#28829=CARTESIAN_POINT('Ctrl Pts',(165.715329054606,4.73996689590845,132.123667425077));
#28830=CARTESIAN_POINT('Ctrl Pts',(165.707564301659,4.77485794512297,131.991237332471));
#28831=CARTESIAN_POINT('Ctrl Pts',(165.699799548712,4.80418622352931,131.857440762736));
#28832=CARTESIAN_POINT('Ctrl Pts',(165.692042507827,4.83348537267611,131.72377708164));
#28833=CARTESIAN_POINT('Ctrl Pts',(165.684285466942,4.85723266288805,131.588750003741));
#28834=CARTESIAN_POINT('Ctrl Pts',(165.676528426057,4.87530834359445,131.452860129808));
#28835=CARTESIAN_POINT('Ctrl Pts',(165.668777234817,4.89337039328945,131.317072731486));
#28836=CARTESIAN_POINT('Ctrl Pts',(165.661026043577,4.90576929525523,131.180424218176));
#28837=CARTESIAN_POINT('Ctrl Pts',(165.653274852337,4.91243637409762,131.043425322076));
#28838=CARTESIAN_POINT('Ctrl Pts',(165.64552695556,4.91910061925364,130.906484654162));
#28839=CARTESIAN_POINT('Ctrl Pts',(165.637779058782,4.92003786769394,130.769194289339));
#28840=CARTESIAN_POINT('Ctrl Pts',(165.630031162005,4.91523132087079,130.632069802864));
#28841=CARTESIAN_POINT('Ctrl Pts',(165.622284885921,4.91042577947363,130.494973999875));
#28842=CARTESIAN_POINT('Ctrl Pts',(165.614538609837,4.89987884630609,130.358044396697));
#28843=CARTESIAN_POINT('Ctrl Pts',(165.606792333753,4.88362584595713,130.221795892235));
#28844=CARTESIAN_POINT('Ctrl Pts',(165.599046000488,4.86737272563222,130.085546382018));
#28845=CARTESIAN_POINT('Ctrl Pts',(165.591299667222,4.84541350038635,129.949978368762));
#28846=CARTESIAN_POINT('Ctrl Pts',(165.583553333957,4.81783526223934,129.815600561524));
#28847=CARTESIAN_POINT('Ctrl Pts',(165.575805265954,4.79025084813711,129.681192661309));
#28848=CARTESIAN_POINT('Ctrl Pts',(165.568057197951,4.75704499576905,129.547975880401));
#28849=CARTESIAN_POINT('Ctrl Pts',(165.560309129948,4.7183556111945,129.416447295773));
#28850=CARTESIAN_POINT('Ctrl Pts',(165.552552827206,4.67962510708158,129.284778921001));
#28851=CARTESIAN_POINT('Ctrl Pts',(165.544796524464,4.63539953928269,129.15480270236));
#28852=CARTESIAN_POINT('Ctrl Pts',(165.537040221722,4.58586645273807,129.026999669376));
#28853=CARTESIAN_POINT('Ctrl Pts',(165.529279779208,4.53630692889376,128.899128424065));
#28854=CARTESIAN_POINT('Ctrl Pts',(165.521519336694,4.48143439808903,128.773433033736));
#28855=CARTESIAN_POINT('Ctrl Pts',(165.51375889418,4.42148359868764,128.650372258954));
#28856=CARTESIAN_POINT('Ctrl Pts',(165.505985993914,4.36143656094079,128.527113936092));
#28857=CARTESIAN_POINT('Ctrl Pts',(165.498213093649,4.29629515002293,128.406499024503));
#28858=CARTESIAN_POINT('Ctrl Pts',(165.490440193383,4.22633933650766,128.288960276629));
#28859=CARTESIAN_POINT('Ctrl Pts',(165.482949857621,4.15892659302169,128.175694358301));
#28860=CARTESIAN_POINT('Ctrl Pts',(165.475459521859,4.0870435692621,128.065285092158));
#28861=CARTESIAN_POINT('Ctrl Pts',(165.467969186097,4.01097640770038,127.958090897499));
#28862=CARTESIAN_POINT('Ctrl Pts',(165.460194851978,3.9320251365881,127.846832402369));
#28863=CARTESIAN_POINT('Ctrl Pts',(165.452420517859,3.84831608733918,127.73868515679));
#28864=CARTESIAN_POINT('Ctrl Pts',(165.44464618374,3.76012273307307,127.634083012256));
#28865=CARTESIAN_POINT('Ctrl Pts',(165.436881430793,3.6720380692342,127.529609780518));
#28866=CARTESIAN_POINT('Ctrl Pts',(165.429116677846,3.57948034607099,127.428673252809));
#28867=CARTESIAN_POINT('Ctrl Pts',(165.421351924899,3.48276615349908,127.331678227462));
#28868=CARTESIAN_POINT('Ctrl Pts',(165.413594884014,3.3861480188262,127.23477953894));
#28869=CARTESIAN_POINT('Ctrl Pts',(165.405837843129,3.285381904443,127.141814837302));
#28870=CARTESIAN_POINT('Ctrl Pts',(165.398080802244,3.1808242518467,127.053155459038));
#28871=CARTESIAN_POINT('Ctrl Pts',(165.390329611004,3.07634544698982,126.964562939502));
#28872=CARTESIAN_POINT('Ctrl Pts',(165.382578419763,2.96808109202777,126.880269532854));
#28873=CARTESIAN_POINT('Ctrl Pts',(165.374827228523,2.85642375969557,126.800609080876));
#28874=CARTESIAN_POINT('Ctrl Pts',(165.367079331746,2.74481388470817,126.720982486716));
#28875=CARTESIAN_POINT('Ctrl Pts',(165.359331434969,2.62981421819218,126.645985157368));
#28876=CARTESIAN_POINT('Ctrl Pts',(165.351583538192,2.51184944818924,126.575909906947));
#28877=CARTESIAN_POINT('Ctrl Pts',(165.343837262108,2.39390935387319,126.505849314759));
#28878=CARTESIAN_POINT('Ctrl Pts',(165.336090986024,2.27300572567125,126.440708953128));
#28879=CARTESIAN_POINT('Ctrl Pts',(165.32834470994,2.14959085641904,126.380737417914));
#28880=CARTESIAN_POINT('Ctrl Pts',(165.320598376674,2.02617507614617,126.320765440004));
#28881=CARTESIAN_POINT('Ctrl Pts',(165.312852043409,1.90024836947892,126.265962535523));
#28882=CARTESIAN_POINT('Ctrl Pts',(165.305105710144,1.77228580311794,126.21653040116));
#28883=CARTESIAN_POINT('Ctrl Pts',(165.297357642141,1.6442945804275,126.167087196813));
#28884=CARTESIAN_POINT('Ctrl Pts',(165.289609574138,1.5142669554514,126.123017296768));
#28885=CARTESIAN_POINT('Ctrl Pts',(165.281861506135,1.38269567471772,126.084473358995));
#28886=CARTESIAN_POINT('Ctrl Pts',(165.274105203393,1.25098455846129,126.045888456267));
#28887=CARTESIAN_POINT('Ctrl Pts',(165.266348900651,1.11772688493576,126.012841357968));
#28888=CARTESIAN_POINT('Ctrl Pts',(165.258592597909,0.983428730526352,125.985434285438));
#28889=CARTESIAN_POINT('Ctrl Pts',(165.250832155395,0.849058897148156,125.958012584928));
#28890=CARTESIAN_POINT('Ctrl Pts',(165.243071712881,0.713647862149207,125.936236970411));
#28891=CARTESIAN_POINT('Ctrl Pts',(165.235311270367,0.577708475606904,125.920157921146));
#28892=CARTESIAN_POINT('Ctrl Pts',(165.227538370101,0.441550867093239,125.904053060364));
#28893=CARTESIAN_POINT('Ctrl Pts',(165.219765469836,0.304863602213619,125.893663068374));
#28894=CARTESIAN_POINT('Ctrl Pts',(165.21199256957,0.168162098785835,125.888986311266));
#28895=CARTESIAN_POINT('Ctrl Pts',(165.204502233809,0.0364300393395799,
125.88447956606));
#28896=CARTESIAN_POINT('Ctrl Pts',(165.197011898047,-0.0953149334006313,
125.885277884535));
#28897=CARTESIAN_POINT('Ctrl Pts',(165.189521562285,-0.226616604130561,
125.891334261313));
#28898=CARTESIAN_POINT('Ctrl Pts',(165.181747228166,-0.362896617615897,
125.897620267459));
#28899=CARTESIAN_POINT('Ctrl Pts',(165.173972894047,-0.499130744036451,
125.909590833477));
#28900=CARTESIAN_POINT('Ctrl Pts',(165.166198559927,-0.634806152942256,
125.927250386016));
#28901=CARTESIAN_POINT('Ctrl Pts',(165.15843380698,-0.770314354031923,125.944888174736));
#28902=CARTESIAN_POINT('Ctrl Pts',(165.150669054033,-0.905264823681669,
125.968200949866));
#28903=CARTESIAN_POINT('Ctrl Pts',(165.142904301086,-1.03914586900888,125.997141158729));
#28904=CARTESIAN_POINT('Ctrl Pts',(165.135147260201,-1.17289394179475,126.026052623769));
#28905=CARTESIAN_POINT('Ctrl Pts',(165.127390219316,-1.3055743243527,126.060580317619));
#28906=CARTESIAN_POINT('Ctrl Pts',(165.119633178431,-1.43668193544038,126.100625072398));
#28907=CARTESIAN_POINT('Ctrl Pts',(165.111881987191,-1.5676906772581,126.140639629115));
#28908=CARTESIAN_POINT('Ctrl Pts',(165.104130795951,-1.69712863594474,126.186162851875));
#28909=CARTESIAN_POINT('Ctrl Pts',(165.096379604711,-1.82450274580134,126.237044907758));
#28910=CARTESIAN_POINT('Ctrl Pts',(165.088631707934,-1.95182271826396,126.287905337409));
#28911=CARTESIAN_POINT('Ctrl Pts',(165.080883811157,-2.0770802242538,126.344119925384));
#28912=CARTESIAN_POINT('Ctrl Pts',(165.07313591438,-2.19979935670297,126.405489642787));
#28913=CARTESIAN_POINT('Ctrl Pts',(165.065389638296,-2.32249281895531,126.466846522969));
#28914=CARTESIAN_POINT('Ctrl Pts',(165.057643362211,-2.44264861434462,126.533356212941));
#28915=CARTESIAN_POINT('Ctrl Pts',(165.049897086127,-2.55981311680882,126.604772558064));
#28916=CARTESIAN_POINT('Ctrl Pts',(165.042150752862,-2.67697848415435,126.676189430366));
#28917=CARTESIAN_POINT('Ctrl Pts',(165.034404419597,-2.79115218067688,126.752512826607));
#28918=CARTESIAN_POINT('Ctrl Pts',(165.026658086331,-2.90190772808446,126.833452081704));
#28919=CARTESIAN_POINT('Ctrl Pts',(165.018910018328,-3.01268807842886,126.914409462585));
#28920=CARTESIAN_POINT('Ctrl Pts',(165.011161950325,-3.12004844086206,126.999984528609));
#28921=CARTESIAN_POINT('Ctrl Pts',(165.003413882322,-3.22359403837451,127.089845233528));
#28922=CARTESIAN_POINT('Ctrl Pts',(164.995657579581,-3.32724968538063,127.179801443473));
#28923=CARTESIAN_POINT('Ctrl Pts',(164.987901276839,-3.42708217266223,127.274052134413));
#28924=CARTESIAN_POINT('Ctrl Pts',(164.980144974097,-3.52273195186391,127.372226783081));
#28925=CARTESIAN_POINT('Ctrl Pts',(164.972384531583,-3.61843278223297,127.470453830515));
#28926=CARTESIAN_POINT('Ctrl Pts',(164.964624089068,-3.70994619545918,127.572608717754));
#28927=CARTESIAN_POINT('Ctrl Pts',(164.956863646554,-3.79695251391848,127.678287254776));
#28928=CARTESIAN_POINT('Ctrl Pts',(164.949090746289,-3.884098502644,127.784135436366));
#28929=CARTESIAN_POINT('Ctrl Pts',(164.941317846023,-3.96672270260528,127.893518259033));
#28930=CARTESIAN_POINT('Ctrl Pts',(164.933544945758,-4.04454789253535,128.006001204001));
#28931=CARTESIAN_POINT('Ctrl Pts',(164.926054609996,-4.11954394078338,128.114395110595));
#28932=CARTESIAN_POINT('Ctrl Pts',(164.918564274234,-4.19008366865925,128.225667398012));
#28933=CARTESIAN_POINT('Ctrl Pts',(164.911073938471,-4.25596002760316,128.339408831842));
#28934=CARTESIAN_POINT('Ctrl Pts',(164.902985512137,-4.32709650177464,128.462232325726));
#28935=CARTESIAN_POINT('Ctrl Pts',(164.894897085803,-4.39300527178131,128.588297777807));
#28936=CARTESIAN_POINT('Ctrl Pts',(164.886808659469,-4.45339117781636,128.717139958448));
#28937=CARTESIAN_POINT('Ctrl Pts',(164.878731658804,-4.51369178302798,128.845800137282));
#28938=CARTESIAN_POINT('Ctrl Pts',(164.87065465814,-4.56848491366523,128.97722892253));
#28939=CARTESIAN_POINT('Ctrl Pts',(164.862577657476,-4.61751995329873,129.110934344182));
#28940=CARTESIAN_POINT('Ctrl Pts',(164.854514161893,-4.66647300430411,129.244416204801));
#28941=CARTESIAN_POINT('Ctrl Pts',(164.84645066631,-4.70968703439096,129.380166791153));
#28942=CARTESIAN_POINT('Ctrl Pts',(164.838387170727,-4.74695864644254,129.51767236027));
#28943=CARTESIAN_POINT('Ctrl Pts',(164.837122661767,-4.75280354173969,129.539235840088));
#28944=CARTESIAN_POINT('Ctrl Pts',(164.835858152806,-4.75850239489081,129.560842435668));
#28945=CARTESIAN_POINT('Ctrl Pts',(164.834593643846,-4.76405452823405,129.582490119308));
#28946=CARTESIAN_POINT('Ctrl Pts',(166.584804846393,-4.76405452823406,129.582490119308));
#28947=CARTESIAN_POINT('Ctrl Pts',(166.583789791378,-4.76848155150402,129.599751015848));
#28948=CARTESIAN_POINT('Ctrl Pts',(166.582774736364,-4.77281387238167,129.617032490968));
#28949=CARTESIAN_POINT('Ctrl Pts',(166.581759681349,-4.77705133042995,129.634333417482));
#28950=CARTESIAN_POINT('Ctrl Pts',(166.571381405794,-4.82037657551116,129.811224108263));
#28951=CARTESIAN_POINT('Ctrl Pts',(166.561003130238,-4.85389270006441,129.99060470522));
#28952=CARTESIAN_POINT('Ctrl Pts',(166.550624854682,-4.87736871096789,130.171543487764));
#28953=CARTESIAN_POINT('Ctrl Pts',(166.540504395719,-4.9002615320052,130.347987398294));
#28954=CARTESIAN_POINT('Ctrl Pts',(166.530383936756,-4.91360693885465,130.525913383609));
#28955=CARTESIAN_POINT('Ctrl Pts',(166.520263477793,-4.91723477504882,130.704434497104));
#28956=CARTESIAN_POINT('Ctrl Pts',(166.51846213054,-4.91788049603701,130.736209589376));
#28957=CARTESIAN_POINT('Ctrl Pts',(166.516660783287,-4.91821847244596,130.768003468096));
#28958=CARTESIAN_POINT('Ctrl Pts',(166.514859436034,-4.91824789572956,130.799811040473));
#28959=CARTESIAN_POINT('',(166.860140564042,-4.91824956784904,130.806422377193));
#28960=CARTESIAN_POINT('Ctrl Pts',(166.930280810341,-4.76405452823404,129.582490119308));
#28961=CARTESIAN_POINT('Ctrl Pts',(166.922599644049,-4.79781228548173,129.714111102471));
#28962=CARTESIAN_POINT('Ctrl Pts',(166.914918477758,-4.82608624198017,129.847034690638));
#28963=CARTESIAN_POINT('Ctrl Pts',(166.907237311466,-4.84880030962948,129.980759609895));
#28964=CARTESIAN_POINT('Ctrl Pts',(166.899387853562,-4.87201203439566,130.117414394414));
#28965=CARTESIAN_POINT('Ctrl Pts',(166.891538395658,-4.88941736099183,130.254905588925));
#28966=CARTESIAN_POINT('Ctrl Pts',(166.883688937754,-4.9009911797719,130.392695075775));
#28967=CARTESIAN_POINT('Ctrl Pts',(166.87583947985,-4.91256499855197,130.530484562626));
#28968=CARTESIAN_POINT('Ctrl Pts',(166.867990021946,-4.91830735559279,130.66857190133));
#28969=CARTESIAN_POINT('Ctrl Pts',(166.860140564042,-4.91824956784904,130.806422377193));
#28970=CARTESIAN_POINT('Ctrl Pts',(166.860140564008,-4.91824956784879,130.806422377793));
#28971=CARTESIAN_POINT('Ctrl Pts',(166.853633145673,-4.91820166019232,130.920704246058));
#28972=CARTESIAN_POINT('Ctrl Pts',(166.847125727338,-4.91417087231532,131.034898519982));
#28973=CARTESIAN_POINT('Ctrl Pts',(166.840618309003,-4.90617335239805,131.148811047555));
#28974=CARTESIAN_POINT('Ctrl Pts',(166.832843974884,-4.89661881190913,131.284900968948));
#28975=CARTESIAN_POINT('Ctrl Pts',(166.825069640765,-4.88138244972333,131.420808602728));
#28976=CARTESIAN_POINT('Ctrl Pts',(166.817295306646,-4.86047214698298,131.556021159901));
#28977=CARTESIAN_POINT('Ctrl Pts',(166.809530553699,-4.83958761432197,131.69106707968));
#28978=CARTESIAN_POINT('Ctrl Pts',(166.801765800752,-4.81304311352321,131.825419244607));
#28979=CARTESIAN_POINT('Ctrl Pts',(166.794001047804,-4.78089846278784,131.958567250285));
#28980=CARTESIAN_POINT('Ctrl Pts',(166.78624400692,-4.7487857385728,132.091583011487));
#28981=CARTESIAN_POINT('Ctrl Pts',(166.778486966035,-4.71108402450377,132.223396615924));
#28982=CARTESIAN_POINT('Ctrl Pts',(166.77072992515,-4.66790458046289,132.35350550756));
#28983=CARTESIAN_POINT('Ctrl Pts',(166.762978733909,-4.62475769837655,132.483516283068));
#28984=CARTESIAN_POINT('Ctrl Pts',(166.755227542669,-4.57614143107031,132.611824534997));
#28985=CARTESIAN_POINT('Ctrl Pts',(166.747476351429,-4.52221740053542,132.737940935214));
#28986=CARTESIAN_POINT('Ctrl Pts',(166.739728454652,-4.46831628915203,132.864003732596));
#28987=CARTESIAN_POINT('Ctrl Pts',(166.731980557875,-4.4091120548184,132.987876172408));
#28988=CARTESIAN_POINT('Ctrl Pts',(166.724232661098,-4.34481508957225,133.109087260777));
#28989=CARTESIAN_POINT('Ctrl Pts',(166.716486385014,-4.28053157386513,133.230272994398));
#28990=CARTESIAN_POINT('Ctrl Pts',(166.70874010893,-4.2111576292577,133.348798138715));
#28991=CARTESIAN_POINT('Ctrl Pts',(166.700993832846,-4.13695022527647,133.464215105331));
#28992=CARTESIAN_POINT('Ctrl Pts',(166.69324749958,-4.06274227351302,133.579632923929));
#28993=CARTESIAN_POINT('Ctrl Pts',(166.685501166315,-3.98370100261904,133.691942190185));
#28994=CARTESIAN_POINT('Ctrl Pts',(166.67775483305,-3.90012722827645,133.800723523784));
#28995=CARTESIAN_POINT('Ctrl Pts',(166.670006765047,-3.81653473816656,133.909529218207));
#28996=CARTESIAN_POINT('Ctrl Pts',(166.662258697044,-3.72840796297389,134.014805097881));
#28997=CARTESIAN_POINT('Ctrl Pts',(166.654510629041,-3.63608832688384,134.116164467675));
#28998=CARTESIAN_POINT('Ctrl Pts',(166.646754326299,-3.54367057238597,134.217631563414));
#28999=CARTESIAN_POINT('Ctrl Pts',(166.638998023557,-3.44705131889053,134.315173544701));
#29000=CARTESIAN_POINT('Ctrl Pts',(166.631241720815,-3.34660961113019,134.408439858259));
#29001=CARTESIAN_POINT('Ctrl Pts',(166.623481278301,-3.24611429460613,134.501755950856));
#29002=CARTESIAN_POINT('Ctrl Pts',(166.615720835787,-3.14179275586374,134.590791574858));
#29003=CARTESIAN_POINT('Ctrl Pts',(166.607960393273,-3.03405673991014,134.675236844146));
#29004=CARTESIAN_POINT('Ctrl Pts',(166.600187493007,-2.92614777653937,134.759817672478));
#29005=CARTESIAN_POINT('Ctrl Pts',(166.592414592742,-2.81481370044383,134.839793192568));
#29006=CARTESIAN_POINT('Ctrl Pts',(166.584641692476,-2.70049555781372,134.914896690237));
#29007=CARTESIAN_POINT('Ctrl Pts',(166.577151356714,-2.59033316761781,134.987269986591));
#29008=CARTESIAN_POINT('Ctrl Pts',(166.569661020952,-2.47740016490256,135.05511917268));
#29009=CARTESIAN_POINT('Ctrl Pts',(166.56217068519,-2.36211063482431,135.118247080067));
#29010=CARTESIAN_POINT('Ctrl Pts',(166.554396351071,-2.2424498671721,135.183768501249));
#29011=CARTESIAN_POINT('Ctrl Pts',(166.546622016952,-2.11987129983826,135.244411114013));
#29012=CARTESIAN_POINT('Ctrl Pts',(166.538847682833,-1.99481061667704,135.299904374009));
#29013=CARTESIAN_POINT('Ctrl Pts',(166.531082929886,-1.86990405963087,135.355329243521));
#29014=CARTESIAN_POINT('Ctrl Pts',(166.523318176939,-1.74252182716003,135.405617230097));
#29015=CARTESIAN_POINT('Ctrl Pts',(166.515553423992,-1.61312567013595,135.450542774439));
#29016=CARTESIAN_POINT('Ctrl Pts',(166.507796383107,-1.48385803119936,135.495423698098));
#29017=CARTESIAN_POINT('Ctrl Pts',(166.500039342222,-1.35258081526154,135.534952651208));
#29018=CARTESIAN_POINT('Ctrl Pts',(166.492282301337,-1.21977697563239,135.568951596046));
#29019=CARTESIAN_POINT('Ctrl Pts',(166.484531110096,-1.08707328441164,135.602924902016));
#29020=CARTESIAN_POINT('Ctrl Pts',(166.476779918856,-0.952845638188494,
135.631376403718));
#29021=CARTESIAN_POINT('Ctrl Pts',(166.469028727616,-0.817593083212366,
135.654177584502));
#29022=CARTESIAN_POINT('Ctrl Pts',(166.461280830839,-0.682398014180036,
135.676969074177));
#29023=CARTESIAN_POINT('Ctrl Pts',(166.453532934062,-0.54617928751503,135.694114954552));
#29024=CARTESIAN_POINT('Ctrl Pts',(166.445785037285,-0.409446885738032,
135.705537650714));
#29025=CARTESIAN_POINT('Ctrl Pts',(166.438038761201,-0.27274308543183,135.716957957495));
#29026=CARTESIAN_POINT('Ctrl Pts',(166.430292485117,-0.135526213098289,
135.722657428765));
#29027=CARTESIAN_POINT('Ctrl Pts',(166.422546209033,0.00168826416244504,
135.722610327805));
#29028=CARTESIAN_POINT('Ctrl Pts',(166.414799875767,0.138903754309233,135.722563226497));
#29029=CARTESIAN_POINT('Ctrl Pts',(166.407053542502,0.276116458382751,135.716769468446));
#29030=CARTESIAN_POINT('Ctrl Pts',(166.399307209237,0.412810941621637,135.705255453101));
#29031=CARTESIAN_POINT('Ctrl Pts',(166.391559141234,0.549536036642225,135.693738859273));
#29032=CARTESIAN_POINT('Ctrl Pts',(166.383811073231,0.685742290387179,135.676499491893));
#29033=CARTESIAN_POINT('Ctrl Pts',(166.376063005228,0.82091981718061,135.653615582636));
#29034=CARTESIAN_POINT('Ctrl Pts',(166.368306702486,0.956241012258197,135.630707352089));
#29035=CARTESIAN_POINT('Ctrl Pts',(166.360550399744,1.09053091021809,135.602142661205));
#29036=CARTESIAN_POINT('Ctrl Pts',(166.352794097002,1.22328969772295,135.568050928443));
#29037=CARTESIAN_POINT('Ctrl Pts',(166.345033654488,1.35611934259005,135.533940999897));
#29038=CARTESIAN_POINT('Ctrl Pts',(166.337273211974,1.48741587456849,135.494298264403));
#29039=CARTESIAN_POINT('Ctrl Pts',(166.32951276946,1.61669601945638,135.44930163368));
#29040=CARTESIAN_POINT('Ctrl Pts',(166.321739869194,1.7461836963098,135.40423277037));
#29041=CARTESIAN_POINT('Ctrl Pts',(166.313966968929,1.8736481540021,135.353792981125));
#29042=CARTESIAN_POINT('Ctrl Pts',(166.306194068663,1.99862660209961,135.298209165067));
#29043=CARTESIAN_POINT('Ctrl Pts',(166.298703732901,2.11906176880764,135.24464596073));
#29044=CARTESIAN_POINT('Ctrl Pts',(166.291213397139,2.23718825716293,135.186306369506));
#29045=CARTESIAN_POINT('Ctrl Pts',(166.283723061377,2.35261636063335,135.12343219861));
#29046=CARTESIAN_POINT('Ctrl Pts',(166.275948727258,2.47242095572996,135.058174134414));
#29047=CARTESIAN_POINT('Ctrl Pts',(166.268174393139,2.58969801312797,134.987824127587));
#29048=CARTESIAN_POINT('Ctrl Pts',(166.26040005902,2.70398441843893,134.912602495467));
#29049=CARTESIAN_POINT('Ctrl Pts',(166.252635306073,2.81812997596933,134.837473567286));
#29050=CARTESIAN_POINT('Ctrl Pts',(166.244870553126,2.92929189143952,134.757485172552));
#29051=CARTESIAN_POINT('Ctrl Pts',(166.237105800178,3.03703080780086,134.672903875043));
#29052=CARTESIAN_POINT('Ctrl Pts',(166.229348759293,3.14466271635165,134.58840658487));
#29053=CARTESIAN_POINT('Ctrl Pts',(166.221591718408,3.24887808596006,134.499325709842));
#29054=CARTESIAN_POINT('Ctrl Pts',(166.213834677523,3.34926608038664,134.405971338517));
#29055=CARTESIAN_POINT('Ctrl Pts',(166.206083486283,3.44957837144565,134.31268736645));
#29056=CARTESIAN_POINT('Ctrl Pts',(166.198332295043,3.5460687470917,134.215136577794));
#29057=CARTESIAN_POINT('Ctrl Pts',(166.190581103803,3.63835933594067,134.113669367905));
#29058=CARTESIAN_POINT('Ctrl Pts',(166.182833207026,3.73061069882754,134.012245284287));
#29059=CARTESIAN_POINT('Ctrl Pts',(166.175085310249,3.81866556267354,133.906908378783));
#29060=CARTESIAN_POINT('Ctrl Pts',(166.167337413472,3.9021830034975,133.798045782996));
#29061=CARTESIAN_POINT('Ctrl Pts',(166.159591137388,3.98568297427323,133.689205958917));
#29062=CARTESIAN_POINT('Ctrl Pts',(166.151844861304,4.06464717207518,133.576842221478));
#29063=CARTESIAN_POINT('Ctrl Pts',(166.144098585219,4.13877532131262,133.461374336423));
#29064=CARTESIAN_POINT('Ctrl Pts',(166.136352251954,4.21290401774719,133.34590559901));
#29065=CARTESIAN_POINT('Ctrl Pts',(166.128605918689,4.28219638316992,133.227332997261));
#29066=CARTESIAN_POINT('Ctrl Pts',(166.120859585423,4.34639602310532,133.106104450584));
#29067=CARTESIAN_POINT('Ctrl Pts',(166.11311151742,4.41061004010498,132.984848755614));
#29068=CARTESIAN_POINT('Ctrl Pts',(166.105363449417,4.46972887925609,132.860936277613));
#29069=CARTESIAN_POINT('Ctrl Pts',(166.097615381414,4.52354275341914,132.734838283971));
#29070=CARTESIAN_POINT('Ctrl Pts',(166.089859078673,4.57741382160803,132.608606271881));
#29071=CARTESIAN_POINT('Ctrl Pts',(166.082102775931,4.62596850823346,132.480184464286));
#29072=CARTESIAN_POINT('Ctrl Pts',(166.074346473189,4.6690455353932,132.350063322139));
#29073=CARTESIAN_POINT('Ctrl Pts',(166.066586030675,4.71214555405938,132.219872730421));
#29074=CARTESIAN_POINT('Ctrl Pts',(166.058825588161,4.74976198057786,132.087981372694));
#29075=CARTESIAN_POINT('Ctrl Pts',(166.051065145646,4.78178411693426,131.954892547386));
#29076=CARTESIAN_POINT('Ctrl Pts',(166.043292245381,4.81385765806671,131.82159007608));
#29077=CARTESIAN_POINT('Ctrl Pts',(166.035519345116,4.84031888772147,131.687086679696));
#29078=CARTESIAN_POINT('Ctrl Pts',(166.02774644485,4.86110855302137,131.551894361448));
#29079=CARTESIAN_POINT('Ctrl Pts',(166.020256109088,4.88114246162151,131.421616624498));
#29080=CARTESIAN_POINT('Ctrl Pts',(166.012765773326,4.89590996361786,131.29069949025));
#29081=CARTESIAN_POINT('Ctrl Pts',(166.005275437564,4.90540385236735,131.159601532551));
#29082=CARTESIAN_POINT('Ctrl Pts',(165.997501103445,4.91525770479442,131.023532955939));
#29083=CARTESIAN_POINT('Ctrl Pts',(165.989726769326,4.91946136581058,130.886838549007));
#29084=CARTESIAN_POINT('Ctrl Pts',(165.981952435207,4.91794986999179,130.750027029909));
#29085=CARTESIAN_POINT('Ctrl Pts',(165.97418768226,4.91644023695651,130.61338411878));
#29086=CARTESIAN_POINT('Ctrl Pts',(165.966422929313,4.90922946567046,130.476624769847));
#29087=CARTESIAN_POINT('Ctrl Pts',(165.958658176366,4.89630434057168,130.340262710871));
#29088=CARTESIAN_POINT('Ctrl Pts',(165.950901135481,4.88339205288936,130.204036088614));
#29089=CARTESIAN_POINT('Ctrl Pts',(165.943144094596,4.86477674270188,130.068206357755));
#29090=CARTESIAN_POINT('Ctrl Pts',(165.935387053711,4.84049722927385,129.9332867769));
#29091=CARTESIAN_POINT('Ctrl Pts',(165.92763586247,4.81623602521575,129.79846893995));
#29092=CARTESIAN_POINT('Ctrl Pts',(165.91988467123,4.78631918888288,129.664560270091));
#29093=CARTESIAN_POINT('Ctrl Pts',(165.91213347999,4.75083726909839,129.532068078468));
#29094=CARTESIAN_POINT('Ctrl Pts',(165.904385583213,4.71537043007632,129.39963219956));
#29095=CARTESIAN_POINT('Ctrl Pts',(165.896637686436,4.67434331294802,129.268611978341));
#29096=CARTESIAN_POINT('Ctrl Pts',(165.888889789659,4.62789734475546,129.139503497899));
#29097=CARTESIAN_POINT('Ctrl Pts',(165.881143513575,4.58146109205817,129.010422024168));
#29098=CARTESIAN_POINT('Ctrl Pts',(165.873397237491,4.52960837516405,128.883251863452));
#29099=CARTESIAN_POINT('Ctrl Pts',(165.865650961407,4.47253004859038,128.758472539748));
#29100=CARTESIAN_POINT('Ctrl Pts',(165.857904628141,4.4154513006775,128.633692294952));
#29101=CARTESIAN_POINT('Ctrl Pts',(165.850158294876,4.3531470287462,128.511303277918));
#29102=CARTESIAN_POINT('Ctrl Pts',(165.84241196161,4.28585549260425,128.391763311961));
#29103=CARTESIAN_POINT('Ctrl Pts',(165.834663893607,4.21854888698936,128.272196575857));
#29104=CARTESIAN_POINT('Ctrl Pts',(165.826915825604,4.14625298648257,128.155480501057));
#29105=CARTESIAN_POINT('Ctrl Pts',(165.819167757602,4.06925088661325,128.042046318957));
#29106=CARTESIAN_POINT('Ctrl Pts',(165.81141145486,3.99216694799579,127.928491577659));
#29107=CARTESIAN_POINT('Ctrl Pts',(165.803655152118,3.91036703830625,127.818226020779));
#29108=CARTESIAN_POINT('Ctrl Pts',(165.795898849376,3.82417662159077,127.711650442108));
#29109=CARTESIAN_POINT('Ctrl Pts',(165.788138406862,3.73794020245469,127.605017980843));
#29110=CARTESIAN_POINT('Ctrl Pts',(165.780377964348,3.64730886520722,127.502079715383));
#29111=CARTESIAN_POINT('Ctrl Pts',(165.772617521833,3.55264621408882,127.403200824198));
#29112=CARTESIAN_POINT('Ctrl Pts',(165.764844621568,3.45783160207912,127.304163203839));
#29113=CARTESIAN_POINT('Ctrl Pts',(165.757071721303,3.35897302634649,127.209198250736));
#29114=CARTESIAN_POINT('Ctrl Pts',(165.749298821037,3.25646922206972,127.118632566256));
#29115=CARTESIAN_POINT('Ctrl Pts',(165.741808485275,3.1576916892695,127.031359172528));
#29116=CARTESIAN_POINT('Ctrl Pts',(165.734318149513,3.05552959200497,126.948170945971));
#29117=CARTESIAN_POINT('Ctrl Pts',(165.726827813751,2.95036484607499,126.869321820102));
#29118=CARTESIAN_POINT('Ctrl Pts',(165.719053479632,2.84121274683937,126.787483105661));
#29119=CARTESIAN_POINT('Ctrl Pts',(165.711279145513,2.72848005235996,126.710059780701));
#29120=CARTESIAN_POINT('Ctrl Pts',(165.703504811394,2.61255964622808,126.637381477061));
#29121=CARTESIAN_POINT('Ctrl Pts',(165.695740058446,2.49678210163666,126.564792742935));
#29122=CARTESIAN_POINT('Ctrl Pts',(165.687975305499,2.37782499014026,126.496937600407));
#29123=CARTESIAN_POINT('Ctrl Pts',(165.680210552552,2.25611338211947,126.434104850506));
#29124=CARTESIAN_POINT('Ctrl Pts',(165.672453511667,2.13452265978367,126.371334506978));
#29125=CARTESIAN_POINT('Ctrl Pts',(165.664696470782,2.01018323045405,126.313576807297));
#29126=CARTESIAN_POINT('Ctrl Pts',(165.656939429897,1.88354789589149,126.26107652053));
#29127=CARTESIAN_POINT('Ctrl Pts',(165.649188238657,1.75700805801999,126.208615824637));
#29128=CARTESIAN_POINT('Ctrl Pts',(165.641437047417,1.62817612077944,126.161404799373));
#29129=CARTESIAN_POINT('Ctrl Pts',(165.633685856177,1.49752784325534,126.119641477513));
#29130=CARTESIAN_POINT('Ctrl Pts',(165.6259379594,1.36693509473416,126.07789590618));
#29131=CARTESIAN_POINT('Ctrl Pts',(165.618190062623,1.23452791298634,126.041593551853));
#29132=CARTESIAN_POINT('Ctrl Pts',(165.610442165846,1.1008001115345,126.010883572983));
#29133=CARTESIAN_POINT('Ctrl Pts',(165.602695889762,0.967100283055891,125.980180017978));
#29134=CARTESIAN_POINT('Ctrl Pts',(165.594949613677,0.832080765145308,125.955066599076));
#29135=CARTESIAN_POINT('Ctrl Pts',(165.587203337593,0.696248156450435,125.935641939398));
#29136=CARTESIAN_POINT('Ctrl Pts',(165.579457004328,0.5604145450701,125.916217136332));
#29137=CARTESIAN_POINT('Ctrl Pts',(165.571710671063,0.42376821795664,125.902481231632));
#29138=CARTESIAN_POINT('Ctrl Pts',(165.563964337797,0.286823140077404,125.894481235258));
#29139=CARTESIAN_POINT('Ctrl Pts',(165.556216269794,0.149847394297581,125.88647944734));
#29140=CARTESIAN_POINT('Ctrl Pts',(165.548468201791,0.0125731548475351,
125.884216146584));
#29141=CARTESIAN_POINT('Ctrl Pts',(165.540720133788,-0.124483751035951,
125.887686247809));
#29142=CARTESIAN_POINT('Ctrl Pts',(165.532963831046,-0.261686322630102,
125.891160037098));
#29143=CARTESIAN_POINT('Ctrl Pts',(165.525207528305,-0.39867070777771,125.900379390934));
#29144=CARTESIAN_POINT('Ctrl Pts',(165.517451225563,-0.534923786042843,
125.915287126031));
#29145=CARTESIAN_POINT('Ctrl Pts',(165.509690783049,-0.671249586678486,
125.930202817836));
#29146=CARTESIAN_POINT('Ctrl Pts',(165.501930340534,-0.806842916348517,
125.950812881788));
#29147=CARTESIAN_POINT('Ctrl Pts',(165.49416989802,-0.941200003091565,125.977008795223));
#29148=CARTESIAN_POINT('Ctrl Pts',(165.486396997755,-1.07577277175787,126.003246760663));
#29149=CARTESIAN_POINT('Ctrl Pts',(165.478624097489,-1.20910495128956,126.035088403447));
#29150=CARTESIAN_POINT('Ctrl Pts',(165.470851197224,-1.34070623660191,126.072374792393));
#29151=CARTESIAN_POINT('Ctrl Pts',(165.463360861462,-1.46752348370828,126.108305727182));
#29152=CARTESIAN_POINT('Ctrl Pts',(165.4558705257,-1.59273320374189,126.149292324551));
#29153=CARTESIAN_POINT('Ctrl Pts',(165.448380189938,-1.71591532042347,126.195150525193));
#29154=CARTESIAN_POINT('Ctrl Pts',(165.440605662801,-1.84377109877684,126.242748635169));
#29155=CARTESIAN_POINT('Ctrl Pts',(165.432831135663,-1.96984739568884,126.295746095503));
#29156=CARTESIAN_POINT('Ctrl Pts',(165.425056608526,-2.09365448306572,126.353990524187));
#29157=CARTESIAN_POINT('Ctrl Pts',(165.417291707369,-2.21730827949702,126.412162837908));
#29158=CARTESIAN_POINT('Ctrl Pts',(165.409526806212,-2.33869810637646,126.475569028751));
#29159=CARTESIAN_POINT('Ctrl Pts',(165.401761905056,-2.45735119984756,126.544007563756));
#29160=CARTESIAN_POINT('Ctrl Pts',(165.39400476058,-2.57588576582875,126.612377732674));
#29161=CARTESIAN_POINT('Ctrl Pts',(165.386247616105,-2.69168870250206,126.685770047397));
#29162=CARTESIAN_POINT('Ctrl Pts',(165.37849047163,-2.80430931143856,126.763935844318));
#29163=CARTESIAN_POINT('Ctrl Pts',(165.370739221275,-2.91684434772171,126.842042248427));
#29164=CARTESIAN_POINT('Ctrl Pts',(165.36298797092,-3.02620154948531,126.924914693036));
#29165=CARTESIAN_POINT('Ctrl Pts',(165.355236720565,-3.13195713878541,127.012259940723));
#29166=CARTESIAN_POINT('Ctrl Pts',(165.347488990716,-3.23766469542691,127.099565517463));
#29167=CARTESIAN_POINT('Ctrl Pts',(165.339741260867,-3.3397735935151,127.191339606851));
#29168=CARTESIAN_POINT('Ctrl Pts',(165.331993531018,-3.43789145070786,127.287247392825));
#29169=CARTESIAN_POINT('Ctrl Pts',(165.324247485209,-3.53598798108525,127.383134332363));
#29170=CARTESIAN_POINT('Ctrl Pts',(165.3165014394,-3.63009491707408,127.483152907841));
#29171=CARTESIAN_POINT('Ctrl Pts',(165.30875539359,-3.71985548819165,127.586930243887));
#29172=CARTESIAN_POINT('Ctrl Pts',(165.301009353988,-3.80961598738343,127.690707496776));
#29173=CARTESIAN_POINT('Ctrl Pts',(165.293263314386,-3.8950298731532,127.798243208386));
#29174=CARTESIAN_POINT('Ctrl Pts',(165.285517274784,-3.97577981994194,127.909130421909));
#29175=CARTESIAN_POINT('Ctrl Pts',(165.277769563929,-4.05654718900209,128.020041559995));
#29176=CARTESIAN_POINT('Ctrl Pts',(165.270021853074,-4.13264838712059,128.134305322645));
#29177=CARTESIAN_POINT('Ctrl Pts',(165.262274142218,-4.20380891123564,128.251485042785));
#29178=CARTESIAN_POINT('Ctrl Pts',(165.254519060828,-4.27503713162572,128.36877623808));
#29179=CARTESIAN_POINT('Ctrl Pts',(165.246763979437,-4.34131508909183,128.488988595856));
#29180=CARTESIAN_POINT('Ctrl Pts',(165.239008898046,-4.40241364061653,128.611659726105));
#29181=CARTESIAN_POINT('Ctrl Pts',(165.23124970306,-4.46354460118404,128.734395925882));
#29182=CARTESIAN_POINT('Ctrl Pts',(165.223490508073,-4.51949052232472,128.859593140357));
#29183=CARTESIAN_POINT('Ctrl Pts',(165.215731313086,-4.5700704781865,128.986769110404));
#29184=CARTESIAN_POINT('Ctrl Pts',(165.207961665366,-4.62071857240156,129.114116404467));
#29185=CARTESIAN_POINT('Ctrl Pts',(165.200192017647,-4.66598613558932,129.243447409415));
#29186=CARTESIAN_POINT('Ctrl Pts',(165.192422369927,-4.70574199340715,129.37426434319));
#29187=CARTESIAN_POINT('Ctrl Pts',(165.188323054731,-4.7267174350182,129.443284183454));
#29188=CARTESIAN_POINT('Ctrl Pts',(165.184223739535,-4.74615944644796,129.51271746702));
#29189=CARTESIAN_POINT('Ctrl Pts',(165.180124424339,-4.76405452823406,129.582490119308));
#29190=CARTESIAN_POINT('Origin',(213.235140564004,0.,130.804360617566));
#29191=CARTESIAN_POINT('',(163.084942816425,-4.76405452823405,129.582490119308));
#29192=CARTESIAN_POINT('',(163.429862020825,-4.76405452823405,129.582490119308));
#29193=CARTESIAN_POINT('',(213.235140564004,-4.76405452823405,129.582490119308));
#29194=CARTESIAN_POINT('',(164.764859435961,-4.91824995258213,130.80504357138));
#29195=CARTESIAN_POINT('Ctrl Pts',(164.764859435961,-4.91824995258213,130.80504357138));
#29196=CARTESIAN_POINT('Ctrl Pts',(164.756654934105,-4.91822972407168,130.95071794709));
#29197=CARTESIAN_POINT('Ctrl Pts',(164.748450432249,-4.91173310152479,131.096239299343));
#29198=CARTESIAN_POINT('Ctrl Pts',(164.740245930392,-4.89882630855481,131.241034249826));
#29199=CARTESIAN_POINT('Ctrl Pts',(164.732027256984,-4.88589722181341,131.386079303146));
#29200=CARTESIAN_POINT('Ctrl Pts',(164.723808583575,-4.86653588615109,131.530395135098));
#29201=CARTESIAN_POINT('Ctrl Pts',(164.715589910167,-4.84085980131171,131.673417259301));
#29202=CARTESIAN_POINT('Ctrl Pts',(164.707348638168,-4.81511311586655,131.816832646289));
#29203=CARTESIAN_POINT('Ctrl Pts',(164.69910736617,-4.78301701189617,131.958946898958));
#29204=CARTESIAN_POINT('Ctrl Pts',(164.690866094171,-4.74473971050206,132.099207381506));
#29205=CARTESIAN_POINT('Ctrl Pts',(164.6826124805,-4.70640508714233,132.23967791038));
#29206=CARTESIAN_POINT('Ctrl Pts',(164.674358866829,-4.66187088218157,132.37828882621));
#29207=CARTESIAN_POINT('Ctrl Pts',(164.666105253158,-4.61135402128945,132.514505977715));
#29208=CARTESIAN_POINT('Ctrl Pts',(164.65783226147,-4.56071855579518,132.651042942857));
#29209=CARTESIAN_POINT('Ctrl Pts',(164.649559269783,-4.50407247160253,132.785174614601));
#29210=CARTESIAN_POINT('Ctrl Pts',(164.641286278095,-4.44168007449386,132.916388358469));
#29211=CARTESIAN_POINT('Ctrl Pts',(164.638399623616,-4.41990980088975,132.962172127598));
#29212=CARTESIAN_POINT('Ctrl Pts',(164.635512969137,-4.39744031709227,133.007600886824));
#29213=CARTESIAN_POINT('Ctrl Pts',(164.632626314659,-4.37428410091448,133.052653673862));
#29214=CARTESIAN_POINT('Ctrl Pts',(164.62485198054,-4.31191980937317,133.173989781799));
#29215=CARTESIAN_POINT('Ctrl Pts',(164.61707764642,-4.24440438761954,133.29292127249));
#29216=CARTESIAN_POINT('Ctrl Pts',(164.609303312301,-4.17194697607602,133.408979877901));
#29217=CARTESIAN_POINT('Ctrl Pts',(164.601538559354,-4.09957886181654,133.524895451454));
#29218=CARTESIAN_POINT('Ctrl Pts',(164.593773806407,-4.0222810812284,133.637944855961));
#29219=CARTESIAN_POINT('Ctrl Pts',(164.58600905346,-3.94030957796668,133.7476824641));
#29220=CARTESIAN_POINT('Ctrl Pts',(164.578252012575,-3.85841948995763,133.8573110793));
#29221=CARTESIAN_POINT('Ctrl Pts',(164.57049497169,-3.77186514953762,133.963634132834));
#29222=CARTESIAN_POINT('Ctrl Pts',(164.562737930805,-3.68094669703134,134.066233465504));
#29223=CARTESIAN_POINT('Ctrl Pts',(164.554986739565,-3.5900968068374,134.168755427219));
#29224=CARTESIAN_POINT('Ctrl Pts',(164.547235548325,-3.49488961336082,134.267558965971));
#29225=CARTESIAN_POINT('Ctrl Pts',(164.539484357085,-3.39566634318057,134.362257910672));
#29226=CARTESIAN_POINT('Ctrl Pts',(164.531736460308,-3.2964852455369,134.456916605795));
#29227=CARTESIAN_POINT('Ctrl Pts',(164.523988563531,-3.19329174839745,134.547473907302));
#29228=CARTESIAN_POINT('Ctrl Pts',(164.516240666754,-3.08646469064485,134.633579699298));
#29229=CARTESIAN_POINT('Ctrl Pts',(164.508494390669,-2.97965997880984,134.719667479819));
#29230=CARTESIAN_POINT('Ctrl Pts',(164.500748114585,-2.86922352237007,134.80130535776));
#29231=CARTESIAN_POINT('Ctrl Pts',(164.493001838501,-2.75556776040104,134.878183070783));
#29232=CARTESIAN_POINT('Ctrl Pts',(164.485255505236,-2.64191115945102,134.9550613513));
#29233=CARTESIAN_POINT('Ctrl Pts',(164.477509171971,-2.52503552939137,135.027179177735));
#29234=CARTESIAN_POINT('Ctrl Pts',(164.469762838705,-2.40538250788096,135.094269480617));
#29235=CARTESIAN_POINT('Ctrl Pts',(164.462014770702,-2.28570269090592,135.161374807906));
#29236=CARTESIAN_POINT('Ctrl Pts',(164.454266702699,-2.16324458576815,135.2234501801));
#29237=CARTESIAN_POINT('Ctrl Pts',(164.446518634696,-2.03847428983192,135.280274561354));
#29238=CARTESIAN_POINT('Ctrl Pts',(164.438762331954,-1.91357138654042,135.337159336236));
#29239=CARTESIAN_POINT('Ctrl Pts',(164.431006029213,-1.78635173985156,135.388781809596));
#29240=CARTESIAN_POINT('Ctrl Pts',(164.423249726471,-1.65730179925442,135.434968980264));
#29241=CARTESIAN_POINT('Ctrl Pts',(164.415489283957,-1.52818298081836,135.481180802416));
#29242=CARTESIAN_POINT('Ctrl Pts',(164.407728841442,-1.39723229506051,135.521951425254));
#29243=CARTESIAN_POINT('Ctrl Pts',(164.399968398928,-1.26495023902372,135.557158104867));
#29244=CARTESIAN_POINT('Ctrl Pts',(164.392195498663,-1.13245583208708,135.592421301368));
#29245=CARTESIAN_POINT('Ctrl Pts',(164.384422598397,-0.998626165907619,
135.622102621489));
#29246=CARTESIAN_POINT('Ctrl Pts',(164.376649698132,-0.863971674351278,
135.64613054275));
#29247=CARTESIAN_POINT('Ctrl Pts',(164.36915936237,-0.734212212737345,135.669284988551));
#29248=CARTESIAN_POINT('Ctrl Pts',(164.361669026608,-0.603687158718285,
135.687189888116));
#29249=CARTESIAN_POINT('Ctrl Pts',(164.354178690846,-0.472854781144197,
135.699827032367));
#29250=CARTESIAN_POINT('Ctrl Pts',(164.346404356727,-0.337061854208649,
135.712943317785));
#29251=CARTESIAN_POINT('Ctrl Pts',(164.338630022608,-0.200507688162279,
135.720426057109));
#29252=CARTESIAN_POINT('Ctrl Pts',(164.330855688489,-0.0636992956689109,
135.722198095791));
#29253=CARTESIAN_POINT('Ctrl Pts',(164.323090935542,0.0729404927076261,
135.723967950593));
#29254=CARTESIAN_POINT('Ctrl Pts',(164.315326182595,0.209833496955411,135.720041103119));
#29255=CARTESIAN_POINT('Ctrl Pts',(164.307561429647,0.3464664543917,135.71039201356));
#29256=CARTESIAN_POINT('Ctrl Pts',(164.299804388762,0.482963706048382,135.700752507614));
#29257=CARTESIAN_POINT('Ctrl Pts',(164.292047347877,0.619201037416439,135.685402097192));
#29258=CARTESIAN_POINT('Ctrl Pts',(164.284290306992,0.754664406141891,135.66436727359));
#29259=CARTESIAN_POINT('Ctrl Pts',(164.276539115752,0.890025620887144,135.643348312513));
#29260=CARTESIAN_POINT('Ctrl Pts',(164.268787924512,1.02461364994013,135.616653530339));
#29261=CARTESIAN_POINT('Ctrl Pts',(164.261036733272,1.15791915532598,135.584361275749));
#29262=CARTESIAN_POINT('Ctrl Pts',(164.253288836495,1.29116800231614,135.552082746228));
#29263=CARTESIAN_POINT('Ctrl Pts',(164.245540939718,1.4231350306351,135.514211567943));
#29264=CARTESIAN_POINT('Ctrl Pts',(164.237793042941,1.55332090619529,135.470877222581));
#29265=CARTESIAN_POINT('Ctrl Pts',(164.230046766857,1.68347954967679,135.427551941829));
#29266=CARTESIAN_POINT('Ctrl Pts',(164.222300490773,1.81185741075988,135.378765890447));
#29267=CARTESIAN_POINT('Ctrl Pts',(164.214554214689,1.9379705235568,135.324698360736));
#29268=CARTESIAN_POINT('Ctrl Pts',(164.206807881423,2.06408456729207,135.27063043191));
#29269=CARTESIAN_POINT('Ctrl Pts',(164.199061548158,2.18793347004784,135.211281101015));
#29270=CARTESIAN_POINT('Ctrl Pts',(164.191315214892,2.30905382277212,135.146877572748));
#29271=CARTESIAN_POINT('Ctrl Pts',(164.183567146889,2.43020129955965,135.082459621757));
#29272=CARTESIAN_POINT('Ctrl Pts',(164.175819078886,2.54861866528459,135.012985404657));
#29273=CARTESIAN_POINT('Ctrl Pts',(164.168071010884,2.66386801922089,134.938727587088));
#29274=CARTESIAN_POINT('Ctrl Pts',(164.160314708142,2.77923986154201,134.864390847426));
#29275=CARTESIAN_POINT('Ctrl Pts',(164.1525584054,2.89143663695182,134.785260563419));
#29276=CARTESIAN_POINT('Ctrl Pts',(164.144802102658,3.00004985683638,134.701652487441));
#29277=CARTESIAN_POINT('Ctrl Pts',(164.137041660144,3.10872104686674,134.617999787316));
#29278=CARTESIAN_POINT('Ctrl Pts',(164.12928121763,3.21380457084478,134.529864784193));
#29279=CARTESIAN_POINT('Ctrl Pts',(164.121520775115,3.31492662996522,134.437602214329));
#29280=CARTESIAN_POINT('Ctrl Pts',(164.11374787485,3.41621101919216,134.345191536397));
#29281=CARTESIAN_POINT('Ctrl Pts',(164.105974974585,3.51352095796986,134.248640326519));
#29282=CARTESIAN_POINT('Ctrl Pts',(164.098202074319,3.60652037043833,134.148339367515));
#29283=CARTESIAN_POINT('Ctrl Pts',(164.090711738557,3.69613902001243,134.051684601015));
#29284=CARTESIAN_POINT('Ctrl Pts',(164.083221402795,3.78175489905831,133.951548211972));
#29285=CARTESIAN_POINT('Ctrl Pts',(164.075731067033,3.86310498225758,133.848305912501));
#29286=CARTESIAN_POINT('Ctrl Pts',(164.067956732914,3.9475394785869,133.741149149866));
#29287=CARTESIAN_POINT('Ctrl Pts',(164.060182398795,4.02764578137131,133.630306865937));
#29288=CARTESIAN_POINT('Ctrl Pts',(164.052408064676,4.10308492557468,133.516163920909));
#29289=CARTESIAN_POINT('Ctrl Pts',(164.044643311729,4.17843109777495,133.40216164686));
#29290=CARTESIAN_POINT('Ctrl Pts',(164.036878558782,4.24912134237368,133.284867128396));
#29291=CARTESIAN_POINT('Ctrl Pts',(164.029113805834,4.31485674099162,133.16469838306));
#29292=CARTESIAN_POINT('Ctrl Pts',(164.021356764949,4.38052685028495,133.044648991016));
#29293=CARTESIAN_POINT('Ctrl Pts',(164.013599724064,4.44125172063751,132.921731393907));
#29294=CARTESIAN_POINT('Ctrl Pts',(164.005842683179,4.49677578747697,132.796392389316));
#29295=CARTESIAN_POINT('Ctrl Pts',(163.998091491939,4.5522579831857,132.671147903843));
#29296=CARTESIAN_POINT('Ctrl Pts',(163.990340300699,4.60254702410623,132.543486001448));
#29297=CARTESIAN_POINT('Ctrl Pts',(163.982589109459,4.64743351758415,132.413877551971));
#29298=CARTESIAN_POINT('Ctrl Pts',(163.974841212682,4.69230093310496,132.284324189542));
#29299=CARTESIAN_POINT('Ctrl Pts',(163.967093315905,4.73177024052611,132.152826294198));
#29300=CARTESIAN_POINT('Ctrl Pts',(163.959345419128,4.76568047418773,132.019873957865));
#29301=CARTESIAN_POINT('Ctrl Pts',(163.951599143044,4.79958361455951,131.886949432295));
#29302=CARTESIAN_POINT('Ctrl Pts',(163.94385286696,4.82792989755778,131.752571449478));
#29303=CARTESIAN_POINT('Ctrl Pts',(163.936106590876,4.85060857149034,131.617244095492));
#29304=CARTESIAN_POINT('Ctrl Pts',(163.92836025761,4.8732874128317,131.481915742549));
#29305=CARTESIAN_POINT('Ctrl Pts',(163.920613924345,4.8902984970063,131.345638390041));
#29306=CARTESIAN_POINT('Ctrl Pts',(163.91286759108,4.90158249384904,131.208924726815));
#29307=CARTESIAN_POINT('Ctrl Pts',(163.905119523077,4.91286901766464,131.072180447513));
#29308=CARTESIAN_POINT('Ctrl Pts',(163.897371455074,4.91842586988551,130.93500005263));
#29309=CARTESIAN_POINT('Ctrl Pts',(163.889623387071,4.91824575579846,130.797899342888));
#29310=CARTESIAN_POINT('Ctrl Pts',(163.881867084329,4.918065450284,130.66065292088));
#29311=CARTESIAN_POINT('Ctrl Pts',(163.874110781587,4.91213599893044,130.523486744779));
#29312=CARTESIAN_POINT('Ctrl Pts',(163.866354478845,4.90050225507937,130.386915159497));
#29313=CARTESIAN_POINT('Ctrl Pts',(163.858594036331,4.88886230194891,130.250270681848));
#29314=CARTESIAN_POINT('Ctrl Pts',(163.850833593817,4.87151203922687,130.114221815001));
#29315=CARTESIAN_POINT('Ctrl Pts',(163.843073151303,4.84854786918652,129.979274790087));
#29316=CARTESIAN_POINT('Ctrl Pts',(163.835300251037,4.82554683502176,129.844111136229));
#29317=CARTESIAN_POINT('Ctrl Pts',(163.827527350772,4.79691396651585,129.710053241441));
#29318=CARTESIAN_POINT('Ctrl Pts',(163.819754450506,4.76279638311187,129.577595083523));
#29319=CARTESIAN_POINT('Ctrl Pts',(163.812264114744,4.72991905980141,129.449952113286));
#29320=CARTESIAN_POINT('Ctrl Pts',(163.804773778982,4.69194895359856,129.323794885232));
#29321=CARTESIAN_POINT('Ctrl Pts',(163.79728344322,4.64905999013475,129.199547771584));
#29322=CARTESIAN_POINT('Ctrl Pts',(163.789509109101,4.60454487858566,129.070589790859));
#29323=CARTESIAN_POINT('Ctrl Pts',(163.781734774982,4.55458953925968,128.943281127661));
#29324=CARTESIAN_POINT('Ctrl Pts',(163.773960440863,4.49933454705722,128.818114989211));
#29325=CARTESIAN_POINT('Ctrl Pts',(163.766195687916,4.44414765169439,128.693103106841));
#29326=CARTESIAN_POINT('Ctrl Pts',(163.758430934969,4.38367425526831,128.570228849701));
#29327=CARTESIAN_POINT('Ctrl Pts',(163.750666182021,4.31810447509082,128.449969654981));
#29328=CARTESIAN_POINT('Ctrl Pts',(163.742909141136,4.25259981974337,128.329829903389));
#29329=CARTESIAN_POINT('Ctrl Pts',(163.735152100251,4.18200903980121,128.212300386477));
#29330=CARTESIAN_POINT('Ctrl Pts',(163.727395059366,4.10656989983062,128.097837622965));
#29331=CARTESIAN_POINT('Ctrl Pts',(163.719643868126,4.03118764910229,127.983461176713));
#29332=CARTESIAN_POINT('Ctrl Pts',(163.711892676886,3.95096453004045,127.872147205767));
#29333=CARTESIAN_POINT('Ctrl Pts',(163.704141485646,3.86618351693116,127.764326394747));
#29334=CARTESIAN_POINT('Ctrl Pts',(163.696393588869,3.78143853801404,127.656551410448));
#29335=CARTESIAN_POINT('Ctrl Pts',(163.688645692092,3.69213975920012,127.552266939838));
#29336=CARTESIAN_POINT('Ctrl Pts',(163.680897795315,3.59861250283509,127.451873314542));
#29337=CARTESIAN_POINT('Ctrl Pts',(163.673151519231,3.50510481035586,127.351500689427));
#29338=CARTESIAN_POINT('Ctrl Pts',(163.665405243147,3.40737066598672,127.255017576655));
#29339=CARTESIAN_POINT('Ctrl Pts',(163.657658967062,3.3057743076256,127.162789625598));
#29340=CARTESIAN_POINT('Ctrl Pts',(163.649912633797,3.20417719930328,127.070560993735));
#29341=CARTESIAN_POINT('Ctrl Pts',(163.642166300532,3.09871810957786,126.98258784905));
#29342=CARTESIAN_POINT('Ctrl Pts',(163.634419967266,2.9897963086944,126.899197228536));
#29343=CARTESIAN_POINT('Ctrl Pts',(163.626671899263,2.88085011552887,126.815787933272));
#29344=CARTESIAN_POINT('Ctrl Pts',(163.61892383126,2.76843997852202,126.736963441868));
#29345=CARTESIAN_POINT('Ctrl Pts',(163.611175763257,2.65299591245853,126.663008694464));
#29346=CARTESIAN_POINT('Ctrl Pts',(163.603419460516,2.53742915106774,126.588975347075));
#29347=CARTESIAN_POINT('Ctrl Pts',(163.595663157774,2.41882234907478,126.519822293777));
#29348=CARTESIAN_POINT('Ctrl Pts',(163.587906855032,2.29763248374708,126.455789814172));
#29349=CARTESIAN_POINT('Ctrl Pts',(163.580146412518,2.17637793573922,126.391723158505));
#29350=CARTESIAN_POINT('Ctrl Pts',(163.572385970003,2.05253793015106,126.332782690209));
#29351=CARTESIAN_POINT('Ctrl Pts',(163.564625527489,1.92659048135476,126.279160933612));
#29352=CARTESIAN_POINT('Ctrl Pts',(163.556852627224,1.80044085053261,126.225453098612));
#29353=CARTESIAN_POINT('Ctrl Pts',(163.549079726958,1.6721773821065,126.177081175132));
#29354=CARTESIAN_POINT('Ctrl Pts',(163.541306826693,1.54229519524159,126.134188394485));
#29355=CARTESIAN_POINT('Ctrl Pts',(163.533816490931,1.41713455302368,126.092854874455));
#29356=CARTESIAN_POINT('Ctrl Pts',(163.526326155169,1.29047113423111,126.056609136849));
#29357=CARTESIAN_POINT('Ctrl Pts',(163.518835819407,1.16275598628657,126.025534236659));
#29358=CARTESIAN_POINT('Ctrl Pts',(163.511061485288,1.03019847968851,125.993281122183));
#29359=CARTESIAN_POINT('Ctrl Pts',(163.503287151169,0.896088014638653,125.966496521821));
#29360=CARTESIAN_POINT('Ctrl Pts',(163.49551281705,0.760915524507925,125.945328756479));
#29361=CARTESIAN_POINT('Ctrl Pts',(163.487748064103,0.625909622390663,125.924187078515));
#29362=CARTESIAN_POINT('Ctrl Pts',(163.479983311156,0.48984468196566,125.908648522269));
#29363=CARTESIAN_POINT('Ctrl Pts',(163.472218558209,0.353225147713974,125.898811203125));
#29364=CARTESIAN_POINT('Ctrl Pts',(163.464461517324,0.216741305909704,125.888983654545));
#29365=CARTESIAN_POINT('Ctrl Pts',(163.456704476438,0.0797043538883314,
125.884846102236));
#29366=CARTESIAN_POINT('Ctrl Pts',(163.448947435553,-0.05737310866623,125.886445267654));
#29367=CARTESIAN_POINT('Ctrl Pts',(163.441196244313,-0.194347200040018,
125.888043227128));
#29368=CARTESIAN_POINT('Ctrl Pts',(163.433445053073,-0.331361351783681,
125.895369288941));
#29369=CARTESIAN_POINT('Ctrl Pts',(163.425693861833,-0.46790026221552,125.908418174367));
#29370=CARTESIAN_POINT('Ctrl Pts',(163.417945965056,-0.60438113996813,125.921461513668));
#29371=CARTESIAN_POINT('Ctrl Pts',(163.410198068279,-0.740386789774988,
125.940222801703));
#29372=CARTESIAN_POINT('Ctrl Pts',(163.402450171502,-0.875404556627693,
125.964644724589));
#29373=CARTESIAN_POINT('Ctrl Pts',(163.394703895418,-1.01039408067422,125.989061538935));
#29374=CARTESIAN_POINT('Ctrl Pts',(163.386957619334,-1.1443957483139,126.019136563383));
#29375=CARTESIAN_POINT('Ctrl Pts',(163.379211343249,-1.27690504889282,126.054760996691));
#29376=CARTESIAN_POINT('Ctrl Pts',(163.371465009984,-1.40941532762526,126.090385692971));
#29377=CARTESIAN_POINT('Ctrl Pts',(163.363718676719,-1.54043283975595,126.131559778348));
#29378=CARTESIAN_POINT('Ctrl Pts',(163.355972343453,-1.66946662447946,126.17812410694));
#29379=CARTESIAN_POINT('Ctrl Pts',(163.34822427545,-1.79852930542436,126.224698863291));
#29380=CARTESIAN_POINT('Ctrl Pts',(163.340476207447,-1.92560700729007,126.276666132176));
#29381=CARTESIAN_POINT('Ctrl Pts',(163.332728139444,-2.05022756837374,126.333818147084));
#29382=CARTESIAN_POINT('Ctrl Pts',(163.324971836703,-2.17498057767278,126.391030903834));
#29383=CARTESIAN_POINT('Ctrl Pts',(163.317215533961,-2.29727087353789,126.453439251005));
#29384=CARTESIAN_POINT('Ctrl Pts',(163.309459231219,-2.41664929456,126.520788597674));
#29385=CARTESIAN_POINT('Ctrl Pts',(163.301698788705,-2.53609143143998,126.588173890717));
#29386=CARTESIAN_POINT('Ctrl Pts',(163.293938346191,-2.6526182646793,126.660505231934));
#29387=CARTESIAN_POINT('Ctrl Pts',(163.286177903676,-2.76580943966262,126.737484518399));
#29388=CARTESIAN_POINT('Ctrl Pts',(163.278405003411,-2.87918231916858,126.814587378849));
#29389=CARTESIAN_POINT('Ctrl Pts',(163.270632103146,-2.98920852604997,126.896352861255));
#29390=CARTESIAN_POINT('Ctrl Pts',(163.26285920288,-3.09549993174442,126.982441827865));
#29391=CARTESIAN_POINT('Ctrl Pts',(163.255368867118,-3.19792737711045,127.065401243694));
#29392=CARTESIAN_POINT('Ctrl Pts',(163.247878531356,-3.29688661447606,127.152375058692));
#29393=CARTESIAN_POINT('Ctrl Pts',(163.240388195594,-3.39206396517385,127.24302868714));
#29394=CARTESIAN_POINT('Ctrl Pts',(163.232729627453,-3.4893789920271,127.335718389282));
#29395=CARTESIAN_POINT('Ctrl Pts',(163.225071059311,-3.58306797339335,127.432567693409));
#29396=CARTESIAN_POINT('Ctrl Pts',(163.21741249117,-3.67274626851651,127.533257147848));
#29397=CARTESIAN_POINT('Ctrl Pts',(163.209762819814,-3.76232038640117,127.633829633636));
#29398=CARTESIAN_POINT('Ctrl Pts',(163.202113148457,-3.84789281451807,127.738233103802));
#29399=CARTESIAN_POINT('Ctrl Pts',(163.1944634771,-3.92911323611359,127.846109066346));
#29400=CARTESIAN_POINT('Ctrl Pts',(163.186820918863,-4.0102581341281,127.9538847194));
#29401=CARTESIAN_POINT('Ctrl Pts',(163.179178360626,-4.08705883121905,128.065126124343));
#29402=CARTESIAN_POINT('Ctrl Pts',(163.171535802389,-4.15920343475139,128.179439694785));
#29403=CARTESIAN_POINT('Ctrl Pts',(163.163898689599,-4.23129663408036,128.293671814949));
#29404=CARTESIAN_POINT('Ctrl Pts',(163.156261576809,-4.29874012499224,128.410971406206));
#29405=CARTESIAN_POINT('Ctrl Pts',(163.14862446402,-4.36126408326984,128.530914190117));
#29406=CARTESIAN_POINT('Ctrl Pts',(163.140990631086,-4.4237611898318,128.650805463061));
#29407=CARTESIAN_POINT('Ctrl Pts',(163.133356798152,-4.48134278053375,128.773337313375));
#29408=CARTESIAN_POINT('Ctrl Pts',(163.125722965218,-4.5337841800003,128.898059468304));
#29409=CARTESIAN_POINT('Ctrl Pts',(163.118089120101,-4.58622566316061,129.022781822282));
#29410=CARTESIAN_POINT('Ctrl Pts',(163.110455274984,-4.63352677233583,129.149694120223));
#29411=CARTESIAN_POINT('Ctrl Pts',(163.102821429866,-4.67551045595483,129.278324891));
#29412=CARTESIAN_POINT('Ctrl Pts',(163.096861892052,-4.70828598994256,129.378743478318));
#29413=CARTESIAN_POINT('Ctrl Pts',(163.090902354239,-4.73782174831892,129.480208908557));
#29414=CARTESIAN_POINT('Ctrl Pts',(163.084942816425,-4.76405452823405,129.582490119308));
#29415=CARTESIAN_POINT('Ctrl Pts',(164.834593643846,-4.76405452823405,129.582490119308));
#29416=CARTESIAN_POINT('Ctrl Pts',(164.826544756193,-4.79939512201895,129.720282558107));
#29417=CARTESIAN_POINT('Ctrl Pts',(164.818495868541,-4.82878719210012,129.859741089387));
#29418=CARTESIAN_POINT('Ctrl Pts',(164.810446980889,-4.85208430067357,130.000332631948));
#29419=CARTESIAN_POINT('Ctrl Pts',(164.802409401942,-4.8753486767581,130.140726643082));
#29420=CARTESIAN_POINT('Ctrl Pts',(164.794371822994,-4.89253510851404,130.282250151103));
#29421=CARTESIAN_POINT('Ctrl Pts',(164.786334244047,-4.9035478438914,130.424358505509));
#29422=CARTESIAN_POINT('Ctrl Pts',(164.779175974695,-4.91335578813071,130.550920233198));
#29423=CARTESIAN_POINT('Ctrl Pts',(164.772017705343,-4.91826760155312,130.677945492592));
#29424=CARTESIAN_POINT('Ctrl Pts',(164.764859435991,-4.9182499525822,130.805043570854));
#29425=CARTESIAN_POINT('',(165.110140563977,-4.9182479540109,130.799874486988));
#29426=CARTESIAN_POINT('Ctrl Pts',(165.180124424339,-4.76405452823406,129.582490119308));
#29427=CARTESIAN_POINT('Ctrl Pts',(165.176727138268,-4.77888498385569,129.640313840693));
#29428=CARTESIAN_POINT('Ctrl Pts',(165.173329852197,-4.79265305198197,129.698370631477));
#29429=CARTESIAN_POINT('Ctrl Pts',(165.169932566126,-4.80535313457782,129.756618132743));
#29430=CARTESIAN_POINT('Ctrl Pts',(165.159153962061,-4.84564681577433,129.941420572318));
#29431=CARTESIAN_POINT('Ctrl Pts',(165.148375357997,-4.8752919794919,130.128621269865));
#29432=CARTESIAN_POINT('Ctrl Pts',(165.137596753933,-4.89406303010228,130.317195224823));
#29433=CARTESIAN_POINT('Ctrl Pts',(165.128444690625,-4.91000144314016,130.477312505667));
#29434=CARTESIAN_POINT('Ctrl Pts',(165.119292627316,-4.91810068477407,130.638419860766));
#29435=CARTESIAN_POINT('Ctrl Pts',(165.110140564008,-4.91824795401041,130.799874486449));
#29436=CARTESIAN_POINT('Ctrl Pts',(165.110140563977,-4.9182479540109,130.799874486988));
#29437=CARTESIAN_POINT('Ctrl Pts',(165.102489678719,-4.91837106722112,130.934846326012));
#29438=CARTESIAN_POINT('Ctrl Pts',(165.09483879346,-4.91293394198934,131.069989105914));
#29439=CARTESIAN_POINT('Ctrl Pts',(165.087187908201,-4.90192116343657,131.204800338314));
#29440=CARTESIAN_POINT('Ctrl Pts',(165.079543020346,-4.89091701761987,131.339505894405));
#29441=CARTESIAN_POINT('Ctrl Pts',(165.071898132491,-4.87434594577441,131.473880020402));
#29442=CARTESIAN_POINT('Ctrl Pts',(165.064253244635,-4.85224459998632,131.607420642971));
#29443=CARTESIAN_POINT('Ctrl Pts',(165.056611766299,-4.83015311110892,131.740901708172));
#29444=CARTESIAN_POINT('Ctrl Pts',(165.048970287964,-4.80253631707366,131.873549612425));
#29445=CARTESIAN_POINT('Ctrl Pts',(165.041328809628,-4.76948263181031,132.004868213277));
#29446=CARTESIAN_POINT('Ctrl Pts',(165.033688916441,-4.73643580320209,132.136159573404));
#29447=CARTESIAN_POINT('Ctrl Pts',(165.026049023253,-4.69795442381423,132.266121787939));
#29448=CARTESIAN_POINT('Ctrl Pts',(165.018409130065,-4.65417774052173,132.394270244599));
#29449=CARTESIAN_POINT('Ctrl Pts',(165.010769059858,-4.61040004290534,132.522421670512));
#29450=CARTESIAN_POINT('Ctrl Pts',(165.003128989651,-4.56132692786859,132.648758873867));
#29451=CARTESIAN_POINT('Ctrl Pts',(164.995488919444,-4.50714692209329,132.772814245459));
#29452=CARTESIAN_POINT('Ctrl Pts',(164.98784691012,-4.45295316495702,132.896901103393));
#29453=CARTESIAN_POINT('Ctrl Pts',(164.980204900796,-4.39365010120368,133.018704609114));
#29454=CARTESIAN_POINT('Ctrl Pts',(164.972562891472,-4.32947338047244,133.137779420585));
#29455=CARTESIAN_POINT('Ctrl Pts',(164.964912864165,-4.26522932563666,133.256979165142));
#29456=CARTESIAN_POINT('Ctrl Pts',(164.957262836858,-4.19610159699709,133.37344414524));
#29457=CARTESIAN_POINT('Ctrl Pts',(164.949612809551,-4.12237072084906,133.486755574016));
#29458=CARTESIAN_POINT('Ctrl Pts',(164.941958298561,-4.04859663101648,133.600133414647));
#29459=CARTESIAN_POINT('Ctrl Pts',(164.934303787571,-3.97021425596207,133.710353697194));
#29460=CARTESIAN_POINT('Ctrl Pts',(164.926649276581,-3.88754520286731,133.817029759401));
#29461=CARTESIAN_POINT('Ctrl Pts',(164.918983534378,-3.80475485217408,133.923862343906));
#29462=CARTESIAN_POINT('Ctrl Pts',(164.911317792174,-3.7176655262465,134.027140019929));
#29463=CARTESIAN_POINT('Ctrl Pts',(164.90365204997,-3.62663680993003,134.126511804878));
#29464=CARTESIAN_POINT('Ctrl Pts',(164.899596347418,-3.57847638562538,134.179086283798));
#29465=CARTESIAN_POINT('Ctrl Pts',(164.895540644865,-3.52921386058134,134.230568105216));
#29466=CARTESIAN_POINT('Ctrl Pts',(164.891484942312,-3.47890617260596,134.280909898779));
#29467=CARTESIAN_POINT('Ctrl Pts',(164.883710608193,-3.38247188779414,134.377409560238));
#29468=CARTESIAN_POINT('Ctrl Pts',(164.875936274074,-3.2818666803904,134.470046614896));
#29469=CARTESIAN_POINT('Ctrl Pts',(164.868161939955,-3.17743268209208,134.558439014892));
#29470=CARTESIAN_POINT('Ctrl Pts',(164.860397187008,-3.07312738936337,134.646722479156));
#29471=CARTESIAN_POINT('Ctrl Pts',(164.852632434061,-2.96500298998962,134.730771447044));
#29472=CARTESIAN_POINT('Ctrl Pts',(164.844867681114,-2.85343927079618,134.810239720881));
#29473=CARTESIAN_POINT('Ctrl Pts',(164.837110640229,-2.74198635826087,134.889629065709));
#29474=CARTESIAN_POINT('Ctrl Pts',(164.829353599344,-2.62710124023978,134.964446545056));
#29475=CARTESIAN_POINT('Ctrl Pts',(164.821596558459,-2.5091974026208,135.034385612431));
#29476=CARTESIAN_POINT('Ctrl Pts',(164.813845367219,-2.39138247720325,135.104271938211));
#29477=CARTESIAN_POINT('Ctrl Pts',(164.806094175979,-2.2705536981992,135.169286975887));
#29478=CARTESIAN_POINT('Ctrl Pts',(164.798342984739,-2.14715390856942,135.229167184572));
#29479=CARTESIAN_POINT('Ctrl Pts',(164.790595087962,-2.02380656714206,135.28902194257));
#29480=CARTESIAN_POINT('Ctrl Pts',(164.782847191184,-1.89789073948527,135.343746041955));
#29481=CARTESIAN_POINT('Ctrl Pts',(164.775099294407,-1.76987407575634,135.393121759581));
#29482=CARTESIAN_POINT('Ctrl Pts',(164.767353018323,-1.64188419035378,135.442487148871));
#29483=CARTESIAN_POINT('Ctrl Pts',(164.759606742239,-1.51179470751058,135.486506241084));
#29484=CARTESIAN_POINT('Ctrl Pts',(164.751860466155,-1.38009310429455,135.525009522746));
#29485=CARTESIAN_POINT('Ctrl Pts',(164.74411413289,-1.24839052888712,135.563513088631));
#29486=CARTESIAN_POINT('Ctrl Pts',(164.736367799624,-1.11507618461801,135.596500653009));
#29487=CARTESIAN_POINT('Ctrl Pts',(164.728621466359,-0.98065216444509,135.623852747954));
#29488=CARTESIAN_POINT('Ctrl Pts',(164.720873398356,-0.84619804094479,135.651210968211));
#29489=CARTESIAN_POINT('Ctrl Pts',(164.713125330353,-0.710634130087389,
135.672931129812));
#29490=CARTESIAN_POINT('Ctrl Pts',(164.70537726235,-0.574471760764326,135.688945068528));
#29491=CARTESIAN_POINT('Ctrl Pts',(164.697620959608,-0.438164676454887,
135.70497602705));
#29492=CARTESIAN_POINT('Ctrl Pts',(164.689864656867,-0.30125825201202,135.715288602173));
#29493=CARTESIAN_POINT('Ctrl Pts',(164.682108354125,-0.164268529847385,
135.719866584667));
#29494=CARTESIAN_POINT('Ctrl Pts',(164.67434791161,-0.027205692143024,135.724447010567));
#29495=CARTESIAN_POINT('Ctrl Pts',(164.666587469096,0.109940141110505,135.723286748391));
#29496=CARTESIAN_POINT('Ctrl Pts',(164.658827026582,0.24665489611004,135.716421735338));
#29497=CARTESIAN_POINT('Ctrl Pts',(164.651054126317,0.383589117770987,135.709545701956));
#29498=CARTESIAN_POINT('Ctrl Pts',(164.643281226051,0.520090488796811,135.696946653504));
#29499=CARTESIAN_POINT('Ctrl Pts',(164.635508325786,0.655651112811216,135.678712336592));
#29500=CARTESIAN_POINT('Ctrl Pts',(164.628017990024,0.78628376668563,135.661140883028));
#29501=CARTESIAN_POINT('Ctrl Pts',(164.620527654262,0.916042579753152,135.638336813516));
#29502=CARTESIAN_POINT('Ctrl Pts',(164.6130373185,1.04448560797531,135.610422714255));
#29503=CARTESIAN_POINT('Ctrl Pts',(164.605262984381,1.1777985926524,135.581450243436));
#29504=CARTESIAN_POINT('Ctrl Pts',(164.597488650262,1.31011634237424,135.546880823988));
#29505=CARTESIAN_POINT('Ctrl Pts',(164.589714316143,1.44093249891663,135.506795794798));
#29506=CARTESIAN_POINT('Ctrl Pts',(164.581949563196,1.57158743623721,135.466760166823));
#29507=CARTESIAN_POINT('Ctrl Pts',(164.574184810249,1.7007440922588,135.421222567542));
#29508=CARTESIAN_POINT('Ctrl Pts',(164.566420057301,1.82790591701633,135.370315394065));
#29509=CARTESIAN_POINT('Ctrl Pts',(164.558663016416,1.95494144285745,135.319458782311));
#29510=CARTESIAN_POINT('Ctrl Pts',(164.550905975531,2.07998571968843,135.26324335391));
#29511=CARTESIAN_POINT('Ctrl Pts',(164.543148934646,2.20255734204255,135.201851290383));
#29512=CARTESIAN_POINT('Ctrl Pts',(164.535397743406,2.32503653218259,135.14050552309));
#29513=CARTESIAN_POINT('Ctrl Pts',(164.527646552166,2.44504643116031,135.073991065209));
#29514=CARTESIAN_POINT('Ctrl Pts',(164.519895360926,2.5621259471246,135.002538042779));
#29515=CARTESIAN_POINT('Ctrl Pts',(164.512147464149,2.67915570117121,134.93111538979));
#29516=CARTESIAN_POINT('Ctrl Pts',(164.504399567372,2.79325721636496,134.854758550289));
#29517=CARTESIAN_POINT('Ctrl Pts',(164.496651670595,2.90399453972257,134.773743286919));
#29518=CARTESIAN_POINT('Ctrl Pts',(164.488905394511,3.01470869921935,134.692744970196));
#29519=CARTESIAN_POINT('Ctrl Pts',(164.481159118427,3.12205975127329,134.607090398522));
#29520=CARTESIAN_POINT('Ctrl Pts',(164.473412842342,3.22564158613382,134.517098073986));
#29521=CARTESIAN_POINT('Ctrl Pts',(164.465666509077,3.32922418561214,134.427105085147));
#29522=CARTESIAN_POINT('Ctrl Pts',(164.457920175812,3.42903721724155,134.332774535968));
#29523=CARTESIAN_POINT('Ctrl Pts',(164.450173842546,3.52470877576302,134.234464276139));
#29524=CARTESIAN_POINT('Ctrl Pts',(164.442425774543,3.62040175926644,134.136132000411));
#29525=CARTESIAN_POINT('Ctrl Pts',(164.43467770654,3.7119511515193,134.033818520727));
#29526=CARTESIAN_POINT('Ctrl Pts',(164.426929638537,3.79902321826983,133.927917188135));
#29527=CARTESIAN_POINT('Ctrl Pts',(164.419173335796,3.88618782624916,133.821903302347));
#29528=CARTESIAN_POINT('Ctrl Pts',(164.411417033054,3.96886535430429,133.712294248825));
#29529=CARTESIAN_POINT('Ctrl Pts',(164.403660730312,4.04676323162127,133.599515427178));
#29530=CARTESIAN_POINT('Ctrl Pts',(164.395900287798,4.12470268538086,133.486676412079));
#29531=CARTESIAN_POINT('Ctrl Pts',(164.388139845283,4.19785719679812,133.370664588344));
#29532=CARTESIAN_POINT('Ctrl Pts',(164.380379402769,4.26597913140994,133.251931885757));
#29533=CARTESIAN_POINT('Ctrl Pts',(164.372606502504,4.33421042139878,133.133008582896));
#29534=CARTESIAN_POINT('Ctrl Pts',(164.364833602238,4.39739281038346,133.011356020095));
#29535=CARTESIAN_POINT('Ctrl Pts',(164.357060701973,4.45532559167427,132.887448934146));
#29536=CARTESIAN_POINT('Ctrl Pts',(164.349570366211,4.51115237044098,132.768046182875));
#29537=CARTESIAN_POINT('Ctrl Pts',(164.342080030449,4.56210446891386,132.646550261889));
#29538=CARTESIAN_POINT('Ctrl Pts',(164.334589694687,4.60804614078636,132.52339925206));
#29539=CARTESIAN_POINT('Ctrl Pts',(164.326815360568,4.65572970511176,132.395578934262));
#29540=CARTESIAN_POINT('Ctrl Pts',(164.319041026449,4.69816644923869,132.265570648371));
#29541=CARTESIAN_POINT('Ctrl Pts',(164.31126669233,4.73515110688718,132.133844373557));
#29542=CARTESIAN_POINT('Ctrl Pts',(164.303501939383,4.77209018425052,132.002280439605));
#29543=CARTESIAN_POINT('Ctrl Pts',(164.295737186436,4.8035904396895,131.869003102258));
#29544=CARTESIAN_POINT('Ctrl Pts',(164.287972433489,4.8294948652594,131.734501686938));
#29545=CARTESIAN_POINT('Ctrl Pts',(164.280215392603,4.85537356218869,131.60013386032));
#29546=CARTESIAN_POINT('Ctrl Pts',(164.272458351719,4.87566741617433,131.464544756596));
#29547=CARTESIAN_POINT('Ctrl Pts',(164.264701310833,4.89026949027675,131.32823786938));
#29548=CARTESIAN_POINT('Ctrl Pts',(164.256950119593,4.90486055284151,131.192033772249));
#29549=CARTESIAN_POINT('Ctrl Pts',(164.249198928353,4.91376833744172,131.055113356191));
#29550=CARTESIAN_POINT('Ctrl Pts',(164.241447737113,4.9169372242215,130.917988939586));
#29551=CARTESIAN_POINT('Ctrl Pts',(164.233699840336,4.92010476413985,130.780922804516));
#29552=CARTESIAN_POINT('Ctrl Pts',(164.225951943559,4.91753824857641,130.643653231391));
#29553=CARTESIAN_POINT('Ctrl Pts',(164.218204046782,4.90923404121606,130.506696056247));
#29554=CARTESIAN_POINT('Ctrl Pts',(164.210457770698,4.90093157091687,130.369767529591));
#29555=CARTESIAN_POINT('Ctrl Pts',(164.202711494614,4.88689381973439,130.23315166094));
#29556=CARTESIAN_POINT('Ctrl Pts',(164.19496521853,4.86716924025654,130.097362280085));
#29557=CARTESIAN_POINT('Ctrl Pts',(164.187218885264,4.84744451517635,129.961571896865));
#29558=CARTESIAN_POINT('Ctrl Pts',(164.179472551999,4.82203293423624,129.82660840052));
#29559=CARTESIAN_POINT('Ctrl Pts',(164.171726218734,4.79103454264045,129.692978111979));
#29560=CARTESIAN_POINT('Ctrl Pts',(164.163978150731,4.76002920916975,129.55931789786));
#29561=CARTESIAN_POINT('Ctrl Pts',(164.156230082728,4.72343466377439,129.42699186643));
#29562=CARTESIAN_POINT('Ctrl Pts',(164.148482014725,4.68140145231587,129.296493413614));
#29563=CARTESIAN_POINT('Ctrl Pts',(164.140725711983,4.63932356745998,129.165856265489));
#29564=CARTESIAN_POINT('Ctrl Pts',(164.132969409241,4.5917955898666,129.037050948808));
#29565=CARTESIAN_POINT('Ctrl Pts',(164.125213106499,4.53901727860459,128.910553550563));
#29566=CARTESIAN_POINT('Ctrl Pts',(164.117452663985,4.48621079796874,128.783988636848));
#29567=CARTESIAN_POINT('Ctrl Pts',(164.109692221471,4.42814856535426,128.659734450074));
#29568=CARTESIAN_POINT('Ctrl Pts',(164.101931778957,4.36507694961207,128.538243611217));
#29569=CARTESIAN_POINT('Ctrl Pts',(164.094158878691,4.30190408571302,128.416557744479));
#29570=CARTESIAN_POINT('Ctrl Pts',(164.086385978426,4.23370596381108,128.297644429485));
#29571=CARTESIAN_POINT('Ctrl Pts',(164.07861307816,4.1607735065459,128.181929133289));
#29572=CARTESIAN_POINT('Ctrl Pts',(164.071122742398,4.09049232780753,128.070420379579));
#29573=CARTESIAN_POINT('Ctrl Pts',(164.063632406636,4.01581522233693,127.961881423098));
#29574=CARTESIAN_POINT('Ctrl Pts',(164.056142070874,3.93703738578363,127.856663264471));
#29575=CARTESIAN_POINT('Ctrl Pts',(164.048367736755,3.85527266361391,127.74745572738));
#29576=CARTESIAN_POINT('Ctrl Pts',(164.040593402636,3.76883110744344,127.641479838522));
#29577=CARTESIAN_POINT('Ctrl Pts',(164.032819068517,3.67799717261996,127.539162329452));
#29578=CARTESIAN_POINT('Ctrl Pts',(164.02505431557,3.58727518250291,127.436970917568));
#29579=CARTESIAN_POINT('Ctrl Pts',(164.017289562622,3.49217184148334,127.338429204217));
#29580=CARTESIAN_POINT('Ctrl Pts',(164.009524809675,3.39301396626784,127.243933776974));
#29581=CARTESIAN_POINT('Ctrl Pts',(164.00176776879,3.29395457605215,127.149532203921));
#29582=CARTESIAN_POINT('Ctrl Pts',(163.994010727905,3.19084894678977,127.0591691873));
#29583=CARTESIAN_POINT('Ctrl Pts',(163.98625368702,3.08406287989156,126.973206846784));
#29584=CARTESIAN_POINT('Ctrl Pts',(163.97850249578,2.97735734119732,126.887309331139));
#29585=CARTESIAN_POINT('Ctrl Pts',(163.97075130454,2.86697719254218,126.805806130327));
#29586=CARTESIAN_POINT('Ctrl Pts',(163.9630001133,2.75332339799587,126.729020959507));
#29587=CARTESIAN_POINT('Ctrl Pts',(163.955252216523,2.63971790934375,126.652268424432));
#29588=CARTESIAN_POINT('Ctrl Pts',(163.947504319746,2.52284186544447,126.580230149393));
#29589=CARTESIAN_POINT('Ctrl Pts',(163.939756422969,2.40312728824704,126.513188015703));
#29590=CARTESIAN_POINT('Ctrl Pts',(163.932010146885,2.28343775275832,126.446159905781));
#29591=CARTESIAN_POINT('Ctrl Pts',(163.9242638708,2.16091120589356,126.384126049386));
#29592=CARTESIAN_POINT('Ctrl Pts',(163.916517594716,2.03600613701787,126.327323419538));
#29593=CARTESIAN_POINT('Ctrl Pts',(163.908771261451,1.91110014612176,126.270520370386));
#29594=CARTESIAN_POINT('Ctrl Pts',(163.901024928186,1.78381595407159,126.218948786684));
#29595=CARTESIAN_POINT('Ctrl Pts',(163.89327859492,1.65463361987969,126.172798176395));
#29596=CARTESIAN_POINT('Ctrl Pts',(163.885530526917,1.52542235619964,126.126637230998));
#29597=CARTESIAN_POINT('Ctrl Pts',(163.877782458914,1.39431247263143,126.085899806219));
#29598=CARTESIAN_POINT('Ctrl Pts',(163.870034390911,1.26180045085764,126.050725936113));
#29599=CARTESIAN_POINT('Ctrl Pts',(163.86227808817,1.12914759373007,126.015514682799));
#29600=CARTESIAN_POINT('Ctrl Pts',(163.854521785428,0.995090000025596,125.9858788965));
#29601=CARTESIAN_POINT('Ctrl Pts',(163.846765482686,0.860136189870434,125.961907850902));
#29602=CARTESIAN_POINT('Ctrl Pts',(163.839005040172,0.725110350803273,125.937924011235));
#29603=CARTESIAN_POINT('Ctrl Pts',(163.831244597658,0.58918772943176,125.919610988913));
#29604=CARTESIAN_POINT('Ctrl Pts',(163.823484155143,0.45288229698264,125.907006159537));
#29605=CARTESIAN_POINT('Ctrl Pts',(163.815711254878,0.316358054952771,125.894381095769));
#29606=CARTESIAN_POINT('Ctrl Pts',(163.807938354612,0.179450164528416,125.887482555823));
#29607=CARTESIAN_POINT('Ctrl Pts',(163.800165454347,0.0426738339851343,
125.886295753578));
#29608=CARTESIAN_POINT('Ctrl Pts',(163.792675118585,-0.0891303324227685,
125.885152094584));
#29609=CARTESIAN_POINT('Ctrl Pts',(163.785184782823,-0.220812030087202,
125.889312101193));
#29610=CARTESIAN_POINT('Ctrl Pts',(163.777694447061,-0.351916391783413,
125.898717141355));
#29611=CARTESIAN_POINT('Ctrl Pts',(163.769920112942,-0.487991615203079,
125.908478776473));
#29612=CARTESIAN_POINT('Ctrl Pts',(163.762145778823,-0.623875904455109,
125.923921949299));
#29613=CARTESIAN_POINT('Ctrl Pts',(163.754371444704,-0.759056483132193,
125.94503799832));
#29614=CARTESIAN_POINT('Ctrl Pts',(163.746606691757,-0.894070463827218,
125.966128023698));
#29615=CARTESIAN_POINT('Ctrl Pts',(163.73884193881,-1.02838207696434,125.992876954883));
#29616=CARTESIAN_POINT('Ctrl Pts',(163.731077185863,-1.16148100977317,126.025224196994));
#29617=CARTESIAN_POINT('Ctrl Pts',(163.723320144978,-1.29444774684561,126.057539311368));
#29618=CARTESIAN_POINT('Ctrl Pts',(163.715563104093,-1.42620382305366,126.095441579647));
#29619=CARTESIAN_POINT('Ctrl Pts',(163.707806063208,-1.5562468522622,126.138818977271));
#29620=CARTESIAN_POINT('Ctrl Pts',(163.700054871968,-1.68619181501131,126.182163663663));
#29621=CARTESIAN_POINT('Ctrl Pts',(163.692303680728,-1.81442593267833,126.23097513799));
#29622=CARTESIAN_POINT('Ctrl Pts',(163.684552489487,-1.94046012365977,126.285091033774));
#29623=CARTESIAN_POINT('Ctrl Pts',(163.67680459271,-2.06644074674768,126.339183928859));
#29624=CARTESIAN_POINT('Ctrl Pts',(163.669056695933,-2.19022294435144,126.398576607402));
#29625=CARTESIAN_POINT('Ctrl Pts',(163.661308799156,-2.31133604332367,126.463057960836));
#29626=CARTESIAN_POINT('Ctrl Pts',(163.653562523072,-2.43242380804632,126.527525826161));
#29627=CARTESIAN_POINT('Ctrl Pts',(163.645816246988,-2.55084323977889,126.597080065527));
#29628=CARTESIAN_POINT('Ctrl Pts',(163.638069970904,-2.66614714170715,126.671463028553));
#29629=CARTESIAN_POINT('Ctrl Pts',(163.630323637639,-2.78145189478281,126.745846540658));
#29630=CARTESIAN_POINT('Ctrl Pts',(163.622577304373,-2.89364074362766,126.825058635608));
#29631=CARTESIAN_POINT('Ctrl Pts',(163.614830971108,-3.00229476620142,126.908797859845));
#29632=CARTESIAN_POINT('Ctrl Pts',(163.607082903105,-3.11097312109015,126.992555836902));
#29633=CARTESIAN_POINT('Ctrl Pts',(163.599334835102,-3.21611476490606,127.080842722013));
#29634=CARTESIAN_POINT('Ctrl Pts',(163.591586767099,-3.31733352255727,127.173316502905));
#29635=CARTESIAN_POINT('Ctrl Pts',(163.583830464357,-3.41865985670864,127.265888566031));
#29636=CARTESIAN_POINT('Ctrl Pts',(163.576074161615,-3.5160546869873,127.362656149934));
#29637=CARTESIAN_POINT('Ctrl Pts',(163.568317858873,-3.60916803736314,127.463239676837));
#29638=CARTESIAN_POINT('Ctrl Pts',(163.560557416359,-3.70233108513772,127.563876888197));
#29639=CARTESIAN_POINT('Ctrl Pts',(163.552796973845,-3.7912078464149,127.6683338032));
#29640=CARTESIAN_POINT('Ctrl Pts',(163.545036531331,-3.87548906204061,127.776198205722));
#29641=CARTESIAN_POINT('Ctrl Pts',(163.537263631065,-3.95990557335569,127.884235761759));
#29642=CARTESIAN_POINT('Ctrl Pts',(163.5294907308,-4.03971156932458,127.995691418059));
#29643=CARTESIAN_POINT('Ctrl Pts',(163.521717830534,-4.11464100727173,128.110123723049));
#29644=CARTESIAN_POINT('Ctrl Pts',(163.514227494772,-4.18684657141375,128.220396125515));
#29645=CARTESIAN_POINT('Ctrl Pts',(163.50673715901,-4.25452381412898,128.333432252367));
#29646=CARTESIAN_POINT('Ctrl Pts',(163.499246823248,-4.31747619737546,128.44881771887));
#29647=CARTESIAN_POINT('Ctrl Pts',(163.491070124136,-4.38619710823455,128.574776323598));
#29648=CARTESIAN_POINT('Ctrl Pts',(163.482893425024,-4.44948688220427,128.7038996195));
#29649=CARTESIAN_POINT('Ctrl Pts',(163.474716725911,-4.50705826035773,128.835703994322));
#29650=CARTESIAN_POINT('Ctrl Pts',(163.466558243417,-4.56450137700018,128.967214726213));
#29651=CARTESIAN_POINT('Ctrl Pts',(163.458399760922,-4.61625136555339,129.101394325791));
#29652=CARTESIAN_POINT('Ctrl Pts',(163.450241278427,-4.66206679866313,129.237734871798));
#29653=CARTESIAN_POINT('Ctrl Pts',(163.44344819256,-4.70021460021492,129.351257581058));
#29654=CARTESIAN_POINT('Ctrl Pts',(163.436655106692,-4.73424876069842,129.466277884052));
#29655=CARTESIAN_POINT('Ctrl Pts',(163.429862020825,-4.76405452823405,129.582490119308));
#29656=CARTESIAN_POINT('Origin',(213.235140564004,0.,130.804360617566));
#29657=CARTESIAN_POINT('',(161.334944359449,-4.76405452823403,129.582490119308));
#29658=CARTESIAN_POINT('',(161.680195102581,-4.76405452823405,129.582490119308));
#29659=CARTESIAN_POINT('',(213.235140564004,-4.76405452823405,129.582490119308));
#29660=CARTESIAN_POINT('',(163.014859436027,-4.91824810772423,130.808674938719));
#29661=CARTESIAN_POINT('Ctrl Pts',(163.014859435991,-4.91824810772368,130.80867493935));
#29662=CARTESIAN_POINT('Ctrl Pts',(163.003397208645,-4.91807088703354,131.010703292268));
#29663=CARTESIAN_POINT('Ctrl Pts',(162.991934981299,-4.90544232132287,131.21220712713));
#29664=CARTESIAN_POINT('Ctrl Pts',(162.980472753952,-4.88057421730792,131.411961121063));
#29665=CARTESIAN_POINT('Ctrl Pts',(162.974295359895,-4.86717192879038,131.519615514723));
#29666=CARTESIAN_POINT('Ctrl Pts',(162.968117965839,-4.85021539564769,131.626762338073));
#29667=CARTESIAN_POINT('Ctrl Pts',(162.961940571782,-4.82974284417397,131.733213200945));
#29668=CARTESIAN_POINT('Ctrl Pts',(162.954166237662,-4.80397786075843,131.86718305419));
#29669=CARTESIAN_POINT('Ctrl Pts',(162.946391903543,-4.77259365760229,132.000292270418));
#29670=CARTESIAN_POINT('Ctrl Pts',(162.938617569424,-4.73565939896706,132.132032685313));
#29671=CARTESIAN_POINT('Ctrl Pts',(162.930852816477,-4.69877065850475,132.26361074192));
#29672=CARTESIAN_POINT('Ctrl Pts',(162.92308806353,-4.65634557654704,132.393822980838));
#29673=CARTESIAN_POINT('Ctrl Pts',(162.915323310583,-4.60850459624918,132.522169817929));
#29674=CARTESIAN_POINT('Ctrl Pts',(162.907566269698,-4.56071113228747,132.650389179131));
#29675=CARTESIAN_POINT('Ctrl Pts',(162.899809228813,-4.50751261039981,132.776746461578));
#29676=CARTESIAN_POINT('Ctrl Pts',(162.892052187928,-4.44907960724067,132.90075602658));
#29677=CARTESIAN_POINT('Ctrl Pts',(162.884300996688,-4.39069066886354,133.024672075005));
#29678=CARTESIAN_POINT('Ctrl Pts',(162.876549805448,-4.32707527217559,133.146243577686));
#29679=CARTESIAN_POINT('Ctrl Pts',(162.868798614208,-4.25845241201014,133.265004053163));
#29680=CARTESIAN_POINT('Ctrl Pts',(162.861050717431,-4.18985871839095,133.383714052269));
#29681=CARTESIAN_POINT('Ctrl Pts',(162.853302820653,-4.11626198952557,133.499615062655));
#29682=CARTESIAN_POINT('Ctrl Pts',(162.845554923876,-4.03792744697405,133.612264639336));
#29683=CARTESIAN_POINT('Ctrl Pts',(162.837808647792,-3.95960929032012,133.724890652155));
#29684=CARTESIAN_POINT('Ctrl Pts',(162.830062371708,-3.87655551429641,133.834266263303));
#29685=CARTESIAN_POINT('Ctrl Pts',(162.822316095624,-3.78907478375688,133.939977836807));
#29686=CARTESIAN_POINT('Ctrl Pts',(162.814569762359,-3.70159340745443,134.045690190649));
#29687=CARTESIAN_POINT('Ctrl Pts',(162.806823429093,-3.60968526068687,134.147738151674));
#29688=CARTESIAN_POINT('Ctrl Pts',(162.799077095828,-3.51369916539395,134.245741334315));
#29689=CARTESIAN_POINT('Ctrl Pts',(162.791329027825,-3.41769157468039,134.343766464089));
#29690=CARTESIAN_POINT('Ctrl Pts',(162.783580959822,-3.31760449173534,134.437744733782));
#29691=CARTESIAN_POINT('Ctrl Pts',(162.775832891819,-3.21382314562898,134.527333065909));
#29692=CARTESIAN_POINT('Ctrl Pts',(162.768076589077,-3.1099314994731,134.617016613581));
#29693=CARTESIAN_POINT('Ctrl Pts',(162.760320286336,-3.00233804335629,134.70230064761));
#29694=CARTESIAN_POINT('Ctrl Pts',(162.752563983594,-2.89146103349163,134.782882473017));
#29695=CARTESIAN_POINT('Ctrl Pts',(162.74480354108,-2.7805248452284,134.86350730737));
#29696=CARTESIAN_POINT('Ctrl Pts',(162.737043098565,-2.66630193659719,134.939424715985));
#29697=CARTESIAN_POINT('Ctrl Pts',(162.729282656051,-2.54923816469362,135.010376290643));
#29698=CARTESIAN_POINT('Ctrl Pts',(162.721509755786,-2.43198647163091,135.081441763067));
#29699=CARTESIAN_POINT('Ctrl Pts',(162.71373685552,-2.31188514488524,135.147525283159));
#29700=CARTESIAN_POINT('Ctrl Pts',(162.705963955255,-2.18940396812855,135.208414809653));
#29701=CARTESIAN_POINT('Ctrl Pts',(162.698473619493,-2.0713752906576,135.267090848489));
#29702=CARTESIAN_POINT('Ctrl Pts',(162.690983283731,-1.951137067367,135.320943841119));
#29703=CARTESIAN_POINT('Ctrl Pts',(162.683492947969,-1.82912399543438,135.369827567597));
#29704=CARTESIAN_POINT('Ctrl Pts',(162.67571861385,-1.70248476079516,135.420564735422));
#29705=CARTESIAN_POINT('Ctrl Pts',(162.667944279731,-1.57353227892646,135.466109099204));
#29706=CARTESIAN_POINT('Ctrl Pts',(162.660169945612,-1.44273146783083,135.506244173571));
#29707=CARTESIAN_POINT('Ctrl Pts',(162.652405192665,-1.31209185704487,135.546329785046));
#29708=CARTESIAN_POINT('Ctrl Pts',(162.644640439717,-1.17960881955273,135.5810192578));
#29709=CARTESIAN_POINT('Ctrl Pts',(162.63687568677,-1.04576777210489,135.610143886642));
#29710=CARTESIAN_POINT('Ctrl Pts',(162.629118645885,-0.912059657472297,
135.639239588491));
#29711=CARTESIAN_POINT('Ctrl Pts',(162.621361605,-0.776996596599036,135.662781362977));
#29712=CARTESIAN_POINT('Ctrl Pts',(162.613604564115,-0.641079371915657,
135.680650221497));
#29713=CARTESIAN_POINT('Ctrl Pts',(162.605853372875,-0.505264643468831,
135.698505604971));
#29714=CARTESIAN_POINT('Ctrl Pts',(162.598102181635,-0.36859741937794,135.710696536804));
#29715=CARTESIAN_POINT('Ctrl Pts',(162.590350990395,-0.231588535762066,
135.717155118927));
#29716=CARTESIAN_POINT('Ctrl Pts',(162.582603093618,-0.0946378845763739,
135.723610955981));
#29717=CARTESIAN_POINT('Ctrl Pts',(162.574855196841,0.0426537475999879,
135.724339270772));
#29718=CARTESIAN_POINT('Ctrl Pts',(162.567107300064,0.17977076054081,135.719324049389));
#29719=CARTESIAN_POINT('Ctrl Pts',(162.55936102398,0.316859091558426,135.714309877082));
#29720=CARTESIAN_POINT('Ctrl Pts',(162.551614747896,0.453772485537455,135.703554572581));
#29721=CARTESIAN_POINT('Ctrl Pts',(162.543868471811,0.589996097926005,135.687094244023));
#29722=CARTESIAN_POINT('Ctrl Pts',(162.536122138546,0.72622071588627,135.670633793958));
#29723=CARTESIAN_POINT('Ctrl Pts',(162.528375805281,0.861755153953806,135.648468282702));
#29724=CARTESIAN_POINT('Ctrl Pts',(162.520629472015,0.996090836200424,135.620685576343));
#29725=CARTESIAN_POINT('Ctrl Pts',(162.512881404012,1.13045660199162,135.592896648239));
#29726=CARTESIAN_POINT('Ctrl Pts',(162.50513333601,1.26362269498177,135.55948810106));
#29727=CARTESIAN_POINT('Ctrl Pts',(162.497385268007,1.39509224864404,135.520598597171));
#29728=CARTESIAN_POINT('Ctrl Pts',(162.489628965265,1.52670152971249,135.481667761055));
#29729=CARTESIAN_POINT('Ctrl Pts',(162.481872662523,1.6566102940577,135.43724444279));
#29730=CARTESIAN_POINT('Ctrl Pts',(162.474116359781,1.78433779812183,135.387516919144));
#29731=CARTESIAN_POINT('Ctrl Pts',(162.466355917267,1.91213347420086,135.337762854421));
#29732=CARTESIAN_POINT('Ctrl Pts',(162.458595474753,2.03774521232653,135.282699100171));
#29733=CARTESIAN_POINT('Ctrl Pts',(162.450835032238,2.16071460969468,135.222561092641));
#29734=CARTESIAN_POINT('Ctrl Pts',(162.443062131973,2.28388140845611,135.162326546243));
#29735=CARTESIAN_POINT('Ctrl Pts',(162.435289231708,2.40439704623602,135.097001655394));
#29736=CARTESIAN_POINT('Ctrl Pts',(162.427516331442,2.52182919716291,135.026867048921));
#29737=CARTESIAN_POINT('Ctrl Pts',(162.42002599568,2.63499239360999,134.959282012052));
#29738=CARTESIAN_POINT('Ctrl Pts',(162.412535659918,2.74529213817591,134.887231047424));
#29739=CARTESIAN_POINT('Ctrl Pts',(162.405045324156,2.85237044743471,134.81100084263));
#29740=CARTESIAN_POINT('Ctrl Pts',(162.397270990037,2.96350866333462,134.731880346452));
#29741=CARTESIAN_POINT('Ctrl Pts',(162.389496655918,3.07152839275741,134.648006812439));
#29742=CARTESIAN_POINT('Ctrl Pts',(162.381722321799,3.17599620089133,134.559654373642));
#29743=CARTESIAN_POINT('Ctrl Pts',(162.373957568852,3.28033526178828,134.47141082133));
#29744=CARTESIAN_POINT('Ctrl Pts',(162.366192815905,3.3811308155156,134.378699597134));
#29745=CARTESIAN_POINT('Ctrl Pts',(162.358428062957,3.47797854600734,134.281837906638));
#29746=CARTESIAN_POINT('Ctrl Pts',(162.350671022072,3.57473008596778,134.185072420539));
#29747=CARTESIAN_POINT('Ctrl Pts',(162.342913981187,3.66754133108121,134.084164946391));
#29748=CARTESIAN_POINT('Ctrl Pts',(162.335156940302,3.7560414877301,133.97947249039));
#29749=CARTESIAN_POINT('Ctrl Pts',(162.327405749062,3.84447490572244,133.874858983785));
#29750=CARTESIAN_POINT('Ctrl Pts',(162.319654557822,3.92860345484192,133.766466473976));
#29751=CARTESIAN_POINT('Ctrl Pts',(162.311903366582,4.00809389112144,133.654688041294));
#29752=CARTESIAN_POINT('Ctrl Pts',(162.304155469805,4.08755054184511,133.542957117428));
#29753=CARTESIAN_POINT('Ctrl Pts',(162.296407573028,4.16237277443135,133.427843450911));
#29754=CARTESIAN_POINT('Ctrl Pts',(162.288659676251,4.23226842140721,133.309772174907));
#29755=CARTESIAN_POINT('Ctrl Pts',(162.280913400167,4.3021494477205,133.191725596869));
#29756=CARTESIAN_POINT('Ctrl Pts',(162.273167124083,4.36710573917915,133.07072297613));
#29757=CARTESIAN_POINT('Ctrl Pts',(162.265420847999,4.42688938852497,132.947216983323));
#29758=CARTESIAN_POINT('Ctrl Pts',(162.257674514733,4.48667347918008,132.823710078822));
#29759=CARTESIAN_POINT('Ctrl Pts',(162.249928181468,4.54128468118888,132.697700117285));
#29760=CARTESIAN_POINT('Ctrl Pts',(162.242181848203,4.59052202106745,132.569662471809));
#29761=CARTESIAN_POINT('Ctrl Pts',(162.2344337802,4.63977038730688,132.441596153191));
#29762=CARTESIAN_POINT('Ctrl Pts',(162.226685712197,4.68364235640963,132.311501611899));
#29763=CARTESIAN_POINT('Ctrl Pts',(162.218937644194,4.7219860204571,132.179871826211));
#29764=CARTESIAN_POINT('Ctrl Pts',(162.211181341452,4.76037043660705,132.04810214282));
#29765=CARTESIAN_POINT('Ctrl Pts',(162.20342503871,4.79321470114337,131.914794331547));
#29766=CARTESIAN_POINT('Ctrl Pts',(162.195668735968,4.82041736300751,131.780454623754));
#29767=CARTESIAN_POINT('Ctrl Pts',(162.187908293454,4.84763454375136,131.646043214814));
#29768=CARTESIAN_POINT('Ctrl Pts',(162.18014785094,4.86920406050837,131.51059919784));
#29769=CARTESIAN_POINT('Ctrl Pts',(162.172387408426,4.8850762145486,131.374635499138));
#29770=CARTESIAN_POINT('Ctrl Pts',(162.16461450816,4.90097384797955,131.238453539436));
#29771=CARTESIAN_POINT('Ctrl Pts',(162.156841607895,4.9111558131901,131.101750621039));
#29772=CARTESIAN_POINT('Ctrl Pts',(162.149068707629,4.91562452846481,130.965042158681));
#29773=CARTESIAN_POINT('Ctrl Pts',(162.141578371867,4.9199307946833,130.833303393277));
#29774=CARTESIAN_POINT('Ctrl Pts',(162.134088036105,4.91893198371118,130.701559787998));
#29775=CARTESIAN_POINT('Ctrl Pts',(162.126597700343,4.91267579515416,130.570267486085));
#29776=CARTESIAN_POINT('Ctrl Pts',(162.118823366224,4.9061824013065,130.433997196641));
#29777=CARTESIAN_POINT('Ctrl Pts',(162.111049032105,4.89400452400106,130.297781445141));
#29778=CARTESIAN_POINT('Ctrl Pts',(162.103274697986,4.87613851703441,130.162133068178));
#29779=CARTESIAN_POINT('Ctrl Pts',(162.095509945039,4.85829452832462,130.026651865716));
#29780=CARTESIAN_POINT('Ctrl Pts',(162.087745192092,4.83477640854833,129.891737030411));
#29781=CARTESIAN_POINT('Ctrl Pts',(162.079980439144,4.8056324890368,129.757900182187));
#29782=CARTESIAN_POINT('Ctrl Pts',(162.072223398259,4.77651751567699,129.624196262607));
#29783=CARTESIAN_POINT('Ctrl Pts',(162.064466357374,4.74178794485278,129.491568578963));
#29784=CARTESIAN_POINT('Ctrl Pts',(162.056709316489,4.7015437129799,129.360522060996));
#29785=CARTESIAN_POINT('Ctrl Pts',(162.048958125249,4.66132982959531,129.229574366227));
#29786=CARTESIAN_POINT('Ctrl Pts',(162.041206934009,4.61560967701055,129.100205836022));
#29787=CARTESIAN_POINT('Ctrl Pts',(162.033455742769,4.56453383833639,128.972909307489));
#29788=CARTESIAN_POINT('Ctrl Pts',(162.025707845992,4.51347970825616,128.845666883377));
#29789=CARTESIAN_POINT('Ctrl Pts',(162.017959949215,4.45707456477479,128.720495071466));
#29790=CARTESIAN_POINT('Ctrl Pts',(162.010212052438,4.39551816080704,128.597869475387));
#29791=CARTESIAN_POINT('Ctrl Pts',(162.002465776354,4.33397463311198,128.475269529938));
#29792=CARTESIAN_POINT('Ctrl Pts',(161.99471950027,4.26728216349097,128.355215090114));
#29793=CARTESIAN_POINT('Ctrl Pts',(161.986973224185,4.19568759663884,128.238159406844));
#29794=CARTESIAN_POINT('Ctrl Pts',(161.97922689092,4.12409250129193,128.121102859496));
#29795=CARTESIAN_POINT('Ctrl Pts',(161.971480557655,4.04759544050142,128.007045446401));
#29796=CARTESIAN_POINT('Ctrl Pts',(161.963734224389,3.96648772804128,127.896413203014));
#29797=CARTESIAN_POINT('Ctrl Pts',(161.955986156386,3.8853618520713,127.785756184304));
#29798=CARTESIAN_POINT('Ctrl Pts',(161.948238088383,3.79962350094601,127.678526176875));
#29799=CARTESIAN_POINT('Ctrl Pts',(161.94049002038,3.70960532131113,127.575117451962));
#29800=CARTESIAN_POINT('Ctrl Pts',(161.932733717639,3.61949146928364,127.471598823026));
#29801=CARTESIAN_POINT('Ctrl Pts',(161.924977414897,3.5250889594336,127.371909884856));
#29802=CARTESIAN_POINT('Ctrl Pts',(161.917221112155,3.4267688617684,127.276409621518));
#29803=CARTESIAN_POINT('Ctrl Pts',(161.909460669641,3.32839628770669,127.180858386814));
#29804=CARTESIAN_POINT('Ctrl Pts',(161.901700227127,3.22610225092481,127.089500541908));
#29805=CARTESIAN_POINT('Ctrl Pts',(161.893939784612,3.12029142747198,127.002655148945));
#29806=CARTESIAN_POINT('Ctrl Pts',(161.886166884347,3.01431074709191,126.915670344047));
#29807=CARTESIAN_POINT('Ctrl Pts',(161.878393984081,2.90480231112118,126.833212701799));
#29808=CARTESIAN_POINT('Ctrl Pts',(161.870621083816,2.79220105971505,126.755558781883));
#29809=CARTESIAN_POINT('Ctrl Pts',(161.863130748054,2.68369314742319,126.680727777556));
#29810=CARTESIAN_POINT('Ctrl Pts',(161.855640412292,2.5723136394021,126.610357468845));
#29811=CARTESIAN_POINT('Ctrl Pts',(161.84815007653,2.45847208468172,126.544654281286));
#29812=CARTESIAN_POINT('Ctrl Pts',(161.840375742411,2.34031419281256,126.476459937401));
#29813=CARTESIAN_POINT('Ctrl Pts',(161.832601408292,2.21912958310019,126.413077589533));
#29814=CARTESIAN_POINT('Ctrl Pts',(161.824827074173,2.09534774863237,126.354787506042));
#29815=CARTESIAN_POINT('Ctrl Pts',(161.817062321226,1.97171846421286,126.296569259868));
#29816=CARTESIAN_POINT('Ctrl Pts',(161.809297568279,1.8454986740834,126.243430956144));
#29817=CARTESIAN_POINT('Ctrl Pts',(161.801532815331,1.71714494284011,126.195608475415));
#29818=CARTESIAN_POINT('Ctrl Pts',(161.793775774446,1.58891869433217,126.147833492649));
#29819=CARTESIAN_POINT('Ctrl Pts',(161.786018733561,1.45856308652389,126.105363961555));
#29820=CARTESIAN_POINT('Ctrl Pts',(161.778261692676,1.32655694918039,126.068388729655));
#29821=CARTESIAN_POINT('Ctrl Pts',(161.770510501436,1.19465035869195,126.031441381065));
#29822=CARTESIAN_POINT('Ctrl Pts',(161.762759310196,1.06109609107479,125.999980189719));
#29823=CARTESIAN_POINT('Ctrl Pts',(161.755008118956,0.926390177995158,125.974144856276));
#29824=CARTESIAN_POINT('Ctrl Pts',(161.747260222179,0.791741518521931,125.948320503539));
#29825=CARTESIAN_POINT('Ctrl Pts',(161.739512325402,0.65594257028796,125.928117326397));
#29826=CARTESIAN_POINT('Ctrl Pts',(161.731764428625,0.519501443425542,125.913624342446));
#29827=CARTESIAN_POINT('Ctrl Pts',(161.724018152541,0.383088857105533,125.899134390114));
#29828=CARTESIAN_POINT('Ctrl Pts',(161.716271876457,0.246034747878417,125.890352296417));
#29829=CARTESIAN_POINT('Ctrl Pts',(161.708525600373,0.108853874176539,125.887315377122));
#29830=CARTESIAN_POINT('Ctrl Pts',(161.700779267107,-0.0283280121632919,
125.884278435409));
#29831=CARTESIAN_POINT('Ctrl Pts',(161.693032933842,-0.165636273975663,
125.886986761376));
#29832=CARTESIAN_POINT('Ctrl Pts',(161.685286600577,-0.302555013355518,
125.895425547065));
#29833=CARTESIAN_POINT('Ctrl Pts',(161.677538532574,-0.439504414737683,
125.903866222562));
#29834=CARTESIAN_POINT('Ctrl Pts',(161.669790464571,-0.576063729957995,
125.918039887346));
#29835=CARTESIAN_POINT('Ctrl Pts',(161.662042396568,-0.711721443823145,
125.937879789606));
#29836=CARTESIAN_POINT('Ctrl Pts',(161.654286093826,-0.847523336321078,
125.95774077795));
#29837=CARTESIAN_POINT('Ctrl Pts',(161.646529791084,-0.982421325824132,
125.983279976987));
#29838=CARTESIAN_POINT('Ctrl Pts',(161.638773488342,-1.115912816468,126.014379234665));
#29839=CARTESIAN_POINT('Ctrl Pts',(161.631013045828,-1.24947555553986,126.045495090953));
#29840=CARTESIAN_POINT('Ctrl Pts',(161.623252603314,-1.38162992339948,126.082176814503));
#29841=CARTESIAN_POINT('Ctrl Pts',(161.6154921608,-1.5118887467382,126.124256400779));
#29842=CARTESIAN_POINT('Ctrl Pts',(161.607719260534,-1.64235667310394,126.166403536942));
#29843=CARTESIAN_POINT('Ctrl Pts',(161.599946360269,-1.7709226073832,126.21396571579));
#29844=CARTESIAN_POINT('Ctrl Pts',(161.592173460003,-1.89711877630473,126.266726497114));
#29845=CARTESIAN_POINT('Ctrl Pts',(161.584683124241,-2.0187273966176,126.317569291141));
#29846=CARTESIAN_POINT('Ctrl Pts',(161.577192788479,-2.13813527500847,126.373239154922));
#29847=CARTESIAN_POINT('Ctrl Pts',(161.569702452717,-2.25494736857407,126.433503101304));
#29848=CARTESIAN_POINT('Ctrl Pts',(161.561927252093,-2.37620194134867,126.496058945046));
#29849=CARTESIAN_POINT('Ctrl Pts',(161.554152051469,-2.49504352236654,126.563763402027));
#29850=CARTESIAN_POINT('Ctrl Pts',(161.546376850845,-2.61100400698034,126.636406546558));
#29851=CARTESIAN_POINT('Ctrl Pts',(161.538611423511,-2.72681873132558,126.708958379947));
#29852=CARTESIAN_POINT('Ctrl Pts',(161.530845996176,-2.83975923728124,126.78643634234));
#29853=CARTESIAN_POINT('Ctrl Pts',(161.523080568841,-2.94938017522137,126.868583738154));
#29854=CARTESIAN_POINT('Ctrl Pts',(161.515241560116,-3.06003982753177,126.951509522497));
#29855=CARTESIAN_POINT('Ctrl Pts',(161.507402551392,-3.16731630438019,127.039193531912));
#29856=CARTESIAN_POINT('Ctrl Pts',(161.499563542667,-3.27077868745617,127.131325109953));
#29857=CARTESIAN_POINT('Ctrl Pts',(161.491812679121,-3.37307769509291,127.22242072099));
#29858=CARTESIAN_POINT('Ctrl Pts',(161.484061815575,-3.47164763608889,127.31786413449));
#29859=CARTESIAN_POINT('Ctrl Pts',(161.476310952028,-3.56610326796046,127.417313150414));
#29860=CARTESIAN_POINT('Ctrl Pts',(161.468563642612,-3.66051558754889,127.516716564356));
#29861=CARTESIAN_POINT('Ctrl Pts',(161.460816333196,-3.75081708343823,127.620121643056));
#29862=CARTESIAN_POINT('Ctrl Pts',(161.45306902378,-3.83665870011573,127.727148716945));
#29863=CARTESIAN_POINT('Ctrl Pts',(161.44532358911,-3.92247954425601,127.834149891695));
#29864=CARTESIAN_POINT('Ctrl Pts',(161.43757815444,-4.00384241336998,127.944771012093));
#29865=CARTESIAN_POINT('Ctrl Pts',(161.429832719771,-4.08043821489942,128.05859896788));
#29866=CARTESIAN_POINT('Ctrl Pts',(161.421925356411,-4.15863535429632,128.174806649609));
#29867=CARTESIAN_POINT('Ctrl Pts',(161.414017993051,-4.23186362596502,128.294356412229));
#29868=CARTESIAN_POINT('Ctrl Pts',(161.40611062969,-4.29984067448549,128.416777480471));
#29869=CARTESIAN_POINT('Ctrl Pts',(161.398361401453,-4.36645828644137,128.536750315375));
#29870=CARTESIAN_POINT('Ctrl Pts',(161.390612173215,-4.42803258524586,128.659480318208));
#29871=CARTESIAN_POINT('Ctrl Pts',(161.382862944977,-4.48434464039871,128.784500174707));
#29872=CARTESIAN_POINT('Ctrl Pts',(161.374876514056,-4.54238039889116,128.913346869768));
#29873=CARTESIAN_POINT('Ctrl Pts',(161.366890083134,-4.59482641609933,129.044625440944));
#29874=CARTESIAN_POINT('Ctrl Pts',(161.358903652213,-4.64149715716548,129.177803762573));
#29875=CARTESIAN_POINT('Ctrl Pts',(161.350917221292,-4.6881678982316,129.310982084201));
#29876=CARTESIAN_POINT('Ctrl Pts',(161.342930790371,-4.72906326476933,129.446059714126));
#29877=CARTESIAN_POINT('Ctrl Pts',(161.334944359449,-4.76405452823403,129.582490119308));
#29878=CARTESIAN_POINT('Ctrl Pts',(163.084942816425,-4.76405452823405,129.582490119308));
#29879=CARTESIAN_POINT('Ctrl Pts',(163.077305556572,-4.79767232933164,129.713565415566));
#29880=CARTESIAN_POINT('Ctrl Pts',(163.06966829672,-4.82586396033538,129.8459805258));
#29881=CARTESIAN_POINT('Ctrl Pts',(163.062031036868,-4.84854190088311,129.979239718618));
#29882=CARTESIAN_POINT('Ctrl Pts',(163.054169103394,-4.87188698319665,130.116419142774));
#29883=CARTESIAN_POINT('Ctrl Pts',(163.046307169921,-4.88938889275877,130.254492623326));
#29884=CARTESIAN_POINT('Ctrl Pts',(163.038445236447,-4.90100955637683,130.392913912873));
#29885=CARTESIAN_POINT('Ctrl Pts',(163.030583302974,-4.9126302199949,130.53133520242));
#29886=CARTESIAN_POINT('Ctrl Pts',(163.0227213695,-4.91836966325008,130.670103837096));
#29887=CARTESIAN_POINT('Ctrl Pts',(163.014859436027,-4.91824810772423,130.80867493872));
#29888=CARTESIAN_POINT('',(163.360140564019,-4.91824999998649,130.804349090908));
#29889=CARTESIAN_POINT('Ctrl Pts',(163.429862020825,-4.76405452823405,129.582490119308));
#29890=CARTESIAN_POINT('Ctrl Pts',(163.421727513463,-4.79974600044378,129.72165062776));
#29891=CARTESIAN_POINT('Ctrl Pts',(163.4135930061,-4.82937292020494,129.862520536798));
#29892=CARTESIAN_POINT('Ctrl Pts',(163.405458498738,-4.85278248757454,130.004557397524));
#29893=CARTESIAN_POINT('Ctrl Pts',(163.397339092563,-4.87614859659454,130.146330575993));
#29894=CARTESIAN_POINT('Ctrl Pts',(163.389219686388,-4.89332031540393,130.289266059976));
#29895=CARTESIAN_POINT('Ctrl Pts',(163.381100280213,-4.9041954478384,130.432809716745));
#29896=CARTESIAN_POINT('Ctrl Pts',(163.374113708152,-4.91355326228837,130.55632590504));
#29897=CARTESIAN_POINT('Ctrl Pts',(163.367127136091,-4.91824970923526,130.680292043314));
#29898=CARTESIAN_POINT('Ctrl Pts',(163.36014056403,-4.91824999998649,130.804349090714));
#29899=CARTESIAN_POINT('Ctrl Pts',(163.360140564008,-4.91824999998649,130.804349091103));
#29900=CARTESIAN_POINT('Ctrl Pts',(163.352027365337,-4.91825033761171,130.948411080773));
#29901=CARTESIAN_POINT('Ctrl Pts',(163.343914166666,-4.91191672099125,131.092351239516));
#29902=CARTESIAN_POINT('Ctrl Pts',(163.335800967995,-4.8993069962004,131.235607669129));
#29903=CARTESIAN_POINT('Ctrl Pts',(163.327677138385,-4.88668074855336,131.379051811434));
#29904=CARTESIAN_POINT('Ctrl Pts',(163.319553308775,-4.86776201198404,131.521810105082));
#29905=CARTESIAN_POINT('Ctrl Pts',(163.311429479165,-4.8426600497321,131.663329013509));
#29906=CARTESIAN_POINT('Ctrl Pts',(163.30328650322,-4.81749892688766,131.805181455322));
#29907=CARTESIAN_POINT('Ctrl Pts',(163.295143527275,-4.78612550029788,131.945788342313));
#29908=CARTESIAN_POINT('Ctrl Pts',(163.28700055133,-4.74869987052856,132.084607703929));
#29909=CARTESIAN_POINT('Ctrl Pts',(163.278847477325,-4.71122782944042,132.223599214677));
#29910=CARTESIAN_POINT('Ctrl Pts',(163.27069440332,-4.66768870775622,132.360798458793));
#29911=CARTESIAN_POINT('Ctrl Pts',(163.262541329315,-4.61829148051881,132.495681658489));
#29912=CARTESIAN_POINT('Ctrl Pts',(163.254369571787,-4.56878105496329,132.63087395552));
#29913=CARTESIAN_POINT('Ctrl Pts',(163.246197814258,-4.51338580912547,132.76373928711));
#29914=CARTESIAN_POINT('Ctrl Pts',(163.23802605673,-4.4523623286491,132.893775070691));
#29915=CARTESIAN_POINT('Ctrl Pts',(163.232283770965,-4.40948119052899,132.985151084526));
#29916=CARTESIAN_POINT('Ctrl Pts',(163.2265414852,-4.36382188014511,133.07513042235));
#29917=CARTESIAN_POINT('Ctrl Pts',(163.220799199435,-4.31548629801546,133.163547145618));
#29918=CARTESIAN_POINT('Ctrl Pts',(163.213024865316,-4.2500459871878,133.283252290318));
#29919=CARTESIAN_POINT('Ctrl Pts',(163.205250531197,-4.17951758610824,133.400422151176));
#29920=CARTESIAN_POINT('Ctrl Pts',(163.197476197078,-4.10412211663965,133.514593949626));
#29921=CARTESIAN_POINT('Ctrl Pts',(163.189711444131,-4.02881956534892,133.628625041538));
#29922=CARTESIAN_POINT('Ctrl Pts',(163.181946691184,-3.94866209372835,133.739665099564));
#29923=CARTESIAN_POINT('Ctrl Pts',(163.174181938237,-3.86391693387252,133.847275172829));
#29924=CARTESIAN_POINT('Ctrl Pts',(163.166424897352,-3.77925594410389,133.954778366253));
#29925=CARTESIAN_POINT('Ctrl Pts',(163.158667856467,-3.69001657417765,134.058858049254));
#29926=CARTESIAN_POINT('Ctrl Pts',(163.150910815582,-3.59650953751703,134.159103857972));
#29927=CARTESIAN_POINT('Ctrl Pts',(163.143159624342,-3.5030730152402,134.259274070545));
#29928=CARTESIAN_POINT('Ctrl Pts',(163.135408433101,-3.40537549762023,134.355615878763));
#29929=CARTESIAN_POINT('Ctrl Pts',(163.127657241861,-3.30376795466278,134.447751944921));
#29930=CARTESIAN_POINT('Ctrl Pts',(163.119909345084,-3.20220359762173,134.539848850792));
#29931=CARTESIAN_POINT('Ctrl Pts',(163.112161448307,-3.09673280958298,134.627743307833));
#29932=CARTESIAN_POINT('Ctrl Pts',(163.10441355153,-2.98774324052898,134.711094981606));
#29933=CARTESIAN_POINT('Ctrl Pts',(163.096667275446,-2.87877646974333,134.794429220006));
#29934=CARTESIAN_POINT('Ctrl Pts',(163.088920999362,-2.76629269235277,134.873222327888));
#29935=CARTESIAN_POINT('Ctrl Pts',(163.081174723278,-2.65071213058344,134.947174668821));
#29936=CARTESIAN_POINT('Ctrl Pts',(163.073428390012,-2.53513071562447,135.021127555654));
#29937=CARTESIAN_POINT('Ctrl Pts',(163.065682056747,-2.4164527999954,135.090239393522));
#29938=CARTESIAN_POINT('Ctrl Pts',(163.057935723482,-2.29512669277534,135.154254469904));
#29939=CARTESIAN_POINT('Ctrl Pts',(163.050187655479,-2.17377341541524,135.218283882019));
#29940=CARTESIAN_POINT('Ctrl Pts',(163.042439587476,-2.0497711120938,135.277214079013));
#29941=CARTESIAN_POINT('Ctrl Pts',(163.034691519473,-1.92359136891616,135.33083599118));
#29942=CARTESIAN_POINT('Ctrl Pts',(163.026935216731,-1.79727752040557,135.384514893353));
#29943=CARTESIAN_POINT('Ctrl Pts',(163.019178913989,-1.66878196955274,135.432874087623));
#29944=CARTESIAN_POINT('Ctrl Pts',(163.011422611247,-1.5385954221819,135.475753042672));
#29945=CARTESIAN_POINT('Ctrl Pts',(163.003662168733,-1.40833939033111,135.518654883511));
#29946=CARTESIAN_POINT('Ctrl Pts',(162.995901726219,-1.27639093953481,135.556070550276));
#29947=CARTESIAN_POINT('Ctrl Pts',(162.988141283705,-1.14325353610117,135.587890111015));
#29948=CARTESIAN_POINT('Ctrl Pts',(162.98036838344,-1.00990240868793,135.619760751337));
#29949=CARTESIAN_POINT('Ctrl Pts',(162.972595483174,-0.875358898569053,
135.646017259078));
#29950=CARTESIAN_POINT('Ctrl Pts',(162.964822582909,-0.74013509854036,135.666601160609));
#29951=CARTESIAN_POINT('Ctrl Pts',(162.957332247147,-0.609827024251047,
135.686436785472));
#29952=CARTESIAN_POINT('Ctrl Pts',(162.949841911385,-0.478887567978155,
135.701005036775));
#29953=CARTESIAN_POINT('Ctrl Pts',(162.942351575623,-0.347775314005544,
135.710299405756));
#29954=CARTESIAN_POINT('Ctrl Pts',(162.934577241504,-0.211691899072754,
135.719946173562));
#29955=CARTESIAN_POINT('Ctrl Pts',(162.926802907384,-0.0749912531742415,
135.723941804092));
#29956=CARTESIAN_POINT('Ctrl Pts',(162.919028573265,0.0618178072596507,
135.722222106181));
#29957=CARTESIAN_POINT('Ctrl Pts',(162.911263820318,0.198458262753396,135.720504527644));
#29958=CARTESIAN_POINT('Ctrl Pts',(162.903499067371,0.335206479754615,135.71308564026));
#29959=CARTESIAN_POINT('Ctrl Pts',(162.895734314424,0.471548710985654,135.699953010287));
#29960=CARTESIAN_POINT('Ctrl Pts',(162.887977273539,0.607755525191009,135.686833423828));
#29961=CARTESIAN_POINT('Ctrl Pts',(162.880220232654,0.743556769427832,135.668011425468));
#29962=CARTESIAN_POINT('Ctrl Pts',(162.872463191769,0.878439244762312,135.643526615521));
#29963=CARTESIAN_POINT('Ctrl Pts',(162.864712000529,1.01322000417254,135.619060269759));
#29964=CARTESIAN_POINT('Ctrl Pts',(162.856960809289,1.14708299063578,135.588939681869));
#29965=CARTESIAN_POINT('Ctrl Pts',(162.849209618049,1.27952103139354,135.553256172611));
#29966=CARTESIAN_POINT('Ctrl Pts',(162.841461721272,1.41190278245102,135.517587829795));
#29967=CARTESIAN_POINT('Ctrl Pts',(162.833713824494,1.54286041566226,135.476361369703));
#29968=CARTESIAN_POINT('Ctrl Pts',(162.825965927717,1.67189806374138,135.429718974165));
#29969=CARTESIAN_POINT('Ctrl Pts',(162.818219651633,1.80090871992625,135.38308633521));
#29970=CARTESIAN_POINT('Ctrl Pts',(162.810473375549,1.92799982237271,135.331040147025));
#29971=CARTESIAN_POINT('Ctrl Pts',(162.802727099465,2.05269213808747,135.273771993657));
#29972=CARTESIAN_POINT('Ctrl Pts',(162.7949807662,2.1773853742525,135.216503417549));
#29973=CARTESIAN_POINT('Ctrl Pts',(162.787234432934,2.29967943306641,135.154012962516));
#29974=CARTESIAN_POINT('Ctrl Pts',(162.779488099669,2.41911685433489,135.086539584818));
#29975=CARTESIAN_POINT('Ctrl Pts',(162.771740031666,2.5385810227859,135.019051096924));
#29976=CARTESIAN_POINT('Ctrl Pts',(162.763991963663,2.65518694037741,134.946577658138));
#29977=CARTESIAN_POINT('Ctrl Pts',(162.75624389566,2.76850380703408,134.86940301992));
#29978=CARTESIAN_POINT('Ctrl Pts',(162.748487592918,2.88194110820509,134.792146359579));
#29979=CARTESIAN_POINT('Ctrl Pts',(162.740731290176,2.99208205186223,134.710178739205));
#29980=CARTESIAN_POINT('Ctrl Pts',(162.732974987434,3.09852633997754,134.623826232409));
#29981=CARTESIAN_POINT('Ctrl Pts',(162.72521454492,3.20502744061439,134.537427636679));
#29982=CARTESIAN_POINT('Ctrl Pts',(162.717454102406,3.30782766140585,134.446639749864));
#29983=CARTESIAN_POINT('Ctrl Pts',(162.709693659892,3.4065623776501,134.351826731524));
#29984=CARTESIAN_POINT('Ctrl Pts',(162.701920759626,3.50545559162617,134.256861510909));
#29985=CARTESIAN_POINT('Ctrl Pts',(162.694147859361,3.60026998883824,134.15785852916));
#29986=CARTESIAN_POINT('Ctrl Pts',(162.686374959096,3.69067957510331,134.055217018027));
#29987=CARTESIAN_POINT('Ctrl Pts',(162.678884623333,3.77780254517988,133.956306784361));
#29988=CARTESIAN_POINT('Ctrl Pts',(162.671394287571,3.86083520208575,133.854018207079));
#29989=CARTESIAN_POINT('Ctrl Pts',(162.663903951809,3.93952419380693,133.748733587981));
#29990=CARTESIAN_POINT('Ctrl Pts',(162.65612961769,4.02119670256608,133.63945707055));
#29991=CARTESIAN_POINT('Ctrl Pts',(162.648355283571,4.09844837790067,133.526606681492));
#29992=CARTESIAN_POINT('Ctrl Pts',(162.640580949452,4.1709501862553,133.410575805588));
#29993=CARTESIAN_POINT('Ctrl Pts',(162.632816196505,4.24336264261067,133.294687927369));
#29994=CARTESIAN_POINT('Ctrl Pts',(162.625051443558,4.31103667409021,133.175627689647));
#29995=CARTESIAN_POINT('Ctrl Pts',(162.617286690611,4.37368412688342,133.053820601817));
#29996=CARTESIAN_POINT('Ctrl Pts',(162.609529649726,4.43626935734329,132.932134494504));
#29997=CARTESIAN_POINT('Ctrl Pts',(162.601772608841,4.49383776669642,132.807707311771));
#29998=CARTESIAN_POINT('Ctrl Pts',(162.594015567956,4.54614527524743,132.680992227351));
#29999=CARTESIAN_POINT('Ctrl Pts',(162.586264376716,4.5984133382994,132.554372699762));
#30000=CARTESIAN_POINT('Ctrl Pts',(162.578513185476,4.64542824861686,132.425469064563));
#30001=CARTESIAN_POINT('Ctrl Pts',(162.570761994236,4.68699269767674,132.294757381661));
#30002=CARTESIAN_POINT('Ctrl Pts',(162.563014097458,4.72853948073707,132.164101254711));
#30003=CARTESIAN_POINT('Ctrl Pts',(162.555266200681,4.76464029183585,132.031638980285));
#30004=CARTESIAN_POINT('Ctrl Pts',(162.547518303904,4.79514672419508,131.897864598327));
#30005=CARTESIAN_POINT('Ctrl Pts',(162.53977202782,4.82564677526629,131.764118199087));
#30006=CARTESIAN_POINT('Ctrl Pts',(162.532025751736,4.85055468836595,131.629060619178));
#30007=CARTESIAN_POINT('Ctrl Pts',(162.524279475652,4.86977261144262,131.49319860675));
#30008=CARTESIAN_POINT('Ctrl Pts',(162.516533142387,4.88899067638157,131.35733559142));
#30009=CARTESIAN_POINT('Ctrl Pts',(162.508786809121,4.90251861272758,131.220668518832));
#30010=CARTESIAN_POINT('Ctrl Pts',(162.501040475856,4.91031019274151,131.083711424901));
#30011=CARTESIAN_POINT('Ctrl Pts',(162.493292407853,4.91810351762577,130.946723660378));
#30012=CARTESIAN_POINT('Ctrl Pts',(162.48554433985,4.92015790773628,130.809446135531));
#30013=CARTESIAN_POINT('Ctrl Pts',(162.477796271847,4.91647923325096,130.672394669261));
#30014=CARTESIAN_POINT('Ctrl Pts',(162.470039969105,4.91279664902662,130.535197543061));
#30015=CARTESIAN_POINT('Ctrl Pts',(162.462283666364,4.90336883895152,130.398227346826));
#30016=CARTESIAN_POINT('Ctrl Pts',(162.454527363622,4.88825376712604,130.261997113375));
#30017=CARTESIAN_POINT('Ctrl Pts',(162.446766921108,4.87313062793161,130.125694169747));
#30018=CARTESIAN_POINT('Ctrl Pts',(162.439006478593,4.85231423788077,129.990132362101));
#30019=CARTESIAN_POINT('Ctrl Pts',(162.431246036079,4.82591388616612,129.855815296662));
#30020=CARTESIAN_POINT('Ctrl Pts',(162.423473135814,4.79947115426317,129.721282613546));
#30021=CARTESIAN_POINT('Ctrl Pts',(162.415700235549,4.76742663947144,129.58799904597));
#30022=CARTESIAN_POINT('Ctrl Pts',(162.407927335283,4.7299400189492,129.456454656587));
#30023=CARTESIAN_POINT('Ctrl Pts',(162.400436999521,4.69381613150577,129.329692237097));
#30024=CARTESIAN_POINT('Ctrl Pts',(162.392946663759,4.65263903371826,129.204545036676));
#30025=CARTESIAN_POINT('Ctrl Pts',(162.385456327997,4.60659342396651,129.08143285101));
#30026=CARTESIAN_POINT('Ctrl Pts',(162.377681993878,4.55880198092614,128.953652829407));
#30027=CARTESIAN_POINT('Ctrl Pts',(162.369907659759,4.5056141700184,128.827660415257));
#30028=CARTESIAN_POINT('Ctrl Pts',(162.36213332564,4.44718310632606,128.703945067893));
#30029=CARTESIAN_POINT('Ctrl Pts',(162.354368572693,4.38882405369765,128.580382188638));
#30030=CARTESIAN_POINT('Ctrl Pts',(162.346603819745,4.3252347707861,128.459091142629));
#30031=CARTESIAN_POINT('Ctrl Pts',(162.338839066798,4.25661749652277,128.340544360051));
#30032=CARTESIAN_POINT('Ctrl Pts',(162.331082025913,4.18806837390321,128.222115319807));
#30033=CARTESIAN_POINT('Ctrl Pts',(162.323324985028,4.1145013925504,128.106425455026));
#30034=CARTESIAN_POINT('Ctrl Pts',(162.315567944143,4.03616588932347,127.993925068339));
#30035=CARTESIAN_POINT('Ctrl Pts',(162.307816752903,3.95788945950889,127.881509519068));
#30036=CARTESIAN_POINT('Ctrl Pts',(162.300065561663,3.87485188790448,127.772278980015));
#30037=CARTESIAN_POINT('Ctrl Pts',(162.292314370423,3.78734704711624,127.666656774435));
#30038=CARTESIAN_POINT('Ctrl Pts',(162.284566473646,3.69987939821988,127.56107946111));
#30039=CARTESIAN_POINT('Ctrl Pts',(162.276818576869,3.60794850542882,127.459107731407));
#30040=CARTESIAN_POINT('Ctrl Pts',(162.269070680092,3.51188980105184,127.361133484807));
#30041=CARTESIAN_POINT('Ctrl Pts',(162.261324404007,3.41585119008487,127.263179732307));
#30042=CARTESIAN_POINT('Ctrl Pts',(162.253578127923,3.31568675851793,127.169222078682));
#30043=CARTESIAN_POINT('Ctrl Pts',(162.245831851839,3.21176995649636,127.079616759386));
#30044=CARTESIAN_POINT('Ctrl Pts',(162.238085518574,3.10785238738509,126.990010778645));
#30045=CARTESIAN_POINT('Ctrl Pts',(162.230339185309,3.0001826886377,126.904757451653));
#30046=CARTESIAN_POINT('Ctrl Pts',(162.222592852043,2.88916834600419,126.824173520086));
#30047=CARTESIAN_POINT('Ctrl Pts',(162.21484478404,2.77812914247757,126.743571542305));
#30048=CARTESIAN_POINT('Ctrl Pts',(162.207096716037,2.66374412095743,126.667641270352));
#30049=CARTESIAN_POINT('Ctrl Pts',(162.199348648034,2.54645042746821,126.596656578194));
#30050=CARTESIAN_POINT('Ctrl Pts',(162.191592345292,2.42903207284633,126.525596442661));
#30051=CARTESIAN_POINT('Ctrl Pts',(162.18383604255,2.30869920592379,126.459492589539));
#30052=CARTESIAN_POINT('Ctrl Pts',(162.176079739809,2.18591478675273,126.398573558758));
#30053=CARTESIAN_POINT('Ctrl Pts',(162.168319297294,2.06306483384016,126.337622013657));
#30054=CARTESIAN_POINT('Ctrl Pts',(162.16055885478,1.93776107846641,126.281860963844));
#30055=CARTESIAN_POINT('Ctrl Pts',(162.152798412266,1.81048629228962,126.231470672692));
#30056=CARTESIAN_POINT('Ctrl Pts',(162.145025512001,1.68300719332704,126.180999490571));
#30057=CARTESIAN_POINT('Ctrl Pts',(162.137252611735,1.55355111016339,126.135916424507));
#30058=CARTESIAN_POINT('Ctrl Pts',(162.12947971147,1.42261665579041,126.096352024417));
#30059=CARTESIAN_POINT('Ctrl Pts',(162.121989375708,1.29644199863962,126.058225889927));
#30060=CARTESIAN_POINT('Ctrl Pts',(162.114499039946,1.16889488741463,126.025224229775));
#30061=CARTESIAN_POINT('Ctrl Pts',(162.107008704184,1.04042834210103,125.997418561804));
#30062=CARTESIAN_POINT('Ctrl Pts',(162.099234370065,0.907090948673375,125.968558633481));
#30063=CARTESIAN_POINT('Ctrl Pts',(162.091460035946,0.772340651378395,125.945205067771));
#30064=CARTESIAN_POINT('Ctrl Pts',(162.083685701827,0.636672008656077,125.927493609343));
#30065=CARTESIAN_POINT('Ctrl Pts',(162.075920948879,0.501170565410721,125.909803978705));
#30066=CARTESIAN_POINT('Ctrl Pts',(162.068156195932,0.364753412594142,125.897742670294));
#30067=CARTESIAN_POINT('Ctrl Pts',(162.060391442985,0.227927334181593,125.891394894825));
#30068=CARTESIAN_POINT('Ctrl Pts',(162.0526344021,0.0912371533594043,125.885053424055));
#30069=CARTESIAN_POINT('Ctrl Pts',(162.044877361215,-0.045860756782652,
125.884414211196));
#30070=CARTESIAN_POINT('Ctrl Pts',(162.03712032033,-0.182852771223678,125.889510881658));
#30071=CARTESIAN_POINT('Ctrl Pts',(162.02936912909,-0.319741478920505,125.894603708681));
#30072=CARTESIAN_POINT('Ctrl Pts',(162.02161793785,-0.456524060752298,125.905423794956));
#30073=CARTESIAN_POINT('Ctrl Pts',(162.01386674661,-0.592685517552422,125.921952713695));
#30074=CARTESIAN_POINT('Ctrl Pts',(162.006118849833,-0.728789102101644,
125.938474607203));
#30075=CARTESIAN_POINT('Ctrl Pts',(161.998370953056,-0.864271699381087,
125.960700460223));
#30076=CARTESIAN_POINT('Ctrl Pts',(161.990623056278,-0.998622283900166,
125.988559895298));
#30077=CARTESIAN_POINT('Ctrl Pts',(161.982876780194,-1.13294476517327,126.01641350278));
#30078=CARTESIAN_POINT('Ctrl Pts',(161.97513050411,-1.26613532210091,126.049898269033));
#30079=CARTESIAN_POINT('Ctrl Pts',(161.967384228026,-1.39769238478051,126.088892553839));
#30080=CARTESIAN_POINT('Ctrl Pts',(161.959637894761,-1.5292504185841,126.127887126492));
#30081=CARTESIAN_POINT('Ctrl Pts',(161.951891561495,-1.65917455923311,126.172391187746));
#30082=CARTESIAN_POINT('Ctrl Pts',(161.94414522823,-1.78697806698588,126.222233114908));
#30083=CARTESIAN_POINT('Ctrl Pts',(161.936397160227,-1.91481019544817,126.272086203825));
#30084=CARTESIAN_POINT('Ctrl Pts',(161.928649092224,-2.04052038183997,126.327279395291));
#30085=CARTESIAN_POINT('Ctrl Pts',(161.920901024221,-2.16364192013101,126.387592941544));
#30086=CARTESIAN_POINT('Ctrl Pts',(161.913144721479,-2.28689431345844,126.447970589752));
#30087=CARTESIAN_POINT('Ctrl Pts',(161.905388418737,-2.40755221111399,126.513479291409));
#30088=CARTESIAN_POINT('Ctrl Pts',(161.897632115996,-2.52517309476479,126.583853076526));
#30089=CARTESIAN_POINT('Ctrl Pts',(161.889871673481,-2.64285675622289,126.654264422251));
#30090=CARTESIAN_POINT('Ctrl Pts',(161.882111230967,-2.75749984715998,126.72954581097));
#30091=CARTESIAN_POINT('Ctrl Pts',(161.874350788453,-2.86868975702159,126.809388509971));
#30092=CARTESIAN_POINT('Ctrl Pts',(161.866577888188,-2.98005815879725,126.889359379561));
#30093=CARTESIAN_POINT('Ctrl Pts',(161.858804987922,-3.08796199418656,126.97390595029));
#30094=CARTESIAN_POINT('Ctrl Pts',(161.851032087657,-3.19202191534508,127.062679290347));
#30095=CARTESIAN_POINT('Ctrl Pts',(161.843541751895,-3.29229899625859,127.148225495887));
#30096=CARTESIAN_POINT('Ctrl Pts',(161.836051416133,-3.38900655673042,127.237696289461));
#30097=CARTESIAN_POINT('Ctrl Pts',(161.828561080371,-3.48183955840474,127.330749189667));
#30098=CARTESIAN_POINT('Ctrl Pts',(161.82089528468,-3.57684715843069,127.425981839313));
#30099=CARTESIAN_POINT('Ctrl Pts',(161.81322948899,-3.66811543703843,127.525286604809));
#30100=CARTESIAN_POINT('Ctrl Pts',(161.8055636933,-3.75526764309748,127.62833354098));
#30101=CARTESIAN_POINT('Ctrl Pts',(161.797906871543,-3.84231782477862,127.731259845672));
#30102=CARTESIAN_POINT('Ctrl Pts',(161.790250049785,-3.92526125595901,127.837919307829));
#30103=CARTESIAN_POINT('Ctrl Pts',(161.782593228028,-4.00375652939198,127.947943855983));
#30104=CARTESIAN_POINT('Ctrl Pts',(161.774943600683,-4.08217804801826,128.057865024164));
#30105=CARTESIAN_POINT('Ctrl Pts',(161.767293973339,-4.15615948783112,128.171144665205));
#30106=CARTESIAN_POINT('Ctrl Pts',(161.759644345994,-4.22539877314241,128.287380627493));
#30107=CARTESIAN_POINT('Ctrl Pts',(161.752000464105,-4.29458605445738,128.403529287689));
#30108=CARTESIAN_POINT('Ctrl Pts',(161.744356582215,-4.35903806333865,128.522629506138));
#30109=CARTESIAN_POINT('Ctrl Pts',(161.736712700326,-4.41849559837807,128.644249576528));
#30110=CARTESIAN_POINT('Ctrl Pts',(161.729072152544,-4.47792719923437,128.765816598685));
#30111=CARTESIAN_POINT('Ctrl Pts',(161.721431604762,-4.53236848364606,128.889900925101));
#30112=CARTESIAN_POINT('Ctrl Pts',(161.713791056981,-4.58160604699629,129.016046022024));
#30113=CARTESIAN_POINT('Ctrl Pts',(161.706151217946,-4.63083904300368,129.142179417559));
#30114=CARTESIAN_POINT('Ctrl Pts',(161.698511378912,-4.67486912729776,129.270372830139));
#30115=CARTESIAN_POINT('Ctrl Pts',(161.690871539878,-4.71353107987097,129.400149870708));
#30116=CARTESIAN_POINT('Ctrl Pts',(161.687312727445,-4.73154070505558,129.460602995878));
#30117=CARTESIAN_POINT('Ctrl Pts',(161.683753915013,-4.7483861898325,129.521399505681));
#30118=CARTESIAN_POINT('Ctrl Pts',(161.680195102581,-4.76405452823405,129.582490119308));
#30119=CARTESIAN_POINT('Origin',(213.235140564004,0.,130.804360617566));
#30120=CARTESIAN_POINT('',(159.584608960876,-4.76405452823403,129.582490119308));
#30121=CARTESIAN_POINT('',(159.930232377634,-4.76405452823406,129.582490119308));
#30122=CARTESIAN_POINT('',(213.235140564004,-4.76405452823405,129.582490119308));
#30123=CARTESIAN_POINT('',(161.264859435953,-4.91824926289724,130.801667940323));
#30124=CARTESIAN_POINT('Ctrl Pts',(161.264859435953,-4.91824926289724,130.801667940323));
#30125=CARTESIAN_POINT('Ctrl Pts',(161.257183648469,-4.91832310684931,130.936545955766));
#30126=CARTESIAN_POINT('Ctrl Pts',(161.249507860985,-4.91284442854529,131.071648809145));
#30127=CARTESIAN_POINT('Ctrl Pts',(161.241832073501,-4.90178411382868,131.206474486908));
#30128=CARTESIAN_POINT('Ctrl Pts',(161.234164972532,-4.8907363158205,131.341147585495));
#30129=CARTESIAN_POINT('Ctrl Pts',(161.226497871563,-4.87411947684391,131.475543735888));
#30130=CARTESIAN_POINT('Ctrl Pts',(161.218830770594,-4.85195648200004,131.609159573379));
#30131=CARTESIAN_POINT('Ctrl Pts',(161.211170404233,-4.8298129546289,131.742658045745));
#30132=CARTESIAN_POINT('Ctrl Pts',(161.203510037872,-4.80213302772327,131.875377174943));
#30133=CARTESIAN_POINT('Ctrl Pts',(161.195849671511,-4.76899146737869,132.006817871097));
#30134=CARTESIAN_POINT('Ctrl Pts',(161.188193700248,-4.73586892184574,132.13818315378));
#30135=CARTESIAN_POINT('Ctrl Pts',(161.180537728986,-4.69729107296994,132.268271074224));
#30136=CARTESIAN_POINT('Ctrl Pts',(161.172881757723,-4.65338385067269,132.396592322061));
#30137=CARTESIAN_POINT('Ctrl Pts',(161.165228052397,-4.6094896235862,132.524875590687));
#30138=CARTESIAN_POINT('Ctrl Pts',(161.157574347071,-4.5602692887005,132.651392846883));
#30139=CARTESIAN_POINT('Ctrl Pts',(161.149920641744,-4.50589862262322,132.775669995909));
#30140=CARTESIAN_POINT('Ctrl Pts',(161.142267448267,-4.4515315926375,132.899938833779));
#30141=CARTESIAN_POINT('Ctrl Pts',(161.13461425479,-4.39201507725591,133.02196749469));
#30142=CARTESIAN_POINT('Ctrl Pts',(161.126961061312,-4.32757276525213,133.141302427699));
#30143=CARTESIAN_POINT('Ctrl Pts',(161.119306626236,-4.26311999859303,133.260656720745));
#30144=CARTESIAN_POINT('Ctrl Pts',(161.11165219116,-4.1937400371374,133.377316063854));
#30145=CARTESIAN_POINT('Ctrl Pts',(161.103997756084,-4.11970196404595,133.490852528951));
#30146=CARTESIAN_POINT('Ctrl Pts',(161.096335620217,-4.04558940450076,133.604503218099));
#30147=CARTESIAN_POINT('Ctrl Pts',(161.088673484349,-3.96680959271754,133.715024417255));
#30148=CARTESIAN_POINT('Ctrl Pts',(161.081011348482,-3.88367452400827,133.822017863522));
#30149=CARTESIAN_POINT('Ctrl Pts',(161.07334537205,-3.8004977847159,133.929064939134));
#30150=CARTESIAN_POINT('Ctrl Pts',(161.065679395617,-3.71296170020457,134.032580434307));
#30151=CARTESIAN_POINT('Ctrl Pts',(161.058013419185,-3.62141697560164,134.132201081189));
#30152=CARTESIAN_POINT('Ctrl Pts',(161.05033524256,-3.52972656007069,134.231980271608));
#30153=CARTESIAN_POINT('Ctrl Pts',(161.042657065935,-3.43401504249612,134.327851946002));
#30154=CARTESIAN_POINT('Ctrl Pts',(161.034978889311,-3.33466875951926,134.419490950872));
#30155=CARTESIAN_POINT('Ctrl Pts',(161.027588327904,-3.23904386825342,134.507697269354));
#30156=CARTESIAN_POINT('Ctrl Pts',(161.020197766498,-3.14005188541437,134.591982143659));
#30157=CARTESIAN_POINT('Ctrl Pts',(161.012807205091,-3.03806278193107,134.672093492978));
#30158=CARTESIAN_POINT('Ctrl Pts',(161.005032870972,-2.93077764845143,134.756364817182));
#30159=CARTESIAN_POINT('Ctrl Pts',(160.997258536853,-2.81981358471956,134.836302344118));
#30160=CARTESIAN_POINT('Ctrl Pts',(160.989484202734,-2.70555596633218,134.911567694832));
#30161=CARTESIAN_POINT('Ctrl Pts',(160.981719449787,-2.59143916024824,134.986740287728));
#30162=CARTESIAN_POINT('Ctrl Pts',(160.97395469684,-2.47403719909126,135.057251948179));
#30163=CARTESIAN_POINT('Ctrl Pts',(160.966189943893,-2.35376855482247,135.122804394302));
#30164=CARTESIAN_POINT('Ctrl Pts',(160.958432903008,-2.23361936306604,135.188291732812));
#30165=CARTESIAN_POINT('Ctrl Pts',(160.950675862123,-2.11060949537768,135.248829473188));
#30166=CARTESIAN_POINT('Ctrl Pts',(160.942918821238,-1.98518613774831,135.304162731103));
#30167=CARTESIAN_POINT('Ctrl Pts',(160.935167629998,-1.85985736284844,135.359454261778));
#30168=CARTESIAN_POINT('Ctrl Pts',(160.927416438757,-1.73211907692423,135.409548964781));
#30169=CARTESIAN_POINT('Ctrl Pts',(160.919665247517,-1.60244246792842,135.454238164285));
#30170=CARTESIAN_POINT('Ctrl Pts',(160.91191735074,-1.47282097495116,135.498908369686));
#30171=CARTESIAN_POINT('Ctrl Pts',(160.904169453963,-1.34126316631299,135.538177513991));
#30172=CARTESIAN_POINT('Ctrl Pts',(160.896421557186,-1.20825937833372,135.571885377561));
#30173=CARTESIAN_POINT('Ctrl Pts',(160.888675281102,-1.07528341187967,135.605586190174));
#30174=CARTESIAN_POINT('Ctrl Pts',(160.880929005018,-0.940862446452899,
135.633727939933));
#30175=CARTESIAN_POINT('Ctrl Pts',(160.873182728934,-0.8055007360917,135.656200642408));
#30176=CARTESIAN_POINT('Ctrl Pts',(160.865436395668,-0.670138026521058,
135.678673510771));
#30177=CARTESIAN_POINT('Ctrl Pts',(160.857690062403,-0.533834943845108,
135.695477184315));
#30178=CARTESIAN_POINT('Ctrl Pts',(160.849943729138,-0.397104266609258,
135.706553113168));
#30179=CARTESIAN_POINT('Ctrl Pts',(160.842195661135,-0.260342969486592,
135.717631522399));
#30180=CARTESIAN_POINT('Ctrl Pts',(160.834447593132,-0.123154276873177,
135.722979602976));
#30181=CARTESIAN_POINT('Ctrl Pts',(160.826699525129,0.0139460000053123,
135.722590845156));
#30182=CARTESIAN_POINT('Ctrl Pts',(160.818943222387,0.151191988689769,135.72220167416));
#30183=CARTESIAN_POINT('Ctrl Pts',(160.811186919645,0.288348982338473,135.716063486102));
#30184=CARTESIAN_POINT('Ctrl Pts',(160.803430616903,0.424902704895101,135.704221917019));
#30185=CARTESIAN_POINT('Ctrl Pts',(160.795670174389,0.561529310285058,135.692374027733));
#30186=CARTESIAN_POINT('Ctrl Pts',(160.787909731875,0.697551615443923,135.674816741886));
#30187=CARTESIAN_POINT('Ctrl Pts',(160.780149289361,0.832463536533581,135.651647232038));
#30188=CARTESIAN_POINT('Ctrl Pts',(160.772376389095,0.96759203021589,135.628440528436));
#30189=CARTESIAN_POINT('Ctrl Pts',(160.76460348883,1.10160619541511,135.599603679791));
#30190=CARTESIAN_POINT('Ctrl Pts',(160.756830588564,1.23401227879488,135.565284557127));
#30191=CARTESIAN_POINT('Ctrl Pts',(160.749340252802,1.36160506753294,135.532213021016));
#30192=CARTESIAN_POINT('Ctrl Pts',(160.74184991704,1.48770436546009,135.494050968957));
#30193=CARTESIAN_POINT('Ctrl Pts',(160.734359581278,1.61188606552938,135.450972972202));
#30194=CARTESIAN_POINT('Ctrl Pts',(160.726585247159,1.74077615250114,135.406261660106));
#30195=CARTESIAN_POINT('Ctrl Pts',(160.71881091304,1.86800864475521,135.356112636514));
#30196=CARTESIAN_POINT('Ctrl Pts',(160.711036578921,1.99309054957259,135.30066722674));
#30197=CARTESIAN_POINT('Ctrl Pts',(160.703271825974,2.11801830212123,135.245290148479));
#30198=CARTESIAN_POINT('Ctrl Pts',(160.695507073027,2.24080038676023,135.184629828377));
#30199=CARTESIAN_POINT('Ctrl Pts',(160.68774232008,2.3609596561781,135.118877110106));
#30200=CARTESIAN_POINT('Ctrl Pts',(160.679985279195,2.48099958171563,135.053189698361));
#30201=CARTESIAN_POINT('Ctrl Pts',(160.67222823831,2.59842153538011,134.982420140244));
#30202=CARTESIAN_POINT('Ctrl Pts',(160.664471197425,2.71276936081772,134.90680689479));
#30203=CARTESIAN_POINT('Ctrl Pts',(160.656720006185,2.82703095567067,134.831250669872));
#30204=CARTESIAN_POINT('Ctrl Pts',(160.648968814945,2.93822271178586,134.750858242793));
#30205=CARTESIAN_POINT('Ctrl Pts',(160.641217623704,3.04591437568117,134.665913242938));
#30206=CARTESIAN_POINT('Ctrl Pts',(160.633469726927,3.15356026774636,134.581004346975));
#30207=CARTESIAN_POINT('Ctrl Pts',(160.62572183015,3.25770872005666,134.491546968356));
#30208=CARTESIAN_POINT('Ctrl Pts',(160.617973933373,3.35795989653583,134.397867038286));
#30209=CARTESIAN_POINT('Ctrl Pts',(160.610227657289,3.45819010263007,134.304206704038));
#30210=CARTESIAN_POINT('Ctrl Pts',(160.602481381205,3.55452436894585,134.206325841971));
#30211=CARTESIAN_POINT('Ctrl Pts',(160.594735105121,3.64659760084184,134.104589246015));
#30212=CARTESIAN_POINT('Ctrl Pts',(160.586988771856,3.73867151240152,134.002851899063));
#30213=CARTESIAN_POINT('Ctrl Pts',(160.57924243859,3.82648406443302,133.897259051307));
#30214=CARTESIAN_POINT('Ctrl Pts',(160.571496105325,3.90970882794232,133.788210470224));
#30215=CARTESIAN_POINT('Ctrl Pts',(160.563748037322,3.99295222906044,133.679137468468));
#30216=CARTESIAN_POINT('Ctrl Pts',(160.555999969319,4.07160556009345,133.566607504173));
#30217=CARTESIAN_POINT('Ctrl Pts',(160.548251901316,4.14538453564261,133.451051025255));
#30218=CARTESIAN_POINT('Ctrl Pts',(160.540495598574,4.21924192436505,133.335371731537));
#30219=CARTESIAN_POINT('Ctrl Pts',(160.532739295832,4.2882143982227,133.216659827713));
#30220=CARTESIAN_POINT('Ctrl Pts',(160.52498299309,4.35206237333402,133.095372656188));
#30221=CARTESIAN_POINT('Ctrl Pts',(160.517222550576,4.41594442603208,132.974020750047));
#30222=CARTESIAN_POINT('Ctrl Pts',(160.509462108062,4.47469636266918,132.850091190504));
#30223=CARTESIAN_POINT('Ctrl Pts',(160.501701665548,4.5281263865952,132.724062284367));
#30224=CARTESIAN_POINT('Ctrl Pts',(160.493928765283,4.5816421811389,132.597831065442));
#30225=CARTESIAN_POINT('Ctrl Pts',(160.486155865017,4.62981885344024,132.46949413171));
#30226=CARTESIAN_POINT('Ctrl Pts',(160.478382964752,4.67251392583976,132.339546819736));
#30227=CARTESIAN_POINT('Ctrl Pts',(160.47089262899,4.71365692481503,132.21432341987));
#30228=CARTESIAN_POINT('Ctrl Pts',(160.463402293228,4.7497098602883,132.087604987909));
#30229=CARTESIAN_POINT('Ctrl Pts',(160.455911957466,4.78059036377997,131.959842697148));
#30230=CARTESIAN_POINT('Ctrl Pts',(160.448137623347,4.81264171094755,131.827236260299));
#30231=CARTESIAN_POINT('Ctrl Pts',(160.440363289227,4.83922218699506,131.693085188945));
#30232=CARTESIAN_POINT('Ctrl Pts',(160.432588955108,4.86018421830598,131.557880641606));
#30233=CARTESIAN_POINT('Ctrl Pts',(160.424824202161,4.88112041578672,131.422842721789));
#30234=CARTESIAN_POINT('Ctrl Pts',(160.417059449214,4.89645188636241,131.286754291887));
#30235=CARTESIAN_POINT('Ctrl Pts',(160.409294696267,4.90608128244058,131.150119945114));
#30236=CARTESIAN_POINT('Ctrl Pts',(160.401537655382,4.91570111446682,131.013621305499));
#30237=CARTESIAN_POINT('Ctrl Pts',(160.393780614497,4.91963011507136,130.876578215514));
#30238=CARTESIAN_POINT('Ctrl Pts',(160.386023573612,4.91782234294213,130.739503345351));
#30239=CARTESIAN_POINT('Ctrl Pts',(160.378272382372,4.91601593406792,130.602531844412));
#30240=CARTESIAN_POINT('Ctrl Pts',(160.370521191132,4.90848136852386,130.465529000347));
#30241=CARTESIAN_POINT('Ctrl Pts',(160.362769999891,4.89522470922947,130.329010106207));
#30242=CARTESIAN_POINT('Ctrl Pts',(160.355022103114,4.88197368436897,130.192549236239));
#30243=CARTESIAN_POINT('Ctrl Pts',(160.347274206337,4.86300544061307,130.056572295411));
#30244=CARTESIAN_POINT('Ctrl Pts',(160.33952630956,4.8383780719501,129.921591850916));
#30245=CARTESIAN_POINT('Ctrl Pts',(160.331780033476,4.81375585480178,129.78663964142));
#30246=CARTESIAN_POINT('Ctrl Pts',(160.324033757392,4.78347693745298,129.65268389802));
#30247=CARTESIAN_POINT('Ctrl Pts',(160.316287481308,4.74765088879886,129.520228965208));
#30248=CARTESIAN_POINT('Ctrl Pts',(160.308541148043,4.71182457568494,129.387773054644));
#30249=CARTESIAN_POINT('Ctrl Pts',(160.300794814777,4.67045115163675,129.256818354178));
#30250=CARTESIAN_POINT('Ctrl Pts',(160.293048481512,4.62369050951024,129.127855581855));
#30251=CARTESIAN_POINT('Ctrl Pts',(160.285300413509,4.5769193956623,128.998863929213));
#30252=CARTESIAN_POINT('Ctrl Pts',(160.277552345506,4.52475879632425,128.871865459839));
#30253=CARTESIAN_POINT('Ctrl Pts',(160.269804277503,4.46741719631762,128.747332018702));
#30254=CARTESIAN_POINT('Ctrl Pts',(160.262047974761,4.41001465297591,128.622666221941));
#30255=CARTESIAN_POINT('Ctrl Pts',(160.254291672019,4.34742027305976,128.500471042566));
#30256=CARTESIAN_POINT('Ctrl Pts',(160.246535369277,4.27988933074522,128.381195254023));
#30257=CARTESIAN_POINT('Ctrl Pts',(160.238774926763,4.21232234513353,128.261855804401));
#30258=CARTESIAN_POINT('Ctrl Pts',(160.231014484249,4.13981375367094,128.145439182086));
#30259=CARTESIAN_POINT('Ctrl Pts',(160.223254041735,4.06266229864699,128.032365287546));
#30260=CARTESIAN_POINT('Ctrl Pts',(160.215481141469,3.98538699325826,127.919109876753));
#30261=CARTESIAN_POINT('Ctrl Pts',(160.207708241204,3.90345416437802,127.809208230425));
#30262=CARTESIAN_POINT('Ctrl Pts',(160.199935340938,3.81720354003233,127.703047960567));
#30263=CARTESIAN_POINT('Ctrl Pts',(160.192445005176,3.73408834313408,127.600746883919));
#30264=CARTESIAN_POINT('Ctrl Pts',(160.184954669414,3.64696402973765,127.501920120489));
#30265=CARTESIAN_POINT('Ctrl Pts',(160.177464333652,3.55616566253962,127.406880839396));
#30266=CARTESIAN_POINT('Ctrl Pts',(160.169689999533,3.46192464765145,127.308238115074));
#30267=CARTESIAN_POINT('Ctrl Pts',(160.161915665414,3.36342694853327,127.213363276888));
#30268=CARTESIAN_POINT('Ctrl Pts',(160.154141331295,3.26100602361524,127.122645965879));
#30269=CARTESIAN_POINT('Ctrl Pts',(160.146376578348,3.15871132333361,127.032040455849));
#30270=CARTESIAN_POINT('Ctrl Pts',(160.138611825401,3.05250330737112,126.945582534937));
#30271=CARTESIAN_POINT('Ctrl Pts',(160.130847072454,2.94275388553613,126.863626849388));
#30272=CARTESIAN_POINT('Ctrl Pts',(160.123090031569,2.83311346837376,126.78175256338));
#30273=CARTESIAN_POINT('Ctrl Pts',(160.115332990684,2.71993895630499,126.704371846295));
#30274=CARTESIAN_POINT('Ctrl Pts',(160.107575949799,2.60363684088095,126.631800460623));
#30275=CARTESIAN_POINT('Ctrl Pts',(160.099824758559,2.48742242978704,126.559283801597));
#30276=CARTESIAN_POINT('Ctrl Pts',(160.092073567319,2.36808544023483,126.491569461282));
#30277=CARTESIAN_POINT('Ctrl Pts',(160.084322376078,2.24606268001862,126.428930867253));
#30278=CARTESIAN_POINT('Ctrl Pts',(160.076574479301,2.12409178273078,126.366318896297));
#30279=CARTESIAN_POINT('Ctrl Pts',(160.068826582524,1.99943773227024,126.308778559038));
#30280=CARTESIAN_POINT('Ctrl Pts',(160.061078685747,1.8725631671527,126.256538034447));
#30281=CARTESIAN_POINT('Ctrl Pts',(160.053332409663,1.74571514145887,126.204308437448));
#30282=CARTESIAN_POINT('Ctrl Pts',(160.045586133579,1.61664788628163,126.157376596798));
#30283=CARTESIAN_POINT('Ctrl Pts',(160.037839857495,1.48584494559068,126.115922939601));
#30284=CARTESIAN_POINT('Ctrl Pts',(160.03009352423,1.35504103934232,126.074468976402));
#30285=CARTESIAN_POINT('Ctrl Pts',(160.022347190964,1.22250179471075,126.038493395462));
#30286=CARTESIAN_POINT('Ctrl Pts',(160.014600857699,1.0887264926785,126.008126919482));
#30287=CARTESIAN_POINT('Ctrl Pts',(160.006852789696,0.954921232594703,125.97775364314));
#30288=CARTESIAN_POINT('Ctrl Pts',(159.999104721693,0.819879745490189,125.95299205782));
#30289=CARTESIAN_POINT('Ctrl Pts',(159.99135665369,0.684111699040778,125.933921803071));
#30290=CARTESIAN_POINT('Ctrl Pts',(159.983600350948,0.548199356696079,125.914831280229));
#30291=CARTESIAN_POINT('Ctrl Pts',(159.975844048206,0.41155930024387,125.901444225582));
#30292=CARTESIAN_POINT('Ctrl Pts',(159.968087745465,0.274707077420868,125.893788442746));
#30293=CARTESIAN_POINT('Ctrl Pts',(159.96032730295,0.137781812445819,125.886128573788));
#30294=CARTESIAN_POINT('Ctrl Pts',(159.952566860436,0.000644546196039986,
125.884206077341));
#30295=CARTESIAN_POINT('Ctrl Pts',(159.944806417922,-0.136189969668989,
125.887996579513));
#30296=CARTESIAN_POINT('Ctrl Pts',(159.937033517657,-0.273244144446389,
125.891793166536));
#30297=CARTESIAN_POINT('Ctrl Pts',(159.929260617391,-0.409994207408434,
125.901321051594));
#30298=CARTESIAN_POINT('Ctrl Pts',(159.921487717126,-0.545930418302852,
125.916503925633));
#30299=CARTESIAN_POINT('Ctrl Pts',(159.913997381364,-0.676925005528741,
125.931134863958));
#30300=CARTESIAN_POINT('Ctrl Pts',(159.906507045602,-0.807163580043379,
125.951016736695));
#30301=CARTESIAN_POINT('Ctrl Pts',(159.89901670984,-0.936201554223454,125.976036921668));
#30302=CARTESIAN_POINT('Ctrl Pts',(159.891242375721,-1.07013204241472,126.002005754559));
#30303=CARTESIAN_POINT('Ctrl Pts',(159.883468041602,-1.20319334308913,126.033592490941));
#30304=CARTESIAN_POINT('Ctrl Pts',(159.875693707483,-1.33487739777685,126.070727193292));
#30305=CARTESIAN_POINT('Ctrl Pts',(159.867928954535,-1.46639916363593,126.107816130441));
#30306=CARTESIAN_POINT('Ctrl Pts',(159.860164201588,-1.59654668801709,126.150439324133));
#30307=CARTESIAN_POINT('Ctrl Pts',(159.852399448641,-1.72482057065621,126.198475571069));
#30308=CARTESIAN_POINT('Ctrl Pts',(159.844642407756,-1.8529670498674,126.246464107728));
#30309=CARTESIAN_POINT('Ctrl Pts',(159.836885366871,-1.97924322690081,126.299854862287));
#30310=CARTESIAN_POINT('Ctrl Pts',(159.829128325986,-2.1031637232194,126.35847651923));
#30311=CARTESIAN_POINT('Ctrl Pts',(159.821377134746,-2.2269907701264,126.417053969125));
#30312=CARTESIAN_POINT('Ctrl Pts',(159.813625943506,-2.34846532022352,126.480854303279));
#30313=CARTESIAN_POINT('Ctrl Pts',(159.805874752266,-2.46712122586535,126.549657817207));
#30314=CARTESIAN_POINT('Ctrl Pts',(159.798126855489,-2.58572669958301,126.618432087806));
#30315=CARTESIAN_POINT('Ctrl Pts',(159.790378958712,-2.70151557406425,126.692205113056));
#30316=CARTESIAN_POINT('Ctrl Pts',(159.782631061935,-2.81404580846085,126.770710998377));
#30317=CARTESIAN_POINT('Ctrl Pts',(159.774884785851,-2.9265525039582,126.849200461959));
#30318=CARTESIAN_POINT('Ctrl Pts',(159.767138509766,-3.03580159474203,126.932420592869));
#30319=CARTESIAN_POINT('Ctrl Pts',(159.759392233682,-3.14137991505379,127.020062097127));
#30320=CARTESIAN_POINT('Ctrl Pts',(159.751645900417,-3.24695901472074,127.107704248335));
#30321=CARTESIAN_POINT('Ctrl Pts',(159.743899567152,-3.34886698902163,127.199767588299));
#30322=CARTESIAN_POINT('Ctrl Pts',(159.736153233886,-3.44672398367913,127.295902716603));
#30323=CARTESIAN_POINT('Ctrl Pts',(159.728405165883,-3.54460289273218,127.392059373702));
#30324=CARTESIAN_POINT('Ctrl Pts',(159.72065709788,-3.63842873809756,127.492289359676));
#30325=CARTESIAN_POINT('Ctrl Pts',(159.712909029877,-3.72785902894052,127.596206923797));
#30326=CARTESIAN_POINT('Ctrl Pts',(159.705152727135,-3.81738436736076,127.70023493274));
#30327=CARTESIAN_POINT('Ctrl Pts',(159.697396424394,-3.90250456370759,127.807958052048));
#30328=CARTESIAN_POINT('Ctrl Pts',(159.689640121652,-3.98291755986778,127.91895756534));
#30329=CARTESIAN_POINT('Ctrl Pts',(159.681879679138,-4.06337347486506,128.030016322414));
#30330=CARTESIAN_POINT('Ctrl Pts',(159.674119236623,-4.13911696774629,128.144354632149));
#30331=CARTESIAN_POINT('Ctrl Pts',(159.666358794109,-4.20989030911008,128.261526244713));
#30332=CARTESIAN_POINT('Ctrl Pts',(159.658585893844,-4.28077726212446,128.378885951552));
#30333=CARTESIAN_POINT('Ctrl Pts',(159.650812993578,-4.34667793191823,128.499087707091));
#30334=CARTESIAN_POINT('Ctrl Pts',(159.643040093313,-4.40738099240258,128.62166140551));
#30335=CARTESIAN_POINT('Ctrl Pts',(159.635549757551,-4.46587734373642,128.739779241248));
#30336=CARTESIAN_POINT('Ctrl Pts',(159.628059421789,-4.51954729189796,128.860099280391));
#30337=CARTESIAN_POINT('Ctrl Pts',(159.620569086027,-4.56824527864363,128.982186603743));
#30338=CARTESIAN_POINT('Ctrl Pts',(159.611787365971,-4.62533912603141,129.125322603264));
#30339=CARTESIAN_POINT('Ctrl Pts',(159.603005645915,-4.67575140335755,129.271268173422));
#30340=CARTESIAN_POINT('Ctrl Pts',(159.59422392586,-4.71923020496151,129.419424035957));
#30341=CARTESIAN_POINT('Ctrl Pts',(159.591018937532,-4.73509828669941,129.473495198223));
#30342=CARTESIAN_POINT('Ctrl Pts',(159.587813949204,-4.75004329422944,129.527860530574));
#30343=CARTESIAN_POINT('Ctrl Pts',(159.584608960876,-4.76405452823403,129.582490119308));
#30344=CARTESIAN_POINT('Ctrl Pts',(161.334944359449,-4.76405452823403,129.582490119308));
#30345=CARTESIAN_POINT('Ctrl Pts',(161.327171216939,-4.79811130280615,129.715276966481));
#30346=CARTESIAN_POINT('Ctrl Pts',(161.319398074429,-4.82657531939697,129.849344857447));
#30347=CARTESIAN_POINT('Ctrl Pts',(161.311624931919,-4.84938052155759,129.984182819989));
#30348=CARTESIAN_POINT('Ctrl Pts',(161.304834897581,-4.86930143585433,130.101967151689));
#30349=CARTESIAN_POINT('Ctrl Pts',(161.298044863242,-4.8849052060667,130.220338818543));
#30350=CARTESIAN_POINT('Ctrl Pts',(161.291254828904,-4.89618035041408,130.338956450504));
#30351=CARTESIAN_POINT('Ctrl Pts',(161.2824563646,-4.91079057918865,130.492660091562));
#30352=CARTESIAN_POINT('Ctrl Pts',(161.273657900295,-4.91816461835232,130.647062382023));
#30353=CARTESIAN_POINT('Ctrl Pts',(161.264859435991,-4.91824926289688,130.801667939662));
#30354=CARTESIAN_POINT('',(161.610140564037,-4.91824795040022,130.808850704879));
#30355=CARTESIAN_POINT('Ctrl Pts',(161.680195102581,-4.76405452823405,129.582490119308));
#30356=CARTESIAN_POINT('Ctrl Pts',(161.672552391556,-4.79770299521974,129.713684981399));
#30357=CARTESIAN_POINT('Ctrl Pts',(161.664909680531,-4.82591915561794,129.846236774025));
#30358=CARTESIAN_POINT('Ctrl Pts',(161.657266969507,-4.84861163807389,129.979649610222));
#30359=CARTESIAN_POINT('Ctrl Pts',(161.649412568595,-4.87193266307583,130.116757751412));
#30360=CARTESIAN_POINT('Ctrl Pts',(161.641558167684,-4.88941948444408,130.254774881735));
#30361=CARTESIAN_POINT('Ctrl Pts',(161.633703766772,-4.90102992760437,130.393156639927));
#30362=CARTESIAN_POINT('Ctrl Pts',(161.62584936586,-4.91264037076467,130.531538398119));
#30363=CARTESIAN_POINT('Ctrl Pts',(161.617994964949,-4.9183744538122,130.670284324455));
#30364=CARTESIAN_POINT('Ctrl Pts',(161.610140564037,-4.91824795040022,130.808850704879));
#30365=CARTESIAN_POINT('Ctrl Pts',(161.610140564008,-4.91824795039975,130.808850705393));
#30366=CARTESIAN_POINT('Ctrl Pts',(161.599381903105,-4.91807467079718,130.998653685444));
#30367=CARTESIAN_POINT('Ctrl Pts',(161.588623242203,-4.90691076602029,131.187975563161));
#30368=CARTESIAN_POINT('Ctrl Pts',(161.5778645813,-4.88494323448938,131.375773479091));
#30369=CARTESIAN_POINT('Ctrl Pts',(161.568614206386,-4.86605539106516,131.537243493439));
#30370=CARTESIAN_POINT('Ctrl Pts',(161.559363831472,-4.8391815661298,131.697587784437));
#30371=CARTESIAN_POINT('Ctrl Pts',(161.550113456558,-4.80446700205628,131.856159024416));
#30372=CARTESIAN_POINT('Ctrl Pts',(161.542339122439,-4.77529168511808,131.98942776355));
#30373=CARTESIAN_POINT('Ctrl Pts',(161.53456478832,-4.74052094061047,132.121692751278));
#30374=CARTESIAN_POINT('Ctrl Pts',(161.526790454201,-4.7002368779166,132.252447753747));
#30375=CARTESIAN_POINT('Ctrl Pts',(161.519025701254,-4.6600024617297,132.383041612361));
#30376=CARTESIAN_POINT('Ctrl Pts',(161.511260948307,-4.61426836073582,132.512128818347));
#30377=CARTESIAN_POINT('Ctrl Pts',(161.503496195359,-4.56316772755854,132.639213023802));
#30378=CARTESIAN_POINT('Ctrl Pts',(161.495739154474,-4.51211784825061,132.766171007431));
#30379=CARTESIAN_POINT('Ctrl Pts',(161.487982113589,-4.45571218884313,132.89112958915));
#30380=CARTESIAN_POINT('Ctrl Pts',(161.480225072704,-4.39413366326438,133.013607641298));
#30381=CARTESIAN_POINT('Ctrl Pts',(161.472473881464,-4.33260157453067,133.135993331794));
#30382=CARTESIAN_POINT('Ctrl Pts',(161.464722690224,-4.26590455903632,133.25590186812));
#30383=CARTESIAN_POINT('Ctrl Pts',(161.456971498984,-4.19427344425517,133.372872509171));
#30384=CARTESIAN_POINT('Ctrl Pts',(161.449223602207,-4.12267277460866,133.489793434579));
#30385=CARTESIAN_POINT('Ctrl Pts',(161.44147570543,-4.04614238044535,133.603778615534));
#30386=CARTESIAN_POINT('Ctrl Pts',(161.433727808653,-3.96495868753456,133.71439251922));
#30387=CARTESIAN_POINT('Ctrl Pts',(161.425981532569,-3.88379197650217,133.824983284862));
#30388=CARTESIAN_POINT('Ctrl Pts',(161.418235256485,-3.79797413398804,133.932203860928));
#30389=CARTESIAN_POINT('Ctrl Pts',(161.4104889804,-3.70782427974217,134.035648622844));
#30390=CARTESIAN_POINT('Ctrl Pts',(161.402742647135,-3.61767376003062,134.139094148366));
#30391=CARTESIAN_POINT('Ctrl Pts',(161.39499631387,-3.52319142164166,134.238763509375));
#30392=CARTESIAN_POINT('Ctrl Pts',(161.387249980604,-3.42473567982982,134.33428534563));
#30393=CARTESIAN_POINT('Ctrl Pts',(161.379501912601,-3.32625788953721,134.429828573339));
#30394=CARTESIAN_POINT('Ctrl Pts',(161.371753844598,-3.2238052057403,134.52122215588));
#30395=CARTESIAN_POINT('Ctrl Pts',(161.364005776596,-3.11777148691773,134.608132958002));
#30396=CARTESIAN_POINT('Ctrl Pts',(161.356249473854,-3.01162507419694,134.695136129958));
#30397=CARTESIAN_POINT('Ctrl Pts',(161.348493171112,-2.90189032647662,134.777646755954));
#30398=CARTESIAN_POINT('Ctrl Pts',(161.34073686837,-2.78899308811763,134.855372912898));
#30399=CARTESIAN_POINT('Ctrl Pts',(161.332976425856,-2.67603559310322,134.933140554633));
#30400=CARTESIAN_POINT('Ctrl Pts',(161.325215983342,-2.55991257499477,135.006118431091));
#30401=CARTESIAN_POINT('Ctrl Pts',(161.317455540827,-2.44107633991098,135.074059595858));
#30402=CARTESIAN_POINT('Ctrl Pts',(161.309682640562,-2.32204933835285,135.142109825814));
#30403=CARTESIAN_POINT('Ctrl Pts',(161.301909740297,-2.20030076358336,135.205107007143));
#30404=CARTESIAN_POINT('Ctrl Pts',(161.294136840031,-2.07630565728573,135.262851155856));
#30405=CARTESIAN_POINT('Ctrl Pts',(161.286646504269,-1.95681808542466,135.318496159316));
#30406=CARTESIAN_POINT('Ctrl Pts',(161.279156168507,-1.83524476470625,135.369263302679));
#30407=CARTESIAN_POINT('Ctrl Pts',(161.271665832745,-1.71202398207716,135.41501750648));
#30408=CARTESIAN_POINT('Ctrl Pts',(161.263891498626,-1.58413124602475,135.462506494824));
#30409=CARTESIAN_POINT('Ctrl Pts',(161.256117164507,-1.45405852918058,135.50474533933));
#30410=CARTESIAN_POINT('Ctrl Pts',(161.248342830388,-1.32227612255046,135.541529489185));
#30411=CARTESIAN_POINT('Ctrl Pts',(161.24057807744,-1.19065612595883,135.578268305862));
#30412=CARTESIAN_POINT('Ctrl Pts',(161.232813324493,-1.05733100491809,135.609565699404));
#30413=CARTESIAN_POINT('Ctrl Pts',(161.225048571546,-0.922790323222832,
135.635265406719));
#30414=CARTESIAN_POINT('Ctrl Pts',(161.217291530661,-0.788383269229369,
135.660939588723));
#30415=CARTESIAN_POINT('Ctrl Pts',(161.209534489776,-0.652763438723616,
135.681027075674));
#30416=CARTESIAN_POINT('Ctrl Pts',(161.201777448891,-0.516434487478315,
135.695421696989));
#30417=CARTESIAN_POINT('Ctrl Pts',(161.194026257651,-0.380208342955726,
135.709805463207));
#30418=CARTESIAN_POINT('Ctrl Pts',(161.186275066411,-0.243274529318622,
135.718504867927));
#30419=CARTESIAN_POINT('Ctrl Pts',(161.178523875171,-0.106145448995003,
135.721465071018));
#30420=CARTESIAN_POINT('Ctrl Pts',(161.170775978394,0.0309253478116268,
135.724424015944));
#30421=CARTESIAN_POINT('Ctrl Pts',(161.163028081617,0.168190856181115,135.721648602429));
#30422=CARTESIAN_POINT('Ctrl Pts',(161.15528018484,0.305135235141163,135.713135979179));
#30423=CARTESIAN_POINT('Ctrl Pts',(161.147533908756,0.442050968289219,135.704625136585));
#30424=CARTESIAN_POINT('Ctrl Pts',(161.139787632671,0.578645315674485,135.690379495562));
#30425=CARTESIAN_POINT('Ctrl Pts',(161.132041356587,0.714404521834894,135.670448290603));
#30426=CARTESIAN_POINT('Ctrl Pts',(161.124295023322,0.850164730138877,135.650516938516));
#30427=CARTESIAN_POINT('Ctrl Pts',(161.116548690057,0.98508939809787,135.624899995535));
#30428=CARTESIAN_POINT('Ctrl Pts',(161.108802356791,1.11867235762289,135.593698277284));
#30429=CARTESIAN_POINT('Ctrl Pts',(161.101054288788,1.25228523212554,135.562489571624));
#30430=CARTESIAN_POINT('Ctrl Pts',(161.093306220785,1.38455541965632,135.52569369091));
#30431=CARTESIAN_POINT('Ctrl Pts',(161.085558152782,1.51498975396465,135.483461931695));
#30432=CARTESIAN_POINT('Ctrl Pts',(161.07780185004,1.64556271543567,135.441185288063));
#30433=CARTESIAN_POINT('Ctrl Pts',(161.070045547299,1.77429555347097,135.393461345741));
#30434=CARTESIAN_POINT('Ctrl Pts',(161.062289244557,1.90071248562887,135.340490588089));
#30435=CARTESIAN_POINT('Ctrl Pts',(161.054528802043,2.02719689030988,135.287491558348));
#30436=CARTESIAN_POINT('Ctrl Pts',(161.046768359528,2.15136257236546,135.229240299248));
#30437=CARTESIAN_POINT('Ctrl Pts',(161.039007917014,2.27275728627645,135.165983868166));
#30438=CARTESIAN_POINT('Ctrl Pts',(161.031235016749,2.39434687375913,135.102625892246));
#30439=CARTESIAN_POINT('Ctrl Pts',(161.023462116483,2.5131562651213,135.034246883493));
#30440=CARTESIAN_POINT('Ctrl Pts',(161.015689216218,2.6287604365361,134.9611384117));
#30441=CARTESIAN_POINT('Ctrl Pts',(161.008198880456,2.74016210512989,134.890687617006));
#30442=CARTESIAN_POINT('Ctrl Pts',(161.000708544694,2.84858729008048,134.815845420196));
#30443=CARTESIAN_POINT('Ctrl Pts',(160.993218208932,2.95368544040804,134.736907550741));
#30444=CARTESIAN_POINT('Ctrl Pts',(160.985443874813,3.06276841904973,134.654976727972));
#30445=CARTESIAN_POINT('Ctrl Pts',(160.977669540694,3.16861263585589,134.568373994637));
#30446=CARTESIAN_POINT('Ctrl Pts',(160.969895206575,3.27079179265738,134.477384455167));
#30447=CARTESIAN_POINT('Ctrl Pts',(160.962130453628,3.3728450227801,134.386507052172));
#30448=CARTESIAN_POINT('Ctrl Pts',(160.954365700681,3.47124189092529,134.291253857568));
#30449=CARTESIAN_POINT('Ctrl Pts',(160.946600947733,3.56558630733806,134.191952291222));
#30450=CARTESIAN_POINT('Ctrl Pts',(160.938843906848,3.65983701954643,134.092749352591));
#30451=CARTESIAN_POINT('Ctrl Pts',(160.931086865963,3.75004302231244,133.989506325595));
#30452=CARTESIAN_POINT('Ctrl Pts',(160.923329825078,3.8358427530691,133.882589562305));
#30453=CARTESIAN_POINT('Ctrl Pts',(160.915578633838,3.92157778158132,133.775753425777));
#30454=CARTESIAN_POINT('Ctrl Pts',(160.907827442598,4.00291290821725,133.665249370943));
#30455=CARTESIAN_POINT('Ctrl Pts',(160.900076251358,4.07952502839383,133.551478854047));
#30456=CARTESIAN_POINT('Ctrl Pts',(160.892328354581,4.15610458637569,133.437756692656));
#30457=CARTESIAN_POINT('Ctrl Pts',(160.884580457804,4.22796491255238,133.320771154106));
#30458=CARTESIAN_POINT('Ctrl Pts',(160.876832561027,4.29482478340195,133.200954688821));
#30459=CARTESIAN_POINT('Ctrl Pts',(160.869086284943,4.36167066860786,133.081163286558));
#30460=CARTESIAN_POINT('Ctrl Pts',(160.861340008859,4.42351798862189,132.958542476608));
#30461=CARTESIAN_POINT('Ctrl Pts',(160.853593732775,4.48013046844121,132.833551108438));
#30462=CARTESIAN_POINT('Ctrl Pts',(160.845847399509,4.53674336616095,132.70855881761));
#30463=CARTESIAN_POINT('Ctrl Pts',(160.838101066244,4.58812118527195,132.581196289781));
#30464=CARTESIAN_POINT('Ctrl Pts',(160.830354732979,4.63407514859685,132.451943871808));
#30465=CARTESIAN_POINT('Ctrl Pts',(160.822606664976,4.68003940299322,132.322662508651));
#30466=CARTESIAN_POINT('Ctrl Pts',(160.814858596973,4.72057725367482,132.19149078148));
#30467=CARTESIAN_POINT('Ctrl Pts',(160.80711052897,4.75554942231088,132.058925384511));
#30468=CARTESIAN_POINT('Ctrl Pts',(160.799354226228,4.79055875978396,131.926219095459));
#30469=CARTESIAN_POINT('Ctrl Pts',(160.791597923486,4.81999049892845,131.79211655637));
#30470=CARTESIAN_POINT('Ctrl Pts',(160.783841620744,4.84375614004254,131.657126422638));
#30471=CARTESIAN_POINT('Ctrl Pts',(160.77608117823,4.86753446559487,131.522064240608));
#30472=CARTESIAN_POINT('Ctrl Pts',(160.768320735716,4.88564061561917,131.38611390733));
#30473=CARTESIAN_POINT('Ctrl Pts',(160.760560293202,4.89803799673453,131.249789450316));
#30474=CARTESIAN_POINT('Ctrl Pts',(160.752787392936,4.91045527922664,131.113246153181));
#30475=CARTESIAN_POINT('Ctrl Pts',(160.745014492671,4.91714546068101,130.97632792289));
#30476=CARTESIAN_POINT('Ctrl Pts',(160.737241592405,4.91812411126045,130.839549944621));
#30477=CARTESIAN_POINT('Ctrl Pts',(160.729751256643,4.91906718542626,130.707744190383));
#30478=CARTESIAN_POINT('Ctrl Pts',(160.722260920881,4.91470678650708,130.576068976024));
#30479=CARTESIAN_POINT('Ctrl Pts',(160.714770585119,4.90510223871495,130.444979079012));
#30480=CARTESIAN_POINT('Ctrl Pts',(160.706996251,4.89513353157412,130.308918868712));
#30481=CARTESIAN_POINT('Ctrl Pts',(160.699221916881,4.87948358387501,130.173058238692));
#30482=CARTESIAN_POINT('Ctrl Pts',(160.691447582762,4.85816183747676,130.037909951584));
#30483=CARTESIAN_POINT('Ctrl Pts',(160.683682829815,4.83686636822538,129.902928222661));
#30484=CARTESIAN_POINT('Ctrl Pts',(160.675918076868,4.80991306860397,129.768657472374));
#30485=CARTESIAN_POINT('Ctrl Pts',(160.668153323921,4.77736331003202,129.635607920688));
#30486=CARTESIAN_POINT('Ctrl Pts',(160.660396283036,4.74484588033915,129.502690515692));
#30487=CARTESIAN_POINT('Ctrl Pts',(160.652639242151,4.70674314563176,129.370992272855));
#30488=CARTESIAN_POINT('Ctrl Pts',(160.644882201266,4.66316789488435,129.241015407249));
#30489=CARTESIAN_POINT('Ctrl Pts',(160.637131010026,4.61962550457248,129.111136558209));
#30490=CARTESIAN_POINT('Ctrl Pts',(160.629379818786,4.57061893627067,128.98297687179));
#30491=CARTESIAN_POINT('Ctrl Pts',(160.621628627545,4.51631130056807,128.857025181936));
#30492=CARTESIAN_POINT('Ctrl Pts',(160.613880730768,4.46202674705934,128.73112702491));
#30493=CARTESIAN_POINT('Ctrl Pts',(160.606132833991,4.40244576185906,128.60743535619));
#30494=CARTESIAN_POINT('Ctrl Pts',(160.598384937214,4.33778016957377,128.486420527108));
#30495=CARTESIAN_POINT('Ctrl Pts',(160.59063866113,4.27312810393636,128.36543101172));
#30496=CARTESIAN_POINT('Ctrl Pts',(160.582892385046,4.20339373089582,128.247117566827));
#30497=CARTESIAN_POINT('Ctrl Pts',(160.575146108962,4.12883538109347,128.131926996626));
#30498=CARTESIAN_POINT('Ctrl Pts',(160.567399775697,4.05427648091835,128.016735576115));
#30499=CARTESIAN_POINT('Ctrl Pts',(160.559653442431,3.97489374536435,127.904667404507));
#30500=CARTESIAN_POINT('Ctrl Pts',(160.551907109166,3.89098926516945,127.796140944597));
#30501=CARTESIAN_POINT('Ctrl Pts',(160.544159041163,3.80706599514796,127.687590180939));
#30502=CARTESIAN_POINT('Ctrl Pts',(160.53641097316,3.7186192045881,127.582583016486));
#30503=CARTESIAN_POINT('Ctrl Pts',(160.528662905157,3.62599149306077,127.481505105397));
#30504=CARTESIAN_POINT('Ctrl Pts',(160.520906602415,3.53326533569931,127.380319767502));
#30505=CARTESIAN_POINT('Ctrl Pts',(160.513150299673,3.43634964549955,127.283072313795));
#30506=CARTESIAN_POINT('Ctrl Pts',(160.505393996932,3.33562453240203,127.190112142248));
#30507=CARTESIAN_POINT('Ctrl Pts',(160.497633554417,3.23484565927881,127.097102355059));
#30508=CARTESIAN_POINT('Ctrl Pts',(160.489873111903,3.13025360993405,127.008384662343));
#30509=CARTESIAN_POINT('Ctrl Pts',(160.482112669389,3.02226107065443,126.924267695572));
#30510=CARTESIAN_POINT('Ctrl Pts',(160.474339769124,2.91409517216366,126.840015696779));
#30511=CARTESIAN_POINT('Ctrl Pts',(160.466566868858,2.80251819378715,126.76037940976));
#30512=CARTESIAN_POINT('Ctrl Pts',(160.458793968593,2.68797199145841,126.685624205068));
#30513=CARTESIAN_POINT('Ctrl Pts',(160.451303632831,2.57758983210879,126.613586540364));
#30514=CARTESIAN_POINT('Ctrl Pts',(160.443813297069,2.46445084290856,126.546081397761));
#30515=CARTESIAN_POINT('Ctrl Pts',(160.436322961307,2.34896970720894,126.48330468445));
#30516=CARTESIAN_POINT('Ctrl Pts',(160.428548627188,2.22911006914954,126.418147772974));
#30517=CARTESIAN_POINT('Ctrl Pts',(160.420774293068,2.10634749433814,126.357878528096));
#30518=CARTESIAN_POINT('Ctrl Pts',(160.412999958949,1.98111848805488,126.302766166842));
#30519=CARTESIAN_POINT('Ctrl Pts',(160.405235206002,1.85604381532991,126.247721726648));
#30520=CARTESIAN_POINT('Ctrl Pts',(160.397470453055,1.72850911355208,126.197821680701));
#30521=CARTESIAN_POINT('Ctrl Pts',(160.389705700108,1.59897681797892,126.153290181842));
#30522=CARTESIAN_POINT('Ctrl Pts',(160.381948659223,1.46957317570777,126.108802912296));
#30523=CARTESIAN_POINT('Ctrl Pts',(160.374191618338,1.33817625530096,126.069673704969));
#30524=CARTESIAN_POINT('Ctrl Pts',(160.366434577453,1.20526954971698,126.036079126816));
#30525=CARTESIAN_POINT('Ctrl Pts',(160.358683386213,1.07246307011349,126.002509882597));
#30526=CARTESIAN_POINT('Ctrl Pts',(160.350932194973,0.938149449039233,125.974467055463));
#30527=CARTESIAN_POINT('Ctrl Pts',(160.343181003733,0.802828121592549,125.952077642545));
#30528=CARTESIAN_POINT('Ctrl Pts',(160.335433106956,0.66756430931989,125.929697745724));
#30529=CARTESIAN_POINT('Ctrl Pts',(160.327685210178,0.531294027448772,125.912966547714));
#30530=CARTESIAN_POINT('Ctrl Pts',(160.319937313401,0.394527492249022,125.901960070858));
#30531=CARTESIAN_POINT('Ctrl Pts',(160.312191037317,0.25778956566009,125.89095589632));
#30532=CARTESIAN_POINT('Ctrl Pts',(160.304444761233,0.120555981675745,125.885674092408));
#30533=CARTESIAN_POINT('Ctrl Pts',(160.296698485149,-0.0166577166577505,
125.886138826819));
#30534=CARTESIAN_POINT('Ctrl Pts',(160.288952151884,-0.15387242787155,125.886603564661));
#30535=CARTESIAN_POINT('Ctrl Pts',(160.281205818618,-0.291066862178625,
125.892814924147));
#30536=CARTESIAN_POINT('Ctrl Pts',(160.273459485353,-0.427725667555909,
125.904744937146));
#30537=CARTESIAN_POINT('Ctrl Pts',(160.26571141735,-0.564415076725132,125.916677621789));
#30538=CARTESIAN_POINT('Ctrl Pts',(160.257963349347,-0.700568228867815,
125.934331474301));
#30539=CARTESIAN_POINT('Ctrl Pts',(160.250215281344,-0.835675478780135,
125.957626711453));
#30540=CARTESIAN_POINT('Ctrl Pts',(160.242458978602,-0.970926322285506,
125.980946707061));
#30541=CARTESIAN_POINT('Ctrl Pts',(160.23470267586,-1.10512865713056,126.009919997891));
#30542=CARTESIAN_POINT('Ctrl Pts',(160.226946373118,-1.23778306619832,126.044415644824));
#30543=CARTESIAN_POINT('Ctrl Pts',(160.219185930604,-1.37050827691844,126.078929703122));
#30544=CARTESIAN_POINT('Ctrl Pts',(160.21142548809,-1.50168354189003,126.118971876474));
#30545=CARTESIAN_POINT('Ctrl Pts',(160.203665045576,-1.63082613369543,126.164361783067));
#30546=CARTESIAN_POINT('Ctrl Pts',(160.19589214531,-1.76017603665388,126.209824553567));
#30547=CARTESIAN_POINT('Ctrl Pts',(160.188119245045,-1.8874863825716,126.260652067141));
#30548=CARTESIAN_POINT('Ctrl Pts',(160.180346344779,-2.0122950737614,126.316616017144));
#30549=CARTESIAN_POINT('Ctrl Pts',(160.172856009017,-2.13256665465224,126.3705455366));
#30550=CARTESIAN_POINT('Ctrl Pts',(160.165365673255,-2.25051503020531,126.429244393995));
#30551=CARTESIAN_POINT('Ctrl Pts',(160.157875337493,-2.36575123167159,126.492469597104));
#30552=CARTESIAN_POINT('Ctrl Pts',(160.150099986099,-2.48537229916469,126.558100589727));
#30553=CARTESIAN_POINT('Ctrl Pts',(160.142324634705,-2.60244967655088,126.628817140122));
#30554=CARTESIAN_POINT('Ctrl Pts',(160.134549283311,-2.7165207419171,126.704397432215));
#30555=CARTESIAN_POINT('Ctrl Pts',(160.126783736502,-2.83044796561676,126.77988241885));
#30556=CARTESIAN_POINT('Ctrl Pts',(160.119018189693,-2.94137609787276,126.860218728868));
#30557=CARTESIAN_POINT('Ctrl Pts',(160.111252642884,-3.04886646503335,126.945138371971));
#30558=CARTESIAN_POINT('Ctrl Pts',(160.103496441674,-3.1562274708204,127.029955816877));
#30559=CARTESIAN_POINT('Ctrl Pts',(160.095740240463,-3.26015864667098,127.119345368188));
#30560=CARTESIAN_POINT('Ctrl Pts',(160.087984039253,-3.36025024047125,127.212995781753));
#30561=CARTESIAN_POINT('Ctrl Pts',(160.080233136657,-3.46027345714688,127.306582218457));
#30562=CARTESIAN_POINT('Ctrl Pts',(160.07248223406,-3.55646202584206,127.404423460644));
#30563=CARTESIAN_POINT('Ctrl Pts',(160.064731331464,-3.64843918916843,127.506167999564));
#30564=CARTESIAN_POINT('Ctrl Pts',(160.056984045247,-3.74037343823166,127.607865067006));
#30565=CARTESIAN_POINT('Ctrl Pts',(160.049236759029,-3.82809993053074,127.713461517755));
#30566=CARTESIAN_POINT('Ctrl Pts',(160.041489472812,-3.91127900413893,127.822569274383));
#30567=CARTESIAN_POINT('Ctrl Pts',(160.033744123531,-3.99443728174649,127.931649752455));
#30568=CARTESIAN_POINT('Ctrl Pts',(160.02599877425,-4.07305016753664,128.044239477975));
#30569=CARTESIAN_POINT('Ctrl Pts',(160.018253424969,-4.1468187700814,128.159917925693));
#30570=CARTESIAN_POINT('Ctrl Pts',(160.010505830616,-4.22060875523721,128.275629904035));
#30571=CARTESIAN_POINT('Ctrl Pts',(160.002758236264,-4.28955143620647,128.394432066875));
#30572=CARTESIAN_POINT('Ctrl Pts',(159.995010641911,-4.35339165714536,128.515875498104));
#30573=CARTESIAN_POINT('Ctrl Pts',(159.987262048063,-4.41724011393877,128.637334596423));
#30574=CARTESIAN_POINT('Ctrl Pts',(159.979513454214,-4.47598462469449,128.761435292019));
#30575=CARTESIAN_POINT('Ctrl Pts',(159.971764860365,-4.52941679935757,128.887705583347));
#30576=CARTESIAN_POINT('Ctrl Pts',(159.96400967179,-4.58289444944049,129.014083341656));
#30577=CARTESIAN_POINT('Ctrl Pts',(159.956254483215,-4.6310505857517,129.142634021231));
#30578=CARTESIAN_POINT('Ctrl Pts',(159.94849929464,-4.67372549519188,129.272866883301));
#30579=CARTESIAN_POINT('Ctrl Pts',(159.942410322305,-4.707231623442,129.375118980286));
#30580=CARTESIAN_POINT('Ctrl Pts',(159.936321349969,-4.73735977013598,129.478407662633));
#30581=CARTESIAN_POINT('Ctrl Pts',(159.930232377634,-4.76405452823406,129.582490119308));
#30582=CARTESIAN_POINT('Origin',(213.235140564004,0.,130.804360617566));
#30583=CARTESIAN_POINT('',(157.83474697768,-4.76405452823405,129.582490119308));
#30584=CARTESIAN_POINT('',(158.179915040683,-4.76405452823403,129.582490119308));
#30585=CARTESIAN_POINT('',(213.235140564004,-4.76405452823405,129.582490119308));
#30586=CARTESIAN_POINT('',(159.514859436045,-4.91824907623685,130.801346219555));
#30587=CARTESIAN_POINT('Ctrl Pts',(159.514859435991,-4.91824907623744,130.801346220521));
#30588=CARTESIAN_POINT('Ctrl Pts',(159.507046905898,-4.91833398470203,130.93988171244));
#30589=CARTESIAN_POINT('Ctrl Pts',(159.499234375806,-4.9125612288758,131.078436147646));
#30590=CARTESIAN_POINT('Ctrl Pts',(159.491421845713,-4.90095264269885,131.216484696604));
#30591=CARTESIAN_POINT('Ctrl Pts',(159.483608395001,-4.88934268857953,131.354549513044));
#30592=CARTESIAN_POINT('Ctrl Pts',(159.475794944289,-4.87189556608927,131.492107944224));
#30593=CARTESIAN_POINT('Ctrl Pts',(159.467981493577,-4.84868503514287,131.628639995254));
#30594=CARTESIAN_POINT('Ctrl Pts',(159.460165539454,-4.82546706759599,131.765215790838));
#30595=CARTESIAN_POINT('Ctrl Pts',(159.45234958533,-4.79648207834992,131.900764175359));
#30596=CARTESIAN_POINT('Ctrl Pts',(159.444533631207,-4.7618549636528,132.034775331244));
#30597=CARTESIAN_POINT('Ctrl Pts',(159.436713589575,-4.72720974002225,132.168856570909));
#30598=CARTESIAN_POINT('Ctrl Pts',(159.428893547944,-4.68691661062925,132.301398612136));
#30599=CARTESIAN_POINT('Ctrl Pts',(159.421073506313,-4.64115025576767,132.431907042676));
#30600=CARTESIAN_POINT('Ctrl Pts',(159.413243026568,-4.59532281242605,132.562589674584));
#30601=CARTESIAN_POINT('Ctrl Pts',(159.405412546822,-4.54400768117739,132.691232915173));
#30602=CARTESIAN_POINT('Ctrl Pts',(159.397582067076,-4.48742784772967,132.817361952369));
#30603=CARTESIAN_POINT('Ctrl Pts',(159.389745547182,-4.43080437064702,132.943588280938));
#30604=CARTESIAN_POINT('Ctrl Pts',(159.381909027288,-4.36890826923445,133.06729620146));
#30605=CARTESIAN_POINT('Ctrl Pts',(159.374072507394,-4.30200796832913,133.188036456042));
#30606=CARTESIAN_POINT('Ctrl Pts',(159.366223609298,-4.23500199483128,133.308967426294));
#30607=CARTESIAN_POINT('Ctrl Pts',(159.358374711203,-4.16297623535751,133.426921045389));
#30608=CARTESIAN_POINT('Ctrl Pts',(159.350525813108,-4.0862421534414,133.541477371732));
#30609=CARTESIAN_POINT('Ctrl Pts',(159.34772436281,-4.05885401385308,133.582365130839));
#30610=CARTESIAN_POINT('Ctrl Pts',(159.344922912512,-4.03086643201579,133.622820408351));
#30611=CARTESIAN_POINT('Ctrl Pts',(159.342121462214,-4.0022947631806,133.662825186372));
#30612=CARTESIAN_POINT('Ctrl Pts',(159.334347128095,-3.92300522517745,133.773842865649));
#30613=CARTESIAN_POINT('Ctrl Pts',(159.326572793976,-3.83896740064877,133.881734828746));
#30614=CARTESIAN_POINT('Ctrl Pts',(159.318798459857,-3.75045608194201,133.986068058536));
#30615=CARTESIAN_POINT('Ctrl Pts',(159.31103370691,-3.66205384552502,134.090272706945));
#30616=CARTESIAN_POINT('Ctrl Pts',(159.303268953963,-3.56918933501307,134.190927053252));
#30617=CARTESIAN_POINT('Ctrl Pts',(159.295504201015,-3.47218037092224,134.287627264592));
#30618=CARTESIAN_POINT('Ctrl Pts',(159.28774716013,-3.37526775750219,134.384231431918));
#30619=CARTESIAN_POINT('Ctrl Pts',(159.279990119245,-3.27421915728784,134.47688900556));
#30620=CARTESIAN_POINT('Ctrl Pts',(159.27223307836,-3.16939214034595,134.565229735631));
#30621=CARTESIAN_POINT('Ctrl Pts',(159.26448188712,-3.06464417427273,134.65350384727));
#30622=CARTESIAN_POINT('Ctrl Pts',(159.25673069588,-2.95612376064952,134.737467344022));
#30623=CARTESIAN_POINT('Ctrl Pts',(159.24897950464,-2.84422448649254,134.816787580507));
#30624=CARTESIAN_POINT('Ctrl Pts',(159.241231607863,-2.7323727725124,134.896074103775));
#30625=CARTESIAN_POINT('Ctrl Pts',(159.233483711086,-2.61714537259464,134.970721066314));
#30626=CARTESIAN_POINT('Ctrl Pts',(159.225735814309,-2.49896786403922,135.040436947969));
#30627=CARTESIAN_POINT('Ctrl Pts',(159.217989538225,-2.3808150756709,135.110138246564));
#30628=CARTESIAN_POINT('Ctrl Pts',(159.210243262141,-2.2597137426329,135.174910317414));
#30629=CARTESIAN_POINT('Ctrl Pts',(159.202496986057,-2.13611691230614,135.234505942435));
#30630=CARTESIAN_POINT('Ctrl Pts',(159.194750652791,-2.01251916961573,135.294102007377));
#30631=CARTESIAN_POINT('Ctrl Pts',(159.187004319526,-1.88642624504282,135.348521380436));
#30632=CARTESIAN_POINT('Ctrl Pts',(159.17925798626,-1.75831381698292,135.397563811798));
#30633=CARTESIAN_POINT('Ctrl Pts',(159.171509918257,-1.63017269903276,135.446617225873));
#30634=CARTESIAN_POINT('Ctrl Pts',(159.163761850255,-1.50001154271935,135.490291162427));
#30635=CARTESIAN_POINT('Ctrl Pts',(159.156013782252,-1.36832355692679,135.528434463947));
#30636=CARTESIAN_POINT('Ctrl Pts',(159.14825747951,-1.236495611576,135.566618304621));
#30637=CARTESIAN_POINT('Ctrl Pts',(159.140501176768,-1.10313797129142,135.599259659329));
#30638=CARTESIAN_POINT('Ctrl Pts',(159.132744874026,-0.968757021240737,
135.626257847526));
#30639=CARTESIAN_POINT('Ctrl Pts',(159.124984431512,-0.834304348030785,
135.653270445469));
#30640=CARTESIAN_POINT('Ctrl Pts',(159.117223988998,-0.698827662766445,
135.674633814512));
#30641=CARTESIAN_POINT('Ctrl Pts',(159.109463546483,-0.56283996679113,135.690299036568));
#30642=CARTESIAN_POINT('Ctrl Pts',(159.101690646218,-0.426633971293907,
135.70598940583));
#30643=CARTESIAN_POINT('Ctrl Pts',(159.093917745953,-0.289915715978825,
135.715963320679));
#30644=CARTESIAN_POINT('Ctrl Pts',(159.086144845687,-0.153200611303244,
135.720223983771));
#30645=CARTESIAN_POINT('Ctrl Pts',(159.078654509925,-0.021455445046401,
135.724329761028));
#30646=CARTESIAN_POINT('Ctrl Pts',(159.071164174163,0.110286487655596,135.723130459872));
#30647=CARTESIAN_POINT('Ctrl Pts',(159.063673838401,0.241569116679861,135.716674474026));
#30648=CARTESIAN_POINT('Ctrl Pts',(159.055899504282,0.377829366485305,135.709973707514));
#30649=CARTESIAN_POINT('Ctrl Pts',(159.048125170163,0.51402642759366,135.697588547125));
#30650=CARTESIAN_POINT('Ctrl Pts',(159.040350836044,0.64964745845715,135.679516127108));
#30651=CARTESIAN_POINT('Ctrl Pts',(159.032586083097,0.785101348520533,135.661465979734));
#30652=CARTESIAN_POINT('Ctrl Pts',(159.024821330149,0.919980237020838,135.637742569779));
#30653=CARTESIAN_POINT('Ctrl Pts',(159.017056577202,1.05377257817957,135.608395007116));
#30654=CARTESIAN_POINT('Ctrl Pts',(159.009299536317,1.18743203489955,135.579076592865));
#30655=CARTESIAN_POINT('Ctrl Pts',(159.001542495432,1.32000671246847,135.5441452255));
#30656=CARTESIAN_POINT('Ctrl Pts',(158.993785454547,1.45099183381639,135.503701609737));
#30657=CARTESIAN_POINT('Ctrl Pts',(158.986034263307,1.58187817826525,135.463288492819));
#30658=CARTESIAN_POINT('Ctrl Pts',(158.978283072067,1.71117698037423,135.417371516297));
#30659=CARTESIAN_POINT('Ctrl Pts',(158.970531880827,1.83839563276808,135.366102013121));
#30660=CARTESIAN_POINT('Ctrl Pts',(158.96278398405,1.96556021384085,135.314854300851));
#30661=CARTESIAN_POINT('Ctrl Pts',(158.955036087273,2.09064604177785,135.258258732497));
#30662=CARTESIAN_POINT('Ctrl Pts',(158.947288190496,2.21317781749103,135.196515784527));
#30663=CARTESIAN_POINT('Ctrl Pts',(158.939541914412,2.335683962198,135.134785751852));
#30664=CARTESIAN_POINT('Ctrl Pts',(158.931795638327,2.45563676841574,135.067910657039));
#30665=CARTESIAN_POINT('Ctrl Pts',(158.924049362243,2.57258336139334,134.996138034269));
#30666=CARTESIAN_POINT('Ctrl Pts',(158.916303028978,2.68953081764425,134.92436488169));
#30667=CARTESIAN_POINT('Ctrl Pts',(158.908556695713,2.80347168315822,134.847694333515));
#30668=CARTESIAN_POINT('Ctrl Pts',(158.900810362447,2.91398036630329,134.766418351534));
#30669=CARTESIAN_POINT('Ctrl Pts',(158.893062294444,3.02451379710167,134.685124168362));
#30670=CARTESIAN_POINT('Ctrl Pts',(158.885314226441,3.1316132011848,134.599222730702));
#30671=CARTESIAN_POINT('Ctrl Pts',(158.877566158438,3.23488481400627,134.509047284831));
#30672=CARTESIAN_POINT('Ctrl Pts',(158.869809855697,3.33826618512695,134.418775999423));
#30673=CARTESIAN_POINT('Ctrl Pts',(158.862053552955,3.43781134330879,134.324221889295));
#30674=CARTESIAN_POINT('Ctrl Pts',(158.854297250213,3.53316186960717,134.225756570339));
#30675=CARTESIAN_POINT('Ctrl Pts',(158.846536807699,3.62856328735242,134.127238697478));
#30676=CARTESIAN_POINT('Ctrl Pts',(158.838776365184,3.7197653523574,134.024805748063));
#30677=CARTESIAN_POINT('Ctrl Pts',(158.83101592267,3.80644961869418,133.918862883233));
#30678=CARTESIAN_POINT('Ctrl Pts',(158.823243022405,3.89327303831072,133.812749949511));
#30679=CARTESIAN_POINT('Ctrl Pts',(158.815470122139,3.97556393187606,133.703116153854));
#30680=CARTESIAN_POINT('Ctrl Pts',(158.807697221874,4.05304640193297,133.590396856792));
#30681=CARTESIAN_POINT('Ctrl Pts',(158.800206886112,4.12771218903637,133.4817751901));
#30682=CARTESIAN_POINT('Ctrl Pts',(158.79271655035,4.19791291560811,133.370288719424));
#30683=CARTESIAN_POINT('Ctrl Pts',(158.785226214588,4.26344277961622,133.256347307464));
#30684=CARTESIAN_POINT('Ctrl Pts',(158.777451880469,4.33145722833588,133.138085772237));
#30685=CARTESIAN_POINT('Ctrl Pts',(158.76967754635,4.39465508046152,133.016804845711));
#30686=CARTESIAN_POINT('Ctrl Pts',(158.761903212231,4.45275672157375,132.892934446996));
#30687=CARTESIAN_POINT('Ctrl Pts',(158.754138459284,4.51078675760594,132.769216707477));
#30688=CARTESIAN_POINT('Ctrl Pts',(158.746373706337,4.5637329147631,132.642916196056));
#30689=CARTESIAN_POINT('Ctrl Pts',(158.738608953389,4.61136000758437,132.514489835769));
#30690=CARTESIAN_POINT('Ctrl Pts',(158.730851912504,4.65893979650574,132.386191030354));
#30691=CARTESIAN_POINT('Ctrl Pts',(158.723094871619,4.70121089937608,132.255770942098));
#30692=CARTESIAN_POINT('Ctrl Pts',(158.715337830734,4.73798519758984,132.123708687606));
#30693=CARTESIAN_POINT('Ctrl Pts',(158.707586639494,4.7747317640193,131.991746022288));
#30694=CARTESIAN_POINT('Ctrl Pts',(158.699835448254,4.8059896720736,131.858144030747));
#30695=CARTESIAN_POINT('Ctrl Pts',(158.692084257014,4.83161997613111,131.723398956674));
#30696=CARTESIAN_POINT('Ctrl Pts',(158.684336360237,4.8572393866256,131.588711152853));
#30697=CARTESIAN_POINT('Ctrl Pts',(158.67658846346,4.87723587748997,131.452881616076));
#30698=CARTESIAN_POINT('Ctrl Pts',(158.668840566683,4.89152120449035,131.316418591355));
#30699=CARTESIAN_POINT('Ctrl Pts',(158.661094290599,4.90580354330827,131.179984111758));
#30700=CARTESIAN_POINT('Ctrl Pts',(158.653348014515,4.91437705381214,131.042916796386));
#30701=CARTESIAN_POINT('Ctrl Pts',(158.64560173843,4.91720520365298,130.905731459863));
#30702=CARTESIAN_POINT('Ctrl Pts',(158.637855405165,4.9200333743706,130.768545110669));
#30703=CARTESIAN_POINT('Ctrl Pts',(158.6301090719,4.91711609173894,130.631241129468));
#30704=CARTESIAN_POINT('Ctrl Pts',(158.622362738634,4.90846894880806,130.494335391033));
#30705=CARTESIAN_POINT('Ctrl Pts',(158.614614670631,4.89981986940952,130.357398993507));
#30706=CARTESIAN_POINT('Ctrl Pts',(158.606866602628,4.88543840100705,130.220861406325));
#30707=CARTESIAN_POINT('Ctrl Pts',(158.599118534625,4.86539207377361,130.085234042504));
#30708=CARTESIAN_POINT('Ctrl Pts',(158.591362231884,4.845324441065,129.949462532305));
#30709=CARTESIAN_POINT('Ctrl Pts',(158.583605929142,4.8195799798263,129.814603565325));
#30710=CARTESIAN_POINT('Ctrl Pts',(158.5758496264,4.78827760683634,129.681159557039));
#30711=CARTESIAN_POINT('Ctrl Pts',(158.568089183886,4.75695852682736,129.547644325667));
#30712=CARTESIAN_POINT('Ctrl Pts',(158.560328741372,4.72007572930198,129.415545934178));
#30713=CARTESIAN_POINT('Ctrl Pts',(158.552568298857,4.67779795999857,129.285351299644));
#30714=CARTESIAN_POINT('Ctrl Pts',(158.544795398592,4.63545232266669,129.154947665125));
#30715=CARTESIAN_POINT('Ctrl Pts',(158.537022498327,4.5876945434294,129.026454261262));
#30716=CARTESIAN_POINT('Ctrl Pts',(158.529249598061,4.53474177411445,128.900338531402));
#30717=CARTESIAN_POINT('Ctrl Pts',(158.521759262299,4.48371397134414,128.778807425988));
#30718=CARTESIAN_POINT('Ctrl Pts',(158.514268926537,4.42786245356357,128.659484405926));
#30719=CARTESIAN_POINT('Ctrl Pts',(158.506778590775,4.36742080884511,128.542764159095));
#30720=CARTESIAN_POINT('Ctrl Pts',(158.499004256656,4.30468750079616,128.421618428629));
#30721=CARTESIAN_POINT('Ctrl Pts',(158.491229922537,4.23681040522234,128.302892982541));
#30722=CARTESIAN_POINT('Ctrl Pts',(158.483455588418,4.16400008682413,128.187055450141));
#30723=CARTESIAN_POINT('Ctrl Pts',(158.475690835471,4.09127950063627,128.071360677148));
#30724=CARTESIAN_POINT('Ctrl Pts',(158.467926082524,4.0136379945863,127.958547064133));
#30725=CARTESIAN_POINT('Ctrl Pts',(158.460161329576,3.93133286748008,127.849059457351));
#30726=CARTESIAN_POINT('Ctrl Pts',(158.452404288691,3.84910948698593,127.739680595202));
#30727=CARTESIAN_POINT('Ctrl Pts',(158.444647247806,3.76223193667793,127.633621475787));
#30728=CARTESIAN_POINT('Ctrl Pts',(158.436890206921,3.6710016282233,127.531299342844));
#30729=CARTESIAN_POINT('Ctrl Pts',(158.429139015681,3.57984011725463,127.429054371819));
#30730=CARTESIAN_POINT('Ctrl Pts',(158.421387824441,3.48433264078649,127.330541068666));
#30731=CARTESIAN_POINT('Ctrl Pts',(158.413636633201,3.38482159918926,127.236144564107));
#30732=CARTESIAN_POINT('Ctrl Pts',(158.405888736424,3.28535285243901,127.141788180581));
#30733=CARTESIAN_POINT('Ctrl Pts',(158.398140839647,3.18188420800949,127.051545384038));
#30734=CARTESIAN_POINT('Ctrl Pts',(158.39039294287,3.07479556866096,126.965765135695));
#30735=CARTESIAN_POINT('Ctrl Pts',(158.382646666786,2.96772932994706,126.88000283073));
#30736=CARTESIAN_POINT('Ctrl Pts',(158.374900390702,2.85704490742315,126.798701461515));
#30737=CARTESIAN_POINT('Ctrl Pts',(158.367154114618,2.74315568258615,126.722170033628));
#30738=CARTESIAN_POINT('Ctrl Pts',(158.359407781352,2.62926561704496,126.645638040803));
#30739=CARTESIAN_POINT('Ctrl Pts',(158.351661448087,2.51217102648917,126.573876277627));
#30740=CARTESIAN_POINT('Ctrl Pts',(158.343915114821,2.39231435939962,126.507150468142));
#30741=CARTESIAN_POINT('Ctrl Pts',(158.336167046819,2.27243085124042,126.440409715875));
#30742=CARTESIAN_POINT('Ctrl Pts',(158.328418978816,2.14978437724043,126.378707351558));
#30743=CARTESIAN_POINT('Ctrl Pts',(158.320670910813,2.02484170536205,126.322262991373));
#30744=CARTESIAN_POINT('Ctrl Pts',(158.312914608071,1.89976624292512,126.26575864145));
#30745=CARTESIAN_POINT('Ctrl Pts',(158.305158305329,1.7723900644575,126.214523620045));
#30746=CARTESIAN_POINT('Ctrl Pts',(158.297402002587,1.64320014375113,126.16872944694));
#30747=CARTESIAN_POINT('Ctrl Pts',(158.289641560073,1.51394127049389,126.122910832107));
#30748=CARTESIAN_POINT('Ctrl Pts',(158.281881117559,1.38286709953899,126.082538966958));
#30749=CARTESIAN_POINT('Ctrl Pts',(158.274120675044,1.25047849920119,126.047735071495));
#30750=CARTESIAN_POINT('Ctrl Pts',(158.266347774779,1.11787737692959,126.012875305729));
#30751=CARTESIAN_POINT('Ctrl Pts',(158.258574874514,0.983957990911603,125.983601454559));
#30752=CARTESIAN_POINT('Ctrl Pts',(158.250801974248,0.849230990338732,125.959983486546));
#30753=CARTESIAN_POINT('Ctrl Pts',(158.243311638486,0.71940165559325,125.937224091161));
#30754=CARTESIAN_POINT('Ctrl Pts',(158.235821302724,0.588822709801794,125.919716547896));
#30755=CARTESIAN_POINT('Ctrl Pts',(158.228330966962,0.457952475113953,125.907477670932));
#30756=CARTESIAN_POINT('Ctrl Pts',(158.220556632843,0.322120255700965,125.894774753227));
#30757=CARTESIAN_POINT('Ctrl Pts',(158.212782298724,0.185543947279615,125.887707672472));
#30758=CARTESIAN_POINT('Ctrl Pts',(158.205007964605,0.048730794997183,125.886352039684));
#30759=CARTESIAN_POINT('Ctrl Pts',(158.197243211658,-0.0879137473025429,
125.884998077593));
#30760=CARTESIAN_POINT('Ctrl Pts',(158.189478458711,-0.224794165498482,
125.889341562095));
#30761=CARTESIAN_POINT('Ctrl Pts',(158.181713705764,-0.361397121550913,
125.899406470682));
#30762=CARTESIAN_POINT('Ctrl Pts',(158.173956664879,-0.497864401621396,
125.90946138266));
#30763=CARTESIAN_POINT('Ctrl Pts',(158.166199623994,-0.634054380578433,
125.925226381552));
#30764=CARTESIAN_POINT('Ctrl Pts',(158.158442583109,-0.769453099079439,
125.946673411619));
#30765=CARTESIAN_POINT('Ctrl Pts',(158.150691391868,-0.904749712353483,
125.968104268314));
#30766=CARTESIAN_POINT('Ctrl Pts',(158.142940200628,-1.03925586826959,125.995208566503));
#30767=CARTESIAN_POINT('Ctrl Pts',(158.135189009388,-1.17246246967853,126.027906407622));
#30768=CARTESIAN_POINT('Ctrl Pts',(158.127441112611,-1.30561245472861,126.060590351285));
#30769=CARTESIAN_POINT('Ctrl Pts',(158.119693215834,-1.43746360494574,126.098863016394));
#30770=CARTESIAN_POINT('Ctrl Pts',(158.111945319057,-1.56751698265293,126.142593402057));
#30771=CARTESIAN_POINT('Ctrl Pts',(158.104199042973,-1.69754315599708,126.186314640266));
#30772=CARTESIAN_POINT('Ctrl Pts',(158.096452766889,-1.82577193448391,126.235491203724));
#30773=CARTESIAN_POINT('Ctrl Pts',(158.088706490805,-1.95171990017145,126.289942327933));
#30774=CARTESIAN_POINT('Ctrl Pts',(158.080960157539,-2.07766879557827,126.344393854087));
#30775=CARTESIAN_POINT('Ctrl Pts',(158.073213824274,-2.20133648572639,126.404119863538));
#30776=CARTESIAN_POINT('Ctrl Pts',(158.065467491009,-2.32226025524325,126.468891742183));
#30777=CARTESIAN_POINT('Ctrl Pts',(158.057719423006,-2.44321110480003,126.53367812604));
#30778=CARTESIAN_POINT('Ctrl Pts',(158.049971355003,-2.56141646640514,126.603512443068));
#30779=CARTESIAN_POINT('Ctrl Pts',(158.042223287,-2.67643927126129,126.67812069607));
#30780=CARTESIAN_POINT('Ctrl Pts',(158.034466984258,-2.7915843237232,126.75280824361));
#30781=CARTESIAN_POINT('Ctrl Pts',(158.026710681516,-2.9035397340804,126.832279649482));
#30782=CARTESIAN_POINT('Ctrl Pts',(158.018954378774,-3.01189797665267,126.916217919473));
#30783=CARTESIAN_POINT('Ctrl Pts',(158.01119393626,-3.12031405328153,127.000200989846));
#30784=CARTESIAN_POINT('Ctrl Pts',(158.003433493746,-3.2251288378874,127.088655422833));
#30785=CARTESIAN_POINT('Ctrl Pts',(157.995673051232,-3.32596961309159,127.181225346107));
#30786=CARTESIAN_POINT('Ctrl Pts',(157.987900150966,-3.42697226686039,127.27394387084));
#30787=CARTESIAN_POINT('Ctrl Pts',(157.980127250701,-3.52398788623438,127.370790811479));
#30788=CARTESIAN_POINT('Ctrl Pts',(157.972354350435,-3.61668158631872,127.471374364117));
#30789=CARTESIAN_POINT('Ctrl Pts',(157.964864014673,-3.70600563692349,127.56830145126));
#30790=CARTESIAN_POINT('Ctrl Pts',(157.957373678911,-3.79131633867925,127.668697961763));
#30791=CARTESIAN_POINT('Ctrl Pts',(157.949883343149,-3.87235181102435,127.772187384692));
#30792=CARTESIAN_POINT('Ctrl Pts',(157.942108314672,-3.95646727996599,127.879610234073));
#30793=CARTESIAN_POINT('Ctrl Pts',(157.934333286195,-4.03624745410983,127.990712287173));
#30794=CARTESIAN_POINT('Ctrl Pts',(157.926558257717,-4.11135287214958,128.105108753962));
#30795=CARTESIAN_POINT('Ctrl Pts',(157.918795709745,-4.1863377306947,128.219321591121));
#30796=CARTESIAN_POINT('Ctrl Pts',(157.911033161772,-4.25666256443127,128.336817987588));
#30797=CARTESIAN_POINT('Ctrl Pts',(157.903270613799,-4.32202819273545,128.457180316929));
#30798=CARTESIAN_POINT('Ctrl Pts',(157.895515248821,-4.38733333561691,128.577431270206));
#30799=CARTESIAN_POINT('Ctrl Pts',(157.887759883844,-4.44768821420025,128.700542541763));
#30800=CARTESIAN_POINT('Ctrl Pts',(157.880004518866,-4.50283681842229,128.826067502489));
#30801=CARTESIAN_POINT('Ctrl Pts',(157.872255468489,-4.557940519357,128.951490257848));
#30802=CARTESIAN_POINT('Ctrl Pts',(157.864506418111,-4.60784622703961,129.079322434733));
#30803=CARTESIAN_POINT('Ctrl Pts',(157.856757367734,-4.65234404438156,129.209093255897));
#30804=CARTESIAN_POINT('Ctrl Pts',(157.849420571049,-4.69447455364886,129.331960198822));
#30805=CARTESIAN_POINT('Ctrl Pts',(157.842083774365,-4.73175751323662,129.456564548009));
#30806=CARTESIAN_POINT('Ctrl Pts',(157.83474697768,-4.76405452823405,129.582490119308));
#30807=CARTESIAN_POINT('Ctrl Pts',(159.584608960876,-4.76405452823403,129.582490119308));
#30808=CARTESIAN_POINT('Ctrl Pts',(159.575875008844,-4.80223670963421,129.731361865092));
#30809=CARTESIAN_POINT('Ctrl Pts',(159.567141056811,-4.83348102434377,129.882197515467));
#30810=CARTESIAN_POINT('Ctrl Pts',(159.558407104779,-4.85760317562201,130.034377208208));
#30811=CARTESIAN_POINT('Ctrl Pts',(159.549722762089,-4.88158831171254,130.185692511661));
#30812=CARTESIAN_POINT('Ctrl Pts',(159.541038419399,-4.89853187053611,130.338336438866));
#30813=CARTESIAN_POINT('Ctrl Pts',(159.53235407671,-4.90830056874771,130.491680926299));
#30814=CARTESIAN_POINT('Ctrl Pts',(159.526522529822,-4.9148602617138,130.594651939817));
#30815=CARTESIAN_POINT('Ctrl Pts',(159.520690982934,-4.91818569755605,130.697938462117));
#30816=CARTESIAN_POINT('Ctrl Pts',(159.514859436045,-4.91824907623685,130.801346219555));
#30817=CARTESIAN_POINT('',(159.860140563974,-4.91824957733792,130.80232161894));
#30818=CARTESIAN_POINT('Ctrl Pts',(159.930232377634,-4.76405452823406,129.582490119308));
#30819=CARTESIAN_POINT('Ctrl Pts',(159.92246762958,-4.79809608066164,129.715217615571));
#30820=CARTESIAN_POINT('Ctrl Pts',(159.914702881527,-4.82655266194119,129.849235873015));
#30821=CARTESIAN_POINT('Ctrl Pts',(159.906938133473,-4.84935554201804,129.984035139723));
#30822=CARTESIAN_POINT('Ctrl Pts',(159.899162618928,-4.87219004025057,130.119021317214));
#30823=CARTESIAN_POINT('Ctrl Pts',(159.891387104383,-4.88935514236526,130.254790279368));
#30824=CARTESIAN_POINT('Ctrl Pts',(159.883611589838,-4.90083404844994,130.390828645339));
#30825=CARTESIAN_POINT('Ctrl Pts',(159.882216964452,-4.90289291847507,130.415228645818));
#30826=CARTESIAN_POINT('Ctrl Pts',(159.880822339066,-4.90476899633132,130.439637318142));
#30827=CARTESIAN_POINT('Ctrl Pts',(159.879427713681,-4.90646236201941,130.464051709973));
#30828=CARTESIAN_POINT('Ctrl Pts',(159.87299866379,-4.91426856761627,130.576599025358));
#30829=CARTESIAN_POINT('Ctrl Pts',(159.866569613899,-4.91820276995444,130.689417998646));
#30830=CARTESIAN_POINT('Ctrl Pts',(159.860140564008,-4.91824957733767,130.802321618344));
#30831=CARTESIAN_POINT('Ctrl Pts',(159.860140563974,-4.91824957733792,130.80232161894));
#30832=CARTESIAN_POINT('Ctrl Pts',(159.852445159348,-4.91830560453543,130.937464299746));
#30833=CARTESIAN_POINT('Ctrl Pts',(159.844749754723,-4.91278728852856,131.072834611119));
#30834=CARTESIAN_POINT('Ctrl Pts',(159.837054350097,-4.90166458996473,131.207928839786));
#30835=CARTESIAN_POINT('Ctrl Pts',(159.829368007524,-4.89055498940976,131.342863982473));
#30836=CARTESIAN_POINT('Ctrl Pts',(159.821681664951,-4.87385416547425,131.477523294776));
#30837=CARTESIAN_POINT('Ctrl Pts',(159.813995322378,-4.85158406506426,131.611401584379));
#30838=CARTESIAN_POINT('Ctrl Pts',(159.806316102376,-4.82933460130636,131.745155815283));
#30839=CARTESIAN_POINT('Ctrl Pts',(159.798636882374,-4.80152619300176,131.878130071634));
#30840=CARTESIAN_POINT('Ctrl Pts',(159.790957662372,-4.76823267337784,132.00982328187));
#30841=CARTESIAN_POINT('Ctrl Pts',(159.783041930184,-4.73391374712471,132.145572509384));
#30842=CARTESIAN_POINT('Ctrl Pts',(159.775126197997,-4.69376641371811,132.279960076937));
#30843=CARTESIAN_POINT('Ctrl Pts',(159.767210465809,-4.64792874228581,132.412446892967));
#30844=CARTESIAN_POINT('Ctrl Pts',(159.759538874211,-4.60350481703267,132.540847490738));
#30845=CARTESIAN_POINT('Ctrl Pts',(159.751867282613,-4.55373652964841,132.667462452084));
#30846=CARTESIAN_POINT('Ctrl Pts',(159.744195691015,-4.498800346222,132.791815901927));
#30847=CARTESIAN_POINT('Ctrl Pts',(159.736524941261,-4.44387019123,132.916155705816));
#30848=CARTESIAN_POINT('Ctrl Pts',(159.728854191507,-4.3837734292531,133.03823412636));
#30849=CARTESIAN_POINT('Ctrl Pts',(159.721183441753,-4.31873446334889,133.157595773173));
#30850=CARTESIAN_POINT('Ctrl Pts',(159.713511792458,-4.25368787039606,133.276971417396));
#30851=CARTESIAN_POINT('Ctrl Pts',(159.705840143164,-4.18369811216107,133.393629303588));
#30852=CARTESIAN_POINT('Ctrl Pts',(159.698168493869,-4.10903503364523,133.507139586475));
#30853=CARTESIAN_POINT('Ctrl Pts',(159.690494203257,-4.03434624893852,133.620688950485));
#30854=CARTESIAN_POINT('Ctrl Pts',(159.682819912645,-3.95498116330527,133.731088222441));
#30855=CARTESIAN_POINT('Ctrl Pts',(159.675145622034,-3.87125202192377,133.837937853314));
#30856=CARTESIAN_POINT('Ctrl Pts',(159.667462889337,-3.78743077450296,133.944905023866));
#30857=CARTESIAN_POINT('Ctrl Pts',(159.65978015664,-3.69923613639072,134.048314445649));
#30858=CARTESIAN_POINT('Ctrl Pts',(159.652097423944,-3.60701976937073,134.147800679219));
#30859=CARTESIAN_POINT('Ctrl Pts',(159.644409615416,-3.5147424768062,134.247352641392));
#30860=CARTESIAN_POINT('Ctrl Pts',(159.636721806889,-3.41843844804785,134.342975974839));
#30861=CARTESIAN_POINT('Ctrl Pts',(159.629033998361,-3.31849409145874,134.434344092384));
#30862=CARTESIAN_POINT('Ctrl Pts',(159.621335500479,-3.21841076929584,134.525839250848));
#30863=CARTESIAN_POINT('Ctrl Pts',(159.613637002596,-3.1146773236678,134.613067132168));
#30864=CARTESIAN_POINT('Ctrl Pts',(159.605938504713,-3.00771107946218,134.695743035805));
#30865=CARTESIAN_POINT('Ctrl Pts',(159.604285699765,-2.98474629588517,134.71349288061));
#30866=CARTESIAN_POINT('Ctrl Pts',(159.602632894816,-2.96163260066913,134.731033077885));
#30867=CARTESIAN_POINT('Ctrl Pts',(159.600980089868,-2.93837427568491,134.748361083906));
#30868=CARTESIAN_POINT('Ctrl Pts',(159.593205755749,-2.82897359313902,134.829867197833));
#30869=CARTESIAN_POINT('Ctrl Pts',(159.58543142163,-2.71600577086117,134.90694704463));
#30870=CARTESIAN_POINT('Ctrl Pts',(159.577657087511,-2.59986469390879,134.979272189787));
#30871=CARTESIAN_POINT('Ctrl Pts',(159.569892334564,-2.48386675045409,135.051508200667));
#30872=CARTESIAN_POINT('Ctrl Pts',(159.562127581617,-2.36470366224649,135.119000964367));
#30873=CARTESIAN_POINT('Ctrl Pts',(159.554362828669,-2.24280137670867,135.181462974963));
#30874=CARTESIAN_POINT('Ctrl Pts',(159.546605787784,-2.12102016623907,135.24386294741));
#30875=CARTESIAN_POINT('Ctrl Pts',(159.538848746899,-1.99650551827106,135.301241933109));
#30876=CARTESIAN_POINT('Ctrl Pts',(159.531091706014,-1.86971097746101,135.353356542302));
#30877=CARTESIAN_POINT('Ctrl Pts',(159.523340514774,-1.74301205340064,135.405431851462));
#30878=CARTESIAN_POINT('Ctrl Pts',(159.515589323534,-1.61403701877965,135.452250537947));
#30879=CARTESIAN_POINT('Ctrl Pts',(159.507838132294,-1.48326223322349,135.493616017946));
#30880=CARTESIAN_POINT('Ctrl Pts',(159.500090235517,-1.35254303043986,135.534963916512));
#30881=CARTESIAN_POINT('Ctrl Pts',(159.49234233874,-1.22002597011408,135.570863100774));
#30882=CARTESIAN_POINT('Ctrl Pts',(159.484594441963,-1.08620531746851,135.601165915971));
#30883=CARTESIAN_POINT('Ctrl Pts',(159.476848165879,-0.952412657218591,
135.631462392471));
#30884=CARTESIAN_POINT('Ctrl Pts',(159.469101889795,-0.817317328100775,
135.656164742082));
#30885=CARTESIAN_POINT('Ctrl Pts',(159.46135561371,-0.681426226591078,135.67517588405));
#30886=CARTESIAN_POINT('Ctrl Pts',(159.453609280445,-0.54553412196414,135.694187166354));
#30887=CARTESIAN_POINT('Ctrl Pts',(159.44586294718,-0.40884662041825,135.707507103015));
#30888=CARTESIAN_POINT('Ctrl Pts',(159.438116613914,-0.271877827622247,
135.715090248624));
#30889=CARTESIAN_POINT('Ctrl Pts',(159.430368545911,-0.134878361614726,
135.722675092425));
#30890=CARTESIAN_POINT('Ctrl Pts',(159.422620477908,0.00240213069945419,
135.724520567133));
#30891=CARTESIAN_POINT('Ctrl Pts',(159.414872409906,0.13944783995033,135.720633327906));
#30892=CARTESIAN_POINT('Ctrl Pts',(159.407116107164,0.27663920301177,135.716741957275));
#30893=CARTESIAN_POINT('Ctrl Pts',(159.399359804422,0.413594893115202,135.707105712795));
#30894=CARTESIAN_POINT('Ctrl Pts',(159.39160350168,0.549801966247687,135.691783339248));
#30895=CARTESIAN_POINT('Ctrl Pts',(159.383843059166,0.686081737196404,135.676452787688));
#30896=CARTESIAN_POINT('Ctrl Pts',(159.376082616652,0.821611708862234,135.655430119748));
#30897=CARTESIAN_POINT('Ctrl Pts',(159.368322174137,0.9558884419229,135.628825390896));
#30898=CARTESIAN_POINT('Ctrl Pts',(159.360549273872,1.09038072791596,135.602177953771));
#30899=CARTESIAN_POINT('Ctrl Pts',(159.352776373607,1.22361537485448,135.569930641185));
#30900=CARTESIAN_POINT('Ctrl Pts',(159.345003473341,1.35510256365665,135.532243875904));
#30901=CARTESIAN_POINT('Ctrl Pts',(159.337513137579,1.48180986195065,135.495927119468));
#30902=CARTESIAN_POINT('Ctrl Pts',(159.330022801817,1.60689425291996,135.454559616627));
#30903=CARTESIAN_POINT('Ctrl Pts',(159.322532466055,1.72993622244429,135.408326704406));
#30904=CARTESIAN_POINT('Ctrl Pts',(159.314758131936,1.85764336563999,135.360340857267));
#30905=CARTESIAN_POINT('Ctrl Pts',(159.306983797817,1.98355469109857,135.306961368943));
#30906=CARTESIAN_POINT('Ctrl Pts',(159.299209463698,2.10718097307052,135.248342099214));
#30907=CARTESIAN_POINT('Ctrl Pts',(159.29144471075,2.23065489669891,135.189795072496));
#30908=CARTESIAN_POINT('Ctrl Pts',(159.283679957803,2.35184903019095,135.126021278895));
#30909=CARTESIAN_POINT('Ctrl Pts',(159.275915204856,2.47029125168392,135.057223676066));
#30910=CARTESIAN_POINT('Ctrl Pts',(159.268158163971,2.588615834692,134.988494403987));
#30911=CARTESIAN_POINT('Ctrl Pts',(159.260401123086,2.70419360908349,134.914751447543));
#30912=CARTESIAN_POINT('Ctrl Pts',(159.252644082201,2.81657465219533,134.836244828591));
#30913=CARTESIAN_POINT('Ctrl Pts',(159.244892890961,2.92887094788952,134.757797412089));
#30914=CARTESIAN_POINT('Ctrl Pts',(159.237141699721,3.0379749914075,134.674593706355));
#30915=CARTESIAN_POINT('Ctrl Pts',(159.229390508481,3.14346390720701,134.586928227879));
#30916=CARTESIAN_POINT('Ctrl Pts',(159.221642611704,3.24890798740281,134.49930000957));
#30917=CARTESIAN_POINT('Ctrl Pts',(159.213894714927,3.3507396958555,134.407214039619));
#30918=CARTESIAN_POINT('Ctrl Pts',(159.20614681815,3.44856764400671,134.311006346352));
#30919=CARTESIAN_POINT('Ctrl Pts',(159.198400542065,3.54637512866016,134.214818777659));
#30920=CARTESIAN_POINT('Ctrl Pts',(159.190654265981,3.6401802402699,134.114511474527));
#30921=CARTESIAN_POINT('Ctrl Pts',(159.182907989897,3.72962731212147,134.010458428797));
#30922=CARTESIAN_POINT('Ctrl Pts',(159.175161656632,3.81907504425073,133.906404614971));
#30923=CARTESIAN_POINT('Ctrl Pts',(159.167415323366,3.9041644175673,133.798605299852));
#30924=CARTESIAN_POINT('Ctrl Pts',(159.159668990101,3.98457931088853,133.687468450745));
#30925=CARTESIAN_POINT('Ctrl Pts',(159.151920922098,4.06501221256767,133.576306713311));
#30926=CARTESIAN_POINT('Ctrl Pts',(159.144172854095,4.14076832206378,133.461806271299));
#30927=CARTESIAN_POINT('Ctrl Pts',(159.136424786092,4.21157443098738,133.344404687017));
#30928=CARTESIAN_POINT('Ctrl Pts',(159.12866848335,4.28245579348614,133.226878326934));
#30929=CARTESIAN_POINT('Ctrl Pts',(159.120912180608,4.34837644392194,133.106445000543));
#30930=CARTESIAN_POINT('Ctrl Pts',(159.113155877867,4.40910854717513,132.98356801516));
#30931=CARTESIAN_POINT('Ctrl Pts',(159.105395435352,4.46987306498049,132.860625446629));
#30932=CARTESIAN_POINT('Ctrl Pts',(159.097634992838,4.52544335923817,132.735236977529));
#30933=CARTESIAN_POINT('Ctrl Pts',(159.089874550324,4.57563990148032,132.607885653289));
#30934=CARTESIAN_POINT('Ctrl Pts',(159.082101650059,4.62591702366828,132.480329893398));
#30935=CARTESIAN_POINT('Ctrl Pts',(159.074328749793,4.67080302740583,132.35080535139));
#30936=CARTESIAN_POINT('Ctrl Pts',(159.066555849528,4.71016812173062,132.219810838355));
#30937=CARTESIAN_POINT('Ctrl Pts',(159.059065513766,4.74810219572142,132.093578305826));
#30938=CARTESIAN_POINT('Ctrl Pts',(159.051575178004,4.78090971266741,131.96598111939));
#30939=CARTESIAN_POINT('Ctrl Pts',(159.044084842242,4.80851984422631,131.837472407346));
#30940=CARTESIAN_POINT('Ctrl Pts',(159.036310508123,4.83717682231556,131.704091248423));
#30941=CARTESIAN_POINT('Ctrl Pts',(159.028536174004,4.86032529396847,131.569305567015));
#30942=CARTESIAN_POINT('Ctrl Pts',(159.020761839885,4.87783026730727,131.433610127571));
#30943=CARTESIAN_POINT('Ctrl Pts',(159.012997086938,4.89531366733088,131.298081920628));
#30944=CARTESIAN_POINT('Ctrl Pts',(159.005232333991,4.90716735809032,131.161646570522));
#30945=CARTESIAN_POINT('Ctrl Pts',(158.997467581044,4.91330690021019,131.024810990319));
#30946=CARTESIAN_POINT('Ctrl Pts',(158.989710540158,4.91944034445029,130.888111317143));
#30947=CARTESIAN_POINT('Ctrl Pts',(158.981953499273,4.91987091688834,130.751012592984));
#30948=CARTESIAN_POINT('Ctrl Pts',(158.974196458388,4.91456577380205,130.614028493442));
#30949=CARTESIAN_POINT('Ctrl Pts',(158.966445267148,4.90926463136541,130.477147694675));
#30950=CARTESIAN_POINT('Ctrl Pts',(158.958694075908,4.89823639781546,130.340381737563));
#30951=CARTESIAN_POINT('Ctrl Pts',(158.950942884668,4.88150028365789,130.204245592635));
#30952=CARTESIAN_POINT('Ctrl Pts',(158.943194987891,4.8647712827954,130.068167309201));
#30953=CARTESIAN_POINT('Ctrl Pts',(158.935447091114,4.84233927406236,129.932718692773));
#30954=CARTESIAN_POINT('Ctrl Pts',(158.927699194337,4.81427541252908,129.798410661148));
#30955=CARTESIAN_POINT('Ctrl Pts',(158.919952918253,4.78621742135064,129.664130723867));
#30956=CARTESIAN_POINT('Ctrl Pts',(158.912206642169,4.75253000051732,129.530991279286));
#30957=CARTESIAN_POINT('Ctrl Pts',(158.904460366084,4.71333555341149,129.399493711611));
#30958=CARTESIAN_POINT('Ctrl Pts',(158.896714032819,4.67414081698108,129.267995173251));
#30959=CARTESIAN_POINT('Ctrl Pts',(158.888967699554,4.62943908483753,129.138138910657));
#30960=CARTESIAN_POINT('Ctrl Pts',(158.881221366288,4.57940272020786,129.010411401826));
#30961=CARTESIAN_POINT('Ctrl Pts',(158.873473298285,4.52935515028136,128.882655289306));
#30962=CARTESIAN_POINT('Ctrl Pts',(158.865725230282,4.47397071322438,128.757029243127));
#30963=CARTESIAN_POINT('Ctrl Pts',(158.857977162279,4.41346986679087,128.633999634359));
#30964=CARTESIAN_POINT('Ctrl Pts',(158.850220859538,4.35290471933774,128.510839268258));
#30965=CARTESIAN_POINT('Ctrl Pts',(158.842464556796,4.2872124727583,128.390281203415));
#30966=CARTESIAN_POINT('Ctrl Pts',(158.834708254054,4.21665977017082,128.272767552889));
#30967=CARTESIAN_POINT('Ctrl Pts',(158.82694781154,4.14606941148154,128.155191181788));
#30968=CARTESIAN_POINT('Ctrl Pts',(158.819187369026,4.07061364266819,128.040662789065));
#30969=CARTESIAN_POINT('Ctrl Pts',(158.811426926511,3.99060182400884,127.929594514956));
#30970=CARTESIAN_POINT('Ctrl Pts',(158.803654026246,3.91046156327514,127.818347944193));
#30971=CARTESIAN_POINT('Ctrl Pts',(158.795881125981,3.82575087918032,127.710572899243));
#30972=CARTESIAN_POINT('Ctrl Pts',(158.788108225715,3.73681928043525,127.606648196496));
#30973=CARTESIAN_POINT('Ctrl Pts',(158.780617889953,3.65112056930974,127.506501418464));
#30974=CARTESIAN_POINT('Ctrl Pts',(158.773127554191,3.56150270689706,127.409930129295));
#30975=CARTESIAN_POINT('Ctrl Pts',(158.765637218429,3.4683086384193,127.317238845794));
#30976=CARTESIAN_POINT('Ctrl Pts',(158.75786288431,3.37158108850939,127.221033144106));
#30977=CARTESIAN_POINT('Ctrl Pts',(158.750088550191,3.27069439177339,127.128702726181));
#30978=CARTESIAN_POINT('Ctrl Pts',(158.742314216072,3.1659918411462,127.040628596779));
#30979=CARTESIAN_POINT('Ctrl Pts',(158.734549463125,3.0614183270553,126.952663010871));
#30980=CARTESIAN_POINT('Ctrl Pts',(158.726784710178,2.95303861235956,126.86894352577));
#30981=CARTESIAN_POINT('Ctrl Pts',(158.71901995723,2.8412335358318,126.789815181609));
#30982=CARTESIAN_POINT('Ctrl Pts',(158.711262916345,2.72953950568233,126.710765428835));
#30983=CARTESIAN_POINT('Ctrl Pts',(158.70350587546,2.61442720113072,126.636297966818));
#30984=CARTESIAN_POINT('Ctrl Pts',(158.695748834575,2.4963110391717,126.566718082121));
#30985=CARTESIAN_POINT('Ctrl Pts',(158.687997643335,2.37828394952865,126.497190668156));
#30986=CARTESIAN_POINT('Ctrl Pts',(158.680246452095,2.2572578467844,126.432543692865));
#30987=CARTESIAN_POINT('Ctrl Pts',(158.672495260855,2.13367637397629,126.373039348053));
#30988=CARTESIAN_POINT('Ctrl Pts',(158.664747364078,2.01014742659118,126.313560294176));
#30989=CARTESIAN_POINT('Ctrl Pts',(158.656999467301,1.88406562083364,126.259219692735));
#30990=CARTESIAN_POINT('Ctrl Pts',(158.649251570524,1.7558992673692,126.210233842503));
#30991=CARTESIAN_POINT('Ctrl Pts',(158.64150529444,1.62775972354296,126.161258239055));
#30992=CARTESIAN_POINT('Ctrl Pts',(158.633759018356,1.49753686429052,126.117635298371));
#30993=CARTESIAN_POINT('Ctrl Pts',(158.626012742271,1.36571868036245,126.079533049431));
#30994=CARTESIAN_POINT('Ctrl Pts',(158.618266409006,1.23389952338227,126.041430519228));
#30995=CARTESIAN_POINT('Ctrl Pts',(158.610520075741,1.10048539381718,126.008848870652));
#30996=CARTESIAN_POINT('Ctrl Pts',(158.602773742475,0.965978745918657,125.981906042878));
#30997=CARTESIAN_POINT('Ctrl Pts',(158.595025674472,0.831441976189031,125.954957181444));
#30998=CARTESIAN_POINT('Ctrl Pts',(158.587277606469,0.695812584553893,125.933649730362));
#30999=CARTESIAN_POINT('Ctrl Pts',(158.579529538466,0.559602105004731,125.918050297235));
#31000=CARTESIAN_POINT('Ctrl Pts',(158.571773235725,0.423246859336932,125.902434284845));
#31001=CARTESIAN_POINT('Ctrl Pts',(158.564016932983,0.286309681103846,125.892538453551));
#31002=CARTESIAN_POINT('Ctrl Pts',(158.556260630241,0.149306659662162,125.888377441854));
#31003=CARTESIAN_POINT('Ctrl Pts',(158.548500187727,0.0122305155829474,
125.8842142093));
#31004=CARTESIAN_POINT('Ctrl Pts',(158.540739745212,-0.124911150981226,
125.885791890843));
#31005=CARTESIAN_POINT('Ctrl Pts',(158.532979302698,-0.261604377988794,
125.893072984784));
#31006=CARTESIAN_POINT('Ctrl Pts',(158.525206402433,-0.398517037099548,
125.900365766984));
#31007=CARTESIAN_POINT('Ctrl Pts',(158.517433502167,-0.534979428690864,
125.913380220297));
#31008=CARTESIAN_POINT('Ctrl Pts',(158.509660601902,-0.670483925809493,
125.932027052658));
#31009=CARTESIAN_POINT('Ctrl Pts',(158.50217026614,-0.801062493141713,125.949996025694));
#31010=CARTESIAN_POINT('Ctrl Pts',(158.494679930378,-0.93075129743161,125.973194930771));
#31011=CARTESIAN_POINT('Ctrl Pts',(158.487189594616,-1.05910876979799,126.001499837131));
#31012=CARTESIAN_POINT('Ctrl Pts',(158.479415260497,-1.19233295474349,126.03087793262));
#31013=CARTESIAN_POINT('Ctrl Pts',(158.471640926378,-1.32454487415725,126.065849921659));
#31014=CARTESIAN_POINT('Ctrl Pts',(158.463866592259,-1.45523841972807,126.10633292456));
#31015=CARTESIAN_POINT('Ctrl Pts',(158.456101839312,-1.58577089718448,126.146766035778));
#31016=CARTESIAN_POINT('Ctrl Pts',(158.448337086364,-1.71478835417376,126.192696532566));
#31017=CARTESIAN_POINT('Ctrl Pts',(158.440572333417,-1.8417946460021,126.243990507097));
#31018=CARTESIAN_POINT('Ctrl Pts',(158.432815292532,-1.96867479339024,126.295233535729));
#31019=CARTESIAN_POINT('Ctrl Pts',(158.425058251647,-2.09354739059707,126.351829295509));
#31020=CARTESIAN_POINT('Ctrl Pts',(158.417301210762,-2.21593158888361,126.413594140527));
#31021=CARTESIAN_POINT('Ctrl Pts',(158.409550019522,-2.33822349629563,126.475312408196));
#31022=CARTESIAN_POINT('Ctrl Pts',(158.401798828282,-2.4580303922667,126.542191826837));
#31023=CARTESIAN_POINT('Ctrl Pts',(158.394047637042,-2.57489188750593,126.614000868075));
#31024=CARTESIAN_POINT('Ctrl Pts',(158.386299740265,-2.69170371349151,126.685779388554));
#31025=CARTESIAN_POINT('Ctrl Pts',(158.378551843488,-2.80557229622117,126.762483160139));
#31026=CARTESIAN_POINT('Ctrl Pts',(158.370803946711,-2.91606252405755,126.843835094572));
#31027=CARTESIAN_POINT('Ctrl Pts',(158.363057670626,-3.02652963972008,126.925170011934));
#31028=CARTESIAN_POINT('Ctrl Pts',(158.355311394542,-3.13361949147905,127.011150926538));
#31029=CARTESIAN_POINT('Ctrl Pts',(158.347565118458,-3.23692694087578,127.10145810171));
#31030=CARTESIAN_POINT('Ctrl Pts',(158.339818785193,-3.3402351528646,127.191765943509));
#31031=CARTESIAN_POINT('Ctrl Pts',(158.332072451928,-3.43976061242328,127.28639985229));
#31032=CARTESIAN_POINT('Ctrl Pts',(158.324326118662,-3.53513250518679,127.385000848066));
#31033=CARTESIAN_POINT('Ctrl Pts',(158.316578050659,-3.63052575582409,127.483623924852));
#31034=CARTESIAN_POINT('Ctrl Pts',(158.308829982656,-3.7217633169883,127.586215575485));
#31035=CARTESIAN_POINT('Ctrl Pts',(158.301081914653,-3.8085126531988,127.692381434968));
#31036=CARTESIAN_POINT('Ctrl Pts',(158.293325611912,-3.89535418763626,127.79866012879));
#31037=CARTESIAN_POINT('Ctrl Pts',(158.28556930917,-3.97769772047951,127.908520316566));
#31038=CARTESIAN_POINT('Ctrl Pts',(158.277813006428,-4.05525197703981,128.021535710172));
#31039=CARTESIAN_POINT('Ctrl Pts',(158.270052563914,-4.13284762664232,128.134611423496));
#31040=CARTESIAN_POINT('Ctrl Pts',(158.2622921214,-4.20564869912791,128.250845367041));
#31041=CARTESIAN_POINT('Ctrl Pts',(158.254531678885,-4.27340893669931,128.369784859402));
#31042=CARTESIAN_POINT('Ctrl Pts',(158.24675877862,-4.34127794901937,128.488915283995));
#31043=CARTESIAN_POINT('Ctrl Pts',(158.238985878355,-4.404089776793,128.610759588768));
#31044=CARTESIAN_POINT('Ctrl Pts',(158.231212978089,-4.46164515919564,128.734842428246));
#31045=CARTESIAN_POINT('Ctrl Pts',(158.223722642327,-4.51710825847412,128.854414543962));
#31046=CARTESIAN_POINT('Ctrl Pts',(158.216232306565,-4.56769032914941,128.976064982847));
#31047=CARTESIAN_POINT('Ctrl Pts',(158.208741970803,-4.61325695891121,129.099355252895));
#31048=CARTESIAN_POINT('Ctrl Pts',(158.199766254412,-4.6678597375636,129.247094757892));
#31049=CARTESIAN_POINT('Ctrl Pts',(158.190790538021,-4.71540475201521,129.39757591567));
#31050=CARTESIAN_POINT('Ctrl Pts',(158.18181482163,-4.75564619449548,129.55016273235));
#31051=CARTESIAN_POINT('Ctrl Pts',(158.181181561314,-4.75848533373057,129.560928132179));
#31052=CARTESIAN_POINT('Ctrl Pts',(158.180548300999,-4.76128813747417,129.571704003721));
#31053=CARTESIAN_POINT('Ctrl Pts',(158.179915040683,-4.76405452823403,129.582490119308));
#31054=CARTESIAN_POINT('Origin',(213.235140564004,0.,130.804360617566));
#31055=CARTESIAN_POINT('',(156.084992794976,-4.76405452823404,129.582490119308));
#31056=CARTESIAN_POINT('',(156.429992618608,-4.76405452823404,129.582490119308));
#31057=CARTESIAN_POINT('',(213.235140564004,-4.76405452823405,129.582490119308));
#31058=CARTESIAN_POINT('',(157.764859435939,-4.9182485252746,130.8081693095));
#31059=CARTESIAN_POINT('Ctrl Pts',(157.764859435939,-4.9182485252746,130.8081693095));
#31060=CARTESIAN_POINT('Ctrl Pts',(157.755849159831,-4.91812493258219,130.967767299479));
#31061=CARTESIAN_POINT('Ctrl Pts',(157.746838883724,-4.91022897793391,131.127042622001));
#31062=CARTESIAN_POINT('Ctrl Pts',(157.737828607616,-4.89467815940805,131.285306330005));
#31063=CARTESIAN_POINT('Ctrl Pts',(157.728765898902,-4.87903684754533,131.444491006319));
#31064=CARTESIAN_POINT('Ctrl Pts',(157.719703190188,-4.85565143099362,131.602652156559));
#31065=CARTESIAN_POINT('Ctrl Pts',(157.710640481474,-4.8246906293771,131.759108434165));
#31066=CARTESIAN_POINT('Ctrl Pts',(157.701515594764,-4.79351740996534,131.916638136741));
#31067=CARTESIAN_POINT('Ctrl Pts',(157.692390708053,-4.75466458056885,132.072439391437));
#31068=CARTESIAN_POINT('Ctrl Pts',(157.683265821343,-4.70835263847484,132.225838191876));
#31069=CARTESIAN_POINT('Ctrl Pts',(157.679322454008,-4.68833869139834,132.292130282745));
#31070=CARTESIAN_POINT('Ctrl Pts',(157.675379086672,-4.66693229571562,132.357973975118));
#31071=CARTESIAN_POINT('Ctrl Pts',(157.671435719337,-4.64415395773542,132.423316169566));
#31072=CARTESIAN_POINT('Ctrl Pts',(157.663661385218,-4.59924654864364,132.552138064279));
#31073=CARTESIAN_POINT('Ctrl Pts',(157.655887051098,-4.54890395692894,132.679294090923));
#31074=CARTESIAN_POINT('Ctrl Pts',(157.648112716979,-4.49326825799374,132.804291472422));
#31075=CARTESIAN_POINT('Ctrl Pts',(157.640347964032,-4.43770112508511,132.92913480582));
#31076=CARTESIAN_POINT('Ctrl Pts',(157.632583211085,-4.37685402179583,133.051824433599));
#31077=CARTESIAN_POINT('Ctrl Pts',(157.624818458138,-4.31091851771169,133.17188349943));
#31078=CARTESIAN_POINT('Ctrl Pts',(157.617061417253,-4.24504850169973,133.291823320905));
#31079=CARTESIAN_POINT('Ctrl Pts',(157.609304376368,-4.17410032930813,133.409137439376));
#31080=CARTESIAN_POINT('Ctrl Pts',(157.601547335483,-4.09831315348778,133.523370061913));
#31081=CARTESIAN_POINT('Ctrl Pts',(157.593796144243,-4.02258312936639,133.637516540741));
#31082=CARTESIAN_POINT('Ctrl Pts',(157.586044953003,-3.94202158045546,133.748585824509));
#31083=CARTESIAN_POINT('Ctrl Pts',(157.578293761763,-3.85691279058616,133.856148091869));
#31084=CARTESIAN_POINT('Ctrl Pts',(157.570545864986,-3.77184017422281,133.963664642397));
#31085=CARTESIAN_POINT('Ctrl Pts',(157.562797968209,-3.68222440297854,134.067676835203));
#31086=CARTESIAN_POINT('Ctrl Pts',(157.555050071432,-3.58839201616392,134.167785330687));
#31087=CARTESIAN_POINT('Ctrl Pts',(157.547303795347,-3.49457925706182,134.267872885631));
#31088=CARTESIAN_POINT('Ctrl Pts',(157.539557519263,-3.39655190398407,134.364058082384));
#31089=CARTESIAN_POINT('Ctrl Pts',(157.531811243179,-3.29467530605241,134.45597638188));
#31090=CARTESIAN_POINT('Ctrl Pts',(157.524064909914,-3.19279795609091,134.547895359897));
#31091=CARTESIAN_POINT('Ctrl Pts',(157.516318576649,-3.08707159485389,134.635547115904));
#31092=CARTESIAN_POINT('Ctrl Pts',(157.508572243383,-2.97789648612514,134.718605829663));
#31093=CARTESIAN_POINT('Ctrl Pts',(157.50082417538,-2.86869692838775,134.801683143845));
#31094=CARTESIAN_POINT('Ctrl Pts',(157.493076107377,-2.75604739741964,134.880165132349));
#31095=CARTESIAN_POINT('Ctrl Pts',(157.485328039374,-2.64037877327346,134.953768165174));
#31096=CARTESIAN_POINT('Ctrl Pts',(157.477571736632,-2.52458721513698,135.027449424178));
#31097=CARTESIAN_POINT('Ctrl Pts',(157.469815433891,-2.40577048441605,135.096241158857));
#31098=CARTESIAN_POINT('Ctrl Pts',(157.462059131149,-2.28438628758989,135.159904481605));
#31099=CARTESIAN_POINT('Ctrl Pts',(157.454298688635,-2.16293730436299,135.223601783386));
#31100=CARTESIAN_POINT('Ctrl Pts',(157.44653824612,-2.03891847788247,135.282165052296));
#31101=CARTESIAN_POINT('Ctrl Pts',(157.438777803606,-1.91280840628421,135.33540321981));
#31102=CARTESIAN_POINT('Ctrl Pts',(157.431004903341,-1.78649589160353,135.388726849956));
#31103=CARTESIAN_POINT('Ctrl Pts',(157.423232003075,-1.65808578978925,135.436708159504));
#31104=CARTESIAN_POINT('Ctrl Pts',(157.41545910281,-1.52807365366,135.479205424775));
#31105=CARTESIAN_POINT('Ctrl Pts',(157.407968767048,-1.40278778615982,135.52015780741));
#31106=CARTESIAN_POINT('Ctrl Pts',(157.400478431286,-1.27601463450529,135.556017857252));
#31107=CARTESIAN_POINT('Ctrl Pts',(157.392988095524,-1.14820549682072,135.586703892528));
#31108=CARTESIAN_POINT('Ctrl Pts',(157.385213761405,-1.01555043683414,135.618553398157));
#31109=CARTESIAN_POINT('Ctrl Pts',(157.377439427286,-0.881359069864842,
135.644929688331));
#31110=CARTESIAN_POINT('Ctrl Pts',(157.369665093167,-0.746122778447592,
135.665685937063));
#31111=CARTESIAN_POINT('Ctrl Pts',(157.36190034022,-0.6110531536731,135.686416605573));
#31112=CARTESIAN_POINT('Ctrl Pts',(157.354135587273,-0.474941549471379,
135.701540954972));
#31113=CARTESIAN_POINT('Ctrl Pts',(157.346370834325,-0.338292706616414,
135.710962405683));
#31114=CARTESIAN_POINT('Ctrl Pts',(157.33861379344,-0.201779585318584,135.720374498876));
#31115=CARTESIAN_POINT('Ctrl Pts',(157.330856752555,-0.064730674756998,
135.724094938677));
#31116=CARTESIAN_POINT('Ctrl Pts',(157.32309971167,0.0723412855547204,135.722078564023));
#31117=CARTESIAN_POINT('Ctrl Pts',(157.31534852043,0.209309878834764,135.720063709933));
#31118=CARTESIAN_POINT('Ctrl Pts',(157.30759732919,0.346301097925988,135.712320658107));
#31119=CARTESIAN_POINT('Ctrl Pts',(157.29984613795,0.482799659600159,135.698856255647));
#31120=CARTESIAN_POINT('Ctrl Pts',(157.292098241173,0.61924020574454,135.685397575916));
#31121=CARTESIAN_POINT('Ctrl Pts',(157.284350344396,0.755188122675336,135.666222420369));
#31122=CARTESIAN_POINT('Ctrl Pts',(157.276602447619,0.890130932202471,135.641389662965));
#31123=CARTESIAN_POINT('Ctrl Pts',(157.268856171535,1.02504551460288,135.616562100039));
#31124=CARTESIAN_POINT('Ctrl Pts',(157.261109895451,1.15895502352692,135.586079359915));
#31125=CARTESIAN_POINT('Ctrl Pts',(157.253363619366,1.29135528181109,135.550051778887));
#31126=CARTESIAN_POINT('Ctrl Pts',(157.245617286101,1.42375651744388,135.514023931911));
#31127=CARTESIAN_POINT('Ctrl Pts',(157.237870952836,1.55464810295783,135.472451265011));
#31128=CARTESIAN_POINT('Ctrl Pts',(157.23012461957,1.68353956420689,135.425494417647));
#31129=CARTESIAN_POINT('Ctrl Pts',(157.222376551567,1.8124598898049,135.378527054622));
#31130=CARTESIAN_POINT('Ctrl Pts',(157.214628483564,1.93937883256479,135.326173245634));
#31131=CARTESIAN_POINT('Ctrl Pts',(157.206880415561,2.06382486534054,135.26864219333));
#31132=CARTESIAN_POINT('Ctrl Pts',(157.19912411282,2.18840316084093,135.211049996338));
#31133=CARTESIAN_POINT('Ctrl Pts',(157.191367810078,2.31050294072448,135.148269728644));
#31134=CARTESIAN_POINT('Ctrl Pts',(157.183611507336,2.42967582054979,135.080557347083));
#31135=CARTESIAN_POINT('Ctrl Pts',(157.175851064822,2.54891230652936,135.012808825386));
#31136=CARTESIAN_POINT('Ctrl Pts',(157.168090622308,2.66521844830249,134.940123151606));
#31137=CARTESIAN_POINT('Ctrl Pts',(157.160330179793,2.77817480052365,134.862799706703));
#31138=CARTESIAN_POINT('Ctrl Pts',(157.152557279528,2.89131248030919,134.785352135342));
#31139=CARTESIAN_POINT('Ctrl Pts',(157.144784379263,3.00108931155435,134.703252149742));
#31140=CARTESIAN_POINT('Ctrl Pts',(157.137011478997,3.10711819971322,134.616840067414));
#31141=CARTESIAN_POINT('Ctrl Pts',(157.129521143235,3.2092926707166,134.533569281937));
#31142=CARTESIAN_POINT('Ctrl Pts',(157.122030807473,3.30798673133394,134.446294671919));
#31143=CARTESIAN_POINT('Ctrl Pts',(157.114540471711,3.40288772271461,134.355351776257));
#31144=CARTESIAN_POINT('Ctrl Pts',(157.106766137592,3.50138691402832,134.260960753063));
#31145=CARTESIAN_POINT('Ctrl Pts',(157.098991803473,3.59611174562021,134.162318784651));
#31146=CARTESIAN_POINT('Ctrl Pts',(157.091217469354,3.6866730843672,134.05975992203));
#31147=CARTESIAN_POINT('Ctrl Pts',(157.083452716407,3.77712281435786,133.957327454041));
#31148=CARTESIAN_POINT('Ctrl Pts',(157.07568796346,3.86341900463223,133.850987986828));
#31149=CARTESIAN_POINT('Ctrl Pts',(157.067923210513,3.94520757534147,133.741113969478));
#31150=CARTESIAN_POINT('Ctrl Pts',(157.060166169628,4.02691491248923,133.631349080552));
#31151=CARTESIAN_POINT('Ctrl Pts',(157.052409128742,4.10412330762623,133.518056939259));
#31152=CARTESIAN_POINT('Ctrl Pts',(157.044652087857,4.17651761724043,133.401644517216));
#31153=CARTESIAN_POINT('Ctrl Pts',(157.036900896617,4.2488573337426,133.285319882686));
#31154=CARTESIAN_POINT('Ctrl Pts',(157.029149705377,4.31638998506244,133.165879981625));
#31155=CARTESIAN_POINT('Ctrl Pts',(157.021398514137,4.37884280868842,133.043762037432));
#31156=CARTESIAN_POINT('Ctrl Pts',(157.01365061736,4.44126908819839,132.921695996623));
#31157=CARTESIAN_POINT('Ctrl Pts',(157.005902720583,4.49861965658127,132.796954523911));
#31158=CARTESIAN_POINT('Ctrl Pts',(156.998154823806,4.5506670391882,132.670000604527));
#31159=CARTESIAN_POINT('Ctrl Pts',(156.990408547722,4.6027035346047,132.543073241165));
#31160=CARTESIAN_POINT('Ctrl Pts',(156.982662271638,4.64943890251702,132.413934713173));
#31161=CARTESIAN_POINT('Ctrl Pts',(156.974915995553,4.69069345190272,132.28306883854));
#31162=CARTESIAN_POINT('Ctrl Pts',(156.967169662288,4.73194830582011,132.152201997885));
#31163=CARTESIAN_POINT('Ctrl Pts',(156.959423329023,4.76772214293298,132.019608158022));
#31164=CARTESIAN_POINT('Ctrl Pts',(156.951676995757,4.79788500051228,131.885786798292));
#31165=CARTESIAN_POINT('Ctrl Pts',(156.943928927754,4.8280546128544,131.751935470196));
#31166=CARTESIAN_POINT('Ctrl Pts',(156.936180859751,4.8526106593448,131.61685645655));
#31167=CARTESIAN_POINT('Ctrl Pts',(156.928432791748,4.87147427615589,131.481059545636));
#31168=CARTESIAN_POINT('Ctrl Pts',(156.920676489007,4.89035794144341,131.34511830815));
#31169=CARTESIAN_POINT('Ctrl Pts',(156.912920186265,4.90353703768245,131.208458037106));
#31170=CARTESIAN_POINT('Ctrl Pts',(156.905163883523,4.91098454586627,131.071594321957));
#31171=CARTESIAN_POINT('Ctrl Pts',(156.897403441009,4.91843602900945,130.934657558523));
#31172=CARTESIAN_POINT('Ctrl Pts',(156.889642998495,4.92014982365658,130.797517525363));
#31173=CARTESIAN_POINT('Ctrl Pts',(156.88188255598,4.91615108703395,130.660688936449));
#31174=CARTESIAN_POINT('Ctrl Pts',(156.874109655715,4.91214593128431,130.523640698137));
#31175=CARTESIAN_POINT('Ctrl Pts',(156.866336755449,4.90240994694233,130.386905293349));
#31176=CARTESIAN_POINT('Ctrl Pts',(156.858563855184,4.88702021871189,130.250992345616));
#31177=CARTESIAN_POINT('Ctrl Pts',(156.851073519422,4.87218994586699,130.120020175877));
#31178=CARTESIAN_POINT('Ctrl Pts',(156.84358318366,4.8521098952129,129.989812009002));
#31179=CARTESIAN_POINT('Ctrl Pts',(156.836092847898,4.82689336538216,129.860812260708));
#31180=CARTESIAN_POINT('Ctrl Pts',(156.828318513779,4.80072074315854,129.726921447749));
#31181=CARTESIAN_POINT('Ctrl Pts',(156.82054417966,4.76893154670519,129.593908370793));
#31182=CARTESIAN_POINT('Ctrl Pts',(156.812769845541,4.73159648664064,129.462280981289));
#31183=CARTESIAN_POINT('Ctrl Pts',(156.805005092594,4.69430743870088,129.330815810778));
#31184=CARTESIAN_POINT('Ctrl Pts',(156.797240339646,4.6514862319889,129.200733302351));
#31185=CARTESIAN_POINT('Ctrl Pts',(156.789475586699,4.60325482966432,129.072532671241));
#31186=CARTESIAN_POINT('Ctrl Pts',(156.781718545814,4.55507133144848,128.944459370806));
#31187=CARTESIAN_POINT('Ctrl Pts',(156.773961504929,4.50148846786972,128.818264591638));
#31188=CARTESIAN_POINT('Ctrl Pts',(156.766204464044,4.44267829290953,128.694433451001));
#31189=CARTESIAN_POINT('Ctrl Pts',(156.758453272804,4.38391246715974,128.57069569239));
#31190=CARTESIAN_POINT('Ctrl Pts',(156.750702081564,4.31992734329849,128.449318376205));
#31191=CARTESIAN_POINT('Ctrl Pts',(156.742950890324,4.25094333495383,128.3307673152));
#31192=CARTESIAN_POINT('Ctrl Pts',(156.735202993547,4.18198864665293,128.212266641558));
#31193=CARTESIAN_POINT('Ctrl Pts',(156.72745509677,4.10803949587497,128.096590171144));
#31194=CARTESIAN_POINT('Ctrl Pts',(156.719707199993,4.02936244960184,127.984179539649));
#31195=CARTESIAN_POINT('Ctrl Pts',(156.711960923909,3.95070186087074,127.871792422035));
#31196=CARTESIAN_POINT('Ctrl Pts',(156.704214647824,3.86731556780952,127.762670104633));
#31197=CARTESIAN_POINT('Ctrl Pts',(156.69646837174,3.77951349280804,127.65722528203));
#31198=CARTESIAN_POINT('Ctrl Pts',(156.688722038475,3.69171076967156,127.551779681056));
#31199=CARTESIAN_POINT('Ctrl Pts',(156.68097570521,3.5994924497257,127.450011929495));
#31200=CARTESIAN_POINT('Ctrl Pts',(156.673229371944,3.50320851105733,127.352301349454));
#31201=CARTESIAN_POINT('Ctrl Pts',(156.665481303941,3.40690301026851,127.254568887807));
#31202=CARTESIAN_POINT('Ctrl Pts',(156.657733235938,3.30653035339417,127.160895684067));
#31203=CARTESIAN_POINT('Ctrl Pts',(156.649985167935,3.20247681193,127.071623641626));
#31204=CARTESIAN_POINT('Ctrl Pts',(156.642228865193,3.09831268112366,126.982256719796));
#31205=CARTESIAN_POINT('Ctrl Pts',(156.634472562452,2.99046014810908,126.897300558266));
#31206=CARTESIAN_POINT('Ctrl Pts',(156.62671625971,2.8793383884614,126.817056577587));
#31207=CARTESIAN_POINT('Ctrl Pts',(156.618955817196,2.76815731978472,126.736769768279));
#31208=CARTESIAN_POINT('Ctrl Pts',(156.611195374681,2.65370387374858,126.661200366551));
#31209=CARTESIAN_POINT('Ctrl Pts',(156.603434932167,2.53642469188915,126.59060542239));
#31210=CARTESIAN_POINT('Ctrl Pts',(156.595662031902,2.41895724307548,126.519897152957));
#31211=CARTESIAN_POINT('Ctrl Pts',(156.587889131636,2.29865533712734,126.454179486085));
#31212=CARTESIAN_POINT('Ctrl Pts',(156.580116231371,2.17598940092134,126.393663032197));
#31213=CARTESIAN_POINT('Ctrl Pts',(156.572625895609,2.05778268047426,126.33534650384));
#31214=CARTESIAN_POINT('Ctrl Pts',(156.565135559847,1.93738110413567,126.281859724446));
#31215=CARTESIAN_POINT('Ctrl Pts',(156.557645224085,1.81521981211289,126.233347590215));
#31216=CARTESIAN_POINT('Ctrl Pts',(156.549870889966,1.688426737572,126.18299610367));
#31217=CARTESIAN_POINT('Ctrl Pts',(156.542096555847,1.55933623162569,126.137844437843));
#31218=CARTESIAN_POINT('Ctrl Pts',(156.534322221728,1.42841386903006,126.098107662054));
#31219=CARTESIAN_POINT('Ctrl Pts',(156.526557468781,1.2976528565455,126.05841985829));
#31220=CARTESIAN_POINT('Ctrl Pts',(156.518792715834,1.16506484988346,126.02413377901));
#31221=CARTESIAN_POINT('Ctrl Pts',(156.511027962886,1.03113577702658,125.99541665118));
#31222=CARTESIAN_POINT('Ctrl Pts',(156.503270922001,0.897339724412969,125.966728045607));
#31223=CARTESIAN_POINT('Ctrl Pts',(156.495513881116,0.762205636079137,125.943597465663));
#31224=CARTESIAN_POINT('Ctrl Pts',(156.487756840231,0.62623465429642,125.926142375189));
#31225=CARTESIAN_POINT('Ctrl Pts',(156.480005648991,0.490366209288719,125.908700447735));
#31226=CARTESIAN_POINT('Ctrl Pts',(156.472254457751,0.35366251322796,125.896925540389));
#31227=CARTESIAN_POINT('Ctrl Pts',(156.464503266511,0.21663460652543,125.890883996094));
#31228=CARTESIAN_POINT('Ctrl Pts',(156.456755369734,0.0796649403385415,
125.884845019616));
#31229=CARTESIAN_POINT('Ctrl Pts',(156.449007472957,-0.0576282726520325,
125.884534576701));
#31230=CARTESIAN_POINT('Ctrl Pts',(156.44125957618,-0.194729385867471,125.889967111875));
#31231=CARTESIAN_POINT('Ctrl Pts',(156.433513300096,-0.331801820485583,
125.895398510679));
#31232=CARTESIAN_POINT('Ctrl Pts',(156.425767024012,-0.468681844843868,
125.906570482638));
#31233=CARTESIAN_POINT('Ctrl Pts',(156.418020747927,-0.604854726675913,
125.92344535277));
#31234=CARTESIAN_POINT('Ctrl Pts',(156.410274414662,-0.741028613705098,
125.940320347469));
#31235=CARTESIAN_POINT('Ctrl Pts',(156.402528081397,-0.876494959794615,
125.962898276263));
#31236=CARTESIAN_POINT('Ctrl Pts',(156.394781748131,-1.01074545880611,125.991089725542));
#31237=CARTESIAN_POINT('Ctrl Pts',(156.387033680128,-1.14502602228603,126.019287488101));
#31238=CARTESIAN_POINT('Ctrl Pts',(156.379285612125,-1.27808981433431,126.053101192314));
#31239=CARTESIAN_POINT('Ctrl Pts',(156.371537544122,-1.40944039276611,126.092390664167));
#31240=CARTESIAN_POINT('Ctrl Pts',(156.363781241381,-1.54093057215585,126.131721893338));
#31241=CARTESIAN_POINT('Ctrl Pts',(156.356024938639,-1.67070352547269,126.176540403429));
#31242=CARTESIAN_POINT('Ctrl Pts',(156.348268635897,-1.79827908443529,126.226656455327));
#31243=CARTESIAN_POINT('Ctrl Pts',(156.340508193383,-1.92592273431503,126.27679925567));
#31244=CARTESIAN_POINT('Ctrl Pts',(156.332747750869,-2.05136629548881,126.332245073791));
#31245=CARTESIAN_POINT('Ctrl Pts',(156.324987308354,-2.17415208386269,126.392757079312));
#31246=CARTESIAN_POINT('Ctrl Pts',(156.317214408089,-2.29713497888443,126.453366224076));
#31247=CARTESIAN_POINT('Ctrl Pts',(156.309441507823,-2.41745123194715,126.519057620489));
#31248=CARTESIAN_POINT('Ctrl Pts',(156.301668607558,-2.53466937331946,126.589549325176));
#31249=CARTESIAN_POINT('Ctrl Pts',(156.294178271796,-2.64762633999865,126.65747847884));
#31250=CARTESIAN_POINT('Ctrl Pts',(156.286687936034,-2.75770627531209,126.729864824214));
#31251=CARTESIAN_POINT('Ctrl Pts',(156.279197600272,-2.8645520700704,126.806420585455));
#31252=CARTESIAN_POINT('Ctrl Pts',(156.271105733385,-2.97997839755708,126.88912435857));
#31253=CARTESIAN_POINT('Ctrl Pts',(156.263013866497,-3.09202648001146,126.976979076286));
#31254=CARTESIAN_POINT('Ctrl Pts',(156.25492199961,-3.200202032726,127.069673212677));
#31255=CARTESIAN_POINT('Ctrl Pts',(156.247218857282,-3.30318094853596,127.15791442271));
#31256=CARTESIAN_POINT('Ctrl Pts',(156.239515714955,-3.40265032657603,127.250540669921));
#31257=CARTESIAN_POINT('Ctrl Pts',(156.231812572627,-3.49821192172148,127.34723805491));
#31258=CARTESIAN_POINT('Ctrl Pts',(156.224116381523,-3.59368728322783,127.443848181337));
#31259=CARTESIAN_POINT('Ctrl Pts',(156.216420190418,-3.68526159703673,127.544521858844));
#31260=CARTESIAN_POINT('Ctrl Pts',(156.208723999314,-3.77257014628933,127.64890541208));
#31261=CARTESIAN_POINT('Ctrl Pts',(156.201033021136,-3.859819558099,127.753218262316));
#31262=CARTESIAN_POINT('Ctrl Pts',(156.193342042959,-3.94280869879852,127.861235685983));
#31263=CARTESIAN_POINT('Ctrl Pts',(156.185651064781,-4.02121049843016,127.972568042215));
#31264=CARTESIAN_POINT('Ctrl Pts',(156.177963565501,-4.09957683419471,128.083850038941));
#31265=CARTESIAN_POINT('Ctrl Pts',(156.170276066221,-4.1733597297056,128.19844365986));
#31266=CARTESIAN_POINT('Ctrl Pts',(156.162588566941,-4.242273434718,128.315927542801));
#31267=CARTESIAN_POINT('Ctrl Pts',(156.154901463274,-4.311183593297,128.433405379792));
#31268=CARTESIAN_POINT('Ctrl Pts',(156.147214359608,-4.37522485144858,128.553772844428));
#31269=CARTESIAN_POINT('Ctrl Pts',(156.139527255941,-4.43415583624978,128.676581239352));
#31270=CARTESIAN_POINT('Ctrl Pts',(156.131840359425,-4.49308523299093,128.799386324861));
#31271=CARTESIAN_POINT('Ctrl Pts',(156.12415346291,-4.54690446386079,128.924631848696));
#31272=CARTESIAN_POINT('Ctrl Pts',(156.116466566394,-4.59541935318012,129.051846985403));
#31273=CARTESIAN_POINT('Ctrl Pts',(156.108776075186,-4.6439569299483,129.179121612854));
#31274=CARTESIAN_POINT('Ctrl Pts',(156.101085583978,-4.68718507680773,129.308367318422));
#31275=CARTESIAN_POINT('Ctrl Pts',(156.093395092771,-4.72495878294843,129.439095968519));
#31276=CARTESIAN_POINT('Ctrl Pts',(156.090594326839,-4.73871542168699,129.486705456596));
#31277=CARTESIAN_POINT('Ctrl Pts',(156.087793560907,-4.75174911450255,129.53451149793));
#31278=CARTESIAN_POINT('Ctrl Pts',(156.084992794976,-4.76405452823404,129.582490119308));
#31279=CARTESIAN_POINT('Ctrl Pts',(157.83474697768,-4.76405452823405,129.582490119308));
#31280=CARTESIAN_POINT('Ctrl Pts',(157.827003930467,-4.79813988220165,129.71538839711));
#31281=CARTESIAN_POINT('Ctrl Pts',(157.819260883253,-4.82667131339279,129.84975804506));
#31282=CARTESIAN_POINT('Ctrl Pts',(157.81151783604,-4.84953480182535,129.98509553935));
#31283=CARTESIAN_POINT('Ctrl Pts',(157.803741436032,-4.87249677360888,130.121015993234));
#31284=CARTESIAN_POINT('Ctrl Pts',(157.795965036024,-4.8897417613054,130.2579122657));
#31285=CARTESIAN_POINT('Ctrl Pts',(157.788188636015,-4.90120637170618,130.395265073167));
#31286=CARTESIAN_POINT('Ctrl Pts',(157.780412236007,-4.91267098210696,130.532617880635));
#31287=CARTESIAN_POINT('Ctrl Pts',(157.772635835999,-4.91835519303655,130.670426824793));
#31288=CARTESIAN_POINT('Ctrl Pts',(157.764859435991,-4.91824852527531,130.808169308574));
#31289=CARTESIAN_POINT('',(158.110140564063,-4.91824875213615,130.800857103449));
#31290=CARTESIAN_POINT('Ctrl Pts',(158.179915040683,-4.76405452823403,129.582490119308));
#31291=CARTESIAN_POINT('Ctrl Pts',(158.170991527053,-4.80303679988543,129.734481404838));
#31292=CARTESIAN_POINT('Ctrl Pts',(158.162068013422,-4.83478472549672,129.888508569464));
#31293=CARTESIAN_POINT('Ctrl Pts',(158.153144499792,-4.8591067013772,130.043923159828));
#31294=CARTESIAN_POINT('Ctrl Pts',(158.14428513534,-4.88325383191697,130.198220508848));
#31295=CARTESIAN_POINT('Ctrl Pts',(158.135425770889,-4.90008131355361,130.353885259974));
#31296=CARTESIAN_POINT('Ctrl Pts',(158.126566406437,-4.90944903895876,130.51026336092));
#31297=CARTESIAN_POINT('Ctrl Pts',(158.121091125646,-4.91523849792619,130.606908443869));
#31298=CARTESIAN_POINT('Ctrl Pts',(158.115615844854,-4.9181796317636,130.703825615994));
#31299=CARTESIAN_POINT('Ctrl Pts',(158.110140564063,-4.91824875213615,130.800857103449));
#31300=CARTESIAN_POINT('Ctrl Pts',(158.110140564008,-4.91824875213684,130.800857104418));
#31301=CARTESIAN_POINT('Ctrl Pts',(158.102369830278,-4.91834685045954,130.93856800569));
#31302=CARTESIAN_POINT('Ctrl Pts',(158.094599096547,-4.91265677724765,131.076325466706));
#31303=CARTESIAN_POINT('Ctrl Pts',(158.086828362817,-4.90119353514655,131.213609922437));
#31304=CARTESIAN_POINT('Ctrl Pts',(158.079057967618,-4.88973079244064,131.350888397383));
#31305=CARTESIAN_POINT('Ctrl Pts',(158.071287572418,-4.87249541273953,131.487693522148));
#31306=CARTESIAN_POINT('Ctrl Pts',(158.063517177219,-4.84955438502098,131.623509767125));
#31307=CARTESIAN_POINT('Ctrl Pts',(158.055745478988,-4.82660951027941,131.759348787378));
#31308=CARTESIAN_POINT('Ctrl Pts',(158.047973780758,-4.79795714719638,131.894198215901));
#31309=CARTESIAN_POINT('Ctrl Pts',(158.040202082527,-4.76371555994939,132.027551987057));
#31310=CARTESIAN_POINT('Ctrl Pts',(158.032427439215,-4.72946099687106,132.160956292552));
#31311=CARTESIAN_POINT('Ctrl Pts',(158.024652795903,-4.68961308972873,132.292863437657));
#31312=CARTESIAN_POINT('Ctrl Pts',(158.016878152591,-4.6443400861399,132.422782140771));
#31313=CARTESIAN_POINT('Ctrl Pts',(158.009093984334,-4.59901161725824,132.552860011123));
#31314=CARTESIAN_POINT('Ctrl Pts',(158.001309816077,-4.54824490514241,132.680944208087));
#31315=CARTESIAN_POINT('Ctrl Pts',(157.993525647821,-4.49225675065279,132.806562492681));
#31316=CARTESIAN_POINT('Ctrl Pts',(157.985736342952,-4.43623165073384,132.932263670192));
#31317=CARTESIAN_POINT('Ctrl Pts',(157.977947038083,-4.37497841552365,133.05549534717));
#31318=CARTESIAN_POINT('Ctrl Pts',(157.970157733214,-4.30875957135957,133.17581038906));
#31319=CARTESIAN_POINT('Ctrl Pts',(157.96235569651,-4.24243249065822,133.296322089222));
#31320=CARTESIAN_POINT('Ctrl Pts',(157.954553659806,-4.17112378757189,133.413907300181));
#31321=CARTESIAN_POINT('Ctrl Pts',(157.946751623102,-4.09513946182071,133.528147659671));
#31322=CARTESIAN_POINT('Ctrl Pts',(157.941265864398,-4.04171345369319,133.608472204427));
#31323=CARTESIAN_POINT('Ctrl Pts',(157.935780105694,-3.98597681923433,133.687143779075));
#31324=CARTESIAN_POINT('Ctrl Pts',(157.93029434699,-3.92804737291623,133.764027304648));
#31325=CARTESIAN_POINT('Ctrl Pts',(157.922520012871,-3.84595063929811,133.872985472209));
#31326=CARTESIAN_POINT('Ctrl Pts',(157.914745678752,-3.7591869293676,133.978697771831));
#31327=CARTESIAN_POINT('Ctrl Pts',(157.906971344633,-3.66804199597895,134.080738339721));
#31328=CARTESIAN_POINT('Ctrl Pts',(157.899206591686,-3.57700939057493,134.182653151731));
#31329=CARTESIAN_POINT('Ctrl Pts',(157.891441838739,-3.48160656298945,134.280904946787));
#31330=CARTESIAN_POINT('Ctrl Pts',(157.883677085792,-3.38216153549143,134.37509813387));
#31331=CARTESIAN_POINT('Ctrl Pts',(157.875920044907,-3.28281527819636,134.469197766953));
#31332=CARTESIAN_POINT('Ctrl Pts',(157.868163004022,-3.17943509257304,134.55924654695));
#31333=CARTESIAN_POINT('Ctrl Pts',(157.860405963137,-3.07238788050573,134.644883469239));
#31334=CARTESIAN_POINT('Ctrl Pts',(157.852654771897,-2.9654213935741,134.730455812058));
#31335=CARTESIAN_POINT('Ctrl Pts',(157.844903580657,-2.85479368848489,134.811622676149));
#31336=CARTESIAN_POINT('Ctrl Pts',(157.837152389417,-2.74090671272816,134.888061568251));
#31337=CARTESIAN_POINT('Ctrl Pts',(157.829404492639,-2.62706814197413,134.964467971784));
#31338=CARTESIAN_POINT('Ctrl Pts',(157.821656595862,-2.50997337970784,135.036150182672));
#31339=CARTESIAN_POINT('Ctrl Pts',(157.813908699085,-2.39005530382696,135.102827635835));
#31340=CARTESIAN_POINT('Ctrl Pts',(157.806162423001,-2.2701623122223,135.169491141513));
#31341=CARTESIAN_POINT('Ctrl Pts',(157.798416146917,-2.14744752317223,135.23115178191));
#31342=CARTESIAN_POINT('Ctrl Pts',(157.790669870833,-2.02237014518254,135.287573980587));
#31343=CARTESIAN_POINT('Ctrl Pts',(157.782923537568,-1.89729184390009,135.343996595761));
#31344=CARTESIAN_POINT('Ctrl Pts',(157.775177204302,-1.76985127526052,135.395180531291));
#31345=CARTESIAN_POINT('Ctrl Pts',(157.767430871037,-1.6405290728496,135.440937741225));
#31346=CARTESIAN_POINT('Ctrl Pts',(157.759682803034,-1.5111779096282,135.486705198168));
#31347=CARTESIAN_POINT('Ctrl Pts',(157.751934735031,-1.37994464264407,135.527043380868));
#31348=CARTESIAN_POINT('Ctrl Pts',(157.744186667028,-1.24732617749561,135.561813767039));
#31349=CARTESIAN_POINT('Ctrl Pts',(157.736430364286,-1.11456676386411,135.596621107591));
#31350=CARTESIAN_POINT('Ctrl Pts',(157.728674061545,-0.980419589966094,
135.625848731418));
#31351=CARTESIAN_POINT('Ctrl Pts',(157.720917758803,-0.845393445290692,
135.649408913007));
#31352=CARTESIAN_POINT('Ctrl Pts',(157.713157316289,-0.71029523309618,135.672981669375));
#31353=CARTESIAN_POINT('Ctrl Pts',(157.705396873774,-0.574317502768465,
135.690880905169));
#31354=CARTESIAN_POINT('Ctrl Pts',(157.69763643126,-0.437974336912093,135.703070809311));
#31355=CARTESIAN_POINT('Ctrl Pts',(157.689863530995,-0.30141230090205,135.71528028177));
#31356=CARTESIAN_POINT('Ctrl Pts',(157.682090630729,-0.164484047843235,
135.721762089238));
#31357=CARTESIAN_POINT('Ctrl Pts',(157.674317730464,-0.0277047386209147,
135.722532585885));
#31358=CARTESIAN_POINT('Ctrl Pts',(157.666827394702,0.104102298185345,135.723275073038));
#31359=CARTESIAN_POINT('Ctrl Pts',(157.65933705894,0.235770724281695,135.718714291907));
#31360=CARTESIAN_POINT('Ctrl Pts',(157.651846723178,0.366845853006052,135.708910258729));
#31361=CARTESIAN_POINT('Ctrl Pts',(157.644072389059,0.502890735075081,135.698734502653));
#31362=CARTESIAN_POINT('Ctrl Pts',(157.63629805494,0.638727391214445,135.682877816325));
#31363=CARTESIAN_POINT('Ctrl Pts',(157.62852372082,0.77384307375465,135.661350421931));
#31364=CARTESIAN_POINT('Ctrl Pts',(157.620758967873,0.908792238291439,135.639849558126));
#31365=CARTESIAN_POINT('Ctrl Pts',(157.612994214926,1.04302181476096,135.612691952491));
#31366=CARTESIAN_POINT('Ctrl Pts',(157.605229461979,1.1760216771865,135.579939752842));
#31367=CARTESIAN_POINT('Ctrl Pts',(157.597472421094,1.30888944227443,135.54722008314));
#31368=CARTESIAN_POINT('Ctrl Pts',(157.589715380209,1.44052954673107,135.508916970248));
#31369=CARTESIAN_POINT('Ctrl Pts',(157.581958339324,1.57043994771253,135.465143967297));
#31370=CARTESIAN_POINT('Ctrl Pts',(157.574207148084,1.70025238224965,135.421403973907));
#31371=CARTESIAN_POINT('Ctrl Pts',(157.566455956844,1.82833734060721,135.372202425128));
#31372=CARTESIAN_POINT('Ctrl Pts',(157.558704765604,1.95420623763486,135.317703175282));
#31373=CARTESIAN_POINT('Ctrl Pts',(157.550956868827,2.0800216370236,135.26322708907));
#31374=CARTESIAN_POINT('Ctrl Pts',(157.543208972049,2.20362249039337,135.2034579352));
#31375=CARTESIAN_POINT('Ctrl Pts',(157.535461075272,2.32453876931873,135.138608253827));
#31376=CARTESIAN_POINT('Ctrl Pts',(157.527714799188,2.44542975516502,135.073772137609));
#31377=CARTESIAN_POINT('Ctrl Pts',(157.519968523104,2.56363693920783,135.003857792397));
#31378=CARTESIAN_POINT('Ctrl Pts',(157.51222224702,2.67871391090342,134.929124228494));
#31379=CARTESIAN_POINT('Ctrl Pts',(157.504475913755,2.79379173207135,134.854390112923));
#31380=CARTESIAN_POINT('Ctrl Pts',(157.496729580489,2.90573896689588,134.774836920613));
#31381=CARTESIAN_POINT('Ctrl Pts',(157.488983247224,3.01413761279812,134.690767378781));
#31382=CARTESIAN_POINT('Ctrl Pts',(157.481235179221,3.12256053382531,134.606679010157));
#31383=CARTESIAN_POINT('Ctrl Pts',(157.473487111218,3.22743297572324,134.518072518988));
#31384=CARTESIAN_POINT('Ctrl Pts',(157.465739043215,3.3283698061565,134.425291091348));
#31385=CARTESIAN_POINT('Ctrl Pts',(157.457982740473,3.42941391345437,134.332411054503));
#31386=CARTESIAN_POINT('Ctrl Pts',(157.450226437731,3.52651376536795,134.23534748246));
#31387=CARTESIAN_POINT('Ctrl Pts',(157.442470134989,3.61932054279237,134.134481016444));
#31388=CARTESIAN_POINT('Ctrl Pts',(157.434709692475,3.71217685398844,134.033560714958));
#31389=CARTESIAN_POINT('Ctrl Pts',(157.426949249961,3.80073527267693,133.928833773503));
#31390=CARTESIAN_POINT('Ctrl Pts',(157.419188807447,3.88468779578029,133.820713347572));
#31391=CARTESIAN_POINT('Ctrl Pts',(157.411415907181,3.96877508692653,133.712419357136));
#31392=CARTESIAN_POINT('Ctrl Pts',(157.403643006916,4.04824148056073,133.600721315091));
#31393=CARTESIAN_POINT('Ctrl Pts',(157.39587010665,4.1228222788664,133.486061480709));
#31394=CARTESIAN_POINT('Ctrl Pts',(157.388379770888,4.19469187729538,133.375569820118));
#31395=CARTESIAN_POINT('Ctrl Pts',(157.380889435126,4.2620247634462,133.262328230597));
#31396=CARTESIAN_POINT('Ctrl Pts',(157.373399099364,4.32462566143182,133.146751693152));
#31397=CARTESIAN_POINT('Ctrl Pts',(157.365624765245,4.38960009149224,133.026793036161));
#31398=CARTESIAN_POINT('Ctrl Pts',(157.357850431126,4.44968244283791,132.903938883975));
#31399=CARTESIAN_POINT('Ctrl Pts',(157.350076097007,4.50460416304322,132.778626151073));
#31400=CARTESIAN_POINT('Ctrl Pts',(157.34231134406,4.55945819713687,132.653467854915));
#31401=CARTESIAN_POINT('Ctrl Pts',(157.334546591113,4.60916409919449,132.525857361444));
#31402=CARTESIAN_POINT('Ctrl Pts',(157.326781838166,4.65349842038315,132.396257446507));
#31403=CARTESIAN_POINT('Ctrl Pts',(157.319024797281,4.69778870809917,132.266786252031));
#31404=CARTESIAN_POINT('Ctrl Pts',(157.311267756396,4.73671790636995,132.135329935787));
#31405=CARTESIAN_POINT('Ctrl Pts',(157.303510715511,4.77011018423933,132.002372258877));
#31406=CARTESIAN_POINT('Ctrl Pts',(157.295759524271,4.803477280732,131.869514846386));
#31407=CARTESIAN_POINT('Ctrl Pts',(157.288008333031,4.83131567292508,131.735158704436));
#31408=CARTESIAN_POINT('Ctrl Pts',(157.280257141791,4.85349912389242,131.599803460815));
#31409=CARTESIAN_POINT('Ctrl Pts',(157.272509245013,4.8756731463014,131.464505746782));
#31410=CARTESIAN_POINT('Ctrl Pts',(157.264761348236,4.89219694476504,131.328210160674));
#31411=CARTESIAN_POINT('Ctrl Pts',(157.257013451459,4.90299527349092,131.191427033864));
#31412=CARTESIAN_POINT('Ctrl Pts',(157.249267175375,4.91379134343922,131.054672519135));
#31413=CARTESIAN_POINT('Ctrl Pts',(157.241520899291,4.91886429508151,130.917431056058));
#31414=CARTESIAN_POINT('Ctrl Pts',(157.233774623207,4.91819074531745,130.780218223862));
#31415=CARTESIAN_POINT('Ctrl Pts',(157.226028289942,4.91751719058141,130.643004378793));
#31416=CARTESIAN_POINT('Ctrl Pts',(157.218281956676,4.91109705171341,130.505819555986));
#31417=CARTESIAN_POINT('Ctrl Pts',(157.210535623411,4.89895908109086,130.369179064306));
#31418=CARTESIAN_POINT('Ctrl Pts',(157.202787555408,4.88681839225398,130.232507972936));
#31419=CARTESIAN_POINT('Ctrl Pts',(157.195039487405,4.86895735826512,130.096381844615));
#31420=CARTESIAN_POINT('Ctrl Pts',(157.187291419402,4.84545653785333,129.961310202541));
#31421=CARTESIAN_POINT('Ctrl Pts',(157.17953511666,4.82193074048988,129.826095004717));
#31422=CARTESIAN_POINT('Ctrl Pts',(157.171778813919,4.79275325010191,129.691936917693));
#31423=CARTESIAN_POINT('Ctrl Pts',(157.164022511177,4.75805576568542,129.559335158739));
#31424=CARTESIAN_POINT('Ctrl Pts',(157.156262068662,4.72333976217676,129.426662626234));
#31425=CARTESIAN_POINT('Ctrl Pts',(157.148501626148,4.68309800877048,129.295548450532));
#31426=CARTESIAN_POINT('Ctrl Pts',(157.140741183634,4.63751162169754,129.166475083983));
#31427=CARTESIAN_POINT('Ctrl Pts',(157.132968283369,4.59185205530909,129.037194517407));
#31428=CARTESIAN_POINT('Ctrl Pts',(157.125195383103,4.54083085591796,128.909961669736));
#31429=CARTESIAN_POINT('Ctrl Pts',(157.117422482838,4.48467703313857,128.785238290678));
#31430=CARTESIAN_POINT('Ctrl Pts',(157.109932147076,4.43056454325988,128.665048920607));
#31431=CARTESIAN_POINT('Ctrl Pts',(157.102441811314,4.37168625648756,128.547190011304));
#31432=CARTESIAN_POINT('Ctrl Pts',(157.094951475552,4.30828575671004,128.432050161275));
#31433=CARTESIAN_POINT('Ctrl Pts',(157.087177141433,4.2424814077137,128.312544748836));
#31434=CARTESIAN_POINT('Ctrl Pts',(157.079402807314,4.17159670856506,128.195590094893));
#31435=CARTESIAN_POINT('Ctrl Pts',(157.071628473195,4.095854088642,128.081648303153));
#31436=CARTESIAN_POINT('Ctrl Pts',(157.063863720247,4.02020481472882,127.967846934489));
#31437=CARTESIAN_POINT('Ctrl Pts',(157.0560989673,3.93970974665174,127.857051362563));
#31438=CARTESIAN_POINT('Ctrl Pts',(157.048334214353,3.85463745128303,127.749699722857));
#31439=CARTESIAN_POINT('Ctrl Pts',(157.040577173468,3.76964965091695,127.642454706311));
#31440=CARTESIAN_POINT('Ctrl Pts',(157.032820132583,3.68009391158809,127.538647119345));
#31441=CARTESIAN_POINT('Ctrl Pts',(157.025063091698,3.58628219428691,127.438686378214));
#31442=CARTESIAN_POINT('Ctrl Pts',(157.017311900458,3.49254122113127,127.338801018254));
#31443=CARTESIAN_POINT('Ctrl Pts',(157.009560709218,3.39455092471505,127.242757013922));
#31444=CARTESIAN_POINT('Ctrl Pts',(157.001809517978,3.29266342190441,127.150930632942));
#31445=CARTESIAN_POINT('Ctrl Pts',(156.994061621201,3.19081922400085,127.059143280623));
#31446=CARTESIAN_POINT('Ctrl Pts',(156.986313724424,3.08508140400256,126.971570247501));
#31447=CARTESIAN_POINT('Ctrl Pts',(156.978565827646,2.97583864595741,126.888550686565));
#31448=CARTESIAN_POINT('Ctrl Pts',(156.970819551562,2.86661873914209,126.805548491531));
#31449=CARTESIAN_POINT('Ctrl Pts',(156.963073275478,2.75389566365159,126.727098110539));
#31450=CARTESIAN_POINT('Ctrl Pts',(156.955326999394,2.63809055175585,126.65349789962));
#31451=CARTESIAN_POINT('Ctrl Pts',(156.947580666129,2.52228458501323,126.579897145401));
#31452=CARTESIAN_POINT('Ctrl Pts',(156.939834332863,2.40339686643112,126.511146842406));
#31453=CARTESIAN_POINT('Ctrl Pts',(156.932087999598,2.28187648131301,126.447501337473));
#31454=CARTESIAN_POINT('Ctrl Pts',(156.924339931595,2.16032888254787,126.383841579572));
#31455=CARTESIAN_POINT('Ctrl Pts',(156.916591863592,2.0361477903483,126.325289075894));
#31456=CARTESIAN_POINT('Ctrl Pts',(156.908843795589,1.90980542497134,126.272051459835));
#31457=CARTESIAN_POINT('Ctrl Pts',(156.901087492847,1.78332878142448,126.218757262204));
#31458=CARTESIAN_POINT('Ctrl Pts',(156.893331190105,1.65468663700184,126.170789388187));
#31459=CARTESIAN_POINT('Ctrl Pts',(156.885574887364,1.52437018385685,126.128306874818));
#31460=CARTESIAN_POINT('Ctrl Pts',(156.877814444849,1.39398417689715,126.085801687253));
#31461=CARTESIAN_POINT('Ctrl Pts',(156.870054002335,1.26192245685782,126.048787799491));
#31462=CARTESIAN_POINT('Ctrl Pts',(156.862293559821,1.12868882231008,126.017373610597));
#31463=CARTESIAN_POINT('Ctrl Pts',(156.854520659556,0.995241309304005,125.985908992858));
#31464=CARTESIAN_POINT('Ctrl Pts',(156.84674775929,0.860618506603748,125.9600621109));
#31465=CARTESIAN_POINT('Ctrl Pts',(156.838974859025,0.725332682606731,125.939889879444));
#31466=CARTESIAN_POINT('Ctrl Pts',(156.831484523263,0.594964839077581,125.920450959413));
#31467=CARTESIAN_POINT('Ctrl Pts',(156.823994187501,0.463981648562595,125.906281310252));
#31468=CARTESIAN_POINT('Ctrl Pts',(156.816503851739,0.332841713031933,125.897386044923));
#31469=CARTESIAN_POINT('Ctrl Pts',(156.80872951762,0.196729566985446,125.888153512905));
#31470=CARTESIAN_POINT('Ctrl Pts',(156.800955183501,0.0600173929501631,
125.884573970625));
#31471=CARTESIAN_POINT('Ctrl Pts',(156.793180849382,-0.0767857996245379,
125.88671006029));
#31472=CARTESIAN_POINT('Ctrl Pts',(156.785416096435,-0.213420394490518,
125.888843517416));
#31473=CARTESIAN_POINT('Ctrl Pts',(156.777651343487,-0.350145397541858,
125.89667858497));
#31474=CARTESIAN_POINT('Ctrl Pts',(156.76988659054,-0.486447026036527,125.910226132965));
#31475=CARTESIAN_POINT('Ctrl Pts',(156.762129549655,-0.622613277832677,
125.923760225345));
#31476=CARTESIAN_POINT('Ctrl Pts',(156.75437250877,-0.758356605358593,125.942995468796));
#31477=CARTESIAN_POINT('Ctrl Pts',(156.746615467885,-0.893163932587293,
125.967890701188));
#31478=CARTESIAN_POINT('Ctrl Pts',(156.738864276645,-1.02786960056188,125.992767159893));
#31479=CARTESIAN_POINT('Ctrl Pts',(156.731113085405,-1.1616402902725,126.02329504115));
#31480=CARTESIAN_POINT('Ctrl Pts',(156.723361894165,-1.29396910925877,126.059381480964));
#31481=CARTESIAN_POINT('Ctrl Pts',(156.715613997388,-1.426241684967,126.095452583079));
#31482=CARTESIAN_POINT('Ctrl Pts',(156.707866100611,-1.55707323242829,126.137077442202));
#31483=CARTESIAN_POINT('Ctrl Pts',(156.700118203834,-1.68596831940623,126.184112367909));
#31484=CARTESIAN_POINT('Ctrl Pts',(156.692371927749,-1.81483644431075,126.231137454924));
#31485=CARTESIAN_POINT('Ctrl Pts',(156.684625651665,-1.94176854738642,126.283570223634));
#31486=CARTESIAN_POINT('Ctrl Pts',(156.676879375581,-2.06628598097567,126.341217632256));
#31487=CARTESIAN_POINT('Ctrl Pts',(156.669133042316,-2.19080433372386,126.398865466418));
#31488=CARTESIAN_POINT('Ctrl Pts',(156.661386709051,-2.31290762663056,126.461727853047));
#31489=CARTESIAN_POINT('Ctrl Pts',(156.653640375785,-2.43213912892105,126.529564444639));
#31490=CARTESIAN_POINT('Ctrl Pts',(156.645892307782,-2.55139733227917,126.597416227765));
#31491=CARTESIAN_POINT('Ctrl Pts',(156.638144239779,-2.66778212554129,126.670244239161));
#31492=CARTESIAN_POINT('Ctrl Pts',(156.630396171776,-2.78086357426937,126.747763417473));
#31493=CARTESIAN_POINT('Ctrl Pts',(156.622639869035,-2.89406520730764,126.825364984091));
#31494=CARTESIAN_POINT('Ctrl Pts',(156.614883566293,-3.00395615955874,126.907667455941));
#31495=CARTESIAN_POINT('Ctrl Pts',(156.607127263551,-3.11013712730472,126.994343542557));
#31496=CARTESIAN_POINT('Ctrl Pts',(156.599366821037,-3.21637476703048,127.08106589081));
#31497=CARTESIAN_POINT('Ctrl Pts',(156.591606378522,-3.31889818456083,127.172166245612));
#31498=CARTESIAN_POINT('Ctrl Pts',(156.583845936008,-3.41734386525934,127.267279339298));
#31499=CARTESIAN_POINT('Ctrl Pts',(156.576073035743,-3.51594757970393,127.362545116966));
#31500=CARTESIAN_POINT('Ctrl Pts',(156.568300135477,-3.61046020672136,127.46183622255));
#31501=CARTESIAN_POINT('Ctrl Pts',(156.560527235212,-3.70055696876274,127.564752433936));
#31502=CARTESIAN_POINT('Ctrl Pts',(156.55303689945,-3.78737848656463,127.663927381809));
#31503=CARTESIAN_POINT('Ctrl Pts',(156.545546563688,-3.87009942762595,127.766468208144));
#31504=CARTESIAN_POINT('Ctrl Pts',(156.538056227926,-3.9484676047014,127.871991841794));
#31505=CARTESIAN_POINT('Ctrl Pts',(156.530240313066,-4.03024217652106,127.982102224358));
#31506=CARTESIAN_POINT('Ctrl Pts',(156.522424398206,-4.10753741834068,128.095810972429));
#31507=CARTESIAN_POINT('Ctrl Pts',(156.514608483347,-4.18002188035116,128.21272018296));
#31508=CARTESIAN_POINT('Ctrl Pts',(156.506805570645,-4.2523857609046,128.329434909286));
#31509=CARTESIAN_POINT('Ctrl Pts',(156.499002657942,-4.31995460066225,128.449339168763));
#31510=CARTESIAN_POINT('Ctrl Pts',(156.49119974524,-4.38243817600167,128.572003411377));
#31511=CARTESIAN_POINT('Ctrl Pts',(156.483404320061,-4.44486179332591,128.694549947786));
#31512=CARTESIAN_POINT('Ctrl Pts',(156.475608894881,-4.50220967899097,128.819850858168));
#31513=CARTESIAN_POINT('Ctrl Pts',(156.467813469701,-4.55423554785991,128.947448762601));
#31514=CARTESIAN_POINT('Ctrl Pts',(156.460025184181,-4.60621376737362,129.074929802905));
#31515=CARTESIAN_POINT('Ctrl Pts',(156.45223689866,-4.65287953135542,129.204703292622));
#31516=CARTESIAN_POINT('Ctrl Pts',(156.44444861314,-4.69403331291715,129.33628898453));
#31517=CARTESIAN_POINT('Ctrl Pts',(156.439629948296,-4.71949543547048,129.417701940679));
#31518=CARTESIAN_POINT('Ctrl Pts',(156.434811283452,-4.74284850274732,129.499808147782));
#31519=CARTESIAN_POINT('Ctrl Pts',(156.429992618608,-4.76405452823405,129.582490119308));
#31520=CARTESIAN_POINT('Origin',(213.235140564004,0.,130.804360617566));
#31521=CARTESIAN_POINT('',(154.334814618358,-4.76405452823406,129.582490119308));
#31522=CARTESIAN_POINT('',(154.680281909745,-4.76405452823406,129.582490119308));
#31523=CARTESIAN_POINT('',(213.235140564004,-4.76405452823405,129.582490119308));
#31524=CARTESIAN_POINT('',(156.014859436047,-4.91824976483825,130.805881527989));
#31525=CARTESIAN_POINT('Ctrl Pts',(156.014859435991,-4.91824976483794,130.80588152897));
#31526=CARTESIAN_POINT('Ctrl Pts',(156.010156282814,-4.91822423215231,130.888447893331));
#31527=CARTESIAN_POINT('Ctrl Pts',(156.005453129637,-4.91611967239412,130.970979563799));
#31528=CARTESIAN_POINT('Ctrl Pts',(156.000749976459,-4.91194054100773,131.053405159977));
#31529=CARTESIAN_POINT('Ctrl Pts',(155.99297564234,-4.90503241735089,131.189655054569));
#31530=CARTESIAN_POINT('Ctrl Pts',(155.985201308221,-4.89244000256113,131.325833109858));
#31531=CARTESIAN_POINT('Ctrl Pts',(155.977426974102,-4.87416121135011,131.461426480528));
#31532=CARTESIAN_POINT('Ctrl Pts',(155.969662221155,-4.85590494711567,131.596852744487));
#31533=CARTESIAN_POINT('Ctrl Pts',(155.961897468208,-4.83197630192374,131.731695373808));
#31534=CARTESIAN_POINT('Ctrl Pts',(155.954132715261,-4.80242516407676,131.865442898043));
#31535=CARTESIAN_POINT('Ctrl Pts',(155.946375674376,-4.77290337683641,131.999057582352));
#31536=CARTESIAN_POINT('Ctrl Pts',(155.938618633491,-4.73777029383005,132.131578946807));
#31537=CARTESIAN_POINT('Ctrl Pts',(155.930861592606,-4.69712738784296,132.262502368177));
#31538=CARTESIAN_POINT('Ctrl Pts',(155.923110401365,-4.65651513098748,132.393327059177));
#31539=CARTESIAN_POINT('Ctrl Pts',(155.915359210125,-4.61040143687021,132.522555833738));
#31540=CARTESIAN_POINT('Ctrl Pts',(155.907608018885,-4.55893838793106,132.649696315359));
#31541=CARTESIAN_POINT('Ctrl Pts',(155.899860122108,-4.50749721216053,132.776782758883));
#31542=CARTESIAN_POINT('Ctrl Pts',(155.892112225331,-4.45071135000565,132.901782313152));
#31543=CARTESIAN_POINT('Ctrl Pts',(155.884364328554,-4.38878200102981,133.024219984719));
#31544=CARTESIAN_POINT('Ctrl Pts',(155.87661805247,-4.32686560633869,133.146632044965));
#31545=CARTESIAN_POINT('Ctrl Pts',(155.868871776386,-4.25980804121466,133.266482939769));
#31546=CARTESIAN_POINT('Ctrl Pts',(155.861125500301,-4.18785752874912,133.383320171611));
#31547=CARTESIAN_POINT('Ctrl Pts',(155.853379167036,-4.11590648516133,133.500158265918));
#31548=CARTESIAN_POINT('Ctrl Pts',(155.845632833771,-4.03906262716851,133.613982319968));
#31549=CARTESIAN_POINT('Ctrl Pts',(155.837886500505,-3.95761856390068,133.724367186937));
#31550=CARTESIAN_POINT('Ctrl Pts',(155.830138432502,-3.87615626179946,133.834776773831));
#31551=CARTESIAN_POINT('Ctrl Pts',(155.822390364499,-3.79009193655109,133.94174532653));
#31552=CARTESIAN_POINT('Ctrl Pts',(155.814642296496,-3.6997594332865,134.044879588087));
#31553=CARTESIAN_POINT('Ctrl Pts',(155.806885993755,-3.60933092356253,134.148123461964));
#31554=CARTESIAN_POINT('Ctrl Pts',(155.799129691013,-3.51462543214212,134.247524609615));
#31555=CARTESIAN_POINT('Ctrl Pts',(155.791373388271,-3.41601511993789,134.342725178045));
#31556=CARTESIAN_POINT('Ctrl Pts',(155.783612945757,-3.31735217644088,134.437976557885));
#31557=CARTESIAN_POINT('Ctrl Pts',(155.775852503242,-3.21478055162372,134.529022631768));
#31558=CARTESIAN_POINT('Ctrl Pts',(155.768092060728,-3.10870589077663,134.61554557072));
#31559=CARTESIAN_POINT('Ctrl Pts',(155.760319160463,-3.00246094946708,134.702207403975));
#31560=CARTESIAN_POINT('Ctrl Pts',(155.752546260197,-2.89270204803302,134.784331358275));
#31561=CARTESIAN_POINT('Ctrl Pts',(155.744773359932,-2.77986496636764,134.861642199027));
#31562=CARTESIAN_POINT('Ctrl Pts',(155.73728302417,-2.67112979684147,134.936142595982));
#31563=CARTESIAN_POINT('Ctrl Pts',(155.729792688408,-2.55953662171019,135.006173577832));
#31564=CARTESIAN_POINT('Ctrl Pts',(155.722302352646,-2.44549561639506,135.071529966525));
#31565=CARTESIAN_POINT('Ctrl Pts',(155.714528018527,-2.32713071170023,135.13936436256));
#31566=CARTESIAN_POINT('Ctrl Pts',(155.706753684408,-2.20575374924236,135.202377572579));
#31567=CARTESIAN_POINT('Ctrl Pts',(155.698979350289,-2.0817950731603,135.26029063675));
#31568=CARTESIAN_POINT('Ctrl Pts',(155.691214597342,-1.95798916506796,135.318132328245));
#31569=CARTESIAN_POINT('Ctrl Pts',(155.683449844395,-1.83160822486209,135.370886216214));
#31570=CARTESIAN_POINT('Ctrl Pts',(155.675685091447,-1.7031095329633,135.418317810825));
#31571=CARTESIAN_POINT('Ctrl Pts',(155.667928050562,-1.57473846777695,135.465702295708));
#31572=CARTESIAN_POINT('Ctrl Pts',(155.660171009677,-1.4442542011232,135.507774872457));
#31573=CARTESIAN_POINT('Ctrl Pts',(155.652413968792,-1.31213613533616,135.544348151816));
#31574=CARTESIAN_POINT('Ctrl Pts',(155.644662777552,-1.1801177008102,135.580893850981));
#31575=CARTESIAN_POINT('Ctrl Pts',(155.636911586312,-1.04646829476294,135.611948403351));
#31576=CARTESIAN_POINT('Ctrl Pts',(155.629160395072,-0.911684371763793,
135.637373618664));
#31577=CARTESIAN_POINT('Ctrl Pts',(155.621412498295,-0.776957735527394,
135.662788027582));
#31578=CARTESIAN_POINT('Ctrl Pts',(155.613664601518,-0.641097924783222,
135.682577785858));
#31579=CARTESIAN_POINT('Ctrl Pts',(155.605916704741,-0.504613318248974,
135.696655422823));
#31580=CARTESIAN_POINT('Ctrl Pts',(155.598170428657,-0.368157261352146,
135.71073011505));
#31581=CARTESIAN_POINT('Ctrl Pts',(155.590424152573,-0.231077057277963,
135.719095022505));
#31582=CARTESIAN_POINT('Ctrl Pts',(155.582677876489,-0.0938875756508093,
135.721714396342));
#31583=CARTESIAN_POINT('Ctrl Pts',(155.574931543223,0.0433029186779331,
135.724333789514));
#31584=CARTESIAN_POINT('Ctrl Pts',(155.567185209958,0.18060230127532,135.721207556975));
#31585=CARTESIAN_POINT('Ctrl Pts',(155.559438876692,0.317494721696234,135.712352076829));
#31586=CARTESIAN_POINT('Ctrl Pts',(155.55169080869,0.454417798225463,135.703494613559));
#31587=CARTESIAN_POINT('Ctrl Pts',(155.543942740687,0.590933341152365,135.688905374846));
#31588=CARTESIAN_POINT('Ctrl Pts',(155.536194672684,0.726530040822484,135.668652669066));
#31589=CARTESIAN_POINT('Ctrl Pts',(155.528438369942,0.86227085427868,135.648378438469));
#31590=CARTESIAN_POINT('Ctrl Pts',(155.5206820672,0.99709048640669,135.622428774651));
#31591=CARTESIAN_POINT('Ctrl Pts',(155.512925764458,1.13048670328439,135.590923358845));
#31592=CARTESIAN_POINT('Ctrl Pts',(155.505165321944,1.26395411773961,135.559401127649));
#31593=CARTESIAN_POINT('Ctrl Pts',(155.49740487943,1.3959962269207,135.522317341569));
#31594=CARTESIAN_POINT('Ctrl Pts',(155.489644436916,1.52612637112357,135.479841487152));
#31595=CARTESIAN_POINT('Ctrl Pts',(155.48187153665,1.65646541178632,135.437297446722));
#31596=CARTESIAN_POINT('Ctrl Pts',(155.474098636385,1.78488598764526,135.389344177701));
#31597=CARTESIAN_POINT('Ctrl Pts',(155.466325736119,1.91092098636537,135.336199543032));
#31598=CARTESIAN_POINT('Ctrl Pts',(155.458835400357,2.03237429541947,135.284986849697));
#31599=CARTESIAN_POINT('Ctrl Pts',(155.451345064595,2.15161218080537,135.228953807267));
#31600=CARTESIAN_POINT('Ctrl Pts',(155.443854728833,2.26824031058236,135.168334604192));
#31601=CARTESIAN_POINT('Ctrl Pts',(155.436080394714,2.38929043134765,135.105417005608));
#31602=CARTESIAN_POINT('Ctrl Pts',(155.428306060595,2.50791244256908,135.037359308717));
#31603=CARTESIAN_POINT('Ctrl Pts',(155.420531726476,2.62363903592074,134.964372789627));
#31604=CARTESIAN_POINT('Ctrl Pts',(155.412766973529,2.73922300658888,134.891476219898));
#31605=CARTESIAN_POINT('Ctrl Pts',(155.405002220582,2.85191833181156,134.813663120641));
#31606=CARTESIAN_POINT('Ctrl Pts',(155.397237467635,2.96128055741714,134.731191467343));
#31607=CARTESIAN_POINT('Ctrl Pts',(155.38948042675,3.0705341629184,134.648801726054));
#31608=CARTESIAN_POINT('Ctrl Pts',(155.381723385865,3.17646094667556,134.561762872424));
#31609=CARTESIAN_POINT('Ctrl Pts',(155.37396634498,3.27864412413066,134.470376952746));
#31610=CARTESIAN_POINT('Ctrl Pts',(155.36621515374,3.38075024445686,134.3790599479));
#31611=CARTESIAN_POINT('Ctrl Pts',(155.3584639625,3.47911808741322,134.28340266155));
#31612=CARTESIAN_POINT('Ctrl Pts',(155.35071277126,3.57336304379692,134.183748079774));
#31613=CARTESIAN_POINT('Ctrl Pts',(155.342964874482,3.66756794356007,134.084135853853));
#31614=CARTESIAN_POINT('Ctrl Pts',(155.335216977705,3.75765317394044,133.980529995064));
#31615=CARTESIAN_POINT('Ctrl Pts',(155.327469080928,3.8432703522719,133.873310936787));
#31616=CARTESIAN_POINT('Ctrl Pts',(155.319722804844,3.92886962133535,133.766114306426));
#31617=CARTESIAN_POINT('Ctrl Pts',(155.31197652876,4.01000245355591,133.655306285229));
#31618=CARTESIAN_POINT('Ctrl Pts',(155.304230252676,4.08636047280824,133.541300724468));
#31619=CARTESIAN_POINT('Ctrl Pts',(155.296483919411,4.1627190557181,133.427294322145));
#31620=CARTESIAN_POINT('Ctrl Pts',(155.288737586145,4.23430253776083,133.310090657995));
#31621=CARTESIAN_POINT('Ctrl Pts',(155.28099125288,4.30084586853458,133.190132584374));
#31622=CARTESIAN_POINT('Ctrl Pts',(155.273243184877,4.36740410122585,133.070147646975));
#31623=CARTESIAN_POINT('Ctrl Pts',(155.265495116874,4.42891974703676,132.947407414503));
#31624=CARTESIAN_POINT('Ctrl Pts',(155.257747048871,4.4851739003829,132.822378988598));
#31625=CARTESIAN_POINT('Ctrl Pts',(155.249990746129,4.54148784131269,132.697217680995));
#31626=CARTESIAN_POINT('Ctrl Pts',(155.242234443388,4.59252895852806,132.569763679046));
#31627=CARTESIAN_POINT('Ctrl Pts',(155.234478140646,4.63812647353636,132.440504217004));
#31628=CARTESIAN_POINT('Ctrl Pts',(155.226717698132,4.68374832531135,132.311175765294));
#31629=CARTESIAN_POINT('Ctrl Pts',(155.218957255618,4.72392067113484,132.180040307015));
#31630=CARTESIAN_POINT('Ctrl Pts',(155.211196813103,4.75852305338228,132.047598894378));
#31631=CARTESIAN_POINT('Ctrl Pts',(155.203423912838,4.79318098244553,131.914944875027));
#31632=CARTESIAN_POINT('Ctrl Pts',(155.195651012573,4.82225099720917,131.780981094267));
#31633=CARTESIAN_POINT('Ctrl Pts',(155.187878112307,4.84566390631248,131.646218307179));
#31634=CARTESIAN_POINT('Ctrl Pts',(155.180387776545,4.86822569719661,131.516354486847));
#31635=CARTESIAN_POINT('Ctrl Pts',(155.172897440783,4.88553450126068,131.385749048762));
#31636=CARTESIAN_POINT('Ctrl Pts',(155.165407105021,4.89757420183388,131.254860340131));
#31637=CARTESIAN_POINT('Ctrl Pts',(155.157632770902,4.91007039131358,131.119008946331));
#31638=CARTESIAN_POINT('Ctrl Pts',(155.149858436783,4.91692961799356,130.982422041169));
#31639=CARTESIAN_POINT('Ctrl Pts',(155.142084102664,4.91807704288308,130.845606984271));
#31640=CARTESIAN_POINT('Ctrl Pts',(155.134319349716,4.91922305367398,130.708960539704));
#31641=CARTESIAN_POINT('Ctrl Pts',(155.126554596769,4.91467126550661,130.572086890057));
#31642=CARTESIAN_POINT('Ctrl Pts',(155.118789843822,4.90439848212926,130.435499409266));
#31643=CARTESIAN_POINT('Ctrl Pts',(155.111032802937,4.89413590182518,130.299047589087));
#31644=CARTESIAN_POINT('Ctrl Pts',(155.103275762052,4.87816366322405,130.16288175948));
#31645=CARTESIAN_POINT('Ctrl Pts',(155.095518721167,4.85651060419171,130.027515836497));
#31646=CARTESIAN_POINT('Ctrl Pts',(155.087767529927,4.83487387389963,129.89225199401));
#31647=CARTESIAN_POINT('Ctrl Pts',(155.080016338687,4.80756491162441,129.757787241978));
#31648=CARTESIAN_POINT('Ctrl Pts',(155.072265147447,4.77466439059804,129.624630555367));
#31649=CARTESIAN_POINT('Ctrl Pts',(155.06451725067,4.74177785317077,129.491530463901));
#31650=CARTESIAN_POINT('Ctrl Pts',(155.056769353893,4.70330457737588,129.359737710847));
#31651=CARTESIAN_POINT('Ctrl Pts',(155.049021457116,4.65937632324956,129.229751033942));
#31652=CARTESIAN_POINT('Ctrl Pts',(155.041275181032,4.61545725796702,129.099791547447));
#31653=CARTESIAN_POINT('Ctrl Pts',(155.033528904947,4.56608560908237,128.971637755806));
#31654=CARTESIAN_POINT('Ctrl Pts',(155.025782628863,4.5114428765635,128.845772801305));
#31655=CARTESIAN_POINT('Ctrl Pts',(155.018036295598,4.45679974068441,128.719906917699));
#31656=CARTESIAN_POINT('Ctrl Pts',(155.010289962333,4.39688559922266,128.596330263575));
#31657=CARTESIAN_POINT('Ctrl Pts',(155.002543629067,4.33192977019051,128.475505205859));
#31658=CARTESIAN_POINT('Ctrl Pts',(154.994795561064,4.26695939475083,128.354653090209));
#31659=CARTESIAN_POINT('Ctrl Pts',(154.987047493061,4.19694527015171,128.236554141426));
#31660=CARTESIAN_POINT('Ctrl Pts',(154.979299425058,4.12216205841675,128.121645010825));
#31661=CARTESIAN_POINT('Ctrl Pts',(154.971543122316,4.0472993661944,128.006613753433));
#31662=CARTESIAN_POINT('Ctrl Pts',(154.963786819575,3.96765767527319,127.89477941467));
#31663=CARTESIAN_POINT('Ctrl Pts',(154.956030516833,3.88355459968167,127.786549037333));
#31664=CARTESIAN_POINT('Ctrl Pts',(154.948270074319,3.79940663574637,127.678260894184));
#31665=CARTESIAN_POINT('Ctrl Pts',(154.940509631804,3.71079279492847,127.573580843542));
#31666=CARTESIAN_POINT('Ctrl Pts',(154.93274918929,3.6180695163552,127.472881060774));
#31667=CARTESIAN_POINT('Ctrl Pts',(154.924976289025,3.52519739014357,127.372019625776));
#31668=CARTESIAN_POINT('Ctrl Pts',(154.917203388759,3.42820292039307,127.275151503302));
#31669=CARTESIAN_POINT('Ctrl Pts',(154.909430488494,3.3274784201976,127.1826109816));
#31670=CARTESIAN_POINT('Ctrl Pts',(154.901940152732,3.23041550929518,127.093434540959));
#31671=CARTESIAN_POINT('Ctrl Pts',(154.89444981697,3.129889286686,127.008276724391));
#31672=CARTESIAN_POINT('Ctrl Pts',(154.886959481208,3.02627666140226,126.927398839169));
#31673=CARTESIAN_POINT('Ctrl Pts',(154.879185147089,2.91873553193722,126.843454444346));
#31674=CARTESIAN_POINT('Ctrl Pts',(154.87141081297,2.80752867984863,126.763855024115));
#31675=CARTESIAN_POINT('Ctrl Pts',(154.863636478851,2.69304250885731,126.688937782912));
#31676=CARTESIAN_POINT('Ctrl Pts',(154.855871725904,2.57869743183989,126.614112870514));
#31677=CARTESIAN_POINT('Ctrl Pts',(154.848106972957,2.46108140124111,126.543958867854));
#31678=CARTESIAN_POINT('Ctrl Pts',(154.84034222001,2.3406137949513,126.478772781747));
#31679=CARTESIAN_POINT('Ctrl Pts',(154.832585179125,2.22026583878635,126.41365143938));
#31680=CARTESIAN_POINT('Ctrl Pts',(154.82482813824,2.09707228481409,126.353488379135));
#31681=CARTESIAN_POINT('Ctrl Pts',(154.817071097355,1.97148109273428,126.298537123077));
#31682=CARTESIAN_POINT('Ctrl Pts',(154.809319906114,1.84598460994937,126.243627306188));
#31683=CARTESIAN_POINT('Ctrl Pts',(154.801568714874,1.71809444465663,126.193921626622));
#31684=CARTESIAN_POINT('Ctrl Pts',(154.793817523634,1.58828241776373,126.149627325107));
#31685=CARTESIAN_POINT('Ctrl Pts',(154.786069626857,1.45852556444507,126.105351849852));
#31686=CARTESIAN_POINT('Ctrl Pts',(154.77832173008,1.32684884340647,126.066483304155));
#31687=CARTESIAN_POINT('Ctrl Pts',(154.770573833303,1.19374307635,126.033180414496));
#31688=CARTESIAN_POINT('Ctrl Pts',(154.762827557219,1.06066515215057,125.999884491084));
#31689=CARTESIAN_POINT('Ctrl Pts',(154.755081281135,0.926159155546655,125.972152002855));
#31690=CARTESIAN_POINT('Ctrl Pts',(154.747335005051,0.790729672995634,125.950091398956));
#31691=CARTESIAN_POINT('Ctrl Pts',(154.739588671785,0.655299190735075,125.928030632211));
#31692=CARTESIAN_POINT('Ctrl Pts',(154.73184233852,0.518945594803852,125.911641896197));
#31693=CARTESIAN_POINT('Ctrl Pts',(154.724096005255,0.382181839577906,125.900982179795));
#31694=CARTESIAN_POINT('Ctrl Pts',(154.716347937252,0.245387457057136,125.890320076223));
#31695=CARTESIAN_POINT('Ctrl Pts',(154.708599869249,0.108183122174561,125.885389575607));
#31696=CARTESIAN_POINT('Ctrl Pts',(154.700851801246,-0.028915336419939,
125.886195617709));
#31697=CARTESIAN_POINT('Ctrl Pts',(154.693095498504,-0.166159504887726,
125.887002516482));
#31698=CARTESIAN_POINT('Ctrl Pts',(154.685339195762,-0.303297180701629,
125.893558134816));
#31699=CARTESIAN_POINT('Ctrl Pts',(154.67758289302,-0.439814229087802,125.90581527161));
#31700=CARTESIAN_POINT('Ctrl Pts',(154.669822450506,-0.57640414073324,125.918078950406));
#31701=CARTESIAN_POINT('Ctrl Pts',(154.662062007992,-0.712372377507485,
125.936050160035));
#31702=CARTESIAN_POINT('Ctrl Pts',(154.654301565478,-0.847213153676408,
125.959630188044));
#31703=CARTESIAN_POINT('Ctrl Pts',(154.646528665212,-0.982270388229838,
125.983248068807));
#31704=CARTESIAN_POINT('Ctrl Pts',(154.638755764947,-1.11619616323684,126.012492676901));
#31705=CARTESIAN_POINT('Ctrl Pts',(154.630982864681,-1.24849717771664,126.047214639174));
#31706=CARTESIAN_POINT('Ctrl Pts',(154.623492528919,-1.3759887170752,126.080674370659));
#31707=CARTESIAN_POINT('Ctrl Pts',(154.616002193157,-1.50197127876108,126.119220048841));
#31708=CARTESIAN_POINT('Ctrl Pts',(154.608511857395,-1.6260212890266,126.162675812441));
#31709=CARTESIAN_POINT('Ctrl Pts',(154.600737434001,-1.7547761716397,126.207779732458));
#31710=CARTESIAN_POINT('Ctrl Pts',(154.592963010608,-1.88185687821755,126.258316418503));
#31711=CARTESIAN_POINT('Ctrl Pts',(154.585188587214,-2.00677083157016,126.314143040203));
#31712=CARTESIAN_POINT('Ctrl Pts',(154.577423765877,-2.1315305058499,126.369900711404));
#31713=CARTESIAN_POINT('Ctrl Pts',(154.56965894454,-2.25412839810567,126.430935160395));
#31714=CARTESIAN_POINT('Ctrl Pts',(154.561894123203,-2.37408793177902,126.497054086254));
#31715=CARTESIAN_POINT('Ctrl Pts',(154.554137034724,-2.49392799971371,126.563107165356));
#31716=CARTESIAN_POINT('Ctrl Pts',(154.546379946246,-2.61113459777468,126.634234457001));
#31717=CARTESIAN_POINT('Ctrl Pts',(154.538622857767,-2.72525228965192,126.710196109361));
#31718=CARTESIAN_POINT('Ctrl Pts',(154.530871639664,-2.8392836200523,126.786100275801));
#31719=CARTESIAN_POINT('Ctrl Pts',(154.52312042156,-2.95023037306813,126.866831304994));
#31720=CARTESIAN_POINT('Ctrl Pts',(154.515369203456,-3.05766315679506,126.952104255111));
#31721=CARTESIAN_POINT('Ctrl Pts',(154.50762138725,-3.16504878982158,127.037339780159));
#31722=CARTESIAN_POINT('Ctrl Pts',(154.499873571045,-3.26892321592966,127.127113018156));
#31723=CARTESIAN_POINT('Ctrl Pts',(154.492125754839,-3.36888760615964,127.221096831635));
#31724=CARTESIAN_POINT('Ctrl Pts',(154.484379588851,-3.46883070483132,127.315060627367));
#31725=CARTESIAN_POINT('Ctrl Pts',(154.476633422864,-3.56486513965299,127.413232946955));
#31726=CARTESIAN_POINT('Ctrl Pts',(154.468887256877,-3.65662694395631,127.515247902071));
#31727=CARTESIAN_POINT('Ctrl Pts',(154.461141063254,-3.74838907563266,127.617263221139));
#31728=CARTESIAN_POINT('Ctrl Pts',(154.453394869631,-3.83587828503477,127.723120912351));
#31729=CARTESIAN_POINT('Ctrl Pts',(154.445648676008,-3.9187693788703,127.832420238331));
#31730=CARTESIAN_POINT('Ctrl Pts',(154.437900777239,-4.00167871926914,127.941743624038));
#31731=CARTESIAN_POINT('Ctrl Pts',(154.43015287847,-4.07998769403529,128.054509840464));
#31732=CARTESIAN_POINT('Ctrl Pts',(154.422404979701,-4.15341334672048,128.170287605331));
#31733=CARTESIAN_POINT('Ctrl Pts',(154.414649257282,-4.22691314295054,128.286182279938));
#31734=CARTESIAN_POINT('Ctrl Pts',(154.406893534862,-4.29551955865376,128.405094246168));
#31735=CARTESIAN_POINT('Ctrl Pts',(154.399137812442,-4.35899445312151,128.526565538952));
#31736=CARTESIAN_POINT('Ctrl Pts',(154.391377962452,-4.42250312872119,128.648101478363));
#31737=CARTESIAN_POINT('Ctrl Pts',(154.383618112462,-4.48087467518851,128.772199104847));
#31738=CARTESIAN_POINT('Ctrl Pts',(154.375858262472,-4.53391878889429,128.898379642264));
#31739=CARTESIAN_POINT('Ctrl Pts',(154.368086922269,-4.58704144640668,129.024747018504));
#31740=CARTESIAN_POINT('Ctrl Pts',(154.360315582066,-4.63482077540106,129.153203101052));
#31741=CARTESIAN_POINT('Ctrl Pts',(154.352544241863,-4.6771158768101,129.283252423718));
#31742=CARTESIAN_POINT('Ctrl Pts',(154.346634367361,-4.70928005117857,129.382151089317));
#31743=CARTESIAN_POINT('Ctrl Pts',(154.34072449286,-4.738273635472,129.481970809709));
#31744=CARTESIAN_POINT('Ctrl Pts',(154.334814618358,-4.76405452823406,129.582490119308));
#31745=CARTESIAN_POINT('Ctrl Pts',(156.084992794976,-4.76405452823404,129.582490119308));
#31746=CARTESIAN_POINT('Ctrl Pts',(156.077293740712,-4.79788100655492,129.714379044893));
#31747=CARTESIAN_POINT('Ctrl Pts',(156.069594686447,-4.82620048638222,129.847572500239));
#31748=CARTESIAN_POINT('Ctrl Pts',(156.061895632183,-4.84893743113397,129.981567295128));
#31749=CARTESIAN_POINT('Ctrl Pts',(156.05405626616,-4.87208874635078,130.118004084141));
#31750=CARTESIAN_POINT('Ctrl Pts',(156.046216900138,-4.88945202110533,130.255271272325));
#31751=CARTESIAN_POINT('Ctrl Pts',(156.038377534115,-4.90100290378361,130.392834677187));
#31752=CARTESIAN_POINT('Ctrl Pts',(156.030538168092,-4.91255378646188,130.530398082049));
#31753=CARTESIAN_POINT('Ctrl Pts',(156.02269880207,-4.91829232350721,130.668257273153));
#31754=CARTESIAN_POINT('Ctrl Pts',(156.014859436047,-4.91824976483825,130.805881527989));
#31755=CARTESIAN_POINT('',(156.360140563953,-4.91824883972711,130.807738934152));
#31756=CARTESIAN_POINT('Ctrl Pts',(156.429992618608,-4.76405452823405,129.582490119308));
#31757=CARTESIAN_POINT('Ctrl Pts',(156.422210727339,-4.79830114839348,129.716017171545));
#31758=CARTESIAN_POINT('Ctrl Pts',(156.414428836071,-4.82694553781918,129.851046419521));
#31759=CARTESIAN_POINT('Ctrl Pts',(156.406646944802,-4.84986811108228,129.987070970252));
#31760=CARTESIAN_POINT('Ctrl Pts',(156.398865314921,-4.87278991439169,130.12309095201));
#31761=CARTESIAN_POINT('Ctrl Pts',(156.391083685041,-4.88999020947882,130.260105791632));
#31762=CARTESIAN_POINT('Ctrl Pts',(156.38330205516,-4.9014005977705,130.397598718324));
#31763=CARTESIAN_POINT('Ctrl Pts',(156.37558155811,-4.91272134554554,130.534011494484));
#31764=CARTESIAN_POINT('Ctrl Pts',(156.367861061059,-4.91834283735024,130.670894495926));
#31765=CARTESIAN_POINT('Ctrl Pts',(156.360140564008,-4.91824883972778,130.807738933169));
#31766=CARTESIAN_POINT('Ctrl Pts',(156.360140563953,-4.91824883972711,130.807738934152));
#31767=CARTESIAN_POINT('Ctrl Pts',(156.351323954703,-4.91814149682635,130.964011765196));
#31768=CARTESIAN_POINT('Ctrl Pts',(156.342507345453,-4.91058202809959,131.119992202956));
#31769=CARTESIAN_POINT('Ctrl Pts',(156.333690736203,-4.89567786746431,131.275021090221));
#31770=CARTESIAN_POINT('Ctrl Pts',(156.3248350287,-4.8807076126391,131.430737470661));
#31771=CARTESIAN_POINT('Ctrl Pts',(156.315979321197,-4.85832749074473,131.585493680049));
#31772=CARTESIAN_POINT('Ctrl Pts',(156.307123613693,-4.82869601254221,131.738639955323));
#31773=CARTESIAN_POINT('Ctrl Pts',(156.298215535422,-4.79888930008775,131.892691905055));
#31774=CARTESIAN_POINT('Ctrl Pts',(156.28930745715,-4.7617453046484,132.045114662076));
#31775=CARTESIAN_POINT('Ctrl Pts',(156.280399378879,-4.71747396232134,132.195267687546));
#31776=CARTESIAN_POINT('Ctrl Pts',(156.273469120624,-4.68303198434525,132.312082921158));
#31777=CARTESIAN_POINT('Ctrl Pts',(156.266538862368,-4.64427720768572,132.427524809799));
#31778=CARTESIAN_POINT('Ctrl Pts',(156.259608604113,-4.6013280870806,132.541301289421));
#31779=CARTESIAN_POINT('Ctrl Pts',(156.251834269994,-4.55314794697554,132.668935258443));
#31780=CARTESIAN_POINT('Ctrl Pts',(156.244059935875,-4.49957690486087,132.794765203604));
#31781=CARTESIAN_POINT('Ctrl Pts',(156.236285601756,-4.440769564856,132.918302133869));
#31782=CARTESIAN_POINT('Ctrl Pts',(156.228520848809,-4.38203469964196,133.041686815908));
#31783=CARTESIAN_POINT('Ctrl Pts',(156.220756095862,-4.31807654304976,133.162783756201));
#31784=CARTESIAN_POINT('Ctrl Pts',(156.212991342914,-4.24909877098898,133.2811211423));
#31785=CARTESIAN_POINT('Ctrl Pts',(156.205234302029,-4.18018950862385,133.399340994038));
#31786=CARTESIAN_POINT('Ctrl Pts',(156.197477261144,-4.10627074787576,133.514806410367));
#31787=CARTESIAN_POINT('Ctrl Pts',(156.189720220259,-4.02759319501525,133.627067849634));
#31788=CARTESIAN_POINT('Ctrl Pts',(156.181969029019,-3.94897497350953,133.739244631676));
#31789=CARTESIAN_POINT('Ctrl Pts',(156.174217837779,-3.86560532634282,133.848221926976));
#31790=CARTESIAN_POINT('Ctrl Pts',(156.166466646539,-3.77777941321032,133.953577308685));
#31791=CARTESIAN_POINT('Ctrl Pts',(156.158718749762,-3.68999082843352,134.058887911547));
#31792=CARTESIAN_POINT('Ctrl Pts',(156.150970852985,-3.59774999459174,134.16057936291));
#31793=CARTESIAN_POINT('Ctrl Pts',(156.143222956208,-3.50139353524727,134.258260786046));
#31794=CARTESIAN_POINT('Ctrl Pts',(156.135476680124,-3.4050572315969,134.355921776335));
#31795=CARTESIAN_POINT('Ctrl Pts',(156.12773040404,-3.30460728920746,134.44957412868));
#31796=CARTESIAN_POINT('Ctrl Pts',(156.119984127955,-3.20041824075269,134.53886274593));
#31797=CARTESIAN_POINT('Ctrl Pts',(156.11223779469,-3.09622842319807,134.628152022289));
#31798=CARTESIAN_POINT('Ctrl Pts',(156.104491461425,-2.98829974136769,134.713077244867));
#31799=CARTESIAN_POINT('Ctrl Pts',(156.096745128159,-2.87704064317679,134.793322913704));
#31800=CARTESIAN_POINT('Ctrl Pts',(156.088997060156,-2.76575662928249,134.873586553002));
#31801=CARTESIAN_POINT('Ctrl Pts',(156.081248992153,-2.65114103195784,134.949168324592));
#31802=CARTESIAN_POINT('Ctrl Pts',(156.07350092415,-2.53363182878062,135.019795686297));
#31803=CARTESIAN_POINT('Ctrl Pts',(156.065744621409,-2.4159977354236,135.090498111603));
#31804=CARTESIAN_POINT('Ctrl Pts',(156.057988318667,-2.29546422848449,135.156235406683));
#31805=CARTESIAN_POINT('Ctrl Pts',(156.050232015925,-2.17249496146798,135.216780441755));
#31806=CARTESIAN_POINT('Ctrl Pts',(156.042471573411,-2.04946006205101,135.277357791535));
#31807=CARTESIAN_POINT('Ctrl Pts',(156.034711130897,-1.92398716962091,135.332737201539));
#31808=CARTESIAN_POINT('Ctrl Pts',(156.026950688382,-1.79655960225933,135.382739878618));
#31809=CARTESIAN_POINT('Ctrl Pts',(156.019177788117,-1.66892747685422,135.432822824433));
#31810=CARTESIAN_POINT('Ctrl Pts',(156.011404887851,-1.53933477597712,135.47751166189));
#31811=CARTESIAN_POINT('Ctrl Pts',(156.003631987586,-1.40828050765929,135.516677359281));
#31812=CARTESIAN_POINT('Ctrl Pts',(155.996141651824,-1.28199039210069,135.55441928492));
#31813=CARTESIAN_POINT('Ctrl Pts',(155.988651316062,-1.15434342596211,135.587032582679));
#31814=CARTESIAN_POINT('Ctrl Pts',(155.9811609803,-1.02579284480649,135.614447113882));
#31815=CARTESIAN_POINT('Ctrl Pts',(155.973386646181,-0.892368229294299,
135.642901075369));
#31816=CARTESIAN_POINT('Ctrl Pts',(155.965612312062,-0.75754747593295,135.665844399354));
#31817=CARTESIAN_POINT('Ctrl Pts',(155.957837977943,-0.621825554031741,
135.683142847063));
#31818=CARTESIAN_POINT('Ctrl Pts',(155.950073224996,-0.48627089726946,135.700419975981));
#31819=CARTESIAN_POINT('Ctrl Pts',(155.942308472049,-0.349817665854264,
135.712066021637));
#31820=CARTESIAN_POINT('Ctrl Pts',(155.934543719101,-0.212972900766116,
135.717997316187));
#31821=CARTESIAN_POINT('Ctrl Pts',(155.926786678216,-0.0762640518279205,
135.723922719693));
#31822=CARTESIAN_POINT('Ctrl Pts',(155.919029637331,0.0608351688299815,
135.724144650713));
#31823=CARTESIAN_POINT('Ctrl Pts',(155.911272596446,0.197811036221584,135.718631047289));
#31824=CARTESIAN_POINT('Ctrl Pts',(155.903521405206,0.334683609045929,135.713121601716));
#31825=CARTESIAN_POINT('Ctrl Pts',(155.895770213966,0.471432624689744,135.701885246432));
#31826=CARTESIAN_POINT('Ctrl Pts',(155.888019022726,0.607543142456625,135.684941975617));
#31827=CARTESIAN_POINT('Ctrl Pts',(155.880271125949,0.743595809622773,135.668005906144));
#31828=CARTESIAN_POINT('Ctrl Pts',(155.872523229172,0.879010131504822,135.64536779365));
#31829=CARTESIAN_POINT('Ctrl Pts',(155.864775332395,1.01327529918402,135.617099570653));
#31830=CARTESIAN_POINT('Ctrl Pts',(155.857029056311,1.14751238148461,135.58883726076));
#31831=CARTESIAN_POINT('Ctrl Pts',(155.849282780227,1.28060040537247,135.554947263365));
#31832=CARTESIAN_POINT('Ctrl Pts',(155.841536504143,1.41203817349923,135.515552744733));
#31833=CARTESIAN_POINT('Ctrl Pts',(155.833790170877,1.54347691186965,135.476157935299));
#31834=CARTESIAN_POINT('Ctrl Pts',(155.826043837612,1.67326499566543,135.431258635794));
#31835=CARTESIAN_POINT('Ctrl Pts',(155.818297504347,1.80091620975991,135.38102794958));
#31836=CARTESIAN_POINT('Ctrl Pts',(155.810549436344,1.92859601045877,135.330786014553));
#31837=CARTESIAN_POINT('Ctrl Pts',(155.802801368341,2.05413762548057,135.275210460173));
#31838=CARTESIAN_POINT('Ctrl Pts',(155.795053300338,2.17707501979339,135.214522453677));
#31839=CARTESIAN_POINT('Ctrl Pts',(155.787296997596,2.3001430734319,135.153769947246));
#31840=CARTESIAN_POINT('Ctrl Pts',(155.779540694854,2.42060102625438,135.087894307885));
#31841=CARTESIAN_POINT('Ctrl Pts',(155.771784392112,2.53800717149881,135.017162851225));
#31842=CARTESIAN_POINT('Ctrl Pts',(155.764023949598,2.65547597993806,134.946393643056));
#31843=CARTESIAN_POINT('Ctrl Pts',(155.756263507084,2.76988940920439,134.870763668902));
#31844=CARTESIAN_POINT('Ctrl Pts',(155.74850306457,2.88083579033065,134.790582915889));
#31845=CARTESIAN_POINT('Ctrl Pts',(155.740730164304,2.99196027243722,134.710273449614));
#31846=CARTESIAN_POINT('Ctrl Pts',(155.732957264039,3.09960627734477,134.625398848341));
#31847=CARTESIAN_POINT('Ctrl Pts',(155.725184363773,3.2033955209944,134.536309196871));
#31848=CARTESIAN_POINT('Ctrl Pts',(155.717694028011,3.30341176420874,134.450458178634));
#31849=CARTESIAN_POINT('Ctrl Pts',(155.710203692249,3.39984655841918,134.360693454934));
#31850=CARTESIAN_POINT('Ctrl Pts',(155.702713356487,3.49239590907836,134.267358434018));
#31851=CARTESIAN_POINT('Ctrl Pts',(155.694939022368,3.58845429649688,134.170484587416));
#31852=CARTESIAN_POINT('Ctrl Pts',(155.687164688249,3.68063107512587,134.069457496327));
#31853=CARTESIAN_POINT('Ctrl Pts',(155.67939035413,3.76854576308079,133.964621033112));
#31854=CARTESIAN_POINT('Ctrl Pts',(155.671625601183,3.85635210403997,133.859913771468));
#31855=CARTESIAN_POINT('Ctrl Pts',(155.663860848236,3.9399065567186,133.751406775469));
#31856=CARTESIAN_POINT('Ctrl Pts',(155.656096095288,4.01886466095661,133.63948140854));
#31857=CARTESIAN_POINT('Ctrl Pts',(155.648339054403,4.09774434289234,133.527667207463));
#31858=CARTESIAN_POINT('Ctrl Pts',(155.640582013518,4.17203653734483,133.412441709409));
#31859=CARTESIAN_POINT('Ctrl Pts',(155.632824972634,4.2414365887779,133.294219795487));
#31860=CARTESIAN_POINT('Ctrl Pts',(155.625073781393,4.31078430509233,133.176087033629));
#31861=CARTESIAN_POINT('Ctrl Pts',(155.617322590153,4.3752470243975,133.05496268934));
#31862=CARTESIAN_POINT('Ctrl Pts',(155.609571398913,4.43456323033953,132.931290804154));
#31863=CARTESIAN_POINT('Ctrl Pts',(155.601823502136,4.49385422531172,132.807671482819));
#31864=CARTESIAN_POINT('Ctrl Pts',(155.594075605359,4.54800288878193,132.681507125917));
#31865=CARTESIAN_POINT('Ctrl Pts',(155.586327708582,4.59679363491687,132.553266372742));
#31866=CARTESIAN_POINT('Ctrl Pts',(155.578581432498,4.64557417507955,132.425052444768));
#31867=CARTESIAN_POINT('Ctrl Pts',(155.570835156414,4.6889988882244,132.294763349622));
#31868=CARTESIAN_POINT('Ctrl Pts',(155.56308888033,4.72690048820667,132.1628873332));
#31869=CARTESIAN_POINT('Ctrl Pts',(155.555342547064,4.76480236796994,132.0310103433));
#31870=CARTESIAN_POINT('Ctrl Pts',(155.547596213799,4.79718094522331,131.897546784504));
#31871=CARTESIAN_POINT('Ctrl Pts',(155.539849880534,4.82391904557718,131.762999289964));
#31872=CARTESIAN_POINT('Ctrl Pts',(155.532101812531,4.85066313374322,131.628421664447));
#31873=CARTESIAN_POINT('Ctrl Pts',(155.524353744528,4.87176415530583,131.492760003555));
#31874=CARTESIAN_POINT('Ctrl Pts',(155.516605676525,4.88715628120619,131.356525942054));
#31875=CARTESIAN_POINT('Ctrl Pts',(155.508849373783,4.90256476604114,131.220147089371));
#31876=CARTESIAN_POINT('Ctrl Pts',(155.501093071041,4.91225219080136,131.083195009938));
#31877=CARTESIAN_POINT('Ctrl Pts',(155.493336768299,4.91620470240323,130.946185814793));
#31878=CARTESIAN_POINT('Ctrl Pts',(155.485576325785,4.92015932357955,130.809103493714));
#31879=CARTESIAN_POINT('Ctrl Pts',(155.477815883271,4.91837293759324,130.671964386921));
#31880=CARTESIAN_POINT('Ctrl Pts',(155.470055440757,4.91088382826134,130.535282398787));
#31881=CARTESIAN_POINT('Ctrl Pts',(155.462282540491,4.90338269674628,130.398380996592));
#31882=CARTESIAN_POINT('Ctrl Pts',(155.454509640226,4.89016058597404,130.261938568805));
#31883=CARTESIAN_POINT('Ctrl Pts',(155.44673673996,4.871307560428,130.126462605903));
#31884=CARTESIAN_POINT('Ctrl Pts',(155.439246404198,4.85313988984843,129.995911535495));
#31885=CARTESIAN_POINT('Ctrl Pts',(155.431756068436,4.82974364735219,129.866258186166));
#31886=CARTESIAN_POINT('Ctrl Pts',(155.424265732674,4.80124343554559,129.737943937684));
#31887=CARTESIAN_POINT('Ctrl Pts',(155.416491398555,4.77166262954591,129.60476461547));
#31888=CARTESIAN_POINT('Ctrl Pts',(155.408717064436,4.73648947696845,129.47260607057));
#31889=CARTESIAN_POINT('Ctrl Pts',(155.400942730317,4.69580762761774,129.341974284579));
#31890=CARTESIAN_POINT('Ctrl Pts',(155.39317797737,4.65517591501052,129.21150349059));
#31891=CARTESIAN_POINT('Ctrl Pts',(155.385413224423,4.60904912880283,129.082556081398));
#31892=CARTESIAN_POINT('Ctrl Pts',(155.377648471476,4.55756193171374,128.955627997338));
#31893=CARTESIAN_POINT('Ctrl Pts',(155.369891430591,4.50612587243467,128.828825980041));
#31894=CARTESIAN_POINT('Ctrl Pts',(155.362134389706,4.44934014335527,128.704039656547));
#31895=CARTESIAN_POINT('Ctrl Pts',(155.354377348821,4.3873891219437,128.581749595558));
#31896=CARTESIAN_POINT('Ctrl Pts',(155.346626157581,4.32548481827929,128.459551754456));
#31897=CARTESIAN_POINT('Ctrl Pts',(155.338874966341,4.25842315138301,128.339846776311));
#31898=CARTESIAN_POINT('Ctrl Pts',(155.3311237751,4.18643634999695,128.223094697533));
#31899=CARTESIAN_POINT('Ctrl Pts',(155.323375878323,4.11448014492177,128.106392241503));
#31900=CARTESIAN_POINT('Ctrl Pts',(155.315627981546,4.03760317356018,127.992640520714));
#31901=CARTESIAN_POINT('Ctrl Pts',(155.307880084769,3.9560831860132,127.882274224619));
#31902=CARTESIAN_POINT('Ctrl Pts',(155.300133808685,3.87458025069021,127.771931014774));
#31903=CARTESIAN_POINT('Ctrl Pts',(155.292387532601,3.78843646312696,127.664972135339));
#31904=CARTESIAN_POINT('Ctrl Pts',(155.284641256517,3.69797217617701,127.561802237718));
#31905=CARTESIAN_POINT('Ctrl Pts',(155.276894923252,3.60750722144029,127.458631578521));
#31906=CARTESIAN_POINT('Ctrl Pts',(155.269148589986,3.51272196143669,127.35925025091));
#31907=CARTESIAN_POINT('Ctrl Pts',(155.261402256721,3.41397594005339,127.264028522517));
#31908=CARTESIAN_POINT('Ctrl Pts',(155.253654188718,3.31520780518326,127.168785469877));
#31909=CARTESIAN_POINT('Ctrl Pts',(155.245906120715,3.21247742531274,127.077704141392));
#31910=CARTESIAN_POINT('Ctrl Pts',(155.238158052712,3.10617967104525,126.991116472001));
#31911=CARTESIAN_POINT('Ctrl Pts',(155.23040174997,2.99976894225953,126.904436776205));
#31912=CARTESIAN_POINT('Ctrl Pts',(155.222645447228,2.88978356885973,126.822260527218));
#31913=CARTESIAN_POINT('Ctrl Pts',(155.214889144486,2.77665028174771,126.744878350654));
#31914=CARTESIAN_POINT('Ctrl Pts',(155.207128701972,2.66345661199391,126.667454872893));
#31915=CARTESIAN_POINT('Ctrl Pts',(155.199368259458,2.54711201220644,126.594830772986));
#31916=CARTESIAN_POINT('Ctrl Pts',(155.191607816944,2.42806953802891,126.52725161954));
#31917=CARTESIAN_POINT('Ctrl Pts',(155.183834916679,2.30883596630377,126.459563982038));
#31918=CARTESIAN_POINT('Ctrl Pts',(155.176062016413,2.18689621371526,126.396937653289));
#31919=CARTESIAN_POINT('Ctrl Pts',(155.168289116148,2.06272592842871,126.339571170494));
#31920=CARTESIAN_POINT('Ctrl Pts',(155.160798780386,1.94306954577844,126.284290103845));
#31921=CARTESIAN_POINT('Ctrl Pts',(155.153308444624,1.82134227046019,126.233893223002));
#31922=CARTESIAN_POINT('Ctrl Pts',(155.145818108862,1.69798279852588,126.188514272809));
#31923=CARTESIAN_POINT('Ctrl Pts',(155.138043774742,1.56994611471888,126.141414765926));
#31924=CARTESIAN_POINT('Ctrl Pts',(155.130269440623,1.43974543984953,126.099572013674));
#31925=CARTESIAN_POINT('Ctrl Pts',(155.122495106504,1.30785168532758,126.063189134516));
#31926=CARTESIAN_POINT('Ctrl Pts',(155.114730353557,1.17612047807048,126.026851094005));
#31927=CARTESIAN_POINT('Ctrl Pts',(155.10696560061,1.04270071608255,125.995959641236));
#31928=CARTESIAN_POINT('Ctrl Pts',(155.099200847663,0.908082436501846,125.970669548516));
#31929=CARTESIAN_POINT('Ctrl Pts',(155.091443806778,0.773597861694302,125.945404574272));
#31930=CARTESIAN_POINT('Ctrl Pts',(155.083686765893,0.637917519969964,125.925729960477));
#31931=CARTESIAN_POINT('Ctrl Pts',(155.075929725008,0.501545387915416,125.91175034427));
#31932=CARTESIAN_POINT('Ctrl Pts',(155.068178533768,0.365276095146332,125.8977812702));
#31933=CARTESIAN_POINT('Ctrl Pts',(155.060427342528,0.228316437781679,125.889498685201));
#31934=CARTESIAN_POINT('Ctrl Pts',(155.052676151288,0.0911789827905253,
125.886955869572));
#31935=CARTESIAN_POINT('Ctrl Pts',(155.04492825451,-0.0459001851239494,
125.884414134707));
#31936=CARTESIAN_POINT('Ctrl Pts',(155.037180357733,-0.183156610284839,
125.887607324356));
#31937=CARTESIAN_POINT('Ctrl Pts',(155.029432460956,-0.320074445430811,
125.896536719759));
#31938=CARTESIAN_POINT('Ctrl Pts',(155.021686184872,-0.456963640317278,
125.905464247326));
#31939=CARTESIAN_POINT('Ctrl Pts',(155.013939908788,-0.593513996175859,
125.920125568571));
#31940=CARTESIAN_POINT('Ctrl Pts',(155.006193632704,-0.729211909777027,
125.940469885535));
#31941=CARTESIAN_POINT('Ctrl Pts',(154.998447299439,-0.864910825069366,
125.960814352676));
#31942=CARTESIAN_POINT('Ctrl Pts',(154.990700966173,-0.999756898903957,
125.986841841278));
#31943=CARTESIAN_POINT('Ctrl Pts',(154.982954632908,-1.13324427238443,126.018449995583));
#31944=CARTESIAN_POINT('Ctrl Pts',(154.975206564905,-1.26676153943657,126.050065228316));
#31945=CARTESIAN_POINT('Ctrl Pts',(154.967458496902,-1.39891912029712,126.087263523545));
#31946=CARTESIAN_POINT('Ctrl Pts',(154.959710428899,-1.52922431149447,126.129892084392));
#31947=CARTESIAN_POINT('Ctrl Pts',(154.951954126157,-1.65966799259981,126.172565951381));
#31948=CARTESIAN_POINT('Ctrl Pts',(154.944197823415,-1.78825497908933,126.220681491126));
#31949=CARTESIAN_POINT('Ctrl Pts',(154.936441520673,-1.91451010092752,126.274036773077));
#31950=CARTESIAN_POINT('Ctrl Pts',(154.928681078159,-2.04083260892575,126.327420532349));
#31951=CARTESIAN_POINT('Ctrl Pts',(154.920920635645,-2.16482041905922,126.386049439258));
#31952=CARTESIAN_POINT('Ctrl Pts',(154.913160193131,-2.28602203986124,126.449675061091));
#31953=CARTESIAN_POINT('Ctrl Pts',(154.905387292865,-2.40741822426469,126.513402820422));
#31954=CARTESIAN_POINT('Ctrl Pts',(154.8976143926,-2.52601894312855,126.582143127366));
#31955=CARTESIAN_POINT('Ctrl Pts',(154.889841492334,-2.64140006203276,126.655603119857));
#31956=CARTESIAN_POINT('Ctrl Pts',(154.882351156572,-2.75258678663672,126.726392656587));
#31957=CARTESIAN_POINT('Ctrl Pts',(154.87486082081,-2.86078367546688,126.801564515699));
#31958=CARTESIAN_POINT('Ctrl Pts',(154.867370485048,-2.96564107926591,126.880821902137));
#31959=CARTESIAN_POINT('Ctrl Pts',(154.859575127744,-3.07476848751448,126.963306808811));
#31960=CARTESIAN_POINT('Ctrl Pts',(154.85177977044,-3.18064515146998,127.050494249024));
#31961=CARTESIAN_POINT('Ctrl Pts',(154.843984413136,-3.28283355226151,127.142095344453));
#31962=CARTESIAN_POINT('Ctrl Pts',(154.836302734693,-3.38353175053798,127.232360630909));
#31963=CARTESIAN_POINT('Ctrl Pts',(154.82862105625,-3.48064819156846,127.326911468719));
#31964=CARTESIAN_POINT('Ctrl Pts',(154.820939377807,-3.57379280059238,127.425427637921));
#31965=CARTESIAN_POINT('Ctrl Pts',(154.813264691756,-3.66685262299287,127.523854130936));
#31966=CARTESIAN_POINT('Ctrl Pts',(154.805590005705,-3.75594752972872,127.62623848939));
#31967=CARTESIAN_POINT('Ctrl Pts',(154.797915319653,-3.84072175893283,127.732221390096));
#31968=CARTESIAN_POINT('Ctrl Pts',(154.7902458715,-3.92543813055292,127.838131958507));
#31969=CARTESIAN_POINT('Ctrl Pts',(154.782576423347,-4.00583944108695,127.947635873119));
#31970=CARTESIAN_POINT('Ctrl Pts',(154.774906975194,-4.08160830550919,128.060338623686));
#31971=CARTESIAN_POINT('Ctrl Pts',(154.767021553074,-4.15951084395384,128.176215117622));
#31972=CARTESIAN_POINT('Ctrl Pts',(154.759136130953,-4.23251587964388,128.295472954516));
#31973=CARTESIAN_POINT('Ctrl Pts',(154.751250708832,-4.30032435264736,128.417648752986));
#31974=CARTESIAN_POINT('Ctrl Pts',(154.74358536649,-4.36624031139867,128.536414661369));
#31975=CARTESIAN_POINT('Ctrl Pts',(154.735920024148,-4.42724573367112,128.657937438946));
#31976=CARTESIAN_POINT('Ctrl Pts',(154.728254681806,-4.48311152563272,128.781764733253));
#31977=CARTESIAN_POINT('Ctrl Pts',(154.720259219796,-4.5413832631991,128.910924839001));
#31978=CARTESIAN_POINT('Ctrl Pts',(154.712263757786,-4.59406258058145,129.042591971584));
#31979=CARTESIAN_POINT('Ctrl Pts',(154.704268295776,-4.64094485693375,129.176228590549));
#31980=CARTESIAN_POINT('Ctrl Pts',(154.696272833765,-4.68782713328608,129.309865209513));
#31981=CARTESIAN_POINT('Ctrl Pts',(154.688277371755,-4.72891223230369,129.445470840835));
#31982=CARTESIAN_POINT('Ctrl Pts',(154.680281909745,-4.76405452823406,129.582490119308));
#31983=CARTESIAN_POINT('Origin',(213.235140564004,0.,130.804360617566));
#31984=CARTESIAN_POINT('',(152.584590056215,-4.76405452823403,129.582490119308));
#31985=CARTESIAN_POINT('',(152.930132636296,-4.76405452823406,129.582490119308));
#31986=CARTESIAN_POINT('',(213.235140564004,-4.76405452823405,129.582490119308));
#31987=CARTESIAN_POINT('',(154.264859436025,-4.91824789998526,130.799815643358));
#31988=CARTESIAN_POINT('Ctrl Pts',(154.264859435991,-4.91824789998582,130.799815643966));
#31989=CARTESIAN_POINT('Ctrl Pts',(154.257201974255,-4.91837282331536,130.934998806114));
#31990=CARTESIAN_POINT('Ctrl Pts',(154.249544512518,-4.91292008139986,131.070338875953));
#31991=CARTESIAN_POINT('Ctrl Pts',(154.241887050782,-4.90187769675906,131.205332073553));
#31992=CARTESIAN_POINT('Ctrl Pts',(154.233959115739,-4.89044527813835,131.345093438159));
#31993=CARTESIAN_POINT('Ctrl Pts',(154.226031180697,-4.87302102558022,131.484482540111));
#31994=CARTESIAN_POINT('Ctrl Pts',(154.218103245655,-4.84965056909455,131.622940131224));
#31995=CARTESIAN_POINT('Ctrl Pts',(154.210453950955,-4.82710150581549,131.756531402126));
#31996=CARTESIAN_POINT('Ctrl Pts',(154.202804656255,-4.79901723311674,131.889255105444));
#31997=CARTESIAN_POINT('Ctrl Pts',(154.195155361554,-4.76549141676183,132.020614957443));
#31998=CARTESIAN_POINT('Ctrl Pts',(154.187507083778,-4.73197005744568,132.151957346006));
#31999=CARTESIAN_POINT('Ctrl Pts',(154.179858806002,-4.69300869217524,132.281935854467));
#32000=CARTESIAN_POINT('Ctrl Pts',(154.172210528225,-4.64875168296609,132.410066335504));
#32001=CARTESIAN_POINT('Ctrl Pts',(154.16456151096,-4.60449039468026,132.538209205091));
#32002=CARTESIAN_POINT('Ctrl Pts',(154.156912493695,-4.55493257575353,132.664503312174));
#32003=CARTESIAN_POINT('Ctrl Pts',(154.149263476429,-4.50027166529154,132.788482085892));
#32004=CARTESIAN_POINT('Ctrl Pts',(154.14161196291,-4.44559291626051,132.91250132004));
#32005=CARTESIAN_POINT('Ctrl Pts',(154.13396044939,-4.38580792617314,133.034203350896));
#32006=CARTESIAN_POINT('Ctrl Pts',(154.126308935871,-4.32115699401076,133.153144408299));
#32007=CARTESIAN_POINT('Ctrl Pts',(154.118649094412,-4.25643569549892,133.272214921656));
#32008=CARTESIAN_POINT('Ctrl Pts',(154.110989252953,-4.1868380770245,133.388518111072));
#32009=CARTESIAN_POINT('Ctrl Pts',(154.103329411493,-4.11264897603279,133.50163729274));
#32010=CARTESIAN_POINT('Ctrl Pts',(154.095664596587,-4.03841170491251,133.614829921389));
#32011=CARTESIAN_POINT('Ctrl Pts',(154.087999781681,-3.95957725044642,133.724834101816));
#32012=CARTESIAN_POINT('Ctrl Pts',(154.080334966775,-3.87647115193746,133.831265715301));
#32013=CARTESIAN_POINT('Ctrl Pts',(154.07265943833,-3.79324889140172,133.937846094186));
#32014=CARTESIAN_POINT('Ctrl Pts',(154.064983909885,-3.70574333233295,134.040843638029));
#32015=CARTESIAN_POINT('Ctrl Pts',(154.05730838144,-3.61431743326588,134.139910430429));
#32016=CARTESIAN_POINT('Ctrl Pts',(154.055411124216,-3.5917185400876,134.164398019633));
#32017=CARTESIAN_POINT('Ctrl Pts',(154.053513866993,-3.56888027694123,134.188645634285));
#32018=CARTESIAN_POINT('Ctrl Pts',(154.051616609769,-3.54580843086088,134.21264840385));
#32019=CARTESIAN_POINT('Ctrl Pts',(154.04384227565,-3.4512676179694,134.311003834035));
#32020=CARTESIAN_POINT('Ctrl Pts',(154.036067941531,-3.35248160871389,134.405578439652));
#32021=CARTESIAN_POINT('Ctrl Pts',(154.028293607412,-3.24978504591324,134.4959835964));
#32022=CARTESIAN_POINT('Ctrl Pts',(154.020528854465,-3.14721504744805,134.586277336873));
#32023=CARTESIAN_POINT('Ctrl Pts',(154.012764101518,-3.04074437526277,134.67241159665));
#32024=CARTESIAN_POINT('Ctrl Pts',(154.004999348571,-2.93074601686428,134.754032863099));
#32025=CARTESIAN_POINT('Ctrl Pts',(153.997242307686,-2.82085691038576,134.835573062156));
#32026=CARTESIAN_POINT('Ctrl Pts',(153.989485266801,-2.70744740224859,134.912608956533));
#32027=CARTESIAN_POINT('Ctrl Pts',(153.981728225916,-2.59092494319348,134.984826022427));
#32028=CARTESIAN_POINT('Ctrl Pts',(153.973977034675,-2.47449035463095,135.056988628869));
#32029=CARTESIAN_POINT('Ctrl Pts',(153.966225843435,-2.35494781867991,135.12433943479));
#32030=CARTESIAN_POINT('Ctrl Pts',(153.958474652195,-2.23273497333086,135.186606343374));
#32031=CARTESIAN_POINT('Ctrl Pts',(153.950726755418,-2.11057407170164,135.248846786861));
#32032=CARTESIAN_POINT('Ctrl Pts',(153.942978858641,-1.98574546563632,135.306007453546));
#32033=CARTESIAN_POINT('Ctrl Pts',(153.935230961864,-1.85871248600596,135.357861573629));
#32034=CARTESIAN_POINT('Ctrl Pts',(153.92748468578,-1.73170607893638,135.409704846948));
#32035=CARTESIAN_POINT('Ctrl Pts',(153.919738409696,-1.60249657721068,135.456243633885));
#32036=CARTESIAN_POINT('Ctrl Pts',(153.911992133612,-1.47156807171687,135.497298979915));
#32037=CARTESIAN_POINT('Ctrl Pts',(153.904245800346,-1.34063859973858,135.538354629006));
#32038=CARTESIAN_POINT('Ctrl Pts',(153.896499467081,-1.20799047172617,135.57392663944));
#32039=CARTESIAN_POINT('Ctrl Pts',(153.888753133815,-1.07412336422445,135.603885808762));
#32040=CARTESIAN_POINT('Ctrl Pts',(153.881005065812,-0.940226278112406,
135.633851687233));
#32041=CARTESIAN_POINT('Ctrl Pts',(153.873256997809,-0.805110050762888,
135.658202138023));
#32042=CARTESIAN_POINT('Ctrl Pts',(153.865508929806,-0.669284589886382,
135.676859073209));
#32043=CARTESIAN_POINT('Ctrl Pts',(153.857752627065,-0.533314772093666,
135.695535837207));
#32044=CARTESIAN_POINT('Ctrl Pts',(153.849996324323,-0.396634602959449,
135.708506944516));
#32045=CARTESIAN_POINT('Ctrl Pts',(153.842240021581,-0.259759712457097,
135.7157461608));
#32046=CARTESIAN_POINT('Ctrl Pts',(153.834479579067,-0.122811767703994,
135.722989240871));
#32047=CARTESIAN_POINT('Ctrl Pts',(153.826719136552,0.0143307147535147,
135.724494329748));
#32048=CARTESIAN_POINT('Ctrl Pts',(153.818958694038,0.151153059825974,135.720287367936));
#32049=CARTESIAN_POINT('Ctrl Pts',(153.811185793773,0.28819504427298,135.716073652735));
#32050=CARTESIAN_POINT('Ctrl Pts',(153.803412893507,0.424915474213501,135.706129591658));
#32051=CARTESIAN_POINT('Ctrl Pts',(153.795639993242,0.560804844014884,135.690533044879));
#32052=CARTESIAN_POINT('Ctrl Pts',(153.78814965748,0.691754292938122,135.67550347186));
#32053=CARTESIAN_POINT('Ctrl Pts',(153.780659321718,0.821931750613826,135.655225289794));
#32054=CARTESIAN_POINT('Ctrl Pts',(153.773168985956,0.950892974261133,135.629812473507));
#32055=CARTESIAN_POINT('Ctrl Pts',(153.765394651837,1.08474380190108,135.603436122565));
#32056=CARTESIAN_POINT('Ctrl Pts',(153.757620317718,1.21770834708445,135.571444539663));
#32057=CARTESIAN_POINT('Ctrl Pts',(153.749845983599,1.34927876656043,135.533909208352));
#32058=CARTESIAN_POINT('Ctrl Pts',(153.742081230652,1.48068703725302,135.496420135983));
#32059=CARTESIAN_POINT('Ctrl Pts',(153.734316477705,1.61070422845986,135.453401015423));
#32060=CARTESIAN_POINT('Ctrl Pts',(153.726551724758,1.73883131113119,135.404974569413));
#32061=CARTESIAN_POINT('Ctrl Pts',(153.718794683873,1.86683113617794,135.356596221232));
#32062=CARTESIAN_POINT('Ctrl Pts',(153.711037642988,1.99294422521703,135.302821372729));
#32063=CARTESIAN_POINT('Ctrl Pts',(153.703280602103,2.11668572338516,135.243822815954));
#32064=CARTESIAN_POINT('Ctrl Pts',(153.695529410862,2.240333907127,135.18486875045));
#32065=CARTESIAN_POINT('Ctrl Pts',(153.687778219622,2.36161370829242,135.120698985069));
#32066=CARTESIAN_POINT('Ctrl Pts',(153.680027028382,2.48005965010008,135.051534642073));
#32067=CARTESIAN_POINT('Ctrl Pts',(153.672279131605,2.59845524922262,134.982399695768));
#32068=CARTESIAN_POINT('Ctrl Pts',(153.664531234828,2.7140190476654,134.908274590725));
#32069=CARTESIAN_POINT('Ctrl Pts',(153.656783338051,2.82630981591932,134.829426565714));
#32070=CARTESIAN_POINT('Ctrl Pts',(153.649037061967,2.9385770953653,134.750595034009));
#32071=CARTESIAN_POINT('Ctrl Pts',(153.641290785883,3.04757238666269,134.667042771917));
#32072=CARTESIAN_POINT('Ctrl Pts',(153.633544509799,3.1528834673512,134.579080329519));
#32073=CARTESIAN_POINT('Ctrl Pts',(153.625798176533,3.25819532542193,134.491117237802));
#32074=CARTESIAN_POINT('Ctrl Pts',(153.618051843268,3.35982261855329,134.39874415145));
#32075=CARTESIAN_POINT('Ctrl Pts',(153.610305510003,3.45738655768207,134.302311625407));
#32076=CARTESIAN_POINT('Ctrl Pts',(153.602557442,3.55497234557872,134.205857503969));
#32077=CARTESIAN_POINT('Ctrl Pts',(153.594809373997,3.64849269074929,134.105342408655));
#32078=CARTESIAN_POINT('Ctrl Pts',(153.587061305994,3.73760627803798,134.001153130832));
#32079=CARTESIAN_POINT('Ctrl Pts',(153.579305003252,3.82681457630779,133.896853119404));
#32080=CARTESIAN_POINT('Ctrl Pts',(153.57154870051,3.91160650626362,133.788871422465));
#32081=CARTESIAN_POINT('Ctrl Pts',(153.563792397768,3.99168128562,133.677627673816));
#32082=CARTESIAN_POINT('Ctrl Pts',(153.556031955254,4.07179880329717,133.566324551029));
#32083=CARTESIAN_POINT('Ctrl Pts',(153.54827151274,4.14719393885572,133.451756233763));
#32084=CARTESIAN_POINT('Ctrl Pts',(153.540511070226,4.217610322319,133.334369754223));
#32085=CARTESIAN_POINT('Ctrl Pts',(153.53273816996,4.28813974441229,133.216794835485));
#32086=CARTESIAN_POINT('Ctrl Pts',(153.524965269695,4.35367425616248,133.096393057743));
#32087=CARTESIAN_POINT('Ctrl Pts',(153.517192369429,4.41400396329998,132.973635167841));
#32088=CARTESIAN_POINT('Ctrl Pts',(153.509702033667,4.4721405336219,132.855339836445));
#32089=CARTESIAN_POINT('Ctrl Pts',(153.502211697905,4.52544402037737,132.734857001755));
#32090=CARTESIAN_POINT('Ctrl Pts',(153.494721362143,4.57377018974149,132.612622023982));
#32091=CARTESIAN_POINT('Ctrl Pts',(153.486947028024,4.62392866050528,132.485752469874));
#32092=CARTESIAN_POINT('Ctrl Pts',(153.479172693905,4.66888382027217,132.356593400263));
#32093=CARTESIAN_POINT('Ctrl Pts',(153.471398359786,4.70842130849739,132.225610716665));
#32094=CARTESIAN_POINT('Ctrl Pts',(153.463633606839,4.7479100703018,132.094789457518));
#32095=CARTESIAN_POINT('Ctrl Pts',(153.455868853892,4.78199433350404,131.962149426815));
#32096=CARTESIAN_POINT('Ctrl Pts',(153.448104100945,4.81050761082926,131.828176806466));
#32097=CARTESIAN_POINT('Ctrl Pts',(153.44034706006,4.83899256836557,131.694337249612));
#32098=CARTESIAN_POINT('Ctrl Pts',(153.432590019175,4.86191747044678,131.559168116956));
#32099=CARTESIAN_POINT('Ctrl Pts',(153.424832978289,4.87916561601989,131.423170728948));
#32100=CARTESIAN_POINT('Ctrl Pts',(153.417081787049,4.89640075463227,131.287275897629));
#32101=CARTESIAN_POINT('Ctrl Pts',(153.409330595809,4.9079676085891,131.150554440464));
#32102=CARTESIAN_POINT('Ctrl Pts',(153.401579404569,4.91380061274046,131.013517498236));
#32103=CARTESIAN_POINT('Ctrl Pts',(153.393831507792,4.91963113770944,130.876538800363));
#32104=CARTESIAN_POINT('Ctrl Pts',(153.386083611015,4.91973264336635,130.739245273915));
#32105=CARTESIAN_POINT('Ctrl Pts',(153.378335714238,4.91409146992764,130.602152586854));
#32106=CARTESIAN_POINT('Ctrl Pts',(153.370589438154,4.90845147650081,130.465088576628));
#32107=CARTESIAN_POINT('Ctrl Pts',(153.36284316207,4.89707120938373,130.328225712614));
#32108=CARTESIAN_POINT('Ctrl Pts',(153.355096885986,4.87998912684664,130.192078669148));
#32109=CARTESIAN_POINT('Ctrl Pts',(153.34735055272,4.86290691821352,130.055930620675));
#32110=CARTESIAN_POINT('Ctrl Pts',(153.339604219455,4.84012285884581,129.920498791218));
#32111=CARTESIAN_POINT('Ctrl Pts',(153.33185788619,4.8117271358061,129.786291350253));
#32112=CARTESIAN_POINT('Ctrl Pts',(153.324109818187,4.7833250537411,129.652053854462));
#32113=CARTESIAN_POINT('Ctrl Pts',(153.316361750184,4.74930888824381,129.519041675201));
#32114=CARTESIAN_POINT('Ctrl Pts',(153.308613682181,4.70981956866713,129.387751040759));
#32115=CARTESIAN_POINT('Ctrl Pts',(153.300857379439,4.67028827937163,129.256320869069));
#32116=CARTESIAN_POINT('Ctrl Pts',(153.293101076697,4.62527232883565,129.12661627217));
#32117=CARTESIAN_POINT('Ctrl Pts',(153.285344773955,4.57496218668788,128.999117129037));
#32118=CARTESIAN_POINT('Ctrl Pts',(153.277584331441,4.52462519250233,128.871549935773));
#32119=CARTESIAN_POINT('Ctrl Pts',(153.269823888927,4.46898853484091,128.746190898957));
#32120=CARTESIAN_POINT('Ctrl Pts',(153.262063446413,4.40828974032399,128.623497341738));
#32121=CARTESIAN_POINT('Ctrl Pts',(153.254290546147,4.34749350671365,128.500606825929));
#32122=CARTESIAN_POINT('Ctrl Pts',(153.246517645882,4.28161908551396,128.380390683314));
#32123=CARTESIAN_POINT('Ctrl Pts',(153.238744745616,4.21094907639826,128.263279954053));
#32124=CARTESIAN_POINT('Ctrl Pts',(153.231254409854,4.14284810012079,128.150426494784));
#32125=CARTESIAN_POINT('Ctrl Pts',(153.223764074092,4.07029431564631,128.040456846637));
#32126=CARTESIAN_POINT('Ctrl Pts',(153.21627373833,3.99357604194475,127.933727680441));
#32127=CARTESIAN_POINT('Ctrl Pts',(153.208499404211,3.91394897157787,127.82295184547));
#32128=CARTESIAN_POINT('Ctrl Pts',(153.200725070092,3.82958315028404,127.715316164351));
#32129=CARTESIAN_POINT('Ctrl Pts',(153.192950735973,3.74075468709309,127.611252815833));
#32130=CARTESIAN_POINT('Ctrl Pts',(153.185185983026,3.65203569704401,127.50731771609));
#32131=CARTESIAN_POINT('Ctrl Pts',(153.177421230079,3.55886525946724,127.406946483633));
#32132=CARTESIAN_POINT('Ctrl Pts',(153.169656477132,3.46156242253508,127.31054198212));
#32133=CARTESIAN_POINT('Ctrl Pts',(153.161899436247,3.36435622815283,127.214233230916));
#32134=CARTESIAN_POINT('Ctrl Pts',(153.154142395362,3.26302607820749,127.121883643638));
#32135=CARTESIAN_POINT('Ctrl Pts',(153.146385354477,3.15793066802292,127.033862380136));
#32136=CARTESIAN_POINT('Ctrl Pts',(153.138634163237,3.05291451110415,126.945907494153));
#32137=CARTESIAN_POINT('Ctrl Pts',(153.130882971996,2.94413904413805,126.862274685124));
#32138=CARTESIAN_POINT('Ctrl Pts',(153.123131780756,2.83199886477588,126.783295398944));
#32139=CARTESIAN_POINT('Ctrl Pts',(153.115383883979,2.71990634798167,126.704349681068));
#32140=CARTESIAN_POINT('Ctrl Pts',(153.107635987202,2.60445228211273,126.630053776858));
#32141=CARTESIAN_POINT('Ctrl Pts',(153.099888090425,2.48606312978482,126.560697909807));
#32142=CARTESIAN_POINT('Ctrl Pts',(153.092141814341,2.36769874191547,126.491356550508));
#32143=CARTESIAN_POINT('Ctrl Pts',(153.084395538257,2.2464008259076,126.426953370479));
#32144=CARTESIAN_POINT('Ctrl Pts',(153.076649262173,2.12262317949043,126.367734207737));
#32145=CARTESIAN_POINT('Ctrl Pts',(153.068902928908,1.99884461937461,126.308514607853));
#32146=CARTESIAN_POINT('Ctrl Pts',(153.061156595642,1.8725866450032,126.254479270349));
#32147=CARTESIAN_POINT('Ctrl Pts',(153.053410262377,1.74432554205993,126.20582699631));
#32148=CARTESIAN_POINT('Ctrl Pts',(153.045662194374,1.61603571593231,126.157163826933));
#32149=CARTESIAN_POINT('Ctrl Pts',(153.037914126371,1.48574223407726,126.11388625846));
#32150=CARTESIAN_POINT('Ctrl Pts',(153.030166058368,1.35393876316582,126.076143946548));
#32151=CARTESIAN_POINT('Ctrl Pts',(153.022409755626,1.2219952099567,126.038361521657));
#32152=CARTESIAN_POINT('Ctrl Pts',(153.014653452884,1.08853883831998,126.006126212926));
#32153=CARTESIAN_POINT('Ctrl Pts',(153.006897150143,0.954076337514759,125.979537159169));
#32154=CARTESIAN_POINT('Ctrl Pts',(152.999136707628,0.819542070024268,125.952933914034));
#32155=CARTESIAN_POINT('Ctrl Pts',(152.991376265114,0.684000989532066,125.931982988373));
#32156=CARTESIAN_POINT('Ctrl Pts',(152.9836158226,0.547966243895212,125.916731738646));
#32157=CARTESIAN_POINT('Ctrl Pts',(152.975842922335,0.411713123208111,125.901456006259));
#32158=CARTESIAN_POINT('Ctrl Pts',(152.968070022069,0.274965143996772,125.891898260949));
#32159=CARTESIAN_POINT('Ctrl Pts',(152.960297121804,0.138237704583411,125.888053731342));
#32160=CARTESIAN_POINT('Ctrl Pts',(152.952806786042,0.00648065198873604,
125.884348960071));
#32161=CARTESIAN_POINT('Ctrl Pts',(152.94531645028,-0.12525702023226,125.885949232798));
#32162=CARTESIAN_POINT('Ctrl Pts',(152.937826114518,-0.25651939136301,125.892804767903));
#32163=CARTESIAN_POINT('Ctrl Pts',(152.930051780399,-0.392758615191718,
125.899920232706));
#32164=CARTESIAN_POINT('Ctrl Pts',(152.92227744628,-0.52891734927641,125.912719872733));
#32165=CARTESIAN_POINT('Ctrl Pts',(152.914503112161,-0.6644827457224,125.931204992805));
#32166=CARTESIAN_POINT('Ctrl Pts',(152.906738359213,-0.799881069933328,
125.949667331619));
#32167=CARTESIAN_POINT('Ctrl Pts',(152.898973606266,-0.934687127784761,
125.97380115663));
#32168=CARTESIAN_POINT('Ctrl Pts',(152.891208853319,-1.06838952534121,126.003555801221));
#32169=CARTESIAN_POINT('Ctrl Pts',(152.883451812434,-1.20195912779154,126.03328089308));
#32170=CARTESIAN_POINT('Ctrl Pts',(152.875694771549,-1.33442687221691,126.06861561036));
#32171=CARTESIAN_POINT('Ctrl Pts',(152.867937730664,-1.46528829039603,126.109457712443));
#32172=CARTESIAN_POINT('Ctrl Pts',(152.860186539424,-1.59605102496232,126.15026901518));
#32173=CARTESIAN_POINT('Ctrl Pts',(152.852435348184,-1.72520947268672,126.196579320095));
#32174=CARTESIAN_POINT('Ctrl Pts',(152.844684156944,-1.85227148908113,126.248235795611));
#32175=CARTESIAN_POINT('Ctrl Pts',(152.836936260167,-1.97927950072866,126.299870315746));
#32176=CARTESIAN_POINT('Ctrl Pts',(152.82918836339,-2.1041924918347,126.356846340187));
#32177=CARTESIAN_POINT('Ctrl Pts',(152.821440466612,-2.22653577569419,126.418961946743));
#32178=CARTESIAN_POINT('Ctrl Pts',(152.813694190528,-2.34885346797617,126.481064560054));
#32179=CARTESIAN_POINT('Ctrl Pts',(152.805947914444,-2.46860217379645,126.548304440186));
#32180=CARTESIAN_POINT('Ctrl Pts',(152.79820163836,-2.58532977391074,126.620432675712));
#32181=CARTESIAN_POINT('Ctrl Pts',(152.790455305095,-2.70205823568137,126.692561443671));
#32182=CARTESIAN_POINT('Ctrl Pts',(152.782708971829,-2.81576521465385,126.769578433514));
#32183=CARTESIAN_POINT('Ctrl Pts',(152.774962638564,-2.92602600979875,126.851190389448));
#32184=CARTESIAN_POINT('Ctrl Pts',(152.767214570561,-3.03631149708442,126.932820621813));
#32185=CARTESIAN_POINT('Ctrl Pts',(152.759466502558,-3.14314895066318,127.019047635328));
#32186=CARTESIAN_POINT('Ctrl Pts',(152.751718434555,-3.24614562209954,127.109536986779));
#32187=CARTESIAN_POINT('Ctrl Pts',(152.743962131813,-3.34925175962384,127.200122511389));
#32188=CARTESIAN_POINT('Ctrl Pts',(152.736205829071,-3.44850866653318,127.294979164767));
#32189=CARTESIAN_POINT('Ctrl Pts',(152.728449526329,-3.54355905661403,127.393734241841));
#32190=CARTESIAN_POINT('Ctrl Pts',(152.720689083815,-3.63866017795002,127.492542027474));
#32191=CARTESIAN_POINT('Ctrl Pts',(152.712928641301,-3.72955004985057,127.59525209014));
#32192=CARTESIAN_POINT('Ctrl Pts',(152.705168198787,-3.81591146103389,127.701458301338));
#32193=CARTESIAN_POINT('Ctrl Pts',(152.697395298521,-3.90241150722139,127.807835004176));
#32194=CARTESIAN_POINT('Ctrl Pts',(152.689622398256,-3.98436833205943,127.917718757189));
#32195=CARTESIAN_POINT('Ctrl Pts',(152.681849497991,-4.06150736445639,128.03067336213));
#32196=CARTESIAN_POINT('Ctrl Pts',(152.674359162229,-4.13584219872345,128.139521782665));
#32197=CARTESIAN_POINT('Ctrl Pts',(152.666868826467,-4.20570327366286,128.251221403806));
#32198=CARTESIAN_POINT('Ctrl Pts',(152.659378490705,-4.270886035677,128.365361738362));
#32199=CARTESIAN_POINT('Ctrl Pts',(152.651270040263,-4.34144778513971,128.488921118812));
#32200=CARTESIAN_POINT('Ctrl Pts',(152.643161589822,-4.40673476032177,128.615703962037));
#32201=CARTESIAN_POINT('Ctrl Pts',(152.63505313938,-4.46645369419116,128.745240791003));
#32202=CARTESIAN_POINT('Ctrl Pts',(152.62664262552,-4.52839733246053,128.879603244518));
#32203=CARTESIAN_POINT('Ctrl Pts',(152.618232111659,-4.58434981356175,129.016928573631));
#32204=CARTESIAN_POINT('Ctrl Pts',(152.609821597798,-4.63403356683683,129.15666041306));
#32205=CARTESIAN_POINT('Ctrl Pts',(152.601411083937,-4.68371732011193,129.296392252489));
#32206=CARTESIAN_POINT('Ctrl Pts',(152.593000570076,-4.72713212829472,129.43853024232));
#32207=CARTESIAN_POINT('Ctrl Pts',(152.584590056215,-4.76405452823404,129.582490119308));
#32208=CARTESIAN_POINT('Ctrl Pts',(154.334814618358,-4.76405452823406,129.582490119308));
#32209=CARTESIAN_POINT('Ctrl Pts',(154.333231156766,-4.77096212897711,129.609422749768));
#32210=CARTESIAN_POINT('Ctrl Pts',(154.331647695174,-4.77763918936648,129.636405591418));
#32211=CARTESIAN_POINT('Ctrl Pts',(154.330064233582,-4.78408511039337,129.663434362713));
#32212=CARTESIAN_POINT('Ctrl Pts',(154.319196767322,-4.82832415579875,129.848935710869));
#32213=CARTESIAN_POINT('Ctrl Pts',(154.308329301063,-4.86178997871693,130.037097735734));
#32214=CARTESIAN_POINT('Ctrl Pts',(154.297461834803,-4.88422663702635,130.226854582392));
#32215=CARTESIAN_POINT('Ctrl Pts',(154.287250081402,-4.90530952942634,130.405162025733));
#32216=CARTESIAN_POINT('Ctrl Pts',(154.277038328001,-4.91665437759487,130.584877919004));
#32217=CARTESIAN_POINT('Ctrl Pts',(154.266826574599,-4.91809324692398,130.76509387514));
#32218=CARTESIAN_POINT('Ctrl Pts',(154.266170861741,-4.9181856390023,130.776665827086));
#32219=CARTESIAN_POINT('Ctrl Pts',(154.265515148883,-4.91823720272719,130.788239831339));
#32220=CARTESIAN_POINT('Ctrl Pts',(154.264859436025,-4.91824789998526,130.799815643358));
#32221=CARTESIAN_POINT('',(154.610140564044,-4.91824949728461,130.806584344098));
#32222=CARTESIAN_POINT('Ctrl Pts',(154.680281909745,-4.76405452823406,129.582490119308));
#32223=CARTESIAN_POINT('Ctrl Pts',(154.672605721356,-4.79779352713309,129.714037963955));
#32224=CARTESIAN_POINT('Ctrl Pts',(154.664929532968,-4.82605516076123,129.846888324421));
#32225=CARTESIAN_POINT('Ctrl Pts',(154.657253344579,-4.8487630813234,129.980540465048));
#32226=CARTESIAN_POINT('Ctrl Pts',(154.64940121449,-4.87199147766924,130.117255973033));
#32227=CARTESIAN_POINT('Ctrl Pts',(154.641549084401,-4.88940843558675,130.254810015955));
#32228=CARTESIAN_POINT('Ctrl Pts',(154.633696954311,-4.9009885182294,130.39266339061));
#32229=CARTESIAN_POINT('Ctrl Pts',(154.625844824222,-4.91256860087204,130.530516765264));
#32230=CARTESIAN_POINT('Ctrl Pts',(154.617992694133,-4.91831185401273,130.668669028351));
#32231=CARTESIAN_POINT('Ctrl Pts',(154.610140564044,-4.91824949728461,130.806584344098));
#32232=CARTESIAN_POINT('Ctrl Pts',(154.610140564008,-4.91824949728433,130.806584344722));
#32233=CARTESIAN_POINT('Ctrl Pts',(154.603067996417,-4.91819333134041,130.930807374822));
#32234=CARTESIAN_POINT('Ctrl Pts',(154.595995428826,-4.91343124279772,131.054919660382));
#32235=CARTESIAN_POINT('Ctrl Pts',(154.588922861235,-4.90398568483504,131.178669935421));
#32236=CARTESIAN_POINT('Ctrl Pts',(154.581148527116,-4.89360290339115,131.314699174184));
#32237=CARTESIAN_POINT('Ctrl Pts',(154.573374192997,-4.87753951515781,131.450511541849));
#32238=CARTESIAN_POINT('Ctrl Pts',(154.565599858878,-4.85580652262352,131.585594306898));
#32239=CARTESIAN_POINT('Ctrl Pts',(154.557835105931,-4.83410031406017,131.720510594511));
#32240=CARTESIAN_POINT('Ctrl Pts',(154.550070352984,-4.80673846530788,131.854698686293));
#32241=CARTESIAN_POINT('Ctrl Pts',(154.542305600037,-4.7737839004359,131.987648551435));
#32242=CARTESIAN_POINT('Ctrl Pts',(154.534548559152,-4.74086206650237,132.120466368896));
#32243=CARTESIAN_POINT('Ctrl Pts',(154.526791518267,-4.70235866413532,132.252048030097));
#32244=CARTESIAN_POINT('Ctrl Pts',(154.519034477382,-4.65838801035674,132.381891665585));
#32245=CARTESIAN_POINT('Ctrl Pts',(154.511283286142,-4.6144505151903,132.511637384977));
#32246=CARTESIAN_POINT('Ctrl Pts',(154.503532094902,-4.5650540998833,132.639647318632));
#32247=CARTESIAN_POINT('Ctrl Pts',(154.495780903662,-4.51036336211174,132.765433131325));
#32248=CARTESIAN_POINT('Ctrl Pts',(154.488033006885,-4.45569586936251,132.891165481692));
#32249=CARTESIAN_POINT('Ctrl Pts',(154.480285110107,-4.39573868524584,133.014675233456));
#32250=CARTESIAN_POINT('Ctrl Pts',(154.47253721333,-4.33070506497477,133.135492682187));
#32251=CARTESIAN_POINT('Ctrl Pts',(154.464790937246,-4.2656850483351,133.256284858511));
#32252=CARTESIAN_POINT('Ctrl Pts',(154.457044661162,-4.19559089287126,133.37438550794));
#32253=CARTESIAN_POINT('Ctrl Pts',(154.449298385078,-4.12068228794628,133.489348614617));
#32254=CARTESIAN_POINT('Ctrl Pts',(154.441552051813,-4.04577313006293,133.604312569924));
#32255=CARTESIAN_POINT('Ctrl Pts',(154.433805718547,-3.96604966523966,133.7161386087));
#32256=CARTESIAN_POINT('Ctrl Pts',(154.426059385282,-3.881815256472,133.824409189546));
#32257=CARTESIAN_POINT('Ctrl Pts',(154.418311317279,-3.7975619839926,133.932704016839));
#32258=CARTESIAN_POINT('Ctrl Pts',(154.410563249276,-3.70879599742448,134.037441493301));
#32259=CARTESIAN_POINT('Ctrl Pts',(154.402815181273,-3.61586106855026,134.138237009312));
#32260=CARTESIAN_POINT('Ctrl Pts',(154.395058878531,-3.5228273673277,134.239139651998));
#32261=CARTESIAN_POINT('Ctrl Pts',(154.38730257579,-3.42561613823736,134.336091677238));
#32262=CARTESIAN_POINT('Ctrl Pts',(154.379546273048,-3.32460855290637,134.428744845603));
#32263=CARTESIAN_POINT('Ctrl Pts',(154.371785830534,-3.2235470567857,134.521447465754));
#32264=CARTESIAN_POINT('Ctrl Pts',(154.364025388019,-3.11868546576502,134.609846405316));
#32265=CARTESIAN_POINT('Ctrl Pts',(154.356264945505,-3.0104374035875,134.693634290321));
#32266=CARTESIAN_POINT('Ctrl Pts',(154.34849204524,-2.90201557201087,134.777556679077));
#32267=CARTESIAN_POINT('Ctrl Pts',(154.340719144974,-2.79019672498729,134.856852995285));
#32268=CARTESIAN_POINT('Ctrl Pts',(154.332946244709,-2.67542352410029,134.931259214478));
#32269=CARTESIAN_POINT('Ctrl Pts',(154.325455908947,-2.56482261816187,135.002960580185));
#32270=CARTESIAN_POINT('Ctrl Pts',(154.317965573185,-2.45147869058044,135.070121053944));
#32271=CARTESIAN_POINT('Ctrl Pts',(154.310475237423,-2.33580701906053,135.132545991624));
#32272=CARTESIAN_POINT('Ctrl Pts',(154.302700903304,-2.21574962095726,135.197337789789));
#32273=CARTESIAN_POINT('Ctrl Pts',(154.294926569185,-2.09280417592404,135.257233108455));
#32274=CARTESIAN_POINT('Ctrl Pts',(154.287152235066,-1.96740800662316,135.311964060414));
#32275=CARTESIAN_POINT('Ctrl Pts',(154.279387482119,-1.84216637689392,135.366627561367));
#32276=CARTESIAN_POINT('Ctrl Pts',(154.271622729171,-1.71448038727301,135.416139204418));
#32277=CARTESIAN_POINT('Ctrl Pts',(154.263857976224,-1.58481315312012,135.460276245259));
#32278=CARTESIAN_POINT('Ctrl Pts',(154.256100935339,-1.4552747062923,135.504369448569));
#32279=CARTESIAN_POINT('Ctrl Pts',(154.248343894454,-1.32375929865986,135.543098547625));
#32280=CARTESIAN_POINT('Ctrl Pts',(154.240586853569,-1.19075095835084,135.576288447876));
#32281=CARTESIAN_POINT('Ctrl Pts',(154.232835662329,-1.05784292066591,135.609453319365));
#32282=CARTESIAN_POINT('Ctrl Pts',(154.225084471089,-0.923444569003787,
135.637087212145));
#32283=CARTESIAN_POINT('Ctrl Pts',(154.217333279849,-0.788055722685048,
135.659064649785));
#32284=CARTESIAN_POINT('Ctrl Pts',(154.209585383072,-0.652724420237518,
135.681032746428));
#32285=CARTESIAN_POINT('Ctrl Pts',(154.201837486295,-0.516403845549539,
135.697349107077));
#32286=CARTESIAN_POINT('Ctrl Pts',(154.194089589518,-0.379604443913512,
135.707939262664));
#32287=CARTESIAN_POINT('Ctrl Pts',(154.186343313434,-0.242833657763301,
135.718527203019));
#32288=CARTESIAN_POINT('Ctrl Pts',(154.17859703735,-0.105584633441303,135.723391290643));
#32289=CARTESIAN_POINT('Ctrl Pts',(154.170850761266,0.0316270148360211,
135.722508927086));
#32290=CARTESIAN_POINT('Ctrl Pts',(154.163104428,0.168839675978609,135.721626557015));
#32291=CARTESIAN_POINT('Ctrl Pts',(154.155358094735,0.306014569568859,135.714997653635));
#32292=CARTESIAN_POINT('Ctrl Pts',(154.147611761469,0.442636431096155,135.7026517535));
#32293=CARTESIAN_POINT('Ctrl Pts',(154.139863693466,0.579288888141884,135.690303088586));
#32294=CARTESIAN_POINT('Ctrl Pts',(154.132115625464,0.715387677377987,135.672234914485));
#32295=CARTESIAN_POINT('Ctrl Pts',(154.124367557461,0.850423398793978,135.648528565241));
#32296=CARTESIAN_POINT('Ctrl Pts',(154.116611254719,0.985602637781775,135.624797020607));
#32297=CARTESIAN_POINT('Ctrl Pts',(154.108854951977,1.11971616627986,135.595415398235));
#32298=CARTESIAN_POINT('Ctrl Pts',(154.101098649235,1.25226496801818,135.560516156694));
#32299=CARTESIAN_POINT('Ctrl Pts',(154.093338206721,1.38488451504305,135.525598288376));
#32300=CARTESIAN_POINT('Ctrl Pts',(154.085577764207,1.515937297818,135.485157048113));
#32301=CARTESIAN_POINT('Ctrl Pts',(154.077817321692,1.6449411401815,135.439374286137));
#32302=CARTESIAN_POINT('Ctrl Pts',(154.070044421427,1.77415207096519,135.393518029607));
#32303=CARTESIAN_POINT('Ctrl Pts',(154.062271521162,1.90130712572271,135.342303262562));
#32304=CARTESIAN_POINT('Ctrl Pts',(154.054498620896,2.02594490379417,135.285959697057));
#32305=CARTESIAN_POINT('Ctrl Pts',(154.047008285134,2.14605178468941,135.231664362078));
#32306=CARTESIAN_POINT('Ctrl Pts',(154.039517949372,2.26382095478368,135.172606782289));
#32307=CARTESIAN_POINT('Ctrl Pts',(154.03202761361,2.3788641867144,135.109031132677));
#32308=CARTESIAN_POINT('Ctrl Pts',(154.024253279491,2.49826931775002,135.043044992987));
#32309=CARTESIAN_POINT('Ctrl Pts',(154.016478945372,2.61511596181641,134.971982390848));
#32310=CARTESIAN_POINT('Ctrl Pts',(154.008704611253,2.72894235423973,134.896066458623));
#32311=CARTESIAN_POINT('Ctrl Pts',(154.000939858306,2.84262846580737,134.820244085999));
#32312=CARTESIAN_POINT('Ctrl Pts',(153.993175105359,2.95330140964259,134.739580499134));
#32313=CARTESIAN_POINT('Ctrl Pts',(153.985410352411,3.06052345948639,134.654344931357));
#32314=CARTESIAN_POINT('Ctrl Pts',(153.977653311526,3.16763901487864,134.569194020746));
#32315=CARTESIAN_POINT('Ctrl Pts',(153.969896270641,3.27131019304707,134.479480407646));
#32316=CARTESIAN_POINT('Ctrl Pts',(153.962139229756,3.37112805296117,134.385516675746));
#32317=CARTESIAN_POINT('Ctrl Pts',(153.954388038516,3.47087063945059,134.291623802627));
#32318=CARTESIAN_POINT('Ctrl Pts',(153.946636847276,3.56676540801466,134.193487457058));
#32319=CARTESIAN_POINT('Ctrl Pts',(153.938885656036,3.65843662722632,134.091460328112));
#32320=CARTESIAN_POINT('Ctrl Pts',(153.931137759259,3.75006888372446,133.989476563417));
#32321=CARTESIAN_POINT('Ctrl Pts',(153.923389862482,3.83748090047573,133.883605594613));
#32322=CARTESIAN_POINT('Ctrl Pts',(153.915641965705,3.92033411639544,133.77423662143));
#32323=CARTESIAN_POINT('Ctrl Pts',(153.907895689621,4.00317000120849,133.664890525878));
#32324=CARTESIAN_POINT('Ctrl Pts',(153.900149413537,4.08144874602431,133.552048192795));
#32325=CARTESIAN_POINT('Ctrl Pts',(153.892403137453,4.15487263604879,133.436131208008));
#32326=CARTESIAN_POINT('Ctrl Pts',(153.884656804187,4.22829706807172,133.320213367548));
#32327=CARTESIAN_POINT('Ctrl Pts',(153.876910470922,4.29686636458563,133.201221160378));
#32328=CARTESIAN_POINT('Ctrl Pts',(153.869164137657,4.360326862478,133.079604058355));
#32329=CARTESIAN_POINT('Ctrl Pts',(153.861416069654,4.42380157190886,132.957959721025));
#32330=CARTESIAN_POINT('Ctrl Pts',(153.853668001651,4.48216502530064,132.833689665681));
#32331=CARTESIAN_POINT('Ctrl Pts',(153.845919933648,4.53521030813904,132.707266428017));
#32332=CARTESIAN_POINT('Ctrl Pts',(153.838163630906,4.58831196813531,132.580708826232));
#32333=CARTESIAN_POINT('Ctrl Pts',(153.830407328164,4.63608401516158,132.451993831836));
#32334=CARTESIAN_POINT('Ctrl Pts',(153.822651025422,4.67836815987875,132.321612878442));
#32335=CARTESIAN_POINT('Ctrl Pts',(153.814890582908,4.72067487291712,132.191162336807));
#32336=CARTESIAN_POINT('Ctrl Pts',(153.807130140394,4.75748774236063,132.059044440857));
#32337=CARTESIAN_POINT('Ctrl Pts',(153.79936969788,4.78869913596625,131.925763153543));
#32338=CARTESIAN_POINT('Ctrl Pts',(153.791596797614,4.8199606328717,131.792267911275));
#32339=CARTESIAN_POINT('Ctrl Pts',(153.783823897349,4.84560261191078,131.657605929912));
#32340=CARTESIAN_POINT('Ctrl Pts',(153.776050997083,4.86556893801303,131.522289563871));
#32341=CARTESIAN_POINT('Ctrl Pts',(153.768560661321,4.88480943786941,131.391892288577));
#32342=CARTESIAN_POINT('Ctrl Pts',(153.761070325559,4.89877973650338,131.260887685943));
#32343=CARTESIAN_POINT('Ctrl Pts',(153.753579989797,4.90747541887456,131.129734365189));
#32344=CARTESIAN_POINT('Ctrl Pts',(153.745805655678,4.9165008006858,130.993608326416));
#32345=CARTESIAN_POINT('Ctrl Pts',(153.738031321559,4.91987228616429,130.856890863237));
#32346=CARTESIAN_POINT('Ctrl Pts',(153.73025698744,4.91752800780147,130.720091079843));
#32347=CARTESIAN_POINT('Ctrl Pts',(153.722492234493,4.91518661855221,130.583459889955));
#32348=CARTESIAN_POINT('Ctrl Pts',(153.714727481546,4.9071434878911,130.446746968868));
#32349=CARTESIAN_POINT('Ctrl Pts',(153.706962728598,4.89338852770775,130.31046611527));
#32350=CARTESIAN_POINT('Ctrl Pts',(153.699205687713,4.87964722914476,130.174320617737));
#32351=CARTESIAN_POINT('Ctrl Pts',(153.691448646828,4.86020542973101,130.038606720166));
#32352=CARTESIAN_POINT('Ctrl Pts',(153.683691605943,4.83510507236268,129.903837435348));
#32353=CARTESIAN_POINT('Ctrl Pts',(153.675940414703,4.81002364336909,129.769169781096));
#32354=CARTESIAN_POINT('Ctrl Pts',(153.668189223463,4.77929222124466,129.635445704528));
#32355=CARTESIAN_POINT('Ctrl Pts',(153.660438032223,4.74300444128178,129.503171956195));
#32356=CARTESIAN_POINT('Ctrl Pts',(153.652690135446,4.70673208459338,129.370954427733));
#32357=CARTESIAN_POINT('Ctrl Pts',(153.644942238669,4.664908170328,129.240186377722));
#32358=CARTESIAN_POINT('Ctrl Pts',(153.637194341892,4.61767714270585,129.111363019153));
#32359=CARTESIAN_POINT('Ctrl Pts',(153.629448065808,4.5704559947965,128.982566607653));
#32360=CARTESIAN_POINT('Ctrl Pts',(153.621701789724,4.51783011774968,128.855714445311));
#32361=CARTESIAN_POINT('Ctrl Pts',(153.61395551364,4.45999328154526,128.731284885454));
#32362=CARTESIAN_POINT('Ctrl Pts',(153.606209180374,4.40215601840248,128.606854407086));
#32363=CARTESIAN_POINT('Ctrl Pts',(153.598462847109,4.33910788414023,128.484846921424));
#32364=CARTESIAN_POINT('Ctrl Pts',(153.590716513844,4.27108992105236,128.365718792946));
#32365=CARTESIAN_POINT('Ctrl Pts',(153.582968445841,4.20305672581325,128.24656398655));
#32366=CARTESIAN_POINT('Ctrl Pts',(153.575220377838,4.13005168090679,128.130290159894));
#32367=CARTESIAN_POINT('Ctrl Pts',(153.567472309835,4.05236050164516,128.017326813105));
#32368=CARTESIAN_POINT('Ctrl Pts',(153.559716007093,3.97458675127365,127.904243407527));
#32369=CARTESIAN_POINT('Ctrl Pts',(153.551959704351,3.89211713940521,127.79447783288));
#32370=CARTESIAN_POINT('Ctrl Pts',(153.544203401609,3.80527956380148,127.688428894339));
#32371=CARTESIAN_POINT('Ctrl Pts',(153.536442959095,3.71839564036896,127.582323354286));
#32372=CARTESIAN_POINT('Ctrl Pts',(153.528682516581,3.62713936787112,127.479938694708));
#32373=CARTESIAN_POINT('Ctrl Pts',(153.520922074067,3.53187656675667,127.381637873946));
#32374=CARTESIAN_POINT('Ctrl Pts',(153.513149173801,3.43646084133686,127.283179251979));
#32375=CARTESIAN_POINT('Ctrl Pts',(153.505376273536,3.33702601860097,127.188817838566));
#32376=CARTESIAN_POINT('Ctrl Pts',(153.49760337327,3.23397281445536,127.09887780181));
#32377=CARTESIAN_POINT('Ctrl Pts',(153.490113037508,3.13466585385538,127.012207311935));
#32378=CARTESIAN_POINT('Ctrl Pts',(153.482622701746,3.03199925907132,126.929642516345));
#32379=CARTESIAN_POINT('Ctrl Pts',(153.475132365984,2.92635648459142,126.851435019026));
#32380=CARTESIAN_POINT('Ctrl Pts',(153.467358031865,2.816708232208,126.770262260676));
#32381=CARTESIAN_POINT('Ctrl Pts',(153.459583697746,2.70350632864995,126.6935266061));
#32382=CARTESIAN_POINT('Ctrl Pts',(153.451809363627,2.5871456567919,126.621555289435));
#32383=CARTESIAN_POINT('Ctrl Pts',(153.44404461068,2.47092838906247,126.549672670985));
#32384=CARTESIAN_POINT('Ctrl Pts',(153.436279857733,2.35156042805369,126.482542911357));
#32385=CARTESIAN_POINT('Ctrl Pts',(153.428515104785,2.2294685942844,126.420452218706));
#32386=CARTESIAN_POINT('Ctrl Pts',(153.4207580639,2.10749802384572,126.358423195405));
#32387=CARTESIAN_POINT('Ctrl Pts',(153.413001023015,1.98280931072624,126.301423455239));
#32388=CARTESIAN_POINT('Ctrl Pts',(153.40524398213,1.85585673827628,126.249695006405));
#32389=CARTESIAN_POINT('Ctrl Pts',(153.39749279089,1.72899990174875,126.198005566396));
#32390=CARTESIAN_POINT('Ctrl Pts',(153.38974159965,1.59988296455461,126.151579652412));
#32391=CARTESIAN_POINT('Ctrl Pts',(153.38199040841,1.46898288244637,126.110612397478));
#32392=CARTESIAN_POINT('Ctrl Pts',(153.374242511633,1.33813843636481,126.06966255472));
#32393=CARTESIAN_POINT('Ctrl Pts',(153.366494614856,1.20551272508072,126.034166873089));
#32394=CARTESIAN_POINT('Ctrl Pts',(153.358746718079,1.07160046093737,126.004271502287));
#32395=CARTESIAN_POINT('Ctrl Pts',(153.351000441995,0.937716208352806,125.974382384953));
#32396=CARTESIAN_POINT('Ctrl Pts',(153.343254165911,0.802546319532186,125.950091333472));
#32397=CARTESIAN_POINT('Ctrl Pts',(153.335507889826,0.666597984084025,125.931493885332));
#32398=CARTESIAN_POINT('Ctrl Pts',(153.327761556561,0.530648645096227,125.912896299909));
#32399=CARTESIAN_POINT('Ctrl Pts',(153.320015223296,0.393921235372095,125.899992454681));
#32400=CARTESIAN_POINT('Ctrl Pts',(153.31226889003,0.256929996519377,125.892826230087));
#32401=CARTESIAN_POINT('Ctrl Pts',(153.304520822027,0.119908079428549,125.885658400667));
#32402=CARTESIAN_POINT('Ctrl Pts',(153.296772754024,-0.0173773940019696,
125.884230769104));
#32403=CARTESIAN_POINT('Ctrl Pts',(153.289024686021,-0.154410637047434,
125.888535110322));
#32404=CARTESIAN_POINT('Ctrl Pts',(153.28126838328,-0.291589520654324,125.892844026246));
#32405=CARTESIAN_POINT('Ctrl Pts',(153.273512080538,-0.428515246974978,
125.902897072102));
#32406=CARTESIAN_POINT('Ctrl Pts',(153.265755777796,-0.564675053171283,
125.918633942155));
#32407=CARTESIAN_POINT('Ctrl Pts',(153.257995335282,-0.700907531955895,
125.934379211449));
#32408=CARTESIAN_POINT('Ctrl Pts',(153.250234892768,-0.836372890086373,
125.955814288627));
#32409=CARTESIAN_POINT('Ctrl Pts',(153.242474450253,-0.97056802554333,125.982827586434));
#32410=CARTESIAN_POINT('Ctrl Pts',(153.234701549988,-1.10497858294505,126.009884248386));
#32411=CARTESIAN_POINT('Ctrl Pts',(153.226928649722,-1.23811446302291,126.042536932039));
#32412=CARTESIAN_POINT('Ctrl Pts',(153.219155749457,-1.36948633723559,126.08062372453));
#32413=CARTESIAN_POINT('Ctrl Pts',(153.211665413695,-1.49608251291339,126.11732596618));
#32414=CARTESIAN_POINT('Ctrl Pts',(153.204175077933,-1.6210404160491,126.159073991267));
#32415=CARTESIAN_POINT('Ctrl Pts',(153.196684742171,-1.74394109856774,126.20568118677));
#32416=CARTESIAN_POINT('Ctrl Pts',(153.188910182228,-1.87150530312345,126.254056913406));
#32417=CARTESIAN_POINT('Ctrl Pts',(153.181135622284,-1.99725717652517,126.307821103664));
#32418=CARTESIAN_POINT('Ctrl Pts',(153.173361062341,-2.12070792118543,126.366818395173));
#32419=CARTESIAN_POINT('Ctrl Pts',(153.165596135869,-2.24400569780601,126.425742583032));
#32420=CARTESIAN_POINT('Ctrl Pts',(153.157831209397,-2.365007669715,126.489886802918));
#32421=CARTESIAN_POINT('Ctrl Pts',(153.150066282924,-2.48324230409938,126.559046645475));
#32422=CARTESIAN_POINT('Ctrl Pts',(153.142309120592,-2.60135871582199,126.628137335192));
#32423=CARTESIAN_POINT('Ctrl Pts',(153.13455195826,-2.71671296144106,126.702233470816));
#32424=CARTESIAN_POINT('Ctrl Pts',(153.126794795928,-2.82885586166695,126.78108364768));
#32425=CARTESIAN_POINT('Ctrl Pts',(153.119043535151,-2.94091344493543,126.859873836287));
#32426=CARTESIAN_POINT('Ctrl Pts',(153.111292274374,-3.04976422741467,126.943410642797));
#32427=CARTESIAN_POINT('Ctrl Pts',(153.103541013597,-3.15498622263056,127.031398253917));
#32428=CARTESIAN_POINT('Ctrl Pts',(153.095793309482,-3.26015993678443,127.119345491964));
#32429=CARTESIAN_POINT('Ctrl Pts',(153.088045605367,-3.36170787752173,127.211739220715));
#32430=CARTESIAN_POINT('Ctrl Pts',(153.080297901253,-3.4592397120966,127.308242244748));
#32431=CARTESIAN_POINT('Ctrl Pts',(153.072551891767,-3.5567502138597,127.404724160998));
#32432=CARTESIAN_POINT('Ctrl Pts',(153.064805882282,-3.65024607946991,127.505313309501));
#32433=CARTESIAN_POINT('Ctrl Pts',(153.057059872797,-3.73937282004578,127.609634655108));
#32434=CARTESIAN_POINT('Ctrl Pts',(153.049313880113,-3.82849936729201,127.713955774426));
#32435=CARTESIAN_POINT('Ctrl Pts',(153.04156788743,-3.91325655476401,127.822008777284));
#32436=CARTESIAN_POINT('Ctrl Pts',(153.033821894747,-3.99332954576843,127.933384790187));
#32437=CARTESIAN_POINT('Ctrl Pts',(153.026074241422,-4.07341970340675,128.044784680696));
#32438=CARTESIAN_POINT('Ctrl Pts',(153.018326588096,-4.14882343868998,128.159508681186));
#32439=CARTESIAN_POINT('Ctrl Pts',(153.01057893477,-4.21926891751633,128.277118471633));
#32440=CARTESIAN_POINT('Ctrl Pts',(153.002824048872,-4.28978015845497,128.394838052919));
#32441=CARTESIAN_POINT('Ctrl Pts',(152.995069162973,-4.35532369948918,128.515448467746));
#32442=CARTESIAN_POINT('Ctrl Pts',(152.987314277075,-4.4156732325677,128.638485975375));
#32443=CARTESIAN_POINT('Ctrl Pts',(152.979555281955,-4.47605474414673,128.761588679118));
#32444=CARTESIAN_POINT('Ctrl Pts',(152.971796286834,-4.53123660676934,128.887120680812));
#32445=CARTESIAN_POINT('Ctrl Pts',(152.964037291714,-4.5810408449334,129.01459866704));
#32446=CARTESIAN_POINT('Ctrl Pts',(152.956268153135,-4.63091019297496,129.142243307279));
#32447=CARTESIAN_POINT('Ctrl Pts',(152.948499014556,-4.67538775094528,129.271838643228));
#32448=CARTESIAN_POINT('Ctrl Pts',(152.940729875978,-4.71434539745154,129.40288620252));
#32449=CARTESIAN_POINT('Ctrl Pts',(152.93719746275,-4.73205836580928,129.462469916612));
#32450=CARTESIAN_POINT('Ctrl Pts',(152.933665049523,-4.74863091835531,129.522353698477));
#32451=CARTESIAN_POINT('Ctrl Pts',(152.930132636296,-4.76405452823406,129.582490119308));
#32452=CARTESIAN_POINT('Origin',(213.235140564004,0.,130.804360617566));
#32453=CARTESIAN_POINT('',(150.83493632599,-4.76405452823404,129.582490119308));
#32454=CARTESIAN_POINT('',(151.179859891219,-4.76405452823403,129.582490119308));
#32455=CARTESIAN_POINT('',(213.235140564004,-4.76405452823405,129.582490119308));
#32456=CARTESIAN_POINT('',(152.514859435946,-4.91824997270806,130.804878746085));
#32457=CARTESIAN_POINT('Ctrl Pts',(152.514859435946,-4.91824997270806,130.804878746085));
#32458=CARTESIAN_POINT('Ctrl Pts',(152.506677763759,-4.91823466848991,130.95015152646));
#32459=CARTESIAN_POINT('Ctrl Pts',(152.498496091571,-4.91177859513664,131.095278734219));
#32460=CARTESIAN_POINT('Ctrl Pts',(152.490314419384,-4.89894595758979,131.23968988044));
#32461=CARTESIAN_POINT('Ctrl Pts',(152.482119495279,-4.88609253492128,131.384334930505));
#32462=CARTESIAN_POINT('Ctrl Pts',(152.473924571174,-4.8668419583285,131.528261284787));
#32463=CARTESIAN_POINT('Ctrl Pts',(152.465729647069,-4.84130974263598,131.670907233945));
#32464=CARTESIAN_POINT('Ctrl Pts',(152.457513011982,-4.81570988391617,131.813931097968));
#32465=CARTESIAN_POINT('Ctrl Pts',(152.449296376895,-4.78379516239512,131.95566745651));
#32466=CARTESIAN_POINT('Ctrl Pts',(152.441079741808,-4.74573183950992,132.095566398982));
#32467=CARTESIAN_POINT('Ctrl Pts',(152.432851336312,-4.70761399054798,132.235665748037));
#32468=CARTESIAN_POINT('Ctrl Pts',(152.424622930817,-4.66333005474041,132.373922121759));
#32469=CARTESIAN_POINT('Ctrl Pts',(152.416394525321,-4.6130950350023,132.509804038069));
#32470=CARTESIAN_POINT('Ctrl Pts',(152.408146922173,-4.56274281218702,132.646002979809));
#32471=CARTESIAN_POINT('Ctrl Pts',(152.399899319025,-4.50641186754353,132.779816091296));
#32472=CARTESIAN_POINT('Ctrl Pts',(152.391651715877,-4.44436463416552,132.910733343623));
#32473=CARTESIAN_POINT('Ctrl Pts',(152.388078099548,-4.41748009542755,132.967458676085));
#32474=CARTESIAN_POINT('Ctrl Pts',(152.38450448322,-4.3895229399061,133.023640680006));
#32475=CARTESIAN_POINT('Ctrl Pts',(152.380930866891,-4.36051705758569,133.079239527092));
#32476=CARTESIAN_POINT('Ctrl Pts',(152.373156532772,-4.29741531418191,133.200193757808));
#32477=CARTESIAN_POINT('Ctrl Pts',(152.365382198653,-4.22917717359203,133.318712059438));
#32478=CARTESIAN_POINT('Ctrl Pts',(152.357607864534,-4.15601462284397,133.434327445723));
#32479=CARTESIAN_POINT('Ctrl Pts',(152.349843111587,-4.08294223840114,133.549800346377));
#32480=CARTESIAN_POINT('Ctrl Pts',(152.34207835864,-4.00495772614946,133.662377122809));
#32481=CARTESIAN_POINT('Ctrl Pts',(152.334313605693,-3.92231973766197,133.771613713958));
#32482=CARTESIAN_POINT('Ctrl Pts',(152.326556564808,-3.83976382638955,133.880741809784));
#32483=CARTESIAN_POINT('Ctrl Pts',(152.318799523923,-3.75256387101605,133.986536012562));
#32484=CARTESIAN_POINT('Ctrl Pts',(152.311042483038,-3.661022551759,134.088579997877));
#32485=CARTESIAN_POINT('Ctrl Pts',(152.303291291798,-3.56955026452293,134.19054703103));
#32486=CARTESIAN_POINT('Ctrl Pts',(152.295540100558,-3.47374338983093,134.288769185972));
#32487=CARTESIAN_POINT('Ctrl Pts',(152.287788909318,-3.37394549867287,134.382862375912));
#32488=CARTESIAN_POINT('Ctrl Pts',(152.280041012541,-3.27419002428064,134.476915573737));
#32489=CARTESIAN_POINT('Ctrl Pts',(152.272293115763,-3.17044719108015,134.56684302932));
#32490=CARTESIAN_POINT('Ctrl Pts',(152.264545218986,-3.06309796218986,134.652296939353));
#32491=CARTESIAN_POINT('Ctrl Pts',(152.256798942902,-2.95577118844407,134.737732974271));
#32492=CARTESIAN_POINT('Ctrl Pts',(152.249052666818,-2.84483982520137,134.818697081595));
#32493=CARTESIAN_POINT('Ctrl Pts',(152.241306390734,-2.73071819255062,134.89488151537));
#32494=CARTESIAN_POINT('Ctrl Pts',(152.233560057469,-2.61659571748002,134.971066511521));
#32495=CARTESIAN_POINT('Ctrl Pts',(152.225813724203,-2.49928325117612,135.042471546646));
#32496=CARTESIAN_POINT('Ctrl Pts',(152.218067390938,-2.37922404884293,135.108832244596));
#32497=CARTESIAN_POINT('Ctrl Pts',(152.210319322935,-2.25913796008374,135.175207803564));
#32498=CARTESIAN_POINT('Ctrl Pts',(152.202571254932,-2.13630425340141,135.236536588402));
#32499=CARTESIAN_POINT('Ctrl Pts',(152.194823186929,-2.01119036303242,135.292600404626));
#32500=CARTESIAN_POINT('Ctrl Pts',(152.187066884187,-1.88594350013187,135.348723806141));
#32501=CARTESIAN_POINT('Ctrl Pts',(152.179310581445,-1.75841196988084,135.399570900957));
#32502=CARTESIAN_POINT('Ctrl Pts',(152.171554278703,-1.62908326586283,135.444971652267));
#32503=CARTESIAN_POINT('Ctrl Pts',(152.163793836189,-1.49968553522143,135.490396635324));
#32504=CARTESIAN_POINT('Ctrl Pts',(152.156033393675,-1.36848909332313,135.530369368785));
#32505=CARTESIAN_POINT('Ctrl Pts',(152.148272951161,-1.23599517511472,135.564770157678));
#32506=CARTESIAN_POINT('Ctrl Pts',(152.140500050895,-1.10328856590655,135.599226169773));
#32507=CARTESIAN_POINT('Ctrl Pts',(152.13272715063,-0.96928070066067,135.628092280804));
#32508=CARTESIAN_POINT('Ctrl Pts',(152.124954250364,-0.834482439163498,
135.651300076774));
#32509=CARTESIAN_POINT('Ctrl Pts',(152.117463914602,-0.70458443400849,135.673664210904));
#32510=CARTESIAN_POINT('Ctrl Pts',(152.10997357884,-0.573952806110955,135.69077423568));
#32511=CARTESIAN_POINT('Ctrl Pts',(152.102483243078,-0.44304592667414,135.702614731978));
#32512=CARTESIAN_POINT('Ctrl Pts',(152.094708908959,-0.307175673114855,
135.714904164292));
#32513=CARTESIAN_POINT('Ctrl Pts',(152.08693457484,-0.170578487542805,135.721555521011));
#32514=CARTESIAN_POINT('Ctrl Pts',(152.079160240721,-0.0337618428896808,
135.722494735345));
#32515=CARTESIAN_POINT('Ctrl Pts',(152.071395487774,0.102886187476517,135.723432792182));
#32516=CARTESIAN_POINT('Ctrl Pts',(152.063630734827,0.239752751578779,135.718672710891));
#32517=CARTESIAN_POINT('Ctrl Pts',(152.05586598188,0.376324440775884,135.708192076515));
#32518=CARTESIAN_POINT('Ctrl Pts',(152.048108940995,0.512760485045863,135.697721851652));
#32519=CARTESIAN_POINT('Ctrl Pts',(152.04035190011,0.648901849946454,135.681542410334));
#32520=CARTESIAN_POINT('Ctrl Pts',(152.032594859225,0.784234663907718,135.659683372484));
#32521=CARTESIAN_POINT('Ctrl Pts',(152.024843667985,0.919465422341192,135.637840818705));
#32522=CARTESIAN_POINT('Ctrl Pts',(152.017092476745,1.05388845907374,135.61032725559));
#32523=CARTESIAN_POINT('Ctrl Pts',(152.009341285505,1.186994922498,135.577224130853));
#32524=CARTESIAN_POINT('Ctrl Pts',(152.001593388727,1.32004481212471,135.544135075826));
#32525=CARTESIAN_POINT('Ctrl Pts',(151.99384549195,1.45177886278894,135.505461278448));
#32526=CARTESIAN_POINT('Ctrl Pts',(151.986097595173,1.5816985378464,135.461335257595));
#32527=CARTESIAN_POINT('Ctrl Pts',(151.978351319089,1.71159103650858,135.417218466955));
#32528=CARTESIAN_POINT('Ctrl Pts',(151.970605043005,1.83966954450535,135.367651846987));
#32529=CARTESIAN_POINT('Ctrl Pts',(151.962858766921,1.96545119631883,135.312817632709));
#32530=CARTESIAN_POINT('Ctrl Pts',(151.955112433656,2.0912337766239,135.257983013657));
#32531=CARTESIAN_POINT('Ctrl Pts',(151.94736610039,2.21471910852384,135.197880878944));
#32532=CARTESIAN_POINT('Ctrl Pts',(151.939619767125,2.33544517461206,135.13274124996));
#32533=CARTESIAN_POINT('Ctrl Pts',(151.931871699122,2.45619827646565,135.067587033408));
#32534=CARTESIAN_POINT('Ctrl Pts',(151.924123631119,2.57419053891233,134.997393263388));
#32535=CARTESIAN_POINT('Ctrl Pts',(151.916375563116,2.68898572913251,134.922435266115));
#32536=CARTESIAN_POINT('Ctrl Pts',(151.908619260374,2.80390292504701,134.847397602591));
#32537=CARTESIAN_POINT('Ctrl Pts',(151.900862957633,2.91561593321185,134.767585811067));
#32538=CARTESIAN_POINT('Ctrl Pts',(151.893106654891,3.02371819465574,134.683318124656));
#32539=CARTESIAN_POINT('Ctrl Pts',(151.885346212377,3.13187815353146,134.599005462043));
#32540=CARTESIAN_POINT('Ctrl Pts',(151.877585769862,3.23642322777542,134.510232418621));
#32541=CARTESIAN_POINT('Ctrl Pts',(151.869825327348,3.33698178488827,134.417355999493));
#32542=CARTESIAN_POINT('Ctrl Pts',(151.862052427083,3.4377017675242,134.324330486891));
#32543=CARTESIAN_POINT('Ctrl Pts',(151.854279526817,3.53442216875508,134.227188712666));
#32544=CARTESIAN_POINT('Ctrl Pts',(151.846506626552,3.62680929775357,134.126323498188));
#32545=CARTESIAN_POINT('Ctrl Pts',(151.83901629079,3.71583792190436,134.029124988319));
#32546=CARTESIAN_POINT('Ctrl Pts',(151.831525955028,3.80084265606436,133.928469286415));
#32547=CARTESIAN_POINT('Ctrl Pts',(151.824035619266,3.88156276685469,133.824733698738));
#32548=CARTESIAN_POINT('Ctrl Pts',(151.816261285147,3.96534340517948,133.717064944725));
#32549=CARTESIAN_POINT('Ctrl Pts',(151.808486951028,4.04477349533657,133.605737084644));
#32550=CARTESIAN_POINT('Ctrl Pts',(151.800712616909,4.11951642132331,133.491137034938));
#32551=CARTESIAN_POINT('Ctrl Pts',(151.792947863962,4.19416723333374,133.376678219551));
#32552=CARTESIAN_POINT('Ctrl Pts',(151.785183111014,4.26414216317996,133.2589555627));
#32553=CARTESIAN_POINT('Ctrl Pts',(151.777418358067,4.32914484261244,133.138388893783));
#32554=CARTESIAN_POINT('Ctrl Pts',(151.769661317182,4.39408296046729,133.017941973382));
#32555=CARTESIAN_POINT('Ctrl Pts',(151.761904276297,4.45405847142686,132.89465700413));
#32556=CARTESIAN_POINT('Ctrl Pts',(151.754147235412,4.50881853543756,132.768982331025));
#32557=CARTESIAN_POINT('Ctrl Pts',(151.746396044172,4.56353730445802,132.643402430169));
#32558=CARTESIAN_POINT('Ctrl Pts',(151.738644852932,4.61304829940446,132.515436769388));
#32559=CARTESIAN_POINT('Ctrl Pts',(151.730893661692,4.65714499782038,132.385557484429));
#32560=CARTESIAN_POINT('Ctrl Pts',(151.723145764915,4.70122295396318,132.25573340163));
#32561=CARTESIAN_POINT('Ctrl Pts',(151.715397868138,4.73989106509696,132.123997681761));
#32562=CARTESIAN_POINT('Ctrl Pts',(151.707649971361,4.77299135187286,131.99084138751));
#32563=CARTESIAN_POINT('Ctrl Pts',(151.699903695277,4.80608471478233,131.857712946685));
#32564=CARTESIAN_POINT('Ctrl Pts',(151.692157419193,4.83361247566719,131.723164901711));
#32565=CARTESIAN_POINT('Ctrl Pts',(151.684411143109,4.85546695340222,131.587702003501));
#32566=CARTESIAN_POINT('Ctrl Pts',(151.676664809843,4.87732159246204,131.452238105335));
#32567=CARTESIAN_POINT('Ctrl Pts',(151.668918476578,4.89350280253579,131.315859726433));
#32568=CARTESIAN_POINT('Ctrl Pts',(151.661172143312,4.90395437544017,131.179079907303));
#32569=CARTESIAN_POINT('Ctrl Pts',(151.653424075309,4.91440828890183,131.042269457282));
#32570=CARTESIAN_POINT('Ctrl Pts',(151.645676007307,4.91912998216698,130.905057777897));
#32571=CARTESIAN_POINT('Ctrl Pts',(151.637927939304,4.91811530048297,130.767960704719));
#32572=CARTESIAN_POINT('Ctrl Pts',(151.630171636562,4.91709954038319,130.63071792314));
#32573=CARTESIAN_POINT('Ctrl Pts',(151.62241533382,4.91033522944226,130.493590382665));
#32574=CARTESIAN_POINT('Ctrl Pts',(151.614659031078,4.89787035113423,130.357092145639));
#32575=CARTESIAN_POINT('Ctrl Pts',(151.606898588564,4.88539881994532,130.220521055394));
#32576=CARTESIAN_POINT('Ctrl Pts',(151.59913814605,4.86722071061565,130.08458032519));
#32577=CARTESIAN_POINT('Ctrl Pts',(151.591377703535,4.84343550520494,129.949775589953));
#32578=CARTESIAN_POINT('Ctrl Pts',(151.58360480327,4.81961211767097,129.814754454188));
#32579=CARTESIAN_POINT('Ctrl Pts',(151.575831903005,4.79016373121001,129.68087333958));
#32580=CARTESIAN_POINT('Ctrl Pts',(151.568059002739,4.75524046952243,129.548625319218));
#32581=CARTESIAN_POINT('Ctrl Pts',(151.560568666977,4.72158675636345,129.421184847509));
#32582=CARTESIAN_POINT('Ctrl Pts',(151.553078331215,4.68284939880394,129.29526109167));
#32583=CARTESIAN_POINT('Ctrl Pts',(151.545587995453,4.63920490252708,129.171277357328));
#32584=CARTESIAN_POINT('Ctrl Pts',(151.537813661334,4.59390561190859,129.042592742015));
#32585=CARTESIAN_POINT('Ctrl Pts',(151.530039327215,4.54317623417197,128.915590529881));
#32586=CARTESIAN_POINT('Ctrl Pts',(151.522264993096,4.48716034390543,128.790763063291));
#32587=CARTESIAN_POINT('Ctrl Pts',(151.514500240149,4.43121348821737,128.666089435397));
#32588=CARTESIAN_POINT('Ctrl Pts',(151.506735487202,4.3699932417442,128.543585573561));
#32589=CARTESIAN_POINT('Ctrl Pts',(151.498970734254,4.30369262457101,128.423727748829));
#32590=CARTESIAN_POINT('Ctrl Pts',(151.491213693369,4.23745785810548,128.303988968578));
#32591=CARTESIAN_POINT('Ctrl Pts',(151.483456652484,4.16615295051874,128.186891335329));
#32592=CARTESIAN_POINT('Ctrl Pts',(151.475699611599,4.09001844093084,128.072889912004));
#32593=CARTESIAN_POINT('Ctrl Pts',(151.467948420359,4.01394134496887,127.958974458038));
#32594=CARTESIAN_POINT('Ctrl Pts',(151.460197229119,3.9330421125199,127.848150890379));
#32595=CARTESIAN_POINT('Ctrl Pts',(151.452446037879,3.84760633432665,127.740848163119));
#32596=CARTESIAN_POINT('Ctrl Pts',(151.444698141102,3.76220686861815,127.633591042382));
#32597=CARTESIAN_POINT('Ctrl Pts',(151.436950244325,3.67227493513176,127.529852090934));
#32598=CARTESIAN_POINT('Ctrl Pts',(151.429202347548,3.57813828711793,127.430029652654));
#32599=CARTESIAN_POINT('Ctrl Pts',(151.421456071464,3.48402133046152,127.330228095077));
#32600=CARTESIAN_POINT('Ctrl Pts',(151.41370979538,3.38570167678715,127.234341705391));
#32601=CARTESIAN_POINT('Ctrl Pts',(151.405963519296,3.28354578305581,127.142733908974));
#32602=CARTESIAN_POINT('Ctrl Pts',(151.39821718603,3.1813891352329,127.051125436329));
#32603=CARTESIAN_POINT('Ctrl Pts',(151.390470852765,3.07539648191876,126.963795880994));
#32604=CARTESIAN_POINT('Ctrl Pts',(151.382724519499,2.96596907672791,126.881069843433));
#32605=CARTESIAN_POINT('Ctrl Pts',(151.374976451496,2.85651716602838,126.79832527995));
#32606=CARTESIAN_POINT('Ctrl Pts',(151.367228383494,2.74362928466882,126.720186521392));
#32607=CARTESIAN_POINT('Ctrl Pts',(151.359480315491,2.62773717397821,126.646935884995));
#32608=CARTESIAN_POINT('Ctrl Pts',(151.351724012749,2.51172189177319,126.57360739695));
#32609=CARTESIAN_POINT('Ctrl Pts',(151.343967710007,2.39269633302623,126.505177618167));
#32610=CARTESIAN_POINT('Ctrl Pts',(151.336211407265,2.27111892918819,126.441884042043));
#32611=CARTESIAN_POINT('Ctrl Pts',(151.328450964751,2.14947663582905,126.378556684233));
#32612=CARTESIAN_POINT('Ctrl Pts',(151.320690522237,2.02528013734966,126.320371157231));
#32613=CARTESIAN_POINT('Ctrl Pts',(151.312930079722,1.89900861121593,126.267517071991));
#32614=CARTESIAN_POINT('Ctrl Pts',(151.305157179457,1.77253438281858,126.214578140681));
#32615=CARTESIAN_POINT('Ctrl Pts',(151.297384279192,1.64397883718975,126.166987889558));
#32616=CARTESIAN_POINT('Ctrl Pts',(151.289611378926,1.5138379562108,126.124886533351));
#32617=CARTESIAN_POINT('Ctrl Pts',(151.282121043164,1.38842802406032,126.08431566749));
#32618=CARTESIAN_POINT('Ctrl Pts',(151.274630707402,1.26154631395382,126.048841637614));
#32619=CARTESIAN_POINT('Ctrl Pts',(151.26714037164,1.13364437053645,126.018544751525));
#32620=CARTESIAN_POINT('Ctrl Pts',(151.259366037521,1.00089298605965,125.987099149791));
#32621=CARTESIAN_POINT('Ctrl Pts',(151.251591703402,0.866621960301331,125.961131414152));
#32622=CARTESIAN_POINT('Ctrl Pts',(151.243817369283,0.731323120408024,125.940786874313));
#32623=CARTESIAN_POINT('Ctrl Pts',(151.236052616336,0.596191024243065,125.920467407302));
#32624=CARTESIAN_POINT('Ctrl Pts',(151.228287863389,0.460034017184144,125.905757404861));
#32625=CARTESIAN_POINT('Ctrl Pts',(151.220523110442,0.323357131622324,125.896751909862));
#32626=CARTESIAN_POINT('Ctrl Pts',(151.212766069557,0.186815995470143,125.887755359248));
#32627=CARTESIAN_POINT('Ctrl Pts',(151.205009028672,0.0497563959710257,
125.884452066421));
#32628=CARTESIAN_POINT('Ctrl Pts',(151.197251987787,-0.0873087922816362,
125.886885631632));
#32629=CARTESIAN_POINT('Ctrl Pts',(151.189500796546,-0.224270618609951,
125.889317361672));
#32630=CARTESIAN_POINT('Ctrl Pts',(151.181749605306,-0.361237635981154,
125.89747733178));
#32631=CARTESIAN_POINT('Ctrl Pts',(151.173998414066,-0.497694584393988,
125.911357126543));
#32632=CARTESIAN_POINT('Ctrl Pts',(151.166250517289,-0.634093534963498,
125.925231022022));
#32633=CARTESIAN_POINT('Ctrl Pts',(151.158502620512,-0.769982459615248,
125.944819867447));
#32634=CARTESIAN_POINT('Ctrl Pts',(151.150754723735,-0.904849061725005,
125.970063229321));
#32635=CARTESIAN_POINT('Ctrl Pts',(151.143008447651,-1.03968745264899,125.995301310827));
#32636=CARTESIAN_POINT('Ctrl Pts',(151.135262171567,-1.17350356233794,126.02619148424));
#32637=CARTESIAN_POINT('Ctrl Pts',(151.127515895483,-1.30579355178939,126.062621879233));
#32638=CARTESIAN_POINT('Ctrl Pts',(151.119769562217,-1.43808451777555,126.099052543147));
#32639=CARTESIAN_POINT('Ctrl Pts',(151.112023228952,-1.56884896411093,126.141023406447));
#32640=CARTESIAN_POINT('Ctrl Pts',(151.104276895686,-1.69759690785262,126.188372337582));
#32641=CARTESIAN_POINT('Ctrl Pts',(151.096528827684,-1.82637368380359,126.235731872182));
#32642=CARTESIAN_POINT('Ctrl Pts',(151.088780759681,-1.95313269169805,126.288471736274));
#32643=CARTESIAN_POINT('Ctrl Pts',(151.081032691678,-2.07740304331496,126.346381293015));
#32644=CARTESIAN_POINT('Ctrl Pts',(151.073276388936,-2.20180547094041,126.404352396721));
#32645=CARTESIAN_POINT('Ctrl Pts',(151.065520086194,-2.32371360372672,126.467504003351));
#32646=CARTESIAN_POINT('Ctrl Pts',(151.057763783452,-2.44267983835396,126.535578792525));
#32647=CARTESIAN_POINT('Ctrl Pts',(151.050003340938,-2.56170956884274,126.603689915264));
#32648=CARTESIAN_POINT('Ctrl Pts',(151.042242898424,-2.67779394170561,126.676729248257));
#32649=CARTESIAN_POINT('Ctrl Pts',(151.034482455909,-2.79051442475252,126.754396135284));
#32650=CARTESIAN_POINT('Ctrl Pts',(151.026709555644,-2.90341585672563,126.832187700092));
#32651=CARTESIAN_POINT('Ctrl Pts',(151.018936655379,-3.012942295377,126.914621428324));
#32652=CARTESIAN_POINT('Ctrl Pts',(151.011163755113,-3.11870768376315,127.00135582586));
#32653=CARTESIAN_POINT('Ctrl Pts',(151.003673419351,-3.22062823387432,127.084937209575));
#32654=CARTESIAN_POINT('Ctrl Pts',(150.996183083589,-3.31905620345581,127.172511806115));
#32655=CARTESIAN_POINT('Ctrl Pts',(150.988692747827,-3.4136799563702,127.263743126509));
#32656=CARTESIAN_POINT('Ctrl Pts',(150.981032940029,-3.51044461198812,127.357038594377));
#32657=CARTESIAN_POINT('Ctrl Pts',(150.973373132231,-3.6035565650681,127.454472638766));
#32658=CARTESIAN_POINT('Ctrl Pts',(150.965713324432,-3.69263305694419,127.555723338758));
#32659=CARTESIAN_POINT('Ctrl Pts',(150.958062429611,-3.78160589912683,127.656856223108));
#32660=CARTESIAN_POINT('Ctrl Pts',(150.95041153479,-3.86655235126987,127.761796635112));
#32661=CARTESIAN_POINT('Ctrl Pts',(150.942760639969,-3.94712422251413,127.87018382764));
#32662=CARTESIAN_POINT('Ctrl Pts',(150.93511687513,-4.02762100763716,127.978470012536));
#32663=CARTESIAN_POINT('Ctrl Pts',(150.927473110291,-4.10375107923227,128.090196269446));
#32664=CARTESIAN_POINT('Ctrl Pts',(150.919829345452,-4.17520488840337,128.204966995516));
#32665=CARTESIAN_POINT('Ctrl Pts',(150.912191096375,-4.24660713631114,128.319654902718));
#32666=CARTESIAN_POINT('Ctrl Pts',(150.904552847297,-4.31333962266588,128.4373825674));
#32667=CARTESIAN_POINT('Ctrl Pts',(150.89691459822,-4.37513506165698,128.557723963641));
#32668=CARTESIAN_POINT('Ctrl Pts',(150.889279639307,-4.43690388236004,128.678013523015));
#32669=CARTESIAN_POINT('Ctrl Pts',(150.881644680393,-4.49373970237022,128.80091421611));
#32670=CARTESIAN_POINT('Ctrl Pts',(150.874009721479,-4.54542054193341,128.925974299614));
#32671=CARTESIAN_POINT('Ctrl Pts',(150.866374930831,-4.59710024251206,129.051031626941));
#32672=CARTESIAN_POINT('Ctrl Pts',(150.858740140183,-4.64362502598018,129.178247880934));
#32673=CARTESIAN_POINT('Ctrl Pts',(150.851105349535,-4.68482067447721,129.307150441775));
#32674=CARTESIAN_POINT('Ctrl Pts',(150.84571567502,-4.71390217088837,129.398147415904));
#32675=CARTESIAN_POINT('Ctrl Pts',(150.840326000505,-4.74032891330032,129.489984306768));
#32676=CARTESIAN_POINT('Ctrl Pts',(150.83493632599,-4.76405452823404,129.582490119308));
#32677=CARTESIAN_POINT('Ctrl Pts',(152.584590056215,-4.76405452823404,129.582490119308));
#32678=CARTESIAN_POINT('Ctrl Pts',(152.576521756221,-4.79947459936531,129.720592439074));
#32679=CARTESIAN_POINT('Ctrl Pts',(152.568453456227,-4.82892004477874,129.860370932365));
#32680=CARTESIAN_POINT('Ctrl Pts',(152.560385156233,-4.85224291862247,130.0012904331));
#32681=CARTESIAN_POINT('Ctrl Pts',(152.552329006894,-4.87553066881171,130.141997712653));
#32682=CARTESIAN_POINT('Ctrl Pts',(152.544272857554,-4.89271417596742,130.283842236169));
#32683=CARTESIAN_POINT('Ctrl Pts',(152.536216708215,-4.90369615824396,130.42627722713));
#32684=CARTESIAN_POINT('Ctrl Pts',(152.529097617474,-4.91340076090857,130.552144757965));
#32685=CARTESIAN_POINT('Ctrl Pts',(152.521978526732,-4.91826328929538,130.678473032375));
#32686=CARTESIAN_POINT('Ctrl Pts',(152.514859435991,-4.91824997270814,130.804878745294));
#32687=CARTESIAN_POINT('',(152.860140563967,-4.91824798336883,130.799906789047));
#32688=CARTESIAN_POINT('Ctrl Pts',(152.930132636296,-4.76405452823406,129.582490119308));
#32689=CARTESIAN_POINT('Ctrl Pts',(152.92616746365,-4.78136769973006,129.649993912207));
#32690=CARTESIAN_POINT('Ctrl Pts',(152.922202291004,-4.79723310715757,129.7178160321));
#32691=CARTESIAN_POINT('Ctrl Pts',(152.918237118358,-4.81164200840415,129.785889093438));
#32692=CARTESIAN_POINT('Ctrl Pts',(152.907308734836,-4.85135427644649,129.973504763228));
#32693=CARTESIAN_POINT('Ctrl Pts',(152.896380351314,-4.88010455357513,130.163515281877));
#32694=CARTESIAN_POINT('Ctrl Pts',(152.885451967792,-4.89766574652585,130.354857227359));
#32695=CARTESIAN_POINT('Ctrl Pts',(152.877014833197,-4.9112236664385,130.502580606975));
#32696=CARTESIAN_POINT('Ctrl Pts',(152.868577698603,-4.91811322570068,130.651097395188));
#32697=CARTESIAN_POINT('Ctrl Pts',(152.860140564008,-4.91824798336817,130.799906788326));
#32698=CARTESIAN_POINT('Ctrl Pts',(152.860140563967,-4.91824798336883,130.799906789047));
#32699=CARTESIAN_POINT('Ctrl Pts',(152.85249111539,-4.91837016011845,130.934823423101));
#32700=CARTESIAN_POINT('Ctrl Pts',(152.844841666814,-4.91293664648777,131.069915127919));
#32701=CARTESIAN_POINT('Ctrl Pts',(152.837192218237,-4.90193101268551,131.204679751972));
#32702=CARTESIAN_POINT('Ctrl Pts',(152.82954893775,-4.89093425321401,131.339335709331));
#32703=CARTESIAN_POINT('Ctrl Pts',(152.821905657263,-4.87437434403013,131.473664710837));
#32704=CARTESIAN_POINT('Ctrl Pts',(152.814262376776,-4.85228692064385,131.607164891501));
#32705=CARTESIAN_POINT('Ctrl Pts',(152.806622729055,-4.83020999516479,131.740601621011));
#32706=CARTESIAN_POINT('Ctrl Pts',(152.798983081334,-4.80261084430478,131.873209916207));
#32707=CARTESIAN_POINT('Ctrl Pts',(152.791343433614,-4.76957687614594,132.004493728947));
#32708=CARTESIAN_POINT('Ctrl Pts',(152.783705522536,-4.73655041726043,132.135747698284));
#32709=CARTESIAN_POINT('Ctrl Pts',(152.776067611458,-4.69809169541259,132.265677393132));
#32710=CARTESIAN_POINT('Ctrl Pts',(152.76842970038,-4.65433897773422,132.393798173069));
#32711=CARTESIAN_POINT('Ctrl Pts',(152.760791762406,-4.61058610598386,132.521919404174));
#32712=CARTESIAN_POINT('Ctrl Pts',(152.753153824432,-4.56153933179913,132.648231326355));
#32713=CARTESIAN_POINT('Ctrl Pts',(152.745515886457,-4.5073862417989,132.772266186881));
#32714=CARTESIAN_POINT('Ctrl Pts',(152.737876158235,-4.45322045891165,132.89633011981));
#32715=CARTESIAN_POINT('Ctrl Pts',(152.730236430012,-4.39394614191575,133.018115560744));
#32716=CARTESIAN_POINT('Ctrl Pts',(152.722596701789,-4.32979805238567,133.137176917247));
#32717=CARTESIAN_POINT('Ctrl Pts',(152.714949039957,-4.26558334714713,133.256361915103));
#32718=CARTESIAN_POINT('Ctrl Pts',(152.707301378124,-4.19648495599278,133.372816825593));
#32719=CARTESIAN_POINT('Ctrl Pts',(152.699653716292,-4.12278258597115,133.486122503214));
#32720=CARTESIAN_POINT('Ctrl Pts',(152.692001702043,-4.04903827065087,133.599492665063));
#32721=CARTESIAN_POINT('Ctrl Pts',(152.684349687793,-3.97068499342522,133.709709698357));
#32722=CARTESIAN_POINT('Ctrl Pts',(152.676697673543,-3.88804361829641,133.816386494733));
#32723=CARTESIAN_POINT('Ctrl Pts',(152.669034281977,-3.80527936870936,133.92322190238));
#32724=CARTESIAN_POINT('Ctrl Pts',(152.661370890411,-3.71821455089191,134.026506256536));
#32725=CARTESIAN_POINT('Ctrl Pts',(152.653707498844,-3.62720812907893,134.12588801484));
#32726=CARTESIAN_POINT('Ctrl Pts',(152.649068164078,-3.57211382089796,134.186052661582));
#32727=CARTESIAN_POINT('Ctrl Pts',(152.644428829312,-3.51557562191086,134.244787764669));
#32728=CARTESIAN_POINT('Ctrl Pts',(152.639789494546,-3.45767897429468,134.302022575678));
#32729=CARTESIAN_POINT('Ctrl Pts',(152.632015160426,-3.36065905535762,134.397933426358));
#32730=CARTESIAN_POINT('Ctrl Pts',(152.624240826307,-3.2594918038901,134.489956352213));
#32731=CARTESIAN_POINT('Ctrl Pts',(152.616466492188,-3.15452167088433,134.577711395114));
#32732=CARTESIAN_POINT('Ctrl Pts',(152.608701739241,-3.04968090418608,134.665358287767));
#32733=CARTESIAN_POINT('Ctrl Pts',(152.600936986294,-2.94104687818329,134.748747514514));
#32734=CARTESIAN_POINT('Ctrl Pts',(152.593172233347,-2.82900148006827,134.827535195964));
#32735=CARTESIAN_POINT('Ctrl Pts',(152.585415192462,-2.71706736702215,134.906244624379));
#32736=CARTESIAN_POINT('Ctrl Pts',(152.577658151577,-2.6017289423239,134.980361379209));
#32737=CARTESIAN_POINT('Ctrl Pts',(152.569901110692,-2.48340155023599,135.04958143665));
#32738=CARTESIAN_POINT('Ctrl Pts',(152.562149919452,-2.36516338975504,135.118749294707));
#32739=CARTESIAN_POINT('Ctrl Pts',(152.554398728212,-2.24394108444064,135.183027608733));
#32740=CARTESIAN_POINT('Ctrl Pts',(152.546647536971,-2.12017907329689,135.242155538431));
#32741=CARTESIAN_POINT('Ctrl Pts',(152.538899640194,-1.99646966430934,135.301258337182));
#32742=CARTESIAN_POINT('Ctrl Pts',(152.531151743417,-1.87022304845567,135.355214937274));
#32743=CARTESIAN_POINT('Ctrl Pts',(152.52340384664,-1.74190819257132,135.403810466315));
#32744=CARTESIAN_POINT('Ctrl Pts',(152.515657570556,-1.61362017738854,135.452395830218));
#32745=CARTESIAN_POINT('Ctrl Pts',(152.507911294472,-1.48326514809356,135.495622215254));
#32746=CARTESIAN_POINT('Ctrl Pts',(152.500165018388,-1.35133160459901,135.533323078499));
#32747=CARTESIAN_POINT('Ctrl Pts',(152.492418685122,-1.21939708720092,135.571024220043));
#32748=CARTESIAN_POINT('Ctrl Pts',(152.484672351857,-1.0858844082703,135.603199650986));
#32749=CARTESIAN_POINT('Ctrl Pts',(152.476926018592,-0.951296378697564,
135.629732961995));
#32750=CARTESIAN_POINT('Ctrl Pts',(152.469177950589,-0.816678209069185,
135.656272214955));
#32751=CARTESIAN_POINT('Ctrl Pts',(152.461429882586,-0.680984593108801,
135.677166758128));
#32752=CARTESIAN_POINT('Ctrl Pts',(152.453681814583,-0.544727265169134,
135.692351541154));
#32753=CARTESIAN_POINT('Ctrl Pts',(152.445925511841,-0.408325121319524,
135.707552462748));
#32754=CARTESIAN_POINT('Ctrl Pts',(152.438169209099,-0.27135845786369,135.717031458539));
#32755=CARTESIAN_POINT('Ctrl Pts',(152.430412906357,-0.134343406322409,
135.720775460892));
#32756=CARTESIAN_POINT('Ctrl Pts',(152.422652463843,0.00274477427746336,
135.724521461532));
#32757=CARTESIAN_POINT('Ctrl Pts',(152.414892021329,0.139881003691061,135.722526375239));
#32758=CARTESIAN_POINT('Ctrl Pts',(152.407131578815,0.276551436399757,135.714829267861));
#32759=CARTESIAN_POINT('Ctrl Pts',(152.399358678549,0.413441264619928,135.707119804402));
#32760=CARTESIAN_POINT('Ctrl Pts',(152.391585778284,0.549863412607578,135.693690066792));
#32761=CARTESIAN_POINT('Ctrl Pts',(152.383812878018,0.685310527535069,135.674630891724));
#32762=CARTESIAN_POINT('Ctrl Pts',(152.376322542256,0.815833798663701,135.656264565677));
#32763=CARTESIAN_POINT('Ctrl Pts',(152.368832206494,0.945451392757213,135.632671039947));
#32764=CARTESIAN_POINT('Ctrl Pts',(152.361341870732,1.07372212018233,135.6039755887));
#32765=CARTESIAN_POINT('Ctrl Pts',(152.353567536613,1.20685627122519,135.574192140697));
#32766=CARTESIAN_POINT('Ctrl Pts',(152.345793202494,1.3389611355373,135.538817906041));
#32767=CARTESIAN_POINT('Ctrl Pts',(152.338018868375,1.469530859409,135.497937304459));
#32768=CARTESIAN_POINT('Ctrl Pts',(152.330254115428,1.59993966776525,135.457107084564));
#32769=CARTESIAN_POINT('Ctrl Pts',(152.322489362481,1.72881673052121,135.410784115765));
#32770=CARTESIAN_POINT('Ctrl Pts',(152.314724609534,1.85566631285052,135.35910381536));
#32771=CARTESIAN_POINT('Ctrl Pts',(152.306967568649,1.98238990638692,135.307474844558));
#32772=CARTESIAN_POINT('Ctrl Pts',(152.299210527764,2.10708966716845,135.250499277694));
#32773=CARTESIAN_POINT('Ctrl Pts',(152.291453486879,2.2292853076384,135.188362223365));
#32774=CARTESIAN_POINT('Ctrl Pts',(152.283702295639,2.35138879942496,135.126272027072));
#32775=CARTESIAN_POINT('Ctrl Pts',(152.275951104399,2.47099158251282,135.059028267233));
#32776=CARTESIAN_POINT('Ctrl Pts',(152.268199913158,2.58763397443632,134.986863872417));
#32777=CARTESIAN_POINT('Ctrl Pts',(152.260452016381,2.70422679023167,134.914730149395));
#32778=CARTESIAN_POINT('Ctrl Pts',(152.252704119604,2.81786138563387,134.8376801563));
#32779=CARTESIAN_POINT('Ctrl Pts',(152.244956222827,2.9281034943823,134.755992304437));
#32780=CARTESIAN_POINT('Ctrl Pts',(152.237209946743,3.03832254285825,134.674321539912));
#32781=CARTESIAN_POINT('Ctrl Pts',(152.229463670659,3.14515020225643,134.588015078895));
#32782=CARTESIAN_POINT('Ctrl Pts',(152.221717394575,3.24818230916322,134.49739388968));
#32783=CARTESIAN_POINT('Ctrl Pts',(152.21397106131,3.35121517662934,134.40677203152));
#32784=CARTESIAN_POINT('Ctrl Pts',(152.206224728044,3.45045214212701,134.311835639813));
#32785=CARTESIAN_POINT('Ctrl Pts',(152.198478394779,3.54552348562038,134.212944821516));
#32786=CARTESIAN_POINT('Ctrl Pts',(152.190730326776,3.6406161196821,134.114031857305));
#32787=CARTESIAN_POINT('Ctrl Pts',(152.182982258773,3.73154100454593,134.011162986117));
#32788=CARTESIAN_POINT('Ctrl Pts',(152.17523419077,3.81796680658291,133.904733583248));
#32789=CARTESIAN_POINT('Ctrl Pts',(152.167477888028,3.90448446299083,133.798191065943));
#32790=CARTESIAN_POINT('Ctrl Pts',(152.159721585287,3.98649323780333,133.688080761642));
#32791=CARTESIAN_POINT('Ctrl Pts',(152.151965282545,4.06370315515527,133.574829843037));
#32792=CARTESIAN_POINT('Ctrl Pts',(152.144204840031,4.14095428176486,133.461518479006));
#32793=CARTESIAN_POINT('Ctrl Pts',(152.136444397516,4.21340124089931,133.345063492427));
#32794=CARTESIAN_POINT('Ctrl Pts',(152.128683955002,4.28079915370848,133.225918312131));
#32795=CARTESIAN_POINT('Ctrl Pts',(152.120911054737,4.34830525963057,133.106581869415));
#32796=CARTESIAN_POINT('Ctrl Pts',(152.113138154471,4.41074594431306,132.98454695142));
#32797=CARTESIAN_POINT('Ctrl Pts',(152.105365254206,4.46792339464244,132.860289507899));
#32798=CARTESIAN_POINT('Ctrl Pts',(152.097874918444,4.52302230063149,132.740549135435));
#32799=CARTESIAN_POINT('Ctrl Pts',(152.090384582682,4.57323387492497,132.618745305601));
#32800=CARTESIAN_POINT('Ctrl Pts',(152.08289424692,4.61842504045398,132.495316917477));
#32801=CARTESIAN_POINT('Ctrl Pts',(152.075119912801,4.66532964275923,132.367208704502));
#32802=CARTESIAN_POINT('Ctrl Pts',(152.067345578682,4.70697420329463,132.236944502857));
#32803=CARTESIAN_POINT('Ctrl Pts',(152.059571244563,4.74315632047991,132.104995532518));
#32804=CARTESIAN_POINT('Ctrl Pts',(152.051806491616,4.7792938464394,131.973209177492));
#32805=CARTESIAN_POINT('Ctrl Pts',(152.044041738668,4.80998222127051,131.839742558469));
#32806=CARTESIAN_POINT('Ctrl Pts',(152.036276985721,4.83506741860027,131.705085947559));
#32807=CARTESIAN_POINT('Ctrl Pts',(152.028519944836,4.86012770095843,131.570563079492));
#32808=CARTESIAN_POINT('Ctrl Pts',(152.020762903951,4.87959580958676,131.43485295347));
#32809=CARTESIAN_POINT('Ctrl Pts',(152.013005863066,4.89336787443554,131.298459704736));
#32810=CARTESIAN_POINT('Ctrl Pts',(152.005254671826,4.90712955366309,131.162169311212));
#32811=CARTESIAN_POINT('Ctrl Pts',(151.997503480586,4.91520369978747,131.02519720776));
#32812=CARTESIAN_POINT('Ctrl Pts',(151.989752289346,4.91753781261068,130.888056041839));
#32813=CARTESIAN_POINT('Ctrl Pts',(151.982004392569,4.91987093337366,130.750973164572));
#32814=CARTESIAN_POINT('Ctrl Pts',(151.974256495792,4.91646886650844,130.613721757843));
#32815=CARTESIAN_POINT('Ctrl Pts',(151.966508599015,4.90733111580762,130.476817670265));
#32816=CARTESIAN_POINT('Ctrl Pts',(151.958762322931,4.89819527652724,130.339942220071));
#32817=CARTESIAN_POINT('Ctrl Pts',(151.951016046847,4.88332616586303,130.203414334371));
#32818=CARTESIAN_POINT('Ctrl Pts',(151.943269770762,4.86277536333299,130.067747538493));
#32819=CARTESIAN_POINT('Ctrl Pts',(151.935523437497,4.8422244091016,129.932079741153));
#32820=CARTESIAN_POINT('Ctrl Pts',(151.927777104232,4.81599173786964,129.797273432875));
#32821=CARTESIAN_POINT('Ctrl Pts',(151.920030770966,4.78418047510694,129.663834316201));
#32822=CARTESIAN_POINT('Ctrl Pts',(151.912282702963,4.75236208843253,129.530365316762));
#32823=CARTESIAN_POINT('Ctrl Pts',(151.90453463496,4.71496271493733,129.398264498411));
#32824=CARTESIAN_POINT('Ctrl Pts',(151.896786566957,4.67213590113458,129.268024331517));
#32825=CARTESIAN_POINT('Ctrl Pts',(151.889030264216,4.62926357048447,129.137645743825));
#32826=CARTESIAN_POINT('Ctrl Pts',(151.881273961474,4.58095239895237,129.009132129898));
#32827=CARTESIAN_POINT('Ctrl Pts',(151.873517658732,4.52740503998275,128.882958351918));
#32828=CARTESIAN_POINT('Ctrl Pts',(151.865757216218,4.47382910117527,128.756717231193));
#32829=CARTESIAN_POINT('Ctrl Pts',(151.857996773704,4.4150115738168,128.632818787851));
#32830=CARTESIAN_POINT('Ctrl Pts',(151.850236331189,4.35120157742595,128.511714134764));
#32831=CARTESIAN_POINT('Ctrl Pts',(151.842463430924,4.28728914756418,128.390415073736));
#32832=CARTESIAN_POINT('Ctrl Pts',(151.834690530658,4.21836843011531,128.271919103256));
#32833=CARTESIAN_POINT('Ctrl Pts',(151.826917630393,4.1447329322676,128.156649911564));
#32834=CARTESIAN_POINT('Ctrl Pts',(151.819427294631,4.0737742702435,128.045571045337));
#32835=CARTESIAN_POINT('Ctrl Pts',(151.811936958869,3.99843784093229,127.93748868057));
#32836=CARTESIAN_POINT('Ctrl Pts',(151.804446623107,3.91902097115459,127.832752014444));
#32837=CARTESIAN_POINT('Ctrl Pts',(151.796672288988,3.83659298662095,127.724044225787));
#32838=CARTESIAN_POINT('Ctrl Pts',(151.788897954869,3.74950792669753,127.618596494705));
#32839=CARTESIAN_POINT('Ctrl Pts',(151.78112362075,3.65805283909787,127.516833813285));
#32840=CARTESIAN_POINT('Ctrl Pts',(151.773358867803,3.56671046171992,127.415196545275));
#32841=CARTESIAN_POINT('Ctrl Pts',(151.765594114856,3.47100903136664,127.317235578704));
#32842=CARTESIAN_POINT('Ctrl Pts',(151.757829361908,3.37127777283058,127.223345504373));
#32843=CARTESIAN_POINT('Ctrl Pts',(151.750072321023,3.27164556878627,127.129548682987));
#32844=CARTESIAN_POINT('Ctrl Pts',(151.742315280138,3.16799178450195,127.039814973813));
#32845=CARTESIAN_POINT('Ctrl Pts',(151.734558239253,3.06068441893629,126.954504263079));
#32846=CARTESIAN_POINT('Ctrl Pts',(151.726807048013,2.95345797469032,126.869257885817));
#32847=CARTESIAN_POINT('Ctrl Pts',(151.719055856773,2.84258373800712,126.788428110365));
#32848=CARTESIAN_POINT('Ctrl Pts',(151.711304665533,2.72846463607351,126.712336205103));
#32849=CARTESIAN_POINT('Ctrl Pts',(151.703556768756,2.6143940378023,126.636276640929));
#32850=CARTESIAN_POINT('Ctrl Pts',(151.695808871979,2.49708164191867,126.564951158246));
#32851=CARTESIAN_POINT('Ctrl Pts',(151.688060975202,2.37696117825879,126.498639003301));
#32852=CARTESIAN_POINT('Ctrl Pts',(151.680314699118,2.25686584121033,126.432340719429));
#32853=CARTESIAN_POINT('Ctrl Pts',(151.672568423034,2.13396394678784,126.371053866246));
#32854=CARTESIAN_POINT('Ctrl Pts',(151.66482214695,2.00871541838373,126.315012621426));
#32855=CARTESIAN_POINT('Ctrl Pts',(151.657075813684,1.8834659654236,126.258970962922));
#32856=CARTESIAN_POINT('Ctrl Pts',(151.649329480419,1.75587020078702,126.208175149726));
#32857=CARTESIAN_POINT('Ctrl Pts',(151.641583147154,1.62640932818071,126.162811764036));
#32858=CARTESIAN_POINT('Ctrl Pts',(151.633835079151,1.49691946370956,126.11743821953));
#32859=CARTESIAN_POINT('Ctrl Pts',(151.626087011148,1.36556402903665,126.077499652596));
#32860=CARTESIAN_POINT('Ctrl Pts',(151.618338943145,1.23284034907297,126.043133072468));
#32861=CARTESIAN_POINT('Ctrl Pts',(151.610582640403,1.09997560880265,126.00872996713));
#32862=CARTESIAN_POINT('Ctrl Pts',(151.602826337661,0.965740097432175,125.979910776536));
#32863=CARTESIAN_POINT('Ctrl Pts',(151.595070034919,0.830642869100312,125.956761677213));
#32864=CARTESIAN_POINT('Ctrl Pts',(151.587309592405,0.695473535310081,125.933600222518));
#32865=CARTESIAN_POINT('Ctrl Pts',(151.579549149891,0.559441955705539,125.91611493907));
#32866=CARTESIAN_POINT('Ctrl Pts',(151.571788707377,0.423062319506636,125.904340073087));
#32867=CARTESIAN_POINT('Ctrl Pts',(151.564015807111,0.286463754608351,125.892546305044));
#32868=CARTESIAN_POINT('Ctrl Pts',(151.556242906846,0.149516407399585,125.8864812901));
#32869=CARTESIAN_POINT('Ctrl Pts',(151.54847000658,0.0127353866029482,125.886127106189));
#32870=CARTESIAN_POINT('Ctrl Pts',(151.540979670818,-0.119073299558426,
125.885785797756));
#32871=CARTESIAN_POINT('Ctrl Pts',(151.533489335056,-0.250727234327518,
125.890747311159));
#32872=CARTESIAN_POINT('Ctrl Pts',(151.525998999294,-0.381771915817088,
125.900950246529));
#32873=CARTESIAN_POINT('Ctrl Pts',(151.518224665175,-0.517785196234352,
125.911540029295));
#32874=CARTESIAN_POINT('Ctrl Pts',(151.510450331056,-0.653572960888895,
125.927810082231));
#32875=CARTESIAN_POINT('Ctrl Pts',(151.502675996937,-0.788622495599073,
125.949748622572));
#32876=CARTESIAN_POINT('Ctrl Pts',(151.49491124399,-0.923505593827125,125.971660125623));
#32877=CARTESIAN_POINT('Ctrl Pts',(151.487146491043,-1.0576518901447,125.999226154124));
#32878=CARTESIAN_POINT('Ctrl Pts',(151.479381738095,-1.19055145009452,126.032383007897));
#32879=CARTESIAN_POINT('Ctrl Pts',(151.47162469721,-1.32331901232838,126.065506929817));
#32880=CARTESIAN_POINT('Ctrl Pts',(151.463867656325,-1.45484192553694,126.104210532487));
#32881=CARTESIAN_POINT('Ctrl Pts',(151.45611061544,-1.58461849481841,126.148378735258));
#32882=CARTESIAN_POINT('Ctrl Pts',(151.4483594242,-1.71429719857956,126.192513630444));
#32883=CARTESIAN_POINT('Ctrl Pts',(151.44060823296,-1.84223181106679,126.242104797879));
#32884=CARTESIAN_POINT('Ctrl Pts',(151.43285704172,-1.967934248109,126.296986896915));
#32885=CARTESIAN_POINT('Ctrl Pts',(151.425109144943,-2.093583258262,126.351845669594));
#32886=CARTESIAN_POINT('Ctrl Pts',(151.417361248166,-2.21700162237641,126.411990745098));
#32887=CARTESIAN_POINT('Ctrl Pts',(151.409613351389,-2.33771996110309,126.477208153652));
#32888=CARTESIAN_POINT('Ctrl Pts',(151.401867075304,-2.45841304815582,126.542411920129));
#32889=CARTESIAN_POINT('Ctrl Pts',(151.39412079922,-2.57640688945399,126.61268572351));
#32890=CARTESIAN_POINT('Ctrl Pts',(151.386374523136,-2.69125586485991,126.68776919597));
#32891=CARTESIAN_POINT('Ctrl Pts',(151.378628189871,-2.80610568805457,126.762853222679));
#32892=CARTESIAN_POINT('Ctrl Pts',(151.370881856606,-2.9178102717946,126.842746775379));
#32893=CARTESIAN_POINT('Ctrl Pts',(151.36313552334,-3.02595253683478,126.927145855998));
#32894=CARTESIAN_POINT('Ctrl Pts',(151.355387455337,-3.13411901958545,127.011563837205));
#32895=CARTESIAN_POINT('Ctrl Pts',(151.347639387334,-3.23872128804158,127.100489113594));
#32896=CARTESIAN_POINT('Ctrl Pts',(151.339891319331,-3.339375256192,127.193577328468));
#32897=CARTESIAN_POINT('Ctrl Pts',(151.332135016589,-3.44013620057762,127.286764478604));
#32898=CARTESIAN_POINT('Ctrl Pts',(151.324378713847,-3.5369401746064,127.384123139604));
#32899=CARTESIAN_POINT('Ctrl Pts',(151.316622411106,-3.62943951933013,127.485271610319));
#32900=CARTESIAN_POINT('Ctrl Pts',(151.308861968591,-3.72198823373946,127.58647406702));
#32901=CARTESIAN_POINT('Ctrl Pts',(151.301101526077,-3.81022748944611,127.69147006475));
#32902=CARTESIAN_POINT('Ctrl Pts',(151.293341083563,-3.89385054230238,127.799845512476));
#32903=CARTESIAN_POINT('Ctrl Pts',(151.285568183298,-3.97760783430676,127.908394934092));
#32904=CARTESIAN_POINT('Ctrl Pts',(151.277795283032,-4.05673388944061,128.020334327126));
#32905=CARTESIAN_POINT('Ctrl Pts',(151.270022382767,-4.1309653571986,128.135220628707));
#32906=CARTESIAN_POINT('Ctrl Pts',(151.262532047005,-4.20249832412462,128.245930523843));
#32907=CARTESIAN_POINT('Ctrl Pts',(151.255041711243,-4.26948622994854,128.359376526981));
#32908=CARTESIAN_POINT('Ctrl Pts',(151.247551375481,-4.33173506274729,128.475143064681));
#32909=CARTESIAN_POINT('Ctrl Pts',(151.239351872804,-4.39987746482186,128.601870098814));
#32910=CARTESIAN_POINT('Ctrl Pts',(151.231152370127,-4.46253770433376,128.731743506672));
#32911=CARTESIAN_POINT('Ctrl Pts',(151.22295286745,-4.51943039138935,128.864275052472));
#32912=CARTESIAN_POINT('Ctrl Pts',(151.214771930565,-4.57619425870915,128.996506512627));
#32913=CARTESIAN_POINT('Ctrl Pts',(151.20659099368,-4.62721648224196,129.131383810757));
#32914=CARTESIAN_POINT('Ctrl Pts',(151.198410056794,-4.67225768868374,129.268394747816));
#32915=CARTESIAN_POINT('Ctrl Pts',(151.192226668269,-4.70630113419362,129.371951573632));
#32916=CARTESIAN_POINT('Ctrl Pts',(151.186043279744,-4.73692864470159,129.476726711108));
#32917=CARTESIAN_POINT('Ctrl Pts',(151.179859891219,-4.76405452823403,129.582490119308));
#32918=CARTESIAN_POINT('Origin',(213.235140564004,0.,130.804360617566));
#32919=CARTESIAN_POINT('',(149.084946415013,-4.76405452823403,129.582490119308));
#32920=CARTESIAN_POINT('',(149.43018764199,-4.76405452823406,129.582490119308));
#32921=CARTESIAN_POINT('',(213.235140564004,-4.76405452823405,129.582490119308));
#32922=CARTESIAN_POINT('',(150.764859436022,-4.91824806144419,130.808727378438));
#32923=CARTESIAN_POINT('Ctrl Pts',(150.764859435991,-4.9182480614437,130.808727378982));
#32924=CARTESIAN_POINT('Ctrl Pts',(150.75358626954,-4.91807160662695,131.007467011822));
#32925=CARTESIAN_POINT('Ctrl Pts',(150.742313103089,-4.90584570983701,131.205693402104));
#32926=CARTESIAN_POINT('Ctrl Pts',(150.731039936638,-4.88177550045476,131.402232698918));
#32927=CARTESIAN_POINT('Ctrl Pts',(150.72410833243,-4.86697529632734,131.523080077754));
#32928=CARTESIAN_POINT('Ctrl Pts',(150.717176728222,-4.84769794250399,131.643290400273));
#32929=CARTESIAN_POINT('Ctrl Pts',(150.710245124014,-4.82399917091086,131.762596006994));
#32930=CARTESIAN_POINT('Ctrl Pts',(150.702470789895,-4.79741915233895,131.89640653932));
#32931=CARTESIAN_POINT('Ctrl Pts',(150.694696455776,-4.76522525707937,132.02932224479));
#32932=CARTESIAN_POINT('Ctrl Pts',(150.686922121657,-4.7274897414526,132.160835389525));
#32933=CARTESIAN_POINT('Ctrl Pts',(150.67915736871,-4.68980073147629,132.292186456063));
#32934=CARTESIAN_POINT('Ctrl Pts',(150.671392615763,-4.64658379670008,132.422138028934));
#32935=CARTESIAN_POINT('Ctrl Pts',(150.663627862816,-4.59796241915813,132.550191266429));
#32936=CARTESIAN_POINT('Ctrl Pts',(150.655870821931,-4.54938933305391,132.678117319643));
#32937=CARTESIAN_POINT('Ctrl Pts',(150.648113781046,-4.49542262416883,132.80414842648));
#32938=CARTESIAN_POINT('Ctrl Pts',(150.640356740161,-4.43623582221752,132.927799995597));
#32939=CARTESIAN_POINT('Ctrl Pts',(150.632605548921,-4.37709365349398,133.051358318104));
#32940=CARTESIAN_POINT('Ctrl Pts',(150.624854357681,-4.31273939520922,133.17254032337));
#32941=CARTESIAN_POINT('Ctrl Pts',(150.617103166441,-4.24339487774415,133.290880871663));
#32942=CARTESIAN_POINT('Ctrl Pts',(150.609355269663,-4.17407983354872,133.409171122066));
#32943=CARTESIAN_POINT('Ctrl Pts',(150.601607372886,-4.09977894591339,133.524621980896));
#32944=CARTESIAN_POINT('Ctrl Pts',(150.593859476109,-4.02076012477245,133.636792625848));
#32945=CARTESIAN_POINT('Ctrl Pts',(150.586113200025,-3.94175783266545,133.748939807119));
#32946=CARTESIAN_POINT('Ctrl Pts',(150.578366923941,-3.85803979504627,133.857807819881));
#32947=CARTESIAN_POINT('Ctrl Pts',(150.570620647857,-3.7699171889696,133.962984914758));
#32948=CARTESIAN_POINT('Ctrl Pts',(150.562874314592,-3.68179393239183,134.068162786028));
#32949=CARTESIAN_POINT('Ctrl Pts',(150.555127981326,-3.58926629356591,134.169649385364));
#32950=CARTESIAN_POINT('Ctrl Pts',(150.547381648061,-3.49268540348365,134.267066457627));
#32951=CARTESIAN_POINT('Ctrl Pts',(150.539633580058,-3.39608288478092,134.364505345767));
#32952=CARTESIAN_POINT('Ctrl Pts',(150.531885512055,-3.29542558381622,134.457872615778));
#32953=CARTESIAN_POINT('Ctrl Pts',(150.524137444052,-3.19110081093237,134.54682754153));
#32954=CARTESIAN_POINT('Ctrl Pts',(150.51638114131,-3.08666516043819,134.635877009636));
#32955=CARTESIAN_POINT('Ctrl Pts',(150.508624838568,-2.97855454965732,134.720504511643));
#32956=CARTESIAN_POINT('Ctrl Pts',(150.500868535826,-2.86718906964377,134.800409904226));
#32957=CARTESIAN_POINT('Ctrl Pts',(150.493108093312,-2.75576415052027,134.880357944723));
#32958=CARTESIAN_POINT('Ctrl Pts',(150.485347650798,-2.6410812273607,134.955578639499));
#32959=CARTESIAN_POINT('Ctrl Pts',(150.477587208284,-2.52358772200415,135.025816299182));
#32960=CARTESIAN_POINT('Ctrl Pts',(150.469814308018,-2.40590560564229,135.096166710592));
#32961=CARTESIAN_POINT('Ctrl Pts',(150.462041407753,-2.28540423495246,135.161517915445));
#32962=CARTESIAN_POINT('Ctrl Pts',(150.454268507487,-2.16255467565798,135.22166073611));
#32963=CARTESIAN_POINT('Ctrl Pts',(150.446778171725,-2.04417100728164,135.279617213754));
#32964=CARTESIAN_POINT('Ctrl Pts',(150.439287835963,-1.92360719327457,135.332737284421));
#32965=CARTESIAN_POINT('Ctrl Pts',(150.431797500201,-1.8012988128428,135.380877376997));
#32966=CARTESIAN_POINT('Ctrl Pts',(150.424023166082,-1.6743530729938,135.430842715814));
#32967=CARTESIAN_POINT('Ctrl Pts',(150.416248831963,-1.54512573884652,135.475601265406));
#32968=CARTESIAN_POINT('Ctrl Pts',(150.408474497844,-1.41408303759758,135.5149393745));
#32969=CARTESIAN_POINT('Ctrl Pts',(150.400709744897,-1.28320183476636,135.554229002891));
#32970=CARTESIAN_POINT('Ctrl Pts',(150.39294499195,-1.15051008721139,135.588111371076));
#32971=CARTESIAN_POINT('Ctrl Pts',(150.385180239002,-1.01649422964589,135.616420731862));
#32972=CARTESIAN_POINT('Ctrl Pts',(150.377423198117,-0.882611478519405,
135.644701975391));
#32973=CARTESIAN_POINT('Ctrl Pts',(150.369666157232,-0.747407614588527,
135.667421146515));
#32974=CARTESIAN_POINT('Ctrl Pts',(150.361909116347,-0.611384135322865,
135.684462307242));
#32975=CARTESIAN_POINT('Ctrl Pts',(150.354157925107,-0.475463232421164,
135.701490617096));
#32976=CARTESIAN_POINT('Ctrl Pts',(150.346406733867,-0.338724330795074,
135.712849390875));
#32977=CARTESIAN_POINT('Ctrl Pts',(150.338655542627,-0.201678670413874,
135.718473841374));
#32978=CARTESIAN_POINT('Ctrl Pts',(150.33090764585,-0.0646912580939631,
135.724095901331));
#32979=CARTESIAN_POINT('Ctrl Pts',(150.323159749073,0.0726022638453508,
135.723988469494));
#32980=CARTESIAN_POINT('Ctrl Pts',(150.315411852296,0.209686207249513,135.718138670855));
#32981=CARTESIAN_POINT('Ctrl Pts',(150.307665576212,0.346741475647902,135.712290095868));
#32982=CARTESIAN_POINT('Ctrl Pts',(150.299919300128,0.483586862347687,135.700701559949));
#32983=CARTESIAN_POINT('Ctrl Pts',(150.292173024043,0.619707752136331,135.683412304569));
#32984=CARTESIAN_POINT('Ctrl Pts',(150.284426690778,0.755829646738368,135.666122921563));
#32985=CARTESIAN_POINT('Ctrl Pts',(150.276680357513,0.891226645908353,135.643132784389));
#32986=CARTESIAN_POINT('Ctrl Pts',(150.268934024247,1.02539071800664,135.614532853352));
#32987=CARTESIAN_POINT('Ctrl Pts',(150.261185956244,1.15958483521864,135.585926517559));
#32988=CARTESIAN_POINT('Ctrl Pts',(150.253437888241,1.29254509364041,135.551707969557));
#32989=CARTESIAN_POINT('Ctrl Pts',(150.245689820238,1.42377548002807,135.512018893713));
#32990=CARTESIAN_POINT('Ctrl Pts',(150.237933517497,1.55514533963208,135.472287635846));
#32991=CARTESIAN_POINT('Ctrl Pts',(150.230177214755,1.68478127972169,135.42707434912));
#32992=CARTESIAN_POINT('Ctrl Pts',(150.222420912013,1.81220371174026,135.376570233239));
#32993=CARTESIAN_POINT('Ctrl Pts',(150.214660469499,1.93969415294749,135.326039161791));
#32994=CARTESIAN_POINT('Ctrl Pts',(150.206900026985,2.06496837507746,135.270211793442));
#32995=CARTESIAN_POINT('Ctrl Pts',(150.19913958447,2.18756941698641,135.209326350505));
#32996=CARTESIAN_POINT('Ctrl Pts',(150.191366684205,2.31036726897179,135.14834316885));
#32997=CARTESIAN_POINT('Ctrl Pts',(150.18359378394,2.43048302272403,135.082285875427));
#32998=CARTESIAN_POINT('Ctrl Pts',(150.175820883674,2.54748606864897,135.011437725552));
#32999=CARTESIAN_POINT('Ctrl Pts',(150.168330547912,2.66023575914113,134.943165084381));
#33000=CARTESIAN_POINT('Ctrl Pts',(150.16084021215,2.77009486543544,134.870444028838));
#33001=CARTESIAN_POINT('Ctrl Pts',(150.153349876388,2.8767071558873,134.793563420353));
#33002=CARTESIAN_POINT('Ctrl Pts',(150.145575542269,2.98736168373615,134.71376786023));
#33003=CARTESIAN_POINT('Ctrl Pts',(150.13780120815,3.09486884979585,134.629238333447));
#33004=CARTESIAN_POINT('Ctrl Pts',(150.130026874031,3.19879689601085,134.540251606416));
#33005=CARTESIAN_POINT('Ctrl Pts',(150.122262121084,3.30259686019714,134.451374547574));
#33006=CARTESIAN_POINT('Ctrl Pts',(150.114497368137,3.40282618687997,134.358051469958));
#33007=CARTESIAN_POINT('Ctrl Pts',(150.10673261519,3.49908249840483,134.260602034461));
#33008=CARTESIAN_POINT('Ctrl Pts',(150.098975574305,3.59524320680414,134.163249387117));
#33009=CARTESIAN_POINT('Ctrl Pts',(150.09121853342,3.68743847990409,134.061778814159));
#33010=CARTESIAN_POINT('Ctrl Pts',(150.083461492535,3.77529970415513,133.956549572294));
#33011=CARTESIAN_POINT('Ctrl Pts',(150.075710301295,3.86309467157351,133.851399684618));
#33012=CARTESIAN_POINT('Ctrl Pts',(150.067959110055,3.94656184601318,133.742497068714));
#33013=CARTESIAN_POINT('Ctrl Pts',(150.060207918814,4.02537038247279,133.63023682618));
#33014=CARTESIAN_POINT('Ctrl Pts',(150.052460022037,4.10414542320216,133.518024297244));
#33015=CARTESIAN_POINT('Ctrl Pts',(150.04471212526,4.17826553994447,133.40245729935));
#33016=CARTESIAN_POINT('Ctrl Pts',(150.036964228483,4.24744115854621,133.283962736291));
#33017=CARTESIAN_POINT('Ctrl Pts',(150.029217952399,4.31660230709979,133.165492959741));
#33018=CARTESIAN_POINT('Ctrl Pts',(150.021471676315,4.38082081777171,133.044097173518));
#33019=CARTESIAN_POINT('Ctrl Pts',(150.013725400231,4.43985154343156,132.920229548948));
#33020=CARTESIAN_POINT('Ctrl Pts',(150.005979066966,4.49888270484277,132.796361010016));
#33021=CARTESIAN_POINT('Ctrl Pts',(149.9982327337,4.55272583663069,132.670020949264));
#33022=CARTESIAN_POINT('Ctrl Pts',(149.990486400435,4.60118286276593,132.541685954367));
#33023=CARTESIAN_POINT('Ctrl Pts',(149.982738332432,4.6496507405162,132.413322219736));
#33024=CARTESIAN_POINT('Ctrl Pts',(149.974990264429,4.69272997437489,132.282963027667));
#33025=CARTESIAN_POINT('Ctrl Pts',(149.967242196426,4.7302716601366,132.151102272008));
#33026=CARTESIAN_POINT('Ctrl Pts',(149.959485893684,4.7678532456487,132.019101373168));
#33027=CARTESIAN_POINT('Ctrl Pts',(149.951729590943,4.79988541917236,131.88559609942));
#33028=CARTESIAN_POINT('Ctrl Pts',(149.943973288201,4.82626981310267,131.751093290306));
#33029=CARTESIAN_POINT('Ctrl Pts',(149.936212845687,4.85266828917847,131.616518692994));
#33030=CARTESIAN_POINT('Ctrl Pts',(149.928452403172,4.87341292012736,131.480945885714));
#33031=CARTESIAN_POINT('Ctrl Pts',(149.920691960658,4.88845713046823,131.344888087797));
#33032=CARTESIAN_POINT('Ctrl Pts',(149.912919060393,4.9035254911111,131.208611877824));
#33033=CARTESIAN_POINT('Ctrl Pts',(149.905146160127,4.91287511820822,131.071849511704));
#33034=CARTESIAN_POINT('Ctrl Pts',(149.897373259862,4.91651156747513,130.935116379899));
#33035=CARTESIAN_POINT('Ctrl Pts',(149.8898829241,4.92001582265155,130.803353841844));
#33036=CARTESIAN_POINT('Ctrl Pts',(149.882392588338,4.91821506946645,130.671618757515));
#33037=CARTESIAN_POINT('Ctrl Pts',(149.874902252576,4.91115978331515,130.54036697134));
#33038=CARTESIAN_POINT('Ctrl Pts',(149.867127918457,4.90383699384507,130.4041387338));
#33039=CARTESIAN_POINT('Ctrl Pts',(149.859353584338,4.89083015822545,130.267999636258));
#33040=CARTESIAN_POINT('Ctrl Pts',(149.851579250219,4.87213875210234,130.132462528));
#33041=CARTESIAN_POINT('Ctrl Pts',(149.843814497272,4.85347038146679,129.997092457115));
#33042=CARTESIAN_POINT('Ctrl Pts',(149.836049744324,4.82913143253088,129.86232328294));
#33043=CARTESIAN_POINT('Ctrl Pts',(149.828284991377,4.7991733501061,129.728666321713));
#33044=CARTESIAN_POINT('Ctrl Pts',(149.820527950492,4.76924502247113,129.595142110464));
#33045=CARTESIAN_POINT('Ctrl Pts',(149.812770909607,4.73370875275085,129.462728292858));
#33046=CARTESIAN_POINT('Ctrl Pts',(149.805013868722,4.69266754916007,129.331929180942));
#33047=CARTESIAN_POINT('Ctrl Pts',(149.797262677482,4.65165729506016,129.201228705652));
#33048=CARTESIAN_POINT('Ctrl Pts',(149.789511486242,4.60515048660142,129.072140883893));
#33049=CARTESIAN_POINT('Ctrl Pts',(149.781760295002,4.55330070414402,128.945157626997));
#33050=CARTESIAN_POINT('Ctrl Pts',(149.774012398225,4.50147295922729,128.818228341372));
#33051=CARTESIAN_POINT('Ctrl Pts',(149.766264501448,4.44430690445549,128.693402202724));
#33052=CARTESIAN_POINT('Ctrl Pts',(149.758516604671,4.3820051841767,128.571153589915));
#33053=CARTESIAN_POINT('Ctrl Pts',(149.750770328587,4.31971649607473,128.448930548881));
#33054=CARTESIAN_POINT('Ctrl Pts',(149.743024052503,4.25229445666001,128.329284309379));
#33055=CARTESIAN_POINT('Ctrl Pts',(149.735277776418,4.17998866512098,128.21266661133));
#33056=CARTESIAN_POINT('Ctrl Pts',(149.727531443153,4.10768233983702,128.096048052435));
#33057=CARTESIAN_POINT('Ctrl Pts',(149.719785109888,4.03049239651298,127.982458411881));
#33058=CARTESIAN_POINT('Ctrl Pts',(149.712038776622,3.94871273692421,127.872321943921));
#33059=CARTESIAN_POINT('Ctrl Pts',(149.704290708619,3.86691476334772,127.762160811662));
#33060=CARTESIAN_POINT('Ctrl Pts',(149.696542640616,3.78052526126477,127.655454704635));
#33061=CARTESIAN_POINT('Ctrl Pts',(149.688794572614,3.68987927119882,127.552595861856));
#33062=CARTESIAN_POINT('Ctrl Pts',(149.681038269872,3.5991369414959,127.449627699475));
#33063=CARTESIAN_POINT('Ctrl Pts',(149.67328196713,3.50412934584402,127.350515263182));
#33064=CARTESIAN_POINT('Ctrl Pts',(149.665525664388,3.40522973261341,127.255615271584));
#33065=CARTESIAN_POINT('Ctrl Pts',(149.657765221874,3.30627733368134,127.160664629004));
#33066=CARTESIAN_POINT('Ctrl Pts',(149.65000477936,3.20342907103866,127.069931169583));
#33067=CARTESIAN_POINT('Ctrl Pts',(149.642244336845,3.0970915554587,126.983731486179));
#33068=CARTESIAN_POINT('Ctrl Pts',(149.63447143658,2.99058333745853,126.89739342739));
#33069=CARTESIAN_POINT('Ctrl Pts',(149.626698536315,2.88057498735286,126.815603921823));
#33070=CARTESIAN_POINT('Ctrl Pts',(149.618925636049,2.76750312073579,126.738636876432));
#33071=CARTESIAN_POINT('Ctrl Pts',(149.611435300287,2.65854170128125,126.66446777701));
#33072=CARTESIAN_POINT('Ctrl Pts',(149.603944964525,2.5467358928218,126.594776770777));
#33073=CARTESIAN_POINT('Ctrl Pts',(149.596454628763,2.43249649337023,126.529767786402));
#33074=CARTESIAN_POINT('Ctrl Pts',(149.588680294644,2.31392567236601,126.462293966625));
#33075=CARTESIAN_POINT('Ctrl Pts',(149.580905960525,2.19235748158222,126.399650478201));
#33076=CARTESIAN_POINT('Ctrl Pts',(149.573131626406,2.06822311222214,126.342114969849));
#33077=CARTESIAN_POINT('Ctrl Pts',(149.565366873459,1.94424172737818,126.284650368869));
#33078=CARTESIAN_POINT('Ctrl Pts',(149.557602120512,1.81770080787187,126.232281385362));
#33079=CARTESIAN_POINT('Ctrl Pts',(149.549837367564,1.68905834571211,126.185241116267));
#33080=CARTESIAN_POINT('Ctrl Pts',(149.542080326679,1.56054365305936,126.13824756823));
#33081=CARTESIAN_POINT('Ctrl Pts',(149.534323285794,1.42993193634857,126.096572335583));
#33082=CARTESIAN_POINT('Ctrl Pts',(149.526566244909,1.29770316604169,126.060401347574));
#33083=CARTESIAN_POINT('Ctrl Pts',(149.518815053669,1.16557411047886,126.024257636388));
#33084=CARTESIAN_POINT('Ctrl Pts',(149.511063862429,1.03183080411126,125.993610010679));
#33085=CARTESIAN_POINT('Ctrl Pts',(149.503312671189,0.896970119812349,125.968595149032));
#33086=CARTESIAN_POINT('Ctrl Pts',(149.495564774412,0.762166754901932,125.943590919369));
#33087=CARTESIAN_POINT('Ctrl Pts',(149.487816877635,0.626247340234282,125.924214763287));
#33088=CARTESIAN_POINT('Ctrl Pts',(149.480068980858,0.489720518402962,125.910552603723));
#33089=CARTESIAN_POINT('Ctrl Pts',(149.472322704774,0.353222255039544,125.896893301988));
#33090=CARTESIAN_POINT('Ctrl Pts',(149.46457642869,0.216117226010545,125.888945658266));
#33091=CARTESIAN_POINT('Ctrl Pts',(149.456830152605,0.0789204073626937,
125.886743854153));
#33092=CARTESIAN_POINT('Ctrl Pts',(149.44908381934,-0.0582774240408593,
125.884542033787));
#33093=CARTESIAN_POINT('Ctrl Pts',(149.441337486075,-0.195566655500435,
125.888086143937));
#33094=CARTESIAN_POINT('Ctrl Pts',(149.433591152809,-0.332431488809621,
125.897358236504));
#33095=CARTESIAN_POINT('Ctrl Pts',(149.425843084806,-0.469326972049227,
125.906632405492));
#33096=CARTESIAN_POINT('Ctrl Pts',(149.418095016803,-0.605797478021365,
125.921637082982));
#33097=CARTESIAN_POINT('Ctrl Pts',(149.4103469488,-0.741331907347136,125.942302404664));
#33098=CARTESIAN_POINT('Ctrl Pts',(149.402590646059,-0.877010384277369,
125.962989689695));
#33099=CARTESIAN_POINT('Ctrl Pts',(149.394834343317,-1.0117504100798,125.9893495779));
#33100=CARTESIAN_POINT('Ctrl Pts',(149.387078040575,-1.14505011742713,126.021260859974));
#33101=CARTESIAN_POINT('Ctrl Pts',(149.379317598061,-1.27842097084193,126.053189174059));
#33102=CARTESIAN_POINT('Ctrl Pts',(149.371557155546,-1.41034959812453,126.09067467913));
#33103=CARTESIAN_POINT('Ctrl Pts',(149.363796713032,-1.54034985768378,126.133546408198));
#33104=CARTESIAN_POINT('Ctrl Pts',(149.356023812767,-1.67055880520047,126.176486958771));
#33105=CARTESIAN_POINT('Ctrl Pts',(149.348250912501,-1.79883283296839,126.224830873735));
#33106=CARTESIAN_POINT('Ctrl Pts',(149.340478012236,-1.92470549391604,126.278358869423));
#33107=CARTESIAN_POINT('Ctrl Pts',(149.332987676474,-2.04600236658388,126.329940987639));
#33108=CARTESIAN_POINT('Ctrl Pts',(149.325497340712,-2.16506915436073,126.386336689635));
#33109=CARTESIAN_POINT('Ctrl Pts',(149.31800700495,-2.28151223992148,126.447310587834));
#33110=CARTESIAN_POINT('Ctrl Pts',(149.310231768601,-2.40238432632126,126.510603674373));
#33111=CARTESIAN_POINT('Ctrl Pts',(149.302456532253,-2.52081210212507,126.579030637407));
#33112=CARTESIAN_POINT('Ctrl Pts',(149.294681295904,-2.63632874284507,126.652378702607));
#33113=CARTESIAN_POINT('Ctrl Pts',(149.286915840311,-2.75170007094013,126.725634500582));
#33114=CARTESIAN_POINT('Ctrl Pts',(149.279150384718,-2.86416722390513,126.803798874773));
#33115=CARTESIAN_POINT('Ctrl Pts',(149.271384929125,-2.97328641825445,126.886612420256));
#33116=CARTESIAN_POINT('Ctrl Pts',(149.263616657703,-3.08244518026236,126.969455994719));
#33117=CARTESIAN_POINT('Ctrl Pts',(149.255848386282,-3.18825320822307,127.056951928444));
#33118=CARTESIAN_POINT('Ctrl Pts',(149.248080114861,-3.29029285746525,127.14879554844));
#33119=CARTESIAN_POINT('Ctrl Pts',(149.240329214054,-3.39210433606394,127.240433797112));
#33120=CARTESIAN_POINT('Ctrl Pts',(149.232578313248,-3.4901639627876,127.336400067624));
#33121=CARTESIAN_POINT('Ctrl Pts',(149.224827412442,-3.5840882724255,127.436350178455));
#33122=CARTESIAN_POINT('Ctrl Pts',(149.217080091668,-3.67796919975373,127.536254123744));
#33123=CARTESIAN_POINT('Ctrl Pts',(149.209332770893,-3.76771834363505,127.6401379636));
#33124=CARTESIAN_POINT('Ctrl Pts',(149.201585450118,-3.85298861839908,127.747620234578));
#33125=CARTESIAN_POINT('Ctrl Pts',(149.193840029964,-3.93823797414069,127.855076137352));
#33126=CARTESIAN_POINT('Ctrl Pts',(149.186094609809,-4.01901040555093,127.966128407808));
#33127=CARTESIAN_POINT('Ctrl Pts',(149.178349189654,-4.09499896150973,128.080362348893));
#33128=CARTESIAN_POINT('Ctrl Pts',(149.170565625101,-4.17136174349028,128.195158865654));
#33129=CARTESIAN_POINT('Ctrl Pts',(149.162782060547,-4.24289315910445,128.313168160968));
#33130=CARTESIAN_POINT('Ctrl Pts',(149.154998495994,-4.30932586238927,128.433940048502));
#33131=CARTESIAN_POINT('Ctrl Pts',(149.1472494548,-4.37546390889053,128.554176262276));
#33132=CARTESIAN_POINT('Ctrl Pts',(149.139500413606,-4.43654823085717,128.677150246));
#33133=CARTESIAN_POINT('Ctrl Pts',(149.131751372412,-4.49236156400216,128.802393924343));
#33134=CARTESIAN_POINT('Ctrl Pts',(149.123950546179,-4.54854788466556,128.928474577045));
#33135=CARTESIAN_POINT('Ctrl Pts',(149.116149719945,-4.59939234242686,129.056855005353));
#33136=CARTESIAN_POINT('Ctrl Pts',(149.108348893712,-4.64472317883897,129.187038864031));
#33137=CARTESIAN_POINT('Ctrl Pts',(149.100548067479,-4.69005401525106,129.31722272271));
#33138=CARTESIAN_POINT('Ctrl Pts',(149.092747241246,-4.72987114286435,129.449209618557));
#33139=CARTESIAN_POINT('Ctrl Pts',(149.084946415013,-4.76405452823403,129.582490119308));
#33140=CARTESIAN_POINT('Ctrl Pts',(150.83493632599,-4.76405452823404,129.582490119308));
#33141=CARTESIAN_POINT('Ctrl Pts',(150.827298245854,-4.79767773639729,129.713586497633));
#33142=CARTESIAN_POINT('Ctrl Pts',(150.819660165717,-4.82587389977647,129.846026514504));
#33143=CARTESIAN_POINT('Ctrl Pts',(150.812022085581,-4.84855461702794,129.979314444193));
#33144=CARTESIAN_POINT('Ctrl Pts',(150.804161643988,-4.87189562027245,130.116482681196));
#33145=CARTESIAN_POINT('Ctrl Pts',(150.796301202394,-4.8893950646696,130.254548500785));
#33146=CARTESIAN_POINT('Ctrl Pts',(150.788440760801,-4.90101392815764,130.392965991319));
#33147=CARTESIAN_POINT('Ctrl Pts',(150.780580319208,-4.91263279164569,130.531383481853));
#33148=CARTESIAN_POINT('Ctrl Pts',(150.772719877615,-4.9183710980918,130.670152180157));
#33149=CARTESIAN_POINT('Ctrl Pts',(150.764859436022,-4.91824806144419,130.808727378438));
#33150=CARTESIAN_POINT('',(151.110140564062,-4.91824999678873,130.804182888505));
#33151=CARTESIAN_POINT('Ctrl Pts',(151.179859891219,-4.76405452823403,129.582490119308));
#33152=CARTESIAN_POINT('Ctrl Pts',(151.171703248589,-4.79983687266862,129.722004937186));
#33153=CARTESIAN_POINT('Ctrl Pts',(151.16354660596,-4.82952429123457,129.863239908004));
#33154=CARTESIAN_POINT('Ctrl Pts',(151.15538996333,-4.85296245138542,130.005650089312));
#33155=CARTESIAN_POINT('Ctrl Pts',(151.147249438033,-4.87635429829,130.147778871494));
#33156=CARTESIAN_POINT('Ctrl Pts',(151.139108912735,-4.89352145798313,130.291077910992));
#33157=CARTESIAN_POINT('Ctrl Pts',(151.130968387437,-4.9043601863316,130.434990579223));
#33158=CARTESIAN_POINT('Ctrl Pts',(151.124025779645,-4.913603943599,130.557725805171));
#33159=CARTESIAN_POINT('Ctrl Pts',(151.117083171854,-4.91824554201133,130.68090699426));
#33160=CARTESIAN_POINT('Ctrl Pts',(151.110140564062,-4.91824999678873,130.804182888505));
#33161=CARTESIAN_POINT('Ctrl Pts',(151.110140564008,-4.91824999678877,130.804182889472));
#33162=CARTESIAN_POINT('Ctrl Pts',(151.102047498551,-4.91825518973788,130.947886798916));
#33163=CARTESIAN_POINT('Ctrl Pts',(151.093954433094,-4.91195784762291,131.09147629153));
#33164=CARTESIAN_POINT('Ctrl Pts',(151.085861367638,-4.89941385205013,131.234391975538));
#33165=CARTESIAN_POINT('Ctrl Pts',(151.07775840512,-4.88685451634673,131.377482432029));
#33166=CARTESIAN_POINT('Ctrl Pts',(151.069655442603,-4.86803331533055,131.519897100418));
#33167=CARTESIAN_POINT('Ctrl Pts',(151.061552480086,-4.84305758079219,131.661084804006));
#33168=CARTESIAN_POINT('Ctrl Pts',(151.053431098674,-4.8180250737541,131.802593442254));
#33169=CARTESIAN_POINT('Ctrl Pts',(151.045309717261,-4.78681012220712,131.942869206641));
#33170=CARTESIAN_POINT('Ctrl Pts',(151.037188335849,-4.74957092612867,132.081372395183));
#33171=CARTESIAN_POINT('Ctrl Pts',(151.029057337182,-4.71228763178285,132.220039597756));
#33172=CARTESIAN_POINT('Ctrl Pts',(151.020926338514,-4.66896595889947,132.356929714758));
#33173=CARTESIAN_POINT('Ctrl Pts',(151.012795339847,-4.61981302748866,132.491521147434));
#33174=CARTESIAN_POINT('Ctrl Pts',(151.00464579797,-4.57054799999613,132.6264195236));
#33175=CARTESIAN_POINT('Ctrl Pts',(150.996496256093,-4.51542525160003,132.759008420918));
#33176=CARTESIAN_POINT('Ctrl Pts',(150.988346714217,-4.4546995750925,132.888787339274));
#33177=CARTESIAN_POINT('Ctrl Pts',(150.981932393367,-4.40690376290869,132.99093340275));
#33178=CARTESIAN_POINT('Ctrl Pts',(150.975518072518,-4.35563793521106,133.091339153192));
#33179=CARTESIAN_POINT('Ctrl Pts',(150.969103751668,-4.30104530403734,133.189773025331));
#33180=CARTESIAN_POINT('Ctrl Pts',(150.961329417549,-4.23487752647494,133.309077598426));
#33181=CARTESIAN_POINT('Ctrl Pts',(150.95355508343,-4.16363718592351,133.425815962002));
#33182=CARTESIAN_POINT('Ctrl Pts',(150.945780749311,-4.08754811721538,133.539526691491));
#33183=CARTESIAN_POINT('Ctrl Pts',(150.938015996364,-4.01155282148424,133.653097282668));
#33184=CARTESIAN_POINT('Ctrl Pts',(150.930251243417,-3.93072090264591,133.763647342098));
#33185=CARTESIAN_POINT('Ctrl Pts',(150.92248649047,-3.84532225986233,133.870739553756));
#33186=CARTESIAN_POINT('Ctrl Pts',(150.914729449585,-3.76000843621474,133.977725399919));
#33187=CARTESIAN_POINT('Ctrl Pts',(150.9069724087,-3.67013715711599,134.081259929191));
#33188=CARTESIAN_POINT('Ctrl Pts',(150.899215367815,-3.57602162823383,134.180934676713));
#33189=CARTESIAN_POINT('Ctrl Pts',(150.891464176575,-3.48197707260397,134.280534258733));
#33190=CARTESIAN_POINT('Ctrl Pts',(150.883712985334,-3.38369490516131,134.37627956944));
#33191=CARTESIAN_POINT('Ctrl Pts',(150.875961794094,-3.28152838637055,134.467795414576));
#33192=CARTESIAN_POINT('Ctrl Pts',(150.868213897317,-3.17940529107565,134.559272363037));
#33193=CARTESIAN_POINT('Ctrl Pts',(150.86046600054,-3.07340141865898,134.646523160974));
#33194=CARTESIAN_POINT('Ctrl Pts',(150.852718103763,-2.96390648363309,134.729209839992));
#33195=CARTESIAN_POINT('Ctrl Pts',(150.844971827679,-2.85443445258724,134.811879222739));
#33196=CARTESIAN_POINT('Ctrl Pts',(150.837225551595,-2.74147312324885,134.889986150088));
#33197=CARTESIAN_POINT('Ctrl Pts',(150.829479275511,-2.62544453403033,134.96323354917));
#33198=CARTESIAN_POINT('Ctrl Pts',(150.821732942245,-2.50941508831524,135.036481488948));
#33199=CARTESIAN_POINT('Ctrl Pts',(150.81398660898,-2.39031866814014,135.104869620177));
#33200=CARTESIAN_POINT('Ctrl Pts',(150.806240275715,-2.26860513087272,135.168144964057));
#33201=CARTESIAN_POINT('Ctrl Pts',(150.798492207712,-2.14686433670245,135.231434478011));
#33202=CARTESIAN_POINT('Ctrl Pts',(150.790744139709,-2.02250560602092,135.289608745949));
#33203=CARTESIAN_POINT('Ctrl Pts',(150.782996071706,-1.8960017888625,135.342461572716));
#33204=CARTESIAN_POINT('Ctrl Pts',(150.775239768964,-1.76936352194175,135.395370572095));
#33205=CARTESIAN_POINT('Ctrl Pts',(150.767483466222,-1.64057597567256,135.442946681492));
#33206=CARTESIAN_POINT('Ctrl Pts',(150.75972716348,-1.51013082398722,135.485032359629));
#33207=CARTESIAN_POINT('Ctrl Pts',(150.751966720966,-1.37961604979662,135.527140500159));
#33208=CARTESIAN_POINT('Ctrl Pts',(150.744206278452,-1.24744228391585,135.563752266027));
#33209=CARTESIAN_POINT('Ctrl Pts',(150.736445835938,-1.11411365251201,135.594760792059));
#33210=CARTESIAN_POINT('Ctrl Pts',(150.728672935672,-0.980570990152776,
135.625819095731));
#33211=CARTESIAN_POINT('Ctrl Pts',(150.720900035407,-0.845870141998508,
135.651256112465));
#33212=CARTESIAN_POINT('Ctrl Pts',(150.713127135141,-0.710523547302674,
135.671016486972));
#33213=CARTESIAN_POINT('Ctrl Pts',(150.705636799379,-0.580097142239193,
135.690058522094));
#33214=CARTESIAN_POINT('Ctrl Pts',(150.698146463617,-0.449071430888062,
135.703829437846));
#33215=CARTESIAN_POINT('Ctrl Pts',(150.690656127855,-0.317905028657354,
135.71232551712));
#33216=CARTESIAN_POINT('Ctrl Pts',(150.682881793736,-0.181765412421204,
135.721143727822));
#33217=CARTESIAN_POINT('Ctrl Pts',(150.675107459617,-0.0450429767317745,
135.724307148691));
#33218=CARTESIAN_POINT('Ctrl Pts',(150.667333125498,0.0917530806579278,
135.72175468706));
#33219=CARTESIAN_POINT('Ctrl Pts',(150.659568372551,0.228380549132573,135.719205371109));
#33220=CARTESIAN_POINT('Ctrl Pts',(150.651803619603,0.365081071632927,135.710954195969));
#33221=CARTESIAN_POINT('Ctrl Pts',(150.644038866656,0.501340834712195,135.696991855453));
#33222=CARTESIAN_POINT('Ctrl Pts',(150.636281825771,0.637465262673801,135.683043382531));
#33223=CARTESIAN_POINT('Ctrl Pts',(150.628524784886,0.773149415981377,135.663395072181));
#33224=CARTESIAN_POINT('Ctrl Pts',(150.620767744001,0.90788034626783,135.638089647969));
#33225=CARTESIAN_POINT('Ctrl Pts',(150.613016552761,1.0425096749123,135.612803306774));
#33226=CARTESIAN_POINT('Ctrl Pts',(150.605265361521,1.17618682863727,135.581868414955));
#33227=CARTESIAN_POINT('Ctrl Pts',(150.597514170281,1.30840519997636,135.545379378885));
#33228=CARTESIAN_POINT('Ctrl Pts',(150.589766273504,1.44056737498005,135.508905851628));
#33229=CARTESIAN_POINT('Ctrl Pts',(150.582018376727,1.57127162468564,135.466882979082));
#33230=CARTESIAN_POINT('Ctrl Pts',(150.57427047995,1.70002295649571,135.419455958931));
#33231=CARTESIAN_POINT('Ctrl Pts',(150.566524203866,1.82874735630267,135.372038859489));
#33232=CARTESIAN_POINT('Ctrl Pts',(150.558777927781,1.95551928412539,135.319219995985));
#33233=CARTESIAN_POINT('Ctrl Pts',(150.551031651697,2.07986068207613,135.261193866147));
#33234=CARTESIAN_POINT('Ctrl Pts',(150.543285318432,2.20420299788708,135.203167307972));
#33235=CARTESIAN_POINT('Ctrl Pts',(150.535538985167,2.32611439373893,135.139933572094));
#33236=CARTESIAN_POINT('Ctrl Pts',(150.527792651901,2.44513887250762,135.071734395038));
#33237=CARTESIAN_POINT('Ctrl Pts',(150.520044583898,2.56419000598339,135.003519945248));
#33238=CARTESIAN_POINT('Ctrl Pts',(150.512296515895,2.6803525967454,134.930338035909));
#33239=CARTESIAN_POINT('Ctrl Pts',(150.504548447892,2.79319757997576,134.852475035628));
#33240=CARTESIAN_POINT('Ctrl Pts',(150.49679214515,2.90616249619667,134.774529281624));
#33241=CARTESIAN_POINT('Ctrl Pts',(150.489035842408,3.01580243902672,134.691892720734));
#33242=CARTESIAN_POINT('Ctrl Pts',(150.481279539667,3.12171910275717,134.604893857255));
#33243=CARTESIAN_POINT('Ctrl Pts',(150.473519097152,3.22769229740017,134.517848559863));
#33244=CARTESIAN_POINT('Ctrl Pts',(150.465758654638,3.32993796190583,134.426436581015));
#33245=CARTESIAN_POINT('Ctrl Pts',(150.457998212124,3.42809369507061,134.331024293098));
#33246=CARTESIAN_POINT('Ctrl Pts',(150.450225311859,3.52640699653218,134.235458840906));
#33247=CARTESIAN_POINT('Ctrl Pts',(150.442452411593,3.6206169778027,134.135880531306));
#33248=CARTESIAN_POINT('Ctrl Pts',(150.434679511328,3.71040008097605,134.032690573068));
#33249=CARTESIAN_POINT('Ctrl Pts',(150.427189175566,3.79691934219794,133.933251829734));
#33250=CARTESIAN_POINT('Ctrl Pts',(150.419698839804,3.87932780109678,133.830459704274));
#33251=CARTESIAN_POINT('Ctrl Pts',(150.412208504042,3.95737443753222,133.724698033631));
#33252=CARTESIAN_POINT('Ctrl Pts',(150.404434169923,4.03838023591081,133.614926377098));
#33253=CARTESIAN_POINT('Ctrl Pts',(150.396659835804,4.11494352760169,133.501607826023));
#33254=CARTESIAN_POINT('Ctrl Pts',(150.388885501685,4.1867376797905,133.385137760816));
#33255=CARTESIAN_POINT('Ctrl Pts',(150.381120748738,4.258443352103,133.268811234556));
#33256=CARTESIAN_POINT('Ctrl Pts',(150.373355995791,4.32539137627902,133.149341251707));
#33257=CARTESIAN_POINT('Ctrl Pts',(150.365591242844,4.38729619404333,133.027155067854));
#33258=CARTESIAN_POINT('Ctrl Pts',(150.357834201959,4.44913952707024,132.905090241041));
#33259=CARTESIAN_POINT('Ctrl Pts',(150.350077161074,4.50594944623636,132.780314928407));
#33260=CARTESIAN_POINT('Ctrl Pts',(150.342320120188,4.55748463496566,132.653283781073));
#33261=CARTESIAN_POINT('Ctrl Pts',(150.334568928948,4.60898096060829,132.526348428914));
#33262=CARTESIAN_POINT('Ctrl Pts',(150.326817737708,4.65521032683379,132.397160988897));
#33263=CARTESIAN_POINT('Ctrl Pts',(150.319066546468,4.69597832668656,132.266198713181));
#33264=CARTESIAN_POINT('Ctrl Pts',(150.311318649691,4.7367289990517,132.135292099925));
#33265=CARTESIAN_POINT('Ctrl Pts',(150.303570752914,4.77202280582424,132.002612523835));
#33266=CARTESIAN_POINT('Ctrl Pts',(150.295822856137,4.80171435033717,131.868654919095));
#33267=CARTESIAN_POINT('Ctrl Pts',(150.288076580053,4.83139968401905,131.734725335397));
#33268=CARTESIAN_POINT('Ctrl Pts',(150.280330303969,4.85548500180989,131.599518636256));
#33269=CARTESIAN_POINT('Ctrl Pts',(150.272584027885,4.87387553819101,131.463542156084));
#33270=CARTESIAN_POINT('Ctrl Pts',(150.264837694619,4.89226621032692,131.327564672164));
#33271=CARTESIAN_POINT('Ctrl Pts',(150.257091361354,4.90496196477,131.190817783313));
#33272=CARTESIAN_POINT('Ctrl Pts',(150.249345028088,4.91191970372013,131.05381579732));
#33273=CARTESIAN_POINT('Ctrl Pts',(150.241596960085,4.91887900080767,130.916783130682));
#33274=CARTESIAN_POINT('Ctrl Pts',(150.233848892082,4.92009770559724,130.779495643613));
#33275=CARTESIAN_POINT('Ctrl Pts',(150.226100824079,4.91558482809408,130.642469109724));
#33276=CARTESIAN_POINT('Ctrl Pts',(150.218344521338,4.911067154251,130.505296942405));
#33277=CARTESIAN_POINT('Ctrl Pts',(150.210588218596,4.90080574239001,130.368386673666));
#33278=CARTESIAN_POINT('Ctrl Pts',(150.202831915854,4.8848616785139,130.232250973978));
#33279=CARTESIAN_POINT('Ctrl Pts',(150.19507147334,4.86890910481085,130.096042614568));
#33280=CARTESIAN_POINT('Ctrl Pts',(150.187311030826,4.84726789723923,129.960610033843));
#33281=CARTESIAN_POINT('Ctrl Pts',(150.179550588311,4.82005040856081,129.826456163423));
#33282=CARTESIAN_POINT('Ctrl Pts',(150.171777688046,4.79278922795327,129.6920869373));
#33283=CARTESIAN_POINT('Ctrl Pts',(150.164004787781,4.75993397196585,129.559000903218));
#33284=CARTESIAN_POINT('Ctrl Pts',(150.156231887515,4.72164729794882,129.427687142746));
#33285=CARTESIAN_POINT('Ctrl Pts',(150.148741551753,4.68475244097071,129.301146968227));
#33286=CARTESIAN_POINT('Ctrl Pts',(150.141251215991,4.64281429956983,129.176252743177));
#33287=CARTESIAN_POINT('Ctrl Pts',(150.133760880229,4.59602012411946,129.053423131192));
#33288=CARTESIAN_POINT('Ctrl Pts',(150.12598654611,4.54745173328399,128.925936397135));
#33289=CARTESIAN_POINT('Ctrl Pts',(150.118212211991,4.49349795623729,128.800270086635));
#33290=CARTESIAN_POINT('Ctrl Pts',(150.110437877872,4.43431488470314,128.676912717898));
#33291=CARTESIAN_POINT('Ctrl Pts',(150.102673124925,4.37520475101538,128.553707376095));
#33292=CARTESIAN_POINT('Ctrl Pts',(150.094908371978,4.31087831324231,128.432805663342));
#33293=CARTESIAN_POINT('Ctrl Pts',(150.087143619031,4.24154068238491,128.314678769985));
#33294=CARTESIAN_POINT('Ctrl Pts',(150.079386578146,4.17227191864001,128.196669201924));
#33295=CARTESIAN_POINT('Ctrl Pts',(150.071629537261,4.09800206326972,128.081429303705));
#33296=CARTESIAN_POINT('Ctrl Pts',(150.063872496376,4.01898318963348,127.969407851832));
#33297=CARTESIAN_POINT('Ctrl Pts',(150.056121305136,3.94002390474433,127.857470876207));
#33298=CARTESIAN_POINT('Ctrl Pts',(150.048370113896,3.85632295433952,127.74874783421));
#33299=CARTESIAN_POINT('Ctrl Pts',(150.040618922655,3.76817678246907,127.643660252368));
#33300=CARTESIAN_POINT('Ctrl Pts',(150.032871025878,3.68006807507323,127.538617335552));
#33301=CARTESIAN_POINT('Ctrl Pts',(150.025123129101,3.58751815468715,127.437207104586));
#33302=CARTESIAN_POINT('Ctrl Pts',(150.017375232324,3.49086483300824,127.339819409821));
#33303=CARTESIAN_POINT('Ctrl Pts',(150.00962895624,3.39423172912051,127.242452086461));
#33304=CARTESIAN_POINT('Ctrl Pts',(150.001882680156,3.29349720646282,127.149105902979));
#33305=CARTESIAN_POINT('Ctrl Pts',(149.994136404072,3.18903687676764,127.060134814931));
#33306=CARTESIAN_POINT('Ctrl Pts',(149.986390070807,3.08457577597028,126.971163070119));
#33307=CARTESIAN_POINT('Ctrl Pts',(149.978643737541,2.97638911089388,126.886566738691));
#33308=CARTESIAN_POINT('Ctrl Pts',(149.970897404276,2.86488628783513,126.80666007597));
#33309=CARTESIAN_POINT('Ctrl Pts',(149.963149336273,2.7533584944923,126.726735518707));
#33310=CARTESIAN_POINT('Ctrl Pts',(149.95540126827,2.6385133831456,126.651502947658));
#33311=CARTESIAN_POINT('Ctrl Pts',(149.947653200267,2.52078975886876,126.581233570687));
#33312=CARTESIAN_POINT('Ctrl Pts',(149.939896897525,2.40294101652282,126.510889510586));
#33313=CARTESIAN_POINT('Ctrl Pts',(149.932140594783,2.28220798617316,126.44551938253));
#33314=CARTESIAN_POINT('Ctrl Pts',(149.924384292042,2.15905501048179,126.385348904048));
#33315=CARTESIAN_POINT('Ctrl Pts',(149.916623849527,2.03583630433914,126.325146310769));
#33316=CARTESIAN_POINT('Ctrl Pts',(149.908863407013,1.91019543721665,126.270149053603));
#33317=CARTESIAN_POINT('Ctrl Pts',(149.901102964499,1.78261626914211,126.220534453815));
#33318=CARTESIAN_POINT('Ctrl Pts',(149.893330064234,1.65483229966107,126.170840208266));
#33319=CARTESIAN_POINT('Ctrl Pts',(149.885557163968,1.52510418159966,126.126546013409));
#33320=CARTESIAN_POINT('Ctrl Pts',(149.877784263703,1.39393131340587,126.087779381543));
#33321=CARTESIAN_POINT('Ctrl Pts',(149.870293927941,1.26752690937505,126.050422014392));
#33322=CARTESIAN_POINT('Ctrl Pts',(149.862803592179,1.13978127082817,126.018197381151));
#33323=CARTESIAN_POINT('Ctrl Pts',(149.855313256417,1.01114784470684,125.99117424068));
#33324=CARTESIAN_POINT('Ctrl Pts',(149.847538922298,0.877637243137432,125.963126509623));
#33325=CARTESIAN_POINT('Ctrl Pts',(149.839764588179,0.742747282670678,125.940593639907));
#33326=CARTESIAN_POINT('Ctrl Pts',(149.83199025406,0.606973338899836,125.923708363168));
#33327=CARTESIAN_POINT('Ctrl Pts',(149.824225501112,0.471366724380364,125.906843896022));
#33328=CARTESIAN_POINT('Ctrl Pts',(149.816460748165,0.334878678450548,125.895613221009));
#33329=CARTESIAN_POINT('Ctrl Pts',(149.808695995218,0.198016494397925,125.890098462324));
#33330=CARTESIAN_POINT('Ctrl Pts',(149.800938954333,0.0612902437953645,
125.884589180975));
#33331=CARTESIAN_POINT('Ctrl Pts',(149.793181913448,-0.0758090173103959,
125.884784533851));
#33332=CARTESIAN_POINT('Ctrl Pts',(149.785424872563,-0.212767468727311,
125.890715019158));
#33333=CARTESIAN_POINT('Ctrl Pts',(149.777673681323,-0.34962263871105,125.896641032241));
#33334=CARTESIAN_POINT('Ctrl Pts',(149.769922490083,-0.486336821343375,
125.908293552443));
#33335=CARTESIAN_POINT('Ctrl Pts',(149.762171298843,-0.622395139168448,
125.925651018375));
#33336=CARTESIAN_POINT('Ctrl Pts',(149.754423402066,-0.758395628578369,
125.94300110692));
#33337=CARTESIAN_POINT('Ctrl Pts',(149.746675505288,-0.89374042060341,125.966051269171));
#33338=CARTESIAN_POINT('Ctrl Pts',(149.738927608511,-1.02791892762871,125.994728018217));
#33339=CARTESIAN_POINT('Ctrl Pts',(149.731181332427,-1.16206936740281,126.023398768704));
#33340=CARTESIAN_POINT('Ctrl Pts',(149.723435056343,-1.29505362534163,126.057693683287));
#33341=CARTESIAN_POINT('Ctrl Pts',(149.715688780259,-1.42637088129404,126.0974880708));
#33342=CARTESIAN_POINT('Ctrl Pts',(149.707942446994,-1.55768910660073,126.137282752067));
#33343=CARTESIAN_POINT('Ctrl Pts',(149.700196113728,-1.68733993120418,126.182576873884));
#33344=CARTESIAN_POINT('Ctrl Pts',(149.692449780463,-1.81483766909694,126.233195853819));
#33345=CARTESIAN_POINT('Ctrl Pts',(149.68470171246,-1.94236395922391,126.283826169522));
#33346=CARTESIAN_POINT('Ctrl Pts',(149.676953644457,-2.06773583987514,126.339783571972));
#33347=CARTESIAN_POINT('Ctrl Pts',(149.669205576454,-2.19048795133432,126.400845476504));
#33348=CARTESIAN_POINT('Ctrl Pts',(149.661449273712,-2.31337052519833,126.461972278356));
#33349=CARTESIAN_POINT('Ctrl Pts',(149.65369297097,-2.43362741728175,126.528214245158));
#33350=CARTESIAN_POINT('Ctrl Pts',(149.645936668228,-2.55081773648536,126.599302718115));
#33351=CARTESIAN_POINT('Ctrl Pts',(149.638176225714,-2.66807060369137,126.670429133131));
#33352=CARTESIAN_POINT('Ctrl Pts',(149.6304157832,-2.7822533113771,126.746406992095));
#33353=CARTESIAN_POINT('Ctrl Pts',(149.622655340686,-2.89295513597643,126.826925056337));
#33354=CARTESIAN_POINT('Ctrl Pts',(149.61488244042,-3.00383466897184,126.907572375323));
#33355=CARTESIAN_POINT('Ctrl Pts',(149.607109540155,-3.1112218461797,126.992774220874));
#33356=CARTESIAN_POINT('Ctrl Pts',(149.599336639889,-3.214739450831,127.082179358442));
#33357=CARTESIAN_POINT('Ctrl Pts',(149.591846304127,-3.31449392980714,127.168334394062));
#33358=CARTESIAN_POINT('Ctrl Pts',(149.584355968365,-3.41065506439533,127.258392216318));
#33359=CARTESIAN_POINT('Ctrl Pts',(149.576865632604,-3.50291990667291,127.352008493298));
#33360=CARTESIAN_POINT('Ctrl Pts',(149.569197320369,-3.59737703667771,127.447849169195));
#33361=CARTESIAN_POINT('Ctrl Pts',(149.561529008135,-3.68806722165813,127.54774133921));
#33362=CARTESIAN_POINT('Ctrl Pts',(149.5538606959,-3.77461559262725,127.651352499848));
#33363=CARTESIAN_POINT('Ctrl Pts',(149.546201379826,-3.86106242847899,127.75484210798));
#33364=CARTESIAN_POINT('Ctrl Pts',(149.538542063751,-3.94337685520339,127.862041727308));
#33365=CARTESIAN_POINT('Ctrl Pts',(149.530882747676,-4.02121958990375,127.97258095236));
#33366=CARTESIAN_POINT('Ctrl Pts',(149.52323064977,-4.09898896532333,128.083016004838));
#33367=CARTESIAN_POINT('Ctrl Pts',(149.515578551863,-4.17229479881784,128.196784077586));
#33368=CARTESIAN_POINT('Ctrl Pts',(149.507926453956,-4.24083735305767,128.313480932111));
#33369=CARTESIAN_POINT('Ctrl Pts',(149.500280175115,-4.30932778386069,128.430089044086));
#33370=CARTESIAN_POINT('Ctrl Pts',(149.492633896274,-4.37306194064365,128.549621160038));
#33371=CARTESIAN_POINT('Ctrl Pts',(149.484987617433,-4.43178314844268,128.67164376161));
#33372=CARTESIAN_POINT('Ctrl Pts',(149.477344690191,-4.49047861693751,128.793612876938));
#33373=CARTESIAN_POINT('Ctrl Pts',(149.469701762948,-4.54416533374774,128.918069944154));
#33374=CARTESIAN_POINT('Ctrl Pts',(149.462058835706,-4.59263257083703,129.04455689789));
#33375=CARTESIAN_POINT('Ctrl Pts',(149.454416774795,-4.6410943141279,129.171029514232));
#33376=CARTESIAN_POINT('Ctrl Pts',(149.446774713884,-4.68433760733893,129.299531185077));
#33377=CARTESIAN_POINT('Ctrl Pts',(149.439132652973,-4.72220003377671,129.429584307216));
#33378=CARTESIAN_POINT('Ctrl Pts',(149.436150982645,-4.7369726552922,129.480326579464));
#33379=CARTESIAN_POINT('Ctrl Pts',(149.433169312318,-4.7509266820847,129.531304846415));
#33380=CARTESIAN_POINT('Ctrl Pts',(149.43018764199,-4.76405452823406,129.582490119308));
#33381=CARTESIAN_POINT('Origin',(213.235140564004,0.,130.804360617566));
#33382=CARTESIAN_POINT('',(147.334614341604,-4.76405452823404,129.582490119308));
#33383=CARTESIAN_POINT('',(147.680233368326,-4.76405452823403,129.582490119308));
#33384=CARTESIAN_POINT('',(213.235140564004,-4.76405452823405,129.582490119308));
#33385=CARTESIAN_POINT('',(149.014859435954,-4.918249342247,130.80181700066));
#33386=CARTESIAN_POINT('Ctrl Pts',(149.014859435953,-4.918249342247,130.80181700066));
#33387=CARTESIAN_POINT('Ctrl Pts',(149.007179426612,-4.91831912604006,130.936748520212));
#33388=CARTESIAN_POINT('Ctrl Pts',(148.99949941727,-4.91283197951487,131.071905857874));
#33389=CARTESIAN_POINT('Ctrl Pts',(148.991819407929,-4.90175849519354,131.206786657104));
#33390=CARTESIAN_POINT('Ctrl Pts',(148.984148181936,-4.89069767521578,131.34151319804));
#33391=CARTESIAN_POINT('Ctrl Pts',(148.976476955943,-4.87406325677253,131.475963433587));
#33392=CARTESIAN_POINT('Ctrl Pts',(148.968805729951,-4.85187782821074,131.609633616379));
#33393=CARTESIAN_POINT('Ctrl Pts',(148.961141337866,-4.82971216352713,131.743184719153));
#33394=CARTESIAN_POINT('Ctrl Pts',(148.953476945781,-4.80200539131236,131.875956758268));
#33395=CARTESIAN_POINT('Ctrl Pts',(148.945812553697,-4.7688319828449,132.007450216015));
#33396=CARTESIAN_POINT('Ctrl Pts',(148.938116687181,-4.73552234515806,132.139483662021));
#33397=CARTESIAN_POINT('Ctrl Pts',(148.930420820666,-4.69670110519183,132.270227594894));
#33398=CARTESIAN_POINT('Ctrl Pts',(148.92272495415,-4.65249580553531,132.399185323286));
#33399=CARTESIAN_POINT('Ctrl Pts',(148.915067460644,-4.60851092165367,132.527500044668));
#33400=CARTESIAN_POINT('Ctrl Pts',(148.907409967138,-4.55919568686713,132.654045953508));
#33401=CARTESIAN_POINT('Ctrl Pts',(148.899752473632,-4.50472583585498,132.778348511724));
#33402=CARTESIAN_POINT('Ctrl Pts',(148.892095580377,-4.45026025459386,132.902641326182));
#33403=CARTESIAN_POINT('Ctrl Pts',(148.884438687122,-4.39064102149756,133.024690772476));
#33404=CARTESIAN_POINT('Ctrl Pts',(148.876781793867,-4.32609179803745,133.144042821938));
#33405=CARTESIAN_POINT('Ctrl Pts',(148.86912374989,-4.26153287374632,133.263412808316));
#33406=CARTESIAN_POINT('Ctrl Pts',(148.861465705913,-4.19204267667199,133.380084239163));
#33407=CARTESIAN_POINT('Ctrl Pts',(148.853807661936,-4.11789028459296,133.49362867162));
#33408=CARTESIAN_POINT('Ctrl Pts',(148.846083003218,-4.04309286587704,133.60816078878));
#33409=CARTESIAN_POINT('Ctrl Pts',(148.8383583445,-3.96355197716302,133.719510895084));
#33410=CARTESIAN_POINT('Ctrl Pts',(148.830633685783,-3.87958705625758,133.827271025669));
#33411=CARTESIAN_POINT('Ctrl Pts',(148.822964187473,-3.79622171385506,133.934261660409));
#33412=CARTESIAN_POINT('Ctrl Pts',(148.815294689164,-3.70849562683673,134.037713159311));
#33413=CARTESIAN_POINT('Ctrl Pts',(148.807625190855,-3.61675985563495,134.137261937612));
#33414=CARTESIAN_POINT('Ctrl Pts',(148.799872951933,-3.52403441423975,134.237884674931));
#33415=CARTESIAN_POINT('Ctrl Pts',(148.792120713011,-3.42721257078373,134.334519698674));
#33416=CARTESIAN_POINT('Ctrl Pts',(148.784368474089,-3.32669194495889,134.426832669335));
#33417=CARTESIAN_POINT('Ctrl Pts',(148.776616235168,-3.22617131913406,134.519145639995));
#33418=CARTESIAN_POINT('Ctrl Pts',(148.768863996246,-3.12195227097812,134.607136339945));
#33419=CARTESIAN_POINT('Ctrl Pts',(148.761111757324,-3.01446250585793,134.690515383305));
#33420=CARTESIAN_POINT('Ctrl Pts',(148.753337423205,-2.90666637665375,134.774132071098));
#33421=CARTESIAN_POINT('Ctrl Pts',(148.745563089086,-2.79521776641346,134.853392647225));
#33422=CARTESIAN_POINT('Ctrl Pts',(148.737788754967,-2.68050410340236,134.927961084893));
#33423=CARTESIAN_POINT('Ctrl Pts',(148.73002400202,-2.56593181472891,135.002437623627));
#33424=CARTESIAN_POINT('Ctrl Pts',(148.722259249073,-2.44810280426747,135.072233318599));
#33425=CARTESIAN_POINT('Ctrl Pts',(148.714494496126,-2.3274373519524,135.137052440814));
#33426=CARTESIAN_POINT('Ctrl Pts',(148.706737455241,-2.20689174626573,135.201807183762));
#33427=CARTESIAN_POINT('Ctrl Pts',(148.698980414356,-2.08351564725758,135.261595006534));
#33428=CARTESIAN_POINT('Ctrl Pts',(148.691223373471,-1.95775778418675,135.316163751675));
#33429=CARTESIAN_POINT('Ctrl Pts',(148.683472182231,-1.83209475609824,135.370691346101));
#33430=CARTESIAN_POINT('Ctrl Pts',(148.675720990991,-1.70405389619313,135.420007541762));
#33431=CARTESIAN_POINT('Ctrl Pts',(148.66796979975,-1.57410765396314,135.463906534953));
#33432=CARTESIAN_POINT('Ctrl Pts',(148.660221902973,-1.44421664235275,135.5077868699));
#33433=CARTESIAN_POINT('Ctrl Pts',(148.652474006196,-1.31242222874879,135.546254456916));
#33434=CARTESIAN_POINT('Ctrl Pts',(148.644726109419,-1.17921571568869,135.57915206415));
#33435=CARTESIAN_POINT('Ctrl Pts',(148.636979833335,-1.04603706655952,135.612042789914));
#33436=CARTESIAN_POINT('Ctrl Pts',(148.629233557251,-0.911447284823557,
135.639365759701));
#33437=CARTESIAN_POINT('Ctrl Pts',(148.621487281167,-0.775951284682872,
135.661014060658));
#33438=CARTESIAN_POINT('Ctrl Pts',(148.613740947901,-0.640454284341493,
135.682662521418));
#33439=CARTESIAN_POINT('Ctrl Pts',(148.605994614636,-0.504051438315701,
135.698636168077));
#33440=CARTESIAN_POINT('Ctrl Pts',(148.598248281371,-0.367255872060017,
135.708879573278));
#33441=CARTESIAN_POINT('Ctrl Pts',(148.590500213368,-0.230429671385745,
135.719125272418));
#33442=CARTESIAN_POINT('Ctrl Pts',(148.582752145365,-0.0932109652763536,
135.723638147398));
#33443=CARTESIAN_POINT('Ctrl Pts',(148.575004077362,0.0438844049726258,
135.722414828481));
#33444=CARTESIAN_POINT('Ctrl Pts',(148.56724777462,0.181125481812562,135.721190209407));
#33445=CARTESIAN_POINT('Ctrl Pts',(148.559491471878,0.318242569367009,135.714217221526));
#33446=CARTESIAN_POINT('Ctrl Pts',(148.551735169136,0.454721678907472,135.701544630571));
#33447=CARTESIAN_POINT('Ctrl Pts',(148.543974726622,0.591273631458189,135.688865275873));
#33448=CARTESIAN_POINT('Ctrl Pts',(148.536214284108,0.727186540256706,135.670480308943));
#33449=CARTESIAN_POINT('Ctrl Pts',(148.528453841594,0.861954922358426,135.646489981216));
#33450=CARTESIAN_POINT('Ctrl Pts',(148.520680941328,0.996939646631087,135.622461142085));
#33451=CARTESIAN_POINT('Ctrl Pts',(148.512908041063,1.13077579077568,135.592809045459));
#33452=CARTESIAN_POINT('Ctrl Pts',(148.505135140797,1.26297051073684,135.557684565238));
#33453=CARTESIAN_POINT('Ctrl Pts',(148.497644805035,1.39035961964847,135.523836948346));
#33454=CARTESIAN_POINT('Ctrl Pts',(148.490154469273,1.51622427800469,135.484908001123));
#33455=CARTESIAN_POINT('Ctrl Pts',(148.482664133511,1.64014144928102,135.441074873249));
#33456=CARTESIAN_POINT('Ctrl Pts',(148.474889799392,1.76875697777074,135.395579799007));
#33457=CARTESIAN_POINT('Ctrl Pts',(148.467115465273,1.89568184136087,135.344657204267));
#33458=CARTESIAN_POINT('Ctrl Pts',(148.459341131154,2.02042391675374,135.288451412712));
#33459=CARTESIAN_POINT('Ctrl Pts',(148.451576378207,2.14501225868712,135.232314889771));
#33460=CARTESIAN_POINT('Ctrl Pts',(148.44381162526,2.26742281187251,135.170908284166));
#33461=CARTESIAN_POINT('Ctrl Pts',(148.436046872313,2.38717959955839,135.104425340562));
#33462=CARTESIAN_POINT('Ctrl Pts',(148.428289831428,2.50681744311466,135.038008428754));
#33463=CARTESIAN_POINT('Ctrl Pts',(148.420532790543,2.62380642683538,134.966525401073));
#33464=CARTESIAN_POINT('Ctrl Pts',(148.412775749658,2.73769185438608,134.890217488888));
#33465=CARTESIAN_POINT('Ctrl Pts',(148.405024558417,2.85149140004965,134.813967121093));
#33466=CARTESIAN_POINT('Ctrl Pts',(148.397273367177,2.96219172451724,134.732899327719));
#33467=CARTESIAN_POINT('Ctrl Pts',(148.389522175937,3.06936430881091,134.647300351975));
#33468=CARTESIAN_POINT('Ctrl Pts',(148.38177427916,3.17649134189743,134.561737758078));
#33469=CARTESIAN_POINT('Ctrl Pts',(148.374026382383,3.28009331212357,134.471648055707));
#33470=CARTESIAN_POINT('Ctrl Pts',(148.366278485606,3.37977237485689,134.377359603943));
#33471=CARTESIAN_POINT('Ctrl Pts',(148.358532209522,3.47943058687919,134.283090875291));
#33472=CARTESIAN_POINT('Ctrl Pts',(148.350785933438,3.57516723975498,134.184625412707));
#33473=CARTESIAN_POINT('Ctrl Pts',(148.343039657354,3.66661946621151,134.082330225799));
#33474=CARTESIAN_POINT('Ctrl Pts',(148.335293324088,3.75807236774757,133.980034283771));
#33475=CARTESIAN_POINT('Ctrl Pts',(148.327546990823,3.84524051918084,133.873908852477));
#33476=CARTESIAN_POINT('Ctrl Pts',(148.319800657557,3.92779993106341,133.764355679055));
#33477=CARTESIAN_POINT('Ctrl Pts',(148.312052589554,4.01037783155359,133.654777971959));
#33478=CARTESIAN_POINT('Ctrl Pts',(148.304304521552,4.08834470348989,133.541771307433));
#33479=CARTESIAN_POINT('Ctrl Pts',(148.296556453549,4.16141888699936,133.425767855945));
#33480=CARTESIAN_POINT('Ctrl Pts',(148.288800150807,4.23457073462087,133.309641114608));
#33481=CARTESIAN_POINT('Ctrl Pts',(148.281043848065,4.3028192975253,133.190511555216));
#33482=CARTESIAN_POINT('Ctrl Pts',(148.273287545323,4.36592778024305,133.068837970114));
#33483=CARTESIAN_POINT('Ctrl Pts',(148.265527102809,4.42906994585831,132.947099444156));
#33484=CARTESIAN_POINT('Ctrl Pts',(148.257766660295,4.48706639955389,132.822814541027));
#33485=CARTESIAN_POINT('Ctrl Pts',(148.25000621778,4.5397282598225,132.696462726193));
#33486=CARTESIAN_POINT('Ctrl Pts',(148.242233317515,4.59247465758425,132.569908080209));
#33487=CARTESIAN_POINT('Ctrl Pts',(148.23446041725,4.6398692139415,132.441280259184));
#33488=CARTESIAN_POINT('Ctrl Pts',(148.226687516984,4.68177246912884,132.311075457809));
#33489=CARTESIAN_POINT('Ctrl Pts',(148.219197181222,4.72215243544235,132.185603928929));
#33490=CARTESIAN_POINT('Ctrl Pts',(148.21170684546,4.75743333187616,132.058668380314));
#33491=CARTESIAN_POINT('Ctrl Pts',(148.204216509698,4.78753553789668,131.930720478302));
#33492=CARTESIAN_POINT('Ctrl Pts',(148.196442175579,4.81877907820772,131.797921392696));
#33493=CARTESIAN_POINT('Ctrl Pts',(148.18866784146,4.8445424461326,131.663611003948));
#33494=CARTESIAN_POINT('Ctrl Pts',(148.180893507341,4.86468106061032,131.528281359802));
#33495=CARTESIAN_POINT('Ctrl Pts',(148.173128754394,4.88479485604551,131.393118497348));
#33496=CARTESIAN_POINT('Ctrl Pts',(148.165364001446,4.89929763366519,131.256939261837));
#33497=CARTESIAN_POINT('Ctrl Pts',(148.157599248499,4.90809511928264,131.120248829714));
#33498=CARTESIAN_POINT('Ctrl Pts',(148.149842207614,4.91688386711335,130.983694160455));
#33499=CARTESIAN_POINT('Ctrl Pts',(148.142085166729,4.91997857473634,130.846629692619));
#33500=CARTESIAN_POINT('Ctrl Pts',(148.134328125844,4.9173364224597,130.709568366558));
#33501=CARTESIAN_POINT('Ctrl Pts',(148.126576934604,4.91469626265065,130.572610399508));
#33502=CARTESIAN_POINT('Ctrl Pts',(148.118825743364,4.90632786150677,130.435655958828));
#33503=CARTESIAN_POINT('Ctrl Pts',(148.111074552124,4.89224041857029,130.299220291115));
#33504=CARTESIAN_POINT('Ctrl Pts',(148.103326655347,4.87815896317286,130.1628426122));
#33505=CARTESIAN_POINT('Ctrl Pts',(148.09557875857,4.85836334062089,130.026983655794));
#33506=CARTESIAN_POINT('Ctrl Pts',(148.087830861793,4.83291476396836,129.892155625957));
#33507=CARTESIAN_POINT('Ctrl Pts',(148.080084585709,4.80747151060945,129.757355799237));
#33508=CARTESIAN_POINT('Ctrl Pts',(148.072338309624,4.77637772762758,129.623586854091));
#33509=CARTESIAN_POINT('Ctrl Pts',(148.06459203354,4.73974605197591,129.491352458689));
#33510=CARTESIAN_POINT('Ctrl Pts',(148.056845700275,4.70311410591752,129.359117087162));
#33511=CARTESIAN_POINT('Ctrl Pts',(148.04909936701,4.66094428999194,129.228416664759));
#33512=CARTESIAN_POINT('Ctrl Pts',(148.041353033744,4.6133994812327,129.099740927118));
#33513=CARTESIAN_POINT('Ctrl Pts',(148.033604965741,4.5658440251431,128.971036373438));
#33514=CARTESIAN_POINT('Ctrl Pts',(148.025856897738,4.5129113164903,128.844357773423));
#33515=CARTESIAN_POINT('Ctrl Pts',(148.018108829735,4.45481270848735,128.720175694197));
#33516=CARTESIAN_POINT('Ctrl Pts',(148.010352526993,4.39665235259258,128.595861632779));
#33517=CARTESIAN_POINT('Ctrl Pts',(148.002596224252,4.33331529566538,128.474049747155));
#33518=CARTESIAN_POINT('Ctrl Pts',(147.99483992151,4.26505953896349,128.35518724853));
#33519=CARTESIAN_POINT('Ctrl Pts',(147.987079478996,4.19676735210905,128.23626130941));
#33520=CARTESIAN_POINT('Ctrl Pts',(147.979319036481,4.12355144303966,128.120288224402));
#33521=CARTESIAN_POINT('Ctrl Pts',(147.971558593967,4.04571310456317,128.007686067665));
#33522=CARTESIAN_POINT('Ctrl Pts',(147.963785693702,3.96774981307556,127.894903151949));
#33523=CARTESIAN_POINT('Ctrl Pts',(147.956012793436,3.88514949970579,127.785502290229));
#33524=CARTESIAN_POINT('Ctrl Pts',(147.948239893171,3.79825424568981,127.679869019306));
#33525=CARTESIAN_POINT('Ctrl Pts',(147.940749557409,3.7145178530339,127.578075783855));
#33526=CARTESIAN_POINT('Ctrl Pts',(147.933259221647,3.62679356729015,127.479781201881));
#33527=CARTESIAN_POINT('Ctrl Pts',(147.925768885885,3.53541835129655,127.385296397079));
#33528=CARTESIAN_POINT('Ctrl Pts',(147.917994551766,3.44057861621496,127.287229172184));
#33529=CARTESIAN_POINT('Ctrl Pts',(147.910220217647,3.34150521196224,127.192955675261));
#33530=CARTESIAN_POINT('Ctrl Pts',(147.902445883528,3.23853396264591,127.102863510274));
#33531=CARTESIAN_POINT('Ctrl Pts',(147.894681130581,3.13568961619176,127.01288237583));
#33532=CARTESIAN_POINT('Ctrl Pts',(147.886916377634,3.02895727411363,126.927072575122));
#33533=CARTESIAN_POINT('Ctrl Pts',(147.879151624686,2.91871099816158,126.845786483902));
#33534=CARTESIAN_POINT('Ctrl Pts',(147.871394583801,2.80857422036444,126.764581127174));
#33535=CARTESIAN_POINT('Ctrl Pts',(147.863637542916,2.69493076676894,126.687890769153));
#33536=CARTESIAN_POINT('Ctrl Pts',(147.855880502031,2.57818904353077,126.616028692047));
#33537=CARTESIAN_POINT('Ctrl Pts',(147.848129310791,2.46153535613417,126.544220806693));
#33538=CARTESIAN_POINT('Ctrl Pts',(147.840378119551,2.34178838121044,126.477234159095));
#33539=CARTESIAN_POINT('Ctrl Pts',(147.832626928311,2.21938658289212,126.415339512789));
#33540=CARTESIAN_POINT('Ctrl Pts',(147.824879031534,2.09703680860363,126.353471173359));
#33541=CARTESIAN_POINT('Ctrl Pts',(147.817131134757,1.9720348033289,126.296690706776));
#33542=CARTESIAN_POINT('Ctrl Pts',(147.80938323798,1.8448445860021,126.24522347157));
#33543=CARTESIAN_POINT('Ctrl Pts',(147.801636961896,1.71768097412686,126.193767002201));
#33544=CARTESIAN_POINT('Ctrl Pts',(147.793890685811,1.58833042283198,126.147621700105));
#33545=CARTESIAN_POINT('Ctrl Pts',(147.786144409727,1.4572775654392,126.106965045574));
#33546=CARTESIAN_POINT('Ctrl Pts',(147.778398076462,1.32622374064434,126.066308090925));
#33547=CARTESIAN_POINT('Ctrl Pts',(147.770651743197,1.19346795808586,126.031139980531));
#33548=CARTESIAN_POINT('Ctrl Pts',(147.762905409931,1.05951028524192,126.001588395404));
#33549=CARTESIAN_POINT('Ctrl Pts',(147.755157341928,0.92552261350576,125.972030192406));
#33550=CARTESIAN_POINT('Ctrl Pts',(147.747409273925,0.790332897609332,125.948091101723));
#33551=CARTESIAN_POINT('Ctrl Pts',(147.739661205922,0.65445128057406,125.929847658936));
#33552=CARTESIAN_POINT('Ctrl Pts',(147.731904903181,0.518425246939145,125.911584826801));
#33553=CARTESIAN_POINT('Ctrl Pts',(147.724148600439,0.381706231309343,125.899029786992));
#33554=CARTESIAN_POINT('Ctrl Pts',(147.716392297697,0.244809941117924,125.892207204324));
#33555=CARTESIAN_POINT('Ctrl Pts',(147.708631855183,0.107840585254747,125.885380980237));
#33556=CARTESIAN_POINT('Ctrl Pts',(147.700871412669,-0.029305842940348,
125.884293312873));
#33557=CARTESIAN_POINT('Ctrl Pts',(147.693110970154,-0.166114749715804,
125.888916695352));
#33558=CARTESIAN_POINT('Ctrl Pts',(147.685338069889,-0.30314327429402,125.893547499696));
#33559=CARTESIAN_POINT('Ctrl Pts',(147.677565169624,-0.439832804653475,
125.903907644672));
#33560=CARTESIAN_POINT('Ctrl Pts',(147.669792269358,-0.575674074501106,
125.919917719707));
#33561=CARTESIAN_POINT('Ctrl Pts',(147.662301933596,-0.706577172025894,
125.935345788187));
#33562=CARTESIAN_POINT('Ctrl Pts',(147.654811597834,-0.836692306918456,
125.956020091728));
#33563=CARTESIAN_POINT('Ctrl Pts',(147.647321262072,-0.965575585355786,
125.981825303909));
#33564=CARTESIAN_POINT('Ctrl Pts',(147.639546927953,-1.0993455124684,126.008608928554));
#33565=CARTESIAN_POINT('Ctrl Pts',(147.631772593834,-1.23221207039511,126.041005061611));
#33566=CARTESIAN_POINT('Ctrl Pts',(147.623998259715,-1.36366763580874,126.078940674159));
#33567=CARTESIAN_POINT('Ctrl Pts',(147.616233506768,-1.49496119398665,126.116829534455));
#33568=CARTESIAN_POINT('Ctrl Pts',(147.608468753821,-1.62484684755778,126.160244183359));
#33569=CARTESIAN_POINT('Ctrl Pts',(147.600704000874,-1.75282594330959,126.209060379827));
#33570=CARTESIAN_POINT('Ctrl Pts',(147.592946959989,-1.88067792841945,126.257828091361));
#33571=CARTESIAN_POINT('Ctrl Pts',(147.585189919104,-2.0066267611702,126.311986535644));
#33572=CARTESIAN_POINT('Ctrl Pts',(147.577432878219,-2.13018811486396,126.371361445697));
#33573=CARTESIAN_POINT('Ctrl Pts',(147.569681686979,-2.25365628998014,126.430691580669));
#33574=CARTESIAN_POINT('Ctrl Pts',(147.561930495739,-2.37474021869379,126.495230182816));
#33575=CARTESIAN_POINT('Ctrl Pts',(147.554179304498,-2.49297509939969,126.564754714151));
#33576=CARTESIAN_POINT('Ctrl Pts',(147.546431407721,-2.61115972712664,126.634249695705));
#33577=CARTESIAN_POINT('Ctrl Pts',(147.538683510944,-2.72649737896388,126.708726193855));
#33578=CARTESIAN_POINT('Ctrl Pts',(147.530935614167,-2.83854764082894,126.78791562812));
#33579=CARTESIAN_POINT('Ctrl Pts',(147.523189338083,-2.95057446419478,126.867088497663));
#33580=CARTESIAN_POINT('Ctrl Pts',(147.515443061999,-3.05931494628822,126.950972116921));
#33581=CARTESIAN_POINT('Ctrl Pts',(147.507696785915,-3.16435781176599,127.039254682587));
#33582=CARTESIAN_POINT('Ctrl Pts',(147.49995045265,-3.26940145264633,127.127537899935));
#33583=CARTESIAN_POINT('Ctrl Pts',(147.492204119384,-3.37074712314723,127.220219876943));
#33584=CARTESIAN_POINT('Ctrl Pts',(147.484457786119,-3.4680171029287,127.316948907387));
#33585=CARTESIAN_POINT('Ctrl Pts',(147.476709718116,-3.56530886564702,127.413699599626));
#33586=CARTESIAN_POINT('Ctrl Pts',(147.468961650113,-3.65852284426262,127.514498873121));
#33587=CARTESIAN_POINT('Ctrl Pts',(147.46121358211,-3.7473189024605,127.618958899452));
#33588=CARTESIAN_POINT('Ctrl Pts',(147.453457279369,-3.83620933416645,127.723529947143));
#33589=CARTESIAN_POINT('Ctrl Pts',(147.445700976627,-3.9206722122305,127.831769221386));
#33590=CARTESIAN_POINT('Ctrl Pts',(147.437944673885,-4.0004080329813,127.943256174845));
#33591=CARTESIAN_POINT('Ctrl Pts',(147.430184231371,-4.0801864111405,128.054802632248));
#33592=CARTESIAN_POINT('Ctrl Pts',(147.422423788856,-4.15523249092599,128.169599895699));
#33593=CARTESIAN_POINT('Ctrl Pts',(147.414663346342,-4.22529126416093,128.287200154762));
#33594=CARTESIAN_POINT('Ctrl Pts',(147.406890446077,-4.29546250195816,128.4049891962));
#33595=CARTESIAN_POINT('Ctrl Pts',(147.399117545811,-4.36063024856198,128.52558988076));
#33596=CARTESIAN_POINT('Ctrl Pts',(147.391344645546,-4.42058604346647,128.648530824932));
#33597=CARTESIAN_POINT('Ctrl Pts',(147.383854309784,-4.47836229420734,128.767002556115));
#33598=CARTESIAN_POINT('Ctrl Pts',(147.376363974022,-4.53129882576064,128.887647070215));
#33599=CARTESIAN_POINT('Ctrl Pts',(147.36887363826,-4.57925273005628,129.010028570042));
#33600=CARTESIAN_POINT('Ctrl Pts',(147.360048375184,-4.6357529770913,129.154220895448));
#33601=CARTESIAN_POINT('Ctrl Pts',(147.351223112107,-4.68548683024461,129.301206282813));
#33602=CARTESIAN_POINT('Ctrl Pts',(147.342397849031,-4.72820390052873,129.450377258169));
#33603=CARTESIAN_POINT('Ctrl Pts',(147.339803346556,-4.74076211478789,129.494231414301));
#33604=CARTESIAN_POINT('Ctrl Pts',(147.33720884408,-4.75271418880937,129.538274308005));
#33605=CARTESIAN_POINT('Ctrl Pts',(147.334614341604,-4.76405452823404,129.582490119308));
#33606=CARTESIAN_POINT('Ctrl Pts',(149.084946415013,-4.76405452823403,129.582490119308));
#33607=CARTESIAN_POINT('Ctrl Pts',(149.077173469471,-4.79811573982622,129.715294266355));
#33608=CARTESIAN_POINT('Ctrl Pts',(149.069400523929,-4.82658340099087,129.849382389387));
#33609=CARTESIAN_POINT('Ctrl Pts',(149.061627578387,-4.84939077464027,129.984243444637));
#33610=CARTESIAN_POINT('Ctrl Pts',(149.054271512637,-4.87097493977352,130.111871611355));
#33611=CARTESIAN_POINT('Ctrl Pts',(149.046915446886,-4.88749009678853,130.240191692275));
#33612=CARTESIAN_POINT('Ctrl Pts',(149.039559381136,-4.89892268279498,130.368769512863));
#33613=CARTESIAN_POINT('Ctrl Pts',(149.031326066088,-4.91171866445289,130.512680910767));
#33614=CARTESIAN_POINT('Ctrl Pts',(149.023092751039,-4.91817453086599,130.657164349066));
#33615=CARTESIAN_POINT('Ctrl Pts',(149.014859435991,-4.91824934224666,130.801817000001));
#33616=CARTESIAN_POINT('',(149.360140564045,-4.91824792773029,130.808875468254));
#33617=CARTESIAN_POINT('Ctrl Pts',(149.43018764199,-4.76405452823406,129.582490119308));
#33618=CARTESIAN_POINT('Ctrl Pts',(149.422542844658,-4.79771342147254,129.7137256332));
#33619=CARTESIAN_POINT('Ctrl Pts',(149.414898047325,-4.82593757969098,129.846322570406));
#33620=CARTESIAN_POINT('Ctrl Pts',(149.407253249992,-4.84863465409383,129.979784936612));
#33621=CARTESIAN_POINT('Ctrl Pts',(149.399401135668,-4.87194724372685,130.116866629151));
#33622=CARTESIAN_POINT('Ctrl Pts',(149.391549021343,-4.8894286189972,130.254860913363));
#33623=CARTESIAN_POINT('Ctrl Pts',(149.383696907019,-4.90103558399918,130.393224062546));
#33624=CARTESIAN_POINT('Ctrl Pts',(149.375844792694,-4.91264254900116,130.531587211729));
#33625=CARTESIAN_POINT('Ctrl Pts',(149.36799267837,-4.91837511993864,130.670318767624));
#33626=CARTESIAN_POINT('Ctrl Pts',(149.360140564045,-4.91824792773029,130.808875468254));
#33627=CARTESIAN_POINT('Ctrl Pts',(149.360140564008,-4.91824792772968,130.808875468915));
#33628=CARTESIAN_POINT('Ctrl Pts',(149.349520212843,-4.91807589430529,130.996279874428));
#33629=CARTESIAN_POINT('Ctrl Pts',(149.338899861678,-4.90718913097012,131.183212342436));
#33630=CARTESIAN_POINT('Ctrl Pts',(149.328279510512,-4.8857697338849,131.368662992144));
#33631=CARTESIAN_POINT('Ctrl Pts',(149.318325676605,-4.86569458592999,131.542475038132));
#33632=CARTESIAN_POINT('Ctrl Pts',(149.308371842698,-4.83636785883871,131.714986206173));
#33633=CARTESIAN_POINT('Ctrl Pts',(149.298418008791,-4.79797539097165,131.885385691341));
#33634=CARTESIAN_POINT('Ctrl Pts',(149.290643674672,-4.76798936994312,132.018474362879));
#33635=CARTESIAN_POINT('Ctrl Pts',(149.282869340553,-4.73241413513519,132.150525240653));
#33636=CARTESIAN_POINT('Ctrl Pts',(149.275095006434,-4.69133487599886,132.281032600011));
#33637=CARTESIAN_POINT('Ctrl Pts',(149.267330253487,-4.65030624337806,132.411379120712));
#33638=CARTESIAN_POINT('Ctrl Pts',(149.259565500539,-4.6037871992689,132.540185538557));
#33639=CARTESIAN_POINT('Ctrl Pts',(149.251800747592,-4.5519139152385,132.666956325378));
#33640=CARTESIAN_POINT('Ctrl Pts',(149.244043706707,-4.5000921524851,132.793601201665));
#33641=CARTESIAN_POINT('Ctrl Pts',(149.236286665822,-4.44292687978926,132.918214110932));
#33642=CARTESIAN_POINT('Ctrl Pts',(149.228529624937,-4.38060393645091,133.040315047882));
#33643=CARTESIAN_POINT('Ctrl Pts',(149.220778433697,-4.3183279913289,133.162323907566));
#33644=CARTESIAN_POINT('Ctrl Pts',(149.213027242457,-4.25090229428091,133.2818242186));
#33645=CARTESIAN_POINT('Ctrl Pts',(149.205276051217,-4.17856047316595,133.39835665353));
#33646=CARTESIAN_POINT('Ctrl Pts',(149.19752815444,-4.10624939925472,133.514839559066));
#33647=CARTESIAN_POINT('Ctrl Pts',(149.189780257663,-4.02902656287279,133.628356765908));
#33648=CARTESIAN_POINT('Ctrl Pts',(149.182032360886,-3.94717103587984,133.738474431993));
#33649=CARTESIAN_POINT('Ctrl Pts',(149.174286084802,-3.86533263129856,133.848569063836));
#33650=CARTESIAN_POINT('Ctrl Pts',(149.166539808717,-3.77886369671074,133.955265255788));
#33651=CARTESIAN_POINT('Ctrl Pts',(149.158793532633,-3.68808581510577,134.058159333362));
#33652=CARTESIAN_POINT('Ctrl Pts',(149.151047199368,-3.59730726339924,134.161054170476));
#33653=CARTESIAN_POINT('Ctrl Pts',(149.143300866103,-3.50221995985908,134.260146544032));
#33654=CARTESIAN_POINT('Ctrl Pts',(149.135554532837,-3.40318457367438,134.355067282443));
#33655=CARTESIAN_POINT('Ctrl Pts',(149.127806464834,-3.30412700920148,134.450009277696));
#33656=CARTESIAN_POINT('Ctrl Pts',(149.120058396831,-3.20111988493779,134.54077750836));
#33657=CARTESIAN_POINT('Ctrl Pts',(149.112310328828,-3.0945590799535,134.627041242883));
#33658=CARTESIAN_POINT('Ctrl Pts',(149.104554026086,-2.98788502087758,134.713396659531));
#33659=CARTESIAN_POINT('Ctrl Pts',(149.096797723345,-2.87765004068806,134.795237770239));
#33660=CARTESIAN_POINT('Ctrl Pts',(149.089041420603,-2.76428175287462,134.872275249564));
#33661=CARTESIAN_POINT('Ctrl Pts',(149.081280978089,-2.65085295699241,134.949353846111));
#33662=CARTESIAN_POINT('Ctrl Pts',(149.073520535574,-2.5342878533267,135.021623496688));
#33663=CARTESIAN_POINT('Ctrl Pts',(149.06576009306,-2.41504024284893,135.088840012769));
#33664=CARTESIAN_POINT('Ctrl Pts',(149.057987192795,-2.2956012055206,135.156164430769));
#33665=CARTESIAN_POINT('Ctrl Pts',(149.050214292529,-2.17347140474658,135.218419326775));
#33666=CARTESIAN_POINT('Ctrl Pts',(149.042441392264,-2.04912709076797,135.275407612217));
#33667=CARTESIAN_POINT('Ctrl Pts',(149.034951056502,-1.92930300580758,135.330324229939));
#33668=CARTESIAN_POINT('Ctrl Pts',(149.02746072074,-1.80742290355297,135.380350381393));
#33669=CARTESIAN_POINT('Ctrl Pts',(149.019970384978,-1.68392588509735,135.425353657595));
#33670=CARTESIAN_POINT('Ctrl Pts',(149.012196050859,-1.55574643965011,135.472063246694));
#33671=CARTESIAN_POINT('Ctrl Pts',(149.00442171674,-1.42541901291683,135.513509519065));
#33672=CARTESIAN_POINT('Ctrl Pts',(148.996647382621,-1.29341513234875,135.549490790481));
#33673=CARTESIAN_POINT('Ctrl Pts',(148.988882629674,-1.16157393476604,135.585427718196));
#33674=CARTESIAN_POINT('Ctrl Pts',(148.981117876727,-1.02806076781331,135.615912944016));
#33675=CARTESIAN_POINT('Ctrl Pts',(148.97335312378,-0.893366137432455,135.640793187859));
#33676=CARTESIAN_POINT('Ctrl Pts',(148.965596082895,-0.75880528765736,135.665648720292));
#33677=CARTESIAN_POINT('Ctrl Pts',(148.95783904201,-0.623065691638389,135.684910278667));
#33678=CARTESIAN_POINT('Ctrl Pts',(148.950082001125,-0.48665164210719,135.698474760262));
#33679=CARTESIAN_POINT('Ctrl Pts',(148.942330809884,-0.350340463471888,
135.712029012775));
#33680=CARTESIAN_POINT('Ctrl Pts',(148.934579618644,-0.213356231155399,
135.719894701325));
#33681=CARTESIAN_POINT('Ctrl Pts',(148.926828427404,-0.076211671919524,
135.722020105937));
#33682=CARTESIAN_POINT('Ctrl Pts',(148.919080530627,0.060874597220272,135.724144607195));
#33683=CARTESIAN_POINT('Ctrl Pts',(148.91133263385,0.198120667647949,135.720533670992));
#33684=CARTESIAN_POINT('Ctrl Pts',(148.903584737073,0.33501069059189,135.711187586157));
#33685=CARTESIAN_POINT('Ctrl Pts',(148.895838460989,0.471872079094039,135.701843456321));
#33686=CARTESIAN_POINT('Ctrl Pts',(148.888092184905,0.608377178442163,135.686766590674));
#33687=CARTESIAN_POINT('Ctrl Pts',(148.880345908821,0.744012542397229,135.666009350173));
#33688=CARTESIAN_POINT('Ctrl Pts',(148.872599575555,0.879648907581739,135.645251956446));
#33689=CARTESIAN_POINT('Ctrl Pts',(148.86485324229,1.01441513809635,135.618814163338));
#33690=CARTESIAN_POINT('Ctrl Pts',(148.857106909024,1.14780568892352,135.586799865792));
#33691=CARTESIAN_POINT('Ctrl Pts',(148.849358841021,1.28122611163969,135.554778398866));
#33692=CARTESIAN_POINT('Ctrl Pts',(148.841610773019,1.41326986154048,135.517178033721));
#33693=CARTESIAN_POINT('Ctrl Pts',(148.833862705016,1.54344470249761,135.474153066148));
#33694=CARTESIAN_POINT('Ctrl Pts',(148.826106402274,1.67375789482481,135.431082371127));
#33695=CARTESIAN_POINT('Ctrl Pts',(148.818350099532,1.80219783855624,135.382575679695));
#33696=CARTESIAN_POINT('Ctrl Pts',(148.81059379679,1.92828998046452,135.328836367721));
#33697=CARTESIAN_POINT('Ctrl Pts',(148.802833354276,2.05444942154553,135.275068373458));
#33698=CARTESIAN_POINT('Ctrl Pts',(148.795072911762,2.1782582111508,135.21606236187));
#33699=CARTESIAN_POINT('Ctrl Pts',(148.787312469247,2.29926561604861,135.152068138704));
#33700=CARTESIAN_POINT('Ctrl Pts',(148.779539568982,2.4204672727753,135.087971186329));
#33701=CARTESIAN_POINT('Ctrl Pts',(148.771766668717,2.53885822044009,135.018870217994));
#33702=CARTESIAN_POINT('Ctrl Pts',(148.763993768451,2.65401521795891,134.945059385328));
#33703=CARTESIAN_POINT('Ctrl Pts',(148.756503432689,2.76498596855541,134.873931762347));
#33704=CARTESIAN_POINT('Ctrl Pts',(148.749013096927,2.87295355894489,134.798430937313));
#33705=CARTESIAN_POINT('Ctrl Pts',(148.741522761165,2.97756924483162,134.718854768121));
#33706=CARTESIAN_POINT('Ctrl Pts',(148.733748427046,3.08615146624547,134.636261444289));
#33707=CARTESIAN_POINT('Ctrl Pts',(148.725974092927,3.19146654658486,134.549016011712));
#33708=CARTESIAN_POINT('Ctrl Pts',(148.718199758808,3.29308993109058,134.457406164538));
#33709=CARTESIAN_POINT('Ctrl Pts',(148.710435005861,3.39458807385724,134.365909218313));
#33710=CARTESIAN_POINT('Ctrl Pts',(148.702670252913,3.49240328570476,134.270058818865));
#33711=CARTESIAN_POINT('Ctrl Pts',(148.694905499966,3.58614147731454,134.170184791106));
#33712=CARTESIAN_POINT('Ctrl Pts',(148.687148459081,3.67978656683091,134.070409959639));
#33713=CARTESIAN_POINT('Ctrl Pts',(148.679391418196,3.76936242867941,133.966619735954));
#33714=CARTESIAN_POINT('Ctrl Pts',(148.671634377311,3.85450973708102,133.85918266627));
#33715=CARTESIAN_POINT('Ctrl Pts',(148.663883186071,3.93959283523504,133.751826615715));
#33716=CARTESIAN_POINT('Ctrl Pts',(148.656131994831,4.02025378537295,133.640829498264));
#33717=CARTESIAN_POINT('Ctrl Pts',(148.648380803591,4.09617193267615,133.526594729551));
#33718=CARTESIAN_POINT('Ctrl Pts',(148.640632906814,4.17205781274156,133.412408513663));
#33719=CARTESIAN_POINT('Ctrl Pts',(148.632885010037,4.24320468333521,133.294987708382));
#33720=CARTESIAN_POINT('Ctrl Pts',(148.62513711326,4.30933395859403,133.174766468008));
#33721=CARTESIAN_POINT('Ctrl Pts',(148.617390837176,4.37544940103404,133.054570375325));
#33722=CARTESIAN_POINT('Ctrl Pts',(148.609644561091,4.43654914748633,132.931575355064));
#33723=CARTESIAN_POINT('Ctrl Pts',(148.601898285007,4.49239972047262,132.80624168646));
#33724=CARTESIAN_POINT('Ctrl Pts',(148.594151951742,4.54825070573514,132.680907092672));
#33725=CARTESIAN_POINT('Ctrl Pts',(148.586405618477,4.59885228107741,132.553234173209));
#33726=CARTESIAN_POINT('Ctrl Pts',(148.578659285211,4.64401859682732,132.423704415165));
#33727=CARTESIAN_POINT('Ctrl Pts',(148.570911217208,4.68919502726045,132.29414564983));
#33728=CARTESIAN_POINT('Ctrl Pts',(148.563163149205,4.72893364733518,132.162729587564));
#33729=CARTESIAN_POINT('Ctrl Pts',(148.555415081202,4.76309820481994,132.029953761207));
#33730=CARTESIAN_POINT('Ctrl Pts',(148.547658778461,4.79729907280299,131.897036819122));
#33731=CARTESIAN_POINT('Ctrl Pts',(148.539902475719,4.82591394642714,131.762757605292));
#33732=CARTESIAN_POINT('Ctrl Pts',(148.532146172977,4.84885742396003,131.627625304412));
#33733=CARTESIAN_POINT('Ctrl Pts',(148.524385730463,4.87181314711771,131.492420879354));
#33734=CARTESIAN_POINT('Ctrl Pts',(148.516625287949,4.88909139341091,131.356362847647));
#33735=CARTESIAN_POINT('Ctrl Pts',(148.508864845434,4.90065869916805,131.219965450031));
#33736=CARTESIAN_POINT('Ctrl Pts',(148.501091945169,4.91224457379128,131.083349095205));
#33737=CARTESIAN_POINT('Ctrl Pts',(148.493319044903,4.91810117116215,130.946392676658));
#33738=CARTESIAN_POINT('Ctrl Pts',(148.485546144638,4.91824719723337,130.809611275244));
#33739=CARTESIAN_POINT('Ctrl Pts',(148.478055808876,4.9183879148891,130.677802222303));
#33740=CARTESIAN_POINT('Ctrl Pts',(148.470565473114,4.9132260523543,130.546155990567));
#33741=CARTESIAN_POINT('Ctrl Pts',(148.463075137352,4.90282370110143,130.415126987958));
#33742=CARTESIAN_POINT('Ctrl Pts',(148.455300803233,4.89202694153906,130.279129980888));
#33743=CARTESIAN_POINT('Ctrl Pts',(148.447526469114,4.87555026158044,130.143367133725));
#33744=CARTESIAN_POINT('Ctrl Pts',(148.439752134995,4.85340622424147,130.008351142124));
#33745=CARTESIAN_POINT('Ctrl Pts',(148.431987382048,4.83128947744946,129.873501545665));
#33746=CARTESIAN_POINT('Ctrl Pts',(148.424222629101,4.80351933304268,129.73939735549));
#33747=CARTESIAN_POINT('Ctrl Pts',(148.416457876153,4.77016026715726,129.606548408522));
#33748=CARTESIAN_POINT('Ctrl Pts',(148.408700835268,4.73683433396637,129.473831409002));
#33749=CARTESIAN_POINT('Ctrl Pts',(148.400943794383,4.69793062062983,129.34236754839));
#33750=CARTESIAN_POINT('Ctrl Pts',(148.393186753498,4.65356497115811,129.212658345874));
#33751=CARTESIAN_POINT('Ctrl Pts',(148.385435562258,4.60923277816776,129.083046958076));
#33752=CARTESIAN_POINT('Ctrl Pts',(148.377684371018,4.55944697345686,128.955187963051));
#33753=CARTESIAN_POINT('Ctrl Pts',(148.369933179778,4.50437364026346,128.829569192782));
#33754=CARTESIAN_POINT('Ctrl Pts',(148.362185283001,4.4493237147058,128.704003813842));
#33755=CARTESIAN_POINT('Ctrl Pts',(148.354437386224,4.3889908871078,128.580677123211));
#33756=CARTESIAN_POINT('Ctrl Pts',(148.346689489447,4.32358984131344,128.460058174068));
#33757=CARTESIAN_POINT('Ctrl Pts',(148.338943213363,4.25820247600797,128.339464455809));
#33758=CARTESIAN_POINT('Ctrl Pts',(148.331196937279,4.18774918746342,128.221577695912));
#33759=CARTESIAN_POINT('Ctrl Pts',(148.323450661194,4.11249102135881,128.106843117763));
#33760=CARTESIAN_POINT('Ctrl Pts',(148.315704327929,4.03723229971554,127.99210769267));
#33761=CARTESIAN_POINT('Ctrl Pts',(148.307957994664,3.95716884417045,127.880524822668));
#33762=CARTESIAN_POINT('Ctrl Pts',(148.300211661398,3.87260528716628,127.772511123889));
#33763=CARTESIAN_POINT('Ctrl Pts',(148.292463593395,3.78802279273987,127.66447323619));
#33764=CARTESIAN_POINT('Ctrl Pts',(148.284715525392,3.69893843247959,127.560006417994));
#33765=CARTESIAN_POINT('Ctrl Pts',(148.27696745739,3.60569714719512,127.459494230816));
#33766=CARTESIAN_POINT('Ctrl Pts',(148.269211154648,3.51235676396302,127.358875218089));
#33767=CARTESIAN_POINT('Ctrl Pts',(148.261454851906,3.41485089653373,127.262219519467));
#33768=CARTESIAN_POINT('Ctrl Pts',(148.253698549164,3.31356177468985,127.169874212609));
#33769=CARTESIAN_POINT('Ctrl Pts',(148.24593810665,3.21221859179179,127.077479618281));
#33770=CARTESIAN_POINT('Ctrl Pts',(148.238177664136,3.10708843051879,126.98940025079));
#33771=CARTESIAN_POINT('Ctrl Pts',(148.230417221621,2.99858584823882,126.90594222375));
#33772=CARTESIAN_POINT('Ctrl Pts',(148.222644321356,2.8899090879814,126.822350222477));
#33773=CARTESIAN_POINT('Ctrl Pts',(148.21487142109,2.7778494081853,126.74339461167));
#33774=CARTESIAN_POINT('Ctrl Pts',(148.207098520825,2.66285027198336,126.669338067265));
#33775=CARTESIAN_POINT('Ctrl Pts',(148.199608185063,2.55203164404766,126.597973664786));
#33776=CARTESIAN_POINT('Ctrl Pts',(148.192117849301,2.43848382808754,126.531158482037));
#33777=CARTESIAN_POINT('Ctrl Pts',(148.184627513539,2.32262269231376,126.469085898284));
#33778=CARTESIAN_POINT('Ctrl Pts',(148.17685317942,2.20236864636197,126.404659813651));
#33779=CARTESIAN_POINT('Ctrl Pts',(148.169078845301,2.07924147005676,126.34513897606));
#33780=CARTESIAN_POINT('Ctrl Pts',(148.161304511182,1.95367929939125,126.290789940416));
#33781=CARTESIAN_POINT('Ctrl Pts',(148.153539758235,1.82827187287941,126.236507885101));
#33782=CARTESIAN_POINT('Ctrl Pts',(148.145775005288,1.70043577828129,126.187385103614));
#33783=CARTESIAN_POINT('Ctrl Pts',(148.13801025234,1.57063480676853,126.14364292967));
#33784=CARTESIAN_POINT('Ctrl Pts',(148.130253211455,1.44096275541034,126.099944201069));
#33785=CARTESIAN_POINT('Ctrl Pts',(148.12249617057,1.30933007889283,126.061615569065));
#33786=CARTESIAN_POINT('Ctrl Pts',(148.114739129685,1.17622133602967,126.028830654183));
#33787=CARTESIAN_POINT('Ctrl Pts',(148.106987938445,1.04321297150498,125.99607046266));
#33788=CARTESIAN_POINT('Ctrl Pts',(148.099236747205,0.908731134302753,125.96884576023));
#33789=CARTESIAN_POINT('Ctrl Pts',(148.091485555965,0.773276023335518,125.947280501464));
#33790=CARTESIAN_POINT('Ctrl Pts',(148.083737659188,0.63787848440392,125.925724408509));
#33791=CARTESIAN_POINT('Ctrl Pts',(148.075989762411,0.501508879754367,125.909823036373));
#33792=CARTESIAN_POINT('Ctrl Pts',(148.068241865634,0.364677878973141,125.89964930016));
#33793=CARTESIAN_POINT('Ctrl Pts',(148.06049558955,0.227875500287496,125.889477692074));
#33794=CARTESIAN_POINT('Ctrl Pts',(148.052749313466,0.0906123070840266,
125.885031365799));
#33795=CARTESIAN_POINT('Ctrl Pts',(148.045003037381,-0.0465960200271926,
125.886331350327));
#33796=CARTESIAN_POINT('Ctrl Pts',(148.037256704116,-0.183805359979067,
125.887631344452));
#33797=CARTESIAN_POINT('Ctrl Pts',(148.029510370851,-0.320959442082866,
125.894677730318));
#33798=CARTESIAN_POINT('Ctrl Pts',(148.021764037585,-0.457543094113758,
125.907439403218));
#33799=CARTESIAN_POINT('Ctrl Pts',(148.014015969582,-0.59415733310647,125.920203934007));
#33800=CARTESIAN_POINT('Ctrl Pts',(148.00626790158,-0.730200498635566,125.938686262315));
#33801=CARTESIAN_POINT('Ctrl Pts',(147.998519833577,-0.865163440602921,
125.962803504039));
#33802=CARTESIAN_POINT('Ctrl Pts',(147.990763530835,-1.00026982279112,125.986946377854));
#33803=CARTESIAN_POINT('Ctrl Pts',(147.983007228093,-1.13429330253283,126.01673605958));
#33804=CARTESIAN_POINT('Ctrl Pts',(147.975250925351,-1.26673526902769,126.052038572428));
#33805=CARTESIAN_POINT('Ctrl Pts',(147.967490482837,-1.39924792378792,126.087359927291));
#33806=CARTESIAN_POINT('Ctrl Pts',(147.959730040323,-1.53017701031113,126.128199859823));
#33807=CARTESIAN_POINT('Ctrl Pts',(147.951969597808,-1.65904090815876,126.174375053058));
#33808=CARTESIAN_POINT('Ctrl Pts',(147.944196697543,-1.78811166977517,126.220624370812));
#33809=CARTESIAN_POINT('Ctrl Pts',(147.936423797278,-1.91511025542533,126.27222591688));
#33810=CARTESIAN_POINT('Ctrl Pts',(147.928650897012,-2.039575965751,126.328948575929));
#33811=CARTESIAN_POINT('Ctrl Pts',(147.92116056125,-2.15951703399633,126.383609223445));
#33812=CARTESIAN_POINT('Ctrl Pts',(147.913670225488,-2.27710590763376,126.443024978527));
#33813=CARTESIAN_POINT('Ctrl Pts',(147.906179889726,-2.39195510428361,126.506950485685));
#33814=CARTESIAN_POINT('Ctrl Pts',(147.898404501985,-2.51117499830053,126.573308739907));
#33815=CARTESIAN_POINT('Ctrl Pts',(147.890629114244,-2.62782026801909,126.644737020951));
#33816=CARTESIAN_POINT('Ctrl Pts',(147.882853726503,-2.74142964393392,126.721010697481));
#33817=CARTESIAN_POINT('Ctrl Pts',(147.87508815081,-2.85489565200044,126.797188121454));
#33818=CARTESIAN_POINT('Ctrl Pts',(147.867322575116,-2.96533306815711,126.878198557428));
#33819=CARTESIAN_POINT('Ctrl Pts',(147.859556999423,-3.07230485350154,126.963771346419));
#33820=CARTESIAN_POINT('Ctrl Pts',(147.851800787942,-3.17914764563016,127.049240946432));
#33821=CARTESIAN_POINT('Ctrl Pts',(147.844044576462,-3.28253282694053,127.139261699393));
#33822=CARTESIAN_POINT('Ctrl Pts',(147.836288364982,-3.38205254619534,127.233519871009));
#33823=CARTESIAN_POINT('Ctrl Pts',(147.828537462695,-3.4815041433458,127.327713522095));
#33824=CARTESIAN_POINT('Ctrl Pts',(147.820786560408,-3.57709525984537,127.426138553648));
#33825=CARTESIAN_POINT('Ctrl Pts',(147.813035658121,-3.66845128540179,127.528441169665));
#33826=CARTESIAN_POINT('Ctrl Pts',(147.805288382774,-3.75976456202871,127.63069591443));
#33827=CARTESIAN_POINT('Ctrl Pts',(147.797541107426,-3.84684643162001,127.736824341951));
#33828=CARTESIAN_POINT('Ctrl Pts',(147.789793832079,-3.92935960264885,127.8464363157));
#33829=CARTESIAN_POINT('Ctrl Pts',(147.782048504219,-4.01185203175431,127.956020735506));
#33830=CARTESIAN_POINT('Ctrl Pts',(147.774303176359,-4.08977781411566,128.069086645999));
#33831=CARTESIAN_POINT('Ctrl Pts',(147.7665578485,-4.16284062645161,128.185211713578));
#33832=CARTESIAN_POINT('Ctrl Pts',(147.758810381406,-4.23592361849478,128.301368854516));
#33833=CARTESIAN_POINT('Ctrl Pts',(147.751062914313,-4.30414074378607,128.420586512747));
#33834=CARTESIAN_POINT('Ctrl Pts',(147.743315447219,-4.36723959620254,128.542414249532));
#33835=CARTESIAN_POINT('Ctrl Pts',(147.735566984875,-4.43034655438534,128.664257636479));
#33836=CARTESIAN_POINT('Ctrl Pts',(147.727818522531,-4.48833375736234,128.788711418972));
#33837=CARTESIAN_POINT('Ctrl Pts',(147.720070060187,-4.54099570167479,128.915302360161));
#33838=CARTESIAN_POINT('Ctrl Pts',(147.712315261109,-4.59370071320322,129.041996828089));
#33839=CARTESIAN_POINT('Ctrl Pts',(147.704560462032,-4.64107162368983,129.170831581822));
#33840=CARTESIAN_POINT('Ctrl Pts',(147.696805662955,-4.68295173121227,129.301314994294));
#33841=CARTESIAN_POINT('Ctrl Pts',(147.691281564745,-4.71278484805569,129.394264299363));
#33842=CARTESIAN_POINT('Ctrl Pts',(147.685757466536,-4.7398327621419,129.488049820932));
#33843=CARTESIAN_POINT('Ctrl Pts',(147.680233368326,-4.76405452823403,129.582490119308));
#33844=CARTESIAN_POINT('Origin',(213.235140564004,0.,130.804360617566));
#33845=CARTESIAN_POINT('',(145.584738356252,-4.76405452823403,129.582490119308));
#33846=CARTESIAN_POINT('',(145.92992189461,-4.76405452823405,129.582490119308));
#33847=CARTESIAN_POINT('',(213.235140564004,-4.76405452823405,129.582490119308));
#33848=CARTESIAN_POINT('',(147.264859436046,-4.91824899899375,130.801222720669));
#33849=CARTESIAN_POINT('Ctrl Pts',(147.264859435991,-4.91824899899438,130.801222721645));
#33850=CARTESIAN_POINT('Ctrl Pts',(147.257057493982,-4.91833725438135,130.939551710121));
#33851=CARTESIAN_POINT('Ctrl Pts',(147.249255551972,-4.91258528675101,131.077906330366));
#33852=CARTESIAN_POINT('Ctrl Pts',(147.241453609963,-4.90101327064487,131.215763076799));
#33853=CARTESIAN_POINT('Ctrl Pts',(147.233651063793,-4.8894403584344,131.35363049847));
#33854=CARTESIAN_POINT('Ctrl Pts',(147.225848517623,-4.8720465317177,131.490999587807));
#33855=CARTESIAN_POINT('Ctrl Pts',(147.218045971453,-4.84890390699558,131.627351482171));
#33856=CARTESIAN_POINT('Ctrl Pts',(147.210241222478,-4.82575474867703,131.763741871229));
#33857=CARTESIAN_POINT('Ctrl Pts',(147.202436473504,-4.79685362473761,131.899114115955));
#33858=CARTESIAN_POINT('Ctrl Pts',(147.194631724529,-4.76232382245233,132.032959361096));
#33859=CARTESIAN_POINT('Ctrl Pts',(147.186823173015,-4.7277771969581,132.166869816762));
#33860=CARTESIAN_POINT('Ctrl Pts',(147.179014621501,-4.68759652835638,132.299251421062));
#33861=CARTESIAN_POINT('Ctrl Pts',(147.171206069987,-4.64195493632828,132.429610577295));
#33862=CARTESIAN_POINT('Ctrl Pts',(147.163387307618,-4.59625366105695,132.560140197721));
#33863=CARTESIAN_POINT('Ctrl Pts',(147.15556854525,-4.54507732862304,132.68864172716));
#33864=CARTESIAN_POINT('Ctrl Pts',(147.147749782881,-4.48864742345066,132.814641038415));
#33865=CARTESIAN_POINT('Ctrl Pts',(147.139925203294,-4.43217553400683,132.940734094101));
#33866=CARTESIAN_POINT('Ctrl Pts',(147.132100623708,-4.37044245397524,133.064320880399));
#33867=CARTESIAN_POINT('Ctrl Pts',(147.124276044121,-4.30371517452387,133.184952720189));
#33868=CARTESIAN_POINT('Ctrl Pts',(147.116439008637,-4.23688167234614,133.305776593028));
#33869=CARTESIAN_POINT('Ctrl Pts',(147.108601973152,-4.16503829201448,133.423635799085));
#33870=CARTESIAN_POINT('Ctrl Pts',(147.100764937668,-4.08849516546904,133.538110852031));
#33871=CARTESIAN_POINT('Ctrl Pts',(147.097318629928,-4.05483560503897,133.588450838601));
#33872=CARTESIAN_POINT('Ctrl Pts',(147.093872322187,-4.02026774482163,133.638136842638));
#33873=CARTESIAN_POINT('Ctrl Pts',(147.090426014447,-3.98482032476812,133.687135329855));
#33874=CARTESIAN_POINT('Ctrl Pts',(147.082651680328,-3.90485645969203,133.797668294309));
#33875=CARTESIAN_POINT('Ctrl Pts',(147.074877346209,-3.82016342318674,133.905046696327));
#33876=CARTESIAN_POINT('Ctrl Pts',(147.06710301209,-3.73101863840657,134.008839199545));
#33877=CARTESIAN_POINT('Ctrl Pts',(147.059338259143,-3.64198371660671,134.112503787779));
#33878=CARTESIAN_POINT('Ctrl Pts',(147.051573506196,-3.54850821508408,134.21259097656));
#33879=CARTESIAN_POINT('Ctrl Pts',(147.043808753249,-3.45091240671159,134.30869887517));
#33880=CARTESIAN_POINT('Ctrl Pts',(147.036051712364,-3.35341353187163,134.40471131806));
#33881=CARTESIAN_POINT('Ctrl Pts',(147.028294671479,-3.25180277090356,134.49675206346));
#33882=CARTESIAN_POINT('Ctrl Pts',(147.020537630594,-3.14643994106533,134.584453044977));
#33883=CARTESIAN_POINT('Ctrl Pts',(147.012786439353,-3.04115656615668,134.672087890501));
#33884=CARTESIAN_POINT('Ctrl Pts',(147.005035248113,-2.93212705352909,134.755389237044));
#33885=CARTESIAN_POINT('Ctrl Pts',(146.997284056873,-2.81974700781337,134.834026841266));
#33886=CARTESIAN_POINT('Ctrl Pts',(146.989536160096,-2.70741472661507,134.912631022408));
#33887=CARTESIAN_POINT('Ctrl Pts',(146.981788263319,-2.59173506434583,134.986575180023));
#33888=CARTESIAN_POINT('Ctrl Pts',(146.974040366542,-2.47313536498654,135.055570389966));
#33889=CARTESIAN_POINT('Ctrl Pts',(146.966294090458,-2.35456047412757,135.1245511676));
#33890=CARTESIAN_POINT('Ctrl Pts',(146.958547814374,-2.23306709883701,135.188584860186));
#33891=CARTESIAN_POINT('Ctrl Pts',(146.95080153829,-2.10910978298848,135.247427012051));
#33892=CARTESIAN_POINT('Ctrl Pts',(146.943055205024,-1.98515155211544,135.306269598275));
#33893=CARTESIAN_POINT('Ctrl Pts',(146.935308871759,-1.85872969758267,135.359920399648));
#33894=CARTESIAN_POINT('Ctrl Pts',(146.927562538494,-1.7303211079499,135.408182065655));
#33895=CARTESIAN_POINT('Ctrl Pts',(146.919814470491,-1.60188376210385,135.456454539527));
#33896=CARTESIAN_POINT('Ctrl Pts',(146.912066402488,-1.47145916172775,135.499335339002));
#33897=CARTESIAN_POINT('Ctrl Pts',(146.904318334485,-1.33954142670635,135.536676311667));
#33898=CARTESIAN_POINT('Ctrl Pts',(146.896562031743,-1.20748348794619,135.574056970763));
#33899=CARTESIAN_POINT('Ctrl Pts',(146.888805729001,-1.07392962127918,135.605885934894));
#33900=CARTESIAN_POINT('Ctrl Pts',(146.881049426259,-0.939386815361894,
135.632065607893));
#33901=CARTESIAN_POINT('Ctrl Pts',(146.873288983745,-0.804772199897945,
135.658259253771));
#33902=CARTESIAN_POINT('Ctrl Pts',(146.865528541231,-0.669167979811934,
135.678797541964));
#33903=CARTESIAN_POINT('Ctrl Pts',(146.857768098717,-0.533087444720832,
135.693634678077));
#33904=CARTESIAN_POINT('Ctrl Pts',(146.849995198451,-0.396788461074094,
135.708495632077));
#33905=CARTESIAN_POINT('Ctrl Pts',(146.842222298186,-0.260012024781023,
135.717637119308));
#33906=CARTESIAN_POINT('Ctrl Pts',(146.83444939792,-0.123273517254129,135.721065479813));
#33907=CARTESIAN_POINT('Ctrl Pts',(146.826959062158,0.0084942011015726,
135.724369210779));
#33908=CARTESIAN_POINT('Ctrl Pts',(146.819468726396,0.140226392444292,135.722367981306));
#33909=CARTESIAN_POINT('Ctrl Pts',(146.811978390634,0.271467289687367,135.715112960449));
#33910=CARTESIAN_POINT('Ctrl Pts',(146.804204056515,0.407684225438265,135.707582863271));
#33911=CARTESIAN_POINT('Ctrl Pts',(146.796429722396,0.543803371143854,135.694368862182));
#33912=CARTESIAN_POINT('Ctrl Pts',(146.788655388277,0.679311877313508,135.675471213297));
#33913=CARTESIAN_POINT('Ctrl Pts',(146.78089063533,0.814653381359636,135.656596854075));
#33914=CARTESIAN_POINT('Ctrl Pts',(146.773125882383,0.94938535973654,135.632052837582));
#33915=CARTESIAN_POINT('Ctrl Pts',(146.765361129436,1.08299657508922,135.601891386706));
#33916=CARTESIAN_POINT('Ctrl Pts',(146.757604088551,1.21647508589972,135.571759892608));
#33917=CARTESIAN_POINT('Ctrl Pts',(146.749847047666,1.34883467001885,135.536022152749));
#33918=CARTESIAN_POINT('Ctrl Pts',(146.742090006781,1.47957117274723,135.4947819427));
#33919=CARTESIAN_POINT('Ctrl Pts',(146.73433881554,1.61020908606156,135.453572832216));
#33920=CARTESIAN_POINT('Ctrl Pts',(146.7265876243,1.73922598289392,135.406869627921));
#33921=CARTESIAN_POINT('Ctrl Pts',(146.71883643306,1.86613018620254,135.354826658604));
#33922=CARTESIAN_POINT('Ctrl Pts',(146.711088536283,1.99298045183982,135.302805808938));
#33923=CARTESIAN_POINT('Ctrl Pts',(146.703340639506,2.1177194489379,135.24544985623));
#33924=CARTESIAN_POINT('Ctrl Pts',(146.695592742729,2.23987310757214,135.182962166517));
#33925=CARTESIAN_POINT('Ctrl Pts',(146.687846466645,2.36200121429415,135.120487547882));
#33926=CARTESIAN_POINT('Ctrl Pts',(146.680100190561,2.48154471038079,135.052883505332));
#33927=CARTESIAN_POINT('Ctrl Pts',(146.672353914477,2.59805223628271,134.980400325237));
#33928=CARTESIAN_POINT('Ctrl Pts',(146.664607581211,2.71456062221672,134.907916610088));
#33929=CARTESIAN_POINT('Ctrl Pts',(146.656861247946,2.82803266128193,134.830553892052));
#33930=CARTESIAN_POINT('Ctrl Pts',(146.649114914681,2.93804454698588,134.748606718208));
#33931=CARTESIAN_POINT('Ctrl Pts',(146.641366846678,3.04808106908861,134.666641192862));
#33932=CARTESIAN_POINT('Ctrl Pts',(146.633618778675,3.15465558243492,134.580089402286));
#33933=CARTESIAN_POINT('Ctrl Pts',(146.625870710672,3.25737635833861,134.489286983538));
#33934=CARTESIAN_POINT('Ctrl Pts',(146.61811440793,3.3602063071056,134.398388058899));
#33935=CARTESIAN_POINT('Ctrl Pts',(146.610358105188,3.45917404324022,134.303229741008));
#33936=CARTESIAN_POINT('Ctrl Pts',(146.602601802446,3.55392341656995,134.204185820669));
#33937=CARTESIAN_POINT('Ctrl Pts',(146.594841359932,3.64872336049306,134.105089037608));
#33938=CARTESIAN_POINT('Ctrl Pts',(146.587080917418,3.739300197298,134.002102813182));
#33939=CARTESIAN_POINT('Ctrl Pts',(146.579320474904,3.82533795328772,133.895634239495));
#33940=CARTESIAN_POINT('Ctrl Pts',(146.571547574638,3.91151382472149,133.788994753002));
#33941=CARTESIAN_POINT('Ctrl Pts',(146.563774674373,3.99313582159533,133.67886206058));
#33942=CARTESIAN_POINT('Ctrl Pts',(146.556001774107,4.06993070172686,133.565673194157));
#33943=CARTESIAN_POINT('Ctrl Pts',(146.548511438345,4.14393389453164,133.456599028134));
#33944=CARTESIAN_POINT('Ctrl Pts',(146.541021102583,4.21345467065687,133.344687291295));
#33945=CARTESIAN_POINT('Ctrl Pts',(146.533530766821,4.27828972683423,133.230349091521));
#33946=CARTESIAN_POINT('Ctrl Pts',(146.525756432702,4.34558302387209,133.111675724153));
#33947=CARTESIAN_POINT('Ctrl Pts',(146.517982098583,4.40804143366448,132.990012341417));
#33948=CARTESIAN_POINT('Ctrl Pts',(146.510207764464,4.46538796401225,132.865790556554));
#33949=CARTESIAN_POINT('Ctrl Pts',(146.502443011517,4.52266381988654,132.741721863938));
#33950=CARTESIAN_POINT('Ctrl Pts',(146.49467825857,4.57484016901265,132.615101394286));
#33951=CARTESIAN_POINT('Ctrl Pts',(146.486913505623,4.6216846117074,132.48638749381));
#33952=CARTESIAN_POINT('Ctrl Pts',(146.479156464738,4.66848252784132,132.357801433795));
#33953=CARTESIAN_POINT('Ctrl Pts',(146.471399423853,4.70995894343115,132.22712644572));
#33954=CARTESIAN_POINT('Ctrl Pts',(146.463642382968,4.7459286598755,132.094842782446));
#33955=CARTESIAN_POINT('Ctrl Pts',(146.455891191727,4.78187125127707,131.96265887531));
#33956=CARTESIAN_POINT('Ctrl Pts',(146.448140000487,4.81231530695156,131.828869083345));
#33957=CARTESIAN_POINT('Ctrl Pts',(146.440388809247,4.83712490462788,131.693970486851));
#33958=CARTESIAN_POINT('Ctrl Pts',(146.43264091247,4.86192395756323,131.559129225859));
#33959=CARTESIAN_POINT('Ctrl Pts',(146.424893015693,4.88109324499556,131.423180481373));
#33960=CARTESIAN_POINT('Ctrl Pts',(146.417145118916,4.89454761815763,131.286633026156));
#33961=CARTESIAN_POINT('Ctrl Pts',(146.409398842832,4.90799917695487,131.150114133724));
#33962=CARTESIAN_POINT('Ctrl Pts',(146.401652566748,4.91573816095844,131.012997168499));
#33963=CARTESIAN_POINT('Ctrl Pts',(146.393906290663,4.91773117231896,130.875797157952));
#33964=CARTESIAN_POINT('Ctrl Pts',(146.386159957398,4.91972419839145,130.738596134625));
#33965=CARTESIAN_POINT('Ctrl Pts',(146.378413624133,4.91597116150519,130.601312455677));
#33966=CARTESIAN_POINT('Ctrl Pts',(146.370667290867,4.90649079469751,130.464461891401));
#33967=CARTESIAN_POINT('Ctrl Pts',(146.362919222864,4.89700830482741,130.32758068039));
#33968=CARTESIAN_POINT('Ctrl Pts',(146.355171154861,4.88179595983298,130.191133167013));
#33969=CARTESIAN_POINT('Ctrl Pts',(146.347423086858,4.8609244017522,130.055630343736));
#33970=CARTESIAN_POINT('Ctrl Pts',(146.339666784117,4.84003066113115,129.919983506445));
#33971=CARTESIAN_POINT('Ctrl Pts',(146.331910481375,4.81346575206809,129.785283751932));
#33972=CARTESIAN_POINT('Ctrl Pts',(146.324154178633,4.78135164748417,129.652032762483));
#33973=CARTESIAN_POINT('Ctrl Pts',(146.316393736119,4.74922040263571,129.518710652969));
#33974=CARTESIAN_POINT('Ctrl Pts',(146.308633293604,4.7115341680602,129.386839225015));
#33975=CARTESIAN_POINT('Ctrl Pts',(146.30087285109,4.66846465037193,129.256904359468));
#33976=CARTESIAN_POINT('Ctrl Pts',(146.293099950825,4.62532599367029,129.126760910939));
#33977=CARTESIAN_POINT('Ctrl Pts',(146.285327050559,4.57678692345388,128.998560602919));
#33978=CARTESIAN_POINT('Ctrl Pts',(146.277554150294,4.52306743298746,128.872769548228));
#33979=CARTESIAN_POINT('Ctrl Pts',(146.270063814532,4.4713007813112,128.751551315223));
#33980=CARTESIAN_POINT('Ctrl Pts',(146.26257347877,4.41472394523929,128.632570489983));
#33981=CARTESIAN_POINT('Ctrl Pts',(146.255083143008,4.35357291109338,128.516220331156));
#33982=CARTESIAN_POINT('Ctrl Pts',(146.247308808889,4.2901033169008,128.395458720691));
#33983=CARTESIAN_POINT('Ctrl Pts',(146.23953447477,4.22150476344376,128.277148661457));
#33984=CARTESIAN_POINT('Ctrl Pts',(146.231760140651,4.14799065811385,128.161756492333));
#33985=CARTESIAN_POINT('Ctrl Pts',(146.223995387704,4.07456715234876,128.046506533744));
#33986=CARTESIAN_POINT('Ctrl Pts',(146.216230634757,3.99624035633337,127.934167636789));
#33987=CARTESIAN_POINT('Ctrl Pts',(146.20846588181,3.91327027201179,127.825183073228));
#33988=CARTESIAN_POINT('Ctrl Pts',(146.200708840925,3.83038259474738,127.716306754671));
#33989=CARTESIAN_POINT('Ctrl Pts',(146.19295180004,3.74286104211641,127.610778448594));
#33990=CARTESIAN_POINT('Ctrl Pts',(146.185194759155,3.6510095600827,127.509013556226));
#33991=CARTESIAN_POINT('Ctrl Pts',(146.177443567914,3.5592273439659,127.407325405554));
#33992=CARTESIAN_POINT('Ctrl Pts',(146.169692376674,3.46312195859176,127.309395308741));
#33993=CARTESIAN_POINT('Ctrl Pts',(146.161941185434,3.3630381423868,127.215606305085));
#33994=CARTESIAN_POINT('Ctrl Pts',(146.154193288657,3.26299686447389,127.121857164258));
#33995=CARTESIAN_POINT('Ctrl Pts',(146.14644539188,3.15898080356209,127.032245882711));
#33996=CARTESIAN_POINT('Ctrl Pts',(146.138697495103,3.0513719795989,126.947119102621));
#33997=CARTESIAN_POINT('Ctrl Pts',(146.130951219019,2.94378566508189,126.862010129217));
#33998=CARTESIAN_POINT('Ctrl Pts',(146.123204942935,2.83260838877351,126.781384033824));
#33999=CARTESIAN_POINT('Ctrl Pts',(146.115458666851,2.71825540551634,126.705547299924));
#34000=CARTESIAN_POINT('Ctrl Pts',(146.107712333585,2.60390157813147,126.629710006214));
#34001=CARTESIAN_POINT('Ctrl Pts',(146.09996600032,2.48637232284625,126.558662360626));
#34002=CARTESIAN_POINT('Ctrl Pts',(146.092219667054,2.36611169748163,126.492667388968));
#34003=CARTESIAN_POINT('Ctrl Pts',(146.084471599052,2.24582414058411,126.426657638193));
#34004=CARTESIAN_POINT('Ctrl Pts',(146.076723531049,2.12280433913469,126.365703000977));
#34005=CARTESIAN_POINT('Ctrl Pts',(146.068975463046,1.99752038931368,126.310020248082));
#34006=CARTESIAN_POINT('Ctrl Pts',(146.061219160304,1.87210328621955,126.254278314894));
#34007=CARTESIAN_POINT('Ctrl Pts',(146.053462857562,1.74441758561998,126.203819617707));
#34008=CARTESIAN_POINT('Ctrl Pts',(146.04570655482,1.614951296374,126.158812708778));
#34009=CARTESIAN_POINT('Ctrl Pts',(146.037946112306,1.48541590707125,126.113781778307));
#34010=CARTESIAN_POINT('Ctrl Pts',(146.030185669792,1.35409840961538,126.074208546838));
#34011=CARTESIAN_POINT('Ctrl Pts',(146.022425227278,1.22150040094184,126.040211183197));
#34012=CARTESIAN_POINT('Ctrl Pts',(146.014652327012,1.08868953417309,126.00615924397));
#34013=CARTESIAN_POINT('Ctrl Pts',(146.006879426747,0.954594431129953,125.97770114049));
#34014=CARTESIAN_POINT('Ctrl Pts',(145.999106526481,0.819726157461254,125.954903731556));
#34015=CARTESIAN_POINT('Ctrl Pts',(145.991616190719,0.689760685252308,125.932935065859));
#34016=CARTESIAN_POINT('Ctrl Pts',(145.984125854957,0.55907758540045,125.916222718075));
#34017=CARTESIAN_POINT('Ctrl Pts',(145.976635519195,0.428135273916304,125.904780712132));
#34018=CARTESIAN_POINT('Ctrl Pts',(145.968861185076,0.292228244893996,125.892904879057));
#34019=CARTESIAN_POINT('Ctrl Pts',(145.961086850957,0.155611447588727,125.886669307992));
#34020=CARTESIAN_POINT('Ctrl Pts',(145.953312516838,0.0187925780154328,
125.886146520812));
#34021=CARTESIAN_POINT('Ctrl Pts',(145.945547763891,-0.117857674529477,
125.88562437792));
#34022=CARTESIAN_POINT('Ctrl Pts',(145.937783010943,-0.254709116625827,
125.890801011904));
#34023=CARTESIAN_POINT('Ctrl Pts',(145.930018257996,-0.391248273787048,
125.901697274978));
#34024=CARTESIAN_POINT('Ctrl Pts',(145.922261217111,-0.527651818331677,
125.912582715729));
#34025=CARTESIAN_POINT('Ctrl Pts',(145.914504176226,-0.663743307980828,
125.92917644959));
#34026=CARTESIAN_POINT('Ctrl Pts',(145.906747135341,-0.799008963697667,
125.951447292724));
#34027=CARTESIAN_POINT('Ctrl Pts',(145.898995944101,-0.934172614531225,
125.973701341241));
#34028=CARTESIAN_POINT('Ctrl Pts',(145.891244752861,-1.0685112868035,126.001623914399));
#34029=CARTESIAN_POINT('Ctrl Pts',(145.883493561621,-1.20151637916289,126.035132016094));
#34030=CARTESIAN_POINT('Ctrl Pts',(145.875745664844,-1.33446494081028,126.068625875951));
#34031=CARTESIAN_POINT('Ctrl Pts',(145.867997768067,-1.4660806715554,126.107700447331));
#34032=CARTESIAN_POINT('Ctrl Pts',(145.86024987129,-1.59586544040504,126.152221694595));
#34033=CARTESIAN_POINT('Ctrl Pts',(145.852503595206,-1.72562306107897,126.196733628974));
#34034=CARTESIAN_POINT('Ctrl Pts',(145.844757319122,-1.85355011208393,126.246689846275));
#34035=CARTESIAN_POINT('Ctrl Pts',(145.837011043038,-1.97916428479939,126.301906642646));
#34036=CARTESIAN_POINT('Ctrl Pts',(145.829264709772,-2.10477938476983,126.357123846615));
#34037=CARTESIAN_POINT('Ctrl Pts',(145.821518376507,-2.22808121447012,126.417601549812));
#34038=CARTESIAN_POINT('Ctrl Pts',(145.813772043242,-2.34860845873968,126.483108325691));
#34039=CARTESIAN_POINT('Ctrl Pts',(145.806023975239,-2.46916269425025,126.548629771358));
#34040=CARTESIAN_POINT('Ctrl Pts',(145.798275907236,-2.58694076447469,126.619182344105));
#34041=CARTESIAN_POINT('Ctrl Pts',(145.790527839233,-2.7015072766123,126.694489391249));
#34042=CARTESIAN_POINT('Ctrl Pts',(145.782771536491,-2.81619555140222,126.769876475618));
#34043=CARTESIAN_POINT('Ctrl Pts',(145.775015233749,-2.92766512248064,126.850027913428));
#34044=CARTESIAN_POINT('Ctrl Pts',(145.767258931007,-3.03551040135156,126.934624235616));
#34045=CARTESIAN_POINT('Ctrl Pts',(145.759498488493,-3.14341324049483,127.019265709408));
#34046=CARTESIAN_POINT('Ctrl Pts',(145.751738045979,-3.24768763588538,127.108356540883));
#34047=CARTESIAN_POINT('Ctrl Pts',(145.743977603465,-3.34796304334593,127.201538595471));
#34048=CARTESIAN_POINT('Ctrl Pts',(145.736204703199,-3.44839942179278,127.294870234166));
#34049=CARTESIAN_POINT('Ctrl Pts',(145.728431802934,-3.54482370887592,127.392305942068));
#34050=CARTESIAN_POINT('Ctrl Pts',(145.720658902668,-3.63690341092675,127.493451883987));
#34051=CARTESIAN_POINT('Ctrl Pts',(145.713168566906,-3.72563578387244,127.590920916145));
#34052=CARTESIAN_POINT('Ctrl Pts',(145.705678231144,-3.81033376296251,127.691834876987));
#34053=CARTESIAN_POINT('Ctrl Pts',(145.698187895382,-3.89073776441627,127.795815668418));
#34054=CARTESIAN_POINT('Ctrl Pts',(145.690403729643,-3.97429584423556,127.903875405656));
#34055=CARTESIAN_POINT('Ctrl Pts',(145.682619563903,-4.05348493014445,128.015594995365));
#34056=CARTESIAN_POINT('Ctrl Pts',(145.674835398163,-4.12796746956741,128.130586574627));
#34057=CARTESIAN_POINT('Ctrl Pts',(145.667063832803,-4.20232944265324,128.245392014781));
#34058=CARTESIAN_POINT('Ctrl Pts',(145.659292267444,-4.27199983210114,128.363458572807));
#34059=CARTESIAN_POINT('Ctrl Pts',(145.651520702085,-4.33668159389262,128.484365829707));
#34060=CARTESIAN_POINT('Ctrl Pts',(145.643756385211,-4.40130302745182,128.605160317244));
#34061=CARTESIAN_POINT('Ctrl Pts',(145.635992068337,-4.46094490469177,128.728789893477));
#34062=CARTESIAN_POINT('Ctrl Pts',(145.628227751463,-4.5153535379215,128.854805414429));
#34063=CARTESIAN_POINT('Ctrl Pts',(145.620469954524,-4.56971648255395,128.980715116284));
#34064=CARTESIAN_POINT('Ctrl Pts',(145.612712157585,-4.61885477749342,129.10900641855));
#34065=CARTESIAN_POINT('Ctrl Pts',(145.604954360646,-4.66256100658676,129.239206336878));
#34066=CARTESIAN_POINT('Ctrl Pts',(145.598215692514,-4.70052562147025,129.352302109716));
#34067=CARTESIAN_POINT('Ctrl Pts',(145.591477024383,-4.73439227538181,129.466837445625));
#34068=CARTESIAN_POINT('Ctrl Pts',(145.584738356252,-4.76405452823403,129.582490119308));
#34069=CARTESIAN_POINT('Ctrl Pts',(147.334614341604,-4.76405452823404,129.582490119308));
#34070=CARTESIAN_POINT('Ctrl Pts',(147.32583785793,-4.80241575731761,129.732059969292));
#34071=CARTESIAN_POINT('Ctrl Pts',(147.317061374255,-4.83377339724143,129.883610054808));
#34072=CARTESIAN_POINT('Ctrl Pts',(147.308284890581,-4.85794144089961,130.03651426621));
#34073=CARTESIAN_POINT('Ctrl Pts',(147.299561109063,-4.88196435718438,130.188500298761));
#34074=CARTESIAN_POINT('Ctrl Pts',(147.290837327545,-4.8988836733556,130.34182405967));
#34075=CARTESIAN_POINT('Ctrl Pts',(147.282113546027,-4.90856448932769,130.495851757707));
#34076=CARTESIAN_POINT('Ctrl Pts',(147.276362176033,-4.91494680809417,130.597398349501));
#34077=CARTESIAN_POINT('Ctrl Pts',(147.27061080604,-4.9181839396096,130.699250520337));
#34078=CARTESIAN_POINT('Ctrl Pts',(147.264859436046,-4.91824899899375,130.801222720669));
#34079=CARTESIAN_POINT('',(147.610140563976,-4.91824964343576,130.802487827118));
#34080=CARTESIAN_POINT('Ctrl Pts',(147.680233368326,-4.76405452823403,129.582490119308));
#34081=CARTESIAN_POINT('Ctrl Pts',(147.672469059238,-4.79809904943347,129.715229190767));
#34082=CARTESIAN_POINT('Ctrl Pts',(147.66470475015,-4.82655828705133,129.849261833059));
#34083=CARTESIAN_POINT('Ctrl Pts',(147.656940441062,-4.84936284072016,129.984078287181));
#34084=CARTESIAN_POINT('Ctrl Pts',(147.64916521746,-4.87219945141112,130.119084256699));
#34085=CARTESIAN_POINT('Ctrl Pts',(147.641389993857,-4.88936546244613,130.254875851216));
#34086=CARTESIAN_POINT('Ctrl Pts',(147.633614770255,-4.90084340470038,130.390939542747));
#34087=CARTESIAN_POINT('Ctrl Pts',(147.631653935474,-4.90373802864088,130.425253465069));
#34088=CARTESIAN_POINT('Ctrl Pts',(147.629693100694,-4.90627115089988,130.45958470123));
#34089=CARTESIAN_POINT('Ctrl Pts',(147.627732265913,-4.90844301354763,130.493925044129));
#34090=CARTESIAN_POINT('Ctrl Pts',(147.621868365278,-4.91493799562629,130.596620263797));
#34091=CARTESIAN_POINT('Ctrl Pts',(147.616004464643,-4.918210435478,130.69952144019));
#34092=CARTESIAN_POINT('Ctrl Pts',(147.610140564008,-4.91824964343554,130.802487826551));
#34093=CARTESIAN_POINT('Ctrl Pts',(147.610140563976,-4.91824964343576,130.802487827118));
#34094=CARTESIAN_POINT('Ctrl Pts',(147.602439734443,-4.91830113368513,130.937709523106));
#34095=CARTESIAN_POINT('Ctrl Pts',(147.59473890491,-4.91277175834642,131.073158991306));
#34096=CARTESIAN_POINT('Ctrl Pts',(147.587038075378,-4.90163137916255,131.208332009262));
#34097=CARTESIAN_POINT('Ctrl Pts',(147.579346385036,-4.89050422115882,131.343344606573));
#34098=CARTESIAN_POINT('Ctrl Pts',(147.571654694695,-4.87377933677944,131.478081012467));
#34099=CARTESIAN_POINT('Ctrl Pts',(147.563963004353,-4.85147857154113,131.612035510315));
#34100=CARTESIAN_POINT('Ctrl Pts',(147.556278517553,-4.8291986917631,131.745864555009));
#34101=CARTESIAN_POINT('Ctrl Pts',(147.548594030753,-4.80135338499484,131.878912757415));
#34102=CARTESIAN_POINT('Ctrl Pts',(147.540909543953,-4.76801638328633,132.01067849906));
#34103=CARTESIAN_POINT('Ctrl Pts',(147.532925173043,-4.73337841804295,132.147586347562));
#34104=CARTESIAN_POINT('Ctrl Pts',(147.524940802132,-4.69281146874443,132.283109172404));
#34105=CARTESIAN_POINT('Ctrl Pts',(147.516956431222,-4.6464570671264,132.416694263513));
#34106=CARTESIAN_POINT('Ctrl Pts',(147.509279785587,-4.60188920839122,132.545130857705));
#34107=CARTESIAN_POINT('Ctrl Pts',(147.501603139952,-4.55197186160213,132.671775895844));
#34108=CARTESIAN_POINT('Ctrl Pts',(147.493926494318,-4.49688180943077,132.796153040112));
#34109=CARTESIAN_POINT('Ctrl Pts',(147.486250759867,-4.44179829620614,132.92051542136));
#34110=CARTESIAN_POINT('Ctrl Pts',(147.478575025416,-4.38154346000645,133.042610079365));
#34111=CARTESIAN_POINT('Ctrl Pts',(147.470899290966,-4.31634202060979,133.161981160321));
#34112=CARTESIAN_POINT('Ctrl Pts',(147.463222729902,-4.25113355955972,133.28136509655));
#34113=CARTESIAN_POINT('Ctrl Pts',(147.455546168839,-4.1809776271877,133.398024522358));
#34114=CARTESIAN_POINT('Ctrl Pts',(147.447869607775,-4.10614438988712,133.511529122092));
#34115=CARTESIAN_POINT('Ctrl Pts',(147.44019048198,-4.0312861508724,133.625071643606));
#34116=CARTESIAN_POINT('Ctrl Pts',(147.432511356185,-3.95174771837245,133.735456909927));
#34117=CARTESIAN_POINT('Ctrl Pts',(147.424832230389,-3.86784166952686,133.842284889494));
#34118=CARTESIAN_POINT('Ctrl Pts',(147.41714468187,-3.78384358970452,133.949230041584));
#34119=CARTESIAN_POINT('Ctrl Pts',(147.409457133352,-3.69546857816107,134.052609805367));
#34120=CARTESIAN_POINT('Ctrl Pts',(147.401769584833,-3.60306865499176,134.152058233826));
#34121=CARTESIAN_POINT('Ctrl Pts',(147.394077036228,-3.51060863365079,134.251571344902));
#34122=CARTESIAN_POINT('Ctrl Pts',(147.386384487622,-3.41411877119594,134.347147750118));
#34123=CARTESIAN_POINT('Ctrl Pts',(147.378691939017,-3.3139858621897,134.438460336576));
#34124=CARTESIAN_POINT('Ctrl Pts',(147.370988573147,-3.21371214624986,134.529901326826));
#34125=CARTESIAN_POINT('Ctrl Pts',(147.363285207277,-3.10978546467493,134.617066278072));
#34126=CARTESIAN_POINT('Ctrl Pts',(147.355581841407,-3.00262359945466,134.699669922679));
#34127=CARTESIAN_POINT('Ctrl Pts',(147.353482774971,-2.9734233929154,134.722178335335));
#34128=CARTESIAN_POINT('Ctrl Pts',(147.351383708536,-2.94398312849165,134.744348332494));
#34129=CARTESIAN_POINT('Ctrl Pts',(147.3492846421,-2.91431158413388,134.76617472894));
#34130=CARTESIAN_POINT('Ctrl Pts',(147.341510307981,-2.80441677767962,134.847013379741));
#34131=CARTESIAN_POINT('Ctrl Pts',(147.333735973862,-2.69098184152859,134.923404131228));
#34132=CARTESIAN_POINT('Ctrl Pts',(147.325961639743,-2.57440265271451,134.995020952668));
#34133=CARTESIAN_POINT('Ctrl Pts',(147.318196886796,-2.4579671373319,135.066549512776));
#34134=CARTESIAN_POINT('Ctrl Pts',(147.310432133849,-2.33839540933109,135.133315646451));
#34135=CARTESIAN_POINT('Ctrl Pts',(147.302667380902,-2.21611515837309,135.195034445958));
#34136=CARTESIAN_POINT('Ctrl Pts',(147.294910340017,-2.09395635788373,135.256691945484));
#34137=CARTESIAN_POINT('Ctrl Pts',(147.287153299132,-1.96909473471167,135.31331191208));
#34138=CARTESIAN_POINT('Ctrl Pts',(147.279396258247,-1.84198530669273,135.364653721351));
#34139=CARTESIAN_POINT('Ctrl Pts',(147.271645067007,-1.7149717328821,135.415956813364));
#34140=CARTESIAN_POINT('Ctrl Pts',(147.263893875767,-1.58571408923612,135.461989524764));
#34141=CARTESIAN_POINT('Ctrl Pts',(147.256142684526,-1.45468992321589,135.502558175119));
#34142=CARTESIAN_POINT('Ctrl Pts',(147.248394787749,-1.32372144596189,135.543109582714));
#34143=CARTESIAN_POINT('Ctrl Pts',(147.240646890972,-1.19098831234639,135.578201432888));
#34144=CARTESIAN_POINT('Ctrl Pts',(147.232898994195,-1.05698567725058,135.607689082348));
#34145=CARTESIAN_POINT('Ctrl Pts',(147.225152718111,-0.9230110726171,135.637170563628));
#34146=CARTESIAN_POINT('Ctrl Pts',(147.217406442027,-0.78776787628935,135.661050091948));
#34147=CARTESIAN_POINT('Ctrl Pts',(147.209660165943,-0.651763566309817,
135.679233673978));
#34148=CARTESIAN_POINT('Ctrl Pts',(147.201913832678,-0.51575825237755,135.697417390235));
#34149=CARTESIAN_POINT('Ctrl Pts',(147.194167499412,-0.378992201099509,
135.70990502449));
#34150=CARTESIAN_POINT('Ctrl Pts',(147.186421166147,-0.241979785258479,
135.716654261682));
#34151=CARTESIAN_POINT('Ctrl Pts',(147.178673098144,-0.104936686436712,
135.72340501032));
#34152=CARTESIAN_POINT('Ctrl Pts',(147.170925030141,0.0323524963162291,
135.724414785513));
#34153=CARTESIAN_POINT('Ctrl Pts',(147.163176962138,0.169372003699001,135.719693382177));
#34154=CARTESIAN_POINT('Ctrl Pts',(147.155420659396,0.306537137044632,135.714966960878));
#34155=CARTESIAN_POINT('Ctrl Pts',(147.147664356654,0.443431631121024,135.704497206777));
#34156=CARTESIAN_POINT('Ctrl Pts',(147.139908053913,0.579542909015048,135.688345986003));
#34157=CARTESIAN_POINT('Ctrl Pts',(147.132147611398,0.715726833596269,135.672186144837));
#34158=CARTESIAN_POINT('Ctrl Pts',(147.124387168884,0.851126323258618,135.650338856992));
#34159=CARTESIAN_POINT('Ctrl Pts',(147.11662672637,0.985238617946266,135.622917240478));
#34160=CARTESIAN_POINT('Ctrl Pts',(147.108853826105,1.11956620159551,135.59545160435));
#34161=CARTESIAN_POINT('Ctrl Pts',(147.101080925839,1.25260208145998,135.56239385212));
#34162=CARTESIAN_POINT('Ctrl Pts',(147.093308025574,1.38385742407199,135.523907385248));
#34163=CARTESIAN_POINT('Ctrl Pts',(147.085817689812,1.51034130436829,135.486819998389));
#34164=CARTESIAN_POINT('Ctrl Pts',(147.07832735405,1.63517156208169,135.444691837802));
#34165=CARTESIAN_POINT('Ctrl Pts',(147.070837018288,1.75792981906361,135.397710790778));
#34166=CARTESIAN_POINT('Ctrl Pts',(147.063062684169,1.8853424926702,135.348948443077));
#34167=CARTESIAN_POINT('Ctrl Pts',(147.055288350049,2.01092654918722,135.294803485775));
#34168=CARTESIAN_POINT('Ctrl Pts',(147.04751401593,2.13419370851755,135.235432753858));
#34169=CARTESIAN_POINT('Ctrl Pts',(147.039749262983,2.25730895209079,135.176135191062));
#34170=CARTESIAN_POINT('Ctrl Pts',(147.031984510036,2.37811263095337,135.111624835952));
#34171=CARTESIAN_POINT('Ctrl Pts',(147.024219757089,2.49613386745074,135.042107516363));
#34172=CARTESIAN_POINT('Ctrl Pts',(147.016462716204,2.6140378835921,134.972659242356));
#34173=CARTESIAN_POINT('Ctrl Pts',(147.008705675319,2.72916462228905,134.898214097482));
#34174=CARTESIAN_POINT('Ctrl Pts',(147.000948634434,2.84106569116859,134.819024837767));
#34175=CARTESIAN_POINT('Ctrl Pts',(146.993197443194,2.95288237458132,134.73989529529));
#34176=CARTESIAN_POINT('Ctrl Pts',(146.985446251954,3.06147791208037,134.656028983848));
#34177=CARTESIAN_POINT('Ctrl Pts',(146.977695060714,3.16643122876389,134.567722988639));
#34178=CARTESIAN_POINT('Ctrl Pts',(146.969947163937,3.27133993748831,134.479454525834));
#34179=CARTESIAN_POINT('Ctrl Pts',(146.962199267159,3.37260920579902,134.38675038351));
#34180=CARTESIAN_POINT('Ctrl Pts',(146.954451370382,3.46984969788895,134.289948966261));
#34181=CARTESIAN_POINT('Ctrl Pts',(146.946705094298,3.5670698493642,134.193167797782));
#34182=CARTESIAN_POINT('Ctrl Pts',(146.938958818214,3.66026262395762,134.092291334772));
#34183=CARTESIAN_POINT('Ctrl Pts',(146.93121254213,3.7490746381389,133.98769572719));
#34184=CARTESIAN_POINT('Ctrl Pts',(146.923466208865,3.83788730791041,133.883099347506));
#34185=CARTESIAN_POINT('Ctrl Pts',(146.915719875599,3.92231889969002,133.774784066492));
#34186=CARTESIAN_POINT('Ctrl Pts',(146.907973542334,4.00205578156489,133.663159768214));
#34187=CARTESIAN_POINT('Ctrl Pts',(146.900225474331,4.08181051996143,133.551510472447));
#34188=CARTESIAN_POINT('Ctrl Pts',(146.892477406328,4.15686822918267,133.436551002923));
#34189=CARTESIAN_POINT('Ctrl Pts',(146.884729338325,4.22695836946702,133.318720576938));
#34190=CARTESIAN_POINT('Ctrl Pts',(146.876973035583,4.29712300238664,133.200764919374));
#34191=CARTESIAN_POINT('Ctrl Pts',(146.869216732841,4.36230931962478,133.079932546624));
#34192=CARTESIAN_POINT('Ctrl Pts',(146.861460430099,4.4222923105662,132.956688144316));
#34193=CARTESIAN_POINT('Ctrl Pts',(146.853699987585,4.48230731623595,132.83337796276));
#34194=CARTESIAN_POINT('Ctrl Pts',(146.845939545071,4.53711330570396,132.707653544664));
#34195=CARTESIAN_POINT('Ctrl Pts',(146.838179102557,4.58653369426326,132.579999019349));
#34196=CARTESIAN_POINT('Ctrl Pts',(146.830406202291,4.6360334168176,132.452139571658));
#34197=CARTESIAN_POINT('Ctrl Pts',(146.822633302026,4.68013013627093,132.322344195595));
#34198=CARTESIAN_POINT('Ctrl Pts',(146.81486040176,4.71869710047028,132.191112483082));
#34199=CARTESIAN_POINT('Ctrl Pts',(146.807370065998,4.75586205837629,132.064651373874));
#34200=CARTESIAN_POINT('Ctrl Pts',(146.799879730236,4.787892247185,131.93685684285));
#34201=CARTESIAN_POINT('Ctrl Pts',(146.792389394474,4.81471959818696,131.808182441066));
#34202=CARTESIAN_POINT('Ctrl Pts',(146.784615060355,4.84256411635641,131.674629310227));
#34203=CARTESIAN_POINT('Ctrl Pts',(146.776840726236,4.86489168042236,131.539705214769));
#34204=CARTESIAN_POINT('Ctrl Pts',(146.769066392117,4.88157031277973,131.403905731705));
#34205=CARTESIAN_POINT('Ctrl Pts',(146.76130163917,4.89822839021328,131.268273609367));
#34206=CARTESIAN_POINT('Ctrl Pts',(146.753536886223,4.90925134065023,131.131768630313));
#34207=CARTESIAN_POINT('Ctrl Pts',(146.745772133276,4.91455781200336,130.994898212221));
#34208=CARTESIAN_POINT('Ctrl Pts',(146.738015092391,4.91985901289433,130.858163735757));
#34209=CARTESIAN_POINT('Ctrl Pts',(146.730258051506,4.9194550185077,130.721064930705));
#34210=CARTESIAN_POINT('Ctrl Pts',(146.722501010621,4.91331611261889,130.584115663073));
#34211=CARTESIAN_POINT('Ctrl Pts',(146.714749819381,4.90718183612675,130.447269669949));
#34212=CARTESIAN_POINT('Ctrl Pts',(146.706998628141,4.89532127370488,130.310573378783));
#34213=CARTESIAN_POINT('Ctrl Pts',(146.699247436901,4.8777567702748,130.17454163362));
#34214=CARTESIAN_POINT('Ctrl Pts',(146.691499540124,4.86019973222719,130.038567705578));
#34215=CARTESIAN_POINT('Ctrl Pts',(146.683751643347,4.83694362493432,129.903258148703));
#34216=CARTESIAN_POINT('Ctrl Pts',(146.67600374657,4.80806271224981,129.769123438185));
#34217=CARTESIAN_POINT('Ctrl Pts',(146.668257470485,4.77918784082964,129.635016785756));
#34218=CARTESIAN_POINT('Ctrl Pts',(146.660511194401,4.74469058655765,129.502084872833));
#34219=CARTESIAN_POINT('Ctrl Pts',(146.652764918317,4.70469640261632,129.370828329227));
#34220=CARTESIAN_POINT('Ctrl Pts',(146.645018585052,4.664701923447,129.239570816716));
#34221=CARTESIAN_POINT('Ctrl Pts',(146.637272251787,4.61921054759512,129.109989072189));
#34222=CARTESIAN_POINT('Ctrl Pts',(146.629525918521,4.5683975964239,128.982568515407));
#34223=CARTESIAN_POINT('Ctrl Pts',(146.621777850518,4.51757326604481,128.855119423676));
#34224=CARTESIAN_POINT('Ctrl Pts',(146.614029782515,4.46142513373345,128.729832845844));
#34225=CARTESIAN_POINT('Ctrl Pts',(146.606281714512,4.40017649209229,128.607173802355));
#34226=CARTESIAN_POINT('Ctrl Pts',(146.598525411771,4.33886275466562,128.484384395373));
#34227=CARTESIAN_POINT('Ctrl Pts',(146.590769109029,4.27243785405228,128.364228451542));
#34228=CARTESIAN_POINT('Ctrl Pts',(146.583012806287,4.20117111969791,128.247146452597));
#34229=CARTESIAN_POINT('Ctrl Pts',(146.575252363773,4.12986634814147,128.130001963464));
#34230=CARTESIAN_POINT('Ctrl Pts',(146.567491921259,4.05371481051523,128.015935013368));
#34231=CARTESIAN_POINT('Ctrl Pts',(146.559731478744,3.97302837018012,127.905355851747));
#34232=CARTESIAN_POINT('Ctrl Pts',(146.551958578479,3.89221240480812,127.794599178639));
#34233=CARTESIAN_POINT('Ctrl Pts',(146.544185678214,3.8068472329173,127.687341788488));
#34234=CARTESIAN_POINT('Ctrl Pts',(146.536412777948,3.71728466270584,127.583960363108));
#34235=CARTESIAN_POINT('Ctrl Pts',(146.528922442186,3.63097791751464,127.484337112941));
#34236=CARTESIAN_POINT('Ctrl Pts',(146.521432106424,3.54077385866447,127.388313142378));
#34237=CARTESIAN_POINT('Ctrl Pts',(146.513941770662,3.4470172787037,127.296190874977));
#34238=CARTESIAN_POINT('Ctrl Pts',(146.506167436543,3.34970588951856,127.200575763808));
#34239=CARTESIAN_POINT('Ctrl Pts',(146.498393102424,3.24825902051891,127.108861182511));
#34240=CARTESIAN_POINT('Ctrl Pts',(146.490618768305,3.14302227756331,127.021426039062));
#34241=CARTESIAN_POINT('Ctrl Pts',(146.482854015357,3.03791522948806,126.934098651614));
#34242=CARTESIAN_POINT('Ctrl Pts',(146.47508926241,2.92902789854883,126.851040455726));
#34243=CARTESIAN_POINT('Ctrl Pts',(146.467324509463,2.81674321681961,126.772594166865));
#34244=CARTESIAN_POINT('Ctrl Pts',(146.459567468578,2.70457005781979,126.694225791964));
#34245=CARTESIAN_POINT('Ctrl Pts',(146.451810427693,2.58900658145499,126.620460430928));
#34246=CARTESIAN_POINT('Ctrl Pts',(146.444053386808,2.47046905540772,126.551600841988));
#34247=CARTESIAN_POINT('Ctrl Pts',(146.436302195568,2.35202091943036,126.4827931806));
#34248=CARTESIAN_POINT('Ctrl Pts',(146.428551004328,2.23060353453201,126.418884123306));
#34249=CARTESIAN_POINT('Ctrl Pts',(146.420799813088,2.10666213156628,126.360133156474));
#34250=CARTESIAN_POINT('Ctrl Pts',(146.413051916311,1.98277340700314,126.30140716037));
#34251=CARTESIAN_POINT('Ctrl Pts',(146.405304019534,1.85636315058457,126.247835061472));
#34252=CARTESIAN_POINT('Ctrl Pts',(146.397556122757,1.72790098097139,126.199630303806));
#34253=CARTESIAN_POINT('Ctrl Pts',(146.389809846673,1.599465682875,126.151435629536));
#34254=CARTESIAN_POINT('Ctrl Pts',(146.382063570588,1.46897969112893,126.108606200591));
#34255=CARTESIAN_POINT('Ctrl Pts',(146.374317294504,1.33693201028251,126.071307072297));
#34256=CARTESIAN_POINT('Ctrl Pts',(146.366570961239,1.20488335468966,126.034007668669));
#34257=CARTESIAN_POINT('Ctrl Pts',(146.358824627974,1.07127336323652,126.00223875343));
#34258=CARTESIAN_POINT('Ctrl Pts',(146.351078294708,0.936605198794484,125.976115204987));
#34259=CARTESIAN_POINT('Ctrl Pts',(146.343330226705,0.801906876351253,125.949985806357));
#34260=CARTESIAN_POINT('Ctrl Pts',(146.335582158702,0.666150293112305,125.929504364656));
#34261=CARTESIAN_POINT('Ctrl Pts',(146.327834090699,0.529847379050967,125.9147343724));
#34262=CARTESIAN_POINT('Ctrl Pts',(146.320077787957,0.393399600630261,125.899948682421));
#34263=CARTESIAN_POINT('Ctrl Pts',(146.312321485216,0.25640472079204,125.890886609946));
#34264=CARTESIAN_POINT('Ctrl Pts',(146.304565182474,0.119378908439775,125.887559651621));
#34265=CARTESIAN_POINT('Ctrl Pts',(146.29680473996,-0.0177200387142628,
125.884230917598));
#34266=CARTESIAN_POINT('Ctrl Pts',(146.289044297445,-0.154849560565692,
125.886643390159));
#34267=CARTESIAN_POINT('Ctrl Pts',(146.281283854931,-0.291495932878982,
125.89475643967));
#34268=CARTESIAN_POINT('Ctrl Pts',(146.273510954666,-0.428361662080005,
125.902882512968));
#34269=CARTESIAN_POINT('Ctrl Pts',(146.2657380544,-0.564742302667943,125.916727410463));
#34270=CARTESIAN_POINT('Ctrl Pts',(146.257965154135,-0.700130780640822,
125.936198751677));
#34271=CARTESIAN_POINT('Ctrl Pts',(146.250474818373,-0.830597546414922,
125.954962260591));
#34272=CARTESIAN_POINT('Ctrl Pts',(146.242984482611,-0.960142729551186,
125.978950188408));
#34273=CARTESIAN_POINT('Ctrl Pts',(146.235494146849,-1.08832552375138,126.008035918711));
#34274=CARTESIAN_POINT('Ctrl Pts',(146.22771981273,-1.22136840755523,126.038224443318));
#34275=CARTESIAN_POINT('Ctrl Pts',(146.219945478611,-1.35336499296447,126.074000595887));
#34276=CARTESIAN_POINT('Ctrl Pts',(146.212171144492,-1.48380968555717,126.115278417439));
#34277=CARTESIAN_POINT('Ctrl Pts',(146.204406391545,-1.61409361672415,126.156505367765));
#34278=CARTESIAN_POINT('Ctrl Pts',(146.196641638598,-1.74282909134756,126.203220379447));
#34279=CARTESIAN_POINT('Ctrl Pts',(146.188876885651,-1.86952078906091,126.255286526966));
#34280=CARTESIAN_POINT('Ctrl Pts',(146.181119844766,-1.99608665479422,126.307300961653));
#34281=CARTESIAN_POINT('Ctrl Pts',(146.173362803881,-2.1206124239477,126.364655807788));
#34282=CARTESIAN_POINT('Ctrl Pts',(146.165605762996,-2.24261837459615,126.427164495798));
#34283=CARTESIAN_POINT('Ctrl Pts',(146.157854571756,-2.36453231960794,126.48962604552));
#34284=CARTESIAN_POINT('Ctrl Pts',(146.150103380515,-2.48392988182947,126.55723352362));
#34285=CARTESIAN_POINT('Ctrl Pts',(146.142352189275,-2.60035208987876,126.629752603493));
#34286=CARTESIAN_POINT('Ctrl Pts',(146.134604292498,-2.71672481538424,126.702240860822));
#34287=CARTESIAN_POINT('Ctrl Pts',(146.126856395721,-2.83012437076388,126.779636361646));
#34288=CARTESIAN_POINT('Ctrl Pts',(146.119108498944,-2.94011733915678,126.861659374194));
#34289=CARTESIAN_POINT('Ctrl Pts',(146.11136222286,-3.05008729939216,126.943665229296));
#34290=CARTESIAN_POINT('Ctrl Pts',(146.103615946776,-3.15665177679296,127.030296437195));
#34291=CARTESIAN_POINT('Ctrl Pts',(146.095869670692,-3.25940758673466,127.121230800951));
#34292=CARTESIAN_POINT('Ctrl Pts',(146.088123337426,-3.3621641551964,127.212165835964));
#34293=CARTESIAN_POINT('Ctrl Pts',(146.080377004161,-3.46111170731605,127.307403831119));
#34294=CARTESIAN_POINT('Ctrl Pts',(146.072630670896,-3.55588162081195,127.406583555828));
#34295=CARTESIAN_POINT('Ctrl Pts',(146.064882602893,-3.65067275737241,127.505785491148));
#34296=CARTESIAN_POINT('Ctrl Pts',(146.05713453489,-3.74128412361966,127.608930629927));
#34297=CARTESIAN_POINT('Ctrl Pts',(146.049386466887,-3.82738559084586,127.715622590234));
#34298=CARTESIAN_POINT('Ctrl Pts',(146.041630164145,-3.9135785677364,127.822427944027));
#34299=CARTESIAN_POINT('Ctrl Pts',(146.033873861403,-3.9952518248,127.932787344805));
#34300=CARTESIAN_POINT('Ctrl Pts',(146.026117558661,-4.0721166876814,128.046272739269));
#34301=CARTESIAN_POINT('Ctrl Pts',(146.018357116147,-4.14902257565452,128.159818704306));
#34302=CARTESIAN_POINT('Ctrl Pts',(146.010596673633,-4.22111475029939,128.276493655097));
#34303=CARTESIAN_POINT('Ctrl Pts',(146.002836231119,-4.28814971398151,128.395843419583));
#34304=CARTESIAN_POINT('Ctrl Pts',(145.995063330853,-4.35529228813831,128.515384774906));
#34305=CARTESIAN_POINT('Ctrl Pts',(145.987290430588,-4.41736125128767,128.63760917561));
#34306=CARTESIAN_POINT('Ctrl Pts',(145.979517530322,-4.47416023985968,128.762040072069));
#34307=CARTESIAN_POINT('Ctrl Pts',(145.97202719456,-4.52889444212961,128.881947592021));
#34308=CARTESIAN_POINT('Ctrl Pts',(145.964536858798,-4.57873505488728,129.003903684428));
#34309=CARTESIAN_POINT('Ctrl Pts',(145.957046523036,-4.62355033753805,129.127469047204));
#34310=CARTESIAN_POINT('Ctrl Pts',(145.948004980227,-4.67764661698982,129.27662411217));
#34311=CARTESIAN_POINT('Ctrl Pts',(145.938963437419,-4.72456322357162,129.428514121794));
#34312=CARTESIAN_POINT('Ctrl Pts',(145.92992189461,-4.76405452823405,129.582490119308));
#34313=CARTESIAN_POINT('Origin',(213.235140564004,0.,130.804360617566));
#34314=CARTESIAN_POINT('',(143.834995515417,-4.76405452823405,129.582490119308));
#34315=CARTESIAN_POINT('',(144.179984458271,-4.76405452823405,129.582490119308));
#34316=CARTESIAN_POINT('',(213.235140564004,-4.76405452823405,129.582490119308));
#34317=CARTESIAN_POINT('',(145.514859435938,-4.9182485978174,130.808074452137));
#34318=CARTESIAN_POINT('Ctrl Pts',(145.514859435938,-4.9182485978174,130.808074452137));
#34319=CARTESIAN_POINT('Ctrl Pts',(145.50589805865,-4.91812871707833,130.966833078993));
#34320=CARTESIAN_POINT('Ctrl Pts',(145.496936681362,-4.91031794769265,131.125276220947));
#34321=CARTESIAN_POINT('Ctrl Pts',(145.487975304074,-4.89493134552557,131.282722598801));
#34322=CARTESIAN_POINT('Ctrl Pts',(145.478965112646,-4.87946092992949,131.441026613752));
#34323=CARTESIAN_POINT('Ctrl Pts',(145.469954921218,-4.85633203283539,131.598322856858));
#34324=CARTESIAN_POINT('Ctrl Pts',(145.46094472979,-4.82571087920542,131.753938193554));
#34325=CARTESIAN_POINT('Ctrl Pts',(145.451874947198,-4.7948872048858,131.910582731359));
#34326=CARTESIAN_POINT('Ctrl Pts',(145.442805164606,-4.75647192550071,132.065523938142));
#34327=CARTESIAN_POINT('Ctrl Pts',(145.433735382015,-4.7106829381227,132.218096561432));
#34328=CARTESIAN_POINT('Ctrl Pts',(145.429070345199,-4.68713140205463,132.296572191626));
#34329=CARTESIAN_POINT('Ctrl Pts',(145.424405308384,-4.66162988630557,132.374421556298));
#34330=CARTESIAN_POINT('Ctrl Pts',(145.419740271569,-4.63421287035937,132.451556457379));
#34331=CARTESIAN_POINT('Ctrl Pts',(145.41196593745,-4.58852211786071,132.580102601175));
#34332=CARTESIAN_POINT('Ctrl Pts',(145.404191603331,-4.53740642405227,132.706949822268));
#34333=CARTESIAN_POINT('Ctrl Pts',(145.396417269212,-4.48101086137801,132.831606217564));
#34334=CARTESIAN_POINT('Ctrl Pts',(145.388652516265,-4.42468480119456,132.956108984995));
#34335=CARTESIAN_POINT('Ctrl Pts',(145.380887763318,-4.36309197867349,133.07842594603));
#34336=CARTESIAN_POINT('Ctrl Pts',(145.373123010371,-4.29642686261107,133.198081419317));
#34337=CARTESIAN_POINT('Ctrl Pts',(145.365365969486,-4.22982795928184,133.3176180491));
#34338=CARTESIAN_POINT('Ctrl Pts',(145.357608928601,-4.15816697705891,133.43449811235));
#34339=CARTESIAN_POINT('Ctrl Pts',(145.349851887716,-4.08168583900318,133.54826728037));
#34340=CARTESIAN_POINT('Ctrl Pts',(145.342100696476,-4.00526237596834,133.661950654176));
#34341=CARTESIAN_POINT('Ctrl Pts',(145.334349505236,-3.92402620942064,133.772527479074));
#34342=CARTESIAN_POINT('Ctrl Pts',(145.326598313996,-3.83826423436866,133.879569672194));
#34343=CARTESIAN_POINT('Ctrl Pts',(145.318850417219,-3.75253871044404,133.986566369527));
#34344=CARTESIAN_POINT('Ctrl Pts',(145.311102520442,-3.66229144783274,134.090031118592));
#34345=CARTESIAN_POINT('Ctrl Pts',(145.303354623665,-3.5678514106888,134.189566574926));
#34346=CARTESIAN_POINT('Ctrl Pts',(145.295608347581,-3.47343112836475,134.289081210588));
#34347=CARTESIAN_POINT('Ctrl Pts',(145.287862071496,-3.37482008491364,134.38466790493));
#34348=CARTESIAN_POINT('Ctrl Pts',(145.280115795412,-3.27238584174091,134.475964349626));
#34349=CARTESIAN_POINT('Ctrl Pts',(145.272369462147,-3.16995084242179,134.567261468251));
#34350=CARTESIAN_POINT('Ctrl Pts',(145.264623128882,-3.06369287893197,134.654268013904));
#34351=CARTESIAN_POINT('Ctrl Pts',(145.256876795616,-2.95401419099952,134.736660608904));
#34352=CARTESIAN_POINT('Ctrl Pts',(145.249128727613,-2.84431094128552,134.819071655153));
#34353=CARTESIAN_POINT('Ctrl Pts',(145.24138065961,-2.73118575531252,134.896866459899));
#34354=CARTESIAN_POINT('Ctrl Pts',(145.233632591607,-2.61507123168629,134.969764021284));
#34355=CARTESIAN_POINT('Ctrl Pts',(145.225876288866,-2.49883330016253,135.042739059065));
#34356=CARTESIAN_POINT('Ctrl Pts',(145.218119986124,-2.37960001602614,135.110806248029));
#34357=CARTESIAN_POINT('Ctrl Pts',(145.210363683382,-2.25783053145275,135.173729491184));
#34358=CARTESIAN_POINT('Ctrl Pts',(145.202603240868,-2.135996054839,135.236686318368));
#34359=CARTESIAN_POINT('Ctrl Pts',(145.194842798354,-2.01162303490017,135.294493564439));
#34360=CARTESIAN_POINT('Ctrl Pts',(145.187082355839,-1.88519122399317,135.346963077773));
#34361=CARTESIAN_POINT('Ctrl Pts',(145.179309455574,-1.75855645351921,135.399516819828));
#34362=CARTESIAN_POINT('Ctrl Pts',(145.171536555309,-1.6298566549969,135.446715571655));
#34363=CARTESIAN_POINT('Ctrl Pts',(145.163763655043,-1.49958823477567,135.488420628777));
#34364=CARTESIAN_POINT('Ctrl Pts',(145.156273319281,-1.3740553997549,135.528609602023));
#34365=CARTESIAN_POINT('Ctrl Pts',(145.148782983519,-1.24706630661079,135.563697283306));
#34366=CARTESIAN_POINT('Ctrl Pts',(145.141292647757,-1.11907274232627,135.593604739542));
#34367=CARTESIAN_POINT('Ctrl Pts',(145.133518313638,-0.98622626314995,135.624646146072));
#34368=CARTESIAN_POINT('Ctrl Pts',(145.125743979519,-0.851876822471075,
135.650205086615));
#34369=CARTESIAN_POINT('Ctrl Pts',(145.1179696454,-0.716516687491695,135.670137729092));
#34370=CARTESIAN_POINT('Ctrl Pts',(145.110204892453,-0.581323371781241,
135.690045806368));
#34371=CARTESIAN_POINT('Ctrl Pts',(145.102440139506,-0.445122223204724,
135.704341325579));
#34372=CARTESIAN_POINT('Ctrl Pts',(145.094675386558,-0.308418561091736,
135.71293078144));
#34373=CARTESIAN_POINT('Ctrl Pts',(145.086918345673,-0.171850674983235,
135.721511706133));
#34374=CARTESIAN_POINT('Ctrl Pts',(145.079161304788,-0.0347816562475976,
135.724397821385));
#34375=CARTESIAN_POINT('Ctrl Pts',(145.071404263903,0.102275490193226,135.721547088161));
#34376=CARTESIAN_POINT('Ctrl Pts',(145.063653072663,0.239229280773723,135.718698504698));
#34377=CARTESIAN_POINT('Ctrl Pts',(145.055901881423,0.376170827580724,135.7101216919));
#34378=CARTESIAN_POINT('Ctrl Pts',(145.048150690183,0.512584898613247,135.695826633416));
#34379=CARTESIAN_POINT('Ctrl Pts',(145.040402793406,0.648940990026757,135.681537650713));
#34380=CARTESIAN_POINT('Ctrl Pts',(145.032654896629,0.784769663543133,135.66153529688));
#34381=CARTESIAN_POINT('Ctrl Pts',(145.024906999852,0.919558808849843,135.635881564387));
#34382=CARTESIAN_POINT('Ctrl Pts',(145.017160723768,1.05431975917307,135.610233198101));
#34383=CARTESIAN_POINT('Ctrl Pts',(145.009414447684,1.18804122997288,135.578935877563));
#34384=CARTESIAN_POINT('Ctrl Pts',(145.0016681716,1.32021972507534,135.542103006091));
#34385=CARTESIAN_POINT('Ctrl Pts',(144.993921838334,1.45239919588937,135.505269862726));
#34386=CARTESIAN_POINT('Ctrl Pts',(144.986175505069,1.58303529166219,135.462901191839));
#34387=CARTESIAN_POINT('Ctrl Pts',(144.978429171803,1.7116385251931,135.415160615568));
#34388=CARTESIAN_POINT('Ctrl Pts',(144.9706811038,1.84027055852649,135.367409348126));
#34389=CARTESIAN_POINT('Ctrl Pts',(144.962933035798,1.96686845727731,135.314283917504));
#34390=CARTESIAN_POINT('Ctrl Pts',(144.955184967795,2.09096197651175,135.255996392793));
#34391=CARTESIAN_POINT('Ctrl Pts',(144.947428665053,2.2151873838152,135.197646919408));
#34392=CARTESIAN_POINT('Ctrl Pts',(144.939672362311,2.33690274016403,135.13412455887));
#34393=CARTESIAN_POINT('Ctrl Pts',(144.931916059569,2.4556612275063,135.065687992718));
#34394=CARTESIAN_POINT('Ctrl Pts',(144.924155617055,2.57448309982909,134.997214899911));
#34395=CARTESIAN_POINT('Ctrl Pts',(144.916395174541,2.69034462839187,134.923822584331));
#34396=CARTESIAN_POINT('Ctrl Pts',(144.908634732026,2.80282819803734,134.845812974676));
#34397=CARTESIAN_POINT('Ctrl Pts',(144.900861831761,2.91549233629462,134.76767813707));
#34398=CARTESIAN_POINT('Ctrl Pts',(144.893088931496,3.02476736771428,134.684911429862));
#34399=CARTESIAN_POINT('Ctrl Pts',(144.88531603123,3.13026827653164,134.597855520612));
#34400=CARTESIAN_POINT('Ctrl Pts',(144.877825695468,3.23193396157277,134.513964312945));
#34401=CARTESIAN_POINT('Ctrl Pts',(144.870335359706,3.33009492829537,134.426090541163));
#34402=CARTESIAN_POINT('Ctrl Pts',(144.862845023944,3.42444056616217,134.334571641191));
#34403=CARTESIAN_POINT('Ctrl Pts',(144.855070689825,3.52236334756429,134.23958277431));
#34404=CARTESIAN_POINT('Ctrl Pts',(144.847296355706,3.61648596246463,134.140366016569));
#34405=CARTESIAN_POINT('Ctrl Pts',(144.839522021587,3.70642131841318,134.037257781553));
#34406=CARTESIAN_POINT('Ctrl Pts',(144.83175726864,3.79624583707327,133.934276618221));
#34407=CARTESIAN_POINT('Ctrl Pts',(144.823992515693,3.88189310995933,133.827413811828));
#34408=CARTESIAN_POINT('Ctrl Pts',(144.816227762745,3.96301133098612,133.717043959946));
#34409=CARTESIAN_POINT('Ctrl Pts',(144.80847072186,4.04404898425213,133.606783728956));
#34410=CARTESIAN_POINT('Ctrl Pts',(144.800713680975,4.12056630747607,133.493023697289));
#34411=CARTESIAN_POINT('Ctrl Pts',(144.79295664009,4.1922506403365,133.376172747388));
#34412=CARTESIAN_POINT('Ctrl Pts',(144.78520544885,4.26388091548393,133.259409915697));
#34413=CARTESIAN_POINT('Ctrl Pts',(144.77745425761,4.33068525100124,133.139561137164));
#34414=CARTESIAN_POINT('Ctrl Pts',(144.76970306637,4.39239355093347,133.017065287471));
#34415=CARTESIAN_POINT('Ctrl Pts',(144.761955169593,4.45407562319214,132.894621501781));
#34416=CARTESIAN_POINT('Ctrl Pts',(144.754207272816,4.51066579225154,132.769533231052));
#34417=CARTESIAN_POINT('Ctrl Pts',(144.746459376039,4.56193940599989,132.642264836639));
#34418=CARTESIAN_POINT('Ctrl Pts',(144.738713099955,4.61320229441356,132.51502306403));
#34419=CARTESIAN_POINT('Ctrl Pts',(144.730966823871,4.65915069355398,132.385602437227));
#34420=CARTESIAN_POINT('Ctrl Pts',(144.723220547787,4.69960786086538,132.254487859084));
#34421=CARTESIAN_POINT('Ctrl Pts',(144.715474214521,4.74006532682238,132.123372313083));
#34422=CARTESIAN_POINT('Ctrl Pts',(144.707727881256,4.77503136479106,131.990563164376));
#34423=CARTESIAN_POINT('Ctrl Pts',(144.699981547991,4.80437905492279,131.856560674171));
#34424=CARTESIAN_POINT('Ctrl Pts',(144.692233479988,4.83373331726623,131.722528175037));
#34425=CARTESIAN_POINT('Ctrl Pts',(144.684485411985,4.85746664449393,131.587302184467));
#34426=CARTESIAN_POINT('Ctrl Pts',(144.676737343982,4.87550327746544,131.451392961366));
#34427=CARTESIAN_POINT('Ctrl Pts',(144.66898104124,4.89355907998513,131.315339292326));
#34428=CARTESIAN_POINT('Ctrl Pts',(144.661224738498,4.90590604218744,131.178601328381));
#34429=CARTESIAN_POINT('Ctrl Pts',(144.653468435756,4.91252028410558,131.041694813904));
#34430=CARTESIAN_POINT('Ctrl Pts',(144.645707993242,4.91913805624378,130.904715228297));
#34431=CARTESIAN_POINT('Ctrl Pts',(144.637947550728,4.92001700883151,130.767567303671));
#34432=CARTESIAN_POINT('Ctrl Pts',(144.630187108214,4.91518543183898,130.630765591319));
#34433=CARTESIAN_POINT('Ctrl Pts',(144.622414207948,4.91034609877014,130.493744272713));
#34434=CARTESIAN_POINT('Ctrl Pts',(144.614641307683,4.89977794759441,130.357070667015));
#34435=CARTESIAN_POINT('Ctrl Pts',(144.606868407417,4.88356116381054,130.221253919078));
#34436=CARTESIAN_POINT('Ctrl Pts',(144.599378071655,4.86793390096474,130.09037445203));
#34437=CARTESIAN_POINT('Ctrl Pts',(144.591887735893,4.84706160827821,129.960290930578));
#34438=CARTESIAN_POINT('Ctrl Pts',(144.584397400131,4.82106028756894,129.831447072524));
#34439=CARTESIAN_POINT('Ctrl Pts',(144.576623066012,4.7940731188822,129.697718060432));
#34440=CARTESIAN_POINT('Ctrl Pts',(144.568848731893,4.76147482305602,129.564900957762));
#34441=CARTESIAN_POINT('Ctrl Pts',(144.561074397774,4.72333920144347,129.433503276116));
#34442=CARTESIAN_POINT('Ctrl Pts',(144.553309644827,4.6852505785763,129.302267530369));
#34443=CARTESIAN_POINT('Ctrl Pts',(144.54554489188,4.64163831609154,129.172448096909));
#34444=CARTESIAN_POINT('Ctrl Pts',(144.537780138932,4.59262741375395,129.044543439296));
#34445=CARTESIAN_POINT('Ctrl Pts',(144.530023098047,4.54366518973551,128.916765818392));
#34446=CARTESIAN_POINT('Ctrl Pts',(144.522266057162,4.48931513548404,128.79089955142));
#34447=CARTESIAN_POINT('Ctrl Pts',(144.514509016277,4.42975225483972,128.667428699314));
#34448=CARTESIAN_POINT('Ctrl Pts',(144.506757825037,4.37023429102696,128.544050957538));
#34449=CARTESIAN_POINT('Ctrl Pts',(144.499006633797,4.30551149448725,128.423065385804));
#34450=CARTESIAN_POINT('Ctrl Pts',(144.491255442557,4.23580711029935,128.304936446514));
#34451=CARTESIAN_POINT('Ctrl Pts',(144.48350754578,4.1661323523342,128.186857715175));
#34452=CARTESIAN_POINT('Ctrl Pts',(144.475759649003,4.09148041615446,128.071633537448));
#34453=CARTESIAN_POINT('Ctrl Pts',(144.468011752226,4.01212055216497,127.959703918174));
#34454=CARTESIAN_POINT('Ctrl Pts',(144.460265476142,3.93277728854825,127.847797712163));
#34455=CARTESIAN_POINT('Ctrl Pts',(144.452519200058,3.84872828192332,127.739185012578));
#34456=CARTESIAN_POINT('Ctrl Pts',(144.444772923973,3.76028596112699,127.634276619775));
#34457=CARTESIAN_POINT('Ctrl Pts',(144.437026590708,3.6718429874695,127.529367452562));
#34458=CARTESIAN_POINT('Ctrl Pts',(144.429280257443,3.57900688692668,127.428162945609));
#34459=CARTESIAN_POINT('Ctrl Pts',(144.421533924177,3.48212994014246,127.331040283582));
#34460=CARTESIAN_POINT('Ctrl Pts',(144.413785856174,3.38523129843776,127.233895871609));
#34461=CARTESIAN_POINT('Ctrl Pts',(144.406037788171,3.28429028585757,127.140835400269));
#34462=CARTESIAN_POINT('Ctrl Pts',(144.398289720168,3.17969524800384,127.052198415272));
#34463=CARTESIAN_POINT('Ctrl Pts',(144.390533417427,3.0749890452991,126.963467225833));
#34464=CARTESIAN_POINT('Ctrl Pts',(144.382777114685,2.96662135827354,126.879169167326));
#34465=CARTESIAN_POINT('Ctrl Pts',(144.375020811943,2.8550131895684,126.799603103073));
#34466=CARTESIAN_POINT('Ctrl Pts',(144.367260369429,2.74334545222313,126.719994572015));
#34467=CARTESIAN_POINT('Ctrl Pts',(144.359499926915,2.62843411434688,126.645123281025));
#34468=CARTESIAN_POINT('Ctrl Pts',(144.3517394844,2.5107273739368,126.575243556492));
#34469=CARTESIAN_POINT('Ctrl Pts',(144.343966584135,2.3928316802175,126.505251654822));
#34470=CARTESIAN_POINT('Ctrl Pts',(144.336193683869,2.27213196109396,126.440267517394));
#34471=CARTESIAN_POINT('Ctrl Pts',(144.328420783604,2.14909991677226,126.380498887106));
#34472=CARTESIAN_POINT('Ctrl Pts',(144.320930447842,2.03054039716113,126.322902997077));
#34473=CARTESIAN_POINT('Ctrl Pts',(144.31344011208,1.90981546237683,126.270150127238));
#34474=CARTESIAN_POINT('Ctrl Pts',(144.305949776318,1.78736112658887,126.222382522282));
#34475=CARTESIAN_POINT('Ctrl Pts',(144.298175442199,1.66026389743988,126.172803794066));
#34476=CARTESIAN_POINT('Ctrl Pts',(144.29040110808,1.53090093223615,126.128438775345));
#34477=CARTESIAN_POINT('Ctrl Pts',(144.282626773961,1.39973910629574,126.089499697368));
#34478=CARTESIAN_POINT('Ctrl Pts',(144.274862021014,1.26873892558363,126.050608608325));
#34479=CARTESIAN_POINT('Ctrl Pts',(144.267097268067,1.13594466637413,126.017130265116));
#34480=CARTESIAN_POINT('Ctrl Pts',(144.259332515119,1.00184326560478,125.989228933628));
#34481=CARTESIAN_POINT('Ctrl Pts',(144.251575474234,0.867875056237084,125.961355314137));
#34482=CARTESIAN_POINT('Ctrl Pts',(144.243818433349,0.732602669219422,125.939047762299));
#34483=CARTESIAN_POINT('Ctrl Pts',(144.236061392464,0.596527952573879,125.922420689187));
#34484=CARTESIAN_POINT('Ctrl Pts',(144.228310201224,0.460555850930619,125.90580615468));
#34485=CARTESIAN_POINT('Ctrl Pts',(144.220559009984,0.323783010469462,125.894863619695));
#34486=CARTESIAN_POINT('Ctrl Pts',(144.212807818744,0.186720865981622,125.889656315097));
#34487=CARTESIAN_POINT('Ctrl Pts',(144.205059921967,0.049716976561534,125.884451223742));
#34488=CARTESIAN_POINT('Ctrl Pts',(144.19731202519,-0.0875755824579162,
125.884976529335));
#34489=CARTESIAN_POINT('Ctrl Pts',(144.189564128413,-0.224641086123712,
125.891243537247));
#34490=CARTESIAN_POINT('Ctrl Pts',(144.181817852329,-0.361677918640931,
125.897509234235));
#34491=CARTESIAN_POINT('Ctrl Pts',(144.174071576245,-0.498487399965087,
125.909514226762));
#34492=CARTESIAN_POINT('Ctrl Pts',(144.166325300161,-0.634555036704846,
125.927217707225));
#34493=CARTESIAN_POINT('Ctrl Pts',(144.158578966895,-0.77062367786499,125.94492131837));
#34494=CARTESIAN_POINT('Ctrl Pts',(144.15083263363,-0.905950075816032,125.968323450946));
#34495=CARTESIAN_POINT('Ctrl Pts',(144.143086300364,-1.04002647812338,125.997331598795));
#34496=CARTESIAN_POINT('Ctrl Pts',(144.135338232361,-1.1741329059114,126.026346242818));
#34497=CARTESIAN_POINT('Ctrl Pts',(144.127590164358,-1.30698839898089,126.060969317612));
#34498=CARTESIAN_POINT('Ctrl Pts',(144.119842096355,-1.43809737762394,126.101057629774));
#34499=CARTESIAN_POINT('Ctrl Pts',(144.112085793614,-1.56934570044976,126.141188548272));
#34500=CARTESIAN_POINT('Ctrl Pts',(144.104329490872,-1.69884342638246,126.186796192781));
#34501=CARTESIAN_POINT('Ctrl Pts',(144.09657318813,-1.82611155103295,126.237687904782));
#34502=CARTESIAN_POINT('Ctrl Pts',(144.088812745616,-1.95344760251353,126.288606779222));
#34503=CARTESIAN_POINT('Ctrl Pts',(144.081052303102,-2.07855132507632,126.344815180623));
#34504=CARTESIAN_POINT('Ctrl Pts',(144.073291860587,-2.20096648476092,126.406073496941));
#34505=CARTESIAN_POINT('Ctrl Pts',(144.065518960322,-2.3235781561274,126.467430150546));
#34506=CARTESIAN_POINT('Ctrl Pts',(144.057746060057,-2.44349229783324,126.533852729033));
#34507=CARTESIAN_POINT('Ctrl Pts',(144.049973159791,-2.56027916441055,126.605056667768));
#34508=CARTESIAN_POINT('Ctrl Pts',(144.042482824029,-2.6728205342191,126.673672163979));
#34509=CARTESIAN_POINT('Ctrl Pts',(144.034992488267,-2.78245779377563,126.746727256012));
#34510=CARTESIAN_POINT('Ctrl Pts',(144.027502152505,-2.88883559228039,126.823931999531));
#34511=CARTESIAN_POINT('Ctrl Pts',(144.019481042626,-3.00275144833393,126.906607563163));
#34512=CARTESIAN_POINT('Ctrl Pts',(144.011459932748,-3.11331865693512,126.994325096411));
#34513=CARTESIAN_POINT('Ctrl Pts',(144.003438822869,-3.22005684860705,127.086778479369));
#34514=CARTESIAN_POINT('Ctrl Pts',(143.995741301339,-3.3224889983866,127.175502099495));
#34515=CARTESIAN_POINT('Ctrl Pts',(143.988043779809,-3.42139467126964,127.268586646072));
#34516=CARTESIAN_POINT('Ctrl Pts',(143.980346258278,-3.51637759337915,127.365716744863));
#34517=CARTESIAN_POINT('Ctrl Pts',(143.972655696484,-3.61127463640881,127.462759023197));
#34518=CARTESIAN_POINT('Ctrl Pts',(143.96496513469,-3.70225570535656,127.563839297074));
#34519=CARTESIAN_POINT('Ctrl Pts',(143.957274572896,-3.78895824126995,127.668602573901));
#34520=CARTESIAN_POINT('Ctrl Pts',(143.949589228179,-3.87560196043033,127.773294782035));
#34521=CARTESIAN_POINT('Ctrl Pts',(143.941903883463,-3.95797266707612,127.881664717766));
#34522=CARTESIAN_POINT('Ctrl Pts',(143.934218538747,-4.03574562371058,127.993321606239));
#34523=CARTESIAN_POINT('Ctrl Pts',(143.926536672775,-4.11348337668676,128.10492795361));
#34524=CARTESIAN_POINT('Ctrl Pts',(143.918854806803,-4.18662729394016,128.219817966861));
#34525=CARTESIAN_POINT('Ctrl Pts',(143.911172940831,-4.25489411663926,128.337569357915));
#34526=CARTESIAN_POINT('Ctrl Pts',(143.903491513211,-4.32315704381489,128.455314029698));
#34527=CARTESIAN_POINT('Ctrl Pts',(143.895810085591,-4.38654322345769,128.575919414166));
#34528=CARTESIAN_POINT('Ctrl Pts',(143.888128657971,-4.44481391950573,128.698936127477));
#34529=CARTESIAN_POINT('Ctrl Pts',(143.880447426527,-4.50308312737967,128.821949699066));
#34530=CARTESIAN_POINT('Ctrl Pts',(143.872766195083,-4.55623694672054,128.947374114459));
#34531=CARTESIAN_POINT('Ctrl Pts',(143.865084963639,-4.60408395472253,129.074738115294));
#34532=CARTESIAN_POINT('Ctrl Pts',(143.85740026354,-4.65195256925087,129.202159630564));
#34533=CARTESIAN_POINT('Ctrl Pts',(143.849715563442,-4.69450945444632,129.331522104781));
#34534=CARTESIAN_POINT('Ctrl Pts',(143.842030863343,-4.73161245236431,129.46233727085));
#34535=CARTESIAN_POINT('Ctrl Pts',(143.839685747368,-4.74293505858744,129.502257727323));
#34536=CARTESIAN_POINT('Ctrl Pts',(143.837340631392,-4.75375011671748,129.542313375196));
#34537=CARTESIAN_POINT('Ctrl Pts',(143.834995515417,-4.76405452823405,129.582490119308));
#34538=CARTESIAN_POINT('Ctrl Pts',(145.584738356252,-4.76405452823403,129.582490119308));
#34539=CARTESIAN_POINT('Ctrl Pts',(145.576986652373,-4.79817595935304,129.715529061376));
#34540=CARTESIAN_POINT('Ctrl Pts',(145.569234948494,-4.82673275080714,129.850046531733));
#34541=CARTESIAN_POINT('Ctrl Pts',(145.561483244616,-4.84960957421066,129.985538267954));
#34542=CARTESIAN_POINT('Ctrl Pts',(145.553712609845,-4.87254226645113,130.121360896519));
#34543=CARTESIAN_POINT('Ctrl Pts',(145.545941975074,-4.8897671214549,130.258162172932));
#34544=CARTESIAN_POINT('Ctrl Pts',(145.538171340304,-4.90121969823317,130.395424764221));
#34545=CARTESIAN_POINT('Ctrl Pts',(145.530400705533,-4.91267227501144,130.53268735551));
#34546=CARTESIAN_POINT('Ctrl Pts',(145.522630070762,-4.91835254938408,130.670410868192));
#34547=CARTESIAN_POINT('Ctrl Pts',(145.514859435991,-4.91824859781811,130.808074451192));
#34548=CARTESIAN_POINT('',(145.860140564062,-4.91824867625418,130.800752151961));
#34549=CARTESIAN_POINT('Ctrl Pts',(145.92992189461,-4.76405452823405,129.582490119308));
#34550=CARTESIAN_POINT('Ctrl Pts',(145.920948441898,-4.80324843157597,129.735306553588));
#34551=CARTESIAN_POINT('Ctrl Pts',(145.911974989186,-4.83512838164778,129.890177542899));
#34552=CARTESIAN_POINT('Ctrl Pts',(145.903001536475,-4.85950097047483,130.046446783114));
#34553=CARTESIAN_POINT('Ctrl Pts',(145.894096396557,-4.88368801649093,130.201526382199));
#34554=CARTESIAN_POINT('Ctrl Pts',(145.885191256639,-4.90048149046819,130.357982889292));
#34555=CARTESIAN_POINT('Ctrl Pts',(145.876286116722,-4.90973963625009,130.515155211782));
#34556=CARTESIAN_POINT('Ctrl Pts',(145.870904265835,-4.91533482740309,130.610142826905));
#34557=CARTESIAN_POINT('Ctrl Pts',(145.865522414949,-4.91817871119236,130.705391516625));
#34558=CARTESIAN_POINT('Ctrl Pts',(145.860140564062,-4.91824867625418,130.800752151961));
#34559=CARTESIAN_POINT('Ctrl Pts',(145.860140564008,-4.91824867625488,130.800752152921));
#34560=CARTESIAN_POINT('Ctrl Pts',(145.852378814537,-4.91834958041379,130.938282043005));
#34561=CARTESIAN_POINT('Ctrl Pts',(145.844617065067,-4.91267751355959,131.075864905963));
#34562=CARTESIAN_POINT('Ctrl Pts',(145.836855315596,-4.90124589904416,131.212982324775));
#34563=CARTESIAN_POINT('Ctrl Pts',(145.8290941807,-4.88981518968292,131.350088886643));
#34564=CARTESIAN_POINT('Ctrl Pts',(145.821333045803,-4.87262587158808,131.486729690643));
#34565=CARTESIAN_POINT('Ctrl Pts',(145.813571910907,-4.84974336629735,131.622390166882));
#34566=CARTESIAN_POINT('Ctrl Pts',(145.805809737665,-4.82685779960359,131.758068792856));
#34567=CARTESIAN_POINT('Ctrl Pts',(145.798047564423,-4.79827759397041,131.89276644696));
#34568=CARTESIAN_POINT('Ctrl Pts',(145.79028539118,-4.76411947705081,132.025977853399));
#34569=CARTESIAN_POINT('Ctrl Pts',(145.782520526355,-4.72994951558522,132.159235451748));
#34570=CARTESIAN_POINT('Ctrl Pts',(145.774755661529,-4.69019788940373,132.291005400603));
#34571=CARTESIAN_POINT('Ctrl Pts',(145.766990796703,-4.64503135568583,132.420797058381));
#34572=CARTESIAN_POINT('Ctrl Pts',(145.759216610126,-4.599810599364,132.550744531563));
#34573=CARTESIAN_POINT('Ctrl Pts',(145.751442423549,-4.54916207961528,132.678708602936));
#34574=CARTESIAN_POINT('Ctrl Pts',(145.743668236972,-4.49330116536668,132.804217537402));
#34575=CARTESIAN_POINT('Ctrl Pts',(145.735889117777,-4.4374048081052,132.929806105629));
#34576=CARTESIAN_POINT('Ctrl Pts',(145.728109998581,-4.37628963952763,133.052936085945));
#34577=CARTESIAN_POINT('Ctrl Pts',(145.720330879385,-4.31021682307232,133.173160735897));
#34578=CARTESIAN_POINT('Ctrl Pts',(145.712538932775,-4.24403505553835,133.293583630846));
#34579=CARTESIAN_POINT('Ctrl Pts',(145.704746986164,-4.17287950881536,133.41109129229));
#34580=CARTESIAN_POINT('Ctrl Pts',(145.696955039554,-4.0970549255999,133.525265613908));
#34581=CARTESIAN_POINT('Ctrl Pts',(145.69083632611,-4.03751282144295,133.614922280144));
#34582=CARTESIAN_POINT('Ctrl Pts',(145.684717612666,-3.975092507965,133.702524059789));
#34583=CARTESIAN_POINT('Ctrl Pts',(145.678598899223,-3.90995826411787,133.787883608152));
#34584=CARTESIAN_POINT('Ctrl Pts',(145.670824565104,-3.82719979227,133.896340010851));
#34585=CARTESIAN_POINT('Ctrl Pts',(145.663050230985,-3.73979418909744,134.001522196541));
#34586=CARTESIAN_POINT('Ctrl Pts',(145.655275896866,-3.64802979451386,134.103006048775));
#34587=CARTESIAN_POINT('Ctrl Pts',(145.647511143918,-3.55637849134542,134.204364831232));
#34588=CARTESIAN_POINT('Ctrl Pts',(145.639746390971,-3.46037934478948,134.30203406182));
#34589=CARTESIAN_POINT('Ctrl Pts',(145.631981638024,-3.36036277911229,134.395620153614));
#34590=CARTESIAN_POINT('Ctrl Pts',(145.624224597139,-3.26044555129847,134.489113294382));
#34591=CARTESIAN_POINT('Ctrl Pts',(145.616467556254,-3.15651912858829,134.578531101451));
#34592=CARTESIAN_POINT('Ctrl Pts',(145.608710515369,-3.04895260360576,134.663514810322));
#34593=CARTESIAN_POINT('Ctrl Pts',(145.600959324129,-2.94146719537606,134.748434432318));
#34594=CARTESIAN_POINT('Ctrl Pts',(145.593208132889,-2.8303474542221,134.828926370334));
#34595=CARTESIAN_POINT('Ctrl Pts',(145.585456941649,-2.7159972832948,134.904670583853));
#34596=CARTESIAN_POINT('Ctrl Pts',(145.577709044872,-2.60169571424069,134.980382604062));
#34597=CARTESIAN_POINT('Ctrl Pts',(145.569961148095,-2.48416677150554,135.051350697791));
#34598=CARTESIAN_POINT('Ctrl Pts',(145.562213251318,-2.36384503284604,135.117296940211));
#34599=CARTESIAN_POINT('Ctrl Pts',(145.554466975233,-2.24354846290036,135.183229388098));
#34600=CARTESIAN_POINT('Ctrl Pts',(145.546720699149,-2.12046060165158,135.244141886315));
#34601=CARTESIAN_POINT('Ctrl Pts',(145.538974423065,-1.99504208311807,135.299801658119));
#34602=CARTESIAN_POINT('Ctrl Pts',(145.5312280898,-1.86962263877354,135.355461840791));
#34603=CARTESIAN_POINT('Ctrl Pts',(145.523481756535,-1.74187286016913,135.405869061088));
#34604=CARTESIAN_POINT('Ctrl Pts',(145.515735423269,-1.61227451667469,135.450838202294));
#34605=CARTESIAN_POINT('Ctrl Pts',(145.507987355266,-1.48264715052979,135.495817414028));
#34606=CARTESIAN_POINT('Ctrl Pts',(145.500239287263,-1.35117076502652,135.53535599521));
#34607=CARTESIAN_POINT('Ctrl Pts',(145.49249121926,-1.21834309978122,135.569318450928));
#34608=CARTESIAN_POINT('Ctrl Pts',(145.484734916518,-1.08537426371269,135.603317002347));
#34609=CARTESIAN_POINT('Ctrl Pts',(145.476978613777,-0.951051658409011,
135.631727492731));
#34610=CARTESIAN_POINT('Ctrl Pts',(145.469222311035,-0.815884597942765,
135.654465295337));
#34611=CARTESIAN_POINT('Ctrl Pts',(145.461461868521,-0.680645394746499,
135.677215233794));
#34612=CARTESIAN_POINT('Ctrl Pts',(145.453701426006,-0.544561226042542,
135.694286402916));
#34613=CARTESIAN_POINT('Ctrl Pts',(145.445940983492,-0.408146382902866,
135.705646121658));
#34614=CARTESIAN_POINT('Ctrl Pts',(145.438168083227,-0.271512554546641,
135.717024076029));
#34615=CARTESIAN_POINT('Ctrl Pts',(145.430395182961,-0.134547381849304,
135.722672242263));
#34616=CARTESIAN_POINT('Ctrl Pts',(145.422622282696,0.00223408340109133,
135.722610110157));
#34617=CARTESIAN_POINT('Ctrl Pts',(145.415131946934,0.134043197857729,135.722550236709));
#34618=CARTESIAN_POINT('Ctrl Pts',(145.407641611172,0.265681421673301,135.717188036997));
#34619=CARTESIAN_POINT('Ctrl Pts',(145.40015127541,0.39669444194589,135.706586293953));
#34620=CARTESIAN_POINT('Ctrl Pts',(145.392376941291,0.532674860702761,135.695582582599));
#34621=CARTESIAN_POINT('Ctrl Pts',(145.384602607172,0.668412475953023,135.678899313778));
#34622=CARTESIAN_POINT('Ctrl Pts',(145.376828273053,0.803394611752564,135.656549830726));
#34623=CARTESIAN_POINT('Ctrl Pts',(145.369063520106,0.938210394133524,135.634227891415));
#34624=CARTESIAN_POINT('Ctrl Pts',(145.361298767158,1.07227216758641,135.606253695416));
#34625=CARTESIAN_POINT('Ctrl Pts',(145.353534014211,1.20507019389738,135.572692494678));
#34626=CARTESIAN_POINT('Ctrl Pts',(145.345776973326,1.33773632333645,135.539164627397));
#34627=CARTESIAN_POINT('Ctrl Pts',(145.338019932441,1.46914082688648,135.500060893493));
#34628=CARTESIAN_POINT('Ctrl Pts',(145.330262891556,1.5987823622354,135.455497900071));
#34629=CARTESIAN_POINT('Ctrl Pts',(145.322511700316,1.7283261338945,135.410968511948));
#34630=CARTESIAN_POINT('Ctrl Pts',(145.314760509076,1.85610921534232,135.360988185263));
#34631=CARTESIAN_POINT('Ctrl Pts',(145.307009317836,1.98164402790863,135.305723745459));
#34632=CARTESIAN_POINT('Ctrl Pts',(145.299261421059,2.10712548483043,135.250482794516));
#34633=CARTESIAN_POINT('Ctrl Pts',(145.291513524282,2.23036021635847,135.189962354554));
#34634=CARTESIAN_POINT('Ctrl Pts',(145.283765627505,2.35087949656811,135.124377822985));
#34635=CARTESIAN_POINT('Ctrl Pts',(145.276019351421,2.47137356674247,135.058807010286));
#34636=CARTESIAN_POINT('Ctrl Pts',(145.268273075336,2.58915297221669,134.988174399745));
#34637=CARTESIAN_POINT('Ctrl Pts',(145.260526799252,2.70377288738724,134.912741714291));
#34638=CARTESIAN_POINT('Ctrl Pts',(145.252780465987,2.81839364865598,134.837308472011));
#34639=CARTESIAN_POINT('Ctrl Pts',(145.245034132722,2.92985454649591,134.757075299044));
#34640=CARTESIAN_POINT('Ctrl Pts',(145.237287799456,3.03773942885925,134.672347461501));
#34641=CARTESIAN_POINT('Ctrl Pts',(145.229539731453,3.1456484712939,134.587600649746));
#34642=CARTESIAN_POINT('Ctrl Pts',(145.22179166345,3.24997959728711,134.49835741193));
#34643=CARTESIAN_POINT('Ctrl Pts',(145.214043595447,3.35034977071012,134.404963272179));
#34644=CARTESIAN_POINT('Ctrl Pts',(145.206287292706,3.4508266187478,134.311469872024));
#34645=CARTESIAN_POINT('Ctrl Pts',(145.198530989964,3.54733381811295,134.213817023985));
#34646=CARTESIAN_POINT('Ctrl Pts',(145.190774687222,3.63952487323465,134.112387485596));
#34647=CARTESIAN_POINT('Ctrl Pts',(145.183014244708,3.73176513349839,134.010903811207));
#34648=CARTESIAN_POINT('Ctrl Pts',(145.175253802194,3.81968440878661,133.90563972987));
#34649=CARTESIAN_POINT('Ctrl Pts',(145.167493359679,3.90297721672312,133.797010264324));
#34650=CARTESIAN_POINT('Ctrl Pts',(145.159720459414,3.98640373366926,133.688206417116));
#34651=CARTESIAN_POINT('Ctrl Pts',(145.151947559149,4.06518871728958,133.576026710085));
#34652=CARTESIAN_POINT('Ctrl Pts',(145.144174658883,4.13907016682952,133.460915005596));
#34653=CARTESIAN_POINT('Ctrl Pts',(145.136684323121,4.21026583958247,133.349987901515));
#34654=CARTESIAN_POINT('Ctrl Pts',(145.129193987359,4.27690814451405,133.236338535707));
#34655=CARTESIAN_POINT('Ctrl Pts',(145.121703651597,4.3388043354624,133.120383070193));
#34656=CARTESIAN_POINT('Ctrl Pts',(145.113929317478,4.40304733930367,133.00003111796));
#34657=CARTESIAN_POINT('Ctrl Pts',(145.106154983359,4.46238072936799,132.876813503651));
#34658=CARTESIAN_POINT('Ctrl Pts',(145.09838064924,4.51653861782784,132.751168768404));
#34659=CARTESIAN_POINT('Ctrl Pts',(145.090615896293,4.57062976153049,132.625678879064));
#34660=CARTESIAN_POINT('Ctrl Pts',(145.082851143346,4.61955794135898,132.497768175986));
#34661=CARTESIAN_POINT('Ctrl Pts',(145.075086390399,4.66310252966831,132.367900786638));
#34662=CARTESIAN_POINT('Ctrl Pts',(145.067329349514,4.70660386887837,132.238162383412));
#34663=CARTESIAN_POINT('Ctrl Pts',(145.059572308629,4.7447321339722,132.106471529671));
#34664=CARTESIAN_POINT('Ctrl Pts',(145.051815267744,4.77731444204252,131.973313047886));
#34665=CARTESIAN_POINT('Ctrl Pts',(145.044064076504,4.80987217954111,131.840254981948));
#34666=CARTESIAN_POINT('Ctrl Pts',(145.036312885264,4.83689219198253,131.705731869111));
#34667=CARTESIAN_POINT('Ctrl Pts',(145.028561694023,4.85825128615566,131.570244096345));
#34668=CARTESIAN_POINT('Ctrl Pts',(145.020813797246,4.87960130214394,131.434813909498));
#34669=CARTESIAN_POINT('Ctrl Pts',(145.013065900469,4.8952951245419,131.29842026358));
#34670=CARTESIAN_POINT('Ctrl Pts',(145.005318003692,4.90526061548313,131.161573938552));
#34671=CARTESIAN_POINT('Ctrl Pts',(144.997571727608,4.91522402185848,131.024756238826));
#34672=CARTESIAN_POINT('Ctrl Pts',(144.989825451524,4.91946145177116,130.887486438019));
#34673=CARTESIAN_POINT('Ctrl Pts',(144.98207917544,4.91795266103117,130.750280248148));
#34674=CARTESIAN_POINT('Ctrl Pts',(144.974332842175,4.91644385915363,130.613073045451));
#34675=CARTESIAN_POINT('Ctrl Pts',(144.966586508909,4.90918875628171,130.475929845569));
#34676=CARTESIAN_POINT('Ctrl Pts',(144.958840175644,4.89621924109144,130.339365772793));
#34677=CARTESIAN_POINT('Ctrl Pts',(144.951092107641,4.88324682146822,130.20277111744));
#34678=CARTESIAN_POINT('Ctrl Pts',(144.943344039638,4.86455748002248,130.066756236403));
#34679=CARTESIAN_POINT('Ctrl Pts',(144.935595971635,4.84023487560304,129.931830153057));
#34680=CARTESIAN_POINT('Ctrl Pts',(144.927839668893,4.81588642083022,129.796760668664));
#34681=CARTESIAN_POINT('Ctrl Pts',(144.920083366151,4.78589281267913,129.662782678944));
#34682=CARTESIAN_POINT('Ctrl Pts',(144.912327063409,4.75038878658295,129.53039459023));
#34683=CARTESIAN_POINT('Ctrl Pts',(144.904566620895,4.71486581091898,129.397935842006));
#34684=CARTESIAN_POINT('Ctrl Pts',(144.896806178381,4.67382667389694,129.267069058522));
#34685=CARTESIAN_POINT('Ctrl Pts',(144.889045735867,4.62745542521647,129.13827558068));
#34686=CARTESIAN_POINT('Ctrl Pts',(144.881272835601,4.58100973729097,129.009275352114));
#34687=CARTESIAN_POINT('Ctrl Pts',(144.873499935336,4.52921498074763,128.882355442295));
#34688=CARTESIAN_POINT('Ctrl Pts',(144.865727035071,4.47230297175938,128.75797619833));
#34689=CARTESIAN_POINT('Ctrl Pts',(144.858236699309,4.41745985765125,128.638118453177));
#34690=CARTESIAN_POINT('Ctrl Pts',(144.850746363547,4.35786522112499,128.520620136372));
#34691=CARTESIAN_POINT('Ctrl Pts',(144.843256027785,4.29376500706537,128.405868356457));
#34692=CARTESIAN_POINT('Ctrl Pts',(144.835481693666,4.22723441390598,128.286765727927));
#34693=CARTESIAN_POINT('Ctrl Pts',(144.827707359547,4.15563909191235,128.170244736165));
#34694=CARTESIAN_POINT('Ctrl Pts',(144.819933025427,4.0792042792977,128.056766122329));
#34695=CARTESIAN_POINT('Ctrl Pts',(144.81216827248,4.00286366575849,127.943427360742));
#34696=CARTESIAN_POINT('Ctrl Pts',(144.804403519533,3.92169564497463,127.833123837928));
#34697=CARTESIAN_POINT('Ctrl Pts',(144.796638766586,3.83597144589743,127.726292046407));
#34698=CARTESIAN_POINT('Ctrl Pts',(144.788881725701,3.750332389303,127.619566361726));
#34699=CARTESIAN_POINT('Ctrl Pts',(144.781124684816,3.66014640298863,127.516305849278));
#34700=CARTESIAN_POINT('Ctrl Pts',(144.773367643931,3.5657279343978,127.416918018738));
#34701=CARTESIAN_POINT('Ctrl Pts',(144.765616452691,3.47138066750932,127.317605137334));
#34702=CARTESIAN_POINT('Ctrl Pts',(144.757865261451,3.37280753951247,127.222159407223));
#34703=CARTESIAN_POINT('Ctrl Pts',(144.750114070211,3.27036295119792,127.130954945722));
#34704=CARTESIAN_POINT('Ctrl Pts',(144.742366173434,3.16796190456571,127.03978924855));
#34705=CARTESIAN_POINT('Ctrl Pts',(144.734618276657,3.06169296173569,126.952861494076));
#34706=CARTESIAN_POINT('Ctrl Pts',(144.726870379879,2.95194686407482,126.870508462975));
#34707=CARTESIAN_POINT('Ctrl Pts',(144.719124103795,2.84222372293164,126.788172658353));
#34708=CARTESIAN_POINT('Ctrl Pts',(144.711377827711,2.72902518620294,126.71040990822));
#34709=CARTESIAN_POINT('Ctrl Pts',(144.703631551627,2.61277419453387,126.637515999527));
#34710=CARTESIAN_POINT('Ctrl Pts',(144.695885218362,2.4965223447265,126.564621552749));
#34711=CARTESIAN_POINT('Ctrl Pts',(144.688138885096,2.37721832625067,126.496596226825));
#34712=CARTESIAN_POINT('Ctrl Pts',(144.680392551831,2.25531276437078,126.433691630172));
#34713=CARTESIAN_POINT('Ctrl Pts',(144.672644483828,2.13337990258558,126.370772946471));
#34714=CARTESIAN_POINT('Ctrl Pts',(144.664896415825,2.00884468546454,126.312977453191));
#34715=CARTESIAN_POINT('Ctrl Pts',(144.657148347822,1.88218058843893,126.260509905339));
#34716=CARTESIAN_POINT('Ctrl Pts',(144.64939204508,1.75538187130373,126.207986594354));
#34717=CARTESIAN_POINT('Ctrl Pts',(144.641635742338,1.62645011625809,126.160802690316));
#34718=CARTESIAN_POINT('Ctrl Pts',(144.633879439596,1.49587747445835,126.119114237288));
#34719=CARTESIAN_POINT('Ctrl Pts',(144.626118997082,1.36523514210817,126.077403533877));
#34720=CARTESIAN_POINT('Ctrl Pts',(144.618358554568,1.23295055482595,126.041194229071));
#34721=CARTESIAN_POINT('Ctrl Pts',(144.610598112054,1.09952816170457,126.010591653158));
#34722=CARTESIAN_POINT('Ctrl Pts',(144.602825211788,0.965891587112881,125.979939951274));
#34723=CARTESIAN_POINT('Ctrl Pts',(144.595052311523,0.831113941354601,125.95491303541));
#34724=CARTESIAN_POINT('Ctrl Pts',(144.587279411257,0.695707829792073,125.935564700908));
#34725=CARTESIAN_POINT('Ctrl Pts',(144.579789075495,0.565224071451377,125.916919727101));
#34726=CARTESIAN_POINT('Ctrl Pts',(144.572298739733,0.434157053073168,125.903547672329));
#34727=CARTESIAN_POINT('Ctrl Pts',(144.564808403971,0.302965399254829,125.895450857817));
#34728=CARTESIAN_POINT('Ctrl Pts',(144.557034069852,0.166799574008043,125.887047050123));
#34729=CARTESIAN_POINT('Ctrl Pts',(144.549259735733,0.0300681432426362,
125.884299779971));
#34730=CARTESIAN_POINT('Ctrl Pts',(144.541485401614,-0.106719511701879,
125.887268589922));
#34731=CARTESIAN_POINT('Ctrl Pts',(144.533720648667,-0.243338588086971,
125.89023374108));
#34732=CARTESIAN_POINT('Ctrl Pts',(144.52595589572,-0.380013363661367,125.898900947369));
#34733=CARTESIAN_POINT('Ctrl Pts',(144.518191142773,-0.516229999033403,
125.91327795106));
#34734=CARTESIAN_POINT('Ctrl Pts',(144.510434101888,-0.652311342122083,
125.927640675307));
#34735=CARTESIAN_POINT('Ctrl Pts',(144.502677061003,-0.787935064251584,
125.947701870537));
#34736=CARTESIAN_POINT('Ctrl Pts',(144.494920020118,-0.922588349466602,
125.973417252143));
#34737=CARTESIAN_POINT('Ctrl Pts',(144.487168828878,-1.05714009159165,125.999113241579));
#34738=CARTESIAN_POINT('Ctrl Pts',(144.479417637638,-1.19072247096256,126.030454857382));
#34739=CARTESIAN_POINT('Ctrl Pts',(144.471666446397,-1.32282916980003,126.067346151679));
#34740=CARTESIAN_POINT('Ctrl Pts',(144.46391854962,-1.45487971976697,126.104221766191));
#34741=CARTESIAN_POINT('Ctrl Pts',(144.456170652843,-1.58545546089066,126.146642262865));
#34742=CARTESIAN_POINT('Ctrl Pts',(144.448422756066,-1.71406184479824,126.194460938104));
#34743=CARTESIAN_POINT('Ctrl Pts',(144.440676479982,-1.84264132702257,126.242269610706));
#34744=CARTESIAN_POINT('Ctrl Pts',(144.432930203898,-1.96925190519468,126.295474079697));
#34745=CARTESIAN_POINT('Ctrl Pts',(144.425183927814,-2.09341611562539,126.353878393207));
#34746=CARTESIAN_POINT('Ctrl Pts',(144.417437594549,-2.21758124260792,126.412283137843));
#34747=CARTESIAN_POINT('Ctrl Pts',(144.409691261283,-2.3392996120335,126.475887637179));
#34748=CARTESIAN_POINT('Ctrl Pts',(144.401944928018,-2.45811596465303,126.544448767913));
#34749=CARTESIAN_POINT('Ctrl Pts',(144.394196860015,-2.57695892537096,126.613025252436));
#34750=CARTESIAN_POINT('Ctrl Pts',(144.386448792012,-2.69289823751659,126.686560381769));
#34751=CARTESIAN_POINT('Ctrl Pts',(144.378700724009,-2.80550570986693,126.764766482705));
#34752=CARTESIAN_POINT('Ctrl Pts',(144.370944421267,-2.91823286277919,126.843055702016));
#34753=CARTESIAN_POINT('Ctrl Pts',(144.363188118525,-3.02762078049908,126.92602558641));
#34754=CARTESIAN_POINT('Ctrl Pts',(144.355431815784,-3.13327215901682,127.013346420807));
#34755=CARTESIAN_POINT('Ctrl Pts',(144.347671373269,-3.2389799268568,127.100713860962));
#34756=CARTESIAN_POINT('Ctrl Pts',(144.339910930755,-3.3409468911488,127.192436617028));
#34757=CARTESIAN_POINT('Ctrl Pts',(144.332150488241,-3.43881176747942,127.28814721529));
#34758=CARTESIAN_POINT('Ctrl Pts',(144.324377587976,-3.53683374519725,127.384011456701));
#34759=CARTESIAN_POINT('Ctrl Pts',(144.31660468771,-3.63074020797275,127.483876047837));
#34760=CARTESIAN_POINT('Ctrl Pts',(144.308831787445,-3.72020882053998,127.587338796988));
#34761=CARTESIAN_POINT('Ctrl Pts',(144.301341451683,-3.80642502368255,127.6870404146));
#34762=CARTESIAN_POINT('Ctrl Pts',(144.293851115921,-3.88852023700126,127.790082886937));
#34763=CARTESIAN_POINT('Ctrl Pts',(144.286360780158,-3.96624460978605,127.896081614815));
#34764=CARTESIAN_POINT('Ctrl Pts',(144.278534089727,-4.04745920737628,128.006840231723));
#34765=CARTESIAN_POINT('Ctrl Pts',(144.270707399296,-4.12415900736794,128.121178041885));
#34766=CARTESIAN_POINT('Ctrl Pts',(144.262880708865,-4.19601447399703,128.238693921265));
#34767=CARTESIAN_POINT('Ctrl Pts',(144.255067153101,-4.26774935356702,128.35601258678));
#34768=CARTESIAN_POINT('Ctrl Pts',(144.247253597336,-4.33465589462292,128.476498373107));
#34769=CARTESIAN_POINT('Ctrl Pts',(144.239440041572,-4.39644600918776,128.599718798404));
#34770=CARTESIAN_POINT('Ctrl Pts',(144.231634058566,-4.45817623787452,128.722819800661));
#34771=CARTESIAN_POINT('Ctrl Pts',(144.22382807556,-4.51479973331902,128.848649828656));
#34772=CARTESIAN_POINT('Ctrl Pts',(144.216022092555,-4.56607252489284,128.976748853564));
#34773=CARTESIAN_POINT('Ctrl Pts',(144.208223432298,-4.61729721774736,129.104727709493));
#34774=CARTESIAN_POINT('Ctrl Pts',(144.200424772042,-4.66318106056448,129.234970968362));
#34775=CARTESIAN_POINT('Ctrl Pts',(144.192626111785,-4.70352698732374,129.366996035417));
#34776=CARTESIAN_POINT('Ctrl Pts',(144.188412227281,-4.72532727993827,129.438333722401));
#34777=CARTESIAN_POINT('Ctrl Pts',(144.184198342776,-4.7455115290801,129.510191247036));
#34778=CARTESIAN_POINT('Ctrl Pts',(144.179984458271,-4.76405452823405,129.582490119308));
#34779=CARTESIAN_POINT('Origin',(213.235140564004,0.,130.804360617566));
#34780=CARTESIAN_POINT('',(142.084824010153,-4.76405452823403,129.582490119308));
#34781=CARTESIAN_POINT('',(142.430282519794,-4.76405452823406,129.582490119308));
#34782=CARTESIAN_POINT('',(213.235140564004,-4.76405452823405,129.582490119308));
#34783=CARTESIAN_POINT('',(143.764859436021,-4.91824970830014,130.806054520038));
#34784=CARTESIAN_POINT('Ctrl Pts',(143.764859435991,-4.91824970829996,130.806054520568));
#34785=CARTESIAN_POINT('Ctrl Pts',(143.759591133558,-4.9182178511643,130.898551757986));
#34786=CARTESIAN_POINT('Ctrl Pts',(143.754322831125,-4.91557679471082,130.991000951387));
#34787=CARTESIAN_POINT('Ctrl Pts',(143.749054528692,-4.91033352930923,131.083300922007));
#34788=CARTESIAN_POINT('Ctrl Pts',(143.741280194573,-4.90259614186322,131.219506240495));
#34789=CARTESIAN_POINT('Ctrl Pts',(143.733505860454,-4.88917500590729,131.355605119116));
#34790=CARTESIAN_POINT('Ctrl Pts',(143.725731526335,-4.87007115802673,131.491084709364));
#34791=CARTESIAN_POINT('Ctrl Pts',(143.717966773388,-4.85099085393131,131.626397333126));
#34792=CARTESIAN_POINT('Ctrl Pts',(143.710202020441,-4.82624182672417,131.761091803671));
#34793=CARTESIAN_POINT('Ctrl Pts',(143.702437267494,-4.79587707724921,131.89465696371));
#34794=CARTESIAN_POINT('Ctrl Pts',(143.694680226609,-4.76554248647153,132.02808946495));
#34795=CARTESIAN_POINT('Ctrl Pts',(143.686923185724,-4.72960335924045,132.160394509042));
#34796=CARTESIAN_POINT('Ctrl Pts',(143.679166144839,-4.68816423824603,132.2910680998));
#34797=CARTESIAN_POINT('Ctrl Pts',(143.671414953599,-4.64675636681517,132.421643148587));
#34798=CARTESIAN_POINT('Ctrl Pts',(143.663663762358,-4.59985687484779,132.550588821693));
#34799=CARTESIAN_POINT('Ctrl Pts',(143.655912571118,-4.54762083920157,132.677413677508));
#34800=CARTESIAN_POINT('Ctrl Pts',(143.648164674341,-4.49540700526386,132.804184629377));
#34801=CARTESIAN_POINT('Ctrl Pts',(143.640416777564,-4.43786128745369,132.928836196033));
#34802=CARTESIAN_POINT('Ctrl Pts',(143.632668880787,-4.37518777302663,133.050894617589));
#34803=CARTESIAN_POINT('Ctrl Pts',(143.624922604703,-4.3125273685477,133.172927507154));
#34804=CARTESIAN_POINT('Ctrl Pts',(143.617176328619,-4.24474147943085,133.292367982967));
#34805=CARTESIAN_POINT('Ctrl Pts',(143.609430052535,-4.1720810786493,133.408765066893));
#34806=CARTESIAN_POINT('Ctrl Pts',(143.601683719269,-4.09942014150519,133.525163010037));
#34807=CARTESIAN_POINT('Ctrl Pts',(143.593937386004,-4.0218848279271,133.638517184816));
#34808=CARTESIAN_POINT('Ctrl Pts',(143.586191052739,-3.93977032961307,133.748404233479));
#34809=CARTESIAN_POINT('Ctrl Pts',(143.578442984736,-3.85763744232646,133.858315890585));
#34810=CARTESIAN_POINT('Ctrl Pts',(143.570694916733,-3.77092356370936,133.964758563429));
#34811=CARTESIAN_POINT('Ctrl Pts',(143.56294684873,-3.67996492657399,134.06734103456));
#34812=CARTESIAN_POINT('Ctrl Pts',(143.555190545988,-3.58890961751671,134.170032531562));
#34813=CARTESIAN_POINT('Ctrl Pts',(143.547434243246,-3.4936007977708,134.268855338332));
#34814=CARTESIAN_POINT('Ctrl Pts',(143.539677940504,-3.39441279970635,134.363453873957));
#34815=CARTESIAN_POINT('Ctrl Pts',(143.53191749799,-3.29517186202071,134.458102899669));
#34816=CARTESIAN_POINT('Ctrl Pts',(143.524157055476,-3.19204791432472,134.548522904085));
#34817=CARTESIAN_POINT('Ctrl Pts',(143.516396612962,-3.08544852910806,134.6343985334));
#34818=CARTESIAN_POINT('Ctrl Pts',(143.508623712696,-2.97867802109489,134.720412017898));
#34819=CARTESIAN_POINT('Ctrl Pts',(143.500850812431,-2.86842124141996,134.801866317045));
#34820=CARTESIAN_POINT('Ctrl Pts',(143.493077912165,-2.75511563733355,134.878488854063));
#34821=CARTESIAN_POINT('Ctrl Pts',(143.485587576403,-2.64592897735447,134.95232596886));
#34822=CARTESIAN_POINT('Ctrl Pts',(143.478097240641,-2.53391157132072,135.021676353868));
#34823=CARTESIAN_POINT('Ctrl Pts',(143.470606904879,-2.41947483603103,135.086337331691));
#34824=CARTESIAN_POINT('Ctrl Pts',(143.46283257076,-2.30069919714137,135.153449950141));
#34825=CARTESIAN_POINT('Ctrl Pts',(143.455058236641,-2.17894090422282,135.21572313665));
#34826=CARTESIAN_POINT('Ctrl Pts',(143.447283902522,-2.05463199154863,135.272880556182));
#34827=CARTESIAN_POINT('Ctrl Pts',(143.439519149575,-1.93047627849945,135.329967534302));
#34828=CARTESIAN_POINT('Ctrl Pts',(143.431754396628,-1.80377655195029,135.381951128208));
#34829=CARTESIAN_POINT('Ctrl Pts',(143.42398964368,-1.67499151125555,135.428599636012));
#34830=CARTESIAN_POINT('Ctrl Pts',(143.416232602796,-1.54633438167882,135.475201811861));
#34831=CARTESIAN_POINT('Ctrl Pts',(143.40847556191,-1.41559642487995,135.516479314335));
#34832=CARTESIAN_POINT('Ctrl Pts',(143.400718521025,-1.28325817500237,135.55224767591));
#34833=CARTESIAN_POINT('Ctrl Pts',(143.392967329785,-1.15101972242861,135.587989064285));
#34834=CARTESIAN_POINT('Ctrl Pts',(143.385216138545,-1.01718375472078,135.618229479418));
#34835=CARTESIAN_POINT('Ctrl Pts',(143.377464947305,-0.882247558453494,
135.642833755665));
#34836=CARTESIAN_POINT('Ctrl Pts',(143.369717050528,-0.747368713669025,
135.667427574438));
#34837=CARTESIAN_POINT('Ctrl Pts',(143.361969153751,-0.611390954216804,
135.686389948826));
#34838=CARTESIAN_POINT('Ctrl Pts',(143.354221256974,-0.474823181854244,
135.699636504426));
#34839=CARTESIAN_POINT('Ctrl Pts',(143.34647498089,-0.338283976525602,135.712880289132));
#34840=CARTESIAN_POINT('Ctrl Pts',(143.338728704806,-0.20115539266414,135.720410595494));
#34841=CARTESIAN_POINT('Ctrl Pts',(143.330982428722,-0.0639525079682787,
135.722194809487));
#34842=CARTESIAN_POINT('Ctrl Pts',(143.323236095456,0.0732513895281564,
135.72397903665));
#34843=CARTESIAN_POINT('Ctrl Pts',(143.315489762191,0.210529198021276,135.72001708172));
#34844=CARTESIAN_POINT('Ctrl Pts',(143.307743428925,0.347365176321654,135.710328462628));
#34845=CARTESIAN_POINT('Ctrl Pts',(143.299995360922,0.484231798090526,135.700637673836));
#34846=CARTESIAN_POINT('Ctrl Pts',(143.292247292919,0.620656002863723,135.68521769657));
#34847=CARTESIAN_POINT('Ctrl Pts',(143.284499224916,0.756126906272655,135.664139950428));
#34848=CARTESIAN_POINT('Ctrl Pts',(143.276742922175,0.891741789769901,135.643039802606));
#34849=CARTESIAN_POINT('Ctrl Pts',(143.268986619433,1.02640096103342,135.616269934209));
#34850=CARTESIAN_POINT('Ctrl Pts',(143.261230316691,1.15960292397994,135.58395308149));
#34851=CARTESIAN_POINT('Ctrl Pts',(143.253469874177,1.29287598082477,135.551618980294));
#34852=CARTESIAN_POINT('Ctrl Pts',(143.245709431663,1.42468990403993,135.513732103493));
#34853=CARTESIAN_POINT('Ctrl Pts',(143.237948989148,1.55455907465073,135.470464896932));
#34854=CARTESIAN_POINT('Ctrl Pts',(143.230176088883,1.68463672278345,135.42712823401));
#34855=CARTESIAN_POINT('Ctrl Pts',(143.222403188618,1.81276301414729,135.378394120956));
#34856=CARTESIAN_POINT('Ctrl Pts',(143.214630288352,1.93847217125534,135.324483260124));
#34857=CARTESIAN_POINT('Ctrl Pts',(143.20713995259,2.05961148386025,135.272532194877));
#34858=CARTESIAN_POINT('Ctrl Pts',(143.199649616828,2.17850607101054,135.215774355758));
#34859=CARTESIAN_POINT('Ctrl Pts',(143.192159281066,2.2947630336431,135.154446327288));
#34860=CARTESIAN_POINT('Ctrl Pts',(143.184384946947,2.4154279143493,135.090793027978));
#34861=CARTESIAN_POINT('Ctrl Pts',(143.176610612828,2.53363344126155,135.022014506187));
#34862=CARTESIAN_POINT('Ctrl Pts',(143.168836278709,2.64891360080973,134.948324878747));
#34863=CARTESIAN_POINT('Ctrl Pts',(143.161071525762,2.76405168786412,134.874726067187));
#34864=CARTESIAN_POINT('Ctrl Pts',(143.153306772815,2.87627125468223,134.796228401195));
#34865=CARTESIAN_POINT('Ctrl Pts',(143.145542019867,2.98512942569717,134.713092556998));
#34866=CARTESIAN_POINT('Ctrl Pts',(143.137784978982,3.09387947724198,134.630039284494));
#34867=CARTESIAN_POINT('Ctrl Pts',(143.130027938098,3.1992744682146,134.542357237094));
#34868=CARTESIAN_POINT('Ctrl Pts',(143.122270897213,3.30089946042062,134.45035099258));
#34869=CARTESIAN_POINT('Ctrl Pts',(143.114519705972,3.40244781642952,134.358414130691));
#34870=CARTESIAN_POINT('Ctrl Pts',(143.106768514732,3.50023154380476,134.262159823669));
#34871=CARTESIAN_POINT('Ctrl Pts',(143.099017323492,3.59386812832307,134.161933392462));
#34872=CARTESIAN_POINT('Ctrl Pts',(143.091269426715,3.68746491479512,134.061749560162));
#34873=CARTESIAN_POINT('Ctrl Pts',(143.083521529938,3.77691779783553,133.957597246583));
#34874=CARTESIAN_POINT('Ctrl Pts',(143.075773633161,3.86188071703885,133.849858998761));
#34875=CARTESIAN_POINT('Ctrl Pts',(143.068027357077,3.9468258638311,133.742143287458));
#34876=CARTESIAN_POINT('Ctrl Pts',(143.060281080993,4.02728267297213,133.630843440699));
#34877=CARTESIAN_POINT('Ctrl Pts',(143.052534804909,4.10294529328026,133.516375179262));
#34878=CARTESIAN_POINT('Ctrl Pts',(143.044788471643,4.17860847211264,133.401906072846));
#34879=CARTESIAN_POINT('Ctrl Pts',(143.037042138378,4.24947717590922,133.284268831235));
#34880=CARTESIAN_POINT('Ctrl Pts',(143.029295805113,4.3152890549469,133.163907912018));
#34881=CARTESIAN_POINT('Ctrl Pts',(143.02154773711,4.38111567209856,133.043520038807));
#34882=CARTESIAN_POINT('Ctrl Pts',(143.013799669107,4.44188302353416,132.920407617231));
#34883=CARTESIAN_POINT('Ctrl Pts',(143.006051601104,4.49737505110536,132.795039072816));
#34884=CARTESIAN_POINT('Ctrl Pts',(142.998295298362,4.55292605626385,132.669537285219));
#34885=CARTESIAN_POINT('Ctrl Pts',(142.99053899562,4.60319037911991,132.54177494293));
#34886=CARTESIAN_POINT('Ctrl Pts',(142.982782692878,4.64800021027819,132.41224031075));
#34887=CARTESIAN_POINT('Ctrl Pts',(142.975022250364,4.69283395779258,132.282636542037));
#34888=CARTESIAN_POINT('Ctrl Pts',(142.96726180785,4.73220730056031,132.151258972923));
#34889=CARTESIAN_POINT('Ctrl Pts',(142.959501365336,4.76600283323565,132.018609379595));
#34890=CARTESIAN_POINT('Ctrl Pts',(142.95172846507,4.79985261750025,131.885746845365));
#34891=CARTESIAN_POINT('Ctrl Pts',(142.943955564805,4.82810661810689,131.751608589213));
#34892=CARTESIAN_POINT('Ctrl Pts',(142.936182664539,4.85069875408796,131.616705777944));
#34893=CARTESIAN_POINT('Ctrl Pts',(142.928692328777,4.87246960902022,131.486707023663));
#34894=CARTESIAN_POINT('Ctrl Pts',(142.921201993015,4.88898306002035,131.355998641791));
#34895=CARTESIAN_POINT('Ctrl Pts',(142.913711657253,4.90022578080569,131.22503906915));
#34896=CARTESIAN_POINT('Ctrl Pts',(142.905937323134,4.91189477276663,131.08911412451));
#34897=CARTESIAN_POINT('Ctrl Pts',(142.898162989015,4.9179224291013,130.952487995927));
#34898=CARTESIAN_POINT('Ctrl Pts',(142.890388654896,4.91823700064761,130.815668489195));
#34899=CARTESIAN_POINT('Ctrl Pts',(142.882623901949,4.91855118451261,130.679017600276));
#34900=CARTESIAN_POINT('Ctrl Pts',(142.874859149002,4.91316629192455,130.542174194608));
#34901=CARTESIAN_POINT('Ctrl Pts',(142.867094396054,4.90206225211436,130.405651777815));
#34902=CARTESIAN_POINT('Ctrl Pts',(142.859337355169,4.89096924099305,130.269264957011));
#34903=CARTESIAN_POINT('Ctrl Pts',(142.851580314284,4.87416841826721,130.133198877792));
#34904=CARTESIAN_POINT('Ctrl Pts',(142.843823273399,4.85169174962129,129.997967271142));
#34905=CARTESIAN_POINT('Ctrl Pts',(142.836072082159,4.82923203080603,129.862837643699));
#34906=CARTESIAN_POINT('Ctrl Pts',(142.828320890919,4.80110504939137,129.728541620392));
#34907=CARTESIAN_POINT('Ctrl Pts',(142.820569699679,4.7673945753897,129.595587675676));
#34908=CARTESIAN_POINT('Ctrl Pts',(142.812821802902,4.73369842923874,129.462690239934));
#34909=CARTESIAN_POINT('Ctrl Pts',(142.805073906125,4.69442360636946,129.331134126444));
#34910=CARTESIAN_POINT('Ctrl Pts',(142.797326009348,4.64970490033501,129.201417261642));
#34911=CARTESIAN_POINT('Ctrl Pts',(142.789579733264,4.60499554848984,129.071727530812));
#34912=CARTESIAN_POINT('Ctrl Pts',(142.78183345718,4.5548447058434,128.943876652803));
#34913=CARTESIAN_POINT('Ctrl Pts',(142.774087181095,4.49943681002503,128.818346656112));
#34914=CARTESIAN_POINT('Ctrl Pts',(142.76634084783,4.44402850519818,128.692815732786));
#34915=CARTESIAN_POINT('Ctrl Pts',(142.758594514565,4.38336322763782,128.569606082636));
#34916=CARTESIAN_POINT('Ctrl Pts',(142.750848181299,4.31767310566619,128.449178668097));
#34917=CARTESIAN_POINT('Ctrl Pts',(142.743100113296,4.25196827284723,128.328724284673));
#34918=CARTESIAN_POINT('Ctrl Pts',(142.735352045293,4.181236543626,128.211053719839));
#34919=CARTESIAN_POINT('Ctrl Pts',(142.72760397729,4.10575523295771,128.096601944874));
#34920=CARTESIAN_POINT('Ctrl Pts',(142.719847674549,4.03019369985416,127.9820285292));
#34921=CARTESIAN_POINT('Ctrl Pts',(142.712091371807,3.94987271714661,127.870681064046));
#34922=CARTESIAN_POINT('Ctrl Pts',(142.704335069065,3.86511237076399,127.762964651259));
#34923=CARTESIAN_POINT('Ctrl Pts',(142.696574626551,3.7803067852324,127.65519074698));
#34924=CARTESIAN_POINT('Ctrl Pts',(142.688814184036,3.69105736904373,127.551052053417));
#34925=CARTESIAN_POINT('Ctrl Pts',(142.681053741522,3.59772282025836,127.450918569298));
#34926=CARTESIAN_POINT('Ctrl Pts',(142.673280841257,3.50423844256942,127.350624342021));
#34927=CARTESIAN_POINT('Ctrl Pts',(142.665507940991,3.40665610614584,127.254348447156));
#34928=CARTESIAN_POINT('Ctrl Pts',(142.657735040726,3.30537015172036,127.162422778638));
#34929=CARTESIAN_POINT('Ctrl Pts',(142.650244704964,3.20776619686285,127.073838839717));
#34930=CARTESIAN_POINT('Ctrl Pts',(142.642754369202,3.10672345697104,126.989294532576));
#34931=CARTESIAN_POINT('Ctrl Pts',(142.63526403344,3.00262042474543,126.909048865292));
#34932=CARTESIAN_POINT('Ctrl Pts',(142.627489699321,2.89457029441094,126.825760659143));
#34933=CARTESIAN_POINT('Ctrl Pts',(142.619715365202,2.78288095846386,126.746839661379));
#34934=CARTESIAN_POINT('Ctrl Pts',(142.611941031083,2.66794086612493,126.672620718037));
#34935=CARTESIAN_POINT('Ctrl Pts',(142.604176278136,2.55314242717736,126.598493242909));
#34936=CARTESIAN_POINT('Ctrl Pts',(142.596411525189,2.43510152840496,126.529056502202));
#34937=CARTESIAN_POINT('Ctrl Pts',(142.588646772241,2.31423934789276,126.464604944355));
#34938=CARTESIAN_POINT('Ctrl Pts',(142.580889731356,2.19349720940202,126.400217400704));
#34939=CARTESIAN_POINT('Ctrl Pts',(142.573132690471,2.0699397082969,126.340805369271));
#34940=CARTESIAN_POINT('Ctrl Pts',(142.565375649586,1.94401633923829,126.286619640565));
#34941=CARTESIAN_POINT('Ctrl Pts',(142.557624458346,1.81818792997186,126.232474773739));
#34942=CARTESIAN_POINT('Ctrl Pts',(142.549873267106,1.689997561608,126.18354851884));
#34943=CARTESIAN_POINT('Ctrl Pts',(142.542122075866,1.55991830784575,126.140045240649));
#34944=CARTESIAN_POINT('Ctrl Pts',(142.534374179089,1.42989434123632,126.096560452511));
#34945=CARTESIAN_POINT('Ctrl Pts',(142.526626282312,1.29798345599256,126.058494180533));
#34946=CARTESIAN_POINT('Ctrl Pts',(142.518878385535,1.16467743093587,126.026002160484));
#34947=CARTESIAN_POINT('Ctrl Pts',(142.511132109451,1.03139929062587,125.993516937064));
#34948=CARTESIAN_POINT('Ctrl Pts',(142.503385833367,0.896726970579325,125.966603738833));
#34949=CARTESIAN_POINT('Ctrl Pts',(142.495639557283,0.761165708065515,125.945367941366));
#34950=CARTESIAN_POINT('Ctrl Pts',(142.487893224017,0.625603444869398,125.924131987141));
#34951=CARTESIAN_POINT('Ctrl Pts',(142.480146890752,0.48915261236676,125.908573577813));
#34952=CARTESIAN_POINT('Ctrl Pts',(142.472400557487,0.352326502337162,125.898746578707));
#34953=CARTESIAN_POINT('Ctrl Pts',(142.464652489484,0.215469751048862,125.888917378912));
#34954=CARTESIAN_POINT('Ctrl Pts',(142.456904421481,0.0782379448882408,
125.884822171377));
#34955=CARTESIAN_POINT('Ctrl Pts',(142.449156353478,-0.0588530669821975,
125.886462755775));
#34956=CARTESIAN_POINT('Ctrl Pts',(142.441400050736,-0.196089780811549,
125.888105083806));
#34957=CARTESIAN_POINT('Ctrl Pts',(142.433643747994,-0.333185009872422,
125.895495376637));
#34958=CARTESIAN_POINT('Ctrl Pts',(142.425887445252,-0.469624916243211,
125.908583304356));
#34959=CARTESIAN_POINT('Ctrl Pts',(142.418127002738,-0.60613764470025,125.921678217496));
#34960=CARTESIAN_POINT('Ctrl Pts',(142.410366560224,-0.741993966444115,
125.94047677141));
#34961=CARTESIAN_POINT('Ctrl Pts',(142.40260611771,-0.876688706002444,125.964877176612));
#34962=CARTESIAN_POINT('Ctrl Pts',(142.394833217444,-1.01159966951435,125.989316751511));
#34963=CARTESIAN_POINT('Ctrl Pts',(142.387060317179,-1.14534494295683,126.019376061976));
#34964=CARTESIAN_POINT('Ctrl Pts',(142.379287416913,-1.2774321437656,126.054902734757));
#34965=CARTESIAN_POINT('Ctrl Pts',(142.371797081151,-1.40471764211793,126.089137923497));
#34966=CARTESIAN_POINT('Ctrl Pts',(142.364306745389,-1.53046323115435,126.128449779128));
#34967=CARTESIAN_POINT('Ctrl Pts',(142.356816409627,-1.65424641549254,126.172659865215));
#34968=CARTESIAN_POINT('Ctrl Pts',(142.3490419539,-1.78272488654235,126.218546907916));
#34969=CARTESIAN_POINT('Ctrl Pts',(142.341267498174,-1.90949612757785,126.269856469942));
#34970=CARTESIAN_POINT('Ctrl Pts',(142.333493042447,-2.03406843387499,126.326442723185));
#34971=CARTESIAN_POINT('Ctrl Pts',(142.325728196272,-2.15848676360114,126.382959033457));
#34972=CARTESIAN_POINT('Ctrl Pts',(142.317963350097,-2.2807112140519,126.444738897361));
#34973=CARTESIAN_POINT('Ctrl Pts',(142.310198503922,-2.40026638362756,126.511587114325));
#34974=CARTESIAN_POINT('Ctrl Pts',(142.302441398069,-2.51970237562632,126.5783686942));
#34975=CARTESIAN_POINT('Ctrl Pts',(142.294684292217,-2.63647404299896,126.650208382986));
#34976=CARTESIAN_POINT('Ctrl Pts',(142.286927186364,-2.75012741506298,126.726863558901));
#34977=CARTESIAN_POINT('Ctrl Pts',(142.279175958326,-2.86369466822685,126.803460650668));
#34978=CARTESIAN_POINT('Ctrl Pts',(142.271424730288,-2.97414800643865,126.884865748838));
#34979=CARTESIAN_POINT('Ctrl Pts',(142.263673502249,-3.08105977891318,126.970791301476));
#34980=CARTESIAN_POINT('Ctrl Pts',(142.255925713781,-3.1879241098019,127.056678725064));
#34981=CARTESIAN_POINT('Ctrl Pts',(142.248177925313,-3.2912496973339,127.147082368081));
#34982=CARTESIAN_POINT('Ctrl Pts',(142.240430136845,-3.39063971587617,127.241672674506));
#34983=CARTESIAN_POINT('Ctrl Pts',(142.232684009192,-3.49000842918814,127.336242704567));
#34984=CARTESIAN_POINT('Ctrl Pts',(142.224937881539,-3.58544296877462,127.434997343353));
#34985=CARTESIAN_POINT('Ctrl Pts',(142.217191753886,-3.67658160752567,127.537568499034));
#34986=CARTESIAN_POINT('Ctrl Pts',(142.2094456092,-3.767720446674,127.64013988025));
#34987=CARTESIAN_POINT('Ctrl Pts',(142.201699464515,-3.8545631066173,127.746527502757));
#34988=CARTESIAN_POINT('Ctrl Pts',(142.193953319829,-3.93678684557427,127.856328664718));
#34989=CARTESIAN_POINT('Ctrl Pts',(142.186205480617,-4.01902857158532,127.966153846499));
#34990=CARTESIAN_POINT('Ctrl Pts',(142.178457641405,-4.09664913200355,128.079393740599));
#34991=CARTESIAN_POINT('Ctrl Pts',(142.170709802193,-4.16936820707962,128.195615360494));
#34992=CARTESIAN_POINT('Ctrl Pts',(142.162954283335,-4.24215936118452,128.31195217907));
#34993=CARTESIAN_POINT('Ctrl Pts',(142.155198764477,-4.31003911935539,128.431276294259));
#34994=CARTESIAN_POINT('Ctrl Pts',(142.147443245619,-4.3727721504203,128.553128336568));
#34995=CARTESIAN_POINT('Ctrl Pts',(142.13968360357,-4.43553853325875,128.675045161044));
#34996=CARTESIAN_POINT('Ctrl Pts',(142.13192396152,-4.49315257281768,128.79949223612));
#34997=CARTESIAN_POINT('Ctrl Pts',(142.124164319471,-4.54542689597396,128.925989675538));
#34998=CARTESIAN_POINT('Ctrl Pts',(142.116393520392,-4.59777638061022,129.052668996502));
#34999=CARTESIAN_POINT('Ctrl Pts',(142.108622721312,-4.64477067816591,129.181404203919));
#35000=CARTESIAN_POINT('Ctrl Pts',(142.100851922233,-4.68627193195673,129.311699087863));
#35001=CARTESIAN_POINT('Ctrl Pts',(142.095509284873,-4.71480518146293,129.401280391881));
#35002=CARTESIAN_POINT('Ctrl Pts',(142.090166647513,-4.74074295468664,129.491598647849));
#35003=CARTESIAN_POINT('Ctrl Pts',(142.084824010153,-4.76405452823403,129.582490119308));
#35004=CARTESIAN_POINT('Ctrl Pts',(143.834995515417,-4.76405452823405,129.582490119308));
#35005=CARTESIAN_POINT('Ctrl Pts',(143.827302392399,-4.7978580186573,129.714289415429));
#35006=CARTESIAN_POINT('Ctrl Pts',(143.819609269382,-4.82616221601706,129.84739236389));
#35007=CARTESIAN_POINT('Ctrl Pts',(143.811916146364,-4.84889145772445,129.981296407612));
#35008=CARTESIAN_POINT('Ctrl Pts',(143.804073361307,-4.87206287417234,130.117805421027));
#35009=CARTESIAN_POINT('Ctrl Pts',(143.79623057625,-4.88944012954329,130.255146585595));
#35010=CARTESIAN_POINT('Ctrl Pts',(143.788387791193,-4.90099868268711,130.3927844098));
#35011=CARTESIAN_POINT('Ctrl Pts',(143.780545006136,-4.91255723583092,130.530422234005));
#35012=CARTESIAN_POINT('Ctrl Pts',(143.772702221078,-4.91829713317609,130.668356284091));
#35013=CARTESIAN_POINT('Ctrl Pts',(143.764859436021,-4.91824970830014,130.806054520038));
#35014=CARTESIAN_POINT('',(144.110140563953,-4.91824891722445,130.807624161739));
#35015=CARTESIAN_POINT('Ctrl Pts',(144.179984458271,-4.76405452823405,129.582490119308));
#35016=CARTESIAN_POINT('Ctrl Pts',(144.172192290088,-4.7983435952176,129.716182671068));
#35017=CARTESIAN_POINT('Ctrl Pts',(144.164400121904,-4.82701755785097,129.851385085608));
#35018=CARTESIAN_POINT('Ctrl Pts',(144.15660795372,-4.84995547360527,129.987589556285));
#35019=CARTESIAN_POINT('Ctrl Pts',(144.148816480302,-4.872891344169,130.123781882698));
#35020=CARTESIAN_POINT('Ctrl Pts',(144.141025006883,-4.89009211292143,130.26097571021));
#35021=CARTESIAN_POINT('Ctrl Pts',(144.133233533465,-4.90148799701282,130.39865323824));
#35022=CARTESIAN_POINT('Ctrl Pts',(144.125535876979,-4.91274666355443,130.534672994666));
#35023=CARTESIAN_POINT('Ctrl Pts',(144.117838220494,-4.91833946612017,130.671164497436));
#35024=CARTESIAN_POINT('Ctrl Pts',(144.110140564008,-4.9182489172251,130.807624160758));
#35025=CARTESIAN_POINT('Ctrl Pts',(144.110140563953,-4.91824891722444,130.807624161739));
#35026=CARTESIAN_POINT('Ctrl Pts',(144.101366046741,-4.91814570099509,130.963173797746));
#35027=CARTESIAN_POINT('Ctrl Pts',(144.09259152953,-4.91065911423936,131.118438323462));
#35028=CARTESIAN_POINT('Ctrl Pts',(144.083817012319,-4.89589425273592,131.272764853806));
#35029=CARTESIAN_POINT('Ctrl Pts',(144.075005960534,-4.88106791458293,131.427733955569));
#35030=CARTESIAN_POINT('Ctrl Pts',(144.06619490875,-4.85890267712743,131.581757060317));
#35031=CARTESIAN_POINT('Ctrl Pts',(144.057383856965,-4.8295547027173,131.734190944003));
#35032=CARTESIAN_POINT('Ctrl Pts',(144.048522408935,-4.80003886778996,131.887496698101));
#35033=CARTESIAN_POINT('Ctrl Pts',(144.039660960905,-4.76325799042229,132.039194826826));
#35034=CARTESIAN_POINT('Ctrl Pts',(144.030799512875,-4.71941960498347,132.188651647154));
#35035=CARTESIAN_POINT('Ctrl Pts',(144.023170727366,-4.68167931259706,132.317318431796));
#35036=CARTESIAN_POINT('Ctrl Pts',(144.015541941856,-4.63870923365158,132.444324367405));
#35037=CARTESIAN_POINT('Ctrl Pts',(144.007913156346,-4.59066958425604,132.569278698012));
#35038=CARTESIAN_POINT('Ctrl Pts',(144.000138822227,-4.54171339262111,132.696617016085));
#35039=CARTESIAN_POINT('Ctrl Pts',(143.992364488108,-4.48737738046281,132.822118527769));
#35040=CARTESIAN_POINT('Ctrl Pts',(143.984590153989,-4.42781912566329,132.945295192211));
#35041=CARTESIAN_POINT('Ctrl Pts',(143.976825401042,-4.36833427108993,133.068320052422));
#35042=CARTESIAN_POINT('Ctrl Pts',(143.969060648094,-4.30364014804724,133.189025417617));
#35043=CARTESIAN_POINT('Ctrl Pts',(143.961295895147,-4.23394330072747,133.306940723921));
#35044=CARTESIAN_POINT('Ctrl Pts',(143.953538854262,-4.16431567729903,133.424738915081));
#35045=CARTESIAN_POINT('Ctrl Pts',(143.945781813377,-4.08969541533217,133.539752227625));
#35046=CARTESIAN_POINT('Ctrl Pts',(143.938024772492,-4.01033595294006,133.651532654352));
#35047=CARTESIAN_POINT('Ctrl Pts',(143.930273581252,-3.93103633613595,133.76322878659));
#35048=CARTESIAN_POINT('Ctrl Pts',(143.922522390012,-3.84700485788766,133.871696568087));
#35049=CARTESIAN_POINT('Ctrl Pts',(143.914771198772,-3.75853924385391,133.976515376545));
#35050=CARTESIAN_POINT('Ctrl Pts',(143.907023301995,-3.67011123006587,134.081289634212));
#35051=CARTESIAN_POINT('Ctrl Pts',(143.899275405218,-3.57725308050513,134.182417705331));
#35052=CARTESIAN_POINT('Ctrl Pts',(143.891527508441,-3.4803037918747,134.27951076954));
#35053=CARTESIAN_POINT('Ctrl Pts',(143.883781232357,-3.38337478294551,134.376583523972));
#35054=CARTESIAN_POINT('Ctrl Pts',(143.876034956273,-3.2823566132104,134.469622673846));
#35055=CARTESIAN_POINT('Ctrl Pts',(143.868288680188,-3.17762596998102,134.558275408475));
#35056=CARTESIAN_POINT('Ctrl Pts',(143.860542346923,-3.07289455365394,134.646928797518));
#35057=CARTESIAN_POINT('Ctrl Pts',(143.852796013658,-2.96445090755763,134.731195454108));
#35058=CARTESIAN_POINT('Ctrl Pts',(143.845049680392,-2.85270539257755,134.810762370468));
#35059=CARTESIAN_POINT('Ctrl Pts',(143.837301612389,-2.74093485296409,134.890347105288));
#35060=CARTESIAN_POINT('Ctrl Pts',(143.829553544386,-2.62586129150441,134.965229778851));
#35061=CARTESIAN_POINT('Ctrl Pts',(143.821805476384,-2.50792433670316,135.035140520122));
#35062=CARTESIAN_POINT('Ctrl Pts',(143.814049173642,-2.38986203710288,135.105125563361));
#35063=CARTESIAN_POINT('Ctrl Pts',(143.8062928709,-2.26893060179689,135.170127918812));
#35064=CARTESIAN_POINT('Ctrl Pts',(143.798536568158,-2.1455950583029,135.229923283294));
#35065=CARTESIAN_POINT('Ctrl Pts',(143.790776125644,-2.0221936869157,135.289750562362));
#35066=CARTESIAN_POINT('Ctrl Pts',(143.78301568313,-1.89638600902053,135.344365157204));
#35067=CARTESIAN_POINT('Ctrl Pts',(143.775255240615,-1.76865642210888,135.393591220078));
#35068=CARTESIAN_POINT('Ctrl Pts',(143.76748234035,-1.64072179232507,135.442896304999));
#35069=CARTESIAN_POINT('Ctrl Pts',(143.759709440085,-1.51085945886281,135.486795446921));
#35070=CARTESIAN_POINT('Ctrl Pts',(143.751936539819,-1.37956920596051,135.525162654134));
#35071=CARTESIAN_POINT('Ctrl Pts',(143.744446204057,-1.25305168445153,135.562135116723));
#35072=CARTESIAN_POINT('Ctrl Pts',(143.736955868295,-1.12520855691546,135.59397078692));
#35073=CARTESIAN_POINT('Ctrl Pts',(143.729465532533,-0.996493477471868,
135.620602286321));
#35074=CARTESIAN_POINT('Ctrl Pts',(143.721691198414,-0.862898126668925,
135.648243527117));
#35075=CARTESIAN_POINT('Ctrl Pts',(143.713916864295,-0.727940208698602,
135.670365733823));
#35076=CARTESIAN_POINT('Ctrl Pts',(143.706142530176,-0.592115500849083,
135.686837683171));
#35077=CARTESIAN_POINT('Ctrl Pts',(143.698377777229,-0.456458184813031,
135.703289332313));
#35078=CARTESIAN_POINT('Ctrl Pts',(143.690613024282,-0.31993658877468,135.714104532645));
#35079=CARTESIAN_POINT('Ctrl Pts',(143.682848271334,-0.183058253629607,
135.719202704376));
#35080=CARTESIAN_POINT('Ctrl Pts',(143.675091230449,-0.0463158679766459,
135.724295812531));
#35081=CARTESIAN_POINT('Ctrl Pts',(143.667334189564,0.0907821635074765,
135.723683177569));
#35082=CARTESIAN_POINT('Ctrl Pts',(143.659577148679,0.227721930184656,135.717335865317));
#35083=CARTESIAN_POINT('Ctrl Pts',(143.651825957439,0.364558429518408,135.710993339622));
#35084=CARTESIAN_POINT('Ctrl Pts',(143.644074766199,0.501236512635953,135.698924762449));
#35085=CARTESIAN_POINT('Ctrl Pts',(143.636323574959,0.637241370091793,135.681153262199));
#35086=CARTESIAN_POINT('Ctrl Pts',(143.628575678182,0.773188421855305,135.66338931531));
#35087=CARTESIAN_POINT('Ctrl Pts',(143.620827781405,0.908462430207474,135.639927316836));
#35088=CARTESIAN_POINT('Ctrl Pts',(143.613079884628,1.04255303356731,135.610842307399));
#35089=CARTESIAN_POINT('Ctrl Pts',(143.605333608544,1.17661558806359,135.581763381919));
#35090=CARTESIAN_POINT('Ctrl Pts',(143.59758733246,1.30949484810539,135.547063867852));
#35091=CARTESIAN_POINT('Ctrl Pts',(143.589841056375,1.44069037537835,135.506869980108));
#35092=CARTESIAN_POINT('Ctrl Pts',(143.58209472311,1.57188687110684,135.466675795661));
#35093=CARTESIAN_POINT('Ctrl Pts',(143.574348389845,1.70139923545008,135.420987271131));
#35094=CARTESIAN_POINT('Ctrl Pts',(143.566602056579,1.82874231601914,135.369980466404));
#35095=CARTESIAN_POINT('Ctrl Pts',(143.558853988576,1.95611391418808,135.318962239056));
#35096=CARTESIAN_POINT('Ctrl Pts',(143.551105920573,2.08131489904073,135.262623506919));
#35097=CARTESIAN_POINT('Ctrl Pts',(143.543357852571,2.20388059048747,135.201188270019));
#35098=CARTESIAN_POINT('Ctrl Pts',(143.535601549829,2.32657654620975,135.139687739017));
#35099=CARTESIAN_POINT('Ctrl Pts',(143.527845247087,2.44663126351085,135.07308005843));
#35100=CARTESIAN_POINT('Ctrl Pts',(143.520088944345,2.56360467103868,135.00163522773));
#35101=CARTESIAN_POINT('Ctrl Pts',(143.512328501831,2.68064051079619,134.930152264773));
#35102=CARTESIAN_POINT('Ctrl Pts',(143.504568059317,2.79459143912766,134.853827224848));
#35103=CARTESIAN_POINT('Ctrl Pts',(143.496807616802,2.90504768167286,134.772972595287));
#35104=CARTESIAN_POINT('Ctrl Pts',(143.489034716537,3.0156812383844,134.691988170696));
#35105=CARTESIAN_POINT('Ctrl Pts',(143.481261816272,3.12280859307257,134.606459870167));
#35106=CARTESIAN_POINT('Ctrl Pts',(143.473488916006,3.22605359975275,134.516740074737));
#35107=CARTESIAN_POINT('Ctrl Pts',(143.465998580244,3.32554539038173,134.430281819861));
#35108=CARTESIAN_POINT('Ctrl Pts',(143.458508244482,3.4214319745268,134.33993173333));
#35109=CARTESIAN_POINT('Ctrl Pts',(143.45101790872,3.51341145369641,134.24603506753));
#35110=CARTESIAN_POINT('Ctrl Pts',(143.443243574601,3.60887836277513,134.148578281107));
#35111=CARTESIAN_POINT('Ctrl Pts',(143.435469240482,3.70043845300352,134.046991955602));
#35112=CARTESIAN_POINT('Ctrl Pts',(143.427694906363,3.78771334279514,133.941622273104));
#35113=CARTESIAN_POINT('Ctrl Pts',(143.419930153416,3.87488067408505,133.836382449324));
#35114=CARTESIAN_POINT('Ctrl Pts',(143.412165400469,3.95777306581054,133.72736884404));
#35115=CARTESIAN_POINT('Ctrl Pts',(143.404400647521,4.03604838566099,133.614964910437));
#35116=CARTESIAN_POINT('Ctrl Pts',(143.396643606636,4.11424596136026,133.502672618005));
#35117=CARTESIAN_POINT('Ctrl Pts',(143.388886565751,4.18783536903886,133.386997017139));
#35118=CARTESIAN_POINT('Ctrl Pts',(143.381129524866,4.25651448430425,133.268354835783));
#35119=CARTESIAN_POINT('Ctrl Pts',(143.373378333626,4.32514180811459,133.14980212342));
#35120=CARTESIAN_POINT('Ctrl Pts',(143.365627142386,4.38886601481198,133.028287620415));
#35121=CARTESIAN_POINT('Ctrl Pts',(143.357875951146,4.44742829589468,132.904256952001));
#35122=CARTESIAN_POINT('Ctrl Pts',(143.350128054369,4.50596568644573,132.78027899993));
#35123=CARTESIAN_POINT('Ctrl Pts',(143.342380157592,4.55934534841643,132.653787362278));
#35124=CARTESIAN_POINT('Ctrl Pts',(143.334632260815,4.60735455270819,132.525251981987));
#35125=CARTESIAN_POINT('Ctrl Pts',(143.326885984731,4.6553537145094,132.396743488527));
#35126=CARTESIAN_POINT('Ctrl Pts',(143.319139708647,4.69798451639225,132.266192468781));
#35127=CARTESIAN_POINT('Ctrl Pts',(143.311393432563,4.73508264740282,132.13408817792));
#35128=CARTESIAN_POINT('Ctrl Pts',(143.303647099297,4.77218105226334,132.001982911895));
#35129=CARTESIAN_POINT('Ctrl Pts',(143.295900766032,4.80374659905278,131.868324728279));
#35130=CARTESIAN_POINT('Ctrl Pts',(143.288154432767,4.82966517522317,131.733616964188));
#35131=CARTESIAN_POINT('Ctrl Pts',(143.280406364764,4.85558955567897,131.598879033226));
#35132=CARTESIAN_POINT('Ctrl Pts',(143.272658296761,4.87586437525329,131.463091437923));
#35133=CARTESIAN_POINT('Ctrl Pts',(143.264910228758,4.890426920573,131.326766204285));
#35134=CARTESIAN_POINT('Ctrl Pts',(143.257153926016,4.90500494313918,131.190296082565));
#35135=CARTESIAN_POINT('Ctrl Pts',(143.249397623274,4.9138585222347,131.053287570433));
#35136=CARTESIAN_POINT('Ctrl Pts',(143.241641320532,4.91697694674696,130.916256853691));
#35137=CARTESIAN_POINT('Ctrl Pts',(143.233880878018,4.92009703565629,130.779152999529));
#35138=CARTESIAN_POINT('Ctrl Pts',(143.226120435504,4.91747587809979,130.642027307844));
#35139=CARTESIAN_POINT('Ctrl Pts',(143.21835999299,4.90915488546698,130.505393440445));
#35140=CARTESIAN_POINT('Ctrl Pts',(143.210587092724,4.90082053523809,130.368540236233));
#35141=CARTESIAN_POINT('Ctrl Pts',(143.202814192459,4.88676810565601,130.232180823148));
#35142=CARTESIAN_POINT('Ctrl Pts',(143.195041292193,4.86709074877401,130.09682213402));
#35143=CARTESIAN_POINT('Ctrl Pts',(143.187550956431,4.84812871337881,129.966384074189));
#35144=CARTESIAN_POINT('Ctrl Pts',(143.180060620669,4.82394366762322,129.836875546604));
#35145=CARTESIAN_POINT('Ctrl Pts',(143.172570284907,4.79466289860887,129.708737164365));
#35146=CARTESIAN_POINT('Ctrl Pts',(143.164795950788,4.76427194033785,129.575740376418));
#35147=CARTESIAN_POINT('Ctrl Pts',(143.157021616669,4.72829495286353,129.443798389073));
#35148=CARTESIAN_POINT('Ctrl Pts',(143.14924728255,4.68681866449419,129.31341666535));
#35149=CARTESIAN_POINT('Ctrl Pts',(143.141482529603,4.64539349194345,129.18319562545));
#35150=CARTESIAN_POINT('Ctrl Pts',(143.133717776656,4.59848262087887,129.054531392195));
#35151=CARTESIAN_POINT('Ctrl Pts',(143.125953023708,4.54622373045415,128.927919077002));
#35152=CARTESIAN_POINT('Ctrl Pts',(143.118195982823,4.49401674429614,128.801432514945));
#35153=CARTESIAN_POINT('Ctrl Pts',(143.110438941938,4.43647245755512,128.676994174302));
#35154=CARTESIAN_POINT('Ctrl Pts',(143.102681901054,4.37377816964122,128.555083492517));
#35155=CARTESIAN_POINT('Ctrl Pts',(143.094930709813,4.31113115997752,128.433264744525));
#35156=CARTESIAN_POINT('Ctrl Pts',(143.087179518573,4.24334205740033,128.313970207636));
#35157=CARTESIAN_POINT('Ctrl Pts',(143.079428327333,4.17064588672128,128.197658496096));
#35158=CARTESIAN_POINT('Ctrl Pts',(143.071680430556,4.09798061385399,128.081396220136));
#35159=CARTESIAN_POINT('Ctrl Pts',(143.063932533779,4.02041262783363,127.968114578849));
#35160=CARTESIAN_POINT('Ctrl Pts',(143.056184637002,3.93822231969323,127.858246562888));
#35161=CARTESIAN_POINT('Ctrl Pts',(143.048438360918,3.85604920399347,127.748401528948));
#35162=CARTESIAN_POINT('Ctrl Pts',(143.040692084834,3.76925592341749,127.641969012899));
#35163=CARTESIAN_POINT('Ctrl Pts',(143.03294580875,3.67816528811141,127.539351708569));
#35164=CARTESIAN_POINT('Ctrl Pts',(143.025199475484,3.58707398039498,127.436733646741));
#35165=CARTESIAN_POINT('Ctrl Pts',(143.017453142219,3.49168551419383,127.337931145218));
#35166=CARTESIAN_POINT('Ctrl Pts',(143.009706808953,3.39236168065779,127.243312276122));
#35167=CARTESIAN_POINT('Ctrl Pts',(143.00195874095,3.29301560423786,127.148672217786));
#35168=CARTESIAN_POINT('Ctrl Pts',(142.994210672948,3.18973268982494,127.058217925808));
#35169=CARTESIAN_POINT('Ctrl Pts',(142.986462604945,3.08290982128859,126.972278925287));
#35170=CARTESIAN_POINT('Ctrl Pts',(142.978706302203,2.97597342013635,126.886248587773));
#35171=CARTESIAN_POINT('Ctrl Pts',(142.970949999461,2.86548985435889,126.804743373508));
#35172=CARTESIAN_POINT('Ctrl Pts',(142.963193696719,2.75188761607232,126.728051305086));
#35173=CARTESIAN_POINT('Ctrl Pts',(142.955433254205,2.63822474485057,126.651318303799));
#35174=CARTESIAN_POINT('Ctrl Pts',(142.947672811691,2.52144021714982,126.579403772049));
#35175=CARTESIAN_POINT('Ctrl Pts',(142.939912369176,2.40198857506541,126.512550516017));
#35176=CARTESIAN_POINT('Ctrl Pts',(142.932139468911,2.28234517860079,126.445589941204));
#35177=CARTESIAN_POINT('Ctrl Pts',(142.924366568646,2.16002646103501,126.383707054661));
#35178=CARTESIAN_POINT('Ctrl Pts',(142.91659366838,2.03550927027305,126.327097494504));
#35179=CARTESIAN_POINT('Ctrl Pts',(142.909103332618,1.91551859303516,126.272545834449));
#35180=CARTESIAN_POINT('Ctrl Pts',(142.901612996856,1.79348679292343,126.222890875819));
#35181=CARTESIAN_POINT('Ctrl Pts',(142.894122661094,1.6698533720046,126.178263690511));
#35182=CARTESIAN_POINT('Ctrl Pts',(142.886348326975,1.54153235235402,126.131944451909));
#35183=CARTESIAN_POINT('Ctrl Pts',(142.878573992856,1.41107938109231,126.09089504337));
#35184=CARTESIAN_POINT('Ctrl Pts',(142.870799658737,1.27896659734406,126.055315713022));
#35185=CARTESIAN_POINT('Ctrl Pts',(142.86303490579,1.14701663079471,126.019780231019));
#35186=CARTESIAN_POINT('Ctrl Pts',(142.855270152843,1.01341129572504,125.989701514557));
#35187=CARTESIAN_POINT('Ctrl Pts',(142.847505399896,0.878641562336831,125.965231350081));
#35188=CARTESIAN_POINT('Ctrl Pts',(142.839748359011,0.744005684147697,125.940785489716));
#35189=CARTESIAN_POINT('Ctrl Pts',(142.831991318126,0.608208091307349,125.921937165197));
#35190=CARTESIAN_POINT('Ctrl Pts',(142.824234277241,0.471753388020811,125.908787943875));
#35191=CARTESIAN_POINT('Ctrl Pts',(142.816483086,0.335401586287345,125.895648638482));
#35192=CARTESIAN_POINT('Ctrl Pts',(142.80873189476,0.198394048022155,125.888199919248));
#35193=CARTESIAN_POINT('Ctrl Pts',(142.80098070352,0.0612436550299411,125.886491945344));
#35194=CARTESIAN_POINT('Ctrl Pts',(142.793232806743,-0.0758484453865517,
125.884784697375));
#35195=CARTESIAN_POINT('Ctrl Pts',(142.785484909966,-0.213082889652012,
125.888813346679));
#35196=CARTESIAN_POINT('Ctrl Pts',(142.777737013189,-0.349943832263288,
125.898576034366));
#35197=CARTESIAN_POINT('Ctrl Pts',(142.769990737105,-0.48677614651575,125.908336679909));
#35198=CARTESIAN_POINT('Ctrl Pts',(142.762244461021,-0.62323472478866,125.923828950288));
#35199=CARTESIAN_POINT('Ctrl Pts',(142.754498184937,-0.758806282589974,
125.944998922034));
#35200=CARTESIAN_POINT('Ctrl Pts',(142.746751851671,-0.89437884114973,125.966169050053));
#35201=CARTESIAN_POINT('Ctrl Pts',(142.739005518406,-1.02906397988825,125.993016902751));
#35202=CARTESIAN_POINT('Ctrl Pts',(142.731259185141,-1.1623564723501,126.025437046961));
#35203=CARTESIAN_POINT('Ctrl Pts',(142.723511117138,-1.29567881474137,126.057864451438));
#35204=CARTESIAN_POINT('Ctrl Pts',(142.715763049135,-1.4276075104468,126.095866538174));
#35205=CARTESIAN_POINT('Ctrl Pts',(142.708014981132,-1.55765079524142,126.139287513896));
#35206=CARTESIAN_POINT('Ctrl Pts',(142.70025867839,-1.68783229158674,126.182754637948));
#35207=CARTESIAN_POINT('Ctrl Pts',(142.692502375648,-1.81612400270989,126.231652031708));
#35208=CARTESIAN_POINT('Ctrl Pts',(142.684746072906,-1.94205199658775,126.285774875871));
#35209=CARTESIAN_POINT('Ctrl Pts',(142.676985630392,-2.06804720202769,126.339926607026));
#35210=CARTESIAN_POINT('Ctrl Pts',(142.669225187878,-2.191675824157,126.399309176669));
#35211=CARTESIAN_POINT('Ctrl Pts',(142.661464745364,-2.31248789215451,126.463671408335));
#35212=CARTESIAN_POINT('Ctrl Pts',(142.653691845098,-2.43349389840871,126.528136959968));
#35213=CARTESIAN_POINT('Ctrl Pts',(142.645918944833,-2.55167397811675,126.597597949552));
#35214=CARTESIAN_POINT('Ctrl Pts',(142.638146044567,-2.66660578745136,126.67175893862));
#35215=CARTESIAN_POINT('Ctrl Pts',(142.630655708805,-2.7773595360207,126.743223988934));
#35216=CARTESIAN_POINT('Ctrl Pts',(142.623165373043,-2.88509682777075,126.819053080459));
#35217=CARTESIAN_POINT('Ctrl Pts',(142.615675037281,-2.98946982659814,126.89894729522));
#35218=CARTESIAN_POINT('Ctrl Pts',(142.607950349053,-3.09710837592991,126.981341185148));
#35219=CARTESIAN_POINT('Ctrl Pts',(142.600225660824,-3.2015278714696,127.06833394483));
#35220=CARTESIAN_POINT('Ctrl Pts',(142.592500972595,-3.30230372306345,127.159642084793));
#35221=CARTESIAN_POINT('Ctrl Pts',(142.584823606184,-3.40246221687705,127.250390866638));
#35222=CARTESIAN_POINT('Ctrl Pts',(142.577146239772,-3.49902125553019,127.345402067541));
#35223=CARTESIAN_POINT('Ctrl Pts',(142.56946887336,-3.59159267859491,127.444353907221));
#35224=CARTESIAN_POINT('Ctrl Pts',(142.561798511355,-3.68407964457878,127.543215468679));
#35225=CARTESIAN_POINT('Ctrl Pts',(142.55412814935,-3.77258595742159,127.646010229757));
#35226=CARTESIAN_POINT('Ctrl Pts',(142.546457787346,-3.85675795738575,127.752377472029));
#35227=CARTESIAN_POINT('Ctrl Pts',(142.53879267214,-3.94087238072502,127.858671955345));
#35228=CARTESIAN_POINT('Ctrl Pts',(142.531127556934,-4.02065814070938,127.968533746617));
#35229=CARTESIAN_POINT('Ctrl Pts',(142.523462441729,-4.09580012770525,128.081567129916));
#35230=CARTESIAN_POINT('Ctrl Pts',(142.515697448234,-4.17192123280728,128.1960733653));
#35231=CARTESIAN_POINT('Ctrl Pts',(142.50793245474,-4.243276407309,128.313834122567));
#35232=CARTESIAN_POINT('Ctrl Pts',(142.500167461245,-4.30958178691302,128.434405368113));
#35233=CARTESIAN_POINT('Ctrl Pts',(142.492506496131,-4.37499886683234,128.553361308838));
#35234=CARTESIAN_POINT('Ctrl Pts',(142.484845531017,-4.43550044605301,128.675052525963));
#35235=CARTESIAN_POINT('Ctrl Pts',(142.477184565903,-4.49085929893384,128.799026276445));
#35236=CARTESIAN_POINT('Ctrl Pts',(142.469367558218,-4.54734573007758,128.925525189551));
#35237=CARTESIAN_POINT('Ctrl Pts',(142.461550550533,-4.59847746135096,129.054400245879));
#35238=CARTESIAN_POINT('Ctrl Pts',(142.453733542848,-4.64406441275163,129.185148218678));
#35239=CARTESIAN_POINT('Ctrl Pts',(142.445916535164,-4.68965136415229,129.315896191477));
#35240=CARTESIAN_POINT('Ctrl Pts',(142.438099527479,-4.72969341376038,129.448516655478));
#35241=CARTESIAN_POINT('Ctrl Pts',(142.430282519794,-4.76405452823406,129.582490119308));
#35242=CARTESIAN_POINT('Origin',(213.235140564004,0.,130.804360617566));
#35243=CARTESIAN_POINT('',(140.334586805861,-4.76405452823407,129.582490119308));
#35244=CARTESIAN_POINT('',(140.680140489264,-4.76405452823406,129.582490119308));
#35245=CARTESIAN_POINT('',(213.235140564004,-4.76405452823405,129.582490119308));
#35246=CARTESIAN_POINT('',(142.01485943596,-4.91824791031056,130.799826830428));
#35247=CARTESIAN_POINT('Ctrl Pts',(142.01485943596,-4.91824791031056,130.799826830428));
#35248=CARTESIAN_POINT('Ctrl Pts',(142.007204362131,-4.9183724598586,130.93493805991));
#35249=CARTESIAN_POINT('Ctrl Pts',(141.999549288301,-4.91292527910308,131.070210728423));
#35250=CARTESIAN_POINT('Ctrl Pts',(141.991894214472,-4.90189328219073,131.205141495994));
#35251=CARTESIAN_POINT('Ctrl Pts',(141.983895337286,-4.89036581813378,131.34613225095));
#35252=CARTESIAN_POINT('Ctrl Pts',(141.975896460099,-4.87274017314778,131.486749237213));
#35253=CARTESIAN_POINT('Ctrl Pts',(141.967897582913,-4.8490622793132,131.626417838106));
#35254=CARTESIAN_POINT('Ctrl Pts',(141.960251120509,-4.82642758686816,131.759932915398));
#35255=CARTESIAN_POINT('Ctrl Pts',(141.952604658105,-4.79826264535518,131.892580951809));
#35256=CARTESIAN_POINT('Ctrl Pts',(141.9449581957,-4.76466051954016,132.023865925482));
#35257=CARTESIAN_POINT('Ctrl Pts',(141.937312894906,-4.73106349838228,132.155130955036));
#35258=CARTESIAN_POINT('Ctrl Pts',(141.929667594112,-4.69203103485191,132.285032944037));
#35259=CARTESIAN_POINT('Ctrl Pts',(141.922022293318,-4.64770690713896,132.413087930641));
#35260=CARTESIAN_POINT('Ctrl Pts',(141.914376395698,-4.60337931929056,132.541152913777));
#35261=CARTESIAN_POINT('Ctrl Pts',(141.906730498079,-4.55375937765899,132.667370227804));
#35262=CARTESIAN_POINT('Ctrl Pts',(141.899084600459,-4.49903996263695,132.791273418143));
#35263=CARTESIAN_POINT('Ctrl Pts',(141.891436347327,-4.44430368991786,132.915214779987));
#35264=CARTESIAN_POINT('Ctrl Pts',(141.883788094196,-4.38446498243226,133.036840232908));
#35265=CARTESIAN_POINT('Ctrl Pts',(141.876139841064,-4.31976361211479,133.155706061764));
#35266=CARTESIAN_POINT('Ctrl Pts',(141.868483341257,-4.25499247799666,133.274700056869));
#35267=CARTESIAN_POINT('Ctrl Pts',(141.86082684145,-4.18534840864223,133.390928135706));
#35268=CARTESIAN_POINT('Ctrl Pts',(141.853170341643,-4.11111575725234,133.503973607046));
#35269=CARTESIAN_POINT('Ctrl Pts',(141.845508990916,-4.03683607435818,133.617090700489));
#35270=CARTESIAN_POINT('Ctrl Pts',(141.837847640188,-3.95796225631683,133.727020847084));
#35271=CARTESIAN_POINT('Ctrl Pts',(141.83018628946,-3.87481940199019,133.833379875422));
#35272=CARTESIAN_POINT('Ctrl Pts',(141.82251410854,-3.79155901575509,133.939889254378));
#35273=CARTESIAN_POINT('Ctrl Pts',(141.814841927619,-3.70401781001808,134.042817136548));
#35274=CARTESIAN_POINT('Ctrl Pts',(141.807169746698,-3.61255838303633,134.141815484924));
#35275=CARTESIAN_POINT('Ctrl Pts',(141.804753551799,-3.58375512576284,134.172992969762));
#35276=CARTESIAN_POINT('Ctrl Pts',(141.8023373569,-3.55456350779432,134.20378101864));
#35277=CARTESIAN_POINT('Ctrl Pts',(141.799921162002,-3.52499552010276,134.234169598509));
#35278=CARTESIAN_POINT('Ctrl Pts',(141.792146827883,-3.42985774141342,134.331947709633));
#35279=CARTESIAN_POINT('Ctrl Pts',(141.784372493764,-3.33049785996596,134.425919224525));
#35280=CARTESIAN_POINT('Ctrl Pts',(141.776598159645,-3.22725287804554,134.515697563149));
#35281=CARTESIAN_POINT('Ctrl Pts',(141.768833406697,-3.12413513633827,134.605365257993));
#35282=CARTESIAN_POINT('Ctrl Pts',(141.76106865375,-3.01714211312096,134.690849804701));
#35283=CARTESIAN_POINT('Ctrl Pts',(141.753303900803,-2.90664894092162,134.771799967668));
#35284=CARTESIAN_POINT('Ctrl Pts',(141.745546859918,-2.7962655120984,134.852669729792));
#35285=CARTESIAN_POINT('Ctrl Pts',(141.737789819033,-2.6823891658225,134.929013841008));
#35286=CARTESIAN_POINT('Ctrl Pts',(141.730032778148,-2.56542925988115,135.000520263605));
#35287=CARTESIAN_POINT('Ctrl Pts',(141.722281586908,-2.44855755431465,135.071972762653));
#35288=CARTESIAN_POINT('Ctrl Pts',(141.714530395668,-2.32860724973823,135.138594631373));
#35289=CARTESIAN_POINT('Ctrl Pts',(141.706779204428,-2.20601763236454,135.200116442017));
#35290=CARTESIAN_POINT('Ctrl Pts',(141.699031307651,-2.08348011884859,135.261612104251));
#35291=CARTESIAN_POINT('Ctrl Pts',(141.691283410874,-1.95830587236612,135.318011844726));
#35292=CARTESIAN_POINT('Ctrl Pts',(141.683535514097,-1.83095959561589,135.369091718269));
#35293=CARTESIAN_POINT('Ctrl Pts',(141.675789238013,-1.70363995696132,135.420160907003));
#35294=CARTESIAN_POINT('Ctrl Pts',(141.668042961928,-1.57414955438306,135.465912296774));
#35295=CARTESIAN_POINT('Ctrl Pts',(141.660296685844,-1.44297355914704,135.506169883168));
#35296=CARTESIAN_POINT('Ctrl Pts',(141.652550352579,-1.31179659559975,135.546427766735));
#35297=CARTESIAN_POINT('Ctrl Pts',(141.644804019314,-1.178934388326,135.581191651297));
#35298=CARTESIAN_POINT('Ctrl Pts',(141.637057686048,-1.04488739110477,135.610335378466));
#35299=CARTESIAN_POINT('Ctrl Pts',(141.629309618045,-0.910810374987649,
135.639485632171));
#35300=CARTESIAN_POINT('Ctrl Pts',(141.621561550042,-0.775548422923046,
135.663013140978));
#35301=CARTESIAN_POINT('Ctrl Pts',(141.613813482039,-0.639611908517401,
135.680842922361));
#35302=CARTESIAN_POINT('Ctrl Pts',(141.606057179298,-0.503530919166858,
135.698691653449));
#35303=CARTESIAN_POINT('Ctrl Pts',(141.598300876556,-0.366774323587707,
135.710830509449));
#35304=CARTESIAN_POINT('Ctrl Pts',(141.590544573814,-0.229857901895721,
135.717236395299));
#35305=CARTESIAN_POINT('Ctrl Pts',(141.5827841313,-0.0928684037868652,135.723645700163));
#35306=CARTESIAN_POINT('Ctrl Pts',(141.575023688786,0.0442806996410358,
135.724315935938));
#35307=CARTESIAN_POINT('Ctrl Pts',(141.567263246271,0.181074900741475,135.719276175622));
#35308=CARTESIAN_POINT('Ctrl Pts',(141.559490346006,0.318088696037493,135.714228325035));
#35309=CARTESIAN_POINT('Ctrl Pts',(141.551717445741,0.45474606054288,135.703452192135));
#35310=CARTESIAN_POINT('Ctrl Pts',(141.543944545475,0.590537972021914,135.68702873716));
#35311=CARTESIAN_POINT('Ctrl Pts',(141.536454209713,0.721393505480238,135.671202316141));
#35312=CARTESIAN_POINT('Ctrl Pts',(141.528963873951,0.851445112221208,135.650132082649));
#35313=CARTESIAN_POINT('Ctrl Pts',(141.521473538189,0.980249251491861,135.62393471363));
#35314=CARTESIAN_POINT('Ctrl Pts',(141.51369920407,1.11393703885156,135.596744063402));
#35315=CARTESIAN_POINT('Ctrl Pts',(141.505924869951,1.24670437866469,135.563943680303));
#35316=CARTESIAN_POINT('Ctrl Pts',(141.498150535832,1.37804387223028,135.525608137948));
#35317=CARTESIAN_POINT('Ctrl Pts',(141.490385782885,1.50922150160793,135.487319840722));
#35318=CARTESIAN_POINT('Ctrl Pts',(141.482621029937,1.63897441430036,135.443510065661));
#35319=CARTESIAN_POINT('Ctrl Pts',(141.47485627699,1.76680433755179,135.394304570961));
#35320=CARTESIAN_POINT('Ctrl Pts',(141.467099236105,1.89450729832135,135.345147947853));
#35321=CARTESIAN_POINT('Ctrl Pts',(141.45934219522,2.02029070801094,135.290606409506));
#35322=CARTESIAN_POINT('Ctrl Pts',(141.451585154335,2.14367077257473,135.230855696216));
#35323=CARTESIAN_POINT('Ctrl Pts',(141.443833963095,2.2669577952725,135.171150041403));
#35324=CARTESIAN_POINT('Ctrl Pts',(141.436082771855,2.38784472982894,135.106243200366));
#35325=CARTESIAN_POINT('Ctrl Pts',(141.428331580615,2.50586745412087,135.036359124758));
#35326=CARTESIAN_POINT('Ctrl Pts',(141.420583683838,2.62384001560638,134.966504751747));
#35327=CARTESIAN_POINT('Ctrl Pts',(141.412835787061,2.7389504523662,134.891677550429));
#35328=CARTESIAN_POINT('Ctrl Pts',(141.405087890284,2.85075916982444,134.81214744051));
#35329=CARTESIAN_POINT('Ctrl Pts',(141.397341614199,2.96254449930937,134.732633966575));
#35330=CARTESIAN_POINT('Ctrl Pts',(141.389595338115,3.07102916484228,134.648419767238));
#35331=CARTESIAN_POINT('Ctrl Pts',(141.381849062031,3.1758028420069,134.559817896141));
#35332=CARTESIAN_POINT('Ctrl Pts',(141.374102728766,3.28057729258664,134.471215371005));
#35333=CARTESIAN_POINT('Ctrl Pts',(141.366356395501,3.38164040160441,134.378225361934));
#35334=CARTESIAN_POINT('Ctrl Pts',(141.358610062235,3.47861552094251,134.281200723173));
#35335=CARTESIAN_POINT('Ctrl Pts',(141.350861994232,3.57561235718655,134.184154356417));
#35336=CARTESIAN_POINT('Ctrl Pts',(141.343113926229,3.66851910572709,134.083071838529));
#35337=CARTESIAN_POINT('Ctrl Pts',(141.335365858226,3.75699681224093,133.978342031392));
#35338=CARTESIAN_POINT('Ctrl Pts',(141.327609555484,3.8455685539141,133.873500916169));
#35339=CARTESIAN_POINT('Ctrl Pts',(141.319853252742,3.92970159763366,133.765005067337));
#35340=CARTESIAN_POINT('Ctrl Pts',(141.312096950001,4.00909772111698,133.653275941867));
#35341=CARTESIAN_POINT('Ctrl Pts',(141.304336507486,4.08853622070192,133.541487183198));
#35342=CARTESIAN_POINT('Ctrl Pts',(141.296576064972,4.16323254949747,133.426462037028));
#35343=CARTESIAN_POINT('Ctrl Pts',(141.288815622458,4.23293306348885,133.308649087875));
#35344=CARTESIAN_POINT('Ctrl Pts',(141.281042722193,4.30274546693306,133.190647014917));
#35345=CARTESIAN_POINT('Ctrl Pts',(141.273269821927,4.36754584468517,133.069848540767));
#35346=CARTESIAN_POINT('Ctrl Pts',(141.265496921662,4.42712717193409,132.946725681233));
#35347=CARTESIAN_POINT('Ctrl Pts',(141.2580065859,4.4845425678604,132.828078647773));
#35348=CARTESIAN_POINT('Ctrl Pts',(141.250516250138,4.53711165381283,132.7072735719));
#35349=CARTESIAN_POINT('Ctrl Pts',(141.243025914376,4.58469284879999,132.58474668375));
#35350=CARTESIAN_POINT('Ctrl Pts',(141.235251580257,4.63407809925764,132.457574151393));
#35351=CARTESIAN_POINT('Ctrl Pts',(141.227477246138,4.67824619819302,132.328143819984));
#35352=CARTESIAN_POINT('Ctrl Pts',(141.219702912019,4.7169856251077,132.196922887279));
#35353=CARTESIAN_POINT('Ctrl Pts',(141.211938159072,4.75567730914099,132.065863672646));
#35354=CARTESIAN_POINT('Ctrl Pts',(141.204173406125,4.78895352332623,131.93301861887));
#35355=CARTESIAN_POINT('Ctrl Pts',(141.196408653177,4.81665074300047,131.798874912311));
#35356=CARTESIAN_POINT('Ctrl Pts',(141.188651612292,4.84432045340566,131.664864439173));
#35357=CARTESIAN_POINT('Ctrl Pts',(141.180894571408,4.86642211786545,131.529558260502));
#35358=CARTESIAN_POINT('Ctrl Pts',(141.173137530523,4.88284208916889,131.393458397854));
#35359=CARTESIAN_POINT('Ctrl Pts',(141.165386339282,4.8992496780443,131.257461169171));
#35360=CARTESIAN_POINT('Ctrl Pts',(141.157635148042,4.9099840553782,131.120671834415));
#35361=CARTESIAN_POINT('Ctrl Pts',(141.149883956802,4.91498276869447,130.983601924012));
#35362=CARTESIAN_POINT('Ctrl Pts',(141.142136060025,4.91997935742423,130.846590271977));
#35363=CARTESIAN_POINT('Ctrl Pts',(141.134388163248,4.91924511653648,130.709298671366));
#35364=CARTESIAN_POINT('Ctrl Pts',(141.126640266471,4.91276952551801,130.572242863739));
#35365=CARTESIAN_POINT('Ctrl Pts',(141.118893990387,4.90629528905358,130.435215725233));
#35366=CARTESIAN_POINT('Ctrl Pts',(141.111147714303,4.89408210968696,130.298424671887));
#35367=CARTESIAN_POINT('Ctrl Pts',(141.103401438219,4.87617157794461,130.162384134395));
#35368=CARTESIAN_POINT('Ctrl Pts',(141.095655104953,4.85826091399083,130.026342592682));
#35369=CARTESIAN_POINT('Ctrl Pts',(141.087908771688,4.834652864773,129.8910519655));
#35370=CARTESIAN_POINT('Ctrl Pts',(141.080162438423,4.80544070905459,129.757019863914));
#35371=CARTESIAN_POINT('Ctrl Pts',(141.07241437042,4.7762220114765,129.622957746768));
#35372=CARTESIAN_POINT('Ctrl Pts',(141.064666302417,4.74139679333162,129.49015509797));
#35373=CARTESIAN_POINT('Ctrl Pts',(141.056918234414,4.70110900204418,129.359107278736));
#35374=CARTESIAN_POINT('Ctrl Pts',(141.049161931672,4.6607783924126,129.22792018032));
#35375=CARTESIAN_POINT('Ctrl Pts',(141.04140562893,4.61497372722213,129.098492011415));
#35376=CARTESIAN_POINT('Ctrl Pts',(141.033649326188,4.56388839373205,128.971301482661));
#35377=CARTESIAN_POINT('Ctrl Pts',(141.025888883674,4.5127757944613,128.844043068493));
#35378=CARTESIAN_POINT('Ctrl Pts',(141.01812844116,4.45637707158025,128.719025030416));
#35379=CARTESIAN_POINT('Ctrl Pts',(141.010367998646,4.39493253116425,128.596703237216));
#35380=CARTESIAN_POINT('Ctrl Pts',(141.00259509838,4.33338935451723,128.474185082214));
#35381=CARTESIAN_POINT('Ctrl Pts',(140.994822198115,4.26678436403662,128.354372163224));
#35382=CARTESIAN_POINT('Ctrl Pts',(140.987049297849,4.19540277802365,128.237693792158));
#35383=CARTESIAN_POINT('Ctrl Pts',(140.979558962087,4.12661609246075,128.125256973773));
#35384=CARTESIAN_POINT('Ctrl Pts',(140.972068626325,4.05339423577779,128.015731018587));
#35385=CARTESIAN_POINT('Ctrl Pts',(140.964578290563,3.9760276927594,127.909470835742));
#35386=CARTESIAN_POINT('Ctrl Pts',(140.956803956444,3.89572777374833,127.799181765768));
#35387=CARTESIAN_POINT('Ctrl Pts',(140.949029622325,3.81070830661618,127.692061637589));
#35388=CARTESIAN_POINT('Ctrl Pts',(140.941255288206,3.72124802607181,127.588540941192));
#35389=CARTESIAN_POINT('Ctrl Pts',(140.933490535259,3.63189799732804,127.485147824801));
#35390=CARTESIAN_POINT('Ctrl Pts',(140.925725782312,3.53811829780334,127.385345606889));
#35391=CARTESIAN_POINT('Ctrl Pts',(140.917961029364,3.4402304221042,127.289535201513));
#35392=CARTESIAN_POINT('Ctrl Pts',(140.910203988479,3.34243977002346,127.193819956384));
#35393=CARTESIAN_POINT('Ctrl Pts',(140.902446947594,3.24054933934156,127.102088905514));
#35394=CARTESIAN_POINT('Ctrl Pts',(140.89468990671,3.13492006591731,127.014709018433));
#35395=CARTESIAN_POINT('Ctrl Pts',(140.886938715469,3.02937044834976,126.927395025205));
#35396=CARTESIAN_POINT('Ctrl Pts',(140.879187524229,2.92008790009538,126.844425912841));
#35397=CARTESIAN_POINT('Ctrl Pts',(140.871436332989,2.80746902909971,126.766130719065));
#35398=CARTESIAN_POINT('Ctrl Pts',(140.863688436212,2.69489802412811,126.687868802836));
#35399=CARTESIAN_POINT('Ctrl Pts',(140.855940539435,2.57899383709904,126.614277076825));
#35400=CARTESIAN_POINT('Ctrl Pts',(140.848192642658,2.46018468939969,126.54564316315));
#35401=CARTESIAN_POINT('Ctrl Pts',(140.840446366574,2.34140039401272,126.477023606211));
#35402=CARTESIAN_POINT('Ctrl Pts',(140.83270009049,2.21971268493754,126.413359994267));
#35403=CARTESIAN_POINT('Ctrl Pts',(140.824953814406,2.09557684798133,126.354895398385));
#35404=CARTESIAN_POINT('Ctrl Pts',(140.81720748114,1.9714400946824,126.29643037093));
#35405=CARTESIAN_POINT('Ctrl Pts',(140.809461147875,1.84485553114223,126.243164602702));
#35406=CARTESIAN_POINT('Ctrl Pts',(140.801714814609,1.71630064437875,126.195293991816));
#35407=CARTESIAN_POINT('Ctrl Pts',(140.793966746606,1.58771696863963,126.147412660638));
#35408=CARTESIAN_POINT('Ctrl Pts',(140.786218678603,1.45716245797747,126.104929027404));
#35409=CARTESIAN_POINT('Ctrl Pts',(140.7784706106,1.32513168091329,126.067989739907));
#35410=CARTESIAN_POINT('Ctrl Pts',(140.770714307859,1.19296057996833,126.031011192895));
#35411=CARTESIAN_POINT('Ctrl Pts',(140.762958005117,1.05931045549533,125.999588868223));
#35412=CARTESIAN_POINT('Ctrl Pts',(140.755201702375,0.924688590851678,125.973818818508));
#35413=CARTESIAN_POINT('Ctrl Pts',(140.747441259861,0.789994874465482,125.948035014541));
#35414=CARTESIAN_POINT('Ctrl Pts',(140.739680817347,0.654328771004443,125.92790955408));
#35415=CARTESIAN_POINT('Ctrl Pts',(140.731920374832,0.518203707090394,125.913486669031));
#35416=CARTESIAN_POINT('Ctrl Pts',(140.724147474567,0.381860123139134,125.899040631087));
#35417=CARTESIAN_POINT('Ctrl Pts',(140.716374574301,0.245056496842509,125.890315486622));
#35418=CARTESIAN_POINT('Ctrl Pts',(140.708601674036,0.108308187928903,125.887303326978));
#35419=CARTESIAN_POINT('Ctrl Pts',(140.701111338274,-0.0234689755073049,
125.884400666923));
#35420=CARTESIAN_POINT('Ctrl Pts',(140.693621002512,-0.155194465620334,
125.886802834603));
#35421=CARTESIAN_POINT('Ctrl Pts',(140.68613066675,-0.286412673175626,125.894457274002));
#35422=CARTESIAN_POINT('Ctrl Pts',(140.678356332631,-0.422606058953481,
125.902401933796));
#35423=CARTESIAN_POINT('Ctrl Pts',(140.670581998512,-0.558684355290657,
125.916030173536));
#35424=CARTESIAN_POINT('Ctrl Pts',(140.662807664393,-0.694134715851532,
125.935340176168));
#35425=CARTESIAN_POINT('Ctrl Pts',(140.655042911446,-0.829418145948654,
125.954626380948));
#35426=CARTESIAN_POINT('Ctrl Pts',(140.647278158498,-0.964074796713364,
125.979580361551));
#35427=CARTESIAN_POINT('Ctrl Pts',(140.639513405551,-1.09759359210719,126.010148339301));
#35428=CARTESIAN_POINT('Ctrl Pts',(140.631756364666,-1.23097977475124,126.040685956505));
#35429=CARTESIAN_POINT('Ctrl Pts',(140.623999323781,-1.36322997240307,126.076826387874));
#35430=CARTESIAN_POINT('Ctrl Pts',(140.616242282896,-1.49384034855565,126.118464323843));
#35431=CARTESIAN_POINT('Ctrl Pts',(140.608491091656,-1.62435223040652,126.160070860321));
#35432=CARTESIAN_POINT('Ctrl Pts',(140.600739900416,-1.7532263811522,126.207166531343));
#35433=CARTESIAN_POINT('Ctrl Pts',(140.592988709176,-1.87997159575207,126.259595512342));
#35434=CARTESIAN_POINT('Ctrl Pts',(140.585240812399,-2.00666294025565,126.312002209625));
#35435=CARTESIAN_POINT('Ctrl Pts',(140.577492915622,-2.13122678778079,126.369737559263));
#35436=CARTESIAN_POINT('Ctrl Pts',(140.569745018845,-2.25318968957502,126.432596753255));
#35437=CARTESIAN_POINT('Ctrl Pts',(140.561998742761,-2.37512707935907,126.495442798459));
#35438=CARTESIAN_POINT('Ctrl Pts',(140.554252466677,-2.49446425827756,126.563410377152));
#35439=CARTESIAN_POINT('Ctrl Pts',(140.546506190592,-2.6107506306574,126.636247830342));
#35440=CARTESIAN_POINT('Ctrl Pts',(140.538759857327,-2.72703786143737,126.709085821201));
#35441=CARTESIAN_POINT('Ctrl Pts',(140.531013524062,-2.84027390940619,126.786793550753));
#35442=CARTESIAN_POINT('Ctrl Pts',(140.523267190796,-2.95003586653442,126.869075183362));
#35443=CARTESIAN_POINT('Ctrl Pts',(140.515519122793,-3.05982240409213,126.951375242372));
#35444=CARTESIAN_POINT('Ctrl Pts',(140.50777105479,-3.16613298991541,127.038251008205));
#35445=CARTESIAN_POINT('Ctrl Pts',(140.500022986787,-3.26857691869624,127.129365653071));
#35446=CARTESIAN_POINT('Ctrl Pts',(140.492266684045,-3.37112972610326,127.220577135665));
#35447=CARTESIAN_POINT('Ctrl Pts',(140.484510381304,-3.46980737463951,127.316036236534));
#35448=CARTESIAN_POINT('Ctrl Pts',(140.476754078562,-3.56425485347275,127.415368082609));
#35449=CARTESIAN_POINT('Ctrl Pts',(140.468993636048,-3.65875274176908,127.51475294508));
#35450=CARTESIAN_POINT('Ctrl Pts',(140.461233193533,-3.74901570438674,127.618014377215));
#35451=CARTESIAN_POINT('Ctrl Pts',(140.453472751019,-3.83472900814064,127.72474432708));
#35452=CARTESIAN_POINT('Ctrl Pts',(140.445699850754,-3.92057990649899,127.831645609336));
#35453=CARTESIAN_POINT('Ctrl Pts',(140.437926950488,-4.00186631927342,127.942026220913));
#35454=CARTESIAN_POINT('Ctrl Pts',(140.430154050223,-4.07831633572203,128.055448300252));
#35455=CARTESIAN_POINT('Ctrl Pts',(140.422663714461,-4.15198720150614,128.164747201312));
#35456=CARTESIAN_POINT('Ctrl Pts',(140.415173378699,-4.22116703478364,128.27687001711));
#35457=CARTESIAN_POINT('Ctrl Pts',(140.407683042937,-4.28565378449886,128.391405022883));
#35458=CARTESIAN_POINT('Ctrl Pts',(140.399553936778,-4.3556399174246,128.515707490818));
#35459=CARTESIAN_POINT('Ctrl Pts',(140.391424830619,-4.42030332323987,128.643214966403));
#35460=CARTESIAN_POINT('Ctrl Pts',(140.38329572446,-4.47935262289568,128.773453642282));
#35461=CARTESIAN_POINT('Ctrl Pts',(140.37517757136,-4.53832236023881,128.903516836143));
#35462=CARTESIAN_POINT('Ctrl Pts',(140.36705941826,-4.59169291274071,129.036303595815));
#35463=CARTESIAN_POINT('Ctrl Pts',(140.35894126516,-4.63921774360707,129.17131383627));
#35464=CARTESIAN_POINT('Ctrl Pts',(140.350823112061,-4.68674257447341,129.306324076725));
#35465=CARTESIAN_POINT('Ctrl Pts',(140.342704958961,-4.72842150515073,129.443557503113));
#35466=CARTESIAN_POINT('Ctrl Pts',(140.334586805861,-4.76405452823407,129.582490119308));
#35467=CARTESIAN_POINT('Ctrl Pts',(142.084824010153,-4.76405452823403,129.582490119308));
#35468=CARTESIAN_POINT('Ctrl Pts',(142.082672268707,-4.77344323938914,129.619096561608));
#35469=CARTESIAN_POINT('Ctrl Pts',(142.080520527261,-4.78240609402808,129.655795966851));
#35470=CARTESIAN_POINT('Ctrl Pts',(142.078368785814,-4.79094161432327,129.692577585385));
#35471=CARTESIAN_POINT('Ctrl Pts',(142.067783894177,-4.83292972472065,129.873514494464));
#35472=CARTESIAN_POINT('Ctrl Pts',(142.05719900254,-4.86468194816004,130.056909269468));
#35473=CARTESIAN_POINT('Ctrl Pts',(142.046614110902,-4.88596847754098,130.241781646242));
#35474=CARTESIAN_POINT('Ctrl Pts',(142.036029219265,-4.90725500692191,130.426654023016));
#35475=CARTESIAN_POINT('Ctrl Pts',(142.025444327628,-4.91807569203257,130.613004631307));
#35476=CARTESIAN_POINT('Ctrl Pts',(142.014859435991,-4.91824791031005,130.79982682988));
#35477=CARTESIAN_POINT('',(142.360140564045,-4.91824942331981,130.806742321652));
#35478=CARTESIAN_POINT('Ctrl Pts',(142.430282519794,-4.76405452823406,129.582490119308));
#35479=CARTESIAN_POINT('Ctrl Pts',(142.422611012822,-4.79777606720098,129.713969887945));
#35480=CARTESIAN_POINT('Ctrl Pts',(142.414939505849,-4.82602628670489,129.846752319787));
#35481=CARTESIAN_POINT('Ctrl Pts',(142.407267998877,-4.84872853961549,129.980337188519));
#35482=CARTESIAN_POINT('Ctrl Pts',(142.399413426405,-4.8719725373614,130.117109798705));
#35483=CARTESIAN_POINT('Ctrl Pts',(142.391558853933,-4.88940039608235,130.254723178035));
#35484=CARTESIAN_POINT('Ctrl Pts',(142.383704281461,-4.90098631039045,130.392637108563));
#35485=CARTESIAN_POINT('Ctrl Pts',(142.375849708989,-4.91257222469854,130.530551039091));
#35486=CARTESIAN_POINT('Ctrl Pts',(142.367995136517,-4.91831623997429,130.668765074869));
#35487=CARTESIAN_POINT('Ctrl Pts',(142.360140564045,-4.91824942331981,130.806742321652));
#35488=CARTESIAN_POINT('Ctrl Pts',(142.360140564008,-4.9182494233195,130.806742322295));
#35489=CARTESIAN_POINT('Ctrl Pts',(142.352502847162,-4.9181844513777,130.940910177508));
#35490=CARTESIAN_POINT('Ctrl Pts',(142.344865130315,-4.91262993299218,131.074940705202));
#35491=CARTESIAN_POINT('Ctrl Pts',(142.337227413469,-4.90161629827904,131.208514953118));
#35492=CARTESIAN_POINT('Ctrl Pts',(142.32945307935,-4.89040566061798,131.344478468636));
#35493=CARTESIAN_POINT('Ctrl Pts',(142.321678745231,-4.87351584157187,131.480190537609));
#35494=CARTESIAN_POINT('Ctrl Pts',(142.313904411111,-4.85096096456765,131.615138504993));
#35495=CARTESIAN_POINT('Ctrl Pts',(142.306139658164,-4.82843388443355,131.749920161068));
#35496=CARTESIAN_POINT('Ctrl Pts',(142.298374905217,-4.80025570163112,131.883939207315));
#35497=CARTESIAN_POINT('Ctrl Pts',(142.29061015227,-4.7664924437661,132.016686005414));
#35498=CARTESIAN_POINT('Ctrl Pts',(142.282853111385,-4.73276272004476,132.149300957521));
#35499=CARTESIAN_POINT('Ctrl Pts',(142.2750960705,-4.69345905613744,132.280645799681));
#35500=CARTESIAN_POINT('Ctrl Pts',(142.267339029615,-4.64869882196989,132.410219367617));
#35501=CARTESIAN_POINT('Ctrl Pts',(142.259587838375,-4.60397234184315,132.539695223118));
#35502=CARTESIAN_POINT('Ctrl Pts',(142.251836647135,-4.55379760893742,132.667402095045));
#35503=CARTESIAN_POINT('Ctrl Pts',(142.244085455895,-4.49834219051421,132.792852659174));
#35504=CARTESIAN_POINT('Ctrl Pts',(142.236337559118,-4.44291034212314,132.918249903467));
#35505=CARTESIAN_POINT('Ctrl Pts',(142.22858966234,-4.38220242995891,133.041392390484));
#35506=CARTESIAN_POINT('Ctrl Pts',(142.220841765563,-4.31643456450761,133.161811722642));
#35507=CARTESIAN_POINT('Ctrl Pts',(142.213095489479,-4.25068045627592,133.282205865672));
#35508=CARTESIAN_POINT('Ctrl Pts',(142.205349213395,-4.17986868732026,133.39987764395));
#35509=CARTESIAN_POINT('Ctrl Pts',(142.197602937311,-4.10426165721733,133.514382630686));
#35510=CARTESIAN_POINT('Ctrl Pts',(142.189856604046,-4.02865406900058,133.628888462672));
#35511=CARTESIAN_POINT('Ctrl Pts',(142.18211027078,-3.94825136443048,133.740227130211));
#35512=CARTESIAN_POINT('Ctrl Pts',(142.174363937515,-3.86335944257491,133.8479829463));
#35513=CARTESIAN_POINT('Ctrl Pts',(142.166615869512,-3.77844850976184,133.955762893557));
#35514=CARTESIAN_POINT('Ctrl Pts',(142.158867801509,-3.68904660107439,134.059958085721));
#35515=CARTESIAN_POINT('Ctrl Pts',(142.151119733506,-3.5954998231538,134.160186012935));
#35516=CARTESIAN_POINT('Ctrl Pts',(142.143363430764,-3.5018536226046,134.260520463582));
#35517=CARTESIAN_POINT('Ctrl Pts',(142.135607128022,-3.40405402011725,134.356878940183));
#35518=CARTESIAN_POINT('Ctrl Pts',(142.12785082528,-3.30248430008892,134.448915530058));
#35519=CARTESIAN_POINT('Ctrl Pts',(142.120090382766,-3.20086036924273,134.541001242632));
#35520=CARTESIAN_POINT('Ctrl Pts',(142.112329940252,-3.09546261162876,134.628760222098));
#35521=CARTESIAN_POINT('Ctrl Pts',(142.104569497738,-2.98670651439929,134.711887618029));
#35522=CARTESIAN_POINT('Ctrl Pts',(142.096796597472,-2.87777583222768,134.795148457435));
#35523=CARTESIAN_POINT('Ctrl Pts',(142.089023697207,-2.76547635776458,134.873762631406));
#35524=CARTESIAN_POINT('Ctrl Pts',(142.081250796941,-2.65025235158391,134.947468814973));
#35525=CARTESIAN_POINT('Ctrl Pts',(142.073760461179,-2.53921702826021,135.018495593113));
#35526=CARTESIAN_POINT('Ctrl Pts',(142.066270125417,-2.42546637581353,135.084964865886));
#35527=CARTESIAN_POINT('Ctrl Pts',(142.058779789655,-2.30941684910832,135.14668452068));
#35528=CARTESIAN_POINT('Ctrl Pts',(142.051005455536,-2.18896726932503,135.210744294945));
#35529=CARTESIAN_POINT('Ctrl Pts',(142.043231121417,-2.06565950238112,135.269890100069));
#35530=CARTESIAN_POINT('Ctrl Pts',(142.035456787298,-1.93993249354175,135.323856715916));
#35531=CARTESIAN_POINT('Ctrl Pts',(142.027692034351,-1.81436043200432,135.377756822732));
#35532=CARTESIAN_POINT('Ctrl Pts',(142.019927281404,-1.68637541668486,135.426490287587));
#35533=CARTESIAN_POINT('Ctrl Pts',(142.012162528457,-1.55644191027044,135.469837189413));
#35534=CARTESIAN_POINT('Ctrl Pts',(142.004405487572,-1.42663745564651,135.513141038485));
#35535=CARTESIAN_POINT('Ctrl Pts',(141.996648446687,-1.29488872967157,135.551068848366));
#35536=CARTESIAN_POINT('Ctrl Pts',(141.988891405802,-1.16168081735598,135.583448474164));
#35537=CARTESIAN_POINT('Ctrl Pts',(141.981140214562,-1.02857335816314,135.615803682236));
#35538=CARTESIAN_POINT('Ctrl Pts',(141.973389023322,-0.894009281242463,
135.642618942111));
#35539=CARTESIAN_POINT('Ctrl Pts',(141.965637832082,-0.758489160464665,
135.663771822224));
#35540=CARTESIAN_POINT('Ctrl Pts',(141.957889935304,-0.623026639353269,
135.684915711799));
#35541=CARTESIAN_POINT('Ctrl Pts',(141.950142038527,-0.486609268051492,
135.700401948114));
#35542=CARTESIAN_POINT('Ctrl Pts',(141.94239414175,-0.349747935708725,135.710159170704));
#35543=CARTESIAN_POINT('Ctrl Pts',(141.934647865666,-0.212915231806296,
135.719914352293));
#35544=CARTESIAN_POINT('Ctrl Pts',(141.926901589582,-0.0756391413089238,
135.72394287603));
#35545=CARTESIAN_POINT('Ctrl Pts',(141.919155313498,0.061564593556896,135.722225282573));
#35546=CARTESIAN_POINT('Ctrl Pts',(141.911408980233,0.198769341229425,135.720507676437));
#35547=CARTESIAN_POINT('Ctrl Pts',(141.903662646967,0.335901341270046,135.713043873362));
#35548=CARTESIAN_POINT('Ctrl Pts',(141.895916313702,0.472445518512196,135.699866545919));
#35549=CARTESIAN_POINT('Ctrl Pts',(141.888168245699,0.609020273876202,135.686686267505));
#35550=CARTESIAN_POINT('Ctrl Pts',(141.880420177696,0.74500655541295,135.667789956206));
#35551=CARTESIAN_POINT('Ctrl Pts',(141.872672109693,0.879895467653373,135.643262045422));
#35552=CARTESIAN_POINT('Ctrl Pts',(141.864915806951,1.01492774143492,135.618708066082));
#35553=CARTESIAN_POINT('Ctrl Pts',(141.85715950421,1.14885993084504,135.58851060097));
#35554=CARTESIAN_POINT('Ctrl Pts',(141.849403201468,1.28119383517219,135.552805143852));
#35555=CARTESIAN_POINT('Ctrl Pts',(141.841642758954,1.41359837008866,135.517080629657));
#35556=CARTESIAN_POINT('Ctrl Pts',(141.833882316439,1.54440254745099,135.475842383191));
#35557=CARTESIAN_POINT('Ctrl Pts',(141.826121873925,1.67312530700521,135.429275186459));
#35558=CARTESIAN_POINT('Ctrl Pts',(141.81834897366,1.80205470376054,135.382633235929));
#35559=CARTESIAN_POINT('Ctrl Pts',(141.810576073394,1.9288956438059,135.330645388866));
#35560=CARTESIAN_POINT('Ctrl Pts',(141.802803173129,2.05318813335255,135.273544161745));
#35561=CARTESIAN_POINT('Ctrl Pts',(141.795312837367,2.1729622778313,135.218518708059));
#35562=CARTESIAN_POINT('Ctrl Pts',(141.787822501605,2.29036976568558,135.158745328104));
#35563=CARTESIAN_POINT('Ctrl Pts',(141.780332165843,2.4050238631082,135.094470555596));
#35564=CARTESIAN_POINT('Ctrl Pts',(141.772557831724,2.52402510548203,135.027758785552));
#35565=CARTESIAN_POINT('Ctrl Pts',(141.764783497605,2.64043700642165,134.95598622135));
#35566=CARTESIAN_POINT('Ctrl Pts',(141.757009163486,2.75379916807868,134.879378802113));
#35567=CARTESIAN_POINT('Ctrl Pts',(141.749244410539,2.86702162100286,134.802865794674));
#35568=CARTESIAN_POINT('Ctrl Pts',(141.741479657591,2.97720149217645,134.721530004696));
#35569=CARTESIAN_POINT('Ctrl Pts',(141.733714904644,3.08390270235017,134.635643325085));
#35570=CARTESIAN_POINT('Ctrl Pts',(141.725957863759,3.19049793537773,134.549841949336));
#35571=CARTESIAN_POINT('Ctrl Pts',(141.718200822874,3.29362108053269,134.459498922534));
#35572=CARTESIAN_POINT('Ctrl Pts',(141.710443781989,3.3928651071469,134.364929311919));
#35573=CARTESIAN_POINT('Ctrl Pts',(141.702692590749,3.49203429306856,134.270431016983));
#35574=CARTESIAN_POINT('Ctrl Pts',(141.694941399509,3.58732990113477,134.171712750978));
#35575=CARTESIAN_POINT('Ctrl Pts',(141.687190208269,3.6783783537984,134.069129483628));
#35576=CARTESIAN_POINT('Ctrl Pts',(141.679442311492,3.76938810844097,133.966589816902));
#35577=CARTESIAN_POINT('Ctrl Pts',(141.671694414715,3.8561540390132,133.860188707885));
#35578=CARTESIAN_POINT('Ctrl Pts',(141.663946517938,3.93833995987237,133.750317410014));
#35579=CARTESIAN_POINT('Ctrl Pts',(141.656200241854,4.02050868920862,133.64046909485));
#35580=CARTESIAN_POINT('Ctrl Pts',(141.64845396577,4.09809908039066,133.527152347535));
#35581=CARTESIAN_POINT('Ctrl Pts',(141.640707689685,4.17081599045296,133.410790558363));
#35582=CARTESIAN_POINT('Ctrl Pts',(141.63296135642,4.24353343729492,133.294427910234));
#35583=CARTESIAN_POINT('Ctrl Pts',(141.625215023155,4.3113771240395,133.175020506944));
#35584=CARTESIAN_POINT('Ctrl Pts',(141.617468689889,4.37409612833673,133.053019356141));
#35585=CARTESIAN_POINT('Ctrl Pts',(141.609720621886,4.43682917812006,132.930990884026));
#35586=CARTESIAN_POINT('Ctrl Pts',(141.601972553883,4.49443508307323,132.806367856213));
#35587=CARTESIAN_POINT('Ctrl Pts',(141.59422448588,4.54670980897447,132.679624059186));
#35588=CARTESIAN_POINT('Ctrl Pts',(141.586468183139,4.59904009307651,132.552745557343));
#35589=CARTESIAN_POINT('Ctrl Pts',(141.578711880397,4.64602773029276,132.423742145728));
#35590=CARTESIAN_POINT('Ctrl Pts',(141.570955577655,4.68751742571277,132.293106212401));
#35591=CARTESIAN_POINT('Ctrl Pts',(141.563195135141,4.72902926543247,132.162400554742));
#35592=CARTESIAN_POINT('Ctrl Pts',(141.555434692627,4.76503721368654,132.030061016245));
#35593=CARTESIAN_POINT('Ctrl Pts',(141.547674250112,4.79543670799164,131.896592205713));
#35594=CARTESIAN_POINT('Ctrl Pts',(141.539901349847,4.82588500226374,131.762909139198));
#35595=CARTESIAN_POINT('Ctrl Pts',(141.532128449582,4.85070678051408,131.628093562804));
#35596=CARTESIAN_POINT('Ctrl Pts',(141.524355549316,4.86984902755901,131.492658163169));
#35597=CARTESIAN_POINT('Ctrl Pts',(141.516865213554,4.8882954057074,131.362146181451));
#35598=CARTESIAN_POINT('Ctrl Pts',(141.509374877792,4.90146798330419,131.231058964857));
#35599=CARTESIAN_POINT('Ctrl Pts',(141.50188454203,4.90936513707526,131.099855140984));
#35600=CARTESIAN_POINT('Ctrl Pts',(141.494110207911,4.91756171383188,130.96367668425));
#35601=CARTESIAN_POINT('Ctrl Pts',(141.486335873792,4.92010089884113,130.82694123094));
#35602=CARTESIAN_POINT('Ctrl Pts',(141.478561539673,4.91692392480242,130.690158252417));
#35603=CARTESIAN_POINT('Ctrl Pts',(141.470796786726,4.91375086610027,130.55354384669));
#35604=CARTESIAN_POINT('Ctrl Pts',(141.463032033779,4.90487567410532,130.416882419396));
#35605=CARTESIAN_POINT('Ctrl Pts',(141.455267280831,4.89029138853252,130.280687821113));
#35606=CARTESIAN_POINT('Ctrl Pts',(141.447510239946,4.87572158827778,130.144628493226));
#35607=CARTESIAN_POINT('Ctrl Pts',(141.439753199061,4.85545402006082,130.00903545787));
#35608=CARTESIAN_POINT('Ctrl Pts',(141.431996158176,4.8295337488552,129.874421463014));
#35609=CARTESIAN_POINT('Ctrl Pts',(141.424244966936,4.8036330243277,129.739908981619));
#35610=CARTESIAN_POINT('Ctrl Pts',(141.416493775696,4.77208815517582,129.606374453538));
#35611=CARTESIAN_POINT('Ctrl Pts',(141.408742584456,4.73499585969154,129.474324049947));
#35612=CARTESIAN_POINT('Ctrl Pts',(141.400994687679,4.69791932942232,129.3423297713));
#35613=CARTESIAN_POINT('Ctrl Pts',(141.393246790902,4.65530016782035,129.211818738156));
#35614=CARTESIAN_POINT('Ctrl Pts',(141.385498894125,4.60728583093167,129.083285275056));
#35615=CARTESIAN_POINT('Ctrl Pts',(141.377752618041,4.5592815376072,128.954778698386));
#35616=CARTESIAN_POINT('Ctrl Pts',(141.370006341957,4.50588445047884,128.828249234971));
#35617=CARTESIAN_POINT('Ctrl Pts',(141.362260065873,4.44729124780882,128.704174049743));
#35618=CARTESIAN_POINT('Ctrl Pts',(141.354513732607,4.38869761261713,128.580097948621));
#35619=CARTESIAN_POINT('Ctrl Pts',(141.346767399342,4.32490795229567,128.458476515363));
#35620=CARTESIAN_POINT('Ctrl Pts',(141.339021066076,4.25616608269245,128.339764638701));
#35621=CARTESIAN_POINT('Ctrl Pts',(141.331272998073,4.18740881882415,128.221026177337));
#35622=CARTESIAN_POINT('Ctrl Pts',(141.323524930071,4.11369733474675,128.105198907396));
#35623=CARTESIAN_POINT('Ctrl Pts',(141.315776862068,4.03531995496797,127.992710581815));
#35624=CARTESIAN_POINT('Ctrl Pts',(141.308020559326,3.95685927477721,127.880102702304));
#35625=CARTESIAN_POINT('Ctrl Pts',(141.300264256584,3.87372301667154,127.770841177293));
#35626=CARTESIAN_POINT('Ctrl Pts',(141.292507953842,3.78624149997771,127.665322808564));
#35627=CARTESIAN_POINT('Ctrl Pts',(141.284747511328,3.6987132917644,127.559748121503));
#35628=CARTESIAN_POINT('Ctrl Pts',(141.276987068814,3.60683546555084,127.457920861709));
#35629=CARTESIAN_POINT('Ctrl Pts',(141.269226626299,3.51097604443836,127.360201753942));
#35630=CARTESIAN_POINT('Ctrl Pts',(141.261453726034,3.41496274127311,127.262325778789));
#35631=CARTESIAN_POINT('Ctrl Pts',(141.253680825769,3.31495535612773,127.168571401663));
#35632=CARTESIAN_POINT('Ctrl Pts',(141.245907925503,3.21135657078749,127.079260345391));
#35633=CARTESIAN_POINT('Ctrl Pts',(141.238417589741,3.11152386224369,126.993195970975));
#35634=CARTESIAN_POINT('Ctrl Pts',(141.230927253979,3.00835657428851,126.911257665823));
#35635=CARTESIAN_POINT('Ctrl Pts',(141.223436918217,2.90223968589053,126.833694695061));
#35636=CARTESIAN_POINT('Ctrl Pts',(141.215662584098,2.79209934341573,126.753190900688));
#35637=CARTESIAN_POINT('Ctrl Pts',(141.207888249979,2.67843242551728,126.677145759963));
#35638=CARTESIAN_POINT('Ctrl Pts',(141.20011391586,2.56163579972067,126.605884097197));
#35639=CARTESIAN_POINT('Ctrl Pts',(141.192349162913,2.44498311532701,126.534710258061));
#35640=CARTESIAN_POINT('Ctrl Pts',(141.184584409966,2.32520872802974,126.468308368852));
#35641=CARTESIAN_POINT('Ctrl Pts',(141.176819657018,2.20274119266995,126.406962034243));
#35642=CARTESIAN_POINT('Ctrl Pts',(141.169062616133,2.08039529379269,126.345676629678));
#35643=CARTESIAN_POINT('Ctrl Pts',(141.161305575248,1.95536191726943,126.289436961172));
#35644=CARTESIAN_POINT('Ctrl Pts',(141.153548534363,1.82809681120627,126.238482267089));
#35645=CARTESIAN_POINT('Ctrl Pts',(141.145797343123,1.70092767674957,126.187565998336));
#35646=CARTESIAN_POINT('Ctrl Pts',(141.138046151883,1.57153052407757,126.141926915961));
#35647=CARTESIAN_POINT('Ctrl Pts',(141.130294960643,1.44038348793601,126.101757246009));
#35648=CARTESIAN_POINT('Ctrl Pts',(141.122547063866,1.30929219278326,126.061604649238));
#35649=CARTESIAN_POINT('Ctrl Pts',(141.114799167089,1.17645286645757,126.026916955608));
#35650=CARTESIAN_POINT('Ctrl Pts',(141.107051270312,1.04236110179102,125.997837300659));
#35651=CARTESIAN_POINT('Ctrl Pts',(141.099304994228,0.908297386230965,125.968763728547));
#35652=CARTESIAN_POINT('Ctrl Pts',(141.091558718144,0.772982135270482,125.945295944603));
#35653=CARTESIAN_POINT('Ctrl Pts',(141.083812442059,0.63692311068484,125.927526397134));
#35654=CARTESIAN_POINT('Ctrl Pts',(141.076066108794,0.500863081742386,125.909756718495));
#35655=CARTESIAN_POINT('Ctrl Pts',(141.068319775529,0.364059655892093,125.897685410896));
#35656=CARTESIAN_POINT('Ctrl Pts',(141.060573442263,0.227027332326683,125.891353223629));
#35657=CARTESIAN_POINT('Ctrl Pts',(141.05282537426,0.0899643213225272,125.885019618313));
#35658=CARTESIAN_POINT('Ctrl Pts',(141.045077306257,-0.0473272989246117,
125.884427708844));
#35659=CARTESIAN_POINT('Ctrl Pts',(141.037329238254,-0.18433180131469,125.889566130558));
#35660=CARTESIAN_POINT('Ctrl Pts',(141.029572935513,-0.321481913720284,
125.894710013448));
#35661=CARTESIAN_POINT('Ctrl Pts',(141.021816632771,-0.458343907380787,
125.905596378804));
#35662=CARTESIAN_POINT('Ctrl Pts',(141.014060330029,-0.59440539605652,125.922161800676));
#35663=CARTESIAN_POINT('Ctrl Pts',(141.006299887515,-0.730539504845583,
125.938736064013));
#35664=CARTESIAN_POINT('Ctrl Pts',(140.998539445001,-0.865871871717929,
125.960995360133));
#35665=CARTESIAN_POINT('Ctrl Pts',(140.990779002486,-0.999900083238783,
125.988825041325));
#35666=CARTESIAN_POINT('Ctrl Pts',(140.983006102221,-1.13414344874324,126.016699397192));
#35667=CARTESIAN_POINT('Ctrl Pts',(140.975233201955,-1.2670780959682,126.050161911757));
#35668=CARTESIAN_POINT('Ctrl Pts',(140.96746030169,-1.39821569104805,126.089047696475));
#35669=CARTESIAN_POINT('Ctrl Pts',(140.959969965928,-1.52458610423091,126.126519884971));
#35670=CARTESIAN_POINT('Ctrl Pts',(140.952479630166,-1.64928756010908,126.169027790788));
#35671=CARTESIAN_POINT('Ctrl Pts',(140.944989294404,-1.77190225433616,126.216382254106));
#35672=CARTESIAN_POINT('Ctrl Pts',(140.937214701506,-1.89917015809501,126.265533812311));
#35673=CARTESIAN_POINT('Ctrl Pts',(140.929440108609,-2.02459294751934,126.32006274775));
#35674=CARTESIAN_POINT('Ctrl Pts',(140.921665515711,-2.14768277363802,126.37981072336));
#35675=CARTESIAN_POINT('Ctrl Pts',(140.913900563774,-2.27061996100675,126.439484607905));
#35676=CARTESIAN_POINT('Ctrl Pts',(140.906135611837,-2.39122959307165,126.504364485944));
#35677=CARTESIAN_POINT('Ctrl Pts',(140.898370659899,-2.50904138553715,126.574243079227));
#35678=CARTESIAN_POINT('Ctrl Pts',(140.89061347956,-2.62673526538269,126.644051734112));
#35679=CARTESIAN_POINT('Ctrl Pts',(140.88285629922,-2.74163654429565,126.718848949515));
#35680=CARTESIAN_POINT('Ctrl Pts',(140.87509911888,-2.85329757877115,126.798380588974));
#35681=CARTESIAN_POINT('Ctrl Pts',(140.866975842646,-2.97022839485252,126.881665680769));
#35682=CARTESIAN_POINT('Ctrl Pts',(140.858852566412,-3.08360526868429,126.970142791753));
#35683=CARTESIAN_POINT('Ctrl Pts',(140.850729290178,-3.1929453900343,127.063467301958));
#35684=CARTESIAN_POINT('Ctrl Pts',(140.842981731391,-3.29722831647514,127.152475370659));
#35685=CARTESIAN_POINT('Ctrl Pts',(140.835234172603,-3.39783919195002,127.245892214331));
#35686=CARTESIAN_POINT('Ctrl Pts',(140.827486613816,-3.49439138665629,127.343376379035));
#35687=CARTESIAN_POINT('Ctrl Pts',(140.819740679673,-3.59092333459718,127.440840101541));
#35688=CARTESIAN_POINT('Ctrl Pts',(140.811994745531,-3.68339802026635,127.542369170494));
#35689=CARTESIAN_POINT('Ctrl Pts',(140.804248811388,-3.77146507988114,127.64758469683));
#35690=CARTESIAN_POINT('Ctrl Pts',(140.796502824113,-3.859532743589,127.752800944889));
#35691=CARTESIAN_POINT('Ctrl Pts',(140.788756836837,-3.94319247059463,127.861703400579));
#35692=CARTESIAN_POINT('Ctrl Pts',(140.781010849561,-4.0221339254761,127.973879784203));
#35693=CARTESIAN_POINT('Ctrl Pts',(140.773263131714,-4.10109301708202,128.086081229742));
#35694=CARTESIAN_POINT('Ctrl Pts',(140.765515413867,-4.1753315146918,128.201557738712));
#35695=CARTESIAN_POINT('Ctrl Pts',(140.757767696019,-4.24458241120132,128.31986807038));
#35696=CARTESIAN_POINT('Ctrl Pts',(140.750012840577,-4.31389710518594,128.43828739559));
#35697=CARTESIAN_POINT('Ctrl Pts',(140.742257985135,-4.37821482655643,128.55954541827));
#35698=CARTESIAN_POINT('Ctrl Pts',(140.734503129693,-4.43731438705389,128.683176020944));
#35699=CARTESIAN_POINT('Ctrl Pts',(140.72674409703,-4.49644578205236,128.806873218337));
#35700=CARTESIAN_POINT('Ctrl Pts',(140.718985064366,-4.55035326234016,128.932945183225));
#35701=CARTESIAN_POINT('Ctrl Pts',(140.711226031703,-4.5988641806459,129.060906772329));
#35702=CARTESIAN_POINT('Ctrl Pts',(140.703457242644,-4.64743609775488,129.189029263434));
#35703=CARTESIAN_POINT('Ctrl Pts',(140.695688453585,-4.69059778190035,129.319045752601));
#35704=CARTESIAN_POINT('Ctrl Pts',(140.687919664526,-4.72822661721739,129.450456588937));
#35705=CARTESIAN_POINT('Ctrl Pts',(140.685326606105,-4.74078633116139,129.49431876271));
#35706=CARTESIAN_POINT('Ctrl Pts',(140.682733547685,-4.75273006249754,129.538336199274));
#35707=CARTESIAN_POINT('Ctrl Pts',(140.680140489264,-4.76405452823406,129.582490119308));
#35708=CARTESIAN_POINT('Origin',(213.235140564004,0.,130.804360617566));
#35709=CARTESIAN_POINT('',(138.584929581679,-4.76405452823406,129.582490119308));
#35710=CARTESIAN_POINT('',(138.929858124837,-4.76405452823407,129.582490119308));
#35711=CARTESIAN_POINT('',(213.235140564004,-4.76405452823405,129.582490119308));
#35712=CARTESIAN_POINT('',(140.264859435961,-4.9182499873584,130.804713249272));
#35713=CARTESIAN_POINT('Ctrl Pts',(140.264859435961,-4.9182499873584,130.804713249272));
#35714=CARTESIAN_POINT('Ctrl Pts',(140.256699920237,-4.9182395995136,130.949595336183));
#35715=CARTESIAN_POINT('Ctrl Pts',(140.248540404513,-4.91182300637272,131.094339296179));
#35716=CARTESIAN_POINT('Ctrl Pts',(140.240380888789,-4.89906240695556,131.23837743205));
#35717=CARTESIAN_POINT('Ctrl Pts',(140.232208991226,-4.88628244368213,131.382634141803));
#35718=CARTESIAN_POINT('Ctrl Pts',(140.224037093662,-4.86713928737667,131.526182566396));
#35719=CARTESIAN_POINT('Ctrl Pts',(140.215865196099,-4.84174648071891,131.668463666366));
#35720=CARTESIAN_POINT('Ctrl Pts',(140.207672433166,-4.81628883841023,131.811108053777));
#35721=CARTESIAN_POINT('Ctrl Pts',(140.199479670233,-4.78454969417094,131.952478325094));
#35722=CARTESIAN_POINT('Ctrl Pts',(140.1912869073,-4.74669336420818,132.092027177154));
#35723=CARTESIAN_POINT('Ctrl Pts',(140.183082921663,-4.70878517745716,132.23176718761));
#35724=CARTESIAN_POINT('Ctrl Pts',(140.174878936027,-4.6647431774351,132.369680489536));
#35725=CARTESIAN_POINT('Ctrl Pts',(140.16667495039,-4.61478046118432,132.505238143307));
#35726=CARTESIAN_POINT('Ctrl Pts',(140.158451938574,-4.56470187447502,132.641110174051));
#35727=CARTESIAN_POINT('Ctrl Pts',(140.150228926759,-4.50867524175657,132.774615333103));
#35728=CARTESIAN_POINT('Ctrl Pts',(140.142005914943,-4.44696114355522,132.905246061899));
#35729=CARTESIAN_POINT('Ctrl Pts',(140.137749083004,-4.41501341561366,132.972870074986));
#35730=CARTESIAN_POINT('Ctrl Pts',(140.133492251064,-4.3815422660966,133.039724218812));
#35731=CARTESIAN_POINT('Ctrl Pts',(140.129235419124,-4.34658843369518,133.105741083844));
#35732=CARTESIAN_POINT('Ctrl Pts',(140.121461085005,-4.28275157668732,133.226308955337));
#35733=CARTESIAN_POINT('Ctrl Pts',(140.113686750886,-4.21379324585066,133.344409676167));
#35734=CARTESIAN_POINT('Ctrl Pts',(140.105912416767,-4.13992826696339,133.459577559154));
#35735=CARTESIAN_POINT('Ctrl Pts',(140.09814766382,-4.06615432006105,133.574603508018));
#35736=CARTESIAN_POINT('Ctrl Pts',(140.090382910873,-3.98748596589034,133.686703484803));
#35737=CARTESIAN_POINT('Ctrl Pts',(140.082618157926,-3.90418455435782,133.79543501116));
#35738=CARTESIAN_POINT('Ctrl Pts',(140.074861117041,-3.82096587896162,133.904058543832));
#35739=CARTESIAN_POINT('Ctrl Pts',(140.067104076156,-3.733123539861,134.009319975609));
#35740=CARTESIAN_POINT('Ctrl Pts',(140.059347035271,-3.64096274595035,134.110804832293));
#35741=CARTESIAN_POINT('Ctrl Pts',(140.051595844031,-3.54887145121118,134.212213158457));
#35742=CARTESIAN_POINT('Ctrl Pts',(140.043844652791,-3.45246844546252,134.309850289931));
#35743=CARTESIAN_POINT('Ctrl Pts',(140.03609346155,-3.35209963137398,134.403334238453));
#35744=CARTESIAN_POINT('Ctrl Pts',(140.028345564773,-3.25177347670899,134.496778453803));
#35745=CARTESIAN_POINT('Ctrl Pts',(140.020597667996,-3.14748515167631,134.586072731168));
#35746=CARTESIAN_POINT('Ctrl Pts',(140.012849771219,-3.0396177295135,134.670871592712));
#35747=CARTESIAN_POINT('Ctrl Pts',(140.005103495135,-2.93177287089005,134.755652716163));
#35748=CARTESIAN_POINT('Ctrl Pts',(139.997357219051,-2.82035071144692,134.835940052717));
#35749=CARTESIAN_POINT('Ctrl Pts',(139.989610942967,-2.70576743693359,134.911428384201));
#35750=CARTESIAN_POINT('Ctrl Pts',(139.981864609702,-2.59118331659255,134.986917272923));
#35751=CARTESIAN_POINT('Ctrl Pts',(139.974118276436,-2.47343836110084,135.057606870798));
#35752=CARTESIAN_POINT('Ctrl Pts',(139.966371943171,-2.35297742678264,135.123235504797));
#35753=CARTESIAN_POINT('Ctrl Pts',(139.958623875168,-2.23248951607342,135.188878835873));
#35754=CARTESIAN_POINT('Ctrl Pts',(139.950875807165,-2.10928475949464,135.249458760793));
#35755=CARTESIAN_POINT('Ctrl Pts',(139.943127739162,-1.98383191083405,135.304759934522));
#35756=CARTESIAN_POINT('Ctrl Pts',(139.93537143642,-1.85824572939299,135.360119882997));
#35757=CARTESIAN_POINT('Ctrl Pts',(139.927615133678,-1.73040704130752,135.410189715111));
#35758=CARTESIAN_POINT('Ctrl Pts',(139.919858830936,-1.60080436619132,135.454802364721));
#35759=CARTESIAN_POINT('Ctrl Pts',(139.912098388422,-1.47113251822506,135.499438825445));
#35760=CARTESIAN_POINT('Ctrl Pts',(139.904337945908,-1.33969518171868,135.538612188323));
#35761=CARTESIAN_POINT('Ctrl Pts',(139.896577503394,-1.20699431094952,135.572205811764));
#35762=CARTESIAN_POINT('Ctrl Pts',(139.888804603129,-1.07408041696197,135.605853362671));
#35763=CARTESIAN_POINT('Ctrl Pts',(139.881031702863,-0.939899318360345,
135.633903194968));
#35764=CARTESIAN_POINT('Ctrl Pts',(139.873258802598,-0.804962281921439,
135.656290005674));
#35765=CARTESIAN_POINT('Ctrl Pts',(139.865768466836,-0.674930546644616,
135.677862999421));
#35766=CARTESIAN_POINT('Ctrl Pts',(139.858278131074,-0.544197185472536,
135.694177515392));
#35767=CARTESIAN_POINT('Ctrl Pts',(139.850787795312,-0.413220654976473,
135.705220924982));
#35768=CARTESIAN_POINT('Ctrl Pts',(139.843013461193,-0.277278109515476,
135.716683048803));
#35769=CARTESIAN_POINT('Ctrl Pts',(139.835239127074,-0.140642966076507,
135.722502776448));
#35770=CARTESIAN_POINT('Ctrl Pts',(139.827464792955,-0.00382313905452457,
135.722609131632));
#35771=CARTESIAN_POINT('Ctrl Pts',(139.819700040008,0.1328280697585,135.722715355742));
#35772=CARTESIAN_POINT('Ctrl Pts',(139.81193528706,0.269663122074555,135.717122217021));
#35773=CARTESIAN_POINT('Ctrl Pts',(139.804170534113,0.406168482318487,135.705810426191));
#35774=CARTESIAN_POINT('Ctrl Pts',(139.796413493228,0.542538263514051,135.694509870391));
#35775=CARTESIAN_POINT('Ctrl Pts',(139.788656452343,0.678578617178914,135.677501997711));
#35776=CARTESIAN_POINT('Ctrl Pts',(139.780899411458,0.813775861568878,135.654819555608));
#35777=CARTESIAN_POINT('Ctrl Pts',(139.773148220218,0.948871152665259,135.632154218511));
#35778=CARTESIAN_POINT('Ctrl Pts',(139.765397028978,1.08312421598248,135.60382289398));
#35779=CARTESIAN_POINT('Ctrl Pts',(139.757645837738,1.21602670513635,135.569910125744));
#35780=CARTESIAN_POINT('Ctrl Pts',(139.749897940961,1.34887270718713,135.536011771339));
#35781=CARTESIAN_POINT('Ctrl Pts',(139.742150044184,1.48036889874304,135.496536787939));
#35782=CARTESIAN_POINT('Ctrl Pts',(139.734402147407,1.61001755907654,135.451620726702));
#35783=CARTESIAN_POINT('Ctrl Pts',(139.726655871323,1.73963909970521,135.406714060936));
#35784=CARTESIAN_POINT('Ctrl Pts',(139.718909595239,1.86741350861953,135.356368709092));
#35785=CARTESIAN_POINT('Ctrl Pts',(139.711163319155,1.99285903856431,135.300769842149));
#35786=CARTESIAN_POINT('Ctrl Pts',(139.703416985889,2.11830549451942,135.245170564788));
#35787=CARTESIAN_POINT('Ctrl Pts',(139.695670652624,2.24142267976915,135.184317853363));
#35788=CARTESIAN_POINT('Ctrl Pts',(139.687924319358,2.36174998567253,135.118444537435));
#35789=CARTESIAN_POINT('Ctrl Pts',(139.680176251356,2.4821042380417,135.052556469635));
#35790=CARTESIAN_POINT('Ctrl Pts',(139.672428183353,2.59966702496357,134.981645747752));
#35791=CARTESIAN_POINT('Ctrl Pts',(139.66468011535,2.71400379768974,134.905990348371));
#35792=CARTESIAN_POINT('Ctrl Pts',(139.656923812608,2.82846208889875,134.830254541532));
#35793=CARTESIAN_POINT('Ctrl Pts',(139.649167509866,2.93968719025207,134.749764199948));
#35794=CARTESIAN_POINT('Ctrl Pts',(139.641411207124,3.0472744874863,134.664840025673));
#35795=CARTESIAN_POINT('Ctrl Pts',(139.63365076461,3.15491920730045,134.579870524809));
#35796=CARTESIAN_POINT('Ctrl Pts',(139.625890322096,3.2589219578543,134.490462730605));
#35797=CARTESIAN_POINT('Ctrl Pts',(139.618129879581,3.35891328672535,134.396975903783));
#35798=CARTESIAN_POINT('Ctrl Pts',(139.610356979316,3.45906513055431,134.303339003607));
#35799=CARTESIAN_POINT('Ctrl Pts',(139.602584079051,3.55519241022837,134.205610264659));
#35800=CARTESIAN_POINT('Ctrl Pts',(139.594811178785,3.64696383231787,134.104184532302));
#35801=CARTESIAN_POINT('Ctrl Pts',(139.587320843023,3.73539913205683,134.006445880792));
#35802=CARTESIAN_POINT('Ctrl Pts',(139.579830507261,3.81978957144916,133.905274595861));
#35803=CARTESIAN_POINT('Ctrl Pts',(139.572340171499,3.89987671871707,133.801049563938));
#35804=CARTESIAN_POINT('Ctrl Pts',(139.56456583738,3.98300039451491,133.692872808252));
#35805=CARTESIAN_POINT('Ctrl Pts',(139.556791503261,4.06175132873342,133.581063497316));
#35806=CARTESIAN_POINT('Ctrl Pts',(139.549017169142,4.13579526687686,133.466010589478));
#35807=CARTESIAN_POINT('Ctrl Pts',(139.541252416195,4.20974795248405,133.351099474067));
#35808=CARTESIAN_POINT('Ctrl Pts',(139.533487663247,4.27900497463091,133.232953041084));
#35809=CARTESIAN_POINT('Ctrl Pts',(139.5257229103,4.34327252617964,133.111992916229));
#35810=CARTESIAN_POINT('Ctrl Pts',(139.517965869415,4.40747624629011,132.991152930675));
#35811=CARTESIAN_POINT('Ctrl Pts',(139.51020882853,4.46670017544205,132.86750515765));
#35812=CARTESIAN_POINT('Ctrl Pts',(139.502451787645,4.52069420746963,132.741499472953));
#35813=CARTESIAN_POINT('Ctrl Pts',(139.494700596405,4.57464752217768,132.615588810124));
#35814=CARTESIAN_POINT('Ctrl Pts',(139.486949405165,4.62337863650188,132.487324132771));
#35815=CARTESIAN_POINT('Ctrl Pts',(139.479198213925,4.6666839058364,132.357178825054));
#35816=CARTESIAN_POINT('Ctrl Pts',(139.471450317148,4.70997076927626,132.227088832565));
#35817=CARTESIAN_POINT('Ctrl Pts',(139.463702420371,4.74783625126156,132.095120169686));
#35818=CARTESIAN_POINT('Ctrl Pts',(139.455954523594,4.7801253646084,131.961764851672));
#35819=CARTESIAN_POINT('Ctrl Pts',(139.44820824751,4.8124077237688,131.828437428716));
#35820=CARTESIAN_POINT('Ctrl Pts',(139.440461971426,4.83911594248892,131.693724307312));
#35821=CARTESIAN_POINT('Ctrl Pts',(139.432715695341,4.8601454142007,131.558130884507));
#35822=CARTESIAN_POINT('Ctrl Pts',(139.424969362076,4.88117504114725,131.422536460782));
#35823=CARTESIAN_POINT('Ctrl Pts',(139.417223028811,4.89652577751942,131.286062109037));
#35824=CARTESIAN_POINT('Ctrl Pts',(139.409476695545,4.90614453919853,131.14922120243));
#35825=CARTESIAN_POINT('Ctrl Pts',(139.401728627542,4.91576545493262,131.01234965125));
#35826=CARTESIAN_POINT('Ctrl Pts',(139.393980559539,4.91965181427796,130.875111771793));
#35827=CARTESIAN_POINT('Ctrl Pts',(139.386232491536,4.91780260259638,130.738023415362));
#35828=CARTESIAN_POINT('Ctrl Pts',(139.378476188795,4.91595142555062,130.600789359794));
#35829=CARTESIAN_POINT('Ctrl Pts',(139.370719886053,4.90835250567635,130.463705536255));
#35830=CARTESIAN_POINT('Ctrl Pts',(139.362963583311,4.895056954802,130.327285705477));
#35831=CARTESIAN_POINT('Ctrl Pts',(139.355203140797,4.88175430769182,130.190793063328));
#35832=CARTESIAN_POINT('Ctrl Pts',(139.347442698283,4.86274902535104,130.054965507103));
#35833=CARTESIAN_POINT('Ctrl Pts',(139.339682255768,4.83814366593952,129.920308056782));
#35834=CARTESIAN_POINT('Ctrl Pts',(139.331909355503,4.81349880782071,129.785434442367));
#35835=CARTESIAN_POINT('Ctrl Pts',(139.324136455238,4.78323599462548,129.651735068953));
#35836=CARTESIAN_POINT('Ctrl Pts',(139.316363554972,4.74750834874858,129.519702086647));
#35837=CARTESIAN_POINT('Ctrl Pts',(139.30887321921,4.71307949279179,129.392468835819));
#35838=CARTESIAN_POINT('Ctrl Pts',(139.301382883448,4.67357631930266,129.266783218347));
#35839=CARTESIAN_POINT('Ctrl Pts',(139.293892547686,4.62917790747561,129.143067457573));
#35840=CARTESIAN_POINT('Ctrl Pts',(139.286118213567,4.5830961163696,129.014660976127));
#35841=CARTESIAN_POINT('Ctrl Pts',(139.278343879448,4.53159458001806,128.887969921171));
#35842=CARTESIAN_POINT('Ctrl Pts',(139.270569545329,4.47481986737682,128.763485751968));
#35843=CARTESIAN_POINT('Ctrl Pts',(139.262804792382,4.41811512449481,128.639154998378));
#35844=CARTESIAN_POINT('Ctrl Pts',(139.255040039435,4.35615029651326,128.517026071271));
#35845=CARTESIAN_POINT('Ctrl Pts',(139.247275286487,4.28912129913806,128.397574057902));
#35846=CARTESIAN_POINT('Ctrl Pts',(139.239518245602,4.22215887590799,128.278240685956));
#35847=CARTESIAN_POINT('Ctrl Pts',(139.231761204717,4.15014248290613,128.161579275467));
#35848=CARTESIAN_POINT('Ctrl Pts',(139.224004163832,4.07331542489305,128.048043416693));
#35849=CARTESIAN_POINT('Ctrl Pts',(139.216252972592,3.99654630276211,127.934593176194));
#35850=CARTESIAN_POINT('Ctrl Pts',(139.208501781352,3.91497395467671,127.824264118428));
#35851=CARTESIAN_POINT('Ctrl Pts',(139.200750590112,3.82888657725357,127.717483451071));
#35852=CARTESIAN_POINT('Ctrl Pts',(139.193002693335,3.74283578926224,127.610748168346));
#35853=CARTESIAN_POINT('Ctrl Pts',(139.185254796558,3.6522740335642,127.507558580146));
#35854=CARTESIAN_POINT('Ctrl Pts',(139.177506899781,3.55753148216963,127.408311027841));
#35855=CARTESIAN_POINT('Ctrl Pts',(139.169760623697,3.46280874887439,127.309084235984));
#35856=CARTESIAN_POINT('Ctrl Pts',(139.162014347613,3.36390722916566,127.213798122489));
#35857=CARTESIAN_POINT('Ctrl Pts',(139.154268071529,3.26119558548824,127.122813875272));
#35858=CARTESIAN_POINT('Ctrl Pts',(139.146521738263,3.15848318361686,127.031828956431));
#35859=CARTESIAN_POINT('Ctrl Pts',(139.138775404998,3.05196089431073,126.945146226476));
#35860=CARTESIAN_POINT('Ctrl Pts',(139.131029071732,2.9420319396852,126.863087837312));
#35861=CARTESIAN_POINT('Ctrl Pts',(139.123281003729,2.83207836723248,126.78101107174));
#35862=CARTESIAN_POINT('Ctrl Pts',(139.115532935726,2.71871692462217,126.703560941487));
#35863=CARTESIAN_POINT('Ctrl Pts',(139.107784867724,2.60238106372923,126.631017130427));
#35864=CARTESIAN_POINT('Ctrl Pts',(139.100028564982,2.48592155969885,126.558396218941));
#35865=CARTESIAN_POINT('Ctrl Pts',(139.09227226224,2.36648165473367,126.490692250363));
#35866=CARTESIAN_POINT('Ctrl Pts',(139.084515959498,2.24452121748061,126.428139923088));
#35867=CARTESIAN_POINT('Ctrl Pts',(139.076755516984,2.12249568626994,126.365554209752));
#35868=CARTESIAN_POINT('Ctrl Pts',(139.06899507447,1.99794729704609,126.308125780131));
#35869=CARTESIAN_POINT('Ctrl Pts',(139.061234631955,1.87135637261259,126.256041324774));
#35870=CARTESIAN_POINT('Ctrl Pts',(139.05346173169,1.74456223318907,126.203873258826));
#35871=CARTESIAN_POINT('Ctrl Pts',(139.045688831425,1.61571937403047,126.157066443535));
#35872=CARTESIAN_POINT('Ctrl Pts',(139.037915931159,1.48532462135564,126.11575807185));
#35873=CARTESIAN_POINT('Ctrl Pts',(139.030425595397,1.35967004638484,126.075951363525));
#35874=CARTESIAN_POINT('Ctrl Pts',(139.022935259635,1.23257474661397,126.041250355883));
#35875=CARTESIAN_POINT('Ctrl Pts',(139.015444923873,1.10449074717846,126.011732606558));
#35876=CARTESIAN_POINT('Ctrl Pts',(139.007670589754,0.971550403974258,125.981095682796));
#35877=CARTESIAN_POINT('Ctrl Pts',(138.999896255635,0.837123792969694,125.955945774123));
#35878=CARTESIAN_POINT('Ctrl Pts',(138.992121921516,0.701703616862046,125.936425213662));
#35879=CARTESIAN_POINT('Ctrl Pts',(138.984357168569,0.566450334018694,125.916928710547));
#35880=CARTESIAN_POINT('Ctrl Pts',(138.976592415622,0.430206305673608,125.903047806997));
#35881=CARTESIAN_POINT('Ctrl Pts',(138.968827662675,0.293477133413694,125.894874469845));
#35882=CARTESIAN_POINT('Ctrl Pts',(138.96107062179,0.156883762495212,125.886709250567));
#35883=CARTESIAN_POINT('Ctrl Pts',(138.953313580905,0.0198065943118101,
125.884240339626));
#35884=CARTESIAN_POINT('Ctrl Pts',(138.94555654002,-0.117241240638398,125.887508214453));
#35885=CARTESIAN_POINT('Ctrl Pts',(138.937805348779,-0.254185726750192,
125.890773624951));
#35886=CARTESIAN_POINT('Ctrl Pts',(138.930054157539,-0.391100534385532,
125.899767200984));
#35887=CARTESIAN_POINT('Ctrl Pts',(138.922302966299,-0.527470464316749,
125.914477390763));
#35888=CARTESIAN_POINT('Ctrl Pts',(138.914555069522,-0.663782433390052,
125.929181328318));
#35889=CARTESIAN_POINT('Ctrl Pts',(138.906807172745,-0.799549597472776,
125.949597005261));
#35890=CARTESIAN_POINT('Ctrl Pts',(138.899059275968,-0.934260037308206,
125.97566087072));
#35891=CARTESIAN_POINT('Ctrl Pts',(138.891312999884,-1.06894229862355,126.001719284181));
#35892=CARTESIAN_POINT('Ctrl Pts',(138.8835667238,-1.20256789175668,126.033423461912));
#35893=CARTESIAN_POINT('Ctrl Pts',(138.875820447716,-1.33463366802653,126.070658468648));
#35894=CARTESIAN_POINT('Ctrl Pts',(138.86807411445,-1.46670041917602,126.107893750245));
#35895=CARTESIAN_POINT('Ctrl Pts',(138.860327781185,-1.59720695419146,126.150659836222));
#35896=CARTESIAN_POINT('Ctrl Pts',(138.85258144792,-1.72566428614893,126.198791615368));
#35897=CARTESIAN_POINT('Ctrl Pts',(138.844833379917,-1.85415038523523,126.246934173291));
#35898=CARTESIAN_POINT('Ctrl Pts',(138.837085311914,-1.98058600205685,126.300444678296));
#35899=CARTESIAN_POINT('Ctrl Pts',(138.829337243911,-2.10450153932347,126.359109631009));
#35900=CARTESIAN_POINT('Ctrl Pts',(138.821580941169,-2.22854877549763,126.417836933532));
#35901=CARTESIAN_POINT('Ctrl Pts',(138.813824638427,-2.35007022785446,126.481729459515));
#35902=CARTESIAN_POINT('Ctrl Pts',(138.806068335685,-2.46861986774926,126.550527168657));
#35903=CARTESIAN_POINT('Ctrl Pts',(138.798307893171,-2.5872327811565,126.619361597209));
#35904=CARTESIAN_POINT('Ctrl Pts',(138.790547450657,-2.70287039209385,126.693106215479));
#35905=CARTESIAN_POINT('Ctrl Pts',(138.782787008143,-2.81511600630547,126.771457825092));
#35906=CARTESIAN_POINT('Ctrl Pts',(138.775014107877,-2.92754180714165,126.849935211665));
#35907=CARTESIAN_POINT('Ctrl Pts',(138.767241207612,-3.03656441902054,126.93303413111));
#35908=CARTESIAN_POINT('Ctrl Pts',(138.759468307346,-3.14179987092302,127.020410745598));
#35909=CARTESIAN_POINT('Ctrl Pts',(138.751977971584,-3.24320974907617,127.10461100006));
#35910=CARTESIAN_POINT('Ctrl Pts',(138.744487635822,-3.34110280358922,127.192783133033));
#35911=CARTESIAN_POINT('Ctrl Pts',(138.73699730006,-3.43516945240252,127.284588764764));
#35912=CARTESIAN_POINT('Ctrl Pts',(138.729335950167,-3.5313837654499,127.37849043876));
#35913=CARTESIAN_POINT('Ctrl Pts',(138.721674600274,-3.62391849594263,127.476509765588));
#35914=CARTESIAN_POINT('Ctrl Pts',(138.714013250381,-3.71239276697578,127.578322334128));
#35915=CARTESIAN_POINT('Ctrl Pts',(138.706360830996,-3.80076390733441,127.680016224111));
#35916=CARTESIAN_POINT('Ctrl Pts',(138.698708411611,-3.88508373587602,127.785494264888));
#35917=CARTESIAN_POINT('Ctrl Pts',(138.691055992225,-3.96500618700098,127.894393435699));
#35918=CARTESIAN_POINT('Ctrl Pts',(138.68341072122,-4.0448539799082,128.003190880175));
#35919=CARTESIAN_POINT('Ctrl Pts',(138.675765450214,-4.12031232660955,128.115402777161));
#35920=CARTESIAN_POINT('Ctrl Pts',(138.668120179208,-4.19107402046465,128.230631490893));
#35921=CARTESIAN_POINT('Ctrl Pts',(138.660480495053,-4.26178400456586,128.34577600019));
#35922=CARTESIAN_POINT('Ctrl Pts',(138.652840810899,-4.32780395415916,128.463932597832));
#35923=CARTESIAN_POINT('Ctrl Pts',(138.645201126745,-4.38886911884744,128.584673495441));
#35924=CARTESIAN_POINT('Ctrl Pts',(138.63756474466,-4.4499078895902,128.705362205708));
#35925=CARTESIAN_POINT('Ctrl Pts',(138.629928362575,-4.50599595419598,128.828632634724));
#35926=CARTESIAN_POINT('Ctrl Pts',(138.62229198049,-4.5569140238837,128.954031554553));
#35927=CARTESIAN_POINT('Ctrl Pts',(138.614655941915,-4.60782980310321,129.079424833511));
#35928=CARTESIAN_POINT('Ctrl Pts',(138.607019903341,-4.65357589110573,129.206946042359));
#35929=CARTESIAN_POINT('Ctrl Pts',(138.599383864766,-4.69398089638185,129.336121397649));
#35930=CARTESIAN_POINT('Ctrl Pts',(138.594565770404,-4.71947515315274,129.417626885738));
#35931=CARTESIAN_POINT('Ctrl Pts',(138.589747676042,-4.74284398389356,129.49979052884));
#35932=CARTESIAN_POINT('Ctrl Pts',(138.584929581679,-4.76405452823406,129.582490119308));
#35933=CARTESIAN_POINT('Ctrl Pts',(140.334586805861,-4.76405452823407,129.582490119308));
#35934=CARTESIAN_POINT('Ctrl Pts',(140.326498474831,-4.79955665325446,129.720912365943));
#35935=CARTESIAN_POINT('Ctrl Pts',(140.318410143802,-4.82905709203218,129.861021019605));
#35936=CARTESIAN_POINT('Ctrl Pts',(140.310321812772,-4.85240638469056,130.002278738757));
#35937=CARTESIAN_POINT('Ctrl Pts',(140.302246511742,-4.87571806251177,130.143308897006));
#35938=CARTESIAN_POINT('Ctrl Pts',(140.294171210711,-4.89289829758937,130.285484095697));
#35939=CARTESIAN_POINT('Ctrl Pts',(140.28609590968,-4.90384827356347,130.428255349897));
#35940=CARTESIAN_POINT('Ctrl Pts',(140.279017085117,-4.91344704376335,130.553408908539));
#35941=CARTESIAN_POINT('Ctrl Pts',(140.271938260554,-4.91825899936649,130.679020142658));
#35942=CARTESIAN_POINT('Ctrl Pts',(140.264859435991,-4.91824998735844,130.804713248748));
#35943=CARTESIAN_POINT('',(140.610140563957,-4.9182480184558,130.799945704706));
#35944=CARTESIAN_POINT('Ctrl Pts',(140.680140489264,-4.76405452823406,129.582490119308));
#35945=CARTESIAN_POINT('Ctrl Pts',(140.675607549706,-4.78385088850951,129.659675827571));
#35946=CARTESIAN_POINT('Ctrl Pts',(140.671074610149,-4.80175451530272,129.737278628265));
#35947=CARTESIAN_POINT('Ctrl Pts',(140.666541670591,-4.8177525850657,129.815197793966));
#35948=CARTESIAN_POINT('Ctrl Pts',(140.655452150913,-4.85689074413086,130.005821584622));
#35949=CARTESIAN_POINT('Ctrl Pts',(140.644362631235,-4.88472582398956,130.198838737255));
#35950=CARTESIAN_POINT('Ctrl Pts',(140.633273111557,-4.90102881052903,130.393143326022));
#35951=CARTESIAN_POINT('Ctrl Pts',(140.625562262374,-4.91236472715027,130.528248670805));
#35952=CARTESIAN_POINT('Ctrl Pts',(140.617851413191,-4.91812596406356,130.663976169357));
#35953=CARTESIAN_POINT('Ctrl Pts',(140.610140564008,-4.91824801845499,130.799945703804));
#35954=CARTESIAN_POINT('Ctrl Pts',(140.610140563957,-4.9182480184558,130.799945704706));
#35955=CARTESIAN_POINT('Ctrl Pts',(140.60249225751,-4.91836908283874,130.934812389576));
#35956=CARTESIAN_POINT('Ctrl Pts',(140.594843951064,-4.91293857030097,131.069858143507));
#35957=CARTESIAN_POINT('Ctrl Pts',(140.587195644617,-4.90193906657004,131.204581119458));
#35958=CARTESIAN_POINT('Ctrl Pts',(140.579553673181,-4.89094867361067,131.339192505806));
#35959=CARTESIAN_POINT('Ctrl Pts',(140.571911701746,-4.87439849772661,131.473481246169));
#35960=CARTESIAN_POINT('Ctrl Pts',(140.56426973031,-4.85232318791553,131.606945655127));
#35961=CARTESIAN_POINT('Ctrl Pts',(140.556631611151,-4.83025900615042,131.740342785388));
#35962=CARTESIAN_POINT('Ctrl Pts',(140.548993491992,-4.8026752939131,131.87291601369));
#35963=CARTESIAN_POINT('Ctrl Pts',(140.541355372833,-4.7696584828474,132.00416936045));
#35964=CARTESIAN_POINT('Ctrl Pts',(140.533719138739,-4.73664982023216,132.135390314277));
#35965=CARTESIAN_POINT('Ctrl Pts',(140.526082904645,-4.69821082266585,132.265291643392));
#35966=CARTESIAN_POINT('Ctrl Pts',(140.518446670551,-4.65447880598773,132.393388656057));
#35967=CARTESIAN_POINT('Ctrl Pts',(140.510810556802,-4.61074747851223,132.521483649954));
#35968=CARTESIAN_POINT('Ctrl Pts',(140.503174443053,-4.56172342825247,132.6477740024));
#35969=CARTESIAN_POINT('Ctrl Pts',(140.495538329304,-4.5075933291255,132.771791795962));
#35970=CARTESIAN_POINT('Ctrl Pts',(140.487900571483,-4.45345157567036,132.895836290825));
#35971=CARTESIAN_POINT('Ctrl Pts',(140.480262813661,-4.39420174905913,133.017606884614));
#35972=CARTESIAN_POINT('Ctrl Pts',(140.47262505584,-4.33007774905487,133.136657714773));
#35973=CARTESIAN_POINT('Ctrl Pts',(140.464979447087,-4.26588783531267,133.255830918539));
#35974=CARTESIAN_POINT('Ctrl Pts',(140.457333838334,-4.19681393595512,133.372278421314));
#35975=CARTESIAN_POINT('Ctrl Pts',(140.449688229581,-4.12313496391443,133.485580700261));
#35976=CARTESIAN_POINT('Ctrl Pts',(140.44203839766,-4.04941529418598,133.598945563424));
#35977=CARTESIAN_POINT('Ctrl Pts',(140.43438856574,-3.97108572103642,133.709161416099));
#35978=CARTESIAN_POINT('Ctrl Pts',(140.42673873382,-3.88846638952164,133.815840685582));
#35979=CARTESIAN_POINT('Ctrl Pts',(140.419077375535,-3.80572257154178,133.922680693781));
#35980=CARTESIAN_POINT('Ctrl Pts',(140.411416017251,-3.71867634798768,134.025973170753));
#35981=CARTESIAN_POINT('Ctrl Pts',(140.403754658966,-3.62768608616077,134.125365995878));
#35982=CARTESIAN_POINT('Ctrl Pts',(140.398534454903,-3.56568823711147,134.193089082337));
#35983=CARTESIAN_POINT('Ctrl Pts',(140.393314250841,-3.50186008474626,134.259002485839));
#35984=CARTESIAN_POINT('Ctrl Pts',(140.388094046778,-3.4363236504197,134.323005645423));
#35985=CARTESIAN_POINT('Ctrl Pts',(140.380319712659,-3.33872169246614,134.418324131314));
#35986=CARTESIAN_POINT('Ctrl Pts',(140.37254537854,-3.23699614572452,134.509729518424));
#35987=CARTESIAN_POINT('Ctrl Pts',(140.364771044421,-3.13149376771814,134.596843952433));
#35988=CARTESIAN_POINT('Ctrl Pts',(140.357006291474,-3.0261214119637,134.683851025688));
#35989=CARTESIAN_POINT('Ctrl Pts',(140.349241538527,-2.91698178480588,134.766577421275));
#35990=CARTESIAN_POINT('Ctrl Pts',(140.341476785579,-2.80445885965293,134.844681590832));
#35991=CARTESIAN_POINT('Ctrl Pts',(140.333719744694,-2.69204769385554,134.922708186226));
#35992=CARTESIAN_POINT('Ctrl Pts',(140.325962703809,-2.57626023638771,134.996121470117));
#35993=CARTESIAN_POINT('Ctrl Pts',(140.318205662924,-2.45751367449571,135.06461995265));
#35994=CARTESIAN_POINT('Ctrl Pts',(140.310454471684,-2.33885666031007,135.133066779944));
#35995=CARTESIAN_POINT('Ctrl Pts',(140.302703280444,-2.21724532062262,135.196605988461));
#35996=CARTESIAN_POINT('Ctrl Pts',(140.294952089204,-2.09312567401196,135.254979448166));
#35997=CARTESIAN_POINT('Ctrl Pts',(140.287204192427,-1.96905878156185,135.313328097594));
#35998=CARTESIAN_POINT('Ctrl Pts',(140.27945629565,-1.84248605562609,135.366515199012));
#35999=CARTESIAN_POINT('Ctrl Pts',(140.271708398873,-1.71387776234049,135.414328738742));
#36000=CARTESIAN_POINT('Ctrl Pts',(140.263962122789,-1.58529637113728,135.46213227691));
#36001=CARTESIAN_POINT('Ctrl Pts',(140.256215846705,-1.45468062574428,135.504564352998));
#36002=CARTESIAN_POINT('Ctrl Pts',(140.248469570621,-1.32252003081739,135.541461400807));
#36003=CARTESIAN_POINT('Ctrl Pts',(140.240723237355,-1.19035846031128,135.578358720982));
#36004=CARTESIAN_POINT('Ctrl Pts',(140.23297690409,-1.05665239408112,135.609720826216));
#36005=CARTESIAN_POINT('Ctrl Pts',(140.225230570825,-0.92190534231808,135.635434370088));
#36006=CARTESIAN_POINT('Ctrl Pts',(140.217482502822,-0.787128114886699,
135.661153672329));
#36007=CARTESIAN_POINT('Ctrl Pts',(140.209734434819,-0.651309821999467,
135.681221822821));
#36008=CARTESIAN_POINT('Ctrl Pts',(140.201986366816,-0.514962584507861,
135.695576887479));
#36009=CARTESIAN_POINT('Ctrl Pts',(140.194230064074,-0.378470435549882,
135.70994720887));
#36010=CARTESIAN_POINT('Ctrl Pts',(140.186473761332,-0.241448608431359,
135.71859227408));
#36011=CARTESIAN_POINT('Ctrl Pts',(140.17871745859,-0.104413304656748,135.721502157558));
#36012=CARTESIAN_POINT('Ctrl Pts',(140.170957016076,0.0326951389856347,
135.724413594127));
#36013=CARTESIAN_POINT('Ctrl Pts',(140.163196573562,0.169816682925836,135.721583757646));
#36014=CARTESIAN_POINT('Ctrl Pts',(140.155436131048,0.306437728970503,135.713054841162));
#36015=CARTESIAN_POINT('Ctrl Pts',(140.147663230782,0.443278091246834,135.704512233304));
#36016=CARTESIAN_POINT('Ctrl Pts',(140.139890330517,0.579615961023312,135.69025230418));
#36017=CARTESIAN_POINT('Ctrl Pts',(140.132117430251,0.714944547821106,135.670368977201));
#36018=CARTESIAN_POINT('Ctrl Pts',(140.124627094489,0.845353599618035,135.651208459241));
#36019=CARTESIAN_POINT('Ctrl Pts',(140.117136758727,0.974825171711792,135.626826351559));
#36020=CARTESIAN_POINT('Ctrl Pts',(140.109646422965,1.10291884522271,135.597350611646));
#36021=CARTESIAN_POINT('Ctrl Pts',(140.101872088846,1.2358692292968,135.566757290096));
#36022=CARTESIAN_POINT('Ctrl Pts',(140.094097754727,1.36775631300523,135.530579551038));
#36023=CARTESIAN_POINT('Ctrl Pts',(140.086323420608,1.49807476589744,135.488904891909));
#36024=CARTESIAN_POINT('Ctrl Pts',(140.07855866766,1.62823261294354,135.447281593073));
#36025=CARTESIAN_POINT('Ctrl Pts',(140.070793914713,1.75682530684741,135.40017497127));
#36026=CARTESIAN_POINT('Ctrl Pts',(140.063029161766,1.88335794629106,135.347723458969));
#36027=CARTESIAN_POINT('Ctrl Pts',(140.055272120881,2.00976491173341,135.29532404225));
#36028=CARTESIAN_POINT('Ctrl Pts',(140.047515079996,2.13411553567006,135.237590448173));
#36029=CARTESIAN_POINT('Ctrl Pts',(140.039758039111,2.25593066625146,135.174710705553));
#36030=CARTESIAN_POINT('Ctrl Pts',(140.032006847871,2.37765393509472,135.111878381036));
#36031=CARTESIAN_POINT('Ctrl Pts',(140.024255656631,2.49684517036757,135.04390781098));
#36032=CARTESIAN_POINT('Ctrl Pts',(140.016504465391,2.61304611602351,134.971034717857));
#36033=CARTESIAN_POINT('Ctrl Pts',(140.008756568614,2.7291976731781,134.898192597742));
#36034=CARTESIAN_POINT('Ctrl Pts',(140.001008671837,2.84236113801716,134.82045230617));
#36035=CARTESIAN_POINT('Ctrl Pts',(139.99326077506,2.95210394709466,134.738094892787));
#36036=CARTESIAN_POINT('Ctrl Pts',(139.985514498976,3.06182380034236,134.655754706799));
#36037=CARTESIAN_POINT('Ctrl Pts',(139.977768222891,3.16812410854656,134.568799554557));
#36038=CARTESIAN_POINT('Ctrl Pts',(139.970021946807,3.27060266960694,134.477552858664));
#36039=CARTESIAN_POINT('Ctrl Pts',(139.962275613542,3.37308198714057,134.386305489208));
#36040=CARTESIAN_POINT('Ctrl Pts',(139.954529280277,3.47173920924471,134.290766772877));
#36041=CARTESIAN_POINT('Ctrl Pts',(139.946782947011,3.56620681480678,134.191299060545));
#36042=CARTESIAN_POINT('Ctrl Pts',(139.939034879008,3.66069557573445,134.091809073107));
#36043=CARTESIAN_POINT('Ctrl Pts',(139.931286811005,3.75099258395434,133.98838862226));
#36044=CARTESIAN_POINT('Ctrl Pts',(139.923538743002,3.83676891873799,133.881435092893));
#36045=CARTESIAN_POINT('Ctrl Pts',(139.91578244026,3.92263641763087,133.774367892042));
#36046=CARTESIAN_POINT('Ctrl Pts',(139.908026137518,4.00397340033536,133.663760417141));
#36047=CARTESIAN_POINT('Ctrl Pts',(139.900269834777,4.0804924966803,133.550041598131));
#36048=CARTESIAN_POINT('Ctrl Pts',(139.892509392262,4.15705243357075,133.436262083963));
#36049=CARTESIAN_POINT('Ctrl Pts',(139.884748949748,4.22878915587345,133.319368249822));
#36050=CARTESIAN_POINT('Ctrl Pts',(139.876988507234,4.29546054942528,133.199815006786));
#36051=CARTESIAN_POINT('Ctrl Pts',(139.869215606969,4.36223896981695,133.08006984627));
#36052=CARTESIAN_POINT('Ctrl Pts',(139.861442706703,4.42393563643457,132.957657095128));
#36053=CARTESIAN_POINT('Ctrl Pts',(139.853669806438,4.48035563707092,132.833053898441));
#36054=CARTESIAN_POINT('Ctrl Pts',(139.846179470676,4.53472462857017,132.712980341811));
#36055=CARTESIAN_POINT('Ctrl Pts',(139.838689134914,4.58419381807425,132.590873116617));
#36056=CARTESIAN_POINT('Ctrl Pts',(139.831198799152,4.62863280268317,132.467171923886));
#36057=CARTESIAN_POINT('Ctrl Pts',(139.823424465033,4.67475670490096,132.338780562833));
#36058=CARTESIAN_POINT('Ctrl Pts',(139.815650130914,4.71560753869031,132.208265272421));
#36059=CARTESIAN_POINT('Ctrl Pts',(139.807875796795,4.75098577467072,132.076098495974));
#36060=CARTESIAN_POINT('Ctrl Pts',(139.800111043848,4.78632041013706,131.944094603266));
#36061=CARTESIAN_POINT('Ctrl Pts',(139.792346290901,4.81619576719131,131.810443648223));
#36062=CARTESIAN_POINT('Ctrl Pts',(139.784581537953,4.84046080673972,131.675636831471));
#36063=CARTESIAN_POINT('Ctrl Pts',(139.776824497069,4.86470174590874,131.54096390675));
#36064=CARTESIAN_POINT('Ctrl Pts',(139.769067456183,4.88334338778184,131.40513778722));
#36065=CARTESIAN_POINT('Ctrl Pts',(139.761310415299,4.89628493304807,131.26866323107));
#36066=CARTESIAN_POINT('Ctrl Pts',(139.753559224058,4.90921671899439,131.132291591443));
#36067=CARTESIAN_POINT('Ctrl Pts',(139.745808032818,4.91645692745254,130.995272876148));
#36068=CARTESIAN_POINT('Ctrl Pts',(139.738056841578,4.91795617982778,130.858120042728));
#36069=CARTESIAN_POINT('Ctrl Pts',(139.730308944801,4.91945479498077,130.721025502921));
#36070=CARTESIAN_POINT('Ctrl Pts',(139.722561048024,4.91521730287863,130.583797348489));
#36071=CARTESIAN_POINT('Ctrl Pts',(139.714813151247,4.90524634744008,130.44695142151));
#36072=CARTESIAN_POINT('Ctrl Pts',(139.707066875163,4.89527747771046,130.310134119748));
#36073=CARTESIAN_POINT('Ctrl Pts',(139.699320599079,4.87957755854499,130.17369927609));
#36074=CARTESIAN_POINT('Ctrl Pts',(139.691574322995,4.85820129448045,130.038160092371));
#36075=CARTESIAN_POINT('Ctrl Pts',(139.683827989729,4.83682487262119,129.902619908134));
#36076=CARTESIAN_POINT('Ctrl Pts',(139.676081656464,4.80977208315887,129.76797578322));
#36077=CARTESIAN_POINT('Ctrl Pts',(139.668335323199,4.77714912800754,129.634732783049));
#36078=CARTESIAN_POINT('Ctrl Pts',(139.660587255196,4.74451886717173,129.501459944033));
#36079=CARTESIAN_POINT('Ctrl Pts',(139.652839187193,4.70631605142454,129.369589233806));
#36080=CARTESIAN_POINT('Ctrl Pts',(139.64509111919,4.6626972222413,129.239612178933));
#36081=CARTESIAN_POINT('Ctrl Pts',(139.637334816448,4.61903203444713,129.109496982899));
#36082=CARTESIAN_POINT('Ctrl Pts',(139.629578513706,4.56993945916475,128.981279833845));
#36083=CARTESIAN_POINT('Ctrl Pts',(139.621822210964,4.51562503670479,128.855434351545));
#36084=CARTESIAN_POINT('Ctrl Pts',(139.61406176845,4.4612816250022,128.729521701722));
#36085=CARTESIAN_POINT('Ctrl Pts',(139.606301325936,4.40171098240527,128.605983592915));
#36086=CARTESIAN_POINT('Ctrl Pts',(139.598540883422,4.33716496986913,128.485269613177));
#36087=CARTESIAN_POINT('Ctrl Pts',(139.590767983156,4.27251534234354,128.364361852641));
#36088=CARTESIAN_POINT('Ctrl Pts',(139.582995082891,4.2028745832306,128.246287617585));
#36089=CARTESIAN_POINT('Ctrl Pts',(139.575222182625,4.12853877339113,128.131468801741));
#36090=CARTESIAN_POINT('Ctrl Pts',(139.567731846863,4.05690525747929,128.020823939062));
#36091=CARTESIAN_POINT('Ctrl Pts',(139.560241511101,3.980912295945,127.913202171038));
#36092=CARTESIAN_POINT('Ctrl Pts',(139.552751175339,3.9008593357625,127.808950878466));
#36093=CARTESIAN_POINT('Ctrl Pts',(139.54497684122,3.81777114326387,127.700746866451));
#36094=CARTESIAN_POINT('Ctrl Pts',(139.537202507101,3.73004580655604,127.595831200548));
#36095=CARTESIAN_POINT('Ctrl Pts',(139.529428172982,3.63797295508169,127.494627117631));
#36096=CARTESIAN_POINT('Ctrl Pts',(139.521663420035,3.54601357516793,127.393547759701));
#36097=CARTESIAN_POINT('Ctrl Pts',(139.513898667088,3.44971760173233,127.29617116989));
#36098=CARTESIAN_POINT('Ctrl Pts',(139.506133914141,3.34941665545385,127.202889927602));
#36099=CARTESIAN_POINT('Ctrl Pts',(139.498376873256,3.24921532948975,127.10970133356));
#36100=CARTESIAN_POINT('Ctrl Pts',(139.490619832371,3.14501723111356,127.02060025695));
#36101=CARTESIAN_POINT('Ctrl Pts',(139.482862791486,3.03719254319538,126.935944337218));
#36102=CARTESIAN_POINT('Ctrl Pts',(139.475111600246,2.92944916671276,126.851352257174));
#36103=CARTESIAN_POINT('Ctrl Pts',(139.467360409006,2.81808495048683,126.77119890226));
#36104=CARTESIAN_POINT('Ctrl Pts',(139.459609217766,2.70350476989094,126.695803082168));
#36105=CARTESIAN_POINT('Ctrl Pts',(139.451861320988,2.58897328892809,126.620439307311));
#36106=CARTESIAN_POINT('Ctrl Pts',(139.444113424211,2.47122888811353,126.549829259974));
#36107=CARTESIAN_POINT('Ctrl Pts',(139.436365527434,2.3507069890986,126.484249540996));
#36108=CARTESIAN_POINT('Ctrl Pts',(139.42861925135,2.2302103006668,126.418683539882));
#36109=CARTESIAN_POINT('Ctrl Pts',(139.420872975266,2.10693761286098,126.358145960917));
#36110=CARTESIAN_POINT('Ctrl Pts',(139.413126699182,1.9813502660582,126.302868177753));
#36111=CARTESIAN_POINT('Ctrl Pts',(139.405380365917,1.85576199219824,126.247589986542));
#36112=CARTESIAN_POINT('Ctrl Pts',(139.397634032651,1.72785938308289,126.197571826109));
#36113=CARTESIAN_POINT('Ctrl Pts',(139.389887699386,1.59812476928206,126.152997345975));
#36114=CARTESIAN_POINT('Ctrl Pts',(139.382139631383,1.46836110231381,126.108412883694));
#36115=CARTESIAN_POINT('Ctrl Pts',(139.37439156338,1.33676498395961,126.069274654544));
#36116=CARTESIAN_POINT('Ctrl Pts',(139.366643495377,1.20383456393023,126.03571663786));
#36117=CARTESIAN_POINT('Ctrl Pts',(139.358887192635,1.07076286386856,126.002122955317));
#36118=CARTESIAN_POINT('Ctrl Pts',(139.351130889893,0.936354408977907,125.974121428334));
#36119=CARTESIAN_POINT('Ctrl Pts',(139.343374587152,0.801118768546406,125.951795133084));
#36120=CARTESIAN_POINT('Ctrl Pts',(139.335614144637,0.665810948781648,125.929456921618));
#36121=CARTESIAN_POINT('Ctrl Pts',(139.327853702123,0.529675451643455,125.912800024967));
#36122=CARTESIAN_POINT('Ctrl Pts',(139.320093259609,0.393226665291511,125.9018555587));
#36123=CARTESIAN_POINT('Ctrl Pts',(139.312320359344,0.256558839234639,125.890893523405));
#36124=CARTESIAN_POINT('Ctrl Pts',(139.304547459078,0.119577109875557,125.885662258204));
#36125=CARTESIAN_POINT('Ctrl Pts',(139.296774558813,-0.0172035327036181,
125.886140705752));
#36126=CARTESIAN_POINT('Ctrl Pts',(139.289284223051,-0.14901185439539,125.886601760527));
#36127=CARTESIAN_POINT('Ctrl Pts',(139.281793887289,-0.28063314778043,125.892364596873));
#36128=CARTESIAN_POINT('Ctrl Pts',(139.274303551527,-0.411613293150797,
125.903365049378));
#36129=CARTESIAN_POINT('Ctrl Pts',(139.266529217408,-0.547559590543532,
125.914782587383));
#36130=CARTESIAN_POINT('Ctrl Pts',(139.258754883288,-0.683245798935054,
125.931878917537));
#36131=CARTESIAN_POINT('Ctrl Pts',(139.250980549169,-0.818159285368155,
125.954639136257));
#36132=CARTESIAN_POINT('Ctrl Pts',(139.243215796222,-0.952906502987066,
125.977371305042));
#36133=CARTESIAN_POINT('Ctrl Pts',(139.235451043275,-1.08688251164536,126.005753409389));
#36134=CARTESIAN_POINT('Ctrl Pts',(139.227686290328,-1.21957777409472,126.039718646186));
#36135=CARTESIAN_POINT('Ctrl Pts',(139.219929249443,-1.35214124173875,126.073650148231));
#36136=CARTESIAN_POINT('Ctrl Pts',(139.212172208558,-1.48342611831749,126.113153651117));
#36137=CARTESIAN_POINT('Ctrl Pts',(139.204415167673,-1.61293141875301,126.158111022366));
#36138=CARTESIAN_POINT('Ctrl Pts',(139.196663976433,-1.74233905823345,126.203034490911));
#36139=CARTESIAN_POINT('Ctrl Pts',(139.188912785193,-1.86996942487607,126.253403513835));
#36140=CARTESIAN_POINT('Ctrl Pts',(139.181161593953,-1.99533545002837,126.309049782445));
#36141=CARTESIAN_POINT('Ctrl Pts',(139.173413697175,-2.1206481912759,126.364672399906));
#36142=CARTESIAN_POINT('Ctrl Pts',(139.165665800398,-2.24369814858787,126.425567643674));
#36143=CARTESIAN_POINT('Ctrl Pts',(139.157917903621,-2.36401725380633,126.491518690692));
#36144=CARTESIAN_POINT('Ctrl Pts',(139.150171627537,-2.484311190862,126.557455942172));
#36145=CARTESIAN_POINT('Ctrl Pts',(139.142425351453,-2.60187506942021,126.628446705544));
#36146=CARTESIAN_POINT('Ctrl Pts',(139.134679075369,-2.71626486253243,126.704227905193));
#36147=CARTESIAN_POINT('Ctrl Pts',(139.126932742104,-2.83065550004381,126.780009664241));
#36148=CARTESIAN_POINT('Ctrl Pts',(139.119186408838,-2.94187167942476,126.860581714205));
#36149=CARTESIAN_POINT('Ctrl Pts',(139.111440075573,-3.04949817968013,126.945637523766));
#36150=CARTESIAN_POINT('Ctrl Pts',(139.10369200757,-3.15714878214377,127.030712380985));
#36151=CARTESIAN_POINT('Ctrl Pts',(139.095943939567,-3.26120779916445,127.120272753491));
#36152=CARTESIAN_POINT('Ctrl Pts',(139.088195871564,-3.36129324804418,127.213971952929));
#36153=CARTESIAN_POINT('Ctrl Pts',(139.080439568822,-3.46148506893041,127.307770736992));
#36154=CARTESIAN_POINT('Ctrl Pts',(139.07268326608,-3.55769459960266,127.405716867427));
#36155=CARTESIAN_POINT('Ctrl Pts',(139.064926963338,-3.64957651107725,127.507426533861));
#36156=CARTESIAN_POINT('Ctrl Pts',(139.057166520824,-3.74150746269457,127.609190485807));
#36157=CARTESIAN_POINT('Ctrl Pts',(139.04940607831,-3.82910594309253,127.7147216756));
#36158=CARTESIAN_POINT('Ctrl Pts',(139.041645635796,-3.91206773449635,127.823604152638));
#36159=CARTESIAN_POINT('Ctrl Pts',(139.03387273553,-3.99516270353274,127.932661417493));
#36160=CARTESIAN_POINT('Ctrl Pts',(139.026099835265,-4.0736058857865,128.045080399306));
#36161=CARTESIAN_POINT('Ctrl Pts',(139.018326935,-4.147136632681,128.160416440323));
#36162=CARTESIAN_POINT('Ctrl Pts',(139.010836599238,-4.21799435171278,128.271559725735));
#36163=CARTESIAN_POINT('Ctrl Pts',(139.003346263476,-4.28429043838581,128.385411401379));
#36164=CARTESIAN_POINT('Ctrl Pts',(138.995855927714,-4.34583341408507,128.501554720509));
#36165=CARTESIAN_POINT('Ctrl Pts',(138.987632903478,-4.4133963908017,128.629058928373));
#36166=CARTESIAN_POINT('Ctrl Pts',(138.979409879243,-4.47542512871843,128.759691239174));
#36167=CARTESIAN_POINT('Ctrl Pts',(138.971186855008,-4.53163609976733,128.89295869181));
#36168=CARTESIAN_POINT('Ctrl Pts',(138.962982749488,-4.58771774621055,129.025919535958));
#36169=CARTESIAN_POINT('Ctrl Pts',(138.954778643968,-4.63800818801278,129.161503136765));
#36170=CARTESIAN_POINT('Ctrl Pts',(138.946574538448,-4.68227009606823,129.299192915958));
#36171=CARTESIAN_POINT('Ctrl Pts',(138.941002400578,-4.71233229523069,129.392710293463));
#36172=CARTESIAN_POINT('Ctrl Pts',(138.935430262708,-4.73961446584328,129.487198686976));
#36173=CARTESIAN_POINT('Ctrl Pts',(138.929858124837,-4.76405452823407,129.582490119308));
#36174=CARTESIAN_POINT('Origin',(213.235140564004,0.,130.804360617566));
#36175=CARTESIAN_POINT('',(136.834948208849,-4.76405452823407,129.582490119308));
#36176=CARTESIAN_POINT('',(137.180179986924,-4.76405452823403,129.582490119308));
#36177=CARTESIAN_POINT('',(213.235140564004,-4.76405452823405,129.582490119308));
#36178=CARTESIAN_POINT('',(138.514859436043,-4.91824802050565,130.808773246294));
#36179=CARTESIAN_POINT('Ctrl Pts',(138.514859435991,-4.91824802050483,130.808773247205));
#36180=CARTESIAN_POINT('Ctrl Pts',(138.503760886087,-4.91807243545752,131.004477596301));
#36181=CARTESIAN_POINT('Ctrl Pts',(138.492662336184,-4.90621248966243,131.19967933262));
#36182=CARTESIAN_POINT('Ctrl Pts',(138.48156378628,-4.88286716168191,131.393250542653));
#36183=CARTESIAN_POINT('Ctrl Pts',(138.473892416269,-4.86673076093358,131.527047875508));
#36184=CARTESIAN_POINT('Ctrl Pts',(138.466221046258,-4.84510800141887,131.66006707746));
#36185=CARTESIAN_POINT('Ctrl Pts',(138.458549676247,-4.81807674258383,131.79194330528));
#36186=CARTESIAN_POINT('Ctrl Pts',(138.450775342128,-4.79068267378781,131.92558955829));
#36187=CARTESIAN_POINT('Ctrl Pts',(138.443001008009,-4.75768027938131,132.058306827762));
#36188=CARTESIAN_POINT('Ctrl Pts',(138.43522667389,-4.71914490506628,132.189587829069));
#36189=CARTESIAN_POINT('Ctrl Pts',(138.427461920942,-4.68065702215611,132.320707038274));
#36190=CARTESIAN_POINT('Ctrl Pts',(138.419697167995,-4.63664983598088,132.450393129695));
#36191=CARTESIAN_POINT('Ctrl Pts',(138.411932415048,-4.58724986287797,132.578148022535));
#36192=CARTESIAN_POINT('Ctrl Pts',(138.404175374163,-4.53789895452477,132.705776027414));
#36193=CARTESIAN_POINT('Ctrl Pts',(138.396418333278,-4.48316605839848,132.831476288512));
#36194=CARTESIAN_POINT('Ctrl Pts',(138.388661292393,-4.42322765084366,132.954765279789));
#36195=CARTESIAN_POINT('Ctrl Pts',(138.380910101153,-4.36333444330832,133.077961297879));
#36196=CARTESIAN_POINT('Ctrl Pts',(138.373158909913,-4.29824370809723,133.198749315287));
#36197=CARTESIAN_POINT('Ctrl Pts',(138.365407718673,-4.22818010291886,133.316665551244));
#36198=CARTESIAN_POINT('Ctrl Pts',(138.357659821896,-4.1581462766416,133.434531669654));
#36199=CARTESIAN_POINT('Ctrl Pts',(138.349911925119,-4.08314398348298,133.549528098856));
#36200=CARTESIAN_POINT('Ctrl Pts',(138.342164028342,-4.00344381182405,133.661215655552));
#36201=CARTESIAN_POINT('Ctrl Pts',(138.334417752258,-3.92376031172279,133.77287984962));
#36202=CARTESIAN_POINT('Ctrl Pts',(138.326671476173,-3.83938111471063,133.881236229854));
#36203=CARTESIAN_POINT('Ctrl Pts',(138.318925200089,-3.75061989851219,133.985874948727));
#36204=CARTESIAN_POINT('Ctrl Pts',(138.311178866824,-3.66185802709886,134.09051444002));
#36205=CARTESIAN_POINT('Ctrl Pts',(138.303432533559,-3.56871432486036,134.191435917044));
#36206=CARTESIAN_POINT('Ctrl Pts',(138.295686200293,-3.47154221882925,134.288263269103));
#36207=CARTESIAN_POINT('Ctrl Pts',(138.28793813229,-3.37434835177861,134.385112304976));
#36208=CARTESIAN_POINT('Ctrl Pts',(138.280190064287,-3.27312456268692,134.477865115547));
#36209=CARTESIAN_POINT('Ctrl Pts',(138.272441996284,-3.1682602288177,134.566183338667));
#36210=CARTESIAN_POINT('Ctrl Pts',(138.264685693542,-3.06328444388646,134.654595427445));
#36211=CARTESIAN_POINT('Ctrl Pts',(138.256929390801,-2.95466068451977,134.738563261528));
#36212=CARTESIAN_POINT('Ctrl Pts',(138.249173088059,-2.84281086104595,134.817789260362));
#36213=CARTESIAN_POINT('Ctrl Pts',(138.241412645545,-2.73090133995354,134.897057544498));
#36214=CARTESIAN_POINT('Ctrl Pts',(138.23365220303,-2.6157626518835,134.971578738105));
#36215=CARTESIAN_POINT('Ctrl Pts',(138.225891760516,-2.49784376683901,135.041099880131));
#36216=CARTESIAN_POINT('Ctrl Pts',(138.218118860251,-2.37973558793199,135.110732623667));
#36217=CARTESIAN_POINT('Ctrl Pts',(138.210345959985,-2.25883863852052,135.175349091667));
#36218=CARTESIAN_POINT('Ctrl Pts',(138.20257305972,-2.13562524892375,135.234742977889));
#36219=CARTESIAN_POINT('Ctrl Pts',(138.195082723958,-2.01689097639495,135.291977746742));
#36220=CARTESIAN_POINT('Ctrl Pts',(138.187592388196,-1.89600603921056,135.34436292706));
#36221=CARTESIAN_POINT('Ctrl Pts',(138.180102052434,-1.77340688246443,135.391757601884));
#36222=CARTESIAN_POINT('Ctrl Pts',(138.172327718315,-1.6461593414268,135.440949260209));
#36223=CARTESIAN_POINT('Ctrl Pts',(138.164553384196,-1.51666194356741,135.484920337067));
#36224=CARTESIAN_POINT('Ctrl Pts',(138.156779050077,-1.38538220800074,135.5234600232));
#36225=CARTESIAN_POINT('Ctrl Pts',(138.14901429713,-1.25426426297534,135.561952212615));
#36226=CARTESIAN_POINT('Ctrl Pts',(138.141249544183,-1.12136872229903,135.595026220709));
#36227=CARTESIAN_POINT('Ctrl Pts',(138.133484791235,-0.987183020622717,
135.622519264424));
#36228=CARTESIAN_POINT('Ctrl Pts',(138.12572775035,-0.853130594077,135.649985001661));
#36229=CARTESIAN_POINT('Ctrl Pts',(138.117970709465,-0.717790937117477,
135.671880727557));
#36230=CARTESIAN_POINT('Ctrl Pts',(138.11021366858,-0.581666243669646,135.688093559023));
#36231=CARTESIAN_POINT('Ctrl Pts',(138.10246247734,-0.44564420291241,135.704294164268));
#36232=CARTESIAN_POINT('Ctrl Pts',(138.0947112861,-0.308838690661705,135.714820359089));
#36233=CARTESIAN_POINT('Ctrl Pts',(138.08696009486,-0.171761331792822,135.719610469547));
#36234=CARTESIAN_POINT('Ctrl Pts',(138.079212198083,-0.0347422344578371,
135.72439854408));
#36235=CARTESIAN_POINT('Ctrl Pts',(138.071464301306,0.102548089782278,135.723455369598));
#36236=CARTESIAN_POINT('Ctrl Pts',(138.063716404529,0.239593883953647,135.71677121047));
#36237=CARTESIAN_POINT('Ctrl Pts',(138.055970128445,0.37661101109924,135.710088449524));
#36238=CARTESIAN_POINT('Ctrl Pts',(138.048223852361,0.51338331966346,135.697667111602));
#36239=CARTESIAN_POINT('Ctrl Pts',(138.040477576277,0.649396442842379,135.67954957006));
#36240=CARTESIAN_POINT('Ctrl Pts',(138.032731243011,0.785410570039183,135.661431894779));
#36241=CARTESIAN_POINT('Ctrl Pts',(138.024984909746,0.92066511312588,135.637617983595));
#36242=CARTESIAN_POINT('Ctrl Pts',(138.017238576481,1.05465260357668,135.608201887661));
#36243=CARTESIAN_POINT('Ctrl Pts',(138.009490508478,1.18867009959695,135.578779204197));
#36244=CARTESIAN_POINT('Ctrl Pts',(138.001742440475,1.32141959655889,135.543751923354));
#36245=CARTESIAN_POINT('Ctrl Pts',(137.993994372472,1.45240595288155,135.503264746247));
#36246=CARTESIAN_POINT('Ctrl Pts',(137.98623806973,1.58353152306256,135.462734538886));
#36247=CARTESIAN_POINT('Ctrl Pts',(137.978481766988,1.71288983518903,135.416732959096));
#36248=CARTESIAN_POINT('Ctrl Pts',(137.970725464246,1.84000247347685,135.365454122429));
#36249=CARTESIAN_POINT('Ctrl Pts',(137.962965021732,1.96718295560701,135.314147916702));
#36250=CARTESIAN_POINT('Ctrl Pts',(137.955204579218,2.09211501965882,135.257559002958));
#36251=CARTESIAN_POINT('Ctrl Pts',(137.947444136704,2.21434316308179,135.195928380747));
#36252=CARTESIAN_POINT('Ctrl Pts',(137.939671236438,2.33676751797156,135.134198823591));
#36253=CARTESIAN_POINT('Ctrl Pts',(137.931898336173,2.45647893676274,135.06741157537));
#36254=CARTESIAN_POINT('Ctrl Pts',(137.924125435907,2.57304854209484,134.995852507398));
#36255=CARTESIAN_POINT('Ctrl Pts',(137.916635100145,2.68538054865303,134.926894791791));
#36256=CARTESIAN_POINT('Ctrl Pts',(137.909144764383,2.79479494580824,134.853506340039));
#36257=CARTESIAN_POINT('Ctrl Pts',(137.901654428621,2.90093726689751,134.7759781767));
#36258=CARTESIAN_POINT('Ctrl Pts',(137.893880094502,3.01110400635121,134.695510509485));
#36259=CARTESIAN_POINT('Ctrl Pts',(137.886105760383,3.11809462533035,134.610328122204));
#36260=CARTESIAN_POINT('Ctrl Pts',(137.878331426264,3.22147905853459,134.520710404376));
#36261=CARTESIAN_POINT('Ctrl Pts',(137.870566673317,3.32473607966456,134.431203132376));
#36262=CARTESIAN_POINT('Ctrl Pts',(137.86280192037,3.42439546526849,134.33727165946));
#36263=CARTESIAN_POINT('Ctrl Pts',(137.855037167422,3.5200567910136,134.239238089986));
#36264=CARTESIAN_POINT('Ctrl Pts',(137.847280126537,3.61562310458133,134.141301888836));
#36265=CARTESIAN_POINT('Ctrl Pts',(137.839523085652,3.707198989338,134.039271977097));
#36266=CARTESIAN_POINT('Ctrl Pts',(137.831766044767,3.79441802546119,133.933509848676));
#36267=CARTESIAN_POINT('Ctrl Pts',(137.824014853527,3.88157128903082,133.827827476298));
#36268=CARTESIAN_POINT('Ctrl Pts',(137.816263662287,3.96437399588384,133.718418789726));
#36269=CARTESIAN_POINT('Ctrl Pts',(137.808512471047,4.04249771224427,133.605680897184));
#36270=CARTESIAN_POINT('Ctrl Pts',(137.80076457427,4.12058822394123,133.492990921254));
#36271=CARTESIAN_POINT('Ctrl Pts',(137.793016677493,4.19400347829145,133.376974874361));
#36272=CARTESIAN_POINT('Ctrl Pts',(137.785268780716,4.26245650519108,133.258061415107));
#36273=CARTESIAN_POINT('Ctrl Pts',(137.777522504632,4.33089521319321,133.139172829986));
#36274=CARTESIAN_POINT('Ctrl Pts',(137.769776228548,4.39437356343792,133.017388376643));
#36275=CARTESIAN_POINT('Ctrl Pts',(137.762029952464,4.45264917800659,132.893163710272));
#36276=CARTESIAN_POINT('Ctrl Pts',(137.754283619198,4.51092522275257,132.768938126902));
#36277=CARTESIAN_POINT('Ctrl Pts',(137.746537285933,4.56399828914259,132.642272648513));
#36278=CARTESIAN_POINT('Ctrl Pts',(137.738790952667,4.61167320594162,132.513645059694));
#36279=CARTESIAN_POINT('Ctrl Pts',(137.731042884664,4.65935879920771,132.384988665618));
#36280=CARTESIAN_POINT('Ctrl Pts',(137.723294816662,4.70164370150549,132.254369653278));
#36281=CARTESIAN_POINT('Ctrl Pts',(137.715546748659,4.73838201786046,132.122282813796));
#36282=CARTESIAN_POINT('Ctrl Pts',(137.707790445917,4.77515938013527,131.99005559085));
#36283=CARTESIAN_POINT('Ctrl Pts',(137.700034143175,4.80637827568231,131.856357801712));
#36284=CARTESIAN_POINT('Ctrl Pts',(137.692277840433,4.83194342399536,131.72169687533));
#36285=CARTESIAN_POINT('Ctrl Pts',(137.684517397919,4.85752221719785,131.586964076356));
#36286=CARTESIAN_POINT('Ctrl Pts',(137.676756955405,4.87744119363868,131.451267502469));
#36287=CARTESIAN_POINT('Ctrl Pts',(137.66899651289,4.8916569028114,131.31512064701));
#36288=CARTESIAN_POINT('Ctrl Pts',(137.661223612625,4.90589543230249,131.178755236532));
#36289=CARTESIAN_POINT('Ctrl Pts',(137.65345071236,4.91441237483225,131.041938490467));
#36290=CARTESIAN_POINT('Ctrl Pts',(137.645677812094,4.91721642334132,130.905185755911));
#36291=CARTESIAN_POINT('Ctrl Pts',(137.638187476332,4.91991853762411,130.773404327717));
#36292=CARTESIAN_POINT('Ctrl Pts',(137.63069714057,4.91731590895363,130.641682645831));
#36293=CARTESIAN_POINT('Ctrl Pts',(137.623206804808,4.90946178664443,130.510476238978));
#36294=CARTESIAN_POINT('Ctrl Pts',(137.615432470689,4.90130987290062,130.374295101329));
#36295=CARTESIAN_POINT('Ctrl Pts',(137.60765813657,4.88747456093996,130.23823770243));
#36296=CARTESIAN_POINT('Ctrl Pts',(137.599883802451,4.86795844827736,130.102816885255));
#36297=CARTESIAN_POINT('Ctrl Pts',(137.592119049504,4.84846638747943,129.967562962134));
#36298=CARTESIAN_POINT('Ctrl Pts',(137.584354296557,4.82330751127265,129.832944443011));
#36299=CARTESIAN_POINT('Ctrl Pts',(137.57658954361,4.79253637604242,129.699472321488));
#36300=CARTESIAN_POINT('Ctrl Pts',(137.568832502725,4.76179580313749,129.566132766358));
#36301=CARTESIAN_POINT('Ctrl Pts',(137.56107546184,4.72545415133071,129.433937721434));
#36302=CARTESIAN_POINT('Ctrl Pts',(137.553318420955,4.68361749681892,129.303390862377));
#36303=CARTESIAN_POINT('Ctrl Pts',(137.545567229715,4.64181239165377,129.172942449722));
#36304=CARTESIAN_POINT('Ctrl Pts',(137.537816038475,4.59452065064799,129.044140119804));
#36305=CARTESIAN_POINT('Ctrl Pts',(137.530064847234,4.54189884572014,128.917474839956));
#36306=CARTESIAN_POINT('Ctrl Pts',(137.522316950457,4.48929940646308,128.790863396231));
#36307=CARTESIAN_POINT('Ctrl Pts',(137.51456905368,4.43137455871004,128.666387556323));
#36308=CARTESIAN_POINT('Ctrl Pts',(137.506821156903,4.36832983073338,128.544520456753));
#36309=CARTESIAN_POINT('Ctrl Pts',(137.499074880819,4.30529829035469,128.422678849152));
#36310=CARTESIAN_POINT('Ctrl Pts',(137.491328604735,4.23714917949465,128.303445243509));
#36311=CARTESIAN_POINT('Ctrl Pts',(137.483582328651,4.16413484258633,128.187269851991));
#36312=CARTESIAN_POINT('Ctrl Pts',(137.475835995386,4.09111996670282,128.071093602893));
#36313=CARTESIAN_POINT('Ctrl Pts',(137.46808966212,4.013240001147,127.957975943986));
#36314=CARTESIAN_POINT('Ctrl Pts',(137.460343328855,3.93079142480495,127.848339332599));
#36315=CARTESIAN_POINT('Ctrl Pts',(137.452595260852,3.84832438467595,127.738678168852));
#36316=CARTESIAN_POINT('Ctrl Pts',(137.444847192849,3.76128693283012,127.632499916262));
#36317=CARTESIAN_POINT('Ctrl Pts',(137.437099124846,3.67001649125362,127.53019476709));
#36318=CARTESIAN_POINT('Ctrl Pts',(137.429342822104,3.57864904636561,127.427780886787));
#36319=CARTESIAN_POINT('Ctrl Pts',(137.421586519362,3.48303988545323,127.329248625019));
#36320=CARTESIAN_POINT('Ctrl Pts',(137.413830216621,3.38356442141867,127.234952421715));
#36321=CARTESIAN_POINT('Ctrl Pts',(137.406069774106,3.28403586433368,127.140605889688));
#36322=CARTESIAN_POINT('Ctrl Pts',(137.398309331592,3.18063718691026,127.050500177914));
#36323=CARTESIAN_POINT('Ctrl Pts',(137.390548889078,3.07377691957879,126.96494939823));
#36324=CARTESIAN_POINT('Ctrl Pts',(137.382775988813,2.96674511065966,126.879261284839));
#36325=CARTESIAN_POINT('Ctrl Pts',(137.375003088547,2.85624092281886,126.798142946693));
#36326=CARTESIAN_POINT('Ctrl Pts',(137.367230188282,2.7427026309104,126.721865627869));
#36327=CARTESIAN_POINT('Ctrl Pts',(137.35973985252,2.63329174189834,126.648361181716));
#36328=CARTESIAN_POINT('Ctrl Pts',(137.352249516758,2.52106377600558,126.579352060385));
#36329=CARTESIAN_POINT('Ctrl Pts',(137.344759180996,2.40643076500545,126.515039688126));
#36330=CARTESIAN_POINT('Ctrl Pts',(137.336984846877,2.28745140855148,126.448288892724));
#36331=CARTESIAN_POINT('Ctrl Pts',(137.329210512758,2.1655041414502,126.386386585021));
#36332=CARTESIAN_POINT('Ctrl Pts',(137.321436178638,2.0410218370425,126.329607783809));
#36333=CARTESIAN_POINT('Ctrl Pts',(137.313671425691,1.91669294594976,126.272898957395));
#36334=CARTESIAN_POINT('Ctrl Pts',(137.305906672744,1.78983558608679,126.221301234658));
#36335=CARTESIAN_POINT('Ctrl Pts',(137.298141919797,1.66090915990418,126.17504492029));
#36336=CARTESIAN_POINT('Ctrl Pts',(137.290384878912,1.5321107852656,126.128834548346));
#36337=CARTESIAN_POINT('Ctrl Pts',(137.282627838027,1.40124779951728,126.087955158435));
#36338=CARTESIAN_POINT('Ctrl Pts',(137.274870797142,1.26880129603253,126.052589754647));
#36339=CARTESIAN_POINT('Ctrl Pts',(137.267119605902,1.13645467148634,126.017251020185));
#36340=CARTESIAN_POINT('Ctrl Pts',(137.259368414662,1.00252728227598,125.987418095772));
#36341=CARTESIAN_POINT('Ctrl Pts',(137.251617223422,0.867516824070355,125.963224632856));
#36342=CARTESIAN_POINT('Ctrl Pts',(137.243869326645,0.732563748910991,125.939041452807));
#36343=CARTESIAN_POINT('Ctrl Pts',(137.236121429868,0.596528904353548,125.920493035777));
#36344=CARTESIAN_POINT('Ctrl Pts',(137.228373533091,0.459921446604906,125.907662206856));
#36345=CARTESIAN_POINT('Ctrl Pts',(137.220627257006,0.32334256419151,125.894834061868));
#36346=CARTESIAN_POINT('Ctrl Pts',(137.212880980922,0.186191695837987,125.887721162624));
#36347=CARTESIAN_POINT('Ctrl Pts',(137.205134704838,0.0489840161228252,
125.886354555282));
#36348=CARTESIAN_POINT('Ctrl Pts',(137.197388371573,-0.0882246764282594,
125.884987937851));
#36349=CARTESIAN_POINT('Ctrl Pts',(137.189642038308,-0.225489790231987,
125.889367700857));
#36350=CARTESIAN_POINT('Ctrl Pts',(137.181895705042,-0.362295645893674,
125.899472756721));
#36351=CARTESIAN_POINT('Ctrl Pts',(137.174147637039,-0.499132138278191,
125.909580075542));
#36352=CARTESIAN_POINT('Ctrl Pts',(137.166399569036,-0.63550877803731,125.925415209735));
#36353=CARTESIAN_POINT('Ctrl Pts',(137.158651501033,-0.770914900545521,
125.946905185077));
#36354=CARTESIAN_POINT('Ctrl Pts',(137.150895198291,-0.906464934292087,
125.96841800022));
#36355=CARTESIAN_POINT('Ctrl Pts',(137.14313889555,-1.04104200355258,125.995597600818));
#36356=CARTESIAN_POINT('Ctrl Pts',(137.135382592808,-1.17414498813358,126.028319724803));
#36357=CARTESIAN_POINT('Ctrl Pts',(137.127622150293,-1.30731901378509,126.061059313571));
#36358=CARTESIAN_POINT('Ctrl Pts',(137.119861707779,-1.43901701182668,126.099347211123));
#36359=CARTESIAN_POINT('Ctrl Pts',(137.112101265265,-1.56875389039883,126.143009494355));
#36360=CARTESIAN_POINT('Ctrl Pts',(137.104328365,-1.69869903412606,126.186741868161));
#36361=CARTESIAN_POINT('Ctrl Pts',(137.096555464734,-1.8266764021414,126.23586572784));
#36362=CARTESIAN_POINT('Ctrl Pts',(137.088782564469,-1.95222089085743,126.290158954392));
#36363=CARTESIAN_POINT('Ctrl Pts',(137.081292228707,-2.07320152117996,126.342478485403));
#36364=CARTESIAN_POINT('Ctrl Pts',(137.073801892945,-2.19192280627911,126.399597935849));
#36365=CARTESIAN_POINT('Ctrl Pts',(137.066311557183,-2.30799256899358,126.461279526454));
#36366=CARTESIAN_POINT('Ctrl Pts',(137.058536284961,-2.4284776888173,126.525307518425));
#36367=CARTESIAN_POINT('Ctrl Pts',(137.05076101274,-2.54648726911118,126.594454459831));
#36368=CARTESIAN_POINT('Ctrl Pts',(137.042985740518,-2.66155578285581,126.668504735497));
#36369=CARTESIAN_POINT('Ctrl Pts',(137.035220256517,-2.77647943787687,126.742461789932));
#36370=CARTESIAN_POINT('Ctrl Pts',(137.027454772516,-2.88846906809892,126.821309685809));
#36371=CARTESIAN_POINT('Ctrl Pts',(137.019689288515,-2.99708247263446,126.904786318399));
#36372=CARTESIAN_POINT('Ctrl Pts',(137.011933107671,-3.10556575681877,126.988162944835));
#36373=CARTESIAN_POINT('Ctrl Pts',(137.004176926827,-3.2106805629706,127.076157027058));
#36374=CARTESIAN_POINT('Ctrl Pts',(136.996420745982,-3.31201302418701,127.168462820582));
#36375=CARTESIAN_POINT('Ctrl Pts',(136.988669840552,-3.41327656350487,127.260705831751));
#36376=CARTESIAN_POINT('Ctrl Pts',(136.980918935122,-3.51076258802983,127.357254457942));
#36377=CARTESIAN_POINT('Ctrl Pts',(136.973168029692,-3.60408968145251,127.457762250485));
#36378=CARTESIAN_POINT('Ctrl Pts',(136.965420717481,-3.69737350964463,127.558223448919));
#36379=CARTESIAN_POINT('Ctrl Pts',(136.95767340527,-3.78650197791445,127.662639875589));
#36380=CARTESIAN_POINT('Ctrl Pts',(136.94992609306,-3.87113027098331,127.770628017686));
#36381=CARTESIAN_POINT('Ctrl Pts',(136.942180694645,-3.95573765857231,127.878589483788));
#36382=CARTESIAN_POINT('Ctrl Pts',(136.93443529623,-4.03584684328171,127.990120601348));
#36383=CARTESIAN_POINT('Ctrl Pts',(136.926689897815,-4.11115334144958,128.10480486419));
#36384=CARTESIAN_POINT('Ctrl Pts',(136.918942015748,-4.18648398752441,128.219525901878));
#36385=CARTESIAN_POINT('Ctrl Pts',(136.91119413368,-4.25700864966831,128.337401781762));
#36386=CARTESIAN_POINT('Ctrl Pts',(136.903446251613,-4.32246617463714,128.457986983292));
#36387=CARTESIAN_POINT('Ctrl Pts',(136.89569736074,-4.38793222244506,128.578587885511));
#36388=CARTESIAN_POINT('Ctrl Pts',(136.887948469866,-4.44832963932198,128.701898464539));
#36389=CARTESIAN_POINT('Ctrl Pts',(136.880199578993,-4.50344373176889,128.827449487219));
#36390=CARTESIAN_POINT('Ctrl Pts',(136.872443501781,-4.55860893714959,128.9531169462));
#36391=CARTESIAN_POINT('Ctrl Pts',(136.864687424568,-4.60848087711548,129.081028639127));
#36392=CARTESIAN_POINT('Ctrl Pts',(136.856931347356,-4.65289325216137,129.21069583271));
#36393=CARTESIAN_POINT('Ctrl Pts',(136.84960363452,-4.69485275330791,129.33320157018));
#36394=CARTESIAN_POINT('Ctrl Pts',(136.842275921685,-4.7319394296721,129.45727383743));
#36395=CARTESIAN_POINT('Ctrl Pts',(136.834948208849,-4.76405452823407,129.582490119308));
#36396=CARTESIAN_POINT('Ctrl Pts',(138.584929581679,-4.76405452823406,129.582490119308));
#36397=CARTESIAN_POINT('Ctrl Pts',(138.577290381644,-4.79768433680502,129.713612232523));
#36398=CARTESIAN_POINT('Ctrl Pts',(138.569651181608,-4.82588585814068,129.84608197248));
#36399=CARTESIAN_POINT('Ctrl Pts',(138.562011981572,-4.84856978594709,129.979403592442));
#36400=CARTESIAN_POINT('Ctrl Pts',(138.554153223984,-4.87190567045693,130.116556996943));
#36401=CARTESIAN_POINT('Ctrl Pts',(138.546294466396,-4.88940194006727,130.254611535898));
#36402=CARTESIAN_POINT('Ctrl Pts',(138.538435708807,-4.90101860449271,130.393021705091));
#36403=CARTESIAN_POINT('Ctrl Pts',(138.530576951219,-4.91263526891816,130.531431874284));
#36404=CARTESIAN_POINT('Ctrl Pts',(138.522718193631,-4.91837235026494,130.670197211417));
#36405=CARTESIAN_POINT('Ctrl Pts',(138.514859436043,-4.91824802050565,130.808773246294));
#36406=CARTESIAN_POINT('',(138.860140564037,-4.91824998799066,130.804016917383));
#36407=CARTESIAN_POINT('Ctrl Pts',(138.929858124837,-4.76405452823407,129.582490119308));
#36408=CARTESIAN_POINT('Ctrl Pts',(138.921678643293,-4.79993071147542,129.722370813269));
#36409=CARTESIAN_POINT('Ctrl Pts',(138.913499161748,-4.82968047010897,129.863982586788));
#36410=CARTESIAN_POINT('Ctrl Pts',(138.905319680203,-4.85314793322502,130.006777894124));
#36411=CARTESIAN_POINT('Ctrl Pts',(138.897157381201,-4.87656609851148,130.149273233001));
#36412=CARTESIAN_POINT('Ctrl Pts',(138.888995082198,-4.89372823319955,130.292946829293));
#36413=CARTESIAN_POINT('Ctrl Pts',(138.880832783196,-4.90452904142768,130.437239460055));
#36414=CARTESIAN_POINT('Ctrl Pts',(138.87393537681,-4.91365607336216,130.559171395245));
#36415=CARTESIAN_POINT('Ctrl Pts',(138.867037970423,-4.91824142933335,130.681545011985));
#36416=CARTESIAN_POINT('Ctrl Pts',(138.860140564037,-4.91824998799067,130.804016917383));
#36417=CARTESIAN_POINT('Ctrl Pts',(138.860140564008,-4.9182499879907,130.804016917894));
#36418=CARTESIAN_POINT('Ctrl Pts',(138.852067034098,-4.91826000602782,130.947372338169));
#36419=CARTESIAN_POINT('Ctrl Pts',(138.843993504189,-4.91199799204111,131.090620741002));
#36420=CARTESIAN_POINT('Ctrl Pts',(138.835919974279,-4.89951787644956,131.233205159156));
#36421=CARTESIAN_POINT('Ctrl Pts',(138.827837244499,-4.88702353963818,131.375952053717));
#36422=CARTESIAN_POINT('Ctrl Pts',(138.819754514719,-4.86829699567183,131.518033115249));
#36423=CARTESIAN_POINT('Ctrl Pts',(138.811671784939,-4.84344365772086,131.658899438793));
#36424=CARTESIAN_POINT('Ctrl Pts',(138.803571331097,-4.81853582059472,131.800074658408));
#36425=CARTESIAN_POINT('Ctrl Pts',(138.795470877255,-4.78747438949765,131.940029478287));
#36426=CARTESIAN_POINT('Ctrl Pts',(138.787370423413,-4.75041567751435,132.078226369255));
#36427=CARTESIAN_POINT('Ctrl Pts',(138.779260814515,-4.71331508212753,132.216579449034));
#36428=CARTESIAN_POINT('Ctrl Pts',(138.771151205617,-4.67020378374145,132.353170311098));
#36429=CARTESIAN_POINT('Ctrl Pts',(138.763041596719,-4.6212870625238,132.487479433411));
#36430=CARTESIAN_POINT('Ctrl Pts',(138.754913574557,-4.57225927349625,132.62209351116));
#36431=CARTESIAN_POINT('Ctrl Pts',(138.746785552396,-4.51739983376362,132.75441517391));
#36432=CARTESIAN_POINT('Ctrl Pts',(138.738657530234,-4.45696176081644,132.88394589476));
#36433=CARTESIAN_POINT('Ctrl Pts',(138.731574454789,-4.40429366741349,132.996824015646));
#36434=CARTESIAN_POINT('Ctrl Pts',(138.724491379345,-4.34738992070749,133.10758294576));
#36435=CARTESIAN_POINT('Ctrl Pts',(138.7174083039,-4.28644493324192,133.215910512713));
#36436=CARTESIAN_POINT('Ctrl Pts',(138.709633969781,-4.21955214081599,133.334810093328));
#36437=CARTESIAN_POINT('Ctrl Pts',(138.701859635662,-4.14760250062957,133.45111263384));
#36438=CARTESIAN_POINT('Ctrl Pts',(138.694085301543,-4.07082265219019,133.564358080774));
#36439=CARTESIAN_POINT('Ctrl Pts',(138.686320548596,-3.99413742805201,133.677463962816));
#36440=CARTESIAN_POINT('Ctrl Pts',(138.678555795649,-3.91263405725212,133.787519927177));
#36441=CARTESIAN_POINT('Ctrl Pts',(138.670791042702,-3.82658509601864,133.894090308887));
#36442=CARTESIAN_POINT('Ctrl Pts',(138.663034001817,-3.74062159982659,134.000554843391));
#36443=CARTESIAN_POINT('Ctrl Pts',(138.655276960932,-3.65012174176799,134.103540382423));
#36444=CARTESIAN_POINT('Ctrl Pts',(138.647519920047,-3.55540120814913,134.202640375266));
#36445=CARTESIAN_POINT('Ctrl Pts',(138.639768728807,-3.46075210402123,134.301665636033));
#36446=CARTESIAN_POINT('Ctrl Pts',(138.632017537567,-3.3618889286371,134.396810901353));
#36447=CARTESIAN_POINT('Ctrl Pts',(138.624266346327,-3.25916721983027,134.487703134314));
#36448=CARTESIAN_POINT('Ctrl Pts',(138.61651844955,-3.15648917049015,134.578556735651));
#36449=CARTESIAN_POINT('Ctrl Pts',(138.608770552772,-3.04995614170784,134.665160641375));
#36450=CARTESIAN_POINT('Ctrl Pts',(138.601022655995,-2.93995989808493,134.747179261652));
#36451=CARTESIAN_POINT('Ctrl Pts',(138.593276379911,-2.8299866633048,134.829180725402));
#36452=CARTESIAN_POINT('Ctrl Pts',(138.585530103827,-2.71655196784174,134.906598577936));
#36453=CARTESIAN_POINT('Ctrl Pts',(138.577783827743,-2.6000796506556,134.979138320959));
#36454=CARTESIAN_POINT('Ctrl Pts',(138.570037494478,-2.48360647369751,135.051678599453));
#36455=CARTESIAN_POINT('Ctrl Pts',(138.562291161212,-2.36409596213738,135.119340489895));
#36456=CARTESIAN_POINT('Ctrl Pts',(138.554544827947,-2.24199950496182,135.181873756581));
#36457=CARTESIAN_POINT('Ctrl Pts',(138.546796759944,-2.11987570513131,135.244421027159));
#36458=CARTESIAN_POINT('Ctrl Pts',(138.539048691941,-1.99516515524824,135.301837210372));
#36459=CARTESIAN_POINT('Ctrl Pts',(138.531300623938,-1.86834195175459,135.353918993256));
#36460=CARTESIAN_POINT('Ctrl Pts',(138.523544321196,-1.7413839590508,135.40605612928));
#36461=CARTESIAN_POINT('Ctrl Pts',(138.515788018455,-1.61230918963471,135.452847390853));
#36462=CARTESIAN_POINT('Ctrl Pts',(138.508031715713,-1.48161026732753,135.494138232576));
#36463=CARTESIAN_POINT('Ctrl Pts',(138.500271273199,-1.35084158707007,135.535451112465));
#36464=CARTESIAN_POINT('Ctrl Pts',(138.492510830684,-1.21844740385234,135.571257620773));
#36465=CARTESIAN_POINT('Ctrl Pts',(138.48475038817,-1.0849324850198,135.601453963067));
#36466=CARTESIAN_POINT('Ctrl Pts',(138.476977487905,-0.951203236186739,
135.63169877921));
#36467=CARTESIAN_POINT('Ctrl Pts',(138.469204587639,-0.816350041386251,
135.65631536236));
#36468=CARTESIAN_POINT('Ctrl Pts',(138.461431687374,-0.680885667340857,
135.675251477615));
#36469=CARTESIAN_POINT('Ctrl Pts',(138.453941351612,-0.550345764507372,
135.693499217384));
#36470=CARTESIAN_POINT('Ctrl Pts',(138.44645101585,-0.419238653289755,135.706472287298));
#36471=CARTESIAN_POINT('Ctrl Pts',(138.438960680088,-0.288022963226061,
135.714169762039));
#36472=CARTESIAN_POINT('Ctrl Pts',(138.431186345969,-0.151832190390304,
135.722159088875));
#36473=CARTESIAN_POINT('Ctrl Pts',(138.42341201185,-0.015093031210281,135.724490182861));
#36474=CARTESIAN_POINT('Ctrl Pts',(138.415637677731,0.121684954106831,135.721105052092));
#36475=CARTESIAN_POINT('Ctrl Pts',(138.407872924784,0.258294372781518,135.717724093195));
#36476=CARTESIAN_POINT('Ctrl Pts',(138.400108171837,0.394942135293119,135.708640936049));
#36477=CARTESIAN_POINT('Ctrl Pts',(138.392343418889,0.531114381065231,135.69384940237));
#36478=CARTESIAN_POINT('Ctrl Pts',(138.384586378004,0.667151378642781,135.679072559851));
#36479=CARTESIAN_POINT('Ctrl Pts',(138.376829337119,0.802713413195336,135.658598665586));
#36480=CARTESIAN_POINT('Ctrl Pts',(138.369072296234,0.93728780593003,135.632473564811));
#36481=CARTESIAN_POINT('Ctrl Pts',(138.361321104994,1.07176071506823,135.606368165178));
#36482=CARTESIAN_POINT('Ctrl Pts',(138.353569913754,1.20524708259767,135.574620115734));
#36483=CARTESIAN_POINT('Ctrl Pts',(138.345818722514,1.33724088511658,135.537326904967));
#36484=CARTESIAN_POINT('Ctrl Pts',(138.338070825737,1.46917858674854,135.500049544809));
#36485=CARTESIAN_POINT('Ctrl Pts',(138.33032292896,1.59962460965452,135.457231816984));
#36486=CARTESIAN_POINT('Ctrl Pts',(138.322575032183,1.72808485426766,135.409021929644));
#36487=CARTESIAN_POINT('Ctrl Pts',(138.314828756099,1.856518227767,135.360822126774));
#36488=CARTESIAN_POINT('Ctrl Pts',(138.307082480015,1.98296628338582,135.307232545174));
#36489=CARTESIAN_POINT('Ctrl Pts',(138.299336203931,2.10695215605658,135.248450589044));
#36490=CARTESIAN_POINT('Ctrl Pts',(138.291589870665,2.23093894396279,135.189668198998));
#36491=CARTESIAN_POINT('Ctrl Pts',(138.2838435374,2.35246315938058,135.125693525426));
#36492=CARTESIAN_POINT('Ctrl Pts',(138.276097204134,2.47107028515328,135.056771076157));
#36493=CARTESIAN_POINT('Ctrl Pts',(138.268349136131,2.5897039721696,134.987833192183));
#36494=CARTESIAN_POINT('Ctrl Pts',(138.260601068128,2.70541893165399,134.913945524074));
#36495=CARTESIAN_POINT('Ctrl Pts',(138.252853000125,2.8177878499451,134.835397046972));
#36496=CARTESIAN_POINT('Ctrl Pts',(138.245096697384,2.93027619525954,134.756765087614));
#36497=CARTESIAN_POINT('Ctrl Pts',(138.237340394642,3.03941107451428,134.673462648338));
#36498=CARTESIAN_POINT('Ctrl Pts',(138.2295840919,3.14479618907911,134.585820651951));
#36499=CARTESIAN_POINT('Ctrl Pts',(138.221823649386,3.25023755085296,134.498131878392));
#36500=CARTESIAN_POINT('Ctrl Pts',(138.214063206872,3.35192487032253,134.406099194816));
#36501=CARTESIAN_POINT('Ctrl Pts',(138.206302764357,3.44949798321141,134.31009117286));
#36502=CARTESIAN_POINT('Ctrl Pts',(138.198529864092,3.54722772912304,134.213929030304));
#36503=CARTESIAN_POINT('Ctrl Pts',(138.190756963826,3.64082980346662,134.113779082763));
#36504=CARTESIAN_POINT('Ctrl Pts',(138.182984063561,3.72998309660246,134.010044501164));
#36505=CARTESIAN_POINT('Ctrl Pts',(138.175493727799,3.81589544296935,133.910080932898));
#36506=CARTESIAN_POINT('Ctrl Pts',(138.168003392037,3.89767665018792,133.806789068257));
#36507=CARTESIAN_POINT('Ctrl Pts',(138.160513056275,3.97507803929305,133.700554265102));
#36508=CARTESIAN_POINT('Ctrl Pts',(138.152738722156,4.05541412559163,133.590291537097));
#36509=CARTESIAN_POINT('Ctrl Pts',(138.144964388037,4.13128619655803,133.476509023064));
#36510=CARTESIAN_POINT('Ctrl Pts',(138.137190053918,4.20237003222244,133.359604084396));
#36511=CARTESIAN_POINT('Ctrl Pts',(138.12942530097,4.27336626341243,133.242843220617));
#36512=CARTESIAN_POINT('Ctrl Pts',(138.121660548023,4.33958579950162,133.122967919644));
#36513=CARTESIAN_POINT('Ctrl Pts',(138.113895795076,4.40074568833152,133.000407167421));
#36514=CARTESIAN_POINT('Ctrl Pts',(138.106138754191,4.46184483229747,132.877968144266));
#36515=CARTESIAN_POINT('Ctrl Pts',(138.098381713306,4.51789415616363,132.752849325327));
#36516=CARTESIAN_POINT('Ctrl Pts',(138.090624672421,4.56865511541544,132.625506822265));
#36517=CARTESIAN_POINT('Ctrl Pts',(138.082873481181,4.61937779543301,132.498260349174));
#36518=CARTESIAN_POINT('Ctrl Pts',(138.075122289941,4.66481990452005,132.368793891428));
#36519=CARTESIAN_POINT('Ctrl Pts',(138.067371098701,4.7047899444922,132.237585875753));
#36520=CARTESIAN_POINT('Ctrl Pts',(138.059623201924,4.74474299613117,132.106433626985));
#36521=CARTESIAN_POINT('Ctrl Pts',(138.051875305147,4.7792284907526,131.97354166572));
#36522=CARTESIAN_POINT('Ctrl Pts',(138.04412740837,4.80810404718821,131.839405802045));
#36523=CARTESIAN_POINT('Ctrl Pts',(138.036381132286,4.83697356347986,131.705297996701));
#36524=CARTESIAN_POINT('Ctrl Pts',(138.028634856202,4.86023539347157,131.569947188461));
#36525=CARTESIAN_POINT('Ctrl Pts',(138.020888580117,4.87779786168906,131.433861279203));
#36526=CARTESIAN_POINT('Ctrl Pts',(138.013142246852,4.89536045954871,131.29777436539));
#36527=CARTESIAN_POINT('Ctrl Pts',(138.005395913587,4.90722356164297,131.160952727481));
#36528=CARTESIAN_POINT('Ctrl Pts',(137.997649580321,4.91334720170772,131.023910926085));
#36529=CARTESIAN_POINT('Ctrl Pts',(137.989901512318,4.91947221311921,130.886838435128));
#36530=CARTESIAN_POINT('Ctrl Pts',(137.982153444315,4.91985518742833,130.749546073077));
#36531=CARTESIAN_POINT('Ctrl Pts',(137.974405376312,4.91450827413372,130.612549549139));
#36532=CARTESIAN_POINT('Ctrl Pts',(137.966649073571,4.90915567807605,130.475407423665));
#36533=CARTESIAN_POINT('Ctrl Pts',(137.958892770829,4.89806104466963,130.338562155683));
#36534=CARTESIAN_POINT('Ctrl Pts',(137.951136468087,4.88128857955614,130.202526034317));
#36535=CARTESIAN_POINT('Ctrl Pts',(137.943376025573,4.86450716247296,130.066417306376));
#36536=CARTESIAN_POINT('Ctrl Pts',(137.935615583059,4.84204193930341,129.931118971075));
#36537=CARTESIAN_POINT('Ctrl Pts',(137.927855140544,4.81400832221518,129.797133266794));
#36538=CARTESIAN_POINT('Ctrl Pts',(137.920082240279,4.78592970307612,129.662932476766));
#36539=CARTESIAN_POINT('Ctrl Pts',(137.912309340013,4.7522649233566,129.530048907728));
#36540=CARTESIAN_POINT('Ctrl Pts',(137.904536439748,4.71317961457157,129.398970642048));
#36541=CARTESIAN_POINT('Ctrl Pts',(137.897046103986,4.67551515521117,129.272657401493));
#36542=CARTESIAN_POINT('Ctrl Pts',(137.889555768224,4.63281752423003,129.148020779814));
#36543=CARTESIAN_POINT('Ctrl Pts',(137.882065432462,4.58527651705627,129.025478293006));
#36544=CARTESIAN_POINT('Ctrl Pts',(137.874291098343,4.53593297814532,128.898289570563));
#36545=CARTESIAN_POINT('Ctrl Pts',(137.866516764224,4.48121523423676,128.772954020323));
#36546=CARTESIAN_POINT('Ctrl Pts',(137.858742430105,4.42128234791134,128.649959201268));
#36547=CARTESIAN_POINT('Ctrl Pts',(137.850977677158,4.36142332351201,128.527115962335));
#36548=CARTESIAN_POINT('Ctrl Pts',(137.843212924211,4.29636211451729,128.406608062896));
#36549=CARTESIAN_POINT('Ctrl Pts',(137.835448171264,4.22630669639728,128.288905435996));
#36550=CARTESIAN_POINT('Ctrl Pts',(137.827691130379,4.15632085830635,128.171319713005));
#36551=CARTESIAN_POINT('Ctrl Pts',(137.819934089494,4.08135088101514,128.056534051604));
#36552=CARTESIAN_POINT('Ctrl Pts',(137.812177048609,4.00165156504272,127.944995685542));
#36553=CARTESIAN_POINT('Ctrl Pts',(137.804425857369,3.92201235094423,127.833541431428));
#36554=CARTESIAN_POINT('Ctrl Pts',(137.796674666129,3.83765112330837,127.72532991526));
#36555=CARTESIAN_POINT('Ctrl Pts',(137.788923474888,3.74886688664438,127.620780851215));
#36556=CARTESIAN_POINT('Ctrl Pts',(137.781175578111,3.66012038564932,127.516276223311));
#36557=CARTESIAN_POINT('Ctrl Pts',(137.773427681334,3.56695486713926,127.415431248875));
#36558=CARTESIAN_POINT('Ctrl Pts',(137.765679784557,3.46971050968245,127.318633714681));
#36559=CARTESIAN_POINT('Ctrl Pts',(137.757933508473,3.372486493649,127.221856428444));
#36560=CARTESIAN_POINT('Ctrl Pts',(137.750187232389,3.27118561265513,127.129125174081));
#36561=CARTESIAN_POINT('Ctrl Pts',(137.742440956305,3.16618562610208,127.040791614138));
#36562=CARTESIAN_POINT('Ctrl Pts',(137.73469462304,3.06118486446276,126.952457402136));
#36563=CARTESIAN_POINT('Ctrl Pts',(137.726948289774,2.95248524195363,126.868521201019));
#36564=CARTESIAN_POINT('Ctrl Pts',(137.719201956509,2.84049807024734,126.789294768116));
#36565=CARTESIAN_POINT('Ctrl Pts',(137.711453888506,2.7284858197908,126.710050593002));
#36566=CARTESIAN_POINT('Ctrl Pts',(137.703705820503,2.61318487424444,126.635518510629));
#36567=CARTESIAN_POINT('Ctrl Pts',(137.6959577525,2.49503568147119,126.565967052701));
#36568=CARTESIAN_POINT('Ctrl Pts',(137.688201449758,2.37676091832962,126.496341674657));
#36569=CARTESIAN_POINT('Ctrl Pts',(137.680445147016,2.25563219835964,126.431707693982));
#36570=CARTESIAN_POINT('Ctrl Pts',(137.672688844275,2.13211522962672,126.372287997437));
#36571=CARTESIAN_POINT('Ctrl Pts',(137.66492840176,2.00853233616872,126.312836586811));
#36572=CARTESIAN_POINT('Ctrl Pts',(137.657167959246,1.88255901296629,126.258605160237));
#36573=CARTESIAN_POINT('Ctrl Pts',(137.649407516732,1.75468019048728,126.2097680903));
#36574=CARTESIAN_POINT('Ctrl Pts',(137.641634616467,1.62659608556954,126.160852622762));
#36575=CARTESIAN_POINT('Ctrl Pts',(137.633861716201,1.49660073973325,126.11734894045));
#36576=CARTESIAN_POINT('Ctrl Pts',(137.626088815936,1.36519431837731,126.079381513319));
#36577=CARTESIAN_POINT('Ctrl Pts',(137.618598480174,1.23856485143018,126.042794297799));
#36578=CARTESIAN_POINT('Ctrl Pts',(137.611108144412,1.11062541922513,126.011347885567));
#36579=CARTESIAN_POINT('Ctrl Pts',(137.60361780865,0.981829878857104,125.985108273946));
#36580=CARTESIAN_POINT('Ctrl Pts',(137.595843474531,0.848151016429937,125.957873779476));
#36581=CARTESIAN_POINT('Ctrl Pts',(137.588069140411,0.713126391188011,125.936162440718));
#36582=CARTESIAN_POINT('Ctrl Pts',(137.580294806292,0.5772521775216,125.920103971356));
#36583=CARTESIAN_POINT('Ctrl Pts',(137.572530053345,0.441545416679736,125.904065292623));
#36584=CARTESIAN_POINT('Ctrl Pts',(137.564765300398,0.304991535250185,125.893665667163));
#36585=CARTESIAN_POINT('Ctrl Pts',(137.557000547451,0.168098317034786,125.888984129614));
#36586=CARTESIAN_POINT('Ctrl Pts',(137.549243506566,0.0313410630940389,
125.884307241834));
#36587=CARTESIAN_POINT('Ctrl Pts',(137.541486465681,-0.105754468711179,
125.885337153207));
#36588=CARTESIAN_POINT('Ctrl Pts',(137.533729424796,-0.242674282057496,
125.892101233603));
#36589=CARTESIAN_POINT('Ctrl Pts',(137.525978233556,-0.379490843106835,
125.898860213155));
#36590=CARTESIAN_POINT('Ctrl Pts',(137.518227042316,-0.516131560542711,
125.911344735497));
#36591=CARTESIAN_POINT('Ctrl Pts',(137.510475851076,-0.652081697699105,
125.929530105433));
#36592=CARTESIAN_POINT('Ctrl Pts',(137.502727954298,-0.787974052421266,
125.947707746102));
#36593=CARTESIAN_POINT('Ctrl Pts',(137.494980057521,-0.9231760239406,125.971581363451));
#36594=CARTESIAN_POINT('Ctrl Pts',(137.487232160744,-1.05717748143791,126.001074363839));
#36595=CARTESIAN_POINT('Ctrl Pts',(137.47948588466,-1.19115090871906,126.030561194928));
#36596=CARTESIAN_POINT('Ctrl Pts',(137.471739608576,-1.3239239398884,126.065664987028));
#36597=CARTESIAN_POINT('Ctrl Pts',(137.463993332492,-1.45499652310436,126.106258002653));
#36598=CARTESIAN_POINT('Ctrl Pts',(137.456246999227,-1.58607007386799,126.146851317926));
#36599=CARTESIAN_POINT('Ctrl Pts',(137.448500665961,-1.71544277816592,126.192933821916));
#36600=CARTESIAN_POINT('Ctrl Pts',(137.440754332696,-1.84263002172215,126.244327978917));
#36601=CARTESIAN_POINT('Ctrl Pts',(137.433006264693,-1.96984574798051,126.295733645282));
#36602=CARTESIAN_POINT('Ctrl Pts',(137.42525819669,-2.0948746771903,126.352453185193));
#36603=CARTESIAN_POINT('Ctrl Pts',(137.417510128687,-2.21725281319327,126.414261185334));
#36604=CARTESIAN_POINT('Ctrl Pts',(137.409753825945,-2.33976101413508,126.476134875752));
#36605=CARTESIAN_POINT('Ctrl Pts',(137.401997523203,-2.45961244448321,126.543107653079));
#36606=CARTESIAN_POINT('Ctrl Pts',(137.394241220461,-2.57636785670945,126.614908179667));
#36607=CARTESIAN_POINT('Ctrl Pts',(137.386480777947,-2.69318558481478,126.686747028358));
#36608=CARTESIAN_POINT('Ctrl Pts',(137.378720335433,-2.8069036781665,126.763418542179));
#36609=CARTESIAN_POINT('Ctrl Pts',(137.370959892919,-2.91711331540635,126.844608988034));
#36610=CARTESIAN_POINT('Ctrl Pts',(137.363186992653,-3.02749987093992,126.925929768001));
#36611=CARTESIAN_POINT('Ctrl Pts',(137.355414092388,-3.13436641069527,127.011783731186));
#36612=CARTESIAN_POINT('Ctrl Pts',(137.347641192122,-3.23733786295673,127.101817353326));
#36613=CARTESIAN_POINT('Ctrl Pts',(137.34015085636,-3.33656604355934,127.188578026521));
#36614=CARTESIAN_POINT('Ctrl Pts',(137.332660520598,-3.43217718898026,127.279219540335));
#36615=CARTESIAN_POINT('Ctrl Pts',(137.325170184836,-3.52387045295582,127.373395725107));
#36616=CARTESIAN_POINT('Ctrl Pts',(137.317499047477,-3.61777700737291,127.469845133021));
#36617=CARTESIAN_POINT('Ctrl Pts',(137.309827910118,-3.70788874961435,127.570325501121));
#36618=CARTESIAN_POINT('Ctrl Pts',(137.302156772759,-3.79383269335377,127.674501745773));
#36619=CARTESIAN_POINT('Ctrl Pts',(137.294494655402,-3.87967558108404,127.778555496215));
#36620=CARTESIAN_POINT('Ctrl Pts',(137.286832538045,-3.96136016024525,127.886296176482));
#36621=CARTESIAN_POINT('Ctrl Pts',(137.279170420688,-4.03854927230723,127.997351027692));
#36622=CARTESIAN_POINT('Ctrl Pts',(137.27151554709,-4.1156654098467,128.108300887737));
#36623=CARTESIAN_POINT('Ctrl Pts',(137.263860673493,-4.18829430409693,128.222558359869));
#36624=CARTESIAN_POINT('Ctrl Pts',(137.256205799895,-4.25613855508317,128.339717101267));
#36625=CARTESIAN_POINT('Ctrl Pts',(137.248556819799,-4.32393057264981,128.456785641924));
#36626=CARTESIAN_POINT('Ctrl Pts',(137.240907839703,-4.38694507721455,128.576750659864));
#36627=CARTESIAN_POINT('Ctrl Pts',(137.233258859608,-4.44492791759091,128.699176808508));
#36628=CARTESIAN_POINT('Ctrl Pts',(137.225613250521,-4.50288520414662,128.821549002295));
#36629=CARTESIAN_POINT('Ctrl Pts',(137.217967641434,-4.55581506643461,128.946379806153));
#36630=CARTESIAN_POINT('Ctrl Pts',(137.210322032347,-4.60350944859244,129.073209607625));
#36631=CARTESIAN_POINT('Ctrl Pts',(137.202677441345,-4.65119747979308,129.200022520511));
#36632=CARTESIAN_POINT('Ctrl Pts',(137.195032850343,-4.69365127397722,129.328833526159));
#36633=CARTESIAN_POINT('Ctrl Pts',(137.187388259341,-4.73071121066212,129.459163790401));
#36634=CARTESIAN_POINT('Ctrl Pts',(137.184985501868,-4.74235945185325,129.500127658345));
#36635=CARTESIAN_POINT('Ctrl Pts',(137.182582744396,-4.75347520330263,129.541241491964));
#36636=CARTESIAN_POINT('Ctrl Pts',(137.180179986924,-4.76405452823403,129.582490119308));
#36637=CARTESIAN_POINT('Origin',(213.235140564004,0.,130.804360617566));
#36638=CARTESIAN_POINT('',(135.084620084674,-4.76405452823407,129.582490119308));
#36639=CARTESIAN_POINT('',(135.430234117584,-4.76405452823404,129.582490119308));
#36640=CARTESIAN_POINT('',(213.235140564004,-4.76405452823405,129.582490119308));
#36641=CARTESIAN_POINT('',(136.764859435954,-4.91824941924801,130.801970519943));
#36642=CARTESIAN_POINT('Ctrl Pts',(136.764859435954,-4.91824941924801,130.801970519943));
#36643=CARTESIAN_POINT('Ctrl Pts',(136.75717491875,-4.91831502016731,130.936961526231));
#36644=CARTESIAN_POINT('Ctrl Pts',(136.749490401545,-4.91281878792003,131.072179136748));
#36645=CARTESIAN_POINT('Ctrl Pts',(136.74180588434,-4.9017310665055,131.207120613289));
#36646=CARTESIAN_POINT('Ctrl Pts',(136.734130242886,-4.89065615160033,131.341906230098));
#36647=CARTESIAN_POINT('Ctrl Pts',(136.726454601431,-4.87400262499367,131.476415951784));
#36648=CARTESIAN_POINT('Ctrl Pts',(136.718778959976,-4.85179282326919,131.6101456153));
#36649=CARTESIAN_POINT('Ctrl Pts',(136.711110247597,-4.82960307112644,131.74375455627));
#36650=CARTESIAN_POINT('Ctrl Pts',(136.703441535218,-4.80186708723321,131.876584447115));
#36651=CARTESIAN_POINT('Ctrl Pts',(136.695772822839,-4.76865909261835,132.008135314463));
#36652=CARTESIAN_POINT('Ctrl Pts',(136.688007968119,-4.7350347707001,132.141335429785));
#36653=CARTESIAN_POINT('Ctrl Pts',(136.680243113399,-4.69580032358549,132.273223816898));
#36654=CARTESIAN_POINT('Ctrl Pts',(136.672478258679,-4.65108650847972,132.403290682684));
#36655=CARTESIAN_POINT('Ctrl Pts',(136.664816681235,-4.60696741422874,132.531627580284));
#36656=CARTESIAN_POINT('Ctrl Pts',(136.657155103791,-4.55751396328245,132.658190728913));
#36657=CARTESIAN_POINT('Ctrl Pts',(136.649493526347,-4.5029020747524,132.78250519461));
#36658=CARTESIAN_POINT('Ctrl Pts',(136.641832628041,-4.44829502712893,132.906808640826));
#36659=CARTESIAN_POINT('Ctrl Pts',(136.634171729735,-4.38853061224154,133.02886343381));
#36660=CARTESIAN_POINT('Ctrl Pts',(136.626510831429,-4.32383268073799,133.148215137685));
#36661=CARTESIAN_POINT('Ctrl Pts',(136.618848864003,-4.25912572029284,133.267583497727));
#36662=CARTESIAN_POINT('Ctrl Pts',(136.611186896577,-4.18948406511449,133.38424766647));
#36663=CARTESIAN_POINT('Ctrl Pts',(136.603524929152,-4.11517699189767,133.497778778167));
#36664=CARTESIAN_POINT('Ctrl Pts',(136.595682544186,-4.03912019845103,133.613983224639));
#36665=CARTESIAN_POINT('Ctrl Pts',(136.587840159219,-3.95817577314425,133.726904853683));
#36666=CARTESIAN_POINT('Ctrl Pts',(136.579997774253,-3.87267802707688,133.836117197685));
#36667=CARTESIAN_POINT('Ctrl Pts',(136.57232439521,-3.78902278498877,133.942975980481));
#36668=CARTESIAN_POINT('Ctrl Pts',(136.564651016167,-3.70100879126266,134.046283463396));
#36669=CARTESIAN_POINT('Ctrl Pts',(136.556977637124,-3.60898789791708,134.145676139211));
#36670=CARTESIAN_POINT('Ctrl Pts',(136.549050749196,-3.51392686880833,134.248352495693));
#36671=CARTESIAN_POINT('Ctrl Pts',(136.541123861268,-3.41458996194518,134.34685058651));
#36672=CARTESIAN_POINT('Ctrl Pts',(136.533196973341,-3.31140286017304,134.440814131656));
#36673=CARTESIAN_POINT('Ctrl Pts',(136.525270085413,-3.2082157584009,134.534777676802));
#36674=CARTESIAN_POINT('Ctrl Pts',(136.517343197485,-3.10117886344023,134.624206435075));
#36675=CARTESIAN_POINT('Ctrl Pts',(136.509416309557,-2.99075052776747,134.708793270738));
#36676=CARTESIAN_POINT('Ctrl Pts',(136.501641975438,-2.88244739726414,134.791752223673));
#36677=CARTESIAN_POINT('Ctrl Pts',(136.493867641319,-2.77051837028484,134.870332911962));
#36678=CARTESIAN_POINT('Ctrl Pts',(136.4860933072,-2.6553529134072,134.944201673423));
#36679=CARTESIAN_POINT('Ctrl Pts',(136.478328554253,-2.54032938766237,135.017979398238));
#36680=CARTESIAN_POINT('Ctrl Pts',(136.470563801305,-2.4220776940936,135.087056541428));
#36681=CARTESIAN_POINT('Ctrl Pts',(136.462799048358,-2.30101990503478,135.151139937837));
#36682=CARTESIAN_POINT('Ctrl Pts',(136.455042007473,-2.18008235227893,135.215159685713));
#36683=CARTESIAN_POINT('Ctrl Pts',(136.447284966588,-2.05634459369694,135.274195375423));
#36684=CARTESIAN_POINT('Ctrl Pts',(136.439527925703,-1.93025688518774,135.327997585724));
#36685=CARTESIAN_POINT('Ctrl Pts',(136.431776734463,-1.80426426040036,135.38175922336));
#36686=CARTESIAN_POINT('Ctrl Pts',(136.424025543223,-1.67592557111555,135.43029508425));
#36687=CARTESIAN_POINT('Ctrl Pts',(136.416274351983,-1.54571451085721,135.473402244434));
#36688=CARTESIAN_POINT('Ctrl Pts',(136.408526455206,-1.41555879377297,135.516491082925));
#36689=CARTESIAN_POINT('Ctrl Pts',(136.400778558429,-1.28353265889378,135.554155687223));
#36690=CARTESIAN_POINT('Ctrl Pts',(136.393030661652,-1.15012835676926,135.586241819087));
#36691=CARTESIAN_POINT('Ctrl Pts',(136.385284385568,-1.01675195994888,135.618321239223));
#36692=CARTESIAN_POINT('Ctrl Pts',(136.377538109484,-0.881998349177671,
135.644824416577));
#36693=CARTESIAN_POINT('Ctrl Pts',(136.369791833399,-0.746373080111705,
135.66564751383));
#36694=CARTESIAN_POINT('Ctrl Pts',(136.362045500134,-0.610746809890719,
135.686470764794));
#36695=CARTESIAN_POINT('Ctrl Pts',(136.354299166869,-0.474249254972687,
135.701613792659));
#36696=CARTESIAN_POINT('Ctrl Pts',(136.346552833603,-0.337393868707141,
135.711024294634));
#36697=CARTESIAN_POINT('Ctrl Pts',(136.3388047656,-0.200507834627103,135.720436904026));
#36698=CARTESIAN_POINT('Ctrl Pts',(136.331056697597,-0.0632641997119973,
135.724114406181));
#36699=CARTESIAN_POINT('Ctrl Pts',(136.323308629594,0.0738211837874544,
135.722056571499));
#36700=CARTESIAN_POINT('Ctrl Pts',(136.315552326853,0.211052263264013,135.719996549725));
#36701=CARTESIAN_POINT('Ctrl Pts',(136.307796024111,0.348124363799805,135.712189020407));
#36702=CARTESIAN_POINT('Ctrl Pts',(136.300039721369,0.48452380304023,135.698685877169));
#36703=CARTESIAN_POINT('Ctrl Pts',(136.292279278855,0.620996042768379,135.685175526897));
#36704=CARTESIAN_POINT('Ctrl Pts',(136.284518836341,0.756794518903235,135.665963560145));
#36705=CARTESIAN_POINT('Ctrl Pts',(136.276758393826,0.891414368124566,135.64115330351));
#36706=CARTESIAN_POINT('Ctrl Pts',(136.268985493561,1.02625032107885,135.616303219248));
#36707=CARTESIAN_POINT('Ctrl Pts',(136.261212593296,1.15990348482117,135.58583697341));
#36708=CARTESIAN_POINT('Ctrl Pts',(136.25343969303,1.29188194283965,135.549908437182));
#36709=CARTESIAN_POINT('Ctrl Pts',(136.245949357268,1.41906265147647,135.515285993745));
#36710=CARTESIAN_POINT('Ctrl Pts',(136.238459021506,1.54468800630241,135.475591593885));
#36711=CARTESIAN_POINT('Ctrl Pts',(136.230968685744,1.66833605699124,135.431004959143));
#36712=CARTESIAN_POINT('Ctrl Pts',(136.223194351625,1.79667226110305,135.384727808592));
#36713=CARTESIAN_POINT('Ctrl Pts',(136.215420017506,1.92328479278158,135.33303352966));
#36714=CARTESIAN_POINT('Ctrl Pts',(136.207645683387,2.04768241638631,135.276069439048));
#36715=CARTESIAN_POINT('Ctrl Pts',(136.19988093044,2.17192673103751,135.219175551587));
#36716=CARTESIAN_POINT('Ctrl Pts',(136.192116177493,2.29396121680107,135.157024935923));
#36717=CARTESIAN_POINT('Ctrl Pts',(136.184351424545,2.41331108512305,135.089814230537));
#36718=CARTESIAN_POINT('Ctrl Pts',(136.176594383661,2.53254241347303,135.02267027977));
#36719=CARTESIAN_POINT('Ctrl Pts',(136.168837342776,2.64909409217947,134.950476431355));
#36720=CARTESIAN_POINT('Ctrl Pts',(136.161080301891,2.76251290177618,134.873476680057));
#36721=CARTESIAN_POINT('Ctrl Pts',(136.15332911065,2.87584618136699,134.79653499487));
#36722=CARTESIAN_POINT('Ctrl Pts',(136.14557791941,2.98605097214634,134.714794839199));
#36723=CARTESIAN_POINT('Ctrl Pts',(136.13782672817,3.0927005055194,134.628545059465));
#36724=CARTESIAN_POINT('Ctrl Pts',(136.130078831393,3.19930470999545,134.542331938188));
#36725=CARTESIAN_POINT('Ctrl Pts',(136.122330934616,3.30235635912813,134.451613250372));
#36726=CARTESIAN_POINT('Ctrl Pts',(136.114583037839,3.40145961447108,134.356719770808));
#36727=CARTESIAN_POINT('Ctrl Pts',(136.106836761755,3.50054213954944,134.261846140914));
#36728=CARTESIAN_POINT('Ctrl Pts',(136.099090485671,3.59567763142809,134.162799726488));
#36729=CARTESIAN_POINT('Ctrl Pts',(136.091344209587,3.68650546364902,134.059949739213));
#36730=CARTESIAN_POINT('Ctrl Pts',(136.083597876321,3.77733396634038,133.957098992723));
#36731=CARTESIAN_POINT('Ctrl Pts',(136.075851543056,3.86385448712737,133.850444910409));
#36732=CARTESIAN_POINT('Ctrl Pts',(136.068105209791,3.94574548811367,133.74039120418));
#36733=CARTESIAN_POINT('Ctrl Pts',(136.060357141788,4.02765482802196,133.630312852186));
#36734=CARTESIAN_POINT('Ctrl Pts',(136.052609073785,4.10493235177089,133.516833674932));
#36735=CARTESIAN_POINT('Ctrl Pts',(136.044861005782,4.17729903545029,133.400387549423));
#36736=CARTESIAN_POINT('Ctrl Pts',(136.03710470304,4.24974263130219,133.283817663586));
#36737=CARTESIAN_POINT('Ctrl Pts',(136.029348400298,4.31726475427772,133.164274863015));
#36738=CARTESIAN_POINT('Ctrl Pts',(136.021592097556,4.37963140609379,133.042219372996));
#36739=CARTESIAN_POINT('Ctrl Pts',(136.013831655042,4.44203134486979,132.920098738288));
#36740=CARTESIAN_POINT('Ctrl Pts',(136.006071212528,4.49927016654367,132.795463096995));
#36741=CARTESIAN_POINT('Ctrl Pts',(135.998310770013,4.55116191175006,132.668793055477));
#36742=CARTESIAN_POINT('Ctrl Pts',(135.990537869748,4.60313695819259,132.541919671963));
#36743=CARTESIAN_POINT('Ctrl Pts',(135.982764969483,4.64974764238295,132.413005729998));
#36744=CARTESIAN_POINT('Ctrl Pts',(135.974992069217,4.6908575276175,132.282548264008));
#36745=CARTESIAN_POINT('Ctrl Pts',(135.967501733455,4.73047296497443,132.156833255509));
#36746=CARTESIAN_POINT('Ctrl Pts',(135.960011397693,4.76498051502194,132.029685293886));
#36747=CARTESIAN_POINT('Ctrl Pts',(135.952521061931,4.79430330812283,131.901556521779));
#36748=CARTESIAN_POINT('Ctrl Pts',(135.944746727812,4.82473788383648,131.768569708335));
#36749=CARTESIAN_POINT('Ctrl Pts',(135.936972393693,4.84968318896769,131.634104979115));
#36750=CARTESIAN_POINT('Ctrl Pts',(135.929198059574,4.86899764036849,131.498655252851));
#36751=CARTESIAN_POINT('Ctrl Pts',(135.921433306627,4.88828828843411,131.36337245627));
#36752=CARTESIAN_POINT('Ctrl Pts',(135.91366855368,4.90196183569212,131.227107461321));
#36753=CARTESIAN_POINT('Ctrl Pts',(135.905903800732,4.90992708485487,131.090366008964));
#36754=CARTESIAN_POINT('Ctrl Pts',(135.898146759847,4.91788442281987,130.953760370144));
#36755=CARTESIAN_POINT('Ctrl Pts',(135.890389718962,4.92014472278587,130.816679603432));
#36756=CARTESIAN_POINT('Ctrl Pts',(135.882632678077,4.91666828826785,130.67963690033));
#36757=CARTESIAN_POINT('Ctrl Pts',(135.874881486837,4.91319447535613,130.542697542196));
#36758=CARTESIAN_POINT('Ctrl Pts',(135.867130295597,4.90399254870659,130.405796579796));
#36759=CARTESIAN_POINT('Ctrl Pts',(135.859379104357,4.8890748441433,130.269449194183));
#36760=CARTESIAN_POINT('Ctrl Pts',(135.85163120758,4.87416348000244,130.133159759847));
#36761=CARTESIAN_POINT('Ctrl Pts',(135.843883310803,4.85354121218845,129.997423822165));
#36762=CARTESIAN_POINT('Ctrl Pts',(135.836135414026,4.82727237055267,129.862753203089));
#36763=CARTESIAN_POINT('Ctrl Pts',(135.828389137942,4.8010090237923,129.728110754202));
#36764=CARTESIAN_POINT('Ctrl Pts',(135.820642861857,4.76910152736892,129.594533564167));
#36765=CARTESIAN_POINT('Ctrl Pts',(135.812896585773,4.73166558211992,129.462524606169));
#36766=CARTESIAN_POINT('Ctrl Pts',(135.805150252508,4.69422936052725,129.330514673711));
#36767=CARTESIAN_POINT('Ctrl Pts',(135.797403919243,4.65126471534227,129.200073372522));
#36768=CARTESIAN_POINT('Ctrl Pts',(135.789657585977,4.60293750174063,129.071689437691));
#36769=CARTESIAN_POINT('Ctrl Pts',(135.781909517974,4.55459946559474,128.943276752168));
#36770=CARTESIAN_POINT('Ctrl Pts',(135.774161449971,4.50089660906874,128.816922715636));
#36771=CARTESIAN_POINT('Ctrl Pts',(135.766413381968,4.44204314593543,128.693096599934));
#36772=CARTESIAN_POINT('Ctrl Pts',(135.758657079226,4.38312713264093,128.569138880362));
#36773=CARTESIAN_POINT('Ctrl Pts',(135.750900776485,4.31904974568052,128.447714802273));
#36774=CARTESIAN_POINT('Ctrl Pts',(135.743144473743,4.25007170383332,128.329269998058));
#36775=CARTESIAN_POINT('Ctrl Pts',(135.735384031229,4.18105684632821,128.210761976285));
#36776=CARTESIAN_POINT('Ctrl Pts',(135.727623588714,4.10713633269439,128.09523672601));
#36777=CARTESIAN_POINT('Ctrl Pts',(135.7198631462,4.02861399509353,127.983110479589));
#36778=CARTESIAN_POINT('Ctrl Pts',(135.712090245935,3.94996560646557,127.870804238163));
#36779=CARTESIAN_POINT('Ctrl Pts',(135.704317345669,3.86670086939134,127.76190821494));
#36780=CARTESIAN_POINT('Ctrl Pts',(135.696544445404,3.77916420564075,127.656805857232));
#36781=CARTESIAN_POINT('Ctrl Pts',(135.689054109642,3.69480972010988,127.555524234964));
#36782=CARTESIAN_POINT('Ctrl Pts',(135.68156377388,3.60648871267436,127.457765476787));
#36783=CARTESIAN_POINT('Ctrl Pts',(135.674073438118,3.51454003382728,127.363838649445));
#36784=CARTESIAN_POINT('Ctrl Pts',(135.666299103999,3.41910509287365,127.266350557895));
#36785=CARTESIAN_POINT('Ctrl Pts',(135.65852476988,3.31945965468791,127.172681895573));
#36786=CARTESIAN_POINT('Ctrl Pts',(135.650750435761,3.21594189661092,127.083218215007));
#36787=CARTESIAN_POINT('Ctrl Pts',(135.642985682814,3.11255171491932,126.993864790432));
#36788=CARTESIAN_POINT('Ctrl Pts',(135.635220929867,3.00529900173171,126.908706289641));
#36789=CARTESIAN_POINT('Ctrl Pts',(135.62745617692,2.89455995687888,126.828092804838));
#36790=CARTESIAN_POINT('Ctrl Pts',(135.619699136035,2.7839308996064,126.747559386485));
#36791=CARTESIAN_POINT('Ctrl Pts',(135.61194209515,2.6698227155848,126.671562229316));
#36792=CARTESIAN_POINT('Ctrl Pts',(135.604185054265,2.55264571044068,126.600412123654));
#36793=CARTESIAN_POINT('Ctrl Pts',(135.596433863024,2.43555706938795,126.529315672839));
#36794=CARTESIAN_POINT('Ctrl Pts',(135.588682671784,2.31540454636224,126.463059200173));
#36795=CARTESIAN_POINT('Ctrl Pts',(135.580931480544,2.19262824558685,126.40191079512));
#36796=CARTESIAN_POINT('Ctrl Pts',(135.573183583767,2.06990412801395,126.34078837977));
#36797=CARTESIAN_POINT('Ctrl Pts',(135.56543568699,1.94455879992063,126.284769887883));
#36798=CARTESIAN_POINT('Ctrl Pts',(135.557687790213,1.81705764346521,126.2340778492));
#36799=CARTESIAN_POINT('Ctrl Pts',(135.549941514129,1.68958315750312,126.183396414198));
#36800=CARTESIAN_POINT('Ctrl Pts',(135.542195238045,1.55995410322297,126.138039360588));
#36801=CARTESIAN_POINT('Ctrl Pts',(135.534448961961,1.4286561853403,126.098181215271));
#36802=CARTESIAN_POINT('Ctrl Pts',(135.526702628695,1.29735729824623,126.05832277573));
#36803=CARTESIAN_POINT('Ctrl Pts',(135.51895629543,1.16438989707475,126.023963439048));
#36804=CARTESIAN_POINT('Ctrl Pts',(135.511209962165,1.0302548172695,125.99522783982));
#36805=CARTESIAN_POINT('Ctrl Pts',(135.503461894162,0.89608969884316,125.966485805454));
#36806=CARTESIAN_POINT('Ctrl Pts',(135.495713826159,0.760756763659207,125.943370096479));
#36807=CARTESIAN_POINT('Ctrl Pts',(135.487965758156,0.624766611181083,125.925954141671));
#36808=CARTESIAN_POINT('Ctrl Pts',(135.480209455414,0.488631926750602,125.908519676979));
#36809=CARTESIAN_POINT('Ctrl Pts',(135.472453152672,0.351839018116533,125.89679711724));
#36810=CARTESIAN_POINT('Ctrl Pts',(135.46469684993,0.21490373329901,125.890807987552));
#36811=CARTESIAN_POINT('Ctrl Pts',(135.456936407416,0.077895361997031,125.884815661286));
#36812=CARTESIAN_POINT('Ctrl Pts',(135.449175964902,-0.059255146132568,
125.884562863309));
#36813=CARTESIAN_POINT('Ctrl Pts',(135.441415522388,-0.196033374314634,
125.890018954774));
#36814=CARTESIAN_POINT('Ctrl Pts',(135.433642622122,-0.333031171051272,
125.895483804841));
#36815=CARTESIAN_POINT('Ctrl Pts',(135.425869721857,-0.469655103727329,
125.906675825836));
#36816=CARTESIAN_POINT('Ctrl Pts',(135.418096821591,-0.605396398879946,
125.923512508608));
#36817=CARTESIAN_POINT('Ctrl Pts',(135.410606485829,-0.736203156042354,
125.939737135551));
#36818=CARTESIAN_POINT('Ctrl Pts',(135.403116150067,-0.866190029849771,
125.961203103802));
#36819=CARTESIAN_POINT('Ctrl Pts',(135.395625814305,-0.994913836728182,
125.98779238697));
#36820=CARTESIAN_POINT('Ctrl Pts',(135.387851480186,-1.12851824586895,126.015389810891));
#36821=CARTESIAN_POINT('Ctrl Pts',(135.380077146067,-1.26118513762943,126.048594140172));
#36822=CARTESIAN_POINT('Ctrl Pts',(135.372302811948,-1.39240734263527,126.0873292572));
#36823=CARTESIAN_POINT('Ctrl Pts',(135.364538059001,-1.52346782800121,126.126016636658));
#36824=CARTESIAN_POINT('Ctrl Pts',(135.356773306054,-1.65308679780187,126.170221132028));
#36825=CARTESIAN_POINT('Ctrl Pts',(135.349008553107,-1.78076636435417,126.219815469126));
#36826=CARTESIAN_POINT('Ctrl Pts',(135.341251512222,-1.90831911776118,126.269360548429));
#36827=CARTESIAN_POINT('Ctrl Pts',(135.333494471336,-2.03393593914977,126.324284675575));
#36828=CARTESIAN_POINT('Ctrl Pts',(135.325737430451,-2.15713357160803,126.38441063858));
#36829=CARTESIAN_POINT('Ctrl Pts',(135.317986239211,-2.28023829977349,126.444491260128));
#36830=CARTESIAN_POINT('Ctrl Pts',(135.310235047971,-2.40092712029292,126.509765738766));
#36831=CARTESIAN_POINT('Ctrl Pts',(135.302483856731,-2.51873659482472,126.580008711251));
#36832=CARTESIAN_POINT('Ctrl Pts',(135.294735959954,-2.6364959971867,126.650221828598));
#36833=CARTESIAN_POINT('Ctrl Pts',(135.286988063177,-2.7513781525014,126.725399039894));
#36834=CARTESIAN_POINT('Ctrl Pts',(135.2792401664,-2.86294428977179,126.805269088711));
#36835=CARTESIAN_POINT('Ctrl Pts',(135.271493890316,-2.97448708981135,126.885122430434));
#36836=CARTESIAN_POINT('Ctrl Pts',(135.263747614231,-3.08271493379622,126.969666429702));
#36837=CARTESIAN_POINT('Ctrl Pts',(135.256001338147,-3.18721845203829,127.058586785434));
#36838=CARTESIAN_POINT('Ctrl Pts',(135.248255004882,-3.29172274170203,127.147507797556));
#36839=CARTESIAN_POINT('Ctrl Pts',(135.240508671617,-3.39250235300254,127.240804977244));
#36840=CARTESIAN_POINT('Ctrl Pts',(135.232762338351,-3.48918171353372,127.338124325499));
#36841=CARTESIAN_POINT('Ctrl Pts',(135.225014270348,-3.5858827247369,127.435465467747));
#36842=CARTESIAN_POINT('Ctrl Pts',(135.217266202345,-3.67848138252594,127.536830293611));
#36843=CARTESIAN_POINT('Ctrl Pts',(135.209518134342,-3.76663991770947,127.641828911351));
#36844=CARTESIAN_POINT('Ctrl Pts',(135.2017618316,-3.8548921488333,127.74693912287));
#36845=CARTESIAN_POINT('Ctrl Pts',(135.194005528859,-3.93869457881135,127.855690541202));
#36846=CARTESIAN_POINT('Ctrl Pts',(135.186249226117,-4.01775026951237,127.967660803639));
#36847=CARTESIAN_POINT('Ctrl Pts',(135.178488783603,-4.09684815461596,128.079690827977));
#36848=CARTESIAN_POINT('Ctrl Pts',(135.170728341088,-4.17119404044526,128.194942791289));
#36849=CARTESIAN_POINT('Ctrl Pts',(135.162967898574,-4.24053564949736,128.312967339129));
#36850=CARTESIAN_POINT('Ctrl Pts',(135.155194998309,-4.30998857185626,128.431181350451));
#36851=CARTESIAN_POINT('Ctrl Pts',(135.147422098043,-4.37442098045509,128.55217649513));
#36852=CARTESIAN_POINT('Ctrl Pts',(135.139649197778,-4.43362728809547,128.675480129433));
#36853=CARTESIAN_POINT('Ctrl Pts',(135.132158862016,-4.4906812973207,128.794301366043));
#36854=CARTESIAN_POINT('Ctrl Pts',(135.124668526254,-4.54288245068104,128.915265884571));
#36855=CARTESIAN_POINT('Ctrl Pts',(135.117178190492,-4.59009049557536,129.037937025975));
#36856=CARTESIAN_POINT('Ctrl Pts',(135.108307742422,-4.64599673583467,129.183210619059));
#36857=CARTESIAN_POINT('Ctrl Pts',(135.099437294352,-4.69504882930383,129.33126094761));
#36858=CARTESIAN_POINT('Ctrl Pts',(135.090566846281,-4.73699786693891,129.481472008833));
#36859=CARTESIAN_POINT('Ctrl Pts',(135.088584592412,-4.74637209939055,129.51503924861));
#36860=CARTESIAN_POINT('Ctrl Pts',(135.086602338543,-4.75539180591618,129.548714296466));
#36861=CARTESIAN_POINT('Ctrl Pts',(135.084620084674,-4.76405452823407,129.582490119308));
#36862=CARTESIAN_POINT('Ctrl Pts',(136.834948208849,-4.76405452823407,129.582490119308));
#36863=CARTESIAN_POINT('Ctrl Pts',(136.827100829603,-4.79844716391908,129.716586483863));
#36864=CARTESIAN_POINT('Ctrl Pts',(136.819253450356,-4.82713745802811,129.851994585027));
#36865=CARTESIAN_POINT('Ctrl Pts',(136.81140607111,-4.85005629057773,129.988188429405));
#36866=CARTESIAN_POINT('Ctrl Pts',(136.803558691863,-4.87297512312734,130.124382273783));
#36867=CARTESIAN_POINT('Ctrl Pts',(136.795711312616,-4.89012250416789,130.261361450188));
#36868=CARTESIAN_POINT('Ctrl Pts',(136.78786393337,-4.90148348379414,130.398598716208));
#36869=CARTESIAN_POINT('Ctrl Pts',(136.780195767577,-4.91258500859702,130.532701844876));
#36870=CARTESIAN_POINT('Ctrl Pts',(136.772527601784,-4.9181839578989,130.667266752074));
#36871=CARTESIAN_POINT('Ctrl Pts',(136.764859435991,-4.91824941924769,130.801970519299));
#36872=CARTESIAN_POINT('',(137.110140564041,-4.91824791103875,130.808893614699));
#36873=CARTESIAN_POINT('Ctrl Pts',(137.180179986924,-4.76405452823403,129.582490119308));
#36874=CARTESIAN_POINT('Ctrl Pts',(137.172532796993,-4.79772505387415,129.713770987757));
#36875=CARTESIAN_POINT('Ctrl Pts',(137.164885607063,-4.82595803982301,129.846417925077));
#36876=CARTESIAN_POINT('Ctrl Pts',(137.157238417133,-4.84866013835519,129.979934802089));
#36877=CARTESIAN_POINT('Ctrl Pts',(137.149388774951,-4.8719632538637,130.116986414428));
#36878=CARTESIAN_POINT('Ctrl Pts',(137.141539132769,-4.88943846897025,130.254954226966));
#36879=CARTESIAN_POINT('Ctrl Pts',(137.133689490587,-4.90104155255462,130.393295218106));
#36880=CARTESIAN_POINT('Ctrl Pts',(137.125839848405,-4.91264463613899,130.531636209247));
#36881=CARTESIAN_POINT('Ctrl Pts',(137.117990206223,-4.91837560247917,130.670349922381));
#36882=CARTESIAN_POINT('Ctrl Pts',(137.110140564041,-4.91824791103875,130.808893614699));
#36883=CARTESIAN_POINT('Ctrl Pts',(137.110140564008,-4.9182479110382,130.808893615287));
#36884=CARTESIAN_POINT('Ctrl Pts',(137.099570896844,-4.9180759724748,130.995444884955));
#36885=CARTESIAN_POINT('Ctrl Pts',(137.08900122968,-4.90728645279196,131.181526057821));
#36886=CARTESIAN_POINT('Ctrl Pts',(137.078431562516,-4.88606103454535,131.366135153477));
#36887=CARTESIAN_POINT('Ctrl Pts',(137.067861895352,-4.86483561629874,131.550744249132));
#36888=CARTESIAN_POINT('Ctrl Pts',(137.057292228188,-4.83317444821162,131.733881895428));
#36889=CARTESIAN_POINT('Ctrl Pts',(137.046722561024,-4.7913059891444,131.914572300485));
#36890=CARTESIAN_POINT('Ctrl Pts',(137.038948226905,-4.76051037516862,132.047475972777));
#36891=CARTESIAN_POINT('Ctrl Pts',(137.031173892785,-4.72413196831382,132.179307847402));
#36892=CARTESIAN_POINT('Ctrl Pts',(137.023399558666,-4.68225903494216,132.30956272765));
#36893=CARTESIAN_POINT('Ctrl Pts',(137.015634805719,-4.64043770621858,132.4396570804));
#36894=CARTESIAN_POINT('Ctrl Pts',(137.007870052772,-4.59313544277444,132.568177937136));
#36895=CARTESIAN_POINT('Ctrl Pts',(137.000105299825,-4.54049143007457,132.694630607784));
#36896=CARTESIAN_POINT('Ctrl Pts',(136.99234825894,-4.48789970415026,132.820957683857));
#36897=CARTESIAN_POINT('Ctrl Pts',(136.984591218055,-4.42997693644635,132.945220303095));
#36898=CARTESIAN_POINT('Ctrl Pts',(136.97683417717,-4.36691188474811,133.066939600352));
#36899=CARTESIAN_POINT('Ctrl Pts',(136.96908298593,-4.30389439089588,133.18856710814));
#36900=CARTESIAN_POINT('Ctrl Pts',(136.96133179469,-4.23574251077828,133.307654765755));
#36901=CARTESIAN_POINT('Ctrl Pts',(136.95358060345,-4.16269266398234,133.42374467641));
#36902=CARTESIAN_POINT('Ctrl Pts',(136.945832706673,-4.08967386531995,133.539785245757));
#36903=CARTESIAN_POINT('Ctrl Pts',(136.938084809895,-4.01176144824017,133.652830272064));
#36904=CARTESIAN_POINT('Ctrl Pts',(136.930336913118,-3.92923712035187,133.762447620098));
#36905=CARTESIAN_POINT('Ctrl Pts',(136.922590637034,-3.84673005477401,133.872042038546));
#36906=CARTESIAN_POINT('Ctrl Pts',(136.91484436095,-3.75961323225081,133.978209892716));
#36907=CARTESIAN_POINT('Ctrl Pts',(136.907098084866,-3.66821068709465,134.08054947317));
#36908=CARTESIAN_POINT('Ctrl Pts',(136.899351751601,-3.5768074672256,134.182889809071));
#36909=CARTESIAN_POINT('Ctrl Pts',(136.891605418335,-3.48111872202904,134.28140152327));
#36910=CARTESIAN_POINT('Ctrl Pts',(136.88385908507,-3.38150736126393,134.375717646514));
#36911=CARTESIAN_POINT('Ctrl Pts',(136.876111017067,-3.2818736932253,134.470054891201));
#36912=CARTESIAN_POINT('Ctrl Pts',(136.868362949064,-3.17831594546179,134.560194406537));
#36913=CARTESIAN_POINT('Ctrl Pts',(136.860614881061,-3.07123200296568,134.645807876928));
#36914=CARTESIAN_POINT('Ctrl Pts',(136.852858578319,-2.96403425038109,134.731512338334));
#36915=CARTESIAN_POINT('Ctrl Pts',(136.845102275577,-2.85330312252009,134.812680901104));
#36916=CARTESIAN_POINT('Ctrl Pts',(136.837345972835,-2.73946798615575,134.889026848157));
#36917=CARTESIAN_POINT('Ctrl Pts',(136.829585530321,-2.62557209255163,134.96541354334));
#36918=CARTESIAN_POINT('Ctrl Pts',(136.821825087807,-2.50856922269159,135.036972290057));
#36919=CARTESIAN_POINT('Ctrl Pts',(136.814064645293,-2.38891465558407,135.10346166672));
#36920=CARTESIAN_POINT('Ctrl Pts',(136.806291745027,-2.26906800834291,135.170057778033));
#36921=CARTESIAN_POINT('Ctrl Pts',(136.798518844762,-2.14656150712895,135.231568081838));
#36922=CARTESIAN_POINT('Ctrl Pts',(136.790745944496,-2.02187259309354,135.287798392287));
#36923=CARTESIAN_POINT('Ctrl Pts',(136.783255608734,-1.90171643515751,135.341984589315));
#36924=CARTESIAN_POINT('Ctrl Pts',(136.775765272972,-1.77953406767676,135.391267895124));
#36925=CARTESIAN_POINT('Ctrl Pts',(136.76827493721,-1.65576538962007,135.435518576115));
#36926=CARTESIAN_POINT('Ctrl Pts',(136.760500603091,-1.52730398451464,135.481447035127));
#36927=CARTESIAN_POINT('Ctrl Pts',(136.752726268972,-1.3967266772231,135.522099199557));
#36928=CARTESIAN_POINT('Ctrl Pts',(136.744951934853,-1.26450621416956,135.557276259235));
#36929=CARTESIAN_POINT('Ctrl Pts',(136.737187181906,-1.13244870101984,135.592409966331));
#36930=CARTESIAN_POINT('Ctrl Pts',(136.729422428959,-0.998752435534629,
135.622081894788));
#36931=CARTESIAN_POINT('Ctrl Pts',(136.721657676012,-0.863908847627266,
135.646141753211));
#36932=CARTESIAN_POINT('Ctrl Pts',(136.713900635127,-0.729199188272466,
135.670177715044));
#36933=CARTESIAN_POINT('Ctrl Pts',(136.706143594242,-0.593344856621078,
135.688612631098));
#36934=CARTESIAN_POINT('Ctrl Pts',(136.698386553357,-0.456850763676913,
135.701346470336));
#36935=CARTESIAN_POINT('Ctrl Pts',(136.690635362117,-0.320459601989821,
135.714070706886));
#36936=CARTESIAN_POINT('Ctrl Pts',(136.682884170877,-0.183430026995121,
135.721102387801));
#36937=CARTESIAN_POINT('Ctrl Pts',(136.675132979637,-0.0462750707891389,
135.722392915175));
#36938=CARTESIAN_POINT('Ctrl Pts',(136.667385082859,0.0908215909015406,
135.723682894041));
#36939=CARTESIAN_POINT('Ctrl Pts',(136.659637186082,0.228043137683621,135.719236568955));
#36940=CARTESIAN_POINT('Ctrl Pts',(136.651889289305,0.364873732101145,135.709057368857));
#36941=CARTESIAN_POINT('Ctrl Pts',(136.644143013221,0.501675704508042,135.698880298028));
#36942=CARTESIAN_POINT('Ctrl Pts',(136.636396737137,0.638086497572104,135.682972766436));
#36943=CARTESIAN_POINT('Ctrl Pts',(136.628650461053,0.773592993303272,135.66139025956));
#36944=CARTESIAN_POINT('Ctrl Pts',(136.620904127788,0.909100489312608,135.639807593367));
#36945=CARTESIAN_POINT('Ctrl Pts',(136.613157794522,1.04370328857031,135.612549929794));
#36946=CARTESIAN_POINT('Ctrl Pts',(136.605411461257,1.17689648786341,135.579724239255));
#36947=CARTESIAN_POINT('Ctrl Pts',(136.597663393254,1.31011951484991,135.546891197631));
#36948=CARTESIAN_POINT('Ctrl Pts',(136.589915325251,1.44193193419066,135.508487741349));
#36949=CARTESIAN_POINT('Ctrl Pts',(136.582167257248,1.57184245811965,135.464671159724));
#36950=CARTESIAN_POINT('Ctrl Pts',(136.574410954507,1.70189105249951,135.420808009315));
#36951=CARTESIAN_POINT('Ctrl Pts',(136.566654651765,1.8300333425375,135.371520366207));
#36952=CARTESIAN_POINT('Ctrl Pts',(136.558898349023,1.95579602180523,135.317014491241));
#36953=CARTESIAN_POINT('Ctrl Pts',(136.551137906509,2.0816258244017,135.262479524848));
#36954=CARTESIAN_POINT('Ctrl Pts',(136.543377463995,2.20507313377636,135.202720947261));
#36955=CARTESIAN_POINT('Ctrl Pts',(136.53561702148,2.32568874568705,135.13799130334));
#36956=CARTESIAN_POINT('Ctrl Pts',(136.527844121215,2.44649798048564,135.073157749649));
#36957=CARTESIAN_POINT('Ctrl Pts',(136.52007122095,2.56446609743282,135.003337382293));
#36958=CARTESIAN_POINT('Ctrl Pts',(136.512298320684,2.67917165387063,134.928826923841));
#36959=CARTESIAN_POINT('Ctrl Pts',(136.504807984922,2.78970737440746,134.857025108233));
#36960=CARTESIAN_POINT('Ctrl Pts',(136.49731764916,2.89721336945666,134.780868452687));
#36961=CARTESIAN_POINT('Ctrl Pts',(136.489827313398,3.00134271432949,134.700656932484));
#36962=CARTESIAN_POINT('Ctrl Pts',(136.482052979279,3.10942015496139,134.617404168113));
#36963=CARTESIAN_POINT('Ctrl Pts',(136.47427864516,3.21420219634503,134.529519269206));
#36964=CARTESIAN_POINT('Ctrl Pts',(136.466504311041,3.31526604286314,134.437292508964));
#36965=CARTESIAN_POINT('Ctrl Pts',(136.458739558094,3.41620533722269,134.345179409962));
#36966=CARTESIAN_POINT('Ctrl Pts',(136.450974805146,3.51343526819386,134.248735357442));
#36967=CARTESIAN_POINT('Ctrl Pts',(136.443210052199,3.60656376149745,134.148292569139));
#36968=CARTESIAN_POINT('Ctrl Pts',(136.435453011314,3.69959975826861,134.04794954203));
#36969=CARTESIAN_POINT('Ctrl Pts',(136.427695970429,3.78854215993315,133.943615967642));
#36970=CARTESIAN_POINT('Ctrl Pts',(136.419938929544,3.87303389081492,133.835662572683));
#36971=CARTESIAN_POINT('Ctrl Pts',(136.412187738304,3.95746190582512,133.72779058622));
#36972=CARTESIAN_POINT('Ctrl Pts',(136.404436547064,4.03744569054372,133.61630451919));
#36973=CARTESIAN_POINT('Ctrl Pts',(136.396685355824,4.11266705179859,133.501609731673));
#36974=CARTESIAN_POINT('Ctrl Pts',(136.388937459047,4.18785644196844,133.386963692499));
#36975=CARTESIAN_POINT('Ctrl Pts',(136.38118956227,4.25828722060567,133.269111971559));
#36976=CARTESIAN_POINT('Ctrl Pts',(136.373441665493,4.32368344982922,133.148490410938));
#36977=CARTESIAN_POINT('Ctrl Pts',(136.365695389409,4.38906599957139,133.027894081747));
#36978=CARTESIAN_POINT('Ctrl Pts',(136.357949113325,4.44941590838845,132.904529408799));
#36979=CARTESIAN_POINT('Ctrl Pts',(136.35020283724,4.5045025049783,132.778858084048));
#36980=CARTESIAN_POINT('Ctrl Pts',(136.342456503975,4.55958950820486,132.65318583162));
#36981=CARTESIAN_POINT('Ctrl Pts',(136.33471017071,4.60941296471849,132.525207251489));
#36982=CARTESIAN_POINT('Ctrl Pts',(136.326963837444,4.65378995923906,132.395404953147));
#36983=CARTESIAN_POINT('Ctrl Pts',(136.319215769441,4.69817689167987,132.265573586482));
#36984=CARTESIAN_POINT('Ctrl Pts',(136.311467701438,4.73711480861872,132.133918058791));
#36985=CARTESIAN_POINT('Ctrl Pts',(136.303719633435,4.7704704889721,132.000936723105));
#36986=CARTESIAN_POINT('Ctrl Pts',(136.295963330694,4.80386162013951,131.867814053272));
#36987=CARTESIAN_POINT('Ctrl Pts',(136.288207027952,4.8316585679088,131.733363140467));
#36988=CARTESIAN_POINT('Ctrl Pts',(136.28045072521,4.85377903168164,131.598093679815));
#36989=CARTESIAN_POINT('Ctrl Pts',(136.272690282696,4.87591130181205,131.46275202178));
#36990=CARTESIAN_POINT('Ctrl Pts',(136.264929840182,4.89236100412251,131.326591333323));
#36991=CARTESIAN_POINT('Ctrl Pts',(136.257169397667,4.9030978058908,131.190126049362));
#36992=CARTESIAN_POINT('Ctrl Pts',(136.249396497402,4.91385184332644,131.053441699213));
#36993=CARTESIAN_POINT('Ctrl Pts',(136.241623597137,4.91887463959558,130.916452167381));
#36994=CARTESIAN_POINT('Ctrl Pts',(136.233850696871,4.91818803574769,130.779672411307));
#36995=CARTESIAN_POINT('Ctrl Pts',(136.226360361109,4.91752639167913,130.647864943895));
#36996=CARTESIAN_POINT('Ctrl Pts',(136.218870025347,4.91156325680349,130.516252572982));
#36997=CARTESIAN_POINT('Ctrl Pts',(136.211379689585,4.90036348755281,130.385289320101));
#36998=CARTESIAN_POINT('Ctrl Pts',(136.203605355466,4.88873907564683,130.249360555681));
#36999=CARTESIAN_POINT('Ctrl Pts',(136.195831021347,4.87143627397818,130.113700522116));
#37000=CARTESIAN_POINT('Ctrl Pts',(136.188056687228,4.84847076625396,129.978821829089));
#37001=CARTESIAN_POINT('Ctrl Pts',(136.180291934281,4.82553356146554,129.844109361996));
#37002=CARTESIAN_POINT('Ctrl Pts',(136.172527181334,4.79694760130631,129.710176701212));
#37003=CARTESIAN_POINT('Ctrl Pts',(136.164762428386,4.76278046423991,129.57753328173));
#37004=CARTESIAN_POINT('Ctrl Pts',(136.157005387501,4.72864726245571,129.445021605562));
#37005=CARTESIAN_POINT('Ctrl Pts',(136.149248346617,4.68894401208142,129.313796998616));
#37006=CARTESIAN_POINT('Ctrl Pts',(136.141491305732,4.64378960787083,129.184360265612));
#37007=CARTESIAN_POINT('Ctrl Pts',(136.133740114491,4.59866925494771,129.055021141855));
#37008=CARTESIAN_POINT('Ctrl Pts',(136.125988923251,4.54810605865902,128.927467576084));
#37009=CARTESIAN_POINT('Ctrl Pts',(136.118237732011,4.49226906873743,128.802186380252));
#37010=CARTESIAN_POINT('Ctrl Pts',(136.110489835234,4.43645581102606,128.676958432269));
#37011=CARTESIAN_POINT('Ctrl Pts',(136.102741938457,4.37537337668544,128.554001289642));
#37012=CARTESIAN_POINT('Ctrl Pts',(136.09499404168,4.30923930084178,128.433782690017));
#37013=CARTESIAN_POINT('Ctrl Pts',(136.087247765596,4.24311905882105,128.313589237532));
#37014=CARTESIAN_POINT('Ctrl Pts',(136.079501489512,4.17194946544494,128.196133530968));
#37015=CARTESIAN_POINT('Ctrl Pts',(136.071755213427,4.09599427175701,128.081859196403));
#37016=CARTESIAN_POINT('Ctrl Pts',(136.064008880162,4.02003851738514,127.967584018291));
#37017=CARTESIAN_POINT('Ctrl Pts',(136.056262546897,3.93929730862969,127.85649058464));
#37018=CARTESIAN_POINT('Ctrl Pts',(136.048516213631,3.85407780834988,127.748993649478));
#37019=CARTESIAN_POINT('Ctrl Pts',(136.040768145628,3.76883922375391,127.641472641122));
#37020=CARTESIAN_POINT('Ctrl Pts',(136.033020077625,3.67912059484687,127.53755004024));
#37021=CARTESIAN_POINT('Ctrl Pts',(136.025272009622,3.58526919089529,127.437607301489));
#37022=CARTESIAN_POINT('Ctrl Pts',(136.017515706881,3.49131804055468,127.337558342405));
#37023=CARTESIAN_POINT('Ctrl Pts',(136.009759404139,3.39322560901152,127.241497980479));
#37024=CARTESIAN_POINT('Ctrl Pts',(136.002003101397,3.29137623172681,127.1497709602));
#37025=CARTESIAN_POINT('Ctrl Pts',(135.994242658883,3.18947249436276,127.057994982449));
#37026=CARTESIAN_POINT('Ctrl Pts',(135.986482216369,3.08380811679827,126.970557203995));
#37027=CARTESIAN_POINT('Ctrl Pts',(135.978721773854,2.97479951212098,126.887761209255));
#37028=CARTESIAN_POINT('Ctrl Pts',(135.970948873589,2.86561591715413,126.804832303033));
#37029=CARTESIAN_POINT('Ctrl Pts',(135.963175973324,2.753077688351,126.726560294169));
#37030=CARTESIAN_POINT('Ctrl Pts',(135.955403073058,2.63762987961105,126.653205154242));
#37031=CARTESIAN_POINT('Ctrl Pts',(135.947912737296,2.52637888951411,126.582516658423));
#37032=CARTESIAN_POINT('Ctrl Pts',(135.940422401534,2.41242645434999,126.516393911388));
#37033=CARTESIAN_POINT('Ctrl Pts',(135.932932065772,2.29618961177886,126.455027757315));
#37034=CARTESIAN_POINT('Ctrl Pts',(135.925157731653,2.17554561399248,126.391334886858));
#37035=CARTESIAN_POINT('Ctrl Pts',(135.917383397534,2.05205839871615,126.332564662121));
#37036=CARTESIAN_POINT('Ctrl Pts',(135.909609063415,1.92616771642072,126.27898096601));
#37037=CARTESIAN_POINT('Ctrl Pts',(135.901844310468,1.80043218314012,126.225463307015));
#37038=CARTESIAN_POINT('Ctrl Pts',(135.89407955752,1.67229943273503,126.177119610253));
#37039=CARTESIAN_POINT('Ctrl Pts',(135.886314804573,1.54223459510521,126.134168382105));
#37040=CARTESIAN_POINT('Ctrl Pts',(135.878557763688,1.41229893970581,126.091259813722));
#37041=CARTESIAN_POINT('Ctrl Pts',(135.870800722803,1.28043538477516,126.053733177323));
#37042=CARTESIAN_POINT('Ctrl Pts',(135.863043681918,1.14712953702657,126.021759140568));
#37043=CARTESIAN_POINT('Ctrl Pts',(135.855292490678,1.01392421625455,125.989809215683));
#37044=CARTESIAN_POINT('Ctrl Pts',(135.847541299438,0.87927914619829,125.963403646777));
#37045=CARTESIAN_POINT('Ctrl Pts',(135.839790108198,0.743695271049467,125.942663341273));
#37046=CARTESIAN_POINT('Ctrl Pts',(135.832042211421,0.6081690226644,125.921931850952));
#37047=CARTESIAN_POINT('Ctrl Pts',(135.824294314644,0.471705148462137,125.906860893922));
#37048=CARTESIAN_POINT('Ctrl Pts',(135.816546417867,0.334814752422365,125.897520275344));
#37049=CARTESIAN_POINT('Ctrl Pts',(135.808800141783,0.197952990902429,125.888181610622));
#37050=CARTESIAN_POINT('Ctrl Pts',(135.801053865698,0.0606652748179095,
125.884570926744));
#37051=CARTESIAN_POINT('Ctrl Pts',(135.793307589614,-0.0765325967660386,
125.886706113218));
#37052=CARTESIAN_POINT('Ctrl Pts',(135.785561256349,-0.213731481113414,
125.888841315454));
#37053=CARTESIAN_POINT('Ctrl Pts',(135.777814923084,-0.350840128718959,
125.896722466594));
#37054=CARTESIAN_POINT('Ctrl Pts',(135.770068589818,-0.487343566245976,
125.910315326507));
#37055=CARTESIAN_POINT('Ctrl Pts',(135.762320521815,-0.623877572771378,
125.923911230447));
#37056=CARTESIAN_POINT('Ctrl Pts',(135.754572453812,-0.759805710557421,
125.943221349683));
#37057=CARTESIAN_POINT('Ctrl Pts',(135.746824385809,-0.894619343478421,
125.968159702305));
#37058=CARTESIAN_POINT('Ctrl Pts',(135.739068083068,-1.02957625793288,125.993124559705));
#37059=CARTESIAN_POINT('Ctrl Pts',(135.731311780326,-1.16341591628201,126.023729528458));
#37060=CARTESIAN_POINT('Ctrl Pts',(135.723555477584,-1.2956405325183,126.059837599074));
#37061=CARTESIAN_POINT('Ctrl Pts',(135.71579503507,-1.42793572101357,126.095964941655));
#37062=CARTESIAN_POINT('Ctrl Pts',(135.708034592555,-1.55861377746305,126.13760112003));
#37063=CARTESIAN_POINT('Ctrl Pts',(135.700274150041,-1.68719420625387,126.184559888867));
#37064=CARTESIAN_POINT('Ctrl Pts',(135.692501249776,-1.81598104376382,126.231594040089));
#37065=CARTESIAN_POINT('Ctrl Pts',(135.68472834951,-1.94266316316723,126.283967706538));
#37066=CARTESIAN_POINT('Ctrl Pts',(135.676955449245,-2.06678128050621,126.341446972754));
#37067=CARTESIAN_POINT('Ctrl Pts',(135.669465113483,-2.1863873916445,126.396836722861));
#37068=CARTESIAN_POINT('Ctrl Pts',(135.661974777721,-2.30361240606622,126.456967173955));
#37069=CARTESIAN_POINT('Ctrl Pts',(135.654484441959,-2.41807034211935,126.52159061638));
#37070=CARTESIAN_POINT('Ctrl Pts',(135.646709017723,-2.53688464341573,126.588673681336));
#37071=CARTESIAN_POINT('Ctrl Pts',(135.638933593486,-2.65309348094871,126.660811054195));
#37072=CARTESIAN_POINT('Ctrl Pts',(135.63115816925,-2.76623695472661,126.737775296587));
#37073=CARTESIAN_POINT('Ctrl Pts',(135.623392564522,-2.87923754069221,126.814642341572));
#37074=CARTESIAN_POINT('Ctrl Pts',(135.615626959795,-2.98918014595701,126.896323907967));
#37075=CARTESIAN_POINT('Ctrl Pts',(135.607861355068,-3.09562938257853,126.982546678058));
#37076=CARTESIAN_POINT('Ctrl Pts',(135.600105132703,-3.20195000779408,127.068665274254));
#37077=CARTESIAN_POINT('Ctrl Pts',(135.592348910338,-3.30478536874702,127.159313901849));
#37078=CARTESIAN_POINT('Ctrl Pts',(135.584592687973,-3.40372953011546,127.254176347937));
#37079=CARTESIAN_POINT('Ctrl Pts',(135.57684178538,-3.50260582850577,127.34897373058));
#37080=CARTESIAN_POINT('Ctrl Pts',(135.569090882787,-3.59759595600647,127.447978912464));
#37081=CARTESIAN_POINT('Ctrl Pts',(135.561339980194,-3.68832746322366,127.550835823357));
#37082=CARTESIAN_POINT('Ctrl Pts',(135.5535927151,-3.77901639014381,127.653644463502));
#37083=CARTESIAN_POINT('Ctrl Pts',(135.545845450005,-3.86545041598168,127.760300942952));
#37084=CARTESIAN_POINT('Ctrl Pts',(135.538098184911,-3.94729463202187,127.870413080456));
#37085=CARTESIAN_POINT('Ctrl Pts',(135.530352877854,-4.02911816282088,127.980497388308));
#37086=CARTESIAN_POINT('Ctrl Pts',(135.522607570797,-4.10635396062298,128.094035301791));
#37087=CARTESIAN_POINT('Ctrl Pts',(135.51486226374,-4.17870828117702,128.210602694528));
#37088=CARTESIAN_POINT('Ctrl Pts',(135.507114921424,-4.25108161451235,128.327200718059));
#37089=CARTESIAN_POINT('Ctrl Pts',(135.499367579107,-4.3185706968598,128.446829481985));
#37090=CARTESIAN_POINT('Ctrl Pts',(135.491620236791,-4.38092588068271,128.569037041333));
#37091=CARTESIAN_POINT('Ctrl Pts',(135.483871903469,-4.44328904069723,128.691260232916));
#37092=CARTESIAN_POINT('Ctrl Pts',(135.476123570148,-4.5005168236209,128.816062525076));
#37093=CARTESIAN_POINT('Ctrl Pts',(135.468375236827,-4.5524066197537,128.942969462832));
#37094=CARTESIAN_POINT('Ctrl Pts',(135.460620817355,-4.60433717421597,129.069976083284));
#37095=CARTESIAN_POINT('Ctrl Pts',(135.452866397883,-4.65092122662039,129.199090286265));
#37096=CARTESIAN_POINT('Ctrl Pts',(135.44511197841,-4.6920050906097,129.329819572972));
#37097=CARTESIAN_POINT('Ctrl Pts',(135.440152691468,-4.71828000015651,129.413426611108));
#37098=CARTESIAN_POINT('Ctrl Pts',(135.435193404526,-4.74230625146068,129.497693918245));
#37099=CARTESIAN_POINT('Ctrl Pts',(135.430234117584,-4.76405452823404,129.582490119308));
#37100=CARTESIAN_POINT('Origin',(213.235140564004,0.,130.804360617566));
#37101=CARTESIAN_POINT('',(133.334729823376,-4.76405452823402,129.582490119308));
#37102=CARTESIAN_POINT('',(133.679929079587,-4.76405452823404,129.582490119308));
#37103=CARTESIAN_POINT('',(213.235140564004,-4.76405452823405,129.582490119308));
#37104=CARTESIAN_POINT('',(135.014859436046,-4.91824892140636,130.801103381751));
#37105=CARTESIAN_POINT('Ctrl Pts',(135.014859435991,-4.91824892140701,130.801103382733));
#37106=CARTESIAN_POINT('Ctrl Pts',(135.00706768985,-4.9183404006375,130.939232086896));
#37107=CARTESIAN_POINT('Ctrl Pts',(134.999275943709,-4.91260854852309,131.07739304955));
#37108=CARTESIAN_POINT('Ctrl Pts',(134.991484197567,-4.90107189874953,131.215064045586));
#37109=CARTESIAN_POINT('Ctrl Pts',(134.983692153207,-4.88953480742615,131.352740310795));
#37110=CARTESIAN_POINT('Ctrl Pts',(134.975900108848,-4.87219250742866,131.489926188914));
#37111=CARTESIAN_POINT('Ctrl Pts',(134.968108064488,-4.84911548938473,131.626103906622));
#37112=CARTESIAN_POINT('Ctrl Pts',(134.960314108631,-4.82603281022766,131.762315030616));
#37113=CARTESIAN_POINT('Ctrl Pts',(134.952520152775,-4.79721267620561,131.897517122828));
#37114=CARTESIAN_POINT('Ctrl Pts',(134.944726196918,-4.76277678234938,132.031202247123));
#37115=CARTESIAN_POINT('Ctrl Pts',(134.936928715398,-4.72832531111852,132.164947845041));
#37116=CARTESIAN_POINT('Ctrl Pts',(134.929131233878,-4.68825311816046,132.297174736941));
#37117=CARTESIAN_POINT('Ctrl Pts',(134.921333752358,-4.64273177880704,132.427390097445));
#37118=CARTESIAN_POINT('Ctrl Pts',(134.913526281164,-4.59715212019576,132.557772282196));
#37119=CARTESIAN_POINT('Ctrl Pts',(134.90571880997,-4.54610950054951,132.686137426018));
#37120=CARTESIAN_POINT('Ctrl Pts',(134.897911338777,-4.48982391918956,132.81201204079));
#37121=CARTESIAN_POINT('Ctrl Pts',(134.890098268532,-4.43349797318495,132.93797692529));
#37122=CARTESIAN_POINT('Ctrl Pts',(134.882285198288,-4.3719217447522,133.061447378862));
#37123=CARTESIAN_POINT('Ctrl Pts',(134.874472128044,-4.30536080807937,133.181975257232));
#37124=CARTESIAN_POINT('Ctrl Pts',(134.866646520133,-4.23869306078745,133.302696547203));
#37125=CARTESIAN_POINT('Ctrl Pts',(134.858820912222,-4.16702482837157,133.420465503421));
#37126=CARTESIAN_POINT('Ctrl Pts',(134.85099530431,-4.09066492895952,133.534863044132));
#37127=CARTESIAN_POINT('Ctrl Pts',(134.846907058433,-4.05077307040069,133.594626487361));
#37128=CARTESIAN_POINT('Ctrl Pts',(134.842818812556,-4.00960142714413,133.653470343483));
#37129=CARTESIAN_POINT('Ctrl Pts',(134.838730566679,-3.9671982273736,133.711338651061));
#37130=CARTESIAN_POINT('Ctrl Pts',(134.83095623256,-3.88656299831506,133.821382804852));
#37131=CARTESIAN_POINT('Ctrl Pts',(134.823181898441,-3.80121788816482,133.928243666845));
#37132=CARTESIAN_POINT('Ctrl Pts',(134.815407564322,-3.71144294060409,134.031491597421));
#37133=CARTESIAN_POINT('Ctrl Pts',(134.807642811375,-3.62177863264288,134.13461228415));
#37134=CARTESIAN_POINT('Ctrl Pts',(134.799878058428,-3.52769560387842,134.234128606638));
#37135=CARTESIAN_POINT('Ctrl Pts',(134.792113305481,-3.42951656767255,134.329640631205));
#37136=CARTESIAN_POINT('Ctrl Pts',(134.784356264596,-3.3314350442696,134.425057791882));
#37137=CARTESIAN_POINT('Ctrl Pts',(134.776599223711,-3.22926588777218,134.516478298438));
#37138=CARTESIAN_POINT('Ctrl Pts',(134.768842182826,-3.1233711492963,134.603536281607));
#37139=CARTESIAN_POINT('Ctrl Pts',(134.761090991586,-3.01755626686638,134.690528613674));
#37140=CARTESIAN_POINT('Ctrl Pts',(134.753339800346,-2.90802169536307,134.773164723247));
#37141=CARTESIAN_POINT('Ctrl Pts',(134.745588609106,-2.79516504237249,134.85111678126));
#37142=CARTESIAN_POINT('Ctrl Pts',(134.737840712329,-2.68235635646991,134.92903570757));
#37143=CARTESIAN_POINT('Ctrl Pts',(134.730092815552,-2.56622871840148,135.002274320232));
#37144=CARTESIAN_POINT('Ctrl Pts',(134.722344918774,-2.44721122299368,135.070546301822));
#37145=CARTESIAN_POINT('Ctrl Pts',(134.71459864269,-2.32821862348028,135.138804002385));
#37146=CARTESIAN_POINT('Ctrl Pts',(134.706852366606,-2.20633770791888,135.202096943917));
#37147=CARTESIAN_POINT('Ctrl Pts',(134.699106090522,-2.08202449983253,135.260183442208));
#37148=CARTESIAN_POINT('Ctrl Pts',(134.691359757257,-1.9577103740944,135.31827036928));
#37149=CARTESIAN_POINT('Ctrl Pts',(134.683613423991,-1.83096427420974,135.371150610916));
#37150=CARTESIAN_POINT('Ctrl Pts',(134.675867090726,-1.70226428123129,135.418629723215));
#37151=CARTESIAN_POINT('Ctrl Pts',(134.668119022723,-1.57353546678149,135.466119468131));
#37152=CARTESIAN_POINT('Ctrl Pts',(134.66037095472,-1.44285225527326,135.508205541562));
#37153=CARTESIAN_POINT('Ctrl Pts',(134.652622886717,-1.31070965928222,135.54474280169));
#37154=CARTESIAN_POINT('Ctrl Pts',(134.644866583975,-1.17842662056782,135.581318894053));
#37155=CARTESIAN_POINT('Ctrl Pts',(134.637110281234,-1.04468147640565,135.612334288174));
#37156=CARTESIAN_POINT('Ctrl Pts',(134.629353978492,-0.909981800154545,
135.637694475876));
#37157=CARTESIAN_POINT('Ctrl Pts',(134.621593535978,-0.775210230630404,
135.663068199074));
#37158=CARTESIAN_POINT('Ctrl Pts',(134.613833093463,-0.639483500586702,
135.682780645364));
#37159=CARTESIAN_POINT('Ctrl Pts',(134.606072650949,-0.503315168893812,
135.696789145737));
#37160=CARTESIAN_POINT('Ctrl Pts',(134.598299750684,-0.366928247706432,
135.710820133799));
#37161=CARTESIAN_POINT('Ctrl Pts',(134.590526850418,-0.230098698736417,
135.719128854669));
#37162=CARTESIAN_POINT('Ctrl Pts',(134.582753950153,-0.0933418552538072,
135.721724785548));
#37163=CARTESIAN_POINT('Ctrl Pts',(134.575263614391,0.0384435324981373,
135.724226347802));
#37164=CARTESIAN_POINT('Ctrl Pts',(134.567773278629,0.17016110109541,135.721423264168));
#37165=CARTESIAN_POINT('Ctrl Pts',(134.560282942867,0.30135540337624,135.713369477138));
#37166=CARTESIAN_POINT('Ctrl Pts',(134.552508608748,0.437523977503984,135.705010328325));
#37167=CARTESIAN_POINT('Ctrl Pts',(134.544734274629,0.573560163861853,135.690967976185));
#37168=CARTESIAN_POINT('Ctrl Pts',(134.53695994051,0.70895112402018,135.671245798691));
#37169=CARTESIAN_POINT('Ctrl Pts',(134.529195187563,0.844175226920348,135.651547927017));
#37170=CARTESIAN_POINT('Ctrl Pts',(134.521430434615,0.978755302631332,135.626184213474));
#37171=CARTESIAN_POINT('Ctrl Pts',(134.513665681668,1.11218044116573,135.595209992029));
#37172=CARTESIAN_POINT('Ctrl Pts',(134.505908640783,1.24547305997129,135.564266534616));
#37173=CARTESIAN_POINT('Ctrl Pts',(134.498151599898,1.37761264600742,135.527723746538));
#37174=CARTESIAN_POINT('Ctrl Pts',(134.490394559013,1.50809568562692,135.485688470376));
#37175=CARTESIAN_POINT('Ctrl Pts',(134.482643367773,1.6384803269714,135.443684893343));
#37176=CARTESIAN_POINT('Ctrl Pts',(134.474892176533,1.76721053775918,135.39619719188));
#37177=CARTESIAN_POINT('Ctrl Pts',(134.467140985293,1.89379558950122,135.343382684893));
#37178=CARTESIAN_POINT('Ctrl Pts',(134.459393088516,2.02032683921959,135.290590625481));
#37179=CARTESIAN_POINT('Ctrl Pts',(134.451645191739,2.14471438322918,135.232476413766));
#37180=CARTESIAN_POINT('Ctrl Pts',(134.443897294962,2.26648539833556,135.169246297814));
#37181=CARTESIAN_POINT('Ctrl Pts',(134.436151018878,2.3882309415705,135.106029408239));
#37182=CARTESIAN_POINT('Ctrl Pts',(134.428404742794,2.50736069779764,135.037698923044));
#37183=CARTESIAN_POINT('Ctrl Pts',(134.42065846671,2.62342483939446,134.964507871516));
#37184=CARTESIAN_POINT('Ctrl Pts',(134.412912133444,2.73948983775018,134.891316279708));
#37185=CARTESIAN_POINT('Ctrl Pts',(134.405165800179,2.85248884561819,134.813264258516));
#37186=CARTESIAN_POINT('Ctrl Pts',(134.397419466914,2.96199985734986,134.730648929389));
#37187=CARTESIAN_POINT('Ctrl Pts',(134.389671398911,3.07153539331361,134.648015099132));
#37188=CARTESIAN_POINT('Ctrl Pts',(134.381923330908,3.17758106676573,134.560816162849));
#37189=CARTESIAN_POINT('Ctrl Pts',(134.374175262905,3.27974719939589,134.46939013594));
#37190=CARTESIAN_POINT('Ctrl Pts',(134.366418960163,3.38202191540753,134.377866940363));
#37191=CARTESIAN_POINT('Ctrl Pts',(134.358662657421,3.48040856220899,134.282107940835));
#37192=CARTESIAN_POINT('Ctrl Pts',(134.350906354679,3.57455327159708,134.182489089222));
#37193=CARTESIAN_POINT('Ctrl Pts',(134.343145912165,3.66874822885115,134.082817068029));
#37194=CARTESIAN_POINT('Ctrl Pts',(134.335385469651,3.7586964810979,133.979281384785));
#37195=CARTESIAN_POINT('Ctrl Pts',(134.327625027137,3.84408453857975,133.872291047473));
#37196=CARTESIAN_POINT('Ctrl Pts',(134.319852126871,3.92960966855198,133.765128959774));
#37197=CARTESIAN_POINT('Ctrl Pts',(134.312079226606,4.01055974420107,133.654501451593));
#37198=CARTESIAN_POINT('Ctrl Pts',(134.30430632634,4.08666418874456,133.540847210066));
#37199=CARTESIAN_POINT('Ctrl Pts',(134.296815990578,4.16000204503434,133.431324586495));
#37200=CARTESIAN_POINT('Ctrl Pts',(134.289325654816,4.2288402945944,133.318991730424));
#37201=CARTESIAN_POINT('Ctrl Pts',(134.281835319054,4.29297814045349,133.204260979683));
#37202=CARTESIAN_POINT('Ctrl Pts',(134.274060984935,4.35954779223176,133.085180177658));
#37203=CARTESIAN_POINT('Ctrl Pts',(134.266286650816,4.4212644452716,132.963138846995));
#37204=CARTESIAN_POINT('Ctrl Pts',(134.258512316697,4.47785373985819,132.838570279066));
#37205=CARTESIAN_POINT('Ctrl Pts',(134.25074756375,4.53437329319673,132.714155230763));
#37206=CARTESIAN_POINT('Ctrl Pts',(134.242982810803,4.58577790087803,132.587219494849));
#37207=CARTESIAN_POINT('Ctrl Pts',(134.235218057855,4.63183795760822,132.458222823725));
#37208=CARTESIAN_POINT('Ctrl Pts',(134.22746101697,4.67785226684053,132.329354273913));
#37209=CARTESIAN_POINT('Ctrl Pts',(134.219703976086,4.71853245822587,132.19842922823));
#37210=CARTESIAN_POINT('Ctrl Pts',(134.211946935201,4.75369626002962,132.065929057993));
#37211=CARTESIAN_POINT('Ctrl Pts',(134.20419574396,4.78883354453696,131.933528807164));
#37212=CARTESIAN_POINT('Ctrl Pts',(134.19644455272,4.81846261971568,131.799556172407));
#37213=CARTESIAN_POINT('Ctrl Pts',(134.18869336148,4.84245059168189,131.66450905221));
#37214=CARTESIAN_POINT('Ctrl Pts',(134.180945464703,4.86642836812017,131.52951933064));
#37215=CARTESIAN_POINT('Ctrl Pts',(134.173197567926,4.88476974179557,131.393456416076));
#37216=CARTESIAN_POINT('Ctrl Pts',(134.165449671149,4.89739266256268,131.256829590179));
#37217=CARTESIAN_POINT('Ctrl Pts',(134.157703395065,4.91001294288687,131.120231343669));
#37218=CARTESIAN_POINT('Ctrl Pts',(134.149957118981,4.91691711361933,130.983069809512));
#37219=CARTESIAN_POINT('Ctrl Pts',(134.142210842897,4.91807491264784,130.845860208937));
#37220=CARTESIAN_POINT('Ctrl Pts',(134.134464509631,4.91923272022296,130.708649595512));
#37221=CARTESIAN_POINT('Ctrl Pts',(134.126718176366,4.91464406815236,130.571391305913));
#37222=CARTESIAN_POINT('Ctrl Pts',(134.118971843101,4.90433082876644,130.434600986845));
#37223=CARTESIAN_POINT('Ctrl Pts',(134.111223775098,4.89401527980205,130.297780034533));
#37224=CARTESIAN_POINT('Ctrl Pts',(134.103475707095,4.87797262191486,130.161427651074));
#37225=CARTESIAN_POINT('Ctrl Pts',(134.095727639092,4.85627660639018,130.026054389448));
#37226=CARTESIAN_POINT('Ctrl Pts',(134.08797133635,4.83455753208206,129.890537251508));
#37227=CARTESIAN_POINT('Ctrl Pts',(134.080215033608,4.80717315956721,129.756001700811));
#37228=CARTESIAN_POINT('Ctrl Pts',(134.072458730866,4.77424851338938,129.622948667864));
#37229=CARTESIAN_POINT('Ctrl Pts',(134.064698288352,4.7413062943365,129.489824620506));
#37230=CARTESIAN_POINT('Ctrl Pts',(134.056937845838,4.70281801918803,129.358185042631));
#37231=CARTESIAN_POINT('Ctrl Pts',(134.049177403323,4.65895834907157,129.228514760854));
#37232=CARTESIAN_POINT('Ctrl Pts',(134.041404503058,4.61502827151903,129.09863632083));
#37233=CARTESIAN_POINT('Ctrl Pts',(134.033631602792,4.56570970895668,128.970733859162));
#37234=CARTESIAN_POINT('Ctrl Pts',(134.025858702527,4.51122548793434,128.845272140873));
#37235=CARTESIAN_POINT('Ctrl Pts',(134.018368366765,4.45872190558375,128.724371272063));
#37236=CARTESIAN_POINT('Ctrl Pts',(134.010878031003,4.40142184769512,128.60573705052));
#37237=CARTESIAN_POINT('Ctrl Pts',(134.003387695241,4.33956369009485,128.489761291093));
#37238=CARTESIAN_POINT('Ctrl Pts',(133.995613361122,4.27536016164765,128.369388275496));
#37239=CARTESIAN_POINT('Ctrl Pts',(133.987839027003,4.2060426922519,128.251497987139));
#37240=CARTESIAN_POINT('Ctrl Pts',(133.980064692884,4.13182752408236,128.136555457189));
#37241=CARTESIAN_POINT('Ctrl Pts',(133.972299939937,4.05770381947484,128.021754583634));
#37242=CARTESIAN_POINT('Ctrl Pts',(133.96453518699,3.97869463592205,127.909894565498));
#37243=CARTESIAN_POINT('Ctrl Pts',(133.956770434042,3.89506266887186,127.801417083621));
#37244=CARTESIAN_POINT('Ctrl Pts',(133.949013393157,3.81151376627034,127.693047343108));
#37245=CARTESIAN_POINT('Ctrl Pts',(133.941256352272,3.7233514544595,127.588053760759));
#37246=CARTESIAN_POINT('Ctrl Pts',(133.933499311387,3.63088220243694,127.4868498799));
#37247=CARTESIAN_POINT('Ctrl Pts',(133.925748120147,3.53848268219638,127.385722317675));
#37248=CARTESIAN_POINT('Ctrl Pts',(133.917996928907,3.44178294913729,127.288379056039));
#37249=CARTESIAN_POINT('Ctrl Pts',(133.910245737667,3.34113006696793,127.195201028672));
#37250=CARTESIAN_POINT('Ctrl Pts',(133.90249784089,3.24051996495884,127.102062604454));
#37251=CARTESIAN_POINT('Ctrl Pts',(133.894749944113,3.13596034191829,127.013086158482));
#37252=CARTESIAN_POINT('Ctrl Pts',(133.887002047336,3.02783532082514,126.928616001049));
#37253=CARTESIAN_POINT('Ctrl Pts',(133.879255771252,2.9197329171555,126.844163512951));
#37254=CARTESIAN_POINT('Ctrl Pts',(133.871509495168,2.80806690677753,126.764215679009));
#37255=CARTESIAN_POINT('Ctrl Pts',(133.863763219083,2.69325440249207,126.689076449254));
#37256=CARTESIAN_POINT('Ctrl Pts',(133.856016885818,2.57844105068655,126.613936664839));
#37257=CARTESIAN_POINT('Ctrl Pts',(133.848270552553,2.46048148576158,126.543605769535));
#37258=CARTESIAN_POINT('Ctrl Pts',(133.840524219287,2.33982135842349,126.478344081171));
#37259=CARTESIAN_POINT('Ctrl Pts',(133.832776151284,2.21913421008648,126.413067777904));
#37260=CARTESIAN_POINT('Ctrl Pts',(133.825028083281,2.09574563973077,126.352863126485));
#37261=CARTESIAN_POINT('Ctrl Pts',(133.817280015278,1.97012505440905,126.297944044224));
#37262=CARTESIAN_POINT('Ctrl Pts',(133.809523712537,1.84437095803453,126.24296659331));
#37263=CARTESIAN_POINT('Ctrl Pts',(133.801767409795,1.71638046674353,126.193286090107));
#37264=CARTESIAN_POINT('Ctrl Pts',(133.794011107053,1.58664260637883,126.149068113102));
#37265=CARTESIAN_POINT('Ctrl Pts',(133.786250664539,1.45683550101181,126.104826535631));
#37266=CARTESIAN_POINT('Ctrl Pts',(133.778490222024,1.32527954307293,126.066053404241));
#37267=CARTESIAN_POINT('Ctrl Pts',(133.77072977951,1.19247703953137,126.032863832207));
#37268=CARTESIAN_POINT('Ctrl Pts',(133.762956879245,1.05946134962138,125.999620981326));
#37269=CARTESIAN_POINT('Ctrl Pts',(133.755183978979,0.925195498496844,125.971979680061));
#37270=CARTESIAN_POINT('Ctrl Pts',(133.747411078714,0.790190949326217,125.950003674973));
#37271=CARTESIAN_POINT('Ctrl Pts',(133.739920742952,0.660094155574433,125.928826553023));
#37272=CARTESIAN_POINT('Ctrl Pts',(133.73243040719,0.529311744174783,125.912910020001));
#37273=CARTESIAN_POINT('Ctrl Pts',(133.724940071428,0.398302208012137,125.902265309069));
#37274=CARTESIAN_POINT('Ctrl Pts',(133.717165737309,0.262325405465818,125.891217000685));
#37275=CARTESIAN_POINT('Ctrl Pts',(133.70939140319,0.125673181662655,125.885813170373));
#37276=CARTESIAN_POINT('Ctrl Pts',(133.701617069071,-0.0111463353276202,
125.886123248171));
#37277=CARTESIAN_POINT('Ctrl Pts',(133.693852316124,-0.14779723449093,125.886432943827));
#37278=CARTESIAN_POINT('Ctrl Pts',(133.686087563176,-0.284614629405755,
125.892442535471));
#37279=CARTESIAN_POINT('Ctrl Pts',(133.678322810229,-0.421084928165682,
125.904169749266));
#37280=CARTESIAN_POINT('Ctrl Pts',(133.670565769344,-0.55741968270108,125.915885315427));
#37281=CARTESIAN_POINT('Ctrl Pts',(133.662808728459,-0.693407640122305,
125.933307169369));
#37282=CARTESIAN_POINT('Ctrl Pts',(133.655051687574,-0.828535220736507,
125.956401000315));
#37283=CARTESIAN_POINT('Ctrl Pts',(133.647300496334,-0.963560900591121,
125.979477416023));
#37284=CARTESIAN_POINT('Ctrl Pts',(133.639549305094,-1.09772711125099,126.008217229468));
#37285=CARTESIAN_POINT('Ctrl Pts',(133.631798113854,-1.23052576600856,126.042534350083));
#37286=CARTESIAN_POINT('Ctrl Pts',(133.624050217077,-1.36326797779543,126.076836885007));
#37287=CARTESIAN_POINT('Ctrl Pts',(133.6163023203,-1.49464341199928,126.116711914735));
#37288=CARTESIAN_POINT('Ctrl Pts',(133.608554423523,-1.62415476276908,126.162022373849));
#37289=CARTESIAN_POINT('Ctrl Pts',(133.600808147439,-1.75363902255623,126.207323354992));
#37290=CARTESIAN_POINT('Ctrl Pts',(133.593061871355,-1.88125960569524,126.258057374989));
#37291=CARTESIAN_POINT('Ctrl Pts',(133.58531559527,-2.00653533075908,126.314037797443));
#37292=CARTESIAN_POINT('Ctrl Pts',(133.577569262005,-2.1318119805791,126.370018633132));
#37293=CARTESIAN_POINT('Ctrl Pts',(133.56982292874,-2.25474338083662,126.431245789052));
#37294=CARTESIAN_POINT('Ctrl Pts',(133.562076595474,-2.37486963367725,126.497485034787));
#37295=CARTESIAN_POINT('Ctrl Pts',(133.554328527472,-2.49502278795956,126.563739114342));
#37296=CARTESIAN_POINT('Ctrl Pts',(133.546580459469,-2.61236920249317,126.635007328455));
#37297=CARTESIAN_POINT('Ctrl Pts',(133.538832391466,-2.72647517660756,126.711010379211));
#37298=CARTESIAN_POINT('Ctrl Pts',(133.531076088724,-2.84070242390967,126.787094206913));
#37299=CARTESIAN_POINT('Ctrl Pts',(133.523319785982,-2.95168202516372,126.867922706621));
#37300=CARTESIAN_POINT('Ctrl Pts',(133.51556348324,-3.05901034408721,126.953173946257));
#37301=CARTESIAN_POINT('Ctrl Pts',(133.507803040726,-3.1663959473658,127.038470687047));
#37302=CARTESIAN_POINT('Ctrl Pts',(133.500042598212,-3.27012608961524,127.128194615716));
#37303=CARTESIAN_POINT('Ctrl Pts',(133.492282155698,-3.36983241359037,127.221985348723));
#37304=CARTESIAN_POINT('Ctrl Pts',(133.484509255432,-3.46969879500853,127.315926642942));
#37305=CARTESIAN_POINT('Ctrl Pts',(133.476736355167,-3.5655281767636,127.413947507589));
#37306=CARTESIAN_POINT('Ctrl Pts',(133.468963454901,-3.65699046873391,127.51565209079));
#37307=CARTESIAN_POINT('Ctrl Pts',(133.461473119139,-3.74512787601217,127.613659456214));
#37308=CARTESIAN_POINT('Ctrl Pts',(133.453982783377,-3.82920999392396,127.715087127994));
#37309=CARTESIAN_POINT('Ctrl Pts',(133.446492447615,-3.90897954508848,127.819555434882));
#37310=CARTESIAN_POINT('Ctrl Pts',(133.438698763919,-3.99197964950509,127.928254559463));
#37311=CARTESIAN_POINT('Ctrl Pts',(133.430905080222,-4.07057665885007,128.040594229956));
#37312=CARTESIAN_POINT('Ctrl Pts',(133.423111396526,-4.14443493069619,128.156183477017));
#37313=CARTESIAN_POINT('Ctrl Pts',(133.415330435805,-4.21817263094185,128.271584027807));
#37314=CARTESIAN_POINT('Ctrl Pts',(133.407549475083,-4.28718679338726,128.390223265882));
#37315=CARTESIAN_POINT('Ctrl Pts',(133.399768514361,-4.35118251058085,128.511677948265));
#37316=CARTESIAN_POINT('Ctrl Pts',(133.391994871904,-4.41511803757263,128.633018398287));
#37317=CARTESIAN_POINT('Ctrl Pts',(133.384221229447,-4.47404432737747,128.757168684957));
#37318=CARTESIAN_POINT('Ctrl Pts',(133.37644758699,-4.52771001302225,128.883677119309));
#37319=CARTESIAN_POINT('Ctrl Pts',(133.368680664419,-4.58132930764104,129.010076194095));
#37320=CARTESIAN_POINT('Ctrl Pts',(133.360913741847,-4.62969690070071,129.138829002326));
#37321=CARTESIAN_POINT('Ctrl Pts',(133.353146819275,-4.67260785241139,129.269460321103));
#37322=CARTESIAN_POINT('Ctrl Pts',(133.347007820642,-4.70652479589331,129.372711702843));
#37323=CARTESIAN_POINT('Ctrl Pts',(133.340868822009,-4.73703364669907,129.477136112303));
#37324=CARTESIAN_POINT('Ctrl Pts',(133.334729823376,-4.76405452823402,129.582490119308));
#37325=CARTESIAN_POINT('Ctrl Pts',(135.084620084674,-4.76405452823407,129.582490119308));
#37326=CARTESIAN_POINT('Ctrl Pts',(135.07579945711,-4.80260188508095,129.732785678617));
#37327=CARTESIAN_POINT('Ctrl Pts',(135.066978829546,-4.83407694623485,129.885078300731));
#37328=CARTESIAN_POINT('Ctrl Pts',(135.058158201982,-4.85829197544408,130.038735288939));
#37329=CARTESIAN_POINT('Ctrl Pts',(135.049393588783,-4.88235322993912,130.191416496393));
#37330=CARTESIAN_POINT('Ctrl Pts',(135.040628975584,-4.8992462793229,130.345444623537));
#37331=CARTESIAN_POINT('Ctrl Pts',(135.031864362385,-4.90883460055151,130.50017987043));
#37332=CARTESIAN_POINT('Ctrl Pts',(135.026196053605,-4.91503562325125,130.600251275586));
#37333=CARTESIAN_POINT('Ctrl Pts',(135.020527744826,-4.91818237243618,130.70061805634));
#37334=CARTESIAN_POINT('Ctrl Pts',(135.014859436046,-4.91824892140636,130.801103381751));
#37335=CARTESIAN_POINT('',(135.360140563978,-4.91824970511146,130.80265748193));
#37336=CARTESIAN_POINT('Ctrl Pts',(135.430234117584,-4.76405452823404,129.582490119308));
#37337=CARTESIAN_POINT('Ctrl Pts',(135.422470239396,-4.79810195755941,129.715240529506));
#37338=CARTESIAN_POINT('Ctrl Pts',(135.414706361208,-4.82656381027021,129.849287313936));
#37339=CARTESIAN_POINT('Ctrl Pts',(135.40694248302,-4.8493700162653,129.984120708852));
#37340=CARTESIAN_POINT('Ctrl Pts',(135.399167540465,-4.87220872357314,130.119146255954));
#37341=CARTESIAN_POINT('Ctrl Pts',(135.39139259791,-4.88937564496455,130.254960265062));
#37342=CARTESIAN_POINT('Ctrl Pts',(135.383617655355,-4.90085264228569,130.391049063044));
#37343=CARTESIAN_POINT('Ctrl Pts',(135.381090709619,-4.90458279839146,130.435279487302));
#37344=CARTESIAN_POINT('Ctrl Pts',(135.378563763883,-4.90771232449835,130.479538949501));
#37345=CARTESIAN_POINT('Ctrl Pts',(135.376036818146,-4.91024178091484,130.523809881587));
#37346=CARTESIAN_POINT('Ctrl Pts',(135.370738066767,-4.91554579693871,130.616641579199));
#37347=CARTESIAN_POINT('Ctrl Pts',(135.365439315388,-4.9182174890166,130.709625109034));
#37348=CARTESIAN_POINT('Ctrl Pts',(135.360140564008,-4.91824970511128,130.802657481398));
#37349=CARTESIAN_POINT('Ctrl Pts',(135.360140563978,-4.91824970511146,130.80265748193));
#37350=CARTESIAN_POINT('Ctrl Pts',(135.352434020783,-4.91829656042319,130.937964452346));
#37351=CARTESIAN_POINT('Ctrl Pts',(135.344727477589,-4.9127555070284,131.073499126688));
#37352=CARTESIAN_POINT('Ctrl Pts',(135.337020934394,-4.9015963568133,131.208756732006));
#37353=CARTESIAN_POINT('Ctrl Pts',(135.329323602338,-4.89045054441684,131.343852672559));
#37354=CARTESIAN_POINT('Ctrl Pts',(135.321626270282,-4.8737000241861,131.478671809661));
#37355=CARTESIAN_POINT('Ctrl Pts',(135.313928938225,-4.85136658957273,131.612707867254));
#37356=CARTESIAN_POINT('Ctrl Pts',(135.306238885862,-4.82905427663341,131.746617161275));
#37357=CARTESIAN_POINT('Ctrl Pts',(135.298548833498,-4.80116961870553,131.879744458713));
#37358=CARTESIAN_POINT('Ctrl Pts',(135.290858781135,-4.76778629558902,132.011587564786));
#37359=CARTESIAN_POINT('Ctrl Pts',(135.282805881684,-4.73282781524928,132.149651550072));
#37360=CARTESIAN_POINT('Ctrl Pts',(135.274752982234,-4.69183914262272,132.286306757394));
#37361=CARTESIAN_POINT('Ctrl Pts',(135.266700082784,-4.64496535698311,132.420986701398));
#37362=CARTESIAN_POINT('Ctrl Pts',(135.259018075935,-4.60025043851293,132.549463687704));
#37363=CARTESIAN_POINT('Ctrl Pts',(135.251336069085,-4.55018055014769,132.676142878261));
#37364=CARTESIAN_POINT('Ctrl Pts',(135.243654062235,-4.49493283453246,132.800547451392));
#37365=CARTESIAN_POINT('Ctrl Pts',(135.235973032723,-4.43969214776671,132.924936197244));
#37366=CARTESIAN_POINT('Ctrl Pts',(135.228292003211,-4.37927510531011,133.047050537171));
#37367=CARTESIAN_POINT('Ctrl Pts',(135.220610973699,-4.3139067855382,133.16643413636));
#37368=CARTESIAN_POINT('Ctrl Pts',(135.212929187623,-4.24853202714298,133.285829494548));
#37369=CARTESIAN_POINT('Ctrl Pts',(135.205247401548,-4.1782052128679,133.4024932277));
#37370=CARTESIAN_POINT('Ctrl Pts',(135.197565615473,-4.10319687070256,133.515994535107));
#37371=CARTESIAN_POINT('Ctrl Pts',(135.189881338679,-4.02816420806,133.629532643833));
#37372=CARTESIAN_POINT('Ctrl Pts',(135.182197061884,-3.94844721793339,133.739905955303));
#37373=CARTESIAN_POINT('Ctrl Pts',(135.17451278509,-3.86435884791437,133.846713943044));
#37374=CARTESIAN_POINT('Ctrl Pts',(135.166820103302,-3.78017850277946,133.953638756417));
#37375=CARTESIAN_POINT('Ctrl Pts',(135.159127421514,-3.69161748003889,134.056990148703));
#37376=CARTESIAN_POINT('Ctrl Pts',(135.151434739725,-3.59902819490115,134.156401654726));
#37377=CARTESIAN_POINT('Ctrl Pts',(135.143737131849,-3.50637961926161,134.255876819931));
#37378=CARTESIAN_POINT('Ctrl Pts',(135.136039523973,-3.40969792771429,134.35140679649));
#37379=CARTESIAN_POINT('Ctrl Pts',(135.128341916097,-3.30937033630008,134.442663936383));
#37380=CARTESIAN_POINT('Ctrl Pts',(135.120633362036,-3.20890007662033,134.53405084614));
#37381=CARTESIAN_POINT('Ctrl Pts',(135.112924807975,-3.10477387357521,134.621152537841));
#37382=CARTESIAN_POINT('Ctrl Pts',(135.105216253913,-2.9974100002693,134.703683168059));
#37383=CARTESIAN_POINT('Ctrl Pts',(135.10267390072,-2.96200039115256,134.73090254145));
#37384=CARTESIAN_POINT('Ctrl Pts',(135.100131547527,-2.92623882241581,134.757625063772));
#37385=CARTESIAN_POINT('Ctrl Pts',(135.097589194333,-2.89014090169641,134.783841567494));
#37386=CARTESIAN_POINT('Ctrl Pts',(135.089814860214,-2.77975604352618,134.864009759663));
#37387=CARTESIAN_POINT('Ctrl Pts',(135.082040526095,-2.66585819687516,134.939708585154));
#37388=CARTESIAN_POINT('Ctrl Pts',(135.074266191976,-2.54884521608402,135.010614429088));
#37389=CARTESIAN_POINT('Ctrl Pts',(135.066501439029,-2.43197644333395,135.081432887907));
#37390=CARTESIAN_POINT('Ctrl Pts',(135.058736686082,-2.31200050631387,135.147469917514));
#37391=CARTESIAN_POINT('Ctrl Pts',(135.050971933135,-2.18934682107491,135.20844321892));
#37392=CARTESIAN_POINT('Ctrl Pts',(135.04321489225,-2.06681495720533,135.269355960784));
#37393=CARTESIAN_POINT('Ctrl Pts',(135.035457851365,-1.94161098562287,135.325214810203));
#37394=CARTESIAN_POINT('Ctrl Pts',(135.02770081048,-1.81419138048192,135.375781917062));
#37395=CARTESIAN_POINT('Ctrl Pts',(135.019949619239,-1.68686786345621,135.426310890873));
#37396=CARTESIAN_POINT('Ctrl Pts',(135.012198427999,-1.55733240047529,135.471555921429));
#37397=CARTESIAN_POINT('Ctrl Pts',(135.004447236759,-1.42606370914016,135.511326238853));
#37398=CARTESIAN_POINT('Ctrl Pts',(134.996699339982,-1.29485081050081,135.55107965283));
#37399=CARTESIAN_POINT('Ctrl Pts',(134.988951443205,-1.1619065220706,135.585362868575));
#37400=CARTESIAN_POINT('Ctrl Pts',(134.981203546428,-1.02772687004141,135.614034259623));
#37401=CARTESIAN_POINT('Ctrl Pts',(134.973457270344,-0.89357528550275,135.642699653233));
#37402=CARTESIAN_POINT('Ctrl Pts',(134.96571099426,-0.75818923345157,135.665755475399));
#37403=CARTESIAN_POINT('Ctrl Pts',(134.957964718176,-0.622076754692063,
135.683110823692));
#37404=CARTESIAN_POINT('Ctrl Pts',(134.95021838491,-0.485963271181158,135.700466300098));
#37405=CARTESIAN_POINT('Ctrl Pts',(134.942472051645,-0.349123738087069,
135.712121169213));
#37406=CARTESIAN_POINT('Ctrl Pts',(134.93472571838,-0.212072776246219,135.718036247894));
#37407=CARTESIAN_POINT('Ctrl Pts',(134.926977650377,-0.0749911227926161,
135.723952651215));
#37408=CARTESIAN_POINT('Ctrl Pts',(134.919229582374,0.0623016630979726,
135.724126689477));
#37409=CARTESIAN_POINT('Ctrl Pts',(134.911481514371,0.199289891304434,135.718571296986));
#37410=CARTESIAN_POINT('Ctrl Pts',(134.903725211629,0.336423712230015,135.713010000157));
#37411=CARTESIAN_POINT('Ctrl Pts',(134.895968908887,0.473251937603753,135.701707124396));
#37412=CARTESIAN_POINT('Ctrl Pts',(134.888212606145,0.609262376606084,135.684727654885));
#37413=CARTESIAN_POINT('Ctrl Pts',(134.880452163631,0.745345408474906,135.667739122921));
#37414=CARTESIAN_POINT('Ctrl Pts',(134.872691721117,0.880609398856398,135.645068024731));
#37415=CARTESIAN_POINT('Ctrl Pts',(134.864931278603,1.01455228559113,135.616830536672));
#37416=CARTESIAN_POINT('Ctrl Pts',(134.857158378337,1.14871018933854,135.58854771929));
#37417=CARTESIAN_POINT('Ctrl Pts',(134.849385478072,1.28154237243552,135.554680752383));
#37418=CARTESIAN_POINT('Ctrl Pts',(134.841612577806,1.4125610051424,135.515396010052));
#37419=CARTESIAN_POINT('Ctrl Pts',(134.834122242044,1.53881678053471,135.477539367056));
#37420=CARTESIAN_POINT('Ctrl Pts',(134.826631906282,1.66338827936151,135.434652109796));
#37421=CARTESIAN_POINT('Ctrl Pts',(134.81914157052,1.78585827494905,135.386924668869));
#37422=CARTESIAN_POINT('Ctrl Pts',(134.811367236401,1.91297175764289,135.337387627513));
#37423=CARTESIAN_POINT('Ctrl Pts',(134.803592902282,2.03822389165481,135.282479207595));
#37424=CARTESIAN_POINT('Ctrl Pts',(134.795818568163,2.16112736063343,135.222359213494));
#37425=CARTESIAN_POINT('Ctrl Pts',(134.788053815216,2.28387936207048,135.162313311912));
#37426=CARTESIAN_POINT('Ctrl Pts',(134.780289062269,2.40428810987845,135.097068785749));
#37427=CARTESIAN_POINT('Ctrl Pts',(134.772524309322,2.52188398805953,135.02683432539));
#37428=CARTESIAN_POINT('Ctrl Pts',(134.764767268437,2.63936306835699,134.956669622888));
#37429=CARTESIAN_POINT('Ctrl Pts',(134.757010227552,2.75403450529529,134.881525048174));
#37430=CARTESIAN_POINT('Ctrl Pts',(134.749253186667,2.86545145340681,134.801656082086));
#37431=CARTESIAN_POINT('Ctrl Pts',(134.741501995427,2.97678438113099,134.721847345806));
#37432=CARTESIAN_POINT('Ctrl Pts',(134.733750804187,3.0848673885647,134.637321536352));
#37433=CARTESIAN_POINT('Ctrl Pts',(134.725999612946,3.18928121704955,134.548378296621));
#37434=CARTESIAN_POINT('Ctrl Pts',(134.718251716169,3.29365066687183,134.459472860139));
#37435=CARTESIAN_POINT('Ctrl Pts',(134.710503819392,3.39435374247058,134.366153980629));
#37436=CARTESIAN_POINT('Ctrl Pts',(134.702755922615,3.49100317521703,134.26876242641));
#37437=CARTESIAN_POINT('Ctrl Pts',(134.695009646531,3.58763239098567,134.171391244406));
#37438=CARTESIAN_POINT('Ctrl Pts',(134.687263370447,3.68020937527026,134.069949359533));
#37439=CARTESIAN_POINT('Ctrl Pts',(134.679517094363,3.76838304081943,133.964815065927));
#37440=CARTESIAN_POINT('Ctrl Pts',(134.671770761098,3.85655735724633,133.859679996244));
#37441=CARTESIAN_POINT('Ctrl Pts',(134.664024427832,3.94032803884466,133.750852762998));
#37442=CARTESIAN_POINT('Ctrl Pts',(134.656278094567,4.01938395459308,133.638745151827));
#37443=CARTESIAN_POINT('Ctrl Pts',(134.648530026564,4.09845757436607,133.526612434934));
#37444=CARTESIAN_POINT('Ctrl Pts',(134.640781958561,4.17281410202161,133.411198197762));
#37445=CARTESIAN_POINT('Ctrl Pts',(134.633033890558,4.24218567645094,133.292943296324));
#37446=CARTESIAN_POINT('Ctrl Pts',(134.625277587816,4.31163097981501,133.17456271217));
#37447=CARTESIAN_POINT('Ctrl Pts',(134.617521285074,4.37608054835242,133.053335770549));
#37448=CARTESIAN_POINT('Ctrl Pts',(134.609764982333,4.43531220429017,132.929728518183));
#37449=CARTESIAN_POINT('Ctrl Pts',(134.602004539818,4.49457547394611,132.806055292906));
#37450=CARTESIAN_POINT('Ctrl Pts',(134.594244097304,4.54861512776828,132.679999584579));
#37451=CARTESIAN_POINT('Ctrl Pts',(134.58648365479,4.59725753135398,132.552046588474));
#37452=CARTESIAN_POINT('Ctrl Pts',(134.578710754525,4.64597802004418,132.423888190861));
#37453=CARTESIAN_POINT('Ctrl Pts',(134.570937854259,4.68928382119304,132.293826790359));
#37454=CARTESIAN_POINT('Ctrl Pts',(134.563164953994,4.72705122615383,132.162362741209));
#37455=CARTESIAN_POINT('Ctrl Pts',(134.555674618232,4.7634456908141,132.035677741382));
#37456=CARTESIAN_POINT('Ctrl Pts',(134.54818428247,4.79469736459525,131.907690601243));
#37457=CARTESIAN_POINT('Ctrl Pts',(134.540693946708,4.820740940943,131.778855277796));
#37458=CARTESIAN_POINT('Ctrl Pts',(134.532919612589,4.84777196740363,131.645135123902));
#37459=CARTESIAN_POINT('Ctrl Pts',(134.525145278469,4.86927779652637,131.510077614055));
#37460=CARTESIAN_POINT('Ctrl Pts',(134.51737094435,4.88512946986935,131.374179119472));
#37461=CARTESIAN_POINT('Ctrl Pts',(134.509606191403,4.90096160744162,131.238448107638));
#37462=CARTESIAN_POINT('Ctrl Pts',(134.501841438456,4.91115340909654,131.101878557876));
#37463=CARTESIAN_POINT('Ctrl Pts',(134.494076685509,4.91562661304959,130.964978373678));
#37464=CARTESIAN_POINT('Ctrl Pts',(134.486319644624,4.92009537415343,130.828214160673));
#37465=CARTESIAN_POINT('Ctrl Pts',(134.478562603739,4.91885682791216,130.691120354972));
#37466=CARTESIAN_POINT('Ctrl Pts',(134.470805562854,4.91188438670001,130.554210993955));
#37467=CARTESIAN_POINT('Ctrl Pts',(134.463054371614,4.90491720346003,130.417404877353));
#37468=CARTESIAN_POINT('Ctrl Pts',(134.455303180374,4.89222475166342,130.280783317462));
#37469=CARTESIAN_POINT('Ctrl Pts',(134.447551989134,4.87383250981955,130.14486101277));
#37470=CARTESIAN_POINT('Ctrl Pts',(134.439804092357,4.8554480851691,130.008996478684));
#37471=CARTESIAN_POINT('Ctrl Pts',(134.432056195579,4.8313687410798,129.873830995308));
#37472=CARTESIAN_POINT('Ctrl Pts',(134.424308298802,4.80167184743674,129.739874576308));
#37473=CARTESIAN_POINT('Ctrl Pts',(134.416562022718,4.77198116574363,129.605946178103));
#37474=CARTESIAN_POINT('Ctrl Pts',(134.408815746634,4.73667535634123,129.473226722679));
#37475=CARTESIAN_POINT('Ctrl Pts',(134.40106947055,4.69588291756345,129.342216066902));
#37476=CARTESIAN_POINT('Ctrl Pts',(134.393323137285,4.65509017766517,129.211204444035));
#37477=CARTESIAN_POINT('Ctrl Pts',(134.385576804019,4.60881084380448,129.081902019275));
#37478=CARTESIAN_POINT('Ctrl Pts',(134.377830470754,4.55722318898415,128.954793136157));
#37479=CARTESIAN_POINT('Ctrl Pts',(134.370082402751,4.50562398146631,128.827655787887));
#37480=CARTESIAN_POINT('Ctrl Pts',(134.362334334748,4.44871423448981,128.702713320944));
#37481=CARTESIAN_POINT('Ctrl Pts',(134.354586266745,4.38672006723145,128.580429387908));
#37482=CARTESIAN_POINT('Ctrl Pts',(134.346829964003,4.32466001183421,128.458015490053));
#37483=CARTESIAN_POINT('Ctrl Pts',(134.339073661261,4.257504918586,128.338266119657));
#37484=CARTESIAN_POINT('Ctrl Pts',(134.331317358519,4.18552679327976,128.22162011081));
#37485=CARTESIAN_POINT('Ctrl Pts',(134.323556916005,4.11351025108077,128.104911844477));
#37486=CARTESIAN_POINT('Ctrl Pts',(134.315796473491,4.03666576646497,127.991310563801));
#37487=CARTESIAN_POINT('Ctrl Pts',(134.308036030977,3.95530769431998,127.881224612219));
#37488=CARTESIAN_POINT('Ctrl Pts',(134.300263130711,3.8738190189749,127.770961940896));
#37489=CARTESIAN_POINT('Ctrl Pts',(134.292490230446,3.78780252252585,127.664226180007));
#37490=CARTESIAN_POINT('Ctrl Pts',(134.284717330181,3.69761229962191,127.561391862831));
#37491=CARTESIAN_POINT('Ctrl Pts',(134.277226994418,3.61070071849538,127.462295832108));
#37492=CARTESIAN_POINT('Ctrl Pts',(134.269736658656,3.51991380575471,127.366822738357));
#37493=CARTESIAN_POINT('Ctrl Pts',(134.262246322894,3.42559818849807,127.275272900682));
#37494=CARTESIAN_POINT('Ctrl Pts',(134.254471988775,3.32770656594715,127.180251923087));
#37495=CARTESIAN_POINT('Ctrl Pts',(134.246697654656,3.225703283835,127.089156576933));
#37496=CARTESIAN_POINT('Ctrl Pts',(134.238923320537,3.11993624813733,127.00236365938));
#37497=CARTESIAN_POINT('Ctrl Pts',(134.23115856759,3.01429956085856,126.91567770634));
#37498=CARTESIAN_POINT('Ctrl Pts',(134.223393814643,2.90490864853648,126.833283877418));
#37499=CARTESIAN_POINT('Ctrl Pts',(134.215629061696,2.79214852235655,126.755522550712));
#37500=CARTESIAN_POINT('Ctrl Pts',(134.207872020811,2.67950039112358,126.677838457653));
#37501=CARTESIAN_POINT('Ctrl Pts',(134.200114979926,2.56349002519221,126.604777930999));
#37502=CARTESIAN_POINT('Ctrl Pts',(134.192357939041,2.44453552750779,126.536641189434));
#37503=CARTESIAN_POINT('Ctrl Pts',(134.184606747801,2.32567073433508,126.468555830316));
#37504=CARTESIAN_POINT('Ctrl Pts',(134.17685555656,2.20386656644816,126.405387059193));
#37505=CARTESIAN_POINT('Ctrl Pts',(134.16910436532,2.07956982601877,126.347391647379));
#37506=CARTESIAN_POINT('Ctrl Pts',(134.161356468543,1.95532591502003,126.289420885162));
#37507=CARTESIAN_POINT('Ctrl Pts',(134.153608571766,1.82859189211915,126.236619273941));
#37508=CARTESIAN_POINT('Ctrl Pts',(134.145860674989,1.69983866657038,126.189197395086));
#37509=CARTESIAN_POINT('Ctrl Pts',(134.138114398905,1.5711123734208,126.141785435866));
#37510=CARTESIAN_POINT('Ctrl Pts',(134.130368122821,1.44036808438728,126.099751105718));
#37511=CARTESIAN_POINT('Ctrl Pts',(134.122621846737,1.30809579969763,126.063256480204));
#37512=CARTESIAN_POINT('Ctrl Pts',(134.114875513472,1.17582253860448,126.026761585294));
#37513=CARTESIAN_POINT('Ctrl Pts',(134.107129180206,1.04202163623152,125.9958065806));
#37514=CARTESIAN_POINT('Ctrl Pts',(134.099382846941,0.907196945425237,125.970503279507));
#37515=CARTESIAN_POINT('Ctrl Pts',(134.091634778938,0.772342061563523,125.945194311914));
#37516=CARTESIAN_POINT('Ctrl Pts',(134.083886710935,0.636463317230123,125.925539638541));
#37517=CARTESIAN_POINT('Ctrl Pts',(134.076138642932,0.500073019410448,125.911599634465));
#37518=CARTESIAN_POINT('Ctrl Pts',(134.06838234019,0.363537764359557,125.897644814786));
#37519=CARTESIAN_POINT('Ctrl Pts',(134.060626037448,0.226490259311975,125.889416836927));
#37520=CARTESIAN_POINT('Ctrl Pts',(134.052869734706,0.0894467335911126,
125.886924055255));
#37521=CARTESIAN_POINT('Ctrl Pts',(134.045109292192,-0.0476699363857279,
125.884429943111));
#37522=CARTESIAN_POINT('Ctrl Pts',(134.037348849678,-0.184782232139447,
125.887677117296));
#37523=CARTESIAN_POINT('Ctrl Pts',(134.029588407164,-0.321376686276765,
125.896621821744));
#37524=CARTESIAN_POINT('Ctrl Pts',(134.021815506898,-0.458190413958243,
125.905580885025));
#37525=CARTESIAN_POINT('Ctrl Pts',(134.014042606633,-0.594484249908106,
125.920255713675));
#37526=CARTESIAN_POINT('Ctrl Pts',(134.006269706368,-0.729751691865504,
125.940550842223));
#37527=CARTESIAN_POINT('Ctrl Pts',(133.998779370606,-0.860101821587794,
125.960108191728));
#37528=CARTESIAN_POINT('Ctrl Pts',(133.991289034844,-0.989498583226331,
125.984884253403));
#37529=CARTESIAN_POINT('Ctrl Pts',(133.983798699082,-1.11750194940005,126.014749729865));
#37530=CARTESIAN_POINT('Ctrl Pts',(133.976024364963,-1.25035860210971,126.045747564945));
#37531=CARTESIAN_POINT('Ctrl Pts',(133.968250030844,-1.38213496233291,126.082326555345));
#37532=CARTESIAN_POINT('Ctrl Pts',(133.960475696725,-1.51232596827186,126.124397665983));
#37533=CARTESIAN_POINT('Ctrl Pts',(133.952710943778,-1.64235652543133,126.166416927737));
#37534=CARTESIAN_POINT('Ctrl Pts',(133.94494619083,-1.77080524734935,126.213914723271));
#37535=CARTESIAN_POINT('Ctrl Pts',(133.937181437883,-1.89717765634108,126.266751114449));
#37536=CARTESIAN_POINT('Ctrl Pts',(133.929424396998,-2.02342455047483,126.319535027778));
#37537=CARTESIAN_POINT('Ctrl Pts',(133.921667356113,-2.14759887722674,126.377646834961));
#37538=CARTESIAN_POINT('Ctrl Pts',(133.913910315228,-2.26922205926168,126.440897049681));
#37539=CARTESIAN_POINT('Ctrl Pts',(133.906159123988,-2.39075352430895,126.504099566922));
#37540=CARTESIAN_POINT('Ctrl Pts',(133.898407932748,-2.50973732846206,126.572432599263));
#37541=CARTESIAN_POINT('Ctrl Pts',(133.890656741508,-2.62571593525527,126.64565903055));
#37542=CARTESIAN_POINT('Ctrl Pts',(133.882908844731,-2.74164524804667,126.718854338651));
#37543=CARTESIAN_POINT('Ctrl Pts',(133.875160947954,-2.8545715740142,126.796938700795));
#37544=CARTESIAN_POINT('Ctrl Pts',(133.867413051177,-2.96406320713384,126.879629752065));
#37545=CARTESIAN_POINT('Ctrl Pts',(133.859666775093,-3.07353193696434,126.96230350615));
#37546=CARTESIAN_POINT('Ctrl Pts',(133.851920499008,-3.17956709122067,127.049581797194));
#37547=CARTESIAN_POINT('Ctrl Pts',(133.844174222924,-3.28176745405261,127.141139979927));
#37548=CARTESIAN_POINT('Ctrl Pts',(133.836427889659,-3.38396857130433,127.232698838523));
#37549=CARTESIAN_POINT('Ctrl Pts',(133.828681556394,-3.48233454944653,127.328537390972));
#37550=CARTESIAN_POINT('Ctrl Pts',(133.820935223128,-3.57649897194036,127.428292169473));
#37551=CARTESIAN_POINT('Ctrl Pts',(133.813187155125,-3.67068448190404,127.528069287365));
#37552=CARTESIAN_POINT('Ctrl Pts',(133.805439087122,-3.76066629559726,127.631764092208));
#37553=CARTESIAN_POINT('Ctrl Pts',(133.797691019119,-3.84611670331799,127.738978199831));
#37554=CARTESIAN_POINT('Ctrl Pts',(133.789934716377,-3.93165792874857,127.846306255883));
#37555=CARTESIAN_POINT('Ctrl Pts',(133.782178413635,-4.0126578835994,127.957160780254));
#37556=CARTESIAN_POINT('Ctrl Pts',(133.774422110894,-4.08883050454563,128.071111970334));
#37557=CARTESIAN_POINT('Ctrl Pts',(133.766661668379,-4.16504378111342,128.185123979595));
#37558=CARTESIAN_POINT('Ctrl Pts',(133.758901225865,-4.23642438651551,128.302235614199));
#37559=CARTESIAN_POINT('Ctrl Pts',(133.751140783351,-4.30273159230308,128.421991228261));
#37560=CARTESIAN_POINT('Ctrl Pts',(133.743367883086,-4.36914524030373,128.541939084666));
#37561=CARTESIAN_POINT('Ctrl Pts',(133.73559498282,-4.43046903884042,128.664539052231));
#37562=CARTESIAN_POINT('Ctrl Pts',(133.727822082555,-4.48650952887424,128.789313394839));
#37563=CARTESIAN_POINT('Ctrl Pts',(133.720331746793,-4.54051280593823,128.909551875806));
#37564=CARTESIAN_POINT('Ctrl Pts',(133.71284141103,-4.58961011391488,129.031809102606));
#37565=CARTESIAN_POINT('Ctrl Pts',(133.705351075268,-4.63367238880688,129.155644979347));
#37566=CARTESIAN_POINT('Ctrl Pts',(133.696877076708,-4.68352110932786,129.295743510919));
#37567=CARTESIAN_POINT('Ctrl Pts',(133.688403078147,-4.72704813717389,129.438202762215));
#37568=CARTESIAN_POINT('Ctrl Pts',(133.679929079587,-4.76405452823404,129.582490119308));
#37569=CARTESIAN_POINT('Origin',(213.235140564004,0.,130.804360617566));
#37570=CARTESIAN_POINT('',(131.584997718909,-4.76405452823404,129.582490119308));
#37571=CARTESIAN_POINT('',(131.929976442121,-4.76405452823405,129.582490119308));
#37572=CARTESIAN_POINT('',(213.235140564004,-4.76405452823405,129.582490119308));
#37573=CARTESIAN_POINT('',(133.264859435937,-4.91824867220211,130.807974601818));
#37574=CARTESIAN_POINT('Ctrl Pts',(133.264859435937,-4.91824867220211,130.807974601818));
#37575=CARTESIAN_POINT('Ctrl Pts',(133.255945198427,-4.91813260923259,130.965923974559));
#37576=CARTESIAN_POINT('Ctrl Pts',(133.247030960918,-4.91040380121572,131.123565068945));
#37577=CARTESIAN_POINT('Ctrl Pts',(133.238116723408,-4.89517488915305,131.280223903716));
#37578=CARTESIAN_POINT('Ctrl Pts',(133.22915699462,-4.87986826066354,131.43768220235));
#37579=CARTESIAN_POINT('Ctrl Pts',(133.220197265831,-4.85698489393969,131.594148056893));
#37580=CARTESIAN_POINT('Ctrl Pts',(133.211237537043,-4.82668855896882,131.748956095651));
#37581=CARTESIAN_POINT('Ctrl Pts',(133.202220640543,-4.79619891768544,131.904751889898));
#37582=CARTESIAN_POINT('Ctrl Pts',(133.193203744043,-4.75820149578884,132.058868513842));
#37583=CARTESIAN_POINT('Ctrl Pts',(133.184186847543,-4.71291164423838,132.21064895788));
#37584=CARTESIAN_POINT('Ctrl Pts',(133.178806172963,-4.6858857209641,132.301221271426));
#37585=CARTESIAN_POINT('Ctrl Pts',(133.173425498383,-4.65626395683687,132.390962109657));
#37586=CARTESIAN_POINT('Ctrl Pts',(133.168044823802,-4.62410006052217,132.479735707741));
#37587=CARTESIAN_POINT('Ctrl Pts',(133.160270489683,-4.57762765770432,132.608001337296));
#37588=CARTESIAN_POINT('Ctrl Pts',(133.152496155564,-4.52574075591298,132.734535052467));
#37589=CARTESIAN_POINT('Ctrl Pts',(133.144721821445,-4.46858741925803,132.858845842373));
#37590=CARTESIAN_POINT('Ctrl Pts',(133.136957068498,-4.4115045189826,132.98300343034));
#37591=CARTESIAN_POINT('Ctrl Pts',(133.129192315551,-4.3491682595744,133.104943192132));
#37592=CARTESIAN_POINT('Ctrl Pts',(133.121427562604,-4.28177600183403,133.224190638997));
#37593=CARTESIAN_POINT('Ctrl Pts',(133.113670521719,-4.21445067903416,133.343319647616));
#37594=CARTESIAN_POINT('Ctrl Pts',(133.105913480834,-4.1420795424037,133.45976132461));
#37595=CARTESIAN_POINT('Ctrl Pts',(133.098156439949,-4.06490727614898,133.573062822356));
#37596=CARTESIAN_POINT('Ctrl Pts',(133.090405248709,-3.9877932061006,133.686278878562));
#37597=CARTESIAN_POINT('Ctrl Pts',(133.082654057469,-3.9058854321526,133.796359147123));
#37598=CARTESIAN_POINT('Ctrl Pts',(133.074902866228,-3.81947344985998,133.902877299515));
#37599=CARTESIAN_POINT('Ctrl Pts',(133.067154969451,-3.73309819496483,134.00935017885));
#37600=CARTESIAN_POINT('Ctrl Pts',(133.059407072674,-3.64222278513193,134.112263650251));
#37601=CARTESIAN_POINT('Ctrl Pts',(133.051659175897,-3.54717859716893,134.211222379112));
#37602=CARTESIAN_POINT('Ctrl Pts',(133.043912899813,-3.45215429040106,134.310160407941));
#37603=CARTESIAN_POINT('Ctrl Pts',(133.036166623729,-3.35296321064494,134.405145057872));
#37604=CARTESIAN_POINT('Ctrl Pts',(133.028420347645,-3.24997511796952,134.495816264744));
#37605=CARTESIAN_POINT('Ctrl Pts',(133.020674014379,-3.14698626505947,134.586488140929));
#37606=CARTESIAN_POINT('Ctrl Pts',(133.012927681114,-3.04020063674487,134.672846252169));
#37607=CARTESIAN_POINT('Ctrl Pts',(133.005181347849,-2.93002243379298,134.754569675321));
#37608=CARTESIAN_POINT('Ctrl Pts',(132.997433279846,-2.81981955719653,134.836311399867));
#37609=CARTESIAN_POINT('Ctrl Pts',(132.989685211843,-2.70622290811392,134.913416138139));
#37610=CARTESIAN_POINT('Ctrl Pts',(132.98193714384,-2.58966678767391,134.985605526839));
#37611=CARTESIAN_POINT('Ctrl Pts',(132.974180841098,-2.4729867900019,135.05787163928));
#37612=CARTESIAN_POINT('Ctrl Pts',(132.966424538356,-2.35334137068296,135.125211760273));
#37613=CARTESIAN_POINT('Ctrl Pts',(132.958668235614,-2.2311911105751,135.187392592192));
#37614=CARTESIAN_POINT('Ctrl Pts',(132.9509077931,-2.10897565519547,135.249606611892));
#37615=CARTESIAN_POINT('Ctrl Pts',(132.943147350586,-1.98425305048594,135.306655693055));
#37616=CARTESIAN_POINT('Ctrl Pts',(132.935386908072,-1.85750418524707,135.358354607932));
#37617=CARTESIAN_POINT('Ctrl Pts',(132.927614007806,-1.73055185147756,135.410136514496));
#37618=CARTESIAN_POINT('Ctrl Pts',(132.919841107541,-1.60156712526531,135.456550959638));
#37619=CARTESIAN_POINT('Ctrl Pts',(132.912068207275,-1.47104724809604,135.497462263212));
#37620=CARTESIAN_POINT('Ctrl Pts',(132.904577871513,-1.34527209722028,135.536886337853));
#37621=CARTESIAN_POINT('Ctrl Pts',(132.897087535751,-1.21807176821434,135.571200350389));
#37622=CARTESIAN_POINT('Ctrl Pts',(132.889597199989,-1.0898985201787,135.600328119355));
#37623=CARTESIAN_POINT('Ctrl Pts',(132.88182286587,-0.956865544487872,135.630560276534));
#37624=CARTESIAN_POINT('Ctrl Pts',(132.874048531751,-0.822363008467457,
135.655300920351));
#37625=CARTESIAN_POINT('Ctrl Pts',(132.866274197632,-0.686884045745631,
135.67440921796));
#37626=CARTESIAN_POINT('Ctrl Pts',(132.858509444685,-0.551572048737166,
135.6934939663));
#37627=CARTESIAN_POINT('Ctrl Pts',(132.850744691738,-0.415286402769419,
135.706960125599));
#37628=CARTESIAN_POINT('Ctrl Pts',(132.84297993879,-0.278532987002799,135.714717268325));
#37629=CARTESIAN_POINT('Ctrl Pts',(132.835222897905,-0.141915396656605,
135.722466706547));
#37630=CARTESIAN_POINT('Ctrl Pts',(132.82746585702,-0.00483134888954567,
135.724518390304));
#37631=CARTESIAN_POINT('Ctrl Pts',(132.819708816135,0.132205904977683,135.720833404147));
#37632=CARTESIAN_POINT('Ctrl Pts',(132.811957624895,0.269139817985589,135.717151196866));
#37633=CARTESIAN_POINT('Ctrl Pts',(132.804206433655,0.406026618089016,135.707740940912));
#37634=CARTESIAN_POINT('Ctrl Pts',(132.796455242415,0.542351143606349,135.692615756113));
#37635=CARTESIAN_POINT('Ctrl Pts',(132.788707345638,0.678617727563854,135.677496999921));
#37636=CARTESIAN_POINT('Ctrl Pts',(132.780959448861,0.81432212448434,135.656668188996));
#37637=CARTESIAN_POINT('Ctrl Pts',(132.773211552084,0.948952610909251,135.630194432022));
#37638=CARTESIAN_POINT('Ctrl Pts',(132.765465276,1.08355493553879,135.603726212787));
#37639=CARTESIAN_POINT('Ctrl Pts',(132.757718999916,1.21708341311615,135.571615471568));
#37640=CARTESIAN_POINT('Ctrl Pts',(132.749972723831,1.34903524711421,135.533978674507));
#37641=CARTESIAN_POINT('Ctrl Pts',(132.742226390566,1.48098805515064,135.49634159962));
#37642=CARTESIAN_POINT('Ctrl Pts',(132.734480057301,1.61136382041381,135.453178494732));
#37643=CARTESIAN_POINT('Ctrl Pts',(132.726733724035,1.73967406078651,135.404655958599));
#37644=CARTESIAN_POINT('Ctrl Pts',(132.718985656032,1.86801303534789,135.35612255618));
#37645=CARTESIAN_POINT('Ctrl Pts',(132.711237588029,1.99428519895787,135.302227472506));
#37646=CARTESIAN_POINT('Ctrl Pts',(132.703489520026,2.11802160631991,135.243185635255));
#37647=CARTESIAN_POINT('Ctrl Pts',(132.695733217285,2.24188952220817,135.184081047637));
#37648=CARTESIAN_POINT('Ctrl Pts',(132.687976914543,2.36321594481492,135.1198189481));
#37649=CARTESIAN_POINT('Ctrl Pts',(132.680220611801,2.48155563903464,135.050660733299));
#37650=CARTESIAN_POINT('Ctrl Pts',(132.672460169287,2.59995849471239,134.981465606677));
#37651=CARTESIAN_POINT('Ctrl Pts',(132.664699726773,2.71537111677318,134.907369368877));
#37652=CARTESIAN_POINT('Ctrl Pts',(132.656939284258,2.82737773572283,134.828676485144));
#37653=CARTESIAN_POINT('Ctrl Pts',(132.649166383993,2.9395641576407,134.749857276608));
#37654=CARTESIAN_POINT('Ctrl Pts',(132.641393483728,3.04833334000829,134.666426914743));
#37655=CARTESIAN_POINT('Ctrl Pts',(132.633620583462,3.1533023601091,134.578730404462));
#37656=CARTESIAN_POINT('Ctrl Pts',(132.6261302477,3.25445549192795,134.494221883223));
#37657=CARTESIAN_POINT('Ctrl Pts',(132.618639911938,3.35207972736444,134.405752205873));
#37658=CARTESIAN_POINT('Ctrl Pts',(132.611149576176,3.44586651570447,134.313660692858));
#37659=CARTESIAN_POINT('Ctrl Pts',(132.603375242057,3.54320925863056,134.218077502137));
#37660=CARTESIAN_POINT('Ctrl Pts',(132.595600907938,3.63672616909146,134.11828963158));
#37661=CARTESIAN_POINT('Ctrl Pts',(132.587826573819,3.72603220965407,134.014635844882));
#37662=CARTESIAN_POINT('Ctrl Pts',(132.580061820872,3.81522818850313,133.911109802213));
#37663=CARTESIAN_POINT('Ctrl Pts',(132.572297067925,3.90022337030979,133.80372761648));
#37664=CARTESIAN_POINT('Ctrl Pts',(132.564532314978,3.98066823578871,133.69286601986));
#37665=CARTESIAN_POINT('Ctrl Pts',(132.556775274093,4.0610332022931,133.582114532541));
#37666=CARTESIAN_POINT('Ctrl Pts',(132.549018233208,4.13685661822656,133.467890825918));
#37667=CARTESIAN_POINT('Ctrl Pts',(132.541261192323,4.20782831804404,133.350605678114));
#37668=CARTESIAN_POINT('Ctrl Pts',(132.533510001083,4.27874649755062,133.233408975953));
#37669=CARTESIAN_POINT('Ctrl Pts',(132.525758809843,4.34482004180623,133.113155760989));
#37670=CARTESIAN_POINT('Ctrl Pts',(132.518007618602,4.40578153142101,132.990286544923));
#37671=CARTESIAN_POINT('Ctrl Pts',(132.510259721825,4.46671711077654,132.867469551551));
#37672=CARTESIAN_POINT('Ctrl Pts',(132.502511825048,4.52254478354295,132.742039117997));
#37673=CARTESIAN_POINT('Ctrl Pts',(132.494763928271,4.57304272847009,132.614460964532));
#37674=CARTESIAN_POINT('Ctrl Pts',(132.487017652187,4.62353011031576,132.486909497667));
#37675=CARTESIAN_POINT('Ctrl Pts',(132.479271376103,4.66868983804943,132.357211567781));
#37676=CARTESIAN_POINT('Ctrl Pts',(132.471525100019,4.70834812413129,132.225853144627));
#37677=CARTESIAN_POINT('Ctrl Pts',(132.463778766754,4.7480067029616,132.094493751815));
#37678=CARTESIAN_POINT('Ctrl Pts',(132.456032433488,4.78216364610665,131.961474215556));
#37679=CARTESIAN_POINT('Ctrl Pts',(132.448286100223,4.81069508130131,131.827295560387));
#37680=CARTESIAN_POINT('Ctrl Pts',(132.44053803222,4.83923290591303,131.693086856838));
#37681=CARTESIAN_POINT('Ctrl Pts',(132.432789964217,4.8621426344308,131.557718900193));
#37682=CARTESIAN_POINT('Ctrl Pts',(132.425041896214,4.87935161520858,131.421702401071));
#37683=CARTESIAN_POINT('Ctrl Pts',(132.417285593472,4.89657888589594,131.285541341995));
#37684=CARTESIAN_POINT('Ctrl Pts',(132.40952929073,4.9080932565402,131.148730752025));
#37685=CARTESIAN_POINT('Ctrl Pts',(132.401772987989,4.91387398709938,131.01178651134));
#37686=CARTESIAN_POINT('Ctrl Pts',(132.394012545474,4.91965780300853,130.874769179391));
#37687=CARTESIAN_POINT('Ctrl Pts',(132.38625210296,4.91970188096682,130.737618445364));
#37688=CARTESIAN_POINT('Ctrl Pts',(132.378491660446,4.91403764264012,130.600848678811));
#37689=CARTESIAN_POINT('Ctrl Pts',(132.370718760181,4.90836431157521,130.463859357287));
#37690=CARTESIAN_POINT('Ctrl Pts',(132.362945859915,4.89696438517229,130.32725261517));
#37691=CARTESIAN_POINT('Ctrl Pts',(132.35517295965,4.87992114675371,130.191537099768));
#37692=CARTESIAN_POINT('Ctrl Pts',(132.347682623888,4.86349747298099,130.060755185199));
#37693=CARTESIAN_POINT('Ctrl Pts',(132.340192288126,4.84183371169264,129.930801129464));
#37694=CARTESIAN_POINT('Ctrl Pts',(132.332701952364,4.81504856359359,129.802117936009));
#37695=CARTESIAN_POINT('Ctrl Pts',(132.324927618245,4.78724784846318,129.668555680161));
#37696=CARTESIAN_POINT('Ctrl Pts',(132.317153284125,4.75384166120601,129.535939473364));
#37697=CARTESIAN_POINT('Ctrl Pts',(132.309378950006,4.71490689117494,129.404776368565));
#37698=CARTESIAN_POINT('Ctrl Pts',(132.301614197059,4.67602010476827,129.273774910571));
#37699=CARTESIAN_POINT('Ctrl Pts',(132.293849444112,4.63161840257915,129.144223362585));
#37700=CARTESIAN_POINT('Ctrl Pts',(132.286084691165,4.58182981634555,129.016619418022));
#37701=CARTESIAN_POINT('Ctrl Pts',(132.27832765028,4.53209068083769,128.889142211496));
#37702=CARTESIAN_POINT('Ctrl Pts',(132.270570609395,4.47697544987471,128.763609120742));
#37703=CARTESIAN_POINT('Ctrl Pts',(132.26281356851,4.41666207067068,128.640503132425));
#37704=CARTESIAN_POINT('Ctrl Pts',(132.25506237727,4.35639417425512,128.517489979292));
#37705=CARTESIAN_POINT('Ctrl Pts',(132.24731118603,4.29093610336416,128.396900635174));
#37706=CARTESIAN_POINT('Ctrl Pts',(132.23955999479,4.22051392625481,128.279198194911));
#37707=CARTESIAN_POINT('Ctrl Pts',(132.231812098013,4.15012168044925,128.161545781325));
#37708=CARTESIAN_POINT('Ctrl Pts',(132.224064201235,4.07476972512276,128.04677816596));
#37709=CARTESIAN_POINT('Ctrl Pts',(132.216316304458,3.99472998412593,127.935333706499));
#37710=CARTESIAN_POINT('Ctrl Pts',(132.208570028374,3.91470698571745,127.823912558817));
#37711=CARTESIAN_POINT('Ctrl Pts',(132.20082375229,3.82999837999571,127.715813501733));
#37712=CARTESIAN_POINT('Ctrl Pts',(132.193077476206,3.74091909066729,127.611445426149));
#37713=CARTESIAN_POINT('Ctrl Pts',(132.185331142941,3.65183914377579,127.507076580143));
#37714=CARTESIAN_POINT('Ctrl Pts',(132.177584809675,3.55838870271194,127.40643906797));
#37715=CARTESIAN_POINT('Ctrl Pts',(132.16983847641,3.46092233762285,127.309907922874));
#37716=CARTESIAN_POINT('Ctrl Pts',(132.162090408407,3.36343414561709,127.213355160297));
#37717=CARTESIAN_POINT('Ctrl Pts',(132.154342340404,3.26192851773738,127.120910869745));
#37718=CARTESIAN_POINT('Ctrl Pts',(132.146594272401,3.15679585930167,127.032912226669));
#37719=CARTESIAN_POINT('Ctrl Pts',(132.138837969659,3.05155146462541,126.944820057589));
#37720=CARTESIAN_POINT('Ctrl Pts',(132.131081666917,2.94267263919339,126.861183225799));
#37721=CARTESIAN_POINT('Ctrl Pts',(132.123325364175,2.83058219711254,126.782298026321));
#37722=CARTESIAN_POINT('Ctrl Pts',(132.115564921661,2.71843192898778,126.703370723438));
#37723=CARTESIAN_POINT('Ctrl Pts',(132.107804479147,2.60306695735331,126.629200317569));
#37724=CARTESIAN_POINT('Ctrl Pts',(132.100044036633,2.48493702005917,126.560038402083));
#37725=CARTESIAN_POINT('Ctrl Pts',(132.092271136367,2.3666174501026,126.490765461751));
#37726=CARTESIAN_POINT('Ctrl Pts',(132.084498236102,2.24552439037618,126.426517261777));
#37727=CARTESIAN_POINT('Ctrl Pts',(132.076725335836,2.12213079693651,126.367498669838));
#37728=CARTESIAN_POINT('Ctrl Pts',(132.069235000074,2.00322287142732,126.310625552375));
#37729=CARTESIAN_POINT('Ctrl Pts',(132.061744664312,1.88217905170354,126.258608546867));
#37730=CARTESIAN_POINT('Ctrl Pts',(132.05425432855,1.75943620974022,126.211587241233));
#37731=CARTESIAN_POINT('Ctrl Pts',(132.046479994431,1.6320395356177,126.162783108504));
#37732=CARTESIAN_POINT('Ctrl Pts',(132.038705660312,1.50240890474879,126.119206380851));
#37733=CARTESIAN_POINT('Ctrl Pts',(132.030931326193,1.37101247571331,126.081066443588));
#37734=CARTESIAN_POINT('Ctrl Pts',(132.023166573246,1.23977798103348,126.042973510388));
#37735=CARTESIAN_POINT('Ctrl Pts',(132.015401820299,1.10678239001659,126.010304143802));
#37736=CARTESIAN_POINT('Ctrl Pts',(132.007637067352,0.972513630511448,125.983219642551));
#37737=CARTESIAN_POINT('Ctrl Pts',(131.999880026467,0.838378228631015,125.956162042008));
#37738=CARTESIAN_POINT('Ctrl Pts',(131.992122985582,0.702972555497661,125.934678344893));
#37739=CARTESIAN_POINT('Ctrl Pts',(131.984365944697,0.566799146288047,125.918879905265));
#37740=CARTESIAN_POINT('Ctrl Pts',(131.976614753456,0.430728426505499,125.903093379363));
#37741=CARTESIAN_POINT('Ctrl Pts',(131.968863562216,0.29389150981188,125.892983622218));
#37742=CARTESIAN_POINT('Ctrl Pts',(131.961112370976,0.156800206426934,125.888610750276));
#37743=CARTESIAN_POINT('Ctrl Pts',(131.953364474199,0.0197671705030495,
125.884239736921));
#37744=CARTESIAN_POINT('Ctrl Pts',(131.945616577422,-0.11751964711912,125.885600771556));
#37745=CARTESIAN_POINT('Ctrl Pts',(131.937868680645,-0.254544462222737,
125.892702019979));
#37746=CARTESIAN_POINT('Ctrl Pts',(131.930122404561,-0.391540614688948,
125.899801782974));
#37747=CARTESIAN_POINT('Ctrl Pts',(131.922376128477,-0.528274483453441,
125.91263935122));
#37748=CARTESIAN_POINT('Ctrl Pts',(131.914629852393,-0.664231833064708,
125.931170786004));
#37749=CARTESIAN_POINT('Ctrl Pts',(131.906883519127,-0.800190186282245,
125.949702357582));
#37750=CARTESIAN_POINT('Ctrl Pts',(131.899137185862,-0.935371621525342,
125.973927826765));
#37751=CARTESIAN_POINT('Ctrl Pts',(131.891390852596,-1.06926895887812,126.003751598277));
#37752=CARTESIAN_POINT('Ctrl Pts',(131.883642784594,-1.20319628161123,126.033582048615));
#37753=CARTESIAN_POINT('Ctrl Pts',(131.875894716591,-1.33583855269275,126.069013211019));
#37754=CARTESIAN_POINT('Ctrl Pts',(131.868146648588,-1.46670107325562,126.109898878004));
#37755=CARTESIAN_POINT('Ctrl Pts',(131.860390345846,-1.59770267606254,126.150827998763));
#37756=CARTESIAN_POINT('Ctrl Pts',(131.852634043104,-1.72692037602514,126.197223087681));
#37757=CARTESIAN_POINT('Ctrl Pts',(131.844877740362,-1.85387635039624,126.248888573975));
#37758=CARTESIAN_POINT('Ctrl Pts',(131.837117297848,-1.98090008499362,126.300581635694));
#37759=CARTESIAN_POINT('Ctrl Pts',(131.829356855334,-2.10565933318112,126.357550537551));
#37760=CARTESIAN_POINT('Ctrl Pts',(131.821596412819,-2.22769932803784,126.419552894717));
#37761=CARTESIAN_POINT('Ctrl Pts',(131.813823512554,-2.34993523232842,126.481654783571));
#37762=CARTESIAN_POINT('Ctrl Pts',(131.806050612289,-2.4694428192147,126.548806082817));
#37763=CARTESIAN_POINT('Ctrl Pts',(131.798277712023,-2.58579408341668,126.620719617113));
#37764=CARTESIAN_POINT('Ctrl Pts',(131.790787376261,-2.69791568609289,126.690018913299));
#37765=CARTESIAN_POINT('Ctrl Pts',(131.783297040499,-2.80710620724367,126.763740044908));
#37766=CARTESIAN_POINT('Ctrl Pts',(131.775806704737,-2.91301206762658,126.841590909854));
#37767=CARTESIAN_POINT('Ctrl Pts',(131.767856330328,-3.02542241463406,126.924223190181));
#37768=CARTESIAN_POINT('Ctrl Pts',(131.759905955918,-3.13451423036537,127.011789730077));
#37769=CARTESIAN_POINT('Ctrl Pts',(131.751955581509,-3.23982082542546,127.103989814303));
#37770=CARTESIAN_POINT('Ctrl Pts',(131.744263365086,-3.34170799176701,127.193196053598));
#37771=CARTESIAN_POINT('Ctrl Pts',(131.736571148663,-3.44005156374033,127.286739352508));
#37772=CARTESIAN_POINT('Ctrl Pts',(131.728878932241,-3.53445722420859,127.384302841338));
#37773=CARTESIAN_POINT('Ctrl Pts',(131.721193684871,-3.62877735431287,127.48177793885));
#37774=CARTESIAN_POINT('Ctrl Pts',(131.713508437502,-3.71916639214806,127.583265698873));
#37775=CARTESIAN_POINT('Ctrl Pts',(131.705823190132,-3.80526392249755,127.688409792755));
#37776=CARTESIAN_POINT('Ctrl Pts',(131.698143165122,-3.89130294695759,127.793482438029));
#37777=CARTESIAN_POINT('Ctrl Pts',(131.690463140112,-3.97305601293349,127.902206167732));
#37778=CARTESIAN_POINT('Ctrl Pts',(131.682783115101,-4.05020070095915,128.014189055735));
#37779=CARTESIAN_POINT('Ctrl Pts',(131.67510657014,-4.12731043241603,128.126121200937));
#37780=CARTESIAN_POINT('Ctrl Pts',(131.66743002518,-4.19981571551304,128.24130923787));
#37781=CARTESIAN_POINT('Ctrl Pts',(131.659753480219,-4.2674357676132,128.35932993641));
#37782=CARTESIAN_POINT('Ctrl Pts',(131.652077418928,-4.33505155922955,128.477343198911));
#37783=CARTESIAN_POINT('Ctrl Pts',(131.644401357637,-4.39778252739333,128.598188425893));
#37784=CARTESIAN_POINT('Ctrl Pts',(131.636725296346,-4.45539255642993,128.72141553173));
#37785=CARTESIAN_POINT('Ctrl Pts',(131.629049422028,-4.51300118220605,128.844639636011));
#37786=CARTESIAN_POINT('Ctrl Pts',(131.62137354771,-4.56548895383169,128.970245139823));
#37787=CARTESIAN_POINT('Ctrl Pts',(131.613697673393,-4.61266718327577,129.097760336648));
#37788=CARTESIAN_POINT('Ctrl Pts',(131.606018456807,-4.65986595530053,129.225331056777));
#37789=CARTESIAN_POINT('Ctrl Pts',(131.598339240222,-4.70175043836995,129.354812753454));
#37790=CARTESIAN_POINT('Ctrl Pts',(131.590660023636,-4.73818130706446,129.485717009958));
#37791=CARTESIAN_POINT('Ctrl Pts',(131.588772588727,-4.7471354617718,129.517891289809));
#37792=CARTESIAN_POINT('Ctrl Pts',(131.586885153818,-4.75576040176345,129.55015144608));
#37793=CARTESIAN_POINT('Ctrl Pts',(131.584997718909,-4.76405452823404,129.582490119308));
#37794=CARTESIAN_POINT('Ctrl Pts',(133.334729823376,-4.76405452823402,129.582490119308));
#37795=CARTESIAN_POINT('Ctrl Pts',(133.32696908606,-4.79821351346672,129.715675484296));
#37796=CARTESIAN_POINT('Ctrl Pts',(133.319208348743,-4.8267966455201,129.85034665783));
#37797=CARTESIAN_POINT('Ctrl Pts',(133.311447611427,-4.84968727538676,129.985998598988));
#37798=CARTESIAN_POINT('Ctrl Pts',(133.303682915521,-4.87258958128452,130.121719733361));
#37799=CARTESIAN_POINT('Ctrl Pts',(133.295918219615,-4.88979349900938,130.258422254787));
#37800=CARTESIAN_POINT('Ctrl Pts',(133.288153523709,-4.90123355226953,130.395590842989));
#37801=CARTESIAN_POINT('Ctrl Pts',(133.280388827803,-4.91267360552968,130.532759431192));
#37802=CARTESIAN_POINT('Ctrl Pts',(133.272624131897,-4.91834976816577,130.670393697661));
#37803=CARTESIAN_POINT('Ctrl Pts',(133.264859435991,-4.91824867220281,130.807974600859));
#37804=CARTESIAN_POINT('',(133.610140564061,-4.91824860178181,130.800652036803));
#37805=CARTESIAN_POINT('Ctrl Pts',(133.679929079587,-4.76405452823404,129.582490119308));
#37806=CARTESIAN_POINT('Ctrl Pts',(133.670903636898,-4.80346910439079,129.736166953544));
#37807=CARTESIAN_POINT('Ctrl Pts',(133.66187819421,-4.83548620139363,129.891917696107));
#37808=CARTESIAN_POINT('Ctrl Pts',(133.652852751521,-4.85991057754177,130.049077729638));
#37809=CARTESIAN_POINT('Ctrl Pts',(133.643900109645,-4.88413794236419,130.20497008262));
#37810=CARTESIAN_POINT('Ctrl Pts',(133.634947467769,-4.90089450501078,130.362248961787));
#37811=CARTESIAN_POINT('Ctrl Pts',(133.625994825893,-4.91003684997578,130.520245861913));
#37812=CARTESIAN_POINT('Ctrl Pts',(133.620710071949,-4.91543358585336,130.613511598736));
#37813=CARTESIAN_POINT('Ctrl Pts',(133.615425318005,-4.91817800441632,130.707027166196));
#37814=CARTESIAN_POINT('Ctrl Pts',(133.610140564061,-4.91824860178181,130.800652036803));
#37815=CARTESIAN_POINT('Ctrl Pts',(133.610140564008,-4.91824860178252,130.800652037749));
#37816=CARTESIAN_POINT('Ctrl Pts',(133.602387431034,-4.91835217342056,130.938006790535));
#37817=CARTESIAN_POINT('Ctrl Pts',(133.59463429806,-4.91269746273253,131.075420857256));
#37818=CARTESIAN_POINT('Ctrl Pts',(133.586881165086,-4.90129633382327,131.212376929189));
#37819=CARTESIAN_POINT('Ctrl Pts',(133.579128914385,-4.88989650231452,131.349317416097));
#37820=CARTESIAN_POINT('Ctrl Pts',(133.571376663685,-4.87275158523712,131.485799623771));
#37821=CARTESIAN_POINT('Ctrl Pts',(133.563624412985,-4.84992545578321,131.621309903535));
#37822=CARTESIAN_POINT('Ctrl Pts',(133.55587138114,-4.82709702628796,131.756833837794));
#37823=CARTESIAN_POINT('Ctrl Pts',(133.548118349296,-4.79858630945917,131.891385265033));
#37824=CARTESIAN_POINT('Ctrl Pts',(133.540365317452,-4.76450851464186,132.024459661253));
#37825=CARTESIAN_POINT('Ctrl Pts',(133.532609840892,-4.73041997428373,132.157576019001));
#37826=CARTESIAN_POINT('Ctrl Pts',(133.524854364331,-4.69076095872476,132.289214041575));
#37827=CARTESIAN_POINT('Ctrl Pts',(133.517098887771,-4.64569675226893,132.418883689082));
#37828=CARTESIAN_POINT('Ctrl Pts',(133.509334287436,-4.60057953092724,132.548705883857));
#37829=CARTESIAN_POINT('Ctrl Pts',(133.5015696871,-4.55004454557834,132.676554709826));
#37830=CARTESIAN_POINT('Ctrl Pts',(133.493805086764,-4.49430575041075,132.801958896581));
#37831=CARTESIAN_POINT('Ctrl Pts',(133.486035753666,-4.43853298073561,132.927439521039));
#37832=CARTESIAN_POINT('Ctrl Pts',(133.478266420568,-4.37755025445433,133.050472188914));
#37833=CARTESIAN_POINT('Ctrl Pts',(133.47049708747,-4.31161738938312,133.170610509287));
#37834=CARTESIAN_POINT('Ctrl Pts',(133.462714826863,-4.24557481763773,133.290948729596));
#37835=CARTESIAN_POINT('Ctrl Pts',(133.454932566257,-4.17456585152711,133.408382646762));
#37836=CARTESIAN_POINT('Ctrl Pts',(133.44715030565,-4.09889399462122,133.522494367652));
#37837=CARTESIAN_POINT('Ctrl Pts',(133.440401354252,-4.0332696586797,133.621454618038));
#37838=CARTESIAN_POINT('Ctrl Pts',(133.433652402854,-3.96413924999595,133.717916702468));
#37839=CARTESIAN_POINT('Ctrl Pts',(133.426903451456,-3.89172427037809,133.811629356114));
#37840=CARTESIAN_POINT('Ctrl Pts',(133.419129117337,-3.80830712694628,133.919579975059));
#37841=CARTESIAN_POINT('Ctrl Pts',(133.411354783218,-3.72026286937863,134.024228149251));
#37842=CARTESIAN_POINT('Ctrl Pts',(133.403580449099,-3.62788241396373,134.12515152531));
#37843=CARTESIAN_POINT('Ctrl Pts',(133.395815696151,-3.53561580920398,134.225950522327));
#37844=CARTESIAN_POINT('Ctrl Pts',(133.388050943204,-3.43902390096166,134.323033569277));
#37845=CARTESIAN_POINT('Ctrl Pts',(133.380286190257,-3.33843950325637,134.416009097914));
#37846=CARTESIAN_POINT('Ctrl Pts',(133.372529149372,-3.23795500739293,134.508892281945));
#37847=CARTESIAN_POINT('Ctrl Pts',(133.364772108487,-3.13348619862717,134.597675802676));
#37848=CARTESIAN_POINT('Ctrl Pts',(133.357015067602,-3.025404346646,134.682003149027));
#37849=CARTESIAN_POINT('Ctrl Pts',(133.349263876362,-2.91740400002994,134.766266903471));
#37850=CARTESIAN_POINT('Ctrl Pts',(133.341512685122,-2.8057963403945,134.846080932754));
#37851=CARTESIAN_POINT('Ctrl Pts',(133.333761493882,-2.6909872115847,134.921127660962));
#37852=CARTESIAN_POINT('Ctrl Pts',(133.326013597105,-2.57622687971727,134.996142492308));
#37853=CARTESIAN_POINT('Ctrl Pts',(133.318265700328,-2.45826811159151,135.06639383913));
#37854=CARTESIAN_POINT('Ctrl Pts',(133.310517803551,-2.33754716871975,135.131606427144));
#37855=CARTESIAN_POINT('Ctrl Pts',(133.302771527467,-2.21685147806679,135.19680537409));
#37856=CARTESIAN_POINT('Ctrl Pts',(133.295025251383,-2.09339510568538,135.256967472991));
#37857=CARTESIAN_POINT('Ctrl Pts',(133.287278975298,-1.96764009403749,135.311862755429));
#37858=CARTESIAN_POINT('Ctrl Pts',(133.279532642033,-1.84188415409466,135.36675844309));
#37859=CARTESIAN_POINT('Ctrl Pts',(133.271786308768,-1.7138298993406,135.416387080296));
#37860=CARTESIAN_POINT('Ctrl Pts',(133.264039975502,-1.58396021707708,135.460566486427));
#37861=CARTESIAN_POINT('Ctrl Pts',(133.256291907499,-1.45406145139839,135.50475578623));
#37862=CARTESIAN_POINT('Ctrl Pts',(133.248543839496,-1.32234681928177,135.543493300778));
#37863=CARTESIAN_POINT('Ctrl Pts',(133.240795771493,-1.1893148759176,135.576646567551));
#37864=CARTESIAN_POINT('Ctrl Pts',(133.233039468752,-1.0561415446212,135.60983507001));
#37865=CARTESIAN_POINT('Ctrl Pts',(133.22528316601,-0.92164848528549,135.637427374189));
#37866=CARTESIAN_POINT('Ctrl Pts',(133.217526863268,-0.786345517693598,
135.659341955254));
#37867=CARTESIAN_POINT('Ctrl Pts',(133.209766420754,-0.650970334833916,
135.681268232792));
#37868=CARTESIAN_POINT('Ctrl Pts',(133.20200597824,-0.514784770402567,135.697510702665));
#37869=CARTESIAN_POINT('Ctrl Pts',(133.194245535725,-0.378303304881688,
135.708039815068));
#37870=CARTESIAN_POINT('Ctrl Pts',(133.18647263546,-0.241602747196285,135.718585829738));
#37871=CARTESIAN_POINT('Ctrl Pts',(133.178699735195,-0.104605730155504,
135.723400145443));
#37872=CARTESIAN_POINT('Ctrl Pts',(133.170926834929,0.032172822635227,135.722505386885));
#37873=CARTESIAN_POINT('Ctrl Pts',(133.163436499167,0.163979130507997,135.721643155055));
#37874=CARTESIAN_POINT('Ctrl Pts',(133.155946163405,0.295582274140959,135.715479735461));
#37875=CARTESIAN_POINT('Ctrl Pts',(133.148455827643,0.426528331227084,135.704080675402));
#37876=CARTESIAN_POINT('Ctrl Pts',(133.140681493524,0.562439247867539,135.692249416517));
#37877=CARTESIAN_POINT('Ctrl Pts',(133.132907159405,0.698072792421624,135.674740183407));
#37878=CARTESIAN_POINT('Ctrl Pts',(133.125132825286,0.83291637966798,135.651569439866));
#37879=CARTESIAN_POINT('Ctrl Pts',(133.117368072339,0.967593784244372,135.628427252195));
#37880=CARTESIAN_POINT('Ctrl Pts',(133.109603319392,1.10148278697197,135.599637502428));
#37881=CARTESIAN_POINT('Ctrl Pts',(133.101838566444,1.23407405628833,135.565268544222));
#37882=CARTESIAN_POINT('Ctrl Pts',(133.094081525559,1.3665336340868,135.53093372175));
#37883=CARTESIAN_POINT('Ctrl Pts',(133.086324484674,1.49769766748849,135.491030815838));
#37884=CARTESIAN_POINT('Ctrl Pts',(133.078567443789,1.62706553329057,135.445679483242));
#37885=CARTESIAN_POINT('Ctrl Pts',(133.070816252549,1.7563358417788,135.400362350438));
#37886=CARTESIAN_POINT('Ctrl Pts',(133.063065061309,1.88381231126709,135.349605097887));
#37887=CARTESIAN_POINT('Ctrl Pts',(133.055313870069,2.00900838763274,135.293577515971));
#37888=CARTESIAN_POINT('Ctrl Pts',(133.047565973292,2.13415125232605,135.237573747271));
#37889=CARTESIAN_POINT('Ctrl Pts',(133.039818076515,2.25701529550406,135.176304263823));
#37890=CARTESIAN_POINT('Ctrl Pts',(133.032070179738,2.37713311111174,135.109987312317));
#37891=CARTESIAN_POINT('Ctrl Pts',(133.024323903654,2.49722580066175,135.043684232889));
#37892=CARTESIAN_POINT('Ctrl Pts',(133.01657762757,2.61457306320791,134.972335974335));
#37893=CARTESIAN_POINT('Ctrl Pts',(133.008831351485,2.72873167457004,134.896206962518));
#37894=CARTESIAN_POINT('Ctrl Pts',(133.00108501822,2.84289112862511,134.820077388734));
#37895=CARTESIAN_POINT('Ctrl Pts',(132.993338684955,2.95386155925588,134.739167208181));
#37896=CARTESIAN_POINT('Ctrl Pts',(132.985592351689,3.06122868036634,134.653784214548));
#37897=CARTESIAN_POINT('Ctrl Pts',(132.977844283686,3.16861984559913,134.568382099986));
#37898=CARTESIAN_POINT('Ctrl Pts',(132.970096215683,3.27240578965933,134.478505422464));
#37899=CARTESIAN_POINT('Ctrl Pts',(132.962348147681,3.37220558681838,134.384502031356));
#37900=CARTESIAN_POINT('Ctrl Pts',(132.954591844939,3.47211145238954,134.290398732325));
#37901=CARTESIAN_POINT('Ctrl Pts',(132.946835542197,3.5680224230967,134.192160226852));
#37902=CARTESIAN_POINT('Ctrl Pts',(132.939079239455,3.65959433974247,134.090171374598));
#37903=CARTESIAN_POINT('Ctrl Pts',(132.931318796941,3.75121513107732,133.988128087822));
#37904=CARTESIAN_POINT('Ctrl Pts',(132.923558354427,3.83849200508441,133.882330767201));
#37905=CARTESIAN_POINT('Ctrl Pts',(132.915797911912,3.92112201140862,133.773196287344));
#37906=CARTESIAN_POINT('Ctrl Pts',(132.908025011647,4.00388466275459,133.663886615132));
#37907=CARTESIAN_POINT('Ctrl Pts',(132.900252111382,4.08198531695467,133.551229399973));
#37908=CARTESIAN_POINT('Ctrl Pts',(132.892479211116,4.15516468002477,133.435670090884));
#37909=CARTESIAN_POINT('Ctrl Pts',(132.884988875354,4.22568378891998,133.324311653757));
#37910=CARTESIAN_POINT('Ctrl Pts',(132.877498539592,4.29163304317731,133.210258722982));
#37911=CARTESIAN_POINT('Ctrl Pts',(132.87000820383,4.35282223350238,133.093928626171));
#37912=CARTESIAN_POINT('Ctrl Pts',(132.862233869711,4.41633143057632,132.973187838382));
#37913=CARTESIAN_POINT('Ctrl Pts',(132.854459535592,4.47491366073867,132.849611327824));
#37914=CARTESIAN_POINT('Ctrl Pts',(132.846685201473,4.52830571061255,132.723639246044));
#37915=CARTESIAN_POINT('Ctrl Pts',(132.838920448526,4.58163195955671,132.597822413597));
#37916=CARTESIAN_POINT('Ctrl Pts',(132.831155695579,4.62978060410419,132.46961624069));
#37917=CARTESIAN_POINT('Ctrl Pts',(132.823390942631,4.67253384597332,132.339486189216));
#37918=CARTESIAN_POINT('Ctrl Pts',(132.815633901746,4.71524462471988,132.209485384743));
#37919=CARTESIAN_POINT('Ctrl Pts',(132.807876860861,4.75257054378033,132.077564873356));
#37920=CARTESIAN_POINT('Ctrl Pts',(132.800119819976,4.78434167470252,131.944210520933));
#37921=CARTESIAN_POINT('Ctrl Pts',(132.792368628736,4.81608884676777,131.810956732063));
#37922=CARTESIAN_POINT('Ctrl Pts',(132.784617437496,4.84228947822081,131.676271633143));
#37923=CARTESIAN_POINT('Ctrl Pts',(132.776866246256,4.86282342413051,131.540656351784));
#37924=CARTESIAN_POINT('Ctrl Pts',(132.769118349479,4.88334864256545,131.405098710537));
#37925=CARTESIAN_POINT('Ctrl Pts',(132.761370452702,4.89821190735741,131.268612058927));
#37926=CARTESIAN_POINT('Ctrl Pts',(132.753622555925,4.90734419123914,131.131707606572));
#37927=CARTESIAN_POINT('Ctrl Pts',(132.745876279841,4.91647456484395,130.994831791678));
#37928=CARTESIAN_POINT('Ctrl Pts',(132.738130003757,4.91987631600756,130.857538739724));
#37929=CARTESIAN_POINT('Ctrl Pts',(132.730383727673,4.91753234020049,130.720344276404));
#37930=CARTESIAN_POINT('Ctrl Pts',(132.722637394407,4.91518834709071,130.583148800344));
#37931=CARTESIAN_POINT('Ctrl Pts',(132.714891061142,4.90709854905556,130.446052305279));
#37932=CARTESIAN_POINT('Ctrl Pts',(132.707144727876,4.893297969888,130.309569711839));
#37933=CARTESIAN_POINT('Ctrl Pts',(132.699396659873,4.87949430017642,130.173056554069));
#37934=CARTESIAN_POINT('Ctrl Pts',(132.691648591871,4.85997734381448,130.0371579604));
#37935=CARTESIAN_POINT('Ctrl Pts',(132.683900523868,4.83483385667072,129.902382435518));
#37936=CARTESIAN_POINT('Ctrl Pts',(132.676144221126,4.80966364672962,129.767463669605));
#37937=CARTESIAN_POINT('Ctrl Pts',(132.668387918384,4.77885503223973,129.633670741792));
#37938=CARTESIAN_POINT('Ctrl Pts',(132.660631615642,4.7425457800787,129.501501229006));
#37939=CARTESIAN_POINT('Ctrl Pts',(132.652871173128,4.70621714857652,129.369261173372));
#37940=CARTESIAN_POINT('Ctrl Pts',(132.645110730614,4.66438214865916,129.238646631421));
#37941=CARTESIAN_POINT('Ctrl Pts',(132.637350288099,4.61722775667497,129.110137814777));
#37942=CARTESIAN_POINT('Ctrl Pts',(132.629577387834,4.56999766827467,128.981422704372));
#37943=CARTESIAN_POINT('Ctrl Pts',(132.621804487569,4.51743127385306,128.854820435469));
#37944=CARTESIAN_POINT('Ctrl Pts',(132.614031587303,4.45976318755155,128.730789935515));
#37945=CARTESIAN_POINT('Ctrl Pts',(132.606541251541,4.40419148144425,128.611268256649));
#37946=CARTESIAN_POINT('Ctrl Pts',(132.599050915779,4.34388270346346,128.494134886282));
#37947=CARTESIAN_POINT('Ctrl Pts',(132.591560580017,4.27908515037673,128.379775428647));
#37948=CARTESIAN_POINT('Ctrl Pts',(132.583786245898,4.21183077836993,128.261079997417));
#37949=CARTESIAN_POINT('Ctrl Pts',(132.576011911779,4.13952748652236,128.144996985566));
#37950=CARTESIAN_POINT('Ctrl Pts',(132.56823757766,4.06240331353629,128.031985754625));
#37951=CARTESIAN_POINT('Ctrl Pts',(132.560472824713,3.98537418920069,127.919113799925));
#37952=CARTESIAN_POINT('Ctrl Pts',(132.552708071766,3.90353622342103,127.809306413561));
#37953=CARTESIAN_POINT('Ctrl Pts',(132.544943318818,3.81716329717726,127.702998428917));
#37954=CARTESIAN_POINT('Ctrl Pts',(132.537186277934,3.7308761577417,127.596796030862));
#37955=CARTESIAN_POINT('Ctrl Pts',(132.529429237049,3.64006326631725,127.494086419289));
#37956=CARTESIAN_POINT('Ctrl Pts',(132.521672196164,3.54504154514848,127.395275182193));
#37957=CARTESIAN_POINT('Ctrl Pts',(132.513921004923,3.4500914805988,127.29653845942));
#37958=CARTESIAN_POINT('Ctrl Pts',(132.506169813683,3.3509391736837,127.201694540305));
#37959=CARTESIAN_POINT('Ctrl Pts',(132.498418622443,3.24794129598594,127.111115377898));
#37960=CARTESIAN_POINT('Ctrl Pts',(132.490670725666,3.14498719513334,127.020574714051));
#37961=CARTESIAN_POINT('Ctrl Pts',(132.482922828889,3.03819106730616,126.934295459365));
#37962=CARTESIAN_POINT('Ctrl Pts',(132.475174932112,2.92794569671138,126.85261200972));
#37963=CARTESIAN_POINT('Ctrl Pts',(132.467428656028,2.81772338707158,126.770945646493));
#37964=CARTESIAN_POINT('Ctrl Pts',(132.459682379944,2.70405358371796,126.693873408746));
#37965=CARTESIAN_POINT('Ctrl Pts',(132.45193610386,2.58736101999869,126.621688503392));
#37966=CARTESIAN_POINT('Ctrl Pts',(132.444189770594,2.47066759488149,126.549503065185));
#37967=CARTESIAN_POINT('Ctrl Pts',(132.436443437329,2.35095169736611,126.482205237036));
#37968=CARTESIAN_POINT('Ctrl Pts',(132.428697104064,2.22866547597977,126.420043879615));
#37969=CARTESIAN_POINT('Ctrl Pts',(132.420949036061,2.10635186944144,126.35786860159));
#37970=CARTESIAN_POINT('Ctrl Pts',(132.413200968058,1.98146714209708,126.30083226034));
#37971=CARTESIAN_POINT('Ctrl Pts',(132.405452900055,1.85448600700744,126.2491367249));
#37972=CARTESIAN_POINT('Ctrl Pts',(132.397696597313,1.72736991485685,126.197386246831));
#37973=CARTESIAN_POINT('Ctrl Pts',(132.389940294571,1.59815332680166,126.15098806119));
#37974=CARTESIAN_POINT('Ctrl Pts',(132.382183991829,1.4673293347643,126.110095213284));
#37975=CARTESIAN_POINT('Ctrl Pts',(132.374423549315,1.336435518023,126.069180539634));
#37976=CARTESIAN_POINT('Ctrl Pts',(132.366663106801,1.20393296535165,126.033777159531));
#37977=CARTESIAN_POINT('Ctrl Pts',(132.358902664286,1.07032675767217,126.00398733059));
#37978=CARTESIAN_POINT('Ctrl Pts',(132.351129764021,0.936506073447491,125.974149680372));
#37979=CARTESIAN_POINT('Ctrl Pts',(132.343356863756,0.801578578866621,125.949943657982));
#37980=CARTESIAN_POINT('Ctrl Pts',(132.33558396349,0.666057197262066,125.931419937394));
#37981=CARTESIAN_POINT('Ctrl Pts',(132.328093627728,0.535462359236508,125.913569600708));
#37982=CARTESIAN_POINT('Ctrl Pts',(132.320603291966,0.404316369734703,125.900995635831));
#37983=CARTESIAN_POINT('Ctrl Pts',(132.313112956204,0.273077858986737,125.893697572169));
#37984=CARTESIAN_POINT('Ctrl Pts',(132.305338622085,0.136863400214587,125.886122800204));
#37985=CARTESIAN_POINT('Ctrl Pts',(132.297564287966,0.000117779352706487,
125.88420790398));
#37986=CARTESIAN_POINT('Ctrl Pts',(132.289789953847,-0.136649269244567,
125.888009324207));
#37987=CARTESIAN_POINT('Ctrl Pts',(132.2820252009,-0.273247764677482,125.891806059523));
#37988=CARTESIAN_POINT('Ctrl Pts',(132.274260447953,-0.409867248239707,
125.90130508338));
#37989=CARTESIAN_POINT('Ctrl Pts',(132.266495695005,-0.545993842930439,
125.916511010021));
#37990=CARTESIAN_POINT('Ctrl Pts',(132.25873865412,-0.681985234767812,125.93170183392));
#37991=CARTESIAN_POINT('Ctrl Pts',(132.250981613236,-0.817484325914376,
125.952588237553));
#37992=CARTESIAN_POINT('Ctrl Pts',(132.243224572351,-0.951978579489092,
125.979122815479));
#37993=CARTESIAN_POINT('Ctrl Pts',(132.23547338111,-1.08637140990116,126.005637383472));
#37994=CARTESIAN_POINT('Ctrl Pts',(132.22772218987,-1.21976052898902,126.037791572446));
#37995=CARTESIAN_POINT('Ctrl Pts',(132.21997099863,-1.3516402124162,126.075486354205));
#37996=CARTESIAN_POINT('Ctrl Pts',(132.212223101853,-1.48346384346045,126.113165114676));
#37997=CARTESIAN_POINT('Ctrl Pts',(132.204475205076,-1.61377893971469,126.156379676994));
#37998=CARTESIAN_POINT('Ctrl Pts',(132.196727308299,-1.74209185499535,126.204980329825));
#37999=CARTESIAN_POINT('Ctrl Pts',(132.188981032215,-1.87037792998007,126.253570816447));
#38000=CARTESIAN_POINT('Ctrl Pts',(132.181234756131,-1.99666229164767,126.307545014208));
#38001=CARTESIAN_POINT('Ctrl Pts',(132.173488480047,-2.1204686779699,126.366704068412));
#38002=CARTESIAN_POINT('Ctrl Pts',(132.165742146781,-2.24427597820225,126.425863559314));
#38003=CARTESIAN_POINT('Ctrl Pts',(132.157995813516,-2.36560491382767,126.490207814469));
#38004=CARTESIAN_POINT('Ctrl Pts',(132.150249480251,-2.48400171399254,126.559490943785));
#38005=CARTESIAN_POINT('Ctrl Pts',(132.142501412248,-2.60242502830046,126.628789588579));
#38006=CARTESIAN_POINT('Ctrl Pts',(132.134753344245,-2.71791456315555,126.703029110977));
#38007=CARTESIAN_POINT('Ctrl Pts',(132.127005276242,-2.83004388641667,126.781919236582));
#38008=CARTESIAN_POINT('Ctrl Pts',(132.1192489735,-2.94229238205684,126.860893207551));
#38009=CARTESIAN_POINT('Ctrl Pts',(132.111492670758,-3.05117321183601,126.944527430008));
#38010=CARTESIAN_POINT('Ctrl Pts',(132.103736368016,-3.15629108617485,127.03248977648));
#38011=CARTESIAN_POINT('Ctrl Pts',(132.095975925502,-3.26146506508811,127.120499071105));
#38012=CARTESIAN_POINT('Ctrl Pts',(132.088215482988,-3.36287179771774,127.212840829614));
#38013=CARTESIAN_POINT('Ctrl Pts',(132.080455040474,-3.46015224326087,127.309145385859));
#38014=CARTESIAN_POINT('Ctrl Pts',(132.072682140208,-3.55758885201153,127.405604538728));
#38015=CARTESIAN_POINT('Ctrl Pts',(132.064909239943,-3.65088567080659,127.506038914897));
#38016=CARTESIAN_POINT('Ctrl Pts',(132.057136339677,-3.73972281860737,127.610044367962));
#38017=CARTESIAN_POINT('Ctrl Pts',(132.049646003915,-3.82533051231844,127.710268960833));
#38018=CARTESIAN_POINT('Ctrl Pts',(132.042155668153,-3.90679695582707,127.813809260897));
#38019=CARTESIAN_POINT('Ctrl Pts',(132.034665332391,-3.98387464421675,127.920279155182));
#38020=CARTESIAN_POINT('Ctrl Pts',(132.026827458088,-4.06452860318,128.031689067232));
#38021=CARTESIAN_POINT('Ctrl Pts',(132.018989583785,-4.14063184094279,128.146659040027));
#38022=CARTESIAN_POINT('Ctrl Pts',(132.011151709482,-4.21185673676159,128.264784690074));
#38023=CARTESIAN_POINT('Ctrl Pts',(132.003327105895,-4.28296103797626,128.382710335392));
#38024=CARTESIAN_POINT('Ctrl Pts',(131.995502502307,-4.34920325460927,128.503780689803));
#38025=CARTESIAN_POINT('Ctrl Pts',(131.98767789872,-4.41029743374626,128.627560303253));
#38026=CARTESIAN_POINT('Ctrl Pts',(131.979860958591,-4.47133177692381,128.751218686302));
#38027=CARTESIAN_POINT('Ctrl Pts',(131.972044018461,-4.52722794482337,128.877580708845));
#38028=CARTESIAN_POINT('Ctrl Pts',(131.964227078332,-4.57774427904976,129.006183657941));
#38029=CARTESIAN_POINT('Ctrl Pts',(131.956417638901,-4.62821214062265,129.134663206827));
#38030=CARTESIAN_POINT('Ctrl Pts',(131.948608199471,-4.67331031006328,129.265379045104));
#38031=CARTESIAN_POINT('Ctrl Pts',(131.940798760041,-4.71284417704997,129.397846193415));
#38032=CARTESIAN_POINT('Ctrl Pts',(131.937191320734,-4.73110618253503,129.459037166457));
#38033=CARTESIAN_POINT('Ctrl Pts',(131.933583881427,-4.74818152974977,129.520601539124));
#38034=CARTESIAN_POINT('Ctrl Pts',(131.929976442121,-4.76405452823405,129.582490119308));
#38035=CARTESIAN_POINT('Origin',(213.235140564004,0.,130.804360617566));
#38036=CARTESIAN_POINT('',(129.834833026848,-4.76405452823404,129.582490119308));
#38037=CARTESIAN_POINT('',(130.180282649887,-4.76405452823405,129.582490119308));
#38038=CARTESIAN_POINT('',(213.235140564004,-4.76405452823405,129.582490119308));
#38039=CARTESIAN_POINT('',(131.514859436023,-4.91824964687546,130.80622435291));
#38040=CARTESIAN_POINT('Ctrl Pts',(131.514859435991,-4.91824964687524,130.806224353474));
#38041=CARTESIAN_POINT('Ctrl Pts',(131.509025984302,-4.91821083134048,130.908655437895));
#38042=CARTESIAN_POINT('Ctrl Pts',(131.503192532613,-4.91497231306959,131.011022270698));
#38043=CARTESIAN_POINT('Ctrl Pts',(131.497359080925,-4.90854456339616,131.113186347799));
#38044=CARTESIAN_POINT('Ctrl Pts',(131.489584746806,-4.89997819887275,131.249342043044));
#38045=CARTESIAN_POINT('Ctrl Pts',(131.481810412686,-4.88572883907578,131.385356701805));
#38046=CARTESIAN_POINT('Ctrl Pts',(131.474036078567,-4.86580064242577,131.520717491386));
#38047=CARTESIAN_POINT('Ctrl Pts',(131.46627132562,-4.8458970054971,131.655911460891));
#38048=CARTESIAN_POINT('Ctrl Pts',(131.458506572673,-4.82032851335909,131.790452781506));
#38049=CARTESIAN_POINT('Ctrl Pts',(131.450741819726,-4.78915127743318,131.923830628044));
#38050=CARTESIAN_POINT('Ctrl Pts',(131.442984778841,-4.75800500717745,132.057076001825));
#38051=CARTESIAN_POINT('Ctrl Pts',(131.435227737956,-4.72126116745904,132.189159822943));
#38052=CARTESIAN_POINT('Ctrl Pts',(131.427470697071,-4.67902736699891,132.319578740931));
#38053=CARTESIAN_POINT('Ctrl Pts',(131.419719505831,-4.63682541537638,132.449899308999));
#38054=CARTESIAN_POINT('Ctrl Pts',(131.411968314591,-4.58914186343657,132.578557102521));
#38055=CARTESIAN_POINT('Ctrl Pts',(131.404217123351,-4.5361347767085,132.70506163299));
#38056=CARTESIAN_POINT('Ctrl Pts',(131.396469226574,-4.48315021940624,132.83151239566));
#38057=CARTESIAN_POINT('Ctrl Pts',(131.388721329797,-4.42484677831832,132.955811355693));
#38058=CARTESIAN_POINT('Ctrl Pts',(131.38097343302,-4.36143142082994,133.077486004318));
#38059=CARTESIAN_POINT('Ctrl Pts',(131.373227156935,-4.29802932846723,133.199135201229));
#38060=CARTESIAN_POINT('Ctrl Pts',(131.365480880851,-4.22951762718827,133.31816083214));
#38061=CARTESIAN_POINT('Ctrl Pts',(131.357734604767,-4.15615003054825,133.434113455016));
#38062=CARTESIAN_POINT('Ctrl Pts',(131.349988271502,-4.08278189232539,133.550066933827));
#38063=CARTESIAN_POINT('Ctrl Pts',(131.342241938237,-4.00455799626143,133.662947028955));
#38064=CARTESIAN_POINT('Ctrl Pts',(131.334495604971,-3.92177610568397,133.772332187407));
#38065=CARTESIAN_POINT('Ctrl Pts',(131.326747536968,-3.83897567667592,133.881741841908));
#38066=CARTESIAN_POINT('Ctrl Pts',(131.318999468965,-3.75161545790435,133.987654690624));
#38067=CARTESIAN_POINT('Ctrl Pts',(131.311251400962,-3.66003405740353,134.089681570098));
#38068=CARTESIAN_POINT('Ctrl Pts',(131.30349509822,-3.56835532310054,134.191816884954));
#38069=CARTESIAN_POINT('Ctrl Pts',(131.295738795479,-3.47244670673212,134.290057688929));
#38070=CARTESIAN_POINT('Ctrl Pts',(131.287982492737,-3.37268469825481,134.384050686365));
#38071=CARTESIAN_POINT('Ctrl Pts',(131.280222050223,-3.27286944378979,134.478093850694));
#38072=CARTESIAN_POINT('Ctrl Pts',(131.272461607708,-3.16919699451058,134.567884435097));
#38073=CARTESIAN_POINT('Ctrl Pts',(131.264701165194,-3.06207683500362,134.653109572621));
#38074=CARTESIAN_POINT('Ctrl Pts',(131.256928264929,-2.95478471670686,134.738471521101));
#38075=CARTESIAN_POINT('Ctrl Pts',(131.249155364663,-2.84403414439618,134.819253146776));
#38076=CARTESIAN_POINT('Ctrl Pts',(131.241382464398,-2.73026421646917,134.895184540783));
#38077=CARTESIAN_POINT('Ctrl Pts',(131.233892128636,-2.62063011199177,134.968355637359));
#38078=CARTESIAN_POINT('Ctrl Pts',(131.226401792874,-2.50819262590463,135.03702285572));
#38079=CARTESIAN_POINT('Ctrl Pts',(131.218911457112,-2.39336440113872,135.100986026636));
#38080=CARTESIAN_POINT('Ctrl Pts',(131.211137122993,-2.2741824293291,135.167374380618));
#38081=CARTESIAN_POINT('Ctrl Pts',(131.203362788874,-2.15204731774808,135.228905236061));
#38082=CARTESIAN_POINT('Ctrl Pts',(131.195588454755,-2.0273927747941,135.285304892963));
#38083=CARTESIAN_POINT('Ctrl Pts',(131.187823701808,-1.9028918574237,135.341635042329));
#38084=CARTESIAN_POINT('Ctrl Pts',(131.180058948861,-1.77587803943621,135.392846415902));
#38085=CARTESIAN_POINT('Ctrl Pts',(131.172294195913,-1.64681142212257,135.438710108322));
#38086=CARTESIAN_POINT('Ctrl Pts',(131.164537155028,-1.51787299559294,135.484528248275));
#38087=CARTESIAN_POINT('Ctrl Pts',(131.156780114143,-1.38688619319223,135.525009146921));
#38088=CARTESIAN_POINT('Ctrl Pts',(131.149023073258,-1.25433266306687,135.559971265302));
#38089=CARTESIAN_POINT('Ctrl Pts',(131.141271882018,-1.12187909258979,135.594907018478));
#38090=CARTESIAN_POINT('Ctrl Pts',(131.133520690778,-0.987861522562395,
135.624332175803));
#38091=CARTESIAN_POINT('Ctrl Pts',(131.125769499538,-0.85277805313735,135.648114601264));
#38092=CARTESIAN_POINT('Ctrl Pts',(131.118021602761,-0.717751997790004,
135.671886918559));
#38093=CARTESIAN_POINT('Ctrl Pts',(131.110273705984,-0.581661328335614,
135.690021206402));
#38094=CARTESIAN_POINT('Ctrl Pts',(131.102525809207,-0.445015450713763,
135.702436189781));
#38095=CARTESIAN_POINT('Ctrl Pts',(131.094779533123,-0.308398156463766,
135.714848576213));
#38096=CARTESIAN_POINT('Ctrl Pts',(131.087033257039,-0.171226274165125,
135.721544002444));
#38097=CARTESIAN_POINT('Ctrl Pts',(131.079286980955,-0.0340150705038945,
135.722492990477));
#38098=CARTESIAN_POINT('Ctrl Pts',(131.071540647689,0.103197146019178,135.723441985516));
#38099=CARTESIAN_POINT('Ctrl Pts',(131.063794314424,0.24044829352818,135.718644455007));
#38100=CARTESIAN_POINT('Ctrl Pts',(131.056047981159,0.377222759200355,135.708123055984));
#38101=CARTESIAN_POINT('Ctrl Pts',(131.048299913156,0.514027854565697,135.697599300767));
#38102=CARTESIAN_POINT('Ctrl Pts',(131.040551845153,0.65035566593594,135.681349156341));
#38103=CARTESIAN_POINT('Ctrl Pts',(131.03280377715,0.78569575315938,135.65944715088));
#38104=CARTESIAN_POINT('Ctrl Pts',(131.025047474408,0.921179681438274,135.637521867708));
#38105=CARTESIAN_POINT('Ctrl Pts',(131.017291171666,1.05567340199217,135.609932786697));
#38106=CARTESIAN_POINT('Ctrl Pts',(131.009534868924,1.18867617515979,135.576805694579));
#38107=CARTESIAN_POINT('Ctrl Pts',(131.00177442641,1.32174993591217,135.543660921535));
#38108=CARTESIAN_POINT('Ctrl Pts',(130.994013983896,1.45333078874808,135.504972357927));
#38109=CARTESIAN_POINT('Ctrl Pts',(130.986253541381,1.58293417341703,135.460915402504));
#38110=CARTESIAN_POINT('Ctrl Pts',(130.978480641116,1.71274560894469,135.416787722945));
#38111=CARTESIAN_POINT('Ctrl Pts',(130.970707740851,1.84057286804668,135.367274571719));
#38112=CARTESIAN_POINT('Ctrl Pts',(130.962934840585,1.9659515253437,135.312599482411));
#38113=CARTESIAN_POINT('Ctrl Pts',(130.955444504823,2.08677235263906,135.259911970317));
#38114=CARTESIAN_POINT('Ctrl Pts',(130.947954169061,2.20531923587244,135.20243143769));
#38115=CARTESIAN_POINT('Ctrl Pts',(130.940463833299,2.32120072341737,135.140396856357));
#38116=CARTESIAN_POINT('Ctrl Pts',(130.93268949918,2.44147589278306,135.076010215018));
#38117=CARTESIAN_POINT('Ctrl Pts',(130.924915165061,2.55926055523696,135.00651341694));
#38118=CARTESIAN_POINT('Ctrl Pts',(130.917140830942,2.67409000923304,134.932123411746));
#38119=CARTESIAN_POINT('Ctrl Pts',(130.909376077995,2.78877794618959,134.857825085586));
#38120=CARTESIAN_POINT('Ctrl Pts',(130.901611325047,2.9005175962659,134.778645761619));
#38121=CARTESIAN_POINT('Ctrl Pts',(130.8938465721,3.0088676789107,134.694848807152));
#38122=CARTESIAN_POINT('Ctrl Pts',(130.886089531215,3.11711014672594,134.611135081001));
#38123=CARTESIAN_POINT('Ctrl Pts',(130.87833249033,3.22196943946388,134.522813088922));
#38124=CARTESIAN_POINT('Ctrl Pts',(130.870575449445,3.32303248066937,134.430189928898));
#38125=CARTESIAN_POINT('Ctrl Pts',(130.862824258205,3.42401930944933,134.33763661672));
#38126=CARTESIAN_POINT('Ctrl Pts',(130.855073066965,3.52121529783151,134.240788855765));
#38127=CARTESIAN_POINT('Ctrl Pts',(130.847321875725,3.61424004074636,134.139994289054));
#38128=CARTESIAN_POINT('Ctrl Pts',(130.839573978948,3.70722524566402,134.039242562723));
#38129=CARTESIAN_POINT('Ctrl Pts',(130.831826082171,3.79604246665503,133.934547653756));
#38130=CARTESIAN_POINT('Ctrl Pts',(130.824078185394,3.88034797839801,133.82629420867));
#38131=CARTESIAN_POINT('Ctrl Pts',(130.81633190931,3.96463585524536,133.71806340787));
#38132=CARTESIAN_POINT('Ctrl Pts',(130.808585633225,4.04441365995016,133.606275859806));
#38133=CARTESIAN_POINT('Ctrl Pts',(130.800839357141,4.11937807760781,133.491349139355));
#38134=CARTESIAN_POINT('Ctrl Pts',(130.793093023876,4.19434304863571,133.37642157054));
#38135=CARTESIAN_POINT('Ctrl Pts',(130.785346690611,4.26449434812018,133.258355110561));
#38136=CARTESIAN_POINT('Ctrl Pts',(130.777600357345,4.32957233673832,133.137595805765));
#38137=CARTESIAN_POINT('Ctrl Pts',(130.769852289342,4.39466489912074,133.01680945776));
#38138=CARTESIAN_POINT('Ctrl Pts',(130.762104221339,4.45468170442435,132.893329409056));
#38139=CARTESIAN_POINT('Ctrl Pts',(130.754356153336,4.50940954994301,132.767625391707));
#38140=CARTESIAN_POINT('Ctrl Pts',(130.746599850595,4.56419556086724,132.641787774632));
#38141=CARTESIAN_POINT('Ctrl Pts',(130.738843547853,4.61368122680096,132.513721826283));
#38142=CARTESIAN_POINT('Ctrl Pts',(130.731087245111,4.65770171366438,132.383916823919));
#38143=CARTESIAN_POINT('Ctrl Pts',(130.723326802597,4.7017456955871,132.254042540716));
#38144=CARTESIAN_POINT('Ctrl Pts',(130.715566360082,4.74031857630529,132.122427729011));
#38145=CARTESIAN_POINT('Ctrl Pts',(130.707805917568,4.77330600710254,131.989574870374));
#38146=CARTESIAN_POINT('Ctrl Pts',(130.700033017303,4.80634639225217,131.856508744534));
#38147=CARTESIAN_POINT('Ctrl Pts',(130.692260117037,4.83378333173931,131.722200983532));
#38148=CARTESIAN_POINT('Ctrl Pts',(130.684487216772,4.85555385743811,131.587163146955));
#38149=CARTESIAN_POINT('Ctrl Pts',(130.67699688101,4.87653296969101,131.457034275879));
#38150=CARTESIAN_POINT('Ctrl Pts',(130.669506545248,4.8922504557149,131.326227793669));
#38151=CARTESIAN_POINT('Ctrl Pts',(130.662016209486,4.90269578010907,131.195202209775));
#38152=CARTESIAN_POINT('Ctrl Pts',(130.654241875367,4.91353714215249,131.059208751043));
#38153=CARTESIAN_POINT('Ctrl Pts',(130.646467541248,4.91873300478485,130.922548461771));
#38154=CARTESIAN_POINT('Ctrl Pts',(130.638693207129,4.91821471133141,130.785729575101));
#38155=CARTESIAN_POINT('Ctrl Pts',(130.630928454182,4.91769705662832,130.649079305481));
#38156=CARTESIAN_POINT('Ctrl Pts',(130.623163701235,4.91147925915879,130.512271214574));
#38157=CARTESIAN_POINT('Ctrl Pts',(130.615398948287,4.89954437438008,130.375818920668));
#38158=CARTESIAN_POINT('Ctrl Pts',(130.607641907402,4.88762134349718,130.239502153103));
#38159=CARTESIAN_POINT('Ctrl Pts',(130.599884866517,4.86999255920737,130.10354086625));
#38160=CARTESIAN_POINT('Ctrl Pts',(130.592127825632,4.84669311382913,129.96844858699));
#38161=CARTESIAN_POINT('Ctrl Pts',(130.584376634392,4.82341123874389,129.83345818187));
#38162=CARTESIAN_POINT('Ctrl Pts',(130.576625443152,4.79446728044548,129.699335863676));
#38163=CARTESIAN_POINT('Ctrl Pts',(130.568874251912,4.75994810262256,129.566589587512));
#38164=CARTESIAN_POINT('Ctrl Pts',(130.561126355135,4.72544359637106,129.433899732058));
#38165=CARTESIAN_POINT('Ctrl Pts',(130.553378458358,4.68536868177046,129.302585132992));
#38166=CARTESIAN_POINT('Ctrl Pts',(130.545630561581,4.63986118089606,129.173142887));
#38167=CARTESIAN_POINT('Ctrl Pts',(130.537884285497,4.59436319920982,129.043727717535));
#38168=CARTESIAN_POINT('Ctrl Pts',(130.530138009413,4.54343502115958,128.916184490721));
#38169=CARTESIAN_POINT('Ctrl Pts',(130.522391733329,4.48726401520176,128.790994103397));
#38170=CARTESIAN_POINT('Ctrl Pts',(130.514645400063,4.43109259460237,128.665802791947));
#38171=CARTESIAN_POINT('Ctrl Pts',(130.506899066798,4.36967842891768,128.54296471135));
#38172=CARTESIAN_POINT('Ctrl Pts',(130.499152733532,4.30325644817831,128.422939402469));
#38173=CARTESIAN_POINT('Ctrl Pts',(130.491404665529,4.23681959269689,128.302887214753));
#38174=CARTESIAN_POINT('Ctrl Pts',(130.483656597526,4.16537287984385,128.185649394194));
#38175=CARTESIAN_POINT('Ctrl Pts',(130.475908529524,4.08919626723004,128.071659215917));
#38176=CARTESIAN_POINT('Ctrl Pts',(130.468152226782,4.01293869320583,127.957547887523));
#38177=CARTESIAN_POINT('Ctrl Pts',(130.46039592404,3.93194139503565,127.846691421999));
#38178=CARTESIAN_POINT('Ctrl Pts',(130.452639621298,3.84652691868793,127.739492965234));
#38179=CARTESIAN_POINT('Ctrl Pts',(130.444879178784,3.76106685406228,127.632237293426));
#38180=CARTESIAN_POINT('Ctrl Pts',(130.43711873627,3.67118516967286,127.52864381584));
#38181=CARTESIAN_POINT('Ctrl Pts',(130.429358293755,3.57724280922148,127.429080340852));
#38182=CARTESIAN_POINT('Ctrl Pts',(130.42158539349,3.48314964415336,127.329357037736));
#38183=CARTESIAN_POINT('Ctrl Pts',(130.413812493225,3.38498305700623,127.23367693802));
#38184=CARTESIAN_POINT('Ctrl Pts',(130.406039592959,3.28313940153916,127.142369529024));
#38185=CARTESIAN_POINT('Ctrl Pts',(130.398549257197,3.18499801947666,127.054381374334));
#38186=CARTESIAN_POINT('Ctrl Pts',(130.391058921435,3.08344250647774,126.970453709439));
#38187=CARTESIAN_POINT('Ctrl Pts',(130.383568585673,2.978852924886,126.890843233626));
#38188=CARTESIAN_POINT('Ctrl Pts',(130.375794251554,2.87029779751921,126.808214302426));
#38189=CARTESIAN_POINT('Ctrl Pts',(130.368019917435,2.75813011640286,126.729974651574));
#38190=CARTESIAN_POINT('Ctrl Pts',(130.360245583316,2.64274036186352,126.656456756303));
#38191=CARTESIAN_POINT('Ctrl Pts',(130.352480830369,2.52749281488413,126.583029465268));
#38192=CARTESIAN_POINT('Ctrl Pts',(130.344716077422,2.40903142198699,126.514312559517));
#38193=CARTESIAN_POINT('Ctrl Pts',(130.336951324474,2.2877791458449,126.450597918206));
#38194=CARTESIAN_POINT('Ctrl Pts',(130.329194283589,2.16664729917275,126.386946559175));
#38195=CARTESIAN_POINT('Ctrl Pts',(130.321437242704,2.04273042940345,126.328287758088));
#38196=CARTESIAN_POINT('Ctrl Pts',(130.313680201819,1.91647954950282,126.274869564607));
#38197=CARTESIAN_POINT('Ctrl Pts',(130.305929010579,1.79032387637273,126.221491654201));
#38198=CARTESIAN_POINT('Ctrl Pts',(130.298177819339,1.66183805507885,126.17334663695));
#38199=CARTESIAN_POINT('Ctrl Pts',(130.290426628099,1.53149639458168,126.130635994112));
#38200=CARTESIAN_POINT('Ctrl Pts',(130.282678731322,1.4012101327673,126.087943504436));
#38201=CARTESIAN_POINT('Ctrl Pts',(130.274930834545,1.26906997132464,126.050680916738));
#38202=CARTESIAN_POINT('Ctrl Pts',(130.267182937768,1.1355686279714,126.019000970302));
#38203=CARTESIAN_POINT('Ctrl Pts',(130.259436661684,1.00209521022124,125.987327650627));
#38204=CARTESIAN_POINT('Ctrl Pts',(130.2516903856,0.867261557064295,125.961234739672));
#38205=CARTESIAN_POINT('Ctrl Pts',(130.243944109515,0.731573537860023,125.940824535536));
#38206=CARTESIAN_POINT('Ctrl Pts',(130.23619777625,0.595884517037618,125.920414180738));
#38207=CARTESIAN_POINT('Ctrl Pts',(130.228451442985,0.459341504199096,125.905686674618));
#38208=CARTESIAN_POINT('Ctrl Pts',(130.220705109719,0.322458109507423,125.896692756951));
#38209=CARTESIAN_POINT('Ctrl Pts',(130.212957041716,0.185544060728592,125.887696825159));
#38210=CARTESIAN_POINT('Ctrl Pts',(130.205208973713,0.0482898684647223,
125.884437062453));
#38211=CARTESIAN_POINT('Ctrl Pts',(130.19746090571,-0.0887886167240415,
125.886912128355));
#38212=CARTESIAN_POINT('Ctrl Pts',(130.189704602969,-0.226012790558119,
125.889389824787));
#38213=CARTESIAN_POINT('Ctrl Pts',(130.181948300227,-0.363060492751894,
125.897614518265));
#38214=CARTESIAN_POINT('Ctrl Pts',(130.174191997485,-0.499418201276451,
125.911532751931));
#38215=CARTESIAN_POINT('Ctrl Pts',(130.166431554971,-0.635848688015792,
125.925458414177));
#38216=CARTESIAN_POINT('Ctrl Pts',(130.158671112457,-0.771588060523373,
125.945083615789));
#38217=CARTESIAN_POINT('Ctrl Pts',(130.150910669942,-0.906131772308056,
125.970303494019));
#38218=CARTESIAN_POINT('Ctrl Pts',(130.143137769677,-1.04089146560313,125.995563857437));
#38219=CARTESIAN_POINT('Ctrl Pts',(130.135364869412,-1.17445128150084,126.026436756413));
#38220=CARTESIAN_POINT('Ctrl Pts',(130.127591969146,-1.30631977409885,126.06276682325));
#38221=CARTESIAN_POINT('Ctrl Pts',(130.120101633384,-1.43339451483387,126.097776200647));
#38222=CARTESIAN_POINT('Ctrl Pts',(130.112611297622,-1.55889847167166,126.137852777012));
#38223=CARTESIAN_POINT('Ctrl Pts',(130.10512096186,-1.68241024325098,126.182815547364));
#38224=CARTESIAN_POINT('Ctrl Pts',(130.097346473652,-1.81060754203999,126.229484019783));
#38225=CARTESIAN_POINT('Ctrl Pts',(130.089571985444,-1.93706461948167,126.281564563924));
#38226=CARTESIAN_POINT('Ctrl Pts',(130.081797497236,-2.0612906615337,126.338908359264));
#38227=CARTESIAN_POINT('Ctrl Pts',(130.074032626073,-2.18536303591096,126.396181220301));
#38228=CARTESIAN_POINT('Ctrl Pts',(130.066267754911,-2.30720951455965,126.458704215773));
#38229=CARTESIAN_POINT('Ctrl Pts',(130.058502883748,-2.42635588845429,126.526279252624));
#38230=CARTESIAN_POINT('Ctrl Pts',(130.05074576037,-2.54538337815762,126.593786863138));
#38231=CARTESIAN_POINT('Ctrl Pts',(130.042988636993,-2.66171578683055,126.666336291502));
#38232=CARTESIAN_POINT('Ctrl Pts',(130.035231513615,-2.77490062623944,126.74368215492));
#38233=CARTESIAN_POINT('Ctrl Pts',(130.027480275489,-2.8879995934364,126.820969336801));
#38234=CARTESIAN_POINT('Ctrl Pts',(130.019729037363,-2.9979554232324,126.9030454906));
#38235=CARTESIAN_POINT('Ctrl Pts',(130.011977799238,-3.10434222180379,126.989620464892));
#38236=CARTESIAN_POINT('Ctrl Pts',(130.00423003788,-3.21068130127053,127.076156606543));
#38237=CARTESIAN_POINT('Ctrl Pts',(129.996482276521,-3.31345423189615,127.167187307716));
#38238=CARTESIAN_POINT('Ctrl Pts',(129.988734515163,-3.412266205948,127.262380606012));
#38239=CARTESIAN_POINT('Ctrl Pts',(129.980988425214,-3.51105686349139,127.35755336845));
#38240=CARTESIAN_POINT('Ctrl Pts',(129.973242335264,-3.60588798304674,127.456886670484));
#38241=CARTESIAN_POINT('Ctrl Pts',(129.965496245315,-3.69640009032173,127.56001023039));
#38242=CARTESIAN_POINT('Ctrl Pts',(129.957750148934,-3.78691227274952,127.66313387592));
#38243=CARTESIAN_POINT('Ctrl Pts',(129.950004052553,-3.87310517804813,127.770047491654));
#38244=CARTESIAN_POINT('Ctrl Pts',(129.942257956172,-3.9546585277464,127.880346426181));
#38245=CARTESIAN_POINT('Ctrl Pts',(129.934510175881,-4.03622960618354,127.990669338398));
#38246=CARTESIAN_POINT('Ctrl Pts',(129.92676239559,-4.11315889006694,128.104378719303));
#38247=CARTESIAN_POINT('Ctrl Pts',(129.919014615299,-4.18516870655706,128.221039894126));
#38248=CARTESIAN_POINT('Ctrl Pts',(129.911259297473,-4.25724857878879,128.337814564379));
#38249=CARTESIAN_POINT('Ctrl Pts',(129.903503979647,-4.32439922019065,128.45754643047));
#38250=CARTESIAN_POINT('Ctrl Pts',(129.895748661821,-4.38638811719911,128.579774735251));
#38251=CARTESIAN_POINT('Ctrl Pts',(129.887989225181,-4.44840993623201,128.702067954936));
#38252=CARTESIAN_POINT('Ctrl Pts',(129.880229788541,-4.50526438665995,128.826859899736));
#38253=CARTESIAN_POINT('Ctrl Pts',(129.8724703519,-4.55676703219201,128.953669590725));
#38254=CARTESIAN_POINT('Ctrl Pts',(129.864700083919,-4.60834156989123,129.080656294438));
#38255=CARTESIAN_POINT('Ctrl Pts',(129.856929815938,-4.65454924940357,129.209666002495));
#38256=CARTESIAN_POINT('Ctrl Pts',(129.849159547956,-4.69525525982363,129.340201777959));
#38257=CARTESIAN_POINT('Ctrl Pts',(129.84438404092,-4.72027265171207,129.420427391242));
#38258=CARTESIAN_POINT('Ctrl Pts',(129.839608533884,-4.7432129639482,129.501229176473));
#38259=CARTESIAN_POINT('Ctrl Pts',(129.834833026848,-4.76405452823404,129.582490119308));
#38260=CARTESIAN_POINT('Ctrl Pts',(131.584997718909,-4.76405452823404,129.582490119308));
#38261=CARTESIAN_POINT('Ctrl Pts',(131.577310227301,-4.79783637010872,129.714205008067));
#38262=CARTESIAN_POINT('Ctrl Pts',(131.569622735692,-4.82612622203509,129.847222924197));
#38263=CARTESIAN_POINT('Ctrl Pts',(131.561935244083,-4.84884825233541,129.981041913586));
#38264=CARTESIAN_POINT('Ctrl Pts',(131.554089276073,-4.87203869363109,130.117619559889));
#38265=CARTESIAN_POINT('Ctrl Pts',(131.546243308063,-4.88942919083452,130.25503123002));
#38266=CARTESIAN_POINT('Ctrl Pts',(131.538397340053,-4.90099496924391,130.392740192968));
#38267=CARTESIAN_POINT('Ctrl Pts',(131.530551372043,-4.9125607476533,130.530449155917));
#38268=CARTESIAN_POINT('Ctrl Pts',(131.522705404033,-4.9183018535908,130.668454974763));
#38269=CARTESIAN_POINT('Ctrl Pts',(131.514859436023,-4.91824964687546,130.806224352909));
#38270=CARTESIAN_POINT('',(131.860140563953,-4.91824899481853,130.807505051778));
#38271=CARTESIAN_POINT('Ctrl Pts',(131.929976442121,-4.76405452823405,129.582490119308));
#38272=CARTESIAN_POINT('Ctrl Pts',(131.922173593699,-4.79838763563934,129.716354384004));
#38273=CARTESIAN_POINT('Ctrl Pts',(131.914370745277,-4.82709221949561,129.851736299158));
#38274=CARTESIAN_POINT('Ctrl Pts',(131.906567896855,-4.85004596951037,129.988127099425));
#38275=CARTESIAN_POINT('Ctrl Pts',(131.898766189335,-4.87299636331966,130.124497957176));
#38276=CARTESIAN_POINT('Ctrl Pts',(131.890964481814,-4.89019752581795,130.26187703042));
#38277=CARTESIAN_POINT('Ctrl Pts',(131.883162774293,-4.90157827896259,130.399745445208));
#38278=CARTESIAN_POINT('Ctrl Pts',(131.875488704198,-4.91277284081155,130.535358306391));
#38279=CARTESIAN_POINT('Ctrl Pts',(131.867814634103,-4.9183359839254,130.671444256286));
#38280=CARTESIAN_POINT('Ctrl Pts',(131.860140564008,-4.91824899481915,130.807505050802));
#38281=CARTESIAN_POINT('Ctrl Pts',(131.860140563953,-4.91824899481853,130.807505051778));
#38282=CARTESIAN_POINT('Ctrl Pts',(131.851406713904,-4.91814999258943,130.962355680208));
#38283=CARTESIAN_POINT('Ctrl Pts',(131.842672863855,-4.91073377224643,131.116928504414));
#38284=CARTESIAN_POINT('Ctrl Pts',(131.833939013806,-4.89610311273186,131.270576631874));
#38285=CARTESIAN_POINT('Ctrl Pts',(131.825171001558,-4.88141522582029,131.424825749494));
#38286=CARTESIAN_POINT('Ctrl Pts',(131.81640298931,-4.859456461858,131.578142736764));
#38287=CARTESIAN_POINT('Ctrl Pts',(131.807634977062,-4.83038066305623,131.729890580599));
#38288=CARTESIAN_POINT('Ctrl Pts',(131.798818421842,-4.80114388983702,131.882478556839));
#38289=CARTESIAN_POINT('Ctrl Pts',(131.790001866623,-4.76471115565391,132.033479782782));
#38290=CARTESIAN_POINT('Ctrl Pts',(131.781185311404,-4.72128763113361,132.182267060909));
#38291=CARTESIAN_POINT('Ctrl Pts',(131.772862777129,-4.68029727127292,132.322717292447));
#38292=CARTESIAN_POINT('Ctrl Pts',(131.764540242853,-4.63307809789463,132.461194792037));
#38293=CARTESIAN_POINT('Ctrl Pts',(131.756217708578,-4.57984097248172,132.597190706916));
#38294=CARTESIAN_POINT('Ctrl Pts',(131.748443374459,-4.53011054340665,132.72422865547));
#38295=CARTESIAN_POINT('Ctrl Pts',(131.74066904034,-4.47501157464565,132.849397083174));
#38296=CARTESIAN_POINT('Ctrl Pts',(131.732894706221,-4.41470461200455,132.972208917435));
#38297=CARTESIAN_POINT('Ctrl Pts',(131.725129953274,-4.35447197230511,133.094869397087));
#38298=CARTESIAN_POINT('Ctrl Pts',(131.717365200327,-4.28904428007655,133.215178714402));
#38299=CARTESIAN_POINT('Ctrl Pts',(131.70960044738,-4.21863094014019,133.332667571516));
#38300=CARTESIAN_POINT('Ctrl Pts',(131.701843406495,-4.14828753572565,133.450039737041));
#38301=CARTESIAN_POINT('Ctrl Pts',(131.69408636561,-4.0729685376213,133.564596683941));
#38302=CARTESIAN_POINT('Ctrl Pts',(131.686329324725,-3.99293010639168,133.675891956063));
#38303=CARTESIAN_POINT('Ctrl Pts',(131.678578133485,-3.91295203276555,133.787103299555));
#38304=CARTESIAN_POINT('Ctrl Pts',(131.670826942245,-3.82826183725292,133.895057547937));
#38305=CARTESIAN_POINT('Ctrl Pts',(131.663075751004,-3.73915980044368,133.999335899043));
#38306=CARTESIAN_POINT('Ctrl Pts',(131.655327854227,-3.65009563437707,134.103569929067));
#38307=CARTESIAN_POINT('Ctrl Pts',(131.64757995745,-3.55662360999035,134.204130872604));
#38308=CARTESIAN_POINT('Ctrl Pts',(131.639832060673,-3.45908508456563,134.300631980066));
#38309=CARTESIAN_POINT('Ctrl Pts',(131.632085784589,-3.3615669620978,134.397112901576));
#38310=CARTESIAN_POINT('Ctrl Pts',(131.624339508505,-3.25998430828257,134.489535401377));
#38311=CARTESIAN_POINT('Ctrl Pts',(131.616593232421,-3.15471595111122,134.577548968325));
#38312=CARTESIAN_POINT('Ctrl Pts',(131.608846899156,-3.04944681687263,134.665563184969));
#38313=CARTESIAN_POINT('Ctrl Pts',(131.60110056589,-2.94049222492938,134.749168153039));
#38314=CARTESIAN_POINT('Ctrl Pts',(131.593354232625,-2.82826443393104,134.828053368542));
#38315=CARTESIAN_POINT('Ctrl Pts',(131.585606164622,-2.71601151029719,134.906956249843));
#38316=CARTESIAN_POINT('Ctrl Pts',(131.577858096619,-2.60048424879594,134.981137050572));
#38317=CARTESIAN_POINT('Ctrl Pts',(131.570110028616,-2.48212391256823,135.050328580841));
#38318=CARTESIAN_POINT('Ctrl Pts',(131.562353725874,-2.36363778156667,135.119593648691));
#38319=CARTESIAN_POINT('Ctrl Pts',(131.554597423132,-2.24231289905267,135.183858655828));
#38320=CARTESIAN_POINT('Ctrl Pts',(131.546841120391,-2.11861564932518,135.24290213398));
#38321=CARTESIAN_POINT('Ctrl Pts',(131.539080677876,-1.99485237865097,135.301977125415));
#38322=CARTESIAN_POINT('Ctrl Pts',(131.531320235362,-1.8687145771405,135.35582488133));
#38323=CARTESIAN_POINT('Ctrl Pts',(131.523559792848,-1.74068770374561,135.40427250591));
#38324=CARTESIAN_POINT('Ctrl Pts',(131.515786892583,-1.61245531024786,135.452797902918));
#38325=CARTESIAN_POINT('Ctrl Pts',(131.508013992317,-1.48232815629695,135.495905722608));
#38326=CARTESIAN_POINT('Ctrl Pts',(131.500241092052,-1.35080678381879,135.533473017931));
#38327=CARTESIAN_POINT('Ctrl Pts',(131.49275075629,-1.22406654451229,135.569674647443));
#38328=CARTESIAN_POINT('Ctrl Pts',(131.485260420528,-1.09603199285238,135.600731510395));
#38329=CARTESIAN_POINT('Ctrl Pts',(131.477770084766,-0.967157184704948,
135.626578991154));
#38330=CARTESIAN_POINT('Ctrl Pts',(131.469995750647,-0.833396049036143,
135.653406487003));
#38331=CARTESIAN_POINT('Ctrl Pts',(131.462221416528,-0.698305967372166,
135.674706756683));
#38332=CARTESIAN_POINT('Ctrl Pts',(131.454447082409,-0.562383506608875,
135.690351597295));
#38333=CARTESIAN_POINT('Ctrl Pts',(131.446682329462,-0.426628558130827,
135.70597715704));
#38334=CARTESIAN_POINT('Ctrl Pts',(131.438917576514,-0.290043656327314,
135.715961111286));
#38335=CARTESIAN_POINT('Ctrl Pts',(131.431152823567,-0.153136823202405,
135.720225971283));
#38336=CARTESIAN_POINT('Ctrl Pts',(131.423395782682,-0.0163659678742974,
135.724486595362));
#38337=CARTESIAN_POINT('Ctrl Pts',(131.415638741797,0.12072579421784,135.72303941712));
#38338=CARTESIAN_POINT('Ctrl Pts',(131.407881700912,0.257624385826948,135.71585863124));
#38339=CARTESIAN_POINT('Ctrl Pts',(131.400130509672,0.394419741143208,135.708683260447));
#38340=CARTESIAN_POINT('Ctrl Pts',(131.392379318432,0.53102182707775,135.695782908591));
#38341=CARTESIAN_POINT('Ctrl Pts',(131.384628127192,0.666915984512446,135.677183837436));
#38342=CARTESIAN_POINT('Ctrl Pts',(131.376880230415,0.802752383305229,135.658592671382));
#38343=CARTESIAN_POINT('Ctrl Pts',(131.369132333638,0.937881065499304,135.634307656319));
#38344=CARTESIAN_POINT('Ctrl Pts',(131.361384436861,1.07179213576307,135.604406938198));
#38345=CARTESIAN_POINT('Ctrl Pts',(131.353638160777,1.20567519471773,135.574512474663));
#38346=CARTESIAN_POINT('Ctrl Pts',(131.345891884693,1.33834076702356,135.539004729726));
#38347=CARTESIAN_POINT('Ctrl Pts',(131.338145608608,1.46928919194417,135.498012962269));
#38348=CARTESIAN_POINT('Ctrl Pts',(131.330399275343,1.60023858349621,135.45702089222));
#38349=CARTESIAN_POINT('Ctrl Pts',(131.322652942078,1.72947042925848,135.410544835671));
#38350=CARTESIAN_POINT('Ctrl Pts',(131.314906608812,1.85650065755731,135.358763802506));
#38351=CARTESIAN_POINT('Ctrl Pts',(131.307158540809,1.9835593333951,135.306971173337));
#38352=CARTESIAN_POINT('Ctrl Pts',(131.299410472806,2.10841504871024,135.249871351095));
#38353=CARTESIAN_POINT('Ctrl Pts',(131.291662404804,2.23060449557428,135.187691160295));
#38354=CARTESIAN_POINT('Ctrl Pts',(131.283906102062,2.35292380683652,135.125444883649));
#38355=CARTESIAN_POINT('Ctrl Pts',(131.27614979932,2.47257083994451,135.058107630008));
#38356=CARTESIAN_POINT('Ctrl Pts',(131.268393496578,2.58910717526307,134.985952072682));
#38357=CARTESIAN_POINT('Ctrl Pts',(131.260633054064,2.70570570953271,134.913758003763));
#38358=CARTESIAN_POINT('Ctrl Pts',(131.25287261155,2.81918991443573,134.836740726321));
#38359=CARTESIAN_POINT('Ctrl Pts',(131.245112169035,2.92915192540314,134.755215216309));
#38360=CARTESIAN_POINT('Ctrl Pts',(131.23733926877,3.03929045715253,134.67355883431));
#38361=CARTESIAN_POINT('Ctrl Pts',(131.229566368505,3.14589519197781,134.587380003809));
#38362=CARTESIAN_POINT('Ctrl Pts',(131.221793468239,3.24859213590686,134.497033389018));
#38363=CARTESIAN_POINT('Ctrl Pts',(131.214303132477,3.34755578724603,134.409971101245));
#38364=CARTESIAN_POINT('Ctrl Pts',(131.206812796715,3.4428906082135,134.319038999838));
#38365=CARTESIAN_POINT('Ctrl Pts',(131.199322460953,3.53429680756048,134.22458416853));
#38366=CARTESIAN_POINT('Ctrl Pts',(131.191548126834,3.62916870073795,134.126548053584));
#38367=CARTESIAN_POINT('Ctrl Pts',(131.183773792715,3.7201087097729,134.02440625798));
#38368=CARTESIAN_POINT('Ctrl Pts',(131.175999458596,3.80674056739808,133.918507260713));
#38369=CARTESIAN_POINT('Ctrl Pts',(131.168234705649,3.89326565900124,133.812738774496));
#38370=CARTESIAN_POINT('Ctrl Pts',(131.160469952702,3.97549291816558,133.703222599466));
#38371=CARTESIAN_POINT('Ctrl Pts',(131.152705199755,4.05308255310777,133.590344264358));
#38372=CARTESIAN_POINT('Ctrl Pts',(131.14494815887,4.13059512493071,133.477578041605));
#38373=CARTESIAN_POINT('Ctrl Pts',(131.137191117985,4.20347901895293,133.361456624327));
#38374=CARTESIAN_POINT('Ctrl Pts',(131.1294340771,4.27143465312082,133.242398571868));
#38375=CARTESIAN_POINT('Ctrl Pts',(131.121682885859,4.33933904141637,133.123430302013));
#38376=CARTESIAN_POINT('Ctrl Pts',(131.113931694619,4.40232237418207,133.001530143058));
#38377=CARTESIAN_POINT('Ctrl Pts',(131.106180503379,4.46012856035861,132.877145287418));
#38378=CARTESIAN_POINT('Ctrl Pts',(131.098432606602,4.51791017736398,132.75281329866));
#38379=CARTESIAN_POINT('Ctrl Pts',(131.090684709825,4.57051885983218,132.625999067452));
#38380=CARTESIAN_POINT('Ctrl Pts',(131.082936813048,4.61774474328205,132.49717382297));
#38381=CARTESIAN_POINT('Ctrl Pts',(131.075190536964,4.66496074809519,132.368375525953));
#38382=CARTESIAN_POINT('Ctrl Pts',(131.06744426088,4.70679605901602,132.237567419224));
#38383=CARTESIAN_POINT('Ctrl Pts',(131.059697984796,4.74308934636998,132.105239749097));
#38384=CARTESIAN_POINT('Ctrl Pts',(131.05195165153,4.77938290163272,131.972911102156));
#38385=CARTESIAN_POINT('Ctrl Pts',(131.044205318265,4.81013424828529,131.839063246475));
#38386=CARTESIAN_POINT('Ctrl Pts',(131.036458985,4.83523233984983,131.704200204476));
#38387=CARTESIAN_POINT('Ctrl Pts',(131.028710916997,4.86033605195797,131.569306960834));
#38388=CARTESIAN_POINT('Ctrl Pts',(131.020962848994,4.87978391825313,131.43339846278));
#38389=CARTESIAN_POINT('Ctrl Pts',(131.013214780991,4.89351634337174,131.296987108585));
#38390=CARTESIAN_POINT('Ctrl Pts',(131.005458478249,4.90726336347519,131.16043077478));
#38391=CARTESIAN_POINT('Ctrl Pts',(130.997702175507,4.91528276883339,131.023370906849));
#38392=CARTESIAN_POINT('Ctrl Pts',(130.989945872765,4.91756699070171,130.886323746234));
#38393=CARTESIAN_POINT('Ctrl Pts',(130.982185430251,4.91985243172801,130.749203439421));
#38394=CARTESIAN_POINT('Ctrl Pts',(130.974424987737,4.91639659972929,130.612096244088));
#38395=CARTESIAN_POINT('Ctrl Pts',(130.966664545223,4.90724403213303,130.475515560442));
#38396=CARTESIAN_POINT('Ctrl Pts',(130.958891644957,4.89807677202273,130.338715625358));
#38397=CARTESIAN_POINT('Ctrl Pts',(130.951118744692,4.88319454434876,130.202444279825));
#38398=CARTESIAN_POINT('Ctrl Pts',(130.943345844426,4.8626935852825,130.067207880236));
#38399=CARTESIAN_POINT('Ctrl Pts',(130.935855508664,4.84293788771695,129.936887664411));
#38400=CARTESIAN_POINT('Ctrl Pts',(130.928365172902,4.8179649348879,129.807528757558));
#38401=CARTESIAN_POINT('Ctrl Pts',(130.92087483714,4.78790469367565,129.679570989778));
#38402=CARTESIAN_POINT('Ctrl Pts',(130.913100503021,4.75670470928147,129.546761664343));
#38403=CARTESIAN_POINT('Ctrl Pts',(130.905326168902,4.71992522005083,129.415041123711));
#38404=CARTESIAN_POINT('Ctrl Pts',(130.897551834783,4.67765602958201,129.2849142936));
#38405=CARTESIAN_POINT('Ctrl Pts',(130.889787081836,4.63543893211273,129.154947833177));
#38406=CARTESIAN_POINT('Ctrl Pts',(130.882022328889,4.58774571449083,129.026571543559));
#38407=CARTESIAN_POINT('Ctrl Pts',(130.874257575941,4.53471706720284,128.900279688897));
#38408=CARTESIAN_POINT('Ctrl Pts',(130.866500535056,4.48174108871494,128.774113269086));
#38409=CARTESIAN_POINT('Ctrl Pts',(130.858743494171,4.42344037663695,128.650027522404));
#38410=CARTESIAN_POINT('Ctrl Pts',(130.850986453286,4.36000514538059,128.528500737267));
#38411=CARTESIAN_POINT('Ctrl Pts',(130.843235262046,4.29661775112552,128.407065596423));
#38412=CARTESIAN_POINT('Ctrl Pts',(130.835484070806,4.22810372481749,128.288185921294));
#38413=CARTESIAN_POINT('Ctrl Pts',(130.827732879566,4.15470087862873,128.172318886966));
#38414=CARTESIAN_POINT('Ctrl Pts',(130.819984982789,4.08132923060768,128.056501099217));
#38415=CARTESIAN_POINT('Ctrl Pts',(130.812237086012,4.00307310423874,127.943693735123));
#38416=CARTESIAN_POINT('Ctrl Pts',(130.804489189235,3.92021552109696,127.834328070497));
#38417=CARTESIAN_POINT('Ctrl Pts',(130.796742913151,3.83737526997536,127.72498528281));
#38418=CARTESIAN_POINT('Ctrl Pts',(130.788996637067,3.74993571254349,127.619083074042));
#38419=CARTESIAN_POINT('Ctrl Pts',(130.781250360982,3.65822210427816,127.517022165524));
#38420=CARTESIAN_POINT('Ctrl Pts',(130.773504027717,3.56650781900381,127.414960503617));
#38421=CARTESIAN_POINT('Ctrl Pts',(130.765757694452,3.47051968125969,127.316740489343));
#38422=CARTESIAN_POINT('Ctrl Pts',(130.758011361186,3.37062171605196,127.222727985682));
#38423=CARTESIAN_POINT('Ctrl Pts',(130.750263293183,3.27070137938763,127.128694428572));
#38424=CARTESIAN_POINT('Ctrl Pts',(130.74251522518,3.16686975761869,127.038870524918));
#38425=CARTESIAN_POINT('Ctrl Pts',(130.734767157177,3.05952573317417,126.953583377768));
#38426=CARTESIAN_POINT('Ctrl Pts',(130.727010854436,2.95206762222299,126.868205586424));
#38427=CARTESIAN_POINT('Ctrl Pts',(130.719254551694,2.84108995807692,126.787374427085));
#38428=CARTESIAN_POINT('Ctrl Pts',(130.711498248952,2.72702297818842,126.711375308659));
#38429=CARTESIAN_POINT('Ctrl Pts',(130.703737806438,2.61289511731818,126.635335627214));
#38430=CARTESIAN_POINT('Ctrl Pts',(130.695977363924,2.49567498919772,126.564133328442));
#38431=CARTESIAN_POINT('Ctrl Pts',(130.688216921409,2.37581860553092,126.498008447096));
#38432=CARTESIAN_POINT('Ctrl Pts',(130.680444021144,2.25576981775671,126.43177741622));
#38433=CARTESIAN_POINT('Ctrl Pts',(130.672671120879,2.13307666777857,126.370640264976));
#38434=CARTESIAN_POINT('Ctrl Pts',(130.664898220613,2.00821718557131,126.314789725145));
#38435=CARTESIAN_POINT('Ctrl Pts',(130.657407884851,1.88789666004443,126.260969493116));
#38436=CARTESIAN_POINT('Ctrl Pts',(130.649917549089,1.76556485707241,126.212058296681));
#38437=CARTESIAN_POINT('Ctrl Pts',(130.642427213327,1.64166206845087,126.168184529936));
#38438=CARTESIAN_POINT('Ctrl Pts',(130.634652879208,1.51306146793932,126.12264727599));
#38439=CARTESIAN_POINT('Ctrl Pts',(130.626878545089,1.3823610342681,126.082392732265));
#38440=CARTESIAN_POINT('Ctrl Pts',(130.61910421097,1.25003411678139,126.047618269132));
#38441=CARTESIAN_POINT('Ctrl Pts',(130.611339458023,1.11787028039417,126.012886662418));
#38442=CARTESIAN_POINT('Ctrl Pts',(130.603574705075,0.984084323037445,125.983621796842));
#38443=CARTESIAN_POINT('Ctrl Pts',(130.595809952128,0.849168129783613,125.95997246736));
#38444=CARTESIAN_POINT('Ctrl Pts',(130.588052911243,0.714385937194814,125.936346626725));
#38445=CARTESIAN_POINT('Ctrl Pts',(130.580295870358,0.578476125268148,125.918325289914));
#38446=CARTESIAN_POINT('Ctrl Pts',(130.572538829473,0.441943907128777,125.906006950725));
#38447=CARTESIAN_POINT('Ctrl Pts',(130.564787638233,0.305514648997078,125.893697900892));
#38448=CARTESIAN_POINT('Ctrl Pts',(130.557036446993,0.168464306696063,125.887083323438));
#38449=CARTESIAN_POINT('Ctrl Pts',(130.549285255753,0.031306057861031,125.886210254549));
#38450=CARTESIAN_POINT('Ctrl Pts',(130.541537358976,-0.105793895059336,
125.885337556738));
#38451=CARTESIAN_POINT('Ctrl Pts',(130.533789462199,-0.24300127315662,125.890201516415));
#38452=CARTESIAN_POINT('Ctrl Pts',(130.526041565422,-0.379800251800693,
125.900797134625));
#38453=CARTESIAN_POINT('Ctrl Pts',(130.518295289338,-0.516570615047478,
125.91139053646));
#38454=CARTESIAN_POINT('Ctrl Pts',(130.510549013253,-0.652932359211966,
125.927713181901));
#38455=CARTESIAN_POINT('Ctrl Pts',(130.502802737169,-0.788372537559546,
125.949708023969));
#38456=CARTESIAN_POINT('Ctrl Pts',(130.495056403904,-0.923813715695663,
125.971703028398));
#38457=CARTESIAN_POINT('Ctrl Pts',(130.487310070639,-1.05833292853073,125.999370250335));
#38458=CARTESIAN_POINT('Ctrl Pts',(130.479563737373,-1.19142560077159,126.032601183109));
#38459=CARTESIAN_POINT('Ctrl Pts',(130.47181566937,-1.32454807819361,126.065839557721));
#38460=CARTESIAN_POINT('Ctrl Pts',(130.464067601367,-1.45624300007764,126.104644027783));
#38461=CARTESIAN_POINT('Ctrl Pts',(130.456319533364,-1.58601955966783,126.148855809401));
#38462=CARTESIAN_POINT('Ctrl Pts',(130.448563230623,-1.7159340473301,126.193114579826));
#38463=CARTESIAN_POINT('Ctrl Pts',(130.440806927881,-1.84392572919052,126.242792015689));
#38464=CARTESIAN_POINT('Ctrl Pts',(130.433050625139,-1.96952192880009,126.297680416523));
#38465=CARTESIAN_POINT('Ctrl Pts',(130.425290182625,-2.09518516288311,126.352598112949));
#38466=CARTESIAN_POINT('Ctrl Pts',(130.41752974011,-2.21845001590423,126.412732144884));
#38467=CARTESIAN_POINT('Ctrl Pts',(130.409769297596,-2.33886805436165,126.477828601414));
#38468=CARTESIAN_POINT('Ctrl Pts',(130.401996397331,-2.45947939854453,126.543029556556));
#38469=CARTESIAN_POINT('Ctrl Pts',(130.394223497065,-2.57723445989045,126.613208654877));
#38470=CARTESIAN_POINT('Ctrl Pts',(130.3864505968,-2.69171270081496,126.688067892459));
#38471=CARTESIAN_POINT('Ctrl Pts',(130.378960261038,-2.80202936932844,126.760205808195));
#38472=CARTESIAN_POINT('Ctrl Pts',(130.371469925276,-2.90930307175307,126.836689322256));
#38473=CARTESIAN_POINT('Ctrl Pts',(130.363979589514,-3.01318779802863,126.917217404831));
#38474=CARTESIAN_POINT('Ctrl Pts',(130.356297479428,-3.11973227464586,126.999807239916));
#38475=CARTESIAN_POINT('Ctrl Pts',(130.348615369343,-3.22306642030545,127.086926619262));
#38476=CARTESIAN_POINT('Ctrl Pts',(130.340933259257,-3.32277383898975,127.178294280966));
#38477=CARTESIAN_POINT('Ctrl Pts',(130.33325992669,-3.42236733276733,127.269557546703));
#38478=CARTESIAN_POINT('Ctrl Pts',(130.325586594123,-3.51834204516812,127.365059177432));
#38479=CARTESIAN_POINT('Ctrl Pts',(130.317913261555,-3.61031183691572,127.464475664049));
#38480=CARTESIAN_POINT('Ctrl Pts',(130.310246939852,-3.70219759898305,127.563801317194));
#38481=CARTESIAN_POINT('Ctrl Pts',(130.302580618148,-3.79008544596941,127.667034421855));
#38482=CARTESIAN_POINT('Ctrl Pts',(130.294914296444,-3.87362394279327,127.773812711276));
#38483=CARTESIAN_POINT('Ctrl Pts',(130.287253225158,-3.95710522679259,127.880517871687));
#38484=CARTESIAN_POINT('Ctrl Pts',(130.279592153871,-4.03624283920432,127.990763073242));
#38485=CARTESIAN_POINT('Ctrl Pts',(130.271931082584,-4.11072408185366,128.104151258022));
#38486=CARTESIAN_POINT('Ctrl Pts',(130.264272468355,-4.18518143688101,128.217503076947));
#38487=CARTESIAN_POINT('Ctrl Pts',(130.256613854127,-4.25498516717711,128.333995543411));
#38488=CARTESIAN_POINT('Ctrl Pts',(130.248955239899,-4.3198647706816,128.453201025891));
#38489=CARTESIAN_POINT('Ctrl Pts',(130.241298355174,-4.3847297227764,128.572379588843));
#38490=CARTESIAN_POINT('Ctrl Pts',(130.233641470449,-4.44467257160386,128.694269595334));
#38491=CARTESIAN_POINT('Ctrl Pts',(130.225984585724,-4.49946819602265,128.818417764541));
#38492=CARTESIAN_POINT('Ctrl Pts',(130.21832467224,-4.55428549540717,128.942615041818));
#38493=CARTESIAN_POINT('Ctrl Pts',(130.210664758757,-4.60395133706325,129.069071900715));
#38494=CARTESIAN_POINT('Ctrl Pts',(130.203004845274,-4.64828828671816,129.197313926876));
#38495=CARTESIAN_POINT('Ctrl Pts',(130.195430780145,-4.69212833073771,129.324118682634));
#38496=CARTESIAN_POINT('Ctrl Pts',(130.187856715016,-4.73075824526441,129.452668417351));
#38497=CARTESIAN_POINT('Ctrl Pts',(130.180282649887,-4.76405452823405,129.582490119308));
#38498=CARTESIAN_POINT('Origin',(213.235140564004,0.,130.804360617566));
#38499=CARTESIAN_POINT('',(128.084583899672,-4.76405452823402,129.582490119308));
#38500=CARTESIAN_POINT('',(128.430147988268,-4.76405452823404,129.582490119308));
#38501=CARTESIAN_POINT('',(213.235140564004,-4.76405452823405,129.582490119308));
#38502=CARTESIAN_POINT('',(129.764859435955,-4.91824792667793,130.799844620641));
#38503=CARTESIAN_POINT('Ctrl Pts',(129.764859435955,-4.91824792667793,130.799844620641));
#38504=CARTESIAN_POINT('Ctrl Pts',(129.757206450161,-4.91837192626011,130.934889151915));
#38505=CARTESIAN_POINT('Ctrl Pts',(129.749553464366,-4.91292969583926,131.070099530846));
#38506=CARTESIAN_POINT('Ctrl Pts',(129.741900478572,-4.90190706987218,131.204972825115));
#38507=CARTESIAN_POINT('Ctrl Pts',(129.734253281609,-4.8908927815808,131.339744099249));
#38508=CARTESIAN_POINT('Ctrl Pts',(129.726606084645,-4.87430652785045,131.474178396558));
#38509=CARTESIAN_POINT('Ctrl Pts',(129.718958887681,-4.85218621156504,131.607773357568));
#38510=CARTESIAN_POINT('Ctrl Pts',(129.711314829052,-4.83007497323841,131.741313492529));
#38511=CARTESIAN_POINT('Ctrl Pts',(129.703670770422,-4.80243425226872,131.874014579584));
#38512=CARTESIAN_POINT('Ctrl Pts',(129.696026711792,-4.76935369971396,132.005380329946));
#38513=CARTESIAN_POINT('Ctrl Pts',(129.688384053555,-4.73627920752195,132.13672201408));
#38514=CARTESIAN_POINT('Ctrl Pts',(129.680741395318,-4.69776696330622,132.266728457751));
#38515=CARTESIAN_POINT('Ctrl Pts',(129.673098737082,-4.65395741868477,132.394915051582));
#38516=CARTESIAN_POINT('Ctrl Pts',(129.665455718965,-4.61014581114452,132.523107681508));
#38517=CARTESIAN_POINT('Ctrl Pts',(129.657812700848,-4.56103653761683,132.649479910392));
#38518=CARTESIAN_POINT('Ctrl Pts',(129.650169682731,-4.50681928080383,132.77356427201));
#38519=CARTESIAN_POINT('Ctrl Pts',(129.642524544391,-4.45258698377443,132.897683055429));
#38520=CARTESIAN_POINT('Ctrl Pts',(129.634879406052,-4.39324404718015,133.019512341041));
#38521=CARTESIAN_POINT('Ctrl Pts',(129.627234267712,-4.32902721326783,133.138607058987));
#38522=CARTESIAN_POINT('Ctrl Pts',(129.619581008545,-4.26474216687697,133.25782828186));
#38523=CARTESIAN_POINT('Ctrl Pts',(129.611927749378,-4.19557307996666,133.374308784386));
#38524=CARTESIAN_POINT('Ctrl Pts',(129.604274490211,-4.12180148796512,133.487630182166));
#38525=CARTESIAN_POINT('Ctrl Pts',(129.596616588164,-4.04798514213191,133.601020326826));
#38526=CARTESIAN_POINT('Ctrl Pts',(129.588958686117,-3.96956096589173,133.711247224781));
#38527=CARTESIAN_POINT('Ctrl Pts',(129.58130078407,-3.88685148376183,133.817924721029));
#38528=CARTESIAN_POINT('Ctrl Pts',(129.573631821169,-3.80402253843159,133.924756299187));
#38529=CARTESIAN_POINT('Ctrl Pts',(129.565962858267,-3.71689619156054,134.02802793669));
#38530=CARTESIAN_POINT('Ctrl Pts',(129.558293895366,-3.62583279854373,134.127389293263));
#38531=CARTESIAN_POINT('Ctrl Pts',(129.554937834989,-3.58598200658362,134.170871406311));
#38532=CARTESIAN_POINT('Ctrl Pts',(129.551581774612,-3.5453776831429,134.213605178592));
#38533=CARTESIAN_POINT('Ctrl Pts',(129.548225714235,-3.50405198933578,134.255563700338));
#38534=CARTESIAN_POINT('Ctrl Pts',(129.540451380116,-3.40832077021414,134.352760869197));
#38535=CARTESIAN_POINT('Ctrl Pts',(129.532677045997,-3.30839069839188,134.446125811215));
#38536=CARTESIAN_POINT('Ctrl Pts',(129.524902711878,-3.20460112313271,134.535274004944));
#38537=CARTESIAN_POINT('Ctrl Pts',(129.51713795893,-3.10093945924917,134.624312331492));
#38538=CARTESIAN_POINT('Ctrl Pts',(129.509373205983,-2.99342804966562,134.709143997468));
#38539=CARTESIAN_POINT('Ctrl Pts',(129.501608453036,-2.88244415803053,134.789420057315));
#38540=CARTESIAN_POINT('Ctrl Pts',(129.493851412151,-2.77157049716099,134.869616385848));
#38541=CARTESIAN_POINT('Ctrl Pts',(129.486094371266,-2.65723153247605,134.945265884942));
#38542=CARTESIAN_POINT('Ctrl Pts',(129.478337330381,-2.53983851364061,135.016059014546));
#38543=CARTESIAN_POINT('Ctrl Pts',(129.470586139141,-2.42253402179426,135.086798758501));
#38544=CARTESIAN_POINT('Ctrl Pts',(129.462834947901,-2.30218039339522,135.152689221322));
#38545=CARTESIAN_POINT('Ctrl Pts',(129.455083756661,-2.17921854660036,135.213463654313));
#38546=CARTESIAN_POINT('Ctrl Pts',(129.447335859884,-2.05630896187026,135.27421225655));
#38547=CARTESIAN_POINT('Ctrl Pts',(129.439587963107,-1.93079371334835,135.329848980901));
#38548=CARTESIAN_POINT('Ctrl Pts',(129.43184006633,-1.80313885834133,135.38015271512));
#38549=CARTESIAN_POINT('Ctrl Pts',(129.424093790246,-1.67551070597798,135.430445926883));
#38550=CARTESIAN_POINT('Ctrl Pts',(129.416347514162,-1.54574420086184,135.475408224152));
#38551=CARTESIAN_POINT('Ctrl Pts',(129.408601238078,-1.41432557665855,135.514866559151));
#38552=CARTESIAN_POINT('Ctrl Pts',(129.400854904812,-1.28290598235291,135.554325185423));
#38553=CARTESIAN_POINT('Ctrl Pts',(129.393108571547,-1.1498346190758,135.588279655925));
#38554=CARTESIAN_POINT('Ctrl Pts',(129.385362238282,-1.01561269929587,135.616606861009));
#38555=CARTESIAN_POINT('Ctrl Pts',(129.377614170279,-0.881360721447727,
135.644940409774));
#38556=CARTESIAN_POINT('Ctrl Pts',(129.369866102276,-0.745958056850334,
135.667644104776));
#38557=CARTESIAN_POINT('Ctrl Pts',(129.362118034273,-0.609915526094017,
135.684646071669));
#38558=CARTESIAN_POINT('Ctrl Pts',(129.354361731531,-0.4737284077169,135.701666108454));
#38559=CARTESIAN_POINT('Ctrl Pts',(129.346605428789,-0.336900453258914,
135.712972263337));
#38560=CARTESIAN_POINT('Ctrl Pts',(129.338849126047,-0.199947573865809,
135.71854458138));
#38561=CARTESIAN_POINT('Ctrl Pts',(129.331088683533,-0.0629215985974926,
135.724119873537));
#38562=CARTESIAN_POINT('Ctrl Pts',(129.323328241019,0.0742290436902866,
135.723955231374));
#38563=CARTESIAN_POINT('Ctrl Pts',(129.315567798505,0.210990031859213,135.718082859305));
#38564=CARTESIAN_POINT('Ctrl Pts',(129.307794898239,0.347970560907605,135.712201060382));
#38565=CARTESIAN_POINT('Ctrl Pts',(129.300021997974,0.484559796088881,135.700593254973));
#38566=CARTESIAN_POINT('Ctrl Pts',(129.292249097708,0.620249217426277,135.683343500379));
#38567=CARTESIAN_POINT('Ctrl Pts',(129.284758761946,0.751005986519056,135.666720817814));
#38568=CARTESIAN_POINT('Ctrl Pts',(129.277268426184,0.880926923214471,135.644859313661));
#38569=CARTESIAN_POINT('Ctrl Pts',(129.269778090422,1.00956920522302,135.617878362663));
#38570=CARTESIAN_POINT('Ctrl Pts',(129.262003756303,1.14308899845174,135.589874420708));
#38571=CARTESIAN_POINT('Ctrl Pts',(129.254229422184,1.27565421315145,135.556266452844));
#38572=CARTESIAN_POINT('Ctrl Pts',(129.246455088065,1.40675791397285,135.517132119981));
#38573=CARTESIAN_POINT('Ctrl Pts',(129.238690335118,1.53770004120033,135.478046016686));
#38574=CARTESIAN_POINT('Ctrl Pts',(129.230925582171,1.66718386733653,135.433447210511));
#38575=CARTESIAN_POINT('Ctrl Pts',(129.223160829223,1.79471189438333,135.38346449045));
#38576=CARTESIAN_POINT('Ctrl Pts',(129.215403788338,1.92211325879585,135.333531413931));
#38577=CARTESIAN_POINT('Ctrl Pts',(129.207646747453,2.04756232818574,135.278225206796));
#38578=CARTESIAN_POINT('Ctrl Pts',(129.199889706568,2.17057638725182,135.217724551076));
#38579=CARTESIAN_POINT('Ctrl Pts',(129.192138515328,2.29349768045864,135.157269519371));
#38580=CARTESIAN_POINT('Ctrl Pts',(129.184387324088,2.41398726889542,135.091628007826));
#38581=CARTESIAN_POINT('Ctrl Pts',(129.176636132848,2.53158240229536,135.021026789186));
#38582=CARTESIAN_POINT('Ctrl Pts',(129.168888236071,2.64912755462682,134.950455577949));
#38583=CARTESIAN_POINT('Ctrl Pts',(129.161140339294,2.7637803642438,134.874929053105));
#38584=CARTESIAN_POINT('Ctrl Pts',(129.153392442517,2.87510288779291,134.794719805296));
#38585=CARTESIAN_POINT('Ctrl Pts',(129.145646166433,2.98640212506993,134.714527335534));
#38586=CARTESIAN_POINT('Ctrl Pts',(129.137899890349,3.09437214489886,134.62965431954));
#38587=CARTESIAN_POINT('Ctrl Pts',(129.130153614265,3.19860453611217,134.54041630292));
#38588=CARTESIAN_POINT('Ctrl Pts',(129.122407280999,3.30283769674538,134.451177627564));
#38589=CARTESIAN_POINT('Ctrl Pts',(129.114660947734,3.40333287671913,134.357574141552));
#38590=CARTESIAN_POINT('Ctrl Pts',(129.106914614469,3.49971558281811,134.259960985357));
#38591=CARTESIAN_POINT('Ctrl Pts',(129.099166546466,3.59611987315585,134.162325969373));
#38592=CARTESIAN_POINT('Ctrl Pts',(129.091418478463,3.68840958237244,134.060679774562));
#38593=CARTESIAN_POINT('Ctrl Pts',(129.08367041046,3.77624812953736,133.955413318913));
#38594=CARTESIAN_POINT('Ctrl Pts',(129.075914107718,3.8641800325555,133.850034984823));
#38595=CARTESIAN_POINT('Ctrl Pts',(129.068157804976,3.94765107245801,133.74102900445));
#38596=CARTESIAN_POINT('Ctrl Pts',(129.060401502234,4.02636559801586,133.628818642323));
#38597=CARTESIAN_POINT('Ctrl Pts',(129.05264105972,4.10512213588609,133.516548390147));
#38598=CARTESIAN_POINT('Ctrl Pts',(129.044880617206,4.17911689001905,133.401070677372));
#38599=CARTESIAN_POINT('Ctrl Pts',(129.037120174691,4.24809895176071,133.282835624208));
#38600=CARTESIAN_POINT('Ctrl Pts',(129.029347274426,4.31719174963176,133.164410769641));
#38601=CARTESIAN_POINT('Ctrl Pts',(129.021574374161,4.38125559218418,133.043220075315));
#38602=CARTESIAN_POINT('Ctrl Pts',(129.013801473895,4.44008633173679,132.919736808513));
#38603=CARTESIAN_POINT('Ctrl Pts',(129.006311138133,4.496778425721,132.800742469494));
#38604=CARTESIAN_POINT('Ctrl Pts',(128.998820802371,4.54861116290541,132.679619628911));
#38605=CARTESIAN_POINT('Ctrl Pts',(128.991330466609,4.59544562037844,132.556805370659));
#38606=CARTESIAN_POINT('Ctrl Pts',(128.98355613249,4.64405582054163,132.429334572478));
#38607=CARTESIAN_POINT('Ctrl Pts',(128.975781798371,4.68743522198056,132.299637775358));
#38608=CARTESIAN_POINT('Ctrl Pts',(128.968007464252,4.72537515208118,132.168183455985));
#38609=CARTESIAN_POINT('Ctrl Pts',(128.960242711305,4.76326832460866,132.036891142313));
#38610=CARTESIAN_POINT('Ctrl Pts',(128.952477958358,4.79573525671448,131.903845988088));
#38611=CARTESIAN_POINT('Ctrl Pts',(128.944713205411,4.82261539240705,131.769536166064));
#38612=CARTESIAN_POINT('Ctrl Pts',(128.936956164526,4.84946883036996,131.635359742448));
#38613=CARTESIAN_POINT('Ctrl Pts',(128.929199123641,4.8707464382231,131.499921531583));
#38614=CARTESIAN_POINT('Ctrl Pts',(128.921442082756,4.88633762680884,131.363724237524));
#38615=CARTESIAN_POINT('Ctrl Pts',(128.913690891515,4.901917057958,131.227629650904));
#38616=CARTESIAN_POINT('Ctrl Pts',(128.905939700275,4.91181856090263,131.090777507335));
#38617=CARTESIAN_POINT('Ctrl Pts',(128.898188509035,4.9159827981546,130.953679707933));
#38618=CARTESIAN_POINT('Ctrl Pts',(128.890440612258,4.92014526549464,130.816640178753));
#38619=CARTESIAN_POINT('Ctrl Pts',(128.882692715481,4.91857530526971,130.67935559137));
#38620=CARTESIAN_POINT('Ctrl Pts',(128.874944818704,4.91126553662678,130.54234174183));
#38621=CARTESIAN_POINT('Ctrl Pts',(128.86719854262,4.90395729702987,130.405356552634));
#38622=CARTESIAN_POINT('Ctrl Pts',(128.859452266536,4.89091165797746,130.268642378798));
#38623=CARTESIAN_POINT('Ctrl Pts',(128.851705990451,4.87217334071108,130.132713388312));
#38624=CARTESIAN_POINT('Ctrl Pts',(128.843959657186,4.85343488512271,129.99678339443));
#38625=CARTESIAN_POINT('Ctrl Pts',(128.836213323921,4.82900372085949,129.861638982765));
#38626=CARTESIAN_POINT('Ctrl Pts',(128.828466990655,4.79897621492929,129.727787187166));
#38627=CARTESIAN_POINT('Ctrl Pts',(128.820718922652,4.76894198454746,129.593905416387));
#38628=CARTESIAN_POINT('Ctrl Pts',(128.812970854649,4.73330900421599,129.461317219101));
#38629=CARTESIAN_POINT('Ctrl Pts',(128.805222786647,4.69222423409643,129.3305170711));
#38630=CARTESIAN_POINT('Ctrl Pts',(128.797466483905,4.65109579859405,129.199577907145));
#38631=CARTESIAN_POINT('Ctrl Pts',(128.789710181163,4.60450411605752,129.070430962242));
#38632=CARTESIAN_POINT('Ctrl Pts',(128.781953878421,4.55264548421063,128.943553760959));
#38633=CARTESIAN_POINT('Ctrl Pts',(128.774193435907,4.50075917385051,128.816608841493));
#38634=CARTESIAN_POINT('Ctrl Pts',(128.766432993393,4.44360047562489,128.691936434745));
#38635=CARTESIAN_POINT('Ctrl Pts',(128.758672550878,4.38141246615946,128.569990938242));
#38636=CARTESIAN_POINT('Ctrl Pts',(128.750899650613,4.31912462698037,128.447849684002));
#38637=CARTESIAN_POINT('Ctrl Pts',(128.743126750347,4.25179153529079,128.328444428349));
#38638=CARTESIAN_POINT('Ctrl Pts',(128.735353850082,4.17970101745098,128.212202739037));
#38639=CARTESIAN_POINT('Ctrl Pts',(128.72786351432,4.11023117151975,128.100186727927));
#38640=CARTESIAN_POINT('Ctrl Pts',(128.720373178558,4.03634395589248,127.991108524229));
#38641=CARTESIAN_POINT('Ctrl Pts',(128.712882842796,3.9583320104045,127.885321262246));
#38642=CARTESIAN_POINT('Ctrl Pts',(128.705108508677,3.87736221829223,127.775523044072));
#38643=CARTESIAN_POINT('Ctrl Pts',(128.697334174558,3.79169225574934,127.668922438209));
#38644=CARTESIAN_POINT('Ctrl Pts',(128.689559840439,3.70160347283512,127.56594822993));
#38645=CARTESIAN_POINT('Ctrl Pts',(128.681795087492,3.61162571629437,127.463100928159));
#38646=CARTESIAN_POINT('Ctrl Pts',(128.674030334544,3.51724022986249,127.363871423));
#38647=CARTESIAN_POINT('Ctrl Pts',(128.666265581597,3.41877094266708,127.268658664053));
#38648=CARTESIAN_POINT('Ctrl Pts',(128.658508540712,3.32039945655615,127.173540471761));
#38649=CARTESIAN_POINT('Ctrl Pts',(128.650751499827,3.21795252072476,127.082431356426));
#38650=CARTESIAN_POINT('Ctrl Pts',(128.642994458942,3.11179329819212,126.995696083661));
#38651=CARTESIAN_POINT('Ctrl Pts',(128.635243267702,3.00571413115434,126.909026218639));
#38652=CARTESIAN_POINT('Ctrl Pts',(128.627492076462,2.89592855111529,126.826723877389));
#38653=CARTESIAN_POINT('Ctrl Pts',(128.619740885222,2.7828351616183,126.749115677274));
#38654=CARTESIAN_POINT('Ctrl Pts',(128.611992988445,2.66978983982918,126.671540462716));
#38655=CARTESIAN_POINT('Ctrl Pts',(128.604245091668,2.55343982651217,126.598655641873));
#38656=CARTESIAN_POINT('Ctrl Pts',(128.596497194891,2.43421508595795,126.530746224831));
#38657=CARTESIAN_POINT('Ctrl Pts',(128.588750918807,2.31501528464934,126.462851012974));
#38658=CARTESIAN_POINT('Ctrl Pts',(128.581004642722,2.19294229168991,126.399929328193));
#38659=CARTESIAN_POINT('Ctrl Pts',(128.573258366638,2.06845286409403,126.342221465599));
#38660=CARTESIAN_POINT('Ctrl Pts',(128.565512033373,1.94396251754531,126.284513177017));
#38661=CARTESIAN_POINT('Ctrl Pts',(128.557765700108,1.81705605547426,126.232018951848));
#38662=CARTESIAN_POINT('Ctrl Pts',(128.550019366842,1.68821214853949,126.184931777977));
#38663=CARTESIAN_POINT('Ctrl Pts',(128.542271298839,1.55933938790537,126.137834059261));
#38664=CARTESIAN_POINT('Ctrl Pts',(128.534523230836,1.42852868618266,126.096145935512));
#38665=CARTESIAN_POINT('Ctrl Pts',(128.526775162833,1.29627549541593,126.06001104123));
#38666=CARTESIAN_POINT('Ctrl Pts',(128.519018860092,1.16388174438403,126.023837742351));
#38667=CARTESIAN_POINT('Ctrl Pts',(128.51126255735,1.03004281952939,125.993229566104));
#38668=CARTESIAN_POINT('Ctrl Pts',(128.503506254608,0.895266579510176,125.968279475348));
#38669=CARTESIAN_POINT('Ctrl Pts',(128.495745812094,0.760418405353534,125.943316067978));
#38670=CARTESIAN_POINT('Ctrl Pts',(128.487985369579,0.624632306081089,125.924016818474));
#38671=CARTESIAN_POINT('Ctrl Pts',(128.480224927065,0.48842196805422,125.910422832549));
#38672=CARTESIAN_POINT('Ctrl Pts',(128.4724520268,0.351992973100564,125.89680702435));
#38673=CARTESIAN_POINT('Ctrl Pts',(128.464679126534,0.215138769027454,125.888914804045));
#38674=CARTESIAN_POINT('Ctrl Pts',(128.456906226269,0.0783746578725998,
125.886735125979));
#38675=CARTESIAN_POINT('Ctrl Pts',(128.449415890507,-0.0534177333533048,
125.884634684701));
#38676=CARTESIAN_POINT('Ctrl Pts',(128.441925554745,-0.185126160221312,
125.887838658321));
#38677=CARTESIAN_POINT('Ctrl Pts',(128.434435218983,-0.316295341861633,
125.896291718374));
#38678=CARTESIAN_POINT('Ctrl Pts',(128.426660884864,-0.452437842892243,
125.905065278768));
#38679=CARTESIAN_POINT('Ctrl Pts',(128.418886550745,-0.588430659050207,
125.919521613221));
#38680=CARTESIAN_POINT('Ctrl Pts',(128.411112216626,-0.723760964562665,
125.939655782874));
#38681=CARTESIAN_POINT('Ctrl Pts',(128.403347463679,-0.858924487568211,
125.959765138962));
#38682=CARTESIAN_POINT('Ctrl Pts',(128.395582710732,-0.993426741493978,
125.985538350479));
#38683=CARTESIAN_POINT('Ctrl Pts',(128.387817957784,-1.12675698713663,126.01691852868));
#38684=CARTESIAN_POINT('Ctrl Pts',(128.380060916899,-1.2599548073004,126.048267539645));
#38685=CARTESIAN_POINT('Ctrl Pts',(128.372303876014,-1.39198255759903,126.085212345906));
#38686=CARTESIAN_POINT('Ctrl Pts',(128.364546835129,-1.52233705190963,126.127644572852));
#38687=CARTESIAN_POINT('Ctrl Pts',(128.356795643889,-1.65259324488082,126.170044801326));
#38688=CARTESIAN_POINT('Ctrl Pts',(128.349044452649,-1.7811783231702,126.217924093309));
#38689=CARTESIAN_POINT('Ctrl Pts',(128.341293261409,-1.90760203938644,126.271123637016));
#38690=CARTESIAN_POINT('Ctrl Pts',(128.333545364632,-2.03397202215126,126.324300569498));
#38691=CARTESIAN_POINT('Ctrl Pts',(128.325797467855,-2.15818211033594,126.382793104929));
#38692=CARTESIAN_POINT('Ctrl Pts',(128.318049571078,-2.2797601106843,126.446393557086));
#38693=CARTESIAN_POINT('Ctrl Pts',(128.310303294994,-2.40131267953607,126.509980705399));
#38694=CARTESIAN_POINT('Ctrl Pts',(128.30255701891,-2.52023390947012,126.578673464091));
#38695=CARTESIAN_POINT('Ctrl Pts',(128.294810742826,-2.63607474508163,126.652217435926));
#38696=CARTESIAN_POINT('Ctrl Pts',(128.28706440956,-2.75191643580355,126.725761950645));
#38697=CARTESIAN_POINT('Ctrl Pts',(128.279318076295,-2.8646773567641,126.804157540416));
#38698=CARTESIAN_POINT('Ctrl Pts',(128.27157174303,-2.97393640860482,126.887105800724));
#38699=CARTESIAN_POINT('Ctrl Pts',(128.263823675027,-3.08321992825324,126.970072636719));
#38700=CARTESIAN_POINT('Ctrl Pts',(128.256075607024,-3.18899970694241,127.057593935656));
#38701=CARTESIAN_POINT('Ctrl Pts',(128.248327539021,-3.29088709696956,127.149330497649));
#38702=CARTESIAN_POINT('Ctrl Pts',(128.240571236279,-3.39288277412696,127.241164558352));
#38703=CARTESIAN_POINT('Ctrl Pts',(128.232814933537,-3.49097750775328,127.33722256944));
#38704=CARTESIAN_POINT('Ctrl Pts',(128.225058630795,-3.58481857555258,127.437127503736));
#38705=CARTESIAN_POINT('Ctrl Pts',(128.217298188281,-3.67870972915533,127.537085760304));
#38706=CARTESIAN_POINT('Ctrl Pts',(128.209537745767,-3.76834243776297,127.640894735516));
#38707=CARTESIAN_POINT('Ctrl Pts',(128.201777303253,-3.85340445794956,127.748144469131));
#38708=CARTESIAN_POINT('Ctrl Pts',(128.194004402987,-3.93860302724253,127.85556636954));
#38709=CARTESIAN_POINT('Ctrl Pts',(128.186231502722,-4.01921601585577,127.966439749486));
#38710=CARTESIAN_POINT('Ctrl Pts',(128.178458602456,-4.09497418347289,128.080325100325));
#38711=CARTESIAN_POINT('Ctrl Pts',(128.170968266694,-4.16797835087439,128.190070431802));
#38712=CARTESIAN_POINT('Ctrl Pts',(128.163477930932,-4.23647437900702,128.302612287507));
#38713=CARTESIAN_POINT('Ctrl Pts',(128.15598759517,-4.30026272684413,128.417537720362));
#38714=CARTESIAN_POINT('Ctrl Pts',(128.147837182824,-4.36967234401632,128.542590814985));
#38715=CARTESIAN_POINT('Ctrl Pts',(128.139686770478,-4.43371036204155,128.670830503645));
#38716=CARTESIAN_POINT('Ctrl Pts',(128.131536358132,-4.49208728454085,128.801778561678));
#38717=CARTESIAN_POINT('Ctrl Pts',(128.123403750017,-4.55033668512407,128.932440569221));
#38718=CARTESIAN_POINT('Ctrl Pts',(128.115271141902,-4.60294950846619,129.065798845733));
#38719=CARTESIAN_POINT('Ctrl Pts',(128.107138533787,-4.6496818656245,129.201350445738));
#38720=CARTESIAN_POINT('Ctrl Pts',(128.099620322415,-4.69288371846655,129.326661485713));
#38721=CARTESIAN_POINT('Ctrl Pts',(128.092102111043,-4.73106039665717,129.453846501046));
#38722=CARTESIAN_POINT('Ctrl Pts',(128.084583899671,-4.76405452823402,129.582490119308));
#38723=CARTESIAN_POINT('Ctrl Pts',(129.834833026848,-4.76405452823404,129.582490119308));
#38724=CARTESIAN_POINT('Ctrl Pts',(129.832113130581,-4.7759248683824,129.628772395389));
#38725=CARTESIAN_POINT('Ctrl Pts',(129.829393234315,-4.78711453292458,129.675203598535));
#38726=CARTESIAN_POINT('Ctrl Pts',(129.826673338048,-4.79762058815034,129.721762005588));
#38727=CARTESIAN_POINT('Ctrl Pts',(129.816060175579,-4.83861570710667,129.903435087876));
#38728=CARTESIAN_POINT('Ctrl Pts',(129.805447013111,-4.86930468188327,130.087512672684));
#38729=CARTESIAN_POINT('Ctrl Pts',(129.794833850643,-4.8894632274617,130.273011005917));
#38730=CARTESIAN_POINT('Ctrl Pts',(129.784842379092,-4.9084409388886,130.44764333862));
#38731=CARTESIAN_POINT('Ctrl Pts',(129.774850907542,-4.91808603712119,130.623535186195));
#38732=CARTESIAN_POINT('Ctrl Pts',(129.764859435991,-4.91824792667734,130.79984462));
#38733=CARTESIAN_POINT('',(130.110140564045,-4.91824934646016,130.806896074964));
#38734=CARTESIAN_POINT('Ctrl Pts',(130.180282649887,-4.76405452823405,129.582490119308));
#38735=CARTESIAN_POINT('Ctrl Pts',(130.172615528694,-4.79775989417285,129.713906829553));
#38736=CARTESIAN_POINT('Ctrl Pts',(130.164948407501,-4.82599960023451,129.846626582253));
#38737=CARTESIAN_POINT('Ctrl Pts',(130.157281286307,-4.84869666132585,129.980149631867));
#38738=CARTESIAN_POINT('Ctrl Pts',(130.149424499264,-4.8719551922682,130.116975715581));
#38739=CARTESIAN_POINT('Ctrl Pts',(130.14156771222,-4.88939322364667,130.254644908175));
#38740=CARTESIAN_POINT('Ctrl Pts',(130.133710925176,-4.90098454109159,130.392616048104));
#38741=CARTESIAN_POINT('Ctrl Pts',(130.125854138133,-4.91257585853652,130.530587188034));
#38742=CARTESIAN_POINT('Ctrl Pts',(130.117997351089,-4.91832050694874,130.668859826868));
#38743=CARTESIAN_POINT('Ctrl Pts',(130.110140564045,-4.91824934646016,130.806896074964));
#38744=CARTESIAN_POINT('Ctrl Pts',(130.110140564008,-4.91824934645982,130.806896075623));
#38745=CARTESIAN_POINT('Ctrl Pts',(130.101937697906,-4.91817505144483,130.951012602406));
#38746=CARTESIAN_POINT('Ctrl Pts',(130.093734831804,-4.91176691442507,131.094961645225));
#38747=CARTESIAN_POINT('Ctrl Pts',(130.085531965701,-4.89906528052872,131.238344994725));
#38748=CARTESIAN_POINT('Ctrl Pts',(130.077757631582,-4.88702720206481,131.374237748821));
#38749=CARTESIAN_POINT('Ctrl Pts',(130.069983297463,-4.86931157806441,131.509844490242));
#38750=CARTESIAN_POINT('Ctrl Pts',(130.062208963344,-4.84593565236954,131.644652659414));
#38751=CARTESIAN_POINT('Ctrl Pts',(130.054444210397,-4.82258853541397,131.779294689566));
#38752=CARTESIAN_POINT('Ctrl Pts',(130.04667945745,-4.79359506271441,131.913139724154));
#38753=CARTESIAN_POINT('Ctrl Pts',(130.038914704503,-4.75902436296635,132.045678536229));
#38754=CARTESIAN_POINT('Ctrl Pts',(130.031157663618,-4.72448799932461,132.178085708886));
#38755=CARTESIAN_POINT('Ctrl Pts',(130.023400622733,-4.68438553028882,132.309188864972));
#38756=CARTESIAN_POINT('Ctrl Pts',(130.015643581848,-4.63883737433938,132.43848756396));
#38757=CARTESIAN_POINT('Ctrl Pts',(130.007892390607,-4.59332356660868,132.567688757794));
#38758=CARTESIAN_POINT('Ctrl Pts',(130.000141199367,-4.5423723753476,132.695087835769));
#38759=CARTESIAN_POINT('Ctrl Pts',(129.992390008127,-4.48615433119391,132.820198502717));
#38760=CARTESIAN_POINT('Ctrl Pts',(129.98464211135,-4.42996018120862,132.945255994295));
#38761=CARTESIAN_POINT('Ctrl Pts',(129.976894214573,-4.36850379055091,133.068026653475));
#38762=CARTESIAN_POINT('Ctrl Pts',(129.969146317796,-4.3020041169719,133.188043406877));
#38763=CARTESIAN_POINT('Ctrl Pts',(129.961400041712,-4.23551835369103,133.308035055362));
#38764=CARTESIAN_POINT('Ctrl Pts',(129.953653765628,-4.16399159519987,133.425273602118));
#38765=CARTESIAN_POINT('Ctrl Pts',(129.945907489543,-4.08768894156549,133.53931622589));
#38766=CARTESIAN_POINT('Ctrl Pts',(129.938161156278,-4.01138572468225,133.653359691499));
#38767=CARTESIAN_POINT('Ctrl Pts',(129.930414823013,-3.93030675971699,133.764206862106));
#38768=CARTESIAN_POINT('Ctrl Pts',(129.922668489747,-3.84476047047476,133.871443920506));
#38769=CARTESIAN_POINT('Ctrl Pts',(129.914920421744,-3.75919502373425,133.978704993902));
#38770=CARTESIAN_POINT('Ctrl Pts',(129.907172353741,-3.66916050574849,134.082354040776));
#38771=CARTESIAN_POINT('Ctrl Pts',(129.899424285738,-3.57500534519222,134.18201066521));
#38772=CARTESIAN_POINT('Ctrl Pts',(129.891667982997,-3.48075011541079,134.28177320589));
#38773=CARTESIAN_POINT('Ctrl Pts',(129.883911680255,-3.38236576352666,134.377534563251));
#38774=CARTESIAN_POINT('Ctrl Pts',(129.876155377513,-3.28023767250429,134.468951164187));
#38775=CARTESIAN_POINT('Ctrl Pts',(129.868394934999,-3.17805507264471,134.560416556915));
#38776=CARTESIAN_POINT('Ctrl Pts',(129.860634492485,-3.07212505399012,134.647532324345));
#38777=CARTESIAN_POINT('Ctrl Pts',(129.85287404997,-2.96286495170588,134.729996150885));
#38778=CARTESIAN_POINT('Ctrl Pts',(129.845101149705,-2.8534294554058,134.812592355679));
#38779=CARTESIAN_POINT('Ctrl Pts',(129.837328249439,-2.74065351480153,134.890521474336));
#38780=CARTESIAN_POINT('Ctrl Pts',(129.829555349174,-2.62498297299513,134.963524891069));
#38781=CARTESIAN_POINT('Ctrl Pts',(129.822065013412,-2.51351734674053,135.033874449719));
#38782=CARTESIAN_POINT('Ctrl Pts',(129.81457467765,-2.39936418450045,135.099650058462));
#38783=CARTESIAN_POINT('Ctrl Pts',(129.807084341888,-2.2829411028674,135.160662143326));
#38784=CARTESIAN_POINT('Ctrl Pts',(129.799310007769,-2.16210380470743,135.223987519932));
#38785=CARTESIAN_POINT('Ctrl Pts',(129.79153567365,-2.03843828506735,135.282381619845));
#38786=CARTESIAN_POINT('Ctrl Pts',(129.783761339531,-1.9123850955499,135.335581899827));
#38787=CARTESIAN_POINT('Ctrl Pts',(129.775996586584,-1.78648725532292,135.38871661522));
#38788=CARTESIAN_POINT('Ctrl Pts',(129.768231833637,-1.65820795683645,135.436670096041));
#38789=CARTESIAN_POINT('Ctrl Pts',(129.760467080689,-1.52801299289409,135.479225252617));
#38790=CARTESIAN_POINT('Ctrl Pts',(129.752710039804,-1.39794734042551,135.521738142811));
#38791=CARTESIAN_POINT('Ctrl Pts',(129.74495299892,-1.26597017810524,135.558863258087));
#38792=CARTESIAN_POINT('Ctrl Pts',(129.737195958035,-1.13256762985092,135.590431409595));
#38793=CARTESIAN_POINT('Ctrl Pts',(129.729444766794,-0.999265681495784,
135.621975755315));
#38794=CARTESIAN_POINT('Ctrl Pts',(129.721693575554,-0.864540865637652,
135.647971388635));
#38795=CARTESIAN_POINT('Ctrl Pts',(129.713942384314,-0.728894492148465,
135.668298927394));
#38796=CARTESIAN_POINT('Ctrl Pts',(129.706194487537,-0.593305771986403,
135.688617826407));
#38797=CARTESIAN_POINT('Ctrl Pts',(129.69844659076,-0.456796659066359,135.703273364538));
#38798=CARTESIAN_POINT('Ctrl Pts',(129.690698693983,-0.319878467463521,
135.712197292574));
#38799=CARTESIAN_POINT('Ctrl Pts',(129.682952417899,-0.182988916194844,
135.721119353916));
#38800=CARTESIAN_POINT('Ctrl Pts',(129.675206141815,-0.0456908463379253,
135.724312164487));
#38801=CARTESIAN_POINT('Ctrl Pts',(129.667459865731,0.0914998909817206,
135.721759404776));
#38802=CARTESIAN_POINT('Ctrl Pts',(129.659713532465,0.228691641012224,135.71920662622));
#38803=CARTESIAN_POINT('Ctrl Pts',(129.6519671992,0.365775666026927,135.710908200026));
#38804=CARTESIAN_POINT('Ctrl Pts',(129.644220865934,0.502237099289631,135.696899933565));
#38805=CARTESIAN_POINT('Ctrl Pts',(129.636472797931,0.638729092144156,135.682888530051));
#38806=CARTESIAN_POINT('Ctrl Pts',(129.628724729928,0.774597826959905,135.663164781763));
#38807=CARTESIAN_POINT('Ctrl Pts',(129.620976661925,0.909334931666526,135.637816218329));
#38808=CARTESIAN_POINT('Ctrl Pts',(129.613220359184,1.04421523657142,135.612440714141));
#38809=CARTESIAN_POINT('Ctrl Pts',(129.605464056442,1.17796112398719,135.581428525266));
#38810=CARTESIAN_POINT('Ctrl Pts',(129.5977077537,1.3100752272218,135.544918175651));
#38811=CARTESIAN_POINT('Ctrl Pts',(129.589947311186,1.44225984373128,135.508388339364));
#38812=CARTESIAN_POINT('Ctrl Pts',(129.582186868672,1.5728105686842,135.466354614792));
#38813=CARTESIAN_POINT('Ctrl Pts',(129.574426426157,1.70124747556007,135.419004708869));
#38814=CARTESIAN_POINT('Ctrl Pts',(129.566653525892,1.82989056076095,135.371578792674));
#38815=CARTESIAN_POINT('Ctrl Pts',(129.558880625626,1.95641268595657,135.318819792021));
#38816=CARTESIAN_POINT('Ctrl Pts',(129.551107725361,2.08035528127459,135.260963019191));
#38817=CARTESIAN_POINT('Ctrl Pts',(129.543617389599,2.19979225106051,135.205209485786));
#38818=CARTESIAN_POINT('Ctrl Pts',(129.536127053837,2.31683370609582,135.144722520591));
#38819=CARTESIAN_POINT('Ctrl Pts',(129.528636718075,2.43109442045933,135.079751006912));
#38820=CARTESIAN_POINT('Ctrl Pts',(129.520862383956,2.54968736453638,135.012316078544));
#38821=CARTESIAN_POINT('Ctrl Pts',(129.513088049837,2.66566020866326,134.939836211839));
#38822=CARTESIAN_POINT('Ctrl Pts',(129.505313715718,2.77855393887726,134.862540144306));
#38823=CARTESIAN_POINT('Ctrl Pts',(129.497548962771,2.8913085376583,134.785339337268));
#38824=CARTESIAN_POINT('Ctrl Pts',(129.489784209823,3.00099125341456,134.703334358105));
#38825=CARTESIAN_POINT('Ctrl Pts',(129.482019456876,3.1071676700656,134.616799749224));
#38826=CARTESIAN_POINT('Ctrl Pts',(129.474262415991,3.21323863080279,134.530351087736));
#38827=CARTESIAN_POINT('Ctrl Pts',(129.466505375106,3.31580992167811,134.439381994927));
#38828=CARTESIAN_POINT('Ctrl Pts',(129.458748334221,3.41447643746844,134.344210009909));
#38829=CARTESIAN_POINT('Ctrl Pts',(129.450997142981,3.51306854807163,134.249109794826));
#38830=CARTESIAN_POINT('Ctrl Pts',(129.443245951741,3.60776146442614,134.149813266428));
#38831=CARTESIAN_POINT('Ctrl Pts',(129.435494760501,3.6981837767078,134.046677661933));
#38832=CARTESIAN_POINT('Ctrl Pts',(129.427746863724,3.7885676570947,133.943585892822));
#38833=CARTESIAN_POINT('Ctrl Pts',(129.419998966947,3.87468428634427,133.836658586325));
#38834=CARTESIAN_POINT('Ctrl Pts',(129.41225107017,3.95619986671324,133.726289035087));
#38835=CARTESIAN_POINT('Ctrl Pts',(129.404504794086,4.03769839578008,133.61594257078));
#38836=CARTESIAN_POINT('Ctrl Pts',(129.396758518002,4.11459755818775,133.502155608229));
#38837=CARTESIAN_POINT('Ctrl Pts',(129.389012241917,4.18660479373594,133.385353326499));
#38838=CARTESIAN_POINT('Ctrl Pts',(129.381265908652,4.25861256082518,133.268550182562));
#38839=CARTESIAN_POINT('Ctrl Pts',(129.373519575387,4.32572812382767,133.148732007838));
#38840=CARTESIAN_POINT('Ctrl Pts',(129.365773242121,4.38770331045398,133.026351329052));
#38841=CARTESIAN_POINT('Ctrl Pts',(129.358025174118,4.44969237599364,132.903943243962));
#38842=CARTESIAN_POINT('Ctrl Pts',(129.350277106115,4.50653859790028,132.778971861631));
#38843=CARTESIAN_POINT('Ctrl Pts',(129.342529038112,4.55804082980524,132.651912201779));
#38844=CARTESIAN_POINT('Ctrl Pts',(129.334772735371,4.60959779889515,132.524717501409));
#38845=CARTESIAN_POINT('Ctrl Pts',(129.327016432629,4.65579928515726,132.395430452844));
#38846=CARTESIAN_POINT('Ctrl Pts',(129.319260129887,4.6964929938642,132.264544380345));
#38847=CARTESIAN_POINT('Ctrl Pts',(129.311499687373,4.7372084220288,132.133588450009));
#38848=CARTESIAN_POINT('Ctrl Pts',(129.303739244859,4.7724101148057,132.001032172856));
#38849=CARTESIAN_POINT('Ctrl Pts',(129.295978802344,4.80199658334589,131.867380784841));
#38850=CARTESIAN_POINT('Ctrl Pts',(129.288205902079,4.83163054671193,131.733514847754));
#38851=CARTESIAN_POINT('Ctrl Pts',(129.280433001814,4.85563120439344,131.598550671972));
#38852=CARTESIAN_POINT('Ctrl Pts',(129.272660101548,4.8739486630581,131.463001257349));
#38853=CARTESIAN_POINT('Ctrl Pts',(129.265169765786,4.89160023596136,131.332379405377));
#38854=CARTESIAN_POINT('Ctrl Pts',(129.257679430024,4.90397460440636,131.201214432306));
#38855=CARTESIAN_POINT('Ctrl Pts',(129.250189094262,4.91107293694543,131.06996496712));
#38856=CARTESIAN_POINT('Ctrl Pts',(129.242414760143,4.91844040492024,130.933739138569));
#38857=CARTESIAN_POINT('Ctrl Pts',(129.234640426024,4.9201471953698,130.79699076191));
#38858=CARTESIAN_POINT('Ctrl Pts',(129.226866091905,4.91613764337911,130.660229656802));
#38859=CARTESIAN_POINT('Ctrl Pts',(129.219101338958,4.91213303280291,130.523637097532));
#38860=CARTESIAN_POINT('Ctrl Pts',(129.211336586011,4.9024261083476,130.387032228071));
#38861=CARTESIAN_POINT('Ctrl Pts',(129.203571833064,4.88701303781143,130.250928931844));
#38862=CARTESIAN_POINT('Ctrl Pts',(129.195814792179,4.87161527575421,130.11496081533));
#38863=CARTESIAN_POINT('Ctrl Pts',(129.188057751294,4.85052268975622,129.97949366664));
#38864=CARTESIAN_POINT('Ctrl Pts',(129.180300710409,4.82378346519847,129.845039949917));
#38865=CARTESIAN_POINT('Ctrl Pts',(129.172549519169,4.79706440489794,129.710687625789));
#38866=CARTESIAN_POINT('Ctrl Pts',(129.164798327929,4.76470725762534,129.577347594365));
#38867=CARTESIAN_POINT('Ctrl Pts',(129.157047136688,4.72681182108834,129.445525428693));
#38868=CARTESIAN_POINT('Ctrl Pts',(129.149299239911,4.68893249112276,129.313759290958));
#38869=CARTESIAN_POINT('Ctrl Pts',(129.141551343134,4.64551966145292,129.183510110814));
#38870=CARTESIAN_POINT('Ctrl Pts',(129.133803446357,4.59672379448664,129.055271306038));
#38871=CARTESIAN_POINT('Ctrl Pts',(129.126057170273,4.54793813456381,128.927059326056));
#38872=CARTESIAN_POINT('Ctrl Pts',(129.118310894189,4.49377181600263,128.800857250165));
#38873=CARTESIAN_POINT('Ctrl Pts',(129.110564618105,4.43442441805971,128.677141037218));
#38874=CARTESIAN_POINT('Ctrl Pts',(129.10281828484,4.37507658202782,128.553423911027));
#38875=CARTESIAN_POINT('Ctrl Pts',(129.095071951574,4.3105477593965,128.432193036901));
#38876=CARTESIAN_POINT('Ctrl Pts',(129.087325618309,4.24108453053319,128.313901810966));
#38877=CARTESIAN_POINT('Ctrl Pts',(129.079577550306,4.17160574586141,128.195584094531));
#38878=CARTESIAN_POINT('Ctrl Pts',(129.071829482303,4.09719055401924,128.080207673327));
#38879=CARTESIAN_POINT('Ctrl Pts',(129.0640814143,4.01812987802596,127.968198537251));
#38880=CARTESIAN_POINT('Ctrl Pts',(129.056325111558,3.93898517540535,127.856070356533));
#38881=CARTESIAN_POINT('Ctrl Pts',(129.048568808816,3.85518535170712,127.747316929886));
#38882=CARTESIAN_POINT('Ctrl Pts',(129.040812506075,3.76706313558302,127.642333040989));
#38883=CARTESIAN_POINT('Ctrl Pts',(129.03305206356,3.67889388597881,127.53729311903));
#38884=CARTESIAN_POINT('Ctrl Pts',(129.025291621046,3.58639791061611,127.436027032265));
#38885=CARTESIAN_POINT('Ctrl Pts',(129.017531178532,3.48994542161163,127.338893258512));
#38886=CARTESIAN_POINT('Ctrl Pts',(129.009758278267,3.39333809850922,127.241603557001));
#38887=CARTESIAN_POINT('Ctrl Pts',(129.001985378001,3.29276185676482,127.148459690266));
#38888=CARTESIAN_POINT('Ctrl Pts',(128.994212477736,3.18862132912109,127.059780923932));
#38889=CARTESIAN_POINT('Ctrl Pts',(128.986722141974,3.08826657197116,126.974325854123));
#38890=CARTESIAN_POINT('Ctrl Pts',(128.979231806212,2.98460241374662,126.893017075662));
#38891=CARTESIAN_POINT('Ctrl Pts',(128.97174147045,2.87801534363086,126.816101505582));
#38892=CARTESIAN_POINT('Ctrl Pts',(128.963967136331,2.76738699235537,126.736269658284));
#38893=CARTESIAN_POINT('Ctrl Pts',(128.956192802212,2.65325927208579,126.660917849291));
#38894=CARTESIAN_POINT('Ctrl Pts',(128.948418468093,2.53603102029232,126.59036848105));
#38895=CARTESIAN_POINT('Ctrl Pts',(128.940653715146,2.4189472418422,126.519906058601));
#38896=CARTESIAN_POINT('Ctrl Pts',(128.932888962198,2.29877086654001,126.454234500356));
#38897=CARTESIAN_POINT('Ctrl Pts',(128.925124209251,2.1759321676689,126.393634797));
#38898=CARTESIAN_POINT('Ctrl Pts',(128.917367168366,2.0532154739253,126.333095282125));
#38899=CARTESIAN_POINT('Ctrl Pts',(128.909610127481,1.927842067156,126.277617769262));
#38900=CARTESIAN_POINT('Ctrl Pts',(128.901853086596,1.80026914333493,126.227438718073));
#38901=CARTESIAN_POINT('Ctrl Pts',(128.894101895356,1.67279242324808,126.177297507298));
#38902=CARTESIAN_POINT('Ctrl Pts',(128.886350704116,1.54311984995728,126.132446947704));
#38903=CARTESIAN_POINT('Ctrl Pts',(128.878599512876,1.41173071948402,126.093076351236));
#38904=CARTESIAN_POINT('Ctrl Pts',(128.870851616099,1.28039743289614,126.053722488322));
#38905=CARTESIAN_POINT('Ctrl Pts',(128.863103719322,1.14734941393881,126.019844068058));
#38906=CARTESIAN_POINT('Ctrl Pts',(128.855355822545,1.01308311756862,125.991581206519));
#38907=CARTESIAN_POINT('Ctrl Pts',(128.847609546461,0.87884490681319,125.963324256962));
#38908=CARTESIAN_POINT('Ctrl Pts',(128.839863270377,0.743389307869076,125.940680610161));
#38909=CARTESIAN_POINT('Ctrl Pts',(128.832116994292,0.607224635862987,125.923739621822));
#38910=CARTESIAN_POINT('Ctrl Pts',(128.824370661027,0.471058958720221,125.906798508428));
#38911=CARTESIAN_POINT('Ctrl Pts',(128.816624327762,0.334184586044954,125.895560185765));
#38912=CARTESIAN_POINT('Ctrl Pts',(128.808877994496,0.197116255549933,125.890062270467));
#38913=CARTESIAN_POINT('Ctrl Pts',(128.801129926493,0.060017229552756,125.884563123949));
#38914=CARTESIAN_POINT('Ctrl Pts',(128.79338185849,-0.0772754501194973,
125.884806958507));
#38915=CARTESIAN_POINT('Ctrl Pts',(128.785633790487,-0.214246135101939,
125.890779270311));
#38916=CARTESIAN_POINT('Ctrl Pts',(128.777877487746,-0.351362394158446,
125.896757929559));
#38917=CARTESIAN_POINT('Ctrl Pts',(128.770121185004,-0.488155583687352,
125.908477211017));
#38918=CARTESIAN_POINT('Ctrl Pts',(128.762364882262,-0.624113713034071,
125.925870570871));
#38919=CARTESIAN_POINT('Ctrl Pts',(128.754604439748,-0.760144407328043,
125.943273214084));
#38920=CARTESIAN_POINT('Ctrl Pts',(128.746843997234,-0.895338768151558,
125.966355904321));
#38921=CARTESIAN_POINT('Ctrl Pts',(128.739083554719,-1.02919508927156,125.995000937659));
#38922=CARTESIAN_POINT('Ctrl Pts',(128.731310654454,-1.16326628844153,126.023691954547));
#38923=CARTESIAN_POINT('Ctrl Pts',(128.723537754188,-1.29599477687142,126.057963060058));
#38924=CARTESIAN_POINT('Ctrl Pts',(128.715764853923,-1.42689323346668,126.097646396075));
#38925=CARTESIAN_POINT('Ctrl Pts',(128.708274518161,-1.55303320145113,126.135887142871));
#38926=CARTESIAN_POINT('Ctrl Pts',(128.700784182399,-1.67747358921217,126.179153354272));
#38927=CARTESIAN_POINT('Ctrl Pts',(128.693293846637,-1.79979775161385,126.227253330667));
#38928=CARTESIAN_POINT('Ctrl Pts',(128.685519220637,-1.92676463849925,126.27717890663));
#38929=CARTESIAN_POINT('Ctrl Pts',(128.677744594637,-2.05185369561391,126.332470574193));
#38930=CARTESIAN_POINT('Ctrl Pts',(128.669969968637,-2.1745780406785,126.392967027384));
#38931=CARTESIAN_POINT('Ctrl Pts',(128.662204991085,-2.29715008266293,126.453388403408));
#38932=CARTESIAN_POINT('Ctrl Pts',(128.654440013534,-2.41736290449301,126.519001541467));
#38933=CARTESIAN_POINT('Ctrl Pts',(128.646675035982,-2.53474748781889,126.589596302032));
#38934=CARTESIAN_POINT('Ctrl Pts',(128.638917837483,-2.65201447377654,126.660120339869));
#38935=CARTESIAN_POINT('Ctrl Pts',(128.631160638985,-2.76645852706476,126.735615867966));
#38936=CARTESIAN_POINT('Ctrl Pts',(128.623403440486,-2.87763355655261,126.815826027431));
#38937=CARTESIAN_POINT('Ctrl Pts',(128.615351129977,-2.99303808802988,126.899087672743));
#38938=CARTESIAN_POINT('Ctrl Pts',(128.607298819468,-3.10491955705152,126.987429589041));
#38939=CARTESIAN_POINT('Ctrl Pts',(128.599246508959,-3.21280959593889,127.080513472107));
#38940=CARTESIAN_POINT('Ctrl Pts',(128.591498952426,-3.31661634490334,127.170074430484));
#38941=CARTESIAN_POINT('Ctrl Pts',(128.583751395894,-3.41672795085056,127.264024689781));
#38942=CARTESIAN_POINT('Ctrl Pts',(128.576003839361,-3.51275955805842,127.362020810143));
#38943=CARTESIAN_POINT('Ctrl Pts',(128.56825793343,-3.60877070591622,127.459996052619));
#38944=CARTESIAN_POINT('Ctrl Pts',(128.560512027499,-3.70070331117244,127.56201516205));
#38945=CARTESIAN_POINT('Ctrl Pts',(128.552766121569,-3.78820897605295,127.667697451676));
#38946=CARTESIAN_POINT('Ctrl Pts',(128.54502018846,-3.87571494796172,127.773380112106));
#38947=CARTESIAN_POINT('Ctrl Pts',(128.537274255352,-3.95879369977514,127.882725676861));
#38948=CARTESIAN_POINT('Ctrl Pts',(128.529528322243,-4.03713703291781,127.995320276107));
#38949=CARTESIAN_POINT('Ctrl Pts',(128.521780684535,-4.11549760659178,128.107939653348));
#38950=CARTESIAN_POINT('Ctrl Pts',(128.514033046827,-4.18912046547083,128.223809166609));
#38951=CARTESIAN_POINT('Ctrl Pts',(128.506285409119,-4.25774088705439,128.342486209477));
#38952=CARTESIAN_POINT('Ctrl Pts',(128.498530775566,-4.32642327047889,128.461270413564));
#38953=CARTESIAN_POINT('Ctrl Pts',(128.490776142012,-4.39009400275787,128.582866869874));
#38954=CARTESIAN_POINT('Ctrl Pts',(128.483021508458,-4.44853431613953,128.706808353466));
#38955=CARTESIAN_POINT('Ctrl Pts',(128.475262715865,-4.50700597278432,128.83081631053));
#38956=CARTESIAN_POINT('Ctrl Pts',(128.467503923273,-4.56024146973399,128.957171441148));
#38957=CARTESIAN_POINT('Ctrl Pts',(128.45974513068,-4.6080706728571,129.085387745048));
#38958=CARTESIAN_POINT('Ctrl Pts',(128.451976857346,-4.65595832016514,129.213760720957));
#38959=CARTESIAN_POINT('Ctrl Pts',(128.444208584013,-4.6984263645923,129.343999039703));
#38960=CARTESIAN_POINT('Ctrl Pts',(128.436440310679,-4.73535478389164,129.475602500686));
#38961=CARTESIAN_POINT('Ctrl Pts',(128.434342869875,-4.74532549039541,129.511135553799));
#38962=CARTESIAN_POINT('Ctrl Pts',(128.432245429071,-4.75489264477029,129.546768074734));
#38963=CARTESIAN_POINT('Ctrl Pts',(128.430147988268,-4.76405452823404,129.582490119308));
#38964=CARTESIAN_POINT('Origin',(213.235140564004,0.,130.804360617566));
#38965=CARTESIAN_POINT('',(126.334922597491,-4.76405452823406,129.582490119308));
#38966=CARTESIAN_POINT('',(126.679856726692,-4.76405452823408,129.582490119308));
#38967=CARTESIAN_POINT('',(213.235140564004,-4.76405452823405,129.582490119308));
#38968=CARTESIAN_POINT('',(128.014859435962,-4.91824999645718,130.804547296181));
#38969=CARTESIAN_POINT('Ctrl Pts',(128.014859435962,-4.91824999645718,130.804547296181));
#38970=CARTESIAN_POINT('Ctrl Pts',(128.006721423039,-4.91824451169638,130.949049250926));
#38971=CARTESIAN_POINT('Ctrl Pts',(127.998583410116,-4.91186636222894,131.09342051706));
#38972=CARTESIAN_POINT('Ctrl Pts',(127.990445397193,-4.89917575400125,131.23709609555));
#38973=CARTESIAN_POINT('Ctrl Pts',(127.982295826442,-4.88646712222452,131.380975726028));
#38974=CARTESIAN_POINT('Ctrl Pts',(127.97414625569,-4.86742816844376,131.524157369783));
#38975=CARTESIAN_POINT('Ctrl Pts',(127.965996684939,-4.84217047593194,131.666084555097));
#38976=CARTESIAN_POINT('Ctrl Pts',(127.957827054933,-4.81685061444324,131.808361078256));
#38977=CARTESIAN_POINT('Ctrl Pts',(127.949657424928,-4.78528146592727,131.949376644164));
#38978=CARTESIAN_POINT('Ctrl Pts',(127.941487794922,-4.74762541554514,132.088586445125));
#38979=CARTESIAN_POINT('Ctrl Pts',(127.933307467654,-4.70992005856948,132.227978526516));
#38980=CARTESIAN_POINT('Ctrl Pts',(127.925127140387,-4.66611199179819,132.365559810819));
#38981=CARTESIAN_POINT('Ctrl Pts',(127.91694681312,-4.61641242277826,132.500803780575));
#38982=CARTESIAN_POINT('Ctrl Pts',(127.908747621784,-4.56659824513116,132.636359626792));
#38983=CARTESIAN_POINT('Ctrl Pts',(127.900548430448,-4.51086552640424,132.769567077166));
#38984=CARTESIAN_POINT('Ctrl Pts',(127.892349239112,-4.44947301394585,132.899920915116));
#38985=CARTESIAN_POINT('Ctrl Pts',(127.887412816527,-4.41251090724346,132.978402024203));
#38986=CARTESIAN_POINT('Ctrl Pts',(127.882476393942,-4.37349812256339,133.055849260602));
#38987=CARTESIAN_POINT('Ctrl Pts',(127.877539971357,-4.33249874537039,133.1321573621));
#38988=CARTESIAN_POINT('Ctrl Pts',(127.869765637238,-4.26792914025671,133.252334406682));
#38989=CARTESIAN_POINT('Ctrl Pts',(127.861991303119,-4.19825317444962,133.370013170446));
#38990=CARTESIAN_POINT('Ctrl Pts',(127.854216969,-4.12368850451715,133.484729282547));
#38991=CARTESIAN_POINT('Ctrl Pts',(127.846452216053,-4.04921572887634,133.599304017292));
#38992=CARTESIAN_POINT('Ctrl Pts',(127.838687463106,-3.96986644787174,133.710923040524));
#38993=CARTESIAN_POINT('Ctrl Pts',(127.830922710159,-3.88590470005901,133.819145473001));
#38994=CARTESIAN_POINT('Ctrl Pts',(127.823165669274,-3.80202634423779,133.927260417433));
#38995=CARTESIAN_POINT('Ctrl Pts',(127.815408628389,-3.71354487644034,134.031985177708));
#38996=CARTESIAN_POINT('Ctrl Pts',(127.807651587504,-3.62076802292836,134.132907145202));
#38997=CARTESIAN_POINT('Ctrl Pts',(127.799900396264,-3.52806113316356,134.233753006655));
#38998=CARTESIAN_POINT('Ctrl Pts',(127.792149205023,-3.4310655686078,134.33080149668));
#38999=CARTESIAN_POINT('Ctrl Pts',(127.784398013783,-3.33012955079288,134.423672739701));
#39000=CARTESIAN_POINT('Ctrl Pts',(127.776650117006,-3.22923643347787,134.516504509967));
#39001=CARTESIAN_POINT('Ctrl Pts',(127.768902220229,-3.12440648105544,134.60516230028));
#39002=CARTESIAN_POINT('Ctrl Pts',(127.761154323452,-3.0160248626873,134.689302971083));
#39003=CARTESIAN_POINT('Ctrl Pts',(127.753408047368,-2.90766591541735,134.773426041472));
#39004=CARTESIAN_POINT('Ctrl Pts',(127.745661771284,-2.79575708856317,134.853033632177));
#39005=CARTESIAN_POINT('Ctrl Pts',(127.7379154952,-2.6807164181129,134.927823064122));
#39006=CARTESIAN_POINT('Ctrl Pts',(127.730169161934,-2.56567489845846,135.002613048146));
#39007=CARTESIAN_POINT('Ctrl Pts',(127.722422828669,-2.44750181686188,135.072584589343));
#39008=CARTESIAN_POINT('Ctrl Pts',(127.714676495404,-2.3266436142832,135.137478727497));
#39009=CARTESIAN_POINT('Ctrl Pts',(127.706928427401,-2.20575834634802,135.202387398244));
#39010=CARTESIAN_POINT('Ctrl Pts',(127.699180359398,-2.08218710527059,135.262216218435));
#39011=CARTESIAN_POINT('Ctrl Pts',(127.691432291395,-1.95639994702006,135.316752700464));
#39012=CARTESIAN_POINT('Ctrl Pts',(127.683675988653,-1.83047910068086,135.371347144515));
#39013=CARTESIAN_POINT('Ctrl Pts',(127.675919685911,-1.70233799187077,135.420637858573));
#39014=CARTESIAN_POINT('Ctrl Pts',(127.668163383169,-1.57246614813139,135.464460753344));
#39015=CARTESIAN_POINT('Ctrl Pts',(127.660402940655,-1.44252498787864,135.508307037714));
#39016=CARTESIAN_POINT('Ctrl Pts',(127.652642498141,-1.31085162722338,135.546679578427));
#39017=CARTESIAN_POINT('Ctrl Pts',(127.644882055627,-1.17794872117338,135.57946479159));
#39018=CARTESIAN_POINT('Ctrl Pts',(127.637109155361,-1.04483246758002,135.612302634488));
#39019=CARTESIAN_POINT('Ctrl Pts',(127.629336255096,-0.910483107752943,
135.639535148655));
#39020=CARTESIAN_POINT('Ctrl Pts',(127.62156335483,-0.77541229651415,135.661100144544));
#39021=CARTESIAN_POINT('Ctrl Pts',(127.614073019068,-0.64525164948536,135.681881198514));
#39022=CARTESIAN_POINT('Ctrl Pts',(127.606582683306,-0.514421399407542,
135.697399601139));
#39023=CARTESIAN_POINT('Ctrl Pts',(127.599092347544,-0.383380071231758,
135.707645514804));
#39024=CARTESIAN_POINT('Ctrl Pts',(127.591318013425,-0.247370271270378,
135.718279905399));
#39025=CARTESIAN_POINT('Ctrl Pts',(127.583543679306,-0.110702233030291,
135.723267788318));
#39026=CARTESIAN_POINT('Ctrl Pts',(127.575769345187,0.026115706451228,135.72254128041));
#39027=CARTESIAN_POINT('Ctrl Pts',(127.56800459224,0.162765030050107,135.721815667858));
#39028=CARTESIAN_POINT('Ctrl Pts',(127.560239839293,0.299563500106598,135.715389678964));
#39029=CARTESIAN_POINT('Ctrl Pts',(127.552475086346,0.43599747314086,135.703247150842));
#39030=CARTESIAN_POINT('Ctrl Pts',(127.544718045461,0.572295938029814,135.691116682851));
#39031=CARTESIAN_POINT('Ctrl Pts',(127.536961004575,0.70823023943381,135.673281009041));
#39032=CARTESIAN_POINT('Ctrl Pts',(127.52920396369,0.843286904469057,135.649776003191));
#39033=CARTESIAN_POINT('Ctrl Pts',(127.52145277245,0.978241722222339,135.626288722649));
#39034=CARTESIAN_POINT('Ctrl Pts',(127.51370158121,1.11231983732729,135.59714068653));
#39035=CARTESIAN_POINT('Ctrl Pts',(127.50595038997,1.24501342745985,135.562419531445));
#39036=CARTESIAN_POINT('Ctrl Pts',(127.498202493193,1.37765061927708,135.527713133777));
#39037=CARTESIAN_POINT('Ctrl Pts',(127.490454596416,1.50890407908477,135.487438427117));
#39038=CARTESIAN_POINT('Ctrl Pts',(127.482706699639,1.63827692051537,135.441733989876));
#39039=CARTESIAN_POINT('Ctrl Pts',(127.474960423555,1.7676226999365,135.396039113018));
#39040=CARTESIAN_POINT('Ctrl Pts',(127.467214147471,1.89508827504052,135.344916894862));
#39041=CARTESIAN_POINT('Ctrl Pts',(127.459467871387,2.0201930346862,135.288555435491));
#39042=CARTESIAN_POINT('Ctrl Pts',(127.451721538121,2.14529871782679,135.232193560072));
#39043=CARTESIAN_POINT('Ctrl Pts',(127.443975204856,2.26804319427376,135.170592526856));
#39044=CARTESIAN_POINT('Ctrl Pts',(127.43622887159,2.38796728121975,135.103987964944));
#39045=CARTESIAN_POINT('Ctrl Pts',(127.428480803587,2.50791822433343,135.037368487403));
#39046=CARTESIAN_POINT('Ctrl Pts',(127.420732735585,2.6250471793982,134.965743441278));
#39047=CARTESIAN_POINT('Ctrl Pts',(127.412984667582,2.73892129783921,134.889393443229));
#39048=CARTESIAN_POINT('Ctrl Pts',(127.40522836484,2.8529164430485,134.812962299493));
#39049=CARTESIAN_POINT('Ctrl Pts',(127.397472062098,2.96364951610314,134.731796390447));
#39050=CARTESIAN_POINT('Ctrl Pts',(127.389715759356,3.07071786244071,134.646218875205));
#39051=CARTESIAN_POINT('Ctrl Pts',(127.381955316842,3.17784335437855,134.560595684666));
#39052=CARTESIAN_POINT('Ctrl Pts',(127.374194874328,3.28129992738204,134.47055645272));
#39053=CARTESIAN_POINT('Ctrl Pts',(127.366434431814,3.38072032279577,134.376462682392));
#39054=CARTESIAN_POINT('Ctrl Pts',(127.358661531548,3.48030031665428,134.282217864391));
#39055=CARTESIAN_POINT('Ctrl Pts',(127.350888631283,3.57583091273973,134.183905782095));
#39056=CARTESIAN_POINT('Ctrl Pts',(127.343115731017,3.66698322729635,134.081923290228));
#39057=CARTESIAN_POINT('Ctrl Pts',(127.335625395255,3.75482192562014,133.983648118819));
#39058=CARTESIAN_POINT('Ctrl Pts',(127.328135059493,3.83859494312531,133.881964999801));
#39059=CARTESIAN_POINT('Ctrl Pts',(127.320644723731,3.91804615921147,133.77725438573));
#39060=CARTESIAN_POINT('Ctrl Pts',(127.312870389612,4.00050979230403,133.668573636901));
#39061=CARTESIAN_POINT('Ctrl Pts',(127.305096055493,4.07857865243919,133.556287018243));
#39062=CARTESIAN_POINT('Ctrl Pts',(127.297321721374,4.15192085901405,133.440785515602));
#39063=CARTESIAN_POINT('Ctrl Pts',(127.289556968427,4.22517267787409,133.32542635824));
#39064=CARTESIAN_POINT('Ctrl Pts',(127.28179221548,4.29370922597723,133.206860527086));
#39065=CARTESIAN_POINT('Ctrl Pts',(127.274027462533,4.35723926818454,133.085511428514));
#39066=CARTESIAN_POINT('Ctrl Pts',(127.266270421648,4.4207062114583,132.964282855578));
#39067=CARTESIAN_POINT('Ctrl Pts',(127.258513380763,4.47917636423823,132.840276860593));
#39068=CARTESIAN_POINT('Ctrl Pts',(127.250756339878,4.53240236351408,132.713944833492));
#39069=CARTESIAN_POINT('Ctrl Pts',(127.243005148638,4.58558822464981,132.587708074355));
#39070=CARTESIAN_POINT('Ctrl Pts',(127.235253957398,4.63353765260243,132.459149133325));
#39071=CARTESIAN_POINT('Ctrl Pts',(127.227502766157,4.67604988816291,132.328742625434));
#39072=CARTESIAN_POINT('Ctrl Pts',(127.21975486938,4.71854405488926,132.198391543787));
#39073=CARTESIAN_POINT('Ctrl Pts',(127.212006972603,4.75560550460681,132.066194828046));
#39074=CARTESIAN_POINT('Ctrl Pts',(127.204259075826,4.78708224803971,131.932645427799));
#39075=CARTESIAN_POINT('Ctrl Pts',(127.196512799742,4.81855240721645,131.799123963208));
#39076=CARTESIAN_POINT('Ctrl Pts',(127.188766523658,4.84444009408906,131.664250757218));
#39077=CARTESIAN_POINT('Ctrl Pts',(127.181020247574,4.86464378052288,131.528531834282));
#39078=CARTESIAN_POINT('Ctrl Pts',(127.173273914309,4.88484761609573,131.3928119095));
#39079=CARTESIAN_POINT('Ctrl Pts',(127.165527581043,4.89936730993927,131.256246642019));
#39080=CARTESIAN_POINT('Ctrl Pts',(127.157781247778,4.90815290396647,131.119349718624));
#39081=CARTESIAN_POINT('Ctrl Pts',(127.150033179775,4.91694046546654,130.982422138113));
#39082=CARTESIAN_POINT('Ctrl Pts',(127.142285111772,4.9199913468817,130.845163143983));
#39083=CARTESIAN_POINT('Ctrl Pts',(127.134537043769,4.91730767372589,130.708088584158));
#39084=CARTESIAN_POINT('Ctrl Pts',(127.126780741027,4.91462114833031,130.57086833986));
#39085=CARTESIAN_POINT('Ctrl Pts',(127.119024438286,4.90618790110359,130.433833312948));
#39086=CARTESIAN_POINT('Ctrl Pts',(127.111268135544,4.89206217033457,130.297496943506));
#39087=CARTESIAN_POINT('Ctrl Pts',(127.10350769303,4.87792890023772,130.161087807239));
#39088=CARTESIAN_POINT('Ctrl Pts',(127.095747250515,4.85809714913368,130.025378458131));
#39089=CARTESIAN_POINT('Ctrl Pts',(127.087986808001,4.83267254748213,129.890873282507));
#39090=CARTESIAN_POINT('Ctrl Pts',(127.080213907736,4.80720713200292,129.756152187235));
#39091=CARTESIAN_POINT('Ctrl Pts',(127.07244100747,4.77613101347324,129.622639509294));
#39092=CARTESIAN_POINT('Ctrl Pts',(127.064668107205,4.73960030730825,129.490826457575));
#39093=CARTESIAN_POINT('Ctrl Pts',(127.057177771443,4.70439758432741,129.363805142302));
#39094=CARTESIAN_POINT('Ctrl Pts',(127.049687435681,4.66413005871302,129.238362320521));
#39095=CARTESIAN_POINT('Ctrl Pts',(127.042197099919,4.61897937653492,129.114919117648));
#39096=CARTESIAN_POINT('Ctrl Pts',(127.0344227658,4.57211679251908,128.986795528219));
#39097=CARTESIAN_POINT('Ctrl Pts',(127.026648431681,4.51984500596098,128.860420325024));
#39098=CARTESIAN_POINT('Ctrl Pts',(127.018874097562,4.46231357475289,128.736284066015));
#39099=CARTESIAN_POINT('Ctrl Pts',(127.011109344615,4.40485304589202,128.61230079385));
#39100=CARTESIAN_POINT('Ctrl Pts',(127.003344591667,4.34214593253155,128.490551327005));
#39101=CARTESIAN_POINT('Ctrl Pts',(126.99557983872,4.27439103873849,128.371509551337));
#39102=CARTESIAN_POINT('Ctrl Pts',(126.987822797835,4.20670344006116,128.252586009639));
#39103=CARTESIAN_POINT('Ctrl Pts',(126.98006575695,4.13397823023816,128.13636514484));
#39104=CARTESIAN_POINT('Ctrl Pts',(126.972308716065,4.05646147065486,128.023299057731));
#39105=CARTESIAN_POINT('Ctrl Pts',(126.964557524825,3.97900316706291,127.910318234638));
#39106=CARTESIAN_POINT('Ctrl Pts',(126.956806333585,3.89676072603435,127.800487775049));
#39107=CARTESIAN_POINT('Ctrl Pts',(126.949055142345,3.81002493938064,127.694233124392));
#39108=CARTESIAN_POINT('Ctrl Pts',(126.941307245568,3.72332601775002,127.588023634795));
#39109=CARTESIAN_POINT('Ctrl Pts',(126.933559348791,3.63213779563943,127.48538723357));
#39110=CARTESIAN_POINT('Ctrl Pts',(126.925811452014,3.53679285158414,127.386718244894));
#39111=CARTESIAN_POINT('Ctrl Pts',(126.91806517593,3.44146785163575,127.288069895643));
#39112=CARTESIAN_POINT('Ctrl Pts',(126.910318899846,3.34198813072477,127.1933875892));
#39113=CARTESIAN_POINT('Ctrl Pts',(126.902572623761,3.23872454311893,127.10303026264));
#39114=CARTESIAN_POINT('Ctrl Pts',(126.894826290496,3.13546019324474,127.012672269082));
#39115=CARTESIAN_POINT('Ctrl Pts',(126.887079957231,3.02841221516904,126.926639576566));
#39116=CARTESIAN_POINT('Ctrl Pts',(126.879333623965,2.91798578456649,126.845251876502));
#39117=CARTESIAN_POINT('Ctrl Pts',(126.871585555962,2.80753462473053,126.763845950227));
#39118=CARTESIAN_POINT('Ctrl Pts',(126.863837487959,2.6937038215193,126.687087318223));
#39119=CARTESIAN_POINT('Ctrl Pts',(126.856089419956,2.57692852129203,126.615253020637));
#39120=CARTESIAN_POINT('Ctrl Pts',(126.848333117215,2.46002911088596,126.543342376704));
#39121=CARTESIAN_POINT('Ctrl Pts',(126.840576814473,2.34017928559209,126.476366727126));
#39122=CARTESIAN_POINT('Ctrl Pts',(126.832820511731,2.2178403342128,126.414557966599));
#39123=CARTESIAN_POINT('Ctrl Pts',(126.825060069217,2.09543608685151,126.352716216875));
#39124=CARTESIAN_POINT('Ctrl Pts',(126.817299626703,1.97054042206953,126.296047012666));
#39125=CARTESIAN_POINT('Ctrl Pts',(126.809539184188,1.8436347902095,126.244734117201));
#39126=CARTESIAN_POINT('Ctrl Pts',(126.801766283923,1.71652543816315,126.193338849721));
#39127=CARTESIAN_POINT('Ctrl Pts',(126.793993383657,1.58740003979422,126.147317204707));
#39128=CARTESIAN_POINT('Ctrl Pts',(126.786220483392,1.45675624724891,126.10680334824));
#39129=CARTESIAN_POINT('Ctrl Pts',(126.77873014763,1.33086168563537,126.067762272504));
#39130=CARTESIAN_POINT('Ctrl Pts',(126.771239811868,1.20355750576431,126.033835572956));
#39131=CARTESIAN_POINT('Ctrl Pts',(126.763749476106,1.07529619651151,126.005098054185));
#39132=CARTESIAN_POINT('Ctrl Pts',(126.755975141987,0.942171820733176,125.975270943656));
#39133=CARTESIAN_POINT('Ctrl Pts',(126.748200807868,0.807594605709832,125.950939793889));
#39134=CARTESIAN_POINT('Ctrl Pts',(126.740426473749,0.672058111432231,125.932243936147));
#39135=CARTESIAN_POINT('Ctrl Pts',(126.732661720802,0.536688653770675,125.91357111938));
#39136=CARTESIAN_POINT('Ctrl Pts',(126.724896967855,0.400362652712045,125.900519829082));
#39137=CARTESIAN_POINT('Ctrl Pts',(126.717132214907,0.263586260303849,125.893178952643));
#39138=CARTESIAN_POINT('Ctrl Pts',(126.709375174022,0.126945716136708,125.885845367265));
#39139=CARTESIAN_POINT('Ctrl Pts',(126.701618133137,-0.010143941286047,
125.884210929698));
#39140=CARTESIAN_POINT('Ctrl Pts',(126.693861092252,-0.14716934457583,125.888312993049));
#39141=CARTESIAN_POINT('Ctrl Pts',(126.686109901012,-0.284091415942997,
125.892411963002));
#39142=CARTESIAN_POINT('Ctrl Pts',(126.678358709772,-0.420948940414114,
125.902238811701));
#39143=CARTESIAN_POINT('Ctrl Pts',(126.670607518532,-0.557226798625999,
125.917778851403));
#39144=CARTESIAN_POINT('Ctrl Pts',(126.662859621755,-0.693446735112906,
125.933312286174));
#39145=CARTESIAN_POINT('Ctrl Pts',(126.655111724978,-0.829087107724373,
125.954554038125));
#39146=CARTESIAN_POINT('Ctrl Pts',(126.647363828201,-0.96363639354055,125.981437441364));
#39147=CARTESIAN_POINT('Ctrl Pts',(126.639617552117,-1.09815753454668,126.008315221175));
#39148=CARTESIAN_POINT('Ctrl Pts',(126.631871276032,-1.23158765957864,126.040832228413));
#39149=CARTESIAN_POINT('Ctrl Pts',(126.624124999948,-1.3634243289211,126.078870467137));
#39150=CARTESIAN_POINT('Ctrl Pts',(126.616378666683,-1.49526197145191,126.116908986649));
#39151=CARTESIAN_POINT('Ctrl Pts',(126.608632333418,-1.62550575917977,126.160468710591));
#39152=CARTESIAN_POINT('Ctrl Pts',(126.600886000152,-1.75366771931936,126.209381554206));
#39153=CARTESIAN_POINT('Ctrl Pts',(126.593137932149,-1.88185838044132,126.258305351513));
#39154=CARTESIAN_POINT('Ctrl Pts',(126.585389864146,-2.00796592107178,126.312584514579));
#39155=CARTESIAN_POINT('Ctrl Pts',(126.577641796143,-2.13152205225228,126.372002689413));
#39156=CARTESIAN_POINT('Ctrl Pts',(126.569885493401,-2.25520950035924,126.43148401459));
#39157=CARTESIAN_POINT('Ctrl Pts',(126.562129190659,-2.37633976926454,126.496115092365));
#39158=CARTESIAN_POINT('Ctrl Pts',(126.554372887918,-2.49446842152646,126.565633172152));
#39159=CARTESIAN_POINT('Ctrl Pts',(126.546612445403,-2.61266012260688,126.635188355831));
#39160=CARTESIAN_POINT('Ctrl Pts',(126.538852002889,-2.72784668662439,126.709635526744));
#39161=CARTESIAN_POINT('Ctrl Pts',(126.531091560375,-2.8396132726981,126.788668955596));
#39162=CARTESIAN_POINT('Ctrl Pts',(126.52331866011,-2.95155927641802,126.867829255924));
#39163=CARTESIAN_POINT('Ctrl Pts',(126.515545759844,-3.06007402165151,126.951590287322));
#39164=CARTESIAN_POINT('Ctrl Pts',(126.507772859579,-3.16477563753202,127.039605880988));
#39165=CARTESIAN_POINT('Ctrl Pts',(126.500282523817,-3.26567108594768,127.124421886127));
#39166=CARTESIAN_POINT('Ctrl Pts',(126.492792188055,-3.36302559792996,127.213188288283));
#39167=CARTESIAN_POINT('Ctrl Pts',(126.485301852293,-3.45653165696864,127.305564829459));
#39168=CARTESIAN_POINT('Ctrl Pts',(126.477638656649,-3.55219562278178,127.400073210711));
#39169=CARTESIAN_POINT('Ctrl Pts',(126.469975461006,-3.6441528984451,127.498678419363));
#39170=CARTESIAN_POINT('Ctrl Pts',(126.462312265362,-3.7320244887104,127.601053532979));
#39171=CARTESIAN_POINT('Ctrl Pts',(126.454658019157,-3.81979345842112,127.703309088147));
#39172=CARTESIAN_POINT('Ctrl Pts',(126.447003772952,-3.9034859687367,127.809325493409));
#39173=CARTESIAN_POINT('Ctrl Pts',(126.439349526747,-3.98275807885899,127.918737435689));
#39174=CARTESIAN_POINT('Ctrl Pts',(126.431702448918,-4.06195594883983,128.028046911187));
#39175=CARTESIAN_POINT('Ctrl Pts',(126.424055371089,-4.13674141584888,128.140745276162));
#39176=CARTESIAN_POINT('Ctrl Pts',(126.416408293261,-4.20680961415279,128.256432845283));
#39177=CARTESIAN_POINT('Ctrl Pts',(126.408766874152,-4.2768259630699,128.372034807386));
#39178=CARTESIAN_POINT('Ctrl Pts',(126.401125455043,-4.34213178084251,128.490621229099));
#39179=CARTESIAN_POINT('Ctrl Pts',(126.393484035934,-4.40246484959004,128.611762544361));
#39180=CARTESIAN_POINT('Ctrl Pts',(126.385845932466,-4.46277173958543,128.732851295937));
#39181=CARTESIAN_POINT('Ctrl Pts',(126.378207828999,-4.51810999373234,128.856492375637));
#39182=CARTESIAN_POINT('Ctrl Pts',(126.370569725531,-4.56826300964923,128.982231056538));
#39183=CARTESIAN_POINT('Ctrl Pts',(126.362932135452,-4.61841265457045,129.107961286013));
#39184=CARTESIAN_POINT('Ctrl Pts',(126.355294545374,-4.66337759932938,129.23578846447));
#39185=CARTESIAN_POINT('Ctrl Pts',(126.347656955295,-4.70298927148318,129.365237629488));
#39186=CARTESIAN_POINT('Ctrl Pts',(126.343412169361,-4.72500447092223,129.437182312208));
#39187=CARTESIAN_POINT('Ctrl Pts',(126.339167383426,-4.7453669856379,129.509627674349));
#39188=CARTESIAN_POINT('Ctrl Pts',(126.334922597491,-4.76405452823406,129.582490119308));
#39189=CARTESIAN_POINT('Ctrl Pts',(128.084583899671,-4.76405452823402,129.582490119308));
#39190=CARTESIAN_POINT('Ctrl Pts',(128.076474900419,-4.79964136864725,129.721242669974));
#39191=CARTESIAN_POINT('Ctrl Pts',(128.068365901168,-4.82919846761125,129.861692018109));
#39192=CARTESIAN_POINT('Ctrl Pts',(128.060256901916,-4.85257484534123,130.003298552017));
#39193=CARTESIAN_POINT('Ctrl Pts',(128.052161851861,-4.87591101074747,130.144661492677));
#39194=CARTESIAN_POINT('Ctrl Pts',(128.044066801806,-4.89308760105199,130.287177319227));
#39195=CARTESIAN_POINT('Ctrl Pts',(128.035971751751,-4.90400426091189,130.430294752433));
#39196=CARTESIAN_POINT('Ctrl Pts',(128.028934313165,-4.91349466836051,130.554714013595));
#39197=CARTESIAN_POINT('Ctrl Pts',(128.021896874578,-4.91825473945302,130.679587598279));
#39198=CARTESIAN_POINT('Ctrl Pts',(128.014859435991,-4.9182499964572,130.804547295668));
#39199=CARTESIAN_POINT('',(128.360140563977,-4.9182480591004,130.799991217711));
#39200=CARTESIAN_POINT('Ctrl Pts',(128.430147988268,-4.76405452823404,129.582490119308));
#39201=CARTESIAN_POINT('Ctrl Pts',(128.425047399786,-4.78633453593721,129.669359531197));
#39202=CARTESIAN_POINT('Ctrl Pts',(128.419946811305,-4.80621721630481,129.756758400623));
#39203=CARTESIAN_POINT('Ctrl Pts',(128.414846222823,-4.82368463813426,129.84454314829));
#39204=CARTESIAN_POINT('Ctrl Pts',(128.403582817055,-4.8622571794244,130.038394355244));
#39205=CARTESIAN_POINT('Ctrl Pts',(128.392319411286,-4.88915397073168,130.234639638687));
#39206=CARTESIAN_POINT('Ctrl Pts',(128.381056005517,-4.90414358667604,130.432125821014));
#39207=CARTESIAN_POINT('Ctrl Pts',(128.374084191681,-4.91342184708737,130.554365659184));
#39208=CARTESIAN_POINT('Ctrl Pts',(128.367112377844,-4.91813886456444,130.677080574109));
#39209=CARTESIAN_POINT('Ctrl Pts',(128.360140564008,-4.91824805909993,130.799991217172));
#39210=CARTESIAN_POINT('Ctrl Pts',(128.360140563977,-4.91824805910041,130.799991217711));
#39211=CARTESIAN_POINT('Ctrl Pts',(128.352493106526,-4.91836783574399,130.934813221745));
#39212=CARTESIAN_POINT('Ctrl Pts',(128.344845649074,-4.91293971375226,131.069818158709));
#39213=CARTESIAN_POINT('Ctrl Pts',(128.337198191623,-4.90194532537492,131.204504453624));
#39214=CARTESIAN_POINT('Ctrl Pts',(128.329557232397,-4.89096027918952,131.339076302407));
#39215=CARTESIAN_POINT('Ctrl Pts',(128.321916273171,-4.8744184074605,131.473329647834));
#39216=CARTESIAN_POINT('Ctrl Pts',(128.314275313945,-4.85235340333965,131.606762955298));
#39217=CARTESIAN_POINT('Ctrl Pts',(128.306638422809,-4.83030014675143,131.740125222117));
#39218=CARTESIAN_POINT('Ctrl Pts',(128.299001531673,-4.80272967054546,131.872667922253));
#39219=CARTESIAN_POINT('Ctrl Pts',(128.291364640537,-4.76972745995375,132.003895119055));
#39220=CARTESIAN_POINT('Ctrl Pts',(128.283729779861,-4.73673402383204,132.135087425798));
#39221=CARTESIAN_POINT('Ctrl Pts',(128.276094919185,-4.69831182247926,132.264964533653));
#39222=CARTESIAN_POINT('Ctrl Pts',(128.268460058509,-4.6545972495114,132.393041676602));
#39223=CARTESIAN_POINT('Ctrl Pts',(128.260825462576,-4.61088419237095,132.521114378405));
#39224=CARTESIAN_POINT('Ctrl Pts',(128.253190866643,-4.56187925896366,132.647386857705));
#39225=CARTESIAN_POINT('Ctrl Pts',(128.24555627071,-4.50776823846932,132.771391011522));
#39226=CARTESIAN_POINT('Ctrl Pts',(128.237920174223,-4.45364658263779,132.895419537935));
#39227=CARTESIAN_POINT('Ctrl Pts',(128.230284077736,-4.39441700591012,133.017178482913));
#39228=CARTESIAN_POINT('Ctrl Pts',(128.22264798125,-4.33031257306284,133.13622169449));
#39229=CARTESIAN_POINT('Ctrl Pts',(128.215004114817,-4.26614291212615,133.255386035931));
#39230=CARTESIAN_POINT('Ctrl Pts',(128.207360248384,-4.19708868173679,133.3718287705));
#39231=CARTESIAN_POINT('Ctrl Pts',(128.199716381951,-4.12342802636981,133.485129979866));
#39232=CARTESIAN_POINT('Ctrl Pts',(128.192068419599,-4.04972790039472,133.598491900987));
#39233=CARTESIAN_POINT('Ctrl Pts',(128.184420457248,-3.97141666865398,133.708708617251));
#39234=CARTESIAN_POINT('Ctrl Pts',(128.176772494896,-3.88881378195585,133.815392074022));
#39235=CARTESIAN_POINT('Ctrl Pts',(128.169112854212,-3.80608476179517,133.922238434953));
#39236=CARTESIAN_POINT('Ctrl Pts',(128.161453213528,-3.71905125886355,134.025540453863));
#39237=CARTESIAN_POINT('Ctrl Pts',(128.153793572844,-3.62807106759501,134.124945414101));
#39238=CARTESIAN_POINT('Ctrl Pts',(128.147995248233,-3.5591993405899,134.200194665493));
#39239=CARTESIAN_POINT('Ctrl Pts',(128.142196923622,-3.48806677687409,134.273211467254));
#39240=CARTESIAN_POINT('Ctrl Pts',(128.136398599011,-3.41484099230444,134.343858330488));
#39241=CARTESIAN_POINT('Ctrl Pts',(128.128624264892,-3.31666061201087,134.438580919527));
#39242=CARTESIAN_POINT('Ctrl Pts',(128.120849930773,-3.21438053947274,134.52936538083));
#39243=CARTESIAN_POINT('Ctrl Pts',(128.113075596654,-3.10834982589523,134.61583597789));
#39244=CARTESIAN_POINT('Ctrl Pts',(128.105310843707,-3.00244978569605,134.702200007668));
#39245=CARTESIAN_POINT('Ctrl Pts',(128.09754609076,-2.89280860159226,134.784260506639));
#39246=CARTESIAN_POINT('Ctrl Pts',(128.089781337812,-2.77981231897982,134.861678270123));
#39247=CARTESIAN_POINT('Ctrl Pts',(128.082024296928,-2.66692826586855,134.939019141192));
#39248=CARTESIAN_POINT('Ctrl Pts',(128.074267256043,-2.55069606617825,135.011726233786));
#39249=CARTESIAN_POINT('Ctrl Pts',(128.066510215158,-2.43153473468002,135.079500603174));
#39250=CARTESIAN_POINT('Ctrl Pts',(128.058759023917,-2.31246326366873,135.147223863383));
#39251=CARTESIAN_POINT('Ctrl Pts',(128.051007832677,-2.19046739596087,135.210021611924));
#39252=CARTESIAN_POINT('Ctrl Pts',(128.043256641437,-2.06599471318216,135.267638438585));
#39253=CARTESIAN_POINT('Ctrl Pts',(128.03550874466,-1.94157493461371,135.325230776559));
#39254=CARTESIAN_POINT('Ctrl Pts',(128.027760847883,-1.81468078879465,135.377646408435));
#39255=CARTESIAN_POINT('Ctrl Pts',(128.020012951106,-1.68578382373529,135.424676187106));
#39256=CARTESIAN_POINT('Ctrl Pts',(128.012266675022,-1.5569138211425,135.471696128161));
#39257=CARTESIAN_POINT('Ctrl Pts',(128.004520398938,-1.42604219966607,135.513332322966));
#39258=CARTESIAN_POINT('Ctrl Pts',(127.996774122854,-1.2936594505664,135.549424188105));
#39259=CARTESIAN_POINT('Ctrl Pts',(127.989027789588,-1.16127572424744,135.585516319667));
#39260=CARTESIAN_POINT('Ctrl Pts',(127.981281456323,-1.0273812252448,135.616063937058));
#39261=CARTESIAN_POINT('Ctrl Pts',(127.973535123058,-0.892480144392583,
135.640956760967));
#39262=CARTESIAN_POINT('Ctrl Pts',(127.965787055055,-0.757548853378283,
135.665855159452));
#39263=CARTESIAN_POINT('Ctrl Pts',(127.958038987052,-0.621610916361356,
135.685096173629));
#39264=CARTESIAN_POINT('Ctrl Pts',(127.950290919049,-0.485178821715212,
135.698620987986));
#39265=CARTESIAN_POINT('Ctrl Pts',(127.942534616307,-0.348601725415501,
135.712160176676));
#39266=CARTESIAN_POINT('Ctrl Pts',(127.934778313565,-0.211529812028351,
135.719970990961));
#39267=CARTESIAN_POINT('Ctrl Pts',(127.927022010823,-0.0744793339138556,
135.722046647735));
#39268=CARTESIAN_POINT('Ctrl Pts',(127.919261568309,0.0626442921672268,
135.72412341235));
#39269=CARTESIAN_POINT('Ctrl Pts',(127.911501125795,0.199746069544796,135.720458930541));
#39270=CARTESIAN_POINT('Ctrl Pts',(127.903740683281,0.336312666382312,135.711098520993));
#39271=CARTESIAN_POINT('Ctrl Pts',(127.895967783015,0.473098492045071,135.701723085285));
#39272=CARTESIAN_POINT('Ctrl Pts',(127.88819488275,0.609347031560676,135.686633493054));
#39273=CARTESIAN_POINT('Ctrl Pts',(127.880421982484,0.744552075578421,135.665926750949));
#39274=CARTESIAN_POINT('Ctrl Pts',(127.872931646722,0.874842075685719,135.645972751076));
#39275=CARTESIAN_POINT('Ctrl Pts',(127.86544131096,1.00416282816048,135.62080296493));
#39276=CARTESIAN_POINT('Ctrl Pts',(127.857950975198,1.13207470119655,135.590548028586));
#39277=CARTESIAN_POINT('Ctrl Pts',(127.850176641079,1.2648363917761,135.559145967136));
#39278=CARTESIAN_POINT('Ctrl Pts',(127.84240230696,1.39650080775607,135.522166064256));
#39279=CARTESIAN_POINT('Ctrl Pts',(127.834627972841,1.52656316067025,135.47969889185));
#39280=CARTESIAN_POINT('Ctrl Pts',(127.826863219894,1.65646522335865,135.437284056439));
#39281=CARTESIAN_POINT('Ctrl Pts',(127.819098466947,1.78476878336023,135.389395527186));
#39282=CARTESIAN_POINT('Ctrl Pts',(127.811333713999,1.91097979120411,135.3361747466));
#39283=CARTESIAN_POINT('Ctrl Pts',(127.803576673114,2.03706544449549,135.283006825644));
#39284=CARTESIAN_POINT('Ctrl Pts',(127.795819632229,2.16106232372884,135.224517343693));
#39285=CARTESIAN_POINT('Ctrl Pts',(127.788062591344,2.28249243051693,135.160897242815));
#39286=CARTESIAN_POINT('Ctrl Pts',(127.780311400104,2.40383096591732,135.097325118349));
#39287=CARTESIAN_POINT('Ctrl Pts',(127.772560208864,2.52260623670097,135.02863025675));
#39288=CARTESIAN_POINT('Ctrl Pts',(127.764809017624,2.63836143022142,134.955051165658));
#39289=CARTESIAN_POINT('Ctrl Pts',(127.757061120847,2.75406742469644,134.881503347643));
#39290=CARTESIAN_POINT('Ctrl Pts',(127.74931322407,2.86675556565846,134.803075638288));
#39291=CARTESIAN_POINT('Ctrl Pts',(127.741565327293,2.97599500850477,134.72005171517));
#39292=CARTESIAN_POINT('Ctrl Pts',(127.733819051209,3.08521160081472,134.637045158866));
#39293=CARTESIAN_POINT('Ctrl Pts',(127.726072775125,3.19098061882793,134.549444537554));
#39294=CARTESIAN_POINT('Ctrl Pts',(127.71832649904,3.29290183666117,134.457575716163));
#39295=CARTESIAN_POINT('Ctrl Pts',(127.710580165775,3.39482380685327,134.365706216617));
#39296=CARTESIAN_POINT('Ctrl Pts',(127.70283383251,3.49289762978401,134.269568715884));
#39297=CARTESIAN_POINT('Ctrl Pts',(127.695087499244,3.58675799688275,134.16952779533));
#39298=CARTESIAN_POINT('Ctrl Pts',(127.687339431241,3.68063938336017,134.069464471305));
#39299=CARTESIAN_POINT('Ctrl Pts',(127.679591363239,3.77030516894693,133.96549627308));
#39300=CARTESIAN_POINT('Ctrl Pts',(127.671843295236,3.85542885800333,133.858022580419));
#39301=CARTESIAN_POINT('Ctrl Pts',(127.664086992494,3.94064301752938,133.750434663438));
#39302=CARTESIAN_POINT('Ctrl Pts',(127.656330689752,4.02130519415403,133.639334116538));
#39303=CARTESIAN_POINT('Ctrl Pts',(127.64857438701,4.09713063404873,133.525151611016));
#39304=CARTESIAN_POINT('Ctrl Pts',(127.640813944496,4.17299654426377,133.410908162853));
#39305=CARTESIAN_POINT('Ctrl Pts',(127.633053501982,4.24402037150442,133.293579812694));
#39306=CARTESIAN_POINT('Ctrl Pts',(127.625293059467,4.30996277526624,133.173622937006));
#39307=CARTESIAN_POINT('Ctrl Pts',(127.617520159202,4.37601103562876,133.053473495892));
#39308=CARTESIAN_POINT('Ctrl Pts',(127.609747258937,4.43696139798907,132.930687447654));
#39309=CARTESIAN_POINT('Ctrl Pts',(127.601974358671,4.49262185826876,132.805743115018));
#39310=CARTESIAN_POINT('Ctrl Pts',(127.594484022909,4.54625892061693,132.685340823589));
#39311=CARTESIAN_POINT('Ctrl Pts',(127.586993687147,4.59498389223406,132.56293472776));
#39312=CARTESIAN_POINT('Ctrl Pts',(127.579503351385,4.63866904922118,132.438965314212));
#39313=CARTESIAN_POINT('Ctrl Pts',(127.571729017266,4.6840105422134,132.310295562669));
#39314=CARTESIAN_POINT('Ctrl Pts',(127.563954683147,4.72406613551407,132.179534019784));
#39315=CARTESIAN_POINT('Ctrl Pts',(127.556180349028,4.7586391793361,132.047154334716));
#39316=CARTESIAN_POINT('Ctrl Pts',(127.548415596081,4.79316961497151,131.914937795779));
#39317=CARTESIAN_POINT('Ctrl Pts',(127.540650843134,4.82223084720667,131.7811074572));
#39318=CARTESIAN_POINT('Ctrl Pts',(127.532886090187,4.84567482982384,131.646155429923));
#39319=CARTESIAN_POINT('Ctrl Pts',(127.525129049302,4.86909552754698,131.511337438902));
#39320=CARTESIAN_POINT('Ctrl Pts',(127.517372008417,4.88691001189204,131.37540035895));
#39321=CARTESIAN_POINT('Ctrl Pts',(127.509614967532,4.89902055802202,131.238849552497));
#39322=CARTESIAN_POINT('Ctrl Pts',(127.501863776291,4.91112197149492,131.10240172007));
#39323=CARTESIAN_POINT('Ctrl Pts',(127.494112585051,4.91752797399816,130.965341470211));
#39324=CARTESIAN_POINT('Ctrl Pts',(127.486361393811,4.91819231037008,130.828182051541));
#39325=CARTESIAN_POINT('Ctrl Pts',(127.478613497034,4.91885636438132,130.691080929282));
#39326=CARTESIAN_POINT('Ctrl Pts',(127.470865600257,4.91378360406405,130.553881112188));
#39327=CARTESIAN_POINT('Ctrl Pts',(127.46311770348,4.90297981336515,130.417098416682));
#39328=CARTESIAN_POINT('Ctrl Pts',(127.455371427396,4.89217828258636,130.280344333167));
#39329=CARTESIAN_POINT('Ctrl Pts',(127.447625151312,4.8756481366858,130.144007587195));
#39330=CARTESIAN_POINT('Ctrl Pts',(127.439878875228,4.85344720319195,130.00860103809));
#39331=CARTESIAN_POINT('Ctrl Pts',(127.432132541962,4.83124610581588,129.873193489445));
#39332=CARTESIAN_POINT('Ctrl Pts',(127.424386208697,4.80337420057413,129.738716537183));
#39333=CARTESIAN_POINT('Ctrl Pts',(127.416639875431,4.76994076188964,129.605674590884));
#39334=CARTESIAN_POINT('Ctrl Pts',(127.408891807429,4.73649983601844,129.472602850763));
#39335=CARTESIAN_POINT('Ctrl Pts',(127.401143739426,4.69749499363828,129.340967135178));
#39336=CARTESIAN_POINT('Ctrl Pts',(127.393395671423,4.65308576538586,129.211258008672));
#39337=CARTESIAN_POINT('Ctrl Pts',(127.385639368681,4.60862933847702,129.081411025763));
#39338=CARTESIAN_POINT('Ctrl Pts',(127.377883065939,4.55875717858758,128.953495092716));
#39339=CARTESIAN_POINT('Ctrl Pts',(127.370126763197,4.50367770527798,128.827982569347));
#39340=CARTESIAN_POINT('Ctrl Pts',(127.362366320683,4.44856883439518,128.702403056165));
#39341=CARTESIAN_POINT('Ctrl Pts',(127.354605878169,4.38824728397169,128.579229859643));
#39342=CARTESIAN_POINT('Ctrl Pts',(127.346845435654,4.32296764706629,128.458911026354));
#39343=CARTESIAN_POINT('Ctrl Pts',(127.339072535389,4.25758321749239,128.338399046591));
#39344=CARTESIAN_POINT('Ctrl Pts',(127.331299635124,4.18722499727909,128.220750922245));
#39345=CARTESIAN_POINT('Ctrl Pts',(127.323526734858,4.11219162998841,128.106386736901));
#39346=CARTESIAN_POINT('Ctrl Pts',(127.316036399096,4.03988591459579,127.996179977759));
#39347=CARTESIAN_POINT('Ctrl Pts',(127.308546063334,3.96323923678638,127.889022794443));
#39348=CARTESIAN_POINT('Ctrl Pts',(127.301055727572,3.88255315259187,127.785260738496));
#39349=CARTESIAN_POINT('Ctrl Pts',(127.293281393453,3.79880783099182,127.677564512662));
#39350=CARTESIAN_POINT('Ctrl Pts',(127.285507059334,3.71044546819425,127.573184799627));
#39351=CARTESIAN_POINT('Ctrl Pts',(127.277732725215,3.61775826463864,127.472543065367));
#39352=CARTESIAN_POINT('Ctrl Pts',(127.269967972268,3.52518528977797,127.372025363051));
#39353=CARTESIAN_POINT('Ctrl Pts',(127.26220321932,3.42829834154304,127.275236758326));
#39354=CARTESIAN_POINT('Ctrl Pts',(127.254438466373,3.32743142421089,127.182567804652));
#39355=CARTESIAN_POINT('Ctrl Pts',(127.246681425488,3.22666468932314,127.08999089109));
#39356=CARTESIAN_POINT('Ctrl Pts',(127.238924384603,3.12192613795301,127.001525748717));
#39357=CARTESIAN_POINT('Ctrl Pts',(127.231167343718,3.0135881231648,126.917527756943));
#39358=CARTESIAN_POINT('Ctrl Pts',(127.223416152478,2.90533180691615,126.833593108708));
#39359=CARTESIAN_POINT('Ctrl Pts',(127.215664961238,2.79348173778971,126.754119144443));
#39360=CARTESIAN_POINT('Ctrl Pts',(127.207913769998,2.6784447243425,126.679422203342));
#39361=CARTESIAN_POINT('Ctrl Pts',(127.200165873221,2.5634566046944,126.604757010433));
#39362=CARTESIAN_POINT('Ctrl Pts',(127.192417976444,2.44528456201122,126.534865014925));
#39363=CARTESIAN_POINT('Ctrl Pts',(127.184670079667,2.3243656936248,126.470020161995));
#39364=CARTESIAN_POINT('Ctrl Pts',(127.176923803583,2.20347211885877,126.40518887321));
#39365=CARTESIAN_POINT('Ctrl Pts',(127.169177527499,2.07983320558443,126.345402811706));
#39366=CARTESIAN_POINT('Ctrl Pts',(127.161431251415,1.95391169406834,126.290890538538));
#39367=CARTESIAN_POINT('Ctrl Pts',(127.153684918149,1.82798925302869,126.236377862972));
#39368=CARTESIAN_POINT('Ctrl Pts',(127.145938584884,1.69978453891325,126.187139208746));
#39369=CARTESIAN_POINT('Ctrl Pts',(127.138192251619,1.56978099128221,126.14335528589));
#39370=CARTESIAN_POINT('Ctrl Pts',(127.130444183616,1.43974833025745,126.099561557929));
#39371=CARTESIAN_POINT('Ctrl Pts',(127.122696115612,1.3079164045647,126.061225116843));
#39372=CARTESIAN_POINT('Ctrl Pts',(127.11494804761,1.17478417025543,126.028476907108));
#39373=CARTESIAN_POINT('Ctrl Pts',(127.107191744868,1.04151044142369,125.995693892187));
#39374=CARTESIAN_POINT('Ctrl Pts',(127.099435442126,0.906934023568071,125.968511066422));
#39375=CARTESIAN_POINT('Ctrl Pts',(127.091679139384,0.771564982243835,125.947008402555));
#39376=CARTESIAN_POINT('Ctrl Pts',(127.08391869687,0.636123690385901,125.925494262068));
#39377=CARTESIAN_POINT('Ctrl Pts',(127.076158254356,0.499889320265314,125.909666369441));
#39378=CARTESIAN_POINT('Ctrl Pts',(127.068397811841,0.363376439920618,125.899552708441));
#39379=CARTESIAN_POINT('Ctrl Pts',(127.060624911576,0.226644416981721,125.889422812095));
#39380=CARTESIAN_POINT('Ctrl Pts',(127.052852011311,0.0896333813806602,
125.885025490484));
#39381=CARTESIAN_POINT('Ctrl Pts',(127.045079111045,-0.0471418145240442,
125.886336551762));
#39382=CARTESIAN_POINT('Ctrl Pts',(127.037588775283,-0.178944887541407,
125.887599952661));
#39383=CARTESIAN_POINT('Ctrl Pts',(127.030098439521,-0.310528662267972,
125.894163898406));
#39384=CARTESIAN_POINT('Ctrl Pts',(127.022608103759,-0.441439418002701,
125.90596146042));
#39385=CARTESIAN_POINT('Ctrl Pts',(127.01483376964,-0.577313694830587,125.918206330582));
#39386=CARTESIAN_POINT('Ctrl Pts',(127.007059435521,-0.712893319056468,
125.936128304444));
#39387=CARTESIAN_POINT('Ctrl Pts',(126.999285101402,-0.847665757943376,
125.959709358155));
#39388=CARTESIAN_POINT('Ctrl Pts',(126.991520348455,-0.98227210184468,125.983261350325));
#39389=CARTESIAN_POINT('Ctrl Pts',(126.983755595508,-1.11607285831267,126.012458478809));
#39390=CARTESIAN_POINT('Ctrl Pts',(126.975990842561,-1.2485589061891,126.047230840035));
#39391=CARTESIAN_POINT('Ctrl Pts',(126.968233801676,-1.38091336705452,126.081968664861));
#39392=CARTESIAN_POINT('Ctrl Pts',(126.960476760791,-1.51195534219338,126.122270604144));
#39393=CARTESIAN_POINT('Ctrl Pts',(126.952719719906,-1.64118457491573,126.168015477959));
#39394=CARTESIAN_POINT('Ctrl Pts',(126.944968528666,-1.77031635486887,126.213725855208));
#39395=CARTESIAN_POINT('Ctrl Pts',(126.937217337425,-1.89763774627782,126.264870867178));
#39396=CARTESIAN_POINT('Ctrl Pts',(126.929466146185,-2.02266271405707,126.32127924337));
#39397=CARTESIAN_POINT('Ctrl Pts',(126.921718249408,-2.1476345428897,126.377663644497));
#39398=CARTESIAN_POINT('Ctrl Pts',(126.913970352631,-2.27031153373802,126.439306800033));
#39399=CARTESIAN_POINT('Ctrl Pts',(126.906222455854,-2.39022694697982,126.505989041675));
#39400=CARTESIAN_POINT('Ctrl Pts',(126.89847617977,-2.51011727650225,126.572657334829));
#39401=CARTESIAN_POINT('Ctrl Pts',(126.890729903686,-2.62724683594767,126.644362427603));
#39402=CARTESIAN_POINT('Ctrl Pts',(126.882983627602,-2.74117320801024,126.72083854634));
#39403=CARTESIAN_POINT('Ctrl Pts',(126.875237294336,-2.85510042105127,126.797315229606));
#39404=CARTESIAN_POINT('Ctrl Pts',(126.867490961071,-2.96582407491677,126.878562791207));
#39405=CARTESIAN_POINT('Ctrl Pts',(126.859744627806,-3.07293082224783,126.964272177936));
#39406=CARTESIAN_POINT('Ctrl Pts',(126.851996559803,-3.18006155539146,127.050000758687));
#39407=CARTESIAN_POINT('Ctrl Pts',(126.8442484918,-3.28357346503124,127.140192908618));
#39408=CARTESIAN_POINT('Ctrl Pts',(126.836500423797,-3.38308668593686,127.234499620561));
#39409=CARTESIAN_POINT('Ctrl Pts',(126.828744121055,-3.48270567067891,127.328906562801));
#39410=CARTESIAN_POINT('Ctrl Pts',(126.820987818313,-3.57831719291506,127.427436533241));
#39411=CARTESIAN_POINT('Ctrl Pts',(126.813231515572,-3.66957826642248,127.529703626506));
#39412=CARTESIAN_POINT('Ctrl Pts',(126.805471073057,-3.76088804871265,127.632025302797));
#39413=CARTESIAN_POINT('Ctrl Pts',(126.797710630543,-3.84784250780809,127.738087774154));
#39414=CARTESIAN_POINT('Ctrl Pts',(126.789950188029,-3.93013996357985,127.847473245823));
#39415=CARTESIAN_POINT('Ctrl Pts',(126.782177287764,-4.0125695305337,127.957034312762));
#39416=CARTESIAN_POINT('Ctrl Pts',(126.774404387498,-4.09032693316647,128.069928717626));
#39417=CARTESIAN_POINT('Ctrl Pts',(126.766631487233,-4.16315423448871,128.185710224261));
#39418=CARTESIAN_POINT('Ctrl Pts',(126.759141151471,-4.23333407996803,128.297282781495));
#39419=CARTESIAN_POINT('Ctrl Pts',(126.751650815709,-4.29893589086485,128.411535910829));
#39420=CARTESIAN_POINT('Ctrl Pts',(126.744160479946,-4.35977072896749,128.528051707655));
#39421=CARTESIAN_POINT('Ctrl Pts',(126.735913192433,-4.42675336053556,128.656342255212));
#39422=CARTESIAN_POINT('Ctrl Pts',(126.727665904919,-4.48814858008666,128.787742683637));
#39423=CARTESIAN_POINT('Ctrl Pts',(126.719418617406,-4.54367471349653,128.92175519942));
#39424=CARTESIAN_POINT('Ctrl Pts',(126.711190605967,-4.59907106776353,129.055454492791));
#39425=CARTESIAN_POINT('Ctrl Pts',(126.702962594528,-4.64862556553197,129.191753406355));
#39426=CARTESIAN_POINT('Ctrl Pts',(126.694734583089,-4.69210291139784,129.330130875853));
#39427=CARTESIAN_POINT('Ctrl Pts',(126.689775297624,-4.71830809730973,129.413535399335));
#39428=CARTESIAN_POINT('Ctrl Pts',(126.684816012158,-4.74230640943244,129.497694534175));
#39429=CARTESIAN_POINT('Ctrl Pts',(126.679856726692,-4.76405452823407,129.582490119308));
#39430=CARTESIAN_POINT('Origin',(213.235140564004,0.,130.804360617566));
#39431=CARTESIAN_POINT('',(124.584949745809,-4.76405452823405,129.582490119308));
#39432=CARTESIAN_POINT('',(124.930172151781,-4.76405452823403,129.582490119308));
#39433=CARTESIAN_POINT('',(213.235140564004,-4.76405452823405,129.582490119308));
#39434=CARTESIAN_POINT('',(126.264859436032,-4.91824798511455,130.808812517913));
#39435=CARTESIAN_POINT('Ctrl Pts',(126.264859435991,-4.91824798511388,130.808812518644));
#39436=CARTESIAN_POINT('Ctrl Pts',(126.253922671906,-4.91807338114146,131.001706659933));
#39437=CARTESIAN_POINT('Ctrl Pts',(126.242985907822,-4.90654741857509,131.194108271543));
#39438=CARTESIAN_POINT('Ctrl Pts',(126.232049143737,-4.8838633796719,131.384930640216));
#39439=CARTESIAN_POINT('Ctrl Pts',(126.223650838651,-4.86644438098075,131.531462508034));
#39440=CARTESIAN_POINT('Ctrl Pts',(126.215252533566,-4.84244679529329,131.677064071246));
#39441=CARTESIAN_POINT('Ctrl Pts',(126.20685422848,-4.81197577865153,131.821254008326));
#39442=CARTESIAN_POINT('Ctrl Pts',(126.199079894361,-4.78376867472872,131.954731029709));
#39443=CARTESIAN_POINT('Ctrl Pts',(126.191305560242,-4.74995900409119,132.087244945294));
#39444=CARTESIAN_POINT('Ctrl Pts',(126.183531226123,-4.71062519903041,132.218288938507));
#39445=CARTESIAN_POINT('Ctrl Pts',(126.175766473176,-4.67133986936906,132.34917143171));
#39446=CARTESIAN_POINT('Ctrl Pts',(126.168001720229,-4.62654406249727,132.478587236115));
#39447=CARTESIAN_POINT('Ctrl Pts',(126.160236967282,-4.57636732436756,132.606039050295));
#39448=CARTESIAN_POINT('Ctrl Pts',(126.152479926396,-4.5262404224815,132.733364277536));
#39449=CARTESIAN_POINT('Ctrl Pts',(126.144722885511,-4.47074336726166,132.858729035026));
#39450=CARTESIAN_POINT('Ctrl Pts',(126.136965844626,-4.41005557514316,132.981650879945));
#39451=CARTESIAN_POINT('Ctrl Pts',(126.129214653386,-4.34941354816091,133.104480028544));
#39452=CARTESIAN_POINT('Ctrl Pts',(126.121463462146,-4.28358874798467,133.224869582249));
#39453=CARTESIAN_POINT('Ctrl Pts',(126.113712270906,-4.21280865132573,133.34235713644));
#39454=CARTESIAN_POINT('Ctrl Pts',(126.105964374129,-4.1420586380958,133.459794755286));
#39455=CARTESIAN_POINT('Ctrl Pts',(126.098216477352,-4.06635771865141,133.574332493623));
#39456=CARTESIAN_POINT('Ctrl Pts',(126.090468580575,-3.98597914979362,133.685532823442));
#39457=CARTESIAN_POINT('Ctrl Pts',(126.082722304491,-3.90561739439972,133.796709892548));
#39458=CARTESIAN_POINT('Ctrl Pts',(126.074976028407,-3.82058016469699,133.904550625068));
#39459=CARTESIAN_POINT('Ctrl Pts',(126.067229752322,-3.73118362745657,134.008647090511));
#39460=CARTESIAN_POINT('Ctrl Pts',(126.059483419057,-3.64178643031121,134.112744324372));
#39461=CARTESIAN_POINT('Ctrl Pts',(126.051737085792,-3.54803011613398,134.213096939402));
#39462=CARTESIAN_POINT('Ctrl Pts',(126.043990752526,-3.45027039490185,134.309330983284));
#39463=CARTESIAN_POINT('Ctrl Pts',(126.036242684523,-3.35248878105783,134.405586578114));
#39464=CARTESIAN_POINT('Ctrl Pts',(126.02849461652,-3.25070225472393,134.497721492255));
#39465=CARTESIAN_POINT('Ctrl Pts',(126.020746548517,-3.14530224565585,134.585399740079));
#39466=CARTESIAN_POINT('Ctrl Pts',(126.012990245775,-3.03979021620393,134.673171173387));
#39467=CARTESIAN_POINT('Ctrl Pts',(126.005233943034,-2.93065733334482,134.756476228086));
#39468=CARTESIAN_POINT('Ctrl Pts',(125.997477640292,-2.81832731104713,134.835019897424));
#39469=CARTESIAN_POINT('Ctrl Pts',(125.989717197778,-2.70593733483443,134.913605487883));
#39470=CARTESIAN_POINT('Ctrl Pts',(125.981956755263,-2.59034714836053,134.987424418911));
#39471=CARTESIAN_POINT('Ctrl Pts',(125.974196312749,-2.47200725315596,135.056226467148));
#39472=CARTESIAN_POINT('Ctrl Pts',(125.966423412484,-2.3534773882458,135.125138962542));
#39473=CARTESIAN_POINT('Ctrl Pts',(125.958650512218,-2.23218933999362,135.189018299303));
#39474=CARTESIAN_POINT('Ctrl Pts',(125.950877611953,-2.10861668581204,135.247661050219));
#39475=CARTESIAN_POINT('Ctrl Pts',(125.943387276191,-1.98953620887186,135.304171989427));
#39476=CARTESIAN_POINT('Ctrl Pts',(125.935896940429,-1.86833462794485,135.355820338244));
#39477=CARTESIAN_POINT('Ctrl Pts',(125.928406604667,-1.74544923784005,135.402467839089));
#39478=CARTESIAN_POINT('Ctrl Pts',(125.920632270548,-1.61790461081815,135.450883994107));
#39479=CARTESIAN_POINT('Ctrl Pts',(125.912857936429,-1.4881419478203,135.494065968866));
#39480=CARTESIAN_POINT('Ctrl Pts',(125.90508360231,-1.3566300425547,135.531805803937));
#39481=CARTESIAN_POINT('Ctrl Pts',(125.897318849363,-1.22528021395888,135.569499128033));
#39482=CARTESIAN_POINT('Ctrl Pts',(125.889554096416,-1.09218580465443,135.601763550466));
#39483=CARTESIAN_POINT('Ctrl Pts',(125.881789343468,-0.957835231167931,
135.628439258346));
#39484=CARTESIAN_POINT('Ctrl Pts',(125.874032302583,-0.823618096564934,
135.655088471538));
#39485=CARTESIAN_POINT('Ctrl Pts',(125.866275261698,-0.688147661637522,
135.67615994085));
#39486=CARTESIAN_POINT('Ctrl Pts',(125.858518220813,-0.551926798158095,
135.691543842285));
#39487=CARTESIAN_POINT('Ctrl Pts',(125.850767029573,-0.415808659891554,
135.7069161426));
#39488=CARTESIAN_POINT('Ctrl Pts',(125.843015838333,-0.278941606394287,
135.716609368413));
#39489=CARTESIAN_POINT('Ctrl Pts',(125.835264647093,-0.141837628489148,
135.72056496133));
#39490=CARTESIAN_POINT('Ctrl Pts',(125.827516750316,-0.00479192343189372,
135.724518873015));
#39491=CARTESIAN_POINT('Ctrl Pts',(125.819768853539,0.132490115765808,135.722739990836));
#39492=CARTESIAN_POINT('Ctrl Pts',(125.812020956762,0.269492682422311,135.715221718903));
#39493=CARTESIAN_POINT('Ctrl Pts',(125.804274680678,0.406466591095302,135.70770501963));
#39494=CARTESIAN_POINT('Ctrl Pts',(125.796528404594,0.543160753375989,135.694451339984));
#39495=CARTESIAN_POINT('Ctrl Pts',(125.788782128509,0.679061069929106,135.675506183632));
#39496=CARTESIAN_POINT('Ctrl Pts',(125.781035795244,0.814962389667395,135.656560887431));
#39497=CARTESIAN_POINT('Ctrl Pts',(125.773289461979,0.950069464764186,135.63192408467));
#39498=CARTESIAN_POINT('Ctrl Pts',(125.765543128713,1.08387540861196,135.601692913864));
#39499=CARTESIAN_POINT('Ctrl Pts',(125.75779506071,1.21771131737312,135.571454972997));
#39500=CARTESIAN_POINT('Ctrl Pts',(125.750046992707,1.35024513379401,135.535620257262));
#39501=CARTESIAN_POINT('Ctrl Pts',(125.742298924704,1.48098260630426,135.494336479159));
#39502=CARTESIAN_POINT('Ctrl Pts',(125.734542621963,1.61185902815617,135.453008824165));
#39503=CARTESIAN_POINT('Ctrl Pts',(125.726786319221,1.74093491889981,135.406220655915));
#39504=CARTESIAN_POINT('Ctrl Pts',(125.719030016479,1.86773305325146,135.354168998618));
#39505=CARTESIAN_POINT('Ctrl Pts',(125.711269573965,1.99459886358531,135.302089559784));
#39506=CARTESIAN_POINT('Ctrl Pts',(125.703509131451,2.11918414015567,135.244741197567));
#39507=CARTESIAN_POINT('Ctrl Pts',(125.695748688936,2.24103485588412,135.182367679828));
#39508=CARTESIAN_POINT('Ctrl Pts',(125.687975788671,2.36308117719877,135.11989403458));
#39509=CARTESIAN_POINT('Ctrl Pts',(125.680202888406,2.48238382507819,135.052379306389));
#39510=CARTESIAN_POINT('Ctrl Pts',(125.67242998814,2.59851567028782,134.980111971965));
#39511=CARTESIAN_POINT('Ctrl Pts',(125.664939652378,2.71042583040586,134.910471737179));
#39512=CARTESIAN_POINT('Ctrl Pts',(125.657449316616,2.81939146402898,134.836418608654));
#39513=CARTESIAN_POINT('Ctrl Pts',(125.649958980854,2.9250598826108,134.758245763298));
#39514=CARTESIAN_POINT('Ctrl Pts',(125.642184646735,3.03473475140013,134.677108970751));
#39515=CARTESIAN_POINT('Ctrl Pts',(125.634410312616,3.14120485872182,134.591276879437));
#39516=CARTESIAN_POINT('Ctrl Pts',(125.626635978497,3.24404184796695,134.501031491628));
#39517=CARTESIAN_POINT('Ctrl Pts',(125.61887122555,3.34675209981358,134.410897323195));
#39518=CARTESIAN_POINT('Ctrl Pts',(125.611106472603,3.4458378514233,134.316360935645));
#39519=CARTESIAN_POINT('Ctrl Pts',(125.603341719655,3.54090064662295,134.217746864864));
#39520=CARTESIAN_POINT('Ctrl Pts',(125.59558467877,3.63586902411424,134.119230738969));
#39521=CARTESIAN_POINT('Ctrl Pts',(125.587827637885,3.72682212714961,134.016645269205));
#39522=CARTESIAN_POINT('Ctrl Pts',(125.580070597,3.81339574321152,133.910354173283));
#39523=CARTESIAN_POINT('Ctrl Pts',(125.57231940576,3.89990407343612,133.804143232303));
#39524=CARTESIAN_POINT('Ctrl Pts',(125.56456821452,3.98203924441768,133.694232529241));
#39525=CARTESIAN_POINT('Ctrl Pts',(125.55681702328,4.05947524577584,133.581021164236));
#39526=CARTESIAN_POINT('Ctrl Pts',(125.549069126503,4.13687833476775,133.467857917081));
#39527=CARTESIAN_POINT('Ctrl Pts',(125.541321229726,4.20958600629661,133.351397120205));
#39528=CARTESIAN_POINT('Ctrl Pts',(125.533573332949,4.27731390494205,133.232069171139));
#39529=CARTESIAN_POINT('Ctrl Pts',(125.525827056865,4.34502763637119,133.112766182907));
#39530=CARTESIAN_POINT('Ctrl Pts',(125.518080780781,4.40776347397505,132.990597575213));
#39531=CARTESIAN_POINT('Ctrl Pts',(125.510334504697,4.46528181802819,132.86602047023));
#39532=CARTESIAN_POINT('Ctrl Pts',(125.502588171431,4.52280058666864,132.741442445648));
#39533=CARTESIAN_POINT('Ctrl Pts',(125.494841838166,4.57510162101877,132.614456243258));
#39534=CARTESIAN_POINT('Ctrl Pts',(125.4870955049,4.62199266187001,132.485540826859));
#39535=CARTESIAN_POINT('Ctrl Pts',(125.479347436897,4.6688942036447,132.356596540747));
#39536=CARTESIAN_POINT('Ctrl Pts',(125.471599368895,4.71038320749897,132.225722548274));
#39537=CARTESIAN_POINT('Ctrl Pts',(125.463851300892,4.74631679309538,132.093414519496));
#39538=CARTESIAN_POINT('Ctrl Pts',(125.45609499815,4.78228856933421,131.960965872171));
#39539=CARTESIAN_POINT('Ctrl Pts',(125.448338695408,4.812693030077,131.827080521866));
#39540=CARTESIAN_POINT('Ctrl Pts',(125.440582392666,4.83743798544688,131.692266468124));
#39541=CARTESIAN_POINT('Ctrl Pts',(125.432821950152,4.86219614794451,131.557380460063));
#39542=CARTESIAN_POINT('Ctrl Pts',(125.425061507638,4.88128873177235,131.421565147856));
#39543=CARTESIAN_POINT('Ctrl Pts',(125.417301065123,4.89467541300868,131.285334279826));
#39544=CARTESIAN_POINT('Ctrl Pts',(125.409528164858,4.90808358373416,131.148884721913));
#39545=CARTESIAN_POINT('Ctrl Pts',(125.401755264593,4.91576752609823,131.012018665699));
#39546=CARTESIAN_POINT('Ctrl Pts',(125.393982364327,4.91773906994455,130.875251395816));
#39547=CARTESIAN_POINT('Ctrl Pts',(125.386492028565,4.91963894320605,130.743455960688));
#39548=CARTESIAN_POINT('Ctrl Pts',(125.379001692803,4.91623453549151,130.611752562238));
#39549=CARTESIAN_POINT('Ctrl Pts',(125.371511357041,4.90758186806153,130.480596396606));
#39550=CARTESIAN_POINT('Ctrl Pts',(125.363737022922,4.89860113211608,130.344467405092));
#39551=CARTESIAN_POINT('Ctrl Pts',(125.355962688803,4.88393785648686,130.208496746491));
#39552=CARTESIAN_POINT('Ctrl Pts',(125.348188354684,4.86359776046143,130.073197238468));
#39553=CARTESIAN_POINT('Ctrl Pts',(125.340423601737,4.84328273178652,129.938064474996));
#39554=CARTESIAN_POINT('Ctrl Pts',(125.33265884879,4.81730486058022,129.803601599262));
#39555=CARTESIAN_POINT('Ctrl Pts',(125.324894095842,4.7857218127802,129.670319263303));
#39556=CARTESIAN_POINT('Ctrl Pts',(125.317137054957,4.7541701337085,129.537169305238));
#39557=CARTESIAN_POINT('Ctrl Pts',(125.309380014072,4.71702444646845,129.405197931532));
#39558=CARTESIAN_POINT('Ctrl Pts',(125.301622973187,4.67439389130825,129.274908162797));
#39559=CARTESIAN_POINT('Ctrl Pts',(125.293871781947,4.63179548418129,129.144716646589));
#39560=CARTESIAN_POINT('Ctrl Pts',(125.286120590707,4.58372056304116,129.01620458133));
#39561=CARTESIAN_POINT('Ctrl Pts',(125.278369399467,4.53032868556305,128.889861972159));
#39562=CARTESIAN_POINT('Ctrl Pts',(125.27062150269,4.47695950105715,128.763573061967));
#39563=CARTESIAN_POINT('Ctrl Pts',(125.262873605913,4.41827800674933,128.639452133297));
#39564=CARTESIAN_POINT('Ctrl Pts',(125.255125709136,4.35449260722029,128.517971062795));
#39565=CARTESIAN_POINT('Ctrl Pts',(125.247379433052,4.29072055022178,128.396515403515));
#39566=CARTESIAN_POINT('Ctrl Pts',(125.239633156967,4.22184689320682,128.277698849975));
#39567=CARTESIAN_POINT('Ctrl Pts',(125.231886880883,4.14812671650236,128.16197006991));
#39568=CARTESIAN_POINT('Ctrl Pts',(125.224140547618,4.07440599561236,128.046240435563));
#39569=CARTESIAN_POINT('Ctrl Pts',(125.216394214353,3.99583889369552,127.93359894992));
#39570=CARTESIAN_POINT('Ctrl Pts',(125.208647881087,3.91272445576253,127.824466257731));
#39571=CARTESIAN_POINT('Ctrl Pts',(125.200899813084,3.82959140492744,127.715309126032));
#39572=CARTESIAN_POINT('Ctrl Pts',(125.193151745081,3.74190922852344,127.609662662353));
#39573=CARTESIAN_POINT('Ctrl Pts',(125.185403677078,3.65001771749608,127.507914997741));
#39574=CARTESIAN_POINT('Ctrl Pts',(125.177647374337,3.55802854307727,127.4060591945));
#39575=CARTESIAN_POINT('Ctrl Pts',(125.169891071595,3.46182135973703,127.308110758407));
#39576=CARTESIAN_POINT('Ctrl Pts',(125.162134768853,3.36177373099847,127.214421837577));
#39577=CARTESIAN_POINT('Ctrl Pts',(125.154374326339,3.261672703828,127.120682912149));
#39578=CARTESIAN_POINT('Ctrl Pts',(125.146613883825,3.15772744310006,127.031208286924));
#39579=CARTESIAN_POINT('Ctrl Pts',(125.13885344131,3.05034838376378,126.946309581075));
#39580=CARTESIAN_POINT('Ctrl Pts',(125.131080541045,2.9427969500288,126.861274588287));
#39581=CARTESIAN_POINT('Ctrl Pts',(125.12330764078,2.83180101922627,126.780830423432));
#39582=CARTESIAN_POINT('Ctrl Pts',(125.115534740514,2.71780050922964,126.705245657659));
#39583=CARTESIAN_POINT('Ctrl Pts',(125.108044404752,2.60794420492189,126.632408588509));
#39584=CARTESIAN_POINT('Ctrl Pts',(125.10055406899,2.49529824024551,126.564083909241));
#39585=CARTESIAN_POINT('Ctrl Pts',(125.093063733228,2.3802758654664,126.500470532216));
#39586=CARTESIAN_POINT('Ctrl Pts',(125.085289399109,2.26089238238665,126.434445234665));
#39587=CARTESIAN_POINT('Ctrl Pts',(125.07751506499,2.1385705577689,126.373286401496));
#39588=CARTESIAN_POINT('Ctrl Pts',(125.069740730871,2.01374493105133,126.317266411383));
#39589=CARTESIAN_POINT('Ctrl Pts',(125.061975977924,1.88907314076279,126.2613154609));
#39590=CARTESIAN_POINT('Ctrl Pts',(125.054211224977,1.76190404128946,126.210490910905));
#39591=CARTESIAN_POINT('Ctrl Pts',(125.04644647203,1.63269842850033,126.16502026531));
#39592=CARTESIAN_POINT('Ctrl Pts',(125.038689431145,1.50362114454748,126.119594781801));
#39593=CARTESIAN_POINT('Ctrl Pts',(125.03093239026,1.37251173893809,126.079512749428));
#39594=CARTESIAN_POINT('Ctrl Pts',(125.023175349375,1.23985241012979,126.044954240338));
#39595=CARTESIAN_POINT('Ctrl Pts',(125.015424158135,1.10729312075292,126.010421792089));
#39596=CARTESIAN_POINT('Ctrl Pts',(125.007672966895,0.973186611428278,125.981404674443));
#39597=CARTESIAN_POINT('Ctrl Pts',(124.999921775654,0.838031382177934,125.958033506755));
#39598=CARTESIAN_POINT('Ctrl Pts',(124.992173878877,0.702933597505588,125.934672272437));
#39599=CARTESIAN_POINT('Ctrl Pts',(124.9844259821,0.566788363879681,125.916952281776));
#39600=CARTESIAN_POINT('Ctrl Pts',(124.976678085323,0.430105332253433,125.904953258949));
#39601=CARTESIAN_POINT('Ctrl Pts',(124.968931809239,0.293450891770855,125.89295674606));
#39602=CARTESIAN_POINT('Ctrl Pts',(124.961185533155,0.156259266268752,125.886678854866));
#39603=CARTESIAN_POINT('Ctrl Pts',(124.953439257071,0.0190458097673841,
125.886147494934));
#39604=CARTESIAN_POINT('Ctrl Pts',(124.945692923806,-0.118168659612549,
125.88561613108));
#39605=CARTESIAN_POINT('Ctrl Pts',(124.93794659054,-0.255404569351039,125.890831384647));
#39606=CARTESIAN_POINT('Ctrl Pts',(124.930200257275,-0.392146377973822,
125.901769029361));
#39607=CARTESIAN_POINT('Ctrl Pts',(124.922452189272,-0.528918808976545,
125.912709123484));
#39608=CARTESIAN_POINT('Ctrl Pts',(124.914704121269,-0.665196529035951,
125.929374127604));
#39609=CARTESIAN_POINT('Ctrl Pts',(124.906956053266,-0.800469327202789,
125.951687960287));
#39610=CARTESIAN_POINT('Ctrl Pts',(124.899199750524,-0.935885894909286,
125.974025508376));
#39611=CARTESIAN_POINT('Ctrl Pts',(124.891443447782,-1.070295020825,126.002023814217));
#39612=CARTESIAN_POINT('Ctrl Pts',(124.883687145041,-1.20319635045958,126.035555567583));
#39613=CARTESIAN_POINT('Ctrl Pts',(124.875926702526,-1.33616861353546,126.069105217856));
#39614=CARTESIAN_POINT('Ctrl Pts',(124.868166260012,-1.46763110221842,126.108194089115));
#39615=CARTESIAN_POINT('Ctrl Pts',(124.860405817498,-1.59709979235588,126.152645308591));
#39616=CARTESIAN_POINT('Ctrl Pts',(124.852632917233,-1.72677631712843,126.197167885109));
#39617=CARTESIAN_POINT('Ctrl Pts',(124.844860016967,-1.85445228314264,126.2470698692));
#39618=CARTESIAN_POINT('Ctrl Pts',(124.837087116702,-1.97966394752975,126.302126314761));
#39619=CARTESIAN_POINT('Ctrl Pts',(124.82959678094,-2.10032385252699,126.355181319848));
#39620=CARTESIAN_POINT('Ctrl Pts',(124.822106445178,-2.21869523568927,126.413022402162));
#39621=CARTESIAN_POINT('Ctrl Pts',(124.814616109416,-2.33438737455136,126.475409399542));
#39622=CARTESIAN_POINT('Ctrl Pts',(124.806840801173,-2.45448106187394,126.540169932366));
#39623=CARTESIAN_POINT('Ctrl Pts',(124.79906549293,-2.5720680717935,126.610034297799));
#39624=CARTESIAN_POINT('Ctrl Pts',(124.791290184687,-2.68668419202054,126.684784047717));
#39625=CARTESIAN_POINT('Ctrl Pts',(124.783524672129,-2.80115591367417,126.759439624519));
#39626=CARTESIAN_POINT('Ctrl Pts',(124.775759159571,-2.91266386903581,126.83896812665));
#39627=CARTESIAN_POINT('Ctrl Pts',(124.767993647013,-3.02076745621588,126.923104759217));
#39628=CARTESIAN_POINT('Ctrl Pts',(124.760237457247,-3.12874126095208,127.007140382576));
#39629=CARTESIAN_POINT('Ctrl Pts',(124.75248126748,-3.23331853092937,127.095772879485));
#39630=CARTESIAN_POINT('Ctrl Pts',(124.744725077714,-3.33408726690759,127.188693990353));
#39631=CARTESIAN_POINT('Ctrl Pts',(124.736974173943,-3.43478732700543,127.281551773651));
#39632=CARTESIAN_POINT('Ctrl Pts',(124.729223270173,-3.53168373067039,127.378692092438));
#39633=CARTESIAN_POINT('Ctrl Pts',(124.721472366403,-3.62439717815534,127.479766182529));
#39634=CARTESIAN_POINT('Ctrl Pts',(124.713725066416,-3.71706751851891,127.580793278217));
#39635=CARTESIAN_POINT('Ctrl Pts',(124.705977766429,-3.80555850919785,127.685750218183));
#39636=CARTESIAN_POINT('Ctrl Pts',(124.698230466441,-3.88952767779987,127.79425139926));
#39637=CARTESIAN_POINT('Ctrl Pts',(124.690485090805,-3.97347598930845,127.902725629741));
#39638=CARTESIAN_POINT('Ctrl Pts',(124.682739715169,-4.05290447591747,128.014742039753));
#39639=CARTESIAN_POINT('Ctrl Pts',(124.674994339533,-4.12751119792334,128.129882280859));
#39640=CARTESIAN_POINT('Ctrl Pts',(124.667246590171,-4.20214078465265,128.245057808996));
#39641=CARTESIAN_POINT('Ctrl Pts',(124.65949884081,-4.27194543615605,128.363358756285));
#39642=CARTESIAN_POINT('Ctrl Pts',(124.651751091448,-4.33666672914206,128.484338043785));
#39643=CARTESIAN_POINT('Ctrl Pts',(124.644002337527,-4.4013964137794,128.605333017251));
#39644=CARTESIAN_POINT('Ctrl Pts',(124.636253583606,-4.46104124962412,128.729006674073));
#39645=CARTESIAN_POINT('Ctrl Pts',(124.628504829684,-4.51538941372329,128.854888508267));
#39646=CARTESIAN_POINT('Ctrl Pts',(124.620749163676,-4.56978605777646,128.98088263228));
#39647=CARTESIAN_POINT('Ctrl Pts',(124.612993497668,-4.61887644198245,129.109088506853));
#39648=CARTESIAN_POINT('Ctrl Pts',(124.605237831659,-4.66249726811931,129.239016474165));
#39649=CARTESIAN_POINT('Ctrl Pts',(124.598475136376,-4.70053324786056,129.352309549289));
#39650=CARTESIAN_POINT('Ctrl Pts',(124.591712441093,-4.73441128232443,129.466911553406));
#39651=CARTESIAN_POINT('Ctrl Pts',(124.584949745809,-4.76405452823405,129.582490119308));
#39652=CARTESIAN_POINT('Ctrl Pts',(126.334922597491,-4.76405452823406,129.582490119308));
#39653=CARTESIAN_POINT('Ctrl Pts',(126.327281976563,-4.79769213240394,129.713642627445));
#39654=CARTESIAN_POINT('Ctrl Pts',(126.319641355634,-4.82589983755495,129.846146911425));
#39655=CARTESIAN_POINT('Ctrl Pts',(126.312000734706,-4.84858740908575,129.979507176672));
#39656=CARTESIAN_POINT('Ctrl Pts',(126.304143851594,-4.87191713572563,130.116642106631));
#39657=CARTESIAN_POINT('Ctrl Pts',(126.296286968481,-4.88940952022633,130.25468174393));
#39658=CARTESIAN_POINT('Ctrl Pts',(126.288430085369,-4.90102358601449,130.393081063212));
#39659=CARTESIAN_POINT('Ctrl Pts',(126.280573202257,-4.91263765180265,130.531480382494));
#39660=CARTESIAN_POINT('Ctrl Pts',(126.272716319145,-4.91837341917953,130.670238922525));
#39661=CARTESIAN_POINT('Ctrl Pts',(126.264859436032,-4.91824798511455,130.808812517913));
#39662=CARTESIAN_POINT('',(126.610140564052,-4.91824997363776,130.803851390504));
#39663=CARTESIAN_POINT('Ctrl Pts',(126.679856726692,-4.76405452823407,129.582490119308));
#39664=CARTESIAN_POINT('Ctrl Pts',(126.671653679144,-4.80002762432874,129.722748675014));
#39665=CARTESIAN_POINT('Ctrl Pts',(126.663450631596,-4.82984162546053,129.864749417658));
#39666=CARTESIAN_POINT('Ctrl Pts',(126.655247584047,-4.85333911657205,130.007942083093));
#39667=CARTESIAN_POINT('Ctrl Pts',(126.647062836702,-4.87678418706063,130.150815299584));
#39668=CARTESIAN_POINT('Ctrl Pts',(126.638878089357,-4.89394079707537,130.294874821921));
#39669=CARTESIAN_POINT('Ctrl Pts',(126.630693342012,-4.90470209545733,130.439558729802));
#39670=CARTESIAN_POINT('Ctrl Pts',(126.623842416025,-4.91370968672766,130.560664330568));
#39671=CARTESIAN_POINT('Ctrl Pts',(126.616991490039,-4.91823737879227,130.68220703363));
#39672=CARTESIAN_POINT('Ctrl Pts',(126.610140564052,-4.91824997363776,130.803851390504));
#39673=CARTESIAN_POINT('Ctrl Pts',(126.610140564008,-4.91824997363784,130.803851391281));
#39674=CARTESIAN_POINT('Ctrl Pts',(126.602085987719,-4.91826478126958,130.946867642582));
#39675=CARTESIAN_POINT('Ctrl Pts',(126.59403141143,-4.91203717351668,131.089784258798));
#39676=CARTESIAN_POINT('Ctrl Pts',(126.585976835141,-4.89961914306179,131.232046618556));
#39677=CARTESIAN_POINT('Ctrl Pts',(126.577913721954,-4.88718795096255,131.374459759597));
#39678=CARTESIAN_POINT('Ctrl Pts',(126.569850608766,-4.86855327872846,131.516216918705));
#39679=CARTESIAN_POINT('Ctrl Pts',(126.561787495578,-4.84381863382357,131.656771378364));
#39680=CARTESIAN_POINT('Ctrl Pts',(126.553707322419,-4.81903165524257,131.797623223798));
#39681=CARTESIAN_POINT('Ctrl Pts',(126.545627149259,-4.78811896234214,131.937266942921));
#39682=CARTESIAN_POINT('Ctrl Pts',(126.537546976099,-4.75123499494181,132.075167088017));
#39683=CARTESIAN_POINT('Ctrl Pts',(126.529458092486,-4.71431126650594,132.213215889914));
#39684=CARTESIAN_POINT('Ctrl Pts',(126.521369208874,-4.67140352368006,132.349517039915));
#39685=CARTESIAN_POINT('Ctrl Pts',(126.513280325261,-4.62271522172352,132.483552995272));
#39686=CARTESIAN_POINT('Ctrl Pts',(126.505173147772,-4.57391680595623,132.617892087301));
#39687=CARTESIAN_POINT('Ctrl Pts',(126.497065970283,-4.51931181977965,132.749955421507));
#39688=CARTESIAN_POINT('Ctrl Pts',(126.488958792793,-4.45915152249253,132.879246340191));
#39689=CARTESIAN_POINT('Ctrl Pts',(126.48121014724,-4.40165175507547,133.002819495389));
#39690=CARTESIAN_POINT('Ctrl Pts',(126.473461501687,-4.33907763532179,133.123859981535));
#39691=CARTESIAN_POINT('Ctrl Pts',(126.465712856134,-4.27168572665355,133.241958639227));
#39692=CARTESIAN_POINT('Ctrl Pts',(126.457938522015,-4.20407039810127,133.360448821494));
#39693=CARTESIAN_POINT('Ctrl Pts',(126.450164187896,-4.13141412440042,133.476311229307));
#39694=CARTESIAN_POINT('Ctrl Pts',(126.442389853777,-4.05394634133551,133.589087197335));
#39695=CARTESIAN_POINT('Ctrl Pts',(126.434625100829,-3.97657403038968,133.701724179062));
#39696=CARTESIAN_POINT('Ctrl Pts',(126.426860347882,-3.89440222776585,133.811281970189));
#39697=CARTESIAN_POINT('Ctrl Pts',(126.419095594935,-3.80770613665861,133.917326572946));
#39698=CARTESIAN_POINT('Ctrl Pts',(126.41133855405,-3.72109615333132,134.023265850708));
#39699=CARTESIAN_POINT('Ctrl Pts',(126.403581513165,-3.62997106981866,134.125698583334));
#39700=CARTESIAN_POINT('Ctrl Pts',(126.39582447228,-3.53464904136758,134.22422014931));
#39701=CARTESIAN_POINT('Ctrl Pts',(126.38807328104,-3.43939889599953,134.322667419407));
#39702=CARTESIAN_POINT('Ctrl Pts',(126.3803220898,-3.3399583760858,134.417209113696));
#39703=CARTESIAN_POINT('Ctrl Pts',(126.37257089856,-3.23668528365419,134.507474366437));
#39704=CARTESIAN_POINT('Ctrl Pts',(126.364823001783,-3.13345608504191,134.597701254038));
#39705=CARTESIAN_POINT('Ctrl Pts',(126.357075105006,-3.02639784751469,134.683655058407));
#39706=CARTESIAN_POINT('Ctrl Pts',(126.349327208229,-2.91590437124619,134.765002580714));
#39707=CARTESIAN_POINT('Ctrl Pts',(126.341580932145,-2.80543400783096,134.846333086872));
#39708=CARTESIAN_POINT('Ctrl Pts',(126.33383465606,-2.69153014960811,134.923058995845));
#39709=CARTESIAN_POINT('Ctrl Pts',(126.326088379976,-2.57461842037946,134.994888394821));
#39710=CARTESIAN_POINT('Ctrl Pts',(126.318342046711,-2.45770582813507,135.066718324024));
#39711=CARTESIAN_POINT('Ctrl Pts',(126.310595713446,-2.33778565369613,135.133651466443));
#39712=CARTESIAN_POINT('Ctrl Pts',(126.30284938018,-2.21531080094182,135.195440338743));
#39713=CARTESIAN_POINT('Ctrl Pts',(126.295101312177,-2.09280852079317,135.257243048232));
#39714=CARTESIAN_POINT('Ctrl Pts',(126.287353244174,-1.96775077290358,135.313899019142));
#39715=CARTESIAN_POINT('Ctrl Pts',(126.279605176171,-1.84061288255488,135.365207828236));
#39716=CARTESIAN_POINT('Ctrl Pts',(126.27184887343,-1.71333986854343,135.416571168942));
#39717=CARTESIAN_POINT('Ctrl Pts',(126.264092570688,-1.5839826588938,135.462575848824));
#39718=CARTESIAN_POINT('Ctrl Pts',(126.256336267946,-1.45303480906168,135.503070324087));
#39719=CARTESIAN_POINT('Ctrl Pts',(126.248575825432,-1.32201706841934,135.543586412471));
#39720=CARTESIAN_POINT('Ctrl Pts',(126.240815382918,-1.18940737378025,135.578586336396));
#39721=CARTESIAN_POINT('Ctrl Pts',(126.233054940403,-1.05571111496386,135.607969376014));
#39722=CARTESIAN_POINT('Ctrl Pts',(126.225282040138,-0.921800235043832,
135.637399583897));
#39723=CARTESIAN_POINT('Ctrl Pts',(126.217509139873,-0.7867996906322,135.661194821285));
#39724=CARTESIAN_POINT('Ctrl Pts',(126.209736239607,-0.651222556919777,
135.679305975604));
#39725=CARTESIAN_POINT('Ctrl Pts',(126.202245903845,-0.520573993515626,
135.696758743845));
#39726=CARTESIAN_POINT('Ctrl Pts',(126.194755568083,-0.389390340648915,
135.7089334872));
#39727=CARTESIAN_POINT('Ctrl Pts',(126.187265232321,-0.258130224993057,
135.715832072176));
#39728=CARTESIAN_POINT('Ctrl Pts',(126.179490898202,-0.121893342156839,
135.722992219098));
#39729=CARTESIAN_POINT('Ctrl Pts',(126.171716564083,0.0148574735939531,
135.72449089982));
#39730=CARTESIAN_POINT('Ctrl Pts',(126.163942229964,0.151612318479945,135.720273225352));
#39731=CARTESIAN_POINT('Ctrl Pts',(126.156177477017,0.288198625241561,135.71606074879));
#39732=CARTESIAN_POINT('Ctrl Pts',(126.14841272407,0.424788564230456,135.706145946218));
#39733=CARTESIAN_POINT('Ctrl Pts',(126.140647971122,0.560868246781902,135.690525767482));
#39734=CARTESIAN_POINT('Ctrl Pts',(126.132890930237,0.696812773073972,135.674921102928));
#39735=CARTESIAN_POINT('Ctrl Pts',(126.125133889353,0.832247665570025,135.653622383415));
#39736=CARTESIAN_POINT('Ctrl Pts',(126.117376848468,0.966660534048905,135.626678574152));
#39737=CARTESIAN_POINT('Ctrl Pts',(126.109625657227,1.10097204073836,135.599755083425));
#39738=CARTESIAN_POINT('Ctrl Pts',(126.101874465987,1.2342626756864,135.567195052793));
#39739=CARTESIAN_POINT('Ctrl Pts',(126.094123274747,1.36602701830681,135.529099049242));
#39740=CARTESIAN_POINT('Ctrl Pts',(126.08637537797,1.49773535756677,135.491019237509));
#39741=CARTESIAN_POINT('Ctrl Pts',(126.078627481193,1.62791831994757,135.447408241031));
#39742=CARTESIAN_POINT('Ctrl Pts',(126.070879584416,1.75608271722196,135.398417272939));
#39743=CARTESIAN_POINT('Ctrl Pts',(126.063133308332,1.88422030526735,135.349436552701));
#39744=CARTESIAN_POINT('Ctrl Pts',(126.055387032248,2.01033980310264,135.295078238788));
#39745=CARTESIAN_POINT('Ctrl Pts',(126.047640756164,2.13396555615088,135.235542634552));
#39746=CARTESIAN_POINT('Ctrl Pts',(126.039894422898,2.25759222177643,135.176006590838));
#39747=CARTESIAN_POINT('Ctrl Pts',(126.032148089633,2.37872475363574,135.111293350177));
#39748=CARTESIAN_POINT('Ctrl Pts',(126.024401756368,2.49691013138188,135.041650182642));
#39749=CARTESIAN_POINT('Ctrl Pts',(126.016653688365,2.61512197592384,134.971991419002));
#39750=CARTESIAN_POINT('Ctrl Pts',(126.008905620362,2.73038501627021,134.897400730059));
#39751=CARTESIAN_POINT('Ctrl Pts',(126.001157552359,2.84227370575046,134.818169686779));
#39752=CARTESIAN_POINT('Ctrl Pts',(125.993401249617,2.95428131186139,134.738854435804));
#39753=CARTESIAN_POINT('Ctrl Pts',(125.985644946875,3.06290708350767,134.654889204942));
#39754=CARTESIAN_POINT('Ctrl Pts',(125.977888644133,3.16775674382266,134.566607323255));
#39755=CARTESIAN_POINT('Ctrl Pts',(125.970128201619,3.27266236555832,134.478278322869));
#39756=CARTESIAN_POINT('Ctrl Pts',(125.962367759105,3.37378757193022,134.38562834487));
#39757=CARTESIAN_POINT('Ctrl Pts',(125.954607316591,3.47077444893512,134.289028146487));
#39758=CARTESIAN_POINT('Ctrl Pts',(125.946834416325,3.56791701788514,134.192272876891));
#39759=CARTESIAN_POINT('Ctrl Pts',(125.93906151606,3.66090771684249,134.091555002503));
#39760=CARTESIAN_POINT('Ctrl Pts',(125.931288615794,3.74942789633278,133.987279641466));
#39761=CARTESIAN_POINT('Ctrl Pts',(125.923798280032,3.83473014433063,133.886794952455));
#39762=CARTESIAN_POINT('Ctrl Pts',(125.91630794427,3.91588106943581,133.783007176151));
#39763=CARTESIAN_POINT('Ctrl Pts',(125.908817608508,3.99263434307331,133.676303177056));
#39764=CARTESIAN_POINT('Ctrl Pts',(125.901043274389,4.07229774040865,133.565553463405));
#39765=CARTESIAN_POINT('Ctrl Pts',(125.89326894027,4.1474757791831,133.451311202667));
#39766=CARTESIAN_POINT('Ctrl Pts',(125.885494606151,4.21784666428545,133.333975722493));
#39767=CARTESIAN_POINT('Ctrl Pts',(125.877729853204,4.28813082356114,133.216784847812));
#39768=CARTESIAN_POINT('Ctrl Pts',(125.869965100257,4.35361941777396,133.09650867074));
#39769=CARTESIAN_POINT('Ctrl Pts',(125.862200347309,4.41403211136707,132.973577891681));
#39770=CARTESIAN_POINT('Ctrl Pts',(125.854443306424,4.4743848022214,132.850769209205));
#39771=CARTESIAN_POINT('Ctrl Pts',(125.846686265539,4.52967145385982,132.725311520285));
#39772=CARTESIAN_POINT('Ctrl Pts',(125.838929224654,4.57965630266858,132.597662380217));
#39773=CARTESIAN_POINT('Ctrl Pts',(125.831178033414,4.62960345751375,132.470109501359));
#39774=CARTESIAN_POINT('Ctrl Pts',(125.823426842174,4.67425662558844,132.340368823311));
#39775=CARTESIAN_POINT('Ctrl Pts',(125.815675650934,4.7134272245756,132.208919929638));
#39776=CARTESIAN_POINT('Ctrl Pts',(125.807927754157,4.75258117501339,132.077526905252));
#39777=CARTESIAN_POINT('Ctrl Pts',(125.80017985738,4.78625707961104,131.944427483174));
#39778=CARTESIAN_POINT('Ctrl Pts',(125.792431960603,4.81431557797499,131.810118331018));
#39779=CARTESIAN_POINT('Ctrl Pts',(125.784685684519,4.84236820710598,131.675837273441));
#39780=CARTESIAN_POINT('Ctrl Pts',(125.776939408435,4.86480568732303,131.540347371576));
#39781=CARTESIAN_POINT('Ctrl Pts',(125.76919313235,4.88153943659325,131.404157075946));
#39782=CARTESIAN_POINT('Ctrl Pts',(125.761446799085,4.8982733093882,131.26796577499));
#39783=CARTESIAN_POINT('Ctrl Pts',(125.75370046582,4.90930331954209,131.131074457999));
#39784=CARTESIAN_POINT('Ctrl Pts',(125.745954132554,4.91459263380777,130.993997919335));
#39785=CARTESIAN_POINT('Ctrl Pts',(125.738206064551,4.91988313257869,130.856890683332));
#39786=CARTESIAN_POINT('Ctrl Pts',(125.730457996548,4.91943036221618,130.719598533718));
#39787=CARTESIAN_POINT('Ctrl Pts',(125.722709928545,4.91324961126213,130.582637096187));
#39788=CARTESIAN_POINT('Ctrl Pts',(125.714953625804,4.90706229133238,130.445530094411));
#39789=CARTESIAN_POINT('Ctrl Pts',(125.707197323062,4.89513484749634,130.308754898037));
#39790=CARTESIAN_POINT('Ctrl Pts',(125.69944102032,4.87753460265541,130.172823395861));
#39791=CARTESIAN_POINT('Ctrl Pts',(125.691680577806,4.85992496403381,130.036819342948));
#39792=CARTESIAN_POINT('Ctrl Pts',(125.683920135292,4.83663655772362,129.901660266602));
#39793=CARTESIAN_POINT('Ctrl Pts',(125.676159692777,4.80778785102174,129.76784769335));
#39794=CARTESIAN_POINT('Ctrl Pts',(125.668386792512,4.77889283381485,129.633820312275));
#39795=CARTESIAN_POINT('Ctrl Pts',(125.660613892246,4.74441977782415,129.501144132331));
#39796=CARTESIAN_POINT('Ctrl Pts',(125.652840991981,4.70453728259173,129.370306218596));
#39797=CARTESIAN_POINT('Ctrl Pts',(125.645350656219,4.66610461651938,129.244224592588));
#39798=CARTESIAN_POINT('Ctrl Pts',(125.637860320457,4.6226490781343,129.119850192736));
#39799=CARTESIAN_POINT('Ctrl Pts',(125.630369984695,4.57436300088649,128.997599371961));
#39800=CARTESIAN_POINT('Ctrl Pts',(125.622595650576,4.5242461423431,128.870713374157));
#39801=CARTESIAN_POINT('Ctrl Pts',(125.614821316457,4.46876645915886,128.745713228533));
#39802=CARTESIAN_POINT('Ctrl Pts',(125.607046982338,4.40808597887739,128.623085516776));
#39803=CARTESIAN_POINT('Ctrl Pts',(125.599282229391,4.34748028186456,128.500608932715));
#39804=CARTESIAN_POINT('Ctrl Pts',(125.591517476444,4.28168671251511,128.380499312054));
#39805=CARTESIAN_POINT('Ctrl Pts',(125.583752723496,4.21091610306165,128.263225313125));
#39806=CARTESIAN_POINT('Ctrl Pts',(125.575995682611,4.14021578397538,128.146067792386));
#39807=CARTESIAN_POINT('Ctrl Pts',(125.568238641726,4.06454846280301,128.031740621227));
#39808=CARTESIAN_POINT('Ctrl Pts',(125.560481600841,3.98417165778152,127.92068947407));
#39809=CARTESIAN_POINT('Ctrl Pts',(125.552730409601,3.90385546553339,127.809722071446));
#39810=CARTESIAN_POINT('Ctrl Pts',(125.544979218361,3.81883708670207,127.702026090923));
#39811=CARTESIAN_POINT('Ctrl Pts',(125.537228027121,3.72941807517629,127.598019418778));
#39812=CARTESIAN_POINT('Ctrl Pts',(125.529480130344,3.64003706911622,127.494056952243));
#39813=CARTESIAN_POINT('Ctrl Pts',(125.521732233567,3.54625940476471,127.393780971186));
#39814=CARTESIAN_POINT('Ctrl Pts',(125.51398433679,3.44842761495544,127.297577184431));
#39815=CARTESIAN_POINT('Ctrl Pts',(125.506238060706,3.35061628944766,127.201393521434));
#39816=CARTESIAN_POINT('Ctrl Pts',(125.498491784621,3.24875280385875,127.109280632382));
#39817=CARTESIAN_POINT('Ctrl Pts',(125.490745508537,3.14321705126064,127.021587873776));
#39818=CARTESIAN_POINT('Ctrl Pts',(125.482999175272,3.03768051962172,126.933894467841));
#39819=CARTESIAN_POINT('Ctrl Pts',(125.475252842007,2.92847196758488,126.850621507323));
#39820=CARTESIAN_POINT('Ctrl Pts',(125.467506508741,2.8160045969575,126.772078240002));
#39821=CARTESIAN_POINT('Ctrl Pts',(125.459758440738,2.70351204004265,126.693517383461));
#39822=CARTESIAN_POINT('Ctrl Pts',(125.452010372735,2.58775953281585,126.619688551576));
#39823=CARTESIAN_POINT('Ctrl Pts',(125.444262304732,2.46918914960827,126.550857589948));
#39824=CARTESIAN_POINT('Ctrl Pts',(125.436506001991,2.35049274838578,126.481953473954));
#39825=CARTESIAN_POINT('Ctrl Pts',(125.428749699249,2.2289728272646,126.418058035696));
#39826=CARTESIAN_POINT('Ctrl Pts',(125.420993396507,2.10509644245668,126.359391322908));
#39827=CARTESIAN_POINT('Ctrl Pts',(125.413232953993,1.98115394109267,126.300693297928));
#39828=CARTESIAN_POINT('Ctrl Pts',(125.405472511479,1.85485282979789,126.24722971151));
#39829=CARTESIAN_POINT('Ctrl Pts',(125.397712068964,1.72667909151098,126.1991719811));
#39830=CARTESIAN_POINT('Ctrl Pts',(125.389939168699,1.5982995973603,126.151037104154));
#39831=CARTESIAN_POINT('Ctrl Pts',(125.382166268433,1.46804184077466,126.108325546431));
#39832=CARTESIAN_POINT('Ctrl Pts',(125.374393368168,1.33640673556999,126.071158730933));
#39833=CARTESIAN_POINT('Ctrl Pts',(125.366903032406,1.20955689800798,126.035343022797));
#39834=CARTESIAN_POINT('Ctrl Pts',(125.359412696644,1.0814284129874,126.004675996831));
#39835=CARTESIAN_POINT('Ctrl Pts',(125.351922360882,0.952475530938753,125.979220886381));
#39836=CARTESIAN_POINT('Ctrl Pts',(125.344148026763,0.818633361173232,125.952800637681));
#39837=CARTESIAN_POINT('Ctrl Pts',(125.336373692644,0.683479074543296,125.931911634402));
#39838=CARTESIAN_POINT('Ctrl Pts',(125.328599358525,0.547509625850272,125.916680567471));
#39839=CARTESIAN_POINT('Ctrl Pts',(125.320834605577,0.411707747350917,125.901468271468));
#39840=CARTESIAN_POINT('Ctrl Pts',(125.31306985263,0.275093090476897,125.891900080925));
#39841=CARTESIAN_POINT('Ctrl Pts',(125.305305099683,0.138173910728253,125.888051937988));
#39842=CARTESIAN_POINT('Ctrl Pts',(125.297548058798,0.00139072103915638,
125.884207617081));
#39843=CARTESIAN_POINT('Ctrl Pts',(125.289791017913,-0.135696001340689,
125.886072048786));
#39844=CARTESIAN_POINT('Ctrl Pts',(125.282033977028,-0.27257210300288,125.893669473627));
#39845=CARTESIAN_POINT('Ctrl Pts',(125.274282785788,-0.409344985331323,
125.90126116919));
#39846=CARTESIAN_POINT('Ctrl Pts',(125.266531594548,-0.545907174300209,
125.914577231053));
#39847=CARTESIAN_POINT('Ctrl Pts',(125.258780403308,-0.681744093107058,
125.933589831128));
#39848=CARTESIAN_POINT('Ctrl Pts',(125.251032506531,-0.817523277600494,
125.952594350342));
#39849=CARTESIAN_POINT('Ctrl Pts',(125.243284609754,-0.952577418655537,
125.977290538144));
#39850=CARTESIAN_POINT('Ctrl Pts',(125.235536712977,-1.08639686115177,126.007598697001));
#39851=CARTESIAN_POINT('Ctrl Pts',(125.227790436893,-1.22018831150554,126.037900516045));
#39852=CARTESIAN_POINT('Ctrl Pts',(125.220044160809,-1.35274519595211,126.07381188488));
#39853=CARTESIAN_POINT('Ctrl Pts',(125.212297884724,-1.48356824948902,126.115202024427));
#39854=CARTESIAN_POINT('Ctrl Pts',(125.204551551459,-1.61439226873209,126.156592469507));
#39855=CARTESIAN_POINT('Ctrl Pts',(125.196805218194,-1.74348205877243,126.203461648067));
#39856=CARTESIAN_POINT('Ctrl Pts',(125.189058884928,-1.87035409502309,126.255629077705));
#39857=CARTESIAN_POINT('Ctrl Pts',(125.181310816925,-1.99725454338729,126.307808189876));
#39858=CARTESIAN_POINT('Ctrl Pts',(125.173562748922,-2.12193588816264,126.365287765485));
#39859=CARTESIAN_POINT('Ctrl Pts',(125.165814680919,-2.24393551394253,126.427839570916));
#39860=CARTESIAN_POINT('Ctrl Pts',(125.158058378177,-2.36606480237567,126.49045785715));
#39861=CARTESIAN_POINT('Ctrl Pts',(125.150302075436,-2.48550632984962,126.558158963301));
#39862=CARTESIAN_POINT('Ctrl Pts',(125.142545772694,-2.60182250868369,126.630668882925));
#39863=CARTESIAN_POINT('Ctrl Pts',(125.13478533018,-2.71820076896485,126.703217503277));
#39864=CARTESIAN_POINT('Ctrl Pts',(125.127024887665,-2.83145003411709,126.780579830863));
#39865=CARTESIAN_POINT('Ctrl Pts',(125.119264445151,-2.94116340013911,126.862439649791));
#39866=CARTESIAN_POINT('Ctrl Pts',(125.111491544886,-3.05105288779586,126.944430877367));
#39867=CARTESIAN_POINT('Ctrl Pts',(125.10371864462,-3.15739483011924,127.030933776837));
#39868=CARTESIAN_POINT('Ctrl Pts',(125.095945744355,-3.25981631434529,127.121592547319));
#39869=CARTESIAN_POINT('Ctrl Pts',(125.088455408593,-3.3585145196348,127.208955643138));
#39870=CARTESIAN_POINT('Ctrl Pts',(125.080965072831,-3.45357213297964,127.300177489754));
#39871=CARTESIAN_POINT('Ctrl Pts',(125.073474737069,-3.54469042092311,127.394910092582));
#39872=CARTESIAN_POINT('Ctrl Pts',(125.06580046413,-3.63804626419334,127.49196900602));
#39873=CARTESIAN_POINT('Ctrl Pts',(125.058126191191,-3.7275791791741,127.593038430459));
#39874=CARTESIAN_POINT('Ctrl Pts',(125.050451918251,-3.81291806288186,127.697780680038));
#39875=CARTESIAN_POINT('Ctrl Pts',(125.042786690845,-3.89815635911944,127.802399471735));
#39876=CARTESIAN_POINT('Ctrl Pts',(125.035121463439,-3.97921020139492,127.910682173425));
#39877=CARTESIAN_POINT('Ctrl Pts',(125.027456236033,-4.05574455568276,128.022253653132));
#39878=CARTESIAN_POINT('Ctrl Pts',(125.019798279898,-4.13220630911704,128.133719295602));
#39879=CARTESIAN_POINT('Ctrl Pts',(125.012140323763,-4.20415687476356,128.248467182711));
#39880=CARTESIAN_POINT('Ctrl Pts',(125.004482367629,-4.27130118908144,128.366088849561));
#39881=CARTESIAN_POINT('Ctrl Pts',(124.996830380284,-4.33839316955069,128.483618839333));
#39882=CARTESIAN_POINT('Ctrl Pts',(124.989178392939,-4.40068615589158,128.604017803311));
#39883=CARTESIAN_POINT('Ctrl Pts',(124.981526405594,-4.45792851807693,128.72684855016));
#39884=CARTESIAN_POINT('Ctrl Pts',(124.973877810681,-4.51514550244192,128.849624841245));
#39885=CARTESIAN_POINT('Ctrl Pts',(124.966229215767,-4.56731614805962,128.974830406805));
#39886=CARTESIAN_POINT('Ctrl Pts',(124.958580620853,-4.61423506686561,129.10200407142));
#39887=CARTESIAN_POINT('Ctrl Pts',(124.950933189818,-4.66114684606942,129.229158384152));
#39888=CARTESIAN_POINT('Ctrl Pts',(124.943285758782,-4.70280834798796,129.358279823902));
#39889=CARTESIAN_POINT('Ctrl Pts',(124.935638327747,-4.73906274128495,129.488888308217));
#39890=CARTESIAN_POINT('Ctrl Pts',(124.933816269092,-4.74770062645131,129.520006773778));
#39891=CARTESIAN_POINT('Ctrl Pts',(124.931994210437,-4.75603178956365,129.551209582994));
#39892=CARTESIAN_POINT('Ctrl Pts',(124.930172151781,-4.76405452823403,129.582490119308));
#39893=CARTESIAN_POINT('Origin',(213.235140564004,0.,130.804360617566));
#39894=CARTESIAN_POINT('',(122.834626183723,-4.76405452823408,129.582490119308));
#39895=CARTESIAN_POINT('',(123.180234630229,-4.76405452823405,129.582490119308));
#39896=CARTESIAN_POINT('',(213.235140564004,-4.76405452823405,129.582490119308));
#39897=CARTESIAN_POINT('',(124.514859435955,-4.91824949338178,130.802128275784));
#39898=CARTESIAN_POINT('Ctrl Pts',(124.514859435955,-4.91824949338178,130.802128275784));
#39899=CARTESIAN_POINT('Ctrl Pts',(124.507170124347,-4.91831079412571,130.937184813825));
#39900=CARTESIAN_POINT('Ctrl Pts',(124.499480812739,-4.91280485829688,131.07246854448));
#39901=CARTESIAN_POINT('Ctrl Pts',(124.49179150113,-4.9017018271335,131.207476308623));
#39902=CARTESIAN_POINT('Ctrl Pts',(124.484111153086,-4.89061173896633,131.34232669187));
#39903=CARTESIAN_POINT('Ctrl Pts',(124.476430805041,-4.87393756511142,131.476901353473));
#39904=CARTESIAN_POINT('Ctrl Pts',(124.468750456997,-4.85170143636514,131.610695681217));
#39905=CARTESIAN_POINT('Ctrl Pts',(124.461077128925,-4.82948563182929,131.744367718606));
#39906=CARTESIAN_POINT('Ctrl Pts',(124.453403800853,-4.80171805088814,131.877260448722));
#39907=CARTESIAN_POINT('Ctrl Pts',(124.445730472781,-4.76847270988192,132.008873414348));
#39908=CARTESIAN_POINT('Ctrl Pts',(124.43789673899,-4.73453239756891,132.143237659761));
#39909=CARTESIAN_POINT('Ctrl Pts',(124.430063005198,-4.69488278740763,132.276267617716));
#39910=CARTESIAN_POINT('Ctrl Pts',(124.422229271407,-4.64965792528211,132.407440228927));
#39911=CARTESIAN_POINT('Ctrl Pts',(124.414563307727,-4.60540161536512,132.535803599461));
#39912=CARTESIAN_POINT('Ctrl Pts',(124.406897344048,-4.55580659448187,132.662387982753));
#39913=CARTESIAN_POINT('Ctrl Pts',(124.399231380368,-4.50104900655704,132.786718028093));
#39914=CARTESIAN_POINT('Ctrl Pts',(124.391566171814,-4.44629681245654,132.911035826465));
#39915=CARTESIAN_POINT('Ctrl Pts',(124.38390096326,-4.38638322374303,133.033099362377));
#39916=CARTESIAN_POINT('Ctrl Pts',(124.376235754706,-4.32153231921454,133.152453775106));
#39917=CARTESIAN_POINT('Ctrl Pts',(124.368569555993,-4.2566730375258,133.271823605523));
#39918=CARTESIAN_POINT('Ctrl Pts',(124.360903357281,-4.18687536283241,133.388483265375));
#39919=CARTESIAN_POINT('Ctrl Pts',(124.353237158568,-4.11240880817546,133.50200345103));
#39920=CARTESIAN_POINT('Ctrl Pts',(124.34527746717,-4.03509137658085,133.619869642496));
#39921=CARTESIAN_POINT('Ctrl Pts',(124.337317775772,-3.9527407162197,133.734350795783));
#39922=CARTESIAN_POINT('Ctrl Pts',(124.329358084373,-3.8657064068974,133.845001510235));
#39923=CARTESIAN_POINT('Ctrl Pts',(124.321680515349,-3.78175693148386,133.95173033367));
#39924=CARTESIAN_POINT('Ctrl Pts',(124.314002946324,-3.69345047191876,134.054895356447));
#39925=CARTESIAN_POINT('Ctrl Pts',(124.3063253773,-3.60113970192494,134.154133133681));
#39926=CARTESIAN_POINT('Ctrl Pts',(124.298642580328,-3.50876607403826,134.253438485669));
#39927=CARTESIAN_POINT('Ctrl Pts',(124.290959783357,-3.41238299107311,134.348810988535));
#39928=CARTESIAN_POINT('Ctrl Pts',(124.283276986385,-3.31237767471077,134.439926213533));
#39929=CARTESIAN_POINT('Ctrl Pts',(124.275583724379,-3.21223613724717,134.531165550095));
#39930=CARTESIAN_POINT('Ctrl Pts',(124.267890462373,-3.10846282832349,134.618135785211));
#39931=CARTESIAN_POINT('Ctrl Pts',(124.260197200367,-3.00147560165349,134.700554564892));
#39932=CARTESIAN_POINT('Ctrl Pts',(124.259371754175,-2.98999643991024,134.709397662634));
#39933=CARTESIAN_POINT('Ctrl Pts',(124.258546307982,-2.97848030367339,134.718188406198));
#39934=CARTESIAN_POINT('Ctrl Pts',(124.25772086179,-2.96692772631653,134.726926477984));
#39935=CARTESIAN_POINT('Ctrl Pts',(124.249946527671,-2.85812160772622,134.809224621986));
#39936=CARTESIAN_POINT('Ctrl Pts',(124.242172193552,-2.745716311579,134.8871225106));
#39937=CARTESIAN_POINT('Ctrl Pts',(124.234397859433,-2.63010332833298,134.96028885862));
#39938=CARTESIAN_POINT('Ctrl Pts',(124.226633106486,-2.51463282775627,135.033365035656));
#39939=CARTESIAN_POINT('Ctrl Pts',(124.218868353539,-2.39596283294063,135.101721067383));
#39940=CARTESIAN_POINT('Ctrl Pts',(124.211103600591,-2.27451719297946,135.165066363353));
#39941=CARTESIAN_POINT('Ctrl Pts',(124.203346559706,-2.15319217454014,135.228348743882));
#39942=CARTESIAN_POINT('Ctrl Pts',(124.195589518821,-2.02909734153275,135.286630112939));
#39943=CARTESIAN_POINT('Ctrl Pts',(124.187832477936,-1.90268445981187,135.339663794741));
#39944=CARTESIAN_POINT('Ctrl Pts',(124.180081286696,-1.77636690702827,135.39265748343));
#39945=CARTESIAN_POINT('Ctrl Pts',(124.172330095456,-1.6477351440007,135.440411211034));
#39946=CARTESIAN_POINT('Ctrl Pts',(124.164578904216,-1.51726409073234,135.48272494086));
#39947=CARTESIAN_POINT('Ctrl Pts',(124.156831007439,-1.38684849114206,135.525020686223));
#39948=CARTESIAN_POINT('Ctrl Pts',(124.149083110662,-1.25459552726443,135.561880912126));
#39949=CARTESIAN_POINT('Ctrl Pts',(124.141335213885,-1.1209983794208,135.593154379656));
#39950=CARTESIAN_POINT('Ctrl Pts',(124.133588937801,-0.987429177220381,
135.624421305451));
#39951=CARTESIAN_POINT('Ctrl Pts',(124.125842661717,-0.852516730758256,
135.650103708287));
#39952=CARTESIAN_POINT('Ctrl Pts',(124.118096385632,-0.716767218410962,
135.670100830228));
#39953=CARTESIAN_POINT('Ctrl Pts',(124.110350052367,-0.581016703991329,
135.690098099783));
#39954=CARTESIAN_POINT('Ctrl Pts',(124.102603719102,-0.444429498147779,
135.704409947723));
#39955=CARTESIAN_POINT('Ctrl Pts',(124.094857385836,-0.307519363098675,
135.712987197763));
#39956=CARTESIAN_POINT('Ctrl Pts',(124.087109317833,-0.170578567974468,
135.721566368619));
#39957=CARTESIAN_POINT('Ctrl Pts',(124.07936124983,-0.0333150898662861,
135.724408361678));
#39958=CARTESIAN_POINT('Ctrl Pts',(124.071613181827,0.103755227135066,135.721516087484));
#39959=CARTESIAN_POINT('Ctrl Pts',(124.063856879086,0.240971224100578,135.718620739346));
#39960=CARTESIAN_POINT('Ctrl Pts',(124.056100576344,0.377993258361073,135.709978957901));
#39961=CARTESIAN_POINT('Ctrl Pts',(124.048344273602,0.514307972970508,135.695645762744));
#39962=CARTESIAN_POINT('Ctrl Pts',(124.040583831088,0.650695442847857,135.681304917529));
#39963=CARTESIAN_POINT('Ctrl Pts',(124.032823388573,0.786374454257362,135.661266662862));
#39964=CARTESIAN_POINT('Ctrl Pts',(124.025062946059,0.920840782211044,135.635637396671));
#39965=CARTESIAN_POINT('Ctrl Pts',(124.017290045794,1.05552296745144,135.609966988107));
#39966=CARTESIAN_POINT('Ctrl Pts',(124.009517145528,1.18898819822462,135.578687721994));
#39967=CARTESIAN_POINT('Ctrl Pts',(124.001744245263,1.3207455037904,135.541956461105));
#39968=CARTESIAN_POINT('Ctrl Pts',(123.994253909501,1.44771309942099,135.50656047407));
#39969=CARTESIAN_POINT('Ctrl Pts',(123.986763573739,1.5730944956195,135.466102092464));
#39970=CARTESIAN_POINT('Ctrl Pts',(123.979273237977,1.69646884389354,135.42076360303));
#39971=CARTESIAN_POINT('Ctrl Pts',(123.971498903858,1.82452096808229,135.373706090987));
#39972=CARTESIAN_POINT('Ctrl Pts',(123.963724569739,1.9508164761754,135.321242043413));
#39973=CARTESIAN_POINT('Ctrl Pts',(123.95595023562,2.07486503839237,135.263521764571));
#39974=CARTESIAN_POINT('Ctrl Pts',(123.948185482673,2.19876072184295,135.205872620814));
#39975=CARTESIAN_POINT('Ctrl Pts',(123.940420729726,2.3204146181523,135.142980298104));
#39976=CARTESIAN_POINT('Ctrl Pts',(123.932655976778,2.43935314455744,135.075044321452));
#39977=CARTESIAN_POINT('Ctrl Pts',(123.924898935894,2.55817353954084,135.00717581977));
#39978=CARTESIAN_POINT('Ctrl Pts',(123.917141895009,2.67428359436808,134.93427382579));
#39979=CARTESIAN_POINT('Ctrl Pts',(123.909384854124,2.78723158323549,134.856585088633));
#39980=CARTESIAN_POINT('Ctrl Pts',(123.901633662883,2.90009439714611,134.778954937157));
#39981=CARTESIAN_POINT('Ctrl Pts',(123.893882471643,3.00979957055717,134.696545448101));
#39982=CARTESIAN_POINT('Ctrl Pts',(123.886131280403,3.115922101071,134.609648060396));
#39983=CARTESIAN_POINT('Ctrl Pts',(123.878383383626,3.2219995266786,134.522787606398));
#39984=CARTESIAN_POINT('Ctrl Pts',(123.870635486849,3.3244970361011,134.431443294751));
#39985=CARTESIAN_POINT('Ctrl Pts',(123.862887590072,3.42302081174617,134.3359483037));
#39986=CARTESIAN_POINT('Ctrl Pts',(123.855141313988,3.52152397834137,134.240473288142));
#39987=CARTESIAN_POINT('Ctrl Pts',(123.847395037904,3.61605478394241,134.140849592074));
#39988=CARTESIAN_POINT('Ctrl Pts',(123.83964876182,3.70625485626919,134.037448615577));
#39989=CARTESIAN_POINT('Ctrl Pts',(123.831902428554,3.79645559443236,133.934046875797));
#39990=CARTESIAN_POINT('Ctrl Pts',(123.824156095289,3.88232527852341,133.826868094568));
#39991=CARTESIAN_POINT('Ctrl Pts',(123.816409762024,3.96354483411237,133.716317933613));
#39992=CARTESIAN_POINT('Ctrl Pts',(123.808661694021,4.04478257825766,133.605743015716));
#39993=CARTESIAN_POINT('Ctrl Pts',(123.800913626018,4.1213678902718,133.491795530748));
#39994=CARTESIAN_POINT('Ctrl Pts',(123.793165558015,4.1930243925468,133.374911046172));
#39995=CARTESIAN_POINT('Ctrl Pts',(123.785409255273,4.26475705220518,133.257902335375));
#39996=CARTESIAN_POINT('Ctrl Pts',(123.777652952531,4.33155023319489,133.137950723328));
#39997=CARTESIAN_POINT('Ctrl Pts',(123.769896649789,4.39317274309023,133.015517851204));
#39998=CARTESIAN_POINT('Ctrl Pts',(123.762136207275,4.45482814277455,132.893019632969));
#39999=CARTESIAN_POINT('Ctrl Pts',(123.754375764761,4.51130721142138,132.768037871932));
#40000=CARTESIAN_POINT('Ctrl Pts',(123.746615322247,4.56242691869805,132.641054297535));
#40001=CARTESIAN_POINT('Ctrl Pts',(123.738842421981,4.61362868786701,132.513866877832));
#40002=CARTESIAN_POINT('Ctrl Pts',(123.731069521716,4.65945377271454,132.384671591879));
#40003=CARTESIAN_POINT('Ctrl Pts',(123.72329662145,4.69976876465451,132.253966295424));
#40004=CARTESIAN_POINT('Ctrl Pts',(123.715806285688,4.73861820509072,132.12801246572));
#40005=CARTESIAN_POINT('Ctrl Pts',(123.708315949926,4.77235113006234,132.000656802601));
#40006=CARTESIAN_POINT('Ctrl Pts',(123.700825614164,4.80089342367698,131.872351908259));
#40007=CARTESIAN_POINT('Ctrl Pts',(123.693051280045,4.83051790702883,131.739182294851));
#40008=CARTESIAN_POINT('Ctrl Pts',(123.685276945926,4.8546442250089,131.604568207798));
#40009=CARTESIAN_POINT('Ctrl Pts',(123.677502611807,4.87313379762867,131.469003418557));
#40010=CARTESIAN_POINT('Ctrl Pts',(123.66973785886,4.89160058350265,131.333605700803));
#40011=CARTESIAN_POINT('Ctrl Pts',(123.661973105913,4.90444439372064,131.197259995765));
#40012=CARTESIAN_POINT('Ctrl Pts',(123.654208352965,4.91157711127343,131.060472590178));
#40013=CARTESIAN_POINT('Ctrl Pts',(123.64645131208,4.91870274451059,130.92382104377));
#40014=CARTESIAN_POINT('Ctrl Pts',(123.638694271195,4.92012855306334,130.786729057759));
#40015=CARTESIAN_POINT('Ctrl Pts',(123.63093723031,4.91581796512449,130.649710055785));
#40016=CARTESIAN_POINT('Ctrl Pts',(123.62318603907,4.91151062783351,130.512794380905));
#40017=CARTESIAN_POINT('Ctrl Pts',(123.61543484783,4.90147551665914,130.375951969703));
#40018=CARTESIAN_POINT('Ctrl Pts',(123.60768365659,4.88572810325017,130.239697918593));
#40019=CARTESIAN_POINT('Ctrl Pts',(123.599935759813,4.86998738291205,130.10350177909));
#40020=CARTESIAN_POINT('Ctrl Pts',(123.592187863036,4.84853923400185,129.967893889879));
#40021=CARTESIAN_POINT('Ctrl Pts',(123.584439966259,4.82145110078454,129.833385671832));
#40022=CARTESIAN_POINT('Ctrl Pts',(123.576693690175,4.7943686338207,129.698905590004));
#40023=CARTESIAN_POINT('Ctrl Pts',(123.568947414091,4.76164860629984,129.565525104832));
#40024=CARTESIAN_POINT('Ctrl Pts',(123.561201138006,4.72340977865622,129.433746475878));
#40025=CARTESIAN_POINT('Ctrl Pts',(123.553454804741,4.68517066874234,129.301966874165));
#40026=CARTESIAN_POINT('Ctrl Pts',(123.545708471476,4.64141278636882,129.171789527742));
#40027=CARTESIAN_POINT('Ctrl Pts',(123.53796213821,4.59230495870758,129.043702153034));
#40028=CARTESIAN_POINT('Ctrl Pts',(123.530214070207,4.5431861336888,128.915586094046));
#40029=CARTESIAN_POINT('Ctrl Pts',(123.522466002204,4.4887151192683,128.789561303092));
#40030=CARTESIAN_POINT('Ctrl Pts',(123.514717934201,4.42910898184085,128.666095739335));
#40031=CARTESIAN_POINT('Ctrl Pts',(123.50696163146,4.36943949430127,128.542498954908));
#40032=CARTESIAN_POINT('Ctrl Pts',(123.499205328718,4.30462415171893,128.421467183767));
#40033=CARTESIAN_POINT('Ctrl Pts',(123.491449025976,4.23492638073328,128.30344446298));
#40034=CARTESIAN_POINT('Ctrl Pts',(123.483688583462,4.16519140994861,128.185358749913));
#40035=CARTESIAN_POINT('Ctrl Pts',(123.475928140947,4.09056903090241,128.0702856152));
#40036=CARTESIAN_POINT('Ctrl Pts',(123.468167698433,4.01136560385153,127.958639433975));
#40037=CARTESIAN_POINT('Ctrl Pts',(123.460394798168,3.93203503242825,127.846814028389));
#40038=CARTESIAN_POINT('Ctrl Pts',(123.452621897902,3.84810895705507,127.738426878845));
#40039=CARTESIAN_POINT('Ctrl Pts',(123.444848997637,3.75993412727321,127.633859328958));
#40040=CARTESIAN_POINT('Ctrl Pts',(123.437358661875,3.67496467465328,127.533093072899));
#40041=CARTESIAN_POINT('Ctrl Pts',(123.429868326113,3.58605021829274,127.435873761006));
#40042=CARTESIAN_POINT('Ctrl Pts',(123.422377990351,3.49353148378359,127.342508391616));
#40043=CARTESIAN_POINT('Ctrl Pts',(123.414603656232,3.39750487333459,127.245603045868));
#40044=CARTESIAN_POINT('Ctrl Pts',(123.406829322113,3.29729109361403,127.152542689075));
#40045=CARTESIAN_POINT('Ctrl Pts',(123.399054987994,3.19323066266481,127.063710808039));
#40046=CARTESIAN_POINT('Ctrl Pts',(123.391290235047,3.0892984768965,126.974988404357));
#40047=CARTESIAN_POINT('Ctrl Pts',(123.3835254821,2.98152936688766,126.890484359063));
#40048=CARTESIAN_POINT('Ctrl Pts',(123.375760729152,2.87030165660958,126.810546467838));
#40049=CARTESIAN_POINT('Ctrl Pts',(123.368003688267,2.75918441926176,126.730687972055));
#40050=CARTESIAN_POINT('Ctrl Pts',(123.360246647382,2.64461573313438,126.655386831842));
#40051=CARTESIAN_POINT('Ctrl Pts',(123.352489606497,2.52700778812089,126.584951334115));
#40052=CARTESIAN_POINT('Ctrl Pts',(123.344738415257,2.40948853217287,126.514568952344));
#40053=CARTESIAN_POINT('Ctrl Pts',(123.336987224017,2.28893491333921,126.449045109768));
#40054=CARTESIAN_POINT('Ctrl Pts',(123.329236032777,2.16578865962575,126.388645211843));
#40055=CARTESIAN_POINT('Ctrl Pts',(123.321488136,2.04269474635566,126.328270985487));
#40056=CARTESIAN_POINT('Ctrl Pts',(123.313740239223,1.91701074016089,126.273016544083));
#40057=CARTESIAN_POINT('Ctrl Pts',(123.305992342446,1.78920336917902,126.223101580334));
#40058=CARTESIAN_POINT('Ctrl Pts',(123.298246066362,1.66142273274387,126.17319705772));
#40059=CARTESIAN_POINT('Ctrl Pts',(123.290499790277,1.53151997893062,126.128629933317));
#40060=CARTESIAN_POINT('Ctrl Pts',(123.282753514193,1.39998186585056,126.089571774172));
#40061=CARTESIAN_POINT('Ctrl Pts',(123.275007180928,1.26844278178604,126.050513326709));
#40062=CARTESIAN_POINT('Ctrl Pts',(123.267260847663,1.13526868915776,126.016964036937));
#40063=CARTESIAN_POINT('Ctrl Pts',(123.259514514397,1.00096117281618,125.989045488417));
#40064=CARTESIAN_POINT('Ctrl Pts',(123.251766446394,0.866623579237726,125.961120687731));
#40065=CARTESIAN_POINT('Ctrl Pts',(123.244018378391,0.7311524395782,125.938829217025));
#40066=CARTESIAN_POINT('Ctrl Pts',(123.236270310388,0.595058790822629,125.922241395551));
#40067=CARTESIAN_POINT('Ctrl Pts',(123.228514007647,0.458820500117439,125.905635944344));
#40068=CARTESIAN_POINT('Ctrl Pts',(123.220757704905,0.321958767390716,125.894746299058));
#40069=CARTESIAN_POINT('Ctrl Pts',(123.213001402163,0.184989562134513,125.88959084428));
#40070=CARTESIAN_POINT('Ctrl Pts',(123.205240959649,0.0479472522894938,
125.884432637882));
#40071=CARTESIAN_POINT('Ctrl Pts',(123.197480517134,-0.089202253611909,
125.885014718659));
#40072=CARTESIAN_POINT('Ctrl Pts',(123.18972007462,-0.225944734832842,125.891303316933));
#40073=CARTESIAN_POINT('Ctrl Pts',(123.181947174355,-0.36290672722415,125.897602010223));
#40074=CARTESIAN_POINT('Ctrl Pts',(123.174174274089,-0.499459999566706,
125.909625492513));
#40075=CARTESIAN_POINT('Ctrl Pts',(123.166401373824,-0.635096290080667,
125.927288159131));
#40076=CARTESIAN_POINT('Ctrl Pts',(123.158911038062,-0.76580185978642,125.944308743328));
#40077=CARTESIAN_POINT('Ctrl Pts',(123.1514207023,-0.895655655795518,125.96656558086));
#40078=CARTESIAN_POINT('Ctrl Pts',(123.143930366538,-1.02421522120527,125.993937949738));
#40079=CARTESIAN_POINT('Ctrl Pts',(123.136156032419,-1.15764916161348,126.022348150302));
#40080=CARTESIAN_POINT('Ctrl Pts',(123.1283816983,-1.29011147118705,126.056359445411));
#40081=CARTESIAN_POINT('Ctrl Pts',(123.120607364181,-1.42109545329787,126.095892631574));
#40082=CARTESIAN_POINT('Ctrl Pts',(123.112842611234,-1.55191800935639,126.135377096617));
#40083=CARTESIAN_POINT('Ctrl Pts',(123.105077858287,-1.68126549230711,126.18036980044));
#40084=CARTESIAN_POINT('Ctrl Pts',(123.09731310534,-1.80864079844571,126.230740440431));
#40085=CARTESIAN_POINT('Ctrl Pts',(123.089556064455,-1.93588959363475,126.281061051592));
#40086=CARTESIAN_POINT('Ctrl Pts',(123.08179902357,-2.06116974888277,126.336748826367));
#40087=CARTESIAN_POINT('Ctrl Pts',(123.074041982685,-2.18399909497111,126.397623614333));
#40088=CARTESIAN_POINT('Ctrl Pts',(123.066290791445,-2.30673581449443,126.458452496148));
#40089=CARTESIAN_POINT('Ctrl Pts',(123.058539600204,-2.42702505465063,126.524460432507));
#40090=CARTESIAN_POINT('Ctrl Pts',(123.050788408964,-2.54440475753456,126.595419243261));
#40091=CARTESIAN_POINT('Ctrl Pts',(123.043040512187,-2.6617345709134,126.666347894628));
#40092=CARTESIAN_POINT('Ctrl Pts',(123.03529261541,-2.77615697270482,126.742223033352));
#40093=CARTESIAN_POINT('Ctrl Pts',(123.027544718633,-2.88723485125613,126.822770737105));
#40094=CARTESIAN_POINT('Ctrl Pts',(123.019798442549,-2.99828949470972,126.903301592014));
#40095=CARTESIAN_POINT('Ctrl Pts',(123.012052166465,-3.10600069016326,126.988502838482));
#40096=CARTESIAN_POINT('Ctrl Pts',(123.004305890381,-3.20996098875319,127.078057689303));
#40097=CARTESIAN_POINT('Ctrl Pts',(122.996559557115,-3.31392205475493,127.167613201197));
#40098=CARTESIAN_POINT('Ctrl Pts',(122.98881322385,-3.41413187242903,127.261522126404));
#40099=CARTESIAN_POINT('Ctrl Pts',(122.981066890585,-3.51021703122026,127.359428186265));
#40100=CARTESIAN_POINT('Ctrl Pts',(122.973318822582,-3.60632370761607,127.457356171509));
#40101=CARTESIAN_POINT('Ctrl Pts',(122.965570754579,-3.69830361330064,127.55928279363));
#40102=CARTESIAN_POINT('Ctrl Pts',(122.957822686576,-3.78582135872236,127.664816112014));
#40103=CARTESIAN_POINT('Ctrl Pts',(122.950066383834,-3.8734321190455,127.770461592465));
#40104=CARTESIAN_POINT('Ctrl Pts',(122.942310081092,-3.95657099560802,127.879721125062));
#40105=CARTESIAN_POINT('Ctrl Pts',(122.93455377835,-4.03494362682191,127.992170547377));
#40106=CARTESIAN_POINT('Ctrl Pts',(122.926793335836,-4.11335808786905,128.104679987335));
#40107=CARTESIAN_POINT('Ctrl Pts',(122.919032893322,-4.18700102482841,128.220382379805));
#40108=CARTESIAN_POINT('Ctrl Pts',(122.911272450808,-4.25562290021923,128.338826842979));
#40109=CARTESIAN_POINT('Ctrl Pts',(122.903499550542,-4.32435493353634,128.45746144372));
#40110=CARTESIAN_POINT('Ctrl Pts',(122.895726650277,-4.38804961656374,128.578846564999));
#40111=CARTESIAN_POINT('Ctrl Pts',(122.887953750011,-4.44650424302869,128.70250832037));
#40112=CARTESIAN_POINT('Ctrl Pts',(122.880463414249,-4.5028338965828,128.821674659447));
#40113=CARTESIAN_POINT('Ctrl Pts',(122.872973078488,-4.55429773741881,128.942954700019));
#40114=CARTESIAN_POINT('Ctrl Pts',(122.865482742726,-4.60075817360164,129.06591093738));
#40115=CARTESIAN_POINT('Ctrl Pts',(122.856565377702,-4.65607006905499,129.212292312697));
#40116=CARTESIAN_POINT('Ctrl Pts',(122.847648012679,-4.70443694400042,129.361434294279));
#40117=CARTESIAN_POINT('Ctrl Pts',(122.838730647656,-4.74561132962465,129.512711992499));
#40118=CARTESIAN_POINT('Ctrl Pts',(122.837362493012,-4.75192854628791,129.535921907631));
#40119=CARTESIAN_POINT('Ctrl Pts',(122.835994338368,-4.75807654452855,129.559182051569));
#40120=CARTESIAN_POINT('Ctrl Pts',(122.834626183723,-4.76405452823408,129.582490119308));
#40121=CARTESIAN_POINT('Ctrl Pts',(124.584949745809,-4.76405452823405,129.582490119308));
#40122=CARTESIAN_POINT('Ctrl Pts',(124.576819535775,-4.79969206700382,129.721440342096));
#40123=CARTESIAN_POINT('Ctrl Pts',(124.56868932574,-4.82920735029006,129.861801844806));
#40124=CARTESIAN_POINT('Ctrl Pts',(124.560559115706,-4.85252381590777,130.002989493462));
#40125=CARTESIAN_POINT('Ctrl Pts',(124.552428905671,-4.87584028152547,130.144177142117));
#40126=CARTESIAN_POINT('Ctrl Pts',(124.544298695637,-4.89295794227717,130.286190445843));
#40127=CARTESIAN_POINT('Ctrl Pts',(124.536168485602,-4.90386265852004,130.428442955208));
#40128=CARTESIAN_POINT('Ctrl Pts',(124.529065469065,-4.91338964238377,130.552722884288));
#40129=CARTESIAN_POINT('Ctrl Pts',(124.521962452528,-4.91819286668434,130.677369535755));
#40130=CARTESIAN_POINT('Ctrl Pts',(124.514859435991,-4.9182494933815,130.802128275159));
#40131=CARTESIAN_POINT('',(124.860140563954,-4.91824790038655,130.808905157512));
#40132=CARTESIAN_POINT('Ctrl Pts',(124.930172151781,-4.76405452823403,129.582490119308));
#40133=CARTESIAN_POINT('Ctrl Pts',(124.922522261014,-4.79773789748411,129.713821064798));
#40134=CARTESIAN_POINT('Ctrl Pts',(124.914872370247,-4.82598054335935,129.846522875123));
#40135=CARTESIAN_POINT('Ctrl Pts',(124.907222479479,-4.84868809827559,129.980099258445));
#40136=CARTESIAN_POINT('Ctrl Pts',(124.899375493568,-4.8719807006071,130.117117162357));
#40137=CARTESIAN_POINT('Ctrl Pts',(124.891528507656,-4.88944903983335,130.255054876221));
#40138=CARTESIAN_POINT('Ctrl Pts',(124.883681521744,-4.90104783706232,130.393370153775));
#40139=CARTESIAN_POINT('Ctrl Pts',(124.875834535832,-4.9126466342913,130.53168543133));
#40140=CARTESIAN_POINT('Ctrl Pts',(124.86798754992,-4.91837590184352,130.670377817801));
#40141=CARTESIAN_POINT('Ctrl Pts',(124.860140564008,-4.91824790038743,130.80890515656));
#40142=CARTESIAN_POINT('Ctrl Pts',(124.860140563954,-4.91824790038655,130.808905157512));
#40143=CARTESIAN_POINT('Ctrl Pts',(124.849923153069,-4.91808123209384,130.989278966611));
#40144=CARTESIAN_POINT('Ctrl Pts',(124.839705742184,-4.90798857365373,131.169211590381));
#40145=CARTESIAN_POINT('Ctrl Pts',(124.8294883313,-4.88813519968135,131.347791691518));
#40146=CARTESIAN_POINT('Ctrl Pts',(124.818986074523,-4.86772834380638,131.531350334552));
#40147=CARTESIAN_POINT('Ctrl Pts',(124.808483817746,-4.83700889931984,131.713480411591));
#40148=CARTESIAN_POINT('Ctrl Pts',(124.797981560969,-4.79620387198005,131.893218496678));
#40149=CARTESIAN_POINT('Ctrl Pts',(124.796996745065,-4.79237750963129,131.910072866991));
#40150=CARTESIAN_POINT('Ctrl Pts',(124.79601192916,-4.78846249740315,131.926906219906));
#40151=CARTESIAN_POINT('Ctrl Pts',(124.795027113256,-4.78445904371179,131.943717770326));
#40152=CARTESIAN_POINT('Ctrl Pts',(124.787252779137,-4.75285497793157,132.076431518577));
#40153=CARTESIAN_POINT('Ctrl Pts',(124.779478445018,-4.71567474704518,132.208039504975));
#40154=CARTESIAN_POINT('Ctrl Pts',(124.771704110899,-4.67300969105515,132.338037079472));
#40155=CARTESIAN_POINT('Ctrl Pts',(124.763939357952,-4.63039721593357,132.467874443577));
#40156=CARTESIAN_POINT('Ctrl Pts',(124.756174605005,-4.58231348595731,132.596104976815));
#40157=CARTESIAN_POINT('Ctrl Pts',(124.748409852058,-4.52890069533131,132.72223484554));
#40158=CARTESIAN_POINT('Ctrl Pts',(124.740652811173,-4.47554095504197,132.848239440302));
#40159=CARTESIAN_POINT('Ctrl Pts',(124.732895770288,-4.41686283867964,132.972147164914));
#40160=CARTESIAN_POINT('Ctrl Pts',(124.725138729403,-4.35305801552037,133.093480312124));
#40161=CARTESIAN_POINT('Ctrl Pts',(124.717387538162,-4.28930130807453,133.214721961065));
#40162=CARTESIAN_POINT('Ctrl Pts',(124.709636346922,-4.22042577028052,133.333392552423));
#40163=CARTESIAN_POINT('Ctrl Pts',(124.701885155682,-4.14667060469276,133.449035637049));
#40164=CARTESIAN_POINT('Ctrl Pts',(124.694137258905,-4.07294678701781,133.564629570279));
#40165=CARTESIAN_POINT('Ctrl Pts',(124.686389362128,-3.99434767631359,133.677198227128));
#40166=CARTESIAN_POINT('Ctrl Pts',(124.678641465351,-3.91115760549944,133.786311195199));
#40167=CARTESIAN_POINT('Ctrl Pts',(124.670895189267,-3.82798493625478,133.895401339189));
#40168=CARTESIAN_POINT('Ctrl Pts',(124.663148913183,-3.74022345394225,134.00103692149));
#40169=CARTESIAN_POINT('Ctrl Pts',(124.655402637099,-3.64819963218999,134.102818212593));
#40170=CARTESIAN_POINT('Ctrl Pts',(124.647656303833,-3.55617513113883,134.204600255022));
#40171=CARTESIAN_POINT('Ctrl Pts',(124.639909970568,-3.45988849006804,134.302527659474));
#40172=CARTESIAN_POINT('Ctrl Pts',(124.632163637303,-3.35970484585868,134.396235672633));
#40173=CARTESIAN_POINT('Ctrl Pts',(124.6244155693,-3.25949876621689,134.489964671052));
#40174=CARTESIAN_POINT('Ctrl Pts',(124.616667501297,-3.15539423232435,134.579472130908));
#40175=CARTESIAN_POINT('Ctrl Pts',(124.608919433294,-3.04779112035167,134.664432164727));
#40176=CARTESIAN_POINT('Ctrl Pts',(124.601163130552,-2.94007364651095,134.749482495082));
#40177=CARTESIAN_POINT('Ctrl Pts',(124.59340682781,-2.82885047416152,134.829975502182));
#40178=CARTESIAN_POINT('Ctrl Pts',(124.585650525068,-2.71455270744954,134.905627087936));
#40179=CARTESIAN_POINT('Ctrl Pts',(124.577890082554,-2.60019393657795,134.981319051219));
#40180=CARTESIAN_POINT('Ctrl Pts',(124.57012964004,-2.48275763610817,135.052164242439));
#40181=CARTESIAN_POINT('Ctrl Pts',(124.562369197526,-2.36270054621509,135.117924015896));
#40182=CARTESIAN_POINT('Ctrl Pts',(124.55459629726,-2.24245073002315,135.18378935278));
#40183=CARTESIAN_POINT('Ctrl Pts',(124.546823396995,-2.11957206789316,135.244552785097));
#40184=CARTESIAN_POINT('Ctrl Pts',(124.539050496729,-1.99454317419499,135.300023036918));
#40185=CARTESIAN_POINT('Ctrl Pts',(124.531560160967,-1.8740593957116,135.353476805364));
#40186=CARTESIAN_POINT('Ctrl Pts',(124.524069825205,-1.75157929051489,135.402015439318));
#40187=CARTESIAN_POINT('Ctrl Pts',(124.516579489443,-1.62754353914853,135.445511885374));
#40188=CARTESIAN_POINT('Ctrl Pts',(124.508805155324,-1.49880493456936,135.490657512403));
#40189=CARTESIAN_POINT('Ctrl Pts',(124.501030821205,-1.36798258530955,135.530514062511));
#40190=CARTESIAN_POINT('Ctrl Pts',(124.493256487086,-1.23555043924825,135.564885606953));
#40191=CARTESIAN_POINT('Ctrl Pts',(124.485491734139,-1.10328150397109,135.599214791537));
#40192=CARTESIAN_POINT('Ctrl Pts',(124.477726981192,-0.969407094117519,
135.628072323127));
#40193=CARTESIAN_POINT('Ctrl Pts',(124.469962228245,-0.834419545362218,
135.651310904583));
#40194=CARTESIAN_POINT('Ctrl Pts',(124.46220518736,-0.699566068143424,135.674526405153));
#40195=CARTESIAN_POINT('Ctrl Pts',(124.454448146475,-0.563602034991586,
135.692133995775));
#40196=CARTESIAN_POINT('Ctrl Pts',(124.44669110559,-0.427032956473006,135.704036720798));
#40197=CARTESIAN_POINT('Ctrl Pts',(124.43893991435,-0.290566865758703,135.715930469885));
#40198=CARTESIAN_POINT('Ctrl Pts',(124.43118872311,-0.153497025767011,135.722127882601));
#40199=CARTESIAN_POINT('Ctrl Pts',(124.423437531869,-0.0163367549181919,
135.722583484917));
#40200=CARTESIAN_POINT('Ctrl Pts',(124.415689635092,0.120765219156459,135.72303889359));
#40201=CARTESIAN_POINT('Ctrl Pts',(124.407941738315,0.257957157498372,135.717757344381));
#40202=CARTESIAN_POINT('Ctrl Pts',(124.400193841538,0.394723253081784,135.706745406215));
#40203=CARTESIAN_POINT('Ctrl Pts',(124.392447565454,0.531460740146428,135.695735771509));
#40204=CARTESIAN_POINT('Ctrl Pts',(124.38470128937,0.667772172174718,135.678998163431));
#40205=CARTESIAN_POINT('Ctrl Pts',(124.376955013286,0.803144778439342,135.656591189928));
#40206=CARTESIAN_POINT('Ctrl Pts',(124.369208680021,0.938518383993701,135.634184051022));
#40207=CARTESIAN_POINT('Ctrl Pts',(124.361462346755,1.07295276423854,135.606107527026));
#40208=CARTESIAN_POINT('Ctrl Pts',(124.35371601349,1.20594367647488,135.572471659863));
#40209=CARTESIAN_POINT('Ctrl Pts',(124.345967945487,1.33896437110383,135.53882826018));
#40210=CARTESIAN_POINT('Ctrl Pts',(124.338219877484,1.47054057552723,135.499623135816));
#40211=CARTESIAN_POINT('Ctrl Pts',(124.330471809481,1.60018196854618,135.455016563778));
#40212=CARTESIAN_POINT('Ctrl Pts',(124.322715506739,1.72996114598048,135.410362583345));
#40213=CARTESIAN_POINT('Ctrl Pts',(124.314959203998,1.85780103396559,135.360295814932));
#40214=CARTESIAN_POINT('Ctrl Pts',(124.307202901256,1.98322959041068,135.305025396709));
#40215=CARTESIAN_POINT('Ctrl Pts',(124.299442458742,2.10872509185302,135.249725479));
#40216=CARTESIAN_POINT('Ctrl Pts',(124.291682016227,2.23180634661166,135.18921654979));
#40217=CARTESIAN_POINT('Ctrl Pts',(124.283921573713,2.35202569607938,135.123753883695));
#40218=CARTESIAN_POINT('Ctrl Pts',(124.276148673448,2.47243803231935,135.058186131117));
#40219=CARTESIAN_POINT('Ctrl Pts',(124.268375773182,2.58997894719704,134.987648951959));
#40220=CARTESIAN_POINT('Ctrl Pts',(124.260602872917,2.70422881209734,134.912441628734));
#40221=CARTESIAN_POINT('Ctrl Pts',(124.253112537155,2.81432540663117,134.839968281144));
#40222=CARTESIAN_POINT('Ctrl Pts',(124.245622201393,2.92136582266444,134.763158617099));
#40223=CARTESIAN_POINT('Ctrl Pts',(124.238131865631,3.02500496797082,134.682314718152));
#40224=CARTESIAN_POINT('Ctrl Pts',(124.230357531512,3.13257362297132,134.598405598205));
#40225=CARTESIAN_POINT('Ctrl Pts',(124.222583197393,3.23681874266201,134.509884489575));
#40226=CARTESIAN_POINT('Ctrl Pts',(124.214808863274,3.3373193062344,134.417044233763));
#40227=CARTESIAN_POINT('Ctrl Pts',(124.207044110327,3.43769601184418,134.324318395268));
#40228=CARTESIAN_POINT('Ctrl Pts',(124.199279357379,3.53433705904816,134.227284263446));
#40229=CARTESIAN_POINT('Ctrl Pts',(124.191514604432,3.62685240313502,134.126276436544));
#40230=CARTESIAN_POINT('Ctrl Pts',(124.183757563547,3.71927585967788,134.025368932039));
#40231=CARTESIAN_POINT('Ctrl Pts',(124.176000522662,3.80758150536502,133.920495873066));
#40232=CARTESIAN_POINT('Ctrl Pts',(124.168243481777,3.89141452785478,133.812030153087));
#40233=CARTESIAN_POINT('Ctrl Pts',(124.160492290537,3.97518433121009,133.703646227951));
#40234=CARTESIAN_POINT('Ctrl Pts',(124.152741099297,4.05448798668088,133.5916753425));
#40235=CARTESIAN_POINT('Ctrl Pts',(124.144989908057,4.12900977453227,133.476524786235));
#40236=CARTESIAN_POINT('Ctrl Pts',(124.13724201128,4.20349988863593,133.361423172028));
#40237=CARTESIAN_POINT('Ctrl Pts',(124.129494114503,4.27321196547824,133.243144902466));
#40238=CARTESIAN_POINT('Ctrl Pts',(124.121746217726,4.3378727253851,133.122127491274));
#40239=CARTESIAN_POINT('Ctrl Pts',(124.113999941642,4.40251995965491,133.001135394316));
#40240=CARTESIAN_POINT('Ctrl Pts',(124.106253665558,4.46211779454859,132.877405640006));
#40241=CARTESIAN_POINT('Ctrl Pts',(124.098507389473,4.51643837348782,132.751401315905));
#40242=CARTESIAN_POINT('Ctrl Pts',(124.090761056208,4.57075935340923,132.625396061668));
#40243=CARTESIAN_POINT('Ctrl Pts',(124.083014722943,4.61980284486769,132.497116563162));
#40244=CARTESIAN_POINT('Ctrl Pts',(124.075268389677,4.66338887375304,132.367046534395));
#40245=CARTESIAN_POINT('Ctrl Pts',(124.067520321674,4.70698466342732,132.236947377348));
#40246=CARTESIAN_POINT('Ctrl Pts',(124.059772253671,4.74512043437139,132.105057262777));
#40247=CARTESIAN_POINT('Ctrl Pts',(124.052024185668,4.7776660015863,131.971875345433));
#40248=CARTESIAN_POINT('Ctrl Pts',(124.044267882927,4.81024615861737,131.838551880762));
#40249=CARTESIAN_POINT('Ctrl Pts',(124.036511580185,4.83722415050561,131.70393425111));
#40250=CARTESIAN_POINT('Ctrl Pts',(124.028755277443,4.85852078083644,131.568532643147));
#40251=CARTESIAN_POINT('Ctrl Pts',(124.020994834929,4.87982877782012,131.433058767269));
#40252=CARTESIAN_POINT('Ctrl Pts',(124.013234392415,4.89544932659802,131.296800467547));
#40253=CARTESIAN_POINT('Ctrl Pts',(124.0054739499,4.90535522652129,131.160272354012));
#40254=CARTESIAN_POINT('Ctrl Pts',(123.997701049635,4.91527702827452,131.023525073429));
#40255=CARTESIAN_POINT('Ctrl Pts',(123.98992814937,4.91946583732034,130.886507504509));
#40256=CARTESIAN_POINT('Ctrl Pts',(123.982155249104,4.91794662899568,130.7497344622));
#40257=CARTESIAN_POINT('Ctrl Pts',(123.974664913342,4.91648264772027,130.61793346449));
#40258=CARTESIAN_POINT('Ctrl Pts',(123.96717457758,4.90971846146985,130.486359831343));
#40259=CARTESIAN_POINT('Ctrl Pts',(123.959684241818,4.89772168923275,130.355467181081));
#40260=CARTESIAN_POINT('Ctrl Pts',(123.951909907699,4.88527005572995,130.219611696201));
#40261=CARTESIAN_POINT('Ctrl Pts',(123.94413557358,4.86714177351287,130.084059503168));
#40262=CARTESIAN_POINT('Ctrl Pts',(123.936361239461,4.8433556463987,129.949323106694));
#40263=CARTESIAN_POINT('Ctrl Pts',(123.928596486514,4.81959883356039,129.814752760788));
#40264=CARTESIAN_POINT('Ctrl Pts',(123.920831733567,4.79019811691197,129.680996592319));
#40265=CARTESIAN_POINT('Ctrl Pts',(123.913066980619,4.7552241747404,129.548563615474));
#40266=CARTESIAN_POINT('Ctrl Pts',(123.905309939734,4.72028496918125,129.416262172928));
#40267=CARTESIAN_POINT('Ctrl Pts',(123.897552898849,4.67978365298778,129.285281682224));
#40268=CARTESIAN_POINT('Ctrl Pts',(123.889795857965,4.63384216725141,129.156122215058));
#40269=CARTESIAN_POINT('Ctrl Pts',(123.882044666724,4.58793532634682,129.02706014805));
#40270=CARTESIAN_POINT('Ctrl Pts',(123.874293475484,4.53659661211821,128.899816738079));
#40271=CARTESIAN_POINT('Ctrl Pts',(123.866542284244,4.47999803452869,128.774877759023));
#40272=CARTESIAN_POINT('Ctrl Pts',(123.858794387467,4.42342351284446,128.649991882366));
#40273=CARTESIAN_POINT('Ctrl Pts',(123.85104649069,4.36159373519336,128.527408843965));
#40274=CARTESIAN_POINT('Ctrl Pts',(123.843298593913,4.294729079923,128.407595048604));
#40275=CARTESIAN_POINT('Ctrl Pts',(123.835552317829,4.22787841129708,128.287806315705));
#40276=CARTESIAN_POINT('Ctrl Pts',(123.827806041745,4.15599515030506,128.170786014839));
#40277=CARTESIAN_POINT('Ctrl Pts',(123.820059765661,4.07934574358167,128.056976158335));
#40278=CARTESIAN_POINT('Ctrl Pts',(123.812313432395,4.00269577104978,127.943165461713));
#40279=CARTESIAN_POINT('Ctrl Pts',(123.80456709913,3.92127980097931,127.832565581022));
#40280=CARTESIAN_POINT('Ctrl Pts',(123.796820765865,3.83540751526397,127.725589392815));
#40281=CARTESIAN_POINT('Ctrl Pts',(123.789072697862,3.74951599904564,127.618589248032));
#40282=CARTESIAN_POINT('Ctrl Pts',(123.781324629859,3.65916642604875,127.515214715355));
#40283=CARTESIAN_POINT('Ctrl Pts',(123.773576561856,3.56470838112846,127.415845128445));
#40284=CARTESIAN_POINT('Ctrl Pts',(123.765820259114,3.47014994507397,127.316369930356));
#40285=CARTESIAN_POINT('Ctrl Pts',(123.758063956372,3.37147458426828,127.220908464678));
#40286=CARTESIAN_POINT('Ctrl Pts',(123.75030765363,3.26906872560912,127.129803129957));
#40287=CARTESIAN_POINT('Ctrl Pts',(123.742547211116,3.16660820985967,127.038649169575));
#40288=CARTESIAN_POINT('Ctrl Pts',(123.734786768602,3.06041353143619,126.951856220198));
#40289=CARTESIAN_POINT('Ctrl Pts',(123.727026326087,2.95090294371566,126.869725325792));
#40290=CARTESIAN_POINT('Ctrl Pts',(123.719253425822,2.8412165598779,126.787462587584));
#40291=CARTESIAN_POINT('Ctrl Pts',(123.711480525557,2.72820395221347,126.709877081059));
#40292=CARTESIAN_POINT('Ctrl Pts',(123.703707625291,2.61231174889679,126.637226063814));
#40293=CARTESIAN_POINT('Ctrl Pts',(123.696217289529,2.50063251908489,126.567216094041));
#40294=CARTESIAN_POINT('Ctrl Pts',(123.688726953767,2.38627968726607,126.501788232925));
#40295=CARTESIAN_POINT('Ctrl Pts',(123.681236618005,2.26967144509646,126.441130782477));
#40296=CARTESIAN_POINT('Ctrl Pts',(123.673462283886,2.14864196598328,126.378173486359));
#40297=CARTESIAN_POINT('Ctrl Pts',(123.665687949767,2.02479928760008,126.320156052226));
#40298=CARTESIAN_POINT('Ctrl Pts',(123.657913615648,1.89858475860032,126.267339681212));
#40299=CARTESIAN_POINT('Ctrl Pts',(123.650148862701,1.77252577772743,126.214588401655));
#40300=CARTESIAN_POINT('Ctrl Pts',(123.642384109754,1.64410111952157,126.167025581009));
#40301=CARTESIAN_POINT('Ctrl Pts',(123.634619356806,1.51377723537512,126.124866890232));
#40302=CARTESIAN_POINT('Ctrl Pts',(123.626862315921,1.38358279074764,126.08275007206));
#40303=CARTESIAN_POINT('Ctrl Pts',(123.619105275036,1.25149324365598,126.046026821829));
#40304=CARTESIAN_POINT('Ctrl Pts',(123.611348234151,1.11799523071876,126.01486484801));
#40305=CARTESIAN_POINT('Ctrl Pts',(123.603597042911,0.984597889671743,125.983726373679));
#40306=CARTESIAN_POINT('Ctrl Pts',(123.595845851671,0.849794576084234,125.958140916765));
#40307=CARTESIAN_POINT('Ctrl Pts',(123.588094660431,0.71408696086437,125.938226333062));
#40308=CARTESIAN_POINT('Ctrl Pts',(123.580346763654,0.578437025000908,125.918320213589));
#40309=CARTESIAN_POINT('Ctrl Pts',(123.572598866877,0.441883937965077,125.904080230124));
#40310=CARTESIAN_POINT('Ctrl Pts',(123.5648509701,0.304939219190822,125.895573075301));
#40311=CARTESIAN_POINT('Ctrl Pts',(123.557104694016,0.168023146299548,125.887067699991));
#40312=CARTESIAN_POINT('Ctrl Pts',(123.549358417932,0.0307159945808324,
125.884292792305));
#40313=CARTESIAN_POINT('Ctrl Pts',(123.541612141847,-0.106466337558215,
125.887263101605));
#40314=CARTESIAN_POINT('Ctrl Pts',(123.533865808582,-0.243649682346075,
125.890233432831));
#40315=CARTESIAN_POINT('Ctrl Pts',(123.526119475317,-0.380707814842109,
125.898949057206));
#40316=CARTESIAN_POINT('Ctrl Pts',(123.518373142051,-0.517125979680275,
125.913372600443));
#40317=CARTESIAN_POINT('Ctrl Pts',(123.510625074048,-0.653574694420693,
125.927799373733));
#40318=CARTESIAN_POINT('Ctrl Pts',(123.502877006045,-0.789382767596694,
125.947936568353));
#40319=CARTESIAN_POINT('Ctrl Pts',(123.495128938042,-0.924042095902742,
125.973695107773));
#40320=CARTESIAN_POINT('Ctrl Pts',(123.487372635301,-1.05884454174529,125.999481023676));
#40321=CARTESIAN_POINT('Ctrl Pts',(123.479616332559,-1.192495419224,126.030900145379));
#40322=CARTESIAN_POINT('Ctrl Pts',(123.471860029817,-1.32449778556986,126.067812435765));
#40323=CARTESIAN_POINT('Ctrl Pts',(123.464099587303,-1.45657060555316,126.104744427352));
#40324=CARTESIAN_POINT('Ctrl Pts',(123.456339144789,-1.5869927896053,126.147175308726));
#40325=CARTESIAN_POINT('Ctrl Pts',(123.448578702274,-1.71528498474409,126.194915913091));
#40326=CARTESIAN_POINT('Ctrl Pts',(123.440805802009,-1.84378312590385,126.242733154913));
#40327=CARTESIAN_POINT('Ctrl Pts',(123.433032901743,-1.97014408480792,126.295877001017));
#40328=CARTESIAN_POINT('Ctrl Pts',(123.425260001478,-2.09391000991764,126.354110744484));
#40329=CARTESIAN_POINT('Ctrl Pts',(123.417769665716,-2.21317673190098,126.410227544694));
#40330=CARTESIAN_POINT('Ctrl Pts',(123.410279329954,-2.3300335432915,126.471070463645));
#40331=CARTESIAN_POINT('Ctrl Pts',(123.402788994192,-2.44409597746751,126.53638944669));
#40332=CARTESIAN_POINT('Ctrl Pts',(123.395013533312,-2.56250028176348,126.604194844679));
#40333=CARTESIAN_POINT('Ctrl Pts',(123.387238072432,-2.67826837869846,126.677038644254));
#40334=CARTESIAN_POINT('Ctrl Pts',(123.379462611551,-2.79094175485048,126.754690608351));
#40335=CARTESIAN_POINT('Ctrl Pts',(123.371696977641,-2.90347272943427,126.832244432482));
#40336=CARTESIAN_POINT('Ctrl Pts',(123.36393134373,-3.01291644728908,126.914594108902));
#40337=CARTESIAN_POINT('Ctrl Pts',(123.356165709819,-3.11883918758244,127.001463671224));
#40338=CARTESIAN_POINT('Ctrl Pts',(123.348409475956,-3.2246337118387,127.088228080761));
#40339=CARTESIAN_POINT('Ctrl Pts',(123.340653242093,-3.32691544683841,127.179501232828));
#40340=CARTESIAN_POINT('Ctrl Pts',(123.33289700823,-3.42528038814454,127.274964447526));
#40341=CARTESIAN_POINT('Ctrl Pts',(123.325146104715,-3.5235777297045,127.370362056644));
#40342=CARTESIAN_POINT('Ctrl Pts',(123.317395201201,-3.61796335350893,127.469943728431));
#40343=CARTESIAN_POINT('Ctrl Pts',(123.309644297686,-3.70806698478605,127.573351131532));
#40344=CARTESIAN_POINT('Ctrl Pts',(123.301897042228,-3.79812820769994,127.67670986469));
#40345=CARTESIAN_POINT('Ctrl Pts',(123.29414978677,-3.88391119257016,127.783890451748));
#40346=CARTESIAN_POINT('Ctrl Pts',(123.286402531312,-3.96508342581776,127.894498681184));
#40347=CARTESIAN_POINT('Ctrl Pts',(123.27865724444,-4.04623503311629,128.005078804954));
#40348=CARTESIAN_POINT('Ctrl Pts',(123.270911957568,-4.12277799061117,128.119084522027));
#40349=CARTESIAN_POINT('Ctrl Pts',(123.263166670696,-4.19442114387112,128.236089928883));
#40350=CARTESIAN_POINT('Ctrl Pts',(123.255419450676,-4.26608217855897,128.353124539141));
#40351=CARTESIAN_POINT('Ctrl Pts',(123.247672230656,-4.33284075699117,128.473160004255));
#40352=CARTESIAN_POINT('Ctrl Pts',(123.239925010636,-4.39444999898795,128.595742889462));
#40353=CARTESIAN_POINT('Ctrl Pts',(123.232176803857,-4.45606708812261,128.718341387989));
#40354=CARTESIAN_POINT('Ctrl Pts',(123.224428597077,-4.51253336610795,128.843487599983));
#40355=CARTESIAN_POINT('Ctrl Pts',(123.216680390298,-4.56364912406604,128.970705869553));
#40356=CARTESIAN_POINT('Ctrl Pts',(123.208926340544,-4.61480342876115,129.098020075276));
#40357=CARTESIAN_POINT('Ctrl Pts',(123.201172290789,-4.66059901697531,129.22740909341));
#40358=CARTESIAN_POINT('Ctrl Pts',(123.193418241035,-4.70088522222651,129.358379569989));
#40359=CARTESIAN_POINT('Ctrl Pts',(123.1890237041,-4.7237170614039,129.432605892364));
#40360=CARTESIAN_POINT('Ctrl Pts',(123.184629167164,-4.74478022412167,129.507339900102));
#40361=CARTESIAN_POINT('Ctrl Pts',(123.180234630229,-4.76405452823405,129.582490119308));
#40362=CARTESIAN_POINT('Origin',(213.235140564004,0.,130.804360617566));
#40363=CARTESIAN_POINT('',(121.084721392599,-4.76405452823403,129.582490119308));
#40364=CARTESIAN_POINT('',(121.429936586327,-4.76405452823403,129.582490119308));
#40365=CARTESIAN_POINT('',(213.235140564004,-4.76405452823405,129.582490119308));
#40366=CARTESIAN_POINT('',(122.764859436046,-4.91824884389311,130.800988371423));
#40367=CARTESIAN_POINT('Ctrl Pts',(122.764859435991,-4.91824884389379,130.800988372406));
#40368=CARTESIAN_POINT('Ctrl Pts',(122.757077499762,-4.91834342005838,130.938922920481));
#40369=CARTESIAN_POINT('Ctrl Pts',(122.749295563533,-4.91263101685004,131.07689628956));
#40370=CARTESIAN_POINT('Ctrl Pts',(122.741513627304,-4.90112854599004,131.214387492516));
#40371=CARTESIAN_POINT('Ctrl Pts',(122.733731688858,-4.88962607185356,131.351878734637));
#40372=CARTESIAN_POINT('Ctrl Pts',(122.725949750412,-4.87233355806728,131.488887425918));
#40373=CARTESIAN_POINT('Ctrl Pts',(122.718167811966,-4.84931988728419,131.624896840587));
#40374=CARTESIAN_POINT('Ctrl Pts',(122.710384244513,-4.82630139900788,131.760934726352));
#40375=CARTESIAN_POINT('Ctrl Pts',(122.702600677061,-4.79755943368696,131.895972538746));
#40376=CARTESIAN_POINT('Ctrl Pts',(122.694817109608,-4.7632141111743,132.029503218903));
#40377=CARTESIAN_POINT('Ctrl Pts',(122.687030285658,-4.72885441923102,132.16308976576));
#40378=CARTESIAN_POINT('Ctrl Pts',(122.679243461708,-4.68888679902929,132.295167551827));
#40379=CARTESIAN_POINT('Ctrl Pts',(122.671456637758,-4.64348129810139,132.425244480365));
#40380=CARTESIAN_POINT('Ctrl Pts',(122.663660039455,-4.59801880225171,132.555484687013));
#40381=CARTESIAN_POINT('Ctrl Pts',(122.655863441152,-4.54710492090752,132.683718655831));
#40382=CARTESIAN_POINT('Ctrl Pts',(122.648066842848,-4.49095818467999,132.809473493679));
#40383=CARTESIAN_POINT('Ctrl Pts',(122.640264859057,-4.43477266518489,132.93531519648));
#40384=CARTESIAN_POINT('Ctrl Pts',(122.632462875266,-4.37334726035518,133.05867401179));
#40385=CARTESIAN_POINT('Ctrl Pts',(122.624660891475,-4.30694614418969,133.179102282158));
#40386=CARTESIAN_POINT('Ctrl Pts',(122.61684628404,-4.24043759072811,133.299725405994));
#40387=CARTESIAN_POINT('Ctrl Pts',(122.609031676606,-4.16893744484744,133.417408184763));
#40388=CARTESIAN_POINT('Ctrl Pts',(122.601217069171,-4.0927532286261,133.531731892635));
#40389=CARTESIAN_POINT('Ctrl Pts',(122.596489752418,-4.04666685453286,133.600890117659));
#40390=CARTESIAN_POINT('Ctrl Pts',(122.591762435665,-3.99886717083042,133.668819733568));
#40391=CARTESIAN_POINT('Ctrl Pts',(122.587035118912,-3.94942912399173,133.735434253124));
#40392=CARTESIAN_POINT('Ctrl Pts',(122.579260784793,-3.86812551891892,133.844985518526));
#40393=CARTESIAN_POINT('Ctrl Pts',(122.571486450674,-3.7821314976183,133.951324880725));
#40394=CARTESIAN_POINT('Ctrl Pts',(122.563712116555,-3.69172971392083,134.054024412769));
#40395=CARTESIAN_POINT('Ctrl Pts',(122.555947363608,-3.60143934234245,134.156597376818));
#40396=CARTESIAN_POINT('Ctrl Pts',(122.548182610661,-3.50675227261767,134.255539145399));
#40397=CARTESIAN_POINT('Ctrl Pts',(122.540417857714,-3.40799364663902,134.350451756689));
#40398=CARTESIAN_POINT('Ctrl Pts',(122.532660816829,-3.30933310911974,134.445270099436));
#40399=CARTESIAN_POINT('Ctrl Pts',(122.524903775944,-3.20660934300837,134.536066979527));
#40400=CARTESIAN_POINT('Ctrl Pts',(122.517146735059,-3.10018661986303,134.622478738384));
#40401=CARTESIAN_POINT('Ctrl Pts',(122.509395543819,-2.99384415092098,134.708825333462));
#40402=CARTESIAN_POINT('Ctrl Pts',(122.501644352579,-2.88380857938552,134.790793143953));
#40403=CARTESIAN_POINT('Ctrl Pts',(122.493893161339,-2.77047950106459,134.868056767216));
#40404=CARTESIAN_POINT('Ctrl Pts',(122.486145264561,-2.65719859062533,134.945287551378));
#40405=CARTESIAN_POINT('Ctrl Pts',(122.478397367784,-2.54062727991032,135.017817905205));
#40406=CARTESIAN_POINT('Ctrl Pts',(122.470649471007,-2.42119639869134,135.085364128598));
#40407=CARTESIAN_POINT('Ctrl Pts',(122.462903194923,-2.30179049983808,135.152896222776));
#40408=CARTESIAN_POINT('Ctrl Pts',(122.455156918839,-2.17952656034801,135.215446067909));
#40409=CARTESIAN_POINT('Ctrl Pts',(122.447410642755,-2.05486206649551,135.27277476021));
#40410=CARTESIAN_POINT('Ctrl Pts',(122.43966430949,-1.93019665239795,135.330103875698));
#40411=CARTESIAN_POINT('Ctrl Pts',(122.431917976224,-1.8031310037848,135.382211598101));
#40412=CARTESIAN_POINT('Ctrl Pts',(122.424171642959,-1.67414437648625,135.428906397335));
#40413=CARTESIAN_POINT('Ctrl Pts',(122.416423574956,-1.54512886352728,135.475611653545));
#40414=CARTESIAN_POINT('Ctrl Pts',(122.408675506953,-1.41419188340241,135.516901441418));
#40415=CARTESIAN_POINT('Ctrl Pts',(122.40092743895,-1.28182932303529,135.552633635107));
#40416=CARTESIAN_POINT('Ctrl Pts',(122.393171136208,-1.14932608616351,135.588403805397));
#40417=CARTESIAN_POINT('Ctrl Pts',(122.385414833466,-1.0153946204819,135.61860448022));
#40418=CARTESIAN_POINT('Ctrl Pts',(122.377658530724,-0.880543065243223,
135.643144242895));
#40419=CARTESIAN_POINT('Ctrl Pts',(122.36989808821,-0.745619535668938,135.667697103181));
#40420=CARTESIAN_POINT('Ctrl Pts',(122.362137645696,-0.609775325071402,
135.686582977114));
#40421=CARTESIAN_POINT('Ctrl Pts',(122.354377203182,-0.473524242544293,
135.699762322659));
#40422=CARTESIAN_POINT('Ctrl Pts',(122.346604302916,-0.337054437683895,
135.712962824858));
#40423=CARTESIAN_POINT('Ctrl Pts',(122.338831402651,-0.200176846306303,
135.720438471486));
#40424=CARTESIAN_POINT('Ctrl Pts',(122.331058502385,-0.0634067344431984,
135.722201876546));
#40425=CARTESIAN_POINT('Ctrl Pts',(122.323568166623,0.0683914393515826,
135.723901177391));
#40426=CARTESIAN_POINT('Ctrl Pts',(122.316077830861,0.200089504363081,135.720296343466));
#40427=CARTESIAN_POINT('Ctrl Pts',(122.308587495099,0.331232350231125,135.711444088698));
#40428=CARTESIAN_POINT('Ctrl Pts',(122.30081316098,0.467347516959299,135.702256198001));
#40429=CARTESIAN_POINT('Ctrl Pts',(122.293038826861,0.603295703098704,135.687386015155));
#40430=CARTESIAN_POINT('Ctrl Pts',(122.285264492742,0.73856410028404,135.666840039864));
#40431=CARTESIAN_POINT('Ctrl Pts',(122.277499739795,0.873665791258854,135.646319385651));
#40432=CARTESIAN_POINT('Ctrl Pts',(122.269734986848,1.00808897738918,135.62013691492));
#40433=CARTESIAN_POINT('Ctrl Pts',(122.261970233901,1.14132309498719,135.588351070666));
#40434=CARTESIAN_POINT('Ctrl Pts',(122.254213193016,1.2744248825815,135.55659679656));
#40435=CARTESIAN_POINT('Ctrl Pts',(122.246456152131,1.40633957405435,135.519250314369));
#40436=CARTESIAN_POINT('Ctrl Pts',(122.238699111246,1.53656431546861,135.476421529725));
#40437=CARTESIAN_POINT('Ctrl Pts',(122.230947920006,1.66669085339236,135.433625042602));
#40438=CARTESIAN_POINT('Ctrl Pts',(122.223196728765,1.79512960799016,135.385354603645));
#40439=CARTESIAN_POINT('Ctrl Pts',(122.215445537525,1.92139081750991,135.33177051605));
#40440=CARTESIAN_POINT('Ctrl Pts',(122.207697640748,2.0475983626474,135.278209203121));
#40441=CARTESIAN_POINT('Ctrl Pts',(122.199949743971,2.17162984434234,135.219338885842));
#40442=CARTESIAN_POINT('Ctrl Pts',(122.192201847194,2.29301370365112,135.155368686665));
#40443=CARTESIAN_POINT('Ctrl Pts',(122.18445557111,2.41437217207336,135.091411868676));
#40444=CARTESIAN_POINT('Ctrl Pts',(122.176709295026,2.53308377404431,135.022357472847));
#40445=CARTESIAN_POINT('Ctrl Pts',(122.168963018942,2.64870023053681,134.948461262007));
#40446=CARTESIAN_POINT('Ctrl Pts',(122.161216685677,2.7643175404838,134.874564505681));
#40447=CARTESIAN_POINT('Ctrl Pts',(122.153470352411,2.87683932993553,134.795826073578));
#40448=CARTESIAN_POINT('Ctrl Pts',(122.145724019146,2.98584540972476,134.71254565051));
#40449=CARTESIAN_POINT('Ctrl Pts',(122.137975951143,3.09487590066947,134.629246577369));
#40450=CARTESIAN_POINT('Ctrl Pts',(122.13022788314,3.20038880466551,134.541403726566));
#40451=CARTESIAN_POINT('Ctrl Pts',(122.122479815137,3.30199650821807,134.449357479323));
#40452=CARTESIAN_POINT('Ctrl Pts',(122.114723512395,3.40371220164725,134.357213404232));
#40453=CARTESIAN_POINT('Ctrl Pts',(122.106967209653,3.50151411336226,134.260857271452));
#40454=CARTESIAN_POINT('Ctrl Pts',(122.099210906912,3.59505067024195,134.160667179978));
#40455=CARTESIAN_POINT('Ctrl Pts',(122.091450464397,3.68863715039857,134.060423614036));
#40456=CARTESIAN_POINT('Ctrl Pts',(122.083690021883,3.7779534850219,133.956342308526));
#40457=CARTESIAN_POINT('Ctrl Pts',(122.075929579369,3.86268867991028,133.848834172155));
#40458=CARTESIAN_POINT('Ctrl Pts',(122.068156679104,3.94755989925581,133.74115345418));
#40459=CARTESIAN_POINT('Ctrl Pts',(122.060383778838,4.02783505404528,133.630035229584));
#40460=CARTESIAN_POINT('Ctrl Pts',(122.052610878573,4.10324624292248,133.515919824451));
#40461=CARTESIAN_POINT('Ctrl Pts',(122.045120542811,4.17591604513422,133.405952801735));
#40462=CARTESIAN_POINT('Ctrl Pts',(122.037630207049,4.24406921730083,133.29320298897));
#40463=CARTESIAN_POINT('Ctrl Pts',(122.030139871287,4.30750747618878,133.178083938654));
#40464=CARTESIAN_POINT('Ctrl Pts',(122.022365537168,4.37335101594443,133.058600114555));
#40465=CARTESIAN_POINT('Ctrl Pts',(122.014591203049,4.43432362529838,132.936185358251));
#40466=CARTESIAN_POINT('Ctrl Pts',(122.00681686893,4.49015358718661,132.811274623191));
#40467=CARTESIAN_POINT('Ctrl Pts',(121.999052115983,4.54591474363659,132.686517829448));
#40468=CARTESIAN_POINT('Ctrl Pts',(121.991287363035,4.59654570505646,132.559271530921));
#40469=CARTESIAN_POINT('Ctrl Pts',(121.983522610088,4.64181966904977,132.429996869168));
#40470=CARTESIAN_POINT('Ctrl Pts',(121.975765569203,4.68704866630361,132.300850604832));
#40471=CARTESIAN_POINT('Ctrl Pts',(121.968008528318,4.72693112606523,132.169680353015));
#40472=CARTESIAN_POINT('Ctrl Pts',(121.960251487433,4.76128771022092,132.036968585656));
#40473=CARTESIAN_POINT('Ctrl Pts',(121.952500296193,4.79561838580935,131.904356897273));
#40474=CARTESIAN_POINT('Ctrl Pts',(121.944749104953,4.82443138257623,131.770206384128));
#40475=CARTESIAN_POINT('Ctrl Pts',(121.936997913713,4.8475968399493,131.635015744447));
#40476=CARTESIAN_POINT('Ctrl Pts',(121.929250016936,4.87075245138502,131.499882564394));
#40477=CARTESIAN_POINT('Ctrl Pts',(121.921502120159,4.88826523165698,131.363710521612));
#40478=CARTESIAN_POINT('Ctrl Pts',(121.913754223382,4.90005623228201,131.227009387793));
#40479=CARTESIAN_POINT('Ctrl Pts',(121.906007947298,4.91184476648389,131.090336848903));
#40480=CARTESIAN_POINT('Ctrl Pts',(121.898261671214,4.91791386810852,130.953135828385));
#40481=CARTESIAN_POINT('Ctrl Pts',(121.89051539513,4.91823641190225,130.815921722135));
#40482=CARTESIAN_POINT('Ctrl Pts',(121.882769061864,4.91855895807692,130.678706603002));
#40483=CARTESIAN_POINT('Ctrl Pts',(121.875022728599,4.91313486085608,130.541478788909));
#40484=CARTESIAN_POINT('Ctrl Pts',(121.867276395333,4.90198913105274,130.404753783865));
#40485=CARTESIAN_POINT('Ctrl Pts',(121.85952832733,4.89084090524046,130.267998160203));
#40486=CARTESIAN_POINT('Ctrl Pts',(121.851780259328,4.87396852892708,130.13174595925));
#40487=CARTESIAN_POINT('Ctrl Pts',(121.844032191325,4.85144885991235,129.996507275582));
#40488=CARTESIAN_POINT('Ctrl Pts',(121.836275888583,4.82890525672543,129.861124858631));
#40489=CARTESIAN_POINT('Ctrl Pts',(121.828519585841,4.80070243549678,129.726758497014));
#40490=CARTESIAN_POINT('Ctrl Pts',(121.820763283099,4.76696846775993,129.593908350898));
#40491=CARTESIAN_POINT('Ctrl Pts',(121.813002840585,4.73321649518879,129.460987298658));
#40492=CARTESIAN_POINT('Ctrl Pts',(121.805242398071,4.69392760566475,129.329584448815));
#40493=CARTESIAN_POINT('Ctrl Pts',(121.797481955556,4.64927940835654,129.200183555789));
#40494=CARTESIAN_POINT('Ctrl Pts',(121.789709055291,4.60455953779834,129.070574936962));
#40495=CARTESIAN_POINT('Ctrl Pts',(121.781936155026,4.5544633104076,128.94297506112));
#40496=CARTESIAN_POINT('Ctrl Pts',(121.77416325476,4.49921637776227,128.817847328263));
#40497=CARTESIAN_POINT('Ctrl Pts',(121.766672918998,4.44597781027703,128.697268303674));
#40498=CARTESIAN_POINT('Ctrl Pts',(121.759182583236,4.38795665384656,128.578985081864));
#40499=CARTESIAN_POINT('Ctrl Pts',(121.751692247474,4.32539366496889,128.463388019361));
#40500=CARTESIAN_POINT('Ctrl Pts',(121.743917913355,4.26045858135254,128.343408059098));
#40501=CARTESIAN_POINT('Ctrl Pts',(121.736143579236,4.19042476460252,128.225941910086));
#40502=CARTESIAN_POINT('Ctrl Pts',(121.728369245117,4.11551128366383,128.111453278548));
#40503=CARTESIAN_POINT('Ctrl Pts',(121.72060449217,4.04069012689533,127.997105744017));
#40504=CARTESIAN_POINT('Ctrl Pts',(121.712839739223,3.96100148351983,127.885728749714));
#40505=CARTESIAN_POINT('Ctrl Pts',(121.705074986275,3.87671073275472,127.777762369195));
#40506=CARTESIAN_POINT('Ctrl Pts',(121.69731794539,3.79250370075155,127.669903222406));
#40507=CARTESIAN_POINT('Ctrl Pts',(121.689560904506,3.70370389664788,127.56544825436));
#40508=CARTESIAN_POINT('Ctrl Pts',(121.681803863621,3.61062030111874,127.464809135159));
#40509=CARTESIAN_POINT('Ctrl Pts',(121.67405267238,3.51760690065301,127.364245908699));
#40510=CARTESIAN_POINT('Ctrl Pts',(121.66630148114,3.42031640315355,127.26749308933));
#40511=CARTESIAN_POINT('Ctrl Pts',(121.6585502899,3.3190981847498,127.174929490999));
#40512=CARTESIAN_POINT('Ctrl Pts',(121.650802393123,3.21792298678888,127.082405234667));
#40513=CARTESIAN_POINT('Ctrl Pts',(121.643054496346,3.11282367611486,126.994066921327));
#40514=CARTESIAN_POINT('Ctrl Pts',(121.635306599569,3.00418646450419,126.910256516622));
#40515=CARTESIAN_POINT('Ctrl Pts',(121.627560323485,2.89557197745617,126.826463643247));
#40516=CARTESIAN_POINT('Ctrl Pts',(121.619814047401,2.7834213708336,126.747197033253));
#40517=CARTESIAN_POINT('Ctrl Pts',(121.612067771317,2.66815359993932,126.672758091956));
#40518=CARTESIAN_POINT('Ctrl Pts',(121.604321438051,2.55288497816469,126.598318601167));
#40519=CARTESIAN_POINT('Ctrl Pts',(121.596575104786,2.43449947463561,126.528707062284));
#40520=CARTESIAN_POINT('Ctrl Pts',(121.588828771521,2.31344431643005,126.46418107551));
#40521=CARTESIAN_POINT('Ctrl Pts',(121.581080703518,2.1923620487613,126.39964063859));
#40522=CARTESIAN_POINT('Ctrl Pts',(121.573332635515,2.06860928170925,126.340188203873));
#40523=CARTESIAN_POINT('Ctrl Pts',(121.565584567512,1.94265671580499,126.286034827294));
#40524=CARTESIAN_POINT('Ctrl Pts',(121.55782826477,1.81657028601448,126.231823895862));
#40525=CARTESIAN_POINT('Ctrl Pts',(121.550071962028,1.68827974676689,126.182923427572));
#40526=CARTESIAN_POINT('Ctrl Pts',(121.542315659286,1.5582751227677,126.139496021003));
#40527=CARTESIAN_POINT('Ctrl Pts',(121.534555216772,1.42820111138641,126.09604543592));
#40528=CARTESIAN_POINT('Ctrl Pts',(121.526794774258,1.29641156781885,126.058073841363));
#40529=CARTESIAN_POINT('Ctrl Pts',(121.519034331744,1.16340949045483,126.025693290788));
#40530=CARTESIAN_POINT('Ctrl Pts',(121.511261431478,1.03019390634876,125.993260760078));
#40531=CARTESIAN_POINT('Ctrl Pts',(121.503488531213,0.89576228241315,125.966437285288));
#40532=CARTESIAN_POINT('Ctrl Pts',(121.495715630947,0.76062646038363,125.945283498373));
#40533=CARTESIAN_POINT('Ctrl Pts',(121.488225295185,0.630403165870012,125.924898704896));
#40534=CARTESIAN_POINT('Ctrl Pts',(121.480734959423,0.499526289109342,125.909778576429));
#40535=CARTESIAN_POINT('Ctrl Pts',(121.473244623661,0.368454382871144,125.899931554949));
#40536=CARTESIAN_POINT('Ctrl Pts',(121.465470289542,0.232412845470919,125.889711180657));
#40537=CARTESIAN_POINT('Ctrl Pts',(121.457695955423,0.0957302588679489,
125.885139291338));
#40538=CARTESIAN_POINT('Ctrl Pts',(121.449921621304,-0.0410848356421021,
125.886282222626));
#40539=CARTESIAN_POINT('Ctrl Pts',(121.442156868357,-0.177731317775314,
125.887423745352));
#40540=CARTESIAN_POINT('Ctrl Pts',(121.43439211541,-0.314509595690544,125.894266071969));
#40541=CARTESIAN_POINT('Ctrl Pts',(121.426627362463,-0.450905979092884,
125.906823801929));
#40542=CARTESIAN_POINT('Ctrl Pts',(121.418870321578,-0.587166891684377,
125.919369059375));
#40543=CARTESIAN_POINT('Ctrl Pts',(121.411113280693,-0.723046277793696,
125.937618387826));
#40544=CARTESIAN_POINT('Ctrl Pts',(121.403356239808,-0.858030776102852,
125.961534350833));
#40545=CARTESIAN_POINT('Ctrl Pts',(121.395605048567,-0.992913481551806,
125.985432278626));
#40546=CARTESIAN_POINT('Ctrl Pts',(121.387853857327,-1.12690225902049,126.014988267395));
#40547=CARTESIAN_POINT('Ctrl Pts',(121.380102666087,-1.25948955527277,126.050113135297));
#40548=CARTESIAN_POINT('Ctrl Pts',(121.37235476931,-1.39202049838762,126.085223074194));
#40549=CARTESIAN_POINT('Ctrl Pts',(121.364606872533,-1.52315076788515,126.125897084687));
#40550=CARTESIAN_POINT('Ctrl Pts',(121.356858975756,-1.65238390148433,126.171995076655));
#40551=CARTESIAN_POINT('Ctrl Pts',(121.349112699672,-1.78159000229808,126.218083425917));
#40552=CARTESIAN_POINT('Ctrl Pts',(121.341366423588,-1.9088993885437,126.269593368643));
#40553=CARTESIAN_POINT('Ctrl Pts',(121.333620147504,-2.03383202381809,126.326335342806));
#40554=CARTESIAN_POINT('Ctrl Pts',(121.325873814238,-2.15876558131646,126.383077735825));
#40555=CARTESIAN_POINT('Ctrl Pts',(121.318127480973,-2.28132199686403,126.445052075673));
#40556=CARTESIAN_POINT('Ctrl Pts',(121.310381147707,-2.40104280695426,126.512021336746));
#40557=CARTESIAN_POINT('Ctrl Pts',(121.302633079704,-2.52079042769038,126.57900559512));
#40558=CARTESIAN_POINT('Ctrl Pts',(121.294885011701,-2.6377008382199,126.650986809731));
#40559=CARTESIAN_POINT('Ctrl Pts',(121.287136943698,-2.75134204607348,126.727683047779));
#40560=CARTESIAN_POINT('Ctrl Pts',(121.279380640957,-2.86510403315464,126.8044607995));
#40561=CARTESIAN_POINT('Ctrl Pts',(121.271624338215,-2.97558955219394,126.885963365975));
#40562=CARTESIAN_POINT('Ctrl Pts',(121.263868035473,-3.0823969340792,126.971866364044));
#40563=CARTESIAN_POINT('Ctrl Pts',(121.256107592959,-3.18926132228037,127.05781521113));
#40564=CARTESIAN_POINT('Ctrl Pts',(121.248347150444,-3.29244336763037,127.148168912241));
#40565=CARTESIAN_POINT('Ctrl Pts',(121.24058670793,-3.39157691346575,127.242564848218));
#40566=CARTESIAN_POINT('Ctrl Pts',(121.232813807665,-3.49086959726937,127.337112316931));
#40567=CARTESIAN_POINT('Ctrl Pts',(121.225040907399,-3.58610052270303,127.435714706125));
#40568=CARTESIAN_POINT('Ctrl Pts',(121.217268007134,-3.67694201542359,127.537974161907));
#40569=CARTESIAN_POINT('Ctrl Pts',(121.209777671372,-3.76448119106748,127.636516228894));
#40570=CARTESIAN_POINT('Ctrl Pts',(121.20228733561,-3.84794433210451,127.738453853171));
#40571=CARTESIAN_POINT('Ctrl Pts',(121.194796999848,-3.92707647708734,127.843405804401));
#40572=CARTESIAN_POINT('Ctrl Pts',(121.186993411415,-4.00951800052268,127.952746941921));
#40573=CARTESIAN_POINT('Ctrl Pts',(121.179189822982,-4.08752191368574,128.065709362174));
#40574=CARTESIAN_POINT('Ctrl Pts',(121.171386234549,-4.16075448563075,128.181898954776));
#40575=CARTESIAN_POINT('Ctrl Pts',(121.163595494578,-4.23386648151851,128.297897243391));
#40576=CARTESIAN_POINT('Ctrl Pts',(121.155804754607,-4.30222257832876,128.417111797096));
#40577=CARTESIAN_POINT('Ctrl Pts',(121.148014014637,-4.36553000502787,128.539116516437));
#40578=CARTESIAN_POINT('Ctrl Pts',(121.14023066725,-4.42877735971003,128.66100546627));
#40579=CARTESIAN_POINT('Ctrl Pts',(121.132447319863,-4.48698539601392,128.785678974622));
#40580=CARTESIAN_POINT('Ctrl Pts',(121.124663972476,-4.53990506589921,128.912682776304));
#40581=CARTESIAN_POINT('Ctrl Pts',(121.116887539582,-4.59277772353407,129.039573751611));
#40582=CARTESIAN_POINT('Ctrl Pts',(121.109111106688,-4.64037122070024,129.168790542686));
#40583=CARTESIAN_POINT('Ctrl Pts',(121.101334673793,-4.68248308927141,129.299855655398));
#40584=CARTESIAN_POINT('Ctrl Pts',(121.095796913395,-4.71247183105595,129.393189861536));
#40585=CARTESIAN_POINT('Ctrl Pts',(121.090259152997,-4.73968170673913,129.487460858209));
#40586=CARTESIAN_POINT('Ctrl Pts',(121.084721392599,-4.76405452823403,129.582490119308));
#40587=CARTESIAN_POINT('Ctrl Pts',(122.834626183723,-4.76405452823408,129.582490119308));
#40588=CARTESIAN_POINT('Ctrl Pts',(122.825759709209,-4.80279549980021,129.733540579468));
#40589=CARTESIAN_POINT('Ctrl Pts',(122.816893234695,-4.83439229329883,129.886605462658));
#40590=CARTESIAN_POINT('Ctrl Pts',(122.808026760181,-4.85865542249204,130.041045120547));
#40591=CARTESIAN_POINT('Ctrl Pts',(122.799219852322,-4.88275554738768,130.194447223563));
#40592=CARTESIAN_POINT('Ctrl Pts',(122.790412944462,-4.89962012903744,130.349205529587));
#40593=CARTESIAN_POINT('Ctrl Pts',(122.781606036603,-4.90911101441911,130.504673930159));
#40594=CARTESIAN_POINT('Ctrl Pts',(122.776023836418,-4.91512674922489,130.603216545616));
#40595=CARTESIAN_POINT('Ctrl Pts',(122.770441636232,-4.91818100174923,130.70204406795));
#40596=CARTESIAN_POINT('Ctrl Pts',(122.764859436046,-4.91824884389311,130.800988371423));
#40597=CARTESIAN_POINT('',(123.110140563952,-4.91824976192362,130.802830310975));
#40598=CARTESIAN_POINT('Ctrl Pts',(123.180234630229,-4.76405452823405,129.582490119308));
#40599=CARTESIAN_POINT('Ctrl Pts',(123.172471174879,-4.79810480510647,129.715251632049));
#40600=CARTESIAN_POINT('Ctrl Pts',(123.164707719529,-4.8265692317211,129.849312316196));
#40601=CARTESIAN_POINT('Ctrl Pts',(123.15694426418,-4.8493770688196,129.984162405603));
#40602=CARTESIAN_POINT('Ctrl Pts',(123.14916959278,-4.87221785694477,130.119207316154));
#40603=CARTESIAN_POINT('Ctrl Pts',(123.141394921381,-4.88938569015853,130.25504352242));
#40604=CARTESIAN_POINT('Ctrl Pts',(123.133620249982,-4.90086176145776,130.391157208116));
#40605=CARTESIAN_POINT('Ctrl Pts',(123.130527290115,-4.90542723132088,130.445306656459));
#40606=CARTESIAN_POINT('Ctrl Pts',(123.127434330247,-4.90909247502338,130.499500032022));
#40607=CARTESIAN_POINT('Ctrl Pts',(123.124341370379,-4.91185859746714,130.553705114957));
#40608=CARTESIAN_POINT('Ctrl Pts',(123.119607768255,-4.9160919931895,130.636662963314));
#40609=CARTESIAN_POINT('Ctrl Pts',(123.114874166132,-4.91822390503836,130.719728964701));
#40610=CARTESIAN_POINT('Ctrl Pts',(123.110140564008,-4.91824976192331,130.80283030999));
#40611=CARTESIAN_POINT('Ctrl Pts',(123.110140563952,-4.91824976192362,130.802830310975));
#40612=CARTESIAN_POINT('Ctrl Pts',(123.102428017502,-4.91829189100263,130.938228886704));
#40613=CARTESIAN_POINT('Ctrl Pts',(123.094715471052,-4.91273854065694,131.07385488417));
#40614=CARTESIAN_POINT('Ctrl Pts',(123.087002924603,-4.90155952306506,131.209202937921));
#40615=CARTESIAN_POINT('Ctrl Pts',(123.079299655817,-4.89039395306417,131.344388177251));
#40616=CARTESIAN_POINT('Ctrl Pts',(123.071596387031,-4.87361620922271,131.479295745428));
#40617=CARTESIAN_POINT('Ctrl Pts',(123.063893118246,-4.85124808336885,131.613418771292));
#40618=CARTESIAN_POINT('Ctrl Pts',(123.056197200275,-4.8289013022153,131.74741381076));
#40619=CARTESIAN_POINT('Ctrl Pts',(123.048501282305,-4.80097481726048,131.880625407544));
#40620=CARTESIAN_POINT('Ctrl Pts',(123.040805364335,-4.76754230610144,132.012550760728));
#40621=CARTESIAN_POINT('Ctrl Pts',(123.033114877499,-4.73413338880946,132.144383012043));
#40622=CARTESIAN_POINT('Ctrl Pts',(123.025424390663,-4.69522627500157,132.274930442014));
#40623=CARTESIAN_POINT('Ctrl Pts',(123.017733903828,-4.65094582541877,132.403699853476));
#40624=CARTESIAN_POINT('Ctrl Pts',(123.010046117276,-4.60668092358835,132.532424051418));
#40625=CARTESIAN_POINT('Ctrl Pts',(123.002358330724,-4.55704656498262,132.659371096231));
#40626=CARTESIAN_POINT('Ctrl Pts',(122.994670544172,-4.5022175488539,132.784062667192));
#40627=CARTESIAN_POINT('Ctrl Pts',(122.986983894752,-4.44739664270996,132.90873579451));
#40628=CARTESIAN_POINT('Ctrl Pts',(122.979297245332,-4.38738276700006,133.031153747441));
#40629=CARTESIAN_POINT('Ctrl Pts',(122.971610595913,-4.32239877614302,133.150858408423));
#40630=CARTESIAN_POINT('Ctrl Pts',(122.963923353924,-4.25740977562546,133.27057229752));
#40631=CARTESIAN_POINT('Ctrl Pts',(122.956236111935,-4.18745008770041,133.387572129125));
#40632=CARTESIAN_POINT('Ctrl Pts',(122.948548869946,-4.11278817141666,133.501425043855));
#40633=CARTESIAN_POINT('Ctrl Pts',(122.940859305564,-4.03810369901763,133.615312354695));
#40634=CARTESIAN_POINT('Ctrl Pts',(122.933169741182,-3.95871439066999,133.72605052528));
#40635=CARTESIAN_POINT('Ctrl Pts',(122.9254801768,-3.8749313152967,133.833236706849));
#40636=CARTESIAN_POINT('Ctrl Pts',(122.917782267932,-3.79105732103234,133.940539203661));
#40637=CARTESIAN_POINT('Ctrl Pts',(122.910084359065,-3.70278028615443,134.044281702914));
#40638=CARTESIAN_POINT('Ctrl Pts',(122.902386450197,-3.6104509844101,134.14409515068));
#40639=CARTESIAN_POINT('Ctrl Pts',(122.894683774628,-3.51806451049176,134.243970404954));
#40640=CARTESIAN_POINT('Ctrl Pts',(122.88698109906,-3.42162105445613,134.339911483451));
#40641=CARTESIAN_POINT('Ctrl Pts',(122.879278423491,-3.32150645419486,134.431587924648));
#40642=CARTESIAN_POINT('Ctrl Pts',(122.871564556849,-3.22124639930248,134.523397560833));
#40643=CARTESIAN_POINT('Ctrl Pts',(122.863850690207,-3.11730485552744,134.610929935339));
#40644=CARTESIAN_POINT('Ctrl Pts',(122.856136823565,-3.01009907664712,134.693896143984));
#40645=CARTESIAN_POINT('Ctrl Pts',(122.852722464565,-2.96264699678834,134.730619156487));
#40646=CARTESIAN_POINT('Ctrl Pts',(122.849308105566,-2.91455575475838,134.766448159479));
#40647=CARTESIAN_POINT('Ctrl Pts',(122.845893746566,-2.86586312402484,134.801360944918));
#40648=CARTESIAN_POINT('Ctrl Pts',(122.838119412447,-2.75499230449017,134.880855707794));
#40649=CARTESIAN_POINT('Ctrl Pts',(122.830345078328,-2.64063576786579,134.95585980224));
#40650=CARTESIAN_POINT('Ctrl Pts',(122.822570744209,-2.52319333105665,135.026052041227));
#40651=CARTESIAN_POINT('Ctrl Pts',(122.814805991262,-2.4058956315549,135.096157774553));
#40652=CARTESIAN_POINT('Ctrl Pts',(122.807041238315,-2.28551993126846,135.161463253064));
#40653=CARTESIAN_POINT('Ctrl Pts',(122.799276485368,-2.16249735672644,135.221688796981));
#40654=CARTESIAN_POINT('Ctrl Pts',(122.791519444483,-2.03959696993951,135.281854524039));
#40655=CARTESIAN_POINT('Ctrl Pts',(122.783762403598,-1.91405528942545,135.33695018641));
#40656=CARTESIAN_POINT('Ctrl Pts',(122.776005362713,-1.78633022874239,135.386740717076));
#40657=CARTESIAN_POINT('Ctrl Pts',(122.768254171473,-1.65870148652097,135.436493700315));
#40658=CARTESIAN_POINT('Ctrl Pts',(122.760502980232,-1.52889300418891,135.480949373456));
#40659=CARTESIAN_POINT('Ctrl Pts',(122.752751788992,-1.3973846517481,135.519919884245));
#40660=CARTESIAN_POINT('Ctrl Pts',(122.745003892215,-1.26593219386545,135.558873831527));
#40661=CARTESIAN_POINT('Ctrl Pts',(122.737255995438,-1.13278167691982,135.592347142465));
#40662=CARTESIAN_POINT('Ctrl Pts',(122.729508098661,-0.998429980033417,
135.620201212672));
#40663=CARTESIAN_POINT('Ctrl Pts',(122.721761822577,-0.86410638662562,135.648049456408));
#40664=CARTESIAN_POINT('Ctrl Pts',(122.714015546493,-0.728582495630703,
135.670280718076));
#40665=CARTESIAN_POINT('Ctrl Pts',(122.706269270409,-0.59236689178891,135.686807189523));
#40666=CARTESIAN_POINT('Ctrl Pts',(122.698522937143,-0.456150282434567,
135.703333782964));
#40667=CARTESIAN_POINT('Ctrl Pts',(122.690776603878,-0.319242338163657,
135.714155455064));
#40668=CARTESIAN_POINT('Ctrl Pts',(122.683030270613,-0.182157908796801,
135.719236156047));
#40669=CARTESIAN_POINT('Ctrl Pts',(122.67528220261,-0.0450427803222785,
135.724317994819));
#40670=CARTESIAN_POINT('Ctrl Pts',(122.667534134607,0.092248521271429,135.7236562897));
#40671=CARTESIAN_POINT('Ctrl Pts',(122.659786066604,0.229200394152558,135.71726711391));
#40672=CARTESIAN_POINT('Ctrl Pts',(122.652029763862,0.366297821113747,135.710871147628));
#40673=CARTESIAN_POINT('Ctrl Pts',(122.64427346112,0.503054707564457,135.698735569038));
#40674=CARTESIAN_POINT('Ctrl Pts',(122.636517158378,0.638959267758077,135.680928479971));
#40675=CARTESIAN_POINT('Ctrl Pts',(122.628756715864,0.774936364307664,135.663111886725));
#40676=CARTESIAN_POINT('Ctrl Pts',(122.62099627335,0.910059843151345,135.639617818276));
#40677=CARTESIAN_POINT('Ctrl Pts',(122.613235830835,1.04382835863018,135.610565505023));
#40678=CARTESIAN_POINT('Ctrl Pts',(122.60546293057,1.17781161120547,135.581466554418));
#40679=CARTESIAN_POINT('Ctrl Pts',(122.597690030305,1.31043517538972,135.546791627786));
#40680=CARTESIAN_POINT('Ctrl Pts',(122.589917130039,1.441212243248,135.506710065705));
#40681=CARTESIAN_POINT('Ctrl Pts',(122.582426794277,1.56723523528109,135.468085569365));
#40682=CARTESIAN_POINT('Ctrl Pts',(122.574936458515,1.69154335917757,135.424440804636));
#40683=CARTESIAN_POINT('Ctrl Pts',(122.567446122753,1.81372055519902,135.375968738364));
#40684=CARTESIAN_POINT('Ctrl Pts',(122.559671788634,1.94053013674339,135.325658838967));
#40685=CARTESIAN_POINT('Ctrl Pts',(122.551897454515,2.06544570698642,135.269988991084));
#40686=CARTESIAN_POINT('Ctrl Pts',(122.544123120396,2.18798093138022,135.209121962567));
#40687=CARTESIAN_POINT('Ctrl Pts',(122.536358367449,2.31036514206116,135.148329947223));
#40688=CARTESIAN_POINT('Ctrl Pts',(122.528593614502,2.4303744970247,135.082353667665));
#40689=CARTESIAN_POINT('Ctrl Pts',(122.520828861555,2.54754065933153,135.011404669101));
#40690=CARTESIAN_POINT('Ctrl Pts',(122.51307182067,2.66459045055429,134.940526138081));
#40691=CARTESIAN_POINT('Ctrl Pts',(122.505314779784,2.77880233654142,134.864684918038));
#40692=CARTESIAN_POINT('Ctrl Pts',(122.497557738899,2.88973103528868,134.78413920515));
#40693=CARTESIAN_POINT('Ctrl Pts',(122.489806547659,3.00057608184155,134.70365423241));
#40694=CARTESIAN_POINT('Ctrl Pts',(122.482055356419,3.10814255415416,134.61847205708));
#40695=CARTESIAN_POINT('Ctrl Pts',(122.474304165179,3.21201302534738,134.52889486865));
#40696=CARTESIAN_POINT('Ctrl Pts',(122.466556268402,3.31583934881922,134.439355752915));
#40697=CARTESIAN_POINT('Ctrl Pts',(122.458808371625,3.41597250011656,134.345425594184));
#40698=CARTESIAN_POINT('Ctrl Pts',(122.451060474848,3.5120272921393,134.247447511876));
#40699=CARTESIAN_POINT('Ctrl Pts',(122.443314198764,3.60806199157032,134.14948992447));
#40700=CARTESIAN_POINT('Ctrl Pts',(122.43556792268,3.70001975507199,134.047486376701));
#40701=CARTESIAN_POINT('Ctrl Pts',(122.427821646595,3.78755180468155,133.941817292861));
#40702=CARTESIAN_POINT('Ctrl Pts',(122.42007531333,3.87508450043256,133.836147428996));
#40703=CARTESIAN_POINT('Ctrl Pts',(122.412328980065,3.95819116769659,133.726812276151));
#40704=CARTESIAN_POINT('Ctrl Pts',(122.404582646799,4.03656318787289,133.614225506277));
#40705=CARTESIAN_POINT('Ctrl Pts',(122.396834578796,4.11495275891997,133.501613523376));
#40706=CARTESIAN_POINT('Ctrl Pts',(122.389086510793,4.18860534970106,133.385748795274));
#40707=CARTESIAN_POINT('Ctrl Pts',(122.38133844279,4.25725578768592,133.267073800362));
#40708=CARTESIAN_POINT('Ctrl Pts',(122.373582140049,4.32597918817317,133.148272676253));
#40709=CARTESIAN_POINT('Ctrl Pts',(122.365825837307,4.38968961980737,133.02665565787));
#40710=CARTESIAN_POINT('Ctrl Pts',(122.358069534565,4.44816774589062,132.902690135759));
#40711=CARTESIAN_POINT('Ctrl Pts',(122.350309092051,4.5066770835107,132.778658449516));
#40712=CARTESIAN_POINT('Ctrl Pts',(122.342548649537,4.55994839922792,132.652276121997));
#40713=CARTESIAN_POINT('Ctrl Pts',(122.334788207022,4.60781101537796,132.524029396448));
#40714=CARTESIAN_POINT('Ctrl Pts',(122.327015306757,4.65575046484836,132.39557679787));
#40715=CARTESIAN_POINT('Ctrl Pts',(122.319242406491,4.69826374298029,132.265254192401));
#40716=CARTESIAN_POINT('Ctrl Pts',(122.311469506226,4.73523018921738,132.133562678061));
#40717=CARTESIAN_POINT('Ctrl Pts',(122.303979170464,4.77085281202079,132.006658481979));
#40718=CARTESIAN_POINT('Ctrl Pts',(122.296488834702,4.80132481273146,131.878483475337));
#40719=CARTESIAN_POINT('Ctrl Pts',(122.28899849894,4.82658364937024,131.749492004269));
#40720=CARTESIAN_POINT('Ctrl Pts',(122.281224164821,4.85280018247748,131.61560978237));
#40721=CARTESIAN_POINT('Ctrl Pts',(122.273449830702,4.87348347975067,131.48042386274));
#40722=CARTESIAN_POINT('Ctrl Pts',(122.265675496583,4.88850760668973,131.344431392406));
#40723=CARTESIAN_POINT('Ctrl Pts',(122.257910743636,4.90351321773507,131.208606520639));
#40724=CARTESIAN_POINT('Ctrl Pts',(122.250145990689,4.91287349294705,131.071977460805));
#40725=CARTESIAN_POINT('Ctrl Pts',(122.242381237741,4.91651326374388,130.935052583388));
#40726=CARTESIAN_POINT('Ctrl Pts',(122.234624196857,4.92014941946904,130.79826370169));
#40727=CARTESIAN_POINT('Ctrl Pts',(122.226867155971,4.918076367268,130.661179975402));
#40728=CARTESIAN_POINT('Ctrl Pts',(122.219110115086,4.91027064909904,130.524315594228));
#40729=CARTESIAN_POINT('Ctrl Pts',(122.211358923846,4.90247081728285,130.387554423547));
#40730=CARTESIAN_POINT('Ctrl Pts',(122.203607732606,4.88894694643506,130.251012657494));
#40731=CARTESIAN_POINT('Ctrl Pts',(122.195856541366,4.86972764770875,130.115204829924));
#40732=CARTESIAN_POINT('Ctrl Pts',(122.188108644589,4.85051651769716,129.979454724303));
#40733=CARTESIAN_POINT('Ctrl Pts',(122.180360747812,4.82561482908048,129.844438323033));
#40734=CARTESIAN_POINT('Ctrl Pts',(122.172612851035,4.79510305490826,129.710665159356));
#40735=CARTESIAN_POINT('Ctrl Pts',(122.164866574951,4.76459766314141,129.576919978141));
#40736=CARTESIAN_POINT('Ctrl Pts',(122.157120298867,4.72848460687843,129.444417898183));
#40737=CARTESIAN_POINT('Ctrl Pts',(122.149374022783,4.68689542484307,129.313657984884));
#40738=CARTESIAN_POINT('Ctrl Pts',(122.141627689517,4.64530593580589,129.182897106345));
#40739=CARTESIAN_POINT('Ctrl Pts',(122.133881356252,4.59824035883419,129.0538787927));
#40740=CARTESIAN_POINT('Ctrl Pts',(122.126135022987,4.54587991196435,128.927086293313));
#40741=CARTESIAN_POINT('Ctrl Pts',(122.118386954984,4.4935077393355,128.800265399625));
#40742=CARTESIAN_POINT('Ctrl Pts',(122.110638886981,4.4358384865056,128.675671673359));
#40743=CARTESIAN_POINT('Ctrl Pts',(122.102890818978,4.37310109084685,128.553767382054));
#40744=CARTESIAN_POINT('Ctrl Pts',(122.095134516236,4.3102970171372,128.431733529416));
#40745=CARTESIAN_POINT('Ctrl Pts',(122.087378213494,4.24241421971074,128.312395169812));
#40746=CARTESIAN_POINT('Ctrl Pts',(122.079621910752,4.16972737062844,128.196189473425));
#40747=CARTESIAN_POINT('Ctrl Pts',(122.071861468238,4.09700172638623,128.079921754558));
#40748=CARTESIAN_POINT('Ctrl Pts',(122.064101025724,4.01946714228137,127.96679035284));
#40749=CARTESIAN_POINT('Ctrl Pts',(122.05634058321,3.9374404530796,127.857201690573));
#40750=CARTESIAN_POINT('Ctrl Pts',(122.048567682944,3.85528208735434,127.747437106858));
#40751=CARTESIAN_POINT('Ctrl Pts',(122.040794782679,3.76861745372003,127.641226930364));
#40752=CARTESIAN_POINT('Ctrl Pts',(122.033021882413,3.67780292015556,127.538943531956));
#40753=CARTESIAN_POINT('Ctrl Pts',(122.025531546651,3.59028972363337,127.440378392715));
#40754=CARTESIAN_POINT('Ctrl Pts',(122.018041210889,3.4989233211436,127.345459713566));
#40755=CARTESIAN_POINT('Ctrl Pts',(122.010550875127,3.40405216148986,127.254485698029));
#40756=CARTESIAN_POINT('Ctrl Pts',(122.002776541008,3.30558393298314,127.160062375044));
#40757=CARTESIAN_POINT('Ctrl Pts',(121.995002206889,3.20302801752754,127.069589639606));
#40758=CARTESIAN_POINT('Ctrl Pts',(121.98722787277,3.09673460832412,126.983442164091));
#40759=CARTESIAN_POINT('Ctrl Pts',(121.979463119823,2.99057219624776,126.89740085764));
#40760=CARTESIAN_POINT('Ctrl Pts',(121.971698366875,2.88068175606293,126.815674448817));
#40761=CARTESIAN_POINT('Ctrl Pts',(121.963933613928,2.76745036379981,126.738600965741));
#40762=CARTESIAN_POINT('Ctrl Pts',(121.956176573043,2.65433143455208,126.661604033137));
#40763=CARTESIAN_POINT('Ctrl Pts',(121.948419532158,2.53787847786143,126.589251048151));
#40764=CARTESIAN_POINT('Ctrl Pts',(121.940662491273,2.41851141644303,126.521839678792));
#40765=CARTESIAN_POINT('Ctrl Pts',(121.932911300033,2.29923437065411,126.454479144872));
#40766=CARTESIAN_POINT('Ctrl Pts',(121.925160108793,2.17704793327744,126.392053000662));
#40767=CARTESIAN_POINT('Ctrl Pts',(121.917408917553,2.05240046124638,126.334815292908));
#40768=CARTESIAN_POINT('Ctrl Pts',(121.909661020776,1.92780596771602,126.277601912705));
#40769=CARTESIAN_POINT('Ctrl Pts',(121.901913123999,1.80075287450881,126.225572745745));
#40770=CARTESIAN_POINT('Ctrl Pts',(121.894165227222,1.67171336402272,126.178935502936));
#40771=CARTESIAN_POINT('Ctrl Pts',(121.886418951138,1.54270084582046,126.132308015633));
#40772=CARTESIAN_POINT('Ctrl Pts',(121.878672675054,1.41170310427758,126.091070341882));
#40773=CARTESIAN_POINT('Ctrl Pts',(121.870926398969,1.27921111714325,126.055381571468));
#40774=CARTESIAN_POINT('Ctrl Pts',(121.863180065704,1.14671815198298,126.019692537608));
#40775=CARTESIAN_POINT('Ctrl Pts',(121.855433732439,1.01273129673073,125.989552590508));
#40776=CARTESIAN_POINT('Ctrl Pts',(121.847687399173,0.877755075537518,125.965070474387));
#40777=CARTESIAN_POINT('Ctrl Pts',(121.83993933117,0.742748627355887,125.940582875666));
#40778=CARTESIAN_POINT('Ctrl Pts',(121.832191263167,0.606752756966128,125.921755698932));
#40779=CARTESIAN_POINT('Ctrl Pts',(121.824443195164,0.470280129382032,125.908646199587));
#40780=CARTESIAN_POINT('Ctrl Pts',(121.816686892423,0.333662457065015,125.89552276731));
#40781=CARTESIAN_POINT('Ctrl Pts',(121.808930589681,0.196567405153723,125.888129188958));
#40782=CARTESIAN_POINT('Ctrl Pts',(121.801174286939,0.0595112442624678,
125.88647067631));
#40783=CARTESIAN_POINT('Ctrl Pts',(121.793413844425,-0.0776180676289099,
125.884811278464));
#40784=CARTESIAN_POINT('Ctrl Pts',(121.785653401911,-0.214708056538748,
125.888893033948));
#40785=CARTESIAN_POINT('Ctrl Pts',(121.777892959396,-0.351245530942734,
125.898669061884));
#40786=CARTESIAN_POINT('Ctrl Pts',(121.770120059131,-0.488002187421583,
125.908460783167));
#40787=CARTESIAN_POINT('Ctrl Pts',(121.762347158866,-0.624204168315074,
125.923964999191));
#40788=CARTESIAN_POINT('Ctrl Pts',(121.7545742586,-0.759345561872103,125.94508316303));
#40789=CARTESIAN_POINT('Ctrl Pts',(121.747083922838,-0.889574225371972,
125.965433628419));
#40790=CARTESIAN_POINT('Ctrl Pts',(121.739593587076,-1.01881777066954,125.990996905867));
#40791=CARTESIAN_POINT('Ctrl Pts',(121.732103251314,-1.14663696560631,126.021641021812));
#40792=CARTESIAN_POINT('Ctrl Pts',(121.724328917195,-1.27930246416974,126.053447018729));
#40793=CARTESIAN_POINT('Ctrl Pts',(121.716554583076,-1.41085371618547,126.090827491513));
#40794=CARTESIAN_POINT('Ctrl Pts',(121.708780248957,-1.54078621119515,126.133690332276));
#40795=CARTESIAN_POINT('Ctrl Pts',(121.70101549601,-1.67055857601678,126.176500348419));
#40796=CARTESIAN_POINT('Ctrl Pts',(121.693250743063,-1.79871578551457,126.224779167758));
#40797=CARTESIAN_POINT('Ctrl Pts',(121.685485990116,-1.9247642230084,126.278383844722));
#40798=CARTESIAN_POINT('Ctrl Pts',(121.677728949231,-2.05068746741723,126.331935280765));
#40799=CARTESIAN_POINT('Ctrl Pts',(121.669971908346,-2.17450575044197,126.390801895643));
#40800=CARTESIAN_POINT('Ctrl Pts',(121.662214867461,-2.2957416570714,126.454791293313));
#40801=CARTESIAN_POINT('Ctrl Pts',(121.654463676221,-2.41688613876073,126.51873243608));
#40802=CARTESIAN_POINT('Ctrl Pts',(121.646712484981,-2.53545177585653,126.587788490556));
#40803=CARTESIAN_POINT('Ctrl Pts',(121.63896129374,-2.65098248376344,126.661719559825));
#40804=CARTESIAN_POINT('Ctrl Pts',(121.631213396963,-2.76646408803754,126.735619206418));
#40805=CARTESIAN_POINT('Ctrl Pts',(121.623465500186,-2.87891300006648,126.814389536439));
#40806=CARTESIAN_POINT('Ctrl Pts',(121.615717603409,-2.9878992406602,126.897745562283));
#40807=CARTESIAN_POINT('Ctrl Pts',(121.607971327325,-3.09686268368186,126.981084151844));
#40808=CARTESIAN_POINT('Ctrl Pts',(121.600225051241,-3.20236458562215,127.069006291904));
#40809=CARTESIAN_POINT('Ctrl Pts',(121.592478775157,-3.30400571427236,127.161184900893));
#40810=CARTESIAN_POINT('Ctrl Pts',(121.584732441892,-3.40564759321437,127.253364190324));
#40811=CARTESIAN_POINT('Ctrl Pts',(121.576986108626,-3.50342835239185,127.349799748736));
#40812=CARTESIAN_POINT('Ctrl Pts',(121.569239775361,-3.59698379458653,127.450125884578));
#40813=CARTESIAN_POINT('Ctrl Pts',(121.561491707358,-3.69056018787395,127.550474487763));
#40814=CARTESIAN_POINT('Ctrl Pts',(121.553743639355,-3.77990911470321,127.654715116222));
#40815=CARTESIAN_POINT('Ctrl Pts',(121.545995571352,-3.86470529652155,127.762447398301));
#40816=CARTESIAN_POINT('Ctrl Pts',(121.53823926861,-3.94959160073084,127.870294179531));
#40817=CARTESIAN_POINT('Ctrl Pts',(121.530482965868,-4.02991525188601,127.981639719741));
#40818=CARTESIAN_POINT('Ctrl Pts',(121.522726663126,-4.10539280829276,128.096052482933));
#40819=CARTESIAN_POINT('Ctrl Pts',(121.514966220612,-4.180910649344,128.210526311662));
#40820=CARTESIAN_POINT('Ctrl Pts',(121.507205778098,-4.25157704046853,128.328070290464));
#40821=CARTESIAN_POINT('Ctrl Pts',(121.499445335584,-4.31715403132347,128.448227316514));
#40822=CARTESIAN_POINT('Ctrl Pts',(121.491672435318,-4.38283629218579,128.568577229289));
#40823=CARTESIAN_POINT('Ctrl Pts',(121.483899535053,-4.44341265373388,128.691548220728));
#40824=CARTESIAN_POINT('Ctrl Pts',(121.476126634787,-4.49869256862852,128.816661385925));
#40825=CARTESIAN_POINT('Ctrl Pts',(121.468636299025,-4.55196291937478,128.937226372426));
#40826=CARTESIAN_POINT('Ctrl Pts',(121.461145963263,-4.60031510325118,129.05978020333));
#40827=CARTESIAN_POINT('Ctrl Pts',(121.453655627501,-4.64362273764029,129.183882005251));
#40828=CARTESIAN_POINT('Ctrl Pts',(121.445749280443,-4.68933566675726,129.314876388909));
#40829=CARTESIAN_POINT('Ctrl Pts',(121.437842933385,-4.72953256361434,129.4478895032));
#40830=CARTESIAN_POINT('Ctrl Pts',(121.429936586327,-4.76405452823403,129.582490119308));
#40831=CARTESIAN_POINT('Origin',(213.235140564004,0.,130.804360617566));
#40832=CARTESIAN_POINT('',(119.334999413688,-4.76405452823402,129.582490119308));
#40833=CARTESIAN_POINT('',(119.679968582935,-4.76405452823404,129.582490119308));
#40834=CARTESIAN_POINT('',(213.235140564004,-4.76405452823405,129.582490119308));
#40835=CARTESIAN_POINT('',(121.014859435936,-4.9182487480187,130.807869907024));
#40836=CARTESIAN_POINT('Ctrl Pts',(121.014859435936,-4.9182487480187,130.807869907024));
#40837=CARTESIAN_POINT('Ctrl Pts',(121.005990668755,-4.91813660439169,130.965038547478));
#40838=CARTESIAN_POINT('Ctrl Pts',(120.997121901573,-4.91048672634217,131.121906140279));
#40839=CARTESIAN_POINT('Ctrl Pts',(120.988253134392,-4.89540936564683,131.277805656865));
#40840=CARTESIAN_POINT('Ctrl Pts',(120.979341933319,-4.88025986515247,131.434451097094));
#40841=CARTESIAN_POINT('Ctrl Pts',(120.970430732247,-4.85761174710443,131.590119028022));
#40842=CARTESIAN_POINT('Ctrl Pts',(120.961519531174,-4.82762636292375,131.744151425408));
#40843=CARTESIAN_POINT('Ctrl Pts',(120.952553434066,-4.79745625855732,131.899132714857));
#40844=CARTESIAN_POINT('Ctrl Pts',(120.943587336958,-4.75985829917768,132.052458112461));
#40845=CARTESIAN_POINT('Ctrl Pts',(120.93462123985,-4.71504533913386,132.203478379733));
#40846=CARTESIAN_POINT('Ctrl Pts',(120.928530618578,-4.68460413775154,132.306065630483));
#40847=CARTESIAN_POINT('Ctrl Pts',(120.922439997307,-4.65083464287957,132.407589637772));
#40848=CARTESIAN_POINT('Ctrl Pts',(120.916349376035,-4.61381590295559,132.507852876467));
#40849=CARTESIAN_POINT('Ctrl Pts',(120.908575041916,-4.56656357187052,132.63583323885));
#40850=CARTESIAN_POINT('Ctrl Pts',(120.900800707797,-4.51390738478452,132.762048759346));
#40851=CARTESIAN_POINT('Ctrl Pts',(120.893026373678,-4.4559983919868,132.886009337478));
#40852=CARTESIAN_POINT('Ctrl Pts',(120.885261620731,-4.39816076684725,133.009817145276));
#40853=CARTESIAN_POINT('Ctrl Pts',(120.877496867784,-4.33508338044493,133.131375189303));
#40854=CARTESIAN_POINT('Ctrl Pts',(120.869732114837,-4.26696647827154,133.250210190988));
#40855=CARTESIAN_POINT('Ctrl Pts',(120.861975073952,-4.19891723076567,133.368927164073));
#40856=CARTESIAN_POINT('Ctrl Pts',(120.854218033067,-4.12583862146679,133.484926140023));
#40857=CARTESIAN_POINT('Ctrl Pts',(120.846460992182,-4.04797808665986,133.597755769066));
#40858=CARTESIAN_POINT('Ctrl Pts',(120.838709800942,-3.97017626708778,133.710500312408));
#40859=CARTESIAN_POINT('Ctrl Pts',(120.830958609702,-3.88759992086172,133.820079945569));
#40860=CARTESIAN_POINT('Ctrl Pts',(120.823207418461,-3.80054113335574,133.926070110163));
#40861=CARTESIAN_POINT('Ctrl Pts',(120.815459521684,-3.71351934815694,134.03201522611));
#40862=CARTESIAN_POINT('Ctrl Pts',(120.807711624907,-3.62201915852423,134.134373606349));
#40863=CARTESIAN_POINT('Ctrl Pts',(120.79996372813,-3.52637434163955,134.232751940785));
#40864=CARTESIAN_POINT('Ctrl Pts',(120.792217452046,-3.43074953158863,134.331109696595));
#40865=CARTESIAN_POINT('Ctrl Pts',(120.784471175962,-3.33098209108957,134.425488782424));
#40866=CARTESIAN_POINT('Ctrl Pts',(120.776724899878,-3.22744396517328,134.515531391616));
#40867=CARTESIAN_POINT('Ctrl Pts',(120.768978566613,-3.12390507496221,134.605574665483));
#40868=CARTESIAN_POINT('Ctrl Pts',(120.761232233347,-3.01659573880367,134.691281142278));
#40869=CARTESIAN_POINT('Ctrl Pts',(120.753485900082,-2.90592210352628,134.77233236529));
#40870=CARTESIAN_POINT('Ctrl Pts',(120.745737832079,-2.79522368365555,134.853401739162));
#40871=CARTESIAN_POINT('Ctrl Pts',(120.737989764076,-2.68115978082898,134.929813553817));
#40872=CARTESIAN_POINT('Ctrl Pts',(120.730241696073,-2.56416638260516,135.001292094826));
#40873=CARTESIAN_POINT('Ctrl Pts',(120.722485393331,-2.44704864240539,135.07284660408));
#40874=CARTESIAN_POINT('Ctrl Pts',(120.714729090589,-2.3269955214092,135.13945716179));
#40875=CARTESIAN_POINT('Ctrl Pts',(120.706972787847,-2.20446901208997,135.200893278338));
#40876=CARTESIAN_POINT('Ctrl Pts',(120.699212345333,-2.08187710668343,135.262362185191));
#40877=CARTESIAN_POINT('Ctrl Pts',(120.691451902819,-1.95680953884554,135.318650987472));
#40878=CARTESIAN_POINT('Ctrl Pts',(120.683691460305,-1.82974831600096,135.369577388169));
#40879=CARTESIAN_POINT('Ctrl Pts',(120.675918560039,-1.7024831232016,135.420585540445));
#40880=CARTESIAN_POINT('Ctrl Pts',(120.668145659774,-1.57321824887618,135.466213958996));
#40881=CARTESIAN_POINT('Ctrl Pts',(120.660372759508,-1.44245175122122,135.50632999304));
#40882=CARTESIAN_POINT('Ctrl Pts',(120.652882423746,-1.31643894513546,135.544987708202));
#40883=CARTESIAN_POINT('Ctrl Pts',(120.645392087984,-1.18903209372321,135.578526780472));
#40884=CARTESIAN_POINT('Ctrl Pts',(120.637901752222,-1.06068391144384,135.606873782827));
#40885=CARTESIAN_POINT('Ctrl Pts',(120.630127418103,-0.927469368824172,
135.636295570392));
#40886=CARTESIAN_POINT('Ctrl Pts',(120.622353083984,-0.792818721502979,
135.660217000709));
#40887=CARTESIAN_POINT('Ctrl Pts',(120.614578749865,-0.657225951261317,
135.678500245386));
#40888=CARTESIAN_POINT('Ctrl Pts',(120.606813996918,-0.521800286990796,
135.696760957598));
#40889=CARTESIAN_POINT('Ctrl Pts',(120.599049243971,-0.3854351937467,135.709397257991));
#40890=CARTESIAN_POINT('Ctrl Pts',(120.591284491024,-0.248637091774711,
135.716321800138));
#40891=CARTESIAN_POINT('Ctrl Pts',(120.583527450139,-0.111974859606116,
135.723239464732));
#40892=CARTESIAN_POINT('Ctrl Pts',(120.575770409253,0.0251191374923183,
135.724456640969));
#40893=CARTESIAN_POINT('Ctrl Pts',(120.568013368368,0.162131420819873,135.719937538425));
#40894=CARTESIAN_POINT('Ctrl Pts',(120.560262177128,0.299040382118771,135.715421843772));
#40895=CARTESIAN_POINT('Ctrl Pts',(120.552510985888,0.435867363127998,135.705178493363));
#40896=CARTESIAN_POINT('Ctrl Pts',(120.544759794648,0.572097291574801,135.689223742718));
#40897=CARTESIAN_POINT('Ctrl Pts',(120.537011897871,0.708269318668056,135.673275773268));
#40898=CARTESIAN_POINT('Ctrl Pts',(120.529264001094,0.843844410416449,135.651621277072));
#40899=CARTESIAN_POINT('Ctrl Pts',(120.521516104317,0.978311249177513,135.624328476612));
#40900=CARTESIAN_POINT('Ctrl Pts',(120.513769828233,1.11274996037468,135.597041385217));
#40901=CARTESIAN_POINT('Ctrl Pts',(120.506023552149,1.2460804967827,135.564118413192));
#40902=CARTESIAN_POINT('Ctrl Pts',(120.498277276064,1.37780078015259,135.525679085188));
#40903=CARTESIAN_POINT('Ctrl Pts',(120.490530942799,1.50952203585168,135.487239473434));
#40904=CARTESIAN_POINT('Ctrl Pts',(120.482784609534,1.63963263948338,135.44328353397));
#40905=CARTESIAN_POINT('Ctrl Pts',(120.475038276268,1.76764513211481,135.393980835995));
#40906=CARTESIAN_POINT('Ctrl Pts',(120.467290208265,1.8956862922563,135.344667097022));
#40907=CARTESIAN_POINT('Ctrl Pts',(120.459542140262,2.02162804166398,135.2900043574));
#40908=CARTESIAN_POINT('Ctrl Pts',(120.451794072259,2.14500275205556,135.230210395425));
#40909=CARTESIAN_POINT('Ctrl Pts',(120.444037769518,2.26850858655761,135.170352883716));
#40910=CARTESIAN_POINT('Ctrl Pts',(120.436281466776,2.38944157962719,135.105353426436));
#40911=CARTESIAN_POINT('Ctrl Pts',(120.428525164034,2.50735809560362,135.035476125669));
#40912=CARTESIAN_POINT('Ctrl Pts',(120.42076472152,2.62533754717509,134.965561529283));
#40913=CARTESIAN_POINT('Ctrl Pts',(120.413004279006,2.74029698607688,134.890764114926));
#40914=CARTESIAN_POINT('Ctrl Pts',(120.405243836491,2.85182250388439,134.811390873109));
#40915=CARTESIAN_POINT('Ctrl Pts',(120.397470936226,2.96352705235385,134.731890214318));
#40916=CARTESIAN_POINT('Ctrl Pts',(120.38969803596,3.07178635518746,134.647799289339));
#40917=CARTESIAN_POINT('Ctrl Pts',(120.381925135695,3.17621959690619,134.559465427652));
#40918=CARTESIAN_POINT('Ctrl Pts',(120.374434799933,3.2768564272362,134.474342724337));
#40919=CARTESIAN_POINT('Ctrl Pts',(120.366944464171,3.37394031388461,134.385280419695));
#40920=CARTESIAN_POINT('Ctrl Pts',(120.359454128409,3.46716477739389,134.292619706123));
#40921=CARTESIAN_POINT('Ctrl Pts',(120.35167979429,3.56392387477278,134.196445733431));
#40922=CARTESIAN_POINT('Ctrl Pts',(120.343905460171,3.6568316154907,134.096090447735));
#40923=CARTESIAN_POINT('Ctrl Pts',(120.336131126052,3.74550503139918,133.991894950285));
#40924=CARTESIAN_POINT('Ctrl Pts',(120.328366373105,3.83406916524751,133.887827864474));
#40925=CARTESIAN_POINT('Ctrl Pts',(120.320601620158,3.91840910644715,133.779930278488));
#40926=CARTESIAN_POINT('Ctrl Pts',(120.312836867211,3.99817763546422,133.668581045147));
#40927=CARTESIAN_POINT('Ctrl Pts',(120.305079826326,4.07786693725367,133.557342405435));
#40928=CARTESIAN_POINT('Ctrl Pts',(120.297322785441,4.15299363623217,133.442659256459));
#40929=CARTESIAN_POINT('Ctrl Pts',(120.289565744556,4.22325007312434,133.324944256796));
#40930=CARTESIAN_POINT('Ctrl Pts',(120.281814553315,4.29345352909089,133.20731802693));
#40931=CARTESIAN_POINT('Ctrl Pts',(120.274063362075,4.35879383370537,133.086664831562));
#40932=CARTESIAN_POINT('Ctrl Pts',(120.266312170835,4.41900625405234,132.963426802088));
#40933=CARTESIAN_POINT('Ctrl Pts',(120.258564274058,4.47919308251453,132.840241152064));
#40934=CARTESIAN_POINT('Ctrl Pts',(120.250816377281,4.53425619027309,132.714473203555));
#40935=CARTESIAN_POINT('Ctrl Pts',(120.243068480504,4.5839765951592,132.586590018494));
#40936=CARTESIAN_POINT('Ctrl Pts',(120.23532220442,4.63368659960846,132.458733583839));
#40937=CARTESIAN_POINT('Ctrl Pts',(120.227575928336,4.67805598252515,132.328763156874));
#40938=CARTESIAN_POINT('Ctrl Pts',(120.219829652252,4.71691391782517,132.197165756244));
#40939=CARTESIAN_POINT('Ctrl Pts',(120.212083318986,4.75577213996561,132.065567384191));
#40940=CARTESIAN_POINT('Ctrl Pts',(120.204336985721,4.789118722589,131.932342389469));
#40941=CARTESIAN_POINT('Ctrl Pts',(120.196590652456,4.81683284560382,131.797992541375));
#40942=CARTESIAN_POINT('Ctrl Pts',(120.188842584453,4.84455317500433,131.663612606564));
#40943=CARTESIAN_POINT('Ctrl Pts',(120.18109451645,4.86663845588384,131.528107699954));
#40944=CARTESIAN_POINT('Ctrl Pts',(120.173346448447,4.88301914678287,131.391988964952));
#40945=CARTESIAN_POINT('Ctrl Pts',(120.165590145705,4.89941724727513,131.255725561339));
#40946=CARTESIAN_POINT('Ctrl Pts',(120.157833842963,4.91009859969219,131.118847414909));
#40947=CARTESIAN_POINT('Ctrl Pts',(120.150077540221,4.9150456046854,130.981870522537));
#40948=CARTESIAN_POINT('Ctrl Pts',(120.142317097707,4.91999525004413,130.844820521472));
#40949=CARTESIAN_POINT('Ctrl Pts',(120.134556655193,4.91920445173975,130.707672060215));
#40950=CARTESIAN_POINT('Ctrl Pts',(120.126796212678,4.91270776196941,130.570939307516));
#40951=CARTESIAN_POINT('Ctrl Pts',(120.119023312413,4.9062006431359,130.433987059263));
#40952=CARTESIAN_POINT('Ctrl Pts',(120.111250412148,4.89396936393437,130.29745224274));
#40953=CARTESIAN_POINT('Ctrl Pts',(120.103477511882,4.87610030242466,130.161842988863));
#40954=CARTESIAN_POINT('Ctrl Pts',(120.09598717612,4.85888082631016,130.031163472942));
#40955=CARTESIAN_POINT('Ctrl Pts',(120.088496840358,4.83642639917832,129.901343698418));
#40956=CARTESIAN_POINT('Ctrl Pts',(120.081006504596,4.80885841622255,129.772825937962));
#40957=CARTESIAN_POINT('Ctrl Pts',(120.073232170477,4.78024518481408,129.639435387557));
#40958=CARTESIAN_POINT('Ctrl Pts',(120.065457836358,4.74603234400435,129.507024990775));
#40959=CARTESIAN_POINT('Ctrl Pts',(120.057683502239,4.70629986829687,129.376101323121));
#40960=CARTESIAN_POINT('Ctrl Pts',(120.049918749292,4.66661635931472,129.245339007187));
#40961=CARTESIAN_POINT('Ctrl Pts',(120.042153996344,4.62142686274248,129.116060145254));
#40962=CARTESIAN_POINT('Ctrl Pts',(120.034389243397,4.57086243754707,128.988761642153));
#40963=CARTESIAN_POINT('Ctrl Pts',(120.026632202512,4.52034823365161,128.86158957372));
#40964=CARTESIAN_POINT('Ctrl Pts',(120.018875161627,4.46446986829211,128.736394310857));
#40965=CARTESIAN_POINT('Ctrl Pts',(120.011118120742,4.40340822546264,128.613657748068));
#40966=CARTESIAN_POINT('Ctrl Pts',(120.003366929502,4.34239262969302,128.491013741875));
#40967=CARTESIAN_POINT('Ctrl Pts',(119.995615738262,4.27620171002332,128.370825093854));
#40968=CARTESIAN_POINT('Ctrl Pts',(119.987864547022,4.20506434951178,128.253553514125));
#40969=CARTESIAN_POINT('Ctrl Pts',(119.980116650245,4.1339572242761,128.136331777945));
#40970=CARTESIAN_POINT('Ctrl Pts',(119.972368753468,4.05790804199699,128.022024977698));
#40971=CARTESIAN_POINT('Ctrl Pts',(119.964620856691,3.97719138989455,127.911069807667));
#40972=CARTESIAN_POINT('Ctrl Pts',(119.956874580607,3.89649162197569,127.800137847065));
#40973=CARTESIAN_POINT('Ctrl Pts',(119.949128304522,3.81112655606539,127.692556438132));
#40974=CARTESIAN_POINT('Ctrl Pts',(119.941382028438,3.72141359907042,127.588732547165));
#40975=CARTESIAN_POINT('Ctrl Pts',(119.933635695173,3.63169997983478,127.484907889793));
#40976=CARTESIAN_POINT('Ctrl Pts',(119.925889361908,3.53763866109004,127.384841101558));
#40977=CARTESIAN_POINT('Ctrl Pts',(119.918143028642,3.43958648934775,127.288905050389));
#40978=CARTESIAN_POINT('Ctrl Pts',(119.910394960639,3.34151235950144,127.192947515006));
#40979=CARTESIAN_POINT('Ctrl Pts',(119.902646892636,3.23944587765031,127.101122830801));
#40980=CARTESIAN_POINT('Ctrl Pts',(119.894898824633,3.13377949436166,127.013765790468));
#40981=CARTESIAN_POINT('Ctrl Pts',(119.887142521891,3.0280008075834,126.926315906034));
#40982=CARTESIAN_POINT('Ctrl Pts',(119.87938621915,2.91861487828964,126.843343400155));
#40983=CARTESIAN_POINT('Ctrl Pts',(119.871629916408,2.80604631638542,126.765141988574));
#40984=CARTESIAN_POINT('Ctrl Pts',(119.863869473894,2.69341767325027,126.686898838544));
#40985=CARTESIAN_POINT('Ctrl Pts',(119.856109031379,2.57760334274872,126.613432066208));
#40986=CARTESIAN_POINT('Ctrl Pts',(119.848348588865,2.45905458591844,126.54499052259));
#40987=CARTESIAN_POINT('Ctrl Pts',(119.8405756886,2.34031552409944,126.476439110531));
#40988=CARTESIAN_POINT('Ctrl Pts',(119.832802788334,2.21883361091768,126.412929228752));
#40989=CARTESIAN_POINT('Ctrl Pts',(119.825029888069,2.09508304075466,126.354662862118));
#40990=CARTESIAN_POINT('Ctrl Pts',(119.817539552307,1.97583111552721,126.298514624675));
#40991=CARTESIAN_POINT('Ctrl Pts',(119.810049216545,1.85447289619021,126.24723541101));
#40992=CARTESIAN_POINT('Ctrl Pts',(119.802558880783,1.73144609633575,126.20096214709));
#40993=CARTESIAN_POINT('Ctrl Pts',(119.794784546664,1.60375469797044,126.152934418303));
#40994=CARTESIAN_POINT('Ctrl Pts',(119.787010212545,1.4738612049472,126.11014759647));
#40995=CARTESIAN_POINT('Ctrl Pts',(119.779235878426,1.34223504175979,126.072808213209));
#40996=CARTESIAN_POINT('Ctrl Pts',(119.771471125479,1.21077109605474,126.035514847402));
#40997=CARTESIAN_POINT('Ctrl Pts',(119.763706372532,1.07757910143104,126.003655668015));
#40998=CARTESIAN_POINT('Ctrl Pts',(119.755941619585,0.943147958568414,125.977389000626));
#40999=CARTESIAN_POINT('Ctrl Pts',(119.7481845787,0.808850334612117,125.951148421661));
#41000=CARTESIAN_POINT('Ctrl Pts',(119.740427537815,0.673316392870307,125.930489375354));
#41001=CARTESIAN_POINT('Ctrl Pts',(119.73267049693,0.537049337052604,125.915520154627));
#41002=CARTESIAN_POINT('Ctrl Pts',(119.724919305689,0.40088504128151,125.900562222306));
#41003=CARTESIAN_POINT('Ctrl Pts',(119.717168114449,0.263989118897879,125.891285617622));
#41004=CARTESIAN_POINT('Ctrl Pts',(119.709416923209,0.126873736584666,125.887747340374));
#41005=CARTESIAN_POINT('Ctrl Pts',(119.701669026432,-0.0101833680332993,
125.884210566987));
#41006=CARTESIAN_POINT('Ctrl Pts',(119.693921129655,-0.147459357044499,
125.886407280231));
#41007=CARTESIAN_POINT('Ctrl Pts',(119.686173232878,-0.284438406080855,
125.894342506026));
#41008=CARTESIAN_POINT('Ctrl Pts',(119.678426956794,-0.421388802053079,
125.902276071944));
#41009=CARTESIAN_POINT('Ctrl Pts',(119.67068068071,-0.55804199153395,125.915945740208));
#41010=CARTESIAN_POINT('Ctrl Pts',(119.662934404626,-0.693884016066977,
125.935304442623));
#41011=CARTESIAN_POINT('Ctrl Pts',(119.65518807136,-0.829727043354971,125.95466328794));
#41012=CARTESIAN_POINT('Ctrl Pts',(119.647441738095,-0.964758506692176,
125.979711196047));
#41013=CARTESIAN_POINT('Ctrl Pts',(119.63969540483,-1.09847181747517,126.01034948609));
#41014=CARTESIAN_POINT('Ctrl Pts',(119.631947336827,-1.23221507242701,126.040994637366));
#41015=CARTESIAN_POINT('Ctrl Pts',(119.624199268824,-1.36463920641229,126.077232574465));
#41016=CARTESIAN_POINT('Ctrl Pts',(119.616451200821,-1.49525041973602,126.118914081239));
#41017=CARTESIAN_POINT('Ctrl Pts',(119.608694898079,-1.62600044821156,126.160639887615));
#41018=CARTESIAN_POINT('Ctrl Pts',(119.600938595337,-1.75493333399475,126.207820701756));
#41019=CARTESIAN_POINT('Ctrl Pts',(119.593182292595,-1.88157245368625,126.260258047858));
#41020=CARTESIAN_POINT('Ctrl Pts',(119.585421850081,-2.00827916448905,126.31272338135));
#41021=CARTESIAN_POINT('Ctrl Pts',(119.577661407567,-2.13268931530129,126.37045067266));
#41022=CARTESIAN_POINT('Ctrl Pts',(119.569900965053,-2.25434962309309,126.433194773153));
#41023=CARTESIAN_POINT('Ctrl Pts',(119.562128064787,-2.37620523081136,126.496039596047));
#41024=CARTESIAN_POINT('Ctrl Pts',(119.554355164522,-2.49530183448049,126.563917127737));
#41025=CARTESIAN_POINT('Ctrl Pts',(119.546582264257,-2.61121318486823,126.636537592812));
#41026=CARTESIAN_POINT('Ctrl Pts',(119.539091928495,-2.72291086570622,126.706518121062));
#41027=CARTESIAN_POINT('Ctrl Pts',(119.531601592733,-2.8316506023576,126.780902560483));
#41028=CARTESIAN_POINT('Ctrl Pts',(119.524111256971,-2.93708060023924,126.859396662065));
#41029=CARTESIAN_POINT('Ctrl Pts',(119.516231596834,-3.04799052175957,126.941970643107));
#41030=CARTESIAN_POINT('Ctrl Pts',(119.508351936697,-3.15561253471809,127.029372439893));
#41031=CARTESIAN_POINT('Ctrl Pts',(119.50047227656,-3.25949339448024,127.121306738807));
#41032=CARTESIAN_POINT('Ctrl Pts',(119.492785051891,-3.36083729687221,127.210995836847));
#41033=CARTESIAN_POINT('Ctrl Pts',(119.485097827223,-3.45862030751185,127.304998364797));
#41034=CARTESIAN_POINT('Ctrl Pts',(119.477410602554,-3.55245005209682,127.402995937051));
#41035=CARTESIAN_POINT('Ctrl Pts',(119.469730357079,-3.64619460911075,127.500904537782));
#41036=CARTESIAN_POINT('Ctrl Pts',(119.462050111604,-3.73599276293087,127.602800683898));
#41037=CARTESIAN_POINT('Ctrl Pts',(119.45436986613,-3.82148622846593,127.708326692018));
#41038=CARTESIAN_POINT('Ctrl Pts',(119.446694849426,-3.90692148938258,127.813780857208));
#41039=CARTESIAN_POINT('Ctrl Pts',(119.439019832722,-3.98805764091882,127.922859659899));
#41040=CARTESIAN_POINT('Ctrl Pts',(119.431344816019,-4.06457456773828,128.035170005529));
#41041=CARTESIAN_POINT('Ctrl Pts',(119.423316032491,-4.14461841198534,128.152657105267));
#41042=CARTESIAN_POINT('Ctrl Pts',(119.415287248964,-4.21960674024664,128.273680422712));
#41043=CARTESIAN_POINT('Ctrl Pts',(119.407258465436,-4.28922167208049,128.39775294072));
#41044=CARTESIAN_POINT('Ctrl Pts',(119.399587505903,-4.35573403016929,128.516295838476));
#41045=CARTESIAN_POINT('Ctrl Pts',(119.39191654637,-4.4173414144964,128.637621624153));
#41046=CARTESIAN_POINT('Ctrl Pts',(119.384245586837,-4.47381247445167,128.761278385755));
#41047=CARTESIAN_POINT('Ctrl Pts',(119.37657473415,-4.53028274783441,128.884933424971));
#41048=CARTESIAN_POINT('Ctrl Pts',(119.368903881464,-4.58161667923464,129.010919009614));
#41049=CARTESIAN_POINT('Ctrl Pts',(119.361233028778,-4.62763056527772,129.138762102375));
#41050=CARTESIAN_POINT('Ctrl Pts',(119.353558968967,-4.67366368937961,129.266658645369));
#41051=CARTESIAN_POINT('Ctrl Pts',(119.345884909155,-4.71437220104739,129.396413868271));
#41052=CARTESIAN_POINT('Ctrl Pts',(119.338210849343,-4.74962193958152,129.527538588642));
#41053=CARTESIAN_POINT('Ctrl Pts',(119.337140370791,-4.75453903561341,129.545829585087));
#41054=CARTESIAN_POINT('Ctrl Pts',(119.33606989224,-4.75934999365132,129.564147210371));
#41055=CARTESIAN_POINT('Ctrl Pts',(119.334999413688,-4.76405452823402,129.582490119308));
#41056=CARTESIAN_POINT('Ctrl Pts',(121.084721392599,-4.76405452823403,129.582490119308));
#41057=CARTESIAN_POINT('Ctrl Pts',(121.076951239219,-4.79825256998917,129.715827765084));
#41058=CARTESIAN_POINT('Ctrl Pts',(121.069181085838,-4.82686303770906,129.850658621233));
#41059=CARTESIAN_POINT('Ctrl Pts',(121.061410932458,-4.84976794993014,129.98647682733));
#41060=CARTESIAN_POINT('Ctrl Pts',(121.053640539447,-4.87267356853512,130.12229922204));
#41061=CARTESIAN_POINT('Ctrl Pts',(121.045870146437,-4.88987320487444,130.259108647659));
#41062=CARTESIAN_POINT('Ctrl Pts',(121.038099753426,-4.90130009637116,130.396389506074));
#41063=CARTESIAN_POINT('Ctrl Pts',(121.030352980948,-4.91269225226841,130.533253056517));
#41064=CARTESIAN_POINT('Ctrl Pts',(121.022606208469,-4.91834670424102,130.670584793771));
#41065=CARTESIAN_POINT('Ctrl Pts',(121.014859435991,-4.91824874801939,130.807869906056));
#41066=CARTESIAN_POINT('',(121.36014056406,-4.91824852912944,130.800556906732));
#41067=CARTESIAN_POINT('Ctrl Pts',(121.429936586327,-4.76405452823403,129.582490119308));
#41068=CARTESIAN_POINT('Ctrl Pts',(121.420856971801,-4.80369940204384,129.737064880598));
#41069=CARTESIAN_POINT('Ctrl Pts',(121.411777357275,-4.83585906930173,129.893733636719));
#41070=CARTESIAN_POINT('Ctrl Pts',(121.402697742749,-4.86033642164795,130.051822956779));
#41071=CARTESIAN_POINT('Ctrl Pts',(121.393695775175,-4.88460444883132,130.208560330265));
#41072=CARTESIAN_POINT('Ctrl Pts',(121.384693807601,-4.90132092246141,130.36669396795));
#41073=CARTESIAN_POINT('Ctrl Pts',(121.375691840026,-4.91034075570341,130.525547552273));
#41074=CARTESIAN_POINT('Ctrl Pts',(121.370508081371,-4.91553480225507,130.617022958717));
#41075=CARTESIAN_POINT('Ctrl Pts',(121.365324322716,-4.9181775165785,130.708736737056));
#41076=CARTESIAN_POINT('Ctrl Pts',(121.36014056406,-4.91824852912944,130.800556906732));
#41077=CARTESIAN_POINT('Ctrl Pts',(121.360140564008,-4.91824852913016,130.800556907659));
#41078=CARTESIAN_POINT('Ctrl Pts',(121.352395684946,-4.91835462656282,130.937742327915));
#41079=CARTESIAN_POINT('Ctrl Pts',(121.344650805883,-4.91271662615867,131.074993328622));
#41080=CARTESIAN_POINT('Ctrl Pts',(121.336905926821,-4.90134485319712,131.211793670396));
#41081=CARTESIAN_POINT('Ctrl Pts',(121.329162189819,-4.88997475711792,131.348573839582));
#41082=CARTESIAN_POINT('Ctrl Pts',(121.321418452817,-4.87287260227552,131.484903092875));
#41083=CARTESIAN_POINT('Ctrl Pts',(121.313674715815,-4.85010073300231,131.620268665222));
#41084=CARTESIAN_POINT('Ctrl Pts',(121.30593044775,-4.82732730204311,131.755643520888));
#41085=CARTESIAN_POINT('Ctrl Pts',(121.298186179686,-4.79888344729425,131.890054178806));
#41086=CARTESIAN_POINT('Ctrl Pts',(121.290441911621,-4.76488287839154,132.022996829777));
#41087=CARTESIAN_POINT('Ctrl Pts',(121.282695439375,-4.73087263221228,132.15597731902));
#41088=CARTESIAN_POINT('Ctrl Pts',(121.274948967129,-4.69130262112038,132.28748859148));
#41089=CARTESIAN_POINT('Ctrl Pts',(121.267202494883,-4.64633667445302,132.41704117184));
#41090=CARTESIAN_POINT('Ctrl Pts',(121.259447091804,-4.60131888698141,132.546743112114));
#41091=CARTESIAN_POINT('Ctrl Pts',(121.251691688725,-4.55089286580262,132.674481480011));
#41092=CARTESIAN_POINT('Ctrl Pts',(121.243936285647,-4.49527116784955,132.799785431985));
#41093=CARTESIAN_POINT('Ctrl Pts',(121.236176345659,-4.4396169312176,132.92516268674));
#41094=CARTESIAN_POINT('Ctrl Pts',(121.228416405671,-4.37876113520666,133.048102338447));
#41095=CARTESIAN_POINT('Ctrl Pts',(121.220656465684,-4.312962269487,133.168158308673));
#41096=CARTESIAN_POINT('Ctrl Pts',(121.212883493517,-4.24705290000236,133.288415902993));
#41097=CARTESIAN_POINT('Ctrl Pts',(121.205110521351,-4.17618407452121,133.405779804192));
#41098=CARTESIAN_POINT('Ctrl Pts',(121.197337549185,-4.10065807548136,133.519832291233));
#41099=CARTESIAN_POINT('Ctrl Pts',(121.189961034019,-4.02898424655723,133.628067581709));
#41100=CARTESIAN_POINT('Ctrl Pts',(121.182584518854,-3.95311672216256,133.733320667862));
#41101=CARTESIAN_POINT('Ctrl Pts',(121.175208003689,-3.8733460673644,133.835263668627));
#41102=CARTESIAN_POINT('Ctrl Pts',(121.16743366957,-3.78927334340142,133.942704503668));
#41103=CARTESIAN_POINT('Ctrl Pts',(121.159659335451,-3.70059369395087,134.046814788587));
#41104=CARTESIAN_POINT('Ctrl Pts',(121.151885001332,-3.60760060089622,134.147173948716));
#41105=CARTESIAN_POINT('Ctrl Pts',(121.144120248384,-3.51472211351787,134.247409425149));
#41106=CARTESIAN_POINT('Ctrl Pts',(121.136355495437,-3.41754102283757,134.343902691014));
#41107=CARTESIAN_POINT('Ctrl Pts',(121.12859074249,-3.31639252029569,134.436264211252));
#41108=CARTESIAN_POINT('Ctrl Pts',(121.120833701605,-3.21534447987269,134.528533996725));
#41109=CARTESIAN_POINT('Ctrl Pts',(121.11307666072,-3.1103371561816,134.616679941212));
#41110=CARTESIAN_POINT('Ctrl Pts',(121.105319619835,-3.00174398221468,134.700347800263));
#41111=CARTESIAN_POINT('Ctrl Pts',(121.097568428595,-2.89323269920491,134.78395256473));
#41112=CARTESIAN_POINT('Ctrl Pts',(121.089817237355,-2.78114125675095,134.863085727742));
#41113=CARTESIAN_POINT('Ctrl Pts',(121.082066046115,-2.66587742435323,134.937432189753));
#41114=CARTESIAN_POINT('Ctrl Pts',(121.074318149338,-2.5506625821588,135.011747052536));
#41115=CARTESIAN_POINT('Ctrl Pts',(121.066570252561,-2.43227835964799,135.081279049261));
#41116=CARTESIAN_POINT('Ctrl Pts',(121.058822355784,-2.31116268592292,135.145755566393));
#41117=CARTESIAN_POINT('Ctrl Pts',(121.0510760797,-2.19007234698567,135.210218596427));
#41118=CARTESIAN_POINT('Ctrl Pts',(121.043329803616,-2.06625203819268,135.269628066684));
#41119=CARTESIAN_POINT('Ctrl Pts',(121.035583527532,-1.94016519332837,135.323756825589));
#41120=CARTESIAN_POINT('Ctrl Pts',(121.027837194266,-1.81407741771963,135.377885984061));
#41121=CARTESIAN_POINT('Ctrl Pts',(121.020090861001,-1.68572343191319,135.426734199168));
#41122=CARTESIAN_POINT('Ctrl Pts',(121.012344527735,-1.55558722324916,135.47012223314));
#41123=CARTESIAN_POINT('Ctrl Pts',(121.004596459732,-1.42542187148351,135.513519983561));
#41124=CARTESIAN_POINT('Ctrl Pts',(120.996848391729,-1.29347387348796,135.551454996042));
#41125=CARTESIAN_POINT('Ctrl Pts',(120.989100323726,-1.16024258155281,135.583797845363));
#41126=CARTESIAN_POINT('Ctrl Pts',(120.981344020985,-1.02686968981539,135.616175069049));
#41127=CARTESIAN_POINT('Ctrl Pts',(120.973587718243,-0.892211160137485,
135.642948164581));
#41128=CARTESIAN_POINT('Ctrl Pts',(120.965831415501,-0.756777299121249,
135.664038712053));
#41129=CARTESIAN_POINT('Ctrl Pts',(120.958070972987,-0.621271152975369,
135.685140516185));
#41130=CARTESIAN_POINT('Ctrl Pts',(120.950310530473,-0.484989239222823,
135.700553684938));
#41131=CARTESIAN_POINT('Ctrl Pts',(120.942550087958,-0.348446208691673,
135.710251800842));
#41132=CARTESIAN_POINT('Ctrl Pts',(120.934777187693,-0.211683987166286,
135.719965485024));
#41133=CARTESIAN_POINT('Ctrl Pts',(120.927004287428,-0.0746602022566778,
135.723945771804));
#41134=CARTESIAN_POINT('Ctrl Pts',(120.919231387162,0.0621103696950562,
135.722218419951));
#41135=CARTESIAN_POINT('Ctrl Pts',(120.9117410514,0.193908986852247,135.720553861689));
#41136=CARTESIAN_POINT('Ctrl Pts',(120.904250715638,0.325472173699212,135.713589450599));
#41137=CARTESIAN_POINT('Ctrl Pts',(120.896760379876,0.456346415344077,135.701393495922));
#41138=CARTESIAN_POINT('Ctrl Pts',(120.888986045757,0.592182793639085,135.688735127917));
#41139=CARTESIAN_POINT('Ctrl Pts',(120.881211711638,0.727707241546074,135.670400579329));
#41140=CARTESIAN_POINT('Ctrl Pts',(120.873437377519,0.862407283560495,135.6464094339));
#41141=CARTESIAN_POINT('Ctrl Pts',(120.865672624572,0.996941319811804,135.622447855413));
#41142=CARTESIAN_POINT('Ctrl Pts',(120.857907871625,1.13065259050813,135.592843618691));
#41143=CARTESIAN_POINT('Ctrl Pts',(120.850143118677,1.26303218961186,135.557668176572));
#41144=CARTESIAN_POINT('Ctrl Pts',(120.842386077792,1.39528030743136,135.522527671198));
#41145=CARTESIAN_POINT('Ctrl Pts',(120.834629036907,1.52619901035321,135.481827071894));
#41146=CARTESIAN_POINT('Ctrl Pts',(120.826871996022,1.6552884128346,135.435689080635));
#41147=CARTESIAN_POINT('Ctrl Pts',(120.819120804782,1.7842804679935,135.389585882394));
#41148=CARTESIAN_POINT('Ctrl Pts',(120.811369613542,1.91144560183515,135.338053584806));
#41149=CARTESIAN_POINT('Ctrl Pts',(120.803618422302,2.0362983028138,135.281264936898));
#41150=CARTESIAN_POINT('Ctrl Pts',(120.795870525525,2.16109793806382,135.224500425682));
#41151=CARTESIAN_POINT('Ctrl Pts',(120.788122628748,2.28358674011956,135.162484169111));
#41152=CARTESIAN_POINT('Ctrl Pts',(120.780374731971,2.4032986401155,135.095437255068));
#41153=CARTESIAN_POINT('Ctrl Pts',(120.772628455887,2.52298549896256,135.028404365795));
#41154=CARTESIAN_POINT('Ctrl Pts',(120.764882179803,2.63989627023486,134.956343103065));
#41155=CARTESIAN_POINT('Ctrl Pts',(120.757135903718,2.75358934759938,134.879520585872));
#41156=CARTESIAN_POINT('Ctrl Pts',(120.749389570453,2.86728326422069,134.802697501594));
#41157=CARTESIAN_POINT('Ctrl Pts',(120.741643237188,2.97775911559259,134.72111331161));
#41158=CARTESIAN_POINT('Ctrl Pts',(120.733896903922,3.08460449692238,134.635078325785));
#41159=CARTESIAN_POINT('Ctrl Pts',(120.726148835919,3.19147380553415,134.549024073022));
#41160=CARTESIAN_POINT('Ctrl Pts',(120.718400767916,3.29471072183496,134.458517286208));
#41161=CARTESIAN_POINT('Ctrl Pts',(120.710652699913,3.39393644461178,134.363908127073));
#41162=CARTESIAN_POINT('Ctrl Pts',(120.702896397172,3.49326762566778,134.269198416197));
#41163=CARTESIAN_POINT('Ctrl Pts',(120.69514009443,3.5885788137006,134.170377893556));
#41164=CARTESIAN_POINT('Ctrl Pts',(120.687383791688,3.67952819863928,134.06783350667));
#41165=CARTESIAN_POINT('Ctrl Pts',(120.679623349174,3.77052612600321,133.965234388758));
#41166=CARTESIAN_POINT('Ctrl Pts',(120.67186290666,3.85715736465253,133.858907749212));
#41167=CARTESIAN_POINT('Ctrl Pts',(120.664102464145,3.93912150747921,133.749272299063));
#41168=CARTESIAN_POINT('Ctrl Pts',(120.65632956388,4.02121722642428,133.639460852356));
#41169=CARTESIAN_POINT('Ctrl Pts',(120.648556663615,4.09863065715541,133.526330303625));
#41170=CARTESIAN_POINT('Ctrl Pts',(120.640783763349,4.17110522206723,133.410327672028));
#41171=CARTESIAN_POINT('Ctrl Pts',(120.633293427587,4.24094515399218,133.298542028284));
#41172=CARTESIAN_POINT('Ctrl Pts',(120.625803091825,4.30619891380052,133.184089758817));
#41173=CARTESIAN_POINT('Ctrl Pts',(120.618312756063,4.36667883611359,133.067389341365));
#41174=CARTESIAN_POINT('Ctrl Pts',(120.610538421944,4.42945187306359,132.946264192114));
#41175=CARTESIAN_POINT('Ctrl Pts',(120.602764087825,4.48728077253792,132.82233336448));
#41176=CARTESIAN_POINT('Ctrl Pts',(120.594989753706,4.53990500536383,132.696038604109));
#41177=CARTESIAN_POINT('Ctrl Pts',(120.587225000759,4.59246438352587,132.569899490743));
#41178=CARTESIAN_POINT('Ctrl Pts',(120.579460247812,4.63983170862671,132.441402598735));
#41179=CARTESIAN_POINT('Ctrl Pts',(120.571695494864,4.68179201981861,132.311014707151));
#41180=CARTESIAN_POINT('Ctrl Pts',(120.56393845398,4.72371065543776,132.180756318659));
#41181=CARTESIAN_POINT('Ctrl Pts',(120.556181413095,4.76023284533896,132.04861103799));
#41182=CARTESIAN_POINT('Ctrl Pts',(120.54842437221,4.79119162182193,131.915065756423));
#41183=CARTESIAN_POINT('Ctrl Pts',(120.540673180969,4.8221270520509,131.78162118239));
#41184=CARTESIAN_POINT('Ctrl Pts',(120.532921989729,4.84750733164166,131.646779088193));
#41185=CARTESIAN_POINT('Ctrl Pts',(120.525170798489,4.86721536839511,131.511041323514));
#41186=CARTESIAN_POINT('Ctrl Pts',(120.517422901712,4.88691502870719,131.375361251005));
#41187=CARTESIAN_POINT('Ctrl Pts',(120.509675004935,4.90094718512941,131.238786651265));
#41188=CARTESIAN_POINT('Ctrl Pts',(120.501927108158,4.90924592355149,131.101829144629));
#41189=CARTESIAN_POINT('Ctrl Pts',(120.494180832074,4.9175429260564,130.964900286551));
#41190=CARTESIAN_POINT('Ctrl Pts',(120.48643455599,4.9201088724178,130.827589070895));
#41191=CARTESIAN_POINT('Ctrl Pts',(120.478688279906,4.91692979840053,130.690411417916));
#41192=CARTESIAN_POINT('Ctrl Pts',(120.47094194664,4.91375070091604,130.553232752322));
#41193=CARTESIAN_POINT('Ctrl Pts',(120.463195613375,4.90482650748803,130.416188042234));
#41194=CARTESIAN_POINT('Ctrl Pts',(120.45544928011,4.89019537572859,130.279791985543));
#41195=CARTESIAN_POINT('Ctrl Pts',(120.447701212107,4.87556096742863,130.143365383901));
#41196=CARTESIAN_POINT('Ctrl Pts',(120.439953144104,4.85521711935837,130.00758811337));
#41197=CARTESIAN_POINT('Ctrl Pts',(120.432205076101,4.82925368119135,129.872968141109));
#41198=CARTESIAN_POINT('Ctrl Pts',(120.424448773359,4.80326264877332,129.73820509314));
#41199=CARTESIAN_POINT('Ctrl Pts',(120.416692470617,4.77164016956917,129.604602184982));
#41200=CARTESIAN_POINT('Ctrl Pts',(120.408936167875,4.73452703679601,129.472656145715));
#41201=CARTESIAN_POINT('Ctrl Pts',(120.401175725361,4.69739409562638,129.340639682874));
#41202=CARTESIAN_POINT('Ctrl Pts',(120.393415282847,4.65476478302499,129.210282222427));
#41203=CARTESIAN_POINT('Ctrl Pts',(120.385654840332,4.60682899506041,129.082062828921));
#41204=CARTESIAN_POINT('Ctrl Pts',(120.377881940067,4.55881625631354,128.953637606263));
#41205=CARTESIAN_POINT('Ctrl Pts',(120.370109039802,4.50548017188069,128.82735766957));
#41206=CARTESIAN_POINT('Ctrl Pts',(120.362336139536,4.44705814517803,128.703680509623));
#41207=CARTESIAN_POINT('Ctrl Pts',(120.354845803774,4.39075990630207,128.584499325965));
#41208=CARTESIAN_POINT('Ctrl Pts',(120.347355468012,4.32973922163128,128.467735242457));
#41209=CARTESIAN_POINT('Ctrl Pts',(120.33986513225,4.26424673061527,128.353772344735));
#41210=CARTESIAN_POINT('Ctrl Pts',(120.332090798131,4.19627107189652,128.235488509108));
#41211=CARTESIAN_POINT('Ctrl Pts',(120.324316464012,4.12326248942005,128.119847778666));
#41212=CARTESIAN_POINT('Ctrl Pts',(120.316542129893,4.04545181392711,128.007308118292));
#41213=CARTESIAN_POINT('Ctrl Pts',(120.308777376946,3.96773703313763,127.894907152992));
#41214=CARTESIAN_POINT('Ctrl Pts',(120.301012623999,3.88523215489806,127.785599972031));
#41215=CARTESIAN_POINT('Ctrl Pts',(120.293247871051,3.79821370206821,127.679819733545));
#41216=CARTESIAN_POINT('Ctrl Pts',(120.285490830166,3.71128167719251,127.574144557483));
#41217=CARTESIAN_POINT('Ctrl Pts',(120.277733789281,3.61984524576229,127.471989652727));
#41218=CARTESIAN_POINT('Ctrl Pts',(120.269976748396,3.52422379307952,127.373758670561));
#41219=CARTESIAN_POINT('Ctrl Pts',(120.262225557156,3.42867444927786,127.275601765143));
#41220=CARTESIAN_POINT('Ctrl Pts',(120.254474365916,3.32894663756933,127.181363171502));
#41221=CARTESIAN_POINT('Ctrl Pts',(120.246723174676,3.2253992871122,127.091412664632));
#41222=CARTESIAN_POINT('Ctrl Pts',(120.238975277899,3.12189594704131,127.001500389128));
#41223=CARTESIAN_POINT('Ctrl Pts',(120.231227381122,3.01457659158679,126.915872831339));
#41224=CARTESIAN_POINT('Ctrl Pts',(120.223479484345,2.9038360332409,126.834861989962));
#41225=CARTESIAN_POINT('Ctrl Pts',(120.215733208261,2.79311863943267,126.753868094307));
#41226=CARTESIAN_POINT('Ctrl Pts',(120.207986932177,2.67898178153047,126.677489224887));
#41227=CARTESIAN_POINT('Ctrl Pts',(120.200240656093,2.56185196984684,126.606015997708));
#41228=CARTESIAN_POINT('Ctrl Pts',(120.192494322827,2.44472129353754,126.53454224293));
#41229=CARTESIAN_POINT('Ctrl Pts',(120.184747989562,2.32459795309918,126.467974406302));
#41230=CARTESIAN_POINT('Ctrl Pts',(120.177001656297,2.20193560356723,126.406558591526));
#41231=CARTESIAN_POINT('Ctrl Pts',(120.169253588294,2.07924578465308,126.345129023104));
#41232=CARTESIAN_POINT('Ctrl Pts',(120.161505520291,1.95401617473662,126.288853947388));
#41233=CARTESIAN_POINT('Ctrl Pts',(120.153757452288,1.82672270691737,126.237932339959));
#41234=CARTESIAN_POINT('Ctrl Pts',(120.146001149546,1.69929395008502,126.186956612438));
#41235=CARTESIAN_POINT('Ctrl Pts',(120.138244846804,1.56979731718857,126.141345864496));
#41236=CARTESIAN_POINT('Ctrl Pts',(120.130488544062,1.43872682264481,126.101250137011));
#41237=CARTESIAN_POINT('Ctrl Pts',(120.122728101548,1.30758637183148,126.06113300923));
#41238=CARTESIAN_POINT('Ctrl Pts',(120.114967659034,1.17487076370234,126.026536865717));
#41239=CARTESIAN_POINT('Ctrl Pts',(120.10720721652,1.04108569229251,125.997560887621));
#41240=CARTESIAN_POINT('Ctrl Pts',(120.099434316254,0.907085857209262,125.968538394712));
#41241=CARTESIAN_POINT('Ctrl Pts',(120.091661415989,0.77201351359351,125.94515416276));
#41242=CARTESIAN_POINT('Ctrl Pts',(120.083888515723,0.636381883741304,125.927455742489));
#41243=CARTESIAN_POINT('Ctrl Pts',(120.076398179961,0.505680805268763,125.910400704375));
#41244=CARTESIAN_POINT('Ctrl Pts',(120.068907844199,0.374460704304341,125.898625295326));
#41245=CARTESIAN_POINT('Ctrl Pts',(120.061417508437,0.243180199716132,125.892126252945));
#41246=CARTESIAN_POINT('Ctrl Pts',(120.053643174318,0.106922154895483,125.885380797396));
#41247=CARTESIAN_POINT('Ctrl Pts',(120.045868840199,-0.0298325889035889,
125.884298346058));
#41248=CARTESIAN_POINT('Ctrl Pts',(120.03809450608,-0.166573963200332,125.888932235697));
#41249=CARTESIAN_POINT('Ctrl Pts',(120.030329753133,-0.303146815974181,
125.893560414481));
#41250=CARTESIAN_POINT('Ctrl Pts',(120.022565000186,-0.439705945039631,
125.903890903918));
#41251=CARTESIAN_POINT('Ctrl Pts',(120.014800247239,-0.575737454828614,
125.919925190047));
#41252=CARTESIAN_POINT('Ctrl Pts',(120.007043206354,-0.71163385620409,125.935943550696));
#41253=CARTESIAN_POINT('Ctrl Pts',(119.999286165469,-0.847003295399503,
125.95765438878));
#41254=CARTESIAN_POINT('Ctrl Pts',(119.991529124584,-0.981333533600314,
125.985007179777));
#41255=CARTESIAN_POINT('Ctrl Pts',(119.983777933343,-1.1155624723242,126.012339343821));
#41256=CARTESIAN_POINT('Ctrl Pts',(119.976026742103,-1.24875338834668,126.045304914481));
#41257=CARTESIAN_POINT('Ctrl Pts',(119.968275550863,-1.38040116951393,126.083801786908));
#41258=CARTESIAN_POINT('Ctrl Pts',(119.960527654086,-1.511992996862,126.122282297137));
#41259=CARTESIAN_POINT('Ctrl Pts',(119.952779757309,-1.64204261937261,126.166289323769));
#41260=CARTESIAN_POINT('Ctrl Pts',(119.945031860532,-1.77005731134371,126.215670153277));
#41261=CARTESIAN_POINT('Ctrl Pts',(119.937285584448,-1.89804522540093,126.26504065338));
#41262=CARTESIAN_POINT('Ctrl Pts',(119.929539308364,-2.02399869105035,126.319782579878));
#41263=CARTESIAN_POINT('Ctrl Pts',(119.921793032279,-2.14744266557274,126.379694182615));
#41264=CARTESIAN_POINT('Ctrl Pts',(119.914046699014,-2.27088755133017,126.439606227607));
#41265=CARTESIAN_POINT('Ctrl Pts',(119.906300365749,-2.39182255726741,126.50468785428));
#41266=CARTESIAN_POINT('Ctrl Pts',(119.898554032483,-2.5097954177409,126.574690414869));
#41267=CARTESIAN_POINT('Ctrl Pts',(119.89080596448,-2.62779469741926,126.644708652046));
#41268=CARTESIAN_POINT('Ctrl Pts',(119.883057896477,-2.74283017547651,126.719649816536));
#41269=CARTESIAN_POINT('Ctrl Pts',(119.875309828474,-2.85447719465501,126.799221043507));
#41270=CARTESIAN_POINT('Ctrl Pts',(119.867553525733,-2.96624287361364,126.878876839724));
#41271=CARTESIAN_POINT('Ctrl Pts',(119.859797222991,-3.07461258083279,126.963172301148));
#41272=CARTESIAN_POINT('Ctrl Pts',(119.852040920249,-3.17919305581108,127.051772900219));
#41273=CARTESIAN_POINT('Ctrl Pts',(119.844280477735,-3.28382934853765,127.140420788098));
#41274=CARTESIAN_POINT('Ctrl Pts',(119.836520035221,-3.38467209184157,127.233378127291));
#41275=CARTESIAN_POINT('Ctrl Pts',(119.828759592706,-3.48136450183492,127.33027307292));
#41276=CARTESIAN_POINT('Ctrl Pts',(119.820986692441,-3.57821213106887,127.427323562918));
#41277=CARTESIAN_POINT('Ctrl Pts',(119.813213792175,-3.67089584873541,127.528324002488));
#41278=CARTESIAN_POINT('Ctrl Pts',(119.80544089191,-3.75909823987637,127.632868305506));
#41279=CARTESIAN_POINT('Ctrl Pts',(119.797950556148,-3.84409425192963,127.733612159776));
#41280=CARTESIAN_POINT('Ctrl Pts',(119.790460220386,-3.92492890685757,127.83764645084));
#41281=CARTESIAN_POINT('Ctrl Pts',(119.782969884624,-4.00135705470864,127.94458356625));
#41282=CARTESIAN_POINT('Ctrl Pts',(119.775120410701,-4.08144969309127,128.056647981717));
#41283=CARTESIAN_POINT('Ctrl Pts',(119.767270936778,-4.1569552162601,128.172253364202));
#41284=CARTESIAN_POINT('Ctrl Pts',(119.759421462855,-4.22754791932674,128.290992030929));
#41285=CARTESIAN_POINT('Ctrl Pts',(119.75158539947,-4.29802001734926,128.409527836998));
#41286=CARTESIAN_POINT('Ctrl Pts',(119.743749336086,-4.36359582221846,128.531185938641));
#41287=CARTESIAN_POINT('Ctrl Pts',(119.735913272701,-4.42399151533761,128.655527879841));
#41288=CARTESIAN_POINT('Ctrl Pts',(119.728084969267,-4.48432739939225,128.779746686843));
#41289=CARTESIAN_POINT('Ctrl Pts',(119.720256665833,-4.53949321192236,128.906643705212));
#41290=CARTESIAN_POINT('Ctrl Pts',(119.7124283624,-4.58924960431368,129.035753501272));
#41291=CARTESIAN_POINT('Ctrl Pts',(119.704607732563,-4.63895722362022,129.164736739059));
#41292=CARTESIAN_POINT('Ctrl Pts',(119.696787102726,-4.68326584723437,129.295928080183));
#41293=CARTESIAN_POINT('Ctrl Pts',(119.68896647289,-4.72198331519722,129.428840122081));
#41294=CARTESIAN_POINT('Ctrl Pts',(119.685967176238,-4.73683188550948,129.479813336584));
#41295=CARTESIAN_POINT('Ctrl Pts',(119.682967879587,-4.7508586051796,129.531039415595));
#41296=CARTESIAN_POINT('Ctrl Pts',(119.679968582935,-4.76405452823404,129.582490119308));
#41297=CARTESIAN_POINT('Origin',(213.235140564004,0.,130.804360617566));
#41298=CARTESIAN_POINT('',(117.5848416735,-4.76405452823405,129.582490119308));
#41299=CARTESIAN_POINT('',(117.930282309765,-4.76405452823403,129.582490119308));
#41300=CARTESIAN_POINT('',(213.235140564004,-4.76405452823405,129.582490119308));
#41301=CARTESIAN_POINT('',(119.264859436025,-4.91824958100419,130.806390753538));
#41302=CARTESIAN_POINT('Ctrl Pts',(119.264859435991,-4.91824958100395,130.806390754133));
#41303=CARTESIAN_POINT('Ctrl Pts',(119.258460835046,-4.91820319810624,130.918758892777));
#41304=CARTESIAN_POINT('Ctrl Pts',(119.252062234102,-4.9143062059521,131.031043513497));
#41305=CARTESIAN_POINT('Ctrl Pts',(119.245663633157,-4.90657370955902,131.143060329943));
#41306=CARTESIAN_POINT('Ctrl Pts',(119.237889299038,-4.89717868538792,131.279161356646));
#41307=CARTESIAN_POINT('Ctrl Pts',(119.230114964919,-4.88210162976514,131.415086755473));
#41308=CARTESIAN_POINT('Ctrl Pts',(119.2223406308,-4.86134982279231,131.550323728542));
#41309=CARTESIAN_POINT('Ctrl Pts',(119.214575877853,-4.84062359056692,131.685394034129));
#41310=CARTESIAN_POINT('Ctrl Pts',(119.206811124906,-4.8142365809479,131.819777219336));
#41311=CARTESIAN_POINT('Ctrl Pts',(119.199046371959,-4.78224801385495,131.952962810007));
#41312=CARTESIAN_POINT('Ctrl Pts',(119.191289331074,-4.75029121825784,132.086016118872));
#41313=CARTESIAN_POINT('Ctrl Pts',(119.183532290189,-4.71274402760884,132.217873822601));
#41314=CARTESIAN_POINT('Ctrl Pts',(119.175775249304,-4.66971711267233,132.348033235097));
#41315=CARTESIAN_POINT('Ctrl Pts',(119.168024058064,-4.62672264466707,132.478094493368));
#41316=CARTESIAN_POINT('Ctrl Pts',(119.160272866824,-4.5782567996865,132.606459639844));
#41317=CARTESIAN_POINT('Ctrl Pts',(119.152521675584,-4.52448062607383,132.732639157296));
#41318=CARTESIAN_POINT('Ctrl Pts',(119.144773778807,-4.47072730876942,132.858765045086));
#41319=CARTESIAN_POINT('Ctrl Pts',(119.13702588203,-4.41166830485938,132.982706792553));
#41320=CARTESIAN_POINT('Ctrl Pts',(119.129277985253,-4.34751345418928,133.103993159548));
#41321=CARTESIAN_POINT('Ctrl Pts',(119.121531709169,-4.28337202333095,133.225254156049));
#41322=CARTESIAN_POINT('Ctrl Pts',(119.113785433085,-4.21413704861652,133.343860531519));
#41323=CARTESIAN_POINT('Ctrl Pts',(119.106039157,-4.14006497478168,133.459364396676));
#41324=CARTESIAN_POINT('Ctrl Pts',(119.098292823735,-4.06599235416361,133.574869114456));
#41325=CARTESIAN_POINT('Ctrl Pts',(119.09054649047,-3.98708277422921,133.687270947119));
#41326=CARTESIAN_POINT('Ctrl Pts',(119.082800157205,-3.90363655890191,133.796150162053));
#41327=CARTESIAN_POINT('Ctrl Pts',(119.075052089202,-3.82017165637327,133.905053759733));
#41328=CARTESIAN_POINT('Ctrl Pts',(119.067304021199,-3.73216833461281,134.010432859682));
#41329=CARTESIAN_POINT('Ctrl Pts',(119.059555953196,-3.63996756432957,134.111900366855));
#41330=CARTESIAN_POINT('Ctrl Pts',(119.051799650454,-3.54766880197041,134.213475714903));
#41331=CARTESIAN_POINT('Ctrl Pts',(119.044043347712,-3.45116394290887,134.311130875734));
#41332=CARTESIAN_POINT('Ctrl Pts',(119.03628704497,-3.35083162073693,134.404514852036));
#41333=CARTESIAN_POINT('Ctrl Pts',(119.028526602456,-3.25044574818363,134.497948670178));
#41334=CARTESIAN_POINT('Ctrl Pts',(119.020766159942,-3.14622863894206,134.587106507345));
#41335=CARTESIAN_POINT('Ctrl Pts',(119.013005717428,-3.0385916745218,134.671677995029));
#41336=CARTESIAN_POINT('Ctrl Pts',(119.005232817162,-2.93078192169069,134.756385244373));
#41337=CARTESIAN_POINT('Ctrl Pts',(118.997459916897,-2.81954166064776,134.836491203183));
#41338=CARTESIAN_POINT('Ctrl Pts',(118.989687016631,-2.70531162466699,134.911728640515));
#41339=CARTESIAN_POINT('Ctrl Pts',(118.982196680869,-2.59523413822036,134.984231007489));
#41340=CARTESIAN_POINT('Ctrl Pts',(118.974706345107,-2.48238073848909,135.052212514715));
#41341=CARTESIAN_POINT('Ctrl Pts',(118.967216009345,-2.36716527924578,135.115475508546));
#41342=CARTESIAN_POINT('Ctrl Pts',(118.959441675226,-2.24758139084821,135.181137138016));
#41343=CARTESIAN_POINT('Ctrl Pts',(118.951667341107,-2.12507398636641,135.241923382344));
#41344=CARTESIAN_POINT('Ctrl Pts',(118.943893006988,-2.00007843225282,135.297563186707));
#41345=CARTESIAN_POINT('Ctrl Pts',(118.936128254041,-1.87523692398849,135.353134419984));
#41346=CARTESIAN_POINT('Ctrl Pts',(118.928363501094,-1.74791372110643,135.403571675569));
#41347=CARTESIAN_POINT('Ctrl Pts',(118.920598748146,-1.61857030978488,135.448648853107));
#41348=CARTESIAN_POINT('Ctrl Pts',(118.912841707261,-1.48935536416287,135.493681259357));
#41349=CARTESIAN_POINT('Ctrl Pts',(118.905084666376,-1.35812456992417,135.533364054141));
#41350=CARTESIAN_POINT('Ctrl Pts',(118.897327625491,-1.22536067137054,135.567518633794));
#41351=CARTESIAN_POINT('Ctrl Pts',(118.889576434251,-1.09269689110566,135.601647457213));
#41352=CARTESIAN_POINT('Ctrl Pts',(118.881825243011,-0.958502684828784,
135.63025626637));
#41353=CARTESIAN_POINT('Ctrl Pts',(118.874074051771,-0.823276947813364,
135.653215959778));
#41354=CARTESIAN_POINT('Ctrl Pts',(118.866326154994,-0.688108685343347,
135.676165894704));
#41355=CARTESIAN_POINT('Ctrl Pts',(118.858578258217,-0.551910148776666,
135.693471424028));
#41356=CARTESIAN_POINT('Ctrl Pts',(118.85083036144,-0.415191229358849,135.705054375144));
#41357=CARTESIAN_POINT('Ctrl Pts',(118.843084085356,-0.278500908591656,
135.716634903357));
#41358=CARTESIAN_POINT('Ctrl Pts',(118.835337809272,-0.141290810810461,
135.722495201356));
#41359=CARTESIAN_POINT('Ctrl Pts',(118.827591533188,-0.00407637259556072,
135.722608928264));
#41360=CARTESIAN_POINT('Ctrl Pts',(118.819845199922,0.133139078505059,135.722722656012));
#41361=CARTESIAN_POINT('Ctrl Pts',(118.812098866657,0.270358479138243,135.7170897277));
#41362=CARTESIAN_POINT('Ctrl Pts',(118.804352533391,0.407066363954133,135.70573593862));
#41363=CARTESIAN_POINT('Ctrl Pts',(118.796604465388,0.543804863552962,135.694379606938));
#41364=CARTESIAN_POINT('Ctrl Pts',(118.788856397385,0.680031229843201,135.677299897507));
#41365=CARTESIAN_POINT('Ctrl Pts',(118.781108329383,0.815235485804568,135.654574444315));
#41366=CARTESIAN_POINT('Ctrl Pts',(118.773352026641,0.950583438458122,135.631824838241));
#41367=CARTESIAN_POINT('Ctrl Pts',(118.765595723899,1.08490672458792,135.603417566941));
#41368=CARTESIAN_POINT('Ctrl Pts',(118.757839421157,1.21770537950975,135.56948146296));
#41369=CARTESIAN_POINT('Ctrl Pts',(118.750078978643,1.35057491307229,135.535527246259));
#41370=CARTESIAN_POINT('Ctrl Pts',(118.742318536129,1.48191781975181,135.496038429462));
#41371=CARTESIAN_POINT('Ctrl Pts',(118.734558093614,1.61125061597757,135.451193357725));
#41372=CARTESIAN_POINT('Ctrl Pts',(118.726785193349,1.74079102868946,135.406276296697));
#41373=CARTESIAN_POINT('Ctrl Pts',(118.719012293084,1.86831451884324,135.355985942027));
#41374=CARTESIAN_POINT('Ctrl Pts',(118.711239392818,1.99335803037674,135.300548650248));
#41375=CARTESIAN_POINT('Ctrl Pts',(118.703749057056,2.11385589530083,135.247126643663));
#41376=CARTESIAN_POINT('Ctrl Pts',(118.696258721294,2.23205068181748,135.188925547492));
#41377=CARTESIAN_POINT('Ctrl Pts',(118.688768385532,2.34755240024224,135.12618671201));
#41378=CARTESIAN_POINT('Ctrl Pts',(118.680994051413,2.46743340142664,135.061069114512));
#41379=CARTESIAN_POINT('Ctrl Pts',(118.673219717294,2.58479283486809,134.990856615378));
#41380=CARTESIAN_POINT('Ctrl Pts',(118.665445383175,2.69916732826432,134.91576898898));
#41381=CARTESIAN_POINT('Ctrl Pts',(118.657680630228,2.8134008653193,134.840773901371));
#41382=CARTESIAN_POINT('Ctrl Pts',(118.649915877281,2.92465645809992,134.760915853448));
#41383=CARTESIAN_POINT('Ctrl Pts',(118.642151124333,3.03249443742238,134.676460893838));
#41384=CARTESIAN_POINT('Ctrl Pts',(118.634394083448,3.14022531054352,134.592089816084));
#41385=CARTESIAN_POINT('Ctrl Pts',(118.626637042563,3.24454501944707,134.503131152129));
#41386=CARTESIAN_POINT('Ctrl Pts',(118.618880001678,3.34504236472383,134.409894508781));
#41387=CARTESIAN_POINT('Ctrl Pts',(118.611128810438,3.4454639241707,134.316728175912));
#41388=CARTESIAN_POINT('Ctrl Pts',(118.603377619198,3.54206857192666,134.219290549752));
#41389=CARTESIAN_POINT('Ctrl Pts',(118.595626427958,3.63447802617195,134.117931582518));
#41390=CARTESIAN_POINT('Ctrl Pts',(118.587878531181,3.72684820393416,134.016615695549));
#41391=CARTESIAN_POINT('Ctrl Pts',(118.580130634404,3.81502647172089,133.911382070703));
#41392=CARTESIAN_POINT('Ctrl Pts',(118.572382737627,3.89867145203174,133.802617439723));
#41393=CARTESIAN_POINT('Ctrl Pts',(118.564636461543,3.98229893561589,133.69387555996));
#41394=CARTESIAN_POINT('Ctrl Pts',(118.556890185459,4.06139477968857,133.581604452919));
#41395=CARTESIAN_POINT('Ctrl Pts',(118.549143909375,4.13565821686171,133.466223532106));
#41396=CARTESIAN_POINT('Ctrl Pts',(118.541397576109,4.20992220223071,133.350841759577));
#41397=CARTESIAN_POINT('Ctrl Pts',(118.533651242844,4.27935349792102,133.232350456224));
#41398=CARTESIAN_POINT('Ctrl Pts',(118.525904909579,4.34369518463098,133.111197240631));
#41399=CARTESIAN_POINT('Ctrl Pts',(118.518156841576,4.40805128021553,132.990016893615));
#41400=CARTESIAN_POINT('Ctrl Pts',(118.510408773573,4.46731531544255,132.866173793381));
#41401=CARTESIAN_POINT('Ctrl Pts',(118.50266070557,4.52127695094842,132.740138961107));
#41402=CARTESIAN_POINT('Ctrl Pts',(118.494904402828,4.57529593752266,132.613970177513));
#41403=CARTESIAN_POINT('Ctrl Pts',(118.487148100086,4.62400111282458,132.485605368636));
#41404=CARTESIAN_POINT('Ctrl Pts',(118.479391797344,4.66723062419794,132.35553480606));
#41405=CARTESIAN_POINT('Ctrl Pts',(118.47163135483,4.71048320846318,132.225394820908));
#41406=CARTESIAN_POINT('Ctrl Pts',(118.463870912316,4.74825419779972,132.093547643647));
#41407=CARTESIAN_POINT('Ctrl Pts',(118.456110469802,4.7804323043577,131.960496442611));
#41408=CARTESIAN_POINT('Ctrl Pts',(118.448337569536,4.81266206606895,131.827231655976));
#41409=CARTESIAN_POINT('Ctrl Pts',(118.440564669271,4.83928092775092,131.692759366947));
#41410=CARTESIAN_POINT('Ctrl Pts',(118.432791769005,4.86022903645285,131.55759150894));
#41411=CARTESIAN_POINT('Ctrl Pts',(118.425301433243,4.88041562863846,131.427337343038));
#41412=CARTESIAN_POINT('Ctrl Pts',(118.417811097481,4.89533656726942,131.29643760757));
#41413=CARTESIAN_POINT('Ctrl Pts',(118.410320761719,4.90498410821736,131.165350867621));
#41414=CARTESIAN_POINT('Ctrl Pts',(118.4025464276,4.91499743861261,131.029293934085));
#41415=CARTESIAN_POINT('Ctrl Pts',(118.394772093481,4.91936131500807,130.892604548121));
#41416=CARTESIAN_POINT('Ctrl Pts',(118.386997759362,4.91801017576041,130.755791351388));
#41417=CARTESIAN_POINT('Ctrl Pts',(118.379233006415,4.91666070167111,130.619146764692));
#41418=CARTESIAN_POINT('Ctrl Pts',(118.371468253468,4.90961022972284,130.48237905802));
#41419=CARTESIAN_POINT('Ctrl Pts',(118.36370350052,4.8968449422271,130.346001943289));
#41420=CARTESIAN_POINT('Ctrl Pts',(118.355946459635,4.88409233339485,130.209760280231));
#41421=CARTESIAN_POINT('Ctrl Pts',(118.34818941875,4.86563624078206,130.073908823839));
#41422=CARTESIAN_POINT('Ctrl Pts',(118.340432377865,4.84151488204095,129.938960877864));
#41423=CARTESIAN_POINT('Ctrl Pts',(118.332681186625,4.81741171340409,129.804114697185));
#41424=CARTESIAN_POINT('Ctrl Pts',(118.324929995385,4.78765185075088,129.670171054056));
#41425=CARTESIAN_POINT('Ctrl Pts',(118.317178804145,4.75232524822748,129.537637365407));
#41426=CARTESIAN_POINT('Ctrl Pts',(118.309430907368,4.71701366045253,129.405160007111));
#41427=CARTESIAN_POINT('Ctrl Pts',(118.301683010591,4.67614013911124,129.274091788381));
#41428=CARTESIAN_POINT('Ctrl Pts',(118.293935113814,4.62984552969398,129.144928957728));
#41429=CARTESIAN_POINT('Ctrl Pts',(118.28618883773,4.58356060411099,129.015793145155));
#41430=CARTESIAN_POINT('Ctrl Pts',(118.278442561646,4.53185697781919,128.888562295696));
#41431=CARTESIAN_POINT('Ctrl Pts',(118.270696285561,4.47492494315906,128.763716156717));
#41432=CARTESIAN_POINT('Ctrl Pts',(118.262949952296,4.41799248823963,128.638869096153));
#41433=CARTESIAN_POINT('Ctrl Pts',(118.255203619031,4.35583171015494,128.516407136919));
#41434=CARTESIAN_POINT('Ctrl Pts',(118.247457285765,4.28868033193859,128.396788381278));
#41435=CARTESIAN_POINT('Ctrl Pts',(118.239709217762,4.22151391563672,128.277142837847));
#41436=CARTESIAN_POINT('Ctrl Pts',(118.231961149759,4.149354866636,128.160342105854));
#41437=CARTESIAN_POINT('Ctrl Pts',(118.224213081757,4.07248577482895,128.046817748214));
#41438=CARTESIAN_POINT('Ctrl Pts',(118.216456779015,3.99553498563633,127.933172735535));
#41439=CARTESIAN_POINT('Ctrl Pts',(118.208700476273,3.91386437338798,127.822811377468));
#41440=CARTESIAN_POINT('Ctrl Pts',(118.200944173531,3.82779893213975,127.716134849004));
#41441=CARTESIAN_POINT('Ctrl Pts',(118.193183731017,3.74168755517409,127.609401384065));
#41442=CARTESIAN_POINT('Ctrl Pts',(118.185423288503,3.65117693318272,127.50635696115));
#41443=CARTESIAN_POINT('Ctrl Pts',(118.177662845988,3.55663024213399,127.407367184655));
#41444=CARTESIAN_POINT('Ctrl Pts',(118.169889945723,3.46193177634333,127.308218500984));
#41445=CARTESIAN_POINT('Ctrl Pts',(118.162117045458,3.36318457607143,127.213137741877));
#41446=CARTESIAN_POINT('Ctrl Pts',(118.154344145192,3.26078699341668,127.122451975833));
#41447=CARTESIAN_POINT('Ctrl Pts',(118.14685380943,3.16211182081559,127.035062865809));
#41448=CARTESIAN_POINT('Ctrl Pts',(118.139363473668,3.06004729788793,126.951754953132));
#41449=CARTESIAN_POINT('Ctrl Pts',(118.131873137906,2.95497504253706,126.872782618787));
#41450=CARTESIAN_POINT('Ctrl Pts',(118.124098803787,2.84591894068824,126.790816024381));
#41451=CARTESIAN_POINT('Ctrl Pts',(118.116324469668,2.73327707081743,126.713260619641));
#41452=CARTESIAN_POINT('Ctrl Pts',(118.108550135549,2.61744192988759,126.640446496674));
#41453=CARTESIAN_POINT('Ctrl Pts',(118.100785382602,2.50174954541655,126.567722110605));
#41454=CARTESIAN_POINT('Ctrl Pts',(118.093020629655,2.38287204802507,126.499727586142));
#41455=CARTESIAN_POINT('Ctrl Pts',(118.085255876708,2.26123416930068,126.436752222336));
#41456=CARTESIAN_POINT('Ctrl Pts',(118.077498835822,2.13971710303224,126.373839406548));
#41457=CARTESIAN_POINT('Ctrl Pts',(118.069741794938,2.01544545638394,126.315936009431));
#41458=CARTESIAN_POINT('Ctrl Pts',(118.061984754053,1.88887174391407,126.263287330606));
#41459=CARTESIAN_POINT('Ctrl Pts',(118.054233562812,1.76239348166538,126.210678354559));
#41460=CARTESIAN_POINT('Ctrl Pts',(118.046482371572,1.63361696853104,126.163316358986));
#41461=CARTESIAN_POINT('Ctrl Pts',(118.038731180332,1.50301773115734,126.12139993416));
#41462=CARTESIAN_POINT('Ctrl Pts',(118.030983283555,1.37247400194338,126.079501324933));
#41463=CARTESIAN_POINT('Ctrl Pts',(118.023235386778,1.24010946080412,126.043043802292));
#41464=CARTESIAN_POINT('Ctrl Pts',(118.015487490001,1.10641774609574,126.012177103381));
#41465=CARTESIAN_POINT('Ctrl Pts',(118.007741213917,0.972753996812022,125.981316861118));
#41466=CARTESIAN_POINT('Ctrl Pts',(117.999994937833,0.837764006855314,125.956045204321));
#41467=CARTESIAN_POINT('Ctrl Pts',(117.992248661749,0.701954258930055,125.936461349825));
#41468=CARTESIAN_POINT('Ctrl Pts',(117.984502328483,0.566143508488181,125.916877350766));
#41469=CARTESIAN_POINT('Ctrl Pts',(117.976755995218,0.429513374965579,125.902981293588));
#41470=CARTESIAN_POINT('Ctrl Pts',(117.969009661952,0.292577767876609,125.894820790633));
#41471=CARTESIAN_POINT('Ctrl Pts',(117.961261593949,0.155611495007877,125.88665846019));
#41472=CARTESIAN_POINT('Ctrl Pts',(117.953513525946,0.0183400026455234,
125.884234263106));
#41473=CARTESIAN_POINT('Ctrl Pts',(117.945765457943,-0.118720876367694,
125.887543718798));
#41474=CARTESIAN_POINT('Ctrl Pts',(117.938009155202,-0.255927425314266,
125.890856691818));
#41475=CARTESIAN_POINT('Ctrl Pts',(117.93025285246,-0.392922522287937,125.899915481174));
#41476=CARTESIAN_POINT('Ctrl Pts',(117.922496549718,-0.529192980181233,
125.914663505042));
#41477=CARTESIAN_POINT('Ctrl Pts',(117.914736107204,-0.665536169721116,
125.929419400374));
#41478=CARTESIAN_POINT('Ctrl Pts',(117.90697566469,-0.801153563120145,125.949870522464));
#41479=CARTESIAN_POINT('Ctrl Pts',(117.899215222175,-0.935541261564568,
125.97590893919));
#41480=CARTESIAN_POINT('Ctrl Pts',(117.89144232191,-1.07014469107282,126.001989155094));
#41481=CARTESIAN_POINT('Ctrl Pts',(117.883669421644,-1.2035141003177,126.033674498575));
#41482=CARTESIAN_POINT('Ctrl Pts',(117.875896521379,-1.33515899826947,126.070806613243));
#41483=CARTESIAN_POINT('Ctrl Pts',(117.868406185617,-1.46201827258748,126.106588882013));
#41484=CARTESIAN_POINT('Ctrl Pts',(117.860915849855,-1.58727594663287,126.147428694059));
#41485=CARTESIAN_POINT('Ctrl Pts',(117.853425514093,-1.71051172868069,126.193142482567));
#41486=CARTESIAN_POINT('Ctrl Pts',(117.845650993255,-1.83842310487397,126.24059066281));
#41487=CARTESIAN_POINT('Ctrl Pts',(117.837876472418,-1.96456133225279,126.293440266656));
#41488=CARTESIAN_POINT('Ctrl Pts',(117.83010195158,-2.0884365056399,126.351539486596));
#41489=CARTESIAN_POINT('Ctrl Pts',(117.82233705528,-2.21215832664063,126.409566782084));
#41490=CARTESIAN_POINT('Ctrl Pts',(117.814572158981,-2.33362231744179,126.472830598264));
#41491=CARTESIAN_POINT('Ctrl Pts',(117.806807262681,-2.452355479164,126.541129956868));
#41492=CARTESIAN_POINT('Ctrl Pts',(117.799050121627,-2.57097005530141,126.609361101005));
#41493=CARTESIAN_POINT('Ctrl Pts',(117.791292980572,-2.68685889348965,126.682617585103));
#41494=CARTESIAN_POINT('Ctrl Pts',(117.783535839518,-2.79957100471094,126.760651274391));
#41495=CARTESIAN_POINT('Ctrl Pts',(117.775784591152,-2.91219749451705,126.838625685622));
#41496=CARTESIAN_POINT('Ctrl Pts',(117.768033342786,-3.02165174067263,126.921369856849));
#41497=CARTESIAN_POINT('Ctrl Pts',(117.760282094421,-3.12750962209338,127.008591047872));
#41498=CARTESIAN_POINT('Ctrl Pts',(117.752534359545,-3.23331952020366,127.095772703233));
#41499=CARTESIAN_POINT('Ctrl Pts',(117.744786624668,-3.33553599594384,127.187427092607));
#41500=CARTESIAN_POINT('Ctrl Pts',(117.737038889792,-3.43376627398198,127.283219859493));
#41501=CARTESIAN_POINT('Ctrl Pts',(117.729292836917,-3.53197522663689,127.378991830169));
#41502=CARTESIAN_POINT('Ctrl Pts',(117.721546784042,-3.62619942358062,127.478900118195));
#41503=CARTESIAN_POINT('Ctrl Pts',(117.713800731166,-3.7160816565156,127.58257226564));
#41504=CARTESIAN_POINT('Ctrl Pts',(117.706054682458,-3.80596384110301,127.686244357319));
#41505=CARTESIAN_POINT('Ctrl Pts',(117.698308633749,-3.89150381048676,127.793680008845));
#41506=CARTESIAN_POINT('Ctrl Pts',(117.69056258504,-3.9723837612152,127.904472634189));
#41507=CARTESIAN_POINT('Ctrl Pts',(117.682814863035,-4.05328118357907,128.015289192885));
#41508=CARTESIAN_POINT('Ctrl Pts',(117.67506714103,-4.12951635417953,128.12946385244));
#41509=CARTESIAN_POINT('Ctrl Pts',(117.667319419025,-4.20081425720144,128.246560265898));
#41510=CARTESIAN_POINT('Ctrl Pts',(117.659564299703,-4.27218023354459,128.363768479864));
#41511=CARTESIAN_POINT('Ctrl Pts',(117.651809180381,-4.33859932528608,128.483903684194));
#41512=CARTESIAN_POINT('Ctrl Pts',(117.644054061059,-4.39984184444552,128.606503750897));
#41513=CARTESIAN_POINT('Ctrl Pts',(117.636294827299,-4.46111685550754,128.729168862432));
#41514=CARTESIAN_POINT('Ctrl Pts',(117.628535593538,-4.51720966197646,128.854301085703));
#41515=CARTESIAN_POINT('Ctrl Pts',(117.620776359778,-4.56793877061906,128.981418366595));
#41516=CARTESIAN_POINT('Ctrl Pts',(117.613006612876,-4.61873661314919,129.108707881243));
#41517=CARTESIAN_POINT('Ctrl Pts',(117.605236865974,-4.66415611414588,129.237987456855));
#41518=CARTESIAN_POINT('Ctrl Pts',(117.597467119072,-4.70406551180002,129.368759446212));
#41519=CARTESIAN_POINT('Ctrl Pts',(117.593258637215,-4.72568242906647,129.439592068122));
#41520=CARTESIAN_POINT('Ctrl Pts',(117.589050155357,-4.74568364887164,129.510862339491));
#41521=CARTESIAN_POINT('Ctrl Pts',(117.5848416735,-4.76405452823405,129.582490119308));
#41522=CARTESIAN_POINT('Ctrl Pts',(119.334999413688,-4.76405452823402,129.582490119308));
#41523=CARTESIAN_POINT('Ctrl Pts',(119.327317254803,-4.7978160474119,129.71412577018));
#41524=CARTESIAN_POINT('Ctrl Pts',(119.319635095917,-4.82609248166911,129.847064070791));
#41525=CARTESIAN_POINT('Ctrl Pts',(119.311952937031,-4.84880778827108,129.98080364024));
#41526=CARTESIAN_POINT('Ctrl Pts',(119.304104020197,-4.87201617995309,130.117446317601));
#41527=CARTESIAN_POINT('Ctrl Pts',(119.296255103362,-4.88941918290399,130.254925008655));
#41528=CARTESIAN_POINT('Ctrl Pts',(119.288406186528,-4.90099174565895,130.392701812871));
#41529=CARTESIAN_POINT('Ctrl Pts',(119.280557269694,-4.91256430841392,130.530478617087));
#41530=CARTESIAN_POINT('Ctrl Pts',(119.272708352859,-4.91830647709806,130.668553094539));
#41531=CARTESIAN_POINT('Ctrl Pts',(119.264859436025,-4.91824958100419,130.806390753538));
#41532=CARTESIAN_POINT('',(119.610140563954,-4.91824907209079,130.807381772652));
#41533=CARTESIAN_POINT('Ctrl Pts',(119.679968582935,-4.76405452823404,129.582490119308));
#41534=CARTESIAN_POINT('Ctrl Pts',(119.672154643786,-4.79843330157376,129.716532434789));
#41535=CARTESIAN_POINT('Ctrl Pts',(119.664340704637,-4.82716957323685,129.852100309024));
#41536=CARTESIAN_POINT('Ctrl Pts',(119.656526765489,-4.85013965485316,129.98868397151));
#41537=CARTESIAN_POINT('Ctrl Pts',(119.648714426812,-4.873105031675,130.12523965856));
#41538=CARTESIAN_POINT('Ctrl Pts',(119.640902088135,-4.89030649992739,130.262810344994));
#41539=CARTESIAN_POINT('Ctrl Pts',(119.633089749459,-4.90167147584519,130.400876038696));
#41540=CARTESIAN_POINT('Ctrl Pts',(119.625440020975,-4.91279989507929,130.53606795925));
#41541=CARTESIAN_POINT('Ctrl Pts',(119.617790292492,-4.9183323969573,130.67173412575));
#41542=CARTESIAN_POINT('Ctrl Pts',(119.610140564008,-4.91824907209139,130.807381771687));
#41543=CARTESIAN_POINT('Ctrl Pts',(119.610140563954,-4.91824907209079,130.807381772653));
#41544=CARTESIAN_POINT('Ctrl Pts',(119.601339038692,-4.91815320121794,130.963453479642));
#41545=CARTESIAN_POINT('Ctrl Pts',(119.59253751343,-4.9106240938899,131.119247980167));
#41546=CARTESIAN_POINT('Ctrl Pts',(119.583735988168,-4.89576630750545,131.274100252677));
#41547=CARTESIAN_POINT('Ctrl Pts',(119.575009108628,-4.88103452998284,131.42763922332));
#41548=CARTESIAN_POINT('Ctrl Pts',(119.566282229087,-4.8590980702172,131.580251715686));
#41549=CARTESIAN_POINT('Ctrl Pts',(119.557555349547,-4.83010909763408,131.731306768889));
#41550=CARTESIAN_POINT('Ctrl Pts',(119.548716501424,-4.80074818750619,131.88429990546));
#41551=CARTESIAN_POINT('Ctrl Pts',(119.539877653302,-4.76415267188377,132.035695156408));
#41552=CARTESIAN_POINT('Ctrl Pts',(119.531038805179,-4.72053075406594,132.184857796997));
#41553=CARTESIAN_POINT('Ctrl Pts',(119.522199957057,-4.67690883624814,132.334020437587));
#41554=CARTESIAN_POINT('Ctrl Pts',(119.513361108934,-4.62626066231785,132.48095029492));
#41555=CARTESIAN_POINT('Ctrl Pts',(119.504522260812,-4.56884265301679,132.625036281839));
#41556=CARTESIAN_POINT('Ctrl Pts',(119.496747926693,-4.51833982928082,132.751769153437));
#41557=CARTESIAN_POINT('Ctrl Pts',(119.488973592573,-4.46247994562957,132.876599858998));
#41558=CARTESIAN_POINT('Ctrl Pts',(119.481199258454,-4.40142650984342,132.999042312242));
#41559=CARTESIAN_POINT('Ctrl Pts',(119.473434505507,-4.34044831696042,133.121333866106));
#41560=CARTESIAN_POINT('Ctrl Pts',(119.46566975256,-4.27428947999307,133.241242677434));
#41561=CARTESIAN_POINT('Ctrl Pts',(119.457904999613,-4.20316225663219,133.358300731767));
#41562=CARTESIAN_POINT('Ctrl Pts',(119.450147958728,-4.13210567783217,133.475242522389));
#41563=CARTESIAN_POINT('Ctrl Pts',(119.442390917843,-4.05609073456338,133.589338858695));
#41564=CARTESIAN_POINT('Ctrl Pts',(119.434633876958,-3.97537630034961,133.700144852125));
#41565=CARTESIAN_POINT('Ctrl Pts',(119.426882685718,-3.89472273351878,133.810867285893));
#41566=CARTESIAN_POINT('Ctrl Pts',(119.419131494478,-3.80937695896858,133.918304000875));
#41567=CARTESIAN_POINT('Ctrl Pts',(119.411380303238,-3.71964180109306,134.022038030555));
#41568=CARTESIAN_POINT('Ctrl Pts',(119.40363240646,-3.62994478305321,134.125727970506));
#41569=CARTESIAN_POINT('Ctrl Pts',(119.395884509683,-3.53586234748065,134.225718060139));
#41570=CARTESIAN_POINT('Ctrl Pts',(119.388136612906,-3.43773819958743,134.32162363497));
#41571=CARTESIAN_POINT('Ctrl Pts',(119.380390336822,-3.33963457715071,134.417509148422));
#41572=CARTESIAN_POINT('Ctrl Pts',(119.372644060738,-3.23749120343779,134.509311573402));
#41573=CARTESIAN_POINT('Ctrl Pts',(119.364897784654,-3.13168903308198,134.596682711294));
#41574=CARTESIAN_POINT('Ctrl Pts',(119.357151451389,-3.02588608171858,134.684054494139));
#41575=CARTESIAN_POINT('Ctrl Pts',(119.349405118123,-2.91642458128109,134.766994675676));
#41576=CARTESIAN_POINT('Ctrl Pts',(119.341658784858,-2.80371867290681,134.845195267201));
#41577=CARTESIAN_POINT('Ctrl Pts',(119.333910716855,-2.69098752482564,134.923413371207));
#41578=CARTESIAN_POINT('Ctrl Pts',(119.326162648852,-2.57501084418768,134.996889550307));
#41579=CARTESIAN_POINT('Ctrl Pts',(119.318414580849,-2.45623151241898,135.065359305655));
#41580=CARTESIAN_POINT('Ctrl Pts',(119.310658278107,-2.33732594056315,135.133901831475));
#41581=CARTESIAN_POINT('Ctrl Pts',(119.302901975365,-2.2156121065791,135.197427108934));
#41582=CARTESIAN_POINT('Ctrl Pts',(119.295145672623,-2.09155773426502,135.255716512879));
#41583=CARTESIAN_POINT('Ctrl Pts',(119.287385230109,-1.96743715039724,135.314037027633));
#41584=CARTESIAN_POINT('Ctrl Pts',(119.279624787595,-1.84097389935401,135.367115949275));
#41585=CARTESIAN_POINT('Ctrl Pts',(119.271864345081,-1.71265448355867,135.414783340316));
#41586=CARTESIAN_POINT('Ctrl Pts',(119.264091444815,-1.58412907804535,135.462527251284));
#41587=CARTESIAN_POINT('Ctrl Pts',(119.25631854455,-1.45374192551523,135.504842151366));
#41588=CARTESIAN_POINT('Ctrl Pts',(119.248545644284,-1.32199430703389,135.54160814273));
#41589=CARTESIAN_POINT('Ctrl Pts',(119.241055308522,-1.19503604633702,135.577037597699));
#41590=CARTESIAN_POINT('Ctrl Pts',(119.23356497276,-1.06681481492169,135.607314502583));
#41591=CARTESIAN_POINT('Ctrl Pts',(119.226074636998,-0.937785053574844,
135.632377006912));
#41592=CARTESIAN_POINT('Ctrl Pts',(119.218300302879,-0.803863089608314,
135.65838976371));
#41593=CARTESIAN_POINT('Ctrl Pts',(119.21052596876,-0.668645850063405,135.678867307075));
#41594=CARTESIAN_POINT('Ctrl Pts',(119.202751634641,-0.532630673043177,
135.693684459227));
#41595=CARTESIAN_POINT('Ctrl Pts',(119.194986881694,-0.396783122572601,
135.708483350563));
#41596=CARTESIAN_POINT('Ctrl Pts',(119.187222128747,-0.260139976207619,
135.717635688765));
#41597=CARTESIAN_POINT('Ctrl Pts',(119.1794573758,-0.123209718235847,135.721067078992));
#41598=CARTESIAN_POINT('Ctrl Pts',(119.171700334915,0.0135845386731426,
135.724495061115));
#41599=CARTESIAN_POINT('Ctrl Pts',(119.16394329403,0.150664951387716,135.722213393219));
#41600=CARTESIAN_POINT('Ctrl Pts',(119.156186253145,0.287517295101176,135.714199399799));
#41601=CARTESIAN_POINT('Ctrl Pts',(119.148435061904,0.424266437397779,135.706191449794));
#41602=CARTESIAN_POINT('Ctrl Pts',(119.140683870664,0.560787464308823,135.692459801282));
#41603=CARTESIAN_POINT('Ctrl Pts',(119.132932679424,0.696565886114431,135.673033848417));
#41604=CARTESIAN_POINT('Ctrl Pts',(119.125184782647,0.832286598468855,135.653616152099));
#41605=CARTESIAN_POINT('Ctrl Pts',(119.11743688587,0.967264947261899,135.628509020339));
#41606=CARTESIAN_POINT('Ctrl Pts',(119.109688989093,1.10099152230572,135.597793701516));
#41607=CARTESIAN_POINT('Ctrl Pts',(119.101942713009,1.23469012463285,135.567084807676));
#41608=CARTESIAN_POINT('Ctrl Pts',(119.094196436925,1.36713709323124,135.530770147622));
#41609=CARTESIAN_POINT('Ctrl Pts',(119.086450160841,1.49783356345753,135.488982019417));
#41610=CARTESIAN_POINT('Ctrl Pts',(119.078703827575,1.62853099845539,135.447193582742));
#41611=CARTESIAN_POINT('Ctrl Pts',(119.07095749431,1.75747753690324,135.399931716361));
#41612=CARTESIAN_POINT('Ctrl Pts',(119.063211161045,1.88419020578014,135.347378373523));
#41613=CARTESIAN_POINT('Ctrl Pts',(119.055463093042,2.01093125108067,135.294813261729));
#41614=CARTESIAN_POINT('Ctrl Pts',(119.047715025039,2.13543707028372,135.236954465237));
#41615=CARTESIAN_POINT('Ctrl Pts',(119.039966957036,2.25724574479005,135.174031624647));
#41616=CARTESIAN_POINT('Ctrl Pts',(119.032210654294,2.37918387900528,135.111041908914));
#41617=CARTESIAN_POINT('Ctrl Pts',(119.024454351552,2.49841879435542,135.042977577426));
#41618=CARTESIAN_POINT('Ctrl Pts',(119.01669804881,2.61451373916802,134.970113967226));
#41619=CARTESIAN_POINT('Ctrl Pts',(119.008937606296,2.73067064734831,134.897211467523));
#41620=CARTESIAN_POINT('Ctrl Pts',(119.001177163782,2.84368392362401,134.819504806466));
#41621=CARTESIAN_POINT('Ctrl Pts',(118.993416721268,2.95314762833095,134.737311436961));
#41622=CARTESIAN_POINT('Ctrl Pts',(118.985643821002,3.06278705389435,134.654986123363));
#41623=CARTESIAN_POINT('Ctrl Pts',(118.977870920737,3.16886521857905,134.568159956276));
#41624=CARTESIAN_POINT('Ctrl Pts',(118.970098020471,3.27101029428391,134.477189869953));
#41625=CARTESIAN_POINT('Ctrl Pts',(118.962607684709,3.36944213919967,134.389526775406));
#41626=CARTESIAN_POINT('Ctrl Pts',(118.955117348947,3.46422166432354,134.298016028646));
#41627=CARTESIAN_POINT('Ctrl Pts',(118.947627013185,3.55505119675834,134.203006531886));
#41628=CARTESIAN_POINT('Ctrl Pts',(118.939852679066,3.64932455852177,134.10439472118));
#41629=CARTESIAN_POINT('Ctrl Pts',(118.932078344947,3.73964111654788,134.001701240381));
#41630=CARTESIAN_POINT('Ctrl Pts',(118.924304010828,3.82562673183133,133.895276852471));
#41631=CARTESIAN_POINT('Ctrl Pts',(118.916539257881,3.91150637752863,133.788983623107));
#41632=CARTESIAN_POINT('Ctrl Pts',(118.908774504934,3.99306545717046,133.678968936492));
#41633=CARTESIAN_POINT('Ctrl Pts',(118.901009751987,4.06996653209188,133.565620382628));
#41634=CARTESIAN_POINT('Ctrl Pts',(118.893252711102,4.14679122778152,133.452384408146));
#41635=CARTESIAN_POINT('Ctrl Pts',(118.885495670217,4.21896690740773,133.33582147738));
#41636=CARTESIAN_POINT('Ctrl Pts',(118.877738629332,4.28619654235699,133.216351965558));
#41637=CARTESIAN_POINT('Ctrl Pts',(118.869987438092,4.35337547891562,133.096972546624));
#41638=CARTESIAN_POINT('Ctrl Pts',(118.862236246851,4.41561560387903,132.974691248772));
#41639=CARTESIAN_POINT('Ctrl Pts',(118.854485055611,4.47266355311984,132.849956815033));
#41640=CARTESIAN_POINT('Ctrl Pts',(118.846737158834,4.52968725546043,132.725275396756));
#41641=CARTESIAN_POINT('Ctrl Pts',(118.838989262057,4.58152300899197,132.598143271139));
#41642=CARTESIAN_POINT('Ctrl Pts',(118.83124136528,4.62796382162741,132.469032936134));
#41643=CARTESIAN_POINT('Ctrl Pts',(118.823495089196,4.67439491984602,132.339949608228));
#41644=CARTESIAN_POINT('Ctrl Pts',(118.815748813112,4.71543318958196,132.208889261659));
#41645=CARTESIAN_POINT('Ctrl Pts',(118.808002537028,4.75092028841816,132.076343115715));
#41646=CARTESIAN_POINT('Ctrl Pts',(118.800256203763,4.78640764921203,131.943795991345));
#41647=CARTESIAN_POINT('Ctrl Pts',(118.792509870497,4.8163436562252,131.809763423379));
#41648=CARTESIAN_POINT('Ctrl Pts',(118.784763537232,4.8406203331648,131.674750100873));
#41649=CARTESIAN_POINT('Ctrl Pts',(118.777015469229,4.86490244669787,131.53970654307));
#41650=CARTESIAN_POINT('Ctrl Pts',(118.769267401226,4.88352263906591,131.403682178403));
#41651=CARTESIAN_POINT('Ctrl Pts',(118.761519333223,4.89642443512322,131.267189758425));
#41652=CARTESIAN_POINT('Ctrl Pts',(118.753763030481,4.90933994336293,131.130552272679));
#41653=CARTESIAN_POINT('Ctrl Pts',(118.746006727739,4.91652487782168,130.993446127754));
#41654=CARTESIAN_POINT('Ctrl Pts',(118.738250424998,4.91797481240323,130.856387601597));
#41655=CARTESIAN_POINT('Ctrl Pts',(118.730489982483,4.91942552085853,130.719255923179));
#41656=CARTESIAN_POINT('Ctrl Pts',(118.722729539969,4.91513514247457,130.582172304754));
#41657=CARTESIAN_POINT('Ctrl Pts',(118.714969097455,4.90515133906645,130.445649865909));
#41658=CARTESIAN_POINT('Ctrl Pts',(118.70719619719,4.89515150877079,130.308908269125));
#41659=CARTESIAN_POINT('Ctrl Pts',(118.699423296924,4.87944003447119,130.172730040728));
#41660=CARTESIAN_POINT('Ctrl Pts',(118.691650396659,4.8581162328911,130.037620941913));
#41661=CARTESIAN_POINT('Ctrl Pts',(118.684160060897,4.83756760520995,129.90742339916));
#41662=CARTESIAN_POINT('Ctrl Pts',(118.676669725135,4.81180767068963,129.778218906481));
#41663=CARTESIAN_POINT('Ctrl Pts',(118.669179389373,4.78096907117315,129.650446494684));
#41664=CARTESIAN_POINT('Ctrl Pts',(118.661405055254,4.7489612167827,129.517829553059));
#41665=CARTESIAN_POINT('Ctrl Pts',(118.653630721135,4.71138058867321,129.386335340093));
#41666=CARTESIAN_POINT('Ctrl Pts',(118.645856387016,4.66832006240529,129.256468225491));
#41667=CARTESIAN_POINT('Ctrl Pts',(118.638091634069,4.6253126043876,129.1267611605));
#41668=CARTESIAN_POINT('Ctrl Pts',(118.630326881121,4.57683880749814,128.998677571551));
#41669=CARTESIAN_POINT('Ctrl Pts',(118.622562128174,4.52304236834297,128.872710857212));
#41670=CARTESIAN_POINT('Ctrl Pts',(118.614805087289,4.46929936056956,128.74686925479));
#41671=CARTESIAN_POINT('Ctrl Pts',(118.607048046404,4.41024438350894,128.623140700112));
#41672=CARTESIAN_POINT('Ctrl Pts',(118.599291005519,4.34607055952594,128.502002314842));
#41673=CARTESIAN_POINT('Ctrl Pts',(118.591539814279,4.28194512952285,128.380955280971));
#41674=CARTESIAN_POINT('Ctrl Pts',(118.583788623039,4.21270871829655,128.262494872732));
#41675=CARTESIAN_POINT('Ctrl Pts',(118.576037431799,4.13860191656769,128.14707680911));
#41676=CARTESIAN_POINT('Ctrl Pts',(118.568289535022,4.06452661220632,128.031707801244));
#41677=CARTESIAN_POINT('Ctrl Pts',(118.560541638245,3.98558524529838,127.919378894462));
#41678=CARTESIAN_POINT('Ctrl Pts',(118.552793741468,3.90206345747345,127.810519633754));
#41679=CARTESIAN_POINT('Ctrl Pts',(118.545047465384,3.81855914060607,127.701683144057));
#41680=CARTESIAN_POINT('Ctrl Pts',(118.5373011893,3.73047654642335,127.596315166817));
#41681=CARTESIAN_POINT('Ctrl Pts',(118.529554913216,3.63814336368036,127.494814436017));
#41682=CARTESIAN_POINT('Ctrl Pts',(118.52180857995,3.54580949935478,127.393312955961));
#41683=CARTESIAN_POINT('Ctrl Pts',(118.514062246685,3.44922524694357,127.295679068516));
#41684=CARTESIAN_POINT('Ctrl Pts',(118.506315913419,3.34875685182013,127.202276413957));
#41685=CARTESIAN_POINT('Ctrl Pts',(118.498567845417,3.24826595749627,127.108852842522));
#41686=CARTESIAN_POINT('Ctrl Pts',(118.490819777414,3.14388947589027,127.019662655649));
#41687=CARTESIAN_POINT('Ctrl Pts',(118.483071709411,3.03602827320992,126.935030522217));
#41688=CARTESIAN_POINT('Ctrl Pts',(118.475315406669,2.92805243435972,126.850308440747));
#41689=CARTESIAN_POINT('Ctrl Pts',(118.467559103927,2.81658478416331,126.770154331563));
#41690=CARTESIAN_POINT('Ctrl Pts',(118.459802801185,2.70205728946686,126.694850979308));
#41691=CARTESIAN_POINT('Ctrl Pts',(118.452042358671,2.58746866799806,126.619507435385));
#41692=CARTESIAN_POINT('Ctrl Pts',(118.444281916157,2.46981728309294,126.549020008017));
#41693=CARTESIAN_POINT('Ctrl Pts',(118.436521473643,2.34956059916619,126.483625951639));
#41694=CARTESIAN_POINT('Ctrl Pts',(118.428748573377,2.22911086853451,126.418126918915));
#41695=CARTESIAN_POINT('Ctrl Pts',(118.420975673112,2.10604783258396,126.357737768429));
#41696=CARTESIAN_POINT('Ctrl Pts',(118.413202772846,1.9808506856456,126.302648318487));
#41697=CARTESIAN_POINT('Ctrl Pts',(118.405712437084,1.86020477035019,126.249561508812));
#41698=CARTESIAN_POINT('Ctrl Pts',(118.398222101322,1.73757749756692,126.201395886994));
#41699=CARTESIAN_POINT('Ctrl Pts',(118.39073176556,1.61340993250517,126.158277164571));
#41700=CARTESIAN_POINT('Ctrl Pts',(118.382957431441,1.48453451647501,126.113523582682));
#41701=CARTESIAN_POINT('Ctrl Pts',(118.375183097322,1.35359146354676,126.074065395416));
#41702=CARTESIAN_POINT('Ctrl Pts',(118.367408763203,1.22105531574398,126.04009708808));
#41703=CARTESIAN_POINT('Ctrl Pts',(118.359644010256,1.08868250689827,126.006170643646));
#41704=CARTESIAN_POINT('Ctrl Pts',(118.351879257308,0.954720884742169,125.977720713375));
#41705=CARTESIAN_POINT('Ctrl Pts',(118.344114504361,0.819663230991687,125.954893095223));
#41706=CARTESIAN_POINT('Ctrl Pts',(118.336357463476,0.684739718406982,125.932088149783));
#41707=CARTESIAN_POINT('Ctrl Pts',(118.328600422591,0.548722723582106,125.914894468466));
#41708=CARTESIAN_POINT('Ctrl Pts',(118.320843381706,0.412118049841507,125.903407467872));
#41709=CARTESIAN_POINT('Ctrl Pts',(118.313092190466,0.27561639074782,125.891929129715));
#41710=CARTESIAN_POINT('Ctrl Pts',(118.305340999226,0.138528322861724,125.886148939147));
#41711=CARTESIAN_POINT('Ctrl Pts',(118.297589807986,0.00136730063314124,
125.886110807625));
#41712=CARTESIAN_POINT('Ctrl Pts',(118.289841911209,-0.135735424502011,
125.886072692309));
#41713=CARTESIAN_POINT('Ctrl Pts',(118.282094014432,-0.272910652161346,
125.891771782123));
#41714=CARTESIAN_POINT('Ctrl Pts',(118.274346117655,-0.409642597701834,
125.903199938232));
#41715=CARTESIAN_POINT('Ctrl Pts',(118.266599841571,-0.546345941866914,
125.914625703818));
#41716=CARTESIAN_POINT('Ctrl Pts',(118.258853565486,-0.682605798988489,
125.931778119478));
#41717=CARTESIAN_POINT('Ctrl Pts',(118.251107289402,-0.817909579096792,
125.954597016841));
#41718=CARTESIAN_POINT('Ctrl Pts',(118.243360956137,-0.953214357986863,
125.977416082647));
#41719=CARTESIAN_POINT('Ctrl Pts',(118.235614622872,-1.08756266025981,126.005901648605));
#41720=CARTESIAN_POINT('Ctrl Pts',(118.227868289606,-1.22045058048202,126.039942138559));
#41721=CARTESIAN_POINT('Ctrl Pts',(118.220120221603,-1.3533682600324,126.073990251646));
#41722=CARTESIAN_POINT('Ctrl Pts',(118.2123721536,-1.48482452809123,126.11359566712));
#41723=CARTESIAN_POINT('Ctrl Pts',(118.204624085597,-1.61432955355883,126.158596616349));
#41724=CARTESIAN_POINT('Ctrl Pts',(118.196867782855,-1.74397221850879,126.203645393122));
#41725=CARTESIAN_POINT('Ctrl Pts',(118.189111480114,-1.87165912832753,126.254101030273));
#41726=CARTESIAN_POINT('Ctrl Pts',(118.181355177372,-1.99691887965533,126.309752953868));
#41727=CARTESIAN_POINT('Ctrl Pts',(118.173594734858,-2.12224548588399,126.365434580569));
#41728=CARTESIAN_POINT('Ctrl Pts',(118.165834292343,-2.24514200217239,126.426317846507));
#41729=CARTESIAN_POINT('Ctrl Pts',(118.158073849829,-2.36516154895495,126.49214611573));
#41730=CARTESIAN_POINT('Ctrl Pts',(118.150300949564,-2.48537376176875,126.558080058334));
#41731=CARTESIAN_POINT('Ctrl Pts',(118.142528049298,-2.60269944129539,126.628974664881));
#41732=CARTESIAN_POINT('Ctrl Pts',(118.134755149033,-2.71671987177647,126.70452937704));
#41733=CARTESIAN_POINT('Ctrl Pts',(118.127264813271,-2.82659537240865,126.7773374851));
#41734=CARTESIAN_POINT('Ctrl Pts',(118.119774477509,-2.93340151044071,126.854472587573));
#41735=CARTESIAN_POINT('Ctrl Pts',(118.112284141747,-3.03679411467708,126.935631553964));
#41736=CARTESIAN_POINT('Ctrl Pts',(118.104605799054,-3.14278186642054,127.018827605026));
#41737=CARTESIAN_POINT('Ctrl Pts',(118.096927456361,-3.2455358106779,127.106529833381));
#41738=CARTESIAN_POINT('Ctrl Pts',(118.089249113669,-3.34464148734229,127.1984548529));
#41739=CARTESIAN_POINT('Ctrl Pts',(118.081579549546,-3.44363385751248,127.290274775497));
#41740=CARTESIAN_POINT('Ctrl Pts',(118.073909985423,-3.53898596087357,127.386307622067));
#41741=CARTESIAN_POINT('Ctrl Pts',(118.0662404213,-3.63031383490147,127.486227931457));
#41742=CARTESIAN_POINT('Ctrl Pts',(118.058577866454,-3.72155824364189,127.586056922864));
#41743=CARTESIAN_POINT('Ctrl Pts',(118.050915311608,-3.80878546702297,127.689766018797));
#41744=CARTESIAN_POINT('Ctrl Pts',(118.043252756762,-3.89164647165308,127.796991201919));
#41745=CARTESIAN_POINT('Ctrl Pts',(118.03559544818,-3.97445074446253,127.904142971981));
#41746=CARTESIAN_POINT('Ctrl Pts',(118.027938139598,-4.05289449986584,128.014805724947));
#41747=CARTESIAN_POINT('Ctrl Pts',(118.020280831016,-4.12666764679549,128.128580881603));
#41748=CARTESIAN_POINT('Ctrl Pts',(118.012626026437,-4.20041666929017,128.242318832833));
#41749=CARTESIAN_POINT('Ctrl Pts',(118.004971221859,-4.26949789797453,128.359166830722));
#41750=CARTESIAN_POINT('Ctrl Pts',(117.997316417281,-4.3336436268644,128.478695986146));
#41751=CARTESIAN_POINT('Ctrl Pts',(117.989663330027,-4.39777496492372,128.598198325696));
#41752=CARTESIAN_POINT('Ctrl Pts',(117.982010242772,-4.45697281923355,128.720380271036));
#41753=CARTESIAN_POINT('Ctrl Pts',(117.974357155518,-4.51101501937698,128.844787562675));
#41754=CARTESIAN_POINT('Ctrl Pts',(117.966701217411,-4.56507735078616,128.969241197287));
#41755=CARTESIAN_POINT('Ctrl Pts',(117.959045279304,-4.61398002821263,129.095921467083));
#41756=CARTESIAN_POINT('Ctrl Pts',(117.951389341198,-4.65754870950382,129.224353313438));
#41757=CARTESIAN_POINT('Ctrl Pts',(117.944353664054,-4.69758758793953,129.342379999834));
#41758=CARTESIAN_POINT('Ctrl Pts',(117.937317986909,-4.73312221386927,129.461885495063));
#41759=CARTESIAN_POINT('Ctrl Pts',(117.930282309765,-4.76405452823403,129.582490119308));
#41760=CARTESIAN_POINT('Origin',(213.235140564004,0.,130.804360617566));
#41761=CARTESIAN_POINT('',(115.834581344104,-4.76405452823405,129.582490119308));
#41762=CARTESIAN_POINT('',(116.180155138321,-4.76405452823404,129.582490119308));
#41763=CARTESIAN_POINT('',(213.235140564004,-4.76405452823405,129.582490119308));
#41764=CARTESIAN_POINT('',(117.514859435962,-4.91824794902791,130.799869027345));
#41765=CARTESIAN_POINT('Ctrl Pts',(117.514859435962,-4.91824794902791,130.799869027345));
#41766=CARTESIAN_POINT('Ctrl Pts',(117.507208240132,-4.91837122232531,130.934852098431));
#41767=CARTESIAN_POINT('Ctrl Pts',(117.499557044301,-4.91293333160114,131.070005300327));
#41768=CARTESIAN_POINT('Ctrl Pts',(117.491905848471,-4.90191906084059,131.204826076086));
#41769=CARTESIAN_POINT('Ctrl Pts',(117.48426061674,-4.89091337569394,131.339541759175));
#41770=CARTESIAN_POINT('Ctrl Pts',(117.47661538501,-4.87433999035582,131.473925132035));
#41771=CARTESIAN_POINT('Ctrl Pts',(117.468970153279,-4.85223575605224,131.607474077912));
#41772=CARTESIAN_POINT('Ctrl Pts',(117.46132828765,-4.83014125397164,131.740964223826));
#41773=CARTESIAN_POINT('Ctrl Pts',(117.453686422022,-4.80252080945946,131.873620276622));
#41774=CARTESIAN_POINT('Ctrl Pts',(117.446044556393,-4.76946303344324,132.004946072716));
#41775=CARTESIAN_POINT('Ctrl Pts',(117.438404246385,-4.73641198685376,132.136245135393));
#41776=CARTESIAN_POINT('Ctrl Pts',(117.430763936377,-4.69792590751848,132.266214089369));
#41777=CARTESIAN_POINT('Ctrl Pts',(117.42312362637,-4.65414423417374,132.394368325097));
#41778=CARTESIAN_POINT('Ctrl Pts',(117.415483110102,-4.61036137888763,132.522526020509));
#41779=CARTESIAN_POINT('Ctrl Pts',(117.407842593835,-4.56128277577274,132.648868519189));
#41780=CARTESIAN_POINT('Ctrl Pts',(117.400202077567,-4.50709713560817,132.772928237104));
#41781=CARTESIAN_POINT('Ctrl Pts',(117.392559593207,-4.45289753795934,132.897019911116));
#41782=CARTESIAN_POINT('Ctrl Pts',(117.384917108846,-4.39358844892161,133.018827266335));
#41783=CARTESIAN_POINT('Ctrl Pts',(117.377274624486,-4.32940569209491,133.137905006635));
#41784=CARTESIAN_POINT('Ctrl Pts',(117.369624105701,-4.26515546094297,133.257107931495));
#41785=CARTESIAN_POINT('Ctrl Pts',(117.361973586917,-4.19602152499452,133.373575158077));
#41786=CARTESIAN_POINT('Ctrl Pts',(117.354323068132,-4.12228457112978,133.486887966378));
#41787=CARTESIAN_POINT('Ctrl Pts',(117.346668040157,-4.04850415695003,133.600267560871));
#41788=CARTESIAN_POINT('Ctrl Pts',(117.339013012182,-3.97011555708345,133.710488708695));
#41789=CARTESIAN_POINT('Ctrl Pts',(117.331357984208,-3.88744052455226,133.817164831346));
#41790=CARTESIAN_POINT('Ctrl Pts',(117.323691752811,-3.80464449399681,133.92399707852));
#41791=CARTESIAN_POINT('Ctrl Pts',(117.316025521414,-3.71754976648684,134.027273636758));
#41792=CARTESIAN_POINT('Ctrl Pts',(117.308359290018,-3.62651604905118,134.126643629062));
#41793=CARTESIAN_POINT('Ctrl Pts',(117.304416282168,-3.5796942608856,134.177753051601));
#41794=CARTESIAN_POINT('Ctrl Pts',(117.300473274318,-3.53183101738966,134.2278296636));
#41795=CARTESIAN_POINT('Ctrl Pts',(117.296530266467,-3.48297861463481,134.276829916566));
#41796=CARTESIAN_POINT('Ctrl Pts',(117.288755932348,-3.3866575024361,134.373442541485));
#41797=CARTESIAN_POINT('Ctrl Pts',(117.280981598229,-3.28616094318428,134.466197450955));
#41798=CARTESIAN_POINT('Ctrl Pts',(117.27320726411,-3.18183062054689,134.554712196372));
#41799=CARTESIAN_POINT('Ctrl Pts',(117.265442511163,-3.07762887570802,134.643117855275));
#41800=CARTESIAN_POINT('Ctrl Pts',(117.257677758216,-2.96960306363289,134.727293497052));
#41801=CARTESIAN_POINT('Ctrl Pts',(117.249913005269,-2.85813256511082,134.80689247912));
#41802=CARTESIAN_POINT('Ctrl Pts',(117.242155964384,-2.74677278065935,134.886412402357));
#41803=CARTESIAN_POINT('Ctrl Pts',(117.234398923499,-2.63197543443788,134.96136448611));
#41804=CARTESIAN_POINT('Ctrl Pts',(117.226641882614,-2.51415365274995,135.031441699455));
#41805=CARTESIAN_POINT('Ctrl Pts',(117.218890691374,-2.39642072138412,135.101466067029));
#41806=CARTESIAN_POINT('Ctrl Pts',(117.211139500134,-2.27566822890966,135.166622682356));
#41807=CARTESIAN_POINT('Ctrl Pts',(117.203388308894,-2.15233870908931,135.226647485676));
#41808=CARTESIAN_POINT('Ctrl Pts',(117.195640412117,-2.02906160760456,135.286646776853));
#41809=CARTESIAN_POINT('Ctrl Pts',(117.187892515339,-1.90321000805651,135.341518423441));
#41810=CARTESIAN_POINT('Ctrl Pts',(117.180144618562,-1.77525130508993,135.391044154314));
#41811=CARTESIAN_POINT('Ctrl Pts',(117.172398342478,-1.64731936832553,135.440559525472));
#41812=CARTESIAN_POINT('Ctrl Pts',(117.164652066394,-1.51728156921669,135.484731064144));
#41813=CARTESIAN_POINT('Ctrl Pts',(117.15690579031,-1.38562518581118,135.523388685606));
#41814=CARTESIAN_POINT('Ctrl Pts',(117.149159457045,-1.2539678305485,135.562046592429));
#41815=CARTESIAN_POINT('Ctrl Pts',(117.141413123779,-1.12069224227625,135.595190390674));
#41816=CARTESIAN_POINT('Ctrl Pts',(117.133666790514,-0.986300373580139,
135.622700023998));
#41817=CARTESIAN_POINT('Ctrl Pts',(117.125918722511,-0.851878408756472,
135.650215817914));
#41818=CARTESIAN_POINT('Ctrl Pts',(117.118170654508,-0.716340049020913,
135.672094857818));
#41819=CARTESIAN_POINT('Ctrl Pts',(117.110422586505,-0.580196543019012,
135.688268380205));
#41820=CARTESIAN_POINT('Ctrl Pts',(117.102666283763,-0.443908342078803,
135.704459092005));
#41821=CARTESIAN_POINT('Ctrl Pts',(117.094909981022,-0.307014098951865,
135.714932126815));
#41822=CARTESIAN_POINT('Ctrl Pts',(117.08715367828,-0.170029836696684,135.719670670567));
#41823=CARTESIAN_POINT('Ctrl Pts',(117.079393235766,-0.0329724618161275,
135.724411743423));
#41824=CARTESIAN_POINT('Ctrl Pts',(117.071632793251,0.104174637164699,135.723412229423));
#41825=CARTESIAN_POINT('Ctrl Pts',(117.063872350737,0.240897344674072,135.716707463202));
#41826=CARTESIAN_POINT('Ctrl Pts',(117.056099450472,0.377839531611117,135.709991933895));
#41827=CARTESIAN_POINT('Ctrl Pts',(117.048326550206,0.514355576104106,135.697552886109));
#41828=CARTESIAN_POINT('Ctrl Pts',(117.040553649941,0.6499374792786,135.679477471092));
#41829=CARTESIAN_POINT('Ctrl Pts',(117.033063314179,0.780590638762682,135.662059142939));
#41830=CARTESIAN_POINT('Ctrl Pts',(117.025572978417,0.910376091141495,135.639407178212));
#41831=CARTESIAN_POINT('Ctrl Pts',(117.018082642655,1.03885174899798,135.611643645026));
#41832=CARTESIAN_POINT('Ctrl Pts',(117.010308308536,1.17219860047123,135.582827449041));
#41833=CARTESIAN_POINT('Ctrl Pts',(117.002533974417,1.30455677780528,135.548413141765));
#41834=CARTESIAN_POINT('Ctrl Pts',(116.994759640298,1.43541982778716,135.508481468532));
#41835=CARTESIAN_POINT('Ctrl Pts',(116.986994887351,1.56612160075525,135.468599007518));
#41836=CARTESIAN_POINT('Ctrl Pts',(116.979230134403,1.69533154226387,135.423212822854));
#41837=CARTESIAN_POINT('Ctrl Pts',(116.971465381456,1.82255294750759,135.37245472956));
#41838=CARTESIAN_POINT('Ctrl Pts',(116.963708340571,1.94964799465829,135.321747049919));
#41839=CARTESIAN_POINT('Ctrl Pts',(116.955951299686,2.07475807518674,135.265678223388));
#41840=CARTESIAN_POINT('Ctrl Pts',(116.948194258801,2.19740157042359,135.204429867112));
#41841=CARTESIAN_POINT('Ctrl Pts',(116.940443067561,2.31995257924716,135.143227698698));
#41842=CARTESIAN_POINT('Ctrl Pts',(116.932691876321,2.44004035677962,135.076853949013));
#41843=CARTESIAN_POINT('Ctrl Pts',(116.924940685081,2.55720354175795,135.005538203496));
#41844=CARTESIAN_POINT('Ctrl Pts',(116.917192788304,2.67431692925667,134.934252769074));
#41845=CARTESIAN_POINT('Ctrl Pts',(116.909444891527,2.78850786322893,134.858029719367));
#41846=CARTESIAN_POINT('Ctrl Pts',(116.90169699475,2.899340067772,134.777144305852));
#41847=CARTESIAN_POINT('Ctrl Pts',(116.893950718666,3.01014908860722,134.696275811822));
#41848=CARTESIAN_POINT('Ctrl Pts',(116.886204442582,3.11760046186363,134.610747124173));
#41849=CARTESIAN_POINT('Ctrl Pts',(116.878458166497,3.22128770475625,134.520876268776));
#41850=CARTESIAN_POINT('Ctrl Pts',(116.870711833232,3.32497571304462,134.431004749972));
#41851=CARTESIAN_POINT('Ctrl Pts',(116.862965499967,3.42489924008829,134.336791255532));
#41852=CARTESIAN_POINT('Ctrl Pts',(116.855219166701,3.52068596145132,134.238593198994));
#41853=CARTESIAN_POINT('Ctrl Pts',(116.847471098698,3.61649413358633,134.140373151682));
#41854=CARTESIAN_POINT('Ctrl Pts',(116.839723030695,3.70816338364981,134.038167046484));
#41855=CARTESIAN_POINT('Ctrl Pts',(116.831974962692,3.79535951657608,133.932367843011));
#41856=CARTESIAN_POINT('Ctrl Pts',(116.824218659951,3.88264832259008,133.826456194885));
#41857=CARTESIAN_POINT('Ctrl Pts',(116.816462357209,3.96545426562535,133.716944122229));
#41858=CARTESIAN_POINT('Ctrl Pts',(116.808706054467,4.04348427646189,133.604256681441));
#41859=CARTESIAN_POINT('Ctrl Pts',(116.800945611953,4.12155593426476,133.491509095974));
#41860=CARTESIAN_POINT('Ctrl Pts',(116.793185169439,4.19484637183213,133.375583095662));
#41861=CARTESIAN_POINT('Ctrl Pts',(116.785424726924,4.26310742516818,133.256930319731));
#41862=CARTESIAN_POINT('Ctrl Pts',(116.777651826659,4.33147805720694,133.13808707183));
#41863=CARTESIAN_POINT('Ctrl Pts',(116.769878926393,4.3948029906503,133.016508648094));
#41864=CARTESIAN_POINT('Ctrl Pts',(116.762106026128,4.45288096251175,132.892669549741));
#41865=CARTESIAN_POINT('Ctrl Pts',(116.754615690366,4.50884765380629,132.773332314545));
#41866=CARTESIAN_POINT('Ctrl Pts',(116.747125354604,4.55994212154052,132.651896197504));
#41867=CARTESIAN_POINT('Ctrl Pts',(116.739635018842,4.60602810603052,132.528799120081));
#41868=CARTESIAN_POINT('Ctrl Pts',(116.731860684723,4.65386145463017,132.401034779553));
#41869=CARTESIAN_POINT('Ctrl Pts',(116.724086350604,4.69645055113279,132.271076322685));
#41870=CARTESIAN_POINT('Ctrl Pts',(116.716312016485,4.73358957854112,132.139393487733));
#41871=CARTESIAN_POINT('Ctrl Pts',(116.708547263538,4.77068283541728,132.007872940107));
#41872=CARTESIAN_POINT('Ctrl Pts',(116.700782510591,4.80233928236949,131.87463261547));
#41873=CARTESIAN_POINT('Ctrl Pts',(116.693017757644,4.82840133802701,131.740161654881));
#41874=CARTESIAN_POINT('Ctrl Pts',(116.685260716759,4.85443750848347,131.605824252744));
#41875=CARTESIAN_POINT('Ctrl Pts',(116.677503675874,4.87489027128026,131.470259028397));
#41876=CARTESIAN_POINT('Ctrl Pts',(116.669746634989,4.88965209941101,131.333969349769));
#41877=CARTESIAN_POINT('Ctrl Pts',(116.661995443748,4.90440279553233,131.197782448247));
#41878=CARTESIAN_POINT('Ctrl Pts',(116.654244252508,4.91347105718386,131.060872566974));
#41879=CARTESIAN_POINT('Ctrl Pts',(116.646493061268,4.91680066406422,130.923751958783));
#41880=CARTESIAN_POINT('Ctrl Pts',(116.638745164491,4.92012885577285,130.786689630508));
#41881=CARTESIAN_POINT('Ctrl Pts',(116.630997267714,4.91772323438627,130.649417143483));
#41882=CARTESIAN_POINT('Ctrl Pts',(116.623249370937,4.90957955898512,130.512450329129));
#41883=CARTESIAN_POINT('Ctrl Pts',(116.615503094853,4.90143758706532,130.37551216528));
#41884=CARTESIAN_POINT('Ctrl Pts',(116.607756818769,4.88755997173819,130.238879936949));
#41885=CARTESIAN_POINT('Ctrl Pts',(116.600010542685,4.86799456330315,130.103067530368));
#41886=CARTESIAN_POINT('Ctrl Pts',(116.592264209419,4.84842901044069,129.967254121252));
#41887=CARTESIAN_POINT('Ctrl Pts',(116.584517876154,4.82317563643801,129.832260932931));
#41888=CARTESIAN_POINT('Ctrl Pts',(116.576771542888,4.79233389297649,129.698594403247));
#41889=CARTESIAN_POINT('Ctrl Pts',(116.569023474885,4.76148524272035,129.564897939871));
#41890=CARTESIAN_POINT('Ctrl Pts',(116.561275406882,4.7250458205954,129.432529107202));
#41891=CARTESIAN_POINT('Ctrl Pts',(116.553527338879,4.68316559405484,129.301981477282));
#41892=CARTESIAN_POINT('Ctrl Pts',(116.545771036138,4.6412408567112,129.171295099787));
#41893=CARTESIAN_POINT('Ctrl Pts',(116.538014733396,4.59386388330079,129.042434164474));
#41894=CARTESIAN_POINT('Ctrl Pts',(116.530258430654,4.54123387473806,128.915874992142));
#41895=CARTESIAN_POINT('Ctrl Pts',(116.52249798814,4.48857577595502,128.78924827137));
#41896=CARTESIAN_POINT('Ctrl Pts',(116.514737545626,4.43065922042154,128.664926115733));
#41897=CARTESIAN_POINT('Ctrl Pts',(116.506977103111,4.36773004630638,128.543361434662));
#41898=CARTESIAN_POINT('Ctrl Pts',(116.499204202846,4.30469985269439,128.421601607173));
#41899=CARTESIAN_POINT('Ctrl Pts',(116.49143130258,4.23664115484876,128.302608439464));
#41900=CARTESIAN_POINT('Ctrl Pts',(116.483658402315,4.16384437652324,128.186807739285));
#41901=CARTESIAN_POINT('Ctrl Pts',(116.476168066553,4.09369394445397,128.075216686243));
#41902=CARTESIAN_POINT('Ctrl Pts',(116.468677730791,4.01914410779989,127.966590275964));
#41903=CARTESIAN_POINT('Ctrl Pts',(116.461187395029,3.9404896506031,127.861279854829));
#41904=CARTESIAN_POINT('Ctrl Pts',(116.45341306091,3.85885298575508,127.751976557069));
#41905=CARTESIAN_POINT('Ctrl Pts',(116.445638726791,3.77253570233343,127.645899423646));
#41906=CARTESIAN_POINT('Ctrl Pts',(116.437864392672,3.68182175532233,127.543475519232));
#41907=CARTESIAN_POINT('Ctrl Pts',(116.430099639725,3.59121960514365,127.441177843127));
#41908=CARTESIAN_POINT('Ctrl Pts',(116.422334886778,3.49623182929369,127.342524727706));
#41909=CARTESIAN_POINT('Ctrl Pts',(116.41457013383,3.39718477941786,127.247913143331));
#41910=CARTESIAN_POINT('Ctrl Pts',(116.406813092945,3.29823610446814,127.153395528515));
#41911=CARTESIAN_POINT('Ctrl Pts',(116.39905605206,3.19523645969594,127.062911724797));
#41912=CARTESIAN_POINT('Ctrl Pts',(116.391299011175,3.08855122182369,126.976824280355));
#41913=CARTESIAN_POINT('Ctrl Pts',(116.383547819935,2.98194643611958,126.890801755124));
#41914=CARTESIAN_POINT('Ctrl Pts',(116.375796628695,2.87166189244234,126.809169234732));
#41915=CARTESIAN_POINT('Ctrl Pts',(116.368045437455,2.75809817516269,126.73225090408));
#41916=CARTESIAN_POINT('Ctrl Pts',(116.360297540678,2.64458272549207,126.65536526577));
#41917=CARTESIAN_POINT('Ctrl Pts',(116.352549643901,2.52779119727969,126.58319005087));
#41918=CARTESIAN_POINT('Ctrl Pts',(116.344801747124,2.40815528178724,126.516007646867));
#41919=CARTESIAN_POINT('Ctrl Pts',(116.33705547104,2.28854439154942,126.448839295975));
#41920=CARTESIAN_POINT('Ctrl Pts',(116.329309194956,2.16609063816533,126.386661869944));
#41921=CARTESIAN_POINT('Ctrl Pts',(116.321562918872,2.04125223293124,126.329712879022));
#41922=CARTESIAN_POINT('Ctrl Pts',(116.313816585606,1.9164129061684,126.272763467716));
#41923=CARTESIAN_POINT('Ctrl Pts',(116.306070252341,1.78918924813218,126.221042730798));
#41924=CARTESIAN_POINT('Ctrl Pts',(116.298323919076,1.66006109538457,126.174740738776));
#41925=CARTESIAN_POINT('Ctrl Pts',(116.290575851073,1.53090402528291,126.128428377743));
#41926=CARTESIAN_POINT('Ctrl Pts',(116.28282778307,1.39984197973823,126.087537308249));
#41927=CARTESIAN_POINT('Ctrl Pts',(116.275079715067,1.26737127595946,126.052208146172));
#41928=CARTESIAN_POINT('Ctrl Pts',(116.267323412325,1.13475978073966,126.016841435842));
#41929=CARTESIAN_POINT('Ctrl Pts',(116.259567109583,1.00073701495387,125.987048542217));
#41930=CARTESIAN_POINT('Ctrl Pts',(116.251810806841,0.865811393742108,125.962919334955));
#41931=CARTESIAN_POINT('Ctrl Pts',(116.244050364327,0.730813758663684,125.938777249209));
#41932=CARTESIAN_POINT('Ctrl Pts',(116.236289921813,0.594912695183648,125.920304925802));
#41933=CARTESIAN_POINT('Ctrl Pts',(116.228529479299,0.458622130368095,125.907540342731));
#41934=CARTESIAN_POINT('Ctrl Pts',(116.220756579033,0.322112779838777,125.894755268817));
#41935=CARTESIAN_POINT('Ctrl Pts',(116.212983678768,0.185213069172185,125.887696265121));
#41936=CARTESIAN_POINT('Ctrl Pts',(116.205210778502,0.048438223620664,125.886349149402));
#41937=CARTESIAN_POINT('Ctrl Pts',(116.19772044274,-0.0833645117811219,
125.885051004733));
#41938=CARTESIAN_POINT('Ctrl Pts',(116.190230106978,-0.215050994901615,
125.889056665568));
#41939=CARTESIAN_POINT('Ctrl Pts',(116.182739771216,-0.346166290106392,
125.898308033044));
#41940=CARTESIAN_POINT('Ctrl Pts',(116.174965437097,-0.482252861579623,
125.90791016893));
#41941=CARTESIAN_POINT('Ctrl Pts',(116.167191102978,-0.618155158294855,
125.923194062412));
#41942=CARTESIAN_POINT('Ctrl Pts',(116.159416768859,-0.753360394044942,
125.944151653007));
#41943=CARTESIAN_POINT('Ctrl Pts',(116.151652015912,-0.888399001425789,
125.965083415243));
#41944=CARTESIAN_POINT('Ctrl Pts',(116.143887262965,-1.02274187448304,125.991674902639));
#41945=CARTESIAN_POINT('Ctrl Pts',(116.136122510017,-1.15587862977411,126.023866118486));
#41946=CARTESIAN_POINT('Ctrl Pts',(116.128365469132,-1.28888315176256,126.056025361564));
#41947=CARTESIAN_POINT('Ctrl Pts',(116.120608428247,-1.42068356237032,126.093773173713));
#41948=CARTESIAN_POINT('Ctrl Pts',(116.112851387362,-1.55077734450439,126.136998119294));
#41949=CARTESIAN_POINT('Ctrl Pts',(116.105100196122,-1.68077302190555,126.180190468608));
#41950=CARTESIAN_POINT('Ctrl Pts',(116.097349004882,-1.80906426297203,126.228851607367));
#41951=CARTESIAN_POINT('Ctrl Pts',(116.089597813642,-1.93516179612806,126.282819742454));
#41952=CARTESIAN_POINT('Ctrl Pts',(116.081849916865,-2.06120573446865,126.336764939644));
#41953=CARTESIAN_POINT('Ctrl Pts',(116.074102020088,-2.18505746066304,126.396012493406));
#41954=CARTESIAN_POINT('Ctrl Pts',(116.066354123311,-2.30624605444866,126.46035184699));
#41955=CARTESIAN_POINT('Ctrl Pts',(116.058607847227,-2.42740929819307,126.524677742168));
#41956=CARTESIAN_POINT('Ctrl Pts',(116.050861571143,-2.54591017247284,126.594093135423));
#41957=CARTESIAN_POINT('Ctrl Pts',(116.043115295059,-2.66130117879128,126.668340900705));
#41958=CARTESIAN_POINT('Ctrl Pts',(116.035368961793,-2.77669303689976,126.742589214066));
#41959=CARTESIAN_POINT('Ctrl Pts',(116.027622628528,-2.88897465245562,126.82166975908));
#41960=CARTESIAN_POINT('Ctrl Pts',(116.019876295262,-2.9977267503754,126.905281573409));
#41961=CARTESIAN_POINT('Ctrl Pts',(116.01212822726,-3.10650320257339,126.988912112024));
#41962=CARTESIAN_POINT('Ctrl Pts',(116.004380159257,-3.21174825441974,127.07707570093));
#41963=CARTESIAN_POINT('Ctrl Pts',(115.996632091254,-3.31307533021835,127.169430780719));
#41964=CARTESIAN_POINT('Ctrl Pts',(115.988875788512,-3.414510097639,127.261884016587));
#41965=CARTESIAN_POINT('Ctrl Pts',(115.98111948577,-3.51201828141911,127.358537378428));
#41966=CARTESIAN_POINT('Ctrl Pts',(115.973363183028,-3.60524946086931,127.459011698933));
#41967=CARTESIAN_POINT('Ctrl Pts',(115.965602740514,-3.69853040060692,127.559539645607));
#41968=CARTESIAN_POINT('Ctrl Pts',(115.957842298,-3.78752953383121,127.663892317217));
#41969=CARTESIAN_POINT('Ctrl Pts',(115.950081855486,-3.87193711844573,127.771657860403));
#41970=CARTESIAN_POINT('Ctrl Pts',(115.94230895522,-3.95648020160871,127.879596398407));
#41971=CARTESIAN_POINT('Ctrl Pts',(115.934536054955,-4.03641677891657,127.990958438268));
#41972=CARTESIAN_POINT('Ctrl Pts',(115.926763154689,-4.11148029045516,128.105302840545));
#41973=CARTESIAN_POINT('Ctrl Pts',(115.919272818927,-4.18381505427524,128.215490535782));
#41974=CARTESIAN_POINT('Ctrl Pts',(115.911782483165,-4.25162473911524,128.32844726111));
#41975=CARTESIAN_POINT('Ctrl Pts',(115.904292147403,-4.31471232137161,128.44375886244));
#41976=CARTESIAN_POINT('Ctrl Pts',(115.896119758503,-4.38354451706451,128.569570478998));
#41977=CARTESIAN_POINT('Ctrl Pts',(115.887947369603,-4.44695528377166,128.698550318887));
#41978=CARTESIAN_POINT('Ctrl Pts',(115.879774980703,-4.50465700191711,128.830215648832));
#41979=CARTESIAN_POINT('Ctrl Pts',(115.871620741564,-4.56223057241044,128.961588568022));
#41980=CARTESIAN_POINT('Ctrl Pts',(115.863466502426,-4.61412024000921,129.09563478355));
#41981=CARTESIAN_POINT('Ctrl Pts',(115.855312263288,-4.66008418077987,129.231847186607));
#41982=CARTESIAN_POINT('Ctrl Pts',(115.848401956893,-4.69903630230064,129.347280328057));
#41983=CARTESIAN_POINT('Ctrl Pts',(115.841491650499,-4.73373342589427,129.464268601472));
#41984=CARTESIAN_POINT('Ctrl Pts',(115.834581344104,-4.76405452823405,129.582490119308));
#41985=CARTESIAN_POINT('Ctrl Pts',(117.5848416735,-4.76405452823405,129.582490119308));
#41986=CARTESIAN_POINT('Ctrl Pts',(117.58155374576,-4.77840700162319,129.638450195223));
#41987=CARTESIAN_POINT('Ctrl Pts',(117.57826581802,-4.7917644510224,129.694628467612));
#41988=CARTESIAN_POINT('Ctrl Pts',(117.57497789028,-4.80412178438199,129.75098654188));
#41989=CARTESIAN_POINT('Ctrl Pts',(117.564226926074,-4.84452816163197,129.935267854337));
#41990=CARTESIAN_POINT('Ctrl Pts',(117.553475961867,-4.87434350039962,130.121948280994));
#41991=CARTESIAN_POINT('Ctrl Pts',(117.542724997661,-4.89334244972931,130.310009798636));
#41992=CARTESIAN_POINT('Ctrl Pts',(117.533436477104,-4.90975698967351,130.472489483155));
#41993=CARTESIAN_POINT('Ctrl Pts',(117.524147956548,-4.91809829573002,130.636000128652));
#41994=CARTESIAN_POINT('Ctrl Pts',(117.514859435991,-4.91824794902745,130.799869026841));
#41995=CARTESIAN_POINT('',(117.860140564046,-4.91824926722357,130.807045381015));
#41996=CARTESIAN_POINT('Ctrl Pts',(117.930282309765,-4.76405452823403,129.582490119308));
#41997=CARTESIAN_POINT('Ctrl Pts',(117.922619279463,-4.79774499717081,129.713848746368));
#41998=CARTESIAN_POINT('Ctrl Pts',(117.914956249162,-4.82597508279731,129.846511022407));
#41999=CARTESIAN_POINT('Ctrl Pts',(117.90729321886,-4.848667424413,129.979977654413));
#42000=CARTESIAN_POINT('Ctrl Pts',(117.899434443058,-4.87193942232638,130.116853576439));
#42001=CARTESIAN_POINT('Ctrl Pts',(117.891575667255,-4.88938690047608,130.254575048808));
#42002=CARTESIAN_POINT('Ctrl Pts',(117.883716891453,-4.90098319599923,130.39260003782));
#42003=CARTESIAN_POINT('Ctrl Pts',(117.87585811565,-4.91257949152238,130.530625026831));
#42004=CARTESIAN_POINT('Ctrl Pts',(117.867999339848,-4.91832464875417,130.668953081738));
#42005=CARTESIAN_POINT('Ctrl Pts',(117.860140564046,-4.91824926722357,130.807045381015));
#42006=CARTESIAN_POINT('Ctrl Pts',(117.860140564008,-4.91824926722321,130.807045381675));
#42007=CARTESIAN_POINT('Ctrl Pts',(117.85137254865,-4.9181651642284,130.961114594403));
#42008=CARTESIAN_POINT('Ctrl Pts',(117.842604533292,-4.91084215645057,131.114982470872));
#42009=CARTESIAN_POINT('Ctrl Pts',(117.833836517934,-4.89633272611262,131.268158954884));
#42010=CARTESIAN_POINT('Ctrl Pts',(117.826062183815,-4.88346765292127,131.403975912001));
#42011=CARTESIAN_POINT('Ctrl Pts',(117.818287849696,-4.86492688042555,131.539472300911));
#42012=CARTESIAN_POINT('Ctrl Pts',(117.810513515577,-4.84073077224359,131.674135676506));
#42013=CARTESIAN_POINT('Ctrl Pts',(117.80274876263,-4.81656448360249,131.808633091525));
#42014=CARTESIAN_POINT('Ctrl Pts',(117.794984009683,-4.7867567953695,131.942299154777));
#42015=CARTESIAN_POINT('Ctrl Pts',(117.787219256735,-4.7513799347683,132.074625069553));
#42016=CARTESIAN_POINT('Ctrl Pts',(117.779462215851,-4.71603821096378,132.206819556364));
#42017=CARTESIAN_POINT('Ctrl Pts',(117.771705174966,-4.67513842281126,132.337676168301));
#42018=CARTESIAN_POINT('Ctrl Pts',(117.763948134081,-4.62880403288357,132.46669520713));
#42019=CARTESIAN_POINT('Ctrl Pts',(117.75619694284,-4.58250458407985,132.595616951698));
#42020=CARTESIAN_POINT('Ctrl Pts',(117.7484457516,-4.53077882247863,132.7227035149));
#42021=CARTESIAN_POINT('Ctrl Pts',(117.74069456036,-4.47380023577484,132.847469648646));
#42022=CARTESIAN_POINT('Ctrl Pts',(117.732946663583,-4.41684586649028,132.972182753457));
#42023=CARTESIAN_POINT('Ctrl Pts',(117.725198766806,-4.35464327462833,133.094577035488));
#42024=CARTESIAN_POINT('Ctrl Pts',(117.717450870029,-4.28741425709157,133.214186762869));
#42025=CARTESIAN_POINT('Ctrl Pts',(117.709704593945,-4.22019930241598,133.333771470475));
#42026=CARTESIAN_POINT('Ctrl Pts',(117.701958317861,-4.14796020483971,133.450572441392));
#42027=CARTESIAN_POINT('Ctrl Pts',(117.694212041777,-4.07096475509683,133.564148476308));
#42028=CARTESIAN_POINT('Ctrl Pts',(117.686465708511,-3.99396873699097,133.677725349617));
#42029=CARTESIAN_POINT('Ctrl Pts',(117.678719375246,-3.91221651604153,133.78807691581));
#42030=CARTESIAN_POINT('Ctrl Pts',(117.670973041981,-3.82601902936198,133.894791242812));
#42031=CARTESIAN_POINT('Ctrl Pts',(117.663224973978,-3.73980223935306,134.001529467748));
#42032=CARTESIAN_POINT('Ctrl Pts',(117.655476905975,-3.64913844833108,134.104628528579));
#42033=CARTESIAN_POINT('Ctrl Pts',(117.647728837972,-3.55437839409314,134.20371015742));
#42034=CARTESIAN_POINT('Ctrl Pts',(117.63997253523,-3.45951762774183,134.302897091394));
#42035=CARTESIAN_POINT('Ctrl Pts',(117.632216232488,-3.36055217212944,134.398057781045));
#42036=CARTESIAN_POINT('Ctrl Pts',(117.624459929746,-3.25786949450717,134.488851005565));
#42037=CARTESIAN_POINT('Ctrl Pts',(117.616699487232,-3.15513201204807,134.579692689163));
#42038=CARTESIAN_POINT('Ctrl Pts',(117.608939044718,-3.0486736576287,134.66616201645));
#42039=CARTESIAN_POINT('Ctrl Pts',(117.601178602204,-2.938913598963,134.747959217871));
#42040=CARTESIAN_POINT('Ctrl Pts',(117.593405701938,-2.82897734370708,134.829887727422));
#42041=CARTESIAN_POINT('Ctrl Pts',(117.585632801673,-2.71572911591568,134.907128903073));
#42042=CARTESIAN_POINT('Ctrl Pts',(117.577859901407,-2.59961632469809,134.979426847803));
#42043=CARTESIAN_POINT('Ctrl Pts',(117.570369565645,-2.48772452591102,135.049096580134));
#42044=CARTESIAN_POINT('Ctrl Pts',(117.562879229883,-2.37317308386355,135.114176087509));
#42045=CARTESIAN_POINT('Ctrl Pts',(117.555388894121,-2.2563807614013,135.174478341619));
#42046=CARTESIAN_POINT('Ctrl Pts',(117.547614560002,-2.13516022253541,135.23706697402));
#42047=CARTESIAN_POINT('Ctrl Pts',(117.539840225883,-2.01114153267069,135.294707204907));
#42048=CARTESIAN_POINT('Ctrl Pts',(117.532065891764,-1.88476683342271,135.347139177669));
#42049=CARTESIAN_POINT('Ctrl Pts',(117.524301138817,-1.75854787969721,135.39950653271));
#42050=CARTESIAN_POINT('Ctrl Pts',(117.51653638587,-1.62997905148056,135.446678252565));
#42051=CARTESIAN_POINT('Ctrl Pts',(117.508771632922,-1.49952745443278,135.488440086992));
#42052=CARTESIAN_POINT('Ctrl Pts',(117.501014592037,-1.36920542375024,135.530160442977));
#42053=CARTESIAN_POINT('Ctrl Pts',(117.493257551152,-1.237004715547,135.566481487964));
#42054=CARTESIAN_POINT('Ctrl Pts',(117.485500510267,-1.10341247463453,135.597236995413));
#42055=CARTESIAN_POINT('Ctrl Pts',(117.477749319027,-0.969920976670225,
135.627969309894));
#42056=CARTESIAN_POINT('Ctrl Pts',(117.469998127787,-0.835040414152658,
135.653144353381));
#42057=CARTESIAN_POINT('Ctrl Pts',(117.462246936547,-0.699272814378756,
135.672645797542));
#42058=CARTESIAN_POINT('Ctrl Pts',(117.45449903977,-0.563562919456384,135.692138953068));
#42059=CARTESIAN_POINT('Ctrl Pts',(117.446751142993,-0.426967123313924,
135.70596324995));
#42060=CARTESIAN_POINT('Ctrl Pts',(117.439003246216,-0.289997146005428,
135.714053552751));
#42061=CARTESIAN_POINT('Ctrl Pts',(117.431256970132,-0.153055819863362,
135.722142163236));
#42062=CARTESIAN_POINT('Ctrl Pts',(117.423510694048,-0.0157408582775557,
135.72449914233));
#42063=CARTESIAN_POINT('Ctrl Pts',(117.415764417964,0.121431797842503,135.721111310958));
#42064=CARTESIAN_POINT('Ctrl Pts',(117.408018084698,0.258605466539949,135.717723454578));
#42065=CARTESIAN_POINT('Ctrl Pts',(117.400271751433,0.395636436829494,135.708590712764));
#42066=CARTESIAN_POINT('Ctrl Pts',(117.392525418167,0.53201006948388,135.693752026368));
#42067=CARTESIAN_POINT('Ctrl Pts',(117.384777350165,0.668414242067658,135.678910016951));
#42068=CARTESIAN_POINT('Ctrl Pts',(117.377029282162,0.804160395496203,135.658359562546));
#42069=CARTESIAN_POINT('Ctrl Pts',(117.369281214159,0.938740699935791,135.632191285763));
#42070=CARTESIAN_POINT('Ctrl Pts',(117.361524911417,1.07346403792456,135.605995197024));
#42071=CARTESIAN_POINT('Ctrl Pts',(117.353768608675,1.20701866734276,135.574169433555));
#42072=CARTESIAN_POINT('Ctrl Pts',(117.346012305933,1.338908073948,135.536855544348));
#42073=CARTESIAN_POINT('Ctrl Pts',(117.338251863419,1.47086787390065,135.499521739595));
#42074=CARTESIAN_POINT('Ctrl Pts',(117.330491420905,1.60116030883881,135.456694094493));
#42075=CARTESIAN_POINT('Ctrl Pts',(117.32273097839,1.72930660375927,135.408563233948));
#42076=CARTESIAN_POINT('Ctrl Pts',(117.314958078125,1.85765861048863,135.360355109472));
#42077=CARTESIAN_POINT('Ctrl Pts',(117.30718517786,1.98385723251042,135.306826910234));
#42078=CARTESIAN_POINT('Ctrl Pts',(117.299412277594,2.10744534086116,135.248216735599));
#42079=CARTESIAN_POINT('Ctrl Pts',(117.291921941832,2.22654071017419,135.191737188442));
#42080=CARTESIAN_POINT('Ctrl Pts',(117.28443160607,2.34321179537716,135.130538879374));
#42081=CARTESIAN_POINT('Ctrl Pts',(117.276941270308,2.45707489270949,135.064873032067));
#42082=CARTESIAN_POINT('Ctrl Pts',(117.269166936189,2.5752551439847,134.996717444201));
#42083=CARTESIAN_POINT('Ctrl Pts',(117.26139260207,2.69078463388255,134.923532960761));
#42084=CARTESIAN_POINT('Ctrl Pts',(117.253618267951,2.80320574933492,134.845551109166));
#42085=CARTESIAN_POINT('Ctrl Pts',(117.245853515004,2.91548831580978,134.767665363233));
#42086=CARTESIAN_POINT('Ctrl Pts',(117.238088762057,3.02466981181543,134.684994233611));
#42087=CARTESIAN_POINT('Ctrl Pts',(117.230324009109,3.13031750053771,134.597814902031));
#42088=CARTESIAN_POINT('Ctrl Pts',(117.222566968224,3.23586025848617,134.510722158192));
#42089=CARTESIAN_POINT('Ctrl Pts',(117.214809927339,3.33787589426502,134.419130370269));
#42090=CARTESIAN_POINT('Ctrl Pts',(117.207052886454,3.43596124310754,134.323359537481));
#42091=CARTESIAN_POINT('Ctrl Pts',(117.199301695214,3.5339726250255,134.227660926223));
#42092=CARTESIAN_POINT('Ctrl Pts',(117.191550503974,3.62805934078759,134.127789814901));
#42093=CARTESIAN_POINT('Ctrl Pts',(117.183799312734,3.71785216205539,134.024105694991));
#42094=CARTESIAN_POINT('Ctrl Pts',(117.176051415957,3.80760681897891,133.920465643597));
#42095=CARTESIAN_POINT('Ctrl Pts',(117.16830351918,3.89307095582263,133.81301610185));
#42096=CARTESIAN_POINT('Ctrl Pts',(117.160555622403,3.97391317511178,133.70215238703));
#42097=CARTESIAN_POINT('Ctrl Pts',(117.152809346319,4.05473848395141,133.591311862509));
#42098=CARTESIAN_POINT('Ctrl Pts',(117.145063070235,4.13094356805814,133.477058901138));
#42099=CARTESIAN_POINT('Ctrl Pts',(117.137316794151,4.20223846083776,133.359820455003));
#42100=CARTESIAN_POINT('Ctrl Pts',(117.129570460885,4.27353387990004,133.242581143442));
#42101=CARTESIAN_POINT('Ctrl Pts',(117.12182412762,4.33991883216861,133.122356637188));
#42102=CARTESIAN_POINT('Ctrl Pts',(117.114077794354,4.40114790461073,132.999600965282));
#42103=CARTESIAN_POINT('Ctrl Pts',(117.106329726351,4.46239068887909,132.876817803094));
#42104=CARTESIAN_POINT('Ctrl Pts',(117.098581658349,4.51847512128156,132.751502697105));
#42105=CARTESIAN_POINT('Ctrl Pts',(117.090833590346,4.56920295075611,132.624131882671));
#42106=CARTESIAN_POINT('Ctrl Pts',(117.083077287604,4.61998469437154,132.496625697019));
#42107=CARTESIAN_POINT('Ctrl Pts',(117.075320984862,4.6653983176665,132.367059802284));
#42108=CARTESIAN_POINT('Ctrl Pts',(117.06756468212,4.70529453174012,132.235928440645));
#42109=CARTESIAN_POINT('Ctrl Pts',(117.059804239606,4.74521203962446,132.104727090251));
#42110=CARTESIAN_POINT('Ctrl Pts',(117.052043797092,4.77960617251255,131.971958986364));
#42111=CARTESIAN_POINT('Ctrl Pts',(117.044283354577,4.8083785189504,131.838129973369));
#42112=CARTESIAN_POINT('Ctrl Pts',(117.036510454312,4.83719705331301,131.704086126161));
#42113=CARTESIAN_POINT('Ctrl Pts',(117.028737554047,4.86037570107255,131.568978352137));
#42114=CARTESIAN_POINT('Ctrl Pts',(117.020964653781,4.87786769259683,131.433319945361));
#42115=CARTESIAN_POINT('Ctrl Pts',(117.013474318019,4.89472380616945,131.302593063375));
#42116=CARTESIAN_POINT('Ctrl Pts',(117.005983982257,4.90629950692592,131.171355194195));
#42117=CARTESIAN_POINT('Ctrl Pts',(116.998493646495,4.91259875520174,131.040064951193));
#42118=CARTESIAN_POINT('Ctrl Pts',(116.990719312376,4.91913684139058,130.903796798721));
#42119=CARTESIAN_POINT('Ctrl Pts',(116.982944978257,4.92001117403477,130.767040565976));
#42120=CARTESIAN_POINT('Ctrl Pts',(116.975170644138,4.91516919266761,130.630306402014));
#42121=CARTESIAN_POINT('Ctrl Pts',(116.967405891191,4.91033317860973,130.49374075069));
#42122=CARTESIAN_POINT('Ctrl Pts',(116.959641138244,4.89979488138778,130.357197501004));
#42123=CARTESIAN_POINT('Ctrl Pts',(116.951876385297,4.88355359702528,130.221190550192));
#42124=CARTESIAN_POINT('Ctrl Pts',(116.944119344412,4.86732844373538,130.0853186834));
#42125=CARTESIAN_POINT('Ctrl Pts',(116.936362303527,4.84541162154993,129.94998244116));
#42126=CARTESIAN_POINT('Ctrl Pts',(116.928605262642,4.81785443447189,129.815693984803));
#42127=CARTESIAN_POINT('Ctrl Pts',(116.920854071402,4.79031802848298,129.681506796415));
#42128=CARTESIAN_POINT('Ctrl Pts',(116.913102880162,4.75714980209572,129.548366202613));
#42129=CARTESIAN_POINT('Ctrl Pts',(116.905351688922,4.71845262873539,129.416777159579));
#42130=CARTESIAN_POINT('Ctrl Pts',(116.897603792144,4.67977190270598,129.285244045398));
#42131=CARTESIAN_POINT('Ctrl Pts',(116.889855895367,4.63556701364667,129.155261544686));
#42132=CARTESIAN_POINT('Ctrl Pts',(116.88210799859,4.58599142475161,129.02732215017));
#42133=CARTESIAN_POINT('Ctrl Pts',(116.874361722506,4.53642620600101,128.899409517818));
#42134=CARTESIAN_POINT('Ctrl Pts',(116.866615446422,4.48149266315989,128.773539505914));
#42135=CARTESIAN_POINT('Ctrl Pts',(116.858869170338,4.42139326908373,128.650186849598));
#42136=CARTESIAN_POINT('Ctrl Pts',(116.851122837073,4.36129343136754,128.526833282721));
#42137=CARTESIAN_POINT('Ctrl Pts',(116.843376503807,4.2960278375656,128.405997459982));
#42138=CARTESIAN_POINT('Ctrl Pts',(116.835630170542,4.22584582342771,128.288131268099));
#42139=CARTESIAN_POINT('Ctrl Pts',(116.827882102539,4.15564809251435,128.1702386809));
#42140=CARTESIAN_POINT('Ctrl Pts',(116.820134034536,4.0805319503897,128.055317383748));
#42141=CARTESIAN_POINT('Ctrl Pts',(116.812385966533,4.00079090780434,127.943791587717));
#42142=CARTESIAN_POINT('Ctrl Pts',(116.804629663791,3.92096511548993,127.832147260743));
#42143=CARTESIAN_POINT('Ctrl Pts',(116.796873361049,3.83650483143241,127.723905962357));
#42144=CARTESIAN_POINT('Ctrl Pts',(116.789117058308,3.74774518127914,127.61946044351));
#42145=CARTESIAN_POINT('Ctrl Pts',(116.781356615793,3.65893815742809,127.514959178946));
#42146=CARTESIAN_POINT('Ctrl Pts',(116.773596173279,3.56582746038873,127.414258017662));
#42147=CARTESIAN_POINT('Ctrl Pts',(116.765835730765,3.46878547757482,127.317713177249));
#42148=CARTESIAN_POINT('Ctrl Pts',(116.7580628305,3.37158771435505,127.221013354488));
#42149=CARTESIAN_POINT('Ctrl Pts',(116.750289930234,3.27044634290115,127.128483449624));
#42150=CARTESIAN_POINT('Ctrl Pts',(116.742517029969,3.16576793191937,127.040440259252));
#42151=CARTESIAN_POINT('Ctrl Pts',(116.735026694207,3.06489484484521,126.955597660617));
#42152=CARTESIAN_POINT('Ctrl Pts',(116.727536358445,2.96073765766425,126.874921421774));
#42153=CARTESIAN_POINT('Ctrl Pts',(116.720046022683,2.85368435545317,126.79865610251));
#42154=CARTESIAN_POINT('Ctrl Pts',(116.712271688563,2.74257209475132,126.719499160486));
#42155=CARTESIAN_POINT('Ctrl Pts',(116.704497354444,2.62798780115533,126.644843475414));
#42156=CARTESIAN_POINT('Ctrl Pts',(116.696723020325,2.51033226730108,126.575009015932));
#42157=CARTESIAN_POINT('Ctrl Pts',(116.688958267378,2.3928217333772,126.505260621179));
#42158=CARTESIAN_POINT('Ctrl Pts',(116.681193514431,2.27224782325015,126.440321827383));
#42159=CARTESIAN_POINT('Ctrl Pts',(116.673428761484,2.14904251270113,126.380471000826));
#42160=CARTESIAN_POINT('Ctrl Pts',(116.665671720599,2.02595957140337,126.320679618953));
#42161=CARTESIAN_POINT('Ctrl Pts',(116.657914679714,1.90025078014564,126.265966317472));
#42162=CARTESIAN_POINT('Ctrl Pts',(116.650157638829,1.77237476582821,126.216564768582));
#42163=CARTESIAN_POINT('Ctrl Pts',(116.642406447589,1.6445951838079,126.167200473784));
#42164=CARTESIAN_POINT('Ctrl Pts',(116.634655256349,1.51465199496312,126.123140098927));
#42165=CARTESIAN_POINT('Ctrl Pts',(116.626904065109,1.38302563883066,126.084570034835));
#42166=CARTESIAN_POINT('Ctrl Pts',(116.619156168331,1.2514552274108,126.046016364049));
#42167=CARTESIAN_POINT('Ctrl Pts',(116.611408271554,1.11820344596504,126.012948472528));
#42168=CARTESIAN_POINT('Ctrl Pts',(116.603660374777,0.983767593178136,125.98550345169));
#42169=CARTESIAN_POINT('Ctrl Pts',(116.595914098693,0.849359861473531,125.958064171759));
#42170=CARTESIAN_POINT('Ctrl Pts',(116.588167822609,0.713768933902753,125.93624550117));
#42171=CARTESIAN_POINT('Ctrl Pts',(116.580421546525,0.577503660108147,125.920133699715));
#42172=CARTESIAN_POINT('Ctrl Pts',(116.57267521326,0.441237380434337,125.904021779326));
#42173=CARTESIAN_POINT('Ctrl Pts',(116.564928879994,0.304297132864337,125.89361685804));
#42174=CARTESIAN_POINT('Ctrl Pts',(116.557182546729,0.167197874557127,125.888953418438));
#42175=CARTESIAN_POINT('Ctrl Pts',(116.549434478726,0.0300679138215044,
125.884288934491));
#42176=CARTESIAN_POINT('Ctrl Pts',(116.541686410723,-0.107220737845377,
125.88536850404));
#42177=CARTESIAN_POINT('Ctrl Pts',(116.53393834272,-0.244152529921328,125.892174484628));
#42178=CARTESIAN_POINT('Ctrl Pts',(116.526182039978,-0.381229854735314,
125.898987698692));
#42179=CARTESIAN_POINT('Ctrl Pts',(116.518425737236,-0.51794917121065,125.911539461991));
#42180=CARTESIAN_POINT('Ctrl Pts',(116.510669434494,-0.653798903249842,
125.929760115308));
#42181=CARTESIAN_POINT('Ctrl Pts',(116.50290899198,-0.789721142381565,125.947990493538));
#42182=CARTESIAN_POINT('Ctrl Pts',(116.495148549466,-0.92477248747973,125.971895722552));
#42183=CARTESIAN_POINT('Ctrl Pts',(116.487388106952,-1.05845195810392,126.001355046584));
#42184=CARTESIAN_POINT('Ctrl Pts',(116.479615206686,-1.19234602288186,126.030861661337));
#42185=CARTESIAN_POINT('Ctrl Pts',(116.471842306421,-1.32486343421377,126.065940087866));
#42186=CARTESIAN_POINT('Ctrl Pts',(116.464069406155,-1.45551790183405,126.106419504702));
#42187=CARTESIAN_POINT('Ctrl Pts',(116.456579070393,-1.58142275045652,126.145427392773));
#42188=CARTESIAN_POINT('Ctrl Pts',(116.449088734631,-1.70559745891545,126.189450306511));
#42189=CARTESIAN_POINT('Ctrl Pts',(116.441598398869,-1.82762655672429,126.238294013622));
#42190=CARTESIAN_POINT('Ctrl Pts',(116.433823739619,-1.95428772175633,126.28899176488));
#42191=CARTESIAN_POINT('Ctrl Pts',(116.426049080369,-2.07903841053544,126.345044123271));
#42192=CARTESIAN_POINT('Ctrl Pts',(116.418274421118,-2.20139272551441,126.406286819805));
#42193=CARTESIAN_POINT('Ctrl Pts',(116.410509417803,-2.32359507945858,126.467453454424));
#42194=CARTESIAN_POINT('Ctrl Pts',(116.402744414487,-2.44340663531066,126.533797427219));
#42195=CARTESIAN_POINT('Ctrl Pts',(116.394979411171,-2.56035965804851,126.605105745099));
#42196=CARTESIAN_POINT('Ctrl Pts',(116.387222194363,-2.67719540387604,126.676342557181));
#42197=CARTESIAN_POINT('Ctrl Pts',(116.379464977555,-2.79117798951135,126.752533605028));
#42198=CARTESIAN_POINT('Ctrl Pts',(116.371707760747,-2.90186289272959,126.833419316779));
#42199=CARTESIAN_POINT('Ctrl Pts',(116.363726401479,-3.01574600312155,126.916642196978));
#42200=CARTESIAN_POINT('Ctrl Pts',(116.355745042211,-3.12613759040226,127.004834978786));
#42201=CARTESIAN_POINT('Ctrl Pts',(116.347763682943,-3.23258342274687,127.097665664177));
#42202=CARTESIAN_POINT('Ctrl Pts',(116.340016127709,-3.33591105628094,127.187776989623));
#42203=CARTESIAN_POINT('Ctrl Pts',(116.332268572475,-3.43552055662054,127.282258021064));
#42204=CARTESIAN_POINT('Ctrl Pts',(116.324521017241,-3.53102885228761,127.380763341774));
#42205=CARTESIAN_POINT('Ctrl Pts',(116.316775138562,-3.62651648016286,127.479247346142));
#42206=CARTESIAN_POINT('Ctrl Pts',(116.309029259882,-3.71790439738277,127.58175362649));
#42207=CARTESIAN_POINT('Ctrl Pts',(116.301283381203,-3.80484618139089,127.687899708385));
#42208=CARTESIAN_POINT('Ctrl Pts',(116.293537501295,-3.89178797918496,127.79404580711));
#42209=CARTESIAN_POINT('Ctrl Pts',(116.285791621387,-3.97428339523463,127.903831405719));
#42210=CARTESIAN_POINT('Ctrl Pts',(116.27804574148,-4.05202637596742,128.01684105513));
#42211=CARTESIAN_POINT('Ctrl Pts',(116.270298182938,-4.12978620462031,128.129875195208));
#42212=CARTESIAN_POINT('Ctrl Pts',(116.262550624397,-4.20279132786444,128.246134453958));
#42213=CARTESIAN_POINT('Ctrl Pts',(116.254803065856,-4.27077931482062,128.365174870928));
#42214=CARTESIAN_POINT('Ctrl Pts',(116.247048651461,-4.33882746469416,128.484320627373));
#42215=CARTESIAN_POINT('Ctrl Pts',(116.239294237065,-4.40184942114921,128.606252115559));
#42216=CARTESIAN_POINT('Ctrl Pts',(116.23153982267,-4.45962884239706,128.730501015143));
#42217=CARTESIAN_POINT('Ctrl Pts',(116.223781267413,-4.51743911788667,128.854816263707));
#42218=CARTESIAN_POINT('Ctrl Pts',(116.216022712156,-4.57000113067515,128.981451028912));
#42219=CARTESIAN_POINT('Ctrl Pts',(116.208264156899,-4.61714726400384,129.109918466001));
#42220=CARTESIAN_POINT('Ctrl Pts',(116.20049639022,-4.66434937205099,129.238538427339));
#42221=CARTESIAN_POINT('Ctrl Pts',(116.192728623541,-4.7061226463963,129.368995032754));
#42222=CARTESIAN_POINT('Ctrl Pts',(116.184960856862,-4.74234966060826,129.500787543654));
#42223=CARTESIAN_POINT('Ctrl Pts',(116.183358950682,-4.74982056960365,129.52796642871));
#42224=CARTESIAN_POINT('Ctrl Pts',(116.181757044501,-4.75705577794431,129.555202098149));
#42225=CARTESIAN_POINT('Ctrl Pts',(116.180155138321,-4.76405452823404,129.582490119308));
#42226=CARTESIAN_POINT('Origin',(213.235140564004,0.,130.804360617566));
#42227=CARTESIAN_POINT('',(114.08491538754,-4.76405452823405,129.582490119308));
#42228=CARTESIAN_POINT('',(114.429855701321,-4.76405452823407,129.582490119308));
#42229=CARTESIAN_POINT('',(213.235140564004,-4.76405452823405,129.582490119308));
#42230=CARTESIAN_POINT('',(115.76485943597,-4.91824999995734,130.80438110132));
#42231=CARTESIAN_POINT('Ctrl Pts',(115.764859435949,-4.91824999995734,130.80438110169));
#42232=CARTESIAN_POINT('Ctrl Pts',(115.756742290709,-4.91824939965866,130.948513163258));
#42233=CARTESIAN_POINT('Ctrl Pts',(115.748625145469,-4.91190868767493,131.092521964845));
#42234=CARTESIAN_POINT('Ctrl Pts',(115.740508000229,-4.89928608984441,131.235845115963));
#42235=CARTESIAN_POINT('Ctrl Pts',(115.732380078311,-4.88664673369991,131.379358549177));
#42236=CARTESIAN_POINT('Ctrl Pts',(115.724252156393,-4.8677088783086,131.522184184355));
#42237=CARTESIAN_POINT('Ctrl Pts',(115.716124234475,-4.84258216027101,131.663768020097));
#42238=CARTESIAN_POINT('Ctrl Pts',(115.707977022248,-4.81739580802846,131.805687882194));
#42239=CARTESIAN_POINT('Ctrl Pts',(115.69982981002,-4.785991283619,131.946359723495));
#42240=CARTESIAN_POINT('Ctrl Pts',(115.691682597793,-4.74852905514042,132.085241125259));
#42241=CARTESIAN_POINT('Ctrl Pts',(115.683525192704,-4.7110199581972,132.224296279582));
#42242=CARTESIAN_POINT('Ctrl Pts',(115.675367787615,-4.66743813284541,132.361556207261));
#42243=CARTESIAN_POINT('Ctrl Pts',(115.667210382525,-4.61799291307658,132.496496698759));
#42244=CARTESIAN_POINT('Ctrl Pts',(115.659034265724,-4.56843427431116,132.631746720991));
#42245=CARTESIAN_POINT('Ctrl Pts',(115.650858148923,-4.51298547576976,132.764666360837));
#42246=CARTESIAN_POINT('Ctrl Pts',(115.642682032122,-4.45190345035901,132.894752621756));
#42247=CARTESIAN_POINT('Ctrl Pts',(115.637069529278,-4.40997363823737,132.984050454355));
#42248=CARTESIAN_POINT('Ctrl Pts',(115.631457026434,-4.36539032889249,133.072013675603));
#42249=CARTESIAN_POINT('Ctrl Pts',(115.62584452359,-4.31824851471123,133.158487382992));
#42250=CARTESIAN_POINT('Ctrl Pts',(115.618070189471,-4.25294855414198,133.278269147458));
#42251=CARTESIAN_POINT('Ctrl Pts',(115.610295855351,-4.18255753523278,133.395521593527));
#42252=CARTESIAN_POINT('Ctrl Pts',(115.602521521232,-4.10729593727613,133.509781683895));
#42253=CARTESIAN_POINT('Ctrl Pts',(115.594756768285,-4.0321270925127,133.623900958912));
#42254=CARTESIAN_POINT('Ctrl Pts',(115.586992015338,-3.95209982499075,133.735034892506));
#42255=CARTESIAN_POINT('Ctrl Pts',(115.579227262391,-3.86748085213096,133.842744220882));
#42256=CARTESIAN_POINT('Ctrl Pts',(115.571470221506,-3.78294592402805,133.950346570835));
#42257=CARTESIAN_POINT('Ctrl Pts',(115.563713180621,-3.69382860624714,134.054530778995));
#42258=CARTESIAN_POINT('Ctrl Pts',(115.555956139736,-3.60043913101427,134.154886117597));
#42259=CARTESIAN_POINT('Ctrl Pts',(115.548204948496,-3.50712008151108,134.255165777459));
#42260=CARTESIAN_POINT('Ctrl Pts',(115.540453757256,-3.40953555235383,134.351622029868));
#42261=CARTESIAN_POINT('Ctrl Pts',(115.532702566016,-3.30803607103304,134.443877126011));
#42262=CARTESIAN_POINT('Ctrl Pts',(115.524954669239,-3.20657972969932,134.536093011277));
#42263=CARTESIAN_POINT('Ctrl Pts',(115.517206772462,-3.10121203439929,134.624111029292));
#42264=CARTESIAN_POINT('Ctrl Pts',(115.509458875685,-2.99232023594627,134.70759039149));
#42265=CARTESIAN_POINT('Ctrl Pts',(115.5017125996,-2.88345121530997,134.791052291605));
#42266=CARTESIAN_POINT('Ctrl Pts',(115.493966323516,-2.77105986786696,134.869977186573));
#42267=CARTESIAN_POINT('Ctrl Pts',(115.486220047432,-2.65556606435359,134.94406494763));
#42268=CARTESIAN_POINT('Ctrl Pts',(115.478473714167,-2.54007140829127,135.018153255587));
#42269=CARTESIAN_POINT('Ctrl Pts',(115.470727380902,-2.42147457953653,135.087404147284));
#42270=CARTESIAN_POINT('Ctrl Pts',(115.462981047636,-2.30022358714223,135.151561384917));
#42271=CARTESIAN_POINT('Ctrl Pts',(115.455232979633,-2.17894544142913,135.215732990118));
#42272=CARTESIAN_POINT('Ctrl Pts',(115.44748491163,-2.05501229483079,135.274808488602));
#42273=CARTESIAN_POINT('Ctrl Pts',(115.439736843627,-1.92889548807974,135.328578258061));
#42274=CARTESIAN_POINT('Ctrl Pts',(115.431980540886,-1.8026446428854,135.382405174671));
#42275=CARTESIAN_POINT('Ctrl Pts',(115.424224238144,-1.67420586166634,135.430914944186));
#42276=CARTESIAN_POINT('Ctrl Pts',(115.416467935402,-1.54406966175244,135.473946460246));
#42277=CARTESIAN_POINT('Ctrl Pts',(115.408707492888,-1.41386400423032,135.517000943522));
#42278=CARTESIAN_POINT('Ctrl Pts',(115.400947050374,-1.28195949863064,135.55457124016));
#42279=CARTESIAN_POINT('Ctrl Pts',(115.393186607859,-1.14885948206551,135.586546828178));
#42280=CARTESIAN_POINT('Ctrl Pts',(115.385413707594,-1.01554580153763,135.618573746248));
#42281=CARTESIAN_POINT('Ctrl Pts',(115.377640807328,-0.881033158849612,
135.644987933173));
#42282=CARTESIAN_POINT('Ctrl Pts',(115.369867907063,-0.745833577909087,
135.665730315147));
#42283=CARTESIAN_POINT('Ctrl Pts',(115.362377571301,-0.615548842282759,
135.68571865929));
#42284=CARTESIAN_POINT('Ctrl Pts',(115.354887235539,-0.484626551266065,
135.700440373528));
#42285=CARTESIAN_POINT('Ctrl Pts',(115.347396899777,-0.353525281199007,
135.709888411601));
#42286=CARTESIAN_POINT('Ctrl Pts',(115.339622565658,-0.217453266630271,
135.719694674909));
#42287=CARTESIAN_POINT('Ctrl Pts',(115.331848231539,-0.0807573978733542,
135.723850528275));
#42288=CARTESIAN_POINT('Ctrl Pts',(115.32407389742,0.0560535842287742,135.722291184196));
#42289=CARTESIAN_POINT('Ctrl Pts',(115.316309144473,0.192695959022425,135.72073376187));
#42290=CARTESIAN_POINT('Ctrl Pts',(115.308544391526,0.329452777701594,135.713475160918));
#42291=CARTESIAN_POINT('Ctrl Pts',(115.300779638578,0.465810307915003,135.700502345451));
#42292=CARTESIAN_POINT('Ctrl Pts',(115.293022597693,0.602032405907284,135.687542414768));
#42293=CARTESIAN_POINT('Ctrl Pts',(115.285265556808,0.737855617954568,135.668879600736));
#42294=CARTESIAN_POINT('Ctrl Pts',(115.277508515923,0.8727666990604,135.644552902126));
#42295=CARTESIAN_POINT('Ctrl Pts',(115.269757324683,1.00757604267033,135.620244548468));
#42296=CARTESIAN_POINT('Ctrl Pts',(115.262006133443,1.14147424124929,135.590280880853));
#42297=CARTESIAN_POINT('Ctrl Pts',(115.254254942203,1.27395401535093,135.554752625524));
#42298=CARTESIAN_POINT('Ctrl Pts',(115.246507045426,1.40637748201465,135.519239470652));
#42299=CARTESIAN_POINT('Ctrl Pts',(115.238759148649,1.53738334642888,135.478166533124));
#42300=CARTESIAN_POINT('Ctrl Pts',(115.231011251872,1.66647557499834,135.431675413475));
#42301=CARTESIAN_POINT('Ctrl Pts',(115.223264975788,1.7955408002565,135.385194018765));
#42302=CARTESIAN_POINT('Ctrl Pts',(115.215518699704,1.92269281826643,135.333296828651));
#42303=CARTESIAN_POINT('Ctrl Pts',(115.20777242362,2.04745217181012,135.276174865346));
#42304=CARTESIAN_POINT('Ctrl Pts',(115.200026090354,2.17221244629894,135.21905248038));
#42305=CARTESIAN_POINT('Ctrl Pts',(115.192279757089,2.29457966560127,135.156705408022));
#42306=CARTESIAN_POINT('Ctrl Pts',(115.184533423824,2.41409608975856,135.089372068182));
#42307=CARTESIAN_POINT('Ctrl Pts',(115.176785355821,2.53363927879037,135.022023649508));
#42308=CARTESIAN_POINT('Ctrl Pts',(115.169037287818,2.65033006174147,134.949686933236));
#42309=CARTESIAN_POINT('Ctrl Pts',(115.161289219815,2.76373730624994,134.872645165695));
#42310=CARTESIAN_POINT('Ctrl Pts',(115.153532917073,2.87726508132752,134.795521517246));
#42311=CARTESIAN_POINT('Ctrl Pts',(115.145776614331,2.98750202282875,134.713683048371));
#42312=CARTESIAN_POINT('Ctrl Pts',(115.138020311589,3.09404745081275,134.627455363269));
#42313=CARTESIAN_POINT('Ctrl Pts',(115.130259869075,3.20064974529975,134.541181655854));
#42314=CARTESIAN_POINT('Ctrl Pts',(115.122499426561,3.30355630713151,134.450514322602));
#42315=CARTESIAN_POINT('Ctrl Pts',(115.114738984047,3.40240208502859,134.355817095448));
#42316=CARTESIAN_POINT('Ctrl Pts',(115.106966083781,3.50140653894346,134.260967851899));
#42317=CARTESIAN_POINT('Ctrl Pts',(115.099193183516,3.59633691151905,134.162076069245));
#42318=CARTESIAN_POINT('Ctrl Pts',(115.09142028325,3.68686674086039,134.059540596866));
#42319=CARTESIAN_POINT('Ctrl Pts',(115.083929947488,3.77410558287503,133.960732547179));
#42320=CARTESIAN_POINT('Ctrl Pts',(115.076439611726,3.85725807425426,133.858541361978));
#42321=CARTESIAN_POINT('Ctrl Pts',(115.068949275964,3.93607041506568,133.753349045849));
#42322=CARTESIAN_POINT('Ctrl Pts',(115.061174941845,4.01787094973278,133.644168331082));
#42323=CARTESIAN_POINT('Ctrl Pts',(115.053400607726,4.09525484291431,133.531408565524));
#42324=CARTESIAN_POINT('Ctrl Pts',(115.045626273607,4.16789260019818,133.41546274803));
#42325=CARTESIAN_POINT('Ctrl Pts',(115.03786152066,4.24044083793802,133.299659823393));
#42326=CARTESIAN_POINT('Ctrl Pts',(115.030096767713,4.30825437235047,133.180678987568));
#42327=CARTESIAN_POINT('Ctrl Pts',(115.022332014765,4.37104455108726,133.058945411915));
#42328=CARTESIAN_POINT('Ctrl Pts',(115.01457497388,4.43377236573335,132.937332743766));
#42329=CARTESIAN_POINT('Ctrl Pts',(115.006817932995,4.49148657550821,132.812973121908));
#42330=CARTESIAN_POINT('Ctrl Pts',(114.99906089211,4.54394256972332,132.686319433682));
#42331=CARTESIAN_POINT('Ctrl Pts',(114.99130970087,4.59635900646514,132.559761255987));
#42332=CARTESIAN_POINT('Ctrl Pts',(114.98355850963,4.64352497126251,132.430912815079));
#42333=CARTESIAN_POINT('Ctrl Pts',(114.97580731839,4.68524259774243,132.300249939274));
#42334=CARTESIAN_POINT('Ctrl Pts',(114.968059421613,4.72694249311824,132.169642598677));
#42335=CARTESIAN_POINT('Ctrl Pts',(114.960311524836,4.76319853724232,132.03722272867));
#42336=CARTESIAN_POINT('Ctrl Pts',(114.952563628059,4.7938617443789,131.903484194913));
#42337=CARTESIAN_POINT('Ctrl Pts',(114.944817351975,4.82451853743356,131.769773636375));
#42338=CARTESIAN_POINT('Ctrl Pts',(114.937071075891,4.84958473318081,131.634745343574));
#42339=CARTESIAN_POINT('Ctrl Pts',(114.929324799806,4.86896188568153,131.498905949622));
#42340=CARTESIAN_POINT('Ctrl Pts',(114.921578466541,4.88833918121999,131.363065552934));
#42341=CARTESIAN_POINT('Ctrl Pts',(114.913832133276,4.90202729450218,131.226414430193));
#42342=CARTESIAN_POINT('Ctrl Pts',(114.90608580001,4.90997939532392,131.089466562777));
#42343=CARTESIAN_POINT('Ctrl Pts',(114.898337732007,4.91793327696351,130.952488026835));
#42344=CARTESIAN_POINT('Ctrl Pts',(114.890589664004,4.92014856739681,130.815213004216));
#42345=CARTESIAN_POINT('Ctrl Pts',(114.882841596001,4.91663053221111,130.678157320345));
#42346=CARTESIAN_POINT('Ctrl Pts',(114.87508529326,4.91310875801575,130.540955972062));
#42347=CARTESIAN_POINT('Ctrl Pts',(114.867328990518,4.90384149593349,130.403974819662));
#42348=CARTESIAN_POINT('Ctrl Pts',(114.859572687776,4.88888610870378,130.267726963549));
#42349=CARTESIAN_POINT('Ctrl Pts',(114.851812245262,4.8739227393336,130.131406387854));
#42350=CARTESIAN_POINT('Ctrl Pts',(114.844051802748,4.85326525433895,129.995820274624));
#42351=CARTESIAN_POINT('Ctrl Pts',(114.836291360233,4.82702235256512,129.861472357836));
#42352=CARTESIAN_POINT('Ctrl Pts',(114.828518459968,4.80073732335564,129.726908773845));
#42353=CARTESIAN_POINT('Ctrl Pts',(114.820745559703,4.76884905102829,129.593587738739));
#42354=CARTESIAN_POINT('Ctrl Pts',(114.812972659437,4.73151663823373,129.461999501987));
#42355=CARTESIAN_POINT('Ctrl Pts',(114.805482323675,4.695541352679,129.335194829093));
#42356=CARTESIAN_POINT('Ctrl Pts',(114.797991987913,4.65451096706779,129.209999451336));
#42357=CARTESIAN_POINT('Ctrl Pts',(114.790501652151,4.60860968761438,129.086833380598));
#42358=CARTESIAN_POINT('Ctrl Pts',(114.782727318032,4.56096804719903,128.958997430852));
#42359=CARTESIAN_POINT('Ctrl Pts',(114.774952983913,4.50792794738468,128.832942762299));
#42360=CARTESIAN_POINT('Ctrl Pts',(114.767178649794,4.44964192945812,128.709159013398));
#42361=CARTESIAN_POINT('Ctrl Pts',(114.759413896847,4.39142774383952,128.585527816905));
#42362=CARTESIAN_POINT('Ctrl Pts',(114.7516491439,4.32798066873539,128.464162321793));
#42363=CARTESIAN_POINT('Ctrl Pts',(114.743884390952,4.25950238920709,128.345535194963));
#42364=CARTESIAN_POINT('Ctrl Pts',(114.736127350067,4.19109212327139,128.227025890268));
#42365=CARTESIAN_POINT('Ctrl Pts',(114.728370309182,4.11766079148668,128.111249877766));
#42366=CARTESIAN_POINT('Ctrl Pts',(114.720613268297,4.03945720274524,127.998657752028));
#42367=CARTESIAN_POINT('Ctrl Pts',(114.712862077057,3.96131258793835,127.886150532887));
#42368=CARTESIAN_POINT('Ctrl Pts',(114.705110885817,3.87840310149067,127.776822741284));
#42369=CARTESIAN_POINT('Ctrl Pts',(114.697359694577,3.79102211963303,127.671098044631));
#42370=CARTESIAN_POINT('Ctrl Pts',(114.6896117978,3.70367827702366,127.565418283795));
#42371=CARTESIAN_POINT('Ctrl Pts',(114.681863901023,3.61186696751373,127.463338872775));
#42372=CARTESIAN_POINT('Ctrl Pts',(114.674116004246,3.51592316383981,127.365252103943));
#42373=CARTESIAN_POINT('Ctrl Pts',(114.666369728162,3.41999942954131,127.267185852748));
#42374=CARTESIAN_POINT('Ctrl Pts',(114.658623452078,3.31994519368586,127.173110861847));
#42375=CARTESIAN_POINT('Ctrl Pts',(114.650877175994,3.21613348862195,127.083383804165));
#42376=CARTESIAN_POINT('Ctrl Pts',(114.643130842728,3.11232101724375,126.993656084139));
#42377=CARTESIAN_POINT('Ctrl Pts',(114.635384509463,3.00475131710103,126.908276617037));
#42378=CARTESIAN_POINT('Ctrl Pts',(114.627638176197,2.89383150241384,126.827562621925));
#42379=CARTESIAN_POINT('Ctrl Pts',(114.619890108195,2.78288684800306,126.746830551472));
#42380=CARTESIAN_POINT('Ctrl Pts',(114.612142040192,2.66859090223326,126.670766262036));
#42381=CARTESIAN_POINT('Ctrl Pts',(114.604393972189,2.55138048982342,126.59964413977));
#42382=CARTESIAN_POINT('Ctrl Pts',(114.596637669447,2.43404550479245,126.528446428066));
#42383=CARTESIAN_POINT('Ctrl Pts',(114.588881366705,2.3137902002494,126.462201579296));
#42384=CARTESIAN_POINT('Ctrl Pts',(114.581125063963,2.19107726805885,126.401138675863));
#42385=CARTESIAN_POINT('Ctrl Pts',(114.573364621449,2.06829884028149,126.34004318132));
#42386=CARTESIAN_POINT('Ctrl Pts',(114.565604178935,1.94306052799632,126.284135302421));
#42387=CARTESIAN_POINT('Ctrl Pts',(114.557843736421,1.81584489124477,126.233595868266));
#42388=CARTESIAN_POINT('Ctrl Pts',(114.550070836155,1.68842503665952,126.182975303726));
#42389=CARTESIAN_POINT('Ctrl Pts',(114.54229793589,1.55902188386952,126.137740534335));
#42390=CARTESIAN_POINT('Ctrl Pts',(114.534525035624,1.42813389250766,126.098022694343));
#42391=CARTESIAN_POINT('Ctrl Pts',(114.527034699862,1.30200400931841,126.059748697877));
#42392=CARTESIAN_POINT('Ctrl Pts',(114.5195443641,1.17449566664806,126.026597563588));
#42393=CARTESIAN_POINT('Ctrl Pts',(114.512054028338,1.04606180034561,125.998641340251));
#42394=CARTESIAN_POINT('Ctrl Pts',(114.504279694219,0.912758324965945,125.969625148209));
#42395=CARTESIAN_POINT('Ctrl Pts',(114.4965053601,0.778035492732118,125.946113658947));
#42396=CARTESIAN_POINT('Ctrl Pts',(114.488731025981,0.64238770263931,125.928243196708));
#42397=CARTESIAN_POINT('Ctrl Pts',(114.480966273034,0.506907086324599,125.910394758216));
#42398=CARTESIAN_POINT('Ctrl Pts',(114.473201520087,0.37050416416255,125.89817356479));
#42399=CARTESIAN_POINT('Ctrl Pts',(114.46543676714,0.233685619905608,125.891665421083));
#42400=CARTESIAN_POINT('Ctrl Pts',(114.457679726255,0.0970029657557192,
125.885163741355));
#42401=CARTESIAN_POINT('Ctrl Pts',(114.44992268537,-0.0400941009984268,
125.884363837726));
#42402=CARTESIAN_POINT('Ctrl Pts',(114.442165644485,-0.177091995100775,
125.889299937598));
#42403=CARTESIAN_POINT('Ctrl Pts',(114.434414453245,-0.313986578025586,
125.894232315118));
#42404=CARTESIAN_POINT('Ctrl Pts',(114.426663262005,-0.45078174802656,125.904892072344));
#42405=CARTESIAN_POINT('Ctrl Pts',(114.418912070764,-0.586962484692938,
125.921261386129));
#42406=CARTESIAN_POINT('Ctrl Pts',(114.411164173987,-0.723085340913494,
125.937623742518));
#42407=CARTESIAN_POINT('Ctrl Pts',(114.40341627721,-0.858593895849701,125.959690782356));
#42408=CARTESIAN_POINT('Ctrl Pts',(114.395668380433,-0.992977041873242,
125.9873927272));
#42409=CARTESIAN_POINT('Ctrl Pts',(114.387922104349,-1.1273320778396,126.015088877395));
#42410=CARTESIAN_POINT('Ctrl Pts',(114.380175828265,-1.26056179046783,126.048417509212));
#42411=CARTESIAN_POINT('Ctrl Pts',(114.372429552181,-1.39216446762645,126.0872575704));
#42412=CARTESIAN_POINT('Ctrl Pts',(114.364683218916,-1.52376811624605,126.126097918298));
#42413=CARTESIAN_POINT('Ctrl Pts',(114.35693688565,-1.65374433045467,126.170449666082));
#42414=CARTESIAN_POINT('Ctrl Pts',(114.349190552385,-1.78160616968763,126.220141761683));
#42415=CARTESIAN_POINT('Ctrl Pts',(114.341442484382,-1.90949664269312,126.269844985485));
#42416=CARTESIAN_POINT('Ctrl Pts',(114.333694416379,-2.03527143417113,126.324890795277));
#42417=CARTESIAN_POINT('Ctrl Pts',(114.325946348376,-2.1584635808476,126.38505999047));
#42418=CARTESIAN_POINT('Ctrl Pts',(114.318190045634,-2.28178665760349,126.445293134199));
#42419=CARTESIAN_POINT('Ctrl Pts',(114.310433742892,-2.40252125453057,126.510660368837));
#42420=CARTESIAN_POINT('Ctrl Pts',(114.30267744015,-2.52022454185894,126.580896243251));
#42421=CARTESIAN_POINT('Ctrl Pts',(114.294916997636,-2.63799065097566,126.651169604664));
#42422=CARTESIAN_POINT('Ctrl Pts',(114.287156555122,-2.7527218997929,126.726316569552));
#42423=CARTESIAN_POINT('Ctrl Pts',(114.279396112608,-2.86400531617679,126.806028889031));
#42424=CARTESIAN_POINT('Ctrl Pts',(114.271623212343,-2.97546737458009,126.885869169801));
#42425=CARTESIAN_POINT('Ctrl Pts',(114.263850312077,-3.08347023211437,126.970289209355));
#42426=CARTESIAN_POINT('Ctrl Pts',(114.256077411812,-3.187634132216,127.05894052075));
#42427=CARTESIAN_POINT('Ctrl Pts',(114.24858707605,-3.28801141217507,127.144369133676));
#42428=CARTESIAN_POINT('Ctrl Pts',(114.241096740288,-3.38482377411824,127.233726515743));
#42429=CARTESIAN_POINT('Ctrl Pts',(114.233606404526,-3.47776577847991,127.326670543316));
#42430=CARTESIAN_POINT('Ctrl Pts',(114.225941058105,-3.57287935991102,127.421786195231));
#42431=CARTESIAN_POINT('Ctrl Pts',(114.218275711685,-3.66425891122612,127.520977943977));
#42432=CARTESIAN_POINT('Ctrl Pts',(114.210610365264,-3.75152731893948,127.62391633449));
#42433=CARTESIAN_POINT('Ctrl Pts',(114.202953988676,-3.83869360693815,127.726734268594));
#42434=CARTESIAN_POINT('Ctrl Pts',(114.195297612088,-3.921758057678,127.833289824629));
#42435=CARTESIAN_POINT('Ctrl Pts',(114.1876412355,-4.00037885486759,127.943215378326));
#42436=CARTESIAN_POINT('Ctrl Pts',(114.179992048955,-4.07892581988254,128.053037701796));
#42437=CARTESIAN_POINT('Ctrl Pts',(114.172342862411,-4.1530371968604,128.166223404336));
#42438=CARTESIAN_POINT('Ctrl Pts',(114.164693675866,-4.22241045974782,128.282370734178));
#42439=CARTESIAN_POINT('Ctrl Pts',(114.157050220695,-4.29173174271236,128.398431037274));
#42440=CARTESIAN_POINT('Ctrl Pts',(114.149406765524,-4.35632177014896,128.517448207599));
#42441=CARTESIAN_POINT('Ctrl Pts',(114.141763310354,-4.41592085388093,128.638990885913));
#42442=CARTESIAN_POINT('Ctrl Pts',(114.134123186136,-4.47549396483498,128.760480596953));
#42443=CARTESIAN_POINT('Ctrl Pts',(114.126483061919,-4.53008028209918,128.884493265514));
#42444=CARTESIAN_POINT('Ctrl Pts',(114.118842937702,-4.57946588518187,129.010572651012));
#42445=CARTESIAN_POINT('Ctrl Pts',(114.111203491232,-4.62884710732094,129.136640852143));
#42446=CARTESIAN_POINT('Ctrl Pts',(114.103564044761,-4.67302838144765,129.264775032536));
#42447=CARTESIAN_POINT('Ctrl Pts',(114.095924598291,-4.71184394696733,129.394499035024));
#42448=CARTESIAN_POINT('Ctrl Pts',(114.092254861374,-4.73048965831579,129.456814146835));
#42449=CARTESIAN_POINT('Ctrl Pts',(114.088585124457,-4.74789794643968,129.519495852102));
#42450=CARTESIAN_POINT('Ctrl Pts',(114.08491538754,-4.76405452823405,129.582490119308));
#42451=CARTESIAN_POINT('Ctrl Pts',(115.834581344104,-4.76405452823405,129.582490119308));
#42452=CARTESIAN_POINT('Ctrl Pts',(115.826451019897,-4.7997288353145,129.721583701182));
#42453=CARTESIAN_POINT('Ctrl Pts',(115.81832069569,-4.82934431273923,129.862384632814));
#42454=CARTESIAN_POINT('Ctrl Pts',(115.810190371483,-4.85274845500096,130.004350933258));
#42455=CARTESIAN_POINT('Ctrl Pts',(115.802074958176,-4.87610967439746,130.14605686952));
#42456=CARTESIAN_POINT('Ctrl Pts',(115.793959544868,-4.89328222023574,130.288923585756));
#42457=CARTESIAN_POINT('Ctrl Pts',(115.78584413156,-4.9041641939585,130.432397418855));
#42458=CARTESIAN_POINT('Ctrl Pts',(115.778849233037,-4.91354366719489,130.556061472082));
#42459=CARTESIAN_POINT('Ctrl Pts',(115.771854334514,-4.91825051724227,130.680176209359));
#42460=CARTESIAN_POINT('Ctrl Pts',(115.764859435991,-4.91824999995734,130.804381100951));
#42461=CARTESIAN_POINT('',(116.110140563973,-4.91824810509851,130.800043304177));
#42462=CARTESIAN_POINT('Ctrl Pts',(116.180155138321,-4.76405452823404,129.582490119308));
#42463=CARTESIAN_POINT('Ctrl Pts',(116.174487017233,-4.78881862777827,129.679044967583));
#42464=CARTESIAN_POINT('Ctrl Pts',(116.168818896145,-4.8106211484576,129.77625532962));
#42465=CARTESIAN_POINT('Ctrl Pts',(116.163150775057,-4.82943794779455,129.873924069003));
#42466=CARTESIAN_POINT('Ctrl Pts',(116.151699131444,-4.86745465149391,130.071250057303));
#42467=CARTESIAN_POINT('Ctrl Pts',(116.140247487831,-4.89338666919524,130.270973357238));
#42468=CARTESIAN_POINT('Ctrl Pts',(116.128795844218,-4.90699959386499,130.471887989657));
#42469=CARTESIAN_POINT('Ctrl Pts',(116.122577417482,-4.91439163099023,130.580987867742));
#42470=CARTESIAN_POINT('Ctrl Pts',(116.116358990745,-4.91815189245368,130.690438661909));
#42471=CARTESIAN_POINT('Ctrl Pts',(116.110140564008,-4.91824810509796,130.800043303551));
#42472=CARTESIAN_POINT('Ctrl Pts',(116.110140563973,-4.91824810509851,130.800043304177));
#42473=CARTESIAN_POINT('Ctrl Pts',(116.102493663682,-4.9183664193317,130.934825911027));
#42474=CARTESIAN_POINT('Ctrl Pts',(116.094846763391,-4.91294007719472,131.069795177394));
#42475=CARTESIAN_POINT('Ctrl Pts',(116.0871998631,-4.90194978904778,131.204449767824));
#42476=CARTESIAN_POINT('Ctrl Pts',(116.079559620593,-4.89096906960994,131.338987121055));
#42477=CARTESIAN_POINT('Ctrl Pts',(116.071919378086,-4.87443407244818,131.473209943396));
#42478=CARTESIAN_POINT('Ctrl Pts',(116.064279135579,-4.85237756615036,131.606616822292));
#42479=CARTESIAN_POINT('Ctrl Pts',(116.056643173303,-4.8303334163909,131.739948963729));
#42480=CARTESIAN_POINT('Ctrl Pts',(116.049007211028,-4.80277397434707,131.872465673803));
#42481=CARTESIAN_POINT('Ctrl Pts',(116.041371248752,-4.76978380949576,132.003671033252));
#42482=CARTESIAN_POINT('Ctrl Pts',(116.033737459343,-4.7368030322277,132.134839057293));
#42483=CARTESIAN_POINT('Ctrl Pts',(116.026103669934,-4.6983947023943,132.264696081564));
#42484=CARTESIAN_POINT('Ctrl Pts',(116.018469880525,-4.65469432108969,132.392757243008));
#42485=CARTESIAN_POINT('Ctrl Pts',(116.010836497449,-4.61099626587797,132.520811587986));
#42486=CARTESIAN_POINT('Ctrl Pts',(116.003203114373,-4.56200684971436,132.647069878375));
#42487=CARTESIAN_POINT('Ctrl Pts',(115.995569731297,-4.50791100562389,132.771063805105));
#42488=CARTESIAN_POINT('Ctrl Pts',(115.987934988556,-4.45380552593009,132.89507981775));
#42489=CARTESIAN_POINT('Ctrl Pts',(115.980300245814,-4.39459197150539,133.016830295155));
#42490=CARTESIAN_POINT('Ctrl Pts',(115.972665503073,-4.33050259955188,133.135868777057));
#42491=CARTESIAN_POINT('Ctrl Pts',(115.96502306968,-4.26634866891172,133.255027169138));
#42492=CARTESIAN_POINT('Ctrl Pts',(115.957380636288,-4.19730930403953,133.371467754463));
#42493=CARTESIAN_POINT('Ctrl Pts',(115.949738202896,-4.12366190715808,133.484770201557));
#42494=CARTESIAN_POINT('Ctrl Pts',(115.942091798843,-4.04997624643288,133.598131515459));
#42495=CARTESIAN_POINT('Ctrl Pts',(115.934445394789,-3.97167802053146,133.708351116492));
#42496=CARTESIAN_POINT('Ctrl Pts',(115.926798990736,-3.88908601119759,133.815040451093));
#42497=CARTESIAN_POINT('Ctrl Pts',(115.919140753492,-3.80636618662677,133.921894892739));
#42498=CARTESIAN_POINT('Ctrl Pts',(115.911482516249,-3.71933956651517,134.025207847914));
#42499=CARTESIAN_POINT('Ctrl Pts',(115.903824279005,-3.62836339690442,134.124625986856));
#42500=CARTESIAN_POINT('Ctrl Pts',(115.897450569751,-3.55264680107667,134.207368567428));
#42501=CARTESIAN_POINT('Ctrl Pts',(115.891076860498,-3.47419521953665,134.287413918513));
#42502=CARTESIAN_POINT('Ctrl Pts',(115.884703151244,-3.39323179600188,134.364579858161));
#42503=CARTESIAN_POINT('Ctrl Pts',(115.876928817125,-3.29447663147852,134.458703040368));
#42504=CARTESIAN_POINT('Ctrl Pts',(115.869154483006,-3.19164582316973,134.548863211813));
#42505=CARTESIAN_POINT('Ctrl Pts',(115.861380148886,-3.08509070302833,134.634686767725));
#42506=CARTESIAN_POINT('Ctrl Pts',(115.853615395939,-2.97866690254939,134.720404553774));
#42507=CARTESIAN_POINT('Ctrl Pts',(115.845850642992,-2.8685282242941,134.801796115346));
#42508=CARTESIAN_POINT('Ctrl Pts',(115.838085890045,-2.75506277134103,134.878524604014));
#42509=CARTESIAN_POINT('Ctrl Pts',(115.83032884916,-2.64171001387542,134.955176884865));
#42510=CARTESIAN_POINT('Ctrl Pts',(115.822571808275,-2.52503737898898,135.027175091975));
#42511=CARTESIAN_POINT('Ctrl Pts',(115.81481476739,-2.40546569345085,135.094222836814));
#42512=CARTESIAN_POINT('Ctrl Pts',(115.80706357615,-2.28598417785108,135.161220020427));
#42513=CARTESIAN_POINT('Ctrl Pts',(115.79931238491,-2.16360830272458,135.223273981998));
#42514=CARTESIAN_POINT('Ctrl Pts',(115.79156119367,-2.03878719615887,135.280132040603));
#42515=CARTESIAN_POINT('Ctrl Pts',(115.783813296893,-1.91401914189283,135.336965933018));
#42516=CARTESIAN_POINT('Ctrl Pts',(115.776065400116,-1.78680827829982,135.388608153071));
#42517=CARTESIAN_POINT('Ctrl Pts',(115.768317503339,-1.65762741779125,135.434852427977));
#42518=CARTESIAN_POINT('Ctrl Pts',(115.760571227254,-1.52847357913397,135.481087029578));
#42519=CARTESIAN_POINT('Ctrl Pts',(115.75282495117,-1.39735093106992,135.521925800256));
#42520=CARTESIAN_POINT('Ctrl Pts',(115.745078675086,-1.26475093328867,135.557211145328));
#42521=CARTESIAN_POINT('Ctrl Pts',(115.737332341821,-1.13214995668436,135.592496750868));
#42522=CARTESIAN_POINT('Ctrl Pts',(115.729586008556,-0.998071986418951,
135.622228748464));
#42523=CARTESIAN_POINT('Ctrl Pts',(115.72183967529,-0.863021875286548,135.646299929998));
#42524=CARTESIAN_POINT('Ctrl Pts',(115.714091607287,-0.727941520618037,
135.670376502107));
#42525=CARTESIAN_POINT('Ctrl Pts',(115.706343539284,-0.59188897670176,135.688789666985));
#42526=CARTESIAN_POINT('Ctrl Pts',(115.698595471281,-0.455377080442616,
135.701483729875));
#42527=CARTESIAN_POINT('Ctrl Pts',(115.690839168539,-0.318720097715708,
135.714191284165));
#42528=CARTESIAN_POINT('Ctrl Pts',(115.683082865798,-0.18160317731009,135.721167558091));
#42529=CARTESIAN_POINT('Ctrl Pts',(115.675326563056,-0.0445426033115799,
135.722408911248));
#42530=CARTESIAN_POINT('Ctrl Pts',(115.667566120542,0.092591124042088,135.723650926953));
#42531=CARTESIAN_POINT('Ctrl Pts',(115.659805678027,0.229668054500501,135.719151935606));
#42532=CARTESIAN_POINT('Ctrl Pts',(115.652045235513,0.366175141605675,135.708960379847));
#42533=CARTESIAN_POINT('Ctrl Pts',(115.644272335248,0.502901362005599,135.698752463699));
#42534=CARTESIAN_POINT('Ctrl Pts',(115.636499434982,0.639055522520417,135.682833767511));
#42535=CARTESIAN_POINT('Ctrl Pts',(115.628726534717,0.774132013685305,135.661304377575));
#42536=CARTESIAN_POINT('Ctrl Pts',(115.621236198955,0.904298134159657,135.640557635192));
#42537=CARTESIAN_POINT('Ctrl Pts',(115.613745863193,1.03346327498792,135.614601103258));
#42538=CARTESIAN_POINT('Ctrl Pts',(115.606255527431,1.16118860772819,135.583568091592));
#42539=CARTESIAN_POINT('Ctrl Pts',(115.598481193312,1.29375668528011,135.551358453856));
#42540=CARTESIAN_POINT('Ctrl Pts',(115.590706859193,1.42519355465844,135.513577757456));
#42541=CARTESIAN_POINT('Ctrl Pts',(115.582932525074,1.55499498808643,135.470319645411));
#42542=CARTESIAN_POINT('Ctrl Pts',(115.575167772127,1.68463645284814,135.427114845122));
#42543=CARTESIAN_POINT('Ctrl Pts',(115.56740301918,1.81264612461156,135.378446182946));
#42544=CARTESIAN_POINT('Ctrl Pts',(115.559638266232,1.93853082406011,135.32445810619));
#42545=CARTESIAN_POINT('Ctrl Pts',(115.551881225347,2.06429049305043,135.270523651154));
#42546=CARTESIAN_POINT('Ctrl Pts',(115.544124184462,2.18792903283064,135.21128044868));
#42547=CARTESIAN_POINT('Ctrl Pts',(115.536367143578,2.30896961618832,135.146922347009));
#42548=CARTESIAN_POINT('Ctrl Pts',(115.528615952337,2.42991892190044,135.082612778282));
#42549=CARTESIAN_POINT('Ctrl Pts',(115.520864761097,2.54827382693229,135.013196170655));
#42550=CARTESIAN_POINT('Ctrl Pts',(115.513113569857,2.66357897896477,134.938913808095));
#42551=CARTESIAN_POINT('Ctrl Pts',(115.50536567308,2.77883512323209,134.864663017521));
#42552=CARTESIAN_POINT('Ctrl Pts',(115.497617776303,2.89104376461658,134.785550796552));
#42553=CARTESIAN_POINT('Ctrl Pts',(115.489869879526,2.99977579332402,134.70186344018));
#42554=CARTESIAN_POINT('Ctrl Pts',(115.482123603442,3.1084850776352,134.6181935894));
#42555=CARTESIAN_POINT('Ctrl Pts',(115.474377327358,3.21371888614757,134.52995074509));
#42556=CARTESIAN_POINT('Ctrl Pts',(115.466631051274,3.31507898402545,134.437463202434));
#42557=CARTESIAN_POINT('Ctrl Pts',(115.458884718008,3.41643983012026,134.344974977055));
#42558=CARTESIAN_POINT('Ctrl Pts',(115.451138384743,3.51392661971633,134.248242254331));
#42559=CARTESIAN_POINT('Ctrl Pts',(115.443392051478,3.60717627032161,134.147631832608));
#42560=CARTESIAN_POINT('Ctrl Pts',(115.435643983475,3.70044680353997,134.046998879878));
#42561=CARTESIAN_POINT('Ctrl Pts',(115.427895915472,3.78947804389538,133.942486786857));
#42562=CARTESIAN_POINT('Ctrl Pts',(115.420147847469,3.87394593293532,133.834496913377));
#42563=CARTESIAN_POINT('Ctrl Pts',(115.412391544727,3.95850359545262,133.726392266976));
#42564=CARTESIAN_POINT('Ctrl Pts',(115.404635241985,4.03848797703091,133.614802764948));
#42565=CARTESIAN_POINT('Ctrl Pts',(115.396878939243,4.11361695073589,133.500160803989));
#42566=CARTESIAN_POINT('Ctrl Pts',(115.389118496729,4.18878602303633,133.385457655164));
#42567=CARTESIAN_POINT('Ctrl Pts',(115.381358054215,4.2590943234009,133.267699136632));
#42568=CARTESIAN_POINT('Ctrl Pts',(115.373597611701,4.32430529385268,133.147343073338));
#42569=CARTESIAN_POINT('Ctrl Pts',(115.365824711435,4.38962094674335,133.026793803808));
#42570=CARTESIAN_POINT('Ctrl Pts',(115.35805181117,4.44982274630815,132.903639008355));
#42571=CARTESIAN_POINT('Ctrl Pts',(115.350278910904,4.50472160371224,132.778358169628));
#42572=CARTESIAN_POINT('Ctrl Pts',(115.342788575142,4.55762474936841,132.657631604951));
#42573=CARTESIAN_POINT('Ctrl Pts',(115.33529823938,4.60560369757696,132.534931174291));
#42574=CARTESIAN_POINT('Ctrl Pts',(115.327807903618,4.64853340817278,132.410698133657));
#42575=CARTESIAN_POINT('Ctrl Pts',(115.320033569499,4.69309081179363,132.281754759529));
#42576=CARTESIAN_POINT('Ctrl Pts',(115.31225923538,4.73234968033078,132.150751809587));
#42577=CARTESIAN_POINT('Ctrl Pts',(115.304484901261,4.76611625087749,132.018164121277));
#42578=CARTESIAN_POINT('Ctrl Pts',(115.296720148314,4.79984120714382,131.885739835444));
#42579=CARTESIAN_POINT('Ctrl Pts',(115.288955395367,4.8280872376851,131.751735072462));
#42580=CARTESIAN_POINT('Ctrl Pts',(115.281190642419,4.85070929464554,131.616642835357));
#42581=CARTESIAN_POINT('Ctrl Pts',(115.273433601534,4.87330888306012,131.481684773766));
#42582=CARTESIAN_POINT('Ctrl Pts',(115.265676560649,4.89029554975478,131.34564177059));
#42583=CARTESIAN_POINT('Ctrl Pts',(115.257919519764,4.9015746479877,131.209019773776));
#42584=CARTESIAN_POINT('Ctrl Pts',(115.250168328524,4.91284524056479,131.072500804673));
#42585=CARTESIAN_POINT('Ctrl Pts',(115.242417137284,4.91841679973631,130.935404099068));
#42586=CARTESIAN_POINT('Ctrl Pts',(115.234665946044,4.91824619548765,130.798243177641));
#42587=CARTESIAN_POINT('Ctrl Pts',(115.226918049267,4.91807566375034,130.661140553263));
#42588=CARTESIAN_POINT('Ctrl Pts',(115.21917015249,4.91216782319093,130.523974157495));
#42589=CARTESIAN_POINT('Ctrl Pts',(115.211422255713,4.90053159757012,130.387259761996));
#42590=CARTESIAN_POINT('Ctrl Pts',(115.203675979629,4.88889780599686,130.250573964202));
#42591=CARTESIAN_POINT('Ctrl Pts',(115.195929703545,4.87153804589188,130.114340367924));
#42592=CARTESIAN_POINT('Ctrl Pts',(115.188183427461,4.84851326563254,129.979071470972));
#42593=CARTESIAN_POINT('Ctrl Pts',(115.180437094195,4.82548831540953,129.843801575497));
#42594=CARTESIAN_POINT('Ctrl Pts',(115.17269076093,4.79679832719209,129.709496778979));
#42595=CARTESIAN_POINT('Ctrl Pts',(115.164944427664,4.76255564386286,129.57666081647));
#42596=CARTESIAN_POINT('Ctrl Pts',(115.157196359661,4.7283052921221,129.443795106269));
#42597=CARTESIAN_POINT('Ctrl Pts',(115.149448291659,4.68849986844778,129.312399263134));
#42598=CARTESIAN_POINT('Ctrl Pts',(115.141700223656,4.64330188672649,129.182962871415));
#42599=CARTESIAN_POINT('Ctrl Pts',(115.133943920914,4.5980558680523,129.053388913159));
#42600=CARTESIAN_POINT('Ctrl Pts',(115.126187618172,4.54740597158711,128.92577893609));
#42601=CARTESIAN_POINT('Ctrl Pts',(115.11843131543,4.4915634884181,128.800604022565));
#42602=CARTESIAN_POINT('Ctrl Pts',(115.110670872916,4.43569120043451,128.67536229942));
#42603=CARTESIAN_POINT('Ctrl Pts',(115.102910430402,4.3746209774216,128.55255857941));
#42604=CARTESIAN_POINT('Ctrl Pts',(115.095149987887,4.3086101351078,128.432639351028));
#42605=CARTESIAN_POINT('Ctrl Pts',(115.087377087622,4.24249332632962,128.312527617655));
#42606=CARTESIAN_POINT('Ctrl Pts',(115.079604187357,4.17142025216563,128.195309963512));
#42607=CARTESIAN_POINT('Ctrl Pts',(115.071831287091,4.0956921078127,128.081404646475));
#42608=CARTESIAN_POINT('Ctrl Pts',(115.064340951329,4.02271687225504,127.971640074623));
#42609=CARTESIAN_POINT('Ctrl Pts',(115.056850615567,3.94541931834231,127.864951446765));
#42610=CARTESIAN_POINT('Ctrl Pts',(115.049360279805,3.86410309998936,127.761682472387));
#42611=CARTESIAN_POINT('Ctrl Pts',(115.041585945686,3.77970375250179,127.654498023456));
#42612=CARTESIAN_POINT('Ctrl Pts',(115.033811611567,3.69070763791452,127.550658131118));
#42613=CARTESIAN_POINT('Ctrl Pts',(115.026037277448,3.59740951683628,127.450582474833));
#42614=CARTESIAN_POINT('Ctrl Pts',(115.018272524501,3.5042263773541,127.35063015285));
#42615=CARTESIAN_POINT('Ctrl Pts',(115.010507771554,3.40675204450105,127.254433119747));
#42616=CARTESIAN_POINT('Ctrl Pts',(115.002743018607,3.30532289377565,127.162379888569));
#42617=CARTESIAN_POINT('Ctrl Pts',(114.994985977722,3.20399448391265,127.070418085959));
#42618=CARTESIAN_POINT('Ctrl Pts',(114.987228936837,3.09871936067409,126.98259215593));
#42619=CARTESIAN_POINT('Ctrl Pts',(114.979471895952,2.98987203352079,126.89925520469));
#42620=CARTESIAN_POINT('Ctrl Pts',(114.971720704712,2.88110678898383,126.815981098494));
#42621=CARTESIAN_POINT('Ctrl Pts',(114.963969513471,2.76877501160242,126.737189469815));
#42622=CARTESIAN_POINT('Ctrl Pts',(114.956218322231,2.65328542804283,126.663194175628));
#42623=CARTESIAN_POINT('Ctrl Pts',(114.948470425454,2.53784493063656,126.589230331414));
#42624=CARTESIAN_POINT('Ctrl Pts',(114.940722528677,2.41924962499331,126.520058977607));
#42625=CARTESIAN_POINT('Ctrl Pts',(114.9329746319,2.29793826792855,126.455951393575));
#42626=CARTESIAN_POINT('Ctrl Pts',(114.925228355816,2.1766522865846,126.391857219467));
#42627=CARTESIAN_POINT('Ctrl Pts',(114.917482079732,2.05265172932757,126.332824890819));
#42628=CARTESIAN_POINT('Ctrl Pts',(114.909735803648,1.92640071916654,126.279080147618));
#42629=CARTESIAN_POINT('Ctrl Pts',(114.901989470382,1.80014877704923,126.225335007685));
#42630=CARTESIAN_POINT('Ctrl Pts',(114.894243137117,1.67164670860619,126.176877684221));
#42631=CARTESIAN_POINT('Ctrl Pts',(114.886496803852,1.54137904447387,126.133885941074));
#42632=CARTESIAN_POINT('Ctrl Pts',(114.878748735849,1.41108220780182,126.090884570224));
#42633=CARTESIAN_POINT('Ctrl Pts',(114.871000667846,1.27901935985217,126.053351337773));
#42634=CARTESIAN_POINT('Ctrl Pts',(114.863252599843,1.1456902445281,126.021414148485));
#42635=CARTESIAN_POINT('Ctrl Pts',(114.855496297101,1.01221942543308,125.989443015972));
#42636=CARTESIAN_POINT('Ctrl Pts',(114.847739994359,0.877480031390909,125.963079898695));
#42637=CARTESIAN_POINT('Ctrl Pts',(114.839983691617,0.74198260532327,125.942401662999));
#42638=CARTESIAN_POINT('Ctrl Pts',(114.832223249103,0.60641286019959,125.921712390705));
#42639=CARTESIAN_POINT('Ctrl Pts',(114.824462806589,0.470084665311837,125.906714088612));
#42640=CARTESIAN_POINT('Ctrl Pts',(114.816702364075,0.333512749509917,125.897431607644));
#42641=CARTESIAN_POINT('Ctrl Pts',(114.808929463809,0.196721596344467,125.888134225614));
#42642=CARTESIAN_POINT('Ctrl Pts',(114.801156563544,0.0596863314958162,
125.884571010537));
#42643=CARTESIAN_POINT('Ctrl Pts',(114.793383663279,-0.0770783494791731,
125.886714636963));
#42644=CARTESIAN_POINT('Ctrl Pts',(114.785893327516,-0.208871289813787,
125.888780337169));
#42645=CARTESIAN_POINT('Ctrl Pts',(114.778402991754,-0.340412669999736,
125.896145149085));
#42646=CARTESIAN_POINT('Ctrl Pts',(114.770912655992,-0.471249185155597,
125.908739383444));
#42647=CARTESIAN_POINT('Ctrl Pts',(114.763138321873,-0.607046406547911,
125.921811132026));
#42648=CARTESIAN_POINT('Ctrl Pts',(114.755363987754,-0.742514422655864,
125.94055808549));
#42649=CARTESIAN_POINT('Ctrl Pts',(114.747589653635,-0.877140819954839,
125.964959100388));
#42650=CARTESIAN_POINT('Ctrl Pts',(114.739824900688,-1.01160130225087,125.989330043215));
#42651=CARTESIAN_POINT('Ctrl Pts',(114.732060147741,-1.14522184849222,126.019341113925));
#42652=CARTESIAN_POINT('Ctrl Pts',(114.724295394794,-1.27749377247639,126.054919311077));
#42653=CARTESIAN_POINT('Ctrl Pts',(114.716538353909,-1.4096343221214,126.090462171462));
#42654=CARTESIAN_POINT('Ctrl Pts',(114.708781313024,-1.54042854001318,126.131561053741));
#42655=CARTESIAN_POINT('Ctrl Pts',(114.701024272139,-1.66937691638695,126.178091735029));
#42656=CARTESIAN_POINT('Ctrl Pts',(114.693273080898,-1.79822805178685,126.224587327167));
#42657=CARTESIAN_POINT('Ctrl Pts',(114.685521889658,-1.92523575002078,126.276506432986));
#42658=CARTESIAN_POINT('Ctrl Pts',(114.677770698418,-2.04991502758049,126.333674826527));
#42659=CARTESIAN_POINT('Ctrl Pts',(114.670022801641,-2.17454131312105,126.390818921975));
#42660=CARTESIAN_POINT('Ctrl Pts',(114.662274904864,-2.29684079166465,126.453207705069));
#42661=CARTESIAN_POINT('Ctrl Pts',(114.654527008087,-2.41634806941997,126.5206186704));
#42662=CARTESIAN_POINT('Ctrl Pts',(114.646780732003,-2.5358303488293,126.58801553481));
#42663=CARTESIAN_POINT('Ctrl Pts',(114.639034455919,-2.65252124888335,126.660432299929));
#42664=CARTESIAN_POINT('Ctrl Pts',(114.631288179835,-2.765979978313,126.737600503904));
#42665=CARTESIAN_POINT('Ctrl Pts',(114.623541846569,-2.87943954526891,126.814769277517));
#42666=CARTESIAN_POINT('Ctrl Pts',(114.615795513304,-2.98966657071328,126.896689340097));
#42667=CARTESIAN_POINT('Ctrl Pts',(114.608049180039,-3.09624959624012,126.983049128001));
#42668=CARTESIAN_POINT('Ctrl Pts',(114.600301112036,-3.20285649029659,127.06942825558));
#42669=CARTESIAN_POINT('Ctrl Pts',(114.592553044033,-3.30581745688504,127.160248840835));
#42670=CARTESIAN_POINT('Ctrl Pts',(114.58480497603,-3.40475476231889,127.255159570715));
#42671=CARTESIAN_POINT('Ctrl Pts',(114.577048673288,-3.50379721949826,127.350171172848));
#42672=CARTESIAN_POINT('Ctrl Pts',(114.569292370546,-3.59880719037784,127.449281332231));
#42673=CARTESIAN_POINT('Ctrl Pts',(114.561536067804,-3.68944404420507,127.55210206278));
#42674=CARTESIAN_POINT('Ctrl Pts',(114.55377562529,-3.78012927365021,127.654977671849));
#42675=CARTESIAN_POINT('Ctrl Pts',(114.546015182776,-3.86643648931334,127.761567494588));
#42676=CARTESIAN_POINT('Ctrl Pts',(114.538254740262,-3.94806655989022,127.871451907569));
#42677=CARTESIAN_POINT('Ctrl Pts',(114.530481839996,-4.02982767030333,127.981512716765));
#42678=CARTESIAN_POINT('Ctrl Pts',(114.522708939731,-4.10689641198569,128.094878361338));
#42679=CARTESIAN_POINT('Ctrl Pts',(114.514936039465,-4.17901756909294,128.211101043263));
#42680=CARTESIAN_POINT('Ctrl Pts',(114.507445703703,-4.248516940477,128.323098737953));
#42681=CARTESIAN_POINT('Ctrl Pts',(114.499955367941,-4.31342204469588,128.437749087283));
#42682=CARTESIAN_POINT('Ctrl Pts',(114.492465032179,-4.37354649094247,128.554633044266));
#42683=CARTESIAN_POINT('Ctrl Pts',(114.484192714557,-4.43994785558427,128.683719542903));
#42684=CARTESIAN_POINT('Ctrl Pts',(114.475920396934,-4.50070748873984,128.81589775137));
#42685=CARTESIAN_POINT('Ctrl Pts',(114.467648079312,-4.55554556162818,128.95066493099));
#42686=CARTESIAN_POINT('Ctrl Pts',(114.4593954003,-4.61025344808148,129.085112171237));
#42687=CARTESIAN_POINT('Ctrl Pts',(114.451142721288,-4.65906768654208,129.222135836395));
#42688=CARTESIAN_POINT('Ctrl Pts',(114.442890042275,-4.70175500412639,129.361210263766));
#42689=CARTESIAN_POINT('Ctrl Pts',(114.438545261957,-4.72422855689706,129.434428649447));
#42690=CARTESIAN_POINT('Ctrl Pts',(114.434200481639,-4.74500467371644,129.508215025666));
#42691=CARTESIAN_POINT('Ctrl Pts',(114.429855701321,-4.76405452823407,129.582490119308));
#42692=CARTESIAN_POINT('Origin',(213.235140564004,0.,130.804360617566));
#42693=CARTESIAN_POINT('',(112.334951030737,-4.76405452823405,129.582490119308));
#42694=CARTESIAN_POINT('',(112.680164151027,-4.76405452823403,129.582490119308));
#42695=CARTESIAN_POINT('',(213.235140564004,-4.76405452823405,129.582490119308));
#42696=CARTESIAN_POINT('',(114.014859436022,-4.91824795544417,130.808845176549));
#42697=CARTESIAN_POINT('Ctrl Pts',(114.014859435991,-4.91824795544367,130.808845177098));
#42698=CARTESIAN_POINT('Ctrl Pts',(114.004073030885,-4.9180744502827,130.999129506488));
#42699=CARTESIAN_POINT('Ctrl Pts',(113.993286625778,-4.90685453025112,131.188930927681));
#42700=CARTESIAN_POINT('Ctrl Pts',(113.982500220672,-4.88477617430655,131.377199852803));
#42701=CARTESIAN_POINT('Ctrl Pts',(113.973386407352,-4.86612139428455,131.536274894077));
#42702=CARTESIAN_POINT('Ctrl Pts',(113.964272594033,-4.83971544491623,131.694256767633));
#42703=CARTESIAN_POINT('Ctrl Pts',(113.955158780713,-4.80569650518746,131.850527030011));
#42704=CARTESIAN_POINT('Ctrl Pts',(113.947384446594,-4.77667741136257,131.983829873726));
#42705=CARTESIAN_POINT('Ctrl Pts',(113.939610112474,-4.74206171732388,132.116135525075));
#42706=CARTESIAN_POINT('Ctrl Pts',(113.931835778355,-4.70193093904607,132.24693765431));
#42707=CARTESIAN_POINT('Ctrl Pts',(113.924071025408,-4.66184961836592,132.377578581611));
#42708=CARTESIAN_POINT('Ctrl Pts',(113.916306272461,-4.61626685072272,132.50671930345));
#42709=CARTESIAN_POINT('Ctrl Pts',(113.908541519514,-4.56531520688374,132.633863316196));
#42710=CARTESIAN_POINT('Ctrl Pts',(113.900784478629,-4.51441416893574,132.760881047717));
#42711=CARTESIAN_POINT('Ctrl Pts',(113.893027437744,-4.45815501108632,132.88590565616));
#42712=CARTESIAN_POINT('Ctrl Pts',(113.885270396859,-4.39672008321279,133.008455799806));
#42713=CARTESIAN_POINT('Ctrl Pts',(113.877519205619,-4.33533148389617,133.130913527435));
#42714=CARTESIAN_POINT('Ctrl Pts',(113.869768014379,-4.26877505791689,133.250900156359));
#42715=CARTESIAN_POINT('Ctrl Pts',(113.862016823139,-4.19728109255979,133.36795467524));
#42716=CARTESIAN_POINT('Ctrl Pts',(113.854268926362,-4.12581751404513,133.484959442827));
#42717=CARTESIAN_POINT('Ctrl Pts',(113.846521029584,-4.04942077344058,133.599034246062));
#42718=CARTESIAN_POINT('Ctrl Pts',(113.838773132807,-3.96836678584156,133.709743228433));
#42719=CARTESIAN_POINT('Ctrl Pts',(113.831026856723,-3.88732975298949,133.820429052872));
#42720=CARTESIAN_POINT('Ctrl Pts',(113.823280580639,-3.80163764168207,133.927750141598));
#42721=CARTESIAN_POINT('Ctrl Pts',(113.815534304555,-3.71160909602127,134.03130049628));
#42722=CARTESIAN_POINT('Ctrl Pts',(113.80778797129,-3.62157988579013,134.134851615346));
#42723=CARTESIAN_POINT('Ctrl Pts',(113.800041638024,-3.52721443384914,134.23463164978));
#42724=CARTESIAN_POINT('Ctrl Pts',(113.792295304759,-3.42887071993867,134.330268819497));
#42725=CARTESIAN_POINT('Ctrl Pts',(113.784547236756,-3.33050498263553,134.425927406496));
#42726=CARTESIAN_POINT('Ctrl Pts',(113.776799168753,-3.22815949079723,134.517441010115));
#42727=CARTESIAN_POINT('Ctrl Pts',(113.76905110075,-3.12222771216706,134.604476033692));
#42728=CARTESIAN_POINT('Ctrl Pts',(113.761294798008,-3.01618334798175,134.691603559128));
#42729=CARTESIAN_POINT('Ctrl Pts',(113.753538495266,-2.90654538558959,134.774242747543));
#42730=CARTESIAN_POINT('Ctrl Pts',(113.745782192525,-2.79373932689858,134.85210117692));
#42731=CARTESIAN_POINT('Ctrl Pts',(113.73802175001,-2.68087306021744,134.930001161685));
#42732=CARTESIAN_POINT('Ctrl Pts',(113.730261307496,-2.56483565857648,135.003115094745));
#42733=CARTESIAN_POINT('Ctrl Pts',(113.722500864982,-2.44607913834008,135.07119549971));
#42734=CARTESIAN_POINT('Ctrl Pts',(113.714727964717,-2.32713197959469,135.139385193384));
#42735=CARTESIAN_POINT('Ctrl Pts',(113.706955064451,-2.20545732687521,135.202525031834));
#42736=CARTESIAN_POINT('Ctrl Pts',(113.699182164186,-2.08152998713914,135.260414474415));
#42737=CARTESIAN_POINT('Ctrl Pts',(113.691691828424,-1.96210771835727,135.316199489944));
#42738=CARTESIAN_POINT('Ctrl Pts',(113.684201492662,-1.84059398485557,135.367109093414));
#42739=CARTESIAN_POINT('Ctrl Pts',(113.6767111569,-1.71742691495417,135.41300769174));
#42740=CARTESIAN_POINT('Ctrl Pts',(113.668936822781,-1.58958992816093,135.460646549372));
#42741=CARTESIAN_POINT('Ctrl Pts',(113.661162488662,-1.45956680842768,135.503037821909));
#42742=CARTESIAN_POINT('Ctrl Pts',(113.653388154543,-1.32782760668504,135.539976407453));
#42743=CARTESIAN_POINT('Ctrl Pts',(113.645623401596,-1.19625076173477,135.576869469491));
#42744=CARTESIAN_POINT('Ctrl Pts',(113.637858648648,-1.06296241566424,135.608323110693));
#42745=CARTESIAN_POINT('Ctrl Pts',(113.630093895701,-0.928451948777212,
135.63418049426));
#42746=CARTESIAN_POINT('Ctrl Pts',(113.622336854816,-0.794075079582346,
135.66001219591));
#42747=CARTESIAN_POINT('Ctrl Pts',(113.614579813931,-0.658478886593955,
135.680258627828));
#42748=CARTESIAN_POINT('Ctrl Pts',(113.606822773046,-0.522166900797256,
135.694813029175));
#42749=CARTESIAN_POINT('Ctrl Pts',(113.599071581806,-0.385957708929306,
135.709356454934));
#42750=CARTESIAN_POINT('Ctrl Pts',(113.591320390566,-0.2490341858447,135.718216352552));
#42751=CARTESIAN_POINT('Ctrl Pts',(113.583569199326,-0.111908669341853,
135.721337281353));
#42752=CARTESIAN_POINT('Ctrl Pts',(113.575821302549,0.025158565158725,135.724456883676));
#42753=CARTESIAN_POINT('Ctrl Pts',(113.568073405772,0.162427232277614,135.721842359718));
#42754=CARTESIAN_POINT('Ctrl Pts',(113.560325508995,0.299381494738817,135.713490253572));
#42755=CARTESIAN_POINT('Ctrl Pts',(113.552579232911,0.436307109320613,135.705139894506));
#42756=CARTESIAN_POINT('Ctrl Pts',(113.544832956827,0.572918060065281,135.691054364256));
#42757=CARTESIAN_POINT('Ctrl Pts',(113.537086680742,0.708700534156355,135.671282295114));
#42758=CARTESIAN_POINT('Ctrl Pts',(113.529340347477,0.844484010562807,135.651510080019));
#42759=CARTESIAN_POINT('Ctrl Pts',(113.521594014212,0.979438611227399,135.626051298607));
#42760=CARTESIAN_POINT('Ctrl Pts',(113.513847680946,1.11305805024376,135.595006173155));
#42761=CARTESIAN_POINT('Ctrl Pts',(113.506099612943,1.24670741240704,135.563954095363));
#42762=CARTESIAN_POINT('Ctrl Pts',(113.49835154494,1.37902063719763,135.527313272605));
#42763=CARTESIAN_POINT('Ctrl Pts',(113.490603476938,1.5095043813704,135.485234423291));
#42764=CARTESIAN_POINT('Ctrl Pts',(113.482847174196,1.64012680521926,135.443110852076));
#42765=CARTESIAN_POINT('Ctrl Pts',(113.475090871454,1.76891549162545,135.39553782912));
#42766=CARTESIAN_POINT('Ctrl Pts',(113.467334568712,1.89539442348939,135.342715279986));
#42767=CARTESIAN_POINT('Ctrl Pts',(113.459574126198,2.02194086096757,135.289864537866));
#42768=CARTESIAN_POINT('Ctrl Pts',(113.451813683684,2.14617473350313,135.231758852242));
#42769=CARTESIAN_POINT('Ctrl Pts',(113.444053241169,2.26764350631388,135.168644750247));
#42770=CARTESIAN_POINT('Ctrl Pts',(113.436280340904,2.38930727158216,135.105429331893));
#42771=CARTESIAN_POINT('Ctrl Pts',(113.428507440639,2.50819672774641,135.037189625513));
#42772=CARTESIAN_POINT('Ctrl Pts',(113.420734540373,2.62388650952542,134.964216702532));
#42773=CARTESIAN_POINT('Ctrl Pts',(113.413244204611,2.73537067633226,134.893896529109));
#42774=CARTESIAN_POINT('Ctrl Pts',(113.405753868849,2.84388350866272,134.819181467877));
#42775=CARTESIAN_POINT('Ctrl Pts',(113.398263533087,2.94907410915593,134.740366837227));
#42776=CARTESIAN_POINT('Ctrl Pts',(113.390489198968,3.05825304323831,134.6585639259));
#42777=CARTESIAN_POINT('Ctrl Pts',(113.382714864849,3.16419869361358,134.572085311093));
#42778=CARTESIAN_POINT('Ctrl Pts',(113.37494053073,3.26648442823714,134.48121559738));
#42779=CARTESIAN_POINT('Ctrl Pts',(113.367175777783,3.36864410483431,134.390457872468));
#42780=CARTESIAN_POINT('Ctrl Pts',(113.359411024835,3.46715255079093,134.295320073365));
#42781=CARTESIAN_POINT('Ctrl Pts',(113.351646271888,3.5616132928583,134.196129155458));
#42782=CARTESIAN_POINT('Ctrl Pts',(113.343889231003,3.65598021518499,134.09703675537));
#42783=CARTESIAN_POINT('Ctrl Pts',(113.336132190118,3.74630716619833,133.993899528923));
#42784=CARTESIAN_POINT('Ctrl Pts',(113.328375149233,3.83223215418175,133.887083404155));
#42785=CARTESIAN_POINT('Ctrl Pts',(113.320623957993,3.91809234546334,133.780347830258));
#42786=CARTESIAN_POINT('Ctrl Pts',(113.312872766753,3.99955693702449,133.669939183488));
#42787=CARTESIAN_POINT('Ctrl Pts',(113.305121575513,4.07630235396087,133.556258541108));
#42788=CARTESIAN_POINT('Ctrl Pts',(113.297373678736,4.15301515204781,133.442626216033));
#42789=CARTESIAN_POINT('Ctrl Pts',(113.289625781959,4.22501254654578,133.325724984672));
#42790=CARTESIAN_POINT('Ctrl Pts',(113.281877885182,4.29201280725482,133.205986967534));
#42791=CARTESIAN_POINT('Ctrl Pts',(113.274131609098,4.35899905295368,133.086273997007));
#42792=CARTESIAN_POINT('Ctrl Pts',(113.266385333014,4.42099005321708,132.963725761965));
#42793=CARTESIAN_POINT('Ctrl Pts',(113.258639056929,4.47774899539122,132.838800834622));
#42794=CARTESIAN_POINT('Ctrl Pts',(113.250892723664,4.53450835654698,132.713874985111));
#42795=CARTESIAN_POINT('Ctrl Pts',(113.243146390399,4.5860354208231,132.58657276424));
#42796=CARTESIAN_POINT('Ctrl Pts',(113.235400057133,4.63214084816174,132.457374297271));
#42797=CARTESIAN_POINT('Ctrl Pts',(113.22765198913,4.67825660049113,132.328146897201));
#42798=CARTESIAN_POINT('Ctrl Pts',(113.219903921127,4.71894816851154,132.197022774176));
#42799=CARTESIAN_POINT('Ctrl Pts',(113.212155853124,4.75407569181712,132.064498458825));
#42800=CARTESIAN_POINT('Ctrl Pts',(113.204399550383,4.78924054907252,131.931833295055));
#42801=CARTESIAN_POINT('Ctrl Pts',(113.196643247641,4.8188294483625,131.797765344753));
#42802=CARTESIAN_POINT('Ctrl Pts',(113.188886944899,4.84275329385569,131.662803159237));
#42803=CARTESIAN_POINT('Ctrl Pts',(113.181126502385,4.86668990822556,131.527768940338));
#42804=CARTESIAN_POINT('Ctrl Pts',(113.173366059871,4.88495539195758,131.391839922498));
#42805=CARTESIAN_POINT('Ctrl Pts',(113.165605617356,4.89751254920902,131.255530089982));
#42806=CARTESIAN_POINT('Ctrl Pts',(113.157832717091,4.91008986432404,131.119001440822));
#42807=CARTESIAN_POINT('Ctrl Pts',(113.150059816826,4.91694052179098,130.982091146081));
#42808=CARTESIAN_POINT('Ctrl Pts',(113.14228691656,4.91807948791812,130.845314408832));
#42809=CARTESIAN_POINT('Ctrl Pts',(113.134796580798,4.91917704975766,130.713509850501));
#42810=CARTESIAN_POINT('Ctrl Pts',(113.127306245036,4.91497098915063,130.581829615806));
#42811=CARTESIAN_POINT('Ctrl Pts',(113.119815909274,4.90552009722783,130.450728551438));
#42812=CARTESIAN_POINT('Ctrl Pts',(113.112041575155,4.89571087186524,130.314656750367));
#42813=CARTESIAN_POINT('Ctrl Pts',(113.104267241036,4.88022017592059,130.178777870509));
#42814=CARTESIAN_POINT('Ctrl Pts',(113.096492906917,4.85905685024213,130.04360468521));
#42815=CARTESIAN_POINT('Ctrl Pts',(113.08872815397,4.83791960647114,129.908598088781));
#42816=CARTESIAN_POINT('Ctrl Pts',(113.080963401023,4.81112370288492,129.774295839008));
#42817=CARTESIAN_POINT('Ctrl Pts',(113.073198648075,4.77872991283661,129.641208227438));
#42818=CARTESIAN_POINT('Ctrl Pts',(113.06544160719,4.74636829675727,129.50825280036));
#42819=CARTESIAN_POINT('Ctrl Pts',(113.057684566305,4.70841995053111,129.376509988119));
#42820=CARTESIAN_POINT('Ctrl Pts',(113.04992752542,4.66499707441347,129.246482137641));
#42821=CARTESIAN_POINT('Ctrl Pts',(113.04217633418,4.62160694382445,129.116552342176));
#42822=CARTESIAN_POINT('Ctrl Pts',(113.03442514294,4.57275062398401,128.988335303638));
#42823=CARTESIAN_POINT('Ctrl Pts',(113.0266739517,4.51859065241145,128.862320046816));
#42824=CARTESIAN_POINT('Ctrl Pts',(113.018926054923,4.46445370027158,128.736358349839));
#42825=CARTESIAN_POINT('Ctrl Pts',(113.011178158146,4.40501773387347,128.612596931754));
#42826=CARTESIAN_POINT('Ctrl Pts',(113.003430261369,4.34049402638364,128.491506391847));
#42827=CARTESIAN_POINT('Ctrl Pts',(112.995683985285,4.27598381586244,128.37044118147));
#42828=CARTESIAN_POINT('Ctrl Pts',(112.987937709201,4.20638816483134,128.252046082824));
#42829=CARTESIAN_POINT('Ctrl Pts',(112.980191433116,4.1319648800591,128.136768202586));
#42830=CARTESIAN_POINT('Ctrl Pts',(112.972445099851,4.05754104591108,128.021489471393));
#42831=CARTESIAN_POINT('Ctrl Pts',(112.964698766586,3.97828971896613,127.909328332985));
#42832=CARTESIAN_POINT('Ctrl Pts',(112.95695243332,3.89451249927829,127.800703603947));
#42833=CARTESIAN_POINT('Ctrl Pts',(112.949204365317,3.81071651826298,127.692054549153));
#42834=CARTESIAN_POINT('Ctrl Pts',(112.941456297314,3.72239286639619,127.586943789153));
#42835=CARTESIAN_POINT('Ctrl Pts',(112.933708229311,3.6298836909918,127.485757379399));
#42836=CARTESIAN_POINT('Ctrl Pts',(112.92595192657,3.53727619573492,127.384463427525));
#42837=CARTESIAN_POINT('Ctrl Pts',(112.918195623828,3.4404745549594,127.287102446621));
#42838=CARTESIAN_POINT('Ctrl Pts',(112.910439321086,3.33985846881852,127.194024279943));
#42839=CARTESIAN_POINT('Ctrl Pts',(112.902678878572,3.2391886808429,127.100896434645));
#42840=CARTESIAN_POINT('Ctrl Pts',(112.894918436058,3.13470068854024,127.012056211482));
#42841=CARTESIAN_POINT('Ctrl Pts',(112.887157993543,3.02680681616963,126.927812725422));
#42842=CARTESIAN_POINT('Ctrl Pts',(112.879385093278,2.91873974297679,126.843434004239));
#42843=CARTESIAN_POINT('Ctrl Pts',(112.871612193013,2.80725618220763,126.763666993564));
#42844=CARTESIAN_POINT('Ctrl Pts',(112.863839292747,2.69279767845374,126.688777581663));
#42845=CARTESIAN_POINT('Ctrl Pts',(112.856348956985,2.58250002961489,126.61661058852));
#42846=CARTESIAN_POINT('Ctrl Pts',(112.848858621223,2.4694402402913,126.548972883109));
#42847=CARTESIAN_POINT('Ctrl Pts',(112.841368285461,2.35403276392831,126.486060858534));
#42848=CARTESIAN_POINT('Ctrl Pts',(112.833593951342,2.2342495780216,126.420763505426));
#42849=CARTESIAN_POINT('Ctrl Pts',(112.825819617223,2.11155772856749,126.360350413054));
#42850=CARTESIAN_POINT('Ctrl Pts',(112.818045283104,1.98639340499948,126.305091309881));
#42851=CARTESIAN_POINT('Ctrl Pts',(112.810280530157,1.86138333527402,126.249900308614));
#42852=CARTESIAN_POINT('Ctrl Pts',(112.80251577721,1.73390720848793,126.199850814684));
#42853=CARTESIAN_POINT('Ctrl Pts',(112.794751024262,1.60442719685361,126.155167522792));
#42854=CARTESIAN_POINT('Ctrl Pts',(112.786993983377,1.47507578659228,126.110528610975));
#42855=CARTESIAN_POINT('Ctrl Pts',(112.779236942492,1.34372481942865,126.071245421395));
#42856=CARTESIAN_POINT('Ctrl Pts',(112.771479901607,1.21085758103656,126.037495087582));
#42857=CARTESIAN_POINT('Ctrl Pts',(112.763728710367,1.07809053886251,126.003770205159));
#42858=CARTESIAN_POINT('Ctrl Pts',(112.755977519127,0.943809878789901,125.975569969518));
#42859=CARTESIAN_POINT('Ctrl Pts',(112.748226327887,0.808514886721858,125.953021963086));
#42860=CARTESIAN_POINT('Ctrl Pts',(112.74047843111,0.673277398634464,125.930483540158));
#42861=CARTESIAN_POINT('Ctrl Pts',(112.732730534333,0.537026820851626,125.913592632487));
#42862=CARTESIAN_POINT('Ctrl Pts',(112.724982637556,0.400273280187613,125.902425860384));
#42863=CARTESIAN_POINT('Ctrl Pts',(112.717236361472,0.263548345416242,125.891261424129));
#42864=CARTESIAN_POINT('Ctrl Pts',(112.709490085388,0.126321046451539,125.885818773613));
#42865=CARTESIAN_POINT('Ctrl Pts',(112.701743809303,-0.0108931023410998,
125.886122680782));
#42866=CARTESIAN_POINT('Ctrl Pts',(112.693997476038,-0.148108264017321,
125.886426590194));
#42867=CARTESIAN_POINT('Ctrl Pts',(112.686251142773,-0.28530988436353,125.892477141069));
#42868=CARTESIAN_POINT('Ctrl Pts',(112.678504809507,-0.421982578929462,
125.904246969335));
#42869=CARTESIAN_POINT('Ctrl Pts',(112.670756741504,-0.55868588039772,125.916019433372));
#42870=CARTESIAN_POINT('Ctrl Pts',(112.663008673501,-0.694859630936441,
125.93351368989));
#42871=CARTESIAN_POINT('Ctrl Pts',(112.655260605498,-0.829994092178677,
125.956650553067));
#42872=CARTESIAN_POINT('Ctrl Pts',(112.647504302757,-0.965272175934534,
125.979812006376));
#42873=CARTESIAN_POINT('Ctrl Pts',(112.639748000015,-1.09950837792602,126.008627979973));
#42874=CARTESIAN_POINT('Ctrl Pts',(112.631991697273,-1.23220312790668,126.042968120189));
#42875=CARTESIAN_POINT('Ctrl Pts',(112.624231254759,-1.36496870107086,126.077326588772));
#42876=CARTESIAN_POINT('Ctrl Pts',(112.616470812244,-1.49619080900436,126.117214985287));
#42877=CARTESIAN_POINT('Ctrl Pts',(112.60871036973,-1.62538651319723,126.162453493849));
#42878=CARTESIAN_POINT('Ctrl Pts',(112.600937469465,-1.75478961380384,126.20776462328));
#42879=CARTESIAN_POINT('Ctrl Pts',(112.593164569199,-1.88215944673707,126.258442882647));
#42880=CARTESIAN_POINT('Ctrl Pts',(112.585391668934,-2.00703364703102,126.31426050708));
#42881=CARTESIAN_POINT('Ctrl Pts',(112.577901333172,-2.12736835560448,126.368049020269));
#42882=CARTESIAN_POINT('Ctrl Pts',(112.57041099741,-2.24538545053348,126.426609591129));
#42883=CARTESIAN_POINT('Ctrl Pts',(112.562920661648,-2.3606956785272,126.489699683508));
#42884=CARTESIAN_POINT('Ctrl Pts',(112.555145317235,-2.48039348186472,126.555190365485));
#42885=CARTESIAN_POINT('Ctrl Pts',(112.547369972822,-2.59755356213865,126.625769574031));
#42886=CARTESIAN_POINT('Ctrl Pts',(112.53959462841,-2.71171303900294,126.701216036077));
#42887=CARTESIAN_POINT('Ctrl Pts',(112.531829087145,-2.82572858368351,126.77656737528));
#42888=CARTESIAN_POINT('Ctrl Pts',(112.524063545881,-2.93675072985558,126.856773543025));
#42889=CARTESIAN_POINT('Ctrl Pts',(112.516298004617,-3.04434049096868,126.94156706399));
#42890=CARTESIAN_POINT('Ctrl Pts',(112.508541805313,-3.15180082139576,127.026258578189));
#42891=CARTESIAN_POINT('Ctrl Pts',(112.50078560601,-3.25583668553785,127.115526213941));
#42892=CARTESIAN_POINT('Ctrl Pts',(112.493029406706,-3.35603796700677,127.209059207877));
#42893=CARTESIAN_POINT('Ctrl Pts',(112.48527850398,-3.45617082271927,127.302528329718));
#42894=CARTESIAN_POINT('Ctrl Pts',(112.477527601253,-3.55247402070944,127.400256749436));
#42895=CARTESIAN_POINT('Ctrl Pts',(112.469776698526,-3.64457039176469,127.50189340017));
#42896=CARTESIAN_POINT('Ctrl Pts',(112.462029410145,-3.73662381710103,127.603482656431));
#42897=CARTESIAN_POINT('Ctrl Pts',(112.454282121764,-3.82447405730881,127.70897622806));
#42898=CARTESIAN_POINT('Ctrl Pts',(112.446534833383,-3.90778099548178,127.817986435744));
#42899=CARTESIAN_POINT('Ctrl Pts',(112.438789479906,-3.99106712754004,127.926969417859));
#42900=CARTESIAN_POINT('Ctrl Pts',(112.43104412643,-4.06981197963845,128.039466977067));
#42901=CARTESIAN_POINT('Ctrl Pts',(112.423298772953,-4.14371616711926,128.155058938094));
#42902=CARTESIAN_POINT('Ctrl Pts',(112.415551153812,-4.21764197299036,128.270684711983));
#42903=CARTESIAN_POINT('Ctrl Pts',(112.407803534671,-4.28672406924796,128.389406369999));
#42904=CARTESIAN_POINT('Ctrl Pts',(112.40005591553,-4.35070677162548,128.510775291089));
#42905=CARTESIAN_POINT('Ctrl Pts',(112.392307296076,-4.41469773496383,128.632159882412));
#42906=CARTESIAN_POINT('Ctrl Pts',(112.384558676621,-4.47358781771709,128.756192067992));
#42907=CARTESIAN_POINT('Ctrl Pts',(112.376810057166,-4.52716807485757,128.882400086106));
#42908=CARTESIAN_POINT('Ctrl Pts',(112.369054792459,-4.5807942826802,129.008716340814));
#42909=CARTESIAN_POINT('Ctrl Pts',(112.361299527752,-4.62910142171835,129.137211792758));
#42910=CARTESIAN_POINT('Ctrl Pts',(112.353544263044,-4.67192919959215,129.267395876104));
#42911=CARTESIAN_POINT('Ctrl Pts',(112.347346518942,-4.70615570477945,129.37143457307));
#42912=CARTESIAN_POINT('Ctrl Pts',(112.341148774839,-4.73688366297584,129.476551328042));
#42913=CARTESIAN_POINT('Ctrl Pts',(112.334951030737,-4.76405452823405,129.582490119308));
#42914=CARTESIAN_POINT('Ctrl Pts',(114.08491538754,-4.76405452823405,129.582490119308));
#42915=CARTESIAN_POINT('Ctrl Pts',(114.077273043215,-4.79770112579015,129.713677692521));
#42916=CARTESIAN_POINT('Ctrl Pts',(114.06963069889,-4.82591584136121,129.846221348947));
#42917=CARTESIAN_POINT('Ctrl Pts',(114.061988354565,-4.84860748928013,129.979625219152));
#42918=CARTESIAN_POINT('Ctrl Pts',(114.054133534808,-4.87193001922921,130.116738035696));
#42919=CARTESIAN_POINT('Ctrl Pts',(114.046278715051,-4.88941780736256,130.2547591488));
#42920=CARTESIAN_POINT('Ctrl Pts',(114.038423895294,-4.90102887405486,130.393144083146));
#42921=CARTESIAN_POINT('Ctrl Pts',(114.030569075537,-4.91263994074715,130.531529017491));
#42922=CARTESIAN_POINT('Ctrl Pts',(114.022714255779,-4.9183743044535,130.67027731309));
#42923=CARTESIAN_POINT('Ctrl Pts',(114.014859436022,-4.91824795544417,130.808845176549));
#42924=CARTESIAN_POINT('',(114.360140564037,-4.91824995380443,130.803686523594));
#42925=CARTESIAN_POINT('Ctrl Pts',(114.429855701321,-4.76405452823407,129.582490119308));
#42926=CARTESIAN_POINT('Ctrl Pts',(114.421628335829,-4.8001277250803,129.723138966325));
#42927=CARTESIAN_POINT('Ctrl Pts',(114.413400970338,-4.8300079357871,129.865541295514));
#42928=CARTESIAN_POINT('Ctrl Pts',(114.405173604846,-4.85353619530554,130.009144003454));
#42929=CARTESIAN_POINT('Ctrl Pts',(114.396965713327,-4.87700876401274,130.152406807319));
#42930=CARTESIAN_POINT('Ctrl Pts',(114.388757821807,-4.89415931337737,130.296864013968));
#42931=CARTESIAN_POINT('Ctrl Pts',(114.380549930287,-4.90487943354696,130.441950897956));
#42932=CARTESIAN_POINT('Ctrl Pts',(114.373746808204,-4.91376481977387,130.562206359675));
#42933=CARTESIAN_POINT('Ctrl Pts',(114.366943686121,-4.91823339802076,130.682894044141));
#42934=CARTESIAN_POINT('Ctrl Pts',(114.360140564037,-4.91824995380443,130.803686523594));
#42935=CARTESIAN_POINT('Ctrl Pts',(114.360140564008,-4.9182499538045,130.803686524113));
#42936=CARTESIAN_POINT('Ctrl Pts',(114.352104374385,-4.91826951031294,130.946372669984));
#42937=CARTESIAN_POINT('Ctrl Pts',(114.344068184762,-4.91207540979104,131.088966543765));
#42938=CARTESIAN_POINT('Ctrl Pts',(114.336031995138,-4.8997177208193,131.230915794289));
#42939=CARTESIAN_POINT('Ctrl Pts',(114.327987899649,-4.88734787456491,131.373004692054));
#42940=CARTESIAN_POINT('Ctrl Pts',(114.319943804161,-4.86880237640859,131.514447356263));
#42941=CARTESIAN_POINT('Ctrl Pts',(114.311899708672,-4.84418284113059,131.654699176139));
#42942=CARTESIAN_POINT('Ctrl Pts',(114.303742850313,-4.8192181869443,131.796917058916));
#42943=CARTESIAN_POINT('Ctrl Pts',(114.295585991954,-4.78800800756211,131.937910097035));
#42944=CARTESIAN_POINT('Ctrl Pts',(114.287429133595,-4.75071072483695,132.077125588572));
#42945=CARTESIAN_POINT('Ctrl Pts',(114.279360225711,-4.71381559617151,132.214840003596));
#42946=CARTESIAN_POINT('Ctrl Pts',(114.271291317826,-4.67096416418026,132.350814710882));
#42947=CARTESIAN_POINT('Ctrl Pts',(114.263222409942,-4.62235864862707,132.484534294887));
#42948=CARTESIAN_POINT('Ctrl Pts',(114.255021576346,-4.57295843851214,132.620440178636));
#42949=CARTESIAN_POINT('Ctrl Pts',(114.24682074275,-4.51761451060067,132.754016210855));
#42950=CARTESIAN_POINT('Ctrl Pts',(114.238619909154,-4.45658795979715,132.884746836298));
#42951=CARTESIAN_POINT('Ctrl Pts',(114.230419075558,-4.39556140899363,133.015477461742));
#42952=CARTESIAN_POINT('Ctrl Pts',(114.222218241962,-4.32885246381835,133.143362382982));
#42953=CARTESIAN_POINT('Ctrl Pts',(114.214017408366,-4.25676823117942,133.26791643965));
#42954=CARTESIAN_POINT('Ctrl Pts',(114.206243074247,-4.18843287201148,133.385992832871));
#42955=CARTESIAN_POINT('Ctrl Pts',(114.198468740128,-4.11507265710095,133.501410814662));
#42956=CARTESIAN_POINT('Ctrl Pts',(114.190694406009,-4.03691981000747,133.61371312483));
#42957=CARTESIAN_POINT('Ctrl Pts',(114.182929653062,-3.95886327931348,133.725877032436));
#42958=CARTESIAN_POINT('Ctrl Pts',(114.175164900115,-3.87602608977212,133.834932590625));
#42959=CARTESIAN_POINT('Ctrl Pts',(114.167400147168,-3.78868608134673,133.940447484907));
#42960=CARTESIAN_POINT('Ctrl Pts',(114.159643106283,-3.70143282024905,134.045857580308));
#42961=CARTESIAN_POINT('Ctrl Pts',(114.151886065398,-3.60968588795588,134.147733710845));
#42962=CARTESIAN_POINT('Ctrl Pts',(114.144129024513,-3.5137658968655,134.245673199202));
#42963=CARTESIAN_POINT('Ctrl Pts',(114.136377833272,-3.41791823978629,134.343538830629));
#42964=CARTESIAN_POINT('Ctrl Pts',(114.128626642032,-3.3179040601478,134.43747345061));
#42965=CARTESIAN_POINT('Ctrl Pts',(114.120875450792,-3.21408341091365,134.527108378319));
#42966=CARTESIAN_POINT('Ctrl Pts',(114.113127554015,-3.11030688822499,134.616705208792));
#42967=CARTESIAN_POINT('Ctrl Pts',(114.105379657238,-3.00272740903509,134.702005726759));
#42968=CARTESIAN_POINT('Ctrl Pts',(114.097631760461,-2.89174079449725,134.782679136732));
#42969=CARTESIAN_POINT('Ctrl Pts',(114.089885484377,-2.78077739596666,134.863335671567));
#42970=CARTESIAN_POINT('Ctrl Pts',(114.082139208293,-2.66640859573317,134.939366793872));
#42971=CARTESIAN_POINT('Ctrl Pts',(114.074392932209,-2.54906178666891,135.010483187136));
#42972=CARTESIAN_POINT('Ctrl Pts',(114.066646598943,-2.43171411137709,135.081600105365));
#42973=CARTESIAN_POINT('Ctrl Pts',(114.058900265678,-2.31138871774528,135.147802019528));
#42974=CARTESIAN_POINT('Ctrl Pts',(114.051153932413,-2.1885400077627,135.208844207832));
#42975=CARTESIAN_POINT('Ctrl Pts',(114.04340586441,-2.06566378666363,135.269900066111));
#42976=CARTESIAN_POINT('Ctrl Pts',(114.035657796407,-1.94026347482909,135.325793725309));
#42977=CARTESIAN_POINT('Ctrl Pts',(114.027909728404,-1.81281560876735,135.376327659345));
#42978=CARTESIAN_POINT('Ctrl Pts',(114.020153425662,-1.68523228959656,135.426915301446));
#42979=CARTESIAN_POINT('Ctrl Pts',(114.01239712292,-1.5555974330923,135.472131694917));
#42980=CARTESIAN_POINT('Ctrl Pts',(114.004640820178,-1.42440550805593,135.511828303182));
#42981=CARTESIAN_POINT('Ctrl Pts',(113.996880377664,-1.29314356193897,135.551546098722));
#42982=CARTESIAN_POINT('Ctrl Pts',(113.98911993515,-1.16032326977921,135.585738141329));
#42983=CARTESIAN_POINT('Ctrl Pts',(113.981359492636,-1.02645062514271,135.614306789473));
#42984=CARTESIAN_POINT('Ctrl Pts',(113.97358659237,-0.892363076252286,135.642921298547));
#42985=CARTESIAN_POINT('Ctrl Pts',(113.965813692105,-0.757220184724024,
135.665894308434));
#42986=CARTESIAN_POINT('Ctrl Pts',(113.958040791839,-0.621535315204801,
135.683179830701));
#42987=CARTESIAN_POINT('Ctrl Pts',(113.950550456077,-0.490782932461883,
135.699836980694));
#42988=CARTESIAN_POINT('Ctrl Pts',(113.943060120315,-0.359527599005925,
135.71121294635));
#42989=CARTESIAN_POINT('Ctrl Pts',(113.935569784553,-0.228227921651108,
135.717312385931));
#42990=CARTESIAN_POINT('Ctrl Pts',(113.927795450434,-0.0919499771221869,
135.723643087618));
#42991=CARTESIAN_POINT('Ctrl Pts',(113.920021116315,0.0448074278476511,
135.724309299543));
#42992=CARTESIAN_POINT('Ctrl Pts',(113.912246782196,0.181534064801489,135.719259237662));
#42993=CARTESIAN_POINT('Ctrl Pts',(113.904482029249,0.318092198394799,135.71421539953));
#42994=CARTESIAN_POINT('Ctrl Pts',(113.896717276302,0.454619252471153,135.703469318929));
#42995=CARTESIAN_POINT('Ctrl Pts',(113.888952523355,0.590601329319836,135.687021073947));
#42996=CARTESIAN_POINT('Ctrl Pts',(113.88119548247,0.726448346852689,135.670589165594));
#42997=CARTESIAN_POINT('Ctrl Pts',(113.873438441585,0.861751078703154,135.648466410065));
#42998=CARTESIAN_POINT('Ctrl Pts',(113.8656814007,0.995997442208604,135.620704890727));
#42999=CARTESIAN_POINT('Ctrl Pts',(113.85793020946,1.13014256948723,135.592964306567));
#43000=CARTESIAN_POINT('Ctrl Pts',(113.85017901822,1.26323253272058,135.559593501269));
#43001=CARTESIAN_POINT('Ctrl Pts',(113.842427826979,1.39476253286651,135.520696116596));
#43002=CARTESIAN_POINT('Ctrl Pts',(113.834679930202,1.52623662925371,135.48181526435));
#43003=CARTESIAN_POINT('Ctrl Pts',(113.826932033425,1.65615170713195,135.43741261524));
#43004=CARTESIAN_POINT('Ctrl Pts',(113.819184136648,1.78401550788889,135.387642381773));
#43005=CARTESIAN_POINT('Ctrl Pts',(113.811437860564,1.91185256229505,135.337882559166));
#43006=CARTESIAN_POINT('Ctrl Pts',(113.80369158448,2.03763882894259,135.282757527206));
#43007=CARTESIAN_POINT('Ctrl Pts',(113.795945308396,2.16089988137072,135.22247048098));
#43008=CARTESIAN_POINT('Ctrl Pts',(113.788198975131,2.28416184368394,135.162182989728));
#43009=CARTESIAN_POINT('Ctrl Pts',(113.780452641865,2.40489820337418,135.09673357995));
#43010=CARTESIAN_POINT('Ctrl Pts',(113.7727063086,2.522657453691,135.026372274802));
#43011=CARTESIAN_POINT('Ctrl Pts',(113.764958240597,2.64044307537546,134.955995212728));
#43012=CARTESIAN_POINT('Ctrl Pts',(113.757210172594,2.75524992546965,134.880704266935));
#43013=CARTESIAN_POINT('Ctrl Pts',(113.749462104591,2.8666542400627,134.800793593412));
#43014=CARTESIAN_POINT('Ctrl Pts',(113.741705801849,2.97817695648711,134.720797989874));
#43015=CARTESIAN_POINT('Ctrl Pts',(113.733949499108,3.08628959535703,134.63617307879));
#43016=CARTESIAN_POINT('Ctrl Pts',(113.726193196366,3.19059991617947,134.547254583119));
#43017=CARTESIAN_POINT('Ctrl Pts',(113.718432753852,3.29496591056093,134.45828862897));
#43018=CARTESIAN_POINT('Ctrl Pts',(113.710672311337,3.39552525660378,134.365024789726));
#43019=CARTESIAN_POINT('Ctrl Pts',(113.702911868823,3.49192230384059,134.267835994473));
#43020=CARTESIAN_POINT('Ctrl Pts',(113.695138968558,3.5884740961753,134.170491183138));
#43021=CARTESIAN_POINT('Ctrl Pts',(113.687366068292,3.68084997394178,134.06920911404));
#43022=CARTESIAN_POINT('Ctrl Pts',(113.679593168027,3.7687337596386,133.964396837526));
#43023=CARTESIAN_POINT('Ctrl Pts',(113.672102832265,3.8534227483598,133.863394751269));
#43024=CARTESIAN_POINT('Ctrl Pts',(113.664612496503,3.93394038427291,133.759114909199));
#43025=CARTESIAN_POINT('Ctrl Pts',(113.657122160741,4.01004269832085,133.651945668121));
#43026=CARTESIAN_POINT('Ctrl Pts',(113.649347826622,4.08903045473632,133.540713072694));
#43027=CARTESIAN_POINT('Ctrl Pts',(113.641573492503,4.1635116755688,133.426015298541));
#43028=CARTESIAN_POINT('Ctrl Pts',(113.633799158384,4.23316700248996,133.308253624771));
#43029=CARTESIAN_POINT('Ctrl Pts',(113.626034405437,4.30273648544601,133.190637081739));
#43030=CARTESIAN_POINT('Ctrl Pts',(113.618269652489,4.36749171107854,133.069964485445));
#43031=CARTESIAN_POINT('Ctrl Pts',(113.610504899542,4.42715497082029,132.946668234796));
#43032=CARTESIAN_POINT('Ctrl Pts',(113.602747858657,4.4867589721712,132.823494443722));
#43033=CARTESIAN_POINT('Ctrl Pts',(113.594990817772,4.54128090291414,132.697702533702));
#43034=CARTESIAN_POINT('Ctrl Pts',(113.587233776887,4.59048778907245,132.569751486716));
#43035=CARTESIAN_POINT('Ctrl Pts',(113.579482585647,4.63965756793541,132.441896928608));
#43036=CARTESIAN_POINT('Ctrl Pts',(113.571731394407,4.6835201403585,132.311886837845));
#43037=CARTESIAN_POINT('Ctrl Pts',(113.563980203167,4.72188984687997,132.180201937062));
#43038=CARTESIAN_POINT('Ctrl Pts',(113.55623230639,4.76024324525248,132.048573005875));
#43039=CARTESIAN_POINT('Ctrl Pts',(113.548484409613,4.79310831195328,131.915271055031));
#43040=CARTESIAN_POINT('Ctrl Pts',(113.540736512836,4.82034871252759,131.780793591269));
#43041=CARTESIAN_POINT('Ctrl Pts',(113.532990236752,4.84758341499731,131.646344257293));
#43042=CARTESIAN_POINT('Ctrl Pts',(113.525243960668,4.86919571401053,131.510720282432));
#43043=CARTESIAN_POINT('Ctrl Pts',(113.517497684584,4.88510012425823,131.374430647012));
#43044=CARTESIAN_POINT('Ctrl Pts',(113.509751351318,4.90100465190866,131.238140005532));
#43045=CARTESIAN_POINT('Ctrl Pts',(113.502005018053,4.91120116140113,131.101184082018));
#43046=CARTESIAN_POINT('Ctrl Pts',(113.494258684788,4.91565595387034,130.964077885509));
#43047=CARTESIAN_POINT('Ctrl Pts',(113.486510616785,4.92011174395943,130.826940985017));
#43048=CARTESIAN_POINT('Ctrl Pts',(113.478762548782,4.91882324570292,130.68965413525));
#43049=CARTESIAN_POINT('Ctrl Pts',(113.471014480779,4.91180888611941,130.552732859283));
#43050=CARTESIAN_POINT('Ctrl Pts',(113.463258178037,4.90478707159103,130.415666061754));
#43051=CARTESIAN_POINT('Ctrl Pts',(113.455501875295,4.89202725930124,130.278966005245));
#43052=CARTESIAN_POINT('Ctrl Pts',(113.447745572553,4.87359988691645,130.14314415925));
#43053=CARTESIAN_POINT('Ctrl Pts',(113.439985130039,4.8551626792882,130.007249821047));
#43054=CARTESIAN_POINT('Ctrl Pts',(113.432224687525,4.83105195279801,129.872235012025));
#43055=CARTESIAN_POINT('Ctrl Pts',(113.424464245011,4.80138922548218,129.738600528276));
#43056=CARTESIAN_POINT('Ctrl Pts',(113.416691344745,4.77167888092311,129.60475152259));
#43057=CARTESIAN_POINT('Ctrl Pts',(113.40891844448,4.73639882607318,129.472287648105));
#43058=CARTESIAN_POINT('Ctrl Pts',(113.401145544214,4.6957206222541,129.341694934562));
#43059=CARTESIAN_POINT('Ctrl Pts',(113.393655208452,4.65652117360567,129.215849595098));
#43060=CARTESIAN_POINT('Ctrl Pts',(113.38616487269,4.61230933807669,129.09174202581));
#43061=CARTESIAN_POINT('Ctrl Pts',(113.378674536928,4.56327998001207,128.969787401115));
#43062=CARTESIAN_POINT('Ctrl Pts',(113.370900202809,4.51239165893472,128.843208829757));
#43063=CARTESIAN_POINT('Ctrl Pts',(113.36312586869,4.45615209229471,128.718548720674));
#43064=CARTESIAN_POINT('Ctrl Pts',(113.355351534571,4.39472626659451,128.596292660232));
#43065=CARTESIAN_POINT('Ctrl Pts',(113.347586781624,4.33337614273474,128.474187269458));
#43066=CARTESIAN_POINT('Ctrl Pts',(113.339822028676,4.26685265103566,128.354480378281));
#43067=CARTESIAN_POINT('Ctrl Pts',(113.332057275729,4.19536947267995,128.237639352955));
#43068=CARTESIAN_POINT('Ctrl Pts',(113.324300234844,4.12395729242486,128.120914375783));
#43069=CARTESIAN_POINT('Ctrl Pts',(113.316543193959,4.04759543125197,128.007049931303));
#43070=CARTESIAN_POINT('Ctrl Pts',(113.308786153074,3.96654411557375,127.896490118093));
#43071=CARTESIAN_POINT('Ctrl Pts',(113.301034961834,3.88555392132284,127.786013678897));
#43072=CARTESIAN_POINT('Ctrl Pts',(113.293283770594,3.79988154168427,127.678837224734));
#43073=CARTESIAN_POINT('Ctrl Pts',(113.285532579354,3.70983106875204,127.575376798495));
#43074=CARTESIAN_POINT('Ctrl Pts',(113.277784682577,3.61981886967329,127.471960345697));
#43075=CARTESIAN_POINT('Ctrl Pts',(113.2700367858,3.52543253444647,127.372257073783));
#43076=CARTESIAN_POINT('Ctrl Pts',(113.262288889023,3.42701693747799,127.276650599333));
#43077=CARTESIAN_POINT('Ctrl Pts',(113.254542612939,3.32862192693073,127.181064123697));
#43078=CARTESIAN_POINT('Ctrl Pts',(113.246796336855,3.22619961133592,127.089573013233));
#43079=CARTESIAN_POINT('Ctrl Pts',(113.23905006077,3.12013200335912,127.002524305451));
#43080=CARTESIAN_POINT('Ctrl Pts',(113.231303727505,3.01406361241533,126.915474955096));
#43081=CARTESIAN_POINT('Ctrl Pts',(113.22355739424,2.90435017761357,126.832868320885));
#43082=CARTESIAN_POINT('Ctrl Pts',(113.215811060974,2.79140677558456,126.755011129596));
#43083=CARTESIAN_POINT('Ctrl Pts',(113.208062992971,2.67843808066414,126.677136502729));
#43084=CARTESIAN_POINT('Ctrl Pts',(113.200314924968,2.56223830100829,126.604013657088));
#43085=CARTESIAN_POINT('Ctrl Pts',(113.192566856965,2.44325112103519,126.535905742314));
#43086=CARTESIAN_POINT('Ctrl Pts',(113.184810554224,2.32413748007085,126.467725441638));
#43087=CARTESIAN_POINT('Ctrl Pts',(113.177054251482,2.20223086076412,126.404570913466));
#43088=CARTESIAN_POINT('Ctrl Pts',(113.16929794874,2.0779996501665,126.346659358351));
#43089=CARTESIAN_POINT('Ctrl Pts',(113.161537506226,1.95370213363082,126.288716894095));
#43090=CARTESIAN_POINT('Ctrl Pts',(113.153777063712,1.82707791437718,126.236023128946));
#43091=CARTESIAN_POINT('Ctrl Pts',(113.146016621197,1.6986140098067,126.188746518858));
#43092=CARTESIAN_POINT('Ctrl Pts',(113.138243720932,1.56994388357256,126.14139401616));
#43093=CARTESIAN_POINT('Ctrl Pts',(113.130470820666,1.43942854298673,126.099476165719));
#43094=CARTESIAN_POINT('Ctrl Pts',(113.122697920401,1.30756963172069,126.063111339084));
#43095=CARTESIAN_POINT('Ctrl Pts',(113.115207584639,1.180504124012,126.028068465496));
#43096=CARTESIAN_POINT('Ctrl Pts',(113.107717248877,1.05219133402489,125.998181962175));
#43097=CARTESIAN_POINT('Ctrl Pts',(113.100226913115,0.923085888692947,125.973512296143));
#43098=CARTESIAN_POINT('Ctrl Pts',(113.092452578996,0.789085371159932,125.947907272225));
#43099=CARTESIAN_POINT('Ctrl Pts',(113.084678244877,0.653806431333827,125.927841378475));
#43100=CARTESIAN_POINT('Ctrl Pts',(113.076903910758,0.517746786012154,125.913438278367));
#43101=CARTESIAN_POINT('Ctrl Pts',(113.069139157811,0.381854822043895,125.899052928793));
#43102=CARTESIAN_POINT('Ctrl Pts',(113.061374404864,0.245184452031789,125.890316527718));
#43103=CARTESIAN_POINT('Ctrl Pts',(113.053609651917,0.108244384340495,125.887301921988));
#43104=CARTESIAN_POINT('Ctrl Pts',(113.045852611032,-0.0285596725451436,
125.884290310407));
#43105=CARTESIAN_POINT('Ctrl Pts',(113.038095570147,-0.165632505700293,
125.886989193357));
#43106=CARTESIAN_POINT('Ctrl Pts',(113.030338529262,-0.302459823683665,
125.895419681116));
#43107=CARTESIAN_POINT('Ctrl Pts',(113.022587338021,-0.439183959122743,
125.903843811378));
#43108=CARTESIAN_POINT('Ctrl Pts',(113.014836146781,-0.575662559263489,
125.91799091933));
#43109=CARTESIAN_POINT('Ctrl Pts',(113.007084955541,-0.711381226234788,
125.937830045027));
#43110=CARTESIAN_POINT('Ctrl Pts',(112.999337058764,-0.847042209151933,
125.957660738565));
#43111=CARTESIAN_POINT('Ctrl Pts',(112.991589161987,-0.981943515261864,
125.983178581694));
#43112=CARTESIAN_POINT('Ctrl Pts',(112.98384126521,-1.11557598402841,126.01430077594));
#43113=CARTESIAN_POINT('Ctrl Pts',(112.976094989126,-1.24918049976328,126.045416460094));
#43114=CARTESIAN_POINT('Ctrl Pts',(112.968348713042,-1.38151632554283,126.082134074954));
#43115=CARTESIAN_POINT('Ctrl Pts',(112.960602436958,-1.5120850017042,126.124319804697));
#43116=CARTESIAN_POINT('Ctrl Pts',(112.952856103692,-1.64265464169388,126.166505845845));
#43117=CARTESIAN_POINT('Ctrl Pts',(112.945109770427,-1.77145673400635,126.21415996222));
#43118=CARTESIAN_POINT('Ctrl Pts',(112.937363437161,-1.89800886166085,126.267098731411));
#43119=CARTESIAN_POINT('Ctrl Pts',(112.929615369158,-2.02458932978722,126.320049355872));
#43120=CARTESIAN_POINT('Ctrl Pts',(112.921867301155,-2.14891847001423,126.378286837252));
#43121=CARTESIAN_POINT('Ctrl Pts',(112.914119233152,-2.27053506482922,126.441580130092));
#43122=CARTESIAN_POINT('Ctrl Pts',(112.906362930411,-2.39228091520811,126.504940691798));
#43123=CARTESIAN_POINT('Ctrl Pts',(112.898606627669,-2.51130811385827,126.573367618083));
#43124=CARTESIAN_POINT('Ctrl Pts',(112.890850324927,-2.6271807491615,126.646584243862));
#43125=CARTESIAN_POINT('Ctrl Pts',(112.883089882413,-2.74311522917913,126.719839947558));
#43126=CARTESIAN_POINT('Ctrl Pts',(112.875329439899,-2.85589146963866,126.79789022222));
#43127=CARTESIAN_POINT('Ctrl Pts',(112.867568997384,-2.96510449897364,126.880416380874));
#43128=CARTESIAN_POINT('Ctrl Pts',(112.859796097119,-3.07449284675872,126.963075017845));
#43129=CARTESIAN_POINT('Ctrl Pts',(112.852023196853,-3.18030625111083,127.050223648203));
#43130=CARTESIAN_POINT('Ctrl Pts',(112.844250296588,-3.28217397203618,127.141504207633));
#43131=CARTESIAN_POINT('Ctrl Pts',(112.836759960826,-3.38033854471555,127.229466488805));
#43132=CARTESIAN_POINT('Ctrl Pts',(112.829269625064,-3.47483910359065,127.321265287964));
#43133=CARTESIAN_POINT('Ctrl Pts',(112.821779289302,-3.56537903908143,127.416550798497));
#43134=CARTESIAN_POINT('Ctrl Pts',(112.814101568287,-3.65818400637564,127.514220060582));
#43135=CARTESIAN_POINT('Ctrl Pts',(112.806423847272,-3.74713767467342,127.615879466278));
#43136=CARTESIAN_POINT('Ctrl Pts',(112.798746126257,-3.83187082516827,127.721188705115));
#43137=CARTESIAN_POINT('Ctrl Pts',(112.791077478074,-3.91650384573452,127.826373499075));
#43138=CARTESIAN_POINT('Ctrl Pts',(112.783408829892,-3.99692601563795,127.935199241451));
#43139=CARTESIAN_POINT('Ctrl Pts',(112.775740181709,-4.07280442560457,128.047288407181));
#43140=CARTESIAN_POINT('Ctrl Pts',(112.767775512486,-4.15161185322238,128.163704378719));
#43141=CARTESIAN_POINT('Ctrl Pts',(112.759810843262,-4.22551736617257,128.283640488079));
#43142=CARTESIAN_POINT('Ctrl Pts',(112.751846174039,-4.29419299984012,128.406634706911));
#43143=CARTESIAN_POINT('Ctrl Pts',(112.744191036869,-4.3601996827535,128.524848984219));
#43144=CARTESIAN_POINT('Ctrl Pts',(112.736535899699,-4.42137513354883,128.645887747828));
#43145=CARTESIAN_POINT('Ctrl Pts',(112.728880762529,-4.47747202685312,128.76931091025));
#43146=CARTESIAN_POINT('Ctrl Pts',(112.721228978975,-4.53354434483844,128.892680002591));
#43147=CARTESIAN_POINT('Ctrl Pts',(112.713577195422,-4.58454236614004,129.018431050676));
#43148=CARTESIAN_POINT('Ctrl Pts',(112.705925411868,-4.63026525524111,129.146100466502));
#43149=CARTESIAN_POINT('Ctrl Pts',(112.69827489598,-4.67598056945924,129.273748731414));
#43150=CARTESIAN_POINT('Ctrl Pts',(112.690624380093,-4.71642235479985,129.40331435413));
#43151=CARTESIAN_POINT('Ctrl Pts',(112.682973864205,-4.75143853263936,129.53431536914));
#43152=CARTESIAN_POINT('Ctrl Pts',(112.682037293146,-4.7557251898085,129.550352426146));
#43153=CARTESIAN_POINT('Ctrl Pts',(112.681100722086,-4.75993059748163,129.566410975894));
#43154=CARTESIAN_POINT('Ctrl Pts',(112.680164151027,-4.76405452823403,129.582490119308));
#43155=CARTESIAN_POINT('Origin',(213.235140564004,0.,130.804360617566));
#43156=CARTESIAN_POINT('',(110.584632631705,-4.76405452823407,129.582490119308));
#43157=CARTESIAN_POINT('',(110.930234911077,-4.76405452823406,129.582490119308));
#43158=CARTESIAN_POINT('',(213.235140564004,-4.76405452823405,129.582490119308));
#43159=CARTESIAN_POINT('',(112.264859435957,-4.91824956414205,130.802290033936));
#43160=CARTESIAN_POINT('Ctrl Pts',(112.264859435957,-4.91824956414205,130.802290033936));
#43161=CARTESIAN_POINT('Ctrl Pts',(112.257165042791,-4.91830645312108,130.937418213418));
#43162=CARTESIAN_POINT('Ctrl Pts',(112.249470649625,-4.91279019552954,131.07277397242));
#43163=CARTESIAN_POINT('Ctrl Pts',(112.241776256459,-4.90167077659974,131.207853691023));
#43164=CARTESIAN_POINT('Ctrl Pts',(112.234090909914,-4.89056443123831,131.342774590722));
#43165=CARTESIAN_POINT('Ctrl Pts',(112.22640556337,-4.87386806018489,131.47741970112));
#43166=CARTESIAN_POINT('Ctrl Pts',(112.218720216826,-4.85160363543908,131.611283926868));
#43167=CARTESIAN_POINT('Ctrl Pts',(112.211041976725,-4.82935979803793,131.745024371787));
#43168=CARTESIAN_POINT('Ctrl Pts',(112.203363736624,-4.80155821467893,131.877984976763));
#43169=CARTESIAN_POINT('Ctrl Pts',(112.195685496523,-4.76827274359631,132.009664772199));
#43170=CARTESIAN_POINT('Ctrl Pts',(112.187782993086,-4.73401508217962,132.145190624794));
#43171=CARTESIAN_POINT('Ctrl Pts',(112.179880489648,-4.69394830635821,132.279359272445));
#43172=CARTESIAN_POINT('Ctrl Pts',(112.17197798621,-4.64820982799618,132.411634227571));
#43173=CARTESIAN_POINT('Ctrl Pts',(112.164307332625,-4.603813261035,132.540028396177));
#43174=CARTESIAN_POINT('Ctrl Pts',(112.15663667904,-4.55407327827764,132.66663803191));
#43175=CARTESIAN_POINT('Ctrl Pts',(112.148966025455,-4.4991662897558,132.790987346377));
#43176=CARTESIAN_POINT('Ctrl Pts',(112.141296200005,-4.44426522907564,132.915323235903));
#43177=CARTESIAN_POINT('Ctrl Pts',(112.133626374556,-4.38419843324348,133.037398923964));
#43178=CARTESIAN_POINT('Ctrl Pts',(112.125956549106,-4.31919024906225,133.156759107386));
#43179=CARTESIAN_POINT('Ctrl Pts',(112.11828580975,-4.25417431876513,133.27613351329));
#43180=CARTESIAN_POINT('Ctrl Pts',(112.110615070395,-4.18421602040058,133.392791420241));
#43181=CARTESIAN_POINT('Ctrl Pts',(112.102944331039,-4.10958514162716,133.506303071842));
#43182=CARTESIAN_POINT('Ctrl Pts',(112.094867754621,-4.03100575473559,133.625820302972));
#43183=CARTESIAN_POINT('Ctrl Pts',(112.086791178203,-3.94724614939418,133.741848862472));
#43184=CARTESIAN_POINT('Ctrl Pts',(112.078714601785,-3.85867157109584,133.853923991054));
#43185=CARTESIAN_POINT('Ctrl Pts',(112.07103253183,-3.7744234848383,133.960524725502));
#43186=CARTESIAN_POINT('Ctrl Pts',(112.063350461875,-3.68581995801667,134.063548816537));
#43187=CARTESIAN_POINT('Ctrl Pts',(112.05566839192,-3.59321451679928,134.16263286662));
#43188=CARTESIAN_POINT('Ctrl Pts',(112.047981149009,-3.50054671688989,134.261783637963));
#43189=CARTESIAN_POINT('Ctrl Pts',(112.040293906098,-3.40387192149152,134.356988807403));
#43190=CARTESIAN_POINT('Ctrl Pts',(112.032606663187,-3.30357817157142,134.447924028132));
#43191=CARTESIAN_POINT('Ctrl Pts',(112.024908858096,-3.20314661922482,134.53898419278));
#43192=CARTESIAN_POINT('Ctrl Pts',(112.017211053004,-3.09908649696322,134.625762449481));
#43193=CARTESIAN_POINT('Ctrl Pts',(112.009513247913,-2.99181647378796,134.707976537411));
#43194=CARTESIAN_POINT('Ctrl Pts',(112.008350636616,-2.97561531784006,134.720393457071));
#43195=CARTESIAN_POINT('Ctrl Pts',(112.007188025319,-2.95934099060744,134.732706349626));
#43196=CARTESIAN_POINT('Ctrl Pts',(112.006025414022,-2.94299498426938,134.744914333107));
#43197=CARTESIAN_POINT('Ctrl Pts',(111.998251079903,-2.83368990944292,134.826548618589));
#43198=CARTESIAN_POINT('Ctrl Pts',(111.990476745784,-2.72081250934746,134.903760820993));
#43199=CARTESIAN_POINT('Ctrl Pts',(111.982702411665,-2.60475628381479,134.976222044367));
#43200=CARTESIAN_POINT('Ctrl Pts',(111.974937658718,-2.48884308720792,135.048593965759));
#43201=CARTESIAN_POINT('Ctrl Pts',(111.967172905771,-2.36975918850557,135.116226353066));
#43202=CARTESIAN_POINT('Ctrl Pts',(111.959408152824,-2.24793019785474,135.178831201314));
#43203=CARTESIAN_POINT('Ctrl Pts',(111.951651111939,-2.12622220947482,135.241373869543));
#43204=CARTESIAN_POINT('Ctrl Pts',(111.943894071054,-2.00177490042135,135.298898758311));
#43205=CARTESIAN_POINT('Ctrl Pts',(111.936137030169,-1.87504152976425,135.35116194643));
#43206=CARTESIAN_POINT('Ctrl Pts',(111.928385838929,-1.74840372972773,135.403385722472));
#43207=CARTESIAN_POINT('Ctrl Pts',(111.920634647688,-1.61948365945458,135.450355547259));
#43208=CARTESIAN_POINT('Ctrl Pts',(111.912883456448,-1.48875744782896,135.491874278776));
#43209=CARTESIAN_POINT('Ctrl Pts',(111.905135559671,-1.3580867983307,135.533375363725));
#43210=CARTESIAN_POINT('Ctrl Pts',(111.897387662894,-1.22561190613693,135.569429845365));
#43211=CARTESIAN_POINT('Ctrl Pts',(111.889639766117,-1.0918268630657,135.599889489712));
#43212=CARTESIAN_POINT('Ctrl Pts',(111.881893490033,-0.958069804941316,
135.630342762558));
#43213=CARTESIAN_POINT('Ctrl Pts',(111.874147213949,-0.823003522018772,
135.655203439204));
#43214=CARTESIAN_POINT('Ctrl Pts',(111.866400937865,-0.687134796638426,
135.674373844832));
#43215=CARTESIAN_POINT('Ctrl Pts',(111.858654604599,-0.551265068305921,
135.693544391973));
#43216=CARTESIAN_POINT('Ctrl Pts',(111.850908271334,-0.414593272826536,
135.707024529658));
#43217=CARTESIAN_POINT('Ctrl Pts',(111.843161938069,-0.277633462249825,
135.714768209929));
#43218=CARTESIAN_POINT('Ctrl Pts',(111.835413870066,-0.140642980473522,
135.722513624345));
#43219=CARTESIAN_POINT('Ctrl Pts',(111.827665802063,-0.00336474552146701,
135.724520002997));
#43220=CARTESIAN_POINT('Ctrl Pts',(111.81991773406,0.133685425790239,135.720793396465));
#43221=CARTESIAN_POINT('Ctrl Pts',(111.812161431318,0.270881255655212,135.717062829251));
#43222=CARTESIAN_POINT('Ctrl Pts',(111.804405128576,0.407848146238273,135.707587115905));
#43223=CARTESIAN_POINT('Ctrl Pts',(111.796648825834,0.544073085024587,135.69242439995));
#43224=CARTESIAN_POINT('Ctrl Pts',(111.78888838332,0.68037073116257,135.677253591197));
#43225=CARTESIAN_POINT('Ctrl Pts',(111.781127940806,0.815925250210358,135.656389791139));
#43226=CARTESIAN_POINT('Ctrl Pts',(111.773367498292,0.950233074196477,135.629942465095));
#43227=CARTESIAN_POINT('Ctrl Pts',(111.765594598026,1.08475650102476,135.603452683455));
#43228=CARTESIAN_POINT('Ctrl Pts',(111.757821697761,1.2180288532253,135.571361556134));
#43229=CARTESIAN_POINT('Ctrl Pts',(111.750048797495,1.34956012402267,135.533828931674));
#43230=CARTESIAN_POINT('Ctrl Pts',(111.742558461733,1.4763099018183,135.497660712652));
#43231=CARTESIAN_POINT('Ctrl Pts',(111.735068125971,1.60144269333784,135.4564398485));
#43232=CARTESIAN_POINT('Ctrl Pts',(111.727577790209,1.72453876751733,135.410351184407));
#43233=CARTESIAN_POINT('Ctrl Pts',(111.71980345609,1.85230206676458,135.362515054606));
#43234=CARTESIAN_POINT('Ctrl Pts',(111.712029121971,1.97827587134586,135.309283182464));
#43235=CARTESIAN_POINT('Ctrl Pts',(111.704254787852,2.10197077551009,135.250808854238));
#43236=CARTESIAN_POINT('Ctrl Pts',(111.696490034905,2.22551323676003,135.192406590395));
#43237=CARTESIAN_POINT('Ctrl Pts',(111.688725281958,2.34678203568538,135.128774891138));
#43238=CARTESIAN_POINT('Ctrl Pts',(111.680960529011,2.46530481286291,135.060116160613));
#43239=CARTESIAN_POINT('Ctrl Pts',(111.673203488126,2.58370987154654,134.991525622908));
#43240=CARTESIAN_POINT('Ctrl Pts',(111.665446447241,2.69937399999404,134.917918184773));
#43241=CARTESIAN_POINT('Ctrl Pts',(111.657689406356,2.81184698280311,134.839543340542));
#43242=CARTESIAN_POINT('Ctrl Pts',(111.649938215116,2.92423514886092,134.76122759939));
#43243=CARTESIAN_POINT('Ctrl Pts',(111.642187023876,3.03343663973857,134.678151830663));
#43244=CARTESIAN_POINT('Ctrl Pts',(111.634435832636,3.13902823498417,134.590610055));
#43245=CARTESIAN_POINT('Ctrl Pts',(111.626687935859,3.24457495098547,134.503105486928));
#43246=CARTESIAN_POINT('Ctrl Pts',(111.618940039082,3.34651452261505,134.411138936247));
#43247=CARTESIAN_POINT('Ctrl Pts',(111.611192142305,3.44445516772763,134.31504597231));
#43248=CARTESIAN_POINT('Ctrl Pts',(111.60344586622,3.54237532576874,134.218973108949));
#43249=CARTESIAN_POINT('Ctrl Pts',(111.595699590136,3.63629794221854,134.118775822833));
#43250=CARTESIAN_POINT('Ctrl Pts',(111.587953314052,3.72586691225441,134.014827688674));
#43251=CARTESIAN_POINT('Ctrl Pts',(111.580206980787,3.81543654346802,133.910878787193));
#43252=CARTESIAN_POINT('Ctrl Pts',(111.572460647522,3.90065220893055,133.803179278599));
#43253=CARTESIAN_POINT('Ctrl Pts',(111.564714314256,3.98119730950177,133.692136759395));
#43254=CARTESIAN_POINT('Ctrl Pts',(111.556966246253,4.06176044758986,133.581069372988));
#43255=CARTESIAN_POINT('Ctrl Pts',(111.54921817825,4.13765070997256,133.466657802671));
#43256=CARTESIAN_POINT('Ctrl Pts',(111.541470110247,4.20859437558527,133.349339290226));
#43257=CARTESIAN_POINT('Ctrl Pts',(111.533713807505,4.27961344097,133.231896090269));
#43258=CARTESIAN_POINT('Ctrl Pts',(111.525957504764,4.34567520492794,133.111540111597));
#43259=CARTESIAN_POINT('Ctrl Pts',(111.518201202022,4.40655128945769,132.988734394162));
#43260=CARTESIAN_POINT('Ctrl Pts',(111.510440759508,4.46745986538682,132.865863131617));
#43261=CARTESIAN_POINT('Ctrl Pts',(111.502680316993,4.5231770881539,132.740539882081));
#43262=CARTESIAN_POINT('Ctrl Pts',(111.494919874479,4.57352286324126,132.613247480228));
#43263=CARTESIAN_POINT('Ctrl Pts',(111.487146974214,4.62394945783614,132.48575073731));
#43264=CARTESIAN_POINT('Ctrl Pts',(111.479374073948,4.66898724527533,132.356278894748));
#43265=CARTESIAN_POINT('Ctrl Pts',(111.471601173683,4.70850585003369,132.225330611161));
#43266=CARTESIAN_POINT('Ctrl Pts',(111.464110837921,4.74658785396819,132.09914262752));
#43267=CARTESIAN_POINT('Ctrl Pts',(111.456620502159,4.77954490387742,131.971583982118));
#43268=CARTESIAN_POINT('Ctrl Pts',(111.449130166397,4.80730564036021,131.843107719926));
#43269=CARTESIAN_POINT('Ctrl Pts',(111.441355832278,4.8361189336041,131.709760241205));
#43270=CARTESIAN_POINT('Ctrl Pts',(111.433581498159,4.85942537042342,131.575001784493));
#43271=CARTESIAN_POINT('Ctrl Pts',(111.425807164039,4.8770893791242,131.439326955677));
#43272=CARTESIAN_POINT('Ctrl Pts',(111.418042411092,4.89473161851294,131.303819333961));
#43273=CARTESIAN_POINT('Ctrl Pts',(111.410277658145,4.90674521575874,131.167397971176));
#43274=CARTESIAN_POINT('Ctrl Pts',(111.402512905198,4.91304513739603,131.030569681065));
#43275=CARTESIAN_POINT('Ctrl Pts',(111.394755864313,4.91933880186232,130.893877290742));
#43276=CARTESIAN_POINT('Ctrl Pts',(111.386998823428,4.91993006616789,130.756779165427));
#43277=CARTESIAN_POINT('Ctrl Pts',(111.379241782543,4.91478548453854,130.61978894187));
#43278=CARTESIAN_POINT('Ctrl Pts',(111.371490591303,4.90964478247818,130.482902023705));
#43279=CARTESIAN_POINT('Ctrl Pts',(111.363739400063,4.89877685863359,130.346123234446));
#43280=CARTESIAN_POINT('Ctrl Pts',(111.355988208823,4.88220031990499,130.209967566783));
#43281=CARTESIAN_POINT('Ctrl Pts',(111.348240312046,4.86563082664764,130.073869768911));
#43282=CARTESIAN_POINT('Ctrl Pts',(111.340492415269,4.84335759141013,129.93839495317));
#43283=CARTESIAN_POINT('Ctrl Pts',(111.332744518491,4.81545117037186,129.804054120404));
#43284=CARTESIAN_POINT('Ctrl Pts',(111.324998242407,4.78755058675529,129.669741388845));
#43285=CARTESIAN_POINT('Ctrl Pts',(111.317251966323,4.75401924058959,129.536562550998));
#43286=CARTESIAN_POINT('Ctrl Pts',(111.309505690239,4.7149789475052,129.405019134195));
#43287=CARTESIAN_POINT('Ctrl Pts',(111.301759356974,4.67593836623427,129.273474746368));
#43288=CARTESIAN_POINT('Ctrl Pts',(111.294013023709,4.6313888681365,129.14356617848));
#43289=CARTESIAN_POINT('Ctrl Pts',(111.286266690443,4.58150224612414,129.01578011022));
#43290=CARTESIAN_POINT('Ctrl Pts',(111.27851862244,4.53160445234873,128.887965425155));
#43291=CARTESIAN_POINT('Ctrl Pts',(111.270770554437,4.47636729847742,128.762274549675));
#43292=CARTESIAN_POINT('Ctrl Pts',(111.263022486434,4.41601069548345,128.639174112926));
#43293=CARTESIAN_POINT('Ctrl Pts',(111.255266183692,4.35558994477336,128.515942843567));
#43294=CARTESIAN_POINT('Ctrl Pts',(111.247509880951,4.2900390483252,128.395307864252));
#43295=CARTESIAN_POINT('Ctrl Pts',(111.239753578209,4.21962413087738,128.277711600267));
#43296=CARTESIAN_POINT('Ctrl Pts',(111.231993135694,4.14917163086796,128.160052571615));
#43297=CARTESIAN_POINT('Ctrl Pts',(111.22423269318,4.07385015156888,128.045435816543));
#43298=CARTESIAN_POINT('Ctrl Pts',(111.216472250666,3.99396856997989,127.934273837604));
#43299=CARTESIAN_POINT('Ctrl Pts',(111.208699350401,3.91395875538463,127.822933411588));
#43300=CARTESIAN_POINT('Ctrl Pts',(111.200926450135,3.82937445162395,127.715059152049));
#43301=CARTESIAN_POINT('Ctrl Pts',(111.19315354987,3.7405647231614,127.611030284772));
#43302=CARTESIAN_POINT('Ctrl Pts',(111.185663214108,3.65498345202751,127.510783128855));
#43303=CARTESIAN_POINT('Ctrl Pts',(111.178172878346,3.56547884150072,127.414106865743));
#43304=CARTESIAN_POINT('Ctrl Pts',(111.170682542584,3.47239347964619,127.321306413995));
#43305=CARTESIAN_POINT('Ctrl Pts',(111.162908208465,3.3757787580033,127.224987404912));
#43306=CARTESIAN_POINT('Ctrl Pts',(111.155133874346,3.27500035020651,127.132538802033));
#43307=CARTESIAN_POINT('Ctrl Pts',(111.147359540227,3.17040110238271,127.044342012225));
#43308=CARTESIAN_POINT('Ctrl Pts',(111.13959478728,3.0659307637839,126.956253917078));
#43309=CARTESIAN_POINT('Ctrl Pts',(111.131830034333,2.95764925037871,126.87240745861));
#43310=CARTESIAN_POINT('Ctrl Pts',(111.124065281385,2.84593699626002,126.793148123093));
#43311=CARTESIAN_POINT('Ctrl Pts',(111.1163082405,2.7343356963266,126.713967509064));
#43312=CARTESIAN_POINT('Ctrl Pts',(111.108551199615,2.61931075347786,126.639365176118));
#43313=CARTESIAN_POINT('Ctrl Pts',(111.10079415873,2.50127622660025,126.569646896339));
#43314=CARTESIAN_POINT('Ctrl Pts',(111.09304296749,2.38333071047802,126.499981191659));
#43315=CARTESIAN_POINT('Ctrl Pts',(111.08529177625,2.26238046299699,126.435192407183));
#43316=CARTESIAN_POINT('Ctrl Pts',(111.07754058501,2.13886881957718,126.375543254529));
#43317=CARTESIAN_POINT('Ctrl Pts',(111.069792688233,2.01540967190009,126.315919454355));
#43318=CARTESIAN_POINT('Ctrl Pts',(111.062044791456,1.8893916448709,126.261431110907));
#43319=CARTESIAN_POINT('Ctrl Pts',(111.054296894679,1.76128279531167,126.21229507171));
#43320=CARTESIAN_POINT('Ctrl Pts',(111.046550618595,1.63320074336187,126.163169310713));
#43321=CARTESIAN_POINT('Ctrl Pts',(111.038804342511,1.50302910360973,126.119393766969));
#43322=CARTESIAN_POINT('Ctrl Pts',(111.031058066427,1.37125566952536,126.081137041311));
#43323=CARTESIAN_POINT('Ctrl Pts',(111.023311733161,1.2394812627197,126.04288003325));
#43324=CARTESIAN_POINT('Ctrl Pts',(111.015565399896,1.10610541344974,126.01014203357));
#43325=CARTESIAN_POINT('Ctrl Pts',(111.00781906663,0.971630437386399,125.983041570288));
#43326=CARTESIAN_POINT('Ctrl Pts',(111.000070998627,0.837125346584189,125.955935038046));
#43327=CARTESIAN_POINT('Ctrl Pts',(110.992322930624,0.701521022381416,125.934468631627));
#43328=CARTESIAN_POINT('Ctrl Pts',(110.984574862621,0.565328920347991,125.918709558156));
#43329=CARTESIAN_POINT('Ctrl Pts',(110.97681855988,0.428992071728189,125.902933735753));
#43330=CARTESIAN_POINT('Ctrl Pts',(110.969062257138,0.292066586370765,125.89287740844));
#43331=CARTESIAN_POINT('Ctrl Pts',(110.961305954396,0.155068536120264,125.88855581961));
#43332=CARTESIAN_POINT('Ctrl Pts',(110.953545511882,0.0179973658855062,
125.884231924218));
#43333=CARTESIAN_POINT('Ctrl Pts',(110.945785069368,-0.119146055662212,
125.885648862181));
#43334=CARTESIAN_POINT('Ctrl Pts',(110.938024626853,-0.255847722878992,
125.892769734237));
#43335=CARTESIAN_POINT('Ctrl Pts',(110.930251726588,-0.392768835747792,
125.899902037349));
#43336=CARTESIAN_POINT('Ctrl Pts',(110.922478826322,-0.529246387724954,
125.912756535399));
#43337=CARTESIAN_POINT('Ctrl Pts',(110.914705926057,-0.664772647547478,
125.931244531367));
#43338=CARTESIAN_POINT('Ctrl Pts',(110.907215590295,-0.795372186455674,
125.949060442113));
#43339=CARTESIAN_POINT('Ctrl Pts',(110.899725254533,-0.925088092888324,
125.972107324191));
#43340=CARTESIAN_POINT('Ctrl Pts',(110.892234918771,-1.05347865300944,126.000261764487));
#43341=CARTESIAN_POINT('Ctrl Pts',(110.884460584652,-1.18673718024092,126.029483688944));
#43342=CARTESIAN_POINT('Ctrl Pts',(110.876686250533,-1.31898999918757,126.064300689578));
#43343=CARTESIAN_POINT('Ctrl Pts',(110.868911916414,-1.44973090474329,126.104630479959));
#43344=CARTESIAN_POINT('Ctrl Pts',(110.861147163467,-1.58031068381783,126.144910567478));
#43345=CARTESIAN_POINT('Ctrl Pts',(110.853382410519,-1.70938188690138,126.190689812532));
#43346=CARTESIAN_POINT('Ctrl Pts',(110.845617657572,-1.83644821268875,126.241834888914));
#43347=CARTESIAN_POINT('Ctrl Pts',(110.837860616687,-1.96338833440977,126.292929167285));
#43348=CARTESIAN_POINT('Ctrl Pts',(110.830103575802,-2.08832718121577,126.349378526158));
#43349=CARTESIAN_POINT('Ctrl Pts',(110.822346534917,-2.21078368944838,126.410999883348));
#43350=CARTESIAN_POINT('Ctrl Pts',(110.814595343677,-2.33314785227431,126.472574771392));
#43351=CARTESIAN_POINT('Ctrl Pts',(110.806844152437,-2.45303305470429,126.539313719524));
#43352=CARTESIAN_POINT('Ctrl Pts',(110.799092961197,-2.56997863639138,126.610985739143));
#43353=CARTESIAN_POINT('Ctrl Pts',(110.79134506442,-2.68687451308767,126.682627296242));
#43354=CARTESIAN_POINT('Ctrl Pts',(110.783597167643,-2.80083292139165,126.759197550812));
#43355=CARTESIAN_POINT('Ctrl Pts',(110.775849270866,-2.9114184251922,126.840419924777));
#43356=CARTESIAN_POINT('Ctrl Pts',(110.768102994782,-3.02198079688953,126.921625308772));
#43357=CARTESIAN_POINT('Ctrl Pts',(110.760356718698,-3.12917135253408,127.007480645277));
#43358=CARTESIAN_POINT('Ctrl Pts',(110.752610442613,-3.23258457918507,127.097666672699));
#43359=CARTESIAN_POINT('Ctrl Pts',(110.744864109348,-3.33599856920837,127.187853365853));
#43360=CARTESIAN_POINT('Ctrl Pts',(110.737117776083,-3.43563487994359,127.282370556746));
#43361=CARTESIAN_POINT('Ctrl Pts',(110.729371442817,-3.53112227652322,127.380859700268));
#43362=CARTESIAN_POINT('Ctrl Pts',(110.721623374814,-3.62663105684415,127.479370899751));
#43363=CARTESIAN_POINT('Ctrl Pts',(110.713875306811,-3.71798880207566,127.581855541202));
#43364=CARTESIAN_POINT('Ctrl Pts',(110.706127238808,-3.80486251473392,127.687919649655));
#43365=CARTESIAN_POINT('Ctrl Pts',(110.698370936067,-3.89182855780733,127.794096484305));
#43366=CARTESIAN_POINT('Ctrl Pts',(110.690614633325,-3.97430080021255,127.903860082515));
#43367=CARTESIAN_POINT('Ctrl Pts',(110.682858330583,-4.05198746781253,128.016784497854));
#43368=CARTESIAN_POINT('Ctrl Pts',(110.675097888069,-4.12971559912601,128.129769184353));
#43369=CARTESIAN_POINT('Ctrl Pts',(110.667337445555,-4.20265285834884,128.245917718584));
#43370=CARTESIAN_POINT('Ctrl Pts',(110.65957700304,-4.27055245726914,128.364777708089));
#43371=CARTESIAN_POINT('Ctrl Pts',(110.651804102775,-4.33856105465366,128.483828502201));
#43372=CARTESIAN_POINT('Ctrl Pts',(110.64403120251,-4.40151565187973,128.605599102109));
#43373=CARTESIAN_POINT('Ctrl Pts',(110.636258302244,-4.45921643111155,128.729614396216));
#43374=CARTESIAN_POINT('Ctrl Pts',(110.628767966482,-4.51481964167916,128.849121422008));
#43375=CARTESIAN_POINT('Ctrl Pts',(110.62127763072,-4.56554426297981,128.97071249055));
#43376=CARTESIAN_POINT('Ctrl Pts',(110.613787294958,-4.61125536884304,129.093949267681));
#43377=CARTESIAN_POINT('Ctrl Pts',(110.604821183356,-4.66597265917731,129.241466646374));
#43378=CARTESIAN_POINT('Ctrl Pts',(110.595855071755,-4.71365072512056,129.391728716157));
#43379=CARTESIAN_POINT('Ctrl Pts',(110.586888960154,-4.75404349510082,129.544101315204));
#43380=CARTESIAN_POINT('Ctrl Pts',(110.586136850671,-4.75743178499588,129.556882873337));
#43381=CARTESIAN_POINT('Ctrl Pts',(110.585384741188,-4.76076883944629,129.569679268592));
#43382=CARTESIAN_POINT('Ctrl Pts',(110.584632631705,-4.76405452823407,129.582490119308));
#43383=CARTESIAN_POINT('Ctrl Pts',(112.334951030737,-4.76405452823405,129.582490119308));
#43384=CARTESIAN_POINT('Ctrl Pts',(112.327186197236,-4.79809550206713,129.71521535964));
#43385=CARTESIAN_POINT('Ctrl Pts',(112.319421363735,-4.82655156713842,129.849230819445));
#43386=CARTESIAN_POINT('Ctrl Pts',(112.311656530233,-4.84935412252618,129.984026748438));
#43387=CARTESIAN_POINT('Ctrl Pts',(112.303880958532,-4.87218821219024,130.119009090401));
#43388=CARTESIAN_POINT('Ctrl Pts',(112.296105386831,-4.88935313945802,130.254773669745));
#43389=CARTESIAN_POINT('Ctrl Pts',(112.288329815129,-4.90083223329311,130.390807134187));
#43390=CARTESIAN_POINT('Ctrl Pts',(112.287044222698,-4.90273015626524,130.413298546911));
#43391=CARTESIAN_POINT('Ctrl Pts',(112.285758630266,-4.90447276423942,130.435797314352));
#43392=CARTESIAN_POINT('Ctrl Pts',(112.284473037835,-4.90606011881192,130.458301123977));
#43393=CARTESIAN_POINT('Ctrl Pts',(112.277935170553,-4.9141325944039,130.572744019767));
#43394=CARTESIAN_POINT('Ctrl Pts',(112.271397303272,-4.91820122599546,130.687472648211));
#43395=CARTESIAN_POINT('Ctrl Pts',(112.264859435991,-4.91824956414179,130.802290033335));
#43396=CARTESIAN_POINT('',(112.610140563967,-4.91824789580415,130.808910114032));
#43397=CARTESIAN_POINT('Ctrl Pts',(112.680164151027,-4.76405452823403,129.582490119308));
#43398=CARTESIAN_POINT('Ctrl Pts',(112.672511249089,-4.79775195816247,129.713875887169));
#43399=CARTESIAN_POINT('Ctrl Pts',(112.66485834715,-4.82600509894512,129.846637463952));
#43400=CARTESIAN_POINT('Ctrl Pts',(112.657205445212,-4.84871854275895,129.980278367056));
#43401=CARTESIAN_POINT('Ctrl Pts',(112.649361298345,-4.87199959229714,130.117258937285));
#43402=CARTESIAN_POINT('Ctrl Pts',(112.641517151477,-4.8894603380112,130.255162923673));
#43403=CARTESIAN_POINT('Ctrl Pts',(112.63367300461,-4.901054442012,130.393448925186));
#43404=CARTESIAN_POINT('Ctrl Pts',(112.625828857743,-4.91264854601281,130.5317349267));
#43405=CARTESIAN_POINT('Ctrl Pts',(112.617984710875,-4.91837601863491,130.67040249058));
#43406=CARTESIAN_POINT('Ctrl Pts',(112.610140564008,-4.91824789580482,130.808910113306));
#43407=CARTESIAN_POINT('Ctrl Pts',(112.610140563967,-4.91824789580415,130.808910114032));
#43408=CARTESIAN_POINT('Ctrl Pts',(112.600025508912,-4.91808268093644,130.987516182108));
#43409=CARTESIAN_POINT('Ctrl Pts',(112.589910453858,-4.90818496828126,131.165688321249));
#43410=CARTESIAN_POINT('Ctrl Pts',(112.579795398803,-4.88871656797851,131.342536592942));
#43411=CARTESIAN_POINT('Ctrl Pts',(112.56942060632,-4.86874825223235,131.523926027792));
#43412=CARTESIAN_POINT('Ctrl Pts',(112.559045813837,-4.83871138131471,131.703923091685));
#43413=CARTESIAN_POINT('Ctrl Pts',(112.548671021353,-4.79882824532939,131.881593430995));
#43414=CARTESIAN_POINT('Ctrl Pts',(112.546891236065,-4.79198633318692,131.912072600245));
#43415=CARTESIAN_POINT('Ctrl Pts',(112.545111450777,-4.78485476703272,131.942483348665));
#43416=CARTESIAN_POINT('Ctrl Pts',(112.543331665489,-4.77743480839001,131.972821020867));
#43417=CARTESIAN_POINT('Ctrl Pts',(112.53555733137,-4.74502346190569,132.105339927322));
#43418=CARTESIAN_POINT('Ctrl Pts',(112.527782997251,-4.70704278471488,132.23671914871));
#43419=CARTESIAN_POINT('Ctrl Pts',(112.520008663132,-4.66358718707587,132.366454600347));
#43420=CARTESIAN_POINT('Ctrl Pts',(112.512243910184,-4.62018514457724,132.496030164635));
#43421=CARTESIAN_POINT('Ctrl Pts',(112.504479157237,-4.57132172982918,132.623965622747));
#43422=CARTESIAN_POINT('Ctrl Pts',(112.49671440429,-4.51714214050766,132.74976801576));
#43423=CARTESIAN_POINT('Ctrl Pts',(112.488957363405,-4.46301636311794,132.875445460064));
#43424=CARTESIAN_POINT('Ctrl Pts',(112.48120032252,-4.40358507243615,132.998993698604));
#43425=CARTESIAN_POINT('Ctrl Pts',(112.473443281635,-4.3390428421268,133.119936199724));
#43426=CARTESIAN_POINT('Ctrl Pts',(112.465692090395,-4.27454928361557,133.240787497163));
#43427=CARTESIAN_POINT('Ctrl Pts',(112.457940899155,-4.20495264035351,133.359036624882));
#43428=CARTESIAN_POINT('Ctrl Pts',(112.450189707915,-4.1304948889987,133.474228598283));
#43429=CARTESIAN_POINT('Ctrl Pts',(112.442441811138,-4.05606878417434,133.589371612022));
#43430=CARTESIAN_POINT('Ctrl Pts',(112.434693914361,-3.97678589236462,133.701459728137));
#43431=CARTESIAN_POINT('Ctrl Pts',(112.426946017584,-3.89293316126326,133.810064273025));
#43432=CARTESIAN_POINT('Ctrl Pts',(112.419199741499,-3.80909797034559,133.918646100182));
#43433=CARTESIAN_POINT('Ctrl Pts',(112.411453465415,-3.72069508027764,134.023745496248));
#43434=CARTESIAN_POINT('Ctrl Pts',(112.403707189331,-3.62805339190574,134.124964726457));
#43435=CARTESIAN_POINT('Ctrl Pts',(112.395960856066,-3.53541101967394,134.226184703843));
#43436=CARTESIAN_POINT('Ctrl Pts',(112.388214522801,-3.43853005066551,134.323524169814));
#43437=CARTESIAN_POINT('Ctrl Pts',(112.380468189535,-3.33777783535336,134.416620600502));
#43438=CARTESIAN_POINT('Ctrl Pts',(112.372720121532,-3.23700305728123,134.509737879491));
#43439=CARTESIAN_POINT('Ctrl Pts',(112.364972053529,-3.13235559489112,134.598609967135));
#43440=CARTESIAN_POINT('Ctrl Pts',(112.357223985526,-3.02423730071441,134.682913416158));
#43441=CARTESIAN_POINT('Ctrl Pts',(112.349467682784,-2.91600409712795,134.76730646389));
#43442=CARTESIAN_POINT('Ctrl Pts',(112.341711380043,-2.80429300170543,134.847120932622));
#43443=CARTESIAN_POINT('Ctrl Pts',(112.333955077301,-2.68953683999136,134.922075353779));
#43444=CARTESIAN_POINT('Ctrl Pts',(112.326194634787,-2.57471942945855,134.997069780369));
#43445=CARTESIAN_POINT('Ctrl Pts',(112.318434192272,-2.45685405002427,135.067198790898));
#43446=CARTESIAN_POINT('Ctrl Pts',(112.310673749758,-2.33639888610519,135.132226524397));
#43447=CARTESIAN_POINT('Ctrl Pts',(112.302900849493,-2.2157503568634,135.197358646186));
#43448=CARTESIAN_POINT('Ctrl Pts',(112.295127949227,-2.09250408713119,135.257372955404));
#43449=CARTESIAN_POINT('Ctrl Pts',(112.287355048962,-1.96713984676166,135.312081093126));
#43450=CARTESIAN_POINT('Ctrl Pts',(112.2798647132,-1.84633291230294,135.36480045224));
#43451=CARTESIAN_POINT('Ctrl Pts',(112.272374377438,-1.72355960793693,135.412592615722));
#43452=CARTESIAN_POINT('Ctrl Pts',(112.264884041676,-1.59926137945267,135.455333215065));
#43453=CARTESIAN_POINT('Ctrl Pts',(112.257109707557,-1.47025034585598,135.499694337224));
#43454=CARTESIAN_POINT('Ctrl Pts',(112.249335373438,-1.33918780229806,135.538753796111));
#43455=CARTESIAN_POINT('Ctrl Pts',(112.241561039319,-1.20654888055078,135.572318551665));
#43456=CARTESIAN_POINT('Ctrl Pts',(112.233796286372,-1.07407342442037,135.605841941658));
#43457=CARTESIAN_POINT('Ctrl Pts',(112.226031533425,-0.9400258309641,135.633884007054));
#43458=CARTESIAN_POINT('Ctrl Pts',(112.218266780477,-0.804899323374295,
135.65630045043));
#43459=CARTESIAN_POINT('Ctrl Pts',(112.210509739592,-0.669907025336778,
135.678694629479));
#43460=CARTESIAN_POINT('Ctrl Pts',(112.202752698707,-0.533838328881824,
135.695474242211));
#43461=CARTESIAN_POINT('Ctrl Pts',(112.194995657822,-0.397199325406341,
135.706545411961));
#43462=CARTESIAN_POINT('Ctrl Pts',(112.187244466582,-0.260663362466276,
135.717608232856));
#43463=CARTESIAN_POINT('Ctrl Pts',(112.179493275342,-0.123558336651192,
135.722971147728));
#43464=CARTESIAN_POINT('Ctrl Pts',(112.171742084102,0.0136021663159125,
135.722591808103));
#43465=CARTESIAN_POINT('Ctrl Pts',(112.163994187325,0.15070437241038,135.722212629708));
#43466=CARTESIAN_POINT('Ctrl Pts',(112.156246290548,0.287861618614307,135.716096052085));
#43467=CARTESIAN_POINT('Ctrl Pts',(112.148498393771,0.424558147445553,135.704251783902));
#43468=CARTESIAN_POINT('Ctrl Pts',(112.140752117687,0.561226082309897,135.692409993284));
#43469=CARTESIAN_POINT('Ctrl Pts',(112.133005841603,0.697433102231994,135.674842928939));
#43470=CARTESIAN_POINT('Ctrl Pts',(112.125259565519,0.832666802748191,135.651612319108));
#43471=CARTESIAN_POINT('Ctrl Pts',(112.117513232253,0.967901501528752,135.628381537794));
#43472=CARTESIAN_POINT('Ctrl Pts',(112.109766898988,1.10216248124526,135.599487193761));
#43473=CARTESIAN_POINT('Ctrl Pts',(112.102020565722,1.23494617839759,135.565042396362));
#43474=CARTESIAN_POINT('Ctrl Pts',(112.09427249772,1.36775961153815,135.53058988529));
#43475=CARTESIAN_POINT('Ctrl Pts',(112.086524429717,1.49909472543948,135.490584545604));
#43476=CARTESIAN_POINT('Ctrl Pts',(112.078776361714,1.62846218363884,135.445189636067));
#43477=CARTESIAN_POINT('Ctrl Pts',(112.071020058972,1.75796713511235,135.39974648028));
#43478=CARTESIAN_POINT('Ctrl Pts',(112.06326375623,1.88549988389046,135.348902441804));
#43479=CARTESIAN_POINT('Ctrl Pts',(112.055507453488,2.01058966971157,135.29286952839));
#43480=CARTESIAN_POINT('Ctrl Pts',(112.047747010974,2.13574621971792,135.236806708523));
#43481=CARTESIAN_POINT('Ctrl Pts',(112.03998656846,2.25845685903948,135.175549669872));
#43482=CARTESIAN_POINT('Ctrl Pts',(112.032226125945,2.37827549129213,135.109356407346));
#43483=CARTESIAN_POINT('Ctrl Pts',(112.02445322568,2.49828646705019,135.043056885518));
#43484=CARTESIAN_POINT('Ctrl Pts',(112.016680325415,2.61539582433666,134.97180550834));
#43485=CARTESIAN_POINT('Ctrl Pts',(112.008907425149,2.7291857641288,134.895904107177));
#43486=CARTESIAN_POINT('Ctrl Pts',(112.001417089387,2.83883915299046,134.82276191313));
#43487=CARTESIAN_POINT('Ctrl Pts',(111.993926753625,2.94541002358644,134.745302086796));
#43488=CARTESIAN_POINT('Ctrl Pts',(111.986436417863,3.04855512894029,134.663828804805));
#43489=CARTESIAN_POINT('Ctrl Pts',(111.978662083744,3.15561101231339,134.579266438565));
#43490=CARTESIAN_POINT('Ctrl Pts',(111.970887749625,3.25931534746992,134.490112400395));
#43491=CARTESIAN_POINT('Ctrl Pts',(111.963113415506,3.3592489040113,134.396662089241));
#43492=CARTESIAN_POINT('Ctrl Pts',(111.955348662559,3.45905930137556,134.303326947244));
#43493=CARTESIAN_POINT('Ctrl Pts',(111.947583909612,3.55510788374279,134.205706331756));
#43494=CARTESIAN_POINT('Ctrl Pts',(111.939819156664,3.6470066504228,134.104137209136));
#43495=CARTESIAN_POINT('Ctrl Pts',(111.932062115779,3.73881414195219,134.0026689664));
#43496=CARTESIAN_POINT('Ctrl Pts',(111.924305074894,3.82647975946374,133.897260308953));
#43497=CARTESIAN_POINT('Ctrl Pts',(111.916548034009,3.909650967098,133.78828628319));
#43498=CARTESIAN_POINT('Ctrl Pts',(111.908796842769,3.9927594546776,133.679394435587));
#43499=CARTESIAN_POINT('Ctrl Pts',(111.901045651529,4.07138004227451,133.566942880837));
#43500=CARTESIAN_POINT('Ctrl Pts',(111.893294460289,4.14519949529019,133.451340822771));
#43501=CARTESIAN_POINT('Ctrl Pts',(111.885546563512,4.21898757306915,133.335787898663));
#43502=CARTESIAN_POINT('Ctrl Pts',(111.877798666735,4.28797836490992,133.217087463325));
#43503=CARTESIAN_POINT('Ctrl Pts',(111.870050769958,4.35190125947188,133.095678685907));
#43504=CARTESIAN_POINT('Ctrl Pts',(111.862304493874,4.41581078274232,132.974295304588));
#43505=CARTESIAN_POINT('Ctrl Pts',(111.85455821779,4.47465433529296,132.850205053766));
#43506=CARTESIAN_POINT('Ctrl Pts',(111.846811941705,4.52820688371257,132.723872399452));
#43507=CARTESIAN_POINT('Ctrl Pts',(111.83906560844,4.58175982744488,132.597538812578));
#43508=CARTESIAN_POINT('Ctrl Pts',(111.831319275175,4.63002153652351,132.468963149141));
#43509=CARTESIAN_POINT('Ctrl Pts',(111.823572941909,4.67281498467728,132.338630209742));
#43510=CARTESIAN_POINT('Ctrl Pts',(111.815824873906,4.71561801612706,132.208268083185));
#43511=CARTESIAN_POINT('Ctrl Pts',(111.808076805903,4.75295022794133,132.076148268971));
#43512=CARTESIAN_POINT('Ctrl Pts',(111.8003287379,4.78468447602984,131.942770705074));
#43513=CARTESIAN_POINT('Ctrl Pts',(111.792572435159,4.81645245165488,131.809251385914));
#43514=CARTESIAN_POINT('Ctrl Pts',(111.784816132417,4.84261048798266,131.674472027722));
#43515=CARTESIAN_POINT('Ctrl Pts',(111.777059829675,4.86308249571701,131.538943289803));
#43516=CARTESIAN_POINT('Ctrl Pts',(111.769299387161,4.8835654299783,131.403342216116));
#43517=CARTESIAN_POINT('Ctrl Pts',(111.761538944647,4.89835624639847,131.266991354232));
#43518=CARTESIAN_POINT('Ctrl Pts',(111.753778502132,4.90743087740996,131.130405470222));
#43519=CARTESIAN_POINT('Ctrl Pts',(111.746005601867,4.91652007582474,130.993600326426));
#43520=CARTESIAN_POINT('Ctrl Pts',(111.738232701602,4.91987474242937,130.856559797655));
#43521=CARTESIAN_POINT('Ctrl Pts',(111.730459801336,4.91752298592275,130.719798537286));
#43522=CARTESIAN_POINT('Ctrl Pts',(111.722969465574,4.91525672168886,130.588008893211));
#43523=CARTESIAN_POINT('Ctrl Pts',(111.715479129812,4.9076917347131,130.456478873341));
#43524=CARTESIAN_POINT('Ctrl Pts',(111.70798879405,4.89489840403446,130.325661675974));
#43525=CARTESIAN_POINT('Ctrl Pts',(111.700214459931,4.88162001033469,130.189884504809));
#43526=CARTESIAN_POINT('Ctrl Pts',(111.692440125812,4.86266691931936,130.054445175243));
#43527=CARTESIAN_POINT('Ctrl Pts',(111.684665791693,4.83806105421889,129.91985606803));
#43528=CARTESIAN_POINT('Ctrl Pts',(111.676901038746,4.81348551364809,129.785432829863));
#43529=CARTESIAN_POINT('Ctrl Pts',(111.669136285799,4.78327112996479,129.651858110093));
#43530=CARTESIAN_POINT('Ctrl Pts',(111.661371532851,4.74749167866028,129.519640483237));
#43531=CARTESIAN_POINT('Ctrl Pts',(111.653614491966,4.71174776401121,129.387554176792));
#43532=CARTESIAN_POINT('Ctrl Pts',(111.645857451081,4.67044988278964,129.25682265586));
#43533=CARTESIAN_POINT('Ctrl Pts',(111.638100410196,4.62372301790605,129.127945240583));
#43534=CARTESIAN_POINT('Ctrl Pts',(111.630349218956,4.57703139011475,128.999165012767));
#43535=CARTESIAN_POINT('Ctrl Pts',(111.622598027716,4.52491906032104,128.872236473647));
#43536=CARTESIAN_POINT('Ctrl Pts',(111.614846836476,4.46756099234455,128.747644341027));
#43537=CARTESIAN_POINT('Ctrl Pts',(111.607098939699,4.41022730307703,128.623105163387));
#43538=CARTESIAN_POINT('Ctrl Pts',(111.599351042922,4.34765247324044,128.500900771571));
#43539=CARTESIAN_POINT('Ctrl Pts',(111.591603146145,4.28005971623759,128.381496220217));
#43540=CARTESIAN_POINT('Ctrl Pts',(111.583856870061,4.21248109818238,128.262116645721));
#43541=CARTESIAN_POINT('Ctrl Pts',(111.576110593977,4.13988683323489,128.145536086782));
#43542=CARTESIAN_POINT('Ctrl Pts',(111.568364317892,4.06254605374773,128.032194925606));
#43543=CARTESIAN_POINT('Ctrl Pts',(111.560617984627,3.98520470334852,127.918852927771));
#43544=CARTESIAN_POINT('Ctrl Pts',(111.552871651362,3.90311698886153,127.808750698358));
#43545=CARTESIAN_POINT('Ctrl Pts',(111.545125318096,3.81659509973955,127.702299221148));
#43546=CARTESIAN_POINT('Ctrl Pts',(111.537377250093,3.7300538346404,127.595823904869));
#43547=CARTESIAN_POINT('Ctrl Pts',(111.52962918209,3.63907666549011,127.493001270978));
#43548=CARTESIAN_POINT('Ctrl Pts',(111.521881114087,3.54401547977851,127.394208518086));
#43549=CARTESIAN_POINT('Ctrl Pts',(111.514124811346,3.44885326190744,127.29531076708));
#43550=CARTESIAN_POINT('Ctrl Pts',(111.506368508604,3.34959862829066,127.200451735011));
#43551=CARTESIAN_POINT('Ctrl Pts',(111.498612205862,3.24664008294344,127.109971461789));
#43552=CARTESIAN_POINT('Ctrl Pts',(111.490851763348,3.14362658552047,127.01944289652));
#43553=CARTESIAN_POINT('Ctrl Pts',(111.483091320833,3.03690554132065,126.933297992364));
#43554=CARTESIAN_POINT('Ctrl Pts',(111.475330878319,2.92689702851175,126.851835241684));
#43555=CARTESIAN_POINT('Ctrl Pts',(111.467557978054,2.81671192027207,126.770241719765));
#43556=CARTESIAN_POINT('Ctrl Pts',(111.459785077788,2.70322912146974,126.69334559054));
#43557=CARTESIAN_POINT('Ctrl Pts',(111.452012177523,2.58689681800423,126.621401388085));
#43558=CARTESIAN_POINT('Ctrl Pts',(111.444521841761,2.47479348679355,126.552072538606));
#43559=CARTESIAN_POINT('Ctrl Pts',(111.437031505999,2.36004449570761,126.487341987861));
#43560=CARTESIAN_POINT('Ctrl Pts',(111.429541170237,2.24306917490219,126.427395488723));
#43561=CARTESIAN_POINT('Ctrl Pts',(111.421766836118,2.12165869925411,126.36517609985));
#43562=CARTESIAN_POINT('Ctrl Pts',(111.413992501999,1.9974651468001,126.307913606181));
#43563=CARTESIAN_POINT('Ctrl Pts',(111.40621816788,1.87093144802186,126.255866517394));
#43564=CARTESIAN_POINT('Ctrl Pts',(111.398453414933,1.74455369071881,126.203883571992));
#43565=CARTESIAN_POINT('Ctrl Pts',(111.390688661986,1.61584188353536,126.157103389921));
#43566=CARTESIAN_POINT('Ctrl Pts',(111.382923909038,1.48526378207196,126.115738798719));
#43567=CARTESIAN_POINT('Ctrl Pts',(111.375166868153,1.35481537261976,126.074415291413));
#43568=CARTESIAN_POINT('Ctrl Pts',(111.367409827268,1.22250472799417,126.038496788143));
#43569=CARTESIAN_POINT('Ctrl Pts',(111.359652786383,1.08881949668664,126.00814803198));
#43570=CARTESIAN_POINT('Ctrl Pts',(111.351901595143,0.955235078452045,125.97782216205));
#43571=CARTESIAN_POINT('Ctrl Pts',(111.344150403903,0.82027851651953,125.953057765207));
#43572=CARTESIAN_POINT('Ctrl Pts',(111.336399212663,0.684452189924092,125.933969641247));
#43573=CARTESIAN_POINT('Ctrl Pts',(111.328651315886,0.548683593140558,125.914889630249));
#43574=CARTESIAN_POINT('Ctrl Pts',(111.320903419109,0.41204635329608,125.901481148018));
#43575=CARTESIAN_POINT('Ctrl Pts',(111.313155522332,0.275052386324319,125.893807772185));
#43576=CARTESIAN_POINT('Ctrl Pts',(111.305409246248,0.1380870755372,125.886136001458));
#43577=CARTESIAN_POINT('Ctrl Pts',(111.297662970164,0.000765576151350478,
125.884196972789));
#43578=CARTESIAN_POINT('Ctrl Pts',(111.28991669408,-0.136396133200972,125.888002294849));
#43579=CARTESIAN_POINT('Ctrl Pts',(111.282170360814,-0.273558855049874,
125.891807644999));
#43580=CARTESIAN_POINT('Ctrl Pts',(111.274424027549,-0.410561393696745,
125.901357419647));
#43581=CARTESIAN_POINT('Ctrl Pts',(111.266677694283,-0.546889230820648,
125.916611111739));
#43582=CARTESIAN_POINT('Ctrl Pts',(111.258929626281,-0.683247597618353,
125.931868219789));
#43583=CARTESIAN_POINT('Ctrl Pts',(111.251181558278,-0.818930573765801,
125.952831743602));
#43584=CARTESIAN_POINT('Ctrl Pts',(111.243433490275,-0.953430607605556,
125.979409515329));
#43585=CARTESIAN_POINT('Ctrl Pts',(111.235677187533,-1.08807358968194,126.006015534227));
#43586=CARTESIAN_POINT('Ctrl Pts',(111.227920884791,-1.22153073380778,126.038247644632));
#43587=CARTESIAN_POINT('Ctrl Pts',(111.220164582049,-1.35330595886695,126.07596278699));
#43588=CARTESIAN_POINT('Ctrl Pts',(111.212404139535,-1.48515151633141,126.113698059055));
#43589=CARTESIAN_POINT('Ctrl Pts',(111.204643697021,-1.61531299514427,126.156922071135));
#43590=CARTESIAN_POINT('Ctrl Pts',(111.196883254507,-1.74331220271663,126.205442741983));
#43591=CARTESIAN_POINT('Ctrl Pts',(111.189110354241,-1.87151688598021,126.254041302519));
#43592=CARTESIAN_POINT('Ctrl Pts',(111.181337453976,-1.997552002033,126.307953359013));
#43593=CARTESIAN_POINT('Ctrl Pts',(111.17356455371,-2.12096114872149,126.366939421859));
#43594=CARTESIAN_POINT('Ctrl Pts',(111.166074217948,-2.23988406207946,126.423781192743));
#43595=CARTESIAN_POINT('Ctrl Pts',(111.158583882186,-2.35636834026842,126.485334324995));
#43596=CARTESIAN_POINT('Ctrl Pts',(111.151093546424,-2.47003104594351,126.551346428244));
#43597=CARTESIAN_POINT('Ctrl Pts',(111.143318048751,-2.58802096408834,126.619871654813));
#43598=CARTESIAN_POINT('Ctrl Pts',(111.135542551079,-2.70334402827948,126.693419189844));
#43599=CARTESIAN_POINT('Ctrl Pts',(111.127767053406,-2.81554312866998,126.771756006015));
#43600=CARTESIAN_POINT('Ctrl Pts',(111.120001390163,-2.92760031993348,126.849993741988));
#43601=CARTESIAN_POINT('Ctrl Pts',(111.112235726919,-3.03654109228594,126.93300848329));
#43602=CARTESIAN_POINT('Ctrl Pts',(111.104470063675,-3.14193340809388,127.020521625008));
#43603=CARTESIAN_POINT('Ctrl Pts',(111.0967138177,-3.24719791669754,127.107928641247));
#43604=CARTESIAN_POINT('Ctrl Pts',(111.088957571725,-3.34892224050942,127.1998229446));
#43605=CARTESIAN_POINT('Ctrl Pts',(111.081201325749,-3.44670432087686,127.29588339989));
#43606=CARTESIAN_POINT('Ctrl Pts',(111.073450420698,-3.54441906883546,127.391877708277));
#43607=CARTESIAN_POINT('Ctrl Pts',(111.065699515648,-3.6381966964812,127.49203218828));
#43608=CARTESIAN_POINT('Ctrl Pts',(111.057948610597,-3.72766911730934,127.595986260612));
#43609=CARTESIAN_POINT('Ctrl Pts',(111.050201364159,-3.81709930501157,127.699891264132));
#43610=CARTESIAN_POINT('Ctrl Pts',(111.042454117721,-3.90222807564878,127.807591995144));
#43611=CARTESIAN_POINT('Ctrl Pts',(111.034706871283,-3.98272532301652,127.918692226378));
#43612=CARTESIAN_POINT('Ctrl Pts',(111.026961603978,-4.06320200634288,128.02976407565));
#43613=CARTESIAN_POINT('Ctrl Pts',(111.019216336672,-4.13904929327087,128.144233379648));
#43614=CARTESIAN_POINT('Ctrl Pts',(111.011471069367,-4.20997862988462,128.261672473413));
#43615=CARTESIAN_POINT('Ctrl Pts',(111.003723969164,-4.28092475173514,128.379139358824));
#43616=CARTESIAN_POINT('Ctrl Pts',(110.995976868962,-4.34695039166321,128.499577105967));
#43617=CARTESIAN_POINT('Ctrl Pts',(110.98822976876,-4.40781144552144,128.622530806781));
#43618=CARTESIAN_POINT('Ctrl Pts',(110.980481686043,-4.46868021799213,128.745500101015));
#43619=CARTESIAN_POINT('Ctrl Pts',(110.972733603326,-4.52438293361868,128.870985630572));
#43620=CARTESIAN_POINT('Ctrl Pts',(110.964985520609,-4.57472279130914,128.998510555912));
#43621=CARTESIAN_POINT('Ctrl Pts',(110.95723183069,-4.62509907940227,129.126127769641));
#43622=CARTESIAN_POINT('Ctrl Pts',(110.949478140771,-4.67010462351842,129.255786959791));
#43623=CARTESIAN_POINT('Ctrl Pts',(110.941724450852,-4.70959178128307,129.386993933828));
#43624=CARTESIAN_POINT('Ctrl Pts',(110.93789460426,-4.72909601193425,129.451802120325));
#43625=CARTESIAN_POINT('Ctrl Pts',(110.934064757668,-4.747254666173,129.516987712106));
#43626=CARTESIAN_POINT('Ctrl Pts',(110.930234911077,-4.76405452823406,129.582490119308));
#43627=CARTESIAN_POINT('Origin',(213.235140564004,0.,130.804360617566));
#43628=CARTESIAN_POINT('',(108.834713077301,-4.76405452823407,129.582490119308));
#43629=CARTESIAN_POINT('',(109.179944404822,-4.76405452823403,129.582490119308));
#43630=CARTESIAN_POINT('',(213.235140564004,-4.76405452823405,129.582490119308));
#43631=CARTESIAN_POINT('',(110.514859436046,-4.91824876687394,130.800877853875));
#43632=CARTESIAN_POINT('Ctrl Pts',(110.514859435991,-4.91824876687464,130.800877854854));
#43633=CARTESIAN_POINT('Ctrl Pts',(110.507086929701,-4.91834630934749,130.938624289666));
#43634=CARTESIAN_POINT('Ctrl Pts',(110.499314423412,-4.91265269404362,131.07641604133));
#43635=CARTESIAN_POINT('Ctrl Pts',(110.491541917122,-4.901183229966,131.213733319147));
#43636=CARTESIAN_POINT('Ctrl Pts',(110.483769695216,-4.88971418553847,131.351045572736));
#43637=CARTESIAN_POINT('Ctrl Pts',(110.475997473311,-4.87246974426606,131.487883001353));
#43638=CARTESIAN_POINT('Ctrl Pts',(110.468225251405,-4.84951719909121,131.6237298861));
#43639=CARTESIAN_POINT('Ctrl Pts',(110.460451674612,-4.82656065272929,131.759600452265));
#43640=CARTESIAN_POINT('Ctrl Pts',(110.452678097819,-4.79789408591347,131.894479749222));
#43641=CARTESIAN_POINT('Ctrl Pts',(110.444904521026,-4.76363606073343,132.027861554787));
#43642=CARTESIAN_POINT('Ctrl Pts',(110.437127949555,-4.72936483805523,132.161294744112));
#43643=CARTESIAN_POINT('Ctrl Pts',(110.429351378083,-4.68949796532972,132.293228919119));
#43644=CARTESIAN_POINT('Ctrl Pts',(110.421574806612,-4.6442039791409,132.423172670471));
#43645=CARTESIAN_POINT('Ctrl Pts',(110.413788670456,-4.59885428425325,132.553276244306));
#43646=CARTESIAN_POINT('Ctrl Pts',(110.406002534301,-4.5480642721441,132.681384139421));
#43647=CARTESIAN_POINT('Ctrl Pts',(110.398216398145,-4.49205102133843,132.807024015192));
#43648=CARTESIAN_POINT('Ctrl Pts',(110.390425085613,-4.43600053181788,132.932747418834));
#43649=CARTESIAN_POINT('Ctrl Pts',(110.38263377308,-4.37472005680413,133.055999188144));
#43650=CARTESIAN_POINT('Ctrl Pts',(110.374842460547,-4.30847238702395,133.176332108278));
#43651=CARTESIAN_POINT('Ctrl Pts',(110.367038434071,-4.24211661362025,133.296861388899));
#43652=CARTESIAN_POINT('Ctrl Pts',(110.359234407595,-4.17077765399009,133.414461975275));
#43653=CARTESIAN_POINT('Ctrl Pts',(110.351430381119,-4.09476175193706,133.528715450801));
#43654=CARTESIAN_POINT('Ctrl Pts',(110.346066811128,-4.04251736086828,133.60723985287));
#43655=CARTESIAN_POINT('Ctrl Pts',(110.340703241137,-3.98806466406905,133.684183871582));
#43656=CARTESIAN_POINT('Ctrl Pts',(110.335339671145,-3.93151367305878,133.75942124318));
#43657=CARTESIAN_POINT('Ctrl Pts',(110.327565337026,-3.84954470470652,133.868475560729));
#43658=CARTESIAN_POINT('Ctrl Pts',(110.319791002907,-3.76290495879544,133.974289482691));
#43659=CARTESIAN_POINT('Ctrl Pts',(110.312016668788,-3.6718796888324,134.076436810634));
#43660=CARTESIAN_POINT('Ctrl Pts',(110.304251915841,-3.58096659937936,134.178458251124));
#43661=CARTESIAN_POINT('Ctrl Pts',(110.296487162894,-3.485678997358,134.276821799475));
#43662=CARTESIAN_POINT('Ctrl Pts',(110.288722409947,-3.38634444114331,134.371131480467));
#43663=CARTESIAN_POINT('Ctrl Pts',(110.280965369061,-3.28710854541023,134.465347491754));
#43664=CARTESIAN_POINT('Ctrl Pts',(110.273208328176,-3.18383397615189,134.555517380869));
#43665=CARTESIAN_POINT('Ctrl Pts',(110.265451287291,-3.07688721187026,134.641279713394));
#43666=CARTESIAN_POINT('Ctrl Pts',(110.257700096051,-2.97002109697588,134.726977371877));
#43667=CARTESIAN_POINT('Ctrl Pts',(110.249948904811,-2.85948860281737,134.808273845938));
#43668=CARTESIAN_POINT('Ctrl Pts',(110.242197713571,-2.74569129861734,134.884846171418));
#43669=CARTESIAN_POINT('Ctrl Pts',(110.234449816794,-2.63194236130693,134.961385951618));
#43670=CARTESIAN_POINT('Ctrl Pts',(110.226701920017,-2.51493169753785,135.03320535897));
#43671=CARTESIAN_POINT('Ctrl Pts',(110.21895402324,-2.39509185606264,135.100023321215));
#43672=CARTESIAN_POINT('Ctrl Pts',(110.211207747156,-2.27527708249874,135.166827306583));
#43673=CARTESIAN_POINT('Ctrl Pts',(110.203461471072,-2.15263464961498,135.228631737509));
#43674=CARTESIAN_POINT('Ctrl Pts',(110.195715194987,-2.02762348948471,135.285200499484));
#43675=CARTESIAN_POINT('Ctrl Pts',(110.187968861722,-1.90261140655054,135.341769679037));
#43676=CARTESIAN_POINT('Ctrl Pts',(110.180222528457,-1.77523091767329,135.393102951336));
#43677=CARTESIAN_POINT('Ctrl Pts',(110.172476195191,-1.64596243570163,135.439011707212));
#43678=CARTESIAN_POINT('Ctrl Pts',(110.164728127188,-1.51666500494999,135.484930744036));
#43679=CARTESIAN_POINT('Ctrl Pts',(110.156980059185,-1.38547910812564,135.525422716342));
#43680=CARTESIAN_POINT('Ctrl Pts',(110.149231991182,-1.25290148812496,135.560348519522));
#43681=CARTESIAN_POINT('Ctrl Pts',(110.141475688441,-1.12018296305187,135.595311442262));
#43682=CARTESIAN_POINT('Ctrl Pts',(110.133719385699,-0.986070138730447,
135.62469627869));
#43683=CARTESIAN_POINT('Ctrl Pts',(110.125963082957,-0.851071701478091,
135.648414707008));
#43684=CARTESIAN_POINT('Ctrl Pts',(110.118202640443,-0.716001211494864,
135.672145794566));
#43685=CARTESIAN_POINT('Ctrl Pts',(110.110442197929,-0.580044554100888,
135.690204396321));
#43686=CARTESIAN_POINT('Ctrl Pts',(110.102681755414,-0.44371576957375,135.70255409867));
#43687=CARTESIAN_POINT('Ctrl Pts',(110.094908855149,-0.307168137979082,
135.714923625858));
#43688=CARTESIAN_POINT('Ctrl Pts',(110.087135954883,-0.170247576243332,
135.72156592123));
#43689=CARTESIAN_POINT('Ctrl Pts',(110.079363054618,-0.0334692640664809,
135.722496735127));
#43690=CARTESIAN_POINT('Ctrl Pts',(110.071872718856,0.0983368119382216,
135.723393711595));
#43691=CARTESIAN_POINT('Ctrl Pts',(110.064382383094,0.230010493240583,135.718987260958));
#43692=CARTESIAN_POINT('Ctrl Pts',(110.056892047332,0.361097023146372,135.709336866476));
#43693=CARTESIAN_POINT('Ctrl Pts',(110.049117713213,0.497153738677194,135.699320574355));
#43694=CARTESIAN_POINT('Ctrl Pts',(110.041343379094,0.63300888698788,135.683623111824));
#43695=CARTESIAN_POINT('Ctrl Pts',(110.033569044975,0.768149708779823,135.662254100075));
#43696=CARTESIAN_POINT('Ctrl Pts',(110.025804292028,0.903123981586423,135.640911423723));
#43697=CARTESIAN_POINT('Ctrl Pts',(110.018039539081,1.0373852970355,135.613911166004));
#43698=CARTESIAN_POINT('Ctrl Pts',(110.010274786134,1.17042345665789,135.581314876778));
#43699=CARTESIAN_POINT('Ctrl Pts',(110.002517745249,1.30332948090445,135.548750962646));
#43700=CARTESIAN_POINT('Ctrl Pts',(109.994760704364,1.43501438966582,135.51060217023));
#43701=CARTESIAN_POINT('Ctrl Pts',(109.987003663479,1.56497600734838,135.466981464142));
#43702=CARTESIAN_POINT('Ctrl Pts',(109.979252472238,1.69483961996419,135.423393652767));
#43703=CARTESIAN_POINT('Ctrl Pts',(109.971501280998,1.82298215902628,135.374342264996));
#43704=CARTESIAN_POINT('Ctrl Pts',(109.963750089758,1.94891484766775,135.319990582371));
#43705=CARTESIAN_POINT('Ctrl Pts',(109.956002192981,2.07479401155744,135.26566200066));
#43706=CARTESIAN_POINT('Ctrl Pts',(109.948254296204,2.19846483490563,135.206037759278));
#43707=CARTESIAN_POINT('Ctrl Pts',(109.940506399427,2.31945704049337,135.141329847317));
#43708=CARTESIAN_POINT('Ctrl Pts',(109.932760123343,2.44042393711999,135.076635470856));
#43709=CARTESIAN_POINT('Ctrl Pts',(109.925013847259,2.55871298593247,135.00685972323));
#43710=CARTESIAN_POINT('Ctrl Pts',(109.917267571175,2.67387747311014,134.932261091329));
#43711=CARTESIAN_POINT('Ctrl Pts',(109.909521237909,2.78904281040582,134.857661908758));
#43712=CARTESIAN_POINT('Ctrl Pts',(109.901774904644,2.90108321190439,134.778239983425));
#43713=CARTESIAN_POINT('Ctrl Pts',(109.894028571379,3.00958032049026,134.694297552404));
#43714=CARTESIAN_POINT('Ctrl Pts',(109.886280503376,3.11810172625134,134.610336323057));
#43715=CARTESIAN_POINT('Ctrl Pts',(109.878532435373,3.22307795097219,134.521852812784));
#43716=CARTESIAN_POINT('Ctrl Pts',(109.87078436737,3.32412346033668,134.429189756014));
#43717=CARTESIAN_POINT('Ctrl Pts',(109.863028064628,3.42527636207105,134.336428215843));
#43718=CARTESIAN_POINT('Ctrl Pts',(109.855271761886,3.52248991461387,134.239478520324));
#43719=CARTESIAN_POINT('Ctrl Pts',(109.847515459144,3.61541485295376,134.13872090157));
#43720=CARTESIAN_POINT('Ctrl Pts',(109.83975501663,3.70838938813142,134.037909505441));
#43721=CARTESIAN_POINT('Ctrl Pts',(109.831994574116,3.79707049548166,133.933286434437));
#43722=CARTESIAN_POINT('Ctrl Pts',(109.824234131602,3.88114968788277,133.825264482761));
#43723=CARTESIAN_POINT('Ctrl Pts',(109.816461231336,3.96536385166748,133.717069124658));
#43724=CARTESIAN_POINT('Ctrl Pts',(109.808688331071,4.04496111097209,133.605464301174));
#43725=CARTESIAN_POINT('Ctrl Pts',(109.800915430805,4.11967624979386,133.490891961024));
#43726=CARTESIAN_POINT('Ctrl Pts',(109.793425095043,4.19167530512428,133.380484614029));
#43727=CARTESIAN_POINT('Ctrl Pts',(109.785934759281,4.25914087445923,133.267322022551));
#43728=CARTESIAN_POINT('Ctrl Pts',(109.778444423519,4.32187719565033,133.151818938435));
#43729=CARTESIAN_POINT('Ctrl Pts',(109.7706700894,4.38699218352695,133.03193651978));
#43730=CARTESIAN_POINT('Ctrl Pts',(109.762895755281,4.44721848983267,132.909152873958));
#43731=CARTESIAN_POINT('Ctrl Pts',(109.755121421162,4.50228705022288,132.78390460038));
#43732=CARTESIAN_POINT('Ctrl Pts',(109.747356668215,4.55728774353399,132.658810684106));
#43733=CARTESIAN_POINT('Ctrl Pts',(109.739591915268,4.6071431825434,132.531258538125));
#43734=CARTESIAN_POINT('Ctrl Pts',(109.73182716232,4.65162937615635,132.401710676063));
#43735=CARTESIAN_POINT('Ctrl Pts',(109.724070121435,4.69607138545471,132.272291482763));
#43736=CARTESIAN_POINT('Ctrl Pts',(109.71631308055,4.7351546357335,132.140880885374));
#43737=CARTESIAN_POINT('Ctrl Pts',(109.708556039665,4.76870272914536,132.007962438577));
#43738=CARTESIAN_POINT('Ctrl Pts',(109.700804848425,4.80222552367885,131.875144226616));
#43739=CARTESIAN_POINT('Ctrl Pts',(109.693053657185,4.83022137435755,131.74082080608));
#43740=CARTESIAN_POINT('Ctrl Pts',(109.685302465945,4.85256345873285,131.605491656455));
#43741=CARTESIAN_POINT('Ctrl Pts',(109.677554569168,4.87489604712636,131.470220025327));
#43742=CARTESIAN_POINT('Ctrl Pts',(109.669806672391,4.89157958505243,131.333943900234));
#43743=CARTESIAN_POINT('Ctrl Pts',(109.662058775614,4.90253822861556,131.197173524002));
#43744=CARTESIAN_POINT('Ctrl Pts',(109.65431249953,4.91349457986669,131.060431757185));
#43745=CARTESIAN_POINT('Ctrl Pts',(109.646566223446,4.91872838749074,130.92319633434));
#43746=CARTESIAN_POINT('Ctrl Pts',(109.638819947362,4.91821566409774,130.785982806934));
#43747=CARTESIAN_POINT('Ctrl Pts',(109.631073614096,4.91770293691993,130.648768266649));
#43748=CARTESIAN_POINT('Ctrl Pts',(109.623327280831,4.91144359554072,130.511576013088));
#43749=CARTESIAN_POINT('Ctrl Pts',(109.615580947565,4.89946578832898,130.374921388462));
#43750=CARTESIAN_POINT('Ctrl Pts',(109.607832879562,4.88748529877037,130.23823616098));
#43751=CARTESIAN_POINT('Ctrl Pts',(109.60008481156,4.86978382924282,130.102089191408));
#43752=CARTESIAN_POINT('Ctrl Pts',(109.592336743557,4.84644134121256,129.966990097016));
#43753=CARTESIAN_POINT('Ctrl Pts',(109.584580440815,4.82307404450828,129.831747417699));
#43754=CARTESIAN_POINT('Ctrl Pts',(109.576824138073,4.79405381963168,129.697555224158));
#43755=CARTESIAN_POINT('Ctrl Pts',(109.569067835331,4.75951178036033,129.564912887683));
#43756=CARTESIAN_POINT('Ctrl Pts',(109.561307392817,4.72495130496253,129.432199756));
#43757=CARTESIAN_POINT('Ctrl Pts',(109.553546950303,4.68486325692695,129.301038503369));
#43758=CARTESIAN_POINT('Ctrl Pts',(109.545786507788,4.63942818688215,129.171911794091));
#43759=CARTESIAN_POINT('Ctrl Pts',(109.538013607523,4.59392018042941,129.042577799157));
#43760=CARTESIAN_POINT('Ctrl Pts',(109.530240707258,4.54304814454427,128.9152852374));
#43761=CARTESIAN_POINT('Ctrl Pts',(109.522467806992,4.4870405474712,128.790496126631));
#43762=CARTESIAN_POINT('Ctrl Pts',(109.51497747123,4.43306896762663,128.670243414364));
#43763=CARTESIAN_POINT('Ctrl Pts',(109.507487135468,4.37432886265035,128.552315575316));
#43764=CARTESIAN_POINT('Ctrl Pts',(109.499996799706,4.31106336079069,128.437101493231));
#43765=CARTESIAN_POINT('Ctrl Pts',(109.492222465587,4.24539912819849,128.317519034204));
#43766=CARTESIAN_POINT('Ctrl Pts',(109.484448131468,4.17465155922289,128.200481377287));
#43767=CARTESIAN_POINT('Ctrl Pts',(109.476673797349,4.09904254146147,128.08645088658));
#43768=CARTESIAN_POINT('Ctrl Pts',(109.468909044402,4.02352670505702,127.972560928261));
#43769=CARTESIAN_POINT('Ctrl Pts',(109.461144291455,3.94316155475029,127.861671084906));
#43770=CARTESIAN_POINT('Ctrl Pts',(109.453379538508,3.85821514369443,127.754219806478));
#43771=CARTESIAN_POINT('Ctrl Pts',(109.445622497623,3.77335310261134,127.646875250173));
#43772=CARTESIAN_POINT('Ctrl Pts',(109.437865456738,3.68391909672332,127.542962767047));
#43773=CARTESIAN_POINT('Ctrl Pts',(109.430108415853,3.5902246069335,127.442892138721));
#43774=CARTESIAN_POINT('Ctrl Pts',(109.422357224612,3.4966007728874,127.342896974434));
#43775=CARTESIAN_POINT('Ctrl Pts',(109.414606033372,3.39872311608172,127.246738182542));
#43776=CARTESIAN_POINT('Ctrl Pts',(109.406854842132,3.29694331212077,127.154792443225));
#43777=CARTESIAN_POINT('Ctrl Pts',(109.399106945355,3.19520676729191,127.0628857833));
#43778=CARTESIAN_POINT('Ctrl Pts',(109.391359048578,3.08957166347778,126.975188875999));
#43779=CARTESIAN_POINT('Ctrl Pts',(109.383611151801,2.98042628694114,126.892041329649));
#43780=CARTESIAN_POINT('Ctrl Pts',(109.375864875717,2.87130374126437,126.808911175973));
#43781=CARTESIAN_POINT('Ctrl Pts',(109.368118599633,2.75867269417907,126.73032872718));
#43782=CARTESIAN_POINT('Ctrl Pts',(109.360372323549,2.6429539279655,126.656592832702));
#43783=CARTESIAN_POINT('Ctrl Pts',(109.352625990283,2.52723430754237,126.582856393923));
#43784=CARTESIAN_POINT('Ctrl Pts',(109.344879657018,2.40842725222696,126.513966790943));
#43785=CARTESIAN_POINT('Ctrl Pts',(109.337133323753,2.28698154889673,126.450178896794));
#43786=CARTESIAN_POINT('Ctrl Pts',(109.32938525575,2.16550864864279,126.386376717788));
#43787=CARTESIAN_POINT('Ctrl Pts',(109.321637187747,2.04139627059726,126.327678702805));
#43788=CARTESIAN_POINT('Ctrl Pts',(109.313889119744,1.91511639132759,126.274293038581));
#43789=CARTESIAN_POINT('Ctrl Pts',(109.306132817002,1.78870230029983,126.220850635438));
#43790=CARTESIAN_POINT('Ctrl Pts',(109.29837651426,1.66011646694844,126.172732014087));
#43791=CARTESIAN_POINT('Ctrl Pts',(109.290620211518,1.52984989668365,126.130096787173));
#43792=CARTESIAN_POINT('Ctrl Pts',(109.282859769004,1.39951379922787,126.087438804556));
#43793=CARTESIAN_POINT('Ctrl Pts',(109.27509932649,1.26749555354112,126.050270153882));
#43794=CARTESIAN_POINT('Ctrl Pts',(109.267338883976,1.13429883079499,126.018699824639));
#43795=CARTESIAN_POINT('Ctrl Pts',(109.25956598371,1.00088828884504,125.987078815901));
#43796=CARTESIAN_POINT('Ctrl Pts',(109.251793083445,0.866295873511378,125.961074161539));
#43797=CARTESIAN_POINT('Ctrl Pts',(109.244020183179,0.73103378613032,125.94074337666));
#43798=CARTESIAN_POINT('Ctrl Pts',(109.236529847417,0.600688816332127,125.921151667022));
#43799=CARTESIAN_POINT('Ctrl Pts',(109.229039511656,0.46972232390649,125.906828503393));
#43800=CARTESIAN_POINT('Ctrl Pts',(109.221549175894,0.338592904515696,125.897779536252));
#43801=CARTESIAN_POINT('Ctrl Pts',(109.213774841774,0.20249167333058,125.888387474771));
#43802=CARTESIAN_POINT('Ctrl Pts',(109.206000507655,0.0657837887511484,
125.884647695859));
#43803=CARTESIAN_POINT('Ctrl Pts',(109.198226173536,-0.0710218135452183,
125.886623438283));
#43804=CARTESIAN_POINT('Ctrl Pts',(109.190461420589,-0.207658815163144,
125.888596745782));
#43805=CARTESIAN_POINT('Ctrl Pts',(109.182696667642,-0.344392907709876,
125.896271553826));
#43806=CARTESIAN_POINT('Ctrl Pts',(109.174931914695,-0.480710321536931,
125.909659334621));
#43807=CARTESIAN_POINT('Ctrl Pts',(109.16717487381,-0.616892342986928,125.923033818483));
#43808=CARTESIAN_POINT('Ctrl Pts',(109.159417832925,-0.752658122724326,
125.942109945206));
#43809=CARTESIAN_POINT('Ctrl Pts',(109.15166079204,-0.887494536828826,125.96684715406));
#43810=CARTESIAN_POINT('Ctrl Pts',(109.1439096008,-1.02222926974439,125.991565708393));
#43811=CARTESIAN_POINT('Ctrl Pts',(109.13615840956,-1.15603564901901,126.021936777276));
#43812=CARTESIAN_POINT('Ctrl Pts',(109.128407218319,-1.28840667369546,126.057868090902));
#43813=CARTESIAN_POINT('Ctrl Pts',(109.120659321542,-1.42072143715549,126.093784132761));
#43814=CARTESIAN_POINT('Ctrl Pts',(109.112911424765,-1.55160168286634,126.135255616829));
#43815=CARTESIAN_POINT('Ctrl Pts',(109.105163527988,-1.68055181051363,126.182139433473));
#43816=CARTESIAN_POINT('Ctrl Pts',(109.097417251904,-1.80947496457415,126.229013443033));
#43817=CARTESIAN_POINT('Ctrl Pts',(109.08967097582,-1.93646843643001,126.281297399768));
#43818=CARTESIAN_POINT('Ctrl Pts',(109.081924699736,-2.06105335248994,126.338798823045));
#43819=CARTESIAN_POINT('Ctrl Pts',(109.07417836647,-2.18563918820699,126.396300670783));
#43820=CARTESIAN_POINT('Ctrl Pts',(109.066432033205,-2.30781607767081,126.459019898078));
#43821=CARTESIAN_POINT('Ctrl Pts',(109.05868569994,-2.42712700871127,126.526716692917));
#43822=CARTESIAN_POINT('Ctrl Pts',(109.050937631937,-2.5464646586083,126.594428647985));
#43823=CARTESIAN_POINT('Ctrl Pts',(109.043189563934,-2.66293473297472,126.667120195803));
#43824=CARTESIAN_POINT('Ctrl Pts',(109.035441495931,-2.77610696355001,126.744506779134));
#43825=CARTESIAN_POINT('Ctrl Pts',(109.027685193189,-2.88939947491825,126.821975609847));
#43826=CARTESIAN_POINT('Ctrl Pts',(109.019928890447,-2.99938681766151,126.904149222982));
#43827=CARTESIAN_POINT('Ctrl Pts',(109.012172587705,-3.10566930472197,126.990700796317));
#43828=CARTESIAN_POINT('Ctrl Pts',(109.004412145191,-3.21200851794623,127.077298564833));
#43829=CARTESIAN_POINT('Ctrl Pts',(108.996651702677,-3.31463864294787,127.168278690297));
#43830=CARTESIAN_POINT('Ctrl Pts',(108.988891260162,-3.41319573721326,127.263276331366));
#43831=CARTESIAN_POINT('Ctrl Pts',(108.981118359897,-3.51191104407552,127.358426471083));
#43832=CARTESIAN_POINT('Ctrl Pts',(108.973345459632,-3.60653998437088,127.457606731077));
#43833=CARTESIAN_POINT('Ctrl Pts',(108.965572559366,-3.69675731167684,127.560417270178));
#43834=CARTESIAN_POINT('Ctrl Pts',(108.958082223604,-3.78369501188966,127.659490387216));
#43835=CARTESIAN_POINT('Ctrl Pts',(108.950591887842,-3.86653608329424,127.761934186653));
#43836=CARTESIAN_POINT('Ctrl Pts',(108.943101552081,-3.94502788982435,127.867365893191));
#43837=CARTESIAN_POINT('Ctrl Pts',(108.935287665741,-4.02691020782528,127.977351800049));
#43838=CARTESIAN_POINT('Ctrl Pts',(108.927473779402,-4.10431997379332,128.09093976861));
#43839=CARTESIAN_POINT('Ctrl Pts',(108.919659893063,-4.17692536949992,128.207732511709));
#43840=CARTESIAN_POINT('Ctrl Pts',(108.911858983755,-4.24941018468157,128.324331289467));
#43841=CARTESIAN_POINT('Ctrl Pts',(108.904058074448,-4.31710632009062,128.444123916064));
#43842=CARTESIAN_POINT('Ctrl Pts',(108.89625716514,-4.37972314083985,128.566681401929));
#43843=CARTESIAN_POINT('Ctrl Pts',(108.888463727543,-4.44227998719784,128.689121502234));
#43844=CARTESIAN_POINT('Ctrl Pts',(108.880670289947,-4.49976702168279,128.814320853177));
#43845=CARTESIAN_POINT('Ctrl Pts',(108.87287685235,-4.55193751326061,128.941822580942));
#43846=CARTESIAN_POINT('Ctrl Pts',(108.865090518563,-4.60406045082571,129.069208089393));
#43847=CARTESIAN_POINT('Ctrl Pts',(108.857304184776,-4.65087634985271,129.198891440245));
#43848=CARTESIAN_POINT('Ctrl Pts',(108.849517850989,-4.69218520904243,129.330392834152));
#43849=CARTESIAN_POINT('Ctrl Pts',(108.844582926426,-4.71836647861593,129.413737509136));
#43850=CARTESIAN_POINT('Ctrl Pts',(108.839648001863,-4.74233653958104,129.497812011167));
#43851=CARTESIAN_POINT('Ctrl Pts',(108.834713077301,-4.76405452823406,129.582490119308));
#43852=CARTESIAN_POINT('Ctrl Pts',(110.584632631705,-4.76405452823407,129.582490119308));
#43853=CARTESIAN_POINT('Ctrl Pts',(110.57571850841,-4.8029970434331,129.734326395034));
#43854=CARTESIAN_POINT('Ctrl Pts',(110.566804385115,-4.83472011272508,129.888195027331));
#43855=CARTESIAN_POINT('Ctrl Pts',(110.55789026182,-4.85903247671165,130.043449024303));
#43856=CARTESIAN_POINT('Ctrl Pts',(110.549039520694,-4.88317197228292,130.197599117416));
#43857=CARTESIAN_POINT('Ctrl Pts',(110.540188779568,-4.90000568966876,130.353114794605));
#43858=CARTESIAN_POINT('Ctrl Pts',(110.531338038442,-4.90939383791824,130.509343318564));
#43859=CARTESIAN_POINT('Ctrl Pts',(110.525845170977,-4.91522022616582,130.606300461948));
#43860=CARTESIAN_POINT('Ctrl Pts',(110.520352303511,-4.91817983312127,130.70353178788));
#43861=CARTESIAN_POINT('Ctrl Pts',(110.514859436046,-4.91824876687394,130.800877853875));
#43862=CARTESIAN_POINT('',(110.860140563956,-4.91824981345875,130.803006027984));
#43863=CARTESIAN_POINT('Ctrl Pts',(110.930234911077,-4.76405452823406,129.582490119308));
#43864=CARTESIAN_POINT('Ctrl Pts',(110.922471870508,-4.79810759213842,129.715262498644));
#43865=CARTESIAN_POINT('Ctrl Pts',(110.914708829939,-4.82657455152162,129.849336840364));
#43866=CARTESIAN_POINT('Ctrl Pts',(110.90694578937,-4.84938399854219,129.984203378262));
#43867=CARTESIAN_POINT('Ctrl Pts',(110.899171379239,-4.87222685172807,130.119267438435));
#43868=CARTESIAN_POINT('Ctrl Pts',(110.891396969109,-4.88939559826073,130.255125624766));
#43869=CARTESIAN_POINT('Ctrl Pts',(110.883622558978,-4.90087076246386,130.391263979808));
#43870=CARTESIAN_POINT('Ctrl Pts',(110.879963680189,-4.90627133102083,130.455334916539));
#43871=CARTESIAN_POINT('Ctrl Pts',(110.8763048014,-4.91041155883166,130.519467917546));
#43872=CARTESIAN_POINT('Ctrl Pts',(110.872645922612,-4.91329340329261,130.583609636455));
#43873=CARTESIAN_POINT('Ctrl Pts',(110.868477469744,-4.9165766038306,130.656684408145));
#43874=CARTESIAN_POINT('Ctrl Pts',(110.864309016876,-4.91822966004416,130.729832970459));
#43875=CARTESIAN_POINT('Ctrl Pts',(110.860140564008,-4.9182498134585,130.80300602708));
#43876=CARTESIAN_POINT('Ctrl Pts',(110.860140563956,-4.91824981345875,130.803006027984));
#43877=CARTESIAN_POINT('Ctrl Pts',(110.852421723757,-4.91828713207212,130.938502613616));
#43878=CARTESIAN_POINT('Ctrl Pts',(110.844702883558,-4.91272086582082,131.074226120841));
#43879=CARTESIAN_POINT('Ctrl Pts',(110.836984043359,-4.90152087846242,131.209670548973));
#43880=CARTESIAN_POINT('Ctrl Pts',(110.829274541677,-4.89033444123204,131.3449511118));
#43881=CARTESIAN_POINT('Ctrl Pts',(110.821565039995,-4.87352787326834,131.479952875333));
#43882=CARTESIAN_POINT('Ctrl Pts',(110.813855538313,-4.85112301637002,131.614168337056));
#43883=CARTESIAN_POINT('Ctrl Pts',(110.806153453313,-4.82873971335402,131.748254681048));
#43884=CARTESIAN_POINT('Ctrl Pts',(110.798451368313,-4.80076890139968,131.881555839073));
#43885=CARTESIAN_POINT('Ctrl Pts',(110.790749283312,-4.76728430710159,132.013568373811));
#43886=CARTESIAN_POINT('Ctrl Pts',(110.783052700285,-4.73382363247239,132.145486605596));
#43887=CARTESIAN_POINT('Ctrl Pts',(110.775356117257,-4.69485711086892,132.276117662544));
#43888=CARTESIAN_POINT('Ctrl Pts',(110.767659534229,-4.65050965366092,132.404967697304));
#43889=CARTESIAN_POINT('Ctrl Pts',(110.759965746648,-4.60617830372207,132.533770932939));
#43890=CARTESIAN_POINT('Ctrl Pts',(110.752271959066,-4.55647003202619,132.660794057457));
#43891=CARTESIAN_POINT('Ctrl Pts',(110.744578171485,-4.50155969320645,132.785558081475));
#43892=CARTESIAN_POINT('Ctrl Pts',(110.736885594092,-4.44665799146452,132.910302480835));
#43893=CARTESIAN_POINT('Ctrl Pts',(110.729193016698,-4.38655600965109,133.032788123049));
#43894=CARTESIAN_POINT('Ctrl Pts',(110.721500439305,-4.3214766702694,133.152556190941));
#43895=CARTESIAN_POINT('Ctrl Pts',(110.713807346968,-4.25639297445367,133.272332276149));
#43896=CARTESIAN_POINT('Ctrl Pts',(110.706114254631,-4.186331447955,133.389390076323));
#43897=CARTESIAN_POINT('Ctrl Pts',(110.698421162294,-4.11156063904084,133.503295995449));
#43898=CARTESIAN_POINT('Ctrl Pts',(110.690725829826,-4.03676805781946,133.617235082529));
#43899=CARTESIAN_POINT('Ctrl Pts',(110.683030497359,-3.95726368435546,133.728020131229));
#43900=CARTESIAN_POINT('Ctrl Pts',(110.675335164891,-3.87335870781698,133.835247514677));
#43901=CARTESIAN_POINT('Ctrl Pts',(110.66763150882,-3.78936297603294,133.942590879893));
#43902=CARTESIAN_POINT('Ctrl Pts',(110.659927852748,-3.70095738281575,134.046368584067));
#43903=CARTESIAN_POINT('Ctrl Pts',(110.652224196677,-3.60849287329806,134.146210740755));
#43904=CARTESIAN_POINT('Ctrl Pts',(110.644515856566,-3.51597214276631,134.246113604273));
#43905=CARTESIAN_POINT('Ctrl Pts',(110.636807516456,-3.41938786237572,134.342075875924));
#43906=CARTESIAN_POINT('Ctrl Pts',(110.629099176346,-3.31912609810012,134.433766217304));
#43907=CARTESIAN_POINT('Ctrl Pts',(110.621379496337,-3.21871683666944,134.525591446242));
#43908=CARTESIAN_POINT('Ctrl Pts',(110.613659816328,-3.11461959280639,134.613131942647));
#43909=CARTESIAN_POINT('Ctrl Pts',(110.605940136319,-3.0072519563348,134.696097856078));
#43910=CARTESIAN_POINT('Ctrl Pts',(110.602026190479,-2.95281561782933,134.738162305817));
#43911=CARTESIAN_POINT('Ctrl Pts',(110.598112244639,-2.89753904253257,134.779051527273));
#43912=CARTESIAN_POINT('Ctrl Pts',(110.594198298799,-2.8414791507417,134.818732212025));
#43913=CARTESIAN_POINT('Ctrl Pts',(110.58642396468,-2.73012647820146,134.897550599899));
#43914=CARTESIAN_POINT('Ctrl Pts',(110.578649630561,-2.61531548912708,134.971857183996));
#43915=CARTESIAN_POINT('Ctrl Pts',(110.570875296441,-2.49744794817247,135.041333217037));
#43916=CARTESIAN_POINT('Ctrl Pts',(110.563110543494,-2.37972566842837,135.110723627076));
#43917=CARTESIAN_POINT('Ctrl Pts',(110.555345790547,-2.25895466544133,135.175295134574));
#43918=CARTESIAN_POINT('Ctrl Pts',(110.5475810376,-2.13556776024288,135.234770689321));
#43919=CARTESIAN_POINT('Ctrl Pts',(110.539823996715,-2.01230340465831,135.29418717211));
#43920=CARTESIAN_POINT('Ctrl Pts',(110.53206695583,-1.88642866720647,135.348517605844));
#43921=CARTESIAN_POINT('Ctrl Pts',(110.524309914945,-1.75840288388109,135.397529715309));
#43922=CARTESIAN_POINT('Ctrl Pts',(110.516558723705,-1.63047364579473,135.446504864361));
#43923=CARTESIAN_POINT('Ctrl Pts',(110.508807532465,-1.5003969542134,135.490169532765));
#43924=CARTESIAN_POINT('Ctrl Pts',(110.501056341225,-1.3686538137581,135.528338792853));
#43925=CARTESIAN_POINT('Ctrl Pts',(110.493308444448,-1.2369666676515,135.566491829987));
#43926=CARTESIAN_POINT('Ctrl Pts',(110.485560547671,-1.10361485613204,135.599153995753));
#43927=CARTESIAN_POINT('Ctrl Pts',(110.477812650894,-0.969096092840138,
135.626189712976));
#43928=CARTESIAN_POINT('Ctrl Pts',(110.47006637481,-0.83460546797363,135.653219774909));
#43929=CARTESIAN_POINT('Ctrl Pts',(110.462320098726,-0.698948759922859,
135.674625652294));
#43930=CARTESIAN_POINT('Ctrl Pts',(110.454573822641,-0.562635078518343,
135.6903226345));
#43931=CARTESIAN_POINT('Ctrl Pts',(110.446827489376,-0.426320390877383,
135.706019732578));
#43932=CARTESIAN_POINT('Ctrl Pts',(110.439081156111,-0.28934910860414,135.716007806661));
#43933=CARTESIAN_POINT('Ctrl Pts',(110.431334822845,-0.152236291425476,
135.72025394168));
#43934=CARTESIAN_POINT('Ctrl Pts',(110.423586754842,-0.0150927687817969,
135.724501027592));
#43935=CARTESIAN_POINT('Ctrl Pts',(110.41583868684,0.122191961135122,135.723003603613));
#43936=CARTESIAN_POINT('Ctrl Pts',(110.408090618837,0.259102403888672,135.715780881278));
#43937=CARTESIAN_POINT('Ctrl Pts',(110.400334316095,0.39615835668985,135.708550482548));
#43938=CARTESIAN_POINT('Ctrl Pts',(110.392578013353,0.532838836640757,135.695582650818));
#43939=CARTESIAN_POINT('Ctrl Pts',(110.384821710611,0.668632482032181,135.676948602043));
#43940=CARTESIAN_POINT('Ctrl Pts',(110.377061268097,0.80449860458091,135.658304607715));
#43941=CARTESIAN_POINT('Ctrl Pts',(110.369300825583,0.939476564836288,135.633988439589));
#43942=CARTESIAN_POINT('Ctrl Pts',(110.361540383068,1.07306575221742,135.604122377687));
#43943=CARTESIAN_POINT('Ctrl Pts',(110.353767482803,1.20686938882162,135.57420837213));
#43944=CARTESIAN_POINT('Ctrl Pts',(110.345994582538,1.33927941967796,135.538726770666));
#43945=CARTESIAN_POINT('Ctrl Pts',(110.338221682272,1.46981007669505,135.497849874073));
#43946=CARTESIAN_POINT('Ctrl Pts',(110.33073134651,1.59559561554375,135.458458955633));
#43947=CARTESIAN_POINT('Ctrl Pts',(110.323241010748,1.71963575822971,135.414058300707));
#43948=CARTESIAN_POINT('Ctrl Pts',(110.315750674986,1.84151562736709,135.364843405239));
#43949=CARTESIAN_POINT('Ctrl Pts',(110.307976340867,1.96801660878642,135.313762512052));
#43950=CARTESIAN_POINT('Ctrl Pts',(110.300202006748,2.0925909864683,135.257333299071));
#43951=CARTESIAN_POINT('Ctrl Pts',(110.292427672629,2.21475342568958,135.195721491589));
#43952=CARTESIAN_POINT('Ctrl Pts',(110.284662919682,2.3367653106224,135.134185615153));
#43953=CARTESIAN_POINT('Ctrl Pts',(110.276898166734,2.45637082575065,135.067480026976));
#43954=CARTESIAN_POINT('Ctrl Pts',(110.269133413787,2.57310293054794,134.995819119246));
#43955=CARTESIAN_POINT('Ctrl Pts',(110.261376372902,2.6897190953728,134.92422938614));
#43956=CARTESIAN_POINT('Ctrl Pts',(110.253619332017,2.80346719824521,134.847694331092));
#43957=CARTESIAN_POINT('Ctrl Pts',(110.245862291132,2.91390353712436,134.766474856055));
#43958=CARTESIAN_POINT('Ctrl Pts',(110.238111099892,3.02425659510152,134.685316629255));
#43959=CARTESIAN_POINT('Ctrl Pts',(110.230359908652,3.13130254637744,134.599481244506));
#43960=CARTESIAN_POINT('Ctrl Pts',(110.222608717412,3.23462581132014,134.509273426694));
#43961=CARTESIAN_POINT('Ctrl Pts',(110.214860820635,3.33790516111914,134.419103949611));
#43962=CARTESIAN_POINT('Ctrl Pts',(110.207112923858,3.4374646776445,134.324565992275));
#43963=CARTESIAN_POINT('Ctrl Pts',(110.199365027081,3.53292126959806,134.226005012491));
#43964=CARTESIAN_POINT('Ctrl Pts',(110.191618750997,3.62835789409032,134.127464649539));
#43965=CARTESIAN_POINT('Ctrl Pts',(110.183872474913,3.7196930292803,134.024903218652));
#43966=CARTESIAN_POINT('Ctrl Pts',(110.176126198829,3.80658021941792,133.918703260185));
#43967=CARTESIAN_POINT('Ctrl Pts',(110.168379865563,3.89346805093704,133.812502517774));
#43968=CARTESIAN_POINT('Ctrl Pts',(110.160633532298,3.97590762431884,133.702663496784));
#43969=CARTESIAN_POINT('Ctrl Pts',(110.152887199032,4.05359284481915,133.58960174015));
#43970=CARTESIAN_POINT('Ctrl Pts',(110.145139131029,4.13129546238618,133.476514664119));
#43971=CARTESIAN_POINT('Ctrl Pts',(110.137391063026,4.20424138706917,133.360203738496));
#43972=CARTESIAN_POINT('Ctrl Pts',(110.129642995023,4.2721681447425,133.241113047656));
#43973=CARTESIAN_POINT('Ctrl Pts',(110.121886692282,4.34016709578204,133.121895785812));
#43974=CARTESIAN_POINT('Ctrl Pts',(110.11413038954,4.40313602969954,132.99989319723));
#43975=CARTESIAN_POINT('Ctrl Pts',(110.106374086798,4.4608584589998,132.875573998961));
#43976=CARTESIAN_POINT('Ctrl Pts',(110.098613644284,4.51861169649858,132.751188447793));
#43977=CARTESIAN_POINT('Ctrl Pts',(110.09085320177,4.57111270012231,132.624484184228));
#43978=CARTESIAN_POINT('Ctrl Pts',(110.083092759255,4.61819375526957,132.495948481465));
#43979=CARTESIAN_POINT('Ctrl Pts',(110.07531985899,4.66535038910622,132.36720644178));
#43980=CARTESIAN_POINT('Ctrl Pts',(110.067546958725,4.70706956887608,132.236627460496));
#43981=CARTESIAN_POINT('Ctrl Pts',(110.059774058459,4.74323368658421,132.104713360845));
#43982=CARTESIAN_POINT('Ctrl Pts',(110.052283722697,4.77808314752173,131.977594670987));
#43983=CARTESIAN_POINT('Ctrl Pts',(110.044793386935,4.80777434601102,131.849236547414));
#43984=CARTESIAN_POINT('Ctrl Pts',(110.037303051173,4.83224750696555,131.720093708551));
#43985=CARTESIAN_POINT('Ctrl Pts',(110.029528717054,4.85764857525613,131.586054379701));
#43986=CARTESIAN_POINT('Ctrl Pts',(110.021754382935,4.87750857425258,131.450745059652));
#43987=CARTESIAN_POINT('Ctrl Pts',(110.013980048816,4.89170459806314,131.314663652818));
#43988=CARTESIAN_POINT('Ctrl Pts',(110.006215295869,4.90588312654309,131.178749954157));
#43989=CARTESIAN_POINT('Ctrl Pts',(109.998450542922,4.91441152846365,131.042066447092));
#43990=CARTESIAN_POINT('Ctrl Pts',(109.990685789974,4.91721773123116,130.905121950258));
#43991=CARTESIAN_POINT('Ctrl Pts',(109.982928749089,4.92002114683852,130.768313468629));
#43992=CARTESIAN_POINT('Ctrl Pts',(109.975171708204,4.91711366549537,130.631244901442));
#43993=CARTESIAN_POINT('Ctrl Pts',(109.967414667319,4.90847495961329,130.49443057167));
#43994=CARTESIAN_POINT('Ctrl Pts',(109.959663476079,4.89984276824651,130.357719414647));
#43995=CARTESIAN_POINT('Ctrl Pts',(109.951912284839,4.88548797947955,130.221262502037));
#43996=CARTESIAN_POINT('Ctrl Pts',(109.944161093599,4.86544233604906,130.085574183998));
#43997=CARTESIAN_POINT('Ctrl Pts',(109.936413196822,4.84540521255178,129.949943537114));
#43998=CARTESIAN_POINT('Ctrl Pts',(109.928665300045,4.81968210214892,129.815081221031));
#43999=CARTESIAN_POINT('Ctrl Pts',(109.920917403268,4.78835657807249,129.681496269691));
#44000=CARTESIAN_POINT('Ctrl Pts',(109.913171127184,4.75703760662045,129.547939261442));
#44001=CARTESIAN_POINT('Ctrl Pts',(109.9054248511,4.7201186416795,129.415659466865));
#44002=CARTESIAN_POINT('Ctrl Pts',(109.897678575016,4.67773425748905,129.2851551414));
#44003=CARTESIAN_POINT('Ctrl Pts',(109.88993224175,4.6353495604267,129.154649852581));
#44004=CARTESIAN_POINT('Ctrl Pts',(109.882185908485,4.58749948437617,129.025920430873));
#44005=CARTESIAN_POINT('Ctrl Pts',(109.87443957522,4.5343681856923,128.899449013559));
#44006=CARTESIAN_POINT('Ctrl Pts',(109.866691507217,4.48122498862258,128.772949273848));
#44007=CARTESIAN_POINT('Ctrl Pts',(109.858943439214,4.4227983668947,128.648708905126));
#44008=CARTESIAN_POINT('Ctrl Pts',(109.851195371211,4.35932006759288,128.527188772759));
#44009=CARTESIAN_POINT('Ctrl Pts',(109.843439068469,4.2957743027989,128.405539487349));
#44010=CARTESIAN_POINT('Ctrl Pts',(109.835682765727,4.22716631661626,128.286616560664));
#44011=CARTESIAN_POINT('Ctrl Pts',(109.827926462985,4.1537734371959,128.17085548278));
#44012=CARTESIAN_POINT('Ctrl Pts',(109.820166020471,4.08034138578597,128.055032619723));
#44013=CARTESIAN_POINT('Ctrl Pts',(109.812405577957,4.00211957526458,127.942375289088));
#44014=CARTESIAN_POINT('Ctrl Pts',(109.804645135443,3.91942730853519,127.833287976985));
#44015=CARTESIAN_POINT('Ctrl Pts',(109.796872235177,3.83660229683811,127.724025548244));
#44016=CARTESIAN_POINT('Ctrl Pts',(109.789099334912,3.74929273740831,127.618344891802));
#44017=CARTESIAN_POINT('Ctrl Pts',(109.781326434646,3.65785725834914,127.516616202311));
#44018=CARTESIAN_POINT('Ctrl Pts',(109.773836098884,3.5697456892651,127.41858560692));
#44019=CARTESIAN_POINT('Ctrl Pts',(109.766345763122,3.47780318264203,127.324224859619));
#44020=CARTESIAN_POINT('Ctrl Pts',(109.75885542736,3.38237999607707,127.233830037297));
#44021=CARTESIAN_POINT('Ctrl Pts',(109.751081093241,3.28333881039114,127.140007867812));
#44022=CARTESIAN_POINT('Ctrl Pts',(109.743306759122,3.18023406183943,127.050161095591));
#44023=CARTESIAN_POINT('Ctrl Pts',(109.735532425003,3.07341821787181,126.964662254341));
#44024=CARTESIAN_POINT('Ctrl Pts',(109.727767672056,2.96673401488562,126.879268782771));
#44025=CARTESIAN_POINT('Ctrl Pts',(109.720002919109,2.8563481188693,126.798212822449));
#44026=CARTESIAN_POINT('Ctrl Pts',(109.712238166162,2.7426496563545,126.721830038991));
#44027=CARTESIAN_POINT('Ctrl Pts',(109.704481125277,2.62906412075577,126.645523119991));
#44028=CARTESIAN_POINT('Ctrl Pts',(109.696724084392,2.5121728885132,126.573880357739));
#44029=CARTESIAN_POINT('Ctrl Pts',(109.688967043507,2.39239768655144,126.50719685854));
#44030=CARTESIAN_POINT('Ctrl Pts',(109.681215852266,2.27271280800103,126.440563645888));
#44031=CARTESIAN_POINT('Ctrl Pts',(109.673464661026,2.15014862879788,126.378882441815));
#44032=CARTESIAN_POINT('Ctrl Pts',(109.665713469786,2.02515504402298,126.322404559083));
#44033=CARTESIAN_POINT('Ctrl Pts',(109.657965573009,1.90021458485566,126.265950680959));
#44034=CARTESIAN_POINT('Ctrl Pts',(109.650217676232,1.77284712934111,126.214695886219));
#44035=CARTESIAN_POINT('Ctrl Pts',(109.642469779455,1.64352611552412,126.168845007616));
#44036=CARTESIAN_POINT('Ctrl Pts',(109.634723503371,1.51423215287529,126.123003720028));
#44037=CARTESIAN_POINT('Ctrl Pts',(109.626977227287,1.38298581299231,126.08256423075));
#44038=CARTESIAN_POINT('Ctrl Pts',(109.619230951203,1.25027903295238,126.047682637898));
#44039=CARTESIAN_POINT('Ctrl Pts',(109.611484617937,1.11757127330078,126.012800787558));
#44040=CARTESIAN_POINT('Ctrl Pts',(109.603738284672,0.983403430101634,125.983477014899));
#44041=CARTESIAN_POINT('Ctrl Pts',(109.595991951406,0.848280680115232,125.959816990944));
#44042=CARTESIAN_POINT('Ctrl Pts',(109.588243883403,0.713127670325847,125.936151668491));
#44043=CARTESIAN_POINT('Ctrl Pts',(109.5804958154,0.577019713255284,125.918152686044));
#44044=CARTESIAN_POINT('Ctrl Pts',(109.572747747397,0.440469812948712,125.905874177207));
#44045=CARTESIAN_POINT('Ctrl Pts',(109.564991444656,0.303774785783503,125.893582618625));
#44046=CARTESIAN_POINT('Ctrl Pts',(109.557235141914,0.166637267115951,125.887023713752));
#44047=CARTESIAN_POINT('Ctrl Pts',(109.549478839172,0.0295735497205978,
125.886199531585));
#44048=CARTESIAN_POINT('Ctrl Pts',(109.541718396658,-0.107563322707545,
125.885374909527));
#44049=CARTESIAN_POINT('Ctrl Pts',(109.533957954144,-0.244625924852864,
125.890291095059));
#44050=CARTESIAN_POINT('Ctrl Pts',(109.526197511629,-0.381101360076507,
125.900898084228));
#44051=CARTESIAN_POINT('Ctrl Pts',(109.518424611364,-0.517795877784491,
125.911522100678));
#44052=CARTESIAN_POINT('Ctrl Pts',(109.510651711099,-0.65390095660709,125.927855129561));
#44053=CARTESIAN_POINT('Ctrl Pts',(109.502878810833,-0.788911294049677,
125.949795546149));
#44054=CARTESIAN_POINT('Ctrl Pts',(109.495388475071,-0.919013665655613,
125.97093837333));
#44055=CARTESIAN_POINT('Ctrl Pts',(109.487898139309,-1.04809920544465,125.997287919293));
#44056=CARTESIAN_POINT('Ctrl Pts',(109.480407803547,-1.17572949275671,126.028709539193));
#44057=CARTESIAN_POINT('Ctrl Pts',(109.472633469428,-1.30819892120478,126.061322519363));
#44058=CARTESIAN_POINT('Ctrl Pts',(109.464859135309,-1.43952019033272,126.099503089383));
#44059=CARTESIAN_POINT('Ctrl Pts',(109.45708480119,-1.56918935971647,126.143156071973));
#44060=CARTESIAN_POINT('Ctrl Pts',(109.449320048243,-1.69869872343773,126.186755256164));
#44061=CARTESIAN_POINT('Ctrl Pts',(109.441555295296,-1.82655967160295,126.235813310318));
#44062=CARTESIAN_POINT('Ctrl Pts',(109.433790542348,-1.95227946682784,126.290184286728));
#44063=CARTESIAN_POINT('Ctrl Pts',(109.426033501463,-2.07787439537986,126.344501261117));
#44064=CARTESIAN_POINT('Ctrl Pts',(109.418276460578,-2.20133204654564,126.404120502365));
#44065=CARTESIAN_POINT('Ctrl Pts',(109.410519419693,-2.3221761853287,126.468846711834));
#44066=CARTESIAN_POINT('Ctrl Pts',(109.402768228453,-2.44292919460732,126.533524110766));
#44067=CARTESIAN_POINT('Ctrl Pts',(109.395017037213,-2.56107227115304,126.603300628479));
#44068=CARTESIAN_POINT('Ctrl Pts',(109.387265845973,-2.67615079914131,126.677933596188));
#44069=CARTESIAN_POINT('Ctrl Pts',(109.379517949196,-2.79118041568475,126.752534842895));
#44070=CARTESIAN_POINT('Ctrl Pts',(109.371770052419,-2.90314774693929,126.831988221928));
#44071=CARTESIAN_POINT('Ctrl Pts',(109.364022155642,-3.01162455648183,126.916006133559));
#44072=CARTESIAN_POINT('Ctrl Pts',(109.356275879557,-3.12007867501439,127.000006470454));
#44073=CARTESIAN_POINT('Ctrl Pts',(109.348529603473,-3.22504341522704,127.088569201543));
#44074=CARTESIAN_POINT('Ctrl Pts',(109.340783327389,-3.32612154334628,127.181364821076));
#44075=CARTESIAN_POINT('Ctrl Pts',(109.333036994124,-3.42720041760151,127.274161125604));
#44076=CARTESIAN_POINT('Ctrl Pts',(109.325290660859,-3.52439233451243,127.371190116524));
#44077=CARTESIAN_POINT('Ctrl Pts',(109.317544327593,-3.61733532967677,127.472083892087));
#44078=CARTESIAN_POINT('Ctrl Pts',(109.30979625959,-3.71029913878046,127.573000262111));
#44079=CARTESIAN_POINT('Ctrl Pts',(109.302048191587,-3.79901186788861,127.67778285151));
#44080=CARTESIAN_POINT('Ctrl Pts',(109.294300123584,-3.883150681651,127.786029315987));
#44081=CARTESIAN_POINT('Ctrl Pts',(109.286543820842,-3.96737891914557,127.894390826093));
#44082=CARTESIAN_POINT('Ctrl Pts',(109.2787875181,-4.04702329018245,128.006223256191));
#44083=CARTESIAN_POINT('Ctrl Pts',(109.271031215359,-4.12180298520095,128.121093352889));
#44084=CARTESIAN_POINT('Ctrl Pts',(109.263270772844,-4.19662259239436,128.236024759216));
#44085=CARTESIAN_POINT('Ctrl Pts',(109.25551033033,-4.26657215067226,128.35399672658));
#44086=CARTESIAN_POINT('Ctrl Pts',(109.247749887816,-4.33141649661511,128.474550712155));
#44087=CARTESIAN_POINT('Ctrl Pts',(109.239976987551,-4.39636493645869,128.59529822169));
#44088=CARTESIAN_POINT('Ctrl Pts',(109.232204087285,-4.45619161633874,128.718635680268));
#44089=CARTESIAN_POINT('Ctrl Pts',(109.22443118702,-4.51070890767654,128.84408303194));
#44090=CARTESIAN_POINT('Ctrl Pts',(109.216940851258,-4.56324435815248,128.964970056394));
#44091=CARTESIAN_POINT('Ctrl Pts',(109.209450515496,-4.61084962622054,129.087815950126));
#44092=CARTESIAN_POINT('Ctrl Pts',(109.201960179734,-4.65340101532632,129.212179078589));
#44093=CARTESIAN_POINT('Ctrl Pts',(109.194621588097,-4.69509037054069,129.334022777397));
#44094=CARTESIAN_POINT('Ctrl Pts',(109.18728299646,-4.73201650924825,129.457574369527));
#44095=CARTESIAN_POINT('Ctrl Pts',(109.179944404822,-4.76405452823403,129.582490119308));
#44096=CARTESIAN_POINT('Origin',(213.235140564004,0.,130.804360617566));
#44097=CARTESIAN_POINT('',(107.085000608365,-4.76405452823403,129.582490119308));
#44098=CARTESIAN_POINT('',(107.429960893282,-4.76405452823407,129.582490119308));
#44099=CARTESIAN_POINT('',(213.235140564004,-4.76405452823405,129.582490119308));
#44100=CARTESIAN_POINT('',(108.764859435936,-4.91824882485165,130.807760521293));
#44101=CARTESIAN_POINT('Ctrl Pts',(108.764859435936,-4.91824882485165,130.807760521293));
#44102=CARTESIAN_POINT('Ctrl Pts',(108.756034552605,-4.91814069778781,130.964175481081));
#44103=CARTESIAN_POINT('Ctrl Pts',(108.747209669273,-4.91056689496297,131.120296647971));
#44104=CARTESIAN_POINT('Ctrl Pts',(108.738384785941,-4.89563530303815,131.275463623443));
#44105=CARTESIAN_POINT('Ctrl Pts',(108.729520287116,-4.88063668219459,131.431327153887));
#44106=CARTESIAN_POINT('Ctrl Pts',(108.720655788291,-4.85821417577054,131.586227746882));
#44107=CARTESIAN_POINT('Ctrl Pts',(108.711791289465,-4.82852675013294,131.739514340625));
#44108=CARTESIAN_POINT('Ctrl Pts',(108.702874025054,-4.79866261124519,131.893713366874));
#44109=CARTESIAN_POINT('Ctrl Pts',(108.693956760643,-4.76144689983342,132.046278963872));
#44110=CARTESIAN_POINT('Ctrl Pts',(108.685039496232,-4.71709001905848,132.196569227868));
#44111=CARTESIAN_POINT('Ctrl Pts',(108.678244306911,-4.68328891272221,132.311094350146));
#44112=CARTESIAN_POINT('Ctrl Pts',(108.671449117589,-4.64534204592225,132.424298633557));
#44113=CARTESIAN_POINT('Ctrl Pts',(108.664653928267,-4.60336077874322,132.535906921662));
#44114=CARTESIAN_POINT('Ctrl Pts',(108.656879594148,-4.55533027034333,132.663597274515));
#44115=CARTESIAN_POINT('Ctrl Pts',(108.649105260029,-4.50190674915696,132.789489923373));
#44116=CARTESIAN_POINT('Ctrl Pts',(108.64133092591,-4.44324424605536,132.913095696327));
#44117=CARTESIAN_POINT('Ctrl Pts',(108.633566172963,-4.38465403924595,133.036549136213));
#44118=CARTESIAN_POINT('Ctrl Pts',(108.625801420016,-4.32083786320501,133.157720958096));
#44119=CARTESIAN_POINT('Ctrl Pts',(108.618036667069,-4.25199884069516,133.276139111126));
#44120=CARTESIAN_POINT('Ctrl Pts',(108.610279626184,-4.18322819007303,133.394439649577));
#44121=CARTESIAN_POINT('Ctrl Pts',(108.602522585299,-4.10944481606034,133.509991626097));
#44122=CARTESIAN_POINT('Ctrl Pts',(108.594765544414,-4.03089889785178,133.622345205494));
#44123=CARTESIAN_POINT('Ctrl Pts',(108.587014353174,-3.95241221173119,133.734614058182));
#44124=CARTESIAN_POINT('Ctrl Pts',(108.579263161934,-3.86917035312413,133.843688995428));
#44125=CARTESIAN_POINT('Ctrl Pts',(108.571511970694,-3.7814679864004,133.94914724472));
#44126=CARTESIAN_POINT('Ctrl Pts',(108.563764073917,-3.69380289552201,134.054560671444));
#44127=CARTESIAN_POINT('Ctrl Pts',(108.55601617714,-3.60168131666245,134.156360167594));
#44128=CARTESIAN_POINT('Ctrl Pts',(108.548268280362,-3.50543941500974,134.25415446216));
#44129=CARTESIAN_POINT('Ctrl Pts',(108.540522004278,-3.40921764508805,134.351928300267));
#44130=CARTESIAN_POINT('Ctrl Pts',(108.532775728194,-3.308877540765,134.445698324743));
#44131=CARTESIAN_POINT('Ctrl Pts',(108.52502945211,-3.20479321825092,134.535108999694));
#44132=CARTESIAN_POINT('Ctrl Pts',(108.517283118845,-3.10070812741009,134.624520334655));
#44133=CARTESIAN_POINT('Ctrl Pts',(108.509536785579,-2.99287905979412,134.70957200112));
#44134=CARTESIAN_POINT('Ctrl Pts',(108.501790452314,-2.88171409324305,134.78994802061));
#44135=CARTESIAN_POINT('Ctrl Pts',(108.494042384311,-2.77052423206849,134.870342039752));
#44136=CARTESIAN_POINT('Ctrl Pts',(108.486294316308,-2.65599730217761,134.946058099321));
#44137=CARTESIAN_POINT('Ctrl Pts',(108.478546248305,-2.53857096140315,135.016823143977));
#44138=CARTESIAN_POINT('Ctrl Pts',(108.470789945563,-2.42101981851632,135.087663398565));
#44139=CARTESIAN_POINT('Ctrl Pts',(108.463033642822,-2.30056344445518,135.153541924713));
#44140=CARTESIAN_POINT('Ctrl Pts',(108.45527734008,-2.17766522618921,135.214231049353));
#44141=CARTESIAN_POINT('Ctrl Pts',(108.447516897566,-2.05470141344358,135.274952565605));
#44142=CARTESIAN_POINT('Ctrl Pts',(108.439756455051,-1.92929351690171,135.330479003201));
#44143=CARTESIAN_POINT('Ctrl Pts',(108.431996012537,-1.80192464475143,135.380631002622));
#44144=CARTESIAN_POINT('Ctrl Pts',(108.424223112272,-1.67435130878047,135.430863510484));
#44145=CARTESIAN_POINT('Ctrl Pts',(108.416450212006,-1.54481107629906,135.475704211666));
#44146=CARTESIAN_POINT('Ctrl Pts',(108.408677311741,-1.41380280375881,135.515023489666));
#44147=CARTESIAN_POINT('Ctrl Pts',(108.401186975979,-1.2875570119156,135.552913412872));
#44148=CARTESIAN_POINT('Ctrl Pts',(108.393696640217,-1.1599483592065,135.585676302073));
#44149=CARTESIAN_POINT('Ctrl Pts',(108.386206304455,-1.03142999867423,135.613241487408));
#44150=CARTESIAN_POINT('Ctrl Pts',(108.378431970336,-0.898038825439874,
135.641851815124));
#44151=CARTESIAN_POINT('Ctrl Pts',(108.370657636217,-0.763245056347442,
135.664953145524));
#44152=CARTESIAN_POINT('Ctrl Pts',(108.362883302098,-0.627543503026194,
135.682410659776));
#44153=CARTESIAN_POINT('Ctrl Pts',(108.355118549151,-0.492009189741419,
135.699846659203));
#44154=CARTESIAN_POINT('Ctrl Pts',(108.347353796204,-0.355569702279653,
135.711652632446));
#44155=CARTESIAN_POINT('Ctrl Pts',(108.339589043256,-0.218731983206265,
135.717744317423));
#44156=CARTESIAN_POINT('Ctrl Pts',(108.331832002371,-0.0820301732845349,
135.723829952053));
#44157=CARTESIAN_POINT('Ctrl Pts',(108.324074961486,0.0550686930768079,
135.724212575665));
#44158=CARTESIAN_POINT('Ctrl Pts',(108.316317920601,0.192050928824161,135.718859524193));
#44159=CARTESIAN_POINT('Ctrl Pts',(108.308566729361,0.328929865201878,135.713510509498));
#44160=CARTESIAN_POINT('Ctrl Pts',(108.300815538121,0.465691956942546,135.702434444206));
#44161=CARTESIAN_POINT('Ctrl Pts',(108.293064346881,0.601822240268474,135.685650718924));
#44162=CARTESIAN_POINT('Ctrl Pts',(108.285316450104,0.737894664592687,135.668874127174));
#44163=CARTESIAN_POINT('Ctrl Pts',(108.277568553327,0.873335427383866,135.646394748121));
#44164=CARTESIAN_POINT('Ctrl Pts',(108.26982065655,1.00763363576269,135.61828391552));
#44165=CARTESIAN_POINT('Ctrl Pts',(108.262074380466,1.14190375185145,135.590178963098));
#44166=CARTESIAN_POINT('Ctrl Pts',(108.254328104382,1.27503140647794,135.556444980241));
#44167=CARTESIAN_POINT('Ctrl Pts',(108.246581828298,1.40651525827599,135.517204545677));
#44168=CARTESIAN_POINT('Ctrl Pts',(108.238835495032,1.53800008065797,135.47796382145));
#44169=CARTESIAN_POINT('Ctrl Pts',(108.231089161767,1.66784070136172,135.433216676214));
#44170=CARTESIAN_POINT('Ctrl Pts',(108.223342828502,1.79555070270169,135.383135643326));
#44171=CARTESIAN_POINT('Ctrl Pts',(108.215594760499,1.92328930381108,135.333043395139));
#44172=CARTESIAN_POINT('Ctrl Pts',(108.207846692496,2.04889597219868,135.277615025115));
#44173=CARTESIAN_POINT('Ctrl Pts',(108.200098624493,2.17190441392461,135.217071154104));
#44174=CARTESIAN_POINT('Ctrl Pts',(108.192342321751,2.29504359048615,135.156462936346));
#44175=CARTESIAN_POINT('Ctrl Pts',(108.184586019009,2.41557867280187,135.090728529902));
#44176=CARTESIAN_POINT('Ctrl Pts',(108.176829716267,2.53306764109497,135.020134732499));
#44177=CARTESIAN_POINT('Ctrl Pts',(108.169069273753,2.65061931678806,134.94950325706));
#44178=CARTESIAN_POINT('Ctrl Pts',(108.161308831239,2.7651213126664,134.874007437792));
#44179=CARTESIAN_POINT('Ctrl Pts',(108.153548388725,2.87616159671256,134.793956779096));
#44180=CARTESIAN_POINT('Ctrl Pts',(108.145775488459,2.98738013248029,134.713777615976));
#44181=CARTESIAN_POINT('Ctrl Pts',(108.138002588194,3.09512554419143,134.629029243903));
#44182=CARTESIAN_POINT('Ctrl Pts',(108.130229687928,3.19901913771574,134.540061304054));
#44183=CARTESIAN_POINT('Ctrl Pts',(108.122739352166,3.29913593742404,134.454327572915));
#44184=CARTESIAN_POINT('Ctrl Pts',(108.115249016404,3.39567587780697,134.364675941216));
#44185=CARTESIAN_POINT('Ctrl Pts',(108.107758680642,3.48833456202035,134.271449460661));
#44186=CARTESIAN_POINT('Ctrl Pts',(108.099984346523,3.58450642840799,134.174688269761));
#44187=CARTESIAN_POINT('Ctrl Pts',(108.092210012404,3.67680155665234,134.073769287628));
#44188=CARTESIAN_POINT('Ctrl Pts',(108.084435678285,3.76483906208055,133.969035940428));
#44189=CARTESIAN_POINT('Ctrl Pts',(108.076670925338,3.85276806915139,133.864431667718));
#44190=CARTESIAN_POINT('Ctrl Pts',(108.068906172391,3.93644964449626,133.756022679665));
#44191=CARTESIAN_POINT('Ctrl Pts',(108.061141419443,4.0155388811991,133.64418993569));
#44192=CARTESIAN_POINT('Ctrl Pts',(108.053384378558,4.09454956535708,133.532468265574));
#44193=CARTESIAN_POINT('Ctrl Pts',(108.045627337673,4.16897676353303,133.417329923871));
#44194=CARTESIAN_POINT('Ctrl Pts',(108.037870296788,4.23851533412164,133.299189434322));
#44195=CARTESIAN_POINT('Ctrl Pts',(108.030119105548,4.30800146513324,133.181138035435));
#44196=CARTESIAN_POINT('Ctrl Pts',(108.022367914308,4.37260610889755,133.060089330511));
#44197=CARTESIAN_POINT('Ctrl Pts',(108.014616723068,4.43206722878328,132.936487054259));
#44198=CARTESIAN_POINT('Ctrl Pts',(108.006868826291,4.49150307610689,132.812937312272));
#44199=CARTESIAN_POINT('Ctrl Pts',(107.999120929514,4.54579957847373,132.686836509186));
#44200=CARTESIAN_POINT('Ctrl Pts',(107.991373032737,4.59474060091079,132.558653031288));
#44201=CARTESIAN_POINT('Ctrl Pts',(107.983626756653,4.64367138594099,132.43049636661));
#44202=CARTESIAN_POINT('Ctrl Pts',(107.975880480569,4.68724877991678,132.300258258669));
#44203=CARTESIAN_POINT('Ctrl Pts',(107.968134204485,4.72530492453977,132.168426756952));
#44204=CARTESIAN_POINT('Ctrl Pts',(107.960387871219,4.7633613500846,132.036594282085));
#44205=CARTESIAN_POINT('Ctrl Pts',(107.952641537954,4.7958963365164,131.9031687656));
#44206=CARTESIAN_POINT('Ctrl Pts',(107.944895204688,4.82279212039432,131.768652702965));
#44207=CARTESIAN_POINT('Ctrl Pts',(107.937147136685,4.84969392739654,131.63410651639));
#44208=CARTESIAN_POINT('Ctrl Pts',(107.929399068683,4.8709539422595,131.498469680999));
#44209=CARTESIAN_POINT('Ctrl Pts',(107.92165100068,4.88650573628719,131.362253754047));
#44210=CARTESIAN_POINT('Ctrl Pts',(107.913894697938,4.90207405894664,131.225893055187));
#44211=CARTESIAN_POINT('Ctrl Pts',(107.906138395196,4.91192199733498,131.088952424369));
#44212=CARTESIAN_POINT('Ctrl Pts',(107.898382092454,4.91603509344909,130.951947956037));
#44213=CARTESIAN_POINT('Ctrl Pts',(107.89062164994,4.92015038484644,130.814870364296));
#44214=CARTESIAN_POINT('Ctrl Pts',(107.882861207426,4.91852473958268,130.677729257896));
#44215=CARTESIAN_POINT('Ctrl Pts',(107.875100764911,4.91119583910588,130.541038585732));
#44216=CARTESIAN_POINT('Ctrl Pts',(107.867327864646,4.90385517362742,130.404128485567));
#44217=CARTESIAN_POINT('Ctrl Pts',(107.859554964381,4.8907929948618,130.267670653986));
#44218=CARTESIAN_POINT('Ctrl Pts',(107.851782064115,4.87209877240557,130.132172686683));
#44219=CARTESIAN_POINT('Ctrl Pts',(107.844291728353,4.85408413202345,130.00160041179));
#44220=CARTESIAN_POINT('Ctrl Pts',(107.836801392591,4.83083987110543,129.871919728997));
#44221=CARTESIAN_POINT('Ctrl Pts',(107.829311056829,4.80249007483505,129.743572163815));
#44222=CARTESIAN_POINT('Ctrl Pts',(107.82153672271,4.77306538742247,129.61035826169));
#44223=CARTESIAN_POINT('Ctrl Pts',(107.813762388591,4.73804716082972,129.478158581438));
#44224=CARTESIAN_POINT('Ctrl Pts',(107.805988054472,4.69751845174746,129.347479202353));
#44225=CARTESIAN_POINT('Ctrl Pts',(107.798223301525,4.65703969067701,129.216960873925));
#44226=CARTESIAN_POINT('Ctrl Pts',(107.790458548578,4.61106407423523,129.087959488522));
#44227=CARTESIAN_POINT('Ctrl Pts',(107.78269379563,4.55972568376157,128.960971143975));
#44228=CARTESIAN_POINT('Ctrl Pts',(107.774936754745,4.50843828330107,128.834108926043));
#44229=CARTESIAN_POINT('Ctrl Pts',(107.76717971386,4.45179885413864,128.709256130229));
#44230=CARTESIAN_POINT('Ctrl Pts',(107.759422672975,4.38999121034556,128.586893541015));
#44231=CARTESIAN_POINT('Ctrl Pts',(107.751671481735,4.32823017617746,128.464623226381));
#44232=CARTESIAN_POINT('Ctrl Pts',(107.743920290495,4.26130886045816,128.344839728093));
#44233=CARTESIAN_POINT('Ctrl Pts',(107.736169099255,4.18945895256576,128.228003354439));
#44234=CARTESIAN_POINT('Ctrl Pts',(107.728421202478,4.11763958280088,128.111216639361));
#44235=CARTESIAN_POINT('Ctrl Pts',(107.720673305701,4.04089599159981,127.997374889912));
#44236=CARTESIAN_POINT('Ctrl Pts',(107.712925408924,3.95950541937726,127.886913120794));
#44237=CARTESIAN_POINT('Ctrl Pts',(107.70517913284,3.87813187230783,127.776474457897));
#44238=CARTESIAN_POINT('Ctrl Pts',(107.697432856756,3.79211350944316,127.669414683585));
#44239=CARTESIAN_POINT('Ctrl Pts',(107.689686580671,3.70177020912853,127.566138824466));
#44240=CARTESIAN_POINT('Ctrl Pts',(107.681940247406,3.61142624192018,127.462862202988));
#44241=CARTESIAN_POINT('Ctrl Pts',(107.674193914141,3.51675753097159,127.363369846705));
#44242=CARTESIAN_POINT('Ctrl Pts',(107.666447580875,3.41812318593567,127.268032444408));
#44243=CARTESIAN_POINT('Ctrl Pts',(107.658699512872,3.31946675242206,127.172673691962));
#44244=CARTESIAN_POINT('Ctrl Pts',(107.650951444869,3.21684319871082,127.0814720167));
#44245=CARTESIAN_POINT('Ctrl Pts',(107.643203376866,3.11064700607623,126.994759816158));
#44246=CARTESIAN_POINT('Ctrl Pts',(107.635447074125,3.00433794686436,126.907955456858));
#44247=CARTESIAN_POINT('Ctrl Pts',(107.627690771383,2.89444896704493,126.825650351465));
#44248=CARTESIAN_POINT('Ctrl Pts',(107.619934468641,2.78140645658704,126.748135625562));
#44249=CARTESIAN_POINT('Ctrl Pts',(107.612174026127,2.66830361193761,126.670579527716));
#44250=CARTESIAN_POINT('Ctrl Pts',(107.604413583612,2.55204421411191,126.59781911125));
#44251=CARTESIAN_POINT('Ctrl Pts',(107.596653141098,2.4330810306136,126.530100475627));
#44252=CARTESIAN_POINT('Ctrl Pts',(107.588880240833,2.31392687685209,126.462273132038));
#44253=CARTESIAN_POINT('Ctrl Pts',(107.581107340567,2.19206061177229,126.399503921837));
#44254=CARTESIAN_POINT('Ctrl Pts',(107.573334440302,2.06795765050916,126.341991939588));
#44255=CARTESIAN_POINT('Ctrl Pts',(107.56584410454,1.94836614448477,126.286570662758));
#44256=CARTESIAN_POINT('Ctrl Pts',(107.558353768778,1.8266980225053,126.236031141104));
#44257=CARTESIAN_POINT('Ctrl Pts',(107.550863433016,1.70339182356023,126.19050763357));
#44258=CARTESIAN_POINT('Ctrl Pts',(107.543089098897,1.57541043260377,126.143258088411));
#44259=CARTESIAN_POINT('Ctrl Pts',(107.535314764778,1.44525889067726,126.101262757879));
#44260=CARTESIAN_POINT('Ctrl Pts',(107.527540430659,1.31340787079371,126.064725312246));
#44261=CARTESIAN_POINT('Ctrl Pts',(107.519775677712,1.1817193455084,126.028232895749));
#44262=CARTESIAN_POINT('Ctrl Pts',(107.512010924765,1.04833588275632,125.997185084115));
#44263=CARTESIAN_POINT('Ctrl Pts',(107.504246171817,0.91374733793175,125.971737223909));
#44264=CARTESIAN_POINT('Ctrl Pts',(107.496489130932,0.779292468347171,125.946314638876));
#44265=CARTESIAN_POINT('Ctrl Pts',(107.488732090047,0.643635280256703,125.926481008906));
#44266=CARTESIAN_POINT('Ctrl Pts',(107.480975049162,0.507279627256514,125.91234156177));
#44267=CARTESIAN_POINT('Ctrl Pts',(107.473223857922,0.371026801114852,125.898212777301));
#44268=CARTESIAN_POINT('Ctrl Pts',(107.465472666682,0.234076945769885,125.889769668827));
#44269=CARTESIAN_POINT('Ctrl Pts',(107.457721475442,0.0969425653892498,
125.887066117384));
#44270=CARTESIAN_POINT('Ctrl Pts',(107.449973578665,-0.0401335292214509,
125.884363715024));
#44271=CARTESIAN_POINT('Ctrl Pts',(107.442225681888,-0.177393602809493,
125.887396025476));
#44272=CARTESIAN_POINT('Ctrl Pts',(107.434477785111,-0.314321809969613,
125.896164934601));
#44273=CARTESIAN_POINT('Ctrl Pts',(107.426731509027,-0.451221374700625,
125.904932009459));
#44274=CARTESIAN_POINT('Ctrl Pts',(107.418985232943,-0.587788821163742,
125.919433271207));
#44275=CARTESIAN_POINT('Ctrl Pts',(107.411238956858,-0.723510486942408,
125.93961852391));
#44276=CARTESIAN_POINT('Ctrl Pts',(107.403492623593,-0.859233154587487,
125.959803925617));
#44277=CARTESIAN_POINT('Ctrl Pts',(107.395746290328,-0.99410964237823,125.985673344488));
#44278=CARTESIAN_POINT('Ctrl Pts',(107.387999957062,-1.12763397179549,126.017125017749));
#44279=CARTESIAN_POINT('Ctrl Pts',(107.380251889059,-1.26118820306053,126.048583734395));
#44280=CARTESIAN_POINT('Ctrl Pts',(107.372503821056,-1.39338929292455,126.085627103379));
#44281=CARTESIAN_POINT('Ctrl Pts',(107.364755753053,-1.52374435916254,126.128102905418));
#44282=CARTESIAN_POINT('Ctrl Pts',(107.356999450312,-1.65423796831636,126.170623851246));
#44283=CARTESIAN_POINT('Ctrl Pts',(107.34924314757,-1.78288126226469,126.218588642307));
#44284=CARTESIAN_POINT('Ctrl Pts',(107.341486844828,-1.90919883461748,126.271795905133));
#44285=CARTESIAN_POINT('Ctrl Pts',(107.333726402314,-2.03558382646206,126.325031566276));
#44286=CARTESIAN_POINT('Ctrl Pts',(107.3259659598,-2.15964026983527,126.383515107933));
#44287=CARTESIAN_POINT('Ctrl Pts',(107.318205517285,-2.28091638239481,126.446998626748));
#44288=CARTESIAN_POINT('Ctrl Pts',(107.31043261702,-2.40238717813653,126.510584054944));
#44289=CARTESIAN_POINT('Ctrl Pts',(107.302659716754,-2.52106838542017,126.57918530385));
#44290=CARTESIAN_POINT('Ctrl Pts',(107.294886816489,-2.63653552685606,126.652510008726));
#44291=CARTESIAN_POINT('Ctrl Pts',(107.287396480727,-2.74780514685642,126.723169175885));
#44292=CARTESIAN_POINT('Ctrl Pts',(107.279906144965,-2.85609006961675,126.798214166777));
#44293=CARTESIAN_POINT('Ctrl Pts',(107.272415809203,-2.9610402982491,126.877348596367));
#44294=CARTESIAN_POINT('Ctrl Pts',(107.264606842501,-3.07045499830437,126.959849320667));
#44295=CARTESIAN_POINT('Ctrl Pts',(107.2567978758,-3.17661290686497,127.04707268425));
#44296=CARTESIAN_POINT('Ctrl Pts',(107.248988909098,-3.27907398866812,127.138728770348));
#44297=CARTESIAN_POINT('Ctrl Pts',(107.24130636499,-3.37987628562483,127.228900998145));
#44298=CARTESIAN_POINT('Ctrl Pts',(107.233623820881,-3.47710021184727,127.323363256761));
#44299=CARTESIAN_POINT('Ctrl Pts',(107.225941276772,-3.57035532253909,127.421795624352));
#44300=CARTESIAN_POINT('Ctrl Pts',(107.218265722842,-3.66352558245395,127.520138430494));
#44301=CARTESIAN_POINT('Ctrl Pts',(107.210590168911,-3.75273393443584,127.622443874409));
#44302=CARTESIAN_POINT('Ctrl Pts',(107.20291461498,-3.83762421044486,127.72835289945));
#44303=CARTESIAN_POINT('Ctrl Pts',(107.195244297365,-3.92245657372734,127.83418967263));
#44304=CARTESIAN_POINT('Ctrl Pts',(107.18757397975,-4.00297647128173,127.943624826383));
#44305=CARTESIAN_POINT('Ctrl Pts',(107.179903662135,-4.07886607850665,128.056264080669));
#44306=CARTESIAN_POINT('Ctrl Pts',(107.171995074321,-4.15711311507403,128.17240235271));
#44307=CARTESIAN_POINT('Ctrl Pts',(107.164086486507,-4.23043721623045,128.291946705557));
#44308=CARTESIAN_POINT('Ctrl Pts',(107.156177898692,-4.29853633508979,128.414429982921));
#44309=CARTESIAN_POINT('Ctrl Pts',(107.148511678719,-4.3645484775137,128.533159618273));
#44310=CARTESIAN_POINT('Ctrl Pts',(107.140845458746,-4.42565100790585,128.654650303783));
#44311=CARTESIAN_POINT('Ctrl Pts',(107.133179238773,-4.48161447020671,128.778449759968));
#44312=CARTESIAN_POINT('Ctrl Pts',(107.125149467038,-4.54023186304472,128.908120103045));
#44313=CARTESIAN_POINT('Ctrl Pts',(107.117119695303,-4.59321060406721,129.040323138286));
#44314=CARTESIAN_POINT('Ctrl Pts',(107.109089923569,-4.64034318807285,129.174514563668));
#44315=CARTESIAN_POINT('Ctrl Pts',(107.101060151834,-4.6874757720785,129.308705989051));
#44316=CARTESIAN_POINT('Ctrl Pts',(107.0930303801,-4.728762059849,129.444885320713));
#44317=CARTESIAN_POINT('Ctrl Pts',(107.085000608365,-4.76405452823403,129.582490119308));
#44318=CARTESIAN_POINT('Ctrl Pts',(108.834713077301,-4.76405452823406,129.582490119308));
#44319=CARTESIAN_POINT('Ctrl Pts',(108.826933119087,-4.79829315580961,129.715986008582));
#44320=CARTESIAN_POINT('Ctrl Pts',(108.819153160872,-4.82693196985436,129.850982631195));
#44321=CARTESIAN_POINT('Ctrl Pts',(108.811373202658,-4.84985164498987,129.986973265028));
#44322=CARTESIAN_POINT('Ctrl Pts',(108.803593423799,-4.87277079174911,130.122960763815));
#44323=CARTESIAN_POINT('Ctrl Pts',(108.795813644939,-4.88997098710633,130.259941849649));
#44324=CARTESIAN_POINT('Ctrl Pts',(108.788033866079,-4.90138409773953,130.39739994511));
#44325=CARTESIAN_POINT('Ctrl Pts',(108.78030905605,-4.91271656786181,130.533886816213));
#44326=CARTESIAN_POINT('Ctrl Pts',(108.77258424602,-4.91834347321842,130.670843599752));
#44327=CARTESIAN_POINT('Ctrl Pts',(108.764859435991,-4.91824882485232,130.80776052032));
#44328=CARTESIAN_POINT('',(109.110140564059,-4.91824845869996,130.800466905272));
#44329=CARTESIAN_POINT('Ctrl Pts',(109.179944404822,-4.76405452823403,129.582490119308));
#44330=CARTESIAN_POINT('Ctrl Pts',(109.170808292833,-4.80393996454638,129.738002830144));
#44331=CARTESIAN_POINT('Ctrl Pts',(109.161672180843,-4.83624795301888,129.895630417634));
#44332=CARTESIAN_POINT('Ctrl Pts',(109.152536068854,-4.86077948173073,130.054690094946));
#44333=CARTESIAN_POINT('Ctrl Pts',(109.143482846257,-4.88508844273259,130.21230666822));
#44334=CARTESIAN_POINT('Ctrl Pts',(109.13442962366,-4.90176134354085,130.371329371744));
#44335=CARTESIAN_POINT('Ctrl Pts',(109.125376401064,-4.91065141233991,130.531073645714));
#44336=CARTESIAN_POINT('Ctrl Pts',(109.120297788729,-4.91563849981933,130.62068585082));
#44337=CARTESIAN_POINT('Ctrl Pts',(109.115219176394,-4.918177252701,130.710524770806));
#44338=CARTESIAN_POINT('Ctrl Pts',(109.110140564059,-4.91824845869996,130.800466905272));
#44339=CARTESIAN_POINT('Ctrl Pts',(109.110140564008,-4.91824845870068,130.800466906176));
#44340=CARTESIAN_POINT('Ctrl Pts',(109.102364397004,-4.9183574864379,130.938182686036));
#44341=CARTESIAN_POINT('Ctrl Pts',(109.094588230001,-4.91267786849137,131.075970964058));
#44342=CARTESIAN_POINT('Ctrl Pts',(109.086812062997,-4.90121868070611,131.213308666097));
#44343=CARTESIAN_POINT('Ctrl Pts',(109.079076477325,-4.88981929476085,131.349929646547));
#44344=CARTESIAN_POINT('Ctrl Pts',(109.071340891652,-4.8727005703394,131.48610435019));
#44345=CARTESIAN_POINT('Ctrl Pts',(109.06360530598,-4.84992360522252,131.621320889553));
#44346=CARTESIAN_POINT('Ctrl Pts',(109.055869424027,-4.82714576772626,131.756542607839));
#44347=CARTESIAN_POINT('Ctrl Pts',(109.048133542075,-4.79870932295161,131.890805702541));
#44348=CARTESIAN_POINT('Ctrl Pts',(109.040397660122,-4.76472675750061,132.023607101612));
#44349=CARTESIAN_POINT('Ctrl Pts',(109.032659799947,-4.73073550201525,132.156442460706));
#44350=CARTESIAN_POINT('Ctrl Pts',(109.024921939771,-4.69119540060019,132.287815001019));
#44351=CARTESIAN_POINT('Ctrl Pts',(109.017184079596,-4.64626909585595,132.417235861159));
#44352=CARTESIAN_POINT('Ctrl Pts',(109.00937811929,-4.60094739921181,132.547795741302));
#44353=CARTESIAN_POINT('Ctrl Pts',(109.001572158984,-4.5501443666063,132.676369038117));
#44354=CARTESIAN_POINT('Ctrl Pts',(108.993766198677,-4.49407649494377,132.802474608332));
#44355=CARTESIAN_POINT('Ctrl Pts',(108.986015200061,-4.4384033966153,132.927692270465));
#44356=CARTESIAN_POINT('Ctrl Pts',(108.978264201445,-4.377539595994,133.050476523415));
#44357=CARTESIAN_POINT('Ctrl Pts',(108.970513202828,-4.31174283950206,133.170381908363));
#44358=CARTESIAN_POINT('Ctrl Pts',(108.962679761677,-4.24524624397538,133.291562652056));
#44359=CARTESIAN_POINT('Ctrl Pts',(108.954846320526,-4.17371137008288,133.409802584944));
#44360=CARTESIAN_POINT('Ctrl Pts',(108.947012879375,-4.09744815581249,133.524673407105));
#44361=CARTESIAN_POINT('Ctrl Pts',(108.939179438224,-4.02118494154209,133.639544229266));
#44362=CARTESIAN_POINT('Ctrl Pts',(108.931345997072,-3.94019367744347,133.751045650442));
#44363=CARTESIAN_POINT('Ctrl Pts',(108.923512555921,-3.85482433608878,133.858785669912));
#44364=CARTESIAN_POINT('Ctrl Pts',(108.915738221802,-3.77009914694037,133.96571273979));
#44365=CARTESIAN_POINT('Ctrl Pts',(108.907963887683,-3.68078739166395,134.069281277589));
#44366=CARTESIAN_POINT('Ctrl Pts',(108.900189553564,-3.58718510686284,134.169072502944));
#44367=CARTESIAN_POINT('Ctrl Pts',(108.892424800617,-3.4936981785124,134.268740744531));
#44368=CARTESIAN_POINT('Ctrl Pts',(108.88466004767,-3.39593150647519,134.364640653717));
#44369=CARTESIAN_POINT('Ctrl Pts',(108.876895294723,-3.29422264719171,134.456384743065));
#44370=CARTESIAN_POINT('Ctrl Pts',(108.869138253838,-3.19261480658105,134.548037710891));
#44371=CARTESIAN_POINT('Ctrl Pts',(108.861381212953,-3.08707285904919,134.635542812854));
#44372=CARTESIAN_POINT('Ctrl Pts',(108.853624172068,-2.97797238705606,134.718548084261));
#44373=CARTESIAN_POINT('Ctrl Pts',(108.845872980828,-2.86895418857785,134.801490760747));
#44374=CARTESIAN_POINT('Ctrl Pts',(108.838121789588,-2.75638311689477,134.879940125178));
#44375=CARTESIAN_POINT('Ctrl Pts',(108.830370598348,-2.64066885205257,134.953583566059));
#44376=CARTESIAN_POINT('Ctrl Pts',(108.82262270157,-2.52500376885939,135.027195706513));
#44377=CARTESIAN_POINT('Ctrl Pts',(108.814874804793,-2.40619847873435,135.096005776607));
#44378=CARTESIAN_POINT('Ctrl Pts',(108.807126908016,-2.2846925621417,135.159743833656));
#44379=CARTESIAN_POINT('Ctrl Pts',(108.799380631932,-2.16321206196751,135.223468558077));
#44380=CARTESIAN_POINT('Ctrl Pts',(108.791634355848,-2.03903240497035,135.282123198249));
#44381=CARTESIAN_POINT('Ctrl Pts',(108.783888079764,-1.9126183990844,135.335483427862));
#44382=CARTESIAN_POINT('Ctrl Pts',(108.776141746499,-1.78620346003888,135.388844051367));
#44383=CARTESIAN_POINT('Ctrl Pts',(108.768395413233,-1.65755449938448,135.436910034288));
#44384=CARTESIAN_POINT('Ctrl Pts',(108.760649079968,-1.52715658656531,135.47950508834));
#44385=CARTESIAN_POINT('Ctrl Pts',(108.752901011965,-1.39672947203777,135.52210968126));
#44386=CARTESIAN_POINT('Ctrl Pts',(108.745152943962,-1.264552997545,135.559240785977));
#44387=CARTESIAN_POINT('Ctrl Pts',(108.737404875959,-1.1311272939735,135.590772019371));
#44388=CARTESIAN_POINT('Ctrl Pts',(108.729648573217,-0.997559783976367,
135.622336764534));
#44389=CARTESIAN_POINT('Ctrl Pts',(108.721892270475,-0.862740773777352,
135.648289659332));
#44390=CARTESIAN_POINT('Ctrl Pts',(108.714135967734,-0.72718103788804,135.668555391692));
#44391=CARTESIAN_POINT('Ctrl Pts',(108.706375525219,-0.591548949686152,
135.688831940484));
#44392=CARTESIAN_POINT('Ctrl Pts',(108.698615082705,-0.45517573658895,135.703415236976));
#44393=CARTESIAN_POINT('Ctrl Pts',(108.690854640191,-0.31857620069985,135.712281997015));
#44394=CARTESIAN_POINT('Ctrl Pts',(108.683081739926,-0.181757383108912,
135.721162990764));
#44395=CARTESIAN_POINT('Ctrl Pts',(108.67530883966,-0.0447119077972331,
135.724309101127));
#44396=CARTESIAN_POINT('Ctrl Pts',(108.667535939395,0.0920456152316443,
135.721749219987));
#44397=CARTESIAN_POINT('Ctrl Pts',(108.660045603633,0.223831657826546,135.719282396973));
#44398=CARTESIAN_POINT('Ctrl Pts',(108.652555267871,0.355350012764772,135.711517252458));
#44399=CARTESIAN_POINT('Ctrl Pts',(108.645064932109,0.486147589374755,135.698524855089));
#44400=CARTESIAN_POINT('Ctrl Pts',(108.63729059799,0.621904395857443,135.685039847024));
#44401=CARTESIAN_POINT('Ctrl Pts',(108.629516263871,0.757314725209164,135.665880662352));
#44402=CARTESIAN_POINT('Ctrl Pts',(108.621741929752,0.891866230632137,135.641070004035));
#44403=CARTESIAN_POINT('Ctrl Pts',(108.613977176804,1.02625191334962,135.616289922637));
#44404=CARTESIAN_POINT('Ctrl Pts',(108.606212423857,1.1597804972938,135.585872295956));
#44405=CARTESIAN_POINT('Ctrl Pts',(108.59844767091,1.29194352080965,135.549891673363));
#44406=CARTESIAN_POINT('Ctrl Pts',(108.590690630025,1.42397527814763,135.513946787232));
#44407=CARTESIAN_POINT('Ctrl Pts',(108.58293358914,1.55464379934905,135.472450002712));
#44408=CARTESIAN_POINT('Ctrl Pts',(108.575176548255,1.68344995505456,135.425527062451));
#44409=CARTESIAN_POINT('Ctrl Pts',(108.567425357015,1.81215897703661,135.378639507143));
#44410=CARTESIAN_POINT('Ctrl Pts',(108.559674165775,1.93900806308132,135.326334074065));
#44411=CARTESIAN_POINT('Ctrl Pts',(108.551922974535,2.06351276221074,135.268786464491));
#44412=CARTESIAN_POINT('Ctrl Pts',(108.544175077758,2.18796454352116,135.211263314187));
#44413=CARTESIAN_POINT('Ctrl Pts',(108.53642718098,2.3100735655871,135.14850258253));
#44414=CARTESIAN_POINT('Ctrl Pts',(108.528679284203,2.42937511400288,135.080728190397));
#44415=CARTESIAN_POINT('Ctrl Pts',(108.520933008119,2.54865170710675,135.012967975207));
#44416=CARTESIAN_POINT('Ctrl Pts',(108.513186732035,2.66512165493384,134.940196378557));
#44417=CARTESIAN_POINT('Ctrl Pts',(108.505440455951,2.77834498536226,134.862683202676));
#44418=CARTESIAN_POINT('Ctrl Pts',(108.497694122686,2.89156915157935,134.78516945461));
#44419=CARTESIAN_POINT('Ctrl Pts',(108.48994778942,3.00154632996856,134.702914278329));
#44420=CARTESIAN_POINT('Ctrl Pts',(108.482201456155,3.1078660123223,134.616230488371));
#44421=CARTESIAN_POINT('Ctrl Pts',(108.474453388152,3.2142095042316,134.52952728618));
#44422=CARTESIAN_POINT('Ctrl Pts',(108.466705320149,3.3168935672912,134.438393743834));
#44423=CARTESIAN_POINT('Ctrl Pts',(108.458957252146,3.41554153884024,134.34318232245));
#44424=CARTESIAN_POINT('Ctrl Pts',(108.451200949404,3.51429435462757,134.247869709234));
#44425=CARTESIAN_POINT('Ctrl Pts',(108.443444646662,3.60900222819488,134.148470831253));
#44426=CARTESIAN_POINT('Ctrl Pts',(108.43568834392,3.69932571126356,134.045374709557));
#44427=CARTESIAN_POINT('Ctrl Pts',(108.427927901406,3.78969740269467,133.942223562357));
#44428=CARTESIAN_POINT('Ctrl Pts',(108.420167458892,3.87567979583365,133.835371543859));
#44429=CARTESIAN_POINT('Ctrl Pts',(108.412407016378,3.95697503795119,133.725239185999));
#44430=CARTESIAN_POINT('Ctrl Pts',(108.404634116112,4.03840078240848,133.614930033901));
#44431=CARTESIAN_POINT('Ctrl Pts',(108.396861215847,4.11512412108769,133.501330343692));
#44432=CARTESIAN_POINT('Ctrl Pts',(108.389088315582,4.18689120226974,133.384888688108));
#44433=CARTESIAN_POINT('Ctrl Pts',(108.381597979819,4.25604936928113,133.272679980003));
#44434=CARTESIAN_POINT('Ctrl Pts',(108.374107644057,4.32060521663931,133.157832612914));
#44435=CARTESIAN_POINT('Ctrl Pts',(108.366617308295,4.38037362983542,133.040766199195));
#44436=CARTESIAN_POINT('Ctrl Pts',(108.358842974176,4.44240818058346,132.91926117682));
#44437=CARTESIAN_POINT('Ctrl Pts',(108.351068640057,4.49948160649857,132.794980624413));
#44438=CARTESIAN_POINT('Ctrl Pts',(108.343294305938,4.55133607226615,132.668367865349));
#44439=CARTESIAN_POINT('Ctrl Pts',(108.335529552991,4.60312663203904,132.541911145196));
#44440=CARTESIAN_POINT('Ctrl Pts',(108.327764800044,4.64971088247962,132.413128295585));
#44441=CARTESIAN_POINT('Ctrl Pts',(108.320000047097,4.69087670813955,132.282487395462));
#44442=CARTESIAN_POINT('Ctrl Pts',(108.312243006212,4.73200164732102,132.151976249724));
#44443=CARTESIAN_POINT('Ctrl Pts',(108.304485965327,4.76771875471989,132.019611096464));
#44444=CARTESIAN_POINT('Ctrl Pts',(108.296728924442,4.79786402957485,131.885879834322));
#44445=CARTESIAN_POINT('Ctrl Pts',(108.288977733202,4.82798657164354,131.752249419964));
#44446=CARTESIAN_POINT('Ctrl Pts',(108.281226541962,4.85254555889622,131.617255327113));
#44447=CARTESIAN_POINT('Ctrl Pts',(108.273475350722,4.8714269562047,131.481400108927));
#44448=CARTESIAN_POINT('Ctrl Pts',(108.265727453944,4.89030032841571,131.345602632832));
#44449=CARTESIAN_POINT('Ctrl Pts',(108.257979557167,4.90350085650142,131.208945145784));
#44450=CARTESIAN_POINT('Ctrl Pts',(108.25023166039,4.91096574195096,131.071939659877));
#44451=CARTESIAN_POINT('Ctrl Pts',(108.242485384306,4.9184290659074,130.934962832564));
#44452=CARTESIAN_POINT('Ctrl Pts',(108.234739108222,4.92015911238442,130.797638541323));
#44453=CARTESIAN_POINT('Ctrl Pts',(108.226992832138,4.91614505795859,130.660482781854));
#44454=CARTESIAN_POINT('Ctrl Pts',(108.219246498873,4.91213097390194,130.523326009932));
#44455=CARTESIAN_POINT('Ctrl Pts',(108.211500165607,4.90237271577029,130.386338163064));
#44456=CARTESIAN_POINT('Ctrl Pts',(108.203753832342,4.88691157358095,130.250033697328));
#44457=CARTESIAN_POINT('Ctrl Pts',(108.196005764339,4.87144696897595,130.113698707152));
#44458=CARTESIAN_POINT('Ctrl Pts',(108.188257696336,4.85027698304612,129.978047791037));
#44459=CARTESIAN_POINT('Ctrl Pts',(108.180509628333,4.82349455594055,129.84358835979));
#44460=CARTESIAN_POINT('Ctrl Pts',(108.172753325591,4.7966836641528,129.70898602346));
#44461=CARTESIAN_POINT('Ctrl Pts',(108.164997022849,4.76424849201689,129.57557808566));
#44462=CARTESIAN_POINT('Ctrl Pts',(108.157240720108,4.72633285387229,129.443860409221));
#44463=CARTESIAN_POINT('Ctrl Pts',(108.149480277593,4.68839697901004,129.312072431092));
#44464=CARTESIAN_POINT('Ctrl Pts',(108.141719835079,4.64497493336955,129.181976882592));
#44465=CARTESIAN_POINT('Ctrl Pts',(108.133959392565,4.5962595257029,129.054051663442));
#44466=CARTESIAN_POINT('Ctrl Pts',(108.1261864923,4.54746591573906,128.925921087374));
#44467=CARTESIAN_POINT('Ctrl Pts',(108.118413592034,4.49336211768305,128.79996816224));
#44468=CARTESIAN_POINT('Ctrl Pts',(108.110640691769,4.43418831542878,128.676648925204));
#44469=CARTESIAN_POINT('Ctrl Pts',(108.103150356007,4.3771656299363,128.557812653056));
#44470=CARTESIAN_POINT('Ctrl Pts',(108.095660020245,4.31543529971967,128.441422183144));
#44471=CARTESIAN_POINT('Ctrl Pts',(108.088169684483,4.24925029762302,128.327860068273));
#44472=CARTESIAN_POINT('Ctrl Pts',(108.080395350364,4.18055587105537,128.2099922113));
#44473=CARTESIAN_POINT('Ctrl Pts',(108.072621016245,4.10684470330988,128.094798047376));
#44474=CARTESIAN_POINT('Ctrl Pts',(108.064846682126,4.02835040861327,127.982734127769));
#44475=CARTESIAN_POINT('Ctrl Pts',(108.057081929179,3.94995285111975,127.870808316927));
#44476=CARTESIAN_POINT('Ctrl Pts',(108.049317176231,3.86678411766896,127.762005391786));
#44477=CARTESIAN_POINT('Ctrl Pts',(108.041552423284,3.77912336275388,127.656756819184));
#44478=CARTESIAN_POINT('Ctrl Pts',(108.033795382399,3.69154967373626,127.551612780948));
#44479=CARTESIAN_POINT('Ctrl Pts',(108.026038341514,3.59949309051094,127.450016368397));
#44480=CARTESIAN_POINT('Ctrl Pts',(108.018281300629,3.50327544960236,127.352369281147));
#44481=CARTESIAN_POINT('Ctrl Pts',(108.010530109389,3.40713036716506,127.254795830325));
#44482=CARTESIAN_POINT('Ctrl Pts',(108.002778918149,3.30683074611415,127.161166054202));
#44483=CARTESIAN_POINT('Ctrl Pts',(107.995027726909,3.20273775988312,127.071847536019));
#44484=CARTESIAN_POINT('Ctrl Pts',(107.987279830132,3.09868901594844,126.98256698059));
#44485=CARTESIAN_POINT('Ctrl Pts',(107.979531933355,2.99085040962496,126.897594292659));
#44486=CARTESIAN_POINT('Ctrl Pts',(107.971784036578,2.87961876706026,126.817259061436));
#44487=CARTESIAN_POINT('Ctrl Pts',(107.964037760494,2.76841039175723,126.736940634612));
#44488=CARTESIAN_POINT('Ctrl Pts',(107.95629148441,2.65381070868957,126.661257963765));
#44489=CARTESIAN_POINT('Ctrl Pts',(107.948545208326,2.53624798932969,126.590499063229));
#44490=CARTESIAN_POINT('Ctrl Pts',(107.94079887506,2.41868440214852,126.519739640366));
#44491=CARTESIAN_POINT('Ctrl Pts',(107.933052541795,2.29815807000165,126.453904261954));
#44492=CARTESIAN_POINT('Ctrl Pts',(107.92530620853,2.1751241376225,126.393236265609));
#44493=CARTESIAN_POINT('Ctrl Pts',(107.917558140527,2.05206265264758,126.332554683086));
#44494=CARTESIAN_POINT('Ctrl Pts',(107.909810072524,1.9264928005869,126.277042958196));
#44495=CARTESIAN_POINT('Ctrl Pts',(107.902062004521,1.79889171694289,126.226897165695));
#44496=CARTESIAN_POINT('Ctrl Pts',(107.894305701779,1.67115501734827,126.176698077649));
#44497=CARTESIAN_POINT('Ctrl Pts',(107.886549399037,1.54138313815597,126.131876457527));
#44498=CARTESIAN_POINT('Ctrl Pts',(107.878793096295,1.41007099797125,126.092579336227));
#44499=CARTESIAN_POINT('Ctrl Pts',(107.871032653781,1.27868877254367,126.053261240869));
#44500=CARTESIAN_POINT('Ctrl Pts',(107.863272211267,1.14576502678259,126.019473615918));
#44501=CARTESIAN_POINT('Ctrl Pts',(107.855511768753,1.01180604909759,125.991312562382));
#44502=CARTESIAN_POINT('Ctrl Pts',(107.847738868487,0.877632028569192,125.963106302223));
#44503=CARTESIAN_POINT('Ctrl Pts',(107.839965968222,0.742419841074156,125.940544727221));
#44504=CARTESIAN_POINT('Ctrl Pts',(107.832193067956,0.606682988854484,125.923672263088));
#44505=CARTESIAN_POINT('Ctrl Pts',(107.824702732194,0.475880513111934,125.907413155526));
#44506=CARTESIAN_POINT('Ctrl Pts',(107.817212396432,0.344591163094445,125.896436738648));
#44507=CARTESIAN_POINT('Ctrl Pts',(107.80972206067,0.213273529313823,125.890736958372));
#44508=CARTESIAN_POINT('Ctrl Pts',(107.801947726551,0.0769769475366263,
125.884821069194));
#44509=CARTESIAN_POINT('Ctrl Pts',(107.794173392432,-0.0597818517023291,
125.884571102853));
#44510=CARTESIAN_POINT('Ctrl Pts',(107.786399058313,-0.19649248469664,125.890037290193));
#44511=CARTESIAN_POINT('Ctrl Pts',(107.778634305366,-0.333034634054338,
125.895496740947));
#44512=CARTESIAN_POINT('Ctrl Pts',(107.770869552419,-0.469528348374439,
125.906658313162));
#44513=CARTESIAN_POINT('Ctrl Pts',(107.763104799471,-0.605459732564249,
125.923520364624));
#44514=CARTESIAN_POINT('Ctrl Pts',(107.755347758586,-0.741256107786986,
125.940365668457));
#44515=CARTESIAN_POINT('Ctrl Pts',(107.747590717701,-0.876490878867187,
125.962900136489));
#44516=CARTESIAN_POINT('Ctrl Pts',(107.739833676816,-1.01065212403799,125.991070126989));
#44517=CARTESIAN_POINT('Ctrl Pts',(107.732082485576,-1.14471219716983,126.019218874281));
#44518=CARTESIAN_POINT('Ctrl Pts',(107.724331294336,-1.27769997468739,126.052994605075));
#44519=CARTESIAN_POINT('Ctrl Pts',(107.716580103096,-1.40911097533662,126.092292141654));
#44520=CARTESIAN_POINT('Ctrl Pts',(107.708832206319,-1.5404661228048,126.131572975731));
#44521=CARTESIAN_POINT('Ctrl Pts',(107.701084309542,-1.67024545253506,126.176370835979));
#44522=CARTESIAN_POINT('Ctrl Pts',(107.693336412765,-1.79795717756498,126.22653001234));
#44523=CARTESIAN_POINT('Ctrl Pts',(107.685590136681,-1.92564218805543,126.276678696483));
#44524=CARTESIAN_POINT('Ctrl Pts',(107.677843860597,-2.05126009043464,126.332186323235));
#44525=CARTESIAN_POINT('Ctrl Pts',(107.670097584512,-2.17433707889527,126.39284825446));
#44526=CARTESIAN_POINT('Ctrl Pts',(107.662351251247,-2.29741497588203,126.453510633477));
#44527=CARTESIAN_POINT('Ctrl Pts',(107.654604917982,-2.41795157083984,126.519327220045));
#44528=CARTESIAN_POINT('Ctrl Pts',(107.646858584716,-2.53549612009413,126.590046617935));
#44529=CARTESIAN_POINT('Ctrl Pts',(107.639110516713,-2.65306699263562,126.660781852944));
#44530=CARTESIAN_POINT('Ctrl Pts',(107.63136244871,-2.76764415121255,126.736421882554));
#44531=CARTESIAN_POINT('Ctrl Pts',(107.623614380707,-2.87880472918655,126.816671262349));
#44532=CARTESIAN_POINT('Ctrl Pts',(107.615858077966,-2.99008344994534,126.897005932139));
#44533=CARTESIAN_POINT('Ctrl Pts',(107.608101775224,-3.09793801892514,126.98195950893));
#44534=CARTESIAN_POINT('Ctrl Pts',(107.600345472482,-3.20197721927498,127.071195077472));
#44535=CARTESIAN_POINT('Ctrl Pts',(107.592585029968,-3.30607194847888,127.160478273724));
#44536=CARTESIAN_POINT('Ctrl Pts',(107.584824587453,-3.40634696569246,127.254047749035));
#44537=CARTESIAN_POINT('Ctrl Pts',(107.577064144939,-3.50244775716352,127.351529493569));
#44538=CARTESIAN_POINT('Ctrl Pts',(107.569291244674,-3.59870281815634,127.449167724454));
#44539=CARTESIAN_POINT('Ctrl Pts',(107.561518344408,-3.69077000026521,127.550730484816));
#44540=CARTESIAN_POINT('Ctrl Pts',(107.553745444143,-3.77833436637443,127.65580976386));
#44541=CARTESIAN_POINT('Ctrl Pts',(107.546255108381,-3.86271554721265,127.75706914643));
#44542=CARTESIAN_POINT('Ctrl Pts',(107.538764772619,-3.94291541820318,127.861593573468));
#44543=CARTESIAN_POINT('Ctrl Pts',(107.531274436857,-4.01869119344353,127.968993947409));
#44544=CARTESIAN_POINT('Ctrl Pts',(107.523412939756,-4.09822181214448,128.081716227862));
#44545=CARTESIAN_POINT('Ctrl Pts',(107.515551442654,-4.17312843613846,128.197960419511));
#44546=CARTESIAN_POINT('Ctrl Pts',(107.507689945552,-4.24308727707193,128.317315499027));
#44547=CARTESIAN_POINT('Ctrl Pts',(107.499842002833,-4.31292549863128,128.436464792758));
#44548=CARTESIAN_POINT('Ctrl Pts',(107.491994060113,-4.37783274116075,128.558713964327));
#44549=CARTESIAN_POINT('Ctrl Pts',(107.484146117394,-4.43752731946132,128.683621512552));
#44550=CARTESIAN_POINT('Ctrl Pts',(107.476306037269,-4.49716209173173,128.808403920022));
#44551=CARTESIAN_POINT('Ctrl Pts',(107.468465957145,-4.55159442764522,128.935839064882));
#44552=CARTESIAN_POINT('Ctrl Pts',(107.460625877021,-4.60058728572763,129.065458754636));
#44553=CARTESIAN_POINT('Ctrl Pts',(107.452793638437,-4.64953114182543,129.194948800554));
#44554=CARTESIAN_POINT('Ctrl Pts',(107.444961399853,-4.69304622271882,129.326618685661));
#44555=CARTESIAN_POINT('Ctrl Pts',(107.437129161269,-4.73094281329889,129.459978543974));
#44556=CARTESIAN_POINT('Ctrl Pts',(107.434739738607,-4.74250412765164,129.500663344913));
#44557=CARTESIAN_POINT('Ctrl Pts',(107.432350315945,-4.75354286155822,129.541505290476));
#44558=CARTESIAN_POINT('Ctrl Pts',(107.429960893282,-4.76405452823407,129.582490119308));
#44559=CARTESIAN_POINT('Origin',(213.235140564004,0.,130.804360617566));
#44560=CARTESIAN_POINT('',(105.334849955158,-4.76405452823402,129.582490119308));
#44561=CARTESIAN_POINT('',(105.680281509498,-4.76405452823405,129.582490119308));
#44562=CARTESIAN_POINT('',(213.235140564004,-4.76405452823405,129.582490119308));
#44563=CARTESIAN_POINT('',(107.014859436026,-4.91824951115124,130.806553460605));
#44564=CARTESIAN_POINT('Ctrl Pts',(107.014859435991,-4.91824951115096,130.806553461225));
#44565=CARTESIAN_POINT('Ctrl Pts',(107.007895685791,-4.91819497880655,130.928862078681));
#44566=CARTESIAN_POINT('Ctrl Pts',(107.000931935591,-4.91357844965842,131.051064671271));
#44567=CARTESIAN_POINT('Ctrl Pts',(106.99396818539,-4.90442104082865,131.172921761445));
#44568=CARTESIAN_POINT('Ctrl Pts',(106.986193851271,-4.89419770514593,131.308963076332));
#44569=CARTESIAN_POINT('Ctrl Pts',(106.978419517152,-4.87829351238314,131.444794178459));
#44570=CARTESIAN_POINT('Ctrl Pts',(106.970645183033,-4.85671886405327,131.579902323762));
#44571=CARTESIAN_POINT('Ctrl Pts',(106.962880430086,-4.83517080454929,131.71484396035));
#44572=CARTESIAN_POINT('Ctrl Pts',(106.955115677139,-4.80796625522953,131.849064030531));
#44573=CARTESIAN_POINT('Ctrl Pts',(106.947350924192,-4.77516754231759,131.982052430094));
#44574=CARTESIAN_POINT('Ctrl Pts',(106.939593883307,-4.74240140554971,132.114908743704));
#44575=CARTESIAN_POINT('Ctrl Pts',(106.931836842422,-4.70405225529482,132.246535444009));
#44576=CARTESIAN_POINT('Ctrl Pts',(106.924079801537,-4.66023382025977,132.376430527909));
#44577=CARTESIAN_POINT('Ctrl Pts',(106.916328610297,-4.61644842904743,132.506227656916));
#44578=CARTESIAN_POINT('Ctrl Pts',(106.908577419057,-4.56720208694562,132.63429539973));
#44579=CARTESIAN_POINT('Ctrl Pts',(106.900826227816,-4.51265881914401,132.760145228535));
#44580=CARTESIAN_POINT('Ctrl Pts',(106.893078331039,-4.45813873368621,132.885941567805));
#44581=CARTESIAN_POINT('Ctrl Pts',(106.885330434262,-4.39832635540693,133.009521509999));
#44582=CARTESIAN_POINT('Ctrl Pts',(106.877582537485,-4.33343438883644,133.130415101053));
#44583=CARTESIAN_POINT('Ctrl Pts',(106.869836261401,-4.2685559962664,133.251283403774));
#44584=CARTESIAN_POINT('Ctrl Pts',(106.862089985317,-4.1986003136435,133.3694661288));
#44585=CARTESIAN_POINT('Ctrl Pts',(106.854343709233,-4.12382650738129,133.4845169562));
#44586=CARTESIAN_POINT('Ctrl Pts',(106.846597375968,-4.04905214915587,133.599568632879));
#44587=CARTESIAN_POINT('Ctrl Pts',(106.838851042702,-3.96945980937418,133.711488037986));
#44588=CARTESIAN_POINT('Ctrl Pts',(106.831104709437,-3.88535236142688,133.819857274844));
#44589=CARTESIAN_POINT('Ctrl Pts',(106.823356641434,-3.80122607819977,133.928250780241));
#44590=CARTESIAN_POINT('Ctrl Pts',(106.815608573431,-3.7125829144453,134.033092226561));
#44591=CARTESIAN_POINT('Ctrl Pts',(106.807860505428,-3.61976619091251,134.133996601518));
#44592=CARTESIAN_POINT('Ctrl Pts',(106.800104202686,-3.52685082066141,134.235008218845));
#44593=CARTESIAN_POINT('Ctrl Pts',(106.792347899944,-3.42975329492943,134.332074117884));
#44594=CARTESIAN_POINT('Ctrl Pts',(106.784591597202,-3.32885437691362,134.424845612674));
#44595=CARTESIAN_POINT('Ctrl Pts',(106.776831154688,-3.22790160610719,134.517666622405));
#44596=CARTESIAN_POINT('Ctrl Pts',(106.769070712174,-3.12314369870628,134.606188408559));
#44597=CARTESIAN_POINT('Ctrl Pts',(106.76131026966,-3.01499391789975,134.690103112576));
#44598=CARTESIAN_POINT('Ctrl Pts',(106.753537369395,-2.90667052546398,134.774152523925));
#44599=CARTESIAN_POINT('Ctrl Pts',(106.745764469129,-2.79494469773725,134.853579847515));
#44600=CARTESIAN_POINT('Ctrl Pts',(106.737991568864,-2.68025878653837,134.92812054022));
#44601=CARTESIAN_POINT('Ctrl Pts',(106.730501233102,-2.56974199708748,134.999951490988));
#44602=CARTESIAN_POINT('Ctrl Pts',(106.72301089734,-2.45647686553973,135.067244767998));
#44603=CARTESIAN_POINT('Ctrl Pts',(106.715520561578,-2.3408784411738,135.129805240509));
#44604=CARTESIAN_POINT('Ctrl Pts',(106.707746227459,-2.22089706741315,135.19473771235));
#44605=CARTESIAN_POINT('Ctrl Pts',(106.699971893339,-2.09802190958741,135.254777093107));
#44606=CARTESIAN_POINT('Ctrl Pts',(106.69219755922,-1.97268997607033,135.309654983178));
#44607=CARTESIAN_POINT('Ctrl Pts',(106.684432806273,-1.84751250296006,135.364465241153));
#44608=CARTESIAN_POINT('Ctrl Pts',(106.676668053326,-1.71988463319152,135.414126509778));
#44609=CARTESIAN_POINT('Ctrl Pts',(106.668903300379,-1.59026922072971,135.458415502083));
#44610=CARTESIAN_POINT('Ctrl Pts',(106.661146259494,-1.46078254412282,135.502660505937));
#44611=CARTESIAN_POINT('Ctrl Pts',(106.653389218609,-1.32931262085163,135.541543726399));
#44612=CARTESIAN_POINT('Ctrl Pts',(106.645632177724,-1.19634327348498,135.574889501714));
#44613=CARTESIAN_POINT('Ctrl Pts',(106.637880986484,-1.06347419933763,135.60821013072));
#44614=CARTESIAN_POINT('Ctrl Pts',(106.630129795244,-0.929108329427115,
135.636001531599));
#44615=CARTESIAN_POINT('Ctrl Pts',(106.622378604004,-0.793745335660902,
135.658137642174));
#44616=CARTESIAN_POINT('Ctrl Pts',(106.614630707227,-0.658439874777875,
135.680264344312));
#44617=CARTESIAN_POINT('Ctrl Pts',(106.606882810449,-0.522138517985745,
135.696740473855));
#44618=CARTESIAN_POINT('Ctrl Pts',(106.599134913672,-0.385351622941781,
135.707490963498));
#44619=CARTESIAN_POINT('Ctrl Pts',(106.591388637588,-0.248593340767475,
135.71823920437));
#44620=CARTESIAN_POINT('Ctrl Pts',(106.583642361504,-0.111350111874335,
135.723264156981));
#44621=CARTESIAN_POINT('Ctrl Pts',(106.57589608542,0.0258624763627931,135.722542618551));
#44622=CARTESIAN_POINT('Ctrl Pts',(106.568149752155,0.163076077471984,135.721821074795));
#44623=CARTESIAN_POINT('Ctrl Pts',(106.560403418889,0.30025864651403,135.715352957408));
#44624=CARTESIAN_POINT('Ctrl Pts',(106.552657085624,0.436894884712721,135.703167198991));
#44625=CARTESIAN_POINT('Ctrl Pts',(106.544909017621,0.573561721649587,135.690978711657));
#44626=CARTESIAN_POINT('Ctrl Pts',(106.537160949618,0.709681594941662,135.673070070116));
#44627=CARTESIAN_POINT('Ctrl Pts',(106.529412881615,0.844745009597477,135.649522011293));
#44628=CARTESIAN_POINT('Ctrl Pts',(106.521656578873,0.979951971257663,135.625948925312));
#44629=CARTESIAN_POINT('Ctrl Pts',(106.513900276131,1.11409984556473,135.596724516365));
#44630=CARTESIAN_POINT('Ctrl Pts',(106.506143973389,1.24668946133791,135.561980658037));
#44631=CARTESIAN_POINT('Ctrl Pts',(106.498383530875,1.37934984418123,135.527218255865));
#44632=CARTESIAN_POINT('Ctrl Pts',(106.490623088361,1.51044993774469,135.486930649152));
#44633=CARTESIAN_POINT('Ctrl Pts',(106.482862645847,1.63950735305299,135.44129912285));
#44634=CARTESIAN_POINT('Ctrl Pts',(106.475089745581,1.7687719427816,135.395594344771));
#44635=CARTESIAN_POINT('Ctrl Pts',(106.467316845316,1.89598693855749,135.344528650185));
#44636=CARTESIAN_POINT('Ctrl Pts',(106.45954394505,2.0206906707943,135.288331210184));
#44637=CARTESIAN_POINT('Ctrl Pts',(106.452053609288,2.14086110825507,135.23417668868));
#44638=CARTESIAN_POINT('Ctrl Pts',(106.444563273526,2.25869941830432,135.175257185627));
#44639=CARTESIAN_POINT('Ctrl Pts',(106.437072937764,2.37381708765086,135.111816420807));
#44640=CARTESIAN_POINT('Ctrl Pts',(106.429298603645,2.49329947841942,135.045970280107));
#44641=CARTESIAN_POINT('Ctrl Pts',(106.421524269526,2.61022933405147,134.975044681666));
#44642=CARTESIAN_POINT('Ctrl Pts',(106.413749935407,2.72414462865895,134.899262216463));
#44643=CARTESIAN_POINT('Ctrl Pts',(106.40598518246,2.83791953284665,134.823573146376));
#44644=CARTESIAN_POINT('Ctrl Pts',(106.398220429513,2.9486869457147,134.743039333666));
#44645=CARTESIAN_POINT('Ctrl Pts',(106.390455676566,3.05600882573884,134.657929498423));
#44646=CARTESIAN_POINT('Ctrl Pts',(106.382698635681,3.16322411215877,134.572904195467));
#44647=CARTESIAN_POINT('Ctrl Pts',(106.374941594796,3.26700037162276,134.483312156033));
#44648=CARTESIAN_POINT('Ctrl Pts',(106.367184553911,3.36692829700471,134.389465484279));
#44649=CARTESIAN_POINT('Ctrl Pts',(106.359433362671,3.4667808659608,134.29568958303));
#44650=CARTESIAN_POINT('Ctrl Pts',(106.351682171431,3.56279059336993,134.197665702254));
#44651=CARTESIAN_POINT('Ctrl Pts',(106.34393098019,3.65458133467947,134.095746090389));
#44652=CARTESIAN_POINT('Ctrl Pts',(106.336183083413,3.74633306247542,133.993869797079));
#44653=CARTESIAN_POINT('Ctrl Pts',(106.328435186636,3.83386910957983,133.888101355824));
#44654=CARTESIAN_POINT('Ctrl Pts',(106.320687289859,3.91685045896313,133.778829569265));
#44655=CARTESIAN_POINT('Ctrl Pts',(106.312941013775,3.999814450437,133.669580640008));
#44656=CARTESIAN_POINT('Ctrl Pts',(106.305194737691,4.07822540295203,133.556830134237));
#44657=CARTESIAN_POINT('Ctrl Pts',(106.297448461607,4.15178510778171,133.440999288545));
#44658=CARTESIAN_POINT('Ctrl Pts',(106.289702128342,4.22534535561237,133.325167587816));
#44659=CARTESIAN_POINT('Ctrl Pts',(106.281955795076,4.29405407470617,133.206255831828));
#44660=CARTESIAN_POINT('Ctrl Pts',(106.274209461811,4.35765707530295,133.084713194814));
#44661=CARTESIAN_POINT('Ctrl Pts',(106.266461393808,4.42127431935072,132.963143339169));
#44662=CARTESIAN_POINT('Ctrl Pts',(106.258713325805,4.47978338845044,132.838941776458));
#44663=CARTESIAN_POINT('Ctrl Pts',(106.250965257802,4.53297681437517,132.712580799525));
#44664=CARTESIAN_POINT('Ctrl Pts',(106.24320895506,4.58622677490601,132.586085524643));
#44665=CARTESIAN_POINT('Ctrl Pts',(106.235452652319,4.63414965478795,132.457426611842));
#44666=CARTESIAN_POINT('Ctrl Pts',(106.227696349577,4.67658658878576,132.327095308866));
#44667=CARTESIAN_POINT('Ctrl Pts',(106.219935907063,4.719046172653,132.19669444415));
#44668=CARTESIAN_POINT('Ctrl Pts',(106.212175464548,4.75601387098987,132.064619786979));
#44669=CARTESIAN_POINT('Ctrl Pts',(106.204415022034,4.78738146093688,131.931375173806));
#44670=CARTESIAN_POINT('Ctrl Pts',(106.196642121769,4.81879940492397,131.797916664551));
#44671=CARTESIAN_POINT('Ctrl Pts',(106.188869221503,4.84459920242897,131.663284830417));
#44672=CARTESIAN_POINT('Ctrl Pts',(106.181096321238,4.86472411789404,131.527991959673));
#44673=CARTESIAN_POINT('Ctrl Pts',(106.173605985476,4.88411744199042,131.397617325563));
#44674=CARTESIAN_POINT('Ctrl Pts',(106.166115649714,4.89824128032734,131.266629187376));
#44675=CARTESIAN_POINT('Ctrl Pts',(106.158625313952,4.90709068033576,131.135486148841));
#44676=CARTESIAN_POINT('Ctrl Pts',(106.150850979833,4.91627560803518,130.99937078214));
#44677=CARTESIAN_POINT('Ctrl Pts',(106.143076645714,4.91980733648867,130.86265736456));
#44678=CARTESIAN_POINT('Ctrl Pts',(106.135302311595,4.91762340151374,130.725854927426));
#44679=CARTESIAN_POINT('Ctrl Pts',(106.127537558648,4.91544215804349,130.589221087069));
#44680=CARTESIAN_POINT('Ctrl Pts',(106.1197728057,4.9075592728743,130.45249883261));
#44681=CARTESIAN_POINT('Ctrl Pts',(106.112008052753,4.89396405568395,130.31620195056));
#44682=CARTESIAN_POINT('Ctrl Pts',(106.104251011868,4.88038234145496,130.180040440494));
#44683=CARTESIAN_POINT('Ctrl Pts',(106.096493970983,4.86109962441651,130.044303848589));
#44684=CARTESIAN_POINT('Ctrl Pts',(106.088736930098,4.83615724613833,129.909505236444));
#44685=CARTESIAN_POINT('Ctrl Pts',(106.080985738858,4.81123367710164,129.77480827698));
#44686=CARTESIAN_POINT('Ctrl Pts',(106.073234547618,4.78065901285627,129.641048272248));
#44687=CARTESIAN_POINT('Ctrl Pts',(106.065483356378,4.74452629467262,129.508732082198));
#44688=CARTESIAN_POINT('Ctrl Pts',(106.057735459601,4.70840893385807,129.376472130058));
#44689=CARTESIAN_POINT('Ctrl Pts',(106.049987562824,4.66673832035942,129.245655148444));
#44690=CARTESIAN_POINT('Ctrl Pts',(106.042239666047,4.61965831786306,129.116776519306));
#44691=CARTESIAN_POINT('Ctrl Pts',(106.034493389963,4.57258816348829,128.9879248488));
#44692=CARTESIAN_POINT('Ctrl Pts',(106.026747113879,4.52011100485186,128.861011091283));
#44693=CARTESIAN_POINT('Ctrl Pts',(106.019000837794,4.46242005112696,128.736513826868));
#44694=CARTESIAN_POINT('Ctrl Pts',(106.011254504529,4.40472867154055,128.612015643443));
#44695=CARTESIAN_POINT('Ctrl Pts',(106.003508171264,4.34182358444637,128.489934343445));
#44696=CARTESIAN_POINT('Ctrl Pts',(105.995761837998,4.27394529707205,128.370726573562));
#44697=CARTESIAN_POINT('Ctrl Pts',(105.988013769995,4.20605180882591,128.251492107925));
#44698=CARTESIAN_POINT('Ctrl Pts',(105.980265701992,4.1331830975575,128.135132792592));
#44699=CARTESIAN_POINT('Ctrl Pts',(105.972517633989,4.05562437496958,128.022078462275));
#44700=CARTESIAN_POINT('Ctrl Pts',(105.964761331248,3.97798322204833,127.90890397647));
#44701=CARTESIAN_POINT('Ctrl Pts',(105.957005028506,3.89564232205637,127.799041815341));
#44702=CARTESIAN_POINT('Ctrl Pts',(105.949248725764,3.80892910509421,127.692891168115));
#44703=CARTESIAN_POINT('Ctrl Pts',(105.94148828325,3.72216960667721,127.586683865092));
#44704=CARTESIAN_POINT('Ctrl Pts',(105.933727840736,3.6310334009882,127.484192315198));
#44705=CARTESIAN_POINT('Ctrl Pts',(105.925967398221,3.53588588280445,127.385779905299));
#44706=CARTESIAN_POINT('Ctrl Pts',(105.918194497956,3.44058562537771,127.287209515063));
#44707=CARTESIAN_POINT('Ctrl Pts',(105.910421597691,3.34126147109483,127.192731619818));
#44708=CARTESIAN_POINT('Ctrl Pts',(105.902648697425,3.23831375563247,127.102670857121));
#44709=CARTESIAN_POINT('Ctrl Pts',(105.895158361663,3.13910844893701,127.015884029998));
#44710=CARTESIAN_POINT('Ctrl Pts',(105.887668025901,3.03653869811844,126.933198956544));
#44711=CARTESIAN_POINT('Ctrl Pts',(105.880177690139,2.93098766249886,126.854867690014));
#44712=CARTESIAN_POINT('Ctrl Pts',(105.87240335602,2.82143462728206,126.773566469706));
#44713=CARTESIAN_POINT('Ctrl Pts',(105.864629021901,2.70832274264279,126.696698184921));
#44714=CARTESIAN_POINT('Ctrl Pts',(105.856854687782,2.59204650763631,126.624590532412));
#44715=CARTESIAN_POINT('Ctrl Pts',(105.849089934835,2.47591357269765,126.55257174614));
#44716=CARTESIAN_POINT('Ctrl Pts',(105.841325181888,2.35662437586141,126.485302122525));
#44717=CARTESIAN_POINT('Ctrl Pts',(105.83356042894,2.23460540189126,126.4230683698));
#44718=CARTESIAN_POINT('Ctrl Pts',(105.825803388055,2.11270761888615,126.360896428514));
#44719=CARTESIAN_POINT('Ctrl Pts',(105.81804634717,1.98808580029047,126.303750580998));
#44720=CARTESIAN_POINT('Ctrl Pts',(105.810289306285,1.86119394548687,126.251873367745));
#44721=CARTESIAN_POINT('Ctrl Pts',(105.802538115045,1.73439778081807,126.200035275502));
#44722=CARTESIAN_POINT('Ctrl Pts',(105.794786923805,1.60533534770429,126.153458056623));
#44723=CARTESIAN_POINT('Ctrl Pts',(105.787035732565,1.4744833728568,126.112337403038));
#44724=CARTESIAN_POINT('Ctrl Pts',(105.779287835788,1.3436870135893,126.071234226828));
#44725=CARTESIAN_POINT('Ctrl Pts',(105.771539939011,1.21110299757035,126.035583120192));
#44726=CARTESIAN_POINT('Ctrl Pts',(105.763792042234,1.07722586550265,126.005530812583));
#44727=CARTESIAN_POINT('Ctrl Pts',(105.75604576615,0.943376737644913,125.975484791269));
#44728=CARTESIAN_POINT('Ctrl Pts',(105.748299490066,0.808235412992326,125.951035325081));
#44729=CARTESIAN_POINT('Ctrl Pts',(105.740553213982,0.672308968826403,125.932278545912));
#44730=CARTESIAN_POINT('Ctrl Pts',(105.732806880716,0.536381521282347,125.913521628284));
#44731=CARTESIAN_POINT('Ctrl Pts',(105.725060547451,0.399669329955497,125.90045753497));
#44732=CARTESIAN_POINT('Ctrl Pts',(105.717314214185,0.2626865846685,125.893130749118));
#44733=CARTESIAN_POINT('Ctrl Pts',(105.709566146183,0.125673163045561,125.885802322483));
#44734=CARTESIAN_POINT('Ctrl Pts',(105.70181807818,-0.011610542769554,125.88421378085));
#44735=CARTESIAN_POINT('Ctrl Pts',(105.694070010177,-0.148648736765858,
125.888357503698));
#44736=CARTESIAN_POINT('Ctrl Pts',(105.686313707435,-0.285832576585611,
125.892505630545));
#44737=CARTESIAN_POINT('Ctrl Pts',(105.678557404693,-0.422769991935293,
125.902398180101));
#44738=CARTESIAN_POINT('Ctrl Pts',(105.670801101951,-0.558948149645208,
125.917975447677));
#44739=CARTESIAN_POINT('Ctrl Pts',(105.663040659437,-0.695198989738231,
125.933561029311));
#44740=CARTESIAN_POINT('Ctrl Pts',(105.655280216923,-0.830689378675953,
125.954837314055));
#44741=CARTESIAN_POINT('Ctrl Pts',(105.647519774409,-0.964916083994161,
125.981693304414));
#44742=CARTESIAN_POINT('Ctrl Pts',(105.639746874143,-1.09935826193583,126.008592406392));
#44743=CARTESIAN_POINT('Ctrl Pts',(105.631973973878,-1.23253232247518,126.041089020265));
#44744=CARTESIAN_POINT('Ctrl Pts',(105.624201073612,-1.36394874763043,126.079021806821));
#44745=CARTESIAN_POINT('Ctrl Pts',(105.61671073785,-1.49058785471391,126.115575641038));
#44746=CARTESIAN_POINT('Ctrl Pts',(105.609220402088,-1.6155946044973,126.157177175431));
#44747=CARTESIAN_POINT('Ctrl Pts',(105.601730066326,-1.73854983046595,126.203640288152));
#44748=CARTESIAN_POINT('Ctrl Pts',(105.593955512711,-1.86617054426714,126.251866425464));
#44749=CARTESIAN_POINT('Ctrl Pts',(105.586180959096,-1.9919852468701,126.305483138132));
#44750=CARTESIAN_POINT('Ctrl Pts',(105.57840640548,-2.11550496011297,126.364335637204));
#44751=CARTESIAN_POINT('Ctrl Pts',(105.570641483894,-2.2388716426454,126.423115222897));
#44752=CARTESIAN_POINT('Ctrl Pts',(105.562876562308,-2.35994864367044,126.487117521491));
#44753=CARTESIAN_POINT('Ctrl Pts',(105.555111640722,-2.47826419198246,126.55613867689));
#44754=CARTESIAN_POINT('Ctrl Pts',(105.54735448184,-2.59646145853393,126.625090830845));
#44755=CARTESIAN_POINT('Ctrl Pts',(105.539597322958,-2.71190243083685,126.699051660647));
#44756=CARTESIAN_POINT('Ctrl Pts',(105.531840164076,-2.82413763580126,126.777770288696));
#44757=CARTESIAN_POINT('Ctrl Pts',(105.524088905317,-2.93628747425554,126.856429043066));
#44758=CARTESIAN_POINT('Ctrl Pts',(105.516337646559,-3.04523608008542,126.939838168783));
#44759=CARTESIAN_POINT('Ctrl Pts',(105.5085863878,-3.15056112065854,127.02770234768));
#44760=CARTESIAN_POINT('Ctrl Pts',(105.500838678779,-3.25583792697191,127.115526288629));
#44761=CARTESIAN_POINT('Ctrl Pts',(105.493090969758,-3.35749417033841,127.207800973286));
#44762=CARTESIAN_POINT('Ctrl Pts',(105.485343260737,-3.45513912225318,127.304189663402));
#44763=CARTESIAN_POINT('Ctrl Pts',(105.477597244306,-3.5527627423227,127.400557296119));
#44764=CARTESIAN_POINT('Ctrl Pts',(105.469851227876,-3.6463765364184,127.501036871708));
#44765=CARTESIAN_POINT('Ctrl Pts',(105.462105211445,-3.73562557533219,127.6052537698));
#44766=CARTESIAN_POINT('Ctrl Pts',(105.454359209777,-3.82487444415469,127.709470469275));
#44767=CARTESIAN_POINT('Ctrl Pts',(105.446613208109,-3.90975832038601,127.817424179934));
#44768=CARTESIAN_POINT('Ctrl Pts',(105.438867206441,-3.9899618872133,127.928706396161));
#44769=CARTESIAN_POINT('Ctrl Pts',(105.431119542087,-4.07018266980003,128.040012499204));
#44770=CARTESIAN_POINT('Ctrl Pts',(105.423371877734,-4.14572091591109,128.154648212115));
#44771=CARTESIAN_POINT('Ctrl Pts',(105.41562421338,-4.21630427677361,128.272175531882));
#44772=CARTESIAN_POINT('Ctrl Pts',(105.407869290037,-4.28695376903883,128.389812966078));
#44773=CARTESIAN_POINT('Ctrl Pts',(105.400114366693,-4.35263890466126,128.51034708153));
#44774=CARTESIAN_POINT('Ctrl Pts',(105.39235944335,-4.41313282912109,128.633314396263));
#44775=CARTESIAN_POINT('Ctrl Pts',(105.384600409942,-4.47365881500711,128.756346882954));
#44776=CARTESIAN_POINT('Ctrl Pts',(105.376841376535,-4.52898795015834,128.881814781216));
#44777=CARTESIAN_POINT('Ctrl Pts',(105.369082343127,-4.57894169052388,129.009234979266));
#44778=CARTESIAN_POINT('Ctrl Pts',(105.361313107293,-4.62896111553639,129.136822723343));
#44779=CARTESIAN_POINT('Ctrl Pts',(105.353543871459,-4.67359090372758,129.266367524707));
#44780=CARTESIAN_POINT('Ctrl Pts',(105.345774635624,-4.71270234562357,129.397371042603));
#44781=CARTESIAN_POINT('Ctrl Pts',(105.342133075469,-4.7310344791148,129.458774403397));
#44782=CARTESIAN_POINT('Ctrl Pts',(105.338491515313,-4.74815499509428,129.520498080905));
#44783=CARTESIAN_POINT('Ctrl Pts',(105.334849955158,-4.76405452823403,129.582490119308));
#44784=CARTESIAN_POINT('Ctrl Pts',(107.085000608365,-4.76405452823403,129.582490119308));
#44785=CARTESIAN_POINT('Ctrl Pts',(107.077323484576,-4.79779703768306,129.714051651536));
#44786=CARTESIAN_POINT('Ctrl Pts',(107.069646360786,-4.82606097313593,129.846915698217));
#44787=CARTESIAN_POINT('Ctrl Pts',(107.061969236997,-4.84877003991418,129.980581422314));
#44788=CARTESIAN_POINT('Ctrl Pts',(107.054117603501,-4.87199530946124,130.117285519477));
#44789=CARTESIAN_POINT('Ctrl Pts',(107.046265970006,-4.88941008467352,130.254827733819));
#44790=CARTESIAN_POINT('Ctrl Pts',(107.038414336511,-4.90098899494674,130.39266906566));
#44791=CARTESIAN_POINT('Ctrl Pts',(107.030562703016,-4.91256790521996,130.530510397501));
#44792=CARTESIAN_POINT('Ctrl Pts',(107.022711069521,-4.91831099639246,130.668650404071));
#44793=CARTESIAN_POINT('Ctrl Pts',(107.014859436026,-4.91824951115124,130.806553460605));
#44794=CARTESIAN_POINT('',(107.360140563954,-4.91824914862615,130.807254496995));
#44795=CARTESIAN_POINT('Ctrl Pts',(107.429960893282,-4.76405452823407,129.582490119308));
#44796=CARTESIAN_POINT('Ctrl Pts',(107.422135445397,-4.79848062666256,129.716716954592));
#44797=CARTESIAN_POINT('Ctrl Pts',(107.414309997512,-4.82724967230215,129.852477377668));
#44798=CARTESIAN_POINT('Ctrl Pts',(107.406484549627,-4.85023658873154,129.989260564916));
#44799=CARTESIAN_POINT('Ctrl Pts',(107.398661175943,-4.87321741228365,130.12600749662));
#44800=CARTESIAN_POINT('Ctrl Pts',(107.39083780226,-4.89041908976492,130.263776279477));
#44801=CARTESIAN_POINT('Ctrl Pts',(107.383014428576,-4.90176762153945,130.40204575713));
#44802=CARTESIAN_POINT('Ctrl Pts',(107.375389807053,-4.91282784480339,130.536802510146));
#44803=CARTESIAN_POINT('Ctrl Pts',(107.367765185531,-4.91832871155599,130.67203447485));
#44804=CARTESIAN_POINT('Ctrl Pts',(107.360140564008,-4.91824914862671,130.807254496045));
#44805=CARTESIAN_POINT('Ctrl Pts',(107.360140563954,-4.91824914862615,130.807254496995));
#44806=CARTESIAN_POINT('Ctrl Pts',(107.351197751379,-4.91815583034193,130.965852179838));
#44807=CARTESIAN_POINT('Ctrl Pts',(107.342254938803,-4.91038646992283,131.124168952794));
#44808=CARTESIAN_POINT('Ctrl Pts',(107.333312126227,-4.89505025752853,131.281504242452));
#44809=CARTESIAN_POINT('Ctrl Pts',(107.324624727898,-4.88015206025675,131.434345903932));
#44810=CARTESIAN_POINT('Ctrl Pts',(107.31593732957,-4.85811346436008,131.586261223086));
#44811=CARTESIAN_POINT('Ctrl Pts',(107.307249931241,-4.82908541778232,131.736625113437));
#44812=CARTESIAN_POINT('Ctrl Pts',(107.298179411542,-4.79877721061071,131.893620174324));
#44813=CARTESIAN_POINT('Ctrl Pts',(107.289108891842,-4.76084924803436,132.048923574273));
#44814=CARTESIAN_POINT('Ctrl Pts',(107.280038372143,-4.71552915031273,132.201846894798));
#44815=CARTESIAN_POINT('Ctrl Pts',(107.270967852443,-4.67020905259109,132.354770215322));
#44816=CARTESIAN_POINT('Ctrl Pts',(107.261897332744,-4.61749699331532,132.505313243214));
#44817=CARTESIAN_POINT('Ctrl Pts',(107.252826813044,-4.55767503340629,132.652814390957));
#44818=CARTESIAN_POINT('Ctrl Pts',(107.245052478925,-4.50640168641018,132.779237489467));
#44819=CARTESIAN_POINT('Ctrl Pts',(107.237278144806,-4.44978295777727,132.903725847237));
#44820=CARTESIAN_POINT('Ctrl Pts',(107.229503810687,-4.38798531120369,133.025794382314));
#44821=CARTESIAN_POINT('Ctrl Pts',(107.22173905774,-4.32626382470649,133.14771247883));
#44822=CARTESIAN_POINT('Ctrl Pts',(107.213974304793,-4.25937629454039,133.267216340907));
#44823=CARTESIAN_POINT('Ctrl Pts',(107.206209551845,-4.18753782340043,133.383839254828));
#44824=CARTESIAN_POINT('Ctrl Pts',(107.19845251096,-4.1157707032428,133.500346337226));
#44825=CARTESIAN_POINT('Ctrl Pts',(107.190695470075,-4.03906263157148,133.613977835055));
#44826=CARTESIAN_POINT('Ctrl Pts',(107.18293842919,-3.95767518527689,133.724290443836));
#44827=CARTESIAN_POINT('Ctrl Pts',(107.17518723795,-3.87634911388864,133.834519865021));
#44828=CARTESIAN_POINT('Ctrl Pts',(107.16743604671,-3.79035092281963,133.941435065496));
#44829=CARTESIAN_POINT('Ctrl Pts',(107.15968485547,-3.69998596904676,134.044620929849));
#44830=CARTESIAN_POINT('Ctrl Pts',(107.151936958693,-3.60965942278974,134.147762937458));
#44831=CARTESIAN_POINT('Ctrl Pts',(107.144189061916,-3.51497006229068,134.247178468017));
#44832=CARTESIAN_POINT('Ctrl Pts',(107.136441165139,-3.41626392795545,134.3424849564));
#44833=CARTESIAN_POINT('Ctrl Pts',(107.128694889055,-3.31757844081566,134.437771508721));
#44834=CARTESIAN_POINT('Ctrl Pts',(107.120948612971,-3.21487813216536,134.528950457107));
#44835=CARTESIAN_POINT('Ctrl Pts',(107.113202336886,-3.10854606916345,134.615675928373));
#44836=CARTESIAN_POINT('Ctrl Pts',(107.105456003621,-3.00221322124248,134.702402039826));
#44837=CARTESIAN_POINT('Ctrl Pts',(107.097709670356,-2.89224886844685,134.784674361452));
#44838=CARTESIAN_POINT('Ctrl Pts',(107.08996333709,-2.77906901905547,134.862187431247));
#44839=CARTESIAN_POINT('Ctrl Pts',(107.082215269087,-2.66586382382171,134.939717859556));
#44840=CARTESIAN_POINT('Ctrl Pts',(107.074467201084,-2.54944202160618,135.01248669434));
#44841=CARTESIAN_POINT('Ctrl Pts',(107.066719133081,-2.43024809570893,135.080232137596));
#44842=CARTESIAN_POINT('Ctrl Pts',(107.05896283034,-2.31092748908857,135.148049581516));
#44843=CARTESIAN_POINT('Ctrl Pts',(107.051206527598,-2.18882921378542,135.210832775345));
#44844=CARTESIAN_POINT('Ctrl Pts',(107.043450224856,-2.0644223157652,135.268365945147));
#44845=CARTESIAN_POINT('Ctrl Pts',(107.035689782342,-1.93994901803767,135.325929822134));
#44846=CARTESIAN_POINT('Ctrl Pts',(107.027929339828,-1.81316500360393,135.378237942642));
#44847=CARTESIAN_POINT('Ctrl Pts',(107.020168897313,-1.68455780033125,135.425123333811));
#44848=CARTESIAN_POINT('Ctrl Pts',(107.012395997048,-1.55574414535866,135.472083989573));
#44849=CARTESIAN_POINT('Ctrl Pts',(107.004623096783,-1.42510182579334,135.513604402052));
#44850=CARTESIAN_POINT('Ctrl Pts',(106.996850196517,-1.29313284326542,135.549567727079));
#44851=CARTESIAN_POINT('Ctrl Pts',(106.989359860755,-1.16596126566158,135.584223694655));
#44852=CARTESIAN_POINT('Ctrl Pts',(106.981869524993,-1.03755810577401,135.613719519549));
#44853=CARTESIAN_POINT('Ctrl Pts',(106.974379189231,-0.908378172471304,
135.637996118747));
#44854=CARTESIAN_POINT('Ctrl Pts',(106.966604855112,-0.774300342734789,
135.663193172583));
#44855=CARTESIAN_POINT('Ctrl Pts',(106.958830520993,-0.638960955833597,
135.68284723083));
#44856=CARTESIAN_POINT('Ctrl Pts',(106.951056186874,-0.502858102648951,
135.696836145466));
#44857=CARTESIAN_POINT('Ctrl Pts',(106.943291433927,-0.366922984067087,
135.710807820015));
#44858=CARTESIAN_POINT('Ctrl Pts',(106.93552668098,-0.230226656502972,135.719128203029));
#44859=CARTESIAN_POINT('Ctrl Pts',(106.927761928032,-0.093278047685706,
135.721725996335));
#44860=CARTESIAN_POINT('Ctrl Pts',(106.920004887147,0.0435345418426454,
135.724321209476));
#44861=CARTESIAN_POINT('Ctrl Pts',(106.912247846263,0.180598525614519,135.721205136474));
#44862=CARTESIAN_POINT('Ctrl Pts',(106.904490805378,0.317399550318383,135.712358232476));
#44863=CARTESIAN_POINT('Ctrl Pts',(106.896739614137,0.454097412305267,135.703517999996));
#44864=CARTESIAN_POINT('Ctrl Pts',(106.888988422897,0.590532321355654,135.68895556366));
#44865=CARTESIAN_POINT('Ctrl Pts',(106.881237231657,0.72618997621252,135.66870344892));
#44866=CARTESIAN_POINT('Ctrl Pts',(106.87348933488,0.86178997294747,135.64845994187));
#44867=CARTESIAN_POINT('Ctrl Pts',(106.865741438103,0.996612986666924,135.622531623766));
#44868=CARTESIAN_POINT('Ctrl Pts',(106.857993541326,1.13015011120318,135.591002842409));
#44869=CARTESIAN_POINT('Ctrl Pts',(106.850247265242,1.26365930265171,135.559480656192));
#44870=CARTESIAN_POINT('Ctrl Pts',(106.842500989158,1.39588275967132,135.522360426674));
#44871=CARTESIAN_POINT('Ctrl Pts',(106.834754713074,1.52632243219733,135.479777486196));
#44872=CARTESIAN_POINT('Ctrl Pts',(106.827008379808,1.65676306759938,135.437194231381));
#44873=CARTESIAN_POINT('Ctrl Pts',(106.819262046543,1.78541952057131,135.389148306474));
#44874=CARTESIAN_POINT('Ctrl Pts',(106.811515713278,1.91180993464163,135.335824601347));
#44875=CARTESIAN_POINT('Ctrl Pts',(106.803767645275,2.03822865296876,135.282488954746));
#44876=CARTESIAN_POINT('Ctrl Pts',(106.796019577272,2.1623799624507,135.223873327984));
#44877=CARTESIAN_POINT('Ctrl Pts',(106.788271509269,2.283803350934,135.160210169234));
#44878=CARTESIAN_POINT('Ctrl Pts',(106.780515206527,2.40535578963962,135.096479348521));
#44879=CARTESIAN_POINT('Ctrl Pts',(106.772758903785,2.52417416893811,135.027690461335));
#44880=CARTESIAN_POINT('Ctrl Pts',(106.765002601043,2.63982342130372,134.954121498248));
#44881=CARTESIAN_POINT('Ctrl Pts',(106.757242158529,2.75553439915754,134.88051326919));
#44882=CARTESIAN_POINT('Ctrl Pts',(106.749481716015,2.86807255905725,134.802120103969));
#44883=CARTESIAN_POINT('Ctrl Pts',(106.741721273501,2.97703390128575,134.719261920676));
#44884=CARTESIAN_POINT('Ctrl Pts',(106.733948373235,3.08617015793393,134.636270726073));
#44885=CARTESIAN_POINT('Ctrl Pts',(106.72617547297,3.19171782171265,134.548800439777));
#44886=CARTESIAN_POINT('Ctrl Pts',(106.718402572704,3.29330724416999,134.45721025285));
#44887=CARTESIAN_POINT('Ctrl Pts',(106.710912236942,3.39120363523365,134.36894959992));
#44888=CARTESIAN_POINT('Ctrl Pts',(106.70342190118,3.48542435242331,134.27686359877));
#44889=CARTESIAN_POINT('Ctrl Pts',(106.695931565418,3.57567385222377,134.181302957172));
#44890=CARTESIAN_POINT('Ctrl Pts',(106.688157231299,3.66934518923912,134.082119104803));
#44891=CARTESIAN_POINT('Ctrl Pts',(106.68038289718,3.75903494954317,133.978877744152));
#44892=CARTESIAN_POINT('Ctrl Pts',(106.672608563061,3.84437113625636,133.871931909194));
#44893=CARTESIAN_POINT('Ctrl Pts',(106.664843810114,3.92960215374607,133.765117875419));
#44894=CARTESIAN_POINT('Ctrl Pts',(106.657079057167,4.01049003166381,133.654608753854));
#44895=CARTESIAN_POINT('Ctrl Pts',(106.649314304219,4.08669969696697,133.540794181406));
#44896=CARTESIAN_POINT('Ctrl Pts',(106.641557263334,4.16283366975624,133.427092651196));
#44897=CARTESIAN_POINT('Ctrl Pts',(106.633800222449,4.23429846049034,133.310092526223));
#44898=CARTESIAN_POINT('Ctrl Pts',(106.626043181564,4.30079960500237,133.190215982024));
#44899=CARTESIAN_POINT('Ctrl Pts',(106.618291990324,4.36725060048396,133.070429837659));
#44900=CARTESIAN_POINT('Ctrl Pts',(106.610540799084,4.42874521131446,132.947771932091));
#44901=CARTESIAN_POINT('Ctrl Pts',(106.602789607844,4.48503280968691,132.822692542333));
#44902=CARTESIAN_POINT('Ctrl Pts',(106.595041711067,4.54129648432857,132.697666314652));
#44903=CARTESIAN_POINT('Ctrl Pts',(106.58729381429,4.59235738813069,132.570221005554));
#44904=CARTESIAN_POINT('Ctrl Pts',(106.579545917513,4.63801140907041,132.440830364256));
#44905=CARTESIAN_POINT('Ctrl Pts',(106.571799641429,4.68365588017314,132.311466788692));
#44906=CARTESIAN_POINT('Ctrl Pts',(106.564053365344,4.72389558803606,132.180159058771));
#44907=CARTESIAN_POINT('Ctrl Pts',(106.55630708926,4.75857518336706,132.047399348557));
#44908=CARTESIAN_POINT('Ctrl Pts',(106.548560755995,4.79325503469494,131.914638658341));
#44909=CARTESIAN_POINT('Ctrl Pts',(106.54081442273,4.82237459277903,131.780426344716));
#44910=CARTESIAN_POINT('Ctrl Pts',(106.533068089464,4.84582895551257,131.645267744671));
#44911=CARTESIAN_POINT('Ctrl Pts',(106.525320021461,4.86928857068803,131.510078876795));
#44912=CARTESIAN_POINT('Ctrl Pts',(106.517571953458,4.88708039915095,131.373943685948));
#44913=CARTESIAN_POINT('Ctrl Pts',(106.509823885455,4.89915108806627,131.237375257964));
#44914=CARTESIAN_POINT('Ctrl Pts',(106.502067582713,4.91123460585341,131.10066168343));
#44915=CARTESIAN_POINT('Ctrl Pts',(106.494311279972,4.91758480317241,130.963514342028));
#44916=CARTESIAN_POINT('Ctrl Pts',(106.48655497723,4.91820039673943,130.826449529086));
#44917=CARTESIAN_POINT('Ctrl Pts',(106.478794534716,4.91881631886727,130.689311560525));
#44918=CARTESIAN_POINT('Ctrl Pts',(106.471034092201,4.91369155307972,130.552256598693));
#44919=CARTESIAN_POINT('Ctrl Pts',(106.463273649687,4.90287688381336,130.415797463538));
#44920=CARTESIAN_POINT('Ctrl Pts',(106.455500749422,4.89204485387983,130.279119272064));
#44921=CARTESIAN_POINT('Ctrl Pts',(106.447727849156,4.87550471514916,130.143039206938));
#44922=CARTESIAN_POINT('Ctrl Pts',(106.439954948891,4.85335886121664,130.008062415414));
#44923=CARTESIAN_POINT('Ctrl Pts',(106.432464613129,4.8320180648569,129.87799237025));
#44924=CARTESIAN_POINT('Ctrl Pts',(106.424974277367,4.80547210318921,129.748947079465));
#44925=CARTESIAN_POINT('Ctrl Pts',(106.417483941605,4.77385628810415,129.621364758305));
#44926=CARTESIAN_POINT('Ctrl Pts',(106.409709607486,4.74104174978028,129.488945114659));
#44927=CARTESIAN_POINT('Ctrl Pts',(106.401935273367,4.702661375356,129.357682101927));
#44928=CARTESIAN_POINT('Ctrl Pts',(106.394160939248,4.65881110891264,129.228079515106));
#44929=CARTESIAN_POINT('Ctrl Pts',(106.386396186301,4.6150148840037,129.098636651891));
#44930=CARTESIAN_POINT('Ctrl Pts',(106.378631433354,4.56576230406105,128.970850509794));
#44931=CARTESIAN_POINT('Ctrl Pts',(106.370866680407,4.5112000664855,128.845213603521));
#44932=CARTESIAN_POINT('Ctrl Pts',(106.363109639522,4.45669202089354,128.719701481595));
#44933=CARTESIAN_POINT('Ctrl Pts',(106.355352598637,4.39688496715423,128.596334703727));
#44934=CARTESIAN_POINT('Ctrl Pts',(106.347595557752,4.33197492842929,128.475589207152));
#44935=CARTESIAN_POINT('Ctrl Pts',(106.339844366511,4.26711383886943,128.354934765696));
#44936=CARTESIAN_POINT('Ctrl Pts',(106.332093175271,4.19715760830539,128.23689801394));
#44937=CARTESIAN_POINT('Ctrl Pts',(106.324341984031,4.12234959709103,128.121933197884));
#44938=CARTESIAN_POINT('Ctrl Pts',(106.316594087254,4.04757338127701,128.007017244941));
#44939=CARTESIAN_POINT('Ctrl Pts',(106.308846190477,3.96794969903147,127.89517095786));
#44940=CARTESIAN_POINT('Ctrl Pts',(106.3010982937,3.88376680145399,127.786822134891));
#44941=CARTESIAN_POINT('Ctrl Pts',(106.293352017616,3.7996015131239,127.67849597616));
#44942=CARTESIAN_POINT('Ctrl Pts',(106.285605741532,3.71087914612315,127.573666134896));
#44943=CARTESIAN_POINT('Ctrl Pts',(106.277859465448,3.61792981034243,127.47272934296));
#44944=CARTESIAN_POINT('Ctrl Pts',(106.270113132182,3.52497978843088,127.371791805931));
#44945=CARTESIAN_POINT('Ctrl Pts',(106.262366798917,3.42780300031751,127.274747663174));
#44946=CARTESIAN_POINT('Ctrl Pts',(106.254620465652,3.32676789817163,127.181958318788));
#44947=CARTESIAN_POINT('Ctrl Pts',(106.246872397649,3.22571016991516,127.089148194871));
#44948=CARTESIAN_POINT('Ctrl Pts',(106.239124329646,3.12079269618089,127.000595029755));
#44949=CARTESIAN_POINT('Ctrl Pts',(106.231376261643,3.0124183121011,126.916621046116));
#44950=CARTESIAN_POINT('Ctrl Pts',(106.223619958901,2.90392874643616,126.832557813928));
#44951=CARTESIAN_POINT('Ctrl Pts',(106.215863656159,2.79197524066403,126.753083725039));
#44952=CARTESIAN_POINT('Ctrl Pts',(106.208107353417,2.67699147501793,126.678478929347));
#44953=CARTESIAN_POINT('Ctrl Pts',(106.200346910903,2.56194633907393,126.603834314829));
#44954=CARTESIAN_POINT('Ctrl Pts',(106.192586468389,2.44386805699931,126.534064370803));
#44955=CARTESIAN_POINT('Ctrl Pts',(106.184826025875,2.3232155289681,126.469403562593));
#44956=CARTESIAN_POINT('Ctrl Pts',(106.177053125609,2.20236931878787,126.404638955113));
#44957=CARTESIAN_POINT('Ctrl Pts',(106.169280225344,2.07894095701078,126.345000043127));
#44958=CARTESIAN_POINT('Ctrl Pts',(106.161507325078,1.95341078456747,126.290673724434));
#44959=CARTESIAN_POINT('Ctrl Pts',(106.154016989316,1.83244395008245,126.238322304264));
#44960=CARTESIAN_POINT('Ctrl Pts',(106.146526653554,1.7095257514868,126.190904041858));
#44961=CARTESIAN_POINT('Ctrl Pts',(106.139036317792,1.5850980110598,126.148541961536));
#44962=CARTESIAN_POINT('Ctrl Pts',(106.131261983673,1.45595255503697,126.104573710064));
#44963=CARTESIAN_POINT('Ctrl Pts',(106.123487649554,1.32477173499468,126.065913341397));
#44964=CARTESIAN_POINT('Ctrl Pts',(106.115713315435,1.19203126805155,126.032752448564));
#44965=CARTESIAN_POINT('Ctrl Pts',(106.107948562488,1.05945439187075,125.999632423568));
#44966=CARTESIAN_POINT('Ctrl Pts',(106.100183809541,0.925322068912722,125.971998482826));
#44967=CARTESIAN_POINT('Ctrl Pts',(106.092419056594,0.790127959276913,125.949993421889));
#44968=CARTESIAN_POINT('Ctrl Pts',(106.084662015709,0.655068126336514,125.928010216688));
#44969=CARTESIAN_POINT('Ctrl Pts',(106.076904974824,0.518948988773026,125.911644827984));
#44970=CARTESIAN_POINT('Ctrl Pts',(106.069147933939,0.382276921367454,125.90098959164));
#44971=CARTESIAN_POINT('Ctrl Pts',(106.061396742699,0.245707919431345,125.890342390492));
#44972=CARTESIAN_POINT('Ctrl Pts',(106.053645551458,0.108587205809336,125.885396800998));
#44973=CARTESIAN_POINT('Ctrl Pts',(106.045894360218,-0.0285715072602836,
125.886193608255));
#44974=CARTESIAN_POINT('Ctrl Pts',(106.038146463441,-0.165671924218207,
125.886990076848));
#44975=CARTESIAN_POINT('Ctrl Pts',(106.030398566664,-0.302809918360973,
125.893524085617));
#44976=CARTESIAN_POINT('Ctrl Pts',(106.022650669887,-0.439469764145238,
125.905784356151));
#44977=CARTESIAN_POINT('Ctrl Pts',(106.014904393803,-0.57610102363581,125.9180420621));
#44978=CARTESIAN_POINT('Ctrl Pts',(106.007158117719,-0.712253944555239,
125.936023612391));
#44979=CARTESIAN_POINT('Ctrl Pts',(105.999411841635,-0.847416312692825,
125.959665719486));
#44980=CARTESIAN_POINT('Ctrl Pts',(105.99166550837,-0.982579678568309,125.983308001101));
#44981=CARTESIAN_POINT('Ctrl Pts',(105.983919175104,-1.1167520919532,126.012610855536));
#44982=CARTESIAN_POINT('Ctrl Pts',(105.976172841839,-1.24943033594581,126.047459641288));
#44983=CARTESIAN_POINT('Ctrl Pts',(105.968424773836,-1.38213829231104,126.082316231183));
#44984=CARTESIAN_POINT('Ctrl Pts',(105.960676705833,-1.51335103538431,126.122721124477));
#44985=CARTESIAN_POINT('Ctrl Pts',(105.95292863783,-1.64257972787296,126.16850957379));
#44986=CARTESIAN_POINT('Ctrl Pts',(105.945172335088,-1.7719457661539,126.214346687612));
#44987=CARTESIAN_POINT('Ctrl Pts',(105.937416032346,-1.89932317244547,126.265578656399));
#44988=CARTESIAN_POINT('Ctrl Pts',(105.929659729605,-2.02424183394526,126.321992040552));
#44989=CARTESIAN_POINT('Ctrl Pts',(105.92189928709,-2.14922716829608,126.378435534226));
#44990=CARTESIAN_POINT('Ctrl Pts',(105.914138844576,-2.27175079387615,126.440065778115));
#44991=CARTESIAN_POINT('Ctrl Pts',(105.906378402062,-2.3913674016154,126.506623420739));
#44992=CARTESIAN_POINT('Ctrl Pts',(105.898605501797,-2.51117602855246,126.5732879076));
#44993=CARTESIAN_POINT('Ctrl Pts',(105.890832601531,-2.6280679787137,126.644895395346));
#44994=CARTESIAN_POINT('Ctrl Pts',(105.883059701266,-2.74162637368244,126.721142782374));
#44995=CARTESIAN_POINT('Ctrl Pts',(105.875569365504,-2.85105663495688,126.794618384827));
#44996=CARTESIAN_POINT('Ctrl Pts',(105.868079029742,-2.95739125085624,126.872402217443));
#44997=CARTESIAN_POINT('Ctrl Pts',(105.86058869398,-3.06028790180302,126.954189060274));
#44998=CARTESIAN_POINT('Ctrl Pts',(105.852913814628,-3.16571967507078,127.037990931281));
#44999=CARTESIAN_POINT('Ctrl Pts',(105.845238935276,-3.26789399701385,127.126275793685));
#45000=CARTESIAN_POINT('Ctrl Pts',(105.837564055923,-3.36639833683841,127.218758115861));
#45001=CARTESIAN_POINT('Ctrl Pts',(105.829897956767,-3.46478998597824,127.311134636646));
#45002=CARTESIAN_POINT('Ctrl Pts',(105.822231857611,-3.55951970969645,127.407698799645));
#45003=CARTESIAN_POINT('Ctrl Pts',(105.814565758455,-3.65020571628105,127.508123172944));
#45004=CARTESIAN_POINT('Ctrl Pts',(105.806906667801,-3.74080881589757,127.608455736265));
#45005=CARTESIAN_POINT('Ctrl Pts',(105.799247577146,-3.82737528171168,127.712641196918));
#45006=CARTESIAN_POINT('Ctrl Pts',(105.791588486492,-3.90955847607444,127.820313770639));
#45007=CARTESIAN_POINT('Ctrl Pts',(105.783934638994,-3.99168541057586,127.927912635323));
#45008=CARTESIAN_POINT('Ctrl Pts',(105.776280791497,-4.06943479897665,128.038993547196));
#45009=CARTESIAN_POINT('Ctrl Pts',(105.768626943999,-4.14249915075095,128.153156391459));
#45010=CARTESIAN_POINT('Ctrl Pts',(105.76097564897,-4.2155391364183,128.267281163749));
#45011=CARTESIAN_POINT('Ctrl Pts',(105.753324353941,-4.28389697206781,128.384485489604));
#45012=CARTESIAN_POINT('Ctrl Pts',(105.745673058913,-4.34730773998133,128.504339209753));
#45013=CARTESIAN_POINT('Ctrl Pts',(105.738023470259,-4.41070436615869,128.624166200377));
#45014=CARTESIAN_POINT('Ctrl Pts',(105.730373881606,-4.46915593470218,128.746641053295));
#45015=CARTESIAN_POINT('Ctrl Pts',(105.722724292953,-4.52244321646789,128.871308518857));
#45016=CARTESIAN_POINT('Ctrl Pts',(105.715072029486,-4.57574913107084,128.996019576595));
#45017=CARTESIAN_POINT('Ctrl Pts',(105.70741976602,-4.62388699108354,129.122924409893));
#45018=CARTESIAN_POINT('Ctrl Pts',(105.699767502553,-4.66668553437845,129.251547304343));
#45019=CARTESIAN_POINT('Ctrl Pts',(105.693272171535,-4.70301344010398,129.360723926349));
#45020=CARTESIAN_POINT('Ctrl Pts',(105.686776840516,-4.73549524688595,129.47113791478));
#45021=CARTESIAN_POINT('Ctrl Pts',(105.680281509498,-4.76405452823405,129.582490119308));
#45022=CARTESIAN_POINT('Origin',(213.235140564004,0.,130.804360617566));
#45023=CARTESIAN_POINT('',(103.584579145176,-4.76405452823405,129.582490119308));
#45024=CARTESIAN_POINT('',(103.930161944428,-4.76405452823404,129.582490119308));
#45025=CARTESIAN_POINT('',(213.235140564004,-4.76405452823405,129.582490119308));
#45026=CARTESIAN_POINT('',(105.264859435952,-4.91824797726599,130.799900054936));
#45027=CARTESIAN_POINT('Ctrl Pts',(105.264859435952,-4.91824797726599,130.799900054936));
#45028=CARTESIAN_POINT('Ctrl Pts',(105.257209733691,-4.91837034801499,130.93482691028));
#45029=CARTESIAN_POINT('Ctrl Pts',(105.249560031429,-4.91293618644247,131.069928051336));
#45030=CARTESIAN_POINT('Ctrl Pts',(105.241910329167,-4.90192925582662,131.20470126423));
#45031=CARTESIAN_POINT('Ctrl Pts',(105.234266762425,-4.8909311534284,131.339366380934));
#45032=CARTESIAN_POINT('Ctrl Pts',(105.226623195683,-4.87436920604566,131.473703692978));
#45033=CARTESIAN_POINT('Ctrl Pts',(105.218979628941,-4.85227924260771,131.607211297492));
#45034=CARTESIAN_POINT('Ctrl Pts',(105.211339652271,-4.83019965450653,131.740656195414));
#45035=CARTESIAN_POINT('Ctrl Pts',(105.203699675602,-4.80259727797285,131.873271763944));
#45036=CARTESIAN_POINT('Ctrl Pts',(105.196059698933,-4.76955971249369,132.004561938786));
#45037=CARTESIAN_POINT('Ctrl Pts',(105.188421429977,-4.73652953168282,132.135822767204));
#45038=CARTESIAN_POINT('Ctrl Pts',(105.180783161021,-4.69806667542035,132.265758400346));
#45039=CARTESIAN_POINT('Ctrl Pts',(105.173144892065,-4.65430959729121,132.393884205017));
#45040=CARTESIAN_POINT('Ctrl Pts',(105.165506567533,-4.61055220078228,132.522010941941));
#45041=CARTESIAN_POINT('Ctrl Pts',(105.157868243,-4.56150063627449,132.648327442905));
#45042=CARTESIAN_POINT('Ctrl Pts',(105.150229918468,-4.50734266928378,132.772365984468));
#45043=CARTESIAN_POINT('Ctrl Pts',(105.142589775233,-4.4531718071604,132.896434059884));
#45044=CARTESIAN_POINT('Ctrl Pts',(105.134949631999,-4.39389228649692,133.018222728364));
#45045=CARTESIAN_POINT('Ctrl Pts',(105.127309488764,-4.32973903783793,133.137286447232));
#45046=CARTESIAN_POINT('Ctrl Pts',(105.119661395806,-4.26551903642628,133.256474054307));
#45047=CARTESIAN_POINT('Ctrl Pts',(105.112013302848,-4.19641537389779,133.372930696015));
#45048=CARTESIAN_POINT('Ctrl Pts',(105.10436520989,-4.12270791310648,133.486237297376));
#45049=CARTESIAN_POINT('Ctrl Pts',(105.096712739397,-4.04895826441624,133.599608751975));
#45050=CARTESIAN_POINT('Ctrl Pts',(105.089060268904,-3.97059980482833,133.709826249315));
#45051=CARTESIAN_POINT('Ctrl Pts',(105.081407798411,-3.88795353957172,133.816502768367));
#45052=CARTESIAN_POINT('Ctrl Pts',(105.073743978962,-3.80518470621165,133.923337493462));
#45053=CARTESIAN_POINT('Ctrl Pts',(105.066080159514,-3.7181156304839,134.026620448661));
#45054=CARTESIAN_POINT('Ctrl Pts',(105.058416340065,-3.6271053942907,134.126000200845));
#45055=CARTESIAN_POINT('Ctrl Pts',(105.053889166277,-3.57334379949745,134.184705838706));
#45056=CARTESIAN_POINT('Ctrl Pts',(105.049361992489,-3.51820760852765,134.242050180961));
#45057=CARTESIAN_POINT('Ctrl Pts',(105.0448348187,-3.46177617688253,134.297967459165));
#45058=CARTESIAN_POINT('Ctrl Pts',(105.037060484581,-3.36486874082114,134.393991960127));
#45059=CARTESIAN_POINT('Ctrl Pts',(105.029286150462,-3.26380941807688,134.486133399984));
#45060=CARTESIAN_POINT('Ctrl Pts',(105.021511816343,-3.15894221405989,134.57401141714));
#45061=CARTESIAN_POINT('Ctrl Pts',(105.013747063396,-3.05420424949947,134.661781132495));
#45062=CARTESIAN_POINT('Ctrl Pts',(105.005982310449,-2.94566803786873,134.745297630913));
#45063=CARTESIAN_POINT('Ctrl Pts',(104.998217557502,-2.83371506303976,134.824216585633));
#45064=CARTESIAN_POINT('Ctrl Pts',(104.990460516617,-2.72187328148395,134.903057156934));
#45065=CARTESIAN_POINT('Ctrl Pts',(104.982703475732,-2.60662180758364,134.977309047969));
#45066=CARTESIAN_POINT('Ctrl Pts',(104.974946434847,-2.48837562897248,135.046667748319));
#45067=CARTESIAN_POINT('Ctrl Pts',(104.967195243607,-2.37021862072443,135.115974144733));
#45068=CARTESIAN_POINT('Ctrl Pts',(104.959444052367,-2.2490717387028,135.180394498164));
#45069=CARTESIAN_POINT('Ctrl Pts',(104.951692861126,-2.12537911587788,135.239667447571));
#45070=CARTESIAN_POINT('Ctrl Pts',(104.943944964349,-2.00173906571718,135.298915204394));
#45071=CARTESIAN_POINT('Ctrl Pts',(104.936197067572,-1.8755557786207,135.35301973993));
#45072=CARTESIAN_POINT('Ctrl Pts',(104.928449170795,-1.74729796925173,135.401765632262));
#45073=CARTESIAN_POINT('Ctrl Pts',(104.920702894711,-1.61906698865174,135.450501328003));
#45074=CARTESIAN_POINT('Ctrl Pts',(104.912956618627,-1.48876271414915,135.493880471287));
#45075=CARTESIAN_POINT('Ctrl Pts',(104.905210342543,-1.35687345011762,135.531735946738));
#45076=CARTESIAN_POINT('Ctrl Pts',(104.897464009277,-1.22498321250932,135.56959170163));
#45077=CARTESIAN_POINT('Ctrl Pts',(104.889717676012,-1.09150833781755,135.601923599463));
#45078=CARTESIAN_POINT('Ctrl Pts',(104.881971342747,-0.956951500145035,
135.628614641648));
#45079=CARTESIAN_POINT('Ctrl Pts',(104.874223274744,-0.822364529401955,
135.655311661106));
#45080=CARTESIAN_POINT('Ctrl Pts',(104.866475206741,-0.686695496952768,
135.676365235176));
#45081=CARTESIAN_POINT('Ctrl Pts',(104.858727138738,-0.55045606055374,135.691709713743));
#45082=CARTESIAN_POINT('Ctrl Pts',(104.850970835996,-0.414071827260159,
135.707070500603));
#45083=CARTESIAN_POINT('Ctrl Pts',(104.843214533254,-0.277116368131101,
135.71671002726));
#45084=CARTESIAN_POINT('Ctrl Pts',(104.835458230512,-0.14010579901636,135.720614621132));
#45085=CARTESIAN_POINT('Ctrl Pts',(104.827697787998,-0.00302210323538782,
135.724521299004));
#45086=CARTESIAN_POINT('Ctrl Pts',(104.819937345484,0.134116370401911,135.722686950205));
#45087=CARTESIAN_POINT('Ctrl Pts',(104.81217690297,0.270795730941145,135.715150038281));
#45088=CARTESIAN_POINT('Ctrl Pts',(104.804404002704,0.407694501323553,135.707601027437));
#45089=CARTESIAN_POINT('Ctrl Pts',(104.796631102439,0.544132296475826,135.694331198206));
#45090=CARTESIAN_POINT('Ctrl Pts',(104.788858202173,0.679601657449962,135.675430792557));
#45091=CARTESIAN_POINT('Ctrl Pts',(104.781367866411,0.810146365927796,135.657217464261));
#45092=CARTESIAN_POINT('Ctrl Pts',(104.773877530649,0.939791524745636,135.633775878336));
#45093=CARTESIAN_POINT('Ctrl Pts',(104.766387194887,1.06809579774052,135.605230791748));
#45094=CARTESIAN_POINT('Ctrl Pts',(104.758612860768,1.20126476624147,135.575603409527));
#45095=CARTESIAN_POINT('Ctrl Pts',(104.750838526649,1.33341100162869,135.540384038075));
#45096=CARTESIAN_POINT('Ctrl Pts',(104.74306419253,1.46402855159239,135.499656504155));
#45097=CARTESIAN_POINT('Ctrl Pts',(104.735299439583,1.59448512709965,135.458979163281));
#45098=CARTESIAN_POINT('Ctrl Pts',(104.727534686635,1.7234163960596,135.412807281929));
#45099=CARTESIAN_POINT('Ctrl Pts',(104.719769933688,1.85032646526505,135.361275696261));
#45100=CARTESIAN_POINT('Ctrl Pts',(104.712012892803,1.97711048560039,135.309795292491));
#45101=CARTESIAN_POINT('Ctrl Pts',(104.704255851918,2.10187694126749,135.252965924214));
#45102=CARTESIAN_POINT('Ctrl Pts',(104.696498811033,2.22414532807544,135.190972136962));
#45103=CARTESIAN_POINT('Ctrl Pts',(104.688747619793,2.34632151134144,135.129025099708));
#45104=CARTESIAN_POINT('Ctrl Pts',(104.680996428553,2.46600302807129,135.061921571389));
#45105=CARTESIAN_POINT('Ctrl Pts',(104.673245237313,2.58272992310162,134.989893941626));
#45106=CARTESIAN_POINT('Ctrl Pts',(104.665497340536,2.69940720608816,134.917896925527));
#45107=CARTESIAN_POINT('Ctrl Pts',(104.657749443759,2.81313203302882,134.84098017543));
#45108=CARTESIAN_POINT('Ctrl Pts',(104.650001546982,2.92346981163792,134.759421593448));
#45109=CARTESIAN_POINT('Ctrl Pts',(104.642255270898,3.03378450996235,134.677880071762));
#45110=CARTESIAN_POINT('Ctrl Pts',(104.634508994813,3.14071325499609,134.591698881754));
#45111=CARTESIAN_POINT('Ctrl Pts',(104.626762718729,3.24385150739914,134.501198517778));
#45112=CARTESIAN_POINT('Ctrl Pts',(104.619016385464,3.34699052114512,134.410697485749));
#45113=CARTESIAN_POINT('Ctrl Pts',(104.611270052199,3.44633869255544,134.315877473996));
#45114=CARTESIAN_POINT('Ctrl Pts',(104.603523718933,3.5415258797701,134.21709815588));
#45115=CARTESIAN_POINT('Ctrl Pts',(104.59577565093,3.6367343834955,134.118296716821));
#45116=CARTESIAN_POINT('Ctrl Pts',(104.588027582927,3.72777977756826,134.015534488521));
#45117=CARTESIAN_POINT('Ctrl Pts',(104.580279514924,3.81433026517127,133.909206457652));
#45118=CARTESIAN_POINT('Ctrl Pts',(104.572523212182,3.90097273966252,133.802765420086));
#45119=CARTESIAN_POINT('Ctrl Pts',(104.564766909441,3.98311051742606,133.692751313156));
#45120=CARTESIAN_POINT('Ctrl Pts',(104.557010606699,4.06045312211073,133.579590969382));
#45121=CARTESIAN_POINT('Ctrl Pts',(104.549250164185,4.13783700687236,133.466370228525));
#45122=CARTESIAN_POINT('Ctrl Pts',(104.54148972167,4.2104204120701,133.350000236358));
#45123=CARTESIAN_POINT('Ctrl Pts',(104.533729279156,4.27795792756222,133.230934134381));
#45124=CARTESIAN_POINT('Ctrl Pts',(104.525956378891,4.34560386026981,133.111676896927));
#45125=CARTESIAN_POINT('Ctrl Pts',(104.518183478625,4.40818753807545,132.989715248914));
#45126=CARTESIAN_POINT('Ctrl Pts',(104.51041057836,4.46551059014517,132.865524907913));
#45127=CARTESIAN_POINT('Ctrl Pts',(104.502920242598,4.52074980488344,132.745849198626));
#45128=CARTESIAN_POINT('Ctrl Pts',(104.495429906836,4.57110410984297,132.624104304988));
#45129=CARTESIAN_POINT('Ctrl Pts',(104.487939571074,4.61643991361667,132.500728969802));
#45130=CARTESIAN_POINT('Ctrl Pts',(104.480165236955,4.66349463817047,132.372675821281));
#45131=CARTESIAN_POINT('Ctrl Pts',(104.472390902836,4.70529185158218,132.242460520324));
#45132=CARTESIAN_POINT('Ctrl Pts',(104.464616568717,4.74162860009793,132.110554049349));
#45133=CARTESIAN_POINT('Ctrl Pts',(104.45685181577,4.7779205668186,131.978810141311));
#45134=CARTESIAN_POINT('Ctrl Pts',(104.449087062823,4.80876535557601,131.845379583531));
#45135=CARTESIAN_POINT('Ctrl Pts',(104.441322309876,4.8340083654595,131.710752467247));
#45136=CARTESIAN_POINT('Ctrl Pts',(104.433565268991,4.8592263036297,131.576259064512));
#45137=CARTESIAN_POINT('Ctrl Pts',(104.425808228106,4.87885346348556,131.440571850102));
#45138=CARTESIAN_POINT('Ctrl Pts',(104.418051187221,4.8927853841564,131.304194837168));
#45139=CARTESIAN_POINT('Ctrl Pts',(104.410299995981,4.90670679865746,131.167920667201));
#45140=CARTESIAN_POINT('Ctrl Pts',(104.402548804741,4.91494148298815,131.030958121469));
#45141=CARTESIAN_POINT('Ctrl Pts',(104.394797613501,4.91743633611711,130.893819785543));
#45142=CARTESIAN_POINT('Ctrl Pts',(104.387049716724,4.91993012886695,130.756739737068));
#45143=CARTESIAN_POINT('Ctrl Pts',(104.379301819946,4.91668893545993,130.619484437085));
#45144=CARTESIAN_POINT('Ctrl Pts',(104.371553923169,4.90771165506752,130.482569733272));
#45145=CARTESIAN_POINT('Ctrl Pts',(104.363807647085,4.89873625252865,130.345683669065));
#45146=CARTESIAN_POINT('Ctrl Pts',(104.356061371001,4.88402717516698,130.209138449196));
#45147=CARTESIAN_POINT('Ctrl Pts',(104.348315094917,4.86363540056671,130.073447659099));
#45148=CARTESIAN_POINT('Ctrl Pts',(104.340568761652,4.84324347543904,129.937755867365));
#45149=CARTESIAN_POINT('Ctrl Pts',(104.332822428387,4.81716882747013,129.802918904611));
#45150=CARTESIAN_POINT('Ctrl Pts',(104.325076095121,4.78551398932964,129.669442593905));
#45151=CARTESIAN_POINT('Ctrl Pts',(104.317328027118,4.75385206230745,129.535936392105));
#45152=CARTESIAN_POINT('Ctrl Pts',(104.309579959115,4.71660754866543,129.403791829029));
#45153=CARTESIAN_POINT('Ctrl Pts',(104.301831891112,4.67393341759135,129.273501554679));
#45154=CARTESIAN_POINT('Ctrl Pts',(104.29407558837,4.63121393194308,129.143072806276));
#45155=CARTESIAN_POINT('Ctrl Pts',(104.286319285629,4.58305342323004,129.014502655542));
#45156=CARTESIAN_POINT('Ctrl Pts',(104.278562982887,4.52965398817584,128.888266201859));
#45157=CARTESIAN_POINT('Ctrl Pts',(104.270802540373,4.47622605223547,128.761962371981));
#45158=CARTESIAN_POINT('Ctrl Pts',(104.263042097859,4.41755378551381,128.637995074258));
#45159=CARTESIAN_POINT('Ctrl Pts',(104.255281655344,4.35388577861308,128.516815713244));
#45160=CARTESIAN_POINT('Ctrl Pts',(104.247508755079,4.29011556617529,128.395441824361));
#45161=CARTESIAN_POINT('Ctrl Pts',(104.239735854814,4.22133378411373,128.276865153931));
#45162=CARTESIAN_POINT('Ctrl Pts',(104.231962954548,4.14783344281394,128.161509733923));
#45163=CARTESIAN_POINT('Ctrl Pts',(104.224472618786,4.07700502405559,128.050347773993));
#45164=CARTESIAN_POINT('Ctrl Pts',(104.216982283024,4.00179532884505,127.942177182324));
#45165=CARTESIAN_POINT('Ctrl Pts',(104.209491947262,3.92250127450789,127.837347504352));
#45166=CARTESIAN_POINT('Ctrl Pts',(104.201717613143,3.84020076200073,127.728543177278));
#45167=CARTESIAN_POINT('Ctrl Pts',(104.193943279024,3.75323935621899,127.622993447023));
#45168=CARTESIAN_POINT('Ctrl Pts',(104.186168944905,3.66190360654968,127.52112364183));
#45169=CARTESIAN_POINT('Ctrl Pts',(104.178404191957,3.57068042002887,127.419379382068));
#45170=CARTESIAN_POINT('Ctrl Pts',(104.17063943901,3.47509387456759,127.321306312013));
#45171=CARTESIAN_POINT('Ctrl Pts',(104.162874686063,3.37547273223597,127.227299408077));
#45172=CARTESIAN_POINT('Ctrl Pts',(104.155117645178,3.27595053502713,127.133385873123));
#45173=CARTESIAN_POINT('Ctrl Pts',(104.147360604293,3.17240199800395,127.043530733932));
#45174=CARTESIAN_POINT('Ctrl Pts',(104.139603563408,3.06519469805296,126.958094307815));
#45175=CARTESIAN_POINT('Ctrl Pts',(104.131852372168,2.95806824396119,126.872722309971));
#45176=CARTESIAN_POINT('Ctrl Pts',(104.124101180928,2.84728882327914,126.79176263536));
#45177=CARTESIAN_POINT('Ctrl Pts',(104.116349989688,2.73325898636117,126.715537024407));
#45178=CARTESIAN_POINT('Ctrl Pts',(104.108602092911,2.61927761516574,126.639343811371));
#45179=CARTESIAN_POINT('Ctrl Pts',(104.100854196134,2.50204889981095,126.567880876892));
#45180=CARTESIAN_POINT('Ctrl Pts',(104.093106299357,2.38200624253308,126.501427975398));
#45181=CARTESIAN_POINT('Ctrl Pts',(104.085360023273,2.26198869559121,126.434988974418));
#45182=CARTESIAN_POINT('Ctrl Pts',(104.077613747188,2.13915871935098,126.373558111144));
#45183=CARTESIAN_POINT('Ctrl Pts',(104.069867471104,2.01397596241131,126.317370102162));
#45184=CARTESIAN_POINT('Ctrl Pts',(104.062121137839,1.88879228140165,126.261181678412));
#45185=CARTESIAN_POINT('Ctrl Pts',(104.054374804574,1.76125614171982,126.210236346277));
#45186=CARTESIAN_POINT('Ctrl Pts',(104.046628471308,1.63184852805071,126.16472125184));
#45187=CARTESIAN_POINT('Ctrl Pts',(104.038880403305,1.50241193444324,126.119195964613));
#45188=CARTESIAN_POINT('Ctrl Pts',(104.031132335302,1.37110340162787,126.079103464606));
#45189=CARTESIAN_POINT('Ctrl Pts',(104.023384267299,1.23842009358668,126.044581343871));
#45190=CARTESIAN_POINT('Ctrl Pts',(104.015627964558,1.10559576814675,126.010022532614));
#45191=CARTESIAN_POINT('Ctrl Pts',(104.007871661816,0.971394127692739,125.981046025599));
#45192=CARTESIAN_POINT('Ctrl Pts',(104.000115359074,0.836324125007024,125.957738595948));
#45193=CARTESIAN_POINT('Ctrl Pts',(103.99235491656,0.70118203139372,125.934418726421));
#45194=CARTESIAN_POINT('Ctrl Pts',(103.984594474045,0.565171039569875,125.91677401361));
#45195=CARTESIAN_POINT('Ctrl Pts',(103.976834031531,0.428805298262543,125.904839306389));
#45196=CARTESIAN_POINT('Ctrl Pts',(103.969061131266,0.292220650561469,125.892885440516));
#45197=CARTESIAN_POINT('Ctrl Pts',(103.961288231,0.155280506170268,125.886659915002));
#45198=CARTESIAN_POINT('Ctrl Pts',(103.953515330735,0.0184999944640169,
125.886145411548));
#45199=CARTESIAN_POINT('Ctrl Pts',(103.946024994973,-0.113308201112205,
125.885649611591));
#45200=CARTESIAN_POINT('Ctrl Pts',(103.938534659211,-0.244967860791525,
125.89045681121));
#45201=CARTESIAN_POINT('Ctrl Pts',(103.931044323449,-0.376024411032684,
125.900506143297));
#45202=CARTESIAN_POINT('Ctrl Pts',(103.92326998933,-0.512050010210392,125.910936498864));
#45203=CARTESIAN_POINT('Ctrl Pts',(103.915495655211,-0.647856751573124,
125.927047385025));
#45204=CARTESIAN_POINT('Ctrl Pts',(103.907721321092,-0.782931907480926,
125.94882761997));
#45205=CARTESIAN_POINT('Ctrl Pts',(103.899956568144,-0.917840595330902,
125.970581012721));
#45206=CARTESIAN_POINT('Ctrl Pts',(103.892191815197,-1.05201910939418,125.997989790637));
#45207=CARTESIAN_POINT('Ctrl Pts',(103.88442706225,-1.18495744090136,126.030990851274));
#45208=CARTESIAN_POINT('Ctrl Pts',(103.876670021365,-1.31776373618322,126.063959134792));
#45209=CARTESIAN_POINT('Ctrl Pts',(103.86891298048,-1.44933192318762,126.10250855407));
#45210=CARTESIAN_POINT('Ctrl Pts',(103.861155939595,-1.57916017247244,126.14652461657));
#45211=CARTESIAN_POINT('Ctrl Pts',(103.853404748355,-1.70889051726429,126.190507486214));
#45212=CARTESIAN_POINT('Ctrl Pts',(103.845653557115,-1.83688316722717,126.239948668593));
#45213=CARTESIAN_POINT('Ctrl Pts',(103.837902365875,-1.962649844731,126.29468339525));
#45214=CARTESIAN_POINT('Ctrl Pts',(103.830154469098,-2.08836306804272,126.349394858188));
#45215=CARTESIAN_POINT('Ctrl Pts',(103.822406572321,-2.21185184287539,126.409395234841));
#45216=CARTESIAN_POINT('Ctrl Pts',(103.814658675544,-2.33264653941025,126.474471105733));
#45217=CARTESIAN_POINT('Ctrl Pts',(103.80691239946,-2.45341596829855,126.539533364157));
#45218=CARTESIAN_POINT('Ctrl Pts',(103.799166123375,-2.57149209583039,126.609668819761));
#45219=CARTESIAN_POINT('Ctrl Pts',(103.791419847291,-2.68642899699944,126.684617627211));
#45220=CARTESIAN_POINT('Ctrl Pts',(103.783673514026,-2.80136674660659,126.759566987915));
#45221=CARTESIAN_POINT('Ctrl Pts',(103.775927180761,-2.91316489612109,126.839329557813));
#45222=CARTESIAN_POINT('Ctrl Pts',(103.768180847495,-3.02140601027084,126.923601827896));
#45223=CARTESIAN_POINT('Ctrl Pts',(103.760432779492,-3.12967136426799,127.00789297017));
#45224=CARTESIAN_POINT('Ctrl Pts',(103.752684711489,-3.23437778937837,127.096695582112));
#45225=CARTESIAN_POINT('Ctrl Pts',(103.744936643486,-3.33514079623731,127.189665757447));
#45226=CARTESIAN_POINT('Ctrl Pts',(103.737180340744,-3.43601089521875,127.28273474259));
#45227=CARTESIAN_POINT('Ctrl Pts',(103.729424038002,-3.53292891595121,127.379979873659));
#45228=CARTESIAN_POINT('Ctrl Pts',(103.721667735261,-3.62554675233683,127.481019857259));
#45229=CARTESIAN_POINT('Ctrl Pts',(103.713907292746,-3.71821402165047,127.58211376894));
#45230=CARTESIAN_POINT('Ctrl Pts',(103.706146850232,-3.80657628159641,127.687006270122));
#45231=CARTESIAN_POINT('Ctrl Pts',(103.698386407718,-3.89032630288535,127.795283629588));
#45232=CARTESIAN_POINT('Ctrl Pts',(103.690613507453,-3.97421076714333,127.903734805484));
#45233=CARTESIAN_POINT('Ctrl Pts',(103.682840607187,-4.05346797106655,128.015581378699));
#45234=CARTESIAN_POINT('Ctrl Pts',(103.675067706922,-4.12783404502062,128.130380595339));
#45235=CARTESIAN_POINT('Ctrl Pts',(103.66757737116,-4.19949672486927,128.241006571292));
#45236=CARTESIAN_POINT('Ctrl Pts',(103.660087035398,-4.26661755370495,128.354373980592));
#45237=CARTESIAN_POINT('Ctrl Pts',(103.652596699636,-4.329002032648,128.470067477485));
#45238=CARTESIAN_POINT('Ctrl Pts',(103.644401642804,-4.39725589557558,128.596645886287));
#45239=CARTESIAN_POINT('Ctrl Pts',(103.636206585971,-4.46003750102258,128.726374192205));
#45240=CARTESIAN_POINT('Ctrl Pts',(103.628011529139,-4.51706109976003,128.858765057452));
#45241=CARTESIAN_POINT('Ctrl Pts',(103.619834970596,-4.57395598200442,128.990857083478));
#45242=CARTESIAN_POINT('Ctrl Pts',(103.611658412052,-4.62511864185374,129.125599385668));
#45243=CARTESIAN_POINT('Ctrl Pts',(103.603481853508,-4.67030931125085,129.262480596376));
#45244=CARTESIAN_POINT('Ctrl Pts',(103.597180950731,-4.70513349954493,129.367962040206));
#45245=CARTESIAN_POINT('Ctrl Pts',(103.590880047953,-4.73641218697444,129.474713050268));
#45246=CARTESIAN_POINT('Ctrl Pts',(103.584579145176,-4.76405452823405,129.582490119308));
#45247=CARTESIAN_POINT('Ctrl Pts',(105.334849955158,-4.76405452823403,129.582490119308));
#45248=CARTESIAN_POINT('Ctrl Pts',(105.330994117609,-4.78088962480231,129.64812990532));
#45249=CARTESIAN_POINT('Ctrl Pts',(105.327138280061,-4.79635579169737,129.714070555088));
#45250=CARTESIAN_POINT('Ctrl Pts',(105.323282442513,-4.81044496211385,129.780250111335));
#45251=CARTESIAN_POINT('Ctrl Pts',(105.312383741536,-4.8502686459327,129.967309650353));
#45252=CARTESIAN_POINT('Ctrl Pts',(105.30148504056,-4.87919273195189,130.156764553182));
#45253=CARTESIAN_POINT('Ctrl Pts',(105.290586339583,-4.89699044628828,130.347559094515));
#45254=CARTESIAN_POINT('Ctrl Pts',(105.282010705053,-4.9109945642069,130.497685633495));
#45255=CARTESIAN_POINT('Ctrl Pts',(105.273435070522,-4.91811079454292,130.648641435253));
#45256=CARTESIAN_POINT('Ctrl Pts',(105.264859435991,-4.91824797726537,130.799900054249));
#45257=CARTESIAN_POINT('',(105.610140564046,-4.91824918613665,130.807190028493));
#45258=CARTESIAN_POINT('Ctrl Pts',(105.680281509498,-4.76405452823405,129.582490119308));
#45259=CARTESIAN_POINT('Ctrl Pts',(105.67262227585,-4.79773136595739,129.713795598474));
#45260=CARTESIAN_POINT('Ctrl Pts',(105.664963042202,-4.8259527168751,129.846405555949));
#45261=CARTESIAN_POINT('Ctrl Pts',(105.657303808554,-4.84864080799001,129.979821123306));
#45262=CARTESIAN_POINT('Ctrl Pts',(105.649443267802,-4.87192520861973,130.116743242706));
#45263=CARTESIAN_POINT('Ctrl Pts',(105.641582727051,-4.88938140979562,130.254513451776));
#45264=CARTESIAN_POINT('Ctrl Pts',(105.6337221863,-4.90098226160684,130.392588916359));
#45265=CARTESIAN_POINT('Ctrl Pts',(105.625861645548,-4.91258311341805,130.530664380942));
#45266=CARTESIAN_POINT('Ctrl Pts',(105.618001104797,-4.91832865954961,130.669044648147));
#45267=CARTESIAN_POINT('Ctrl Pts',(105.610140564046,-4.91824918613665,130.807190028493));
#45268=CARTESIAN_POINT('Ctrl Pts',(105.610140564008,-4.91824918613627,130.807190029158));
#45269=CARTESIAN_POINT('Ctrl Pts',(105.600807399395,-4.91815482384702,130.971216095075));
#45270=CARTESIAN_POINT('Ctrl Pts',(105.591474234781,-4.90985562625394,131.13500317217));
#45271=CARTESIAN_POINT('Ctrl Pts',(105.582141070167,-4.89341873628665,131.297955728825));
#45272=CARTESIAN_POINT('Ctrl Pts',(105.574366736048,-4.87972714508784,131.433691856217));
#45273=CARTESIAN_POINT('Ctrl Pts',(105.566592401929,-4.86036191113187,131.569072871748));
#45274=CARTESIAN_POINT('Ctrl Pts',(105.55881806781,-4.83534651705842,131.703586463764));
#45275=CARTESIAN_POINT('Ctrl Pts',(105.551053314863,-4.81036195222251,131.8379342798));
#45276=CARTESIAN_POINT('Ctrl Pts',(105.543288561915,-4.77974115299095,131.971416418671));
#45277=CARTESIAN_POINT('Ctrl Pts',(105.535523808968,-4.74355944243922,132.103524532761));
#45278=CARTESIAN_POINT('Ctrl Pts',(105.527766768083,-4.70741366807248,132.235501435211));
#45279=CARTESIAN_POINT('Ctrl Pts',(105.520009727198,-4.66571807635992,132.366106654058));
#45280=CARTESIAN_POINT('Ctrl Pts',(105.512252686313,-4.61859916939185,132.494841251881));
#45281=CARTESIAN_POINT('Ctrl Pts',(105.504501495073,-4.57151579515805,132.623478769942));
#45282=CARTESIAN_POINT('Ctrl Pts',(105.496750303833,-4.51901737993361,132.750248109131));
#45283=CARTESIAN_POINT('Ctrl Pts',(105.488999112593,-4.46128036204199,132.87466508642));
#45284=CARTESIAN_POINT('Ctrl Pts',(105.481251215816,-4.40356788392312,132.999029183175));
#45285=CARTESIAN_POINT('Ctrl Pts',(105.473503319039,-4.3406213957967,133.121042552691));
#45286=CARTESIAN_POINT('Ctrl Pts',(105.465755422262,-4.27266552549797,133.24024082187));
#45287=CARTESIAN_POINT('Ctrl Pts',(105.458009146177,-4.20472387010231,133.359414157341));
#45288=CARTESIAN_POINT('Ctrl Pts',(105.450262870093,-4.13177511028703,133.475773224316));
#45289=CARTESIAN_POINT('Ctrl Pts',(105.442516594009,-4.05408971753009,133.588878461775));
#45290=CARTESIAN_POINT('Ctrl Pts',(105.434770260744,-3.97640375131739,133.701984534151));
#45291=CARTESIAN_POINT('Ctrl Pts',(105.427023927479,-3.89398130374241,133.811836406812));
#45292=CARTESIAN_POINT('Ctrl Pts',(105.419277594213,-3.80713581370514,133.918024048077));
#45293=CARTESIAN_POINT('Ctrl Pts',(105.41152952621,-3.72027087522229,134.024235469329));
#45294=CARTESIAN_POINT('Ctrl Pts',(105.403781458207,-3.6289811707438,134.126780723745));
#45295=CARTESIAN_POINT('Ctrl Pts',(105.396033390204,-3.53361973419242,134.225283685486));
#45296=CARTESIAN_POINT('Ctrl Pts',(105.388277087462,-3.43815694637166,134.323891337347));
#45297=CARTESIAN_POINT('Ctrl Pts',(105.380520784721,-3.33861405423218,134.418447833072));
#45298=CARTESIAN_POINT('Ctrl Pts',(105.372764481979,-3.23538059495422,134.508614316801));
#45299=CARTESIAN_POINT('Ctrl Pts',(105.365004039465,-3.13209203687054,134.598828925096));
#45300=CARTESIAN_POINT('Ctrl Pts',(105.35724359695,-3.02510929153961,134.684648608087));
#45301=CARTESIAN_POINT('Ctrl Pts',(105.349483154436,-2.91485334369152,134.765776153365));
#45302=CARTESIAN_POINT('Ctrl Pts',(105.341710254171,-2.80442040320796,134.847033931781));
#45303=CARTESIAN_POINT('Ctrl Pts',(105.333937353905,-2.69070408468396,134.923584302226));
#45304=CARTESIAN_POINT('Ctrl Pts',(105.32616445364,-2.57415334665718,134.995174095925));
#45305=CARTESIAN_POINT('Ctrl Pts',(105.318674117878,-2.46183952153143,135.064161420299));
#45306=CARTESIAN_POINT('Ctrl Pts',(105.311183782116,-2.3468940444245,135.12854241476));
#45307=CARTESIAN_POINT('Ctrl Pts',(105.303693446354,-2.22973680891774,135.188132603591));
#45308=CARTESIAN_POINT('Ctrl Pts',(105.295919112235,-2.10813752121747,135.249982172544));
#45309=CARTESIAN_POINT('Ctrl Pts',(105.288144778116,-1.98377025668619,135.306866398525));
#45310=CARTESIAN_POINT('Ctrl Pts',(105.280370443997,-1.85707873056852,135.35852812118));
#45311=CARTESIAN_POINT('Ctrl Pts',(105.27260569105,-1.73054334043396,135.410126175379));
#45312=CARTESIAN_POINT('Ctrl Pts',(105.264840938102,-1.60168974665206,135.456514386301));
#45313=CARTESIAN_POINT('Ctrl Pts',(105.257076185155,-1.47098635043047,135.497481351081));
#45314=CARTESIAN_POINT('Ctrl Pts',(105.24931914427,-1.3404127706647,135.538407626894));
#45315=CARTESIAN_POINT('Ctrl Pts',(105.241562103385,-1.20799341532432,135.573923255702));
#45316=CARTESIAN_POINT('Ctrl Pts',(105.2338050625,-1.07421643206328,135.603864979434));
#45317=CARTESIAN_POINT('Ctrl Pts',(105.22605387126,-0.940540331066034,135.633784123878));
#45318=CARTESIAN_POINT('Ctrl Pts',(105.21830268002,-0.805509019937553,135.658137644663));
#45319=CARTESIAN_POINT('Ctrl Pts',(105.21055148878,-0.669625224796948,135.676812271591));
#45320=CARTESIAN_POINT('Ctrl Pts',(105.202803592003,-0.533799183894003,
135.695478961306));
#45321=CARTESIAN_POINT('Ctrl Pts',(105.195055695226,-0.397121766136255,
135.708471504673));
#45322=CARTESIAN_POINT('Ctrl Pts',(105.187307798449,-0.260105078594647,
135.715727882452));
#45323=CARTESIAN_POINT('Ctrl Pts',(105.179561522365,-0.123117051990335,
135.722982742352));
#45324=CARTESIAN_POINT('Ctrl Pts',(105.171815246281,0.0142097130680153,
135.724503802631));
#45325=CARTESIAN_POINT('Ctrl Pts',(105.164068970196,0.151359205005327,135.720281025136));
#45326=CARTESIAN_POINT('Ctrl Pts',(105.156322636931,0.288509709349126,135.716058216469));
#45327=CARTESIAN_POINT('Ctrl Pts',(105.148576303666,0.425482547180669,135.706091497453));
#45328=CARTESIAN_POINT('Ctrl Pts',(105.1408299704,0.561763325851781,135.690422940974));
#45329=CARTESIAN_POINT('Ctrl Pts',(105.133081902397,0.698074623658279,135.67475087563));
#45330=CARTESIAN_POINT('Ctrl Pts',(105.125333834394,0.833693165576224,135.653374476612));
#45331=CARTESIAN_POINT('Ctrl Pts',(105.117585766391,0.968111682826347,135.626387456155));
#45332=CARTESIAN_POINT('Ctrl Pts',(105.10982946365,1.1026730616762,135.599371753572));
#45333=CARTESIAN_POINT('Ctrl Pts',(105.102073160908,1.23603148418099,135.566733594824));
#45334=CARTESIAN_POINT('Ctrl Pts',(105.094316858166,1.36769130694644,135.528617548704));
#45335=CARTESIAN_POINT('Ctrl Pts',(105.086556415652,1.4994214005236,135.490481158902));
#45336=CARTESIAN_POINT('Ctrl Pts',(105.078795973138,1.62945071741313,135.446861180265));
#45337=CARTESIAN_POINT('Ctrl Pts',(105.071035530623,1.75730165187032,135.397951148603));
#45338=CARTESIAN_POINT('Ctrl Pts',(105.063262630358,1.88535782399748,135.348962602216));
#45339=CARTESIAN_POINT('Ctrl Pts',(105.055489730093,2.01122826650921,135.294667187901));
#45340=CARTESIAN_POINT('Ctrl Pts',(105.047716829827,2.13445730828998,135.235305783283));
#45341=CARTESIAN_POINT('Ctrl Pts',(105.040226494065,2.25320666400672,135.178102315245));
#45342=CARTESIAN_POINT('Ctrl Pts',(105.032736158303,2.36950305608668,135.116194930029));
#45343=CARTESIAN_POINT('Ctrl Pts',(105.025245822541,2.48296431714824,135.049837182366));
#45344=CARTESIAN_POINT('Ctrl Pts',(105.017471488422,2.60072749640885,134.980963460532));
#45345=CARTESIAN_POINT('Ctrl Pts',(105.009697154303,2.71580935108983,134.907077072235));
#45346=CARTESIAN_POINT('Ctrl Pts',(105.001922820184,2.8277536859747,134.828412326224));
#45347=CARTESIAN_POINT('Ctrl Pts',(104.994158067237,2.93956005947158,134.749844527483));
#45348=CARTESIAN_POINT('Ctrl Pts',(104.98639331429,3.04823628996613,134.666510310809));
#45349=CARTESIAN_POINT('Ctrl Pts',(104.978628561342,3.15335133594567,134.578689486993));
#45350=CARTESIAN_POINT('Ctrl Pts',(104.970871520457,3.25836198017967,134.490955888057));
#45351=CARTESIAN_POINT('Ctrl Pts',(104.963114479572,3.35981818063514,134.398744798986));
#45352=CARTESIAN_POINT('Ctrl Pts',(104.955357438687,3.45731872794115,134.302378667252));
#45353=CARTESIAN_POINT('Ctrl Pts',(104.947606247447,3.55474574932591,134.206085205967));
#45354=CARTESIAN_POINT('Ctrl Pts',(104.939855056207,3.64822277807761,134.105643212481));
#45355=CARTESIAN_POINT('Ctrl Pts',(104.932103864967,3.73738278102539,134.001414419208));
#45356=CARTESIAN_POINT('Ctrl Pts',(104.92435596819,3.82650488859355,133.897229925953));
#45357=CARTESIAN_POINT('Ctrl Pts',(104.916608071413,3.91131336612629,133.789262130538));
#45358=CARTESIAN_POINT('Ctrl Pts',(104.908860174636,3.99147922869732,133.677908360231));
#45359=CARTESIAN_POINT('Ctrl Pts',(104.901113898552,4.07162832229813,133.566577882733));
#45360=CARTESIAN_POINT('Ctrl Pts',(104.893367622468,4.14713650429643,133.451863156228));
#45361=CARTESIAN_POINT('Ctrl Pts',(104.885621346383,4.21771641244897,133.334192890002));
#45362=CARTESIAN_POINT('Ctrl Pts',(104.877875013118,4.28829684160625,133.216521755161));
#45363=CARTESIAN_POINT('Ctrl Pts',(104.870128679853,4.35394872322201,133.095895372343));
#45364=CARTESIAN_POINT('Ctrl Pts',(104.862382346587,4.41442941261409,132.972769256072));
#45365=CARTESIAN_POINT('Ctrl Pts',(104.854634278584,4.4749236462372,132.849615566561));
#45366=CARTESIAN_POINT('Ctrl Pts',(104.846886210581,4.53024421090618,132.723961380512));
#45367=CARTESIAN_POINT('Ctrl Pts',(104.839138142578,4.5801957582119,132.596284131268));
#45368=CARTESIAN_POINT('Ctrl Pts',(104.831381839837,4.63020039461657,132.468471185124));
#45369=CARTESIAN_POINT('Ctrl Pts',(104.823625537095,4.6748244721258,132.338631245329));
#45370=CARTESIAN_POINT('Ctrl Pts',(104.815869234353,4.71392171319714,132.207259453672));
#45371=CARTESIAN_POINT('Ctrl Pts',(104.808108791839,4.75303982164326,132.075817544935));
#45372=CARTESIAN_POINT('Ctrl Pts',(104.800348349325,4.78662512015525,131.942842534084));
#45373=CARTESIAN_POINT('Ctrl Pts',(104.79258790681,4.81458227832083,131.808840855191));
#45374=CARTESIAN_POINT('Ctrl Pts',(104.784815006545,4.84258431579862,131.674624064907));
#45375=CARTESIAN_POINT('Ctrl Pts',(104.777042106279,4.86494009474285,131.539377699109));
#45376=CARTESIAN_POINT('Ctrl Pts',(104.769269206014,4.88160597095454,131.403615327052));
#45377=CARTESIAN_POINT('Ctrl Pts',(104.761778870252,4.89766600058711,131.272788259184));
#45378=CARTESIAN_POINT('Ctrl Pts',(104.75428853449,4.90844260471322,131.141482356961));
#45379=CARTESIAN_POINT('Ctrl Pts',(104.746798198728,4.91394253530475,131.01015620115));
#45380=CARTESIAN_POINT('Ctrl Pts',(104.739023864609,4.91965099743632,130.873850774226));
#45381=CARTESIAN_POINT('Ctrl Pts',(104.73124953049,4.91969283987632,130.737091752946));
#45382=CARTESIAN_POINT('Ctrl Pts',(104.723475196371,4.91401860855399,130.600389596867));
#45383=CARTESIAN_POINT('Ctrl Pts',(104.715710443424,4.90835137021465,130.463855913978));
#45384=CARTESIAN_POINT('Ctrl Pts',(104.707945690477,4.89698209072647,130.327379343729));
#45385=CARTESIAN_POINT('Ctrl Pts',(104.700180937529,4.87991319436435,130.191473778118));
#45386=CARTESIAN_POINT('Ctrl Pts',(104.692423896644,4.86286125107073,130.055703195831));
#45387=CARTESIAN_POINT('Ctrl Pts',(104.68466685576,4.84012100483368,129.920502874975));
#45388=CARTESIAN_POINT('Ctrl Pts',(104.676909814875,4.811746876377,129.786384655091));
#45389=CARTESIAN_POINT('Ctrl Pts',(104.669158623634,4.78339414507133,129.652367574801));
#45390=CARTESIAN_POINT('Ctrl Pts',(104.661407432394,4.74941606863021,129.519431352194));
#45391=CARTESIAN_POINT('Ctrl Pts',(104.653656241154,4.70991859238451,129.388080307878));
#45392=CARTESIAN_POINT('Ctrl Pts',(104.645908344377,4.67043790361981,129.256785091259));
#45393=CARTESIAN_POINT('Ctrl Pts',(104.6381604476,4.62544259319947,129.127074086529));
#45394=CARTESIAN_POINT('Ctrl Pts',(104.630412550823,4.57508911941733,128.999438843115));
#45395=CARTESIAN_POINT('Ctrl Pts',(104.622666274739,4.52474617849641,128.871830298242));
#45396=CARTESIAN_POINT('Ctrl Pts',(104.614919998655,4.46904744695803,128.746297014485));
#45397=CARTESIAN_POINT('Ctrl Pts',(104.607173722571,4.40819828375385,128.623312485679));
#45398=CARTESIAN_POINT('Ctrl Pts',(104.599427389305,4.34734867137498,128.500327049028));
#45399=CARTESIAN_POINT('Ctrl Pts',(104.59168105604,4.28134872484304,128.379890755291));
#45400=CARTESIAN_POINT('Ctrl Pts',(104.583934722775,4.21045052605094,128.262453965036));
#45401=CARTESIAN_POINT('Ctrl Pts',(104.576186654772,4.13953645009884,128.144990875626));
#45402=CARTESIAN_POINT('Ctrl Pts',(104.568438586769,4.0637221411481,128.030528960977));
#45403=CARTESIAN_POINT('Ctrl Pts',(104.560690518766,3.98330368680443,127.919490637621));
#45404=CARTESIAN_POINT('Ctrl Pts',(104.552934216024,3.90279976277044,127.808334301413));
#45405=CARTESIAN_POINT('Ctrl Pts',(104.545177913282,3.81768214806065,127.700609142209));
#45406=CARTESIAN_POINT('Ctrl Pts',(104.53742161054,3.72828835289985,127.596705863679));
#45407=CARTESIAN_POINT('Ctrl Pts',(104.529661168026,3.63884684557892,127.492747128842));
#45408=CARTESIAN_POINT('Ctrl Pts',(104.521900725512,3.54512487711405,127.392614624558));
#45409=CARTESIAN_POINT('Ctrl Pts',(104.514140282998,3.44749699641711,127.296662294991));
#45410=CARTESIAN_POINT('Ctrl Pts',(104.506367382732,3.34971239477908,127.200555934226));
#45411=CARTESIAN_POINT('Ctrl Pts',(104.498594482467,3.24800964144666,127.108643419962));
#45412=CARTESIAN_POINT('Ctrl Pts',(104.490821582201,3.14279722602412,127.021239068026));
#45413=CARTESIAN_POINT('Ctrl Pts',(104.483331246439,3.04140954691542,126.93701208444));
#45414=CARTESIAN_POINT('Ctrl Pts',(104.475840910677,2.93676319036127,126.856971374702));
#45415=CARTESIAN_POINT('Ctrl Pts',(104.468350574915,2.82924762295476,126.781359132293));
#45416=CARTESIAN_POINT('Ctrl Pts',(104.460576240796,2.71765557013216,126.702880028732));
#45417=CARTESIAN_POINT('Ctrl Pts',(104.452801906677,2.60261894917284,126.628923233976));
#45418=CARTESIAN_POINT('Ctrl Pts',(104.445027572558,2.48454049302679,126.559806270993));
#45419=CARTESIAN_POINT('Ctrl Pts',(104.437262819611,2.36660755802506,126.490774488491));
#45420=CARTESIAN_POINT('Ctrl Pts',(104.429498066664,2.24564058098356,126.426570865473));
#45421=CARTESIAN_POINT('Ctrl Pts',(104.421733313716,2.12207322417457,126.367471133508));
#45422=CARTESIAN_POINT('Ctrl Pts',(104.413976272831,1.99862859620628,126.30843010023));
#45423=CARTESIAN_POINT('Ctrl Pts',(104.406219231946,1.87258907864562,126.254483037553));
#45424=CARTESIAN_POINT('Ctrl Pts',(104.398462191061,1.74441471232456,126.205860821554));
#45425=CARTESIAN_POINT('Ctrl Pts',(104.390710999821,1.61633700329036,126.157275271946));
#45426=CARTESIAN_POINT('Ctrl Pts',(104.382959808581,1.48612801398442,126.114006714498));
#45427=CARTESIAN_POINT('Ctrl Pts',(104.375208617341,1.35426930965596,126.07623861201));
#45428=CARTESIAN_POINT('Ctrl Pts',(104.367460720564,1.2224666487942,126.038486561973));
#45429=CARTESIAN_POINT('Ctrl Pts',(104.359712823787,1.08901604255386,126.006230424538));
#45430=CARTESIAN_POINT('Ctrl Pts',(104.35196492701,0.954415614920289,125.979604261386));
#45431=CARTESIAN_POINT('Ctrl Pts',(104.344218650926,0.819843342794435,125.952983667854));
#45432=CARTESIAN_POINT('Ctrl Pts',(104.336472374842,0.684122110968675,125.931990781976));
#45433=CARTESIAN_POINT('Ctrl Pts',(104.328726098757,0.547761284745379,125.916708764433));
#45434=CARTESIAN_POINT('Ctrl Pts',(104.320979765492,0.411399451937533,125.901426634082));
#45435=CARTESIAN_POINT('Ctrl Pts',(104.313233432227,0.274398403843937,125.89185549973));
#45436=CARTESIAN_POINT('Ctrl Pts',(104.305487098961,0.137273297987871,125.888026708629));
#45437=CARTESIAN_POINT('Ctrl Pts',(104.297739030958,0.000117483915200584,
125.884197060098));
#45438=CARTESIAN_POINT('Ctrl Pts',(104.289990962955,-0.137162052464567,
125.886112324635));
#45439=CARTESIAN_POINT('Ctrl Pts',(104.282242894952,-0.274049877575846,
125.893751721808));
#45440=CARTESIAN_POINT('Ctrl Pts',(104.274486592211,-0.411083188696826,
125.901399238222));
#45441=CARTESIAN_POINT('Ctrl Pts',(104.266730289469,-0.547723565934234,
125.914783018251));
#45442=CARTESIAN_POINT('Ctrl Pts',(104.258973986727,-0.683459866704315,
125.93383028986));
#45443=CARTESIAN_POINT('Ctrl Pts',(104.251213544213,-0.819268614025057,
125.952887727571));
#45444=CARTESIAN_POINT('Ctrl Pts',(104.243453101698,-0.954171939020441,
125.977614609547));
#45445=CARTESIAN_POINT('Ctrl Pts',(104.235692659184,-1.0876696056067,126.007887132646));
#45446=CARTESIAN_POINT('Ctrl Pts',(104.227919758919,-1.22138157449873,126.038208251887));
#45447=CARTESIAN_POINT('Ctrl Pts',(104.220146858653,-1.3536829982512,126.074092699589));
#45448=CARTESIAN_POINT('Ctrl Pts',(104.212373958388,-1.48408863544707,126.115366697263));
#45449=CARTESIAN_POINT('Ctrl Pts',(104.204883622626,-1.60975369925739,126.155140281158));
#45450=CARTESIAN_POINT('Ctrl Pts',(104.197393286864,-1.73365812707501,126.199918265949));
#45451=CARTESIAN_POINT('Ctrl Pts',(104.189902951102,-1.85538763845819,126.249503893853));
#45452=CARTESIAN_POINT('Ctrl Pts',(104.182128258453,-1.98173838792778,126.300971949358));
#45453=CARTESIAN_POINT('Ctrl Pts',(104.174353565804,-2.10614608482347,126.357782929116));
#45454=CARTESIAN_POINT('Ctrl Pts',(104.166578873156,-2.22812583433463,126.419769607122));
#45455=CARTESIAN_POINT('Ctrl Pts',(104.158813843926,-2.3499539712278,126.481679239859));
#45456=CARTESIAN_POINT('Ctrl Pts',(104.151048814697,-2.4693598201718,126.548751595043));
#45457=CARTESIAN_POINT('Ctrl Pts',(104.143283785468,-2.58587694680721,126.620770833843));
#45458=CARTESIAN_POINT('Ctrl Pts',(104.135526550199,-2.70227712219174,126.692717785072));
#45459=CARTESIAN_POINT('Ctrl Pts',(104.12776931493,-2.81579401519334,126.769601533965));
#45460=CARTESIAN_POINT('Ctrl Pts',(104.120012079662,-2.92598468896782,126.851159805259));
#45461=CARTESIAN_POINT('Ctrl Pts',(104.11210165736,-3.03835136769242,126.934328659336));
#45462=CARTESIAN_POINT('Ctrl Pts',(104.104191235059,-3.14725870223143,127.022358424044));
#45463=CARTESIAN_POINT('Ctrl Pts',(104.096280812758,-3.25226629346806,127.114923395052));
#45464=CARTESIAN_POINT('Ctrl Pts',(104.088533257867,-3.35511188704357,127.205582549076));
#45465=CARTESIAN_POINT('Ctrl Pts',(104.080785702977,-3.45421645976481,127.30059169383));
#45466=CARTESIAN_POINT('Ctrl Pts',(104.073038148086,-3.54919873451535,127.399603444813));
#45467=CARTESIAN_POINT('Ctrl Pts',(104.065292295697,-3.64416013719751,127.498593438262));
#45468=CARTESIAN_POINT('Ctrl Pts',(104.057546443309,-3.73500077404149,127.601584005824));
#45469=CARTESIAN_POINT('Ctrl Pts',(104.04980059092,-3.82137620686658,127.708190895459));
#45470=CARTESIAN_POINT('Ctrl Pts',(104.042054763247,-3.90775136408046,127.814797444927));
#45471=CARTESIAN_POINT('Ctrl Pts',(104.034308935575,-3.98966110018621,127.925019989339));
#45472=CARTESIAN_POINT('Ctrl Pts',(104.026563107902,-4.06680151471503,128.038441511299));
#45473=CARTESIAN_POINT('Ctrl Pts',(104.018529677612,-4.14680615318612,128.156074374886));
#45474=CARTESIAN_POINT('Ctrl Pts',(104.010496247323,-4.2216801926709,128.277147994697));
#45475=CARTESIAN_POINT('Ctrl Pts',(104.002462817033,-4.29113456301106,128.401165406054));
#45476=CARTESIAN_POINT('Ctrl Pts',(103.994708493788,-4.35817586653774,128.520874056161));
#45477=CARTESIAN_POINT('Ctrl Pts',(103.986954170543,-4.42016766575189,128.643324982946));
#45478=CARTESIAN_POINT('Ctrl Pts',(103.979199847298,-4.47689781571174,128.768048016275));
#45479=CARTESIAN_POINT('Ctrl Pts',(103.971441345739,-4.53365853396177,128.89283825496));
#45480=CARTESIAN_POINT('Ctrl Pts',(103.963682844179,-4.58515180761465,129.019902677904));
#45481=CARTESIAN_POINT('Ctrl Pts',(103.95592434262,-4.63121437594359,129.148753035271));
#45482=CARTESIAN_POINT('Ctrl Pts',(103.948156950967,-4.67732972515105,129.277751036056));
#45483=CARTESIAN_POINT('Ctrl Pts',(103.940389559314,-4.71800183383925,129.408538683573));
#45484=CARTESIAN_POINT('Ctrl Pts',(103.932622167662,-4.75311776225026,129.54061436112));
#45485=CARTESIAN_POINT('Ctrl Pts',(103.93180209325,-4.75682527123209,129.554558795539));
#45486=CARTESIAN_POINT('Ctrl Pts',(103.930982018839,-4.76047089301986,129.568517579997));
#45487=CARTESIAN_POINT('Ctrl Pts',(103.930161944428,-4.76405452823404,129.582490119308));
#45488=CARTESIAN_POINT('Origin',(213.235140564004,0.,130.804360617566));
#45489=CARTESIAN_POINT('',(101.834907966042,-4.76405452823403,129.582490119308));
#45490=CARTESIAN_POINT('',(102.179855052771,-4.76405452823403,129.582490119308));
#45491=CARTESIAN_POINT('',(213.235140564004,-4.76405452823405,129.582490119308));
#45492=CARTESIAN_POINT('',(103.514859436023,-4.91824999784073,130.804214879153));
#45493=CARTESIAN_POINT('Ctrl Pts',(103.514859435991,-4.91824999784074,130.80421487972));
#45494=CARTESIAN_POINT('Ctrl Pts',(103.506762540919,-4.91825425810335,130.947986981988));
#45495=CARTESIAN_POINT('Ctrl Pts',(103.498665645847,-4.91195000582023,131.091643240942));
#45496=CARTESIAN_POINT('Ctrl Pts',(103.490568750775,-4.89939349982138,131.234623788669));
#45497=CARTESIAN_POINT('Ctrl Pts',(103.482461820269,-4.88682143106815,131.377781549002));
#45498=CARTESIAN_POINT('Ctrl Pts',(103.474354889763,-4.86798167668567,131.520261592361));
#45499=CARTESIAN_POINT('Ctrl Pts',(103.466247959256,-4.84298193936281,131.661512294637));
#45500=CARTESIAN_POINT('Ctrl Pts',(103.458122472384,-4.81792497886648,131.803086312848));
#45501=CARTESIAN_POINT('Ctrl Pts',(103.449996985511,-4.78667990419565,131.943425031803));
#45502=CARTESIAN_POINT('Ctrl Pts',(103.441871498638,-4.74940528021162,132.081988320302));
#45503=CARTESIAN_POINT('Ctrl Pts',(103.433736303412,-4.71208612040582,132.220717164593));
#45504=CARTESIAN_POINT('Ctrl Pts',(103.425601108185,-4.66872313664903,132.357666024962));
#45505=CARTESIAN_POINT('Ctrl Pts',(103.417465912958,-4.61952380494145,132.492312891204));
#45506=CARTESIAN_POINT('Ctrl Pts',(103.409312148305,-4.57021217065619,132.627267102883));
#45507=CARTESIAN_POINT('Ctrl Pts',(103.401158383651,-4.51503767883914,132.759908502117));
#45508=CARTESIAN_POINT('Ctrl Pts',(103.393004618998,-4.4542554661105,132.889736196479));
#45509=CARTESIAN_POINT('Ctrl Pts',(103.38671943794,-4.40740260386084,132.989811511395));
#45510=CARTESIAN_POINT('Ctrl Pts',(103.380434256881,-4.35721869783343,133.088215438985));
#45511=CARTESIAN_POINT('Ctrl Pts',(103.374149075823,-4.30383826976654,133.184730170848));
#45512=CARTESIAN_POINT('Ctrl Pts',(103.366374741704,-4.23781037345589,133.304112216641));
#45513=CARTESIAN_POINT('Ctrl Pts',(103.358600407585,-4.16670690980976,133.420934000183));
#45514=CARTESIAN_POINT('Ctrl Pts',(103.350826073466,-4.09075117267524,133.534733834867));
#45515=CARTESIAN_POINT('Ctrl Pts',(103.343061320519,-4.01488904419838,133.648393421426));
#45516=CARTESIAN_POINT('Ctrl Pts',(103.335296567572,-3.9341867555989,133.759038147273));
#45517=CARTESIAN_POINT('Ctrl Pts',(103.327531814624,-3.84891369327921,133.86623038034));
#45518=CARTESIAN_POINT('Ctrl Pts',(103.319774773739,-3.76372532536722,133.973316148569));
#45519=CARTESIAN_POINT('Ctrl Pts',(103.312017732854,-3.67397545987754,134.076955944029));
#45520=CARTESIAN_POINT('Ctrl Pts',(103.304260691969,-3.57997682350484,134.176740935037));
#45521=CARTESIAN_POINT('Ctrl Pts',(103.296509500729,-3.48604907223497,134.276450677408));
#45522=CARTESIAN_POINT('Ctrl Pts',(103.288758309489,-3.38787919450686,134.372311117979));
#45523=CARTESIAN_POINT('Ctrl Pts',(103.281007118249,-3.28582001078081,134.463946648697));
#45524=CARTESIAN_POINT('Ctrl Pts',(103.273259221472,-3.18380420493035,134.55554323187));
#45525=CARTESIAN_POINT('Ctrl Pts',(103.265511324695,-3.07790267119138,134.642918216047));
#45526=CARTESIAN_POINT('Ctrl Pts',(103.257763427918,-2.96850472767904,134.725733176282));
#45527=CARTESIAN_POINT('Ctrl Pts',(103.250017151834,-2.85912966785807,134.808530813412));
#45528=CARTESIAN_POINT('Ctrl Pts',(103.242270875749,-2.74625996452902,134.886770088052));
#45529=CARTESIAN_POINT('Ctrl Pts',(103.234524599665,-2.63031730761799,134.960153432872));
#45530=CARTESIAN_POINT('Ctrl Pts',(103.2267782664,-2.51437379484491,135.03353731939));
#45531=CARTESIAN_POINT('Ctrl Pts',(103.219031933135,-2.39535761358128,135.10206499547));
#45532=CARTESIAN_POINT('Ctrl Pts',(103.211285599869,-2.27371832437165,135.165482955212));
#45533=CARTESIAN_POINT('Ctrl Pts',(103.203537531866,-2.15205179488608,135.228915116967));
#45534=CARTESIAN_POINT('Ctrl Pts',(103.195789463863,-2.02776133515433,135.287235104679));
#45535=CARTESIAN_POINT('Ctrl Pts',(103.18804139586,-1.90131955320651,135.34023616911));
#45536=CARTESIAN_POINT('Ctrl Pts',(103.180285093118,-1.77474338742851,135.393293563703));
#45537=CARTESIAN_POINT('Ctrl Pts',(103.172528790377,-1.64601169314672,135.441020591127));
#45538=CARTESIAN_POINT('Ctrl Pts',(103.164772487635,-1.51561595930304,135.483259133927));
#45539=CARTESIAN_POINT('Ctrl Pts',(103.15701204512,-1.38515062932988,135.525520220709));
#45540=CARTESIAN_POINT('Ctrl Pts',(103.149251602606,-1.25301986655555,135.562286881093));
#45541=CARTESIAN_POINT('Ctrl Pts',(103.141491160092,-1.11972767154515,135.593451659097));
#45542=CARTESIAN_POINT('Ctrl Pts',(103.133718259827,-0.986221504070382,
135.62466646557));
#45543=CARTESIAN_POINT('Ctrl Pts',(103.125945359561,-0.851550562937025,
135.650261346466));
#45544=CARTESIAN_POINT('Ctrl Pts',(103.118172459296,-0.716227222165132,
135.670180345909));
#45545=CARTESIAN_POINT('Ctrl Pts',(103.110682123534,-0.585823225691153,
135.689375239548));
#45546=CARTESIAN_POINT('Ctrl Pts',(103.103191787772,-0.454813745110329,
135.703299719881));
#45547=CARTESIAN_POINT('Ctrl Pts',(103.09570145201,-0.323657391158878,135.711949532262));
#45548=CARTESIAN_POINT('Ctrl Pts',(103.087927117891,-0.187528204181233,
135.720927304908));
#45549=CARTESIAN_POINT('Ctrl Pts',(103.080152783772,-0.0508095702230775,
135.724250974724));
#45550=CARTESIAN_POINT('Ctrl Pts',(103.072378449653,0.0859893849184933,
135.721858852256));
#45551=CARTESIAN_POINT('Ctrl Pts',(103.064613696706,0.222619747573554,135.719469677866));
#45552=CARTESIAN_POINT('Ctrl Pts',(103.056848943759,0.359329847301274,135.711378733828));
#45553=CARTESIAN_POINT('Ctrl Pts',(103.049084190812,0.495605881915482,135.697576111728));
#45554=CARTESIAN_POINT('Ctrl Pts',(103.041327149927,0.631746565251048,135.683787198587));
#45555=CARTESIAN_POINT('Ctrl Pts',(103.033570109042,0.767453654962441,135.664297935892));
#45556=CARTESIAN_POINT('Ctrl Pts',(103.025813068157,0.902214152959024,135.639150445956));
#45557=CARTESIAN_POINT('Ctrl Pts',(103.018061876916,1.03687302701615,135.614021919937));
#45558=CARTESIAN_POINT('Ctrl Pts',(103.010310685676,1.17058634742248,135.58324373114));
#45559=CARTESIAN_POINT('Ctrl Pts',(103.002559494436,1.30284739640677,135.54690969208));
#45560=CARTESIAN_POINT('Ctrl Pts',(102.994811597659,1.43505223091689,135.510591095957));
#45561=CARTESIAN_POINT('Ctrl Pts',(102.987063700882,1.56580564546732,135.468721449535));
#45562=CARTESIAN_POINT('Ctrl Pts',(102.979315804105,1.69461247761578,135.421445370222));
#45563=CARTESIAN_POINT('Ctrl Pts',(102.971569528021,1.82339236615171,135.374179180046));
#45564=CARTESIAN_POINT('Ctrl Pts',(102.963823251937,1.95022611540291,135.321508941043));
#45565=CARTESIAN_POINT('Ctrl Pts',(102.956076975853,2.07463543984101,135.26362859048));
#45566=CARTESIAN_POINT('Ctrl Pts',(102.948330642587,2.19904568264041,135.205747812657));
#45567=CARTESIAN_POINT('Ctrl Pts',(102.940584309322,2.32103111043598,135.14265701145));
#45568=CARTESIAN_POINT('Ctrl Pts',(102.932837976057,2.44013544307972,135.074597388745));
#45569=CARTESIAN_POINT('Ctrl Pts',(102.925089908054,2.55926644831302,135.006522524559));
#45570=CARTESIAN_POINT('Ctrl Pts',(102.917341840051,2.67551473513075,134.933476818601));
#45571=CARTESIAN_POINT('Ctrl Pts',(102.909593772048,2.78845090335968,134.85574613638));
#45572=CARTESIAN_POINT('Ctrl Pts',(102.901837469306,2.90150710149216,134.777932841064));
#45573=CARTESIAN_POINT('Ctrl Pts',(102.894081166564,3.01124382656967,134.695424844914));
#45574=CARTESIAN_POINT('Ctrl Pts',(102.886324863822,3.11726238812015,134.60855018515));
#45575=CARTESIAN_POINT('Ctrl Pts',(102.878564421308,3.22333753496915,134.521629157763));
#45576=CARTESIAN_POINT('Ctrl Pts',(102.870803978794,3.32569027238873,134.430337082917));
#45577=CARTESIAN_POINT('Ctrl Pts',(102.86304353628,3.42395777000255,134.335039907977));
#45578=CARTESIAN_POINT('Ctrl Pts',(102.855270636014,3.52238301532733,134.239589753553));
#45579=CARTESIAN_POINT('Ctrl Pts',(102.847497735749,3.61670964671316,134.140121935012));
#45580=CARTESIAN_POINT('Ctrl Pts',(102.839724835483,3.70661363622307,134.037037281612));
#45581=CARTESIAN_POINT('Ctrl Pts',(102.832234499721,3.7932493892609,133.937700015016));
#45582=CARTESIAN_POINT('Ctrl Pts',(102.824744163959,3.87577827326778,133.835004550364));
#45583=CARTESIAN_POINT('Ctrl Pts',(102.817253828197,3.95394881838397,133.729334430115));
#45584=CARTESIAN_POINT('Ctrl Pts',(102.809479494078,4.03508322347669,133.619657795142));
#45585=CARTESIAN_POINT('Ctrl Pts',(102.801705159959,4.11177928221597,133.50642906104));
#45586=CARTESIAN_POINT('Ctrl Pts',(102.79393082584,4.18370989859002,133.390043225107));
#45587=CARTESIAN_POINT('Ctrl Pts',(102.786166072892,4.25555186690805,133.273800824315));
#45588=CARTESIAN_POINT('Ctrl Pts',(102.778401319945,4.32263987477437,133.154409392698));
#45589=CARTESIAN_POINT('Ctrl Pts',(102.770636566998,4.38468786332751,133.032295850846));
#45590=CARTESIAN_POINT('Ctrl Pts',(102.762879526113,4.44667422494365,132.910303593885));
#45591=CARTESIAN_POINT('Ctrl Pts',(102.755122485228,4.50363035309214,132.785594953347));
#45592=CARTESIAN_POINT('Ctrl Pts',(102.747365444343,4.5553143984703,132.658624297194));
#45593=CARTESIAN_POINT('Ctrl Pts',(102.739614253103,4.60695946850756,132.531749390602));
#45594=CARTESIAN_POINT('Ctrl Pts',(102.731863061863,4.65334022239725,132.402616224343));
#45595=CARTESIAN_POINT('Ctrl Pts',(102.724111870623,4.69426169393441,132.271701822385));
#45596=CARTESIAN_POINT('Ctrl Pts',(102.716363973846,4.73516577275474,132.14084306254));
#45597=CARTESIAN_POINT('Ctrl Pts',(102.708616077069,4.77061506780431,132.008204945136));
#45598=CARTESIAN_POINT('Ctrl Pts',(102.700868180292,4.80046360240816,131.874282233599));
#45599=CARTESIAN_POINT('Ctrl Pts',(102.693121904208,4.83030589334202,131.740387535806));
#45600=CARTESIAN_POINT('Ctrl Pts',(102.685375628123,4.85454966912681,131.605209159719));
#45601=CARTESIAN_POINT('Ctrl Pts',(102.677629352039,4.87309956966692,131.469254328329));
#45602=CARTESIAN_POINT('Ctrl Pts',(102.669883018774,4.89164960713816,131.333298493351));
#45603=CARTESIAN_POINT('Ctrl Pts',(102.662136685509,4.90450563264091,131.196566579008));
#45604=CARTESIAN_POINT('Ctrl Pts',(102.654390352243,4.91162394558918,131.059572842224));
#45605=CARTESIAN_POINT('Ctrl Pts',(102.64664228424,4.91874385263427,130.922548426643));
#45606=CARTESIAN_POINT('Ctrl Pts',(102.638894216237,4.92012346999734,130.78526246231));
#45607=CARTESIAN_POINT('Ctrl Pts',(102.631146148234,4.91577120314387,130.648230733042));
#45608=CARTESIAN_POINT('Ctrl Pts',(102.623389845493,4.9114143106494,130.511053364822));
#45609=CARTESIAN_POINT('Ctrl Pts',(102.615633542751,4.90131337711345,130.37413116282));
#45610=CARTESIAN_POINT('Ctrl Pts',(102.607877240009,4.88552888760048,130.237976868751));
#45611=CARTESIAN_POINT('Ctrl Pts',(102.600116797495,4.86973597343017,130.101749905037));
#45612=CARTESIAN_POINT('Ctrl Pts',(102.59235635498,4.84825352001566,129.966292051878));
#45613=CARTESIAN_POINT('Ctrl Pts',(102.584595912466,4.82119329055999,129.832106372237));
#45614=CARTESIAN_POINT('Ctrl Pts',(102.576823012201,4.79408962162168,129.697705285832));
#45615=CARTESIAN_POINT('Ctrl Pts',(102.569050111935,4.76139037712837,129.56458083382));
#45616=CARTESIAN_POINT('Ctrl Pts',(102.56127721167,4.72325764107054,129.433222288086));
#45617=CARTESIAN_POINT('Ctrl Pts',(102.553786875908,4.68651112601932,129.306638956363));
#45618=CARTESIAN_POINT('Ctrl Pts',(102.546296540146,4.64471940080725,129.181695661791));
#45619=CARTESIAN_POINT('Ctrl Pts',(102.538806204384,4.59806922496722,129.058811287152));
#45620=CARTESIAN_POINT('Ctrl Pts',(102.531031870265,4.54965029353087,128.931267714098));
#45621=CARTESIAN_POINT('Ctrl Pts',(102.523257536146,4.49584384588066,128.805538251188));
#45622=CARTESIAN_POINT('Ctrl Pts',(102.515483202027,4.43680540104545,128.682111599247));
#45623=CARTESIAN_POINT('Ctrl Pts',(102.50771844908,4.3778397158172,128.558837059625));
#45624=CARTESIAN_POINT('Ctrl Pts',(102.499953696133,4.31365503002414,128.437860033489));
#45625=CARTESIAN_POINT('Ctrl Pts',(102.492188943186,4.24445590224847,128.31965195127));
#45626=CARTESIAN_POINT('Ctrl Pts',(102.484431902301,4.17532550402208,128.201561274984));
#45627=CARTESIAN_POINT('Ctrl Pts',(102.476674861416,4.10119077130081,128.086234404903));
#45628=CARTESIAN_POINT('Ctrl Pts',(102.468917820531,4.02230325126411,127.974120412677));
#45629=CARTESIAN_POINT('Ctrl Pts',(102.46116662929,3.94347522092014,127.862090966485));
#45630=CARTESIAN_POINT('Ctrl Pts',(102.45341543805,3.85990176129532,127.753269894051));
#45631=CARTESIAN_POINT('Ctrl Pts',(102.44566424681,3.77187882216869,127.64807906907));
#45632=CARTESIAN_POINT('Ctrl Pts',(102.437916350033,3.68389329513897,127.542932952996));
#45633=CARTESIAN_POINT('Ctrl Pts',(102.430168453256,3.59146230033177,127.441414314772));
#45634=CARTESIAN_POINT('Ctrl Pts',(102.422420556479,3.49492319227238,127.343913400425));
#45635=CARTESIAN_POINT('Ctrl Pts',(102.414674280395,3.39840427811325,127.246432881169));
#45636=CARTESIAN_POINT('Ctrl Pts',(102.406928004311,3.29777923486006,127.152968691791));
#45637=CARTESIAN_POINT('Ctrl Pts',(102.399181728227,3.19342325911923,127.063875227858));
#45638=CARTESIAN_POINT('Ctrl Pts',(102.391435394961,3.08906651304643,126.974781106258));
#45639=CARTESIAN_POINT('Ctrl Pts',(102.383689061696,2.98097907687159,126.890058028336));
#45640=CARTESIAN_POINT('Ctrl Pts',(102.375942728431,2.86956998827437,126.810020729062));
#45641=CARTESIAN_POINT('Ctrl Pts',(102.368194660428,2.75813595038452,126.72996550599));
#45642=CARTESIAN_POINT('Ctrl Pts',(102.360446592425,2.64337909733524,126.654598377711));
#45643=CARTESIAN_POINT('Ctrl Pts',(102.352698524422,2.5257379160186,126.584191066223));
#45644=CARTESIAN_POINT('Ctrl Pts',(102.34494222168,2.40797170425388,126.513708925005));
#45645=CARTESIAN_POINT('Ctrl Pts',(102.337185918938,2.28731537656628,126.448197331769));
#45646=CARTESIAN_POINT('Ctrl Pts',(102.329429616196,2.16423301073741,126.387882548138));
#45647=CARTESIAN_POINT('Ctrl Pts',(102.321669173682,2.04108495214395,126.327535572692));
#45648=CARTESIAN_POINT('Ctrl Pts',(102.313908731168,1.91550863310748,126.27239109079));
#45649=CARTESIAN_POINT('Ctrl Pts',(102.306148288654,1.78798770548679,126.222626990703));
#45650=CARTESIAN_POINT('Ctrl Pts',(102.298375388389,1.66026206995221,126.172783004865));
#45651=CARTESIAN_POINT('Ctrl Pts',(102.290602488123,1.53058595782255,126.12833678729));
#45652=CARTESIAN_POINT('Ctrl Pts',(102.282829587858,1.39945861774678,126.08941643553));
#45653=CARTESIAN_POINT('Ctrl Pts',(102.275339252096,1.27309808676921,126.051910936591));
#45654=CARTESIAN_POINT('Ctrl Pts',(102.267848916333,1.14539030616624,126.019536595987));
#45655=CARTESIAN_POINT('Ctrl Pts',(102.260358580571,1.01678864197639,125.992362704012));
#45656=CARTESIAN_POINT('Ctrl Pts',(102.252584246452,0.883311006604902,125.964158505664));
#45657=CARTESIAN_POINT('Ctrl Pts',(102.244809912333,0.748447549364895,125.941467548134));
#45658=CARTESIAN_POINT('Ctrl Pts',(102.237035578214,0.612693489935831,125.924423143593));
#45659=CARTESIAN_POINT('Ctrl Pts',(102.229270825267,0.477106735251679,125.907399744756));
#45660=CARTESIAN_POINT('Ctrl Pts',(102.22150607232,0.340631946446295,125.896009101064));
#45661=CARTESIAN_POINT('Ctrl Pts',(102.213741319372,0.203776320201726,125.89033393125));
#45662=CARTESIAN_POINT('Ctrl Pts',(102.205984278487,0.0670566208946548,
125.884664398095));
#45663=CARTESIAN_POINT('Ctrl Pts',(102.198227237602,-0.0700427750091018,
125.884699058044));
#45664=CARTESIAN_POINT('Ctrl Pts',(102.190470196717,-0.207008083417117,
125.890469011527));
#45665=CARTESIAN_POINT('Ctrl Pts',(102.182719005477,-0.343870105220161,
125.896234613843));
#45666=CARTESIAN_POINT('Ctrl Pts',(102.174967814237,-0.480597851755358,
125.907726884596));
#45667=CARTESIAN_POINT('Ctrl Pts',(102.167216622997,-0.616676420648657,
125.924924865892));
#45668=CARTESIAN_POINT('Ctrl Pts',(102.15946872622,-0.752697152520348,125.942115537587));
#45669=CARTESIAN_POINT('Ctrl Pts',(102.151720829443,-0.888068868461948,
125.965007047609));
#45670=CARTESIAN_POINT('Ctrl Pts',(102.143972932666,-1.02228089507594,125.993526507553));
#45671=CARTESIAN_POINT('Ctrl Pts',(102.136226656582,-1.15646484742743,126.022040001841));
#45672=CARTESIAN_POINT('Ctrl Pts',(102.128480380498,-1.28948921077608,126.056179023231));
#45673=CARTESIAN_POINT('Ctrl Pts',(102.120734104414,-1.42085301916542,126.095819467653));
#45674=CARTESIAN_POINT('Ctrl Pts',(102.112987771148,-1.55221779725219,126.135460204691));
#45675=CARTESIAN_POINT('Ctrl Pts',(102.105241437883,-1.68192162162514,126.180602332847));
#45676=CARTESIAN_POINT('Ctrl Pts',(102.097495104617,-1.80947860198397,126.231071839076));
#45677=CARTESIAN_POINT('Ctrl Pts',(102.089747036614,-1.93706414784448,126.281552647601));
#45678=CARTESIAN_POINT('Ctrl Pts',(102.081998968611,-2.06250152953885,126.337363064376));
#45679=CARTESIAN_POINT('Ctrl Pts',(102.074250900608,-2.18532512678099,126.398281050336));
#45680=CARTESIAN_POINT('Ctrl Pts',(102.066494597867,-2.30827926240373,126.459263780656));
#45681=CARTESIAN_POINT('Ctrl Pts',(102.058738295125,-2.42861371348762,126.525364749951));
#45682=CARTESIAN_POINT('Ctrl Pts',(102.050981992383,-2.54588727434374,126.596315816375));
#45683=CARTESIAN_POINT('Ctrl Pts',(102.043221549869,-2.66322342763066,126.667304751518));
#45684=CARTESIAN_POINT('Ctrl Pts',(102.035461107355,-2.77749510983936,126.743148725783));
#45685=CARTESIAN_POINT('Ctrl Pts',(102.02770066484,-2.88829123288586,126.823536982119));
#45686=CARTESIAN_POINT('Ctrl Pts',(102.019927764575,-2.99926521570494,126.90405428482));
#45687=CARTESIAN_POINT('Ctrl Pts',(102.012154864309,-3.10675218345438,126.989130204315));
#45688=CARTESIAN_POINT('Ctrl Pts',(102.004381964044,-3.21037450794547,127.078413948432));
#45689=CARTESIAN_POINT('Ctrl Pts',(101.996891628282,-3.31022989993145,127.164452003557));
#45690=CARTESIAN_POINT('Ctrl Pts',(101.98940129252,-3.40649652441835,127.254397054364));
#45691=CARTESIAN_POINT('Ctrl Pts',(101.981910956758,-3.4988710301033,127.34790512426));
#45692=CARTESIAN_POINT('Ctrl Pts',(101.974243153007,-3.5934341583345,127.443628674158));
#45693=CARTESIAN_POINT('Ctrl Pts',(101.966575349257,-3.68423567913244,127.543407681893));
#45694=CARTESIAN_POINT('Ctrl Pts',(101.958907545506,-3.77090036107563,127.646910138249));
#45695=CARTESIAN_POINT('Ctrl Pts',(101.951248733512,-3.85746341447274,127.750291221008));
#45696=CARTESIAN_POINT('Ctrl Pts',(101.943589921519,-3.93989901778072,127.857386766542));
#45697=CARTESIAN_POINT('Ctrl Pts',(101.935931109525,-4.01786747906985,127.967826820282));
#45698=CARTESIAN_POINT('Ctrl Pts',(101.928279510985,-4.09576250574849,128.078162856036));
#45699=CARTESIAN_POINT('Ctrl Pts',(101.920627912444,-4.16919852661075,128.191836809296));
#45700=CARTESIAN_POINT('Ctrl Pts',(101.912976313904,-4.23787535416553,128.308444844737));
#45701=CARTESIAN_POINT('Ctrl Pts',(101.905330520193,-4.30650008054961,128.424964416349));
#45702=CARTESIAN_POINT('Ctrl Pts',(101.897684726482,-4.3703725950023,128.544413295145));
#45703=CARTESIAN_POINT('Ctrl Pts',(101.890038932771,-4.42923573631129,128.666358312917));
#45704=CARTESIAN_POINT('Ctrl Pts',(101.882396487143,-4.48807310152065,128.788249931111));
#45705=CARTESIAN_POINT('Ctrl Pts',(101.874754041516,-4.54190528299562,128.912635151929));
#45706=CARTESIAN_POINT('Ctrl Pts',(101.867111595889,-4.59052103767788,129.039056206101));
#45707=CARTESIAN_POINT('Ctrl Pts',(101.8594699867,-4.63913147153866,129.165463423938));
#45708=CARTESIAN_POINT('Ctrl Pts',(101.851828377512,-4.68252646635379,129.29390565779));
#45709=CARTESIAN_POINT('Ctrl Pts',(101.844186768323,-4.7205430662157,129.42390553952));
#45710=CARTESIAN_POINT('Ctrl Pts',(101.841093834229,-4.73593024906338,129.476522868729));
#45711=CARTESIAN_POINT('Ctrl Pts',(101.838000900136,-4.75043689666253,129.529395180487));
#45712=CARTESIAN_POINT('Ctrl Pts',(101.834907966042,-4.76405452823403,129.582490119308));
#45713=CARTESIAN_POINT('Ctrl Pts',(103.584579145176,-4.76405452823405,129.582490119308));
#45714=CARTESIAN_POINT('Ctrl Pts',(103.576426818607,-4.79981914816621,129.72193582962));
#45715=CARTESIAN_POINT('Ctrl Pts',(103.568274492038,-4.82949477661317,129.863099609191));
#45716=CARTESIAN_POINT('Ctrl Pts',(103.56012216547,-4.85292737657309,130.005437004066));
#45717=CARTESIAN_POINT('Ctrl Pts',(103.551985756864,-4.87631422281494,130.147496475662));
#45718=CARTESIAN_POINT('Ctrl Pts',(103.543849348258,-4.893482295562,130.290724669727));
#45719=CARTESIAN_POINT('Ctrl Pts',(103.535712939652,-4.90432814903514,130.434565445773));
#45720=CARTESIAN_POINT('Ctrl Pts',(103.528761771776,-4.91359407358562,130.557452757631));
#45721=CARTESIAN_POINT('Ctrl Pts',(103.521810603899,-4.91824634039976,130.680786823101));
#45722=CARTESIAN_POINT('Ctrl Pts',(103.514859436023,-4.91824999784073,130.804214879153));
#45723=CARTESIAN_POINT('',(103.860140563968,-4.91824815621127,130.800101929457));
#45724=CARTESIAN_POINT('Ctrl Pts',(103.930161944428,-4.76405452823404,129.582490119308));
#45725=CARTESIAN_POINT('Ctrl Pts',(103.923926405382,-4.79130314982063,129.688732081319));
#45726=CARTESIAN_POINT('Ctrl Pts',(103.917690866335,-4.81496624846374,129.795769395495));
#45727=CARTESIAN_POINT('Ctrl Pts',(103.911455327289,-4.8350123008557,129.903339467385));
#45728=CARTESIAN_POINT('Ctrl Pts',(103.899799266646,-4.87248428212411,130.104419642177));
#45729=CARTESIAN_POINT('Ctrl Pts',(103.888143206003,-4.89742086526062,130.3079032426));
#45730=CARTESIAN_POINT('Ctrl Pts',(103.876487145359,-4.9095839965138,130.512524972595));
#45731=CARTESIAN_POINT('Ctrl Pts',(103.871038284909,-4.91526989733962,130.608179523988));
#45732=CARTESIAN_POINT('Ctrl Pts',(103.865589424458,-4.91816501337355,130.70408244416));
#45733=CARTESIAN_POINT('Ctrl Pts',(103.860140564008,-4.91824815621066,130.800101928748));
#45734=CARTESIAN_POINT('Ctrl Pts',(103.860140563968,-4.91824815621127,130.800101929457));
#45735=CARTESIAN_POINT('Ctrl Pts',(103.85249393019,-4.91836483431793,130.934850440796));
#45736=CARTESIAN_POINT('Ctrl Pts',(103.844847296412,-4.91293966118262,131.069789198067));
#45737=CARTESIAN_POINT('Ctrl Pts',(103.837200662635,-4.90195245746252,131.204417072678));
#45738=CARTESIAN_POINT('Ctrl Pts',(103.829560842582,-4.89097504416677,131.338924983735));
#45739=CARTESIAN_POINT('Ctrl Pts',(103.82192102253,-4.87444549097799,131.473122163232));
#45740=CARTESIAN_POINT('Ctrl Pts',(103.814281202478,-4.85239567383066,131.606507291865));
#45741=CARTESIAN_POINT('Ctrl Pts',(103.806645871143,-4.83035881188223,131.739814051102));
#45742=CARTESIAN_POINT('Ctrl Pts',(103.799010539807,-4.80280820171784,131.872309311373));
#45743=CARTESIAN_POINT('Ctrl Pts',(103.791375208472,-4.7698275283597,132.003497145323));
#45744=CARTESIAN_POINT('Ctrl Pts',(103.783742189454,-4.73685684301134,132.134645249783));
#45745=CARTESIAN_POINT('Ctrl Pts',(103.776109170435,-4.69845946167205,132.264486324024));
#45746=CARTESIAN_POINT('Ctrl Pts',(103.768476151417,-4.65477002326167,132.392535385356));
#45747=CARTESIAN_POINT('Ctrl Pts',(103.76084367754,-4.61108370510527,132.520575301557));
#45748=CARTESIAN_POINT('Ctrl Pts',(103.753211203664,-4.56210621177099,132.646823077398));
#45749=CARTESIAN_POINT('Ctrl Pts',(103.745578729788,-4.50802164934403,132.770810177444));
#45750=CARTESIAN_POINT('Ctrl Pts',(103.737945034529,-4.45392843206285,132.894817118462));
#45751=CARTESIAN_POINT('Ctrl Pts',(103.73031133927,-4.39472668245777,133.016562294646));
#45752=CARTESIAN_POINT('Ctrl Pts',(103.722677644011,-4.33064787817129,133.135598918939));
#45753=CARTESIAN_POINT('Ctrl Pts',(103.715036335704,-4.2665051684046,133.25475425788));
#45754=CARTESIAN_POINT('Ctrl Pts',(103.707395027398,-4.19747588163011,133.371195294228));
#45755=CARTESIAN_POINT('Ctrl Pts',(103.699753719092,-4.12383670458569,133.484501266191));
#45756=CARTESIAN_POINT('Ctrl Pts',(103.6921085634,-4.05016045033656,133.597864287525));
#45757=CARTESIAN_POINT('Ctrl Pts',(103.684463407707,-3.97186991796053,133.70808877289));
#45758=CARTESIAN_POINT('Ctrl Pts',(103.676818252015,-3.88928324582296,133.814785653381));
#45759=CARTESIAN_POINT('Ctrl Pts',(103.669161105421,-3.80656704216425,133.921649880598));
#45760=CARTESIAN_POINT('Ctrl Pts',(103.661503958827,-3.71954149868936,134.024975142375));
#45761=CARTESIAN_POINT('Ctrl Pts',(103.653846812233,-3.62856333795136,134.12440747943));
#45762=CARTESIAN_POINT('Ctrl Pts',(103.646900442648,-3.54603025321083,134.214609978948));
#45763=CARTESIAN_POINT('Ctrl Pts',(103.639954073062,-3.4602449279693,134.301609058963));
#45764=CARTESIAN_POINT('Ctrl Pts',(103.633007703477,-3.37149686224685,134.385169460601));
#45765=CARTESIAN_POINT('Ctrl Pts',(103.625233369358,-3.27217057290244,134.478689748207));
#45766=CARTESIAN_POINT('Ctrl Pts',(103.617459035238,-3.16879283925618,134.568222288876));
#45767=CARTESIAN_POINT('Ctrl Pts',(103.609684701119,-3.06171726098981,134.653395623416));
#45768=CARTESIAN_POINT('Ctrl Pts',(103.601919948172,-2.9547736438041,134.738463989433));
#45769=CARTESIAN_POINT('Ctrl Pts',(103.594155195225,-2.84414155262642,134.819183597613));
#45770=CARTESIAN_POINT('Ctrl Pts',(103.586390442278,-2.73021113383673,134.895219968262));
#45771=CARTESIAN_POINT('Ctrl Pts',(103.578633401393,-2.61639387234488,134.971180818516));
#45772=CARTESIAN_POINT('Ctrl Pts',(103.570876360508,-2.49928512560967,135.042467472221));
#45773=CARTESIAN_POINT('Ctrl Pts',(103.563119319623,-2.37930751680441,135.108786108033));
#45774=CARTESIAN_POINT('Ctrl Pts',(103.555368128383,-2.25942038404725,135.175054732445));
#45775=CARTESIAN_POINT('Ctrl Pts',(103.547616937143,-2.13666903618474,135.236362607613));
#45776=CARTESIAN_POINT('Ctrl Pts',(103.539865745903,-2.01150413112362,135.292459791267));
#45777=CARTESIAN_POINT('Ctrl Pts',(103.532117849126,-1.88639242448628,135.348533132121));
#45778=CARTESIAN_POINT('Ctrl Pts',(103.524369952349,-1.75886955696481,135.39940002673));
#45779=CARTESIAN_POINT('Ctrl Pts',(103.516622055572,-1.6294095878515,135.444857084273));
#45780=CARTESIAN_POINT('Ctrl Pts',(103.508875779487,-1.49997669897281,135.490304633179));
#45781=CARTESIAN_POINT('Ctrl Pts',(103.501129503403,-1.36860788311919,135.530344466433));
#45782=CARTESIAN_POINT('Ctrl Pts',(103.493383227319,-1.23579555019815,135.564821983926));
#45783=CARTESIAN_POINT('Ctrl Pts',(103.485636894054,-1.10298223688664,135.599299755925));
#45784=CARTESIAN_POINT('Ctrl Pts',(103.477890560789,-0.968725763667167,
135.628215031995));
#45785=CARTESIAN_POINT('Ctrl Pts',(103.470144227523,-0.833531626586319,
135.651463679187));
#45786=CARTESIAN_POINT('Ctrl Pts',(103.46239615952,-0.698307213715842,135.674717532753));
#45787=CARTESIAN_POINT('Ctrl Pts',(103.454648091517,-0.562145104377292,
135.692302166028));
#45788=CARTESIAN_POINT('Ctrl Pts',(103.446900023514,-0.425558465003698,
135.704165007066));
#45789=CARTESIAN_POINT('Ctrl Pts',(103.439143720772,-0.288826659724283,
135.716040456073));
#45790=CARTESIAN_POINT('Ctrl Pts',(103.431387418031,-0.151669813218047,
135.722181931132));
#45791=CARTESIAN_POINT('Ctrl Pts',(103.423631115289,-0.0146042221654386,
135.722588934673));
#45792=CARTESIAN_POINT('Ctrl Pts',(103.415870672775,0.122534524920174,135.722996155445));
#45793=CARTESIAN_POINT('Ctrl Pts',(103.40811023026,0.259581529023418,135.717662821271));
#45794=CARTESIAN_POINT('Ctrl Pts',(103.400349787746,0.396024048075988,135.706640496953));
#45795=CARTESIAN_POINT('Ctrl Pts',(103.392576887481,0.532685596772845,135.695600478622));
#45796=CARTESIAN_POINT('Ctrl Pts',(103.384803987215,0.668740333044529,135.678853268351));
#45797=CARTESIAN_POINT('Ctrl Pts',(103.37703108695,0.803683266047643,135.656502028363));
#45798=CARTESIAN_POINT('Ctrl Pts',(103.369540751188,0.933720683534809,135.634963312249));
#45799=CARTESIAN_POINT('Ctrl Pts',(103.362050415426,1.06272542645402,135.608220996356));
#45800=CARTESIAN_POINT('Ctrl Pts',(103.354560079664,1.19025948598856,135.576411059306));
#45801=CARTESIAN_POINT('Ctrl Pts',(103.346785745545,1.32262903815395,135.543395038825));
#45802=CARTESIAN_POINT('Ctrl Pts',(103.339011411426,1.45383349048909,135.504814948884));
#45803=CARTESIAN_POINT('Ctrl Pts',(103.331237077307,1.58336919459099,135.460767500144));
#45804=CARTESIAN_POINT('Ctrl Pts',(103.32347232436,1.71274525751454,135.416774335948));
#45805=CARTESIAN_POINT('Ctrl Pts',(103.315707571413,1.84045629759499,135.367327344283));
#45806=CARTESIAN_POINT('Ctrl Pts',(103.307942818465,1.96601002394501,135.312573971906));
#45807=CARTESIAN_POINT('Ctrl Pts',(103.30018577758,2.09143904856393,135.25787498135));
#45808=CARTESIAN_POINT('Ctrl Pts',(103.292428736695,2.21471466741992,135.197880253631));
#45809=CARTESIAN_POINT('Ctrl Pts',(103.28467169581,2.33536124214426,135.132786535979));
#45810=CARTESIAN_POINT('Ctrl Pts',(103.27692050457,2.45591683634859,135.067741906006));
#45811=CARTESIAN_POINT('Ctrl Pts',(103.26916931333,2.57384698994551,134.997606124607));
#45812=CARTESIAN_POINT('Ctrl Pts',(103.26141812209,2.68869782781654,134.922623243139));
#45813=CARTESIAN_POINT('Ctrl Pts',(103.253670225313,2.80349985101726,134.847672231397));
#45814=CARTESIAN_POINT('Ctrl Pts',(103.245922328536,2.91522483489166,134.767878430345));
#45815=CARTESIAN_POINT('Ctrl Pts',(103.238174431759,3.02344542035482,134.683530741785));
#45816=CARTESIAN_POINT('Ctrl Pts',(103.230428155675,3.13164336840455,134.599200696944));
#45817=CARTESIAN_POINT('Ctrl Pts',(103.222681879591,3.23633806793841,134.510318899509));
#45818=CARTESIAN_POINT('Ctrl Pts',(103.214935603506,3.33713328992503,134.417216062747));
#45819=CARTESIAN_POINT('Ctrl Pts',(103.207189270241,3.43792925595908,134.324112538721));
#45820=CARTESIAN_POINT('Ctrl Pts',(103.199442936976,3.53482539981158,134.226788178471));
#45821=CARTESIAN_POINT('Ctrl Pts',(103.19169660371,3.62746087852322,134.125611983736));
#45822=CARTESIAN_POINT('Ctrl Pts',(103.183948535707,3.72011710230821,134.024413131292));
#45823=CARTESIAN_POINT('Ctrl Pts',(103.176200467704,3.80851049834654,133.919361016208));
#45824=CARTESIAN_POINT('Ctrl Pts',(103.168452399701,3.89231945738096,133.810858963515));
#45825=CARTESIAN_POINT('Ctrl Pts',(103.16069609696,3.97621748957416,133.70224159355));
#45826=CARTESIAN_POINT('Ctrl Pts',(103.152939794218,4.05552111225531,133.590167271384));
#45827=CARTESIAN_POINT('Ctrl Pts',(103.145183491476,4.12995083583871,133.475070103088));
#45828=CARTESIAN_POINT('Ctrl Pts',(103.137423048962,4.20442028480668,133.359911503967));
#45829=CARTESIAN_POINT('Ctrl Pts',(103.129662606447,4.27401045299499,133.241727180648));
#45830=CARTESIAN_POINT('Ctrl Pts',(103.121902163933,4.33848757372001,133.120976389587));
#45831=CARTESIAN_POINT('Ctrl Pts',(103.114129263668,4.40306819884322,133.000031758637));
#45832=CARTESIAN_POINT('Ctrl Pts',(103.106356363402,4.46251920481258,132.876512779516));
#45833=CARTESIAN_POINT('Ctrl Pts',(103.098583463137,4.51665442504361,132.750900077026));
#45834=CARTESIAN_POINT('Ctrl Pts',(103.091093127375,4.56882169366067,132.629853712671));
#45835=CARTESIAN_POINT('Ctrl Pts',(103.083602791613,4.61605284058172,132.506863493891));
#45836=CARTESIAN_POINT('Ctrl Pts',(103.076112455851,4.65822551400895,132.382371429676));
#45837=CARTESIAN_POINT('Ctrl Pts',(103.068338121732,4.70199717716743,132.253159211008));
#45838=CARTESIAN_POINT('Ctrl Pts',(103.060563787613,4.74045786618925,132.121919708371));
#45839=CARTESIAN_POINT('Ctrl Pts',(103.052789453494,4.77341671222796,131.989128929905));
#45840=CARTESIAN_POINT('Ctrl Pts',(103.045024700547,4.80633493943454,131.856501804206));
#45841=CARTESIAN_POINT('Ctrl Pts',(103.0372599476,4.83376472161489,131.722327582417));
#45842=CARTESIAN_POINT('Ctrl Pts',(103.029495194652,4.85556401464997,131.587100141377));
#45843=CARTESIAN_POINT('Ctrl Pts',(103.021738153767,4.87734165631981,131.452007010138));
#45844=CARTESIAN_POINT('Ctrl Pts',(103.013981112883,4.89349987591688,131.315863124864));
#45845=CARTESIAN_POINT('Ctrl Pts',(103.006224071998,4.90394710830169,131.179175000267));
#45846=CARTESIAN_POINT('Ctrl Pts',(102.998472880757,4.91438646234729,131.042589953248));
#45847=CARTESIAN_POINT('Ctrl Pts',(102.990721689517,4.91912337173111,130.905461872065));
#45848=CARTESIAN_POINT('Ctrl Pts',(102.982970498277,4.91811783318378,130.768304530429));
#45849=CARTESIAN_POINT('Ctrl Pts',(102.9752226015,4.91711272201716,130.631205484321));
#45850=CARTESIAN_POINT('Ctrl Pts',(102.967474704723,4.91037002013292,130.494077592631));
#45851=CARTESIAN_POINT('Ctrl Pts',(102.959726807946,4.89790179077492,130.357436563141));
#45852=CARTESIAN_POINT('Ctrl Pts',(102.951980531862,4.88543616950173,130.220824116009));
#45853=CARTESIAN_POINT('Ctrl Pts',(102.944234255778,4.86724743846475,130.084698717611));
#45854=CARTESIAN_POINT('Ctrl Pts',(102.936487979694,4.84339966463173,129.949572485252));
#45855=CARTESIAN_POINT('Ctrl Pts',(102.928741646428,4.81955171475988,129.814445255421));
#45856=CARTESIAN_POINT('Ctrl Pts',(102.920995313163,4.79004470668492,129.680317591362));
#45857=CARTESIAN_POINT('Ctrl Pts',(102.913248979898,4.75499404758626,129.547692534929));
#45858=CARTESIAN_POINT('Ctrl Pts',(102.905500911895,4.71993553913543,129.415037778033));
#45859=CARTESIAN_POINT('Ctrl Pts',(102.897752843892,4.67933100917168,129.283886676271));
#45860=CARTESIAN_POINT('Ctrl Pts',(102.890004775889,4.63334594880947,129.154727815652));
#45861=CARTESIAN_POINT('Ctrl Pts',(102.882248473147,4.58731201497794,129.025431683459));
#45862=CARTESIAN_POINT('Ctrl Pts',(102.874492170405,4.53588625878769,128.898132391004));
#45863=CARTESIAN_POINT('Ctrl Pts',(102.866735867663,4.47928283502318,128.773299725725));
#45864=CARTESIAN_POINT('Ctrl Pts',(102.858975425149,4.42264920030707,128.648400433494));
#45865=CARTESIAN_POINT('Ctrl Pts',(102.851214982635,4.3608325676844,128.525970740534));
#45866=CARTESIAN_POINT('Ctrl Pts',(102.843454540121,4.29409296601832,128.406455560711));
#45867=CARTESIAN_POINT('Ctrl Pts',(102.835681639855,4.22724622801887,128.286748524511));
#45868=CARTESIAN_POINT('Ctrl Pts',(102.82790873959,4.15546093354346,128.169965684115));
#45869=CARTESIAN_POINT('Ctrl Pts',(102.820135839324,4.07904081826292,128.056523456189));
#45870=CARTESIAN_POINT('Ctrl Pts',(102.812645503562,4.00539876666256,127.94720513899));
#45871=CARTESIAN_POINT('Ctrl Pts',(102.8051551678,3.92745320093368,127.840989019974));
#45872=CARTESIAN_POINT('Ctrl Pts',(102.797664832038,3.84550986162237,127.738216953831));
#45873=CARTESIAN_POINT('Ctrl Pts',(102.789890497919,3.76045961569588,127.631548253563));
#45874=CARTESIAN_POINT('Ctrl Pts',(102.7821161638,3.67083304710242,127.528252029747));
#45875=CARTESIAN_POINT('Ctrl Pts',(102.774341829681,3.57692746569745,127.428746159776));
#45876=CARTESIAN_POINT('Ctrl Pts',(102.766577076734,3.48313761452899,127.329362921897));
#45877=CARTESIAN_POINT('Ctrl Pts',(102.758812323787,3.38507950900481,127.233761025032));
#45878=CARTESIAN_POINT('Ctrl Pts',(102.751047570839,3.28309188338035,127.142326927418));
#45879=CARTESIAN_POINT('Ctrl Pts',(102.743290529954,3.18120555330349,127.050983643438));
#45880=CARTESIAN_POINT('Ctrl Pts',(102.735533489069,3.07539775920484,126.963800180176));
#45881=CARTESIAN_POINT('Ctrl Pts',(102.727776448184,2.96604515306411,126.881127357551));
#45882=CARTESIAN_POINT('Ctrl Pts',(102.720025256944,2.85677501057386,126.798516879145));
#45883=CARTESIAN_POINT('Ctrl Pts',(102.712274065704,2.74396568743165,126.720410505705));
#45884=CARTESIAN_POINT('Ctrl Pts',(102.704522874464,2.62802781326745,126.647119600354));
#45885=CARTESIAN_POINT('Ctrl Pts',(102.696774977687,2.51213921579291,126.573859845593));
#45886=CARTESIAN_POINT('Ctrl Pts',(102.68902708091,2.39312504178207,126.505411696658));
#45887=CARTESIAN_POINT('Ctrl Pts',(102.681279184133,2.27142569127575,126.442043757053));
#45888=CARTESIAN_POINT('Ctrl Pts',(102.673532908049,2.14975179765018,126.378689072656));
#45889=CARTESIAN_POINT('Ctrl Pts',(102.665786631964,2.02539419129638,126.320412664328));
#45890=CARTESIAN_POINT('Ctrl Pts',(102.65804035588,1.89881836076769,126.267437442626));
#45891=CARTESIAN_POINT('Ctrl Pts',(102.650294022615,1.77224159588514,126.214461829873));
#45892=CARTESIAN_POINT('Ctrl Pts',(102.64254768935,1.64344693480621,126.166787632774));
#45893=CARTESIAN_POINT('Ctrl Pts',(102.634801356084,1.51291998128912,126.124589662411));
#45894=CARTESIAN_POINT('Ctrl Pts',(102.627053288081,1.38236379716589,126.082382242104));
#45895=CARTESIAN_POINT('Ctrl Pts',(102.619305220078,1.25007492059564,126.045653609097));
#45896=CARTESIAN_POINT('Ctrl Pts',(102.611557152075,1.11655386481506,126.0145286237));
#45897=CARTESIAN_POINT('Ctrl Pts',(102.603800849334,0.982890901267192,125.983370558297));
#45898=CARTESIAN_POINT('Ctrl Pts',(102.596044546592,0.847993523856434,125.957828126403));
#45899=CARTESIAN_POINT('Ctrl Pts',(102.58828824385,0.712372733952538,125.937975085118));
#45900=CARTESIAN_POINT('Ctrl Pts',(102.580527801336,0.576679559149422,125.918111447667));
#45901=CARTESIAN_POINT('Ctrl Pts',(102.572767358822,0.440262591185438,125.903943291874));
#45902=CARTESIAN_POINT('Ctrl Pts',(102.565006916307,0.303636700648433,125.895492334905));
#45903=CARTESIAN_POINT('Ctrl Pts',(102.557234016042,0.166791486102861,125.887027811709));
#45904=CARTESIAN_POINT('Ctrl Pts',(102.549461115776,0.0297370698987304,
125.884298835203));
#45905=CARTESIAN_POINT('Ctrl Pts',(102.541688215511,-0.107012028281012,
125.887274947344));
#45906=CARTESIAN_POINT('Ctrl Pts',(102.534197879749,-0.23878995229145,125.890142870312));
#45907=CARTESIAN_POINT('Ctrl Pts',(102.526707543987,-0.370284063617012,
125.898308275492));
#45908=CARTESIAN_POINT('Ctrl Pts',(102.519217208225,-0.50104148999333,125.911698715513));
#45909=CARTESIAN_POINT('Ctrl Pts',(102.511442874106,-0.636756623933761,
125.925596858136));
#45910=CARTESIAN_POINT('Ctrl Pts',(102.503668539987,-0.772108012106316,
125.945168096527));
#45911=CARTESIAN_POINT('Ctrl Pts',(102.495894205868,-0.906583379186386,
125.970388168422));
#45912=CARTESIAN_POINT('Ctrl Pts',(102.488129452921,-1.04089301739485,125.995577158832));
#45913=CARTESIAN_POINT('Ctrl Pts',(102.480364699974,-1.17432840205142,126.026401059698));
#45914=CARTESIAN_POINT('Ctrl Pts',(102.472599947026,-1.30638130075887,126.062783774413));
#45915=CARTESIAN_POINT('Ctrl Pts',(102.464842906141,-1.43830304266579,126.099130353302));
#45916=CARTESIAN_POINT('Ctrl Pts',(102.457085865256,-1.56884465668163,126.141024655642));
#45917=CARTESIAN_POINT('Ctrl Pts',(102.449328824371,-1.69750739847636,126.188339420191));
#45918=CARTESIAN_POINT('Ctrl Pts',(102.441577633131,-1.82607311469665,126.235618504307));
#45919=CARTESIAN_POINT('Ctrl Pts',(102.433826441891,-1.95276241343844,126.288309780094));
#45920=CARTESIAN_POINT('Ctrl Pts',(102.426075250651,-2.07709138074198,126.346236072587));
#45921=CARTESIAN_POINT('Ctrl Pts',(102.418327353874,-2.20136750491775,126.40413774486));
#45922=CARTESIAN_POINT('Ctrl Pts',(102.410579457097,-2.32328493930456,126.467269843673));
#45923=CARTESIAN_POINT('Ctrl Pts',(102.40283156032,-2.44237965318738,126.535407034755));
#45924=CARTESIAN_POINT('Ctrl Pts',(102.395085284236,-2.56144945502352,126.603529973005));
#45925=CARTESIAN_POINT('Ctrl Pts',(102.387339008152,-2.67769737166177,126.676655727039));
#45926=CARTESIAN_POINT('Ctrl Pts',(102.379592732068,-2.79068425420331,126.754513156754));
#45927=CARTESIAN_POINT('Ctrl Pts',(102.371846398802,-2.90367197078797,126.832371161196));
#45928=CARTESIAN_POINT('Ctrl Pts',(102.364100065537,-3.01339828330809,126.914960689177));
#45929=CARTESIAN_POINT('Ctrl Pts',(102.356353732272,-3.11945363755738,127.001967678162));
#45930=CARTESIAN_POINT('Ctrl Pts',(102.348605664269,-3.22553274216849,127.088994151759));
#45931=CARTESIAN_POINT('Ctrl Pts',(102.340857596266,-3.32793895044865,127.180439806947));
#45932=CARTESIAN_POINT('Ctrl Pts',(102.333109528263,-3.42629667425205,127.275951037811));
#45933=CARTESIAN_POINT('Ctrl Pts',(102.325353225521,-3.52475893381458,127.371563779147));
#45934=CARTESIAN_POINT('Ctrl Pts',(102.317596922779,-3.61916383270866,127.471250454908));
#45935=CARTESIAN_POINT('Ctrl Pts',(102.309840620037,-3.70917310827423,127.574621012682));
#45936=CARTESIAN_POINT('Ctrl Pts',(102.302080177523,-3.79923042450018,127.678046742436));
#45937=CARTESIAN_POINT('Ctrl Pts',(102.294319735009,-3.88488719858575,127.78515996683));
#45938=CARTESIAN_POINT('Ctrl Pts',(102.286559292495,-3.96584685913581,127.895539249317));
#45939=CARTESIAN_POINT('Ctrl Pts',(102.278786392229,-4.04693648332046,128.006095722427));
#45940=CARTESIAN_POINT('Ctrl Pts',(102.271013491964,-4.12331370824213,128.119928405902));
#45941=CARTESIAN_POINT('Ctrl Pts',(102.263240591698,-4.19472604865866,128.236587956444));
#45942=CARTESIAN_POINT('Ctrl Pts',(102.255750255936,-4.26354237062437,128.349006638477));
#45943=CARTESIAN_POINT('Ctrl Pts',(102.248259920174,-4.32774836308428,128.464049959393));
#45944=CARTESIAN_POINT('Ctrl Pts',(102.240769584412,-4.38716018954261,128.581297745357));
#45945=CARTESIAN_POINT('Ctrl Pts',(102.232471443257,-4.45297936479825,128.711190277413));
#45946=CARTESIAN_POINT('Ctrl Pts',(102.224173302102,-4.51310129049722,128.844156401856));
#45947=CARTESIAN_POINT('Ctrl Pts',(102.215875160946,-4.56724797383606,128.979688316031));
#45948=CARTESIAN_POINT('Ctrl Pts',(102.207597026909,-4.62126410756482,129.114893457863));
#45949=CARTESIAN_POINT('Ctrl Pts',(102.199318892872,-4.66933361053416,129.252651766697));
#45950=CARTESIAN_POINT('Ctrl Pts',(102.191040758835,-4.71122522047061,129.392432862863));
#45951=CARTESIAN_POINT('Ctrl Pts',(102.187312190147,-4.73009369305051,129.455391908461));
#45952=CARTESIAN_POINT('Ctrl Pts',(102.183583621459,-4.74770947080646,129.518760988469));
#45953=CARTESIAN_POINT('Ctrl Pts',(102.179855052771,-4.76405452823403,129.582490119308));
#45954=CARTESIAN_POINT('Origin',(213.235140564004,0.,130.804360617566));
#45955=CARTESIAN_POINT('',(100.084952068471,-4.76405452823407,129.582490119308));
#45956=CARTESIAN_POINT('',(100.43015599918,-4.76405452823403,129.582490119308));
#45957=CARTESIAN_POINT('',(213.235140564004,-4.76405452823405,129.582490119308));
#45958=CARTESIAN_POINT('',(101.764859436032,-4.91824793163316,130.808871214655));
#45959=CARTESIAN_POINT('Ctrl Pts',(101.764859435991,-4.91824793163249,130.808871215387));
#45960=CARTESIAN_POINT('Ctrl Pts',(101.754213180585,-4.91807564840936,130.996724719397));
#45961=CARTESIAN_POINT('Ctrl Pts',(101.74356692518,-4.90713724480048,131.184104547583));
#45962=CARTESIAN_POINT('Ctrl Pts',(101.732920669774,-4.88561573720794,131.369994713821));
#45963=CARTESIAN_POINT('Ctrl Pts',(101.723101557498,-4.86576630739908,131.541442452369));
#45964=CARTESIAN_POINT('Ctrl Pts',(101.713282445222,-4.83691494772115,131.711623822433));
#45965=CARTESIAN_POINT('Ctrl Pts',(101.703463332945,-4.79923915487164,131.879761285618));
#45966=CARTESIAN_POINT('Ctrl Pts',(101.695688998826,-4.76940914645777,132.012885012079));
#45967=CARTESIAN_POINT('Ctrl Pts',(101.687914664707,-4.73398871171512,132.144977496555));
#45968=CARTESIAN_POINT('Ctrl Pts',(101.680140330588,-4.69306244728092,132.275532914893));
#45969=CARTESIAN_POINT('Ctrl Pts',(101.672375577641,-4.65218662081001,132.405927435345));
#45970=CARTESIAN_POINT('Ctrl Pts',(101.664610824694,-4.60581858148159,132.53478828926));
#45971=CARTESIAN_POINT('Ctrl Pts',(101.656846071747,-4.55409391996521,132.661619789205));
#45972=CARTESIAN_POINT('Ctrl Pts',(101.649089030862,-4.5024206321118,132.788325318315));
#45973=CARTESIAN_POINT('Ctrl Pts',(101.641331989977,-4.4454014563364,132.91300514488));
#45974=CARTESIAN_POINT('Ctrl Pts',(101.633574949092,-4.38322166920146,133.035179046113));
#45975=CARTESIAN_POINT('Ctrl Pts',(101.625823757852,-4.32108877232769,133.157260815055));
#45976=CARTESIAN_POINT('Ctrl Pts',(101.618072566612,-4.25380318681832,133.276840073049));
#45977=CARTESIAN_POINT('Ctrl Pts',(101.610321375372,-4.18159800199837,133.393457219121));
#45978=CARTESIAN_POINT('Ctrl Pts',(101.602573478595,-4.10942350630805,133.510024799795));
#45979=CARTESIAN_POINT('Ctrl Pts',(101.594825581818,-4.03233377545255,133.623632440844));
#45980=CARTESIAN_POINT('Ctrl Pts',(101.58707768504,-3.95060737259751,133.733845973406));
#45981=CARTESIAN_POINT('Ctrl Pts',(101.579331408956,-3.86889806514414,133.844036451672));
#45982=CARTESIAN_POINT('Ctrl Pts',(101.571585132872,-3.78255424758454,133.950833919784));
#45983=CARTESIAN_POINT('Ctrl Pts',(101.563838856788,-3.69189702954403,134.053834326606));
#45984=CARTESIAN_POINT('Ctrl Pts',(101.556092523523,-3.60123914229259,134.156835493754));
#45985=CARTESIAN_POINT('Ctrl Pts',(101.548346190257,-3.50626804933434,134.256039250205));
#45986=CARTESIAN_POINT('Ctrl Pts',(101.540599856992,-3.40734398690799,134.351076001887));
#45987=CARTESIAN_POINT('Ctrl Pts',(101.532851788989,-3.3083977711239,134.446134036392));
#45988=CARTESIAN_POINT('Ctrl Pts',(101.525103720986,-3.20549710623059,134.537022938417));
#45989=CARTESIAN_POINT('Ctrl Pts',(101.517355652983,-3.09903748337889,134.623411512633));
#45990=CARTESIAN_POINT('Ctrl Pts',(101.509599350241,-2.99246471397299,134.709891901654));
#45991=CARTESIAN_POINT('Ctrl Pts',(101.5018430475,-2.8823257347227,134.79186216156));
#45992=CARTESIAN_POINT('Ctrl Pts',(101.494086744758,-2.76904781970824,134.869032465904));
#45993=CARTESIAN_POINT('Ctrl Pts',(101.486326302244,-2.65570944485981,134.946243958362));
#45994=CARTESIAN_POINT('Ctrl Pts',(101.478565859729,-2.53922912786052,135.018650184191));
#45995=CARTESIAN_POINT('Ctrl Pts',(101.470805417215,-2.42006038315897,135.086006423137));
#45996=CARTESIAN_POINT('Ctrl Pts',(101.46303251695,-2.30070033820905,135.153470788298));
#45997=CARTESIAN_POINT('Ctrl Pts',(101.455259616684,-2.17864358972124,135.215868788766));
#45998=CARTESIAN_POINT('Ctrl Pts',(101.447486716419,-2.05436615660382,135.273002777898));
#45999=CARTESIAN_POINT('Ctrl Pts',(101.439996380657,-1.93460652121634,135.328059802614));
#46000=CARTESIAN_POINT('Ctrl Pts',(101.432506044895,-1.81278513787602,135.378228774261));
#46001=CARTESIAN_POINT('Ctrl Pts',(101.425015709133,-1.68934095217909,135.42337676928));
#46002=CARTESIAN_POINT('Ctrl Pts',(101.417241375014,-1.56121634266132,135.470236564251));
#46003=CARTESIAN_POINT('Ctrl Pts',(101.409467040895,-1.43093758424745,135.511835563741));
#46004=CARTESIAN_POINT('Ctrl Pts',(101.401692706776,-1.29897596767261,135.547971530985));
#46005=CARTESIAN_POINT('Ctrl Pts',(101.393927953829,-1.16717698199653,135.584062963879));
#46006=CARTESIAN_POINT('Ctrl Pts',(101.386163200882,-1.03369963820886,135.614704658324));
#46007=CARTESIAN_POINT('Ctrl Pts',(101.378398447934,-0.89903426225641,135.639742759423));
#46008=CARTESIAN_POINT('Ctrl Pts',(101.370641407049,-0.764502637853893,
135.664755992327));
#46009=CARTESIAN_POINT('Ctrl Pts',(101.362884366164,-0.628785711371234,
135.684176636613));
#46010=CARTESIAN_POINT('Ctrl Pts',(101.355127325279,-0.492387654347936,
135.697900998553));
#46011=CARTESIAN_POINT('Ctrl Pts',(101.347376134039,-0.356092456160276,
135.711615010844));
#46012=CARTESIAN_POINT('Ctrl Pts',(101.339624942799,-0.219117537239844,
135.71964125196));
#46013=CARTESIAN_POINT('Ctrl Pts',(101.331873751559,-0.081975563375735,
135.721927400998));
#46014=CARTESIAN_POINT('Ctrl Pts',(101.324125854782,0.0551081214910062,
135.724212578361));
#46015=CARTESIAN_POINT('Ctrl Pts',(101.316377958005,0.192358329989765,135.720762509506));
#46016=CARTESIAN_POINT('Ctrl Pts',(101.308630061228,0.329259213364727,135.711576878636));
#46017=CARTESIAN_POINT('Ctrl Pts',(101.300883785144,0.466131460026223,135.702393169203));
#46018=CARTESIAN_POINT('Ctrl Pts',(101.29313750906,0.602654137065751,135.687476310294));
#46019=CARTESIAN_POINT('Ctrl Pts',(101.285391232976,0.738313737225168,135.666878061023));
#46020=CARTESIAN_POINT('Ctrl Pts',(101.27764489971,0.873974338792844,135.646279659701));
#46021=CARTESIAN_POINT('Ctrl Pts',(101.269898566445,1.00877146423259,135.619999843022));
#46022=CARTESIAN_POINT('Ctrl Pts',(101.262152233179,1.14219944709981,135.588141913314));
#46023=CARTESIAN_POINT('Ctrl Pts',(101.254404165176,1.27565731023858,135.556276849243));
#46024=CARTESIAN_POINT('Ctrl Pts',(101.246656097174,1.4077450404833,135.5188312772));
#46025=CARTESIAN_POINT('Ctrl Pts',(101.238908029171,1.53797022119512,135.475958915924));
#46026=CARTESIAN_POINT('Ctrl Pts',(101.231151726429,1.66833380677878,135.433040989392));
#46027=CARTESIAN_POINT('Ctrl Pts',(101.223395423687,1.7968305165352,135.384684874565));
#46028=CARTESIAN_POINT('Ctrl Pts',(101.215639120945,1.92298555918795,135.331093390953));
#46029=CARTESIAN_POINT('Ctrl Pts',(101.207878678431,2.0492079345855,135.277473303953));
#46030=CARTESIAN_POINT('Ctrl Pts',(101.200118235917,2.17308579955428,135.218612448048));
#46031=CARTESIAN_POINT('Ctrl Pts',(101.192357793403,2.29416812837713,135.154760100514));
#46032=CARTESIAN_POINT('Ctrl Pts',(101.184584893137,2.41544482930339,135.090805251524));
#46033=CARTESIAN_POINT('Ctrl Pts',(101.176811992872,2.53391668825988,135.021843095604));
#46034=CARTESIAN_POINT('Ctrl Pts',(101.169039092606,2.64916011968079,134.948167288104));
#46035=CARTESIAN_POINT('Ctrl Pts',(101.161548756844,2.76021416208956,134.877169781784));
#46036=CARTESIAN_POINT('Ctrl Pts',(101.154058421082,2.86827017214438,134.801795556439));
#46037=CARTESIAN_POINT('Ctrl Pts',(101.14656808532,2.97297905667257,134.722342060999));
#46038=CARTESIAN_POINT('Ctrl Pts',(101.138793751201,3.0816580103826,134.639876062131));
#46039=CARTESIAN_POINT('Ctrl Pts',(101.131019417082,3.18707527795657,134.552754128327));
#46040=CARTESIAN_POINT('Ctrl Pts',(101.123245082963,3.2888059677232,134.461263455921));
#46041=CARTESIAN_POINT('Ctrl Pts',(101.115480330016,3.39041128350656,134.369885537592));
#46042=CARTESIAN_POINT('Ctrl Pts',(101.107715577069,3.48833877354339,134.274149852301));
#46043=CARTESIAN_POINT('Ctrl Pts',(101.099950824121,3.58219396220099,134.174385762824));
#46044=CARTESIAN_POINT('Ctrl Pts',(101.092193783236,3.67595593256203,134.074720760447));
#46045=CARTESIAN_POINT('Ctrl Pts',(101.084436742351,3.76565338445493,133.971035599106));
#46046=CARTESIAN_POINT('Ctrl Pts',(101.076679701466,3.85092656037782,133.863698403603));
#46047=CARTESIAN_POINT('Ctrl Pts',(101.068928510226,3.93613543113548,133.756442151915));
#46048=CARTESIAN_POINT('Ctrl Pts',(101.061177318986,4.01692642457587,133.64553965267));
#46049=CARTESIAN_POINT('Ctrl Pts',(101.053426127746,4.09297841326089,133.531393945393));
#46050=CARTESIAN_POINT('Ctrl Pts',(101.045678230969,4.16899807782195,133.417296753087));
#46051=CARTESIAN_POINT('Ctrl Pts',(101.037930334192,4.24028252739919,133.29995941906));
#46052=CARTESIAN_POINT('Ctrl Pts',(101.030182437415,4.30655266745259,133.179815770785));
#46053=CARTESIAN_POINT('Ctrl Pts',(101.022436161331,4.37280894522136,133.059697253972));
#46054=CARTESIAN_POINT('Ctrl Pts',(101.014689885247,4.43405281104514,132.936773932651));
#46055=CARTESIAN_POINT('Ctrl Pts',(101.006943609163,4.49005024811696,132.811505812086));
#46056=CARTESIAN_POINT('Ctrl Pts',(100.999197275897,4.54604809854909,132.686236766821));
#46057=CARTESIAN_POINT('Ctrl Pts',(100.991450942632,4.59679928339698,132.5586232447));
#46058=CARTESIAN_POINT('Ctrl Pts',(100.983704609366,4.64211738876953,132.429146514656));
#46059=CARTESIAN_POINT('Ctrl Pts',(100.975956541363,4.68744564281757,132.299640789197));
#46060=CARTESIAN_POINT('Ctrl Pts',(100.968208473361,4.72733826716322,132.168271394474));
#46061=CARTESIAN_POINT('Ctrl Pts',(100.960460405358,4.76165842651478,132.035535703287));
#46062=CARTESIAN_POINT('Ctrl Pts',(100.952704102616,4.79601506174014,131.902658939028));
#46063=CARTESIAN_POINT('Ctrl Pts',(100.944947799874,4.82478730314989,131.768413356666));
#46064=CARTESIAN_POINT('Ctrl Pts',(100.937191497132,4.8478891522596,131.633308040449));
#46065=CARTESIAN_POINT('Ctrl Pts',(100.929431054618,4.87100333152177,131.498130614456));
#46066=CARTESIAN_POINT('Ctrl Pts',(100.921670612104,4.88844103832387,131.362092927881));
#46067=CARTESIAN_POINT('Ctrl Pts',(100.913910169589,4.90016820628043,131.225709181891));
#46068=CARTESIAN_POINT('Ctrl Pts',(100.906137269324,4.91191419972807,131.089106500603));
#46069=CARTESIAN_POINT('Ctrl Pts',(100.898364369059,4.91793131844436,130.952157040596));
#46070=CARTESIAN_POINT('Ctrl Pts',(100.890591468793,4.9182376646476,130.815375904293));
#46071=CARTESIAN_POINT('Ctrl Pts',(100.883101133031,4.91853287439472,130.683567106826));
#46072=CARTESIAN_POINT('Ctrl Pts',(100.875610797269,4.91352531675243,130.551914915346));
#46073=CARTESIAN_POINT('Ctrl Pts',(100.868120461507,4.90327655054314,130.420873810239));
#46074=CARTESIAN_POINT('Ctrl Pts',(100.860346127388,4.89263919924793,130.284864241802));
#46075=CARTESIAN_POINT('Ctrl Pts',(100.852571793269,4.8763216570013,130.149082175728));
#46076=CARTESIAN_POINT('Ctrl Pts',(100.84479745915,4.85433588588463,130.014040322045));
#46077=CARTESIAN_POINT('Ctrl Pts',(100.837032706203,4.83237721026595,129.879164895377));
#46078=CARTESIAN_POINT('Ctrl Pts',(100.829267953256,4.80476426723189,129.745028248185));
#46079=CARTESIAN_POINT('Ctrl Pts',(100.821503200308,4.77156093529912,129.612140292615));
#46080=CARTESIAN_POINT('Ctrl Pts',(100.813746159424,4.73839058138372,129.479384323235));
#46081=CARTESIAN_POINT('Ctrl Pts',(100.805989118539,4.69964098236137,129.347874954238));
#46082=CARTESIAN_POINT('Ctrl Pts',(100.798232077654,4.65542739433689,129.218113840246));
#46083=CARTESIAN_POINT('Ctrl Pts',(100.790480886413,4.61124714812307,129.08845058012));
#46084=CARTESIAN_POINT('Ctrl Pts',(100.782729695173,4.56161123997121,128.960533319433));
#46085=CARTESIAN_POINT('Ctrl Pts',(100.774978503933,4.50668518122186,128.834850084501));
#46086=CARTESIAN_POINT('Ctrl Pts',(100.767230607156,4.45178246751264,128.709220268296));
#46087=CARTESIAN_POINT('Ctrl Pts',(100.759482710379,4.39159423144577,128.585822946821));
#46088=CARTESIAN_POINT('Ctrl Pts',(100.751734813602,4.32633460694478,128.465127424562));
#46089=CARTESIAN_POINT('Ctrl Pts',(100.743988537518,4.26108863335041,128.344457149204));
#46090=CARTESIAN_POINT('Ctrl Pts',(100.736242261434,4.19077356719554,128.226487892627));
#46091=CARTESIAN_POINT('Ctrl Pts',(100.728495985349,4.11564993213761,128.11166518388));
#46092=CARTESIAN_POINT('Ctrl Pts',(100.720749652084,4.04052574253412,127.996841627537));
#46093=CARTESIAN_POINT('Ctrl Pts',(100.713003318819,3.96059312724813,127.885164992536));
#46094=CARTESIAN_POINT('Ctrl Pts',(100.705256985554,3.87615623020115,127.777052251778));
#46095=CARTESIAN_POINT('Ctrl Pts',(100.697508917551,3.79170042409646,127.66891529992));
#46096=CARTESIAN_POINT('Ctrl Pts',(100.689760849547,3.70273856963225,127.564344138517));
#46097=CARTESIAN_POINT('Ctrl Pts',(100.682012781545,3.6096151578123,127.463722733121));
#46098=CARTESIAN_POINT('Ctrl Pts',(100.674256478803,3.51639277332208,127.362994386097));
#46099=CARTESIAN_POINT('Ctrl Pts',(100.666500176061,3.41900026213164,127.26622446813));
#46100=CARTESIAN_POINT('Ctrl Pts',(100.658743873319,3.31781944695446,127.173760504649));
#46101=CARTESIAN_POINT('Ctrl Pts',(100.650983430805,3.21658462852966,127.081247190367));
#46102=CARTESIAN_POINT('Ctrl Pts',(100.643222988291,3.1115577764932,126.993044661274));
#46103=CARTESIAN_POINT('Ctrl Pts',(100.635462545776,3.00315308913531,126.909459516676));
#46104=CARTESIAN_POINT('Ctrl Pts',(100.627689645511,2.89457438094963,126.825740193783));
#46105=CARTESIAN_POINT('Ctrl Pts',(100.619916745246,2.78260732127804,126.746653293083));
#46106=CARTESIAN_POINT('Ctrl Pts',(100.61214384498,2.6676950650687,126.672462010109));
#46107=CARTESIAN_POINT('Ctrl Pts',(100.604653509218,2.55696015881852,126.600967767147));
#46108=CARTESIAN_POINT('Ctrl Pts',(100.597163173456,2.44349073431964,126.534019541934));
#46109=CARTESIAN_POINT('Ctrl Pts',(100.589672837694,2.32770243283911,126.471811201038));
#46110=CARTESIAN_POINT('Ctrl Pts',(100.581898503575,2.20752398271535,126.40724421199));
#46111=CARTESIAN_POINT('Ctrl Pts',(100.574124169456,2.08446665481643,126.347579099044));
#46112=CARTESIAN_POINT('Ctrl Pts',(100.566349835337,1.95896827240795,126.293082930458));
#46113=CARTESIAN_POINT('Ctrl Pts',(100.55858508239,1.83362455553967,126.238653923529));
#46114=CARTESIAN_POINT('Ctrl Pts',(100.550820329442,1.7058461251156,126.189381340265));
#46115=CARTESIAN_POINT('Ctrl Pts',(100.543055576495,1.57609651256555,126.145487057833));
#46116=CARTESIAN_POINT('Ctrl Pts',(100.53529853561,1.44647576915993,126.101636371821));
#46117=CARTESIAN_POINT('Ctrl Pts',(100.527541494725,1.31488810770054,126.063153480686));
#46118=CARTESIAN_POINT('Ctrl Pts',(100.51978445384,1.18181788316917,126.030212572781));
#46119=CARTESIAN_POINT('Ctrl Pts',(100.5120332626,1.04884800792934,125.997296505871));
#46120=CARTESIAN_POINT('Ctrl Pts',(100.50428207136,0.914398172927853,125.969914197207));
#46121=CARTESIAN_POINT('Ctrl Pts',(100.49653088012,0.778968431447635,125.948190187556));
#46122=CARTESIAN_POINT('Ctrl Pts',(100.488782983343,0.643596251220161,125.926475411187));
#46123=CARTESIAN_POINT('Ctrl Pts',(100.481035086566,0.507245378095775,125.910414212405));
#46124=CARTESIAN_POINT('Ctrl Pts',(100.473287189789,0.370426395846859,125.900080104814));
#46125=CARTESIAN_POINT('Ctrl Pts',(100.465540913705,0.233636033179553,125.889748158895));
#46126=CARTESIAN_POINT('Ctrl Pts',(100.45779463762,0.0963781457603969,125.885140950738));
#46127=CARTESIAN_POINT('Ctrl Pts',(100.450048361536,-0.0408316108026457,
125.886280113746));
#46128=CARTESIAN_POINT('Ctrl Pts',(100.442302028271,-0.178042380216942,
125.887419285162));
#46129=CARTESIAN_POINT('Ctrl Pts',(100.434555695006,-0.315204627114432,
125.89430490914));
#46130=CARTESIAN_POINT('Ctrl Pts',(100.42680936174,-0.451803143166616,125.906906484823));
#46131=CARTESIAN_POINT('Ctrl Pts',(100.419061293737,-0.588432249509362,
125.91951088254));
#46132=CARTESIAN_POINT('Ctrl Pts',(100.411313225734,-0.724496984559048,
125.937833743201));
#46133=CARTESIAN_POINT('Ctrl Pts',(100.403565157731,-0.859488101419582,
125.961792779526));
#46134=CARTESIAN_POINT('Ctrl Pts',(100.395808854989,-0.994622688445529,
125.9857772798));
#46135=CARTESIAN_POINT('Ctrl Pts',(100.388052552248,-1.12868099234083,126.015409853366));
#46136=CARTESIAN_POINT('Ctrl Pts',(100.380296249506,-1.26116424561469,126.050557107945));
#46137=CARTESIAN_POINT('Ctrl Pts',(100.372535806992,-1.3937182091898,126.085723121672));
#46138=CARTESIAN_POINT('Ctrl Pts',(100.364775364477,-1.52469507389019,126.126409565364));
#46139=CARTESIAN_POINT('Ctrl Pts',(100.357014921963,-1.65361300474393,126.172433686683));
#46140=CARTESIAN_POINT('Ctrl Pts',(100.349242021698,-1.78273788610517,126.218531690006));
#46141=CARTESIAN_POINT('Ctrl Pts',(100.341469121432,-1.90979686622148,126.269984346747));
#46142=CARTESIAN_POINT('Ctrl Pts',(100.333696221167,-2.03432897516291,126.32656108171));
#46143=CARTESIAN_POINT('Ctrl Pts',(100.326205885405,-2.15433402826569,126.381081109848));
#46144=CARTESIAN_POINT('Ctrl Pts',(100.318715549643,-2.27199246179451,126.440358999271));
#46145=CARTESIAN_POINT('Ctrl Pts',(100.311225213881,-2.38691650605695,126.504149848823));
#46146=CARTESIAN_POINT('Ctrl Pts',(100.30344983315,-2.50621398853184,126.570368261213));
#46147=CARTESIAN_POINT('Ctrl Pts',(100.295674452419,-2.62294279564377,126.641659705483));
#46148=CARTESIAN_POINT('Ctrl Pts',(100.287899071688,-2.73664139615496,126.717800091726));
#46149=CARTESIAN_POINT('Ctrl Pts',(100.280133501568,-2.85019653710222,126.7938444076));
#46150=CARTESIAN_POINT('Ctrl Pts',(100.272367931448,-2.96072875769736,126.874725275215));
#46151=CARTESIAN_POINT('Ctrl Pts',(100.264602361327,-3.06780070301104,126.960172548662));
#46152=CARTESIAN_POINT('Ctrl Pts',(100.256846151872,-3.17474358315738,127.045516823451));
#46153=CARTESIAN_POINT('Ctrl Pts',(100.249089942417,-3.27823419171602,127.13541629879));
#46154=CARTESIAN_POINT('Ctrl Pts',(100.241333732962,-3.37786431027174,127.229557718959));
#46155=CARTESIAN_POINT('Ctrl Pts',(100.233582830663,-3.47742625730071,127.323634723221));
#46156=CARTESIAN_POINT('Ctrl Pts',(100.225831928365,-3.57313268662067,127.42194763052));
#46157=CARTESIAN_POINT('Ctrl Pts',(100.218081026066,-3.66460857344863,127.524143084245));
#46158=CARTESIAN_POINT('Ctrl Pts',(100.210333748674,-3.75604167925621,127.626290743672));
#46159=CARTESIAN_POINT('Ctrl Pts',(100.202586471281,-3.84324791968253,127.732317045537));
#46160=CARTESIAN_POINT('Ctrl Pts',(100.194839193889,-3.92588954582157,127.841832248671));
#46161=CARTESIAN_POINT('Ctrl Pts',(100.187093861953,-4.00851041942263,127.951319950913));
#46162=CARTESIAN_POINT('Ctrl Pts',(100.179348530017,-4.08656872574872,128.064294498307));
#46163=CARTESIAN_POINT('Ctrl Pts',(100.17160319808,-4.15976764618254,128.180333904235));
#46164=CARTESIAN_POINT('Ctrl Pts',(100.163855706677,-4.23298697512897,128.296405662987));
#46165=CARTESIAN_POINT('Ctrl Pts',(100.156108215273,-4.30134399763379,128.415543659899));
#46166=CARTESIAN_POINT('Ctrl Pts',(100.148360723869,-4.36458577743344,128.537297748141));
#46167=CARTESIAN_POINT('Ctrl Pts',(100.140612236397,-4.42783568800787,128.65906748988));
#46168=CARTESIAN_POINT('Ctrl Pts',(100.132863748925,-4.48596887283135,128.783453642227));
#46169=CARTESIAN_POINT('Ctrl Pts',(100.125115261453,-4.53877927208194,128.909983204847));
#46170=CARTESIAN_POINT('Ctrl Pts',(100.117360388149,-4.59163319445624,129.036617045448));
#46171=CARTESIAN_POINT('Ctrl Pts',(100.109605514844,-4.63915542495276,129.165397460993));
#46172=CARTESIAN_POINT('Ctrl Pts',(100.10185064154,-4.68118868151468,129.295832994167));
#46173=CARTESIAN_POINT('Ctrl Pts',(100.09621778385,-4.71172010906225,129.390576617584));
#46174=CARTESIAN_POINT('Ctrl Pts',(100.090584926161,-4.73935655762074,129.486193106731));
#46175=CARTESIAN_POINT('Ctrl Pts',(100.084952068471,-4.76405452823407,129.582490119308));
#46176=CARTESIAN_POINT('Ctrl Pts',(101.834907966042,-4.76405452823403,129.582490119308));
#46177=CARTESIAN_POINT('Ctrl Pts',(101.827263594172,-4.79771132031781,129.71371744083));
#46178=CARTESIAN_POINT('Ctrl Pts',(101.819619222302,-4.82593387413391,129.846305308646));
#46179=CARTESIAN_POINT('Ctrl Pts',(101.811974850433,-4.84863003077733,129.979757751245));
#46180=CARTESIAN_POINT('Ctrl Pts',(101.804122281366,-4.87194432534955,130.116844818761));
#46181=CARTESIAN_POINT('Ctrl Pts',(101.796269712299,-4.88942680470606,130.254843783683));
#46182=CARTESIAN_POINT('Ctrl Pts',(101.788417143233,-4.9010344707148,130.393210791632));
#46183=CARTESIAN_POINT('Ctrl Pts',(101.780564574166,-4.91264213672354,130.531577799582));
#46184=CARTESIAN_POINT('Ctrl Pts',(101.772712005099,-4.91837500595534,130.670312392003));
#46185=CARTESIAN_POINT('Ctrl Pts',(101.764859436032,-4.91824793163316,130.808871214656));
#46186=CARTESIAN_POINT('',(102.110140564045,-4.91824992859335,130.803522529585));
#46187=CARTESIAN_POINT('Ctrl Pts',(102.179855052771,-4.76405452823403,129.582490119308));
#46188=CARTESIAN_POINT('Ctrl Pts',(102.171602591026,-4.80023113444554,129.72354215787));
#46189=CARTESIAN_POINT('Ctrl Pts',(102.16335012928,-4.83017959017385,129.866359169411));
#46190=CARTESIAN_POINT('Ctrl Pts',(102.155097667534,-4.8537393744369,130.010385084227));
#46191=CARTESIAN_POINT('Ctrl Pts',(102.146865913599,-4.87724004039645,130.154049596424));
#46192=CARTESIAN_POINT('Ctrl Pts',(102.138634159663,-4.89438395406626,130.298916657161));
#46193=CARTESIAN_POINT('Ctrl Pts',(102.130402405727,-4.90506114365806,130.444418622967));
#46194=CARTESIAN_POINT('Ctrl Pts',(102.1236484585,-4.91382150938374,130.56379932922));
#46195=CARTESIAN_POINT('Ctrl Pts',(102.116894511272,-4.91822949455648,130.683607076022));
#46196=CARTESIAN_POINT('Ctrl Pts',(102.110140564044,-4.91824992859335,130.803522529585));
#46197=CARTESIAN_POINT('Ctrl Pts',(102.110140564008,-4.91824992859346,130.803522530233));
#46198=CARTESIAN_POINT('Ctrl Pts',(102.102122208341,-4.91827418807359,130.945887390996));
#46199=CARTESIAN_POINT('Ctrl Pts',(102.094103852674,-4.91211271718102,131.088167320966));
#46200=CARTESIAN_POINT('Ctrl Pts',(102.086085497007,-4.89981367422495,131.229812166368));
#46201=CARTESIAN_POINT('Ctrl Pts',(102.078059836677,-4.88750342692988,131.371586049198));
#46202=CARTESIAN_POINT('Ctrl Pts',(102.070034176346,-4.86904448769284,131.512723345161));
#46203=CARTESIAN_POINT('Ctrl Pts',(102.062008516015,-4.84453659176315,131.652681472884));
#46204=CARTESIAN_POINT('Ctrl Pts',(102.053701303064,-4.81916892080687,131.797549548949));
#46205=CARTESIAN_POINT('Ctrl Pts',(102.045394090112,-4.78732024247637,131.941153806296));
#46206=CARTESIAN_POINT('Ctrl Pts',(102.037086877161,-4.74915763238618,132.082908561621));
#46207=CARTESIAN_POINT('Ctrl Pts',(102.02903725149,-4.71217835574289,132.220267832916));
#46208=CARTESIAN_POINT('Ctrl Pts',(102.020987625819,-4.66927105687257,132.355890290011));
#46209=CARTESIAN_POINT('Ctrl Pts',(102.012938000147,-4.62063717517419,132.489262738729));
#46210=CARTESIAN_POINT('Ctrl Pts',(102.004501993556,-4.56966887387285,132.62903704656));
#46211=CARTESIAN_POINT('Ctrl Pts',(101.996065986965,-4.51241084531998,132.76633959036));
#46212=CARTESIAN_POINT('Ctrl Pts',(101.987629980373,-4.44914929363851,132.900608128099));
#46213=CARTESIAN_POINT('Ctrl Pts',(101.979193973782,-4.38588774195708,133.034876665838));
#46214=CARTESIAN_POINT('Ctrl Pts',(101.97075796719,-4.31662293608384,133.166110848154));
#46215=CARTESIAN_POINT('Ctrl Pts',(101.962321960599,-4.2416929995932,133.293782952105));
#46216=CARTESIAN_POINT('Ctrl Pts',(101.95454762648,-4.17264014200159,133.411441180918));
#46217=CARTESIAN_POINT('Ctrl Pts',(101.946773292361,-4.09857870427127,133.52641045983));
#46218=CARTESIAN_POINT('Ctrl Pts',(101.938998958242,-4.01974368913189,133.638234950733));
#46219=CARTESIAN_POINT('Ctrl Pts',(101.931234205295,-3.94100583110288,133.749921627945));
#46220=CARTESIAN_POINT('Ctrl Pts',(101.923469452348,-3.85750632420618,133.858470912103));
#46221=CARTESIAN_POINT('Ctrl Pts',(101.9157046994,-3.76952563487839,133.963452188017));
#46222=CARTESIAN_POINT('Ctrl Pts',(101.907947658515,-3.68163232921173,134.068329195048));
#46223=CARTESIAN_POINT('Ctrl Pts',(101.90019061763,-3.58926694785408,134.169644948438));
#46224=CARTESIAN_POINT('Ctrl Pts',(101.892433576745,-3.49275254847463,134.266998729992));
#46225=CARTESIAN_POINT('Ctrl Pts',(101.884682385505,-3.39631093135439,134.364279096302));
#46226=CARTESIAN_POINT('Ctrl Pts',(101.876931194265,-3.29572679805333,134.457603161193));
#46227=CARTESIAN_POINT('Ctrl Pts',(101.869180003025,-3.19136243912891,134.546604442415));
#46228=CARTESIAN_POINT('Ctrl Pts',(101.861432106248,-3.08704243784112,134.635567895717));
#46229=CARTESIAN_POINT('Ctrl Pts',(101.853684209471,-2.97894570338572,134.720211966438));
#46230=CARTESIAN_POINT('Ctrl Pts',(101.845936312694,-2.86747006322841,134.800208274696));
#46231=CARTESIAN_POINT('Ctrl Pts',(101.83819003661,-2.75601774137181,134.88018784945));
#46232=CARTESIAN_POINT('Ctrl Pts',(101.830443760526,-2.64118823710544,134.955521367725));
#46233=CARTESIAN_POINT('Ctrl Pts',(101.822697484442,-2.52341069653454,135.025922120033));
#46234=CARTESIAN_POINT('Ctrl Pts',(101.814951151176,-2.40563228655666,135.096323392024));
#46235=CARTESIAN_POINT('Ctrl Pts',(101.807204817911,-2.28490613243383,135.161791624795));
#46236=CARTESIAN_POINT('Ctrl Pts',(101.799458484645,-2.16168811742724,135.222084867163));
#46237=CARTESIAN_POINT('Ctrl Pts',(101.791710416642,-2.03844250860028,135.282391611784));
#46238=CARTESIAN_POINT('Ctrl Pts',(101.783962348639,-1.91270427957439,135.337520888111));
#46239=CARTESIAN_POINT('Ctrl Pts',(101.776214280636,-1.78495116042607,135.387278074535));
#46240=CARTESIAN_POINT('Ctrl Pts',(101.768457977895,-1.65706226374269,135.437088143489));
#46241=CARTESIAN_POINT('Ctrl Pts',(101.760701675153,-1.52715456405104,135.481514575038));
#46242=CARTESIAN_POINT('Ctrl Pts',(101.752945372411,-1.39572342517542,135.520411845332));
#46243=CARTESIAN_POINT('Ctrl Pts',(101.745184929897,-1.2642221375434,135.559329876271));
#46244=CARTESIAN_POINT('Ctrl Pts',(101.737424487382,-1.13119616956762,135.592712770561));
#46245=CARTESIAN_POINT('Ctrl Pts',(101.729664044868,-0.997152099810959,
135.620465968609));
#46246=CARTESIAN_POINT('Ctrl Pts',(101.721891144603,-0.862892850613838,
135.648263718554));
#46247=CARTESIAN_POINT('Ctrl Pts',(101.714118244337,-0.727612619738735,
135.670413649664));
#46248=CARTESIAN_POINT('Ctrl Pts',(101.706345344072,-0.591825042265724,
135.686872899358));
#46249=CARTESIAN_POINT('Ctrl Pts',(101.69885500831,-0.460973685263137,135.702733813866));
#46250=CARTESIAN_POINT('Ctrl Pts',(101.691364672548,-0.329651534934086,
135.713310580282));
#46251=CARTESIAN_POINT('Ctrl Pts',(101.683874336786,-0.198317161239635,
135.718610648451));
#46252=CARTESIAN_POINT('Ctrl Pts',(101.676100002667,-0.0620032048473757,
135.724111670316));
#46253=CARTESIAN_POINT('Ctrl Pts',(101.668325668548,0.0747557217455648,
135.723945388758));
#46254=CARTESIAN_POINT('Ctrl Pts',(101.660551334429,0.211449084311424,135.718063126596));
#46255=CARTESIAN_POINT('Ctrl Pts',(101.652786581482,0.347973984524278,135.712188113796));
#46256=CARTESIAN_POINT('Ctrl Pts',(101.645021828535,0.484433094627608,135.700611153365));
#46257=CARTESIAN_POINT('Ctrl Pts',(101.637257075588,0.620312526907382,135.683335451633));
#46258=CARTESIAN_POINT('Ctrl Pts',(101.629500034703,0.756057001819729,135.666076908372));
#46259=CARTESIAN_POINT('Ctrl Pts',(101.621742993818,0.891222559332021,135.643130936594));
#46260=CARTESIAN_POINT('Ctrl Pts',(101.613985952933,1.02529744331558,135.614552735895));
#46261=CARTESIAN_POINT('Ctrl Pts',(101.606234761692,1.15927122038591,135.585996086239));
#46262=CARTESIAN_POINT('Ctrl Pts',(101.598483570452,1.2921555802066,135.551815742842));
#46263=CARTESIAN_POINT('Ctrl Pts',(101.590732379212,1.4234463639851,135.512118418405));
#46264=CARTESIAN_POINT('Ctrl Pts',(101.582984482435,1.55468134567855,135.472437966389));
#46265=CARTESIAN_POINT('Ctrl Pts',(101.575236585658,1.68432372500326,135.427245310004));
#46266=CARTESIAN_POINT('Ctrl Pts',(101.567488688881,1.81188219120261,135.376697655417));
#46267=CARTESIAN_POINT('Ctrl Pts',(101.559742412797,1.93941397492059,135.32616057431));
#46268=CARTESIAN_POINT('Ctrl Pts',(101.551996136713,2.06486234932414,135.270270866981));
#46269=CARTESIAN_POINT('Ctrl Pts',(101.544249860629,2.18775413364865,135.209234612722));
#46270=CARTESIAN_POINT('Ctrl Pts',(101.536503527363,2.31064682513239,135.148197907907));
#46271=CARTESIAN_POINT('Ctrl Pts',(101.528757194098,2.43098253872352,135.082014754265));
#46272=CARTESIAN_POINT('Ctrl Pts',(101.521010860832,2.5483112979989,135.010937918768));
#46273=CARTESIAN_POINT('Ctrl Pts',(101.513262792829,2.66566633223666,134.939845166107));
#46274=CARTESIAN_POINT('Ctrl Pts',(101.505514724826,2.78001273786896,134.863856753399));
#46275=CARTESIAN_POINT('Ctrl Pts',(101.497766656824,2.89092854944727,134.783269410752));
#46276=CARTESIAN_POINT('Ctrl Pts',(101.490010354082,3.00196224366982,134.702596418918));
#46277=CARTESIAN_POINT('Ctrl Pts',(101.48225405134,3.10955774360974,134.617314963419));
#46278=CARTESIAN_POINT('Ctrl Pts',(101.474497748598,3.21332485968227,134.527763148672));
#46279=CARTESIAN_POINT('Ctrl Pts',(101.466737306084,3.31714735938924,134.438163537425));
#46280=CARTESIAN_POINT('Ctrl Pts',(101.45897686357,3.4171371188395,134.344289292863));
#46281=CARTESIAN_POINT('Ctrl Pts',(101.451216421055,3.51294076428022,134.246515502105));
#46282=CARTESIAN_POINT('Ctrl Pts',(101.44344352079,3.60889820223751,134.148584756179));
#46283=CARTESIAN_POINT('Ctrl Pts',(101.435670620525,3.70065583579107,134.046742245416));
#46284=CARTESIAN_POINT('Ctrl Pts',(101.427897720259,3.7878999711285,133.941396937283));
#46285=CARTESIAN_POINT('Ctrl Pts',(101.420407384497,3.87197256239157,133.83988119645));
#46286=CARTESIAN_POINT('Ctrl Pts',(101.412917048735,3.95185392550212,133.73511315274));
#46287=CARTESIAN_POINT('Ctrl Pts',(101.405426712973,4.02730245996136,133.627482640874));
#46288=CARTESIAN_POINT('Ctrl Pts',(101.397652378854,4.10561164853672,133.515771285438));
#46289=CARTESIAN_POINT('Ctrl Pts',(101.389878044735,4.17939329149829,133.400622248037));
#46290=CARTESIAN_POINT('Ctrl Pts',(101.382103710616,4.24833047913458,133.282438744372));
#46291=CARTESIAN_POINT('Ctrl Pts',(101.374338957669,4.31718270784833,133.164400891313));
#46292=CARTESIAN_POINT('Ctrl Pts',(101.366574204722,4.38120216537198,133.043336347365));
#46293=CARTESIAN_POINT('Ctrl Pts',(101.358809451774,4.44011378041843,132.919679193913));
#46294=CARTESIAN_POINT('Ctrl Pts',(101.351052410889,4.49896688361818,132.79614485849));
#46295=CARTESIAN_POINT('Ctrl Pts',(101.343295370004,4.55272207313581,132.670023388635));
#46296=CARTESIAN_POINT('Ctrl Pts',(101.335538329119,4.6011491732647,132.541775176002));
#46297=CARTESIAN_POINT('Ctrl Pts',(101.327787137879,4.64953975414088,132.413623676343));
#46298=CARTESIAN_POINT('Ctrl Pts',(101.320035946639,4.69261010556833,132.283348990438));
#46299=CARTESIAN_POINT('Ctrl Pts',(101.312284755399,4.73017749782027,132.151432962177));
#46300=CARTESIAN_POINT('Ctrl Pts',(101.304536858622,4.76772892292823,132.019573001747));
#46301=CARTESIAN_POINT('Ctrl Pts',(101.296788961845,4.79978193390504,131.88607346169));
#46302=CARTESIAN_POINT('Ctrl Pts',(101.289041065068,4.8262032272866,131.751432669433));
#46303=CARTESIAN_POINT('Ctrl Pts',(101.281294788984,4.85261899390317,131.616820041128));
#46304=CARTESIAN_POINT('Ctrl Pts',(101.2735485129,4.87340531086086,131.481067018867));
#46305=CARTESIAN_POINT('Ctrl Pts',(101.265802236815,4.8884797927422,131.344683093918));
#46306=CARTESIAN_POINT('Ctrl Pts',(101.25805590355,4.90355438589991,131.208298162214));
#46307=CARTESIAN_POINT('Ctrl Pts',(101.250309570285,4.91291701689544,131.071282707129));
#46308=CARTESIAN_POINT('Ctrl Pts',(101.242563237019,4.91653712249402,130.934151933293));
#46309=CARTESIAN_POINT('Ctrl Pts',(101.234815169016,4.92015803879016,130.796990449971));
#46310=CARTESIAN_POINT('Ctrl Pts',(101.227067101013,4.91803386038523,130.659713987266));
#46311=CARTESIAN_POINT('Ctrl Pts',(101.21931903301,4.91018615209169,130.52283794653));
#46312=CARTESIAN_POINT('Ctrl Pts',(101.211562730269,4.90233010316038,130.38581643231));
#46313=CARTESIAN_POINT('Ctrl Pts',(101.203806427527,4.88873839523614,130.249196581135));
#46314=CARTESIAN_POINT('Ctrl Pts',(101.196050124785,4.86948457814034,130.11348942425));
#46315=CARTESIAN_POINT('Ctrl Pts',(101.188289682271,4.85022048470262,129.97770983637));
#46316=CARTESIAN_POINT('Ctrl Pts',(101.180529239757,4.82528833146388,129.842844297696));
#46317=CARTESIAN_POINT('Ctrl Pts',(101.172768797242,4.79481268269693,129.709392855324));
#46318=CARTESIAN_POINT('Ctrl Pts',(101.164995896977,4.76428811171308,129.57572718485));
#46319=CARTESIAN_POINT('Ctrl Pts',(101.157222996712,4.72820236531896,129.443480524322));
#46320=CARTESIAN_POINT('Ctrl Pts',(101.149450096446,4.68672996025863,129.313137850132));
#46321=CARTESIAN_POINT('Ctrl Pts',(101.141959760684,4.6467651815851,129.187533460463));
#46322=CARTESIAN_POINT('Ctrl Pts',(101.134469424922,4.60179868719937,129.063697320594));
#46323=CARTESIAN_POINT('Ctrl Pts',(101.12697908916,4.55202786512049,128.942043411055));
#46324=CARTESIAN_POINT('Ctrl Pts',(101.119204755041,4.50036996719478,128.81577695656));
#46325=CARTESIAN_POINT('Ctrl Pts',(101.111430420922,4.44337260107701,128.691461503345));
#46326=CARTESIAN_POINT('Ctrl Pts',(101.103656086803,4.38120370611486,128.569581624461));
#46327=CARTESIAN_POINT('Ctrl Pts',(101.095891333856,4.31911142875964,128.447851951634));
#46328=CARTESIAN_POINT('Ctrl Pts',(101.088126580909,4.25186047976347,128.328552225725));
#46329=CARTESIAN_POINT('Ctrl Pts',(101.080361827962,4.17966738134106,128.212148503588));
#46330=CARTESIAN_POINT('Ctrl Pts',(101.072604787077,4.1075459861218,128.09586039527));
#46331=CARTESIAN_POINT('Ctrl Pts',(101.064847746192,4.0304924145653,127.982462896758));
#46332=CARTESIAN_POINT('Ctrl Pts',(101.057090705307,3.94876959161668,127.872398514328));
#46333=CARTESIAN_POINT('Ctrl Pts',(101.049339514067,3.86710839648473,127.762417132305));
#46334=CARTESIAN_POINT('Ctrl Pts',(101.041588322827,3.78078519066078,127.655764175967));
#46335=CARTESIAN_POINT('Ctrl Pts',(101.033837131587,3.69010659317586,127.552853829398));
#46336=CARTESIAN_POINT('Ctrl Pts',(101.02608923481,3.59946653651344,127.449987222472));
#46337=CARTESIAN_POINT('Ctrl Pts',(101.018341338032,3.50447502793151,127.350860354241));
#46338=CARTESIAN_POINT('Ctrl Pts',(101.010593441255,3.40547927062977,127.25585473483));
#46339=CARTESIAN_POINT('Ctrl Pts',(101.002847165171,3.30650422110637,127.160868988547));
#46340=CARTESIAN_POINT('Ctrl Pts',(100.995100889087,3.20352687080224,127.070003046907));
#46341=CARTESIAN_POINT('Ctrl Pts',(100.987354613003,3.09693133782097,126.983601615571));
#46342=CARTESIAN_POINT('Ctrl Pts',(100.979608279738,2.99033501797548,126.89719954644));
#46343=CARTESIAN_POINT('Ctrl Pts',(100.971861946472,2.88012076588038,126.815262299557));
#46344=CARTESIAN_POINT('Ctrl Pts',(100.964115613207,2.76670551760895,126.738094069326));
#46345=CARTESIAN_POINT('Ctrl Pts',(100.956367545204,2.65326487077887,126.660908557806));
#46346=CARTESIAN_POINT('Ctrl Pts',(100.948619477201,2.53662212451889,126.588494408001));
#46347=CARTESIAN_POINT('Ctrl Pts',(100.940871409198,2.41722255689327,126.521112063846));
#46348=CARTESIAN_POINT('Ctrl Pts',(100.933115106456,2.29769608998664,126.453658104934));
#46349=CARTESIAN_POINT('Ctrl Pts',(100.925358803714,2.17540728978875,126.391246827062));
#46350=CARTESIAN_POINT('Ctrl Pts',(100.917602500973,2.05082585683438,126.334092575553));
#46351=CARTESIAN_POINT('Ctrl Pts',(100.909842058458,1.926177931018,126.2769078191));
#46352=CARTESIAN_POINT('Ctrl Pts',(100.902081615944,1.79923529591329,126.224985827807));
#46353=CARTESIAN_POINT('Ctrl Pts',(100.89432117343,1.67048598533729,126.178492089896));
#46354=CARTESIAN_POINT('Ctrl Pts',(100.886548273165,1.5415299949383,126.131923716108));
#46355=CARTESIAN_POINT('Ctrl Pts',(100.878775372899,1.41076190664602,126.090801126231));
#46356=CARTESIAN_POINT('Ctrl Pts',(100.871002472634,1.27868407539881,126.055239635971));
#46357=CARTESIAN_POINT('Ctrl Pts',(100.863512136872,1.1514076060016,126.020970895457));
#46358=CARTESIAN_POINT('Ctrl Pts',(100.85602180111,1.02291526572459,125.991866022236));
#46359=CARTESIAN_POINT('Ctrl Pts',(100.848531465348,0.8936620411581,125.967982714766));
#46360=CARTESIAN_POINT('Ctrl Pts',(100.840757131229,0.759508141296226,125.943193864434));
#46361=CARTESIAN_POINT('Ctrl Pts',(100.83298279711,0.62410956108497,125.923951823762));
#46362=CARTESIAN_POINT('Ctrl Pts',(100.82520846299,0.487964760875024,125.91037722419));
#46363=CARTESIAN_POINT('Ctrl Pts',(100.817443710043,0.351987746964005,125.896819354098));
#46364=CARTESIAN_POINT('Ctrl Pts',(100.809678957096,0.215266728184087,125.888915066222));
#46365=CARTESIAN_POINT('Ctrl Pts',(100.801914204149,0.078310846914143,125.886734109406));
#46366=CARTESIAN_POINT('Ctrl Pts',(100.794157163264,-0.0585090078438774,
125.884555318747));
#46367=CARTESIAN_POINT('Ctrl Pts',(100.786400122379,-0.195562872490565,
125.888088552935));
#46368=CARTESIAN_POINT('Ctrl Pts',(100.778643081494,-0.332336336609006,
125.897351791217));
#46369=CARTESIAN_POINT('Ctrl Pts',(100.770891890254,-0.469006658793839,
125.906608044019));
#46370=CARTESIAN_POINT('Ctrl Pts',(100.763140699014,-0.60539661283996,125.921585673834));
#46371=CARTESIAN_POINT('Ctrl Pts',(100.755389507774,-0.740991998868861,
125.942250590005));
#46372=CARTESIAN_POINT('Ctrl Pts',(100.747641610997,-0.876529753241944,
125.962906723035));
#46373=CARTESIAN_POINT('Ctrl Pts',(100.73989371422,-1.01127322558911,125.989245275916));
#46374=CARTESIAN_POINT('Ctrl Pts',(100.732145817443,-1.14471376882555,126.021180352307));
#46375=CARTESIAN_POINT('Ctrl Pts',(100.724399541358,-1.27812639917681,126.053108748568));
#46376=CARTESIAN_POINT('Ctrl Pts',(100.716653265274,-1.41023626253643,126.090631248869));
#46377=CARTESIAN_POINT('Ctrl Pts',(100.70890698919,-1.54054572305174,126.133611005599));
#46378=CARTESIAN_POINT('Ctrl Pts',(100.701160655925,-1.67085614548207,126.176591079596));
#46379=CARTESIAN_POINT('Ctrl Pts',(100.69341432266,-1.79936576725781,126.225028367945));
#46380=CARTESIAN_POINT('Ctrl Pts',(100.685667989394,-1.92559329688056,126.278736515024));
#46381=CARTESIAN_POINT('Ctrl Pts',(100.677919921391,-2.05184909428363,126.33245668967));
#46382=CARTESIAN_POINT('Ctrl Pts',(100.670171853388,-2.17582142290059,126.391449918809));
#46383=CARTESIAN_POINT('Ctrl Pts',(100.662423785385,-2.29705048020335,126.455482353703));
#46384=CARTESIAN_POINT('Ctrl Pts',(100.654667482643,-2.41840838119069,126.519582843031));
#46385=CARTESIAN_POINT('Ctrl Pts',(100.646911179901,-2.53701684042041,126.588733053866));
#46386=CARTESIAN_POINT('Ctrl Pts',(100.63915487716,-2.65244163848967,126.66265367273));
#46387=CARTESIAN_POINT('Ctrl Pts',(100.631394434645,-2.76792804224895,126.736613745253));
#46388=CARTESIAN_POINT('Ctrl Pts',(100.623633992131,-2.88022707905069,126.81534907481));
#46389=CARTESIAN_POINT('Ctrl Pts',(100.615873549617,-2.98893572476966,126.898538515153));
#46390=CARTESIAN_POINT('Ctrl Pts',(100.608100649352,-3.09781887925745,126.981861498572));
#46391=CARTESIAN_POINT('Ctrl Pts',(100.600327749086,-3.20309982468353,127.069652630493));
#46392=CARTESIAN_POINT('Ctrl Pts',(100.592554848821,-3.30441000756219,127.161551596436));
#46393=CARTESIAN_POINT('Ctrl Pts',(100.585064513059,-3.40203731010833,127.250109803489));
#46394=CARTESIAN_POINT('Ctrl Pts',(100.577574177297,-3.49597731276188,127.342482153554));
#46395=CARTESIAN_POINT('Ctrl Pts',(100.570083841535,-3.58593554081042,127.438317040954));
#46396=CARTESIAN_POINT('Ctrl Pts',(100.562402357742,-3.67818943872558,127.536597566379));
#46397=CARTESIAN_POINT('Ctrl Pts',(100.55472087395,-3.76656340649161,127.638847946972));
#46398=CARTESIAN_POINT('Ctrl Pts',(100.547039390158,-3.85069011045177,127.744725224947));
#46399=CARTESIAN_POINT('Ctrl Pts',(100.539367008347,-3.934717130587,127.8504770463));
#46400=CARTESIAN_POINT('Ctrl Pts',(100.531694626536,-4.01450664646612,127.959846909533));
#46401=CARTESIAN_POINT('Ctrl Pts',(100.524022244724,-4.08972787390997,128.072454876172));
#46402=CARTESIAN_POINT('Ctrl Pts',(100.516200057596,-4.1664178160439,128.187261543635));
#46403=CARTESIAN_POINT('Ctrl Pts',(100.508377870467,-4.23835890669656,128.305433798632));
#46404=CARTESIAN_POINT('Ctrl Pts',(100.500555683338,-4.30524298001553,128.426532628512));
#46405=CARTESIAN_POINT('Ctrl Pts',(100.492896842392,-4.37073035215044,128.545102621994));
#46406=CARTESIAN_POINT('Ctrl Pts',(100.485238001445,-4.43136962217265,128.666477797822));
#46407=CARTESIAN_POINT('Ctrl Pts',(100.477579160499,-4.48691512220699,128.790216693064));
#46408=CARTESIAN_POINT('Ctrl Pts',(100.469675300279,-4.5442376167169,128.91791420481));
#46409=CARTESIAN_POINT('Ctrl Pts',(100.461771440059,-4.59613473198388,129.048128836655));
#46410=CARTESIAN_POINT('Ctrl Pts',(100.453867579839,-4.64238822044992,129.180348710858));
#46411=CARTESIAN_POINT('Ctrl Pts',(100.445963719619,-4.68864170891593,129.312568585062));
#46412=CARTESIAN_POINT('Ctrl Pts',(100.4380598594,-4.72925140293648,129.446793261984));
#46413=CARTESIAN_POINT('Ctrl Pts',(100.43015599918,-4.76405452823403,129.582490119308));
#46414=CARTESIAN_POINT('Origin',(213.235140564004,0.,130.804360617566));
#46415=CARTESIAN_POINT('',(98.3346394208835,-4.76405452823406,129.582490119308));
#46416=CARTESIAN_POINT('',(98.680234964937,-4.76405452823403,129.582490119308));
#46417=CARTESIAN_POINT('',(213.235140564004,-4.76405452823405,129.582490119308));
#46418=CARTESIAN_POINT('',(100.014859435958,-4.91824963103853,130.802455548176));
#46419=CARTESIAN_POINT('Ctrl Pts',(100.014859435958,-4.91824963103853,130.802455548176));
#46420=CARTESIAN_POINT('Ctrl Pts',(100.007159673393,-4.91830200268018,130.937661545693));
#46421=CARTESIAN_POINT('Ctrl Pts',(99.9994599108281,-4.91277480486665,131.073095304347));
#46422=CARTESIAN_POINT('Ctrl Pts',(99.991760148263,-4.90163791460517,131.208252702912));
#46423=CARTESIAN_POINT('Ctrl Pts',(99.984069510433,-4.89051422230582,131.343249930892));
#46424=CARTESIAN_POINT('Ctrl Pts',(99.9763788726031,-4.8737940927686,131.477971056342));
#46425=CARTESIAN_POINT('Ctrl Pts',(99.9686882347731,-4.85149938723206,131.611910466298));
#46426=CARTESIAN_POINT('Ctrl Pts',(99.9610047852629,-4.82922552021042,131.745724685168));
#46427=CARTESIAN_POINT('Ctrl Pts',(99.9533213357526,-4.80138750806904,131.878758250946));
#46428=CARTESIAN_POINT('Ctrl Pts',(99.9456378862424,-4.76805909856987,132.010509652737));
#46429=CARTESIAN_POINT('Ctrl Pts',(99.9376667229096,-4.73348267617179,132.147194606755));
#46430=CARTESIAN_POINT('Ctrl Pts',(99.9296955595768,-4.69299668467984,132.282499065602));
#46431=CARTESIAN_POINT('Ctrl Pts',(99.921724396244,-4.64674198262771,132.415872953661));
#46432=CARTESIAN_POINT('Ctrl Pts',(99.91404874757,-4.60220207952328,132.544302276243));
#46433=CARTESIAN_POINT('Ctrl Pts',(99.906373098896,-4.55231370292702,132.670941207271));
#46434=CARTESIAN_POINT('Ctrl Pts',(99.898697450222,-4.49725357121119,132.795313499662));
#46435=CARTESIAN_POINT('Ctrl Pts',(99.8910226996253,-4.44219988172028,132.919671240068));
#46436=CARTESIAN_POINT('Ctrl Pts',(99.8833479490286,-4.38197580186486,133.041762504411));
#46437=CARTESIAN_POINT('Ctrl Pts',(99.875673198432,-4.31680598721369,133.161131529483));
#46438=CARTESIAN_POINT('Ctrl Pts',(99.8679976074016,-4.25162903605579,133.280513626217));
#46439=CARTESIAN_POINT('Ctrl Pts',(99.8603220163711,-4.18150546430801,133.397172540643));
#46440=CARTESIAN_POINT('Ctrl Pts',(99.8526464253407,-4.10670537338365,133.510678048822));
#46441=CARTESIAN_POINT('Ctrl Pts',(99.8449682550301,-4.03188014688457,133.624221699016));
#46442=CARTESIAN_POINT('Ctrl Pts',(99.8372900847196,-3.95237549516136,133.734609502517));
#46443=CARTESIAN_POINT('Ctrl Pts',(99.829611914409,-3.86850392847026,133.841441521643));
#46444=CARTESIAN_POINT('Ctrl Pts',(99.8219253177721,-3.78454031782061,133.948390782432));
#46445=CARTESIAN_POINT('Ctrl Pts',(99.8142387211352,-3.69620047320614,134.05177615626));
#46446=CARTESIAN_POINT('Ctrl Pts',(99.8065521244983,-3.60383634289496,134.15123179467));
#46447=CARTESIAN_POINT('Ctrl Pts',(99.7988605133256,-3.51141195662625,134.250752315353));
#46448=CARTESIAN_POINT('Ctrl Pts',(99.7911689021529,-3.41495834033394,134.346337716751));
#46449=CARTESIAN_POINT('Ctrl Pts',(99.7834772909802,-3.31486221150036,134.437660987927));
#46450=CARTESIAN_POINT('Ctrl Pts',(99.7757748872528,-3.21462563186727,134.529112400188));
#46451=CARTESIAN_POINT('Ctrl Pts',(99.7680724835255,-3.11073664445713,134.616289492766));
#46452=CARTESIAN_POINT('Ctrl Pts',(99.7603700797981,-3.00361294062392,134.698907107906));
#46453=CARTESIAN_POINT('Ctrl Pts',(99.7583567086171,-2.97561132116425,134.720502953988));
#46454=CARTESIAN_POINT('Ctrl Pts',(99.7563433374361,-2.94738882210631,134.741787501222));
#46455=CARTESIAN_POINT('Ctrl Pts',(99.7543299662552,-2.91895318845925,134.762756169565));
#46456=CARTESIAN_POINT('Ctrl Pts',(99.7465556321361,-2.80915320773641,134.843723571537));
#46457=CARTESIAN_POINT('Ctrl Pts',(99.738781298017,-2.69580788640631,134.920247226605));
#46458=CARTESIAN_POINT('Ctrl Pts',(99.7310069638979,-2.57931271909312,134.992000640255));
#46459=CARTESIAN_POINT('Ctrl Pts',(99.7232422109509,-2.46296112166225,135.063665624235));
#46460=CARTESIAN_POINT('Ctrl Pts',(99.7154774580038,-2.34346773177088,135.130571860979));
#46461=CARTESIAN_POINT('Ctrl Pts',(99.7077127050567,-2.22125990484847,135.192433941659));
#46462=CARTESIAN_POINT('Ctrl Pts',(99.6999556641717,-2.09917345646267,135.254234580047));
#46463=CARTESIAN_POINT('Ctrl Pts',(99.6921986232867,-1.97437828280437,135.31100085692));
#46464=CARTESIAN_POINT('Ctrl Pts',(99.6844415824017,-1.8473291193632,135.362491614724));
#46465=CARTESIAN_POINT('Ctrl Pts',(99.6766903911616,-1.72037576468422,135.413943542948));
#46466=CARTESIAN_POINT('Ctrl Pts',(99.6689391999214,-1.59117216434632,135.460127724433));
#46467=CARTESIAN_POINT('Ctrl Pts',(99.6611880086813,-1.46019563847152,135.50084991915));
#46468=CARTESIAN_POINT('Ctrl Pts',(99.6534401119042,-1.32927478111422,135.541554805847));
#46469=CARTESIAN_POINT('Ctrl Pts',(99.6456922151272,-1.19658286951013,135.576802207212));
#46470=CARTESIAN_POINT('Ctrl Pts',(99.6379443183501,-1.06261488866523,135.606446899682));
#46471=CARTESIAN_POINT('Ctrl Pts',(99.630198042266,-0.928674931034093,135.636085391122));
#46472=CARTESIAN_POINT('Ctrl Pts',(99.6224517661819,-0.793459816582142,
135.660123420356));
#46473=CARTESIAN_POINT('Ctrl Pts',(99.6147054900978,-0.657476912834559,
135.678466399306));
#46474=CARTESIAN_POINT('Ctrl Pts',(99.6069591568325,-0.521493005292072,
135.696809513659));
#46475=CARTESIAN_POINT('Ctrl Pts',(99.5992128235672,-0.384741684600638,
135.709457441578));
#46476=CARTESIAN_POINT('Ctrl Pts',(99.5914664903018,-0.247737273592604,
135.716367265136));
#46477=CARTESIAN_POINT('Ctrl Pts',(99.5837184222989,-0.11070218139702,135.723278636102));
#46478=CARTESIAN_POINT('Ctrl Pts',(99.5759703542959,0.0265857235032949,
135.724449326));
#46479=CARTESIAN_POINT('Ctrl Pts',(99.568222286293,0.163610670680727,135.719888525221));
#46480=CARTESIAN_POINT('Ctrl Pts',(99.5604659835511,0.300781249603198,135.71532287717));
#46481=CARTESIAN_POINT('Ctrl Pts',(99.5527096808093,0.437687921150294,135.705013583047));
#46482=CARTESIAN_POINT('Ctrl Pts',(99.5449533780674,0.573818036248256,135.689021908155));
#46483=CARTESIAN_POINT('Ctrl Pts',(99.5371929355533,0.710020808087536,135.673021698024));
#46484=CARTESIAN_POINT('Ctrl Pts',(99.5294324930391,0.84544581175113,135.651333125692));
#46485=CARTESIAN_POINT('Ctrl Pts',(99.5216720505249,0.979590154943948,135.62406871981));
#46486=CARTESIAN_POINT('Ctrl Pts',(99.5138991502595,1.11394983854523,135.596760546683));
#46487=CARTESIAN_POINT('Ctrl Pts',(99.5061262499941,1.24702437371728,135.563858747301));
#46488=CARTESIAN_POINT('Ctrl Pts',(99.4983533497286,1.3783247358068,135.525526150055));
#46489=CARTESIAN_POINT('Ctrl Pts',(99.4908630139665,1.50485199900952,135.488587039273));
#46490=CARTESIAN_POINT('Ctrl Pts',(99.4833726782045,1.62973154901008,135.446605220029));
#46491=CARTESIAN_POINT('Ctrl Pts',(99.4758823424424,1.75254478772631,135.399768089109));
#46492=CARTESIAN_POINT('Ctrl Pts',(99.4681080083233,1.88001452771585,135.351155114135));
#46493=CARTESIAN_POINT('Ctrl Pts',(99.4603336742042,2.0056619607795,135.297157389952));
#46494=CARTESIAN_POINT('Ctrl Pts',(99.4525593400851,2.12899862333067,135.237931179129));
#46495=CARTESIAN_POINT('Ctrl Pts',(99.4447945871381,2.25218328446766,135.178777959318));
#46496=CARTESIAN_POINT('Ctrl Pts',(99.437029834191,2.37306249234812,135.11440924141));
#46497=CARTESIAN_POINT('Ctrl Pts',(99.429265081244,2.49116512839206,135.045030301187));
#46498=CARTESIAN_POINT('Ctrl Pts',(99.421508040359,2.60915046323331,134.975720269106));
#46499=CARTESIAN_POINT('Ctrl Pts',(99.413750999474,2.72436437932463,134.901410114367));
#46500=CARTESIAN_POINT('Ctrl Pts',(99.405993958589,2.83635818834796,134.82235206727));
#46501=CARTESIAN_POINT('Ctrl Pts',(99.3982427673489,2.94826754196849,134.743353638461));
#46502=CARTESIAN_POINT('Ctrl Pts',(99.3904915761088,3.05696130381164,134.659614668465));
#46503=CARTESIAN_POINT('Ctrl Pts',(99.3827403848687,3.16201805105393,134.571431748738));
#46504=CARTESIAN_POINT('Ctrl Pts',(99.3749924880916,3.26703014637637,134.483286309104));
#46505=CARTESIAN_POINT('Ctrl Pts',(99.3672445913145,3.36840800280452,134.390700927245));
#46506=CARTESIAN_POINT('Ctrl Pts',(99.3594966945374,3.46576188815781,134.294013551182));
#46507=CARTESIAN_POINT('Ctrl Pts',(99.3517504184533,3.56309540917699,134.197346400034));
#46508=CARTESIAN_POINT('Ctrl Pts',(99.3440041423693,3.65640635613809,134.096579236717));
#46509=CARTESIAN_POINT('Ctrl Pts',(99.3362578662852,3.74534090487162,133.992087796732));
#46510=CARTESIAN_POINT('Ctrl Pts',(99.3285115330198,3.83427611009972,133.887595585416));
#46511=CARTESIAN_POINT('Ctrl Pts',(99.3207651997545,3.91883459923561,133.779379340302));
#46512=CARTESIAN_POINT('Ctrl Pts',(99.3130188664891,3.99870226016051,133.66784857757));
#46513=CARTESIAN_POINT('Ctrl Pts',(99.3052707984862,4.07858780689437,133.556292838296));
#46514=CARTESIAN_POINT('Ctrl Pts',(99.2975227304832,4.15378020750377,133.441421422194));
#46515=CARTESIAN_POINT('Ctrl Pts',(99.2897746624802,4.22400840761036,133.32367322916));
#46516=CARTESIAN_POINT('Ctrl Pts',(99.2820183597384,4.29431124708375,133.205799891946));
#46517=CARTESIAN_POINT('Ctrl Pts',(99.2742620569965,4.35963914606689,133.085044006483));
#46518=CARTESIAN_POINT('Ctrl Pts',(99.2665057542547,4.41976654944531,132.961869994348));
#46519=CARTESIAN_POINT('Ctrl Pts',(99.2587453117405,4.47992604462927,132.838630240535));
#46520=CARTESIAN_POINT('Ctrl Pts',(99.2509848692264,4.5348793568942,132.712970146399));
#46521=CARTESIAN_POINT('Ctrl Pts',(99.2432244267122,4.58444933421086,132.585373633957));
#46522=CARTESIAN_POINT('Ctrl Pts',(99.2354515264468,4.63409888565576,132.457572292265));
#46523=CARTESIAN_POINT('Ctrl Pts',(99.2276786261814,4.67834770679495,132.327828690721));
#46524=CARTESIAN_POINT('Ctrl Pts',(99.2199057259159,4.71706845999541,132.196642272339));
#46525=CARTESIAN_POINT('Ctrl Pts',(99.2124153901538,4.75438161628592,132.070224810701));
#46526=CARTESIAN_POINT('Ctrl Pts',(99.2049250543917,4.78656156989748,131.942467909748));
#46527=CARTESIAN_POINT('Ctrl Pts',(99.1974347186295,4.81353972056436,131.81382504044));
#46528=CARTESIAN_POINT('Ctrl Pts',(99.1896603845104,4.84154075601318,131.680304637645));
#46529=CARTESIAN_POINT('Ctrl Pts',(99.1818860503913,4.86402644804321,131.5454068048));
#46530=CARTESIAN_POINT('Ctrl Pts',(99.1741117162723,4.88086423827874,131.409626963889));
#46531=CARTESIAN_POINT('Ctrl Pts',(99.1663469633251,4.89768127744267,131.274014459498));
#46532=CARTESIAN_POINT('Ctrl Pts',(99.1585822103781,4.90886421654812,131.137522494107));
#46533=CARTESIAN_POINT('Ctrl Pts',(99.150817457431,4.9143311088241,131.000658389697));
#46534=CARTESIAN_POINT('Ctrl Pts',(99.143060416546,4.91979257130559,130.863930220645));
#46535=CARTESIAN_POINT('Ctrl Pts',(99.1353033756609,4.91954926945457,130.726831036248));
#46536=CARTESIAN_POINT('Ctrl Pts',(99.1275463347759,4.9135708847692,130.589874667331));
#46537=CARTESIAN_POINT('Ctrl Pts',(99.1197951435358,4.90759700843023,130.453021578277));
#46538=CARTESIAN_POINT('Ctrl Pts',(99.1120439522957,4.89589667463061,130.31631147935));
#46539=CARTESIAN_POINT('Ctrl Pts',(99.1042927610556,4.87849162483249,130.180259240433));
#46540=CARTESIAN_POINT('Ctrl Pts',(99.0965448642785,4.86109397264482,130.044264827347));
#46541=CARTESIAN_POINT('Ctrl Pts',(99.0887969675014,4.83799647642319,129.908928105145));
#46542=CARTESIAN_POINT('Ctrl Pts',(99.0810490707244,4.80927280164692,129.77475963571));
#46543=CARTESIAN_POINT('Ctrl Pts',(99.0733027946403,4.78055513524419,129.640619231426));
#46544=CARTESIAN_POINT('Ctrl Pts',(99.0655565185561,4.74621371295018,129.507646975896));
#46545=CARTESIAN_POINT('Ctrl Pts',(99.057810242472,4.70637340107757,129.376343645633));
#46546=CARTESIAN_POINT('Ctrl Pts',(99.0500639092067,4.6665327951129,129.245039346118));
#46547=CARTESIAN_POINT('Ctrl Pts',(99.0423175759414,4.62119333208913,129.115404370574));
#46548=CARTESIAN_POINT('Ctrl Pts',(99.034571242676,4.57052976429298,128.987924343921));
#46549=CARTESIAN_POINT('Ctrl Pts',(99.0268231746731,4.51985485074218,128.860415769001));
#46550=CARTESIAN_POINT('Ctrl Pts',(99.0190751066701,4.46385360425319,128.735063466515));
#46551=CARTESIAN_POINT('Ctrl Pts',(99.0113270386671,4.40274877222889,128.612332718305));
#46552=CARTESIAN_POINT('Ctrl Pts',(99.0035707359253,4.3415789972618,128.489471530396));
#46553=CARTESIAN_POINT('Ctrl Pts',(98.9958144331834,4.27529497596077,128.36923781308));
#46554=CARTESIAN_POINT('Ctrl Pts',(98.9880581304416,4.20416552130183,128.25207236347));
#46555=CARTESIAN_POINT('Ctrl Pts',(98.9802976879274,4.13299810271118,128.134844379131));
#46556=CARTESIAN_POINT('Ctrl Pts',(98.9725372454132,4.05698031422455,128.020688250865));
#46557=CARTESIAN_POINT('Ctrl Pts',(98.964776802899,3.97642353813905,127.910014593361));
#46558=CARTESIAN_POINT('Ctrl Pts',(98.9570039026336,3.89573744516513,127.799163272676));
#46559=CARTESIAN_POINT('Ctrl Pts',(98.9492310023682,3.81049804731964,127.691805900461));
#46560=CARTESIAN_POINT('Ctrl Pts',(98.9414581021027,3.72105671105376,127.588319570623));
#46561=CARTESIAN_POINT('Ctrl Pts',(98.9339677663407,3.63486679264991,127.48859522954));
#46562=CARTESIAN_POINT('Ctrl Pts',(98.9264774305786,3.54477534458148,127.392465597583));
#46563=CARTESIAN_POINT('Ctrl Pts',(98.9189870948165,3.45112680469209,127.30023350223));
#46564=CARTESIAN_POINT('Ctrl Pts',(98.9112127606974,3.35392755194935,127.204504398948));
#46565=CARTESIAN_POINT('Ctrl Pts',(98.9034384265783,3.25258825045728,127.112670975699));
#46566=CARTESIAN_POINT('Ctrl Pts',(98.8956640924592,3.14745406172249,127.025112545284));
#46567=CARTESIAN_POINT('Ctrl Pts',(98.8878993395122,3.04244944147934,126.937662022809));
#46568=CARTESIAN_POINT('Ctrl Pts',(98.8801345865651,2.93365953708844,126.854476258127));
#46569=CARTESIAN_POINT('Ctrl Pts',(98.872369833618,2.82146687866708,126.7758984153));
#46570=CARTESIAN_POINT('Ctrl Pts',(98.864612792733,2.70938565157577,126.697398617094));
#46571=CARTESIAN_POINT('Ctrl Pts',(98.856855751848,2.59390871429774,126.623497855831));
#46572=CARTESIAN_POINT('Ctrl Pts',(98.8490987109631,2.47545197936939,126.554499377439));
#46573=CARTESIAN_POINT('Ctrl Pts',(98.841347519723,2.35708457358679,126.485552931336));
#46574=CARTESIAN_POINT('Ctrl Pts',(98.8335963284829,2.23574217931364,126.421501605732));
#46575=CARTESIAN_POINT('Ctrl Pts',(98.8258451372428,2.11186972295615,126.362605408669));
#46576=CARTESIAN_POINT('Ctrl Pts',(98.8180972404657,1.98804991569626,126.303734244061));
#46577=CARTESIAN_POINT('Ctrl Pts',(98.8103493436886,1.86170253747707,126.250014017653));
#46578=CARTESIAN_POINT('Ctrl Pts',(98.8026014469116,1.73329695646108,126.201658723762));
#46579=CARTESIAN_POINT('Ctrl Pts',(98.7948551708274,1.60491823512436,126.153313544756));
#46580=CARTESIAN_POINT('Ctrl Pts',(98.7871088947433,1.47448253299151,126.11033120379));
#46581=CARTESIAN_POINT('Ctrl Pts',(98.7793626186592,1.34247866081608,126.072877329235));
#46582=CARTESIAN_POINT('Ctrl Pts',(98.7716162853939,1.21047381421841,126.035423178204));
#46583=CARTESIAN_POINT('Ctrl Pts',(98.7638699521285,1.07690115059797,126.003497681735));
#46584=CARTESIAN_POINT('Ctrl Pts',(98.7561236188632,0.942263697832593,125.97721630791));
#46585=CARTESIAN_POINT('Ctrl Pts',(98.7483755508602,0.807596093943093,125.950929048553));
#46586=CARTESIAN_POINT('Ctrl Pts',(98.7406274828573,0.671863610066019,125.930288501868));
#46587=CARTESIAN_POINT('Ctrl Pts',(98.7328794148543,0.535578101404049,125.915358760357));
#46588=CARTESIAN_POINT('Ctrl Pts',(98.7251231121125,0.399147746881654,125.900413151338));
#46589=CARTESIAN_POINT('Ctrl Pts',(98.7173668093706,0.262163582717695,125.891190514639));
#46590=CARTESIAN_POINT('Ctrl Pts',(98.7096105066288,0.125141763985987,125.887702951894));
#46591=CARTESIAN_POINT('Ctrl Pts',(98.7018500641146,-0.0119531874161191,
125.884213527733));
#46592=CARTESIAN_POINT('Ctrl Pts',(98.6940896216004,-0.149085442710467,
125.886465270376));
#46593=CARTESIAN_POINT('Ctrl Pts',(98.6863291790862,-0.285741230392769,
125.894418152348));
#46594=CARTESIAN_POINT('Ctrl Pts',(98.6785562788208,-0.422616390077281,
125.902383800991));
#46595=CARTESIAN_POINT('Ctrl Pts',(98.6707833785554,-0.559013164463572,
125.916068838473));
#46596=CARTESIAN_POINT('Ctrl Pts',(98.6630104782899,-0.694424371619658,
125.935381478711));
#46597=CARTESIAN_POINT('Ctrl Pts',(98.6555201425279,-0.824913040315651,
125.953992055832));
#46598=CARTESIAN_POINT('Ctrl Pts',(98.6480298067659,-0.954486250500531,
125.977828128445));
#46599=CARTESIAN_POINT('Ctrl Pts',(98.6405394710038,-1.08270304777291,126.006763596885));
#46600=CARTESIAN_POINT('Ctrl Pts',(98.6327651368848,-1.21578122388396,126.036796162407));
#46601=CARTESIAN_POINT('Ctrl Pts',(98.6249908027657,-1.34781965152687,126.072417578408));
#46602=CARTESIAN_POINT('Ctrl Pts',(98.6172164686466,-1.47831263587522,126.113542478572));
#46603=CARTESIAN_POINT('Ctrl Pts',(98.6094517156995,-1.60864479928285,126.154616695973));
#46604=CARTESIAN_POINT('Ctrl Pts',(98.6016869627524,-1.73743493971715,126.201180785891));
#46605=CARTESIAN_POINT('Ctrl Pts',(98.5939222098053,-1.86418757666274,126.253098403464));
#46606=CARTESIAN_POINT('Ctrl Pts',(98.5861651689203,-1.99081432110224,126.304964455726));
#46607=CARTESIAN_POINT('Ctrl Pts',(98.5784081280354,-2.11540722981075,126.362173306946));
#46608=CARTESIAN_POINT('Ctrl Pts',(98.5706510871504,-2.23748636251614,126.424538949957));
#46609=CARTESIAN_POINT('Ctrl Pts',(98.5628998959103,-2.35947343439792,126.486857562552));
#46610=CARTESIAN_POINT('Ctrl Pts',(98.5551487046702,-2.47895015671362,126.55432504942));
#46611=CARTESIAN_POINT('Ctrl Pts',(98.5473975134301,-2.59545728374445,126.626707622072));
#46612=CARTESIAN_POINT('Ctrl Pts',(98.539649616653,-2.7119148921386,126.6990594302));
#46613=CARTESIAN_POINT('Ctrl Pts',(98.5319017198759,-2.82540508418448,126.776321963277));
#46614=CARTESIAN_POINT('Ctrl Pts',(98.5241538230988,-2.93549411544786,126.858215997729));
#46615=CARTESIAN_POINT('Ctrl Pts',(98.5164075470147,-3.04556011845922,126.940092901714));
#46616=CARTESIAN_POINT('Ctrl Pts',(98.5086612709306,-3.15222606230903,127.026599146855));
#46617=CARTESIAN_POINT('Ctrl Pts',(98.5009149948465,-3.25508838500562,127.117413009001));
#46618=CARTESIAN_POINT('Ctrl Pts',(98.4931686615812,-3.35795146700837,127.208227541515));
#46619=CARTESIAN_POINT('Ctrl Pts',(98.4854223283158,-3.45701057874577,127.303349495727));
#46620=CARTESIAN_POINT('Ctrl Pts',(98.4776759950505,-3.5518966747943,127.402418073359));
#46621=CARTESIAN_POINT('Ctrl Pts',(98.4699279270476,-3.64680401992537,127.501508836711));
#46622=CARTESIAN_POINT('Ctrl Pts',(98.4621798590446,-3.73753621940716,127.604547699883));
#46623=CARTESIAN_POINT('Ctrl Pts',(98.4544317910417,-3.82376268016293,127.711138668159));
#46624=CARTESIAN_POINT('Ctrl Pts',(98.4466754882999,-3.91008078342812,127.817842922586));
#46625=CARTESIAN_POINT('Ctrl Pts',(98.438919185558,-3.99188333563701,127.928106519079));
#46626=CARTESIAN_POINT('Ctrl Pts',(98.4311628828162,-4.06888116091525,128.041501742985));
#46627=CARTESIAN_POINT('Ctrl Pts',(98.423402440302,-4.14592008225131,128.154957489338));
#46628=CARTESIAN_POINT('Ctrl Pts',(98.4156419977878,-4.21814896102131,128.271547861405));
#46629=CARTESIAN_POINT('Ctrl Pts',(98.4078815552736,-4.28532376742706,128.39081897284));
#46630=CARTESIAN_POINT('Ctrl Pts',(98.4001086550082,-4.35260640879552,128.510281548853));
#46631=CARTESIAN_POINT('Ctrl Pts',(98.3923357547427,-4.41481858741458,128.632433115135));
#46632=CARTESIAN_POINT('Ctrl Pts',(98.3845628544773,-4.47176338128977,128.756797352547));
#46633=CARTESIAN_POINT('Ctrl Pts',(98.3770725187151,-4.52663808847352,128.876640636677));
#46634=CARTESIAN_POINT('Ctrl Pts',(98.3695821829529,-4.57662161061937,128.998538227587));
#46635=CARTESIAN_POINT('Ctrl Pts',(98.3620918471907,-4.62158169232119,129.122050977903));
#46636=CARTESIAN_POINT('Ctrl Pts',(98.3529410384216,-4.67650861722246,129.27294428824));
#46637=CARTESIAN_POINT('Ctrl Pts',(98.3437902296526,-4.72408470636501,129.426648390468));
#46638=CARTESIAN_POINT('Ctrl Pts',(98.3346394208835,-4.76405452823406,129.582490119308));
#46639=CARTESIAN_POINT('Ctrl Pts',(100.084952068471,-4.76405452823407,129.582490119308));
#46640=CARTESIAN_POINT('Ctrl Pts',(100.077187675489,-4.79809848252394,129.715226980395));
#46641=CARTESIAN_POINT('Ctrl Pts',(100.069423282507,-4.8265572118817,129.849256871815));
#46642=CARTESIAN_POINT('Ctrl Pts',(100.061658889525,-4.84936144496104,129.984070035744));
#46643=CARTESIAN_POINT('Ctrl Pts',(100.053883610672,-4.87219765013864,130.119072211061));
#46644=CARTESIAN_POINT('Ctrl Pts',(100.046108331819,-4.88936348605365,130.254859464739));
#46645=CARTESIAN_POINT('Ctrl Pts',(100.038333052966,-4.90084161242132,130.39091829697));
#46646=CARTESIAN_POINT('Ctrl Pts',(100.036481232,-4.90357533238947,130.42332312809));
#46647=CARTESIAN_POINT('Ctrl Pts',(100.034629411034,-4.9059866557627,130.455743372047));
#46648=CARTESIAN_POINT('Ctrl Pts',(100.032777590068,-4.90807578324186,130.488172116107));
#46649=CARTESIAN_POINT('Ctrl Pts',(100.026804872043,-4.91481389107284,130.592765242415));
#46650=CARTESIAN_POINT('Ctrl Pts',(100.020832154017,-4.91820900626066,130.697576041031));
#46651=CARTESIAN_POINT('Ctrl Pts',(100.014859435991,-4.91824963103831,130.802455547603));
#46652=CARTESIAN_POINT('',(100.360140563971,-4.91824789728292,130.808908515121));
#46653=CARTESIAN_POINT('Ctrl Pts',(100.43015599918,-4.76405452823403,129.582490119308));
#46654=CARTESIAN_POINT('Ctrl Pts',(100.422499773494,-4.79776724258496,129.713935480901));
#46655=CARTESIAN_POINT('Ctrl Pts',(100.414843547808,-4.82603171654888,129.846761741419));
#46656=CARTESIAN_POINT('Ctrl Pts',(100.407187322122,-4.84875148222177,129.980472199058));
#46657=CARTESIAN_POINT('Ctrl Pts',(100.399346195769,-4.87201993859153,130.117411813425));
#46658=CARTESIAN_POINT('Ctrl Pts',(100.391505069417,-4.88947237101566,130.255278441819));
#46659=CARTESIAN_POINT('Ctrl Pts',(100.383663943065,-4.90106137271956,130.393531597977));
#46660=CARTESIAN_POINT('Ctrl Pts',(100.375822816713,-4.91265037442346,130.531784754135));
#46661=CARTESIAN_POINT('Ctrl Pts',(100.36798169036,-4.91837595373029,130.670423987494));
#46662=CARTESIAN_POINT('Ctrl Pts',(100.360140564008,-4.91824789728353,130.80890851446));
#46663=CARTESIAN_POINT('Ctrl Pts',(100.360140563971,-4.91824789728292,130.808908515121));
#46664=CARTESIAN_POINT('Ctrl Pts',(100.350122548475,-4.91808428919946,130.985839746017));
#46665=CARTESIAN_POINT('Ctrl Pts',(100.340104532979,-4.90836974886036,131.162344238964));
#46666=CARTESIAN_POINT('Ctrl Pts',(100.330086517483,-4.88926273780238,131.3375518996));
#46667=CARTESIAN_POINT('Ctrl Pts',(100.319830746939,-4.86970226484551,131.516917719681));
#46668=CARTESIAN_POINT('Ctrl Pts',(100.309574976395,-4.84029819124037,131.694924725954));
#46669=CARTESIAN_POINT('Ctrl Pts',(100.299319205851,-4.80126838982909,131.870664941541));
#46670=CARTESIAN_POINT('Ctrl Pts',(100.296758209808,-4.79152215315772,131.914549503385));
#46671=CARTESIAN_POINT('Ctrl Pts',(100.294197213765,-4.78117592073932,131.958292825173));
#46672=CARTESIAN_POINT('Ctrl Pts',(100.291636217722,-4.77023354346506,132.001880973677));
#46673=CARTESIAN_POINT('Ctrl Pts',(100.283861883603,-4.73701611729094,132.134200127798));
#46674=CARTESIAN_POINT('Ctrl Pts',(100.276087549484,-4.69823640118361,132.265345715872));
#46675=CARTESIAN_POINT('Ctrl Pts',(100.268313215365,-4.65399187215868,132.394814237255));
#46676=CARTESIAN_POINT('Ctrl Pts',(100.260548462417,-4.60980187056156,132.524123200256));
#46677=CARTESIAN_POINT('Ctrl Pts',(100.25278370947,-4.56016058169338,132.651758842545));
#46678=CARTESIAN_POINT('Ctrl Pts',(100.245018956523,-4.50521620132081,132.777229098194));
#46679=CARTESIAN_POINT('Ctrl Pts',(100.237261915638,-4.45032639248137,132.902574735017));
#46680=CARTESIAN_POINT('Ctrl Pts',(100.229504874753,-4.39014412972855,133.025758909359));
#46681=CARTESIAN_POINT('Ctrl Pts',(100.221747833868,-4.32486688390532,133.146306282819));
#46682=CARTESIAN_POINT('Ctrl Pts',(100.213996642628,-4.25963886416082,133.266762750568));
#46683=CARTESIAN_POINT('Ctrl Pts',(100.206245451388,-4.18932369435945,133.384586032884));
#46684=CARTESIAN_POINT('Ctrl Pts',(100.198494260148,-4.11416611629642,133.499322626578));
#46685=CARTESIAN_POINT('Ctrl Pts',(100.190746363371,-4.03904048220912,133.614010454159));
#46686=CARTESIAN_POINT('Ctrl Pts',(100.182998466594,-3.95907674715038,133.725613876076));
#46687=CARTESIAN_POINT('Ctrl Pts',(100.175250569816,-3.87456446295535,133.833705973398));
#46688=CARTESIAN_POINT('Ctrl Pts',(100.167504293732,-3.7900698569083,133.941775460184));
#46689=CARTESIAN_POINT('Ctrl Pts',(100.159758017648,-3.70102883488634,134.046334775518));
#46690=CARTESIAN_POINT('Ctrl Pts',(100.152011741564,-3.60777271276643,134.146988194117));
#46691=CARTESIAN_POINT('Ctrl Pts',(100.144265408299,-3.51451590225101,134.247642355716));
#46692=CARTESIAN_POINT('Ctrl Pts',(100.136519075033,-3.41704419526475,134.344390276256));
#46693=CARTESIAN_POINT('Ctrl Pts',(100.128772741768,-3.31572714226006,134.436871674752));
#46694=CARTESIAN_POINT('Ctrl Pts',(100.121024673765,-3.21438740000391,134.529373783816));
#46695=CARTESIAN_POINT('Ctrl Pts',(100.113276605762,-3.10920088686629,134.61760720606));
#46696=CARTESIAN_POINT('Ctrl Pts',(100.105528537759,-3.00057141684857,134.701250946391));
#46697=CARTESIAN_POINT('Ctrl Pts',(100.097772235017,-2.89182649413733,134.784983584285));
#46698=CARTESIAN_POINT('Ctrl Pts',(100.090015932275,-2.77963161513725,134.864116557094));
#46699=CARTESIAN_POINT('Ctrl Pts',(100.082259629534,-2.66442131075266,134.938371036192));
#46700=CARTESIAN_POINT('Ctrl Pts',(100.074499187019,-2.54914951515972,135.012665147141));
#46701=CARTESIAN_POINT('Ctrl Pts',(100.066738744505,-2.43085942430564,135.082075378324));
#46702=CARTESIAN_POINT('Ctrl Pts',(100.058978301991,-2.31001064987067,135.146368662237));
#46703=CARTESIAN_POINT('Ctrl Pts',(100.051205401726,-2.18896787825445,135.210765155437));
#46704=CARTESIAN_POINT('Ctrl Pts',(100.04343250146,-2.06535856785564,135.270028117703));
#46705=CARTESIAN_POINT('Ctrl Pts',(100.035659601195,-1.93966362623258,135.323972114096));
#46706=CARTESIAN_POINT('Ctrl Pts',(100.028169265433,-1.81853801234627,135.375955110343));
#46707=CARTESIAN_POINT('Ctrl Pts',(100.020678929671,-1.69547605822335,135.422999032394));
#46708=CARTESIAN_POINT('Ctrl Pts',(100.013188593909,-1.57091995854025,135.464982201256));
#46709=CARTESIAN_POINT('Ctrl Pts',(100.00541425979,-1.44164127647739,135.508557174727));
#46710=CARTESIAN_POINT('Ctrl Pts',(99.9976399256709,-1.31034339519215,135.54681809503));
#46711=CARTESIAN_POINT('Ctrl Pts',(99.9898655915518,-1.17750261274296,135.579574817943));
#46712=CARTESIAN_POINT('Ctrl Pts',(99.9821008386047,-1.04482554468581,135.612291171123));
#46713=CARTESIAN_POINT('Ctrl Pts',(99.9743360856576,-0.910609734809486,
135.639516731215));
#46714=CARTESIAN_POINT('Ctrl Pts',(99.9665713327105,-0.775349275547373,
135.661110205861));
#46715=CARTESIAN_POINT('Ctrl Pts',(99.9588142918255,-0.640223158880329,
135.682682233564));
#46716=CARTESIAN_POINT('Ctrl Pts',(99.9510572509405,-0.504054841197791,
135.698633246633));
#46717=CARTESIAN_POINT('Ctrl Pts',(99.9433002100555,-0.367350975973875,
135.708872450863));
#46718=CARTESIAN_POINT('Ctrl Pts',(99.9355490188154,-0.230750200198219,
135.719103933629));
#46719=CARTESIAN_POINT('Ctrl Pts',(99.9277978275753,-0.0936150690367489,
135.723632151932));
#46720=CARTESIAN_POINT('Ctrl Pts',(99.9200466363352,0.0435405835159097,
135.722417884423));
#46721=CARTESIAN_POINT('Ctrl Pts',(99.9122987395581,0.180637941257673,135.721204133011));
#46722=CARTESIAN_POINT('Ctrl Pts',(99.9045508427809,0.317755412911561,135.714252753627));
#46723=CARTESIAN_POINT('Ctrl Pts',(99.8968029460039,0.45437730965064,135.70157659432));
#46724=CARTESIAN_POINT('Ctrl Pts',(99.8890566699198,0.590970628034148,135.688903086593));
#46725=CARTESIAN_POINT('Ctrl Pts',(99.8813103938356,0.727068188648891,135.670507216934));
#46726=CARTESIAN_POINT('Ctrl Pts',(99.8735641177515,0.862157972282204,135.646453831593));
#46727=CARTESIAN_POINT('Ctrl Pts',(99.8658177844862,0.99724875311752,135.622400268696));
#46728=CARTESIAN_POINT('Ctrl Pts',(99.8580714512209,1.13133135721577,135.592689175317));
#46729=CARTESIAN_POINT('Ctrl Pts',(99.8503251179555,1.26390291893541,135.557436724048));
#46730=CARTESIAN_POINT('Ctrl Pts',(99.8425770499525,1.39650416913711,135.522176378236));
#46731=CARTESIAN_POINT('Ctrl Pts',(99.8348289819496,1.52759332584556,135.48137230564));
#46732=CARTESIAN_POINT('Ctrl Pts',(99.8270809139466,1.65668205546671,135.435190740729));
#46733=CARTESIAN_POINT('Ctrl Pts',(99.8193246112047,1.78590798212587,135.388960093501));
#46734=CARTESIAN_POINT('Ctrl Pts',(99.8115683084629,1.9131288659241,135.337340669008));
#46735=CARTESIAN_POINT('Ctrl Pts',(99.803812005721,2.03787524587325,135.280547336723));
#46736=CARTESIAN_POINT('Ctrl Pts',(99.7960515632068,2.1626882067215,135.223723692126));
#46737=CARTESIAN_POINT('Ctrl Pts',(99.7882911206927,2.28502368351798,135.161720813935));
#46738=CARTESIAN_POINT('Ctrl Pts',(99.7805306781785,2.40443715863196,135.094799407794));
#46739=CARTESIAN_POINT('Ctrl Pts',(99.7727577779131,2.52404232685722,135.02777057347));
#46740=CARTESIAN_POINT('Ctrl Pts',(99.7649848776476,2.64071578702214,134.955807638518));
#46741=CARTESIAN_POINT('Ctrl Pts',(99.7572119773822,2.75404158517801,134.879214971971));
#46742=CARTESIAN_POINT('Ctrl Pts',(99.7497216416201,2.86324770512137,134.805406641777));
#46743=CARTESIAN_POINT('Ctrl Pts',(99.742231305858,2.96934508125772,134.727299523456));
#46744=CARTESIAN_POINT('Ctrl Pts',(99.7347409700959,3.07199232457968,134.645199877444));
#46745=CARTESIAN_POINT('Ctrl Pts',(99.7269666359768,3.17853146933025,134.559987398401));
#46746=CARTESIAN_POINT('Ctrl Pts',(99.7191923018577,3.28169117715037,134.470203734325));
#46747=CARTESIAN_POINT('Ctrl Pts',(99.7114179677386,3.38105402358604,134.376146830666));
#46748=CARTESIAN_POINT('Ctrl Pts',(99.7036532147915,3.48029441419379,134.282205843735));
#46749=CARTESIAN_POINT('Ctrl Pts',(99.6958884618445,3.57574697260873,134.184002361948));
#46750=CARTESIAN_POINT('Ctrl Pts',(99.6881237088974,3.66702575653928,134.081875707291));
#46751=CARTESIAN_POINT('Ctrl Pts',(99.6803666680124,3.75821388109476,133.979850486268));
#46752=CARTESIAN_POINT('Ctrl Pts',(99.6726096271274,3.84523622194897,133.873910136304));
#46753=CARTESIAN_POINT('Ctrl Pts',(99.6648525862424,3.92774253278796,133.764431842829));
#46754=CARTESIAN_POINT('Ctrl Pts',(99.6571013950023,4.01018662497609,133.655036107787));
#46755=CARTESIAN_POINT('Ctrl Pts',(99.6493502037621,4.08812123138416,133.542108050672));
#46756=CARTESIAN_POINT('Ctrl Pts',(99.641599012522,4.16123561415702,133.426058774481));
#46757=CARTESIAN_POINT('Ctrl Pts',(99.6338511157449,4.23431892136685,133.310058822328));
#46758=CARTESIAN_POINT('Ctrl Pts',(99.6261032189679,4.30258587172688,133.190940619703));
#46759=CARTESIAN_POINT('Ctrl Pts',(99.6183553221908,4.36576853225753,133.069144974906));
#46760=CARTESIAN_POINT('Ctrl Pts',(99.6106090461067,4.42893797633766,132.947374807132));
#46761=CARTESIAN_POINT('Ctrl Pts',(99.6028627700226,4.48702506607574,132.822928658009));
#46762=CARTESIAN_POINT('Ctrl Pts',(99.5951164939385,4.5398075995663,132.696272354783));
#46763=CARTESIAN_POINT('Ctrl Pts',(99.5873701606731,4.59259052268554,132.56961511661));
#46764=CARTESIAN_POINT('Ctrl Pts',(99.5796238274078,4.64006866102898,132.44074805266));
#46765=CARTESIAN_POINT('Ctrl Pts',(99.5718774941424,4.68206794272422,132.310157032163));
#46766=CARTESIAN_POINT('Ctrl Pts',(99.5641294261394,4.72407662986739,132.179536766713));
#46767=CARTESIAN_POINT('Ctrl Pts',(99.5563813581365,4.76060389919301,132.047192148604));
#46768=CARTESIAN_POINT('Ctrl Pts',(99.5486332901335,4.79152565223085,131.913623880508));
#46769=CARTESIAN_POINT('Ctrl Pts',(99.5408769873916,4.8224802692758,131.779913654468));
#46770=CARTESIAN_POINT('Ctrl Pts',(99.5331206846498,4.84781738074743,131.644977562033));
#46771=CARTESIAN_POINT('Ctrl Pts',(99.5253643819079,4.86746400728748,131.509326716227));
#46772=CARTESIAN_POINT('Ctrl Pts',(99.5176039393938,4.88712111982367,131.373603469479));
#46773=CARTESIAN_POINT('Ctrl Pts',(99.5098434968796,4.90108165580695,131.237165097963));
#46774=CARTESIAN_POINT('Ctrl Pts',(99.5020830543654,4.90932468164281,131.100526504718));
#46775=CARTESIAN_POINT('Ctrl Pts',(99.4943101541,4.91758093991554,130.963668567074));
#46776=CARTESIAN_POINT('Ctrl Pts',(99.4865372538345,4.92010133977055,130.826610156539));
#46777=CARTESIAN_POINT('Ctrl Pts',(99.4787643535691,4.91691712222713,130.689865745848));
#46778=CARTESIAN_POINT('Ctrl Pts',(99.4712740178071,4.91384865901198,130.558092338925));
#46779=CARTESIAN_POINT('Ctrl Pts',(99.4637836820451,4.90548315163427,130.426610806224));
#46780=CARTESIAN_POINT('Ctrl Pts',(99.4562933462831,4.89189373657571,130.295873909233));
#46781=CARTESIAN_POINT('Ctrl Pts',(99.448519012164,4.87778907471478,130.160180083056));
#46782=CARTESIAN_POINT('Ctrl Pts',(99.4407446780449,4.85801187721498,130.024858635711));
#46783=CARTESIAN_POINT('Ctrl Pts',(99.4329703439258,4.83258718590767,129.890421805007));
#46784=CARTESIAN_POINT('Ctrl Pts',(99.4252055909787,4.80719382826012,129.756150655683));
#46785=CARTESIAN_POINT('Ctrl Pts',(99.4174408380317,4.77616689714709,129.622762334272));
#46786=CARTESIAN_POINT('Ctrl Pts',(99.4096760850846,4.73958326253042,129.490764956778));
#46787=CARTESIAN_POINT('Ctrl Pts',(99.4019190441996,4.70303596329543,129.35889868094));
#46788=CARTESIAN_POINT('Ctrl Pts',(99.3941620033146,4.66094304735403,129.228420974086));
#46789=CARTESIAN_POINT('Ctrl Pts',(99.3864049624296,4.61343253480448,129.099830386298));
#46790=CARTESIAN_POINT('Ctrl Pts',(99.3786537711894,4.565957850302,128.971336769672));
#46791=CARTESIAN_POINT('Ctrl Pts',(99.3709025799493,4.51307383598483,128.844727804787));
#46792=CARTESIAN_POINT('Ctrl Pts',(99.3631513887092,4.45495840304577,128.72048713541));
#46793=CARTESIAN_POINT('Ctrl Pts',(99.3554034919321,4.39686767071599,128.596299271633));
#46794=CARTESIAN_POINT('Ctrl Pts',(99.347655595155,4.33355010742735,128.474478054732));
#46795=CARTESIAN_POINT('Ctrl Pts',(99.339907698378,4.26523175336659,128.355487171964));
#46796=CARTESIAN_POINT('Ctrl Pts',(99.3321614222939,4.19692769003272,128.236521179524));
#46797=CARTESIAN_POINT('Ctrl Pts',(99.3244151462097,4.12362511113706,128.120384682449));
#46798=CARTESIAN_POINT('Ctrl Pts',(99.3166688701256,4.04559582477728,128.007516416499));
#46799=CARTESIAN_POINT('Ctrl Pts',(99.3089225368603,3.96756596242304,127.89464731738));
#46800=CARTESIAN_POINT('Ctrl Pts',(99.3011762035949,3.8848095453101,127.785046819124));
#46801=CARTESIAN_POINT('Ctrl Pts',(99.2934298703296,3.79764125888202,127.67912399751));
#46802=CARTESIAN_POINT('Ctrl Pts',(99.2856818023266,3.71045345172064,127.573177455216));
#46803=CARTESIAN_POINT('Ctrl Pts',(99.2779337343236,3.61885205760961,127.470910530241));
#46804=CARTESIAN_POINT('Ctrl Pts',(99.2701856663207,3.5231912536341,127.372698272169));
#46805=CARTESIAN_POINT('Ctrl Pts',(99.2624293635788,3.42742878021768,127.27438163294));
#46806=CARTESIAN_POINT('Ctrl Pts',(99.254673060837,3.32759855170705,127.180128549516));
#46807=CARTESIAN_POINT('Ctrl Pts',(99.2469167580951,3.22409113483882,127.090276690572));
#46808=CARTESIAN_POINT('Ctrl Pts',(99.2391563155809,3.12052847294559,127.000376874985));
#46809=CARTESIAN_POINT('Ctrl Pts',(99.2313958730668,3.01328501755718,126.914883208183));
#46810=CARTESIAN_POINT('Ctrl Pts',(99.2236354305526,2.90278265606604,126.83409161986));
#46811=CARTESIAN_POINT('Ctrl Pts',(99.2158625302872,2.79210290637438,126.753170337708));
#46812=CARTESIAN_POINT('Ctrl Pts',(99.2080896300217,2.67815412158125,126.676966435197));
#46813=CARTESIAN_POINT('Ctrl Pts',(99.2003167297563,2.56138602870343,126.605731713452));
#46814=CARTESIAN_POINT('Ctrl Pts',(99.1928263939943,2.44886275012272,126.537086553272));
#46815=CARTESIAN_POINT('Ctrl Pts',(99.1853360582323,2.33372185183422,126.473055711512));
#46816=CARTESIAN_POINT('Ctrl Pts',(99.1778457224702,2.21638378695495,126.413822385023));
#46817=CARTESIAN_POINT('Ctrl Pts',(99.1700713883511,2.09459681368174,126.352343208956));
#46818=CARTESIAN_POINT('Ctrl Pts',(99.1622970542321,1.9700569891946,126.295837777632));
#46819=CARTESIAN_POINT('Ctrl Pts',(99.154522720113,1.84320880939055,126.244561899696));
#46820=CARTESIAN_POINT('Ctrl Pts',(99.1467579671659,1.71651695863145,126.193349214697));
#46821=CARTESIAN_POINT('Ctrl Pts',(99.1389932142188,1.58752277193361,126.147353404658));
#46822=CARTESIAN_POINT('Ctrl Pts',(99.1312284612717,1.45669529177267,126.106784445812));
#46823=CARTESIAN_POINT('Ctrl Pts',(99.1234714203867,1.32599775130947,126.066255780629));
#46824=CARTESIAN_POINT('Ctrl Pts',(99.1157143795017,1.19347091196947,126.031143355294));
#46825=CARTESIAN_POINT('Ctrl Pts',(99.1079573386168,1.05960341604697,126.00160894137));
#46826=CARTESIAN_POINT('Ctrl Pts',(99.1002061473766,0.925836870644291,125.972096799578));
#46827=CARTESIAN_POINT('Ctrl Pts',(99.0924549561365,0.790732061231549,125.948154380459));
#46828=CARTESIAN_POINT('Ctrl Pts',(99.0847037648964,0.654792056354769,125.929893423561));
#46829=CARTESIAN_POINT('Ctrl Pts',(99.0769558681193,0.51890982960638,125.911640228056));
#46830=CARTESIAN_POINT('Ctrl Pts',(99.0692079713422,0.382193500096363,125.899063743913));
#46831=CARTESIAN_POINT('Ctrl Pts',(99.0614600745651,0.24515536128886,125.892224431411));
#46832=CARTESIAN_POINT('Ctrl Pts',(99.053713798481,0.108145887905796,125.885386549546));
#46833=CARTESIAN_POINT('Ctrl Pts',(99.0459675223969,-0.0291848706485858,
125.884283471747));
#46834=CARTESIAN_POINT('Ctrl Pts',(99.0382212463128,-0.166320874636657,
125.888923665559));
#46835=CARTESIAN_POINT('Ctrl Pts',(99.0304749130475,-0.303457890931464,
125.893563893623));
#46836=CARTESIAN_POINT('Ctrl Pts',(99.0227285797821,-0.440399759049679,
125.903947464675));
#46837=CARTESIAN_POINT('Ctrl Pts',(99.0149822465168,-0.576632216781138,
125.92003074039));
#46838=CARTESIAN_POINT('Ctrl Pts',(99.0072341785138,-0.712895182826937,
125.936117617844));
#46839=CARTESIAN_POINT('Ctrl Pts',(98.9994861105109,-0.848448034163486,
125.957906694038));
#46840=CARTESIAN_POINT('Ctrl Pts',(98.9917380425079,-0.982783789588957,
125.985302713222));
#46841=CARTESIAN_POINT('Ctrl Pts',(98.9839817397661,-1.117262318654,126.012727849221));
#46842=CARTESIAN_POINT('Ctrl Pts',(98.9762254370242,-1.25052078412346,126.045771753956));
#46843=CARTESIAN_POINT('Ctrl Pts',(98.9684691342824,-1.38206398491655,126.084288350736));
#46844=CARTESIAN_POINT('Ctrl Pts',(98.9607086917682,-1.51367739427659,126.122825504984));
#46845=CARTESIAN_POINT('Ctrl Pts',(98.952948249254,-1.64357334466874,126.166841046089));
#46846=CARTESIAN_POINT('Ctrl Pts',(98.9451878067398,-1.77127482161698,126.216139985468));
#46847=CARTESIAN_POINT('Ctrl Pts',(98.9374149064744,-1.89918129631281,126.265518063882));
#46848=CARTESIAN_POINT('Ctrl Pts',(98.929642006209,-2.02488589923686,126.320196333034));
#46849=CARTESIAN_POINT('Ctrl Pts',(98.9218691059435,-2.1479336945329,126.379932529509));
#46850=CARTESIAN_POINT('Ctrl Pts',(98.9143787701815,-2.26650839253174,126.437497164775));
#46851=CARTESIAN_POINT('Ctrl Pts',(98.9068884344194,-2.38261582114992,126.499758229454));
#46852=CARTESIAN_POINT('Ctrl Pts',(98.8993980986574,-2.49587458650939,126.566461006802));
#46853=CARTESIAN_POINT('Ctrl Pts',(98.8916225640437,-2.61344574464242,126.635703530845));
#46854=CARTESIAN_POINT('Ctrl Pts',(98.8838470294301,-2.72831950036794,126.709952084004));
#46855=CARTESIAN_POINT('Ctrl Pts',(98.8760714948165,-2.84004016436807,126.788970857247));
#46856=CARTESIAN_POINT('Ctrl Pts',(98.8679116394048,-2.95728283770591,126.871895285791));
#46857=CARTESIAN_POINT('Ctrl Pts',(98.8597517839932,-3.07105237575799,126.960073382573));
#46858=CARTESIAN_POINT('Ctrl Pts',(98.8515919285816,-3.18085032049864,127.053177564037));
#46859=CARTESIAN_POINT('Ctrl Pts',(98.8438359823462,-3.2852133163126,127.141673130355));
#46860=CARTESIAN_POINT('Ctrl Pts',(98.8360800361107,-3.38598806948694,127.234618568138));
#46861=CARTESIAN_POINT('Ctrl Pts',(98.8283240898753,-3.48277611758001,127.331688220504));
#46862=CARTESIAN_POINT('Ctrl Pts',(98.8205734095931,-3.57949845076016,127.428691966761));
#46863=CARTESIAN_POINT('Ctrl Pts',(98.8128227293109,-3.67223918936309,127.529814080812));
#46864=CARTESIAN_POINT('Ctrl Pts',(98.8050720490286,-3.760634296572,127.634689853915));
#46865=CARTESIAN_POINT('Ctrl Pts',(98.7973249525395,-3.84898853126834,127.739517134103));
#46866=CARTESIAN_POINT('Ctrl Pts',(98.7895778560505,-3.93300088211774,127.848094320907));
#46867=CARTESIAN_POINT('Ctrl Pts',(98.7818307595614,-4.01234570138409,127.960021496595));
#46868=CARTESIAN_POINT('Ctrl Pts',(98.7740855674892,-4.09167101584442,128.071921157975));
#46869=CARTESIAN_POINT('Ctrl Pts',(98.766340375417,-4.16633085777311,128.187168849741));
#46870=CARTESIAN_POINT('Ctrl Pts',(98.7585951833448,-4.23604149092616,128.305333697012));
#46871=CARTESIAN_POINT('Ctrl Pts',(98.7508481870581,-4.30576836291918,128.423526070358));
#46872=CARTESIAN_POINT('Ctrl Pts',(98.7431011907714,-4.37054352053089,128.544636622193));
#46873=CARTESIAN_POINT('Ctrl Pts',(98.7353541944847,-4.43012799617072,128.668207767219));
#46874=CARTESIAN_POINT('Ctrl Pts',(98.7276061435344,-4.48972058354506,128.791795735022));
#46875=CARTESIAN_POINT('Ctrl Pts',(98.7198580925841,-4.54412091917249,128.917844607592));
#46876=CARTESIAN_POINT('Ctrl Pts',(98.7121100416338,-4.59313758346951,129.045875416656));
#46877=CARTESIAN_POINT('Ctrl Pts',(98.7043566509114,-4.64218802888359,129.173994461502));
#46878=CARTESIAN_POINT('Ctrl Pts',(98.6966032601891,-4.68584726356118,129.304097801933));
#46879=CARTESIAN_POINT('Ctrl Pts',(98.6888498694667,-4.72397323480069,129.435689751584));
#46880=CARTESIAN_POINT('Ctrl Pts',(98.6859782346235,-4.73809400742304,129.48442765752));
#46881=CARTESIAN_POINT('Ctrl Pts',(98.6831065997802,-4.75145625339996,129.533369636936));
#46882=CARTESIAN_POINT('Ctrl Pts',(98.680234964937,-4.76405452823403,129.582490119308));
#46883=CARTESIAN_POINT('Origin',(213.235140564004,0.,130.804360617566));
#46884=CARTESIAN_POINT('',(96.5847048906856,-4.76405452823403,129.582490119308));
#46885=CARTESIAN_POINT('',(96.929952524335,-4.76405452823408,129.582490119308));
#46886=CARTESIAN_POINT('',(213.235140564004,-4.76405452823405,129.582490119308));
#46887=CARTESIAN_POINT('',(98.2648594360458,-4.91824869076816,130.800771988677));
#46888=CARTESIAN_POINT('Ctrl Pts',(98.264859435991,-4.91824869076887,130.800771989647));
#46889=CARTESIAN_POINT('Ctrl Pts',(98.2570959853869,-4.9183490653254,130.938336273932));
#46890=CARTESIAN_POINT('Ctrl Pts',(98.2493325347827,-4.9126735820973,131.075952301792));
#46891=CARTESIAN_POINT('Ctrl Pts',(98.2415690841786,-4.90123596697668,131.213101438275));
#46892=CARTESIAN_POINT('Ctrl Pts',(98.2338061956604,-4.8897991799573,131.350240644946));
#46893=CARTESIAN_POINT('Ctrl Pts',(98.2260433071422,-4.87260112265808,131.486912640666));
#46894=CARTESIAN_POINT('Ctrl Pts',(98.218280418624,-4.84970751694911,131.622602673774));
#46895=CARTESIAN_POINT('Ctrl Pts',(98.2105164413888,-4.82681070049466,131.758311736918));
#46896=CARTESIAN_POINT('Ctrl Pts',(98.2027524641536,-4.7982168100034,131.893038180506));
#46897=CARTESIAN_POINT('Ctrl Pts',(98.1949884869183,-4.76404286757597,132.026276579651));
#46898=CARTESIAN_POINT('Ctrl Pts',(98.1872217698146,-4.72985686533635,132.159561997957));
#46899=CARTESIAN_POINT('Ctrl Pts',(98.1794550527109,-4.69008698798128,132.291357950785));
#46900=CARTESIAN_POINT('Ctrl Pts',(98.1716883356072,-4.64490027831379,132.421173676339));
#46901=CARTESIAN_POINT('Ctrl Pts',(98.1639122580396,-4.59965910952808,132.551145856081));
#46902=CARTESIAN_POINT('Ctrl Pts',(98.1561361804719,-4.54898819716927,132.679132674873));
#46903=CARTESIAN_POINT('Ctrl Pts',(98.1483601029043,-4.49310318454982,132.804662303684));
#46904=CARTESIAN_POINT('Ctrl Pts',(98.1405790537656,-4.43718244230799,132.93027218883));
#46905=CARTESIAN_POINT('Ctrl Pts',(98.1327980046268,-4.37604113030625,133.053421406858));
#46906=CARTESIAN_POINT('Ctrl Pts',(98.1250169554881,-4.30994067306685,133.173663143024));
#46907=CARTESIAN_POINT('Ctrl Pts',(98.1172230976868,-4.2437314055069,133.294102813402));
#46908=CARTESIAN_POINT('Ctrl Pts',(98.1094292398855,-4.17254688458937,133.411625108483));
#46909=CARTESIAN_POINT('Ctrl Pts',(98.1016353820842,-4.09669209365738,133.525811876043));
#46910=CARTESIAN_POINT('Ctrl Pts',(98.0956383291821,-4.03832495305826,133.613673895499));
#46911=CARTESIAN_POINT('Ctrl Pts',(98.08964127628,-3.9771935914175,133.699561650248));
#46912=CARTESIAN_POINT('Ctrl Pts',(98.0836442233779,-3.91345253844182,133.783298732375));
#46913=CARTESIAN_POINT('Ctrl Pts',(98.0758698892588,-3.83082124420054,133.891852061025));
#46914=CARTESIAN_POINT('Ctrl Pts',(98.0680955551398,-3.7435389841468,133.997136621775));
#46915=CARTESIAN_POINT('Ctrl Pts',(98.0603212210207,-3.65189360089321,134.09872796051));
#46916=CARTESIAN_POINT('Ctrl Pts',(98.0525564680736,-3.5603611623839,134.200194097));
#46917=CARTESIAN_POINT('Ctrl Pts',(98.0447917151265,-3.46447655898354,134.297975780222));
#46918=CARTESIAN_POINT('Ctrl Pts',(98.0370269621794,-3.3645697534118,134.391679036236));
#46919=CARTESIAN_POINT('Ctrl Pts',(98.0292699212944,-3.26476217668785,134.485289224854));
#46920=CARTESIAN_POINT('Ctrl Pts',(98.0215128804093,-3.16094063116001,134.574828781714));
#46921=CARTESIAN_POINT('Ctrl Pts',(98.0137558395244,-3.05347378869415,134.659938509952));
#46922=CARTESIAN_POINT('Ctrl Pts',(98.0060046482842,-2.94608798781016,134.744984056283));
#46923=CARTESIAN_POINT('Ctrl Pts',(97.9982534570441,-2.83506266685036,134.825606181443));
#46924=CARTESIAN_POINT('Ctrl Pts',(97.990502265804,-2.72080135357165,134.901484371726));
#46925=CARTESIAN_POINT('Ctrl Pts',(97.9827543690269,-2.60658860439903,134.977330311754));
#46926=CARTESIAN_POINT('Ctrl Pts',(97.9750064722498,-2.48914292344931,135.048436111337));
#46927=CARTESIAN_POINT('Ctrl Pts',(97.9672585754728,-2.36889856242752,135.11452333647));
#46928=CARTESIAN_POINT('Ctrl Pts',(97.9595122993887,-2.24867935393405,135.18059673758));
#46929=CARTESIAN_POINT('Ctrl Pts',(97.9517660233046,-2.12566297221762,135.241653464115));
#46930=CARTESIAN_POINT('Ctrl Pts',(97.9440197472205,-2.00030977814471,135.297460199587));
#46931=CARTESIAN_POINT('Ctrl Pts',(97.9362734139551,-1.8749556587429,135.353267347012));
#46932=CARTESIAN_POINT('Ctrl Pts',(97.9285270806897,-1.74726504973267,135.403824267034));
#46933=CARTESIAN_POINT('Ctrl Pts',(97.9207807474244,-1.61771950317931,135.448945278387));
#46934=CARTESIAN_POINT('Ctrl Pts',(97.9130326794214,-1.48814494579918,135.494076394277));
#46935=CARTESIAN_POINT('Ctrl Pts',(97.9052846114185,-1.35671499341734,135.533769050572));
#46936=CARTESIAN_POINT('Ctrl Pts',(97.8975365434155,-1.22392722649592,135.567887169055));
#46937=CARTESIAN_POINT('Ctrl Pts',(97.8897802406737,-1.09099833115553,135.602041548681));
#46938=CARTESIAN_POINT('Ctrl Pts',(97.8820239379318,-0.95670911779455,135.630609457849));
#46939=CARTESIAN_POINT('Ctrl Pts',(97.87426763519,-0.821568800945488,135.653505672915));
#46940=CARTESIAN_POINT('Ctrl Pts',(97.8665071926758,-0.686356355639959,
135.67641410838));
#46941=CARTESIAN_POINT('Ctrl Pts',(97.8587467501616,-0.550292289373433,
135.693644768788));
#46942=CARTESIAN_POINT('Ctrl Pts',(97.8509863076474,-0.413890854559451,
135.70516437032));
#46943=CARTESIAN_POINT('Ctrl Pts',(97.843213407382,-0.277270456053341,135.71670246414));
#46944=CARTESIAN_POINT('Ctrl Pts',(97.8354405071166,-0.140311997601334,
135.722511162123));
#46945=CARTESIAN_POINT('Ctrl Pts',(97.8276676068512,-0.00353055348150193,
135.722609350366));
#46946=CARTESIAN_POINT('Ctrl Pts',(97.8201772710891,0.128278540613648,135.72270396922));
#46947=CARTESIAN_POINT('Ctrl Pts',(97.812686935327,0.259922958993352,135.717496065152));
#46948=CARTESIAN_POINT('Ctrl Pts',(97.805196599565,0.390948315480429,135.707047888556));
#46949=CARTESIAN_POINT('Ctrl Pts',(97.7974222654459,0.526941538182246,135.696203566168));
#46950=CARTESIAN_POINT('Ctrl Pts',(97.7896479313268,0.662698614501715,135.679679405626));
#46951=CARTESIAN_POINT('Ctrl Pts',(97.7818735972077,0.797706853207384,135.657488149256));
#46952=CARTESIAN_POINT('Ctrl Pts',(97.7741088442606,0.93254870632488,135.635324241625));
#46953=CARTESIAN_POINT('Ctrl Pts',(97.7663440913135,1.06664317599071,135.607507197424));
#46954=CARTESIAN_POINT('Ctrl Pts',(97.7585793383664,1.19948044785995,135.574101671093));
#46955=CARTESIAN_POINT('Ctrl Pts',(97.7508222974815,1.33218578387774,135.540729323602));
#46956=CARTESIAN_POINT('Ctrl Pts',(97.7430652565965,1.46363603029548,135.501779634579));
#46957=CARTESIAN_POINT('Ctrl Pts',(97.7353082157115,1.59332970847138,135.457368623427));
#46958=CARTESIAN_POINT('Ctrl Pts',(97.7275570244714,1.72292558363578,135.412991102964));
#46959=CARTESIAN_POINT('Ctrl Pts',(97.7198058332313,1.85076715879369,135.363160583994));
#46960=CARTESIAN_POINT('Ctrl Pts',(97.7120546419912,1.9763666600752,135.30804332036));
#46961=CARTESIAN_POINT('Ctrl Pts',(97.7043067452141,2.10191277821837,135.252949483033));
#46962=CARTESIAN_POINT('Ctrl Pts',(97.696558848437,2.22521836055197,135.192573526946));
#46963=CARTESIAN_POINT('Ctrl Pts',(97.6888109516599,2.34581442900797,135.127130299975));
#46964=CARTESIAN_POINT('Ctrl Pts',(97.6810646755758,2.46638527136635,135.061700762317));
#46965=CARTESIAN_POINT('Ctrl Pts',(97.6733183994917,2.58424738377636,134.99120624846));
#46966=CARTESIAN_POINT('Ctrl Pts',(97.6655721234076,2.69895563417696,134.915907959777));
#46967=CARTESIAN_POINT('Ctrl Pts',(97.6578257901422,2.8136647313278,134.84060911526));
#46968=CARTESIAN_POINT('Ctrl Pts',(97.6500794568769,2.9252195931753,134.760506639707));
#46969=CARTESIAN_POINT('Ctrl Pts',(97.6423331236116,3.0332037101579,134.675905311249));
#46970=CARTESIAN_POINT('Ctrl Pts',(97.6345850556086,3.14121200943464,134.59128503691));
#46971=CARTESIAN_POINT('Ctrl Pts',(97.6268369876056,3.24564766494756,134.502164145956));
#46972=CARTESIAN_POINT('Ctrl Pts',(97.6190889196027,3.34612723584534,134.408887713321));
#46973=CARTESIAN_POINT('Ctrl Pts',(97.6113326168608,3.44671359762679,134.315512145384));
#46974=CARTESIAN_POINT('Ctrl Pts',(97.603576314119,3.54333518871336,134.217972479631));
#46975=CARTESIAN_POINT('Ctrl Pts',(97.5958200113771,3.63564506514554,134.116651067207));
#46976=CARTESIAN_POINT('Ctrl Pts',(97.5880595688629,3.72800421013829,134.015275576495));
#46977=CARTESIAN_POINT('Ctrl Pts',(97.5802991263488,3.81604680410408,133.910114616843));
#46978=CARTESIAN_POINT('Ctrl Pts',(97.5725386838346,3.89946687843218,133.801582852655));
#46979=CARTESIAN_POINT('Ctrl Pts',(97.5647657835692,3.98302086606922,133.692876863644));
#46980=CARTESIAN_POINT('Ctrl Pts',(97.5569928833038,4.06193728038319,133.580789576828));
#46981=CARTESIAN_POINT('Ctrl Pts',(97.5492199830384,4.13595360055248,133.465764547182));
#46982=CARTESIAN_POINT('Ctrl Pts',(97.5417296472763,4.20727924104815,133.354920967094));
#46983=CARTESIAN_POINT('Ctrl Pts',(97.5342393115142,4.27405470758821,133.241349790189));
#46984=CARTESIAN_POINT('Ctrl Pts',(97.5267489757521,4.33608676636349,133.125466952284));
#46985=CARTESIAN_POINT('Ctrl Pts',(97.5189746416331,4.4004707895011,133.005190381359));
#46986=CARTESIAN_POINT('Ctrl Pts',(97.511200307514,4.45994856105055,132.882042395813));
#46987=CARTESIAN_POINT('Ctrl Pts',(97.5034259733949,4.51425367935687,132.756461224838));
#46988=CARTESIAN_POINT('Ctrl Pts',(97.4956612204478,4.56849187145831,132.631034821433));
#46989=CARTESIAN_POINT('Ctrl Pts',(97.4878964675007,4.61756994064574,132.50318155449));
#46990=CARTESIAN_POINT('Ctrl Pts',(97.4801317145536,4.66126671542612,132.373365292562));
#46991=CARTESIAN_POINT('Ctrl Pts',(97.4723746736686,4.70492008995378,132.243677965976));
#46992=CARTESIAN_POINT('Ctrl Pts',(97.4646176327836,4.74320268250534,132.112031892484));
#46993=CARTESIAN_POINT('Ctrl Pts',(97.4568605918986,4.77594104203629,131.978911691591));
#46994=CARTESIAN_POINT('Ctrl Pts',(97.4491094006584,4.80865471331567,131.845891877677));
#46995=CARTESIAN_POINT('Ctrl Pts',(97.4413582094183,4.83583238050986,131.711400527154));
#46996=CARTESIAN_POINT('Ctrl Pts',(97.4336070181782,4.85735026399335,131.575937882254));
#46997=CARTESIAN_POINT('Ctrl Pts',(97.4258591214011,4.87885900180233,131.440532812592));
#46998=CARTESIAN_POINT('Ctrl Pts',(97.418111224624,4.8947126791678,131.30415765495));
#46999=CARTESIAN_POINT('Ctrl Pts',(97.4103633278469,4.90483855959238,131.167323104382));
#47000=CARTESIAN_POINT('Ctrl Pts',(97.4026170517628,4.91496232190106,131.030517176653));
#47001=CARTESIAN_POINT('Ctrl Pts',(97.3948707756787,4.91936064158377,130.89325243679));
#47002=CARTESIAN_POINT('Ctrl Pts',(97.3871244995946,4.91801267000309,130.756044572726));
#47003=CARTESIAN_POINT('Ctrl Pts',(97.3793781663292,4.916664688472,130.618835695824));
#47004=CARTESIAN_POINT('Ctrl Pts',(97.3716318330639,4.9095703348766,130.481684086506));
#47005=CARTESIAN_POINT('Ctrl Pts',(97.3638854997985,4.89676089409853,130.345104906086));
#47006=CARTESIAN_POINT('Ctrl Pts',(97.3561374317955,4.88394858473499,130.208495139705));
#47007=CARTESIAN_POINT('Ctrl Pts',(97.3483893637925,4.8654186779277,130.07245844649));
#47008=CARTESIAN_POINT('Ctrl Pts',(97.3406412957895,4.84125423584634,129.937503947522));
#47009=CARTESIAN_POINT('Ctrl Pts',(97.3328849930477,4.8170641115084,129.802406017306));
#47010=CARTESIAN_POINT('Ctrl Pts',(97.3251286903058,4.78722755833888,129.668392964381));
#47011=CARTESIAN_POINT('Ctrl Pts',(97.317372387564,4.75187872750089,129.535963352659));
#47012=CARTESIAN_POINT('Ctrl Pts',(97.3096119450498,4.71651102992761,129.403463059266));
#47013=CARTESIAN_POINT('Ctrl Pts',(97.3018515025356,4.67562530885795,129.272548264076));
#47014=CARTESIAN_POINT('Ctrl Pts',(97.2940910600215,4.62940504968989,129.143700523385));
#47015=CARTESIAN_POINT('Ctrl Pts',(97.286318159756,4.58311059365847,129.014645944862));
#47016=CARTESIAN_POINT('Ctrl Pts',(97.2785452594906,4.53146463436087,128.887665414063));
#47017=CARTESIAN_POINT('Ctrl Pts',(97.2707723592251,4.47469844824211,128.763219549487));
#47018=CARTESIAN_POINT('Ctrl Pts',(97.2632820234631,4.41999585597459,128.643297605549));
#47019=CARTESIAN_POINT('Ctrl Pts',(97.2557916877012,4.36053897908826,128.525729519124));
#47020=CARTESIAN_POINT('Ctrl Pts',(97.2483013519392,4.29657330857259,128.410902686755));
#47021=CARTESIAN_POINT('Ctrl Pts',(97.2405270178201,4.23018236021695,128.291722160136));
#47022=CARTESIAN_POINT('Ctrl Pts',(97.232752683701,4.15872366059314,128.175117332189));
#47023=CARTESIAN_POINT('Ctrl Pts',(97.2249783495819,4.08242190772916,128.061549207754));
#47024=CARTESIAN_POINT('Ctrl Pts',(97.2172135966348,4.00621418995636,127.948121045883));
#47025=CARTESIAN_POINT('Ctrl Pts',(97.2094488436878,3.92517551067917,127.837722462541));
#47026=CARTESIAN_POINT('Ctrl Pts',(97.2016840907407,3.83957658705373,127.730790267851));
#47027=CARTESIAN_POINT('Ctrl Pts',(97.1939270498557,3.75406268148615,127.623964279724));
#47028=CARTESIAN_POINT('Ctrl Pts',(97.1861700089707,3.6639977878252,127.520598132035));
#47029=CARTESIAN_POINT('Ctrl Pts',(97.1784129680857,3.56969587566003,127.421099702739));
#47030=CARTESIAN_POINT('Ctrl Pts',(97.1706617768456,3.47546507730038,127.321676305983));
#47031=CARTESIAN_POINT('Ctrl Pts',(97.1629105856055,3.37700388808234,127.226115104769));
#47032=CARTESIAN_POINT('Ctrl Pts',(97.1551593943654,3.27466627005367,127.13479063155));
#47033=CARTESIAN_POINT('Ctrl Pts',(97.1474114975883,3.17237214824225,127.043504973667));
#47034=CARTESIAN_POINT('Ctrl Pts',(97.1396636008112,3.06620516563591,126.956452722045));
#47035=CARTESIAN_POINT('Ctrl Pts',(97.1319157040341,2.95655566859566,126.873971115113));
#47036=CARTESIAN_POINT('Ctrl Pts',(97.12416942795,2.84692910786626,126.791506761554));
#47037=CARTESIAN_POINT('Ctrl Pts',(97.1164231518659,2.73382179390314,126.713611385864));
#47038=CARTESIAN_POINT('Ctrl Pts',(97.1086768757818,2.61765632037175,126.640581270516));
#47039=CARTESIAN_POINT('Ctrl Pts',(97.1009305425164,2.5014899893333,126.567550616077));
#47040=CARTESIAN_POINT('Ctrl Pts',(97.093184209251,2.38226578467078,126.499385501728));
#47041=CARTESIAN_POINT('Ctrl Pts',(97.0854378759856,2.26043403643116,126.436338063888));
#47042=CARTESIAN_POINT('Ctrl Pts',(97.0776898079827,2.13857500481642,126.373276507011));
#47043=CARTESIAN_POINT('Ctrl Pts',(97.0699417399797,2.01410761480864,126.315335086839));
#47044=CARTESIAN_POINT('Ctrl Pts',(97.0621936719767,1.88750510152241,126.262719113195));
#47045=CARTESIAN_POINT('Ctrl Pts',(97.0544373692349,1.76076803357838,126.210047218668));
#47046=CARTESIAN_POINT('Ctrl Pts',(97.046681066493,1.63189167091894,126.162712227308));
#47047=CARTESIAN_POINT('Ctrl Pts',(97.0389247637511,1.50136798146454,126.120870759914));
#47048=CARTESIAN_POINT('Ctrl Pts',(97.031164321237,1.37077462758691,126.079006960468));
#47049=CARTESIAN_POINT('Ctrl Pts',(97.0234038787228,1.23853257176621,126.042642630976));
#47050=CARTESIAN_POINT('Ctrl Pts',(97.0156434362086,1.10514613929213,126.011883692915));
#47051=CARTESIAN_POINT('Ctrl Pts',(97.0078705359432,0.971545583075235,125.981075377877));
#47052=CARTESIAN_POINT('Ctrl Pts',(97.0000976356777,0.83679736371519,125.955890507554));
#47053=CARTESIAN_POINT('Ctrl Pts',(96.9923247354123,0.701414023169202,125.936383478076));
#47054=CARTESIAN_POINT('Ctrl Pts',(96.9848343996503,0.570952208062481,125.917585578254));
#47055=CARTESIAN_POINT('Ctrl Pts',(96.9773440638883,0.439900952978621,125.904059910211));
#47056=CARTESIAN_POINT('Ctrl Pts',(96.9698537281263,0.308718879479279,125.895809332721));
#47057=CARTESIAN_POINT('Ctrl Pts',(96.9620793940072,0.172562997791085,125.887245932078));
#47058=CARTESIAN_POINT('Ctrl Pts',(96.9543050598881,0.0358348809967539,
125.884338402151));
#47059=CARTESIAN_POINT('Ctrl Pts',(96.946530725769,-0.10095615970339,125.8871468825));
#47060=CARTESIAN_POINT('Ctrl Pts',(96.9387659728219,-0.237578617671331,
125.889951901649));
#47061=CARTESIAN_POINT('Ctrl Pts',(96.9310012198748,-0.374263458117102,
125.898458906728));
#47062=CARTESIAN_POINT('Ctrl Pts',(96.9232364669277,-0.510496851076634,
125.912676242267));
#47063=CARTESIAN_POINT('Ctrl Pts',(96.9154794260428,-0.646594935109353,
125.926879456949));
#47064=CARTESIAN_POINT('Ctrl Pts',(96.9077223851578,-0.782242077623067,
125.946781675071));
#47065=CARTESIAN_POINT('Ctrl Pts',(96.8999653442728,-0.91692541110914,125.972339213126));
#47066=CARTESIAN_POINT('Ctrl Pts',(96.8922141530327,-1.05150717884621,125.997877478043));
#47067=CARTESIAN_POINT('Ctrl Pts',(96.8844629617925,-1.18512620168211,126.02906250163));
#47068=CARTESIAN_POINT('Ctrl Pts',(96.8767117705524,-1.31727604972572,126.06579892953));
#47069=CARTESIAN_POINT('Ctrl Pts',(96.8689638737753,-1.44936973055835,126.102519743469));
#47070=CARTESIAN_POINT('Ctrl Pts',(96.8612159769982,-1.57999510266655,126.14478716437));
#47071=CARTESIAN_POINT('Ctrl Pts',(96.8534680802212,-1.70865744606722,126.192455068392));
#47072=CARTESIAN_POINT('Ctrl Pts',(96.8457218041371,-1.83729287607921,126.240113001317));
#47073=CARTESIAN_POINT('Ctrl Pts',(96.837975528053,-1.96396572775514,126.293169034659));
#47074=CARTESIAN_POINT('Ctrl Pts',(96.8302292519689,-2.08819830806037,126.351427776313));
#47075=CARTESIAN_POINT('Ctrl Pts',(96.8224829187036,-2.21243180542237,126.409686948019));
#47076=CARTESIAN_POINT('Ctrl Pts',(96.8147365854383,-2.33422464149312,126.473148738675));
#47077=CARTESIAN_POINT('Ctrl Pts',(96.8069902521729,-2.45312127237363,126.541570558751));
#47078=CARTESIAN_POINT('Ctrl Pts',(96.79924218417,-2.57204452933009,126.61000770142));
#47079=CARTESIAN_POINT('Ctrl Pts',(96.791494116167,-2.68806995169109,126.683406888832));
#47080=CARTESIAN_POINT('Ctrl Pts',(96.783746048164,-2.80076901134863,126.761480949858));
#47081=CARTESIAN_POINT('Ctrl Pts',(96.7759897454222,-2.91358784890822,126.839637988925));
#47082=CARTESIAN_POINT('Ctrl Pts',(96.7682334426803,-3.02307293973397,126.922479603747));
#47083=CARTESIAN_POINT('Ctrl Pts',(96.7604771399385,-3.12882659363299,127.009676545146));
#47084=CARTESIAN_POINT('Ctrl Pts',(96.7527166974243,-3.23463669144135,127.096920026179));
#47085=CARTESIAN_POINT('Ctrl Pts',(96.7449562549102,-3.33671109309735,127.188523204692));
#47086=CARTESIAN_POINT('Ctrl Pts',(96.737195812396,-3.43468808372314,127.284119030682));
#47087=CARTESIAN_POINT('Ctrl Pts',(96.7294229121306,-3.53282235571221,127.379868315578));
#47088=CARTESIAN_POINT('Ctrl Pts',(96.7216500118651,-3.6268458043593,127.479622771209));
#47089=CARTESIAN_POINT('Ctrl Pts',(96.7138771115997,-3.71643562321466,127.582980583947));
#47090=CARTESIAN_POINT('Ctrl Pts',(96.7063867758376,-3.8027686264921,127.682581079849));
#47091=CARTESIAN_POINT('Ctrl Pts',(96.6988964400755,-3.88498455856165,127.785527258357));
#47092=CARTESIAN_POINT('Ctrl Pts',(96.6914061043134,-3.9628331180997,127.891434813397));
#47093=CARTESIAN_POINT('Ctrl Pts',(96.6835815201943,-4.04415558774659,128.002068381716));
#47094=CARTESIAN_POINT('Ctrl Pts',(96.6757569360752,-4.1209701239629,128.116284831714));
#47095=CARTESIAN_POINT('Ctrl Pts',(96.6679323519561,-4.19294682236243,128.233683662493));
#47096=CARTESIAN_POINT('Ctrl Pts',(96.660120876721,-4.26480293490392,128.350885809638));
#47097=CARTESIAN_POINT('Ctrl Pts',(96.6523094014859,-4.33183715470952,128.471259392883));
#47098=CARTESIAN_POINT('Ctrl Pts',(96.6444979262508,-4.3937609826322,128.594372497689));
#47099=CARTESIAN_POINT('Ctrl Pts',(96.636694006948,-4.45562491249,128.717366516886));
#47100=CARTESIAN_POINT('Ctrl Pts',(96.6288900876451,-4.51238811216936,128.843094445365));
#47101=CARTESIAN_POINT('Ctrl Pts',(96.6210861683423,-4.56380616556344,128.971096767035));
#47102=CARTESIAN_POINT('Ctrl Pts',(96.6132895369372,-4.61517620083963,129.098979550329));
#47103=CARTESIAN_POINT('Ctrl Pts',(96.6054929055322,-4.66121088771008,129.229132141857));
#47104=CARTESIAN_POINT('Ctrl Pts',(96.5976962741271,-4.70171268672026,129.361072401708));
#47105=CARTESIAN_POINT('Ctrl Pts',(96.5933658129799,-4.72420848752097,129.434355610745));
#47106=CARTESIAN_POINT('Ctrl Pts',(96.5890353518328,-4.74499823409669,129.508189917686));
#47107=CARTESIAN_POINT('Ctrl Pts',(96.5847048906856,-4.76405452823403,129.582490119308));
#47108=CARTESIAN_POINT('Ctrl Pts',(98.3346394208835,-4.76405452823406,129.582490119308));
#47109=CARTESIAN_POINT('Ctrl Pts',(98.3256757393383,-4.80320699701511,129.735145000864));
#47110=CARTESIAN_POINT('Ctrl Pts',(98.3167120577931,-4.83506113694242,129.889850790442));
#47111=CARTESIAN_POINT('Ctrl Pts',(98.3077483762479,-4.85942388963773,130.045952730398));
#47112=CARTESIAN_POINT('Ctrl Pts',(98.2988521815638,-4.88360321706305,130.200879390991));
#47113=CARTESIAN_POINT('Ctrl Pts',(98.2899559868796,-4.90040345683945,130.357181120761));
#47114=CARTESIAN_POINT('Ctrl Pts',(98.2810597921955,-4.90968317106223,130.51419821082));
#47115=CARTESIAN_POINT('Ctrl Pts',(98.2756596734789,-4.91531609168038,130.609509853266));
#47116=CARTESIAN_POINT('Ctrl Pts',(98.2702595547623,-4.91817887198582,130.705084709376));
#47117=CARTESIAN_POINT('Ctrl Pts',(98.2648594360457,-4.91824869076816,130.800771988677));
#47118=CARTESIAN_POINT('',(98.6101405639625,-4.91824985933626,130.803184335762));
#47119=CARTESIAN_POINT('Ctrl Pts',(98.680234964937,-4.76405452823403,129.582490119308));
#47120=CARTESIAN_POINT('Ctrl Pts',(98.6724723310953,-4.79811031872045,129.715273129546));
#47121=CARTESIAN_POINT('Ctrl Pts',(98.6647096972535,-4.82657976979179,129.849360886975));
#47122=CARTESIAN_POINT('Ctrl Pts',(98.6569470634118,-4.84939080559483,129.984243627672));
#47123=CARTESIAN_POINT('Ctrl Pts',(98.6491729046658,-4.87223570812522,130.119326623941));
#47124=CARTESIAN_POINT('Ctrl Pts',(98.6413987459199,-4.88940536950229,130.255206573573));
#47125=CARTESIAN_POINT('Ctrl Pts',(98.6336245871739,-4.90087964554873,130.391369379952));
#47126=CARTESIAN_POINT('Ctrl Pts',(98.6293998830641,-4.90711510108216,130.465364211612));
#47127=CARTESIAN_POINT('Ctrl Pts',(98.6251751789543,-4.91166953074298,130.539442574513));
#47128=CARTESIAN_POINT('Ctrl Pts',(98.6209504748445,-4.91454614522429,130.613522337965));
#47129=CARTESIAN_POINT('Ctrl Pts',(98.6173471712325,-4.91699964612792,130.676705905923));
#47130=CARTESIAN_POINT('Ctrl Pts',(98.6137438676204,-4.91823473268887,130.739937093408));
#47131=CARTESIAN_POINT('Ctrl Pts',(98.6101405640085,-4.91824985933606,130.803184334955));
#47132=CARTESIAN_POINT('Ctrl Pts',(98.6101405639625,-4.91824985933626,130.803184335762));
#47133=CARTESIAN_POINT('Ctrl Pts',(98.6024151385632,-4.91828229060402,130.938785411579));
#47134=CARTESIAN_POINT('Ctrl Pts',(98.5946897131639,-4.91270248946855,131.074612686756));
#47135=CARTESIAN_POINT('Ctrl Pts',(98.5869642877645,-4.90148042372996,131.210159481897));
#47136=CARTESIAN_POINT('Ctrl Pts',(98.5792482557868,-4.8902720030128,131.345541464339));
#47137=CARTESIAN_POINT('Ctrl Pts',(98.5715322238092,-4.87343499719098,131.480643254024));
#47138=CARTESIAN_POINT('Ctrl Pts',(98.5638161918315,-4.85099135081706,131.614956680225));
#47139=CARTESIAN_POINT('Ctrl Pts',(98.5561076368954,-4.82856945293771,131.749139953118));
#47140=CARTESIAN_POINT('Ctrl Pts',(98.5483990819594,-4.80055178889892,131.882535994059));
#47141=CARTESIAN_POINT('Ctrl Pts',(98.5406905270234,-4.76701218668155,132.014640698593));
#47142=CARTESIAN_POINT('Ctrl Pts',(98.5329875398277,-4.73349680947091,132.14664998645));
#47143=CARTESIAN_POINT('Ctrl Pts',(98.525284552632,-4.69446752830021,132.277369411346));
#47144=CARTESIAN_POINT('Ctrl Pts',(98.5175815654363,-4.65004935656035,132.406304450555));
#47145=CARTESIAN_POINT('Ctrl Pts',(98.5098814630934,-4.60564781991039,132.535191202186));
#47146=CARTESIAN_POINT('Ctrl Pts',(98.5021813607504,-4.55586153363794,132.662294522571));
#47147=CARTESIAN_POINT('Ctrl Pts',(98.4944812584075,-4.5008654577651,132.787134733192));
#47148=CARTESIAN_POINT('Ctrl Pts',(98.4867824355351,-4.44587852019431,132.911954200014));
#47149=CARTESIAN_POINT('Ctrl Pts',(98.4790836126627,-4.38568367425209,133.034510942316));
#47150=CARTESIAN_POINT('Ctrl Pts',(98.4713847897903,-4.32050395869148,133.154345427183));
#47151=CARTESIAN_POINT('Ctrl Pts',(98.4636855262004,-4.25532051193083,133.274186771952));
#47152=CARTESIAN_POINT('Ctrl Pts',(98.4559862626104,-4.18515181732883,133.391305201108));
#47153=CARTESIAN_POINT('Ctrl Pts',(98.4482869990204,-4.11026655844159,133.505266369542));
#47154=CARTESIAN_POINT('Ctrl Pts',(98.4405855745342,-4.03536028205367,133.619259522627));
#47155=CARTESIAN_POINT('Ctrl Pts',(98.4328841500479,-3.95573502574528,133.730093321226));
#47156=CARTESIAN_POINT('Ctrl Pts',(98.4251827255616,-3.87170214278111,133.837363350846));
#47157=CARTESIAN_POINT('Ctrl Pts',(98.4174729964773,-3.78757864550064,133.944749051856));
#47158=CARTESIAN_POINT('Ctrl Pts',(98.409763267393,-3.69903827632902,134.048562998609));
#47159=CARTESIAN_POINT('Ctrl Pts',(98.4020535383087,-3.60643219335031,134.148434465026));
#47160=CARTESIAN_POINT('Ctrl Pts',(98.3943392058232,-3.51377081621609,134.248365563686));
#47161=CARTESIAN_POINT('Ctrl Pts',(98.3866248733376,-3.41703917144957,134.34434921535));
#47162=CARTESIAN_POINT('Ctrl Pts',(98.3789105408521,-3.31662359250585,134.436053199288));
#47163=CARTESIAN_POINT('Ctrl Pts',(98.3711847186851,-3.21605845519007,134.527893766599));
#47164=CARTESIAN_POINT('Ctrl Pts',(98.3634588965182,-3.1117987301916,134.615441683928));
#47165=CARTESIAN_POINT('Ctrl Pts',(98.3557330743512,-3.00426238077046,134.698406150169));
#47166=CARTESIAN_POINT('Ctrl Pts',(98.3513229999113,-2.94287819463539,134.745764148332));
#47167=CARTESIAN_POINT('Ctrl Pts',(98.3469129254714,-2.8804268792548,134.791629486694));
#47168=CARTESIAN_POINT('Ctrl Pts',(98.3425028510316,-2.81698988540556,134.835954725115));
#47169=CARTESIAN_POINT('Ctrl Pts',(98.3347285169125,-2.70515948607426,134.914093817343));
#47170=CARTESIAN_POINT('Ctrl Pts',(98.3269541827934,-2.58989829891362,134.987700137634));
#47171=CARTESIAN_POINT('Ctrl Pts',(98.3191798486743,-2.47161002143893,135.056457390268));
#47172=CARTESIAN_POINT('Ctrl Pts',(98.3114150957272,-2.35346752369467,135.125129905733));
#47173=CARTESIAN_POINT('Ctrl Pts',(98.3036503427802,-2.23230569322079,135.188965049496));
#47174=CARTESIAN_POINT('Ctrl Pts',(98.2958855898331,-2.1085590295129,135.247688411186));
#47175=CARTESIAN_POINT('Ctrl Pts',(98.2881285489481,-1.98493527273594,135.306353448006));
#47176=CARTESIAN_POINT('Ctrl Pts',(98.2803715080631,-1.85873214268023,135.359916639869));
#47177=CARTESIAN_POINT('Ctrl Pts',(98.2726144671781,-1.73041038075421,135.408148511972));
#47178=CARTESIAN_POINT('Ctrl Pts',(98.264863275938,-1.60218538726696,135.456344012045));
#47179=CARTESIAN_POINT('Ctrl Pts',(98.2571120846979,-1.47184530647509,135.499216057703));
#47180=CARTESIAN_POINT('Ctrl Pts',(98.2493608934577,-1.33987225979488,135.536582652713));
#47181=CARTESIAN_POINT('Ctrl Pts',(98.2416129966807,-1.20795530517992,135.573933365924));
#47182=CARTESIAN_POINT('Ctrl Pts',(98.2338650999036,-1.07440714048701,135.60578317621));
#47183=CARTESIAN_POINT('Ctrl Pts',(98.2261172031265,-0.939726295431838,
135.63199953863));
#47184=CARTESIAN_POINT('Ctrl Pts',(98.2183709270424,-0.805073622705975,
135.658210417153));
#47185=CARTESIAN_POINT('Ctrl Pts',(98.2106246509583,-0.669289124408354,
135.67879011705));
#47186=CARTESIAN_POINT('Ctrl Pts',(98.2028783748742,-0.532882416594516,
135.693657028358));
#47187=CARTESIAN_POINT('Ctrl Pts',(98.1951320416089,-0.396474701857627,
135.708524049411));
#47188=CARTESIAN_POINT('Ctrl Pts',(98.1873857083435,-0.259445157103111,
135.717678155366));
#47189=CARTESIAN_POINT('Ctrl Pts',(98.1796393750782,-0.122309032878326,
135.721089567079));
#47190=CARTESIAN_POINT('Ctrl Pts',(98.1718913070752,0.014857802030737,135.724501742753));
#47191=CARTESIAN_POINT('Ctrl Pts',(98.1641432390723,0.152130873134605,135.722168655401));
#47192=CARTESIAN_POINT('Ctrl Pts',(98.1563951710693,0.288994812493648,135.714112654161));
#47193=CARTESIAN_POINT('Ctrl Pts',(98.1486388683274,0.426004212476236,135.706048090908));
#47194=CARTESIAN_POINT('Ctrl Pts',(98.1408825655856,0.562603221182044,135.692248486566));
#47195=CARTESIAN_POINT('Ctrl Pts',(98.1331262628437,0.69828091988794,135.672788168575));
#47196=CARTESIAN_POINT('Ctrl Pts',(98.1253658203296,0.834031033866721,135.653317464026));
#47197=CARTESIAN_POINT('Ctrl Pts',(98.1176053778154,0.968858473875881,135.628180097266));
#47198=CARTESIAN_POINT('Ctrl Pts',(98.1098449353013,1.10226338296286,135.597501393412));
#47199=CARTESIAN_POINT('Ctrl Pts',(98.1020720350358,1.23588244545332,135.566773441379));
#47200=CARTESIAN_POINT('Ctrl Pts',(98.0942991347704,1.36807403647961,135.530486479867));
#47201=CARTESIAN_POINT('Ctrl Pts',(98.0865262345049,1.49835344579429,135.488815763469));
#47202=CARTESIAN_POINT('Ctrl Pts',(98.0790358987429,1.62389687042671,135.448659882574));
#47203=CARTESIAN_POINT('Ctrl Pts',(98.0715455629808,1.74766443554663,135.403504982735));
#47204=CARTESIAN_POINT('Ctrl Pts',(98.0640552272188,1.86924246149423,135.353549081748));
#47205=CARTESIAN_POINT('Ctrl Pts',(98.0562808930997,1.99543015524821,135.301699087592));
#47206=CARTESIAN_POINT('Ctrl Pts',(98.0485065589806,2.11965872421962,135.244512600519));
#47207=CARTESIAN_POINT('Ctrl Pts',(98.0407322248615,2.24144385149432,135.182158297119));
#47208=CARTESIAN_POINT('Ctrl Pts',(98.0329674719144,2.3630788894839,135.119880839825));
#47209=CARTESIAN_POINT('Ctrl Pts',(98.0252027189673,2.48227613275066,135.05244841483));
#47210=CARTESIAN_POINT('Ctrl Pts',(98.0174379660202,2.59856985448748,134.980078253356));
#47211=CARTESIAN_POINT('Ctrl Pts',(98.0096809251352,2.71474807166018,134.907779970947));
#47212=CARTESIAN_POINT('Ctrl Pts',(98.0019238842502,2.82802817644063,134.830553916928));
#47213=CARTESIAN_POINT('Ctrl Pts',(97.9941668433652,2.93796806319306,134.748663689359));
#47214=CARTESIAN_POINT('Ctrl Pts',(97.986415652125,3.04782504342185,134.666835215848));
#47215=CARTESIAN_POINT('Ctrl Pts',(97.9786644608849,3.15434650703443,134.58034980234));
#47216=CARTESIAN_POINT('Ctrl Pts',(97.9709132696448,3.25711873704543,134.48951469783));
#47217=CARTESIAN_POINT('Ctrl Pts',(97.9631653728677,3.35984728611713,134.398718200663));
#47218=CARTESIAN_POINT('Ctrl Pts',(97.9554174760906,3.45882947865587,134.30357594786));
#47219=CARTESIAN_POINT('Ctrl Pts',(97.9476695793135,3.55368433336097,134.204435722814));
#47220=CARTESIAN_POINT('Ctrl Pts',(97.9399233032294,3.64851934647537,134.105316235765));
#47221=CARTESIAN_POINT('Ctrl Pts',(97.9321770271453,3.73922846889674,134.002200722212));
#47222=CARTESIAN_POINT('Ctrl Pts',(97.9244307510611,3.82546757992572,133.895473824396));
#47223=CARTESIAN_POINT('Ctrl Pts',(97.9166844177958,3.91170732755224,133.788746138746));
#47224=CARTESIAN_POINT('Ctrl Pts',(97.9089380845304,3.99347675222295,133.678407319736));
#47225=CARTESIAN_POINT('Ctrl Pts',(97.9011917512651,4.07047229439274,133.564874765887));
#47226=CARTESIAN_POINT('Ctrl Pts',(97.8934436832621,4.14748507918008,133.451316787211));
#47227=CARTESIAN_POINT('Ctrl Pts',(97.8856956152591,4.21972163472643,133.334563974013));
#47228=CARTESIAN_POINT('Ctrl Pts',(97.8779475472562,4.28692219503683,133.215062000193));
#47229=CARTESIAN_POINT('Ctrl Pts',(97.8701912445143,4.3541941769026,133.095433018253));
#47230=CARTESIAN_POINT('Ctrl Pts',(97.8624349417724,4.41641927976647,132.973049380323));
#47231=CARTESIAN_POINT('Ctrl Pts',(97.8546786390306,4.47338387335798,132.848381112591));
#47232=CARTESIAN_POINT('Ctrl Pts',(97.8469181965164,4.53037887066826,132.72364630565));
#47233=CARTESIAN_POINT('Ctrl Pts',(97.8391577540022,4.58210761675472,132.596624801111));
#47234=CARTESIAN_POINT('Ctrl Pts',(97.8313973114881,4.62840536629358,132.46780488407));
#47235=CARTESIAN_POINT('Ctrl Pts',(97.8236244112226,4.67477743709015,132.338778173862));
#47236=CARTESIAN_POINT('Ctrl Pts',(97.8158515109572,4.71570097257844,132.207947655416));
#47237=CARTESIAN_POINT('Ctrl Pts',(97.8080786106917,4.75106142168296,132.075815858578));
#47238=CARTESIAN_POINT('Ctrl Pts',(97.8005882749297,4.78513642939482,131.948487385375));
#47239=CARTESIAN_POINT('Ctrl Pts',(97.7930979391677,4.81404572544429,131.819950901228));
#47240=CARTESIAN_POINT('Ctrl Pts',(97.7856076034057,4.83773230385249,131.690661480006));
#47241=CARTESIAN_POINT('Ctrl Pts',(97.7778332692866,4.86231696608044,131.556470011082));
#47242=CARTESIAN_POINT('Ctrl Pts',(97.7700589351675,4.88135293088056,131.42104230455));
#47243=CARTESIAN_POINT('Ctrl Pts',(97.7622846010484,4.89472032552374,131.284877003764));
#47244=CARTESIAN_POINT('Ctrl Pts',(97.7545198481013,4.90807124604772,131.148879514542));
#47245=CARTESIAN_POINT('Ctrl Pts',(97.7467550951542,4.91576745865379,131.012146625102));
#47246=CARTESIAN_POINT('Ctrl Pts',(97.7389903422071,4.9177399894071,130.875187583379));
#47247=CARTESIAN_POINT('Ctrl Pts',(97.7312333013221,4.91971056101505,130.738364571308));
#47248=CARTESIAN_POINT('Ctrl Pts',(97.7234762604371,4.91596875826757,130.601316242348));
#47249=CARTESIAN_POINT('Ctrl Pts',(97.7157192195521,4.90649738478277,130.464557033683));
#47250=CARTESIAN_POINT('Ctrl Pts',(97.707968028312,4.89703315373438,130.3279009562));
#47251=CARTESIAN_POINT('Ctrl Pts',(97.7002168370719,4.88184797897018,130.191533953494));
#47252=CARTESIAN_POINT('Ctrl Pts',(97.6924656458317,4.86097673363409,130.055970172966));
#47253=CARTESIAN_POINT('Ctrl Pts',(97.6847177490546,4.84011435913408,129.920464010662));
#47254=CARTESIAN_POINT('Ctrl Pts',(97.6769698522775,4.81357078012432,129.78576077714));
#47255=CARTESIAN_POINT('Ctrl Pts',(97.6692219555005,4.7814326669225,129.652368988175));
#47256=CARTESIAN_POINT('Ctrl Pts',(97.6614756794164,4.74930127632112,129.519005101897));
#47257=CARTESIAN_POINT('Ctrl Pts',(97.6537294033323,4.71157777074786,129.386952494377));
#47258=CARTESIAN_POINT('Ctrl Pts',(97.6459831272482,4.66839975497106,129.256708592631));
#47259=CARTESIAN_POINT('Ctrl Pts',(97.6382367939828,4.62522142046395,129.126463729454));
#47260=CARTESIAN_POINT('Ctrl Pts',(97.6304904607175,4.57658861843661,128.998027969798));
#47261=CARTESIAN_POINT('Ctrl Pts',(97.6227441274521,4.52268843673838,128.871882321001));
#47262=CARTESIAN_POINT('Ctrl Pts',(97.6149960594491,4.46877618446803,128.745708422762));
#47263=CARTESIAN_POINT('Ctrl Pts',(97.6072479914461,4.40959435886156,128.621826015355));
#47264=CARTESIAN_POINT('Ctrl Pts',(97.5994999234431,4.34537750812776,128.500694544899));
#47265=CARTESIAN_POINT('Ctrl Pts',(97.5917436207013,4.28109240696095,128.379434334475));
#47266=CARTESIAN_POINT('Ctrl Pts',(97.5839873179594,4.2117617743161,128.260931247441));
#47267=CARTESIAN_POINT('Ctrl Pts',(97.5762310152175,4.13766558415761,128.145619077631));
#47268=CARTESIAN_POINT('Ctrl Pts',(97.5684705727034,4.06352984663144,128.030245362243));
#47269=CARTESIAN_POINT('Ctrl Pts',(97.5607101301892,3.98462370823129,127.91806627725));
#47270=CARTESIAN_POINT('Ctrl Pts',(97.552949687675,3.90126892816643,127.809484357581));
#47271=CARTESIAN_POINT('Ctrl Pts',(97.5451767874096,3.81778033960878,127.700728132575));
#47272=CARTESIAN_POINT('Ctrl Pts',(97.5374038871442,3.7298290896713,127.59558091222));
#47273=CARTESIAN_POINT('Ctrl Pts',(97.5296309868788,3.63777605329274,127.494410701239));
#47274=CARTESIAN_POINT('Ctrl Pts',(97.5221406511168,3.54906937665477,127.396918282261));
#47275=CARTESIAN_POINT('Ctrl Pts',(97.5146503153548,3.45655417286324,127.303118963381));
#47276=CARTESIAN_POINT('Ctrl Pts',(97.5071599795928,3.36058249532988,127.213306683888));
#47277=CARTESIAN_POINT('Ctrl Pts',(97.4993856454738,3.26097202247225,127.12008914452));
#47278=CARTESIAN_POINT('Ctrl Pts',(97.4916113113547,3.15732226140873,127.030871664821));
#47279=CARTESIAN_POINT('Ctrl Pts',(97.4838369772356,3.04998794077722,126.946024626026));
#47280=CARTESIAN_POINT('Ctrl Pts',(97.4760722242885,2.9427859001033,126.861282153624));
#47281=CARTESIAN_POINT('Ctrl Pts',(97.4683074713414,2.83190863864512,126.780899645361));
#47282=CARTESIAN_POINT('Ctrl Pts',(97.4605427183944,2.71774731901665,126.705210391912));
#47283=CARTESIAN_POINT('Ctrl Pts',(97.4527856775094,2.60369938602014,126.629596314097));
#47284=CARTESIAN_POINT('Ctrl Pts',(97.4450286366244,2.48637420967266,126.558666429327));
#47285=CARTESIAN_POINT('Ctrl Pts',(97.4372715957394,2.36619530548107,126.49271327127));
#47286=CARTESIAN_POINT('Ctrl Pts',(97.4295204044993,2.2461070291359,126.426809849003));
#47287=CARTESIAN_POINT('Ctrl Pts',(97.4217692132591,2.12316964976652,126.365875870686));
#47288=CARTESIAN_POINT('Ctrl Pts',(97.414018022019,1.99783458393054,126.310159905787));
#47289=CARTESIAN_POINT('Ctrl Pts',(97.4062701252419,1.87255278884078,126.25446762166));
#47290=CARTESIAN_POINT('Ctrl Pts',(97.3985222284649,1.74487569066665,126.203989098405));
#47291=CARTESIAN_POINT('Ctrl Pts',(97.3907743316878,1.61527796555632,126.15892628303));
#47292=CARTESIAN_POINT('Ctrl Pts',(97.3830280556036,1.4857073494961,126.113872893824));
#47293=CARTESIAN_POINT('Ctrl Pts',(97.3752817795196,1.3542172746543,126.074233087518));
#47294=CARTESIAN_POINT('Ctrl Pts',(97.3675355034354,1.22130061920716,126.040159964778));
#47295=CARTESIAN_POINT('Ctrl Pts',(97.3597891701701,1.08838298259992,126.006086590518));
#47296=CARTESIAN_POINT('Ctrl Pts',(97.3520428369047,0.954039123093512,125.977580078904));
#47297=CARTESIAN_POINT('Ctrl Pts',(97.3442965036394,0.818774851338005,125.954743023846));
#47298=CARTESIAN_POINT('Ctrl Pts',(97.3365484356364,0.683480288086327,125.931900854588));
#47299=CARTESIAN_POINT('Ctrl Pts',(97.3288003676334,0.547265287866364,125.914730733388));
#47300=CARTESIAN_POINT('Ctrl Pts',(97.3210522996304,0.410643174745097,125.903283670044));
#47301=CARTESIAN_POINT('Ctrl Pts',(97.3132959968886,0.273875858016367,125.891824440624));
#47302=CARTESIAN_POINT('Ctrl Pts',(97.3055396941468,0.136700954273868,125.886100452274));
#47303=CARTESIAN_POINT('Ctrl Pts',(97.2977833914049,-0.000365240678962547,
125.886110631128));
#47304=CARTESIAN_POINT('Ctrl Pts',(97.2900229488907,-0.137504591987303,
125.886120815415));
#47305=CARTESIAN_POINT('Ctrl Pts',(97.2822625063765,-0.274534728463636,
125.891871248824));
#47306=CARTESIAN_POINT('Ctrl Pts',(97.2745020638624,-0.41094306736016,125.90330880618));
#47307=CARTESIAN_POINT('Ctrl Pts',(97.2667291635969,-0.547570381031765,
125.914764724119));
#47308=CARTESIAN_POINT('Ctrl Pts',(97.2589562633315,-0.683573514359819,
125.931925960635));
#47309=CARTESIAN_POINT('Ctrl Pts',(97.2511833630661,-0.818447792830363,
125.954687816963));
#47310=CARTESIAN_POINT('Ctrl Pts',(97.243693027304,-0.948419051550785,125.976622222479));
#47311=CARTESIAN_POINT('Ctrl Pts',(97.236202691542,-1.07734180251876,126.003757060566));
#47312=CARTESIAN_POINT('Ctrl Pts',(97.22871235578,-1.20477845281854,126.035955020081));
#47313=CARTESIAN_POINT('Ctrl Pts',(97.2209380216609,-1.33704690244797,126.069373775018));
#47314=CARTESIAN_POINT('Ctrl Pts',(97.2131636875418,-1.46813332253031,126.108353027479));
#47315=CARTESIAN_POINT('Ctrl Pts',(97.2053893534227,-1.59753436134945,126.15279453432));
#47316=CARTESIAN_POINT('Ctrl Pts',(97.1976246004756,-1.72677592495342,126.197181270975));
#47317=CARTESIAN_POINT('Ctrl Pts',(97.1898598475285,-1.85433587385178,126.24701674208));
#47318=CARTESIAN_POINT('Ctrl Pts',(97.1820950945814,-1.97972236821465,126.302152003198));
#47319=CARTESIAN_POINT('Ctrl Pts',(97.1743380536963,-2.10498432694351,126.357232503197));
#47320=CARTESIAN_POINT('Ctrl Pts',(97.1665810128113,-2.22807677148156,126.417602161604));
#47321=CARTESIAN_POINT('Ctrl Pts',(97.1588239719263,-2.34852466449414,126.483062784419));
#47322=CARTESIAN_POINT('Ctrl Pts',(97.1510727806863,-2.46888172681226,126.548474042868));
#47323=CARTESIAN_POINT('Ctrl Pts',(97.1433215894462,-2.58659786497023,126.618968438223));
#47324=CARTESIAN_POINT('Ctrl Pts',(97.1355703982062,-2.70121994876031,126.694300538818));
#47325=CARTESIAN_POINT('Ctrl Pts',(97.1278225014291,-2.81579331510837,126.769600621261));
#47326=CARTESIAN_POINT('Ctrl Pts',(97.120074604652,-2.92727491659795,126.849734105133));
#47327=CARTESIAN_POINT('Ctrl Pts',(97.1123267078749,-3.03523827544131,126.934410789235));
#47328=CARTESIAN_POINT('Ctrl Pts',(97.1045804317908,-3.14317905067756,127.019069760801));
#47329=CARTESIAN_POINT('Ctrl Pts',(97.0968341557066,-3.24760273965558,127.108269801194));
#47330=CARTESIAN_POINT('Ctrl Pts',(97.0890878796225,-3.34811412175674,127.201678992694));
#47331=CARTESIAN_POINT('Ctrl Pts',(97.0813415463572,-3.44862624580946,127.295088873718));
#47332=CARTESIAN_POINT('Ctrl Pts',(97.0735952130919,-3.54522571897084,127.392707701699));
#47333=CARTESIAN_POINT('Ctrl Pts',(97.0658488798266,-3.63755282306729,127.494165378325));
#47334=CARTESIAN_POINT('Ctrl Pts',(97.0581008118236,-3.72990060317879,127.595645775694));
#47335=CARTESIAN_POINT('Ctrl Pts',(97.0503527438206,-3.81797384728278,127.700966443276));
#47336=CARTESIAN_POINT('Ctrl Pts',(97.0426046758177,-3.90145217519436,127.809723079036));
#47337=CARTESIAN_POINT('Ctrl Pts',(97.0348483730758,-3.98501922486635,127.918595302644));
#47338=CARTESIAN_POINT('Ctrl Pts',(97.0270920703339,-4.06398136453394,128.030910478637));
#47339=CARTESIAN_POINT('Ctrl Pts',(97.0193357675921,-4.13806042717554,128.146233652287));
#47340=CARTESIAN_POINT('Ctrl Pts',(97.0115753250779,-4.21217902804339,128.261618377387));
#47341=CARTESIAN_POINT('Ctrl Pts',(97.0038148825637,-4.28140916146843,128.380013961819));
#47342=CARTESIAN_POINT('Ctrl Pts',(96.9960544400495,-4.34551845966848,128.500960439746));
#47343=CARTESIAN_POINT('Ctrl Pts',(96.9882815397841,-4.40973067180539,128.622101071697));
#47344=CARTESIAN_POINT('Ctrl Pts',(96.9805086395186,-4.4688054531182,128.745800427099));
#47345=CARTESIAN_POINT('Ctrl Pts',(96.9727357392532,-4.52255810074129,128.871577316748));
#47346=CARTESIAN_POINT('Ctrl Pts',(96.9652454034911,-4.57435670422879,128.992781899647));
#47347=CARTESIAN_POINT('Ctrl Pts',(96.957755067729,-4.62121329245976,129.11591530411));
#47348=CARTESIAN_POINT('Ctrl Pts',(96.9502647319669,-4.66300685952642,129.240535150799));
#47349=CARTESIAN_POINT('Ctrl Pts',(96.9434939960896,-4.70078530003539,129.353182713445));
#47350=CARTESIAN_POINT('Ctrl Pts',(96.9367232602123,-4.73449998266919,129.467257394704));
#47351=CARTESIAN_POINT('Ctrl Pts',(96.929952524335,-4.76405452823407,129.582490119308));
#47352=CARTESIAN_POINT('Origin',(213.235140564004,0.,130.804360617566));
#47353=CARTESIAN_POINT('',(94.8350013119177,-4.76405452823406,129.582490119308));
#47354=CARTESIAN_POINT('',(95.1799533855057,-4.76405452823404,129.582490119308));
#47355=CARTESIAN_POINT('',(213.235140564004,-4.76405452823405,129.582490119308));
#47356=CARTESIAN_POINT('',(96.5148594359362,-4.91824890228215,130.807646603022));
#47357=CARTESIAN_POINT('Ctrl Pts',(96.5148594359362,-4.91824890228215,130.807646603022));
#47358=CARTESIAN_POINT('Ctrl Pts',(96.5060769269297,-4.91814488454752,130.963333569976));
#47359=CARTESIAN_POINT('Ctrl Pts',(96.4972944179233,-4.91064446456671,131.118734022512));
#47360=CARTESIAN_POINT('Ctrl Pts',(96.4885119089168,-4.89585318662738,131.273193890159));
#47361=CARTESIAN_POINT('Ctrl Pts',(96.4796923871704,-4.88099957277427,131.428304708795));
#47362=CARTESIAN_POINT('Ctrl Pts',(96.470872865424,-4.85879362968525,131.58246682585));
#47363=CARTESIAN_POINT('Ctrl Pts',(96.4620533436776,-4.82939196962361,131.73503578444));
#47364=CARTESIAN_POINT('Ctrl Pts',(96.4531830551799,-4.79982106832561,131.888482957359));
#47365=CARTESIAN_POINT('Ctrl Pts',(96.4443127666822,-4.76297146670377,132.04031840757));
#47366=CARTESIAN_POINT('Ctrl Pts',(96.4354424781845,-4.7190511585257,132.189907161612));
#47367=CARTESIAN_POINT('Ctrl Pts',(96.4279478122898,-4.68194210216631,132.316297383692));
#47368=CARTESIAN_POINT('Ctrl Pts',(96.4204531463951,-4.63978623720257,132.441084028861));
#47369=CARTESIAN_POINT('Ctrl Pts',(96.4129584805004,-4.59273507530652,132.563896803767));
#47370=CARTESIAN_POINT('Ctrl Pts',(96.4051841463814,-4.54392816938009,132.691292415476));
#47371=CARTESIAN_POINT('Ctrl Pts',(96.3974098122623,-4.48973929372166,132.816857527698));
#47372=CARTESIAN_POINT('Ctrl Pts',(96.3896354781432,-4.43032545407694,132.940103915216));
#47373=CARTESIAN_POINT('Ctrl Pts',(96.3818707251961,-4.37098483667964,133.063198412577));
#47374=CARTESIAN_POINT('Ctrl Pts',(96.374105972249,-4.30643223573233,133.183979522251));
#47375=CARTESIAN_POINT('Ctrl Pts',(96.366341219302,-4.23687364374173,133.301976438597));
#47376=CARTESIAN_POINT('Ctrl Pts',(96.358584178417,-4.1673841383253,133.419856158744));
#47377=CARTESIAN_POINT('Ctrl Pts',(96.350827137532,-4.09289873366908,133.534956854013));
#47378=CARTESIAN_POINT('Ctrl Pts',(96.343070096647,-4.01367034260699,133.64683022046));
#47379=CARTESIAN_POINT('Ctrl Pts',(96.3353189054069,-3.93450169829108,133.758619222331));
#47380=CARTESIAN_POINT('Ctrl Pts',(96.3275677141668,-3.85059741186087,133.867185421851));
#47381=CARTESIAN_POINT('Ctrl Pts',(96.3198165229267,-3.76225471576301,133.972107848047));
#47382=CARTESIAN_POINT('Ctrl Pts',(96.3120686261496,-3.67394956766743,134.076985679413));
#47383=CARTESIAN_POINT('Ctrl Pts',(96.3043207293725,-3.58121001318023,134.178222519257));
#47384=CARTESIAN_POINT('Ctrl Pts',(96.2965728325955,-3.48437459303877,134.275429150149));
#47385=CARTESIAN_POINT('Ctrl Pts',(96.2888265565114,-3.38755942877967,134.372615447509));
#47386=CARTESIAN_POINT('Ctrl Pts',(96.2810802804273,-3.28665037877241,134.465772935949));
#47387=CARTESIAN_POINT('Ctrl Pts',(96.2733340043432,-3.1820237165437,134.554548363513));
#47388=CARTESIAN_POINT('Ctrl Pts',(96.2655876710778,-3.07739628198474,134.643324446398));
#47389=CARTESIAN_POINT('Ctrl Pts',(96.2578413378125,-2.9690514785574,134.727718150913));
#47390=CARTESIAN_POINT('Ctrl Pts',(96.2500950045471,-2.8573992999917,134.807415988518));
#47391=CARTESIAN_POINT('Ctrl Pts',(96.2423469365442,-2.74572211769482,134.887131673901));
#47392=CARTESIAN_POINT('Ctrl Pts',(96.2345988685412,-2.63073640457746,134.962149172698));
#47393=CARTESIAN_POINT('Ctrl Pts',(96.2268508005383,-2.51288147252894,135.032198098776));
#47394=CARTESIAN_POINT('Ctrl Pts',(96.2190944977964,-2.39490128285606,135.102321473686));
#47395=CARTESIAN_POINT('Ctrl Pts',(96.2113381950546,-2.27404611928539,135.167465527119));
#47396=CARTESIAN_POINT('Ctrl Pts',(96.2035818923127,-2.15078074611151,135.227405410992));
#47397=CARTESIAN_POINT('Ctrl Pts',(96.1958214497986,-2.02744958249652,135.287377286586));
#47398=CARTESIAN_POINT('Ctrl Pts',(96.1880610072844,-1.90170600428682,135.342139301944));
#47399=CARTESIAN_POINT('Ctrl Pts',(96.1803005647702,-1.77403420253166,135.391515041689));
#47400=CARTESIAN_POINT('Ctrl Pts',(96.1725276645048,-1.64615745066616,135.440970043754));
#47401=CARTESIAN_POINT('Ctrl Pts',(96.1647547642394,-1.51634666018989,135.485021365978));
#47402=CARTESIAN_POINT('Ctrl Pts',(96.156981863974,-1.38510146732424,135.523542430944));
#47403=CARTESIAN_POINT('Ctrl Pts',(96.1494915282119,-1.25862736780407,135.56066315817));
#47404=CARTESIAN_POINT('Ctrl Pts',(96.1420011924497,-1.13082164237983,135.592648650262));
#47405=CARTESIAN_POINT('Ctrl Pts',(96.1345108566876,-1.00213786588589,135.619430997141));
#47406=CARTESIAN_POINT('Ctrl Pts',(96.1267365225685,-0.868575004895484,
135.647228804841));
#47407=CARTESIAN_POINT('Ctrl Pts',(96.1189621884494,-0.733643108864154,
135.669509179295));
#47408=CARTESIAN_POINT('Ctrl Pts',(96.1111878543303,-0.597837800933942,
135.686140316229));
#47409=CARTESIAN_POINT('Ctrl Pts',(96.1034231013832,-0.462199860908578,
135.702750956772));
#47410=CARTESIAN_POINT('Ctrl Pts',(96.0956583484362,-0.325691035044379,
135.713726165392));
#47411=CARTESIAN_POINT('Ctrl Pts',(96.0878935954891,-0.188818769441456,
135.718984767469));
#47412=CARTESIAN_POINT('Ctrl Pts',(96.0801365546041,-0.0520824473022909,
135.724238146628));
#47413=CARTESIAN_POINT('Ctrl Pts',(96.072379513719,0.0850162080731771,135.723786203438));
#47414=CARTESIAN_POINT('Ctrl Pts',(96.064622472834,0.221963320313328,135.717599401396));
#47415=CARTESIAN_POINT('Ctrl Pts',(96.0568712815939,0.358807159670751,135.71141726487));
#47416=CARTESIAN_POINT('Ctrl Pts',(96.0491200903538,0.495499294373461,135.699508895121));
#47417=CARTESIAN_POINT('Ctrl Pts',(96.0413688991137,0.631524888220994,135.68189681713));
#47418=CARTESIAN_POINT('Ctrl Pts',(96.0336210023366,0.767492667562634,135.664292224742));
#47419=CARTESIAN_POINT('Ctrl Pts',(96.0258731055595,0.902794082589508,135.640988795814));
#47420=CARTESIAN_POINT('Ctrl Pts',(96.0181252087825,1.03691868411676,135.612060972729));
#47421=CARTESIAN_POINT('Ctrl Pts',(96.0103789326983,1.17101522966885,135.58313920072));
#47422=CARTESIAN_POINT('Ctrl Pts',(96.0026326566142,1.30393506941985,135.548595457055));
#47423=CARTESIAN_POINT('Ctrl Pts',(95.9948863805301,1.43517761746382,135.50855537));
#47424=CARTESIAN_POINT('Ctrl Pts',(95.9871400472648,1.56642113431028,135.468514987378));
#47425=CARTESIAN_POINT('Ctrl Pts',(95.9793937139994,1.69598696079417,135.422978294492));
#47426=CARTESIAN_POINT('Ctrl Pts',(95.971647380734,1.82338973850166,135.372120782464));
#47427=CARTESIAN_POINT('Ctrl Pts',(95.963899312731,1.95082104717796,135.321251881248));
#47428=CARTESIAN_POINT('Ctrl Pts',(95.9561512447281,2.07608798014407,135.265059934742));
#47429=CARTESIAN_POINT('Ctrl Pts',(95.9484031767252,2.19872559508115,135.20376839817));
#47430=CARTESIAN_POINT('Ctrl Pts',(95.9406468739833,2.32149355073488,135.142411720223));
#47431=CARTESIAN_POINT('Ctrl Pts',(95.9328905712414,2.44162625582511,135.075944800427));
#47432=CARTESIAN_POINT('Ctrl Pts',(95.9251342684996,2.55868332283812,135.004637122265));
#47433=CARTESIAN_POINT('Ctrl Pts',(95.9173738259854,2.67580286673239,134.933291385049));
#47434=CARTESIAN_POINT('Ctrl Pts',(95.9096133834712,2.78984317667386,134.857099958395));
#47435=CARTESIAN_POINT('Ctrl Pts',(95.901852940957,2.90039411232023,134.776374849126));
#47436=CARTESIAN_POINT('Ctrl Pts',(95.8940800406916,3.01112251414267,134.695520152746));
#47437=CARTESIAN_POINT('Ctrl Pts',(95.8863071404261,3.11835004218567,134.610117473961));
#47438=CARTESIAN_POINT('Ctrl Pts',(95.8785342401607,3.22170013770037,134.520518752689));
#47439=CARTESIAN_POINT('Ctrl Pts',(95.8710439043987,3.32129319691959,134.434177170621));
#47440=CARTESIAN_POINT('Ctrl Pts',(95.8635535686367,3.4172856137117,134.343939533942));
#47441=CARTESIAN_POINT('Ctrl Pts',(95.8560632328747,3.50937508512537,134.250150740949));
#47442=CARTESIAN_POINT('Ctrl Pts',(95.8482888987556,3.60495615683794,134.152805917362));
#47443=CARTESIAN_POINT('Ctrl Pts',(95.8405145646365,3.69663525257884,134.051326978382));
#47444=CARTESIAN_POINT('Ctrl Pts',(95.8327402305174,3.78403358526469,133.946059662365));
#47445=CARTESIAN_POINT('Ctrl Pts',(95.8249754775703,3.87132420731645,133.840922078907));
#47446=CARTESIAN_POINT('Ctrl Pts',(95.8172107246233,3.95434431595511,133.73200570592));
#47447=CARTESIAN_POINT('Ctrl Pts',(95.8094459716762,4.03275132966307,133.619693595315));
#47448=CARTESIAN_POINT('Ctrl Pts',(95.8016889307912,4.11108046841973,133.507493034682));
#47449=CARTESIAN_POINT('Ctrl Pts',(95.7939318899062,4.18480540786601,133.391903766746));
#47450=CARTESIAN_POINT('Ctrl Pts',(95.7861748490212,4.25362353537386,133.273342165049));
#47451=CARTESIAN_POINT('Ctrl Pts',(95.778423657781,4.32238976659642,133.154869971579));
#47452=CARTESIAN_POINT('Ctrl Pts',(95.7706724665409,4.38625635556175,133.033430242604));
#47453=CARTESIAN_POINT('Ctrl Pts',(95.7629212753008,4.44496397163262,132.909468299702));
#47454=CARTESIAN_POINT('Ctrl Pts',(95.7551733785237,4.50364663540059,132.785559043933));
#47455=CARTESIAN_POINT('Ctrl Pts',(95.7474254817466,4.55717452039897,132.659130058982));
#47456=CARTESIAN_POINT('Ctrl Pts',(95.7396775849696,4.60533434685947,132.530651038132));
#47457=CARTESIAN_POINT('Ctrl Pts',(95.7319313088855,4.65348409932249,132.402198892323));
#47458=CARTESIAN_POINT('Ctrl Pts',(95.7241850328014,4.69626788958109,132.271697929427));
#47459=CARTESIAN_POINT('Ctrl Pts',(95.7164387567173,4.73352083334267,132.139637211688));
#47460=CARTESIAN_POINT('Ctrl Pts',(95.708692423452,4.770774052097,132.007575519108));
#47461=CARTESIAN_POINT('Ctrl Pts',(95.7009460901865,4.8024962367413,131.873954424991));
#47462=CARTESIAN_POINT('Ctrl Pts',(95.6931997569212,4.82857268484914,131.739277132357));
#47463=CARTESIAN_POINT('Ctrl Pts',(95.6854516889182,4.85465497259673,131.604569679676));
#47464=CARTESIAN_POINT('Ctrl Pts',(95.6777036209153,4.8750889336455,131.468805941577));
#47465=CARTESIAN_POINT('Ctrl Pts',(95.6699555529123,4.8898112545244,131.332497870206));
#47466=CARTESIAN_POINT('Ctrl Pts',(95.6621992501705,4.90454922246114,131.196044928995));
#47467=CARTESIAN_POINT('Ctrl Pts',(95.6544429474286,4.91356338190181,131.059046888174));
#47468=CARTESIAN_POINT('Ctrl Pts',(95.6466866446868,4.91684241672453,130.922019920634));
#47469=CARTESIAN_POINT('Ctrl Pts',(95.6389262021726,4.92012320166686,130.784919817676));
#47470=CARTESIAN_POINT('Ctrl Pts',(95.6311657596585,4.91766276968259,130.647791147948));
#47471=CARTESIAN_POINT('Ctrl Pts',(95.6234053171443,4.90950193007445,130.511147621443));
#47472=CARTESIAN_POINT('Ctrl Pts',(95.6156324168789,4.90132798996209,130.374284742619));
#47473=CARTESIAN_POINT('Ctrl Pts',(95.6078595166134,4.8874353956562,130.237908952476));
#47474=CARTESIAN_POINT('Ctrl Pts',(95.600086616348,4.86791670497473,130.102527292675));
#47475=CARTESIAN_POINT('Ctrl Pts',(95.592596280586,4.84910756786409,129.972067097213));
#47476=CARTESIAN_POINT('Ctrl Pts',(95.5851059448239,4.8250743344845,129.842530311516));
#47477=CARTESIAN_POINT('Ctrl Pts',(95.5776156090619,4.79594377541159,129.714357697574));
#47478=CARTESIAN_POINT('Ctrl Pts',(95.5698412749428,4.76570872233749,129.581325380018));
#47479=CARTESIAN_POINT('Ctrl Pts',(95.5620669408237,4.72988640757497,129.449341315004));
#47480=CARTESIAN_POINT('Ctrl Pts',(95.5542926067046,4.68856296692414,129.318911066862));
#47481=CARTESIAN_POINT('Ctrl Pts',(95.5465278537575,4.64729045372073,129.188641562343));
#47482=CARTESIAN_POINT('Ctrl Pts',(95.5387631008105,4.60053042105274,129.059922433664));
#47483=CARTESIAN_POINT('Ctrl Pts',(95.5309983478634,4.54841996766372,128.933248953272));
#47484=CARTESIAN_POINT('Ctrl Pts',(95.5232413069784,4.49636127111167,128.806701286766));
#47485=CARTESIAN_POINT('Ctrl Pts',(95.5154842660934,4.43896287694115,128.682195584467));
#47486=CARTESIAN_POINT('Ctrl Pts',(95.5077272252084,4.37641152248942,128.560211503019));
#47487=CARTESIAN_POINT('Ctrl Pts',(95.4999760339683,4.31390733850062,128.438319410716));
#47488=CARTESIAN_POINT('Ctrl Pts',(95.4922248427281,4.24625810652563,128.318945500782));
#47489=CARTESIAN_POINT('Ctrl Pts',(95.484473651488,4.17369831367707,128.202548662618));
#47490=CARTESIAN_POINT('Ctrl Pts',(95.4767257547109,4.10116936067607,128.086201296216));
#47491=CARTESIAN_POINT('Ctrl Pts',(95.4689778579339,4.02373420431497,127.972828816012));
#47492=CARTESIAN_POINT('Ctrl Pts',(95.4612299611568,3.94167272792981,127.86286454101));
#47493=CARTESIAN_POINT('Ctrl Pts',(95.4534836850727,3.85962841703646,127.752923268163));
#47494=CARTESIAN_POINT('Ctrl Pts',(95.4457374089886,3.7729599446594,127.64638909561));
#47495=CARTESIAN_POINT('Ctrl Pts',(95.4379911329045,3.68198964872925,127.543665095265));
#47496=CARTESIAN_POINT('Ctrl Pts',(95.4302447996391,3.59101868127703,127.440940336636));
#47497=CARTESIAN_POINT('Ctrl Pts',(95.4224984663738,3.49574608610839,127.342026099029));
#47498=CARTESIAN_POINT('Ctrl Pts',(95.4147521331084,3.39653322271067,127.247290878367));
#47499=CARTESIAN_POINT('Ctrl Pts',(95.4070040651054,3.29729814128009,127.15253444241));
#47500=CARTESIAN_POINT('Ctrl Pts',(95.3992559971025,3.19412131846217,127.061959155604));
#47501=CARTESIAN_POINT('Ctrl Pts',(95.3915079290995,3.08739925162051,126.975895008005));
#47502=CARTESIAN_POINT('Ctrl Pts',(95.3837516263577,2.9805637592962,126.889739390406));
#47503=CARTESIAN_POINT('Ctrl Pts',(95.3759953236158,2.87017580092754,126.808104735347));
#47504=CARTESIAN_POINT('Ctrl Pts',(95.3682390208739,2.75666353074768,126.731279567458));
#47505=CARTESIAN_POINT('Ctrl Pts',(95.3604785783598,2.64309067565135,126.654413395665));
#47506=CARTESIAN_POINT('Ctrl Pts',(95.3527181358456,2.52639051853612,126.582362031234));
#47507=CARTESIAN_POINT('Ctrl Pts',(95.3449576933314,2.40701731659418,126.515368812944));
#47508=CARTESIAN_POINT('Ctrl Pts',(95.337184793066,2.28745248619112,126.448268051192));
#47509=CARTESIAN_POINT('Ctrl Pts',(95.3294118928006,2.1652063850125,126.386241838504));
#47510=CARTESIAN_POINT('Ctrl Pts',(95.3216389925351,2.04075563133009,126.329486371769));
#47511=CARTESIAN_POINT('Ctrl Pts',(95.3141486567731,1.92082897601657,126.274794109209));
#47512=CARTESIAN_POINT('Ctrl Pts',(95.3066583210111,1.7988554598522,126.224996152327));
#47513=CARTESIAN_POINT('Ctrl Pts',(95.2991679852491,1.67527443097365,126.180224088069));
#47514=CARTESIAN_POINT('Ctrl Pts',(95.29139365113,1.54700778982344,126.133754477387));
#47515=CARTESIAN_POINT('Ctrl Pts',(95.2836193170109,1.41660302180681,126.092552194308));
#47516=CARTESIAN_POINT('Ctrl Pts',(95.2758449828918,1.28453203101504,126.056818040211));
#47517=CARTESIAN_POINT('Ctrl Pts',(95.2680802299447,1.15262380591599,126.021127925266));
#47518=CARTESIAN_POINT('Ctrl Pts',(95.2603154769976,1.0190538176086,125.990892631872));
#47519=CARTESIAN_POINT('Ctrl Pts',(95.2525507240505,0.884312858049897,125.966264521829));
#47520=CARTESIAN_POINT('Ctrl Pts',(95.2447936831655,0.749705725111924,125.941660872772));
#47521=CARTESIAN_POINT('Ctrl Pts',(95.2370366422805,0.613930317500038,125.922653394081));
#47522=CARTESIAN_POINT('Ctrl Pts',(95.2292796013955,0.477491120026485,125.909344244478));
#47523=CARTESIAN_POINT('Ctrl Pts',(95.2215284101554,0.341154812412719,125.896045131409));
#47524=CARTESIAN_POINT('Ctrl Pts',(95.2137772189152,0.204156098833551,125.888435832006));
#47525=CARTESIAN_POINT('Ctrl Pts',(95.2060260276751,0.0670078019502721,
125.886567106551));
#47526=CARTESIAN_POINT('Ctrl Pts',(95.198278130898,-0.0700822032480007,
125.884699175355));
#47527=CARTESIAN_POINT('Ctrl Pts',(95.1905302341209,-0.207321275190314,
125.888566970652));
#47528=CARTESIAN_POINT('Ctrl Pts',(95.1827823373439,-0.344193566549059,
125.898169238171));
#47529=CARTESIAN_POINT('Ctrl Pts',(95.1750360612598,-0.48103722717517,125.907769497103));
#47530=CARTESIAN_POINT('Ctrl Pts',(95.1672897851757,-0.617513870063609,
125.923101814986));
#47531=CARTESIAN_POINT('Ctrl Pts',(95.1595435090915,-0.753110147871704,
125.944112870005));
#47532=CARTESIAN_POINT('Ctrl Pts',(95.1517971758262,-0.888707426620626,
125.965124080123));
#47533=CARTESIAN_POINT('Ctrl Pts',(95.1440508425608,-1.02342394096716,125.991814051157));
#47534=CARTESIAN_POINT('Ctrl Pts',(95.1363045092955,-1.15675434122567,126.024077942184));
#47535=CARTESIAN_POINT('Ctrl Pts',(95.1285564412925,-1.29011459990268,126.056349058486));
#47536=CARTESIAN_POINT('Ctrl Pts',(95.1208083732895,-1.42208774688537,126.094196486698));
#47537=CARTESIAN_POINT('Ctrl Pts',(95.1130603052866,-1.55218183568265,126.137465010047));
#47538=CARTESIAN_POINT('Ctrl Pts',(95.1053040025447,-1.68241419002592,126.180779519698));
#47539=CARTESIAN_POINT('Ctrl Pts',(95.0975476998029,-1.81076312521467,126.229526510326));
#47540=CARTESIAN_POINT('Ctrl Pts',(95.089791397061,-1.9367544694845,126.28350171826));
#47541=CARTESIAN_POINT('Ctrl Pts',(95.0820309545469,-2.06281305912837,126.337505734388));
#47542=CARTESIAN_POINT('Ctrl Pts',(95.0742705120327,-2.18651119810527,126.396743359262));
#47543=CARTESIAN_POINT('Ctrl Pts',(95.0665100695185,-2.30739862150147,126.460963943994));
#47544=CARTESIAN_POINT('Ctrl Pts',(95.058737169253,-2.4284801041215,126.525287621311));
#47545=CARTESIAN_POINT('Ctrl Pts',(95.0509642689876,-2.54674151724374,126.594610045389));
#47546=CARTESIAN_POINT('Ctrl Pts',(95.0431913687222,-2.66176017105028,126.668636272991));
#47547=CARTESIAN_POINT('Ctrl Pts',(95.0357010329602,-2.77259760707675,126.739971460759));
#47548=CARTESIAN_POINT('Ctrl Pts',(95.0282106971981,-2.88042370340878,126.8156742223));
#47549=CARTESIAN_POINT('Ctrl Pts',(95.020720361436,-2.98489027382289,126.895446047543));
#47550=CARTESIAN_POINT('Ctrl Pts',(95.0129820677061,-3.09281507619549,126.977858616847));
#47551=CARTESIAN_POINT('Ctrl Pts',(95.0052437739762,-3.19751468618271,127.064889917331));
#47552=CARTESIAN_POINT('Ctrl Pts',(94.9975054802462,-3.29856204254205,127.156255422537));
#47553=CARTESIAN_POINT('Ctrl Pts',(94.9898273074911,-3.39882433364356,127.246911083502));
#47554=CARTESIAN_POINT('Ctrl Pts',(94.9821491347359,-3.49549059162687,127.341833600504));
#47555=CARTESIAN_POINT('Ctrl Pts',(94.9744709619808,-3.58817228842645,127.440701495261));
#47556=CARTESIAN_POINT('Ctrl Pts',(94.966799791251,-3.68076946516975,127.539479228525));
#47557=CARTESIAN_POINT('Ctrl Pts',(94.9591286205212,-3.76938903420821,127.642194895289));
#47558=CARTESIAN_POINT('Ctrl Pts',(94.9514574497914,-3.85367693199277,127.748488047198));
#47559=CARTESIAN_POINT('Ctrl Pts',(94.943791524058,-3.93790719975773,127.854708523474));
#47560=CARTESIAN_POINT('Ctrl Pts',(94.9361255983246,-4.01781143930909,127.964501307338));
#47561=CARTESIAN_POINT('Ctrl Pts',(94.9284596725912,-4.09307410386974,128.077470916326));
#47562=CARTESIAN_POINT('Ctrl Pts',(94.9206714758684,-4.16953720276554,128.192242382824));
#47563=CARTESIAN_POINT('Ctrl Pts',(94.9128832791456,-4.24120910544823,128.310292574397));
#47564=CARTESIAN_POINT('Ctrl Pts',(94.9050950824228,-4.30780306291853,128.431173765755));
#47565=CARTESIAN_POINT('Ctrl Pts',(94.8974332980193,-4.37331611592385,128.550092901929));
#47566=CARTESIAN_POINT('Ctrl Pts',(94.8897715136158,-4.43391464534115,128.671751456445));
#47567=CARTESIAN_POINT('Ctrl Pts',(94.8821097292122,-4.48937106750423,128.795696762971));
#47568=CARTESIAN_POINT('Ctrl Pts',(94.8742583263298,-4.54619995877645,128.92270954298));
#47569=CARTESIAN_POINT('Ctrl Pts',(94.8664069234474,-4.59762869126989,129.052123353862));
#47570=CARTESIAN_POINT('Ctrl Pts',(94.858555520565,-4.64346444194557,129.183428466337));
#47571=CARTESIAN_POINT('Ctrl Pts',(94.8507041176826,-4.68930019262124,129.314733578813));
#47572=CARTESIAN_POINT('Ctrl Pts',(94.8428527148001,-4.7295428368851,129.447929558527));
#47573=CARTESIAN_POINT('Ctrl Pts',(94.8350013119177,-4.76405452823406,129.582490119308));
#47574=CARTESIAN_POINT('Ctrl Pts',(96.5847048906856,-4.76405452823403,129.582490119308));
#47575=CARTESIAN_POINT('Ctrl Pts',(96.5769147324208,-4.79833529931696,129.716150325477));
#47576=CARTESIAN_POINT('Ctrl Pts',(96.569124574156,-4.82700348682742,129.851318908786));
#47577=CARTESIAN_POINT('Ctrl Pts',(96.5613344158913,-4.84993841038099,129.98748824197));
#47578=CARTESIAN_POINT('Ctrl Pts',(96.553544867975,-4.87287153701372,130.123646906468));
#47579=CARTESIAN_POINT('Ctrl Pts',(96.5457553200588,-4.89007222053425,130.260805787351));
#47580=CARTESIAN_POINT('Ctrl Pts',(96.5379657721426,-4.90147094549081,130.398447285672));
#47581=CARTESIAN_POINT('Ctrl Pts',(96.530263660092,-4.9127417224079,130.534543790151));
#47582=CARTESIAN_POINT('Ctrl Pts',(96.5225615480415,-4.91834012405208,130.671111761788));
#47583=CARTESIAN_POINT('Ctrl Pts',(96.514859435991,-4.9182489022828,130.80764660205));
#47584=CARTESIAN_POINT('',(96.8601405640579,-4.91824839088665,130.800382170524));
#47585=CARTESIAN_POINT('Ctrl Pts',(96.929952524335,-4.76405452823407,129.582490119308));
#47586=CARTESIAN_POINT('Ctrl Pts',(96.9207574310496,-4.80419149538206,129.738983545055));
#47587=CARTESIAN_POINT('Ctrl Pts',(96.9115623377642,-4.83665391359241,129.897613593837));
#47588=CARTESIAN_POINT('Ctrl Pts',(96.9023672444788,-4.86124082596128,130.057687533474));
#47589=CARTESIAN_POINT('Ctrl Pts',(96.8932607227116,-4.88559090547952,130.216219564682));
#47590=CARTESIAN_POINT('Ctrl Pts',(96.8841542009443,-4.90221640676791,130.376167729082));
#47591=CARTESIAN_POINT('Ctrl Pts',(96.8750476791771,-4.91096885746551,130.536838761442));
#47592=CARTESIAN_POINT('Ctrl Pts',(96.870078640804,-4.91574469444108,130.624510053034));
#47593=CARTESIAN_POINT('Ctrl Pts',(96.865109602431,-4.91817721769542,130.712396222853));
#47594=CARTESIAN_POINT('Ctrl Pts',(96.8601405640579,-4.91824839088665,130.800382170524));
#47595=CARTESIAN_POINT('Ctrl Pts',(96.8601405640084,-4.91824839088736,130.8003821714));
#47596=CARTESIAN_POINT('Ctrl Pts',(96.8522937533478,-4.91836078334458,130.939324361083));
#47597=CARTESIAN_POINT('Ctrl Pts',(96.8444469426872,-4.91258087579584,131.078346812634));
#47598=CARTESIAN_POINT('Ctrl Pts',(96.8366001320266,-4.90091673110298,131.216911532357));
#47599=CARTESIAN_POINT('Ctrl Pts',(96.8288723439396,-4.88942951135199,131.353374464453));
#47600=CARTESIAN_POINT('Ctrl Pts',(96.8211445558527,-4.87223536073034,131.489393051659));
#47601=CARTESIAN_POINT('Ctrl Pts',(96.8134167677656,-4.84939441297877,131.624456276541));
#47602=CARTESIAN_POINT('Ctrl Pts',(96.805688903088,-4.82655323884909,131.759520840045));
#47603=CARTESIAN_POINT('Ctrl Pts',(96.7979610384104,-4.79806522128852,131.893629635197));
#47604=CARTESIAN_POINT('Ctrl Pts',(96.7902331737327,-4.76404190096828,132.026280348284));
#47605=CARTESIAN_POINT('Ctrl Pts',(96.7825035423692,-4.73001080249401,132.158961386974));
#47606=CARTESIAN_POINT('Ctrl Pts',(96.7747739110056,-4.6904419807485,132.290183300077));
#47607=CARTESIAN_POINT('Ctrl Pts',(96.7670442796421,-4.64549716040654,132.419457888678));
#47608=CARTESIAN_POINT('Ctrl Pts',(96.7591086820181,-4.59935472582714,132.552177169831));
#47609=CARTESIAN_POINT('Ctrl Pts',(96.7511730843941,-4.54754591949674,132.682843477103));
#47610=CARTESIAN_POINT('Ctrl Pts',(96.7432374867701,-4.49029844563479,132.810950493856));
#47611=CARTESIAN_POINT('Ctrl Pts',(96.7354949775542,-4.43444391331513,132.93594041961));
#47612=CARTESIAN_POINT('Ctrl Pts',(96.7277524683382,-4.37341256186794,133.058493840385));
#47613=CARTESIAN_POINT('Ctrl Pts',(96.7200099591223,-4.30746209298632,133.178166292002));
#47614=CARTESIAN_POINT('Ctrl Pts',(96.7119778172943,-4.23904454191752,133.302315463477));
#47615=CARTESIAN_POINT('Ctrl Pts',(96.7039456754663,-4.16533294617827,133.423363531095));
#47616=CARTESIAN_POINT('Ctrl Pts',(96.6959135336382,-4.08666308125691,133.540848863985));
#47617=CARTESIAN_POINT('Ctrl Pts',(96.6878813918102,-4.00799321633556,133.658334196876));
#47618=CARTESIAN_POINT('Ctrl Pts',(96.6798492499822,-3.92436541508682,133.772256464385));
#47619=CARTESIAN_POINT('Ctrl Pts',(96.6718171081542,-3.83615976287862,133.882194488354));
#47620=CARTESIAN_POINT('Ctrl Pts',(96.6640427740351,-3.75078524806782,133.988603830847));
#47621=CARTESIAN_POINT('Ctrl Pts',(96.656268439916,-3.66084469644549,134.091626783757));
#47622=CARTESIAN_POINT('Ctrl Pts',(96.6484941057969,-3.56663668836502,134.190846376536));
#47623=CARTESIAN_POINT('Ctrl Pts',(96.6407293528498,-3.47254478323504,134.289943690035));
#47624=CARTESIAN_POINT('Ctrl Pts',(96.6329645999027,-3.37419615262093,134.385246688935));
#47625=CARTESIAN_POINT('Ctrl Pts',(96.6251998469557,-3.27193070545506,134.476369947783));
#47626=CARTESIAN_POINT('Ctrl Pts',(96.6174428060707,-3.16976682977294,134.567402701726));
#47627=CARTESIAN_POINT('Ctrl Pts',(96.6096857651856,-3.06369416929632,134.654263718631));
#47628=CARTESIAN_POINT('Ctrl Pts',(96.6019287243006,-2.95409044203545,134.736603326603));
#47629=CARTESIAN_POINT('Ctrl Pts',(96.5941775330605,-2.84456936779828,134.818880841636));
#47630=CARTESIAN_POINT('Ctrl Pts',(96.5864263418204,-2.73152283824858,134.896643500518));
#47631=CARTESIAN_POINT('Ctrl Pts',(96.5786751505803,-2.6153624287966,134.969581191382));
#47632=CARTESIAN_POINT('Ctrl Pts',(96.5709272538032,-2.49925139061693,135.042487881782));
#47633=CARTESIAN_POINT('Ctrl Pts',(96.5631793570262,-2.38002943525141,135.110573475463));
#47634=CARTESIAN_POINT('Ctrl Pts',(96.5554314602491,-2.25813777823766,135.173570710591));
#47635=CARTESIAN_POINT('Ctrl Pts',(96.547685184165,-2.13627161833095,135.236554768056));
#47636=CARTESIAN_POINT('Ctrl Pts',(96.5399389080808,-2.01173721465227,135.294452404676));
#47637=CARTESIAN_POINT('Ctrl Pts',(96.5321926319967,-1.88500073206192,135.347042127712));
#47638=CARTESIAN_POINT('Ctrl Pts',(96.5244462987314,-1.75826331393148,135.399632238954));
#47639=CARTESIAN_POINT('Ctrl Pts',(96.516699965466,-1.62932414556343,135.446914208585));
#47640=CARTESIAN_POINT('Ctrl Pts',(96.5089536322007,-1.4986693605315,135.488714704343));
#47641=CARTESIAN_POINT('Ctrl Pts',(96.5012055641977,-1.36798531626644,135.530524561032));
#47642=CARTESIAN_POINT('Ctrl Pts',(96.4934574961947,-1.235585263124,135.56685038208));
#47643=CARTESIAN_POINT('Ctrl Pts',(96.4857094281917,-1.10197009205432,135.597568831145));
#47644=CARTESIAN_POINT('Ctrl Pts',(96.4779531254499,-0.968212913190873,
135.628319928142));
#47645=CARTESIAN_POINT('Ctrl Pts',(96.470196822708,-0.833238418238962,135.653451660511));
#47646=CARTESIAN_POINT('Ctrl Pts',(96.4624405199662,-0.697557830692655,
135.672891826806));
#47647=CARTESIAN_POINT('Ctrl Pts',(96.454680077452,-0.561804826331418,135.692342368902));
#47648=CARTESIAN_POINT('Ctrl Pts',(96.4469196349378,-0.425345367248886,
135.706095252743));
#47649=CARTESIAN_POINT('Ctrl Pts',(96.4391591924236,-0.288694387747627,
135.714130328355));
#47650=CARTESIAN_POINT('Ctrl Pts',(96.4313862921582,-0.151824043962769,
135.722178302584));
#47651=CARTESIAN_POINT('Ctrl Pts',(96.4236133918928,-0.014761956519537,
135.724490119951));
#47652=CARTESIAN_POINT('Ctrl Pts',(96.4158404916273,0.121977449986141,135.72109780438));
#47653=CARTESIAN_POINT('Ctrl Pts',(96.4083501558653,0.253746034639001,135.717828808024));
#47654=CARTESIAN_POINT('Ctrl Pts',(96.4008598201033,0.385214684207991,135.709263217823));
#47655=CARTESIAN_POINT('Ctrl Pts',(96.3933694843413,0.515930749031297,135.695474859199));
#47656=CARTESIAN_POINT('Ctrl Pts',(96.3855951502222,0.651602953183148,135.681163710767));
#47657=CARTESIAN_POINT('Ctrl Pts',(96.3778208161031,0.786894146299921,135.661180599962));
#47658=CARTESIAN_POINT('Ctrl Pts',(96.370046481984,0.921292129275798,135.635551348125));
#47659=CARTESIAN_POINT('Ctrl Pts',(96.362281729037,1.05552447874915,135.60995368205));
#47660=CARTESIAN_POINT('Ctrl Pts',(96.3545169760899,1.18886542799099,135.578723792547));
#47661=CARTESIAN_POINT('Ctrl Pts',(96.3467522231428,1.32080697857008,135.541939322755));
#47662=CARTESIAN_POINT('Ctrl Pts',(96.3389951822578,1.45261748294063,135.505191387817));
#47663=CARTESIAN_POINT('Ctrl Pts',(96.3312381413729,1.58303098045092,135.46289995576));
#47664=CARTESIAN_POINT('Ctrl Pts',(96.3234811004879,1.71154911642052,135.415193805243));
#47665=CARTESIAN_POINT('Ctrl Pts',(96.3157299092478,1.83997033586431,135.367523630304));
#47666=CARTESIAN_POINT('Ctrl Pts',(96.3079787180076,1.96649867367134,135.314446999934));
#47667=CARTESIAN_POINT('Ctrl Pts',(96.3002275267675,2.09065075738291,135.256142561143));
#47668=CARTESIAN_POINT('Ctrl Pts',(96.2924796299904,2.21475007314721,135.197862903293));
#47669=CARTESIAN_POINT('Ctrl Pts',(96.2847317332133,2.33647479042863,135.13436002217));
#47670=CARTESIAN_POINT('Ctrl Pts',(96.2769838364362,2.45536156650153,135.065860663354));
#47671=CARTESIAN_POINT('Ctrl Pts',(96.2692375603521,2.57422347402385,134.997375633126));
#47672=CARTESIAN_POINT('Ctrl Pts',(96.261491284268,2.69024828256869,134.923896399135));
#47673=CARTESIAN_POINT('Ctrl Pts',(96.2537450081839,2.80299767052856,134.845695436844));
#47674=CARTESIAN_POINT('Ctrl Pts',(96.2459986749186,2.91574789077865,134.767493897292));
#47675=CARTESIAN_POINT('Ctrl Pts',(96.2382523416532,3.0252223209407,134.684570782709));
#47676=CARTESIAN_POINT('Ctrl Pts',(96.2305060083879,3.13101236460376,134.597241400717));
#47677=CARTESIAN_POINT('Ctrl Pts',(96.2227579403849,3.23682609921375,134.509892461916));
#47678=CARTESIAN_POINT('Ctrl Pts',(96.2150098723819,3.33895350403678,134.418135541027));
#47679=CARTESIAN_POINT('Ctrl Pts',(96.2072618043789,3.43702006892149,134.322325385487));
#47680=CARTESIAN_POINT('Ctrl Pts',(96.1995055016371,3.5351908601183,134.226413401773));
#47681=CARTESIAN_POINT('Ctrl Pts',(96.1917491988953,3.62929190978506,134.126439851716));
#47682=CARTESIAN_POINT('Ctrl Pts',(96.1839928961534,3.71898614401388,134.022795815474));
#47683=CARTESIAN_POINT('Ctrl Pts',(96.1762324536392,3.80872825075628,133.919096461289));
#47684=CARTESIAN_POINT('Ctrl Pts',(96.168472011125,3.89405861227602,133.811723023279));
#47685=CARTESIAN_POINT('Ctrl Pts',(96.1607115686109,3.97468194125959,133.701097838704));
#47686=CARTESIAN_POINT('Ctrl Pts',(96.1529386683454,4.05543469396812,133.590295068761));
#47687=CARTESIAN_POINT('Ctrl Pts',(96.14516576808,4.13146509758381,133.476230446552));
#47688=CARTESIAN_POINT('Ctrl Pts',(96.1373928678146,4.20252203568043,133.359354081769));
#47689=CARTESIAN_POINT('Ctrl Pts',(96.1299025320525,4.27099587509585,133.24672646724));
#47690=CARTESIAN_POINT('Ctrl Pts',(96.1224121962905,4.33485141786226,133.131488258241));
#47691=CARTESIAN_POINT('Ctrl Pts',(96.1149218605284,4.39390610720005,133.014060186197));
#47692=CARTESIAN_POINT('Ctrl Pts',(96.1071475264093,4.45519987303315,132.892179793111));
#47693=CARTESIAN_POINT('Ctrl Pts',(96.0993731922903,4.51151571051237,132.767554121192));
#47694=CARTESIAN_POINT('Ctrl Pts',(96.0915988581712,4.56259848773544,132.640628055118));
#47695=CARTESIAN_POINT('Ctrl Pts',(96.0838341052241,4.61361831000094,132.513858414078));
#47696=CARTESIAN_POINT('Ctrl Pts',(96.076069352277,4.65941775958474,132.38479437896));
#47697=CARTESIAN_POINT('Ctrl Pts',(96.0683045993299,4.69978757429792,132.253905311246));
#47698=CARTESIAN_POINT('Ctrl Pts',(96.060547558445,4.74011729314194,132.123146244399));
#47699=CARTESIAN_POINT('Ctrl Pts',(96.05279051756,4.77502799452796,131.990566123389));
#47700=CARTESIAN_POINT('Ctrl Pts',(96.045033476675,4.80435865071069,131.856653836133));
#47701=CARTESIAN_POINT('Ctrl Pts',(96.0372822854349,4.83366718841754,131.722842533173));
#47702=CARTESIAN_POINT('Ctrl Pts',(96.0295310941947,4.85740397329008,131.587701443924));
#47703=CARTESIAN_POINT('Ctrl Pts',(96.0217799029546,4.87545803149665,131.451733806395));
#47704=CARTESIAN_POINT('Ctrl Pts',(96.0140320061775,4.89350441624688,131.31582395874));
#47705=CARTESIAN_POINT('Ctrl Pts',(96.0062841094004,4.90587282684568,131.179088648277));
#47706=CARTESIAN_POINT('Ctrl Pts',(95.9985362126233,4.91250358270869,131.042040259888));
#47707=CARTESIAN_POINT('Ctrl Pts',(95.9907899365392,4.91913295156051,130.905020539067));
#47708=CARTESIAN_POINT('Ctrl Pts',(95.9830436604551,4.92002703404573,130.767688260843));
#47709=CARTESIAN_POINT('Ctrl Pts',(95.975297384371,4.91517814795374,130.630559477242));
#47710=CARTESIAN_POINT('Ctrl Pts',(95.9675510511057,4.91032922606837,130.493429681386));
#47711=CARTESIAN_POINT('Ctrl Pts',(95.9598047178404,4.89973726482899,130.356503773872));
#47712=CARTESIAN_POINT('Ctrl Pts',(95.952058384575,4.88344668512806,130.220295949903));
#47713=CARTESIAN_POINT('Ctrl Pts',(95.9443103165721,4.86715245726478,130.084057623137));
#47714=CARTESIAN_POINT('Ctrl Pts',(95.9365622485691,4.8451571179372,129.948538088034));
#47715=CARTESIAN_POINT('Ctrl Pts',(95.9288141805661,4.81755669432605,129.814244180244));
#47716=CARTESIAN_POINT('Ctrl Pts',(95.9210578778243,4.78992693665619,129.679807543292));
#47717=CARTESIAN_POINT('Ctrl Pts',(95.9133015750825,4.75668027348595,129.546599519332));
#47718=CARTESIAN_POINT('Ctrl Pts',(95.9055452723406,4.71796353494803,129.415115086567));
#47719=CARTESIAN_POINT('Ctrl Pts',(95.8977848298264,4.6792261321209,129.283560476601));
#47720=CARTESIAN_POINT('Ctrl Pts',(95.8900243873122,4.63501296246106,129.153731660787));
#47721=CARTESIAN_POINT('Ctrl Pts',(95.8822639447981,4.58551974025954,129.026105356308));
#47722=CARTESIAN_POINT('Ctrl Pts',(95.8744910445326,4.53594706714405,128.898274174756));
#47723=CARTESIAN_POINT('Ctrl Pts',(95.8667181442672,4.48107756030123,128.772652928414));
#47724=CARTESIAN_POINT('Ctrl Pts',(95.8589452440018,4.42115417520255,128.649696183927));
#47725=CARTESIAN_POINT('Ctrl Pts',(95.8514549082397,4.36340915608987,128.531209226811));
#47726=CARTESIAN_POINT('Ctrl Pts',(95.8439645724777,4.30097146776716,128.415196683385));
#47727=CARTESIAN_POINT('Ctrl Pts',(95.8364742367156,4.23409640709906,128.30203955945));
#47728=CARTESIAN_POINT('Ctrl Pts',(95.8286999025965,4.16468575817969,128.184592048768));
#47729=CARTESIAN_POINT('Ctrl Pts',(95.8209255684774,4.09027473655954,128.069848719925));
#47730=CARTESIAN_POINT('Ctrl Pts',(95.8131512343583,4.01109973129416,127.958264693653));
#47731=CARTESIAN_POINT('Ctrl Pts',(95.8053864814112,3.93202230214679,127.846818184722));
#47732=CARTESIAN_POINT('Ctrl Pts',(95.7976217284642,3.84819279533263,127.738523547134));
#47733=CARTESIAN_POINT('Ctrl Pts',(95.7898569755171,3.75989298663368,127.63381054044));
#47734=CARTESIAN_POINT('Ctrl Pts',(95.782099934632,3.67168087854936,127.529201536181));
#47735=CARTESIAN_POINT('Ctrl Pts',(95.774342893747,3.57900755471945,127.428167380526));
#47736=CARTESIAN_POINT('Ctrl Pts',(95.766585852862,3.48219729096509,127.331107806541));
#47737=CARTESIAN_POINT('Ctrl Pts',(95.7588346616219,3.3854600325841,127.234121425935));
#47738=CARTESIAN_POINT('Ctrl Pts',(95.7510834703818,3.28459231883076,127.141103936817));
#47739=CARTESIAN_POINT('Ctrl Pts',(95.7433322791417,3.17995755403037,127.052420717053));
#47740=CARTESIAN_POINT('Ctrl Pts',(95.7355843823646,3.07536726179589,126.963775190022));
#47741=CARTESIAN_POINT('Ctrl Pts',(95.7278364855875,2.96701340060214,126.879460520642));
#47742=CARTESIAN_POINT('Ctrl Pts',(95.7200885888104,2.8552947955475,126.799803876425));
#47743=CARTESIAN_POINT('Ctrl Pts',(95.7123423127263,2.7435995596166,126.72016389466));
#47744=CARTESIAN_POINT('Ctrl Pts',(95.7045960366422,2.62854129791653,126.645180226836));
#47745=CARTESIAN_POINT('Ctrl Pts',(95.6968497605581,2.51055002720985,126.575138274939));
#47746=CARTESIAN_POINT('Ctrl Pts',(95.6891034272928,2.39255788551865,126.505095806008));
#47747=CARTESIAN_POINT('Ctrl Pts',(95.6813570940274,2.27163302781073,126.439995325366));
#47748=CARTESIAN_POINT('Ctrl Pts',(95.6736107607621,2.14823207165186,126.380077395526));
#47749=CARTESIAN_POINT('Ctrl Pts',(95.6658626927591,2.02480348070446,126.32014604748));
#47750=CARTESIAN_POINT('Ctrl Pts',(95.6581146247561,1.8988980395363,126.265399730425));
#47751=CARTESIAN_POINT('Ctrl Pts',(95.6503665567531,1.7709940683723,126.216031611022));
#47752=CARTESIAN_POINT('Ctrl Pts',(95.6426102540113,1.64295415934549,126.166611022595));
#47753=CARTESIAN_POINT('Ctrl Pts',(95.6348539512694,1.51291184260174,126.122580191177));
#47754=CARTESIAN_POINT('Ctrl Pts',(95.6270976485276,1.38136292259538,126.084083132229));
#47755=CARTESIAN_POINT('Ctrl Pts',(95.6193372060134,1.24974379096955,126.045565526242));
#47756=CARTESIAN_POINT('Ctrl Pts',(95.6115767634992,1.11661683311413,126.012587671866));
#47757=CARTESIAN_POINT('Ctrl Pts',(95.603816320985,0.982488913052441,125.985242586408));
#47758=CARTESIAN_POINT('Ctrl Pts',(95.5960434207196,0.848145678946153,125.957853604192));
#47759=CARTESIAN_POINT('Ctrl Pts',(95.5882705204542,0.712798657908766,125.936115522167));
#47760=CARTESIAN_POINT('Ctrl Pts',(95.5804976201887,0.576961613100181,125.920069639388));
#47761=CARTESIAN_POINT('Ctrl Pts',(95.5730072844267,0.446062587022976,125.904607064866));
#47762=CARTESIAN_POINT('Ctrl Pts',(95.5655169486646,0.314708852929088,125.894430046893));
#47763=CARTESIAN_POINT('Ctrl Pts',(95.5580266129026,0.183358955980787,125.88952973993));
#47764=CARTESIAN_POINT('Ctrl Pts',(95.5502522787835,0.0470288877670453,
125.884443636339));
#47765=CARTESIAN_POINT('Ctrl Pts',(95.5424779446644,-0.0897288992641427,
125.885026164257));
#47766=CARTESIAN_POINT('Ctrl Pts',(95.5347036105453,-0.226403725093196,
125.891324446748));
#47767=CARTESIAN_POINT('Ctrl Pts',(95.5269388575982,-0.362910111414581,
125.897614967169));
#47768=CARTESIAN_POINT('Ctrl Pts',(95.5191741046511,-0.499333353163979,
125.909607208567));
#47769=CARTESIAN_POINT('Ctrl Pts',(95.511409351704,-0.635159574766587,125.927296400531));
#47770=CARTESIAN_POINT('Ctrl Pts',(95.5036523108189,-0.77085089185127,125.94496802334));
#47771=CARTESIAN_POINT('Ctrl Pts',(95.4958952699339,-0.90594598364137,125.968325286296));
#47772=CARTESIAN_POINT('Ctrl Pts',(95.4881382290489,-1.03993326438723,125.99731143245));
#47773=CARTESIAN_POINT('Ctrl Pts',(95.4803870378088,-1.17381950428168,126.026275719927));
#47774=CARTESIAN_POINT('Ctrl Pts',(95.4726358465687,-1.30659921538332,126.060860359283));
#47775=CARTESIAN_POINT('Ctrl Pts',(95.4648846553285,-1.43776856603156,126.100957103829));
#47776=CARTESIAN_POINT('Ctrl Pts',(95.4571367585514,-1.56888216620698,126.14103680619));
#47777=CARTESIAN_POINT('Ctrl Pts',(95.4493888617744,-1.69838639413649,126.186623840053));
#47778=CARTESIAN_POINT('Ctrl Pts',(95.4416409649973,-1.82579041982071,126.2375595046));
#47779=CARTESIAN_POINT('Ctrl Pts',(95.4338946889132,-1.95316779532917,126.288484514503));
#47780=CARTESIAN_POINT('Ctrl Pts',(95.4261484128291,-2.07844547962043,126.344755784654));
#47781=CARTESIAN_POINT('Ctrl Pts',(95.418402136745,-2.20115092135606,126.406165796516));
#47782=CARTESIAN_POINT('Ctrl Pts',(95.4106558034796,-2.32385726887573,126.467576261693));
#47783=CARTESIAN_POINT('Ctrl Pts',(95.4029094702142,-2.44399098632657,126.534125369298));
#47784=CARTESIAN_POINT('Ctrl Pts',(95.3951631369488,-2.56110286870544,126.605558983956));
#47785=CARTESIAN_POINT('Ctrl Pts',(95.3874150689459,-2.67824097747775,126.677008595676));
#47786=CARTESIAN_POINT('Ctrl Pts',(95.3796670009429,-2.79235557087524,126.753344687536));
#47787=CARTESIAN_POINT('Ctrl Pts',(95.37191893294,-2.90302558854828,126.834269246485));
#47788=CARTESIAN_POINT('Ctrl Pts',(95.3641626301981,-3.01381322763347,126.915279813018));
#47789=CARTESIAN_POINT('Ctrl Pts',(95.3564063274562,-3.12114866178335,127.00088835719));
#47790=CARTESIAN_POINT('Ctrl Pts',(95.3486500247144,-3.22464273229404,127.090755588546));
#47791=CARTESIAN_POINT('Ctrl Pts',(95.3408895822002,-3.32819204070653,127.180670784749));
#47792=CARTESIAN_POINT('Ctrl Pts',(95.333129139686,-3.42789561610189,127.274848928926));
#47793=CARTESIAN_POINT('Ctrl Pts',(95.3253686971718,-3.52340122800027,127.372913860143));
#47794=CARTESIAN_POINT('Ctrl Pts',(95.3175957969064,-3.61906015398533,127.471136213894));
#47795=CARTESIAN_POINT('Ctrl Pts',(95.309822896641,-3.71050738895328,127.573257531603));
#47796=CARTESIAN_POINT('Ctrl Pts',(95.3020499963755,-3.79743048530101,127.678867892921));
#47797=CARTESIAN_POINT('Ctrl Pts',(95.2945596606136,-3.88119370814933,127.780639051588));
#47798=CARTESIAN_POINT('Ctrl Pts',(95.2870693248516,-3.96075582336749,127.885649741409));
#47799=CARTESIAN_POINT('Ctrl Pts',(95.2795789890897,-4.03587641809858,127.993509394122));
#47800=CARTESIAN_POINT('Ctrl Pts',(95.2717050370586,-4.11484430128238,128.106893060561));
#47801=CARTESIAN_POINT('Ctrl Pts',(95.2638310850276,-4.1891508090201,128.223779619484));
#47802=CARTESIAN_POINT('Ctrl Pts',(95.2559571329966,-4.25847407000337,128.343754664227));
#47803=CARTESIAN_POINT('Ctrl Pts',(95.2480968834774,-4.327676692354,128.463520924426));
#47804=CARTESIAN_POINT('Ctrl Pts',(95.2402366339582,-4.39191315701078,128.586364638088));
#47805=CARTESIAN_POINT('Ctrl Pts',(95.232376384439,-4.45090391106428,128.71184121814));
#47806=CARTESIAN_POINT('Ctrl Pts',(95.2245241066918,-4.50983483739389,128.837190541332));
#47807=CARTESIAN_POINT('Ctrl Pts',(95.2166718289445,-4.56353047892363,128.965167078036));
#47808=CARTESIAN_POINT('Ctrl Pts',(95.2088195511973,-4.61175609847826,129.095299837298));
#47809=CARTESIAN_POINT('Ctrl Pts',(95.2009752780905,-4.65993255666154,129.225299938755));
#47810=CARTESIAN_POINT('Ctrl Pts',(95.1931310049836,-4.7026499690485,129.357451531393));
#47811=CARTESIAN_POINT('Ctrl Pts',(95.1852867318768,-4.73972105968052,129.491262243901));
#47812=CARTESIAN_POINT('Ctrl Pts',(95.1835089497531,-4.74812264403829,129.521588354354));
#47813=CARTESIAN_POINT('Ctrl Pts',(95.1817311676294,-4.75623441118283,129.551999601612));
#47814=CARTESIAN_POINT('Ctrl Pts',(95.1799533855056,-4.76405452823405,129.582490119308));
#47815=CARTESIAN_POINT('Origin',(213.235140564004,0.,130.804360617566));
#47816=CARTESIAN_POINT('',(93.084857876857,-4.76405452823403,129.582490119308));
#47817=CARTESIAN_POINT('',(93.4302802594722,-4.76405452823405,129.582490119308));
#47818=CARTESIAN_POINT('',(213.235140564004,-4.76405452823405,129.582490119308));
#47819=CARTESIAN_POINT('',(94.7648594360276,-4.91824943780232,130.806712224922));
#47820=CARTESIAN_POINT('Ctrl Pts',(94.7648594359911,-4.91824943780201,130.806712225562));
#47821=CARTESIAN_POINT('Ctrl Pts',(94.7573305365351,-4.91818620258719,130.938964948065));
#47822=CARTESIAN_POINT('Ctrl Pts',(94.7498016370792,-4.91278901830967,131.071085735199));
#47823=CARTESIAN_POINT('Ctrl Pts',(94.7422727376233,-4.90208663697329,131.202769535774));
#47824=CARTESIAN_POINT('Ctrl Pts',(94.7344984035042,-4.89103536860852,131.338746097785));
#47825=CARTESIAN_POINT('Ctrl Pts',(94.7267240693851,-4.87430462804154,131.474477869941));
#47826=CARTESIAN_POINT('Ctrl Pts',(94.718949735266,-4.85190793781127,131.609452180995));
#47827=CARTESIAN_POINT('Ctrl Pts',(94.7111849823189,-4.82953884950005,131.744260148273));
#47828=CARTESIAN_POINT('Ctrl Pts',(94.7034202293718,-4.80151776855422,131.878312129854));
#47829=CARTESIAN_POINT('Ctrl Pts',(94.6956554764247,-4.76791012519175,132.011098410375));
#47830=CARTESIAN_POINT('Ctrl Pts',(94.6878984355397,-4.73433586141442,132.143752805691));
#47831=CARTESIAN_POINT('Ctrl Pts',(94.6801413946547,-4.69518617259555,132.275143625096));
#47832=CARTESIAN_POINT('Ctrl Pts',(94.6723843537697,-4.65057784117023,132.40476956709));
#47833=CARTESIAN_POINT('Ctrl Pts',(94.6646331625296,-4.60600314923467,132.534297757153));
#47834=CARTESIAN_POINT('Ctrl Pts',(94.6568819712895,-4.55597813485301,132.662063350706));
#47835=CARTESIAN_POINT('Ctrl Pts',(94.6491307800494,-4.5006697939834,132.787578827453));
#47836=CARTESIAN_POINT('Ctrl Pts',(94.6413828832723,-4.44538496063406,132.913040956774));
#47837=CARTESIAN_POINT('Ctrl Pts',(94.6336349864952,-4.38482142435525,133.036254514394));
#47838=CARTESIAN_POINT('Ctrl Pts',(94.6258870897181,-4.3191947464801,133.156750849751));
#47839=CARTESIAN_POINT('Ctrl Pts',(94.618140813634,-4.25358179629116,133.277221979872));
#47840=CARTESIAN_POINT('Ctrl Pts',(94.6103945375499,-4.18290799799347,133.39497667515));
#47841=CARTESIAN_POINT('Ctrl Pts',(94.6026482614658,-4.10743523007492,133.509570201543));
#47842=CARTESIAN_POINT('Ctrl Pts',(94.5949019282004,-4.03196190503353,133.624164573839));
#47843=CARTESIAN_POINT('Ctrl Pts',(94.587155594935,-3.951689754728,133.735597404176));
#47844=CARTESIAN_POINT('Ctrl Pts',(94.5794092616697,-3.86692419079314,133.843452647294));
#47845=CARTESIAN_POINT('Ctrl Pts',(94.5716611936667,-3.78213964419796,133.951332043847));
#47846=CARTESIAN_POINT('Ctrl Pts',(94.5639131256637,-3.69285992315453,134.0556319516));
#47847=CARTESIAN_POINT('Ctrl Pts',(94.5561650576607,-3.59943068573003,134.155969455292));
#47848=CARTESIAN_POINT('Ctrl Pts',(94.5484087549189,-3.50590215060024,134.256413598877));
#47849=CARTESIAN_POINT('Ctrl Pts',(94.540652452177,-3.40821555618238,134.352886639311));
#47850=CARTESIAN_POINT('Ctrl Pts',(94.5328961494351,-3.30675378116922,134.445042214908));
#47851=CARTESIAN_POINT('Ctrl Pts',(94.525135706921,-3.20523785295179,134.53724697671));
#47852=CARTESIAN_POINT('Ctrl Pts',(94.5173752644068,-3.09994302923442,134.625129431645));
#47853=CARTESIAN_POINT('Ctrl Pts',(94.5096148218926,-2.99128443957162,134.708384242504));
#47854=CARTESIAN_POINT('Ctrl Pts',(94.5018419216272,-2.88245142149436,134.791772701377));
#47855=CARTESIAN_POINT('Ctrl Pts',(94.4940690213618,-2.77024416712548,134.870518446537));
#47856=CARTESIAN_POINT('Ctrl Pts',(94.4862961210963,-2.65510663043712,134.944359632482));
#47857=CARTESIAN_POINT('Ctrl Pts',(94.4788057853343,-2.54415463322166,135.015516505324));
#47858=CARTESIAN_POINT('Ctrl Pts',(94.4713154495723,-2.4304819669379,135.08211905854));
#47859=CARTESIAN_POINT('Ctrl Pts',(94.4638251138103,-2.31450486099081,135.14397469153));
#47860=CARTESIAN_POINT('Ctrl Pts',(94.4560507796912,-2.19413044782092,135.208175599646));
#47861=CARTESIAN_POINT('Ctrl Pts',(94.4482764455721,-2.07089208983531,135.267465892051));
#47862=CARTESIAN_POINT('Ctrl Pts',(94.440502111453,-1.94522842113553,135.321579834308));
#47863=CARTESIAN_POINT('Ctrl Pts',(94.4327373585059,-1.81971962167662,135.375627085968));
#47864=CARTESIAN_POINT('Ctrl Pts',(94.4249726055589,-1.69179181431925,135.424510527416));
#47865=CARTESIAN_POINT('Ctrl Pts',(94.4172078526118,-1.56190920366396,135.468009693345));
#47866=CARTESIAN_POINT('Ctrl Pts',(94.4094508117268,-1.43215559424861,135.511465655288));
#47867=CARTESIAN_POINT('Ctrl Pts',(94.4016937708417,-1.30045141361129,135.549547860595));
#47868=CARTESIAN_POINT('Ctrl Pts',(94.3939367299567,-1.1672815446597,135.582083595931));
#47869=CARTESIAN_POINT('Ctrl Pts',(94.3861855387166,-1.03421210014219,135.614594795816));
#47870=CARTESIAN_POINT('Ctrl Pts',(94.3784343474765,-0.899679545574676,
135.641567758598));
#47871=CARTESIAN_POINT('Ctrl Pts',(94.3706831562363,-0.764184310983108,
135.662879466078));
#47872=CARTESIAN_POINT('Ctrl Pts',(94.3629352594592,-0.628746665480602,
135.684182115514));
#47873=CARTESIAN_POINT('Ctrl Pts',(94.3551873626822,-0.492347539159849,
135.699828234747));
#47874=CARTESIAN_POINT('Ctrl Pts',(94.3474394659051,-0.355497737178362,
135.709745864553));
#47875=CARTESIAN_POINT('Ctrl Pts',(94.339693189821,-0.218676561225309,135.719661419805));
#47876=CARTESIAN_POINT('Ctrl Pts',(94.3319469137369,-0.0814052868184683,
135.723850840828));
#47877=CARTESIAN_POINT('Ctrl Pts',(94.3242006376528,0.0558003669780375,
135.722294063796));
#47878=CARTESIAN_POINT('Ctrl Pts',(94.3164543043874,0.193007033595418,135.720737275272));
#47879=CARTESIAN_POINT('Ctrl Pts',(94.3087079711221,0.330147687695843,135.71343420849));
#47880=CARTESIAN_POINT('Ctrl Pts',(94.3009616378567,0.46670721617134,135.700416932282));
#47881=CARTESIAN_POINT('Ctrl Pts',(94.2932135698538,0.603297326206309,135.687396740946));
#47882=CARTESIAN_POINT('Ctrl Pts',(94.2854655018508,0.739305662528221,135.668659830907));
#47883=CARTESIAN_POINT('Ctrl Pts',(94.2777174338478,0.874223231053945,135.644290039033));
#47884=CARTESIAN_POINT('Ctrl Pts',(94.269961131106,1.00928419157722,135.619894346655));
#47885=CARTESIAN_POINT('Ctrl Pts',(94.2622048283641,1.14325168316288,135.589853882983));
#47886=CARTESIAN_POINT('Ctrl Pts',(94.2544485256223,1.27562734663058,135.554303557753));
#47887=CARTESIAN_POINT('Ctrl Pts',(94.2466880831081,1.40807366297571,135.518734258244));
#47888=CARTESIAN_POINT('Ctrl Pts',(94.2389276405939,1.53892608546125,135.477649354486));
#47889=CARTESIAN_POINT('Ctrl Pts',(94.2311671980797,1.66770333758238,135.431233064513));
#47890=CARTESIAN_POINT('Ctrl Pts',(94.2233942978143,1.79668731438083,135.38474226299));
#47891=CARTESIAN_POINT('Ctrl Pts',(94.2156213975489,1.9235891017804,135.332903120746));
#47892=CARTESIAN_POINT('Ctrl Pts',(94.2078484972835,2.04794843377789,135.27594761494));
#47893=CARTESIAN_POINT('Ctrl Pts',(94.2003581615215,2.16778699081442,135.221062585233));
#47894=CARTESIAN_POINT('Ctrl Pts',(94.1928678257595,2.28526445785325,135.161426858583));
#47895=CARTESIAN_POINT('Ctrl Pts',(94.1853774899975,2.39999381239291,135.097286515246));
#47896=CARTESIAN_POINT('Ctrl Pts',(94.1776031558784,2.51907316528185,135.030714271297));
#47897=CARTESIAN_POINT('Ctrl Pts',(94.1698288217593,2.63556911022584,134.959078201723));
#47898=CARTESIAN_POINT('Ctrl Pts',(94.1620544876402,2.74902098487157,134.882603705862));
#47899=CARTESIAN_POINT('Ctrl Pts',(94.1542897346931,2.8623330402212,134.806223457983));
#47900=CARTESIAN_POINT('Ctrl Pts',(94.146524981746,2.97260816864958,134.725016864697));
#47901=CARTESIAN_POINT('Ctrl Pts',(94.1387602287989,3.07940997252379,134.639255307596));
#47902=CARTESIAN_POINT('Ctrl Pts',(94.1310031879139,3.18610569934069,134.553578930083));
#47903=CARTESIAN_POINT('Ctrl Pts',(94.1232461470289,3.28933466389771,134.463356835035));
#47904=CARTESIAN_POINT('Ctrl Pts',(94.1154891061439,3.38868946651886,134.368903612398));
#47905=CARTESIAN_POINT('Ctrl Pts',(94.1077379149038,3.48796934491049,134.274521617671));
#47906=CARTESIAN_POINT('Ctrl Pts',(94.0999867236637,3.583380594297,134.175915114588));
#47907=CARTESIAN_POINT('Ctrl Pts',(94.0922355324236,3.67454922133108,134.073438634762));
#47908=CARTESIAN_POINT('Ctrl Pts',(94.0844876356465,3.76567909926674,133.971005710174));
#47909=CARTESIAN_POINT('Ctrl Pts',(94.0767397388694,3.85256968200841,133.864706371799));
#47910=CARTESIAN_POINT('Ctrl Pts',(94.0689918420923,3.93488432555971,133.754931478766));
#47911=CARTESIAN_POINT('Ctrl Pts',(94.0612455660082,4.01718175066207,133.645179548275));
#47912=CARTESIAN_POINT('Ctrl Pts',(94.0534992899241,4.09490490607276,133.531953821786));
#47913=CARTESIAN_POINT('Ctrl Pts',(94.04575301384,4.16775815277707,133.415677343369));
#47914=CARTESIAN_POINT('Ctrl Pts',(94.0380066805747,4.2406119372675,133.299400006626));
#47915=CARTESIAN_POINT('Ctrl Pts',(94.0302603473094,4.30859553373807,133.180072204323));
#47916=CARTESIAN_POINT('Ctrl Pts',(94.022514014044,4.3714574913892,133.058144649694));
#47917=CARTESIAN_POINT('Ctrl Pts',(94.014765946041,4.43433352653985,132.936189790236));
#47918=CARTESIAN_POINT('Ctrl Pts',(94.007017878038,4.49208546143721,132.811634367381));
#47919=CARTESIAN_POINT('Ctrl Pts',(93.9992698100351,4.54450870667887,132.684951928144));
#47920=CARTESIAN_POINT('Ctrl Pts',(93.9915135072932,4.59698766796945,132.558134849302));
#47921=CARTESIAN_POINT('Ctrl Pts',(93.9837572045514,4.64412647663145,132.42918660008));
#47922=CARTESIAN_POINT('Ctrl Pts',(93.9760009018095,4.68576926073752,132.298599386179));
#47923=CARTESIAN_POINT('Ctrl Pts',(93.9682404592953,4.72743427085134,132.167942473951));
#47924=CARTESIAN_POINT('Ctrl Pts',(93.9604800167812,4.76359730833694,132.035645230945));
#47925=CARTESIAN_POINT('Ctrl Pts',(93.952719574267,4.79415321933547,131.902212143063));
#47926=CARTESIAN_POINT('Ctrl Pts',(93.9449466740016,4.82475818139496,131.768564856542));
#47927=CARTESIAN_POINT('Ctrl Pts',(93.9371737737361,4.84973795870201,131.633778466133));
#47928=CARTESIAN_POINT('Ctrl Pts',(93.9294008734707,4.86903893519409,131.49836559598));
#47929=CARTESIAN_POINT('Ctrl Pts',(93.9219105377087,4.88763827257452,131.367875324742));
#47930=CARTESIAN_POINT('Ctrl Pts',(93.9144202019466,4.90096448725339,131.236803637648));
#47931=CARTESIAN_POINT('Ctrl Pts',(93.9069298661845,4.90901541840449,131.10560916008));
#47932=CARTESIAN_POINT('Ctrl Pts',(93.8991555320654,4.91737160305718,130.96944040402));
#47933=CARTESIAN_POINT('Ctrl Pts',(93.8913811979463,4.92007105269916,130.832708020789));
#47934=CARTESIAN_POINT('Ctrl Pts',(93.8836068638272,4.91705440292345,130.69592141252));
#47935=CARTESIAN_POINT('Ctrl Pts',(93.8758421108801,4.91404147089899,130.55930338152));
#47936=CARTESIAN_POINT('Ctrl Pts',(93.8680773579331,4.90532646461207,130.422631645567));
#47937=CARTESIAN_POINT('Ctrl Pts',(93.860312604986,4.89090182150286,130.286420046728));
#47938=CARTESIAN_POINT('Ctrl Pts',(93.852555564101,4.87649150515253,130.150343735169));
#47939=CARTESIAN_POINT('Ctrl Pts',(93.844798523216,4.85638287821656,130.014727037521));
#47940=CARTESIAN_POINT('Ctrl Pts',(93.837041482331,4.83062040465032,129.880082754218));
#47941=CARTESIAN_POINT('Ctrl Pts',(93.8292902910908,4.80487735876579,129.745540007216));
#47942=CARTESIAN_POINT('Ctrl Pts',(93.8215390998507,4.77348902588368,129.611968597406));
#47943=CARTESIAN_POINT('Ctrl Pts',(93.8137879086106,4.73655153095094,129.47987480898));
#47944=CARTESIAN_POINT('Ctrl Pts',(93.8060400118335,4.69962973543887,129.347837163937));
#47945=CARTESIAN_POINT('Ctrl Pts',(93.7982921150564,4.65716357390278,129.21727626691));
#47946=CARTESIAN_POINT('Ctrl Pts',(93.7905442182794,4.60929992289413,129.088686614934));
#47947=CARTESIAN_POINT('Ctrl Pts',(93.7827979421952,4.56144628392941,128.96012386114));
#47948=CARTESIAN_POINT('Ctrl Pts',(93.7750516661111,4.5081975375087,128.8335318984));
#47949=CARTESIAN_POINT('Ctrl Pts',(93.767305390027,4.44974980247846,128.709388121841));
#47950=CARTESIAN_POINT('Ctrl Pts',(93.7595590567616,4.39130163600036,128.585243428881));
#47951=CARTESIAN_POINT('Ctrl Pts',(93.7518127234963,4.32765457086784,128.463547311887));
#47952=CARTESIAN_POINT('Ctrl Pts',(93.7440663902309,4.25905188959048,128.344754945049));
#47953=CARTESIAN_POINT('Ctrl Pts',(93.7363183222279,4.19043384521836,128.225935975485));
#47954=CARTESIAN_POINT('Ctrl Pts',(93.728570254225,4.11685817185928,128.110022388548));
#47955=CARTESIAN_POINT('Ctrl Pts',(93.720822186222,4.03861269245762,127.997442274824));
#47956=CARTESIAN_POINT('Ctrl Pts',(93.7130658834802,3.96028405282926,127.884742509616));
#47957=CARTESIAN_POINT('Ctrl Pts',(93.7053095807383,3.87727591626608,127.775383616408));
#47958=CARTESIAN_POINT('Ctrl Pts',(93.6975532779964,3.78991813678017,127.669762783871));
#47959=CARTESIAN_POINT('Ctrl Pts',(93.6897928354823,3.70251373181701,127.564085578316));
#47960=CARTESIAN_POINT('Ctrl Pts',(93.6820323929681,3.61075531951605,127.462150699305));
#47961=CARTESIAN_POINT('Ctrl Pts',(93.6742719504539,3.51501049992361,127.364319302708));
#47962=CARTESIAN_POINT('Ctrl Pts',(93.6664990501885,3.41911198224693,127.26633085847));
#47963=CARTESIAN_POINT('Ctrl Pts',(93.658726149923,3.31921455444623,127.172459328));
#47964=CARTESIAN_POINT('Ctrl Pts',(93.6509532496576,3.21572052094178,127.083026905885));
#47965=CARTESIAN_POINT('Ctrl Pts',(93.6434629138956,3.11598875624116,126.99684557758));
#47966=CARTESIAN_POINT('Ctrl Pts',(93.6359725781336,3.01291757829159,126.914786407275));
#47967=CARTESIAN_POINT('Ctrl Pts',(93.6284822423716,2.90689167363581,126.837099111155));
#47968=CARTESIAN_POINT('Ctrl Pts',(93.6207079082525,2.79684576457891,126.75646627759));
#47969=CARTESIAN_POINT('Ctrl Pts',(93.6129335741334,2.68326805657351,126.680287961144));
#47970=CARTESIAN_POINT('Ctrl Pts',(93.6051592400143,2.56655503614888,126.608889451068));
#47971=CARTESIAN_POINT('Ctrl Pts',(93.5973944870672,2.44998585409105,126.537578933274));
#47972=CARTESIAN_POINT('Ctrl Pts',(93.5896297341201,2.33028937811493,126.47103670321));
#47973=CARTESIAN_POINT('Ctrl Pts',(93.581864981173,2.20789383035681,126.409546867659));
#47974=CARTESIAN_POINT('Ctrl Pts',(93.574107940288,2.0856198475822,126.34811810468));
#47975=CARTESIAN_POINT('Ctrl Pts',(93.566350899403,1.96065247494643,126.291731924326));
#47976=CARTESIAN_POINT('Ctrl Pts',(93.558593858518,1.83344717983344,126.240628098973));
#47977=CARTESIAN_POINT('Ctrl Pts',(93.5508426672779,1.70633781122309,126.189562811413));
#47978=CARTESIAN_POINT('Ctrl Pts',(93.5430914760378,1.57699424058588,126.143772095165));
#47979=CARTESIAN_POINT('Ctrl Pts',(93.5353402847976,1.44589437703271,126.103448736562));
#47980=CARTESIAN_POINT('Ctrl Pts',(93.5275923880206,1.31485023441875,126.063142516461));
#47981=CARTESIAN_POINT('Ctrl Pts',(93.5198444912435,1.18205165646947,126.028299146896));
#47982=CARTESIAN_POINT('Ctrl Pts',(93.5120965944664,1.04799406790868,125.999062344188));
#47983=CARTESIAN_POINT('Ctrl Pts',(93.5043503183824,0.913964521305467,125.969831657189));
#47984=CARTESIAN_POINT('Ctrl Pts',(93.4966040422982,0.77867686966836,125.946205287594));
#47985=CARTESIAN_POINT('Ctrl Pts',(93.4888577662142,0.642638766066019,125.928276278791));
#47986=CARTESIAN_POINT('Ctrl Pts',(93.4811114329488,0.506599658261301,125.910347137639));
#47987=CARTESIAN_POINT('Ctrl Pts',(93.4733650996835,0.369810475050688,125.898115492285));
#47988=CARTESIAN_POINT('Ctrl Pts',(93.4656187664181,0.232785667511623,125.891622695032));
#47989=CARTESIAN_POINT('Ctrl Pts',(93.4578706984151,0.0957301742169731,
125.885128443762));
#47990=CARTESIAN_POINT('Ctrl Pts',(93.4501226304122,-0.0415606579529346,
125.884375616444));
#47991=CARTESIAN_POINT('Ctrl Pts',(93.4423745624092,-0.178571088931887,
125.889353452902));
#47992=CARTESIAN_POINT('Ctrl Pts',(93.4346182596674,-0.315727136227329,
125.894336579864));
#47993=CARTESIAN_POINT('Ctrl Pts',(93.4268619569255,-0.452601795686883,
125.905062523048));
#47994=CARTESIAN_POINT('Ctrl Pts',(93.4191056541837,-0.588682607081849,
125.921468457112));
#47995=CARTESIAN_POINT('Ctrl Pts',(93.4113452116695,-0.724836048903355,
125.937883147517));
#47996=CARTESIAN_POINT('Ctrl Pts',(93.4035847691554,-0.860194412733907,
125.959983806516));
#47997=CARTESIAN_POINT('Ctrl Pts',(93.3958243266412,-0.994255151106295,
125.987656375348));
#47998=CARTESIAN_POINT('Ctrl Pts',(93.3880514263758,-1.12853109567718,126.015373366645));
#47999=CARTESIAN_POINT('Ctrl Pts',(93.3802785261103,-1.26150487269735,126.048680046737));
#48000=CARTESIAN_POINT('Ctrl Pts',(93.3725056258449,-1.39268795537226,126.087412099566));
#48001=CARTESIAN_POINT('Ctrl Pts',(93.3650152900828,-1.51910220256204,126.124736144715));
#48002=CARTESIAN_POINT('Ctrl Pts',(93.3575249543208,-1.64385339591185,126.167097859895));
#48003=CARTESIAN_POINT('Ctrl Pts',(93.3500346185588,-1.76652350964976,126.214308575121));
#48004=CARTESIAN_POINT('Ctrl Pts',(93.3422600320179,-1.89384883197644,126.26331088995));
#48005=CARTESIAN_POINT('Ctrl Pts',(93.334485445477,-2.01933534701955,126.317692732156));
#48006=CARTESIAN_POINT('Ctrl Pts',(93.3267108589361,-2.14249502174921,126.377296336998));
#48007=CARTESIAN_POINT('Ctrl Pts',(93.3189459119137,-2.26550199382955,126.436826040797));
#48008=CARTESIAN_POINT('Ctrl Pts',(93.3111809648912,-2.38618751743574,126.501564456171));
#48009=CARTESIAN_POINT('Ctrl Pts',(93.3034160178688,-2.50408106651856,126.571304856676));
#48010=CARTESIAN_POINT('Ctrl Pts',(93.2956588410081,-2.62185664287882,126.640975469945));
#48011=CARTESIAN_POINT('Ctrl Pts',(93.2879016641474,-2.73684547044058,126.715637909341));
#48012=CARTESIAN_POINT('Ctrl Pts',(93.2801444872867,-2.84859960869798,126.795038563674));
#48013=CARTESIAN_POINT('Ctrl Pts',(93.2720075451855,-2.96582485299805,126.878326406495));
#48014=CARTESIAN_POINT('Ctrl Pts',(93.2638706030843,-3.07949028666099,126.966827943532));
#48015=CARTESIAN_POINT('Ctrl Pts',(93.255733660983,-3.18911028308469,127.060197337897));
#48016=CARTESIAN_POINT('Ctrl Pts',(93.2479861016518,-3.29348455730325,127.14909866146));
#48017=CARTESIAN_POINT('Ctrl Pts',(93.2402385423207,-3.39419123848658,127.242412495729));
#48018=CARTESIAN_POINT('Ctrl Pts',(93.2324909829895,-3.49084335641013,127.339797770177));
#48019=CARTESIAN_POINT('Ctrl Pts',(93.2247450433043,-3.5874752689745,127.437162685998));
#48020=CARTESIAN_POINT('Ctrl Pts',(93.2169991036192,-3.68005402955596,127.538597071215));
#48021=CARTESIAN_POINT('Ctrl Pts',(93.2092531639341,-3.76822889688579,127.643722384048));
#48022=CARTESIAN_POINT('Ctrl Pts',(93.2015071661177,-3.8564044259445,127.748848485819));
#48023=CARTESIAN_POINT('Ctrl Pts',(93.1937611683014,-3.94017574517851,127.857665270521));
#48024=CARTESIAN_POINT('Ctrl Pts',(93.186015170485,-4.01923210866512,127.969760765881));
#48025=CARTESIAN_POINT('Ctrl Pts',(93.1782674370955,-4.09830618557037,128.081881377427));
#48026=CARTESIAN_POINT('Ctrl Pts',(93.170519703706,-4.17266297993153,128.197281841703));
#48027=CARTESIAN_POINT('Ctrl Pts',(93.1627719703165,-4.24203504556325,128.315521182264));
#48028=CARTESIAN_POINT('Ctrl Pts',(93.1550170718371,-4.31147126635622,128.433869870354));
#48029=CARTESIAN_POINT('Ctrl Pts',(93.1472621733577,-4.37591335644257,128.555062339154));
#48030=CARTESIAN_POINT('Ctrl Pts',(93.1395072748783,-4.43513966213504,128.678632685808));
#48031=CARTESIAN_POINT('Ctrl Pts',(93.1317481956758,-4.49439789716756,128.80226965015));
#48032=CARTESIAN_POINT('Ctrl Pts',(93.1239891164731,-4.54843459148819,128.92828668781));
#48033=CARTESIAN_POINT('Ctrl Pts',(93.1162300372706,-4.59707661442089,129.056198821952));
#48034=CARTESIAN_POINT('Ctrl Pts',(93.1084611478687,-4.64578013794245,129.184272681925));
#48035=CARTESIAN_POINT('Ctrl Pts',(93.1006922584668,-4.68907524859617,129.314246052368));
#48036=CARTESIAN_POINT('Ctrl Pts',(93.0929233690649,-4.7268388313816,129.445619389575));
#48037=CARTESIAN_POINT('Ctrl Pts',(93.0902348716622,-4.73990727514232,129.491082371165));
#48038=CARTESIAN_POINT('Ctrl Pts',(93.0875463742596,-4.75231372960658,129.536712923651));
#48039=CARTESIAN_POINT('Ctrl Pts',(93.084857876857,-4.76405452823403,129.582490119308));
#48040=CARTESIAN_POINT('Ctrl Pts',(94.8350013119177,-4.76405452823406,129.582490119308));
#48041=CARTESIAN_POINT('Ctrl Pts',(94.8273289265629,-4.79777932866022,129.713982604325));
#48042=CARTESIAN_POINT('Ctrl Pts',(94.8196565412081,-4.82603167565206,129.846777706001));
#48043=CARTESIAN_POINT('Ctrl Pts',(94.8119841558533,-4.84873498274878,129.980375102179));
#48044=CARTESIAN_POINT('Ctrl Pts',(94.8041300358823,-4.87197605960158,130.117136999407));
#48045=CARTESIAN_POINT('Ctrl Pts',(94.7962759159114,-4.889401876088,130.254739227271));
#48046=CARTESIAN_POINT('Ctrl Pts',(94.7884217959404,-4.90098670095333,130.392641757689));
#48047=CARTESIAN_POINT('Ctrl Pts',(94.7805676759695,-4.91257152581865,130.530544288107));
#48048=CARTESIAN_POINT('Ctrl Pts',(94.7727135559985,-4.91831540452579,130.668746675627));
#48049=CARTESIAN_POINT('Ctrl Pts',(94.7648594360275,-4.91824943780232,130.806712224922));
#48050=CARTESIAN_POINT('',(95.110140563956,-4.91824922401509,130.807123401486));
#48051=CARTESIAN_POINT('Ctrl Pts',(95.1799533855056,-4.76405452823405,129.582490119308));
#48052=CARTESIAN_POINT('Ctrl Pts',(95.172116002983,-4.79852964635118,129.716908081614));
#48053=CARTESIAN_POINT('Ctrl Pts',(95.1642786204605,-4.82733257278166,129.852867781761));
#48054=CARTESIAN_POINT('Ctrl Pts',(95.1564412379379,-4.85033683341142,129.989857293477));
#48055=CARTESIAN_POINT('Ctrl Pts',(95.1486064182765,-4.873333571539,130.126802008973));
#48056=CARTESIAN_POINT('Ctrl Pts',(95.1407715986151,-4.89053535270011,130.264775493699));
#48057=CARTESIAN_POINT('Ctrl Pts',(95.1329367789537,-4.90186675161587,130.403255379626));
#48058=CARTESIAN_POINT('Ctrl Pts',(95.1253380406386,-4.91285670911659,130.537562544377));
#48059=CARTESIAN_POINT('Ctrl Pts',(95.1177393023236,-4.91832493420278,130.672345688801));
#48060=CARTESIAN_POINT('Ctrl Pts',(95.1101405640085,-4.91824922401561,130.807123400555));
#48061=CARTESIAN_POINT('Ctrl Pts',(95.110140563956,-4.91824922401509,130.807123401486));
#48062=CARTESIAN_POINT('Ctrl Pts',(95.1015424548622,-4.91816355654752,130.959626806792));
#48063=CARTESIAN_POINT('Ctrl Pts',(95.0929443457683,-4.91098067842199,131.111875745966));
#48064=CARTESIAN_POINT('Ctrl Pts',(95.0843462366745,-4.89679575169032,131.263244512171));
#48065=CARTESIAN_POINT('Ctrl Pts',(95.0756985162661,-4.88252897756011,131.415486680119));
#48066=CARTESIAN_POINT('Ctrl Pts',(95.0670507958577,-4.86117920513635,131.566838266414));
#48067=CARTESIAN_POINT('Ctrl Pts',(95.0584030754493,-4.83289334049698,131.716679104653));
#48068=CARTESIAN_POINT('Ctrl Pts',(95.0497295757736,-4.80452315434503,131.866966625582));
#48069=CARTESIAN_POINT('Ctrl Pts',(95.0410560760979,-4.76917557784388,132.015734171589));
#48070=CARTESIAN_POINT('Ctrl Pts',(95.0323825764223,-4.72704749906738,132.162375714706));
#48071=CARTESIAN_POINT('Ctrl Pts',(95.0236768895022,-4.68476308353893,132.309561442681));
#48072=CARTESIAN_POINT('Ctrl Pts',(95.0149712025821,-4.63564786483374,132.454605157963));
#48073=CARTESIAN_POINT('Ctrl Pts',(95.006265515662,-4.57994812761617,132.596916951645));
#48074=CARTESIAN_POINT('Ctrl Pts',(95.0045541322003,-4.56899854833866,132.624892923254));
#48075=CARTESIAN_POINT('Ctrl Pts',(95.0028427487386,-4.55779465553684,132.65276339691));
#48076=CARTESIAN_POINT('Ctrl Pts',(95.0011313652769,-4.54633852747124,132.680524004942));
#48077=CARTESIAN_POINT('Ctrl Pts',(94.9933570311578,-4.49429655716773,132.806632645708));
#48078=CARTESIAN_POINT('Ctrl Pts',(94.9855826970387,-4.43692108158099,132.930774042726));
#48079=CARTESIAN_POINT('Ctrl Pts',(94.9778083629196,-4.37438151415451,133.05246413634));
#48080=CARTESIAN_POINT('Ctrl Pts',(94.9700436099725,-4.31191902115552,133.174004257789));
#48081=CARTESIAN_POINT('Ctrl Pts',(94.9622788570254,-4.24430527633272,133.293098742356));
#48082=CARTESIAN_POINT('Ctrl Pts',(94.9545141040783,-4.17175821941467,133.40928219436));
#48083=CARTESIAN_POINT('Ctrl Pts',(94.9467570631933,-4.09928321725629,133.525350251322));
#48084=CARTESIAN_POINT('Ctrl Pts',(94.9390000223083,-4.02188485962807,133.638512700018));
#48085=CARTESIAN_POINT('Ctrl Pts',(94.9312429814233,-3.93982741709419,133.748327836475));
#48086=CARTESIAN_POINT('Ctrl Pts',(94.9234917901832,-3.85783185471631,133.858060160484));
#48087=CARTESIAN_POINT('Ctrl Pts',(94.9157405989431,-3.77118443382339,133.964449884669));
#48088=CARTESIAN_POINT('Ctrl Pts',(94.907989407703,-3.68019303266012,134.067083760105));
#48089=CARTESIAN_POINT('Ctrl Pts',(94.9002415109259,-3.58924030526937,134.169674013406));
#48090=CARTESIAN_POINT('Ctrl Pts',(94.8924936141488,-3.49394752859292,134.268511301012));
#48091=CARTESIAN_POINT('Ctrl Pts',(94.8847457173717,-3.39466306540784,134.363215171331));
#48092=CARTESIAN_POINT('Ctrl Pts',(94.8769994412876,-3.29539937039219,134.457899231642));
#48093=CARTESIAN_POINT('Ctrl Pts',(94.8692531652036,-3.19214593240241,134.548451324765));
#48094=CARTESIAN_POINT('Ctrl Pts',(94.8615068891195,-3.0852879169283,134.63452791576));
#48095=CARTESIAN_POINT('Ctrl Pts',(94.8537605558541,-2.97842911265261,134.720605142153));
#48096=CARTESIAN_POINT('Ctrl Pts',(94.8460142225888,-2.86796598226844,134.802206555236));
#48097=CARTESIAN_POINT('Ctrl Pts',(94.8382678893234,-2.75431638578097,134.879029231026));
#48098=CARTESIAN_POINT('Ctrl Pts',(94.8305198213205,-2.64064133825442,134.955869110722));
#48099=CARTESIAN_POINT('Ctrl Pts',(94.8227717533175,-2.52377872851369,135.027927904713));
#48100=CARTESIAN_POINT('Ctrl Pts',(94.8150236853145,-2.4041746252623,135.094946525545));
#48101=CARTESIAN_POINT('Ctrl Pts',(94.8072673825727,-2.28444340534651,135.162036374565));
#48102=CARTESIAN_POINT('Ctrl Pts',(94.7995110798309,-2.16196521312088,135.224075158309));
#48103=CARTESIAN_POINT('Ctrl Pts',(94.791754777089,-2.037210399338,135.280849962056));
#48104=CARTESIAN_POINT('Ctrl Pts',(94.7839943345748,-1.91238900015462,135.337655068224));
#48105=CARTESIAN_POINT('Ctrl Pts',(94.7762338920607,-1.78528892035869,135.389190449303));
#48106=CARTESIAN_POINT('Ctrl Pts',(94.7684734495465,-1.65639869519593,135.435292103245));
#48107=CARTESIAN_POINT('Ctrl Pts',(94.7607005492811,-1.5273015640014,135.481467763655));
#48108=CARTESIAN_POINT('Ctrl Pts',(94.7529276490156,-1.39640891840004,135.522192149977));
#48109=CARTESIAN_POINT('Ctrl Pts',(94.7451547487502,-1.26422346198469,135.557351476033));
#48110=CARTESIAN_POINT('Ctrl Pts',(94.7376644129881,-1.13684327986367,135.591232672026));
#48111=CARTESIAN_POINT('Ctrl Pts',(94.730174077226,-1.0082629495304,135.619946323951));
#48112=CARTESIAN_POINT('Ctrl Pts',(94.7226837414639,-0.878937631082016,
135.643436118441));
#48113=CARTESIAN_POINT('Ctrl Pts',(94.7149094073448,-0.744708903878587,
135.667816535628));
#48114=CARTESIAN_POINT('Ctrl Pts',(94.7071350732257,-0.609252384671647,
135.686646380469));
#48115=CARTESIAN_POINT('Ctrl Pts',(94.6993607391066,-0.473066898663637,
135.699806539225));
#48116=CARTESIAN_POINT('Ctrl Pts',(94.6915959861596,-0.337049249095979,
135.712950479261));
#48117=CARTESIAN_POINT('Ctrl Pts',(94.6838312332125,-0.200304805665102,
135.720438598774));
#48118=CARTESIAN_POINT('Ctrl Pts',(94.6760664802654,-0.0633429206830855,
135.722202698896));
#48119=CARTESIAN_POINT('Ctrl Pts',(94.6683094393804,0.0734829318239427,
135.723965046889));
#48120=CARTESIAN_POINT('Ctrl Pts',(94.6605523984954,0.21052540769693,135.720014684248));
#48121=CARTESIAN_POINT('Ctrl Pts',(94.6527953576104,0.347270044179051,135.710335197496));
#48122=CARTESIAN_POINT('Ctrl Pts',(94.6450441663703,0.483911560466989,135.70066301012));
#48123=CARTESIAN_POINT('Ctrl Pts',(94.6372929751302,0.620255296011304,135.685270325576));
#48124=CARTESIAN_POINT('Ctrl Pts',(94.6295417838901,0.755787157075454,135.664192799411));
#48125=CARTESIAN_POINT('Ctrl Pts',(94.621793887113,0.891261413483313,135.643124231758));
#48126=CARTESIAN_POINT('Ctrl Pts',(94.6140459903359,1.02592409621296,135.616375688094));
#48127=CARTESIAN_POINT('Ctrl Pts',(94.6062980935588,1.15926682197451,135.584034612513));
#48128=CARTESIAN_POINT('Ctrl Pts',(94.5985518174748,1.29258165531247,135.551700301987));
#48129=CARTESIAN_POINT('Ctrl Pts',(94.5908055413907,1.42457670116469,135.513775878507));
#48130=CARTESIAN_POINT('Ctrl Pts',(94.5830592653066,1.55475474250059,135.470399703683));
#48131=CARTESIAN_POINT('Ctrl Pts',(94.5753129320412,1.68493374478114,135.427023208666));
#48132=CARTESIAN_POINT('Ctrl Pts',(94.5675665987759,1.813295344865,135.378195005592));
#48133=CARTESIAN_POINT('Ctrl Pts',(94.5598202655106,1.93935882068549,135.324102914106));
#48134=CARTESIAN_POINT('Ctrl Pts',(94.5520721975076,2.06545052754733,135.269998709071));
#48135=CARTESIAN_POINT('Ctrl Pts',(94.5443241295046,2.18924272683591,135.21062842406));
#48136=CARTESIAN_POINT('Ctrl Pts',(94.5365760615016,2.31027632990805,135.146227306211));
#48137=CARTESIAN_POINT('Ctrl Pts',(94.5288197587598,2.43143856893385,135.081757742088));
#48138=CARTESIAN_POINT('Ctrl Pts',(94.5210634560179,2.54983600932203,135.012246848201));
#48139=CARTESIAN_POINT('Ctrl Pts',(94.5133071532761,2.66503528381516,134.937975258352));
#48140=CARTESIAN_POINT('Ctrl Pts',(94.5055467107619,2.78029604362976,134.863664027519));
#48141=CARTESIAN_POINT('Ctrl Pts',(94.4977862682478,2.89235491701066,134.78458726302));
#48142=CARTESIAN_POINT('Ctrl Pts',(94.4900258257336,3.00080985915818,134.701067336281));
#48143=CARTESIAN_POINT('Ctrl Pts',(94.4822529254682,3.10943890280701,134.617413335941));
#48144=CARTESIAN_POINT('Ctrl Pts',(94.4744800252028,3.21445215457224,134.52930217168));
#48145=CARTESIAN_POINT('Ctrl Pts',(94.4667071249373,3.31548215934863,134.437095278058));
#48146=CARTESIAN_POINT('Ctrl Pts',(94.4592167891753,3.41283946897272,134.348240337274));
#48147=CARTESIAN_POINT('Ctrl Pts',(94.4517264534132,3.50649788684419,134.255582494017));
#48148=CARTESIAN_POINT('Ctrl Pts',(94.4442361176511,3.59616400978133,134.159474248615));
#48149=CARTESIAN_POINT('Ctrl Pts',(94.436461783532,3.68922985102259,134.059722029878));
#48150=CARTESIAN_POINT('Ctrl Pts',(94.4286874494129,3.77828949011739,133.955936615023));
#48151=CARTESIAN_POINT('Ctrl Pts',(94.4209131152939,3.86297308609639,133.848473295933));
#48152=CARTESIAN_POINT('Ctrl Pts',(94.4131483623468,3.94755231711168,133.74114241578));
#48153=CARTESIAN_POINT('Ctrl Pts',(94.4053836093997,4.02776599597515,133.630142954221));
#48154=CARTESIAN_POINT('Ctrl Pts',(94.3976188564526,4.10328142768276,133.51586658063));
#48155=CARTESIAN_POINT('Ctrl Pts',(94.3898618155676,4.17872185639902,133.401703707945));
#48156=CARTESIAN_POINT('Ctrl Pts',(94.3821047746826,4.24947311008669,133.284270724247));
#48157=CARTESIAN_POINT('Ctrl Pts',(94.3743477337976,4.31524329993689,133.163991589741));
#48158=CARTESIAN_POINT('Ctrl Pts',(94.3665965425574,4.38096389197532,133.043803158666));
#48159=CARTESIAN_POINT('Ctrl Pts',(94.3588453513173,4.44171070996742,132.920773190514));
#48160=CARTESIAN_POINT('Ctrl Pts',(94.3510941600772,4.4972358717138,132.7953534796));
#48161=CARTESIAN_POINT('Ctrl Pts',(94.3433462633001,4.5527374337853,132.669987075409));
#48162=CARTESIAN_POINT('Ctrl Pts',(94.335598366523,4.60302159577734,132.542233305363));
#48163=CARTESIAN_POINT('Ctrl Pts',(94.3278504697459,4.64788713329477,132.412567152391));
#48164=CARTESIAN_POINT('Ctrl Pts',(94.3201041936618,4.69274328590893,132.282928122782));
#48165=CARTESIAN_POINT('Ctrl Pts',(94.3123579175777,4.73218294080165,132.151377875167));
#48166=CARTESIAN_POINT('Ctrl Pts',(94.3046116414936,4.7660537475623,132.018409520143));
#48167=CARTESIAN_POINT('Ctrl Pts',(94.2968653082282,4.79992480434952,131.885440183576));
#48168=CARTESIAN_POINT('Ctrl Pts',(94.2891189749629,4.82822683446862,131.75105309758));
#48169=CARTESIAN_POINT('Ctrl Pts',(94.2813726416975,4.85085801388609,131.615754228348));
#48170=CARTESIAN_POINT('Ctrl Pts',(94.2736245736945,4.87349426139927,131.480425059872));
#48171=CARTESIAN_POINT('Ctrl Pts',(94.2658765056916,4.89045706667438,131.344184087385));
#48172=CARTESIAN_POINT('Ctrl Pts',(94.2581284376886,4.90169620116392,131.207544711988));
#48173=CARTESIAN_POINT('Ctrl Pts',(94.2503721349467,4.91294728073934,131.070760114637));
#48174=CARTESIAN_POINT('Ctrl Pts',(94.2426158322048,4.91846250560974,130.933576658805));
#48175=CARTESIAN_POINT('Ctrl Pts',(94.234859529463,4.91824373535125,130.796510638064));
#48176=CARTESIAN_POINT('Ctrl Pts',(94.2270990869488,4.91802484832848,130.659371461059));
#48177=CARTESIAN_POINT('Ctrl Pts',(94.2193386444346,4.9120658850375,130.522350234443));
#48178=CARTESIAN_POINT('Ctrl Pts',(94.2115782019205,4.90042075065456,130.38595945952));
#48179=CARTESIAN_POINT('Ctrl Pts',(94.203805301655,4.8887569224681,130.249349738018));
#48180=CARTESIAN_POINT('Ctrl Pts',(94.1960324013896,4.8713887322074,130.113372878659));
#48181=CARTESIAN_POINT('Ctrl Pts',(94.1882595011242,4.84842164654532,129.978533396042));
#48182=CARTESIAN_POINT('Ctrl Pts',(94.1807691653621,4.82628947229773,129.848595668258));
#48183=CARTESIAN_POINT('Ctrl Pts',(94.1732788296002,4.79895846715251,129.719714361185));
#48184=CARTESIAN_POINT('Ctrl Pts',(94.1657884938381,4.7665666080338,129.592326858268));
#48185=CARTESIAN_POINT('Ctrl Pts',(94.158014159719,4.73294660173122,129.46010941946));
#48186=CARTESIAN_POINT('Ctrl Pts',(94.1502398256,4.69376790319095,129.32908247096));
#48187=CARTESIAN_POINT('Ctrl Pts',(94.1424654914809,4.64912952145985,129.199749214394));
#48188=CARTESIAN_POINT('Ctrl Pts',(94.1347007385338,4.60454615254482,129.070575349507));
#48189=CARTESIAN_POINT('Ctrl Pts',(94.1269359855867,4.55451661462139,128.943091389425));
#48190=CARTESIAN_POINT('Ctrl Pts',(94.1191712326396,4.49919060044921,128.81778894674));
#48191=CARTESIAN_POINT('Ctrl Pts',(94.1114141917546,4.44391953685423,128.692610956207));
#48192=CARTESIAN_POINT('Ctrl Pts',(94.1036571508696,4.38336262260845,128.569610526551));
#48193=CARTESIAN_POINT('Ctrl Pts',(94.0959001099846,4.31771877440675,128.44926239294));
#48194=CARTESIAN_POINT('Ctrl Pts',(94.0881489187445,4.25212442874161,128.329005014793));
#48195=CARTESIAN_POINT('Ctrl Pts',(94.0803977275043,4.18145097109365,128.211396293416));
#48196=CARTESIAN_POINT('Ctrl Pts',(94.0726465362642,4.10594452243216,128.096888984989));
#48197=CARTESIAN_POINT('Ctrl Pts',(94.0648986394871,4.0304701660256,127.982430345222));
#48198=CARTESIAN_POINT('Ctrl Pts',(94.0571507427101,3.95016711892722,127.871070822348));
#48199=CARTESIAN_POINT('Ctrl Pts',(94.049402845933,3.86532623102535,127.763236452023));
#48200=CARTESIAN_POINT('Ctrl Pts',(94.0416565698489,3.78050309000828,127.655424638324));
#48201=CARTESIAN_POINT('Ctrl Pts',(94.0339102937648,3.69114423782945,127.551136817544));
#48202=CARTESIAN_POINT('Ctrl Pts',(94.0261640176807,3.59758219328283,127.450767704722));
#48203=CARTESIAN_POINT('Ctrl Pts',(94.0184176844154,3.50401945808245,127.350397850999));
#48204=CARTESIAN_POINT('Ctrl Pts',(94.01067135115,3.40625373518845,127.253947048936));
#48205=CARTESIAN_POINT('Ctrl Pts',(94.0029250178847,3.30465566991289,127.161774453065));
#48206=CARTESIAN_POINT('Ctrl Pts',(93.9951769498817,3.20303485245505,127.069581215781));
#48207=CARTESIAN_POINT('Ctrl Pts',(93.9874288818787,3.09758027434805,126.981668353791));
#48208=CARTESIAN_POINT('Ctrl Pts',(93.9796808138758,2.98869672472144,126.898355631632));
#48209=CARTESIAN_POINT('Ctrl Pts',(93.9719245111339,2.87969745236249,126.814954363721));
#48210=CARTESIAN_POINT('Ctrl Pts',(93.964168208392,2.76726223949295,126.736163240068));
#48211=CARTESIAN_POINT('Ctrl Pts',(93.9564119056502,2.65182646366289,126.662259765448));
#48212=CARTESIAN_POINT('Ctrl Pts',(93.948651463136,2.53632907628349,126.588316846318));
#48213=CARTESIAN_POINT('Ctrl Pts',(93.9408910206219,2.41782827247352,126.519266970985));
#48214=CARTESIAN_POINT('Ctrl Pts',(93.9331305781077,2.29678437116164,126.455341806973));
#48215=CARTESIAN_POINT('Ctrl Pts',(93.9253576778423,2.17554615943368,126.391314024613));
#48216=CARTESIAN_POINT('Ctrl Pts',(93.9175847775768,2.05175704551348,126.33242756107));
#48217=CARTESIAN_POINT('Ctrl Pts',(93.9098118773114,1.925898499132,126.278866386707));
#48218=CARTESIAN_POINT('Ctrl Pts',(93.9023215415494,1.8046152279297,126.227252295944));
#48219=CARTESIAN_POINT('Ctrl Pts',(93.8948312057873,1.68141065830259,126.180583150053));
#48220=CARTESIAN_POINT('Ctrl Pts',(93.8873408700253,1.55672735322792,126.138979281575));
#48221=CARTESIAN_POINT('Ctrl Pts',(93.8795665359062,1.42731664274494,126.095797989779));
#48222=CARTESIAN_POINT('Ctrl Pts',(93.8717922017871,1.29590291654227,126.057936872284));
#48223=CARTESIAN_POINT('Ctrl Pts',(93.864017867668,1.16296304920575,126.025584622745));
#48224=CARTESIAN_POINT('Ctrl Pts',(93.8562531147209,1.03018701837464,125.993272244461));
#48225=CARTESIAN_POINT('Ctrl Pts',(93.8484883617738,0.895888964937103,125.966455317233));
#48226=CARTESIAN_POINT('Ctrl Pts',(93.8407236088267,0.760563409083274,125.945273628916));
#48227=CARTESIAN_POINT('Ctrl Pts',(93.8329665679417,0.625372260479276,125.924112978551));
#48228=CARTESIAN_POINT('Ctrl Pts',(93.8252095270567,0.489156024122194,125.908576488886));
#48229=CARTESIAN_POINT('Ctrl Pts',(93.8174524861717,0.352421627485681,125.898753411625));
#48230=CARTESIAN_POINT('Ctrl Pts',(93.8097012949316,0.215790343321218,125.888937742023));
#48231=CARTESIAN_POINT('Ctrl Pts',(93.8019501036915,0.0786420650212302,
125.884826936862));
#48232=CARTESIAN_POINT('Ctrl Pts',(93.7941989124513,-0.0585092564234095,
125.886458653373));
#48233=CARTESIAN_POINT('Ctrl Pts',(93.7864510156743,-0.195602284897711,
125.888089676361));
#48234=CARTESIAN_POINT('Ctrl Pts',(93.7787031188972,-0.332697963825081,
125.895458361964));
#48235=CARTESIAN_POINT('Ctrl Pts',(93.7709552221201,-0.469280645872262,
125.908550292614));
#48236=CARTESIAN_POINT('Ctrl Pts',(93.763208946036,-0.605834757766741,125.921639484713));
#48237=CARTESIAN_POINT('Ctrl Pts',(93.7554626699519,-0.741875697287455,
125.940449503322));
#48238=CARTESIAN_POINT('Ctrl Pts',(93.7477163938678,-0.876891644963057,
125.964913944082));
#48239=CARTESIAN_POINT('Ctrl Pts',(93.7399700606024,-1.01190858929571,125.989378565433));
#48240=CARTESIAN_POINT('Ctrl Pts',(93.7322237273371,-1.14590014198443,126.019497622516));
#48241=CARTESIAN_POINT('Ctrl Pts',(93.7244773940717,-1.2783637933063,126.05515341273));
#48242=CARTESIAN_POINT('Ctrl Pts',(93.7167293260688,-1.41085710894435,126.090817187811));
#48243=CARTESIAN_POINT('Ctrl Pts',(93.7089812580658,-1.5418214648957,126.132020061705));
#48244=CARTESIAN_POINT('Ctrl Pts',(93.7012331900628,-1.67076903578876,126.178594314395));
#48245=CARTESIAN_POINT('Ctrl Pts',(93.6934768873209,-1.79985365369474,126.225218066755));
#48246=CARTESIAN_POINT('Ctrl Pts',(93.6857205845791,-1.92691683644267,126.277224468759));
#48247=CARTESIAN_POINT('Ctrl Pts',(93.6779642818372,-2.05148977920767,126.334397223051));
#48248=CARTESIAN_POINT('Ctrl Pts',(93.6702038393231,-2.17612921030305,126.391600492163));
#48249=CARTESIAN_POINT('Ctrl Pts',(93.6624433968089,-2.29827540501672,126.453975430271));
#48250=CARTESIAN_POINT('Ctrl Pts',(93.6546829542947,-2.41748464127521,126.521259979979));
#48251=CARTESIAN_POINT('Ctrl Pts',(93.6469100540293,-2.53688524278272,126.588652540819));
#48252=CARTESIAN_POINT('Ctrl Pts',(93.6391371537639,-2.65333913210431,126.660970256323));
#48253=CARTESIAN_POINT('Ctrl Pts',(93.6313642534984,-2.76643128361256,126.737907492845));
#48254=CARTESIAN_POINT('Ctrl Pts',(93.6238739177364,-2.8754122505514,126.812047867027));
#48255=CARTESIAN_POINT('Ctrl Pts',(93.6163835819744,-2.98127140405043,126.890477547477));
#48256=CARTESIAN_POINT('Ctrl Pts',(93.6088932462124,-3.083668288835,126.972889236108));
#48257=CARTESIAN_POINT('Ctrl Pts',(93.601221527421,-3.18854477637049,127.057296573827));
#48258=CARTESIAN_POINT('Ctrl Pts',(93.5935498086296,-3.29013999903654,127.146163892061));
#48259=CARTESIAN_POINT('Ctrl Pts',(93.5858780898382,-3.38804334928593,127.239203492577));
#48260=CARTESIAN_POINT('Ctrl Pts',(93.578215153484,-3.48583462164936,127.332136583135));
#48261=CARTESIAN_POINT('Ctrl Pts',(93.5705522171298,-3.57994213498176,127.429232187488));
#48262=CARTESIAN_POINT('Ctrl Pts',(93.5628892807756,-3.66998626290684,127.530160884414));
#48263=CARTESIAN_POINT('Ctrl Pts',(93.5552333529899,-3.75994803592049,127.630997271334));
#48264=CARTESIAN_POINT('Ctrl Pts',(93.5475774252043,-3.84585354721556,127.735659482425));
#48265=CARTESIAN_POINT('Ctrl Pts',(93.5399214974187,-3.92735854934403,127.843779950299));
#48266=CARTESIAN_POINT('Ctrl Pts',(93.5322708107495,-4.0088077545497,127.95182640076));
#48267=CARTESIAN_POINT('Ctrl Pts',(93.5246201240804,-4.08586220121889,128.06332607961));
#48268=CARTESIAN_POINT('Ctrl Pts',(93.5169694374112,-4.15821699315964,128.177877322302));
#48269=CARTESIAN_POINT('Ctrl Pts',(93.5093213530922,-4.23054717391102,128.292389600854));
#48270=CARTESIAN_POINT('Ctrl Pts',(93.5016732687731,-4.29818066069358,128.409951042302));
#48271=CARTESIAN_POINT('Ctrl Pts',(93.494025184454,-4.36085531655467,128.53013020475));
#48272=CARTESIAN_POINT('Ctrl Pts',(93.4863787967934,-4.42351606860911,128.650282706535));
#48273=CARTESIAN_POINT('Ctrl Pts',(93.4787324091328,-4.48121999544925,128.773051416107));
#48274=CARTESIAN_POINT('Ctrl Pts',(93.4710860214722,-4.53375080004373,128.897980082205));
#48275=CARTESIAN_POINT('Ctrl Pts',(93.4634371328192,-4.58629878649579,129.022949610166));
#48276=CARTESIAN_POINT('Ctrl Pts',(93.4557882441662,-4.63367011290399,129.1500801358));
#48277=CARTESIAN_POINT('Ctrl Pts',(93.4481393555132,-4.67569658534787,129.278895277328));
#48278=CARTESIAN_POINT('Ctrl Pts',(93.4421863234996,-4.70840525025724,129.379150451139));
#48279=CARTESIAN_POINT('Ctrl Pts',(93.4362332914858,-4.73787732419656,129.480425598061));
#48280=CARTESIAN_POINT('Ctrl Pts',(93.4302802594722,-4.76405452823405,129.582490119308));
#48281=CARTESIAN_POINT('Origin',(213.235140564004,0.,130.804360617566));
#48282=CARTESIAN_POINT('',(91.3345773084523,-4.76405452823402,129.582490119308));
#48283=CARTESIAN_POINT('',(91.6801684115835,-4.76405452823408,129.582490119308));
#48284=CARTESIAN_POINT('',(213.235140564004,-4.76405452823405,129.582490119308));
#48285=CARTESIAN_POINT('',(93.0148594359418,-4.91824801126209,130.799937698111));
#48286=CARTESIAN_POINT('Ctrl Pts',(93.0148594359418,-4.91824801126209,130.799937698111));
#48287=CARTESIAN_POINT('Ctrl Pts',(93.0072109324117,-4.91836930348058,130.934813591398));
#48288=CARTESIAN_POINT('Ctrl Pts',(92.9995624288815,-4.91293826055421,131.069867794249));
#48289=CARTESIAN_POINT('Ctrl Pts',(92.9919139253514,-4.90193765537652,131.204598403516));
#48290=CARTESIAN_POINT('Ctrl Pts',(92.9842717249816,-4.89094611583876,131.339217980782));
#48291=CARTESIAN_POINT('Ctrl Pts',(92.9766295246119,-4.87439417693943,131.473514095127));
#48292=CARTESIAN_POINT('Ctrl Pts',(92.9689873242421,-4.85231667526038,131.606985028788));
#48293=CARTESIAN_POINT('Ctrl Pts',(92.9613489341719,-4.8302501811303,131.740389415616));
#48294=CARTESIAN_POINT('Ctrl Pts',(92.9537105441017,-4.80266366750942,131.872969043028));
#48295=CARTESIAN_POINT('Ctrl Pts',(92.9460721540315,-4.76964375173622,132.004227920239));
#48296=CARTESIAN_POINT('Ctrl Pts',(92.9384356206848,-4.73663186237339,132.135454891323));
#48297=CARTESIAN_POINT('Ctrl Pts',(92.9307990873382,-4.69818929472312,132.265361359725));
#48298=CARTESIAN_POINT('Ctrl Pts',(92.9231625539915,-4.65445354555209,132.393462645378));
#48299=CARTESIAN_POINT('Ctrl Pts',(92.9155261128608,-4.61071832451822,132.521562384126));
#48300=CARTESIAN_POINT('Ctrl Pts',(92.9078896717301,-4.5616901795235,132.647856601963));
#48301=CARTESIAN_POINT('Ctrl Pts',(92.9002532305995,-4.50755595806729,132.771877414799));
#48302=CARTESIAN_POINT('Ctrl Pts',(92.8926151174588,-4.45340988384364,132.895925382173));
#48303=CARTESIAN_POINT('Ctrl Pts',(92.8849770043181,-4.39415567179046,133.017698585535));
#48304=CARTESIAN_POINT('Ctrl Pts',(92.8773388911774,-4.33002738554203,133.136751215848));
#48305=CARTESIAN_POINT('Ctrl Pts',(92.8696929113169,-4.26583305166541,133.255926462004));
#48306=CARTESIAN_POINT('Ctrl Pts',(92.8620469314565,-4.19675481207021,133.372375185258));
#48307=CARTESIAN_POINT('Ctrl Pts',(92.854400951596,-4.12307173061472,133.485677936853));
#48308=CARTESIAN_POINT('Ctrl Pts',(92.846750723838,-4.04934771285196,133.599043636361));
#48309=CARTESIAN_POINT('Ctrl Pts',(92.83910049608,-3.97101399334953,133.709259556717));
#48310=CARTESIAN_POINT('Ctrl Pts',(92.831450268322,-3.88839085368846,133.81593821601));
#48311=CARTESIAN_POINT('Ctrl Pts',(92.8237885431259,-3.80564354067381,133.922777201418));
#48312=CARTESIAN_POINT('Ctrl Pts',(92.8161268179297,-3.7185941946397,134.026068003277));
#48313=CARTESIAN_POINT('Ctrl Pts',(92.8084650927336,-3.62760129596635,134.125458613712));
#48314=CARTESIAN_POINT('Ctrl Pts',(92.8033565188001,-3.56693037154647,134.191728842506));
#48315=CARTESIAN_POINT('Ctrl Pts',(92.7982479448665,-3.50450699143506,134.256265915611));
#48316=CARTESIAN_POINT('Ctrl Pts',(92.793139370933,-3.44044546173787,134.318975544881));
#48317=CARTESIAN_POINT('Ctrl Pts',(92.7853650368139,-3.34295529275445,134.414408363662));
#48318=CARTESIAN_POINT('Ctrl Pts',(92.7775907026948,-3.2413369513081,134.50593291957));
#48319=CARTESIAN_POINT('Ctrl Pts',(92.7698163685757,-3.13593675180432,134.593170952115));
#48320=CARTESIAN_POINT('Ctrl Pts',(92.7620516156286,-3.0306664486267,134.680301471581));
#48321=CARTESIAN_POINT('Ctrl Pts',(92.7542868626816,-2.9216238592902,134.763155731905));
#48322=CARTESIAN_POINT('Ctrl Pts',(92.7465221097345,-2.80919255661363,134.841391734905));
#48323=CARTESIAN_POINT('Ctrl Pts',(92.7387650688495,-2.69687292229196,134.919550032805));
#48324=CARTESIAN_POINT('Ctrl Pts',(92.7310080279645,-2.5811715913987,134.99309897969));
#48325=CARTESIAN_POINT('Ctrl Pts',(92.7232509870795,-2.4625053975201,135.061736596932));
#48326=CARTESIAN_POINT('Ctrl Pts',(92.7154997958394,-2.34392869074138,135.130322454014));
#48327=CARTESIAN_POINT('Ctrl Pts',(92.7077486045993,-2.22239190831499,135.194004158428));
#48328=CARTESIAN_POINT('Ctrl Pts',(92.6999974133592,-2.0983407659613,135.252523057541));
#48329=CARTESIAN_POINT('Ctrl Pts',(92.6922495165821,-1.97434234865203,135.311017084561));
#48330=CARTESIAN_POINT('Ctrl Pts',(92.684501619805,-1.84783204977505,135.364352504182));
#48331=CARTESIAN_POINT('Ctrl Pts',(92.6767537230279,-1.71927988664383,135.412316751676));
#48332=CARTESIAN_POINT('Ctrl Pts',(92.6690074469438,-1.59075461385388,135.460270966083));
#48333=CARTESIAN_POINT('Ctrl Pts',(92.6612611708597,-1.46018869242984,135.502856106548));
#48334=CARTESIAN_POINT('Ctrl Pts',(92.6535148947756,-1.32807143497694,135.53990803324));
#48335=CARTESIAN_POINT('Ctrl Pts',(92.6457685615102,-1.19595320226419,135.576960233441));
#48336=CARTESIAN_POINT('Ctrl Pts',(92.6380222282448,-1.06228398711339,135.608479032793));
#48337=CARTESIAN_POINT('Ctrl Pts',(92.6302758949795,-0.927567166517519,
135.634350494791));
#48338=CARTESIAN_POINT('Ctrl Pts',(92.6225278269765,-0.79282017702392,135.660227750524));
#48339=CARTESIAN_POINT('Ctrl Pts',(92.6147797589735,-0.657025499126192,
135.680455078613));
#48340=CARTESIAN_POINT('Ctrl Pts',(92.6070316909705,-0.520695180731654,
135.694969944763));
#48341=CARTESIAN_POINT('Ctrl Pts',(92.5992753882286,-0.384219968852467,
135.709500237485));
#48342=CARTESIAN_POINT('Ctrl Pts',(92.5915190854868,-0.247208368656059,
135.718305898791));
#48343=CARTESIAN_POINT('Ctrl Pts',(92.583762782745,-0.11017656965865,135.721376398098));
#48344=CARTESIAN_POINT('Ctrl Pts',(92.5760023402308,0.0269283673357381,
135.724448536223));
#48345=CARTESIAN_POINT('Ctrl Pts',(92.5682418977166,0.164053133912697,135.721779420596));
#48346=CARTESIAN_POINT('Ctrl Pts',(92.5604814552025,0.300684082777564,135.713410642251));
#48347=CARTESIAN_POINT('Ctrl Pts',(92.552708554937,0.437534363771167,135.705028429601));
#48348=CARTESIAN_POINT('Ctrl Pts',(92.5449356546716,0.573888853830151,135.690928310645));
#48349=CARTESIAN_POINT('Ctrl Pts',(92.5371627544062,0.709240652737029,135.671203614726));
#48350=CARTESIAN_POINT('Ctrl Pts',(92.5296724186441,0.839672072823583,135.652195961187));
#48351=CARTESIAN_POINT('Ctrl Pts',(92.522182082882,0.969172134028587,135.627965622701));
#48352=CARTESIAN_POINT('Ctrl Pts',(92.51469174712,1.09730026779709,135.598640040461));
#48353=CARTESIAN_POINT('Ctrl Pts',(92.5069174130009,1.23028641870085,135.568202569857));
#48354=CARTESIAN_POINT('Ctrl Pts',(92.4991430788818,1.3622158154141,135.532179439297));
#48355=CARTESIAN_POINT('Ctrl Pts',(92.4913687447627,1.4925830252785,135.490657553863));
#48356=CARTESIAN_POINT('Ctrl Pts',(92.4836039918156,1.62278956920763,135.449186840443));
#48357=CARTESIAN_POINT('Ctrl Pts',(92.4758392388686,1.75143738802246,135.40223097332));
#48358=CARTESIAN_POINT('Ctrl Pts',(92.4680744859215,1.8780314184895,135.349927804801));
#48359=CARTESIAN_POINT('Ctrl Pts',(92.4603174450365,2.00449971398099,135.297676584526));
#48360=CARTESIAN_POINT('Ctrl Pts',(92.4525604041514,2.12891792151989,135.240088780337));
#48361=CARTESIAN_POINT('Ctrl Pts',(92.4448033632664,2.25080666919891,135.177351859312));
#48362=CARTESIAN_POINT('Ctrl Pts',(92.4370521720263,2.37260349962482,135.114662248688));
#48363=CARTESIAN_POINT('Ctrl Pts',(92.4293009807862,2.49187432071027,135.04683142828));
#48364=CARTESIAN_POINT('Ctrl Pts',(92.4215497895461,2.60816060043538,134.974094583281));
#48365=CARTESIAN_POINT('Ctrl Pts',(92.4138018927691,2.72439745538974,134.901388653382));
#48366=CARTESIAN_POINT('Ctrl Pts',(92.406053995992,2.83765196118316,134.823781053074));
#48367=CARTESIAN_POINT('Ctrl Pts',(92.3983060992149,2.947491225251,134.741552324807));
#48368=CARTESIAN_POINT('Ctrl Pts',(92.3905598231308,3.05730751331267,134.659340797018));
#48369=CARTESIAN_POINT('Ctrl Pts',(92.3828135470468,3.16370966783957,134.572510298126));
#48370=CARTESIAN_POINT('Ctrl Pts',(92.3750672709627,3.26629510792696,134.481383779097));
#48371=CARTESIAN_POINT('Ctrl Pts',(92.3673209376973,3.36888130527698,134.390256587391));
#48372=CARTESIAN_POINT('Ctrl Pts',(92.3595746044319,3.4676504396714,134.294833571915));
#48373=CARTESIAN_POINT('Ctrl Pts',(92.3518282711666,3.56223456554194,134.195476652525));
#48374=CARTESIAN_POINT('Ctrl Pts',(92.3440802031636,3.65683987287185,134.096097482842));
#48375=CARTESIAN_POINT('Ctrl Pts',(92.3363321351606,3.74725803723358,133.992782939333));
#48376=CARTESIAN_POINT('Ctrl Pts',(92.3285840671576,3.83315967235341,133.885930021091));
#48377=CARTESIAN_POINT('Ctrl Pts',(92.3208277644158,3.91915260475304,133.778963538297));
#48378=CARTESIAN_POINT('Ctrl Pts',(92.3130714616739,4.0006191735992,133.668451473707));
#48379=CARTESIAN_POINT('Ctrl Pts',(92.305315158932,4.07727150617325,133.554822420145));
#48380=CARTESIAN_POINT('Ctrl Pts',(92.2975547164179,4.15396475040527,133.441132719336));
#48381=CARTESIAN_POINT('Ctrl Pts',(92.2897942739037,4.22583843362858,133.324323047446));
#48382=CARTESIAN_POINT('Ctrl Pts',(92.2820338313895,4.29264990864926,133.204848031462));
#48383=CARTESIAN_POINT('Ctrl Pts',(92.274260931124,4.35956863538084,133.085181223576));
#48384=CARTESIAN_POINT('Ctrl Pts',(92.2664880308587,4.42140873848766,132.962840870619));
#48385=CARTESIAN_POINT('Ctrl Pts',(92.2587151305932,4.47797474663897,132.83830388889));
#48386=CARTESIAN_POINT('Ctrl Pts',(92.2512247948313,4.53248443791231,132.718294140137));
#48387=CARTESIAN_POINT('Ctrl Pts',(92.2437344590693,4.58209671420049,132.596244981204));
#48388=CARTESIAN_POINT('Ctrl Pts',(92.2362441233073,4.62668065732355,132.472595959971));
#48389=CARTESIAN_POINT('Ctrl Pts',(92.2284697891882,4.67295501420153,132.344258748514));
#48390=CARTESIAN_POINT('Ctrl Pts',(92.2206954550691,4.71395879571134,132.213791428643));
#48391=CARTESIAN_POINT('Ctrl Pts',(92.21292112095,4.74949191886304,132.081666209488));
#48392=CARTESIAN_POINT('Ctrl Pts',(92.2051563680029,4.78498125061609,131.949703822857));
#48393=CARTESIAN_POINT('Ctrl Pts',(92.1973916150559,4.81501323821375,131.816087976252));
#48394=CARTESIAN_POINT('Ctrl Pts',(92.1896268621088,4.83943626693423,131.68130969293));
#48395=CARTESIAN_POINT('Ctrl Pts',(92.1818698212237,4.86383503835838,131.546665273299));
#48396=CARTESIAN_POINT('Ctrl Pts',(92.1741127803387,4.88263586798179,131.410861096765));
#48397=CARTESIAN_POINT('Ctrl Pts',(92.1663557394537,4.8957373649403,131.274401803025));
#48398=CARTESIAN_POINT('Ctrl Pts',(92.1586045482136,4.90882898195795,131.1380454143));
#48399=CARTESIAN_POINT('Ctrl Pts',(92.1508533569735,4.91622978382848,131.001035279306));
#48400=CARTESIAN_POINT('Ctrl Pts',(92.1431021657333,4.91788979075825,130.863884297356));
#48401=CARTESIAN_POINT('Ctrl Pts',(92.1353542689562,4.91954909214079,130.726791608233));
#48402=CARTESIAN_POINT('Ctrl Pts',(92.1276063721792,4.9154724468168,130.589558581337));
#48403=CARTESIAN_POINT('Ctrl Pts',(92.1198584754021,4.90566189408938,130.45270106149));
#48404=CARTESIAN_POINT('Ctrl Pts',(92.112112199318,4.89585339351811,130.315872169287));
#48405=CARTESIAN_POINT('Ctrl Pts',(92.1043659232339,4.88031339917199,130.179419017614));
#48406=CARTESIAN_POINT('Ctrl Pts',(92.0966196471498,4.85909601403103,130.043854872073));
#48407=CARTESIAN_POINT('Ctrl Pts',(92.0888733138844,4.83787847226814,129.908289725828));
#48408=CARTESIAN_POINT('Ctrl Pts',(92.0811269806191,4.8109835165383,129.773613985074));
#48409=CARTESIAN_POINT('Ctrl Pts',(92.0733806473537,4.77851675670007,129.640332839359));
#48410=CARTESIAN_POINT('Ctrl Pts',(92.0656325793508,4.74604272615621,129.507021846257));
#48411=CARTESIAN_POINT('Ctrl Pts',(92.0578845113478,4.70799450110639,129.37510644944));
#48412=CARTESIAN_POINT('Ctrl Pts',(92.0501364433448,4.6645280468046,129.245078358617));
#48413=CARTESIAN_POINT('Ctrl Pts',(92.042380140603,4.62101539583777,129.114912072391));
#48414=CARTESIAN_POINT('Ctrl Pts',(92.0346238378611,4.57207313642727,128.98663747045));
#48415=CARTESIAN_POINT('Ctrl Pts',(92.0268675351193,4.51790625361711,128.860728413154));
#48416=CARTESIAN_POINT('Ctrl Pts',(92.0191070926051,4.46371046031056,128.734752154403));
#48417=CARTESIAN_POINT('Ctrl Pts',(92.0113466500909,4.40428465652239,128.611144308248));
#48418=CARTESIAN_POINT('Ctrl Pts',(92.0035862075767,4.33988017607665,128.490354757635));
#48419=CARTESIAN_POINT('Ctrl Pts',(91.9958133073113,4.27537230784138,128.369371304912));
#48420=CARTESIAN_POINT('Ctrl Pts',(91.9880404070458,4.2058699902978,128.251215525663));
#48421=CARTESIAN_POINT('Ctrl Pts',(91.9802675067804,4.13166880960557,128.136309660363));
#48422=CARTESIAN_POINT('Ctrl Pts',(91.9727771710183,4.06016502873254,128.025580912696));
#48423=CARTESIAN_POINT('Ctrl Pts',(91.9652868352563,3.98429826188994,127.917870147941));
#48424=CARTESIAN_POINT('Ctrl Pts',(91.9577964994942,3.90436754868442,127.813525097635));
#48425=CARTESIAN_POINT('Ctrl Pts',(91.9500221653751,3.82140623819378,127.705223773033));
#48426=CARTESIAN_POINT('Ctrl Pts',(91.942247831256,3.73380393243871,127.600205357129));
#48427=CARTESIAN_POINT('Ctrl Pts',(91.9344734971369,3.64184976459086,127.49889342598));
#48428=CARTESIAN_POINT('Ctrl Pts',(91.9267087441898,3.55000892203682,127.397706352732));
#48429=CARTESIAN_POINT('Ctrl Pts',(91.9189439912427,3.45382714895903,127.300216962177));
#48430=CARTESIAN_POINT('Ctrl Pts',(91.9111792382956,3.35363560566992,127.206818222141));
#48431=CARTESIAN_POINT('Ctrl Pts',(91.9034221974106,3.25354357403432,127.113512247049));
#48432=CARTESIAN_POINT('Ctrl Pts',(91.8956651565256,3.14944998179012,127.024289102003));
#48433=CARTESIAN_POINT('Ctrl Pts',(91.8879081156406,3.04172459236721,126.939506860088));
#48434=CARTESIAN_POINT('Ctrl Pts',(91.8801569244005,2.93408043949786,126.854788553122));
#48435=CARTESIAN_POINT('Ctrl Pts',(91.8724057331603,2.82281024678311,126.774504724283));
#48436=CARTESIAN_POINT('Ctrl Pts',(91.8646545419201,2.70831851564428,126.698974657596));
#48437=CARTESIAN_POINT('Ctrl Pts',(91.8569066451431,2.59387544654557,126.623476693203));
#48438=CARTESIAN_POINT('Ctrl Pts',(91.849158748366,2.47621388800146,126.55272868723));
#48439=CARTESIAN_POINT('Ctrl Pts',(91.8414108515889,2.35576893716289,126.487007750681));
#48440=CARTESIAN_POINT('Ctrl Pts',(91.8336645755048,2.23534918081146,126.421300561535));
#48441=CARTESIAN_POINT('Ctrl Pts',(91.8259182994207,2.11214753322513,126.360618537362));
#48442=CARTESIAN_POINT('Ctrl Pts',(91.8181720233366,1.98662506327313,126.305193592385));
#48443=CARTESIAN_POINT('Ctrl Pts',(91.8104256900712,1.86110166674277,126.249768238274));
#48444=CARTESIAN_POINT('Ctrl Pts',(91.8026793568058,1.73325777131264,126.199600198719));
#48445=CARTESIAN_POINT('Ctrl Pts',(91.7949330235405,1.60357549196744,126.154873688446));
#48446=CARTESIAN_POINT('Ctrl Pts',(91.7871849555375,1.4738641711753,126.110137161981));
#48447=CARTESIAN_POINT('Ctrl Pts',(91.7794368875345,1.34231401677578,126.070844717105));
#48448=CARTESIAN_POINT('Ctrl Pts',(91.7716888195315,1.20942302110151,126.03713091694));
#48449=CARTESIAN_POINT('Ctrl Pts',(91.7639325167897,1.07639078729545,126.003381285347));
#48450=CARTESIAN_POINT('Ctrl Pts',(91.7561762140478,0.942015245064114,125.975222238676));
#48451=CARTESIAN_POINT('Ctrl Pts',(91.748419911306,0.806805865972816,125.952737450302));
#48452=CARTESIAN_POINT('Ctrl Pts',(91.7406594687918,0.671524321564729,125.93024066112));
#48453=CARTESIAN_POINT('Ctrl Pts',(91.7328990262776,0.535408441334497,125.913424212737));
#48454=CARTESIAN_POINT('Ctrl Pts',(91.7251385837635,0.398972576618193,125.90231982361));
#48455=CARTESIAN_POINT('Ctrl Pts',(91.717365683498,0.26231769293964,125.891197608733));
#48456=CARTESIAN_POINT('Ctrl Pts',(91.7095927832326,0.125342189191165,125.885805792091));
#48457=CARTESIAN_POINT('Ctrl Pts',(91.7018198829672,-0.0114389202177289,
125.886123919968));
#48458=CARTESIAN_POINT('Ctrl Pts',(91.6943295472052,-0.143247691767026,
125.886430483095));
#48459=CARTESIAN_POINT('Ctrl Pts',(91.6868392114433,-0.27487564930785,125.892039043366));
#48460=CARTESIAN_POINT('Ctrl Pts',(91.6793488756814,-0.405868598236534,
125.902885967681));
#48461=CARTESIAN_POINT('Ctrl Pts',(91.6715745415623,-0.541828184639833,
125.914144156429));
#48462=CARTESIAN_POINT('Ctrl Pts',(91.6638002074432,-0.677534338281038,
125.931081438273));
#48463=CARTESIAN_POINT('Ctrl Pts',(91.6560258733241,-0.812474409086707,
125.953683510493));
#48464=CARTESIAN_POINT('Ctrl Pts',(91.648261120377,-0.947248178315323,125.976257727679));
#48465=CARTESIAN_POINT('Ctrl Pts',(91.6404963674299,-1.08125736135097,126.004482780474));
#48466=CARTESIAN_POINT('Ctrl Pts',(91.6327316144828,-1.21399234299605,126.038292463034));
#48467=CARTESIAN_POINT('Ctrl Pts',(91.6249745735978,-1.34659549038584,126.07206856534));
#48468=CARTESIAN_POINT('Ctrl Pts',(91.6172175327129,-1.47792657847998,126.111418163285));
#48469=CARTESIAN_POINT('Ctrl Pts',(91.6094604918279,-1.60748448408262,126.156223711672));
#48470=CARTESIAN_POINT('Ctrl Pts',(91.6017093005877,-1.73694468906136,126.200995471847));
#48471=CARTESIAN_POINT('Ctrl Pts',(91.5939581093476,-1.86463400510768,126.251214865784));
#48472=CARTESIAN_POINT('Ctrl Pts',(91.5862069181074,-1.99006516663053,126.306714155797));
#48473=CARTESIAN_POINT('Ctrl Pts',(91.5784590213303,-2.11544301656323,126.362189857131));
#48474=CARTESIAN_POINT('Ctrl Pts',(91.5707111245532,-2.23856426411182,126.422940833338));
#48475=CARTESIAN_POINT('Ctrl Pts',(91.5629632277762,-2.35896058730359,126.488750810129));
#48476=CARTESIAN_POINT('Ctrl Pts',(91.5552169516921,-2.47933172617984,126.554547020891));
#48477=CARTESIAN_POINT('Ctrl Pts',(91.547470675608,-2.5969787316091,126.62539993995));
#48478=CARTESIAN_POINT('Ctrl Pts',(91.5397243995239,-2.71145726859929,126.701047012312));
#48479=CARTESIAN_POINT('Ctrl Pts',(91.5319780662586,-2.82593665064412,126.776694643084));
#48480=CARTESIAN_POINT('Ctrl Pts',(91.5242317329932,-2.93724719139532,126.857136282234));
#48481=CARTESIAN_POINT('Ctrl Pts',(91.5164853997279,-3.04497331086037,126.942065885331));
#48482=CARTESIAN_POINT('Ctrl Pts',(91.5087373317249,-3.15272355484296,127.027014507824));
#48483=CARTESIAN_POINT('Ctrl Pts',(91.500989263722,-3.25688747328116,127.116452852188));
#48484=CARTESIAN_POINT('Ctrl Pts',(91.493241195719,-3.35708267738909,127.210034678023));
#48485=CARTESIAN_POINT('Ctrl Pts',(91.4854848929772,-3.45738437015242,127.303715963736));
#48486=CARTESIAN_POINT('Ctrl Pts',(91.4777285902353,-3.55370863650405,127.401549260579));
#48487=CARTESIAN_POINT('Ctrl Pts',(91.4699722874934,-3.64570969783685,127.5031511632));
#48488=CARTESIAN_POINT('Ctrl Pts',(91.4622118449793,-3.73775986290624,127.604807293815));
#48489=CARTESIAN_POINT('Ctrl Pts',(91.4544514024651,-3.82548197527734,127.710235737739));
#48490=CARTESIAN_POINT('Ctrl Pts',(91.4466909599509,-3.90857132985244,127.819020901226));
#48491=CARTESIAN_POINT('Ctrl Pts',(91.4389180596855,-3.99179406683566,127.927980696316));
#48492=CARTESIAN_POINT('Ctrl Pts',(91.4311451594201,-4.07036896046935,128.040307658369));
#48493=CARTESIAN_POINT('Ctrl Pts',(91.4233722591547,-4.14403484117663,128.155557435445));
#48494=CARTESIAN_POINT('Ctrl Pts',(91.4158819233926,-4.21502278156739,128.266617592828));
#48495=CARTESIAN_POINT('Ctrl Pts',(91.4083915876306,-4.28145226721218,128.380391485229));
#48496=CARTESIAN_POINT('Ctrl Pts',(91.4009012518685,-4.34313133116246,128.496462590621));
#48497=CARTESIAN_POINT('Ctrl Pts',(91.3926828135285,-4.41080594549865,128.623816457394));
#48498=CARTESIAN_POINT('Ctrl Pts',(91.3844643751885,-4.47295643192316,128.754301941354));
#48499=CARTESIAN_POINT('Ctrl Pts',(91.3762459368485,-4.5292989044717,128.887426999401));
#48500=CARTESIAN_POINT('Ctrl Pts',(91.3680463489467,-4.58551214561941,129.020246711641));
#48501=CARTESIAN_POINT('Ctrl Pts',(91.3598467610449,-4.6359438082404,129.155693628935));
#48502=CARTESIAN_POINT('Ctrl Pts',(91.3516471731431,-4.68035617042155,129.293252024348));
#48503=CARTESIAN_POINT('Ctrl Pts',(91.3459572182461,-4.71117532142097,129.388708171044));
#48504=CARTESIAN_POINT('Ctrl Pts',(91.3402672633492,-4.73909685092036,129.485180514248));
#48505=CARTESIAN_POINT('Ctrl Pts',(91.3345773084523,-4.76405452823403,129.582490119308));
#48506=CARTESIAN_POINT('Ctrl Pts',(93.084857876857,-4.76405452823403,129.582490119308));
#48507=CARTESIAN_POINT('Ctrl Pts',(93.0804342494867,-4.78337272363488,129.657811469982));
#48508=CARTESIAN_POINT('Ctrl Pts',(93.0760106221163,-4.80088849673471,129.733529841816));
#48509=CARTESIAN_POINT('Ctrl Pts',(93.0715869947459,-4.81658988703912,129.809551629583));
#48510=CARTESIAN_POINT('Ctrl Pts',(93.0605294465413,-4.855837966869,129.999579973393));
#48511=CARTESIAN_POINT('Ctrl Pts',(93.0494718983367,-4.88385096599703,130.192001803521));
#48512=CARTESIAN_POINT('Ctrl Pts',(93.0384143501322,-4.90040027604376,130.385719724855));
#48513=CARTESIAN_POINT('Ctrl Pts',(93.0305627120851,-4.91215145180274,130.523273093232));
#48514=CARTESIAN_POINT('Ctrl Pts',(93.022711074038,-4.9181234976515,130.661479671936));
#48515=CARTESIAN_POINT('Ctrl Pts',(93.014859435991,-4.91824801126131,130.799937697244));
#48516=CARTESIAN_POINT('',(93.3601405640463,-4.91824910373096,130.807329817729));
#48517=CARTESIAN_POINT('Ctrl Pts',(93.4302802594722,-4.76405452823405,129.582490119308));
#48518=CARTESIAN_POINT('Ctrl Pts',(93.4226245287869,-4.79771899093888,129.713747348465));
#48519=CARTESIAN_POINT('Ctrl Pts',(93.4149687981016,-4.82593248599096,129.846310103717));
#48520=CARTESIAN_POINT('Ctrl Pts',(93.4073130674163,-4.84861679233564,129.979679913547));
#48521=CARTESIAN_POINT('Ctrl Pts',(93.3994509835213,-4.87191253338415,130.116644584464));
#48522=CARTESIAN_POINT('Ctrl Pts',(93.3915888996263,-4.88937673586048,130.25445997831));
#48523=CARTESIAN_POINT('Ctrl Pts',(93.3837268157313,-4.90098172523436,130.392582532405));
#48524=CARTESIAN_POINT('Ctrl Pts',(93.3758647318363,-4.91258671460823,130.5307050865));
#48525=CARTESIAN_POINT('Ctrl Pts',(93.3680026479413,-4.9183325338315,130.669134345982));
#48526=CARTESIAN_POINT('Ctrl Pts',(93.3601405640462,-4.91824910373096,130.807329817729));
#48527=CARTESIAN_POINT('Ctrl Pts',(93.3601405640084,-4.91824910373056,130.807329818395));
#48528=CARTESIAN_POINT('Ctrl Pts',(93.3502422501388,-4.9181440657384,130.981317042771));
#48529=CARTESIAN_POINT('Ctrl Pts',(93.3403439362691,-4.90880728885546,131.155023738731));
#48530=CARTESIAN_POINT('Ctrl Pts',(93.3304456223994,-4.89032341902961,131.32773421242));
#48531=CARTESIAN_POINT('Ctrl Pts',(93.3226712882803,-4.87580581717025,131.463384480334));
#48532=CARTESIAN_POINT('Ctrl Pts',(93.3148969541612,-4.85561683933991,131.598645105893));
#48533=CARTESIAN_POINT('Ctrl Pts',(93.3071226200421,-4.82978308632962,131.733003929879));
#48534=CARTESIAN_POINT('Ctrl Pts',(93.299357867095,-4.8039811711111,131.867197168623));
#48535=CARTESIAN_POINT('Ctrl Pts',(93.291593114148,-4.77254839554594,132.000490436883));
#48536=CARTESIAN_POINT('Ctrl Pts',(93.2838283612009,-4.73556317577024,132.132375854974));
#48537=CARTESIAN_POINT('Ctrl Pts',(93.2760713203159,-4.69861469023621,132.26413028261));
#48538=CARTESIAN_POINT('Ctrl Pts',(93.2683142794309,-4.65612484000902,132.394479268743));
#48539=CARTESIAN_POINT('Ctrl Pts',(93.2605572385459,-4.60822316200892,132.522924655251));
#48540=CARTESIAN_POINT('Ctrl Pts',(93.2528060473058,-4.56035760703691,132.651273180094));
#48541=CARTESIAN_POINT('Ctrl Pts',(93.2450548560657,-4.5070884835375,132.777720597787));
#48542=CARTESIAN_POINT('Ctrl Pts',(93.2373036648256,-4.44859517392466,132.901783808301));
#48543=CARTESIAN_POINT('Ctrl Pts',(93.2295557680485,-4.3901267255287,133.025794288642));
#48544=CARTESIAN_POINT('Ctrl Pts',(93.2218078712715,-4.32643867364319,133.147422224393));
#48545=CARTESIAN_POINT('Ctrl Pts',(93.2140599744944,-4.25775846871242,133.266204618434));
#48546=CARTESIAN_POINT('Ctrl Pts',(93.2063136984103,-4.18909263019994,133.384962165758));
#48547=CARTESIAN_POINT('Ctrl Pts',(93.1985674223262,-4.11543691128902,133.500875017062));
#48548=CARTESIAN_POINT('Ctrl Pts',(93.1908211462421,-4.03706445417912,133.613505265907));
#48549=CARTESIAN_POINT('Ctrl Pts',(93.1830748129768,-3.95869141854148,133.726136346163));
#48550=CARTESIAN_POINT('Ctrl Pts',(93.1753284797114,-3.8756017985349,133.835484454692));
#48551=CARTESIAN_POINT('Ctrl Pts',(93.1675821464461,-3.78811152323129,133.941141475398));
#48552=CARTESIAN_POINT('Ctrl Pts',(93.1598340784431,-3.7006016550872,134.046822157262));
#48553=CARTESIAN_POINT('Ctrl Pts',(93.1520860104401,-3.60868941992628,134.148809805409));
#48554=CARTESIAN_POINT('Ctrl Pts',(93.1443379424372,-3.5127301347151,134.246730449987));
#48555=CARTESIAN_POINT('Ctrl Pts',(93.1365816396953,-3.41666886283366,134.344755165792));
#48556=CARTESIAN_POINT('Ctrl Pts',(93.1288253369535,-3.31655222276564,134.438703963766));
#48557=CARTESIAN_POINT('Ctrl Pts',(93.1210690342116,-3.21277180718587,134.528240365551));
#48558=CARTESIAN_POINT('Ctrl Pts',(93.1133085916975,-3.10893600087347,134.617824555609));
#48559=CARTESIAN_POINT('Ctrl Pts',(93.1055481491833,-3.00143282891633,134.702991414223));
#48560=CARTESIAN_POINT('Ctrl Pts',(93.0977877066691,-2.89068507746093,134.783446297147));
#48561=CARTESIAN_POINT('Ctrl Pts',(93.0900148064037,-2.77975954388325,134.864030333391));
#48562=CARTESIAN_POINT('Ctrl Pts',(93.0822419061383,-2.66557934842697,134.939887062027));
#48563=CARTESIAN_POINT('Ctrl Pts',(93.0744690058728,-2.54859498242178,135.01076605191));
#48564=CARTESIAN_POINT('Ctrl Pts',(93.0669786701108,-2.43586329278592,135.079068411977));
#48565=CARTESIAN_POINT('Ctrl Pts',(93.0594883343487,-2.32052803996489,135.142748507863));
#48566=CARTESIAN_POINT('Ctrl Pts',(93.0519979985866,-2.20301023271641,135.201624423281));
#48567=CARTESIAN_POINT('Ctrl Pts',(93.0442236644676,-2.0810367020881,135.262732636926));
#48568=CARTESIAN_POINT('Ctrl Pts',(93.0364493303484,-1.95632547136498,135.318858750135));
#48569=CARTESIAN_POINT('Ctrl Pts',(93.0286749962294,-1.82932181297873,135.369748308339));
#48570=CARTESIAN_POINT('Ctrl Pts',(93.0209102432823,-1.70247467525088,135.420575149711));
#48571=CARTESIAN_POINT('Ctrl Pts',(93.0131454903352,-1.57334109062139,135.466178132769));
#48572=CARTESIAN_POINT('Ctrl Pts',(93.0053807373881,-1.44239073848878,135.506348709854));
#48573=CARTESIAN_POINT('Ctrl Pts',(92.9976236965031,-1.31157044809198,135.546479388957));
#48574=CARTESIAN_POINT('Ctrl Pts',(92.9898666556181,-1.17893735246257,135.581188285542));
#48575=CARTESIAN_POINT('Ctrl Pts',(92.9821096147331,-1.04498058400846,135.610315116055));
#48576=CARTESIAN_POINT('Ctrl Pts',(92.974358423493,-0.911124833395652,135.639419981798));
#48577=CARTESIAN_POINT('Ctrl Pts',(92.9666072322529,-0.775947777291451,
135.662951077451));
#48578=CARTESIAN_POINT('Ctrl Pts',(92.9588560410128,-0.639952822008436,
135.680798195153));
#48579=CARTESIAN_POINT('Ctrl Pts',(92.9511081442357,-0.504015668209016,
135.698637727354));
#48580=CARTESIAN_POINT('Ctrl Pts',(92.9433602474586,-0.367261693468156,
135.710798035764));
#48581=CARTESIAN_POINT('Ctrl Pts',(92.9356123506815,-0.230203372897379,
135.717220219631));
#48582=CARTESIAN_POINT('Ctrl Pts',(92.9278660745974,-0.0931737219726303,
135.723641060116));
#48583=CARTESIAN_POINT('Ctrl Pts',(92.9201197985133,0.0441597578643789,
135.724326145217));
#48584=CARTESIAN_POINT('Ctrl Pts',(92.9123735224292,0.181281003493984,135.719268578075));
#48585=CARTESIAN_POINT('Ctrl Pts',(92.9046271891639,0.318403261321476,135.714210973599));
#48586=CARTESIAN_POINT('Ctrl Pts',(92.8968808558986,0.45531289111586,135.703410646702));
#48587=CARTESIAN_POINT('Ctrl Pts',(92.8891345226332,0.591495765869051,135.686912800744));
#48588=CARTESIAN_POINT('Ctrl Pts',(92.8813864546302,0.727709137832818,135.670411260208));
#48589=CARTESIAN_POINT('Ctrl Pts',(92.8736383866273,0.863195042845044,135.648209708688));
#48590=CARTESIAN_POINT('Ctrl Pts',(92.8658903186243,0.997446791977944,135.620404944571));
#48591=CARTESIAN_POINT('Ctrl Pts',(92.8581340158824,1.13184122546744,135.592570629219));
#48592=CARTESIAN_POINT('Ctrl Pts',(92.8503777131406,1.26499849941334,135.559121284612));
#48593=CARTESIAN_POINT('Ctrl Pts',(92.8426214103987,1.3964238596358,135.520204493983));
#48594=CARTESIAN_POINT('Ctrl Pts',(92.8348609678846,1.52791936553024,135.481266932291));
#48595=CARTESIAN_POINT('Ctrl Pts',(92.8271005253704,1.65768074608685,135.436856236473));
#48596=CARTESIAN_POINT('Ctrl Pts',(92.8193400828562,1.78523158251724,135.387168846074));
#48597=CARTESIAN_POINT('Ctrl Pts',(92.8115671825908,1.9129871748737,135.337401693066));
#48598=CARTESIAN_POINT('Ctrl Pts',(92.8037942823254,2.03852477369988,135.282341075608));
#48599=CARTESIAN_POINT('Ctrl Pts',(92.7960213820599,2.16139018261328,135.222230640666));
#48600=CARTESIAN_POINT('Ctrl Pts',(92.7885310462979,2.2797891244343,135.164305371442));
#48601=CARTESIAN_POINT('Ctrl Pts',(92.7810407105358,2.39570651398725,135.101691204079));
#48602=CARTESIAN_POINT('Ctrl Pts',(92.7735503747737,2.50876173443079,135.03464401497));
#48603=CARTESIAN_POINT('Ctrl Pts',(92.7657760406546,2.62610347791886,134.965054711309));
#48604=CARTESIAN_POINT('Ctrl Pts',(92.7580017065355,2.74073343298251,134.890469156042));
#48605=CARTESIAN_POINT('Ctrl Pts',(92.7502273724164,2.85219683916137,134.811124430567));
#48606=CARTESIAN_POINT('Ctrl Pts',(92.7424626194694,2.96352287665397,134.731877490375));
#48607=CARTESIAN_POINT('Ctrl Pts',(92.7346978665223,3.07168981459971,134.647883274631));
#48608=CARTESIAN_POINT('Ctrl Pts',(92.7269331135752,3.1762683227598,134.559424212811));
#48609=CARTESIAN_POINT('Ctrl Pts',(92.7191760726902,3.28074296207123,134.471053009778));
#48610=CARTESIAN_POINT('Ctrl Pts',(92.7114190318052,3.38163596770642,134.378226036477));
#48611=CARTESIAN_POINT('Ctrl Pts',(92.7036619909202,3.4785481005572,134.281268176678));
#48612=CARTESIAN_POINT('Ctrl Pts',(92.69591079968,3.5753871512148,134.184383433556));
#48613=CARTESIAN_POINT('Ctrl Pts',(92.6881596084399,3.66825102913052,134.083374279821));
#48614=CARTESIAN_POINT('Ctrl Pts',(92.6804084171998,3.7567749099017,133.978604675422));
#48615=CARTESIAN_POINT('Ctrl Pts',(92.6726605204227,3.84526116566209,133.873879600899));
#48616=CARTESIAN_POINT('Ctrl Pts',(92.6649126236457,3.92941084127455,133.765397552604));
#48617=CARTESIAN_POINT('Ctrl Pts',(92.6571647268686,4.00889737655199,133.653557853065));
#48618=CARTESIAN_POINT('Ctrl Pts',(92.6494184507845,4.08836728495977,133.54174154798));
#48619=CARTESIAN_POINT('Ctrl Pts',(92.6416721747004,4.16317576686614,133.426569307138));
#48620=CARTESIAN_POINT('Ctrl Pts',(92.6339258986163,4.23303807502707,133.308471581136));
#48621=CARTESIAN_POINT('Ctrl Pts',(92.6261795653509,4.30290089889565,133.190372983363));
#48622=CARTESIAN_POINT('Ctrl Pts',(92.6184332320856,4.36781727710403,133.069349193835));
#48623=CARTESIAN_POINT('Ctrl Pts',(92.6106868988202,4.4275473423119,132.945857195683));
#48624=CARTESIAN_POINT('Ctrl Pts',(92.6029388308173,4.48729078365374,132.822337542354));
#48625=CARTESIAN_POINT('Ctrl Pts',(92.5951907628143,4.54184543066538,132.696348932408));
#48626=CARTESIAN_POINT('Ctrl Pts',(92.5874426948113,4.59101884482935,132.56836997948));
#48627=CARTESIAN_POINT('Ctrl Pts',(92.5796863920694,4.64024452108309,132.440255008999));
#48628=CARTESIAN_POINT('Ctrl Pts',(92.5719300893276,4.68407739924502,132.310145835412));
#48629=CARTESIAN_POINT('Ctrl Pts',(92.5641737865857,4.72237421855145,132.178538481767));
#48630=CARTESIAN_POINT('Ctrl Pts',(92.5564133440716,4.76069147802347,132.046860885315));
#48631=CARTESIAN_POINT('Ctrl Pts',(92.5486529015574,4.7934666976438,131.913683894938));
#48632=CARTESIAN_POINT('Ctrl Pts',(92.5408924590433,4.82060763157436,131.779514515629));
#48633=CARTESIAN_POINT('Ctrl Pts',(92.5331195587778,4.84779213454149,131.645129755721));
#48634=CARTESIAN_POINT('Ctrl Pts',(92.5253466585124,4.86932421626879,131.509749809753));
#48635=CARTESIAN_POINT('Ctrl Pts',(92.517573758247,4.88516335960771,131.37388850314));
#48636=CARTESIAN_POINT('Ctrl Pts',(92.5100834224849,4.9004267101899,131.242966097236));
#48637=CARTESIAN_POINT('Ctrl Pts',(92.5025930867229,4.91040381835462,131.111597027558));
#48638=CARTESIAN_POINT('Ctrl Pts',(92.4951027509609,4.91510422745994,130.980239825278));
#48639=CARTESIAN_POINT('Ctrl Pts',(92.4873284168418,4.91998285400513,130.843902174749));
#48640=CARTESIAN_POINT('Ctrl Pts',(92.4795540827227,4.91919220469049,130.707145432589));
#48641=CARTESIAN_POINT('Ctrl Pts',(92.4717797486036,4.91268593367374,130.570480349941));
#48642=CARTESIAN_POINT('Ctrl Pts',(92.4640149956565,4.90618768105453,130.433983694794));
#48643=CARTESIAN_POINT('Ctrl Pts',(92.4562502427094,4.89398784059295,130.29757886117));
#48644=CARTESIAN_POINT('Ctrl Pts',(92.4484854897623,4.87609196472543,130.161779716792));
#48645=CARTESIAN_POINT('Ctrl Pts',(92.4407284488774,4.85821386329412,130.026115450037));
#48646=CARTESIAN_POINT('Ctrl Pts',(92.4329714079923,4.83465103565366,129.891056060464));
#48647=CARTESIAN_POINT('Ctrl Pts',(92.4252143671073,4.80546101723211,129.757113046854));
#48648=CARTESIAN_POINT('Ctrl Pts',(92.4174631758672,4.77629301123049,129.623271040712));
#48649=CARTESIAN_POINT('Ctrl Pts',(92.4097119846271,4.74150634380554,129.490544115301));
#48650=CARTESIAN_POINT('Ctrl Pts',(92.401960793387,4.70121002826787,129.359435936964));
#48651=CARTESIAN_POINT('Ctrl Pts',(92.3942128966099,4.66093083973923,129.2283834831));
#48652=CARTESIAN_POINT('Ctrl Pts',(92.3864649998328,4.61514677527553,129.098948780839));
#48653=CARTESIAN_POINT('Ctrl Pts',(92.3787171030557,4.56401728247269,128.971622418098));
#48654=CARTESIAN_POINT('Ctrl Pts',(92.3709708269716,4.51289848485752,128.844322689286));
#48655=CARTESIAN_POINT('Ctrl Pts',(92.3632245508875,4.45643662855871,128.719130785358));
#48656=CARTESIAN_POINT('Ctrl Pts',(92.3554782748034,4.39483995101448,128.596518941298));
#48657=CARTESIAN_POINT('Ctrl Pts',(92.347731941538,4.33324281877761,128.473906192144));
#48658=CARTESIAN_POINT('Ctrl Pts',(92.3399856082727,4.26651096516788,128.35387389022));
#48659=CARTESIAN_POINT('Ctrl Pts',(92.3322392750073,4.19489920888033,128.236870853256));
#48660=CARTESIAN_POINT('Ctrl Pts',(92.3244912070044,4.12327141563648,128.119841614274));
#48661=CARTESIAN_POINT('Ctrl Pts',(92.3167431390014,4.04676174918654,128.005843323556));
#48662=CARTESIAN_POINT('Ctrl Pts',(92.3089950709984,3.96566886301975,127.89529658744));
#48663=CARTESIAN_POINT('Ctrl Pts',(92.3012387682566,3.88448979036846,127.784632360936));
#48664=CARTESIAN_POINT('Ctrl Pts',(92.2934824655147,3.79871799907069,127.67742733271));
#48665=CARTESIAN_POINT('Ctrl Pts',(92.2857261627728,3.70869337142207,127.574070144672));
#48666=CARTESIAN_POINT('Ctrl Pts',(92.2779657202587,3.61862069491903,127.47065779179));
#48667=CARTESIAN_POINT('Ctrl Pts',(92.2702052777445,3.52429092793046,127.371097654954));
#48668=CARTESIAN_POINT('Ctrl Pts',(92.2624448352304,3.4260807669873,127.275741391781));
#48669=CARTESIAN_POINT('Ctrl Pts',(92.2546719349649,3.32771295037511,127.180232054269));
#48670=CARTESIAN_POINT('Ctrl Pts',(92.2468990346995,3.2254525837968,127.088940336457));
#48671=CARTESIAN_POINT('Ctrl Pts',(92.2391261344341,3.11971006261793,127.002178061757));
#48672=CARTESIAN_POINT('Ctrl Pts',(92.231635798672,3.01781154843319,126.918569814283));
#48673=CARTESIAN_POINT('Ctrl Pts',(92.22414546291,2.9126799002159,126.839167599589));
#48674=CARTESIAN_POINT('Ctrl Pts',(92.2166551271479,2.80470605164371,126.764211235876));
#48675=CARTESIAN_POINT('Ctrl Pts',(92.2088807930288,2.69263834178503,126.68641287885));
#48676=CARTESIAN_POINT('Ctrl Pts',(92.2011064589097,2.57715365618677,126.613157714904));
#48677=CARTESIAN_POINT('Ctrl Pts',(92.1933321247906,2.45865665318967,126.544760809576));
#48678=CARTESIAN_POINT('Ctrl Pts',(92.1855673718435,2.34030568715847,126.476448197321));
#48679=CARTESIAN_POINT('Ctrl Pts',(92.1778026188965,2.21895012567846,126.412982124173));
#48680=CARTESIAN_POINT('Ctrl Pts',(92.1700378659494,2.09502530144347,126.354635676762));
#48681=CARTESIAN_POINT('Ctrl Pts',(92.1622808250644,1.97122356109095,126.296347179866));
#48682=CARTESIAN_POINT('Ctrl Pts',(92.1545237841794,1.84485798766824,126.24316835502));
#48683=CARTESIAN_POINT('Ctrl Pts',(92.1467667432944,1.71639001889204,126.195327273626));
#48684=CARTESIAN_POINT('Ctrl Pts',(92.1390155520542,1.58801892881042,126.147522269564));
#48685=CARTESIAN_POINT('Ctrl Pts',(92.1312643608141,1.45754896398517,126.105047132858));
#48686=CARTESIAN_POINT('Ctrl Pts',(92.123513169574,1.32546279753335,126.068082391484));
#48687=CARTESIAN_POINT('Ctrl Pts',(92.1157652727969,1.19343277122579,126.031133361112));
#48688=CARTESIAN_POINT('Ctrl Pts',(92.1080173760198,1.05978828525221,125.999690173027));
#48689=CARTESIAN_POINT('Ctrl Pts',(92.1002694792428,0.925028270440346,125.973883854203));
#48690=CARTESIAN_POINT('Ctrl Pts',(92.0925232031587,0.790296444518492,125.948082933505));
#48691=CARTESIAN_POINT('Ctrl Pts',(92.0847769270745,0.654449937638121,125.927916610237));
#48692=CARTESIAN_POINT('Ctrl Pts',(92.0770306509904,0.517998611886916,125.913464942888));
#48693=CARTESIAN_POINT('Ctrl Pts',(92.069284317725,0.381546278883022,125.89901316886));
#48694=CARTESIAN_POINT('Ctrl Pts',(92.0615379844597,0.244489506890172,125.890276176104));
#48695=CARTESIAN_POINT('Ctrl Pts',(92.0537916511944,0.1073436347066,125.887282175382));
#48696=CARTESIAN_POINT('Ctrl Pts',(92.0460435831914,-0.0298329503441449,
125.884287504175));
#48697=CARTESIAN_POINT('Ctrl Pts',(92.0382955151884,-0.167098284493242,
125.887038392729));
#48698=CARTESIAN_POINT('Ctrl Pts',(92.0305474471855,-0.303937070211306,
125.895510923406));
#48699=CARTESIAN_POINT('Ctrl Pts',(92.0227911444436,-0.440921289819233,
125.90399245879));
#48700=CARTESIAN_POINT('Ctrl Pts',(92.0150348417018,-0.57747766455898,125.918207759607));
#48701=CARTESIAN_POINT('Ctrl Pts',(92.0072785389599,-0.713095504301106,
125.938080943704));
#48702=CARTESIAN_POINT('Ctrl Pts',(91.9995180964457,-0.848785727367769,
125.957964734717));
#48703=CARTESIAN_POINT('Ctrl Pts',(91.9917576539316,-0.983536033368037,
125.98351235339));
#48704=CARTESIAN_POINT('Ctrl Pts',(91.9839972114174,-1.11684694911122,126.014596953797));
#48705=CARTESIAN_POINT('Ctrl Pts',(91.976224311152,-1.25037186737114,126.045731453964));
#48706=CARTESIAN_POINT('Ctrl Pts',(91.9684514108865,-1.38245240106622,126.082420593129));
#48707=CARTESIAN_POINT('Ctrl Pts',(91.9606785106211,-1.51260437560883,126.124487642218));
#48708=CARTESIAN_POINT('Ctrl Pts',(91.9531881748591,-1.63802499804342,126.165025448113));
#48709=CARTESIAN_POINT('Ctrl Pts',(91.9456978390971,-1.76165455389711,126.210556844692));
#48710=CARTESIAN_POINT('Ctrl Pts',(91.9382075033351,-1.88307996812429,126.260882555976));
#48711=CARTESIAN_POINT('Ctrl Pts',(91.9304327771396,-2.00911561976703,126.313119016164));
#48712=CARTESIAN_POINT('Ctrl Pts',(91.9226580509441,-2.13317571388074,126.37068651974));
#48713=CARTESIAN_POINT('Ctrl Pts',(91.9148833247487,-2.25477637635929,126.433414889796));
#48714=CARTESIAN_POINT('Ctrl Pts',(91.9071182694565,-2.37622578100307,126.496065232666));
#48715=CARTESIAN_POINT('Ctrl Pts',(91.8993532141643,-2.49522149708592,126.56386349092));
#48716=CARTESIAN_POINT('Ctrl Pts',(91.8915881588722,-2.61129840819856,126.636590987915));
#48717=CARTESIAN_POINT('Ctrl Pts',(91.883830904992,-2.72725869891749,126.709245416897));
#48718=CARTESIAN_POINT('Ctrl Pts',(91.8760736511119,-2.840305691509,126.786819022479));
#48719=CARTESIAN_POINT('Ctrl Pts',(91.8683163972317,-2.94999805092592,126.869046835663));
#48720=CARTESIAN_POINT('Ctrl Pts',(91.8604768978297,-3.06085341280244,126.952146461156));
#48721=CARTESIAN_POINT('Ctrl Pts',(91.8526373984277,-3.16828222908446,127.039999384072));
#48722=CARTESIAN_POINT('Ctrl Pts',(91.8447978990257,-3.27185763377978,127.1322861784));
#48723=CARTESIAN_POINT('Ctrl Pts',(91.8370503435242,-3.37421827638199,127.223490606699));
#48724=CARTESIAN_POINT('Ctrl Pts',(91.8293027880226,-3.47281511362822,127.319025190661));
#48725=CARTESIAN_POINT('Ctrl Pts',(91.8215552325211,-3.56726867283482,127.418540587158));
#48726=CARTESIAN_POINT('Ctrl Pts',(91.8138094054638,-3.66170115988376,127.518033782225));
#48727=CARTESIAN_POINT('Ctrl Pts',(91.8060635784066,-3.75199193937431,127.621505739236));
#48728=CARTESIAN_POINT('Ctrl Pts',(91.7983177513493,-3.83779856660814,127.728570438662));
#48729=CARTESIAN_POINT('Ctrl Pts',(91.7905719749466,-3.92360463270164,127.835634437929));
#48730=CARTESIAN_POINT('Ctrl Pts',(91.7828261985438,-4.00492636114638,127.946290827345));
#48731=CARTESIAN_POINT('Ctrl Pts',(91.7750804221411,-4.0814620126222,128.060121032176));
#48732=CARTESIAN_POINT('Ctrl Pts',(91.767171087928,-4.159613771112,128.17635484616));
#48733=CARTESIAN_POINT('Ctrl Pts',(91.7592617537148,-4.23277481175118,128.295897670547));
#48734=CARTESIAN_POINT('Ctrl Pts',(91.7513524195017,-4.30067131094419,128.418274001845));
#48735=CARTESIAN_POINT('Ctrl Pts',(91.7435983649255,-4.36723483526734,128.538247785498));
#48736=CARTESIAN_POINT('Ctrl Pts',(91.7358443103493,-4.42873849149336,128.660944467187));
#48737=CARTESIAN_POINT('Ctrl Pts',(91.7280902557731,-4.48497180747443,128.785893142312));
#48738=CARTESIAN_POINT('Ctrl Pts',(91.7201032817415,-4.54289428274695,128.914595076725));
#48739=CARTESIAN_POINT('Ctrl Pts',(91.7121163077099,-4.59522464169714,129.045686007565));
#48740=CARTESIAN_POINT('Ctrl Pts',(91.7041293336783,-4.6417874480562,129.178632365499));
#48741=CARTESIAN_POINT('Ctrl Pts',(91.6961423596467,-4.68835025441526,129.311578723434));
#48742=CARTESIAN_POINT('Ctrl Pts',(91.6881553856151,-4.7291454272762,129.446380064493));
#48743=CARTESIAN_POINT('Ctrl Pts',(91.6801684115835,-4.76405452823407,129.582490119308));
#48744=CARTESIAN_POINT('Origin',(213.235140564004,0.,130.804360617566));
#48745=CARTESIAN_POINT('',(89.5849003473043,-4.76405452823408,129.582490119308));
#48746=CARTESIAN_POINT('',(89.9298547845941,-4.76405452823405,129.582490119308));
#48747=CARTESIAN_POINT('',(213.235140564004,-4.76405452823405,129.582490119308));
#48748=CARTESIAN_POINT('',(91.2648594360222,-4.91824999011832,130.804048846578));
#48749=CARTESIAN_POINT('Ctrl Pts',(91.2648594359911,-4.91824999011835,130.80404884713));
#48750=CARTESIAN_POINT('Ctrl Pts',(91.2567821902965,-4.91825908170041,130.947470635016));
#48751=CARTESIAN_POINT('Ctrl Pts',(91.2487049446019,-4.91199033781274,131.090783981988));
#48752=CARTESIAN_POINT('Ctrl Pts',(91.2406276989073,-4.89949806352798,131.233431460185));
#48753=CARTESIAN_POINT('Ctrl Pts',(91.2325411218347,-4.88699135732701,131.376243734351));
#48754=CARTESIAN_POINT('Ctrl Pts',(91.2244545447621,-4.86824680681819,131.5183882668));
#48755=CARTESIAN_POINT('Ctrl Pts',(91.2163679676895,-4.84337019359417,131.659315721828));
#48756=CARTESIAN_POINT('Ctrl Pts',(91.2082635352129,-4.8184386520642,131.800554348891));
#48757=CARTESIAN_POINT('Ctrl Pts',(91.2001591027363,-4.78734803810946,131.940570190156));
#48758=CARTESIAN_POINT('Ctrl Pts',(91.1920546702598,-4.75025502706789,132.078825305314));
#48759=CARTESIAN_POINT('Ctrl Pts',(91.1839409951308,-4.71311971351996,132.217238092705));
#48760=CARTESIAN_POINT('Ctrl Pts',(91.1758273200019,-4.66996844606161,132.353885823443));
#48761=CARTESIAN_POINT('Ctrl Pts',(91.1677136448729,-4.62100685794723,132.488248583348));
#48762=CARTESIAN_POINT('Ctrl Pts',(91.1595815322751,-4.57193400980094,132.622916668417));
#48763=CARTESIAN_POINT('Ctrl Pts',(91.1514494196773,-4.51702456936365,132.755289085));
#48764=CARTESIAN_POINT('Ctrl Pts',(91.1433173070796,-4.45653189461077,132.884866934504));
#48765=CARTESIAN_POINT('Ctrl Pts',(91.1363627474049,-4.40479873039393,132.995681544613));
#48766=CARTESIAN_POINT('Ctrl Pts',(91.1294081877302,-4.34898303515304,133.104452624606));
#48767=CARTESIAN_POINT('Ctrl Pts',(91.1224536280556,-4.28926854451115,133.210884753237));
#48768=CARTESIAN_POINT('Ctrl Pts',(91.1146792939365,-4.2225151591471,133.329862656611));
#48769=CARTESIAN_POINT('Ctrl Pts',(91.1069049598174,-4.1507018855291,133.446249448752));
#48770=CARTESIAN_POINT('Ctrl Pts',(91.0991306256983,-4.07405482378452,133.559584810857));
#48771=CARTESIAN_POINT('Ctrl Pts',(91.0913658727512,-3.9975022226934,133.672780497258));
#48772=CARTESIAN_POINT('Ctrl Pts',(91.0836011198041,-3.91612790346948,133.782931915379));
#48773=CARTESIAN_POINT('Ctrl Pts',(91.075836366857,-3.83020391151471,133.889603081088));
#48774=CARTESIAN_POINT('Ctrl Pts',(91.068079325972,-3.74436526048018,133.996168299491));
#48775=CARTESIAN_POINT('Ctrl Pts',(91.060322285087,-3.6539861729963,134.09925984184));
#48776=CARTESIAN_POINT('Ctrl Pts',(91.052565244202,-3.5593818586381,134.198470787684));
#48777=CARTESIAN_POINT('Ctrl Pts',(91.0448140529619,-3.46484888612909,134.297606917782));
#48778=CARTESIAN_POINT('Ctrl Pts',(91.0370628617217,-3.36609729755123,134.392867994372));
#48779=CARTESIAN_POINT('Ctrl Pts',(91.0293116704816,-3.2634821932607,134.483880564077));
#48780=CARTESIAN_POINT('Ctrl Pts',(91.0215637737045,-3.16091070312698,134.574854451011));
#48781=CARTESIAN_POINT('Ctrl Pts',(91.0138158769274,-3.0544792551696,134.661583163637));
#48782=CARTESIAN_POINT('Ctrl Pts',(91.0060679801503,-2.94457922037927,134.743730653169));
#48783=CARTESIAN_POINT('Ctrl Pts',(90.9983217040662,-2.83470217430705,134.825860959218));
#48784=CARTESIAN_POINT('Ctrl Pts',(90.9905754279821,-2.7213582975207,134.903411714345));
#48785=CARTESIAN_POINT('Ctrl Pts',(90.982829151898,-2.60497108351019,134.97608792368));
#48786=CARTESIAN_POINT('Ctrl Pts',(90.9750828186327,-2.48858301035571,135.048764669494));
#48787=CARTESIAN_POINT('Ctrl Pts',(90.9673364853673,-2.3691518867714,135.116566590639));
#48788=CARTESIAN_POINT('Ctrl Pts',(90.959590152102,-2.24712880813484,135.179242922514));
#48789=CARTESIAN_POINT('Ctrl Pts',(90.951842084099,-2.12507840327604,135.24193329032));
#48790=CARTESIAN_POINT('Ctrl Pts',(90.944094016096,-2.00043523604083,135.299495606191));
#48791=CARTESIAN_POINT('Ctrl Pts',(90.9363459480931,-1.87367316424428,135.35172600162));
#48792=CARTESIAN_POINT('Ctrl Pts',(90.9285896453512,-1.74677636820917,135.404011908135));
#48793=CARTESIAN_POINT('Ctrl Pts',(90.9208333426094,-1.61775653106513,135.450954424926));
#48794=CARTESIAN_POINT('Ctrl Pts',(90.9130770398675,-1.48710609515371,135.492398429301));
#48795=CARTESIAN_POINT('Ctrl Pts',(90.9053165973534,-1.35638592717075,135.533864553589));
#48796=CARTESIAN_POINT('Ctrl Pts',(90.8975561548392,-1.22403380337619,135.569826215315));
#48797=CARTESIAN_POINT('Ctrl Pts',(90.889795712325,-1.09055436911228,135.600179028485));
#48798=CARTESIAN_POINT('Ctrl Pts',(90.8820228120596,-0.956860661810738,
135.630580566685));
#48799=CARTESIAN_POINT('Ctrl Pts',(90.8742499117942,-0.822036412513276,
135.655355193125));
#48800=CARTESIAN_POINT('Ctrl Pts',(90.8664770115287,-0.686594326366148,
135.674450071929));
#48801=CARTESIAN_POINT('Ctrl Pts',(90.8589866757667,-0.556075901208769,
135.692850803793));
#48802=CARTESIAN_POINT('Ctrl Pts',(90.8514963400047,-0.424984085664462,
135.705977534244));
#48803=CARTESIAN_POINT('Ctrl Pts',(90.8440060042427,-0.293777507871708,
135.713828800411));
#48804=CARTESIAN_POINT('Ctrl Pts',(90.8362316701236,-0.157596192802371,
135.721977749721));
#48805=CARTESIAN_POINT('Ctrl Pts',(90.8284573360045,-0.0208598598023733,
135.724469112826));
#48806=CARTESIAN_POINT('Ctrl Pts',(90.8206830018854,0.115921999242919,135.721244300611));
#48807=CARTESIAN_POINT('Ctrl Pts',(90.8129182489383,0.252535286871484,135.718023462689));
#48808=CARTESIAN_POINT('Ctrl Pts',(90.8051534959913,0.389193601805164,135.709100475377));
#48809=CARTESIAN_POINT('Ctrl Pts',(90.7973887430442,0.525383091062019,135.694468558105));
#48810=CARTESIAN_POINT('Ctrl Pts',(90.7896317021592,0.661437314998209,135.67985117346));
#48811=CARTESIAN_POINT('Ctrl Pts',(90.7818746612742,0.797023253698014,135.659536184282));
#48812=CARTESIAN_POINT('Ctrl Pts',(90.7741176203892,0.931628174985949,135.63356883487));
#48813=CARTESIAN_POINT('Ctrl Pts',(90.7663664291491,1.06613158965539,135.607621067637));
#48814=CARTESIAN_POINT('Ctrl Pts',(90.7586152379089,1.19965507709207,135.576029498155));
#48815=CARTESIAN_POINT('Ctrl Pts',(90.7508640466688,1.33169249997644,135.538891021736));
#48816=CARTESIAN_POINT('Ctrl Pts',(90.7431161498917,1.46367380343406,135.50176833016));
#48817=CARTESIAN_POINT('Ctrl Pts',(90.7353682531147,1.59416992300471,135.459103526339));
#48818=CARTESIAN_POINT('Ctrl Pts',(90.7276203563376,1.72268658574751,135.411044239195));
#48819=CARTESIAN_POINT('Ctrl Pts',(90.7198740802535,1.85117636557488,135.362995005018));
#48820=CARTESIAN_POINT('Ctrl Pts',(90.7121278041695,1.9776871461959,135.309553668841));
#48821=CARTESIAN_POINT('Ctrl Pts',(90.7043815280854,2.10174183149495,135.250917075798));
#48822=CARTESIAN_POINT('Ctrl Pts',(90.69663519482,2.22579743253743,135.192280049913));
#48823=CARTESIAN_POINT('Ctrl Pts',(90.6888888615547,2.34739654861116,135.128447857709));
#48824=CARTESIAN_POINT('Ctrl Pts',(90.6811425282894,2.46608437628631,135.059664474112));
#48825=CARTESIAN_POINT('Ctrl Pts',(90.6733944602864,2.58479878327754,134.990865686954));
#48826=CARTESIAN_POINT('Ctrl Pts',(90.6656463922834,2.70060026633855,134.917113698047));
#48827=CARTESIAN_POINT('Ctrl Pts',(90.6578983242805,2.81306117339638,134.838696981484));
#48828=CARTESIAN_POINT('Ctrl Pts',(90.6501420215387,2.92564160524469,134.760196922701));
#48829=CARTESIAN_POINT('Ctrl Pts',(90.6423857187968,3.03487404756369,134.677022456641));
#48830=CARTESIAN_POINT('Ctrl Pts',(90.6346294160549,3.14036181412377,134.589504041387));
#48831=CARTESIAN_POINT('Ctrl Pts',(90.6268689735408,3.24590588268112,134.501938914919));
#48832=CARTESIAN_POINT('Ctrl Pts',(90.6191085310266,3.34770100297013,134.41002548134));
#48833=CARTESIAN_POINT('Ctrl Pts',(90.6113480885124,3.44538657896237,134.314131889886));
#48834=CARTESIAN_POINT('Ctrl Pts',(90.603575188247,3.54322896851331,134.218084361527));
#48835=CARTESIAN_POINT('Ctrl Pts',(90.5958022879816,3.63694836340132,134.118044192917));
#48836=CARTESIAN_POINT('Ctrl Pts',(90.5880293877162,3.72622318165434,134.014414178334));
#48837=CARTESIAN_POINT('Ctrl Pts',(90.5805390519541,3.81225263539495,133.91455137581));
#48838=CARTESIAN_POINT('Ctrl Pts',(90.573048716192,3.89415485389067,133.811355437125));
#48839=CARTESIAN_POINT('Ctrl Pts',(90.5655583804299,3.97168070667275,133.705211428405));
#48840=CARTESIAN_POINT('Ctrl Pts',(90.5577840463108,4.05214597572579,133.595042937333));
#48841=CARTESIAN_POINT('Ctrl Pts',(90.5500097121917,4.12815135802207,133.481349430419));
#48842=CARTESIAN_POINT('Ctrl Pts',(90.5422353780726,4.19937216807081,133.364527888768));
#48843=CARTESIAN_POINT('Ctrl Pts',(90.5344706251255,4.27050520483626,133.247850319226));
#48844=CARTESIAN_POINT('Ctrl Pts',(90.5267058721785,4.33686520018545,133.12805271591));
#48845=CARTESIAN_POINT('Ctrl Pts',(90.5189411192314,4.39816869934376,133.005563732822));
#48846=CARTESIAN_POINT('Ctrl Pts',(90.5111840783464,4.45941131100252,132.883196407519));
#48847=CARTESIAN_POINT('Ctrl Pts',(90.5034270374614,4.51560724699439,132.758143369425));
#48848=CARTESIAN_POINT('Ctrl Pts',(90.4956699965764,4.56651742836434,132.630860450291));
#48849=CARTESIAN_POINT('Ctrl Pts',(90.4879188053363,4.6173892179705,132.503673516196));
#48850=CARTESIAN_POINT('Ctrl Pts',(90.4801676140961,4.6629830422971,132.374260409662));
#48851=CARTESIAN_POINT('Ctrl Pts',(90.472416422856,4.70310684253171,132.243099332633));
#48852=CARTESIAN_POINT('Ctrl Pts',(90.4646685260789,4.74321358908094,132.11199400256));
#48853=CARTESIAN_POINT('Ctrl Pts',(90.4569206293018,4.77785482146942,131.979142552712));
#48854=CARTESIAN_POINT('Ctrl Pts',(90.4491727325247,4.8068875774922,131.845040625951));
#48855=CARTESIAN_POINT('Ctrl Pts',(90.4414264564406,4.83591426048827,131.710966750422));
#48856=CARTESIAN_POINT('Ctrl Pts',(90.4336801803565,4.85933471794867,131.575643300133));
#48857=CARTESIAN_POINT('Ctrl Pts',(90.4259339042724,4.87705667915491,131.439578069161));
#48858=CARTESIAN_POINT('Ctrl Pts',(90.4181875710071,4.89477877118064,131.303511833786));
#48859=CARTESIAN_POINT('Ctrl Pts',(90.4104412377417,4.90680223251936,131.166704194493));
#48860=CARTESIAN_POINT('Ctrl Pts',(90.4026949044763,4.91308649382261,131.029669664694));
#48861=CARTESIAN_POINT('Ctrl Pts',(90.3949468364734,4.91937216244262,130.892604446962));
#48862=CARTESIAN_POINT('Ctrl Pts',(90.3871987684704,4.91991605561335,130.755312628097));
#48863=CARTESIAN_POINT('Ctrl Pts',(90.3794507004674,4.91472971836706,130.618309931194));
#48864=CARTESIAN_POINT('Ctrl Pts',(90.3716943977255,4.90953786901984,130.481161626194));
#48865=CARTESIAN_POINT('Ctrl Pts',(90.3639380949837,4.89860363832411,130.344303448292));
#48866=CARTESIAN_POINT('Ctrl Pts',(90.3561817922418,4.88199063142803,130.208247761515));
#48867=CARTESIAN_POINT('Ctrl Pts',(90.3484213497276,4.86536875766992,130.072119457721));
#48868=CARTESIAN_POINT('Ctrl Pts',(90.3406609072134,4.84306213187583,129.936794884074));
#48869=CARTESIAN_POINT('Ctrl Pts',(90.3329004646993,4.81518557746513,129.802776413881));
#48870=CARTESIAN_POINT('Ctrl Pts',(90.3251275644338,4.78726427313458,129.668542805342));
#48871=CARTESIAN_POINT('Ctrl Pts',(90.3173546641684,4.75375526815799,129.5356198694));
#48872=CARTESIAN_POINT('Ctrl Pts',(90.309581763903,4.71482362185967,129.404495882224));
#48873=CARTESIAN_POINT('Ctrl Pts',(90.302091428141,4.67730723896732,129.278138582264));
#48874=CARTESIAN_POINT('Ctrl Pts',(90.2946010923789,4.63475572276177,129.153452000694));
#48875=CARTESIAN_POINT('Ctrl Pts',(90.2871107566169,4.58735837917409,129.030853875678));
#48876=CARTESIAN_POINT('Ctrl Pts',(90.2793364224978,4.53816395089799,128.90360740549));
#48877=CARTESIAN_POINT('Ctrl Pts',(90.2715620883788,4.4835931492296,128.778207807174));
#48878=CARTESIAN_POINT('Ctrl Pts',(90.2637877542597,4.42380446517697,128.655142825815));
#48879=CARTESIAN_POINT('Ctrl Pts',(90.2560230013126,4.36408946533396,128.532229511046));
#48880=CARTESIAN_POINT('Ctrl Pts',(90.2482582483655,4.29916954723883,128.411645436735));
#48881=CARTESIAN_POINT('Ctrl Pts',(90.2404934954184,4.22925213541458,128.293860779368));
#48882=CARTESIAN_POINT('Ctrl Pts',(90.2327364545334,4.15940416654941,128.176193107384));
#48883=CARTESIAN_POINT('Ctrl Pts',(90.2249794136484,4.0845687799809,128.061319653203));
#48884=CARTESIAN_POINT('Ctrl Pts',(90.2172223727634,4.00500025185449,127.949687948915));
#48885=CARTESIAN_POINT('Ctrl Pts',(90.2094711815233,3.92549172697409,127.838140426963));
#48886=CARTESIAN_POINT('Ctrl Pts',(90.2017199902832,3.84125739101632,127.7298301061));
#48887=CARTESIAN_POINT('Ctrl Pts',(90.193968799043,3.75259575634186,127.625177050676));
#48888=CARTESIAN_POINT('Ctrl Pts',(90.186220902266,3.66397180522734,127.520568475592));
#48889=CARTESIAN_POINT('Ctrl Pts',(90.1784730054889,3.5709245501868,127.419614371973));
#48890=CARTESIAN_POINT('Ctrl Pts',(90.1707251087118,3.47379371503351,127.322702925045));
#48891=CARTESIAN_POINT('Ctrl Pts',(90.1629788326277,3.3766831975569,127.225811749902));
#48892=CARTESIAN_POINT('Ctrl Pts',(90.1552325565436,3.27549107560323,127.132961825398));
#48893=CARTESIAN_POINT('Ctrl Pts',(90.1474862804595,3.17059469613377,127.044505256605));
#48894=CARTESIAN_POINT('Ctrl Pts',(90.1397399471941,3.06569754234328,126.956048034845));
#48895=CARTESIAN_POINT('Ctrl Pts',(90.1319936139288,2.9570963753553,126.871984485549));
#48896=CARTESIAN_POINT('Ctrl Pts',(90.1242472806634,2.84520214115207,126.792626847924));
#48897=CARTESIAN_POINT('Ctrl Pts',(90.1164992126605,2.73328284901083,126.713251438707));
#48898=CARTESIAN_POINT('Ctrl Pts',(90.1087511446575,2.61806934103788,126.638584264343));
#48899=CARTESIAN_POINT('Ctrl Pts',(90.1010030766545,2.50000175005002,126.5688943726));
#48900=CARTESIAN_POINT('Ctrl Pts',(90.0932467739127,2.38180867542152,126.499130413611));
#48901=CARTESIAN_POINT('Ctrl Pts',(90.0854904711708,2.26075579555368,126.434354503466));
#48902=CARTESIAN_POINT('Ctrl Pts',(90.077734168429,2.13730855694855,126.374790074625));
#48903=CARTESIAN_POINT('Ctrl Pts',(90.0699737259148,2.01379543083509,126.315193854454));
#48904=CARTESIAN_POINT('Ctrl Pts',(90.0622132834007,1.88788575832351,126.260814812948));
#48905=CARTESIAN_POINT('Ctrl Pts',(90.0544528408865,1.76006426516806,126.211827890957));
#48906=CARTESIAN_POINT('Ctrl Pts',(90.0466799406211,1.63203758160441,126.162762330809));
#48907=CARTESIAN_POINT('Ctrl Pts',(90.0389070403556,1.50209331533099,126.11910631202));
#48908=CARTESIAN_POINT('Ctrl Pts',(90.0311341400902,1.37073148551301,126.080984890703));
#48909=CARTESIAN_POINT('Ctrl Pts',(90.0236438043282,1.24414498908985,126.044249279072));
#48910=CARTESIAN_POINT('Ctrl Pts',(90.0161534685662,1.11624250281998,126.012652931799));
#48911=CARTESIAN_POINT('Ctrl Pts',(90.0086631328042,0.98747780613174,125.986262378126));
#48912=CARTESIAN_POINT('Ctrl Pts',(90.0008887986851,0.853830956830725,125.958871218588));
#48913=CARTESIAN_POINT('Ctrl Pts',(89.993114464566,0.718831871998949,125.937001633612));
#48914=CARTESIAN_POINT('Ctrl Pts',(89.9853401304469,0.582976573649635,125.920783918355));
#48915=CARTESIAN_POINT('Ctrl Pts',(89.9775753774998,0.447288704814077,125.904586189983));
#48916=CARTESIAN_POINT('Ctrl Pts',(89.9698106245527,0.310747106489839,125.894026518108));
#48917=CARTESIAN_POINT('Ctrl Pts',(89.9620458716057,0.173859469494193,125.889184532483));
#48918=CARTESIAN_POINT('Ctrl Pts',(89.9542888307206,0.0371077912286443,
125.884347355987));
#48919=CARTESIAN_POINT('Ctrl Pts',(89.9465317898356,-0.0999888535562237,
125.88521657823));
#48920=CARTESIAN_POINT('Ctrl Pts',(89.9387747489505,-0.236916500970071,
125.891820171517));
#48921=CARTESIAN_POINT('Ctrl Pts',(89.9310235577104,-0.373740890178559,
125.898418784983));
#48922=CARTESIAN_POINT('Ctrl Pts',(89.9232723664704,-0.51039614675082,125.910743143411));
#48923=CARTESIAN_POINT('Ctrl Pts',(89.9155211752303,-0.646367505429397,
125.928769154941));
#48924=CARTESIAN_POINT('Ctrl Pts',(89.9077732784532,-0.782281072654214,
125.946787504935));
#48925=CARTESIAN_POINT('Ctrl Pts',(89.9000253816761,-0.917510933352707,
125.970502636888));
#48926=CARTESIAN_POINT('Ctrl Pts',(89.892277484899,-1.05154686728138,125.999838555132));
#48927=CARTESIAN_POINT('Ctrl Pts',(89.8845312088149,-1.18555476378207,126.029168336935));
#48928=CARTESIAN_POINT('Ctrl Pts',(89.8767849327307,-1.31836884858427,126.064116482865));
#48929=CARTESIAN_POINT('Ctrl Pts',(89.8690386566466,-1.44948892046989,126.104555841627));
#48930=CARTESIAN_POINT('Ctrl Pts',(89.8612923233813,-1.58060996025446,126.144995498905));
#48931=CARTESIAN_POINT('Ctrl Pts',(89.8535459901159,-1.71003658856958,126.190926334675));
#48932=CARTESIAN_POINT('Ctrl Pts',(89.8457996568505,-1.83728398338421,126.242171381366));
#48933=CARTESIAN_POINT('Ctrl Pts',(89.8380515888476,-1.96455987436968,126.293427904029));
#48934=CARTESIAN_POINT('Ctrl Pts',(89.8303035208446,-2.08965519815141,126.350000859712));
#48935=CARTESIAN_POINT('Ctrl Pts',(89.8225554528417,-2.21210569468498,126.4116653791));
#48936=CARTESIAN_POINT('Ctrl Pts',(89.8147991500998,-2.33468633306404,126.473395436273));
#48937=CARTESIAN_POINT('Ctrl Pts',(89.8070428473579,-2.45461617926756,126.540227690829));
#48938=CARTESIAN_POINT('Ctrl Pts',(89.7992865446161,-2.57145566803669,126.611891320144));
#48939=CARTESIAN_POINT('Ctrl Pts',(89.7915261021019,-2.68835751755942,126.683593198497));
#48940=CARTESIAN_POINT('Ctrl Pts',(89.7837656595877,-2.80216539878034,126.760131371712));
#48941=CARTESIAN_POINT('Ctrl Pts',(89.7760052170735,-2.91247012289832,126.841192586089));
#48942=CARTESIAN_POINT('Ctrl Pts',(89.7682323168081,-3.02295191795154,126.922383927122));
#48943=CARTESIAN_POINT('Ctrl Pts',(89.7604594165426,-3.12991901294711,127.008112574038));
#48944=CARTESIAN_POINT('Ctrl Pts',(89.7526865162772,-3.23299592206444,127.098025442435));
#48945=CARTESIAN_POINT('Ctrl Pts',(89.7451961805151,-3.33232572590036,127.184669751588));
#48946=CARTESIAN_POINT('Ctrl Pts',(89.7377058447531,-3.42804304573703,127.27519913819));
#48947=CARTESIAN_POINT('Ctrl Pts',(89.730215508991,-3.5198466297751,127.369267785435));
#48948=CARTESIAN_POINT('Ctrl Pts',(89.7225449396728,-3.61385920509875,127.465599926247));
#48949=CARTESIAN_POINT('Ctrl Pts',(89.7148743703545,-3.70408235314633,127.565966974299));
#48950=CARTESIAN_POINT('Ctrl Pts',(89.7072038010363,-3.79014272504406,127.670034344458));
#48951=CARTESIAN_POINT('Ctrl Pts',(89.6995422470002,-3.87610194949049,127.773979403395));
#48952=CARTESIAN_POINT('Ctrl Pts',(89.6918806929641,-3.95790787116681,127.881615831503));
#48953=CARTESIAN_POINT('Ctrl Pts',(89.684219138928,-4.03522292249679,127.992571324561));
#48954=CARTESIAN_POINT('Ctrl Pts',(89.6765648235771,-4.11246492607275,128.103421986161));
#48955=CARTESIAN_POINT('Ctrl Pts',(89.6689105082262,-4.18522426871552,128.21758514882));
#48956=CARTESIAN_POINT('Ctrl Pts',(89.6612561928753,-4.25320310047533,128.334654876267));
#48957=CARTESIAN_POINT('Ctrl Pts',(89.6536077566286,-4.32112971925222,128.451634685138));
#48958=CARTESIAN_POINT('Ctrl Pts',(89.6459593203818,-4.38428293318778,128.571516269498));
#48959=CARTESIAN_POINT('Ctrl Pts',(89.6383108841352,-4.44240810535641,128.693864636057));
#48960=CARTESIAN_POINT('Ctrl Pts',(89.6306658150064,-4.50050768872443,128.816159140446));
#48961=CARTESIAN_POINT('Ctrl Pts',(89.6230207458776,-4.55358346182154,128.940917903946));
#48962=CARTESIAN_POINT('Ctrl Pts',(89.6153756767489,-4.60142685460908,129.067681613207));
#48963=CARTESIAN_POINT('Ctrl Pts',(89.607731596945,-4.64926405613048,129.194428918366));
#48964=CARTESIAN_POINT('Ctrl Pts',(89.6000875171411,-4.69187007989412,129.323180278017));
#48965=CARTESIAN_POINT('Ctrl Pts',(89.5924434373372,-4.72908476756752,129.45345709634));
#48966=CARTESIAN_POINT('Ctrl Pts',(89.5899290739929,-4.74132577615913,129.496308984991));
#48967=CARTESIAN_POINT('Ctrl Pts',(89.5874147106486,-4.75298386921147,129.5393257878));
#48968=CARTESIAN_POINT('Ctrl Pts',(89.5849003473043,-4.76405452823408,129.582490119308));
#48969=CARTESIAN_POINT('Ctrl Pts',(91.3345773084523,-4.76405452823403,129.582490119308));
#48970=CARTESIAN_POINT('Ctrl Pts',(91.3264022802331,-4.7999124076053,129.722299446757));
#48971=CARTESIAN_POINT('Ctrl Pts',(91.318227252014,-4.8296500169407,129.863837736042));
#48972=CARTESIAN_POINT('Ctrl Pts',(91.3100522237949,-4.85311178198504,130.006557951452));
#48973=CARTESIAN_POINT('Ctrl Pts',(91.3018941690471,-4.87652483434178,130.148981842812));
#48974=CARTESIAN_POINT('Ctrl Pts',(91.2937361142993,-4.89368797434029,130.292582447441));
#48975=CARTESIAN_POINT('Ctrl Pts',(91.2855780595515,-4.90449620518163,130.436801049796));
#48976=CARTESIAN_POINT('Ctrl Pts',(91.2786718517084,-4.91364592173953,130.558889424231));
#48977=CARTESIAN_POINT('Ctrl Pts',(91.2717656438653,-4.91824221661868,130.681420327672));
#48978=CARTESIAN_POINT('Ctrl Pts',(91.2648594360222,-4.91824999011832,130.804048846578));
#48979=CARTESIAN_POINT('',(91.6101405639636,-4.91824821216763,130.800167049889));
#48980=CARTESIAN_POINT('Ctrl Pts',(91.6801684115835,-4.76405452823407,129.582490119308));
#48981=CARTESIAN_POINT('Ctrl Pts',(91.6733655675631,-4.79378808787393,129.698420817074));
#48982=CARTESIAN_POINT('Ctrl Pts',(91.6665627235426,-4.81925245143363,129.815300578257));
#48983=CARTESIAN_POINT('Ctrl Pts',(91.6597598795222,-4.84040749075737,129.932788253433));
#48984=CARTESIAN_POINT('Ctrl Pts',(91.6478811714655,-4.87734712002086,130.13793800984));
#48985=CARTESIAN_POINT('Ctrl Pts',(91.636002463409,-4.90125243413717,130.345500572299));
#48986=CARTESIAN_POINT('Ctrl Pts',(91.6241237553524,-4.91188095687709,130.554143655774));
#48987=CARTESIAN_POINT('Ctrl Pts',(91.619462691571,-4.91605146280719,130.636012720573));
#48988=CARTESIAN_POINT('Ctrl Pts',(91.6148016277897,-4.91817819283374,130.718047855595));
#48989=CARTESIAN_POINT('Ctrl Pts',(91.6101405640084,-4.91824821216696,130.800167049099));
#48990=CARTESIAN_POINT('Ctrl Pts',(91.6101405639636,-4.91824821216763,130.800167049889));
#48991=CARTESIAN_POINT('Ctrl Pts',(91.6024939071275,-4.91836308159171,130.934886788097));
#48992=CARTESIAN_POINT('Ctrl Pts',(91.5948472502914,-4.91293846637897,131.069800215564));
#48993=CARTESIAN_POINT('Ctrl Pts',(91.5872005934553,-4.90195333028209,131.204406377744));
#48994=CARTESIAN_POINT('Ctrl Pts',(91.5795609026991,-4.89097820160899,131.338889914141));
#48995=CARTESIAN_POINT('Ctrl Pts',(91.5719212119429,-4.87445266018738,131.473066342139));
#48996=CARTESIAN_POINT('Ctrl Pts',(91.5642815211867,-4.85240772185146,131.606434406825));
#48997=CARTESIAN_POINT('Ctrl Pts',(91.556646523981,-4.83037632713072,131.739720534981));
#48998=CARTESIAN_POINT('Ctrl Pts',(91.5490115267753,-4.80283234498052,131.872198890597));
#48999=CARTESIAN_POINT('Ctrl Pts',(91.5413765295696,-4.76985860792635,132.003373512781));
#49000=CARTESIAN_POINT('Ctrl Pts',(91.5337439811993,-4.73689544680993,132.13450606225));
#49001=CARTESIAN_POINT('Ctrl Pts',(91.5261114328291,-4.69850609087948,132.264335318513));
#49002=CARTESIAN_POINT('Ctrl Pts',(91.5184788844588,-4.6548243478885,132.392376156786));
#49003=CARTESIAN_POINT('Ctrl Pts',(91.5108470172819,-4.61114650342711,132.520405567608));
#49004=CARTESIAN_POINT('Ctrl Pts',(91.503215150105,-4.56217734141902,132.646646495816));
#49005=CARTESIAN_POINT('Ctrl Pts',(91.4955832829282,-4.50810017087201,132.770630159588));
#49006=CARTESIAN_POINT('Ctrl Pts',(91.4879503300651,-4.45401530747093,132.8946314609));
#49007=CARTESIAN_POINT('Ctrl Pts',(91.480317377202,-4.39482115247596,133.016374489488));
#49008=CARTESIAN_POINT('Ctrl Pts',(91.4726844243389,-4.33074843260344,133.135412113351));
#49009=CARTESIAN_POINT('Ctrl Pts',(91.4650439343352,-4.26661244428113,133.254567280623));
#49010=CARTESIAN_POINT('Ctrl Pts',(91.4574034443316,-4.19758846088063,133.37101135136));
#49011=CARTESIAN_POINT('Ctrl Pts',(91.4497629543279,-4.12395248100192,133.484323116732));
#49012=CARTESIAN_POINT('Ctrl Pts',(91.4421187382377,-4.05028059059438,133.597690141577));
#49013=CARTESIAN_POINT('Ctrl Pts',(91.4344745221474,-3.97199245886475,133.707921490589));
#49014=CARTESIAN_POINT('Ctrl Pts',(91.4268303060572,-3.88940560700759,133.814627563649));
#49015=CARTESIAN_POINT('Ctrl Pts',(91.4191739385419,-3.80668747315459,133.921503259184));
#49016=CARTESIAN_POINT('Ctrl Pts',(91.4115175710265,-3.7196572275666,134.024842174677));
#49017=CARTESIAN_POINT('Ctrl Pts',(91.4038612035112,-3.62867109466048,134.124289705555));
#49018=CARTESIAN_POINT('Ctrl Pts',(91.3963448875772,-3.53934929562656,134.221918125225));
#49019=CARTESIAN_POINT('Ctrl Pts',(91.3888285716432,-3.44621541074271,134.315796117543));
#49020=CARTESIAN_POINT('Ctrl Pts',(91.3813122557092,-3.34963699643573,134.405626374853));
#49021=CARTESIAN_POINT('Ctrl Pts',(91.3735379215901,-3.24974326284253,134.49854030243));
#49022=CARTESIAN_POINT('Ctrl Pts',(91.365763587471,-3.14582243455883,134.587441894661));
#49023=CARTESIAN_POINT('Ctrl Pts',(91.357989253352,-3.0382303658925,134.671961851699));
#49024=CARTESIAN_POINT('Ctrl Pts',(91.3502245004049,-2.93077089483532,134.756377645444));
#49025=CARTESIAN_POINT('Ctrl Pts',(91.3424597474578,-2.81964949024835,134.836422309136));
#49026=CARTESIAN_POINT('Ctrl Pts',(91.3346949945108,-2.70525832735585,134.911763744211));
#49027=CARTESIAN_POINT('Ctrl Pts',(91.3269379536258,-2.59098077937866,134.98703034911));
#49028=CARTESIAN_POINT('Ctrl Pts',(91.3191809127408,-2.47344026030279,135.057602807858));
#49029=CARTESIAN_POINT('Ctrl Pts',(91.3114238718558,-2.35306117404527,135.12318987718));
#49030=CARTESIAN_POINT('Ctrl Pts',(91.3036726806157,-2.23277286659336,135.188727486783));
#49031=CARTESIAN_POINT('Ctrl Pts',(91.2959214893755,-2.10965059459207,135.249287003763));
#49032=CARTESIAN_POINT('Ctrl Pts',(91.2881702981354,-1.98414652906802,135.304621233762));
#49033=CARTESIAN_POINT('Ctrl Pts',(91.2804224013584,-1.85869580611949,135.359931945238));
#49034=CARTESIAN_POINT('Ctrl Pts',(91.2726745045812,-1.7308656600761,135.410021629511));
#49035=CARTESIAN_POINT('Ctrl Pts',(91.2649266078042,-1.6011313795446,135.454689785263));
#49036=CARTESIAN_POINT('Ctrl Pts',(91.2571803317201,-1.47142423662783,135.4993485974));
#49037=CARTESIAN_POINT('Ctrl Pts',(91.249434055636,-1.33981412090444,135.53858800954));
#49038=CARTESIAN_POINT('Ctrl Pts',(91.2416877795519,-1.20679437425347,135.572256421877));
#49039=CARTESIAN_POINT('Ctrl Pts',(91.2339414462865,-1.07377364568095,135.605925082748));
#49040=CARTESIAN_POINT('Ctrl Pts',(91.2261951130212,-0.93934364443041,135.634022565825));
#49041=CARTESIAN_POINT('Ctrl Pts',(91.2184487797558,-0.804010491069592,
135.656447817189));
#49042=CARTESIAN_POINT('Ctrl Pts',(91.2107007117529,-0.668647030787413,
135.678878090533));
#49043=CARTESIAN_POINT('Ctrl Pts',(91.2029526437499,-0.532380401563536,
135.695633540598));
#49044=CARTESIAN_POINT('Ctrl Pts',(91.1952045757469,-0.395724080343547,
135.706664720203));
#49045=CARTESIAN_POINT('Ctrl Pts',(91.1874482730051,-0.25892251915932,135.717707623878));
#49046=CARTESIAN_POINT('Ctrl Pts',(91.1796919702632,-0.121730828950221,
135.723014072495));
#49047=CARTESIAN_POINT('Ctrl Pts',(91.1719356675214,0.0153347001402445,
135.722586711339));
#49048=CARTESIAN_POINT('Ctrl Pts',(91.1641752250072,0.152473385230736,135.722159122088));
#49049=CARTESIAN_POINT('Ctrl Pts',(91.156414782493,0.289485384651345,135.715991642716));
#49050=CARTESIAN_POINT('Ctrl Pts',(91.1486543399788,0.425858279723248,135.704138958276));
#49051=CARTESIAN_POINT('Ctrl Pts',(91.1408814397134,0.562450092673031,135.692267246855));
#49052=CARTESIAN_POINT('Ctrl Pts',(91.133108539448,0.698400363143223,135.674692143074));
#49053=CARTESIAN_POINT('Ctrl Pts',(91.1253356391826,0.833204737624504,135.651519881269));
#49054=CARTESIAN_POINT('Ctrl Pts',(91.1178453034205,0.963108633542396,135.629189989547));
#49055=CARTESIAN_POINT('Ctrl Pts',(91.1103549676584,1.09194819823657,135.601662880641));
#49056=CARTESIAN_POINT('Ctrl Pts',(91.1028646318964,1.21928625874606,135.569077196937));
#49057=CARTESIAN_POINT('Ctrl Pts',(91.0950902977773,1.3514523805225,135.535256017131));
#49058=CARTESIAN_POINT('Ctrl Pts',(91.0873159636582,1.4824195539852,135.495877963249));
#49059=CARTESIAN_POINT('Ctrl Pts',(91.0795416295391,1.61168472876788,135.451042810008));
#49060=CARTESIAN_POINT('Ctrl Pts',(91.071776876592,1.74079059577531,135.406262912087));
#49061=CARTESIAN_POINT('Ctrl Pts',(91.0640121236449,1.8681982717929,135.356039423211));
#49062=CARTESIAN_POINT('Ctrl Pts',(91.0562473706978,1.99341637260455,135.300522784118));
#49063=CARTESIAN_POINT('Ctrl Pts',(91.0484903298129,2.11851010503312,135.245061284933));
#49064=CARTESIAN_POINT('Ctrl Pts',(91.0407332889279,2.24141823494115,135.184317255096));
#49065=CARTESIAN_POINT('Ctrl Pts',(91.0329762480429,2.36166633042866,135.118490333536));
#49066=CARTESIAN_POINT('Ctrl Pts',(91.0252250568027,2.48182374589196,135.052713052571));
#49067=CARTESIAN_POINT('Ctrl Pts',(91.0174738655626,2.59932477810744,134.981860696308));
#49068=CARTESIAN_POINT('Ctrl Pts',(91.0097226743225,2.71371704597576,134.906180074451));
#49069=CARTESIAN_POINT('Ctrl Pts',(91.0019747775454,2.8280606940788,134.830531618877));
#49070=CARTESIAN_POINT('Ctrl Pts',(90.9942268807683,2.93929788043286,134.750059194531));
#49071=CARTESIAN_POINT('Ctrl Pts',(90.9864789839913,3.04700301249826,134.665054299319));
#49072=CARTESIAN_POINT('Ctrl Pts',(90.9787327079072,3.1546856149719,134.580067185298));
#49073=CARTESIAN_POINT('Ctrl Pts',(90.9709864318231,3.25883732602677,134.490549728285));
#49074=CARTESIAN_POINT('Ctrl Pts',(90.963240155739,3.35906393711825,134.396835047378));
#49075=CARTESIAN_POINT('Ctrl Pts',(90.9554938224737,3.45929128805959,134.30311967469));
#49076=CARTESIAN_POINT('Ctrl Pts',(90.9477474892083,3.55559319564597,134.205207283306));
#49077=CARTESIAN_POINT('Ctrl Pts',(90.940001155943,3.64761106982197,134.103469064679));
#49078=CARTESIAN_POINT('Ctrl Pts',(90.93225308794,3.73964955076301,134.001708062483));
#49079=CARTESIAN_POINT('Ctrl Pts',(90.924505019937,3.82740182703436,133.896119818081));
#49080=CARTESIAN_POINT('Ctrl Pts',(90.9167569519341,3.91054875049141,133.787109606759));
#49081=CARTESIAN_POINT('Ctrl Pts',(90.9090006491922,3.99378404348823,133.677983538087));
#49082=CARTESIAN_POINT('Ctrl Pts',(90.9012443464504,4.07240396864752,133.565428548738));
#49083=CARTESIAN_POINT('Ctrl Pts',(90.8934880437085,4.14613168408876,133.449880438073));
#49084=CARTESIAN_POINT('Ctrl Pts',(90.8857276011944,4.21989875023162,133.334270655902));
#49085=CARTESIAN_POINT('Ctrl Pts',(90.8779671586802,4.28876820755461,133.215664907159));
#49086=CARTESIAN_POINT('Ctrl Pts',(90.8702067161661,4.35250908932965,133.094523862796));
#49087=CARTESIAN_POINT('Ctrl Pts',(90.8624338159006,4.4163522936268,132.973188352075));
#49088=CARTESIAN_POINT('Ctrl Pts',(90.8546609156352,4.47505030302207,132.849309766327));
#49089=CARTESIAN_POINT('Ctrl Pts',(90.8468880153697,4.52841988007978,132.723369854698));
#49090=CARTESIAN_POINT('Ctrl Pts',(90.8393976796076,4.57984933858214,132.602008176079));
#49091=CARTESIAN_POINT('Ctrl Pts',(90.8319073438455,4.62633093404965,132.478732726624));
#49092=CARTESIAN_POINT('Ctrl Pts',(90.8244170080834,4.66774500758555,132.353986251924));
#49093=CARTESIAN_POINT('Ctrl Pts',(90.8166426739643,4.71072930830667,132.224509976721));
#49094=CARTESIAN_POINT('Ctrl Pts',(90.8088683398452,4.74839039263825,132.093038784518));
#49095=CARTESIAN_POINT('Ctrl Pts',(90.8010940057261,4.78054029286684,131.960049836507));
#49096=CARTESIAN_POINT('Ctrl Pts',(90.7933292527791,4.81265057121667,131.827224785489));
#49097=CARTESIAN_POINT('Ctrl Pts',(90.785564499832,4.83926308861544,131.692886076769));
#49098=CARTESIAN_POINT('Ctrl Pts',(90.7777997468849,4.86023880994435,131.557528442696));
#49099=CARTESIAN_POINT('Ctrl Pts',(90.7700427059999,4.88119369789114,131.422305247733));
#49100=CARTESIAN_POINT('Ctrl Pts',(90.7622856651149,4.89652287164194,131.28606552522));
#49101=CARTESIAN_POINT('Ctrl Pts',(90.7545286242299,4.90613785105258,131.149316337868));
#49102=CARTESIAN_POINT('Ctrl Pts',(90.7467774329897,4.91574557973249,131.012670274142));
#49103=CARTESIAN_POINT('Ctrl Pts',(90.7390262417496,4.91964766380053,130.875515898711));
#49104=CARTESIAN_POINT('Ctrl Pts',(90.7312750505095,4.91780722821489,130.73836721928));
#49105=CARTESIAN_POINT('Ctrl Pts',(90.7235271537324,4.91596757486348,130.601276831697));
#49106=CARTESIAN_POINT('Ctrl Pts',(90.7157792569553,4.90839026150749,130.464192525409));
#49107=CARTESIAN_POINT('Ctrl Pts',(90.7080313601782,4.8950904904269,130.327629925212));
#49108=CARTESIAN_POINT('Ctrl Pts',(90.7002850840941,4.88179350137171,130.191095890967));
#49109=CARTESIAN_POINT('Ctrl Pts',(90.69253880801,4.86277647339259,130.055083734626));
#49110=CARTESIAN_POINT('Ctrl Pts',(90.6847925319259,4.83810658967367,129.920105174011));
#49111=CARTESIAN_POINT('Ctrl Pts',(90.6770461986606,4.81343652384725,129.785125617015));
#49112=CARTESIAN_POINT('Ctrl Pts',(90.6692998653952,4.78311358930753,129.651180055564));
#49113=CARTESIAN_POINT('Ctrl Pts',(90.6615535321299,4.7472562532542,129.518770819676));
#49114=CARTESIAN_POINT('Ctrl Pts',(90.6538054641269,4.71139088719918,129.386331931658));
#49115=CARTESIAN_POINT('Ctrl Pts',(90.6460573961239,4.66998875556181,129.255430431122));
#49116=CARTESIAN_POINT('Ctrl Pts',(90.638309328121,4.6232183205521,129.126553887632));
#49117=CARTESIAN_POINT('Ctrl Pts',(90.6305530253791,4.57639817736729,128.997540372618));
#49118=CARTESIAN_POINT('Ctrl Pts',(90.6227967226373,4.52419846705199,128.870556481898));
#49119=CARTESIAN_POINT('Ctrl Pts',(90.6150404198955,4.46683620015233,128.746070690586));
#49120=CARTESIAN_POINT('Ctrl Pts',(90.6072799773813,4.40944331728365,128.621518457458));
#49121=CARTESIAN_POINT('Ctrl Pts',(90.5995195348671,4.34688256568907,128.499467328225));
#49122=CARTESIAN_POINT('Ctrl Pts',(90.5917590923529,4.27941667773097,128.38036062564));
#49123=CARTESIAN_POINT('Ctrl Pts',(90.5839861920874,4.21184248754027,128.261062722402));
#49124=CARTESIAN_POINT('Ctrl Pts',(90.576213291822,4.13934763278347,128.144719023184));
#49125=CARTESIAN_POINT('Ctrl Pts',(90.5684403915566,4.06223837835029,128.031744088012));
#49126=CARTESIAN_POINT('Ctrl Pts',(90.5609500557946,3.98793223954252,127.9228760763));
#49127=CARTESIAN_POINT('Ctrl Pts',(90.5534597200326,3.90934155030137,127.817136402007));
#49128=CARTESIAN_POINT('Ctrl Pts',(90.5459693842705,3.82677412647474,127.714865052357));
#49129=CARTESIAN_POINT('Ctrl Pts',(90.5381950501515,3.74107613367761,127.608716053401));
#49130=CARTESIAN_POINT('Ctrl Pts',(90.5304207160324,3.65082243222353,127.505967325787));
#49131=CARTESIAN_POINT('Ctrl Pts',(90.5226463819133,3.55631287019784,127.407034929357));
#49132=CARTESIAN_POINT('Ctrl Pts',(90.5148816289662,3.4619197827609,127.308224458264));
#49133=CARTESIAN_POINT('Ctrl Pts',(90.5071168760191,3.36328153814516,127.213221240201));
#49134=CARTESIAN_POINT('Ctrl Pts',(90.499352123072,3.26073921681105,127.122409664274));
#49135=CARTESIAN_POINT('Ctrl Pts',(90.491595082187,3.15829874195586,127.031688283683));
#49136=CARTESIAN_POINT('Ctrl Pts',(90.483838041302,3.05196219774392,126.945150517803));
#49137=CARTESIAN_POINT('Ctrl Pts',(90.476081000417,2.94210836471689,126.863144887266));
#49138=CARTESIAN_POINT('Ctrl Pts',(90.4683298091768,2.83233737331973,126.781201097813));
#49139=CARTESIAN_POINT('Ctrl Pts',(90.4605786179367,2.71905468460876,126.703782873872));
#49140=CARTESIAN_POINT('Ctrl Pts',(90.4528274266965,2.60267281596168,126.631199073179));
#49141=CARTESIAN_POINT('Ctrl Pts',(90.4450795299194,2.48634041271368,126.558646122537));
#49142=CARTESIAN_POINT('Ctrl Pts',(90.4373316331424,2.36691178044942,126.490923714845));
#49143=CARTESIAN_POINT('Ctrl Pts',(90.4295837363653,2.24482894611593,126.428297767791));
#49144=CARTESIAN_POINT('Ctrl Pts',(90.4218374602812,2.12277164887941,126.365684920735));
#49145=CARTESIAN_POINT('Ctrl Pts',(90.4140911841971,1.99806160154545,126.30816659218));
#49146=CARTESIAN_POINT('Ctrl Pts',(90.406344908113,1.87116564096279,126.255962854993));
#49147=CARTESIAN_POINT('Ctrl Pts',(90.3985985748476,1.7442687436634,126.20375873245));
#49148=CARTESIAN_POINT('Ctrl Pts',(90.3908522415823,1.61518626248192,126.156869428302));
#49149=CARTESIAN_POINT('Ctrl Pts',(90.3831059083169,1.48440485630412,126.115466794383));
#49150=CARTESIAN_POINT('Ctrl Pts',(90.3753578403139,1.35359416253691,126.074054888632));
#49151=CARTESIAN_POINT('Ctrl Pts',(90.367609772311,1.22108415935881,126.038132216061));
#49152=CARTESIAN_POINT('Ctrl Pts',(90.359861704308,1.0873761107933,126.007820587901));
#49153=CARTESIAN_POINT('Ctrl Pts',(90.3521054015661,0.953525955722621,125.977476744183));
#49154=CARTESIAN_POINT('Ctrl Pts',(90.3443490988243,0.818475593614946,125.952755944155));
#49155=CARTESIAN_POINT('Ctrl Pts',(90.3365927960824,0.682736465352775,125.933728832943));
#49156=CARTESIAN_POINT('Ctrl Pts',(90.3288323535683,0.546924889030731,125.914691566389));
#49157=CARTESIAN_POINT('Ctrl Pts',(90.3210719110541,0.410424202971469,125.901354081903));
#49158=CARTESIAN_POINT('Ctrl Pts',(90.3133114685399,0.273749400421997,125.893734962085));
#49159=CARTESIAN_POINT('Ctrl Pts',(90.3055385682745,0.136855195346147,125.886103611379));
#49160=CARTESIAN_POINT('Ctrl Pts',(90.297765668009,-0.000213293611603577,
125.884208974567));
#49161=CARTESIAN_POINT('Ctrl Pts',(90.2899927677436,-0.136941741707901,
125.888017462143));
#49162=CARTESIAN_POINT('Ctrl Pts',(90.2825024319816,-0.26869976631716,125.891687501602));
#49163=CARTESIAN_POINT('Ctrl Pts',(90.2750120962196,-0.400141736222104,
125.900653197474));
#49164=CARTESIAN_POINT('Ctrl Pts',(90.2675217604576,-0.530815228556763,
125.914839346968));
#49165=CARTESIAN_POINT('Ctrl Pts',(90.2597474263385,-0.6664432460714,125.929563368632));
#49166=CARTESIAN_POINT('Ctrl Pts',(90.2519730922194,-0.801672990813378,
125.94995816673));
#49167=CARTESIAN_POINT('Ctrl Pts',(90.2441987581003,-0.935992344640633,
125.975996361084));
#49168=CARTESIAN_POINT('Ctrl Pts',(90.2364340051532,-1.07014616186876,126.00200246569));
#49169=CARTESIAN_POINT('Ctrl Pts',(90.2286692522061,-1.20339144044358,126.03363805452));
#49170=CARTESIAN_POINT('Ctrl Pts',(90.220904499259,-1.33522042060583,126.070823938623));
#49171=CARTESIAN_POINT('Ctrl Pts',(90.213147458374,-1.46691846636626,126.107972889182));
#49172=CARTESIAN_POINT('Ctrl Pts',(90.205390417489,-1.59720263923891,126.150661059174));
#49173=CARTESIAN_POINT('Ctrl Pts',(90.197633376604,-1.72557497880962,126.198758153718));
#49174=CARTESIAN_POINT('Ctrl Pts',(90.1898821853638,-1.85385051180152,126.246818977869));
#49175=CARTESIAN_POINT('Ctrl Pts',(90.1821309941237,-1.9802167165337,126.300280471128));
#49176=CARTESIAN_POINT('Ctrl Pts',(90.1743798028835,-2.10419076652649,126.358962516095));
#49177=CARTESIAN_POINT('Ctrl Pts',(90.1666319061064,-2.22811212424007,126.417619619626));
#49178=CARTESIAN_POINT('Ctrl Pts',(90.1588840093293,-2.34964299677482,126.481492694776));
#49179=CARTESIAN_POINT('Ctrl Pts',(90.1511361125522,-2.4683207336868,126.550353586759));
#49180=CARTESIAN_POINT('Ctrl Pts',(90.1433898364681,-2.58697364577476,126.619200074529));
#49181=CARTESIAN_POINT('Ctrl Pts',(90.135643560384,-2.70277427138817,126.693032107776));
#49182=CARTESIAN_POINT('Ctrl Pts',(90.1278972842998,-2.81528512027138,126.771575878198));
#49183=CARTESIAN_POINT('Ctrl Pts',(90.1201509510345,-2.9277967996838,126.850120228412));
#49184=CARTESIAN_POINT('Ctrl Pts',(90.1124046177692,-3.03701833333117,126.933376161409));
#49185=CARTESIAN_POINT('Ctrl Pts',(90.1046582845038,-3.14254208638309,127.0210271274));
#49186=CARTESIAN_POINT('Ctrl Pts',(90.0969102165008,-3.24808947074835,127.108697722217));
#49187=CARTESIAN_POINT('Ctrl Pts',(90.0891621484978,-3.34993712602023,127.200765058785));
#49188=CARTESIAN_POINT('Ctrl Pts',(90.0814140804948,-3.44771162351129,127.29687325143));
#49189=CARTESIAN_POINT('Ctrl Pts',(90.073657777753,-3.54559003690134,127.393083589005));
#49190=CARTESIAN_POINT('Ctrl Pts',(90.0659014750111,-3.63938636560129,127.493343087217));
#49191=CARTESIAN_POINT('Ctrl Pts',(90.0581451722692,-3.72876472757801,127.597259641783));
#49192=CARTESIAN_POINT('Ctrl Pts',(90.0503847297551,-3.81819079347783,127.701231659743));
#49193=CARTESIAN_POINT('Ctrl Pts',(90.0426242872409,-3.90319395194257,127.808864316674));
#49194=CARTESIAN_POINT('Ctrl Pts',(90.0348638447267,-3.98348020247577,127.919734378522));
#49195=CARTESIAN_POINT('Ctrl Pts',(90.0270909444613,-4.06389533562576,128.030782418835));
#49196=CARTESIAN_POINT('Ctrl Pts',(90.0193180441958,-4.13957821360021,128.145077923101));
#49197=CARTESIAN_POINT('Ctrl Pts',(90.0115451439304,-4.21027909111514,128.262170019397));
#49198=CARTESIAN_POINT('Ctrl Pts',(90.0040548081685,-4.27840981364644,128.375005523054));
#49199=CARTESIAN_POINT('Ctrl Pts',(89.9965644724066,-4.34191431516899,128.490437552582));
#49200=CARTESIAN_POINT('Ctrl Pts',(89.9890741366447,-4.40061132031051,128.608044822865));
#49201=CARTESIAN_POINT('Ctrl Pts',(89.98074935034,-4.46584738449569,128.738753969171));
#49202=CARTESIAN_POINT('Ctrl Pts',(89.9724245640352,-4.52532942677357,128.872518646867));
#49203=CARTESIAN_POINT('Ctrl Pts',(89.9640997777305,-4.57878128013611,129.008825864025));
#49204=CARTESIAN_POINT('Ctrl Pts',(89.9557953738861,-4.63210226163665,129.144799345714));
#49205=CARTESIAN_POINT('Ctrl Pts',(89.9474909700418,-4.67942238345934,129.283302669902));
#49206=CARTESIAN_POINT('Ctrl Pts',(89.9391865661974,-4.72051238125432,129.423800614913));
#49207=CARTESIAN_POINT('Ctrl Pts',(89.9360759723297,-4.73590352763438,129.476427155527));
#49208=CARTESIAN_POINT('Ctrl Pts',(89.9329653784619,-4.75042102772514,129.529333307741));
#49209=CARTESIAN_POINT('Ctrl Pts',(89.9298547845941,-4.76405452823405,129.582490119308));
#49210=CARTESIAN_POINT('Origin',(213.235140564004,0.,130.804360617566));
#49211=CARTESIAN_POINT('',(87.8349528638408,-4.76405452823403,129.582490119308));
#49212=CARTESIAN_POINT('',(88.1801477108009,-4.76405452823403,129.582490119308));
#49213=CARTESIAN_POINT('',(213.235140564004,-4.76405452823405,129.582490119308));
#49214=CARTESIAN_POINT('',(89.5148594360324,-4.91824791378463,130.808890634465));
#49215=CARTESIAN_POINT('Ctrl Pts',(89.5148594359911,-4.91824791378396,130.808890635194));
#49216=CARTESIAN_POINT('Ctrl Pts',(89.5043441766185,-4.91807698000317,130.994473734362));
#49217=CARTESIAN_POINT('Ctrl Pts',(89.4938289172459,-4.90739846811374,131.179592062533));
#49218=CARTESIAN_POINT('Ctrl Pts',(89.4833136578734,-4.88639072837316,131.363260172199));
#49219=CARTESIAN_POINT('Ctrl Pts',(89.4727984003083,-4.8653829922438,131.546928250292));
#49220=CARTESIAN_POINT('Ctrl Pts',(89.4622831427433,-4.83404617532037,131.729146731365));
#49221=CARTESIAN_POINT('Ctrl Pts',(89.4517678851783,-4.79260396698406,131.908955691857));
#49222=CARTESIAN_POINT('Ctrl Pts',(89.4439935510592,-4.76196414934318,132.041895368116));
#49223=CARTESIAN_POINT('Ctrl Pts',(89.4362192169401,-4.72574028641383,132.173769790985));
#49224=CARTESIAN_POINT('Ctrl Pts',(89.428444882821,-4.68402005236109,132.304073660644));
#49225=CARTESIAN_POINT('Ctrl Pts',(89.4206801298739,-4.64235123476817,132.43421694243));
#49226=CARTESIAN_POINT('Ctrl Pts',(89.4129153769269,-4.59519964193923,132.562793153437));
#49227=CARTESIAN_POINT('Ctrl Pts',(89.4051506239798,-4.54270387942175,132.689307440791));
#49228=CARTESIAN_POINT('Ctrl Pts',(89.3973935830948,-4.49026025643574,132.815696072372));
#49229=CARTESIAN_POINT('Ctrl Pts',(89.3896365422098,-4.43248317560102,132.940026497001));
#49230=CARTESIAN_POINT('Ctrl Pts',(89.3818795013248,-4.36956083329973,133.061819628621));
#49231=CARTESIAN_POINT('Ctrl Pts',(89.3741283100847,-4.30668594122627,133.183520915092));
#49232=CARTESIAN_POINT('Ctrl Pts',(89.3663771188446,-4.23867368947907,133.302688371102));
#49233=CARTESIAN_POINT('Ctrl Pts',(89.3586259276045,-4.1657599607861,133.418863823074));
#49234=CARTESIAN_POINT('Ctrl Pts',(89.3508780308274,-4.09287722237272,133.53498989738));
#49235=CARTESIAN_POINT('Ctrl Pts',(89.3431301340503,-4.01509735785471,133.64812616647));
#49236=CARTESIAN_POINT('Ctrl Pts',(89.3353822372732,-3.93270156814569,133.757840165219));
#49237=CARTESIAN_POINT('Ctrl Pts',(89.3276359611891,-3.85032301385957,133.867531214165));
#49238=CARTESIAN_POINT('Ctrl Pts',(89.319889685105,-3.76333068954983,133.973801104242));
#49239=CARTESIAN_POINT('Ctrl Pts',(89.3121434090209,-3.6720481584663,134.076247746488));
#49240=CARTESIAN_POINT('Ctrl Pts',(89.3043970757555,-3.58076495355592,134.178695144971));
#49241=CARTESIAN_POINT('Ctrl Pts',(89.2966507424901,-3.4851917387692,134.277318947407));
#49242=CARTESIAN_POINT('Ctrl Pts',(89.2889044092248,-3.38569099349451,134.371751759433));
#49243=CARTESIAN_POINT('Ctrl Pts',(89.2811563412218,-3.2861679657178,134.466205719032));
#49244=CARTESIAN_POINT('Ctrl Pts',(89.2734082732188,-3.1827159407914,134.556466551543));
#49245=CARTESIAN_POINT('Ctrl Pts',(89.2656602052159,-3.07573241861856,134.642205475238));
#49246=CARTESIAN_POINT('Ctrl Pts',(89.257903902474,-2.96863519308523,134.728035523281));
#49247=CARTESIAN_POINT('Ctrl Pts',(89.2501475997321,-2.85799927821717,134.809333817241));
#49248=CARTESIAN_POINT('Ctrl Pts',(89.2423912969903,-2.74425370443405,134.885813136976));
#49249=CARTESIAN_POINT('Ctrl Pts',(89.2346308544761,-2.63044742121331,134.962333276027));
#49250=CARTESIAN_POINT('Ctrl Pts',(89.2268704119619,-2.51352850507649,135.034029111586));
#49251=CARTESIAN_POINT('Ctrl Pts',(89.2191099694478,-2.39395195175127,135.100658688604));
#49252=CARTESIAN_POINT('Ctrl Pts',(89.2113370691823,-2.27418344352713,135.167395225334));
#49253=CARTESIAN_POINT('Ctrl Pts',(89.2035641689169,-2.15174912212869,135.22904907564));
#49254=CARTESIAN_POINT('Ctrl Pts',(89.1957912686514,-2.02712620077586,135.285425494203));
#49255=CARTESIAN_POINT('Ctrl Pts',(89.1883009328894,-1.90703363652032,135.339752487947));
#49256=CARTESIAN_POINT('Ctrl Pts',(89.1808105971274,-1.78490911747776,135.389178968742));
#49257=CARTESIAN_POINT('Ctrl Pts',(89.1733202613653,-1.66119239025523,135.433574687477));
#49258=CARTESIAN_POINT('Ctrl Pts',(89.1655459272463,-1.53278490571734,135.479653683381));
#49259=CARTESIAN_POINT('Ctrl Pts',(89.1577715931272,-1.40225533615003,135.520458868357));
#49260=CARTESIAN_POINT('Ctrl Pts',(89.1499972590081,-1.27007619462908,135.55579087827));
#49261=CARTESIAN_POINT('Ctrl Pts',(89.142232506061,-1.13805995208687,135.591079344639));
#49262=CARTESIAN_POINT('Ctrl Pts',(89.1344677531139,-1.00439855663392,135.620907956887));
#49263=CARTESIAN_POINT('Ctrl Pts',(89.1267030001668,-0.869583261690838,
135.645125847722));
#49264=CARTESIAN_POINT('Ctrl Pts',(89.1189459592818,-0.734901867199259,
135.669319685007));
#49265=CARTESIAN_POINT('Ctrl Pts',(89.1111889183968,-0.599069236262726,
135.68791382202));
#49266=CARTESIAN_POINT('Ctrl Pts',(89.1034318775118,-0.462590162292759,
135.700807635992));
#49267=CARTESIAN_POINT('Ctrl Pts',(89.0956806862717,-0.326214008254124,
135.713691726638));
#49268=CARTESIAN_POINT('Ctrl Pts',(89.0879294950315,-0.189192769153895,
135.720884013836));
#49269=CARTESIAN_POINT('Ctrl Pts',(89.0801783037914,-0.0520394197748442,
135.722335298396));
#49270=CARTESIAN_POINT('Ctrl Pts',(89.0724304070143,0.0850556357720356,
135.723785966122));
#49271=CARTESIAN_POINT('Ctrl Pts',(89.0646825102372,0.222282299794044,135.719500480213));
#49272=CARTESIAN_POINT('Ctrl Pts',(89.0569346134602,0.359124731170519,135.709481664998));
#49273=CARTESIAN_POINT('Ctrl Pts',(89.0491883373761,0.495938538060332,135.699464945503));
#49274=CARTESIAN_POINT('Ctrl Pts',(89.041442061292,0.632367882496771,135.683717310684));
#49275=CARTESIAN_POINT('Ctrl Pts',(89.0336957852079,0.767899581808212,135.66229364456));
#49276=CARTESIAN_POINT('Ctrl Pts',(89.0259494519425,0.90343228158387,135.640869820291));
#49277=CARTESIAN_POINT('Ctrl Pts',(89.0182031186771,1.03806693684196,135.613769942154));
#49278=CARTESIAN_POINT('Ctrl Pts',(89.0104567854118,1.17129851933729,135.581100388696));
#49279=CARTESIAN_POINT('Ctrl Pts',(89.0027087174088,1.30455993812167,135.548423519119));
#49280=CARTESIAN_POINT('Ctrl Pts',(88.9949606494058,1.43641727926142,135.51017458535));
#49281=CARTESIAN_POINT('Ctrl Pts',(88.9872125814028,1.56637907097063,135.466510300762));
#49282=CARTESIAN_POINT('Ctrl Pts',(88.979456278661,1.69647898761862,135.422799609253));
#49283=CARTESIAN_POINT('Ctrl Pts',(88.9716999759192,1.82467895923258,135.373662194409));
#49284=CARTESIAN_POINT('Ctrl Pts',(88.9639436731774,1.95050543795275,135.319303762171));
#49285=CARTESIAN_POINT('Ctrl Pts',(88.9561832306632,2.07639907405327,135.264916317202));
#49286=CARTESIAN_POINT('Ctrl Pts',(88.948422788149,2.19991634111552,135.205302472128));
#49287=CARTESIAN_POINT('Ctrl Pts',(88.9406623456348,2.32060773920036,135.140714245127));
#49288=CARTESIAN_POINT('Ctrl Pts',(88.9328894453694,2.44149288183189,135.076022335371));
#49289=CARTESIAN_POINT('Ctrl Pts',(88.925116545104,2.55954275356234,135.006340285328));
#49290=CARTESIAN_POINT('Ctrl Pts',(88.9173436448386,2.67433556423744,134.931964323393));
#49291=CARTESIAN_POINT('Ctrl Pts',(88.9098533090765,2.78495536709909,134.860292115016));
#49292=CARTESIAN_POINT('Ctrl Pts',(88.9023629733145,2.89255055082243,134.784261518578));
#49293=CARTESIAN_POINT('Ctrl Pts',(88.8948726375524,2.99677383935875,134.704172102527));
#49294=CARTESIAN_POINT('Ctrl Pts',(88.8870983034333,3.10494878555767,134.621046071925));
#49295=CARTESIAN_POINT('Ctrl Pts',(88.8793239693143,3.20983376405457,134.53328404746));
#49296=CARTESIAN_POINT('Ctrl Pts',(88.8715496351952,3.31100563929601,134.441175806581));
#49297=CARTESIAN_POINT('Ctrl Pts',(88.8637848822481,3.41205282924321,134.349181080877));
#49298=CARTESIAN_POINT('Ctrl Pts',(88.856020129301,3.50939573462108,134.252851056919));
#49299=CARTESIAN_POINT('Ctrl Pts',(88.8482553763539,3.60264189203036,134.152517492667));
#49300=CARTESIAN_POINT('Ctrl Pts',(88.8404983354689,3.6957954360415,134.052283581126));
#49301=CARTESIAN_POINT('Ctrl Pts',(88.8327412945839,3.78486006504195,133.948054326982));
#49302=CARTESIAN_POINT('Ctrl Pts',(88.8249842536989,3.86947826907545,133.840200038163));
#49303=CARTESIAN_POINT('Ctrl Pts',(88.8172330624588,3.95403266186306,133.732427083103));
#49304=CARTESIAN_POINT('Ctrl Pts',(88.8094818712187,4.03414706344264,133.621034840917));
#49305=CARTESIAN_POINT('Ctrl Pts',(88.8017306799786,4.1095028057418,133.506428298454));
#49306=CARTESIAN_POINT('Ctrl Pts',(88.7939827832015,4.18482651984035,133.391870466829));
#49307=CARTESIAN_POINT('Ctrl Pts',(88.7862348864244,4.25539538302532,133.274101378114));
#49308=CARTESIAN_POINT('Ctrl Pts',(88.7784869896473,4.32093294675865,133.153556550671));
#49309=CARTESIAN_POINT('Ctrl Pts',(88.7707407135633,4.38645680144647,133.033036938607));
#49310=CARTESIAN_POINT('Ctrl Pts',(88.7629944374792,4.44695126341655,132.909743085976));
#49311=CARTESIAN_POINT('Ctrl Pts',(88.755248161395,4.50218512038031,132.784136414046));
#49312=CARTESIAN_POINT('Ctrl Pts',(88.7475018281297,4.55741938506786,132.658528814916));
#49313=CARTESIAN_POINT('Ctrl Pts',(88.7397554948643,4.60739280988365,132.530608720311));
#49314=CARTESIAN_POINT('Ctrl Pts',(88.732009161599,4.65192191401102,132.400858525001));
#49315=CARTESIAN_POINT('Ctrl Pts',(88.724261093596,4.69646099012249,132.271079273035));
#49316=CARTESIAN_POINT('Ctrl Pts',(88.716513025593,4.73555319255742,132.139469474556));
#49317=CARTESIAN_POINT('Ctrl Pts',(88.7087649575901,4.76906471620876,132.006527326102));
#49318=CARTESIAN_POINT('Ctrl Pts',(88.7010086548482,4.80261185630625,131.873443885151));
#49319=CARTESIAN_POINT('Ctrl Pts',(88.6932523521064,4.83056637366972,131.739025645249));
#49320=CARTESIAN_POINT('Ctrl Pts',(88.6854960493645,4.85284537034838,131.603782204708));
#49321=CARTESIAN_POINT('Ctrl Pts',(88.6777356068504,4.87513625799839,131.46846658067));
#49322=CARTESIAN_POINT('Ctrl Pts',(88.6699751643362,4.89174554170988,131.332325266288));
#49323=CARTESIAN_POINT('Ctrl Pts',(88.662214721822,4.902642285817,131.195872660572));
#49324=CARTESIAN_POINT('Ctrl Pts',(88.6544418215566,4.91355652234512,131.05920100902));
#49325=CARTESIAN_POINT('Ctrl Pts',(88.6466689212912,4.91873987934418,130.92221745846));
#49326=CARTESIAN_POINT('Ctrl Pts',(88.6388960210257,4.91821359427175,130.785436991578));
#49327=CARTESIAN_POINT('Ctrl Pts',(88.6314056852637,4.91770644098734,130.653628839197));
#49328=CARTESIAN_POINT('Ctrl Pts',(88.6239153495017,4.91189757186654,130.522009569351));
#49329=CARTESIAN_POINT('Ctrl Pts',(88.6164250137396,4.90085131114236,130.39103327928));
#49330=CARTESIAN_POINT('Ctrl Pts',(88.6086506796205,4.88938622808539,130.255090983363));
#49331=CARTESIAN_POINT('Ctrl Pts',(88.6008763455014,4.87224244418924,130.119410762527));
#49332=CARTESIAN_POINT('Ctrl Pts',(88.5931020113824,4.84943504232513,129.984505244485));
#49333=CARTESIAN_POINT('Ctrl Pts',(88.5853372584353,4.82665574854547,129.849765985439));
#49334=CARTESIAN_POINT('Ctrl Pts',(88.5775725054882,4.79822678927128,129.715799911309));
#49335=CARTESIAN_POINT('Ctrl Pts',(88.5698077525411,4.76421514581565,129.583116535951));
#49336=CARTESIAN_POINT('Ctrl Pts',(88.5620507116561,4.73023728320381,129.450564943591));
#49337=CARTESIAN_POINT('Ctrl Pts',(88.5542936707711,4.69068786726586,129.319293890966));
#49338=CARTESIAN_POINT('Ctrl Pts',(88.5465366298861,4.64568520568527,129.189804321806));
#49339=CARTESIAN_POINT('Ctrl Pts',(88.538785438646,4.60071648096183,129.060412401738));
#49340=CARTESIAN_POINT('Ctrl Pts',(88.5310342474059,4.55030282377528,128.932799658923));
#49341=CARTESIAN_POINT('Ctrl Pts',(88.5232830561657,4.49461271315434,128.80745310312));
#49342=CARTESIAN_POINT('Ctrl Pts',(88.5155351593886,4.43894627231599,128.682159822946));
#49343=CARTESIAN_POINT('Ctrl Pts',(88.5077872626115,4.37800799687756,128.559131170614));
#49344=CARTESIAN_POINT('Ctrl Pts',(88.5000393658345,4.31201487358479,128.438835138421));
#49345=CARTESIAN_POINT('Ctrl Pts',(88.4922930897503,4.24603555463073,128.318564269565));
#49346=CARTESIAN_POINT('Ctrl Pts',(88.4845468136662,4.17500367890266,128.20102522645));
#49347=CARTESIAN_POINT('Ctrl Pts',(88.4768005375821,4.09918247729292,128.08666194399));
#49348=CARTESIAN_POINT('Ctrl Pts',(88.4690542043168,4.02336071598834,127.972297817327));
#49349=CARTESIAN_POINT('Ctrl Pts',(88.4613078710514,3.94274977429366,127.861109823953));
#49350=CARTESIAN_POINT('Ctrl Pts',(88.4535615377861,3.8576563287277,127.753513077631));
#49351=CARTESIAN_POINT('Ctrl Pts',(88.4458134697831,3.77254382707466,127.645892235764));
#49352=CARTESIAN_POINT('Ctrl Pts',(88.4380654017801,3.68294706652733,127.541864547881));
#49353=CARTESIAN_POINT('Ctrl Pts',(88.4303173337771,3.58921286901418,127.441811875406));
#49354=CARTESIAN_POINT('Ctrl Pts',(88.4225610310352,3.4953790496804,127.34165286576));
#49355=CARTESIAN_POINT('Ctrl Pts',(88.4148047282934,3.39739927699039,127.245477596574));
#49356=CARTESIAN_POINT('Ctrl Pts',(88.4070484255516,3.29565748206928,127.153631262577));
#49357=CARTESIAN_POINT('Ctrl Pts',(88.3992879830374,3.19386138448877,127.061735907426));
#49358=CARTESIAN_POINT('Ctrl Pts',(88.3915275405232,3.0882995645272,126.97417434078));
#49359=CARTESIAN_POINT('Ctrl Pts',(88.383767098009,2.97938807915765,126.891250634921));
#49360=CARTESIAN_POINT('Ctrl Pts',(88.3759941977436,2.87030175940308,126.808193812568));
#49361=CARTESIAN_POINT('Ctrl Pts',(88.3682212974782,2.75785534980964,126.729789952438));
#49362=CARTESIAN_POINT('Ctrl Pts',(88.3604483972127,2.64249359926074,126.656299547576));
#49363=CARTESIAN_POINT('Ctrl Pts',(88.3529580614507,2.53132553892318,126.585480704042));
#49364=CARTESIAN_POINT('Ctrl Pts',(88.3454677256887,2.41745068390158,126.519224439819));
#49365=CARTESIAN_POINT('Ctrl Pts',(88.3379773899267,2.30128584788295,126.457722087755));
#49366=CARTESIAN_POINT('Ctrl Pts',(88.3302030558076,2.18071658679904,126.393887855321));
#49367=CARTESIAN_POINT('Ctrl Pts',(88.3224287216885,2.05729834039006,126.334972932714));
#49368=CARTESIAN_POINT('Ctrl Pts',(88.3146543875694,1.93147054953006,126.28124171809));
#49369=CARTESIAN_POINT('Ctrl Pts',(88.3068896346223,1.80579783017681,126.227576722386));
#49370=CARTESIAN_POINT('Ctrl Pts',(88.2991248816753,1.6777218309918,126.179082875603));
#49371=CARTESIAN_POINT('Ctrl Pts',(88.2913601287282,1.54770742544596,126.135979229149));
#49372=CARTESIAN_POINT('Ctrl Pts',(88.2836030878432,1.4178221520406,126.092918393844));
#49373=CARTESIAN_POINT('Ctrl Pts',(88.2758460469582,1.28600267231488,126.055237227153));
#49374=CARTESIAN_POINT('Ctrl Pts',(88.2680890060732,1.15273439261057,126.023106965793));
#49375=CARTESIAN_POINT('Ctrl Pts',(88.260337814833,1.01956661155247,125.991000934113));
#49376=CARTESIAN_POINT('Ctrl Pts',(88.2525866235929,0.884952583710046,125.964437567087));
#49377=CARTESIAN_POINT('Ctrl Pts',(88.2448354323528,0.749393111216389,125.943538359207));
#49378=CARTESIAN_POINT('Ctrl Pts',(88.2370875355757,0.6138912551148,125.922648034047));
#49379=CARTESIAN_POINT('Ctrl Pts',(88.2293396387986,0.477445139180659,125.907417139308));
#49380=CARTESIAN_POINT('Ctrl Pts',(88.2215917420216,0.340565785224577,125.897916079162));
#49381=CARTESIAN_POINT('Ctrl Pts',(88.2138454659375,0.203715063478565,125.888417006433));
#49382=CARTESIAN_POINT('Ctrl Pts',(88.2060991898533,0.0664316737464815,
125.884645411356));
#49383=CARTESIAN_POINT('Ctrl Pts',(88.1983529137692,-0.0707686062289486,
125.886619787991));
#49384=CARTESIAN_POINT('Ctrl Pts',(88.1906065805039,-0.207969898985678,
125.888594179199));
#49385=CARTESIAN_POINT('Ctrl Pts',(88.1828602472385,-0.345087689836836,
125.896314621131));
#49386=CARTESIAN_POINT('Ctrl Pts',(88.1751139139732,-0.481606965666912,
125.909747477274));
#49387=CARTESIAN_POINT('Ctrl Pts',(88.1673658459702,-0.618156814042252,
125.923183341611));
#49388=CARTESIAN_POINT('Ctrl Pts',(88.1596177779672,-0.754107491674002,
125.942334127454));
#49389=CARTESIAN_POINT('Ctrl Pts',(88.1518697099643,-0.888950262007253,
125.967114449117));
#49390=CARTESIAN_POINT('Ctrl Pts',(88.1441134072224,-1.02393634484146,125.991921107601));
#49391=CARTESIAN_POINT('Ctrl Pts',(88.1363571044805,-1.15781178306082,126.022369183089));
#49392=CARTESIAN_POINT('Ctrl Pts',(88.1286008017387,-1.2900786304122,126.058322249637));
#49393=CARTESIAN_POINT('Ctrl Pts',(88.1208403592245,-1.42241607256257,126.094294505419));
#49394=CARTESIAN_POINT('Ctrl Pts',(88.1130799167104,-1.55314284063411,126.135777488636));
#49395=CARTESIAN_POINT('Ctrl Pts',(88.1053194741962,-1.68177822104757,126.182585517271));
#49396=CARTESIAN_POINT('Ctrl Pts',(88.0975465739308,-1.81062009839329,126.229468686308));
#49397=CARTESIAN_POINT('Ctrl Pts',(88.0897736736653,-1.93736351747529,126.281693833825));
#49398=CARTESIAN_POINT('Ctrl Pts',(88.0820007733999,-2.06154892048095,126.339027582846));
#49399=CARTESIAN_POINT('Ctrl Pts',(88.0745104376379,-2.1812198712832,126.394277105674));
#49400=CARTESIAN_POINT('Ctrl Pts',(88.0670201018759,-2.29851528353681,126.454270117095));
#49401=CARTESIAN_POINT('Ctrl Pts',(88.0595297661138,-2.41304888551663,126.518759360029));
#49402=CARTESIAN_POINT('Ctrl Pts',(88.051754348916,-2.53194162502168,126.585703057148));
#49403=CARTESIAN_POINT('Ctrl Pts',(88.0439789317182,-2.6482348313707,126.657704103374));
#49404=CARTESIAN_POINT('Ctrl Pts',(88.0362035145204,-2.7614683395498,126.734535600177));
#49405=CARTESIAN_POINT('Ctrl Pts',(88.0284379153951,-2.87455886700438,126.811270081324));
#49406=CARTESIAN_POINT('Ctrl Pts',(88.0206723162697,-2.98459706372859,126.892822658075));
#49407=CARTESIAN_POINT('Ctrl Pts',(88.0129067171443,-3.09114722263641,126.978920523866));
#49408=CARTESIAN_POINT('Ctrl Pts',(88.0051504969231,-3.19756869556548,127.06491440494));
#49409=CARTESIAN_POINT('Ctrl Pts',(87.9973942767018,-3.300510218846,127.15544239732));
#49410=CARTESIAN_POINT('Ctrl Pts',(87.9896380564805,-3.39956548708786,127.250188764447));
#49411=CARTESIAN_POINT('Ctrl Pts',(87.9818871539942,-3.49855284213875,127.344870172605));
#49412=CARTESIAN_POINT('Ctrl Pts',(87.974136251508,-3.59365896174388,127.443763932585));
#49413=CARTESIAN_POINT('Ctrl Pts',(87.9663853490217,-3.68451097936713,127.546514411033));
#49414=CARTESIAN_POINT('Ctrl Pts',(87.958638082001,-3.77532038396717,127.64921669563));
#49415=CARTESIAN_POINT('Ctrl Pts',(87.9508908149804,-3.86187939899171,127.755771806658));
#49416=CARTESIAN_POINT('Ctrl Pts',(87.9431435479597,-3.94385265596307,127.865787955447));
#49417=CARTESIAN_POINT('Ctrl Pts',(87.9353982369455,-4.02580521657647,127.975776327695));
#49418=CARTESIAN_POINT('Ctrl Pts',(87.9276529259312,-4.10317409112435,128.089223684663));
#49419=CARTESIAN_POINT('Ctrl Pts',(87.9199076149169,-4.17566503793127,128.205706243953));
#49420=CARTESIAN_POINT('Ctrl Pts',(87.9121602487679,-4.24817521942896,128.322219710633));
#49421=CARTESIAN_POINT('Ctrl Pts',(87.9044128826188,-4.31580467586253,128.441769659617));
#49422=CARTESIAN_POINT('Ctrl Pts',(87.8966655164698,-4.37830322785507,128.563904434675));
#49423=CARTESIAN_POINT('Ctrl Pts',(87.8889171584985,-4.44080978094808,128.686054845497));
#49424=CARTESIAN_POINT('Ctrl Pts',(87.8811688005273,-4.49818395030201,128.810790389823));
#49425=CARTESIAN_POINT('Ctrl Pts',(87.873420442556,-4.55022256848223,128.937636845881));
#49426=CARTESIAN_POINT('Ctrl Pts',(87.8656659507611,-4.6023023819335,129.064583717251));
#49427=CARTESIAN_POINT('Ctrl Pts',(87.8579114589662,-4.64903806660193,129.193644473272));
#49428=CARTESIAN_POINT('Ctrl Pts',(87.8501569671712,-4.69027535515693,129.3243267817));
#49429=CARTESIAN_POINT('Ctrl Pts',(87.8450889327278,-4.71722644418757,129.409735659262));
#49430=CARTESIAN_POINT('Ctrl Pts',(87.8400208982843,-4.7418299522699,129.495836834929));
#49431=CARTESIAN_POINT('Ctrl Pts',(87.8349528638408,-4.76405452823403,129.582490119308));
#49432=CARTESIAN_POINT('Ctrl Pts',(89.5849003473043,-4.76405452823408,129.582490119308));
#49433=CARTESIAN_POINT('Ctrl Pts',(89.5772536419592,-4.7977227201108,129.71376188845));
#49434=CARTESIAN_POINT('Ctrl Pts',(89.569606936614,-4.8259539416985,129.846398820212));
#49435=CARTESIAN_POINT('Ctrl Pts',(89.5619602312689,-4.84865503925609,129.979904813537));
#49436=CARTESIAN_POINT('Ctrl Pts',(89.5541100987295,-4.8719600597287,130.116962499835));
#49437=CARTESIAN_POINT('Ctrl Pts',(89.54625996619,-4.88943651653312,130.254935691279));
#49438=CARTESIAN_POINT('Ctrl Pts',(89.5384098336506,-4.90104037889306,130.39328122504));
#49439=CARTESIAN_POINT('Ctrl Pts',(89.5305597011112,-4.912644241253,130.531626758801));
#49440=CARTESIAN_POINT('Ctrl Pts',(89.5227095685718,-4.91837552381983,130.670344177938));
#49441=CARTESIAN_POINT('Ctrl Pts',(89.5148594360324,-4.91824791378463,130.808890634465));
#49442=CARTESIAN_POINT('',(89.8601405640521,-4.91824989813527,130.803359621866));
#49443=CARTESIAN_POINT('Ctrl Pts',(89.9298547845941,-4.76405452823405,129.582490119308));
#49444=CARTESIAN_POINT('Ctrl Pts',(89.9215764202743,-4.80033798051544,129.723958749075));
#49445=CARTESIAN_POINT('Ctrl Pts',(89.9132980559544,-4.8303567890655,129.867204046601));
#49446=CARTESIAN_POINT('Ctrl Pts',(89.9050196916345,-4.85394887088816,130.011666842326));
#49447=CARTESIAN_POINT('Ctrl Pts',(89.8967633333281,-4.87747823891274,130.155745618927));
#49448=CARTESIAN_POINT('Ctrl Pts',(89.8885069750216,-4.8946148997633,130.301035139103));
#49449=CARTESIAN_POINT('Ctrl Pts',(89.8802506167151,-4.90524731660639,130.446964723038));
#49450=CARTESIAN_POINT('Ctrl Pts',(89.8735472658275,-4.91387979332768,130.565445192234));
#49451=CARTESIAN_POINT('Ctrl Pts',(89.8668439149397,-4.91822567592008,130.684347215093));
#49452=CARTESIAN_POINT('Ctrl Pts',(89.8601405640521,-4.91824989813527,130.803359621866));
#49453=CARTESIAN_POINT('Ctrl Pts',(89.8601405640085,-4.91824989813543,130.80335962264));
#49454=CARTESIAN_POINT('Ctrl Pts',(89.8521395031509,-4.9182788095368,130.945411788095));
#49455=CARTESIAN_POINT('Ctrl Pts',(89.8441384422934,-4.9121491106778,131.087386340008));
#49456=CARTESIAN_POINT('Ctrl Pts',(89.8361373814359,-4.89990706363619,131.228735251855));
#49457=CARTESIAN_POINT('Ctrl Pts',(89.8281295892336,-4.88765471728043,131.370203081466));
#49458=CARTESIAN_POINT('Ctrl Pts',(89.8201217970312,-4.86927979946688,131.511043870025));
#49459=CARTESIAN_POINT('Ctrl Pts',(89.8121140048289,-4.84488017921743,131.650716991398));
#49460=CARTESIAN_POINT('Ctrl Pts',(89.8040983150251,-4.82045649509702,131.79052786393));
#49461=CARTESIAN_POINT('Ctrl Pts',(89.7960826252213,-4.78999632098478,131.929168425915));
#49462=CARTESIAN_POINT('Ctrl Pts',(89.7880669354174,-4.75364812777663,132.066110410427));
#49463=CARTESIAN_POINT('Ctrl Pts',(89.7800364422495,-4.71723280677881,132.203305299195));
#49464=CARTESIAN_POINT('Ctrl Pts',(89.7720059490815,-4.67490783011908,132.338795001309));
#49465=CARTESIAN_POINT('Ctrl Pts',(89.7639754559136,-4.62687122199029,132.472067353661));
#49466=CARTESIAN_POINT('Ctrl Pts',(89.7559363960225,-4.57878336964621,132.605481877524));
#49467=CARTESIAN_POINT('Ctrl Pts',(89.7478973361315,-4.52497186587371,132.736674008009));
#49468=CARTESIAN_POINT('Ctrl Pts',(89.7398582762404,-4.46568186199103,132.865153807089));
#49469=CARTESIAN_POINT('Ctrl Pts',(89.7318046094637,-4.4062841288068,132.993867052587));
#49470=CARTESIAN_POINT('Ctrl Pts',(89.7237509426869,-4.34138816872011,133.119857807639));
#49471=CARTESIAN_POINT('Ctrl Pts',(89.7156972759102,-4.27128431534761,133.242661944303));
#49472=CARTESIAN_POINT('Ctrl Pts',(89.7140070215508,-4.25657134707327,133.268435325932));
#49473=CARTESIAN_POINT('Ctrl Pts',(89.7123167671913,-4.24162913377656,133.294068454993));
#49474=CARTESIAN_POINT('Ctrl Pts',(89.7106265128319,-4.22646059051327,133.3195572181));
#49475=CARTESIAN_POINT('Ctrl Pts',(89.7028521787128,-4.15669279327702,133.436792922634));
#49476=CARTESIAN_POINT('Ctrl Pts',(89.6950778445937,-4.08193287710072,133.55130923844));
#49477=CARTESIAN_POINT('Ctrl Pts',(89.6873035104746,-4.00241861517591,133.662651766381));
#49478=CARTESIAN_POINT('Ctrl Pts',(89.6795387575275,-3.92300234747264,133.773857074607));
#49479=CARTESIAN_POINT('Ctrl Pts',(89.6717740045805,-3.83884361732605,133.881896062399));
#49480=CARTESIAN_POINT('Ctrl Pts',(89.6640092516334,-3.75022550725323,133.986339829825));
#49481=CARTESIAN_POINT('Ctrl Pts',(89.6562522107484,-3.66169541393663,134.090679862229));
#49482=CARTESIAN_POINT('Ctrl Pts',(89.6484951698634,-3.56871500614797,134.19143148418));
#49483=CARTESIAN_POINT('Ctrl Pts',(89.6407381289784,-3.47160977485632,134.28819595145));
#49484=CARTESIAN_POINT('Ctrl Pts',(89.6329869377383,-3.37457777137482,134.384887447884));
#49485=CARTESIAN_POINT('Ctrl Pts',(89.6252357464982,-3.2734274115934,134.477597499527));
#49486=CARTESIAN_POINT('Ctrl Pts',(89.617484555258,-3.16852321023861,134.565961836286));
#49487=CARTESIAN_POINT('Ctrl Pts',(89.609736658481,-3.0636635959678,134.654288615845));
#49488=CARTESIAN_POINT('Ctrl Pts',(89.6019887617039,-2.95505361181128,134.738273102803));
#49489=CARTESIAN_POINT('Ctrl Pts',(89.5942408649268,-2.84309307680544,134.817589345052));
#49490=CARTESIAN_POINT('Ctrl Pts',(89.5864945888427,-2.73115596153001,134.896888996053));
#49491=CARTESIAN_POINT('Ctrl Pts',(89.5787483127586,-2.61587000828068,134.971522118788));
#49492=CARTESIAN_POINT('Ctrl Pts',(89.5710020366745,-2.49766610049364,135.041204621414));
#49493=CARTESIAN_POINT('Ctrl Pts',(89.5632557034092,-2.37946132015228,135.110887638421));
#49494=CARTESIAN_POINT('Ctrl Pts',(89.5555093701438,-2.25833887909073,135.175619763851));
#49495=CARTESIAN_POINT('Ctrl Pts',(89.5477630368785,-2.13475612494927,135.235161826094));
#49496=CARTESIAN_POINT('Ctrl Pts',(89.5400149688755,-2.01114569530671,135.294717222368));
#49497=CARTESIAN_POINT('Ctrl Pts',(89.5322669008725,-1.88507420836676,135.349080072989));
#49498=CARTESIAN_POINT('Ctrl Pts',(89.5245188328696,-1.75702057007165,135.398058668031));
#49499=CARTESIAN_POINT('Ctrl Pts',(89.5167625301277,-1.6288308348459,135.447089318106));
#49500=CARTESIAN_POINT('Ctrl Pts',(89.5090062273859,-1.49865510574455,135.490724141497));
#49501=CARTESIAN_POINT('Ctrl Pts',(89.501249924644,-1.36698962325895,135.528820632467));
#49502=CARTESIAN_POINT('Ctrl Pts',(89.4934894821298,-1.23525386694098,135.566937456682));
#49503=CARTESIAN_POINT('Ctrl Pts',(89.4857290396157,-1.10202715247588,135.599509965641));
#49504=CARTESIAN_POINT('Ctrl Pts',(89.4779685971015,-0.967816624651894,
135.626446685187));
#49505=CARTESIAN_POINT('Ctrl Pts',(89.4701956968361,-0.833390650173906,
135.653426645947));
#49506=CARTESIAN_POINT('Ctrl Pts',(89.4624227965706,-0.69797809281063,135.674752677509));
#49507=CARTESIAN_POINT('Ctrl Pts',(89.4546498963052,-0.5620928390424,135.690385044725));
#49508=CARTESIAN_POINT('Ctrl Pts',(89.4471595605432,-0.431147356522391,
135.705449136018));
#49509=CARTESIAN_POINT('Ctrl Pts',(89.4396692247811,-0.299763255507869,
135.715226311269));
#49510=CARTESIAN_POINT('Ctrl Pts',(89.4321788890191,-0.168399052114349,
135.71972681163));
#49511=CARTESIAN_POINT('Ctrl Pts',(89.4244045549,-0.0320541350223629,135.724397949831));
#49512=CARTESIAN_POINT('Ctrl Pts',(89.4166302207808,0.104701245541517,135.72339918095));
#49513=CARTESIAN_POINT('Ctrl Pts',(89.4088558866618,0.241356268496753,135.716684936476));
#49514=CARTESIAN_POINT('Ctrl Pts',(89.4010911337147,0.377842876349129,135.709978966709));
#49515=CARTESIAN_POINT('Ctrl Pts',(89.3933263807676,0.514228985937299,135.697571555438));
#49516=CARTESIAN_POINT('Ctrl Pts',(89.3855616278205,0.650000738586185,135.679469037113));
#49517=CARTESIAN_POINT('Ctrl Pts',(89.3778045869355,0.785637640816571,135.661384498464));
#49518=CARTESIAN_POINT('Ctrl Pts',(89.3700475460505,0.920661015381237,135.63761616071));
#49519=CARTESIAN_POINT('Ctrl Pts',(89.3622905051655,1.05455945164876,135.608222337624));
#49520=CARTESIAN_POINT('Ctrl Pts',(89.3545393139254,1.18835691406383,135.578850680649));
#49521=CARTESIAN_POINT('Ctrl Pts',(89.3467881226853,1.32103074639363,135.54386206572));
#49522=CARTESIAN_POINT('Ctrl Pts',(89.3390369314451,1.452077448777,135.503366272516));
#49523=CARTESIAN_POINT('Ctrl Pts',(89.331289034668,1.58306845281589,135.462887691105));
#49524=CARTESIAN_POINT('Ctrl Pts',(89.323541137891,1.71243332964075,135.416906702075));
#49525=CARTESIAN_POINT('Ctrl Pts',(89.3157932411139,1.83968173455635,135.36558349943));
#49526=CARTESIAN_POINT('Ctrl Pts',(89.3080469650298,1.96690352184888,135.314271032493));
#49527=CARTESIAN_POINT('Ctrl Pts',(89.3003006889457,2.09200935547267,135.257618720809));
#49528=CARTESIAN_POINT('Ctrl Pts',(89.2925544128616,2.21452731789317,135.195835520239));
#49529=CARTESIAN_POINT('Ctrl Pts',(89.2848080795962,2.33704618471353,135.134051863599));
#49530=CARTESIAN_POINT('Ctrl Pts',(89.2770617463309,2.45697679312138,135.067137418533));
#49531=CARTESIAN_POINT('Ctrl Pts',(89.2693154130656,2.57387071369496,134.995347686466));
#49532=CARTESIAN_POINT('Ctrl Pts',(89.2615673450626,2.69079081185164,134.923541877586));
#49533=CARTESIAN_POINT('Ctrl Pts',(89.2538192770596,2.80467253587353,134.84685881374));
#49534=CARTESIAN_POINT('Ctrl Pts',(89.2460712090566,2.91509573441053,134.765597788163));
#49535=CARTESIAN_POINT('Ctrl Pts',(89.2383149063148,3.02563629203691,134.684250397402));
#49536=CARTESIAN_POINT('Ctrl Pts',(89.2305586035729,3.13271066605606,134.598315557623));
#49537=CARTESIAN_POINT('Ctrl Pts',(89.222802300831,3.23593073225011,134.508133742175));
#49538=CARTESIAN_POINT('Ctrl Pts',(89.2150418583169,3.33920589010144,134.417903793978));
#49539=CARTESIAN_POINT('Ctrl Pts',(89.2072814158027,3.43862235780159,134.323422622641));
#49540=CARTESIAN_POINT('Ctrl Pts',(89.1995209732885,3.5338290514067,134.225067459424));
#49541=CARTESIAN_POINT('Ctrl Pts',(89.1917480730231,3.62918857924831,134.126554407767));
#49542=CARTESIAN_POINT('Ctrl Pts',(89.1839751727576,3.720324568476,134.024155229151));
#49543=CARTESIAN_POINT('Ctrl Pts',(89.1762022724922,3.80692582059041,133.918280793008));
#49544=CARTESIAN_POINT('Ctrl Pts',(89.1687119367301,3.89037889905559,133.816255159299));
#49545=CARTESIAN_POINT('Ctrl Pts',(89.1612216009681,3.96962102933123,133.711002796168));
#49546=CARTESIAN_POINT('Ctrl Pts',(89.153731265206,4.04441298842942,133.602915001801));
#49547=CARTESIAN_POINT('Ctrl Pts',(89.1459569310869,4.1220407073889,133.49072902586));
#49548=CARTESIAN_POINT('Ctrl Pts',(89.1381825969679,4.19512003847368,133.375132992101));
#49549=CARTESIAN_POINT('Ctrl Pts',(89.1304082628488,4.26333653233225,133.256532037875));
#49550=CARTESIAN_POINT('Ctrl Pts',(89.1226435099017,4.33146895545883,133.138077248725));
#49551=CARTESIAN_POINT('Ctrl Pts',(89.1148787569546,4.39475027260884,133.016625243214));
#49552=CARTESIAN_POINT('Ctrl Pts',(89.1071140040075,4.45290805996824,132.892611769121));
#49553=CARTESIAN_POINT('Ctrl Pts',(89.0993569631225,4.51100808419343,132.768721466959));
#49554=CARTESIAN_POINT('Ctrl Pts',(89.0915999222374,4.5639945405674,132.642275110746));
#49555=CARTESIAN_POINT('Ctrl Pts',(89.0838428813524,4.61164006018283,132.513734484752));
#49556=CARTESIAN_POINT('Ctrl Pts',(89.0760916901123,4.65924964994126,132.385290792243));
#49557=CARTESIAN_POINT('Ctrl Pts',(89.0683404988721,4.70152618438521,132.254756338572));
#49558=CARTESIAN_POINT('Ctrl Pts',(89.060589307632,4.73828987029396,132.12261407103));
#49559=CARTESIAN_POINT('Ctrl Pts',(89.0528414108549,4.7750379306555,131.990527967476));
#49560=CARTESIAN_POINT('Ctrl Pts',(89.0450935140778,4.8062776981722,131.856835785081));
#49561=CARTESIAN_POINT('Ctrl Pts',(89.0373456173007,4.83187890531025,131.722036653495));
#49562=CARTESIAN_POINT('Ctrl Pts',(89.0295993412166,4.85747475722766,131.587265718981));
#49563=CARTESIAN_POINT('Ctrl Pts',(89.0218530651325,4.87743432188516,131.451388679697));
#49564=CARTESIAN_POINT('Ctrl Pts',(89.0141067890484,4.89167831680965,131.314915518977));
#49565=CARTESIAN_POINT('Ctrl Pts',(89.006360455783,4.90592241688007,131.178441350842));
#49566=CARTESIAN_POINT('Ctrl Pts',(88.9986141225177,4.91445082244292,131.041371441343));
#49567=CARTESIAN_POINT('Ctrl Pts',(88.9908677892523,4.91723610702654,130.904221171613));
#49568=CARTESIAN_POINT('Ctrl Pts',(88.9831197212494,4.92002201535532,130.767040188031));
#49569=CARTESIAN_POINT('Ctrl Pts',(88.9753716532464,4.91706223551421,130.629779199217));
#49570=CARTESIAN_POINT('Ctrl Pts',(88.9676235852434,4.90838146931043,130.492953465705));
#49571=CARTESIAN_POINT('Ctrl Pts',(88.9598672825016,4.89969147708502,130.355982312176));
#49572=CARTESIAN_POINT('Ctrl Pts',(88.9521109797597,4.88526837717211,130.219447728834));
#49573=CARTESIAN_POINT('Ctrl Pts',(88.9443546770178,4.8651888288226,130.083860289738));
#49574=CARTESIAN_POINT('Ctrl Pts',(88.9365942345037,4.84509856341354,129.948200483544));
#49575=CARTESIAN_POINT('Ctrl Pts',(88.9288337919895,4.81934590729644,129.813489212709));
#49576=CARTESIAN_POINT('Ctrl Pts',(88.9210733494753,4.78805846636481,129.680225756808));
#49577=CARTESIAN_POINT('Ctrl Pts',(88.9133004492099,4.75672080005546,129.546748374577));
#49578=CARTESIAN_POINT('Ctrl Pts',(88.9055275489444,4.71983069928783,129.414723828453));
#49579=CARTESIAN_POINT('Ctrl Pts',(88.897754648679,4.67756562976158,129.284636023512));
#49580=CARTESIAN_POINT('Ctrl Pts',(88.8902643129171,4.63683700197232,129.159277237953));
#49581=CARTESIAN_POINT('Ctrl Pts',(88.8827739771551,4.59111751497956,129.035717116296));
#49582=CARTESIAN_POINT('Ctrl Pts',(88.8752836413932,4.54060707316218,128.914368429844));
#49583=CARTESIAN_POINT('Ctrl Pts',(88.8675093072741,4.48818151259042,128.788418771061));
#49584=CARTESIAN_POINT('Ctrl Pts',(88.859734973155,4.43042845905312,128.664452580269));
#49585=CARTESIAN_POINT('Ctrl Pts',(88.8519606390359,4.36751879852014,128.542953399245));
#49586=CARTESIAN_POINT('Ctrl Pts',(88.8441958860888,4.30468666852132,128.421603955104));
#49587=CARTESIAN_POINT('Ctrl Pts',(88.8364311331417,4.23671075423634,128.302715815156));
#49588=CARTESIAN_POINT('Ctrl Pts',(88.8286663801946,4.16381041088863,128.186753709592));
#49589=CARTESIAN_POINT('Ctrl Pts',(88.8209093393096,4.0909824731898,128.070906779225));
#49590=CARTESIAN_POINT('Ctrl Pts',(88.8131522984246,4.01324004649786,127.957980428667));
#49591=CARTESIAN_POINT('Ctrl Pts',(88.8053952575396,3.93084874454786,127.848415555494));
#49592=CARTESIAN_POINT('Ctrl Pts',(88.7976440662995,3.84851957451912,127.738933306044));
#49593=CARTESIAN_POINT('Ctrl Pts',(88.7898928750593,3.76154874124641,127.632807799592));
#49594=CARTESIAN_POINT('Ctrl Pts',(88.7821416838191,3.67024537933595,127.530451346074));
#49595=CARTESIAN_POINT('Ctrl Pts',(88.7743937870421,3.57898082379033,127.428138396779));
#49596=CARTESIAN_POINT('Ctrl Pts',(88.766645890265,3.48338766179843,127.329591605414));
#49597=CARTESIAN_POINT('Ctrl Pts',(88.7588979934879,3.38381541248751,127.23519036151));
#49598=CARTESIAN_POINT('Ctrl Pts',(88.7511517174038,3.28426399154462,127.140808864312));
#49599=CARTESIAN_POINT('Ctrl Pts',(88.7434054413197,3.18073542239457,127.050571458568));
#49600=CARTESIAN_POINT('Ctrl Pts',(88.7356591652356,3.07361591434535,126.964820505315));
#49601=CARTESIAN_POINT('Ctrl Pts',(88.7279128319703,2.96649561556424,126.879068919069));
#49602=CARTESIAN_POINT('Ctrl Pts',(88.7201664987049,2.85578463020576,126.797804095729));
#49603=CARTESIAN_POINT('Ctrl Pts',(88.7124201654396,2.74190173833597,126.721327686054));
#49604=CARTESIAN_POINT('Ctrl Pts',(88.7046720974366,2.62799334318199,126.644834150018));
#49605=CARTESIAN_POINT('Ctrl Pts',(88.6969240294336,2.51091195255865,126.573131379383));
#49606=CARTESIAN_POINT('Ctrl Pts',(88.6891759614306,2.3911044216764,126.506477102725));
#49607=CARTESIAN_POINT('Ctrl Pts',(88.6814196586888,2.27116955792493,126.439751985109));
#49608=CARTESIAN_POINT('Ctrl Pts',(88.6736633559469,2.14850310829263,126.37808627021));
#49609=CARTESIAN_POINT('Ctrl Pts',(88.6659070532051,2.02357606939264,126.321691440181));
#49610=CARTESIAN_POINT('Ctrl Pts',(88.6581466106909,1.89858235317024,126.265266510532));
#49611=CARTESIAN_POINT('Ctrl Pts',(88.6503861681768,1.77132600612046,126.214118217084));
#49612=CARTESIAN_POINT('Ctrl Pts',(88.6426257256626,1.64229606039197,126.168409074191));
#49613=CARTESIAN_POINT('Ctrl Pts',(88.6348528253972,1.51305898433995,126.122626554924));
#49614=CARTESIAN_POINT('Ctrl Pts',(88.6270799251317,1.38204299400097,126.082300749423));
#49615=CARTESIAN_POINT('Ctrl Pts',(88.6193070248663,1.24975113696537,126.047543913282));
#49616=CARTESIAN_POINT('Ctrl Pts',(88.6118166891043,1.1222684221569,126.014050575683));
#49617=CARTESIAN_POINT('Ctrl Pts',(88.6043263533424,0.993601292921839,125.985728411053));
#49618=CARTESIAN_POINT('Ctrl Pts',(88.5968360175804,0.86420507864751,125.962632347151));
#49619=CARTESIAN_POINT('Ctrl Pts',(88.5890616834613,0.729902767578985,125.938660588965));
#49620=CARTESIAN_POINT('Ctrl Pts',(88.5812873493422,0.594389564226906,125.920243114391));
#49621=CARTESIAN_POINT('Ctrl Pts',(88.5735130152231,0.45816465402444,125.907497518366));
#49622=CARTESIAN_POINT('Ctrl Pts',(88.565748262276,0.322107628848937,125.894767630149));
#49623=CARTESIAN_POINT('Ctrl Pts',(88.5579835093289,0.185341027548832,125.887695748369));
#49624=CARTESIAN_POINT('Ctrl Pts',(88.5502187563818,0.0483744076508083,
125.886348521283));
#49625=CARTESIAN_POINT('Ctrl Pts',(88.5424617154968,-0.0884561750692558,
125.885002632282));
#49626=CARTESIAN_POINT('Ctrl Pts',(88.5347046746118,-0.225485992625819,
125.889370086782));
#49627=CARTESIAN_POINT('Ctrl Pts',(88.5269476337268,-0.362200534688017,
125.899465732334));
#49628=CARTESIAN_POINT('Ctrl Pts',(88.5191964424866,-0.498811979251213,
125.909553764682));
#49629=CARTESIAN_POINT('Ctrl Pts',(88.5114452512465,-0.635108233224452,
125.92536136136));
#49630=CARTESIAN_POINT('Ctrl Pts',(88.5036940600063,-0.770575313775685,
125.946851302258));
#49631=CARTESIAN_POINT('Ctrl Pts',(88.4959461632292,-0.905984817203335,
125.968332109359));
#49632=CARTESIAN_POINT('Ctrl Pts',(88.4881982664521,-1.04056546281879,125.99549039601));
#49633=CARTESIAN_POINT('Ctrl Pts',(88.480450369675,-1.17380913583667,126.028237171179));
#49634=CARTESIAN_POINT('Ctrl Pts',(88.4727040935909,-1.30702493715075,126.060977096429));
#49635=CARTESIAN_POINT('Ctrl Pts',(88.4649578175068,-1.43890394271133,126.099303091761));
#49636=CARTESIAN_POINT('Ctrl Pts',(88.4572115414227,-1.56894935891606,126.143075282848));
#49637=CARTESIAN_POINT('Ctrl Pts',(88.4494652081574,-1.69899573508643,126.186847797052));
#49638=CARTESIAN_POINT('Ctrl Pts',(88.441718874892,-1.82720812435417,126.236066462513));
#49639=CARTESIAN_POINT('Ctrl Pts',(88.4339725416267,-1.95310637853767,126.290541997305));
#49640=CARTESIAN_POINT('Ctrl Pts',(88.4262244736237,-2.07903282676219,126.345029731515));
#49641=CARTESIAN_POINT('Ctrl Pts',(88.4184764056207,-2.20264374992861,126.404776522398));
#49642=CARTESIAN_POINT('Ctrl Pts',(88.4107283376177,-2.32348077753159,126.4695457266));
#49643=CARTESIAN_POINT('Ctrl Pts',(88.4029720348758,-2.44444623216557,126.534383768283));
#49644=CARTESIAN_POINT('Ctrl Pts',(88.395215732134,-2.56263155689463,126.604254701281));
#49645=CARTESIAN_POINT('Ctrl Pts',(88.3874594293921,-2.67760424062142,126.678876574074));
#49646=CARTESIAN_POINT('Ctrl Pts',(88.3796989868779,-2.79263828873143,126.753538274807));
#49647=CARTESIAN_POINT('Ctrl Pts',(88.3719385443638,-2.90445596059346,126.832955741693));
#49648=CARTESIAN_POINT('Ctrl Pts',(88.3641781018496,-3.01265619445776,126.91680538111));
#49649=CARTESIAN_POINT('Ctrl Pts',(88.3564052015841,-3.12103012094296,127.000789623413));
#49650=CARTESIAN_POINT('Ctrl Pts',(88.3486323013187,-3.22577470621888,127.089220003765));
#49651=CARTESIAN_POINT('Ctrl Pts',(88.3408594010533,-3.32652359696477,127.181733970872));
#49652=CARTESIAN_POINT('Ctrl Pts',(88.3333690652913,-3.4236100117603,127.270884822246));
#49653=CARTESIAN_POINT('Ctrl Pts',(88.3258787295293,-3.51698597720932,127.363827300324));
#49654=CARTESIAN_POINT('Ctrl Pts',(88.3183883937673,-3.60635916437889,127.460208013393));
#49655=CARTESIAN_POINT('Ctrl Pts',(88.3107028301196,-3.69806177160779,127.559100790464));
#49656=CARTESIAN_POINT('Ctrl Pts',(88.3030172664718,-3.78585555100518,127.661943210462));
#49657=CARTESIAN_POINT('Ctrl Pts',(88.2953317028241,-3.86937505516217,127.76838964521));
#49658=CARTESIAN_POINT('Ctrl Pts',(88.2876552722435,-3.95279530970278,127.874709585339));
#49659=CARTESIAN_POINT('Ctrl Pts',(88.279978841663,-4.03195114367966,127.984624712708));
#49660=CARTESIAN_POINT('Ctrl Pts',(88.2723024110824,-4.10651389843591,128.097752654736));
#49661=CARTESIAN_POINT('Ctrl Pts',(88.2646228527257,-4.18110703392854,128.21092669096));
#49662=CARTESIAN_POINT('Ctrl Pts',(88.2569432943689,-4.25110307235286,128.327315865827));
#49663=CARTESIAN_POINT('Ctrl Pts',(88.2492637360121,-4.31621279932073,128.446503511319));
#49664=CARTESIAN_POINT('Ctrl Pts',(88.2416008776309,-4.38118093860825,128.565431971232));
#49665=CARTESIAN_POINT('Ctrl Pts',(88.2339380192497,-4.44128377905166,128.687146405816));
#49666=CARTESIAN_POINT('Ctrl Pts',(88.2262751608685,-4.49627730081323,128.811203951197));
#49667=CARTESIAN_POINT('Ctrl Pts',(88.2185872525239,-4.55145059696731,128.935667041979));
#49668=CARTESIAN_POINT('Ctrl Pts',(88.2108993441793,-4.60148089862532,129.062488243117));
#49669=CARTESIAN_POINT('Ctrl Pts',(88.2032114358347,-4.64616873835184,129.191196299444));
#49670=CARTESIAN_POINT('Ctrl Pts',(88.1955235274901,-4.69085657807836,129.319904355771));
#49671=CARTESIAN_POINT('Ctrl Pts',(88.1878356191455,-4.73020181031948,129.450498885946));
#49672=CARTESIAN_POINT('Ctrl Pts',(88.1801477108009,-4.76405452823403,129.582490119308));
#49673=CARTESIAN_POINT('Origin',(213.235140564004,0.,130.804360617566));
#49674=CARTESIAN_POINT('',(86.0846345799593,-4.7702492504123,129.580946905181));
#49675=CARTESIAN_POINT('',(86.430234796612,-4.76405452823404,129.582490119308));
#49676=CARTESIAN_POINT('',(213.235140564004,-4.76405452823405,129.582490119308));
#49677=CARTESIAN_POINT('',(87.7648579073645,-4.92391445715771,130.802649439709));
#49678=CARTESIAN_POINT('Ctrl Pts',(87.764857441322,-4.9256415109711,130.802657025058));
#49679=CARTESIAN_POINT('Ctrl Pts',(87.6774498003774,-4.91862979770035,132.339650290333));
#49680=CARTESIAN_POINT('Ctrl Pts',(87.4972262848284,-3.31659732523356,135.521305288248));
#49681=CARTESIAN_POINT('Ctrl Pts',(87.2241868946751,2.10597827242213,136.227139918491));
#49682=CARTESIAN_POINT('Ctrl Pts',(86.9457392708622,5.70067050458257,131.963686123471));
#49683=CARTESIAN_POINT('Ctrl Pts',(86.6672916470494,4.0567250362683,126.634868824723));
#49684=CARTESIAN_POINT('Ctrl Pts',(86.3888440232364,-1.31515255834102,125.1376107926));
#49685=CARTESIAN_POINT('Ctrl Pts',(86.1946250008731,-4.21909290079494,127.725505074334));
#49686=CARTESIAN_POINT('Ctrl Pts',(86.0932218531139,-4.7337430531318,129.434338303608));
#49687=CARTESIAN_POINT('Ctrl Pts',(86.0846345799591,-4.77024925041304,129.580946905184));
#49688=CARTESIAN_POINT('Ctrl Pts',(87.8349528638408,-4.76405452823403,129.582490119308));
#49689=CARTESIAN_POINT('Ctrl Pts',(87.8271889033113,-4.79810140232196,129.715238364644));
#49690=CARTESIAN_POINT('Ctrl Pts',(87.8194249427818,-4.82656275471006,129.849282444912));
#49691=CARTESIAN_POINT('Ctrl Pts',(87.8116609822523,-4.84936864420704,129.984112597098));
#49692=CARTESIAN_POINT('Ctrl Pts',(87.8038859863517,-4.87220694904848,130.119134391264));
#49693=CARTESIAN_POINT('Ctrl Pts',(87.796110990451,-4.88937369504103,130.254944101439));
#49694=CARTESIAN_POINT('Ctrl Pts',(87.7883359945504,-4.90085087283581,130.391028082282));
#49695=CARTESIAN_POINT('Ctrl Pts',(87.7859180438006,-4.90442016740642,130.433348923054));
#49696=CARTESIAN_POINT('Ctrl Pts',(87.7835000930507,-4.90743957424586,130.475696300847));
#49697=CARTESIAN_POINT('Ctrl Pts',(87.7810821423009,-4.90990957711857,130.518054824716));
#49698=CARTESIAN_POINT('Ctrl Pts',(87.7756745735309,-4.91543355662776,130.612786543645));
#49699=CARTESIAN_POINT('Ctrl Pts',(87.770267004761,-4.91821617968026,130.707679669371));
#49700=CARTESIAN_POINT('Ctrl Pts',(87.764859435991,-4.91824969360065,130.802624559646));
#49701=CARTESIAN_POINT('',(88.1101405639545,-4.91824790478202,130.8089003981));
#49702=CARTESIAN_POINT('Ctrl Pts',(88.1801477108009,-4.76405452823403,129.582490119308));
#49703=CARTESIAN_POINT('Ctrl Pts',(88.1724878463956,-4.79778375826004,129.713999875267));
#49704=CARTESIAN_POINT('Ctrl Pts',(88.1648279819903,-4.82606040748949,129.846895763953));
#49705=CARTESIAN_POINT('Ctrl Pts',(88.1571681175851,-4.84878692862279,129.980680835541));
#49706=CARTESIAN_POINT('Ctrl Pts',(88.149330191989,-4.87204175041555,130.117575874605));
#49707=CARTESIAN_POINT('Ctrl Pts',(88.1414922663929,-4.88948514735401,130.255401512422));
#49708=CARTESIAN_POINT('Ctrl Pts',(88.1336543407968,-4.9010686352311,130.393618246664));
#49709=CARTESIAN_POINT('Ctrl Pts',(88.1258164152007,-4.91265212310819,130.531834980907));
#49710=CARTESIAN_POINT('Ctrl Pts',(88.1179784896046,-4.9183757082134,130.670442363389));
#49711=CARTESIAN_POINT('Ctrl Pts',(88.1101405640085,-4.9182479047829,130.808900397146));
#49712=CARTESIAN_POINT('Ctrl Pts',(88.1101405639545,-4.91824790478202,130.8089003981));
#49713=CARTESIAN_POINT('Ctrl Pts',(88.1002146810802,-4.91808605556142,130.984242484372));
#49714=CARTESIAN_POINT('Ctrl Pts',(88.0902887982059,-4.90854396835757,131.159164971997));
#49715=CARTESIAN_POINT('Ctrl Pts',(88.0803629153316,-4.88977686091136,131.332816209831));
#49716=CARTESIAN_POINT('Ctrl Pts',(88.0702186323547,-4.87059681909521,131.510288311625));
#49717=CARTESIAN_POINT('Ctrl Pts',(88.0600743493779,-4.8417813266888,131.68643285966));
#49718=CARTESIAN_POINT('Ctrl Pts',(88.049930066401,-4.80354409539745,131.860365913988));
#49719=CARTESIAN_POINT('Ctrl Pts',(88.0466003009189,-4.79099308383976,131.917457803265));
#49720=CARTESIAN_POINT('Ctrl Pts',(88.0432705354368,-4.77742733571033,131.974311603233));
#49721=CARTESIAN_POINT('Ctrl Pts',(88.0399407699546,-4.76285551578117,132.030896551933));
#49722=CARTESIAN_POINT('Ctrl Pts',(88.0321664358355,-4.72883324080123,132.163011050585));
#49723=CARTESIAN_POINT('Ctrl Pts',(88.0243921017164,-4.68925592277407,132.293918145695));
#49724=CARTESIAN_POINT('Ctrl Pts',(88.0166177675973,-4.64422410186059,132.42311493932));
#49725=CARTESIAN_POINT('Ctrl Pts',(88.0088530146503,-4.5992477786418,132.552152509443));
#49726=CARTESIAN_POINT('Ctrl Pts',(88.0010882617032,-4.54883045512982,132.679483606324));
#49727=CARTESIAN_POINT('Ctrl Pts',(87.9933235087561,-4.49312331969054,132.804617075262));
#49728=CARTESIAN_POINT('Ctrl Pts',(87.9855664678711,-4.43747151336355,132.929626259873));
#49729=CARTESIAN_POINT('Ctrl Pts',(87.9778094269861,-4.37654050861573,133.052441805383));
#49730=CARTESIAN_POINT('Ctrl Pts',(87.9700523861011,-4.31053066615113,133.172589584256));
#49731=CARTESIAN_POINT('Ctrl Pts',(87.9623011948609,-4.24457060222231,133.292646758755));
#49732=CARTESIAN_POINT('Ctrl Pts',(87.9545500036208,-4.1735395114369,133.410039829681));
#49733=CARTESIAN_POINT('Ctrl Pts',(87.9467988123807,-4.09768489165824,133.524316792061));
#49734=CARTESIAN_POINT('Ctrl Pts',(87.9390509156036,-4.02186251211626,133.638545183685));
#49735=CARTESIAN_POINT('Ctrl Pts',(87.9313030188266,-3.94122089689439,133.749659775897));
#49736=CARTESIAN_POINT('Ctrl Pts',(87.9235551220495,-3.85605219123975,133.857235420262));
#49737=CARTESIAN_POINT('Ctrl Pts',(87.9158088459654,-3.7709013010423,133.964788562121));
#49738=CARTESIAN_POINT('Ctrl Pts',(87.9080625698812,-3.68122544651445,134.068803922239));
#49739=CARTESIAN_POINT('Ctrl Pts',(87.9003162937971,-3.58735834628673,134.168887799478));
#49740=CARTESIAN_POINT('Ctrl Pts',(87.8925699605318,-3.49349055315347,134.268972415514));
#49741=CARTESIAN_POINT('Ctrl Pts',(87.8848236272664,-3.39543172003968,134.365125205593));
#49742=CARTESIAN_POINT('Ctrl Pts',(87.877077294001,-3.29355358368351,134.456988144964));
#49743=CARTESIAN_POINT('Ctrl Pts',(87.869329225998,-3.191652632425,134.548871656404));
#49744=CARTESIAN_POINT('Ctrl Pts',(87.8615811579951,-3.08593096626504,134.636463143726));
#49745=CARTESIAN_POINT('Ctrl Pts',(87.8538330899921,-2.9767943457115,134.719444075915));
#49746=CARTESIAN_POINT('Ctrl Pts',(87.8460767872502,-2.8675417334589,134.802513201227));
#49747=CARTESIAN_POINT('Ctrl Pts',(87.8383204845084,-2.75486722830405,134.880961745812));
#49748=CARTESIAN_POINT('Ctrl Pts',(87.8305641817665,-2.63920705040945,134.954513531323));
#49749=CARTESIAN_POINT('Ctrl Pts',(87.8228037392523,-2.52348514119538,135.028104573637));
#49750=CARTESIAN_POINT('Ctrl Pts',(87.8150432967381,-2.40477472220454,135.096793453451));
#49751=CARTESIAN_POINT('Ctrl Pts',(87.8072828542239,-2.28353681534967,135.160349905368));
#49752=CARTESIAN_POINT('Ctrl Pts',(87.7995099539585,-2.16210428664381,135.224008383743));
#49753=CARTESIAN_POINT('Ctrl Pts',(87.7917370536931,-2.03813651596725,135.282517803047));
#49754=CARTESIAN_POINT('Ctrl Pts',(87.7839641534276,-1.91211553076332,135.335695659197));
#49755=CARTESIAN_POINT('Ctrl Pts',(87.7764738176656,-1.79067572579969,135.386940366329));
#49756=CARTESIAN_POINT('Ctrl Pts',(87.7689834819036,-1.66732968202179,135.433234303722));
#49757=CARTESIAN_POINT('Ctrl Pts',(87.7614931461416,-1.54252032660781,135.474458486401));
#49758=CARTESIAN_POINT('Ctrl Pts',(87.7537188120225,-1.41297878654797,135.517245696497));
#49759=CARTESIAN_POINT('Ctrl Pts',(87.7459444779035,-1.28145043282677,135.554706660444));
#49760=CARTESIAN_POINT('Ctrl Pts',(87.7381701437844,-1.14841271213979,135.586654136903));
#49761=CARTESIAN_POINT('Ctrl Pts',(87.7304053908373,-1.01553894855373,135.618562240953));
#49762=CARTESIAN_POINT('Ctrl Pts',(87.7226406378902,-0.881159895673808,
135.644970286889));
#49763=CARTESIAN_POINT('Ctrl Pts',(87.7148758849431,-0.745770496865722,
135.665739992651));
#49764=CARTESIAN_POINT('Ctrl Pts',(87.7071188440581,-0.610515568717097,
135.686489069649));
#49765=CARTESIAN_POINT('Ctrl Pts',(87.6993618031731,-0.474252675574064,
135.701610891983));
#49766=CARTESIAN_POINT('Ctrl Pts',(87.6916047622881,-0.337489014213713,
135.711017751276));
#49767=CARTESIAN_POINT('Ctrl Pts',(87.683853571048,-0.200828487394539,135.720417516782));
#49768=CARTESIAN_POINT('Ctrl Pts',(87.6761023798079,-0.063668332479496,
135.72411087072));
#49769=CARTESIAN_POINT('Ctrl Pts',(87.6683511885678,0.0734773873054794,
135.722061720323));
#49770=CARTESIAN_POINT('Ctrl Pts',(87.6606032917907,0.210564816501158,135.720013440869));
#49771=CARTESIAN_POINT('Ctrl Pts',(87.6528553950136,0.3476374326663,135.712227517309));
#49772=CARTESIAN_POINT('Ctrl Pts',(87.6451074982366,0.484179634738213,135.698719936599));
#49773=CARTESIAN_POINT('Ctrl Pts',(87.6373612221525,0.620693275125056,135.685215181384));
#49774=CARTESIAN_POINT('Ctrl Pts',(87.6296149460684,0.7566763332871,135.665991188077));
#49775=CARTESIAN_POINT('Ctrl Pts',(87.6218686699843,0.891617194235736,135.641115918534));
#49776=CARTESIAN_POINT('Ctrl Pts',(87.6141223367189,1.02655905128706,135.616240465367));
#49777=CARTESIAN_POINT('Ctrl Pts',(87.6063760034536,1.16045831128667,135.585713723598));
#49778=CARTESIAN_POINT('Ctrl Pts',(87.5986296701883,1.29281282508547,135.54965492475));
#49779=CARTESIAN_POINT('Ctrl Pts',(87.5908816021854,1.42519697875995,135.513588050784));
#49780=CARTESIAN_POINT('Ctrl Pts',(87.5831335341824,1.55603532071835,135.471986757289));
#49781=CARTESIAN_POINT('Ctrl Pts',(87.5753854661794,1.68484053833069,135.425020248279));
#49782=CARTESIAN_POINT('Ctrl Pts',(87.5676291634375,1.8137826516612,135.378003822703));
#49783=CARTESIAN_POINT('Ctrl Pts',(87.5598728606957,1.94068695626284,135.325610924969));
#49784=CARTESIAN_POINT('Ctrl Pts',(87.5521165579539,2.06508530781696,135.268059278311));
#49785=CARTESIAN_POINT('Ctrl Pts',(87.5443561154397,2.18955005451696,135.210476914606));
#49786=CARTESIAN_POINT('Ctrl Pts',(87.5365956729255,2.31150583560229,135.147730494415));
#49787=CARTESIAN_POINT('Ctrl Pts',(87.5288352304114,2.43050972866737,135.080083424455));
#49788=CARTESIAN_POINT('Ctrl Pts',(87.5210623301459,2.54970465734618,135.012327761414));
#49789=CARTESIAN_POINT('Ctrl Pts',(87.5132894298805,2.66593789701143,134.9396559353));
#49790=CARTESIAN_POINT('Ctrl Pts',(87.5055165296151,2.77879535420176,134.862374841539));
#49791=CARTESIAN_POINT('Ctrl Pts',(87.498026193853,2.88755015855358,134.787903110194));
#49792=CARTESIAN_POINT('Ctrl Pts',(87.4905358580909,2.99317010875273,134.709151594175));
#49793=CARTESIAN_POINT('Ctrl Pts',(87.4830455223288,3.09531568641119,134.626428626374));
#49794=CARTESIAN_POINT('Ctrl Pts',(87.4752711882097,3.20133414469208,134.540569192108));
#49795=CARTESIAN_POINT('Ctrl Pts',(87.4674968540906,3.30394540255489,134.450159229093));
#49796=CARTESIAN_POINT('Ctrl Pts',(87.4597225199715,3.40273385695808,134.355499218242));
#49797=CARTESIAN_POINT('Ctrl Pts',(87.4519577670245,3.50140056342012,134.260955867394));
#49798=CARTESIAN_POINT('Ctrl Pts',(87.4441930140774,3.59625356085309,134.162173158274));
#49799=CARTESIAN_POINT('Ctrl Pts',(87.4364282611303,3.68690897966526,134.059492755923));
#49800=CARTESIAN_POINT('Ctrl Pts',(87.4286712202453,3.77747435823745,133.956914337194));
#49801=CARTESIAN_POINT('Ctrl Pts',(87.4209141793603,3.86385019778957,133.85044622037));
#49802=CARTESIAN_POINT('Ctrl Pts',(87.4131571384753,3.94568855453173,133.740467715943));
#49803=CARTESIAN_POINT('Ctrl Pts',(87.4054059472351,4.02746519633245,133.630572147161));
#49804=CARTESIAN_POINT('Ctrl Pts',(87.397654755995,4.10471093365639,133.517171772271));
#49805=CARTESIAN_POINT('Ctrl Pts',(87.3899035647549,4.17711753690626,133.400679578204));
#49806=CARTESIAN_POINT('Ctrl Pts',(87.3821556679778,4.24949336541828,133.284236896427));
#49807=CARTESIAN_POINT('Ctrl Pts',(87.3744077712007,4.31703394464075,133.164705340483));
#49808=CARTESIAN_POINT('Ctrl Pts',(87.3666598744236,4.37947402988349,133.042527341489));
#49809=CARTESIAN_POINT('Ctrl Pts',(87.3589135983395,4.44190105400645,132.920374899498));
#49810=CARTESIAN_POINT('Ctrl Pts',(87.3511673222554,4.49922952849361,132.795577463472));
#49811=CARTESIAN_POINT('Ctrl Pts',(87.3434210461713,4.55124009117904,132.668602204632));
#49812=CARTESIAN_POINT('Ctrl Pts',(87.3356747129059,4.6032510377946,132.541626008489));
#49813=CARTESIAN_POINT('Ctrl Pts',(87.3279283796406,4.64994384608303,132.412472319243));
#49814=CARTESIAN_POINT('Ctrl Pts',(87.3201820463753,4.69114740502095,132.281628056747));
#49815=CARTESIAN_POINT('Ctrl Pts',(87.3124339783723,4.73236019121023,132.150754492586));
#49816=CARTESIAN_POINT('Ctrl Pts',(87.3046859103693,4.76808116451588,132.018189974659));
#49817=CARTESIAN_POINT('Ctrl Pts',(87.2969378423663,4.79818927668619,131.884435951787));
#49818=CARTESIAN_POINT('Ctrl Pts',(87.2891815396245,4.82832938811641,131.750539773548));
#49819=CARTESIAN_POINT('Ctrl Pts',(87.2814252368826,4.85284463585599,131.615451946977));
#49820=CARTESIAN_POINT('Ctrl Pts',(87.2736689341407,4.87166515318884,131.479684019874));
#49821=CARTESIAN_POINT('Ctrl Pts',(87.2659084916266,4.89049571559848,131.343843629341));
#49822=CARTESIAN_POINT('Ctrl Pts',(87.2581480491124,4.90362545383212,131.207322803966));
#49823=CARTESIAN_POINT('Ctrl Pts',(87.2503876065982,4.91103656904408,131.070636564681));
#49824=CARTESIAN_POINT('Ctrl Pts',(87.2426147063328,4.9184595812361,130.933730904509));
#49825=CARTESIAN_POINT('Ctrl Pts',(87.2348418060673,4.9201456209472,130.79665969096));
#49826=CARTESIAN_POINT('Ctrl Pts',(87.2270689058019,4.91612906035938,130.659937197062));
#49827=CARTESIAN_POINT('Ctrl Pts',(87.2195785700399,4.91225851186607,130.528184910202));
#49828=CARTESIAN_POINT('Ctrl Pts',(87.2120882342779,4.90309279407344,130.396756736768));
#49829=CARTESIAN_POINT('Ctrl Pts',(87.204597898516,4.88870779819585,130.266104984656));
#49830=CARTESIAN_POINT('Ctrl Pts',(87.1968235643969,4.87377739082723,130.130499531651));
#49831=CARTESIAN_POINT('Ctrl Pts',(87.1890492302778,4.85317681969433,129.995300980914));
#49832=CARTESIAN_POINT('Ctrl Pts',(87.1812748961587,4.82693424430148,129.861021408326));
#49833=CARTESIAN_POINT('Ctrl Pts',(87.1735101432116,4.80072401053742,129.72690732331));
#49834=CARTESIAN_POINT('Ctrl Pts',(87.1657453902645,4.76888568170904,129.593710343012));
#49835=CARTESIAN_POINT('Ctrl Pts',(87.1579806373174,4.73149921940028,129.461938106091));
#49836=CARTESIAN_POINT('Ctrl Pts',(87.1502235964324,4.69414988985295,129.330296747214));
#49837=CARTESIAN_POINT('Ctrl Pts',(87.1424665555474,4.65126349896016,129.200077689336));
#49838=CARTESIAN_POINT('Ctrl Pts',(87.1347095146624,4.60297109926411,129.071778694008));
#49839=CARTESIAN_POINT('Ctrl Pts',(87.1269583234223,4.55471511724237,128.943576449951));
#49840=CARTESIAN_POINT('Ctrl Pts',(87.1192071321822,4.50106137803836,128.817291750842));
#49841=CARTESIAN_POINT('Ctrl Pts',(87.1114559409421,4.44219073362551,128.693407148493));
#49842=CARTESIAN_POINT('Ctrl Pts',(87.103708044165,4.38334511080693,128.569575200405));
#49843=CARTESIAN_POINT('Ctrl Pts',(87.0959601473879,4.31928716032181,128.448141672548));
#49844=CARTESIAN_POINT('Ctrl Pts',(87.0882122506108,4.25024574076486,128.329568867618));
#49845=CARTESIAN_POINT('Ctrl Pts',(87.0804659745267,4.18121876318452,128.211020865563));
#49846=CARTESIAN_POINT('Ctrl Pts',(87.0727196984426,4.10721058659468,128.095332733831));
#49847=CARTESIAN_POINT('Ctrl Pts',(87.0649734223585,4.02849568476616,127.982941545482));
#49848=CARTESIAN_POINT('Ctrl Pts',(87.0572270890931,3.94978020188212,127.870549527486));
#49849=CARTESIAN_POINT('Ctrl Pts',(87.0494807558278,3.86635814871267,127.761454821673));
#49850=CARTESIAN_POINT('Ctrl Pts',(87.0417344225625,3.77854669503138,127.656064580665));
#49851=CARTESIAN_POINT('Ctrl Pts',(87.0339863545595,3.69071557658399,127.550650738243));
#49852=CARTESIAN_POINT('Ctrl Pts',(87.0262382865565,3.59849335183553,127.448943311723));
#49853=CARTESIAN_POINT('Ctrl Pts',(87.0184902185535,3.50223647434234,127.351315187763));
#49854=CARTESIAN_POINT('Ctrl Pts',(87.0107339158117,3.40587729389422,127.25358330347));
#49855=CARTESIAN_POINT('Ctrl Pts',(87.0029776130699,3.30547516973552,127.159939661273));
#49856=CARTESIAN_POINT('Ctrl Pts',(86.995221310328,3.20142271685164,127.070719546102));
#49857=CARTESIAN_POINT('Ctrl Pts',(86.9874608678139,3.09731472804061,126.981451811468));
#49858=CARTESIAN_POINT('Ctrl Pts',(86.9797004252997,2.98955283540926,126.896612550017));
#49859=CARTESIAN_POINT('Ctrl Pts',(86.9719399827855,2.87856071994148,126.816495117814));
#49860=CARTESIAN_POINT('Ctrl Pts',(86.96416708252,2.76739043007645,126.736249073997));
#49861=CARTESIAN_POINT('Ctrl Pts',(86.9563941822546,2.65297988170643,126.660740221963));
#49862=CARTESIAN_POINT('Ctrl Pts',(86.9486212819892,2.53578032630071,126.590217620556));
#49863=CARTESIAN_POINT('Ctrl Pts',(86.9411309462271,2.42284126994121,126.522258693346));
#49864=CARTESIAN_POINT('Ctrl Pts',(86.933640610465,2.30731273103825,126.458929933258));
#49865=CARTESIAN_POINT('Ctrl Pts',(86.926150274703,2.18961627009005,126.40041197433));
#49866=CARTESIAN_POINT('Ctrl Pts',(86.9183759405839,2.06745731205271,126.339675289204));
#49867=CARTESIAN_POINT('Ctrl Pts',(86.9106016064648,1.94257583040136,126.283929014055));
#49868=CARTESIAN_POINT('Ctrl Pts',(86.9028272723457,1.81541786997739,126.233426247017));
#49869=CARTESIAN_POINT('Ctrl Pts',(86.8950625193986,1.68841662037529,126.182985720125));
#49870=CARTESIAN_POINT('Ctrl Pts',(86.8872977664515,1.55914483409,126.137775986509));
#49871=CARTESIAN_POINT('Ctrl Pts',(86.8795330135044,1.42807282309185,126.098004163318));
#49872=CARTESIAN_POINT('Ctrl Pts',(86.8717759726194,1.2971309946629,126.058271842062));
#49873=CARTESIAN_POINT('Ctrl Pts',(86.8640189317344,1.1643928714391,126.023966795765));
#49874=CARTESIAN_POINT('Ctrl Pts',(86.8562618908494,1.03034807141074,125.99524781849));
#49875=CARTESIAN_POINT('Ctrl Pts',(86.8485106996093,0.896404355608625,125.966550498418));
#49876=CARTESIAN_POINT('Ctrl Pts',(86.8407595083692,0.761156305074167,125.94343094422));
#49877=CARTESIAN_POINT('Ctrl Pts',(86.8330083171291,0.625107659223032,125.925997831048));
#49878=CARTESIAN_POINT('Ctrl Pts',(86.825260420352,0.4891168376756,125.908572127415));
#49879=CARTESIAN_POINT('Ctrl Pts',(86.8175125235749,0.35232648457384,125.896828107388));
#49880=CARTESIAN_POINT('Ctrl Pts',(86.8097646267978,0.215249251929158,125.89082311165));
#49881=CARTESIAN_POINT('Ctrl Pts',(86.8020183507137,0.0782006928865948,
125.884819372027));
#49882=CARTESIAN_POINT('Ctrl Pts',(86.7942720746296,-0.0591342359945297,
125.884552285972));
#49883=CARTESIAN_POINT('Ctrl Pts',(86.7865257985455,-0.196239452993261,
125.890027179592));
#49884=CARTESIAN_POINT('Ctrl Pts',(86.7787794652801,-0.333345682071464,
125.895502113627));
#49885=CARTESIAN_POINT('Ctrl Pts',(86.7710331320148,-0.470221805229798,
125.906719096315));
#49886=CARTESIAN_POINT('Ctrl Pts',(86.7632867987494,-0.606353835425051,
125.923631359682));
#49887=CARTESIAN_POINT('Ctrl Pts',(86.7555387307465,-0.742516351444593,
125.940547410433));
#49888=CARTESIAN_POINT('Ctrl Pts',(86.7477906627435,-0.877934055009452,
125.963161231607));
#49889=CARTESIAN_POINT('Ctrl Pts',(86.7400425947405,-1.01210055415978,125.991374483078));
#49890=CARTESIAN_POINT('Ctrl Pts',(86.7322862919987,-1.14640964706219,126.019617719929));
#49891=CARTESIAN_POINT('Ctrl Pts',(86.7245299892569,-1.27946449593388,126.05347219454));
#49892=CARTESIAN_POINT('Ctrl Pts',(86.716773686515,-1.41077079807924,126.092788818497));
#49893=CARTESIAN_POINT('Ctrl Pts',(86.7090132440008,-1.54214718235162,126.13212642692));
#49894=CARTESIAN_POINT('Ctrl Pts',(86.7012528014866,-1.67177279098091,126.176931866037));
#49895=CARTESIAN_POINT('Ctrl Pts',(86.6934923589724,-1.79917180527986,126.227007247158));
#49896=CARTESIAN_POINT('Ctrl Pts',(86.685719458707,-1.92677533178653,126.277163013726));
#49897=CARTESIAN_POINT('Ctrl Pts',(86.6779465584416,-2.05214476355159,126.332605469414));
#49898=CARTESIAN_POINT('Ctrl Pts',(86.6701736581761,-2.1748266478739,126.39308958597));
#49899=CARTESIAN_POINT('Ctrl Pts',(86.6626833224141,-2.29304873668383,126.451374952539));
#49900=CARTESIAN_POINT('Ctrl Pts',(86.6551929866521,-2.40877501332709,126.514341642537));
#49901=CARTESIAN_POINT('Ctrl Pts',(86.6477026508901,-2.52162564152507,126.581732622288));
#49902=CARTESIAN_POINT('Ctrl Pts',(86.6399270791868,-2.63877368123814,126.651689886136));
#49903=CARTESIAN_POINT('Ctrl Pts',(86.6321515074835,-2.75319386935908,126.726636714134));
#49904=CARTESIAN_POINT('Ctrl Pts',(86.6243759357803,-2.86443195400119,126.80633452418));
#49905=CARTESIAN_POINT('Ctrl Pts',(86.6162867216482,-2.98015703771763,126.889247096518));
#49906=CARTESIAN_POINT('Ctrl Pts',(86.6081975075162,-3.09243753941397,126.977301815903));
#49907=CARTESIAN_POINT('Ctrl Pts',(86.6001082933842,-3.20078964714923,127.070176811538));
#49908=CARTESIAN_POINT('Ctrl Pts',(86.5923522785462,-3.30467867043511,127.159226233703));
#49909=CARTESIAN_POINT('Ctrl Pts',(86.5845962637082,-3.40495611958501,127.252706476487));
#49910=CARTESIAN_POINT('Ctrl Pts',(86.5768402488702,-3.5012252238783,127.350289831641));
#49911=CARTESIAN_POINT('Ctrl Pts',(86.5690895258958,-3.59742864457262,127.447806606495));
#49912=CARTESIAN_POINT('Ctrl Pts',(86.5613388029213,-3.68962888826259,127.54942064671));
#49913=CARTESIAN_POINT('Ctrl Pts',(86.5535880799469,-3.77746381088411,127.65476537056));
#49914=CARTESIAN_POINT('Ctrl Pts',(86.5458409666259,-3.8652578271761,127.760061033446));
#49915=CARTESIAN_POINT('Ctrl Pts',(86.5380938533049,-3.94869031867422,127.869083622547));
#49916=CARTESIAN_POINT('Ctrl Pts',(86.5303467399839,-4.02743771144179,127.981431546024));
#49917=CARTESIAN_POINT('Ctrl Pts',(86.5226015569098,-4.1061654837518,128.093751477239));
#49918=CARTESIAN_POINT('Ctrl Pts',(86.5148563738356,-4.18021025782734,128.209394773103));
#49919=CARTESIAN_POINT('Ctrl Pts',(86.5071111907615,-4.24929053015312,128.327929101685));
#49920=CARTESIAN_POINT('Ctrl Pts',(86.4993643122063,-4.31838592468953,128.446489378356));
#49921=CARTESIAN_POINT('Ctrl Pts',(86.4916174336511,-4.38251444595739,128.567941616334));
#49922=CARTESIAN_POINT('Ctrl Pts',(86.483870555096,-4.44143950327054,128.691827019895));
#49923=CARTESIAN_POINT('Ctrl Pts',(86.4761226398207,-4.50037244618458,128.815729002326));
#49924=CARTESIAN_POINT('Ctrl Pts',(86.4683747245455,-4.55410037778972,128.942064442426));
#49925=CARTESIAN_POINT('Ctrl Pts',(86.4606268092702,-4.60243436192303,129.070353406886));
#49926=CARTESIAN_POINT('Ctrl Pts',(86.4528737656282,-4.65080033845505,129.198727286169));
#49927=CARTESIAN_POINT('Ctrl Pts',(86.4451207219862,-4.6937651104652,129.329056902511));
#49928=CARTESIAN_POINT('Ctrl Pts',(86.4373676783443,-4.73118920099771,129.460845896075));
#49929=CARTESIAN_POINT('Ctrl Pts',(86.4349900511002,-4.74266605335986,129.501261649687));
#49930=CARTESIAN_POINT('Ctrl Pts',(86.4326124238561,-4.75362218332535,129.541814564842));
#49931=CARTESIAN_POINT('Ctrl Pts',(86.4302347966119,-4.76405452823404,129.582490119308));
#49932=CARTESIAN_POINT('Origin',(213.235140564004,0.,130.804360617566));
#49933=CARTESIAN_POINT('',(84.3346156335084,-4.75804253168638,129.583987249709));
#49934=CARTESIAN_POINT('',(84.6799609333917,-4.76405452823403,129.582490119308));
#49935=CARTESIAN_POINT('',(213.235140564004,-4.76405452823405,129.582490119308));
#49936=CARTESIAN_POINT('',(86.014859435991,-4.91323682400955,130.800674691398));
#49937=CARTESIAN_POINT('Ctrl Pts',(86.014859435991,-4.91323682400955,130.800674691398));
#49938=CARTESIAN_POINT('Ctrl Pts',(85.9538892158643,-4.90576278147865,131.879764980307));
#49939=CARTESIAN_POINT('Ctrl Pts',(85.8001031211331,-4.02348310616932,134.61268188659));
#49940=CARTESIAN_POINT('Ctrl Pts',(85.5535011517979,0.497709270771224,136.600390751394));
#49941=CARTESIAN_POINT('Ctrl Pts',(85.2750535279847,5.14538832177028,133.518519575448));
#49942=CARTESIAN_POINT('Ctrl Pts',(84.9966059041722,5.06470687125616,127.942468911244));
#49943=CARTESIAN_POINT('Ctrl Pts',(84.7181582803589,0.329807230743486,124.996356913967));
#49944=CARTESIAN_POINT('Ctrl Pts',(84.4974948568047,-3.66267472747781,126.891296693768));
#49945=CARTESIAN_POINT('Ctrl Pts',(84.3696473078543,-4.60768184021397,128.982085784445));
#49946=CARTESIAN_POINT('Ctrl Pts',(84.3346156335084,-4.75804253168638,129.583987249709));
#49947=CARTESIAN_POINT('Ctrl Pts',(86.0846345799591,-4.77024925041304,129.580946905184));
#49948=CARTESIAN_POINT('Ctrl Pts',(86.0613761986364,-4.86912523137873,129.978032068211));
#49949=CARTESIAN_POINT('Ctrl Pts',(86.0381178173137,-4.91608795577263,130.389032854305));
#49950=CARTESIAN_POINT('Ctrl Pts',(86.014859435991,-4.91323682400955,130.800674691398));
#49951=CARTESIAN_POINT('',(86.3601405639686,-4.91824989921154,130.803364924019));
#49952=CARTESIAN_POINT('Ctrl Pts',(86.4302347966119,-4.76405452823404,129.582490119308));
#49953=CARTESIAN_POINT('Ctrl Pts',(86.4224725614478,-4.79811298491391,129.715283524994));
#49954=CARTESIAN_POINT('Ctrl Pts',(86.4147103262837,-4.8265848866449,129.849384456535));
#49955=CARTESIAN_POINT('Ctrl Pts',(86.4069480911196,-4.84939749013098,129.984283154633));
#49956=CARTESIAN_POINT('Ctrl Pts',(86.3991741738781,-4.87224442633088,130.119384873766));
#49957=CARTESIAN_POINT('Ctrl Pts',(86.3914002566367,-4.88941500410759,130.255286370261));
#49958=CARTESIAN_POINT('Ctrl Pts',(86.3836263393952,-4.90088841095131,130.391473410325));
#49959=CARTESIAN_POINT('Ctrl Pts',(86.3788359019558,-4.90795854509265,130.47539448579));
#49960=CARTESIAN_POINT('Ctrl Pts',(86.3740454645165,-4.91286634404094,130.559423971005));
#49961=CARTESIAN_POINT('Ctrl Pts',(86.3692550270772,-4.91561677684126,130.643442111058));
#49962=CARTESIAN_POINT('Ctrl Pts',(86.3662168727209,-4.91736113515921,130.696727449076));
#49963=CARTESIAN_POINT('Ctrl Pts',(86.3631787183647,-4.91823910390381,130.750041304561));
#49964=CARTESIAN_POINT('Ctrl Pts',(86.3601405640085,-4.9182498992114,130.803364923318));
#49965=CARTESIAN_POINT('Ctrl Pts',(86.3601405639686,-4.91824989921154,130.803364924019));
#49966=CARTESIAN_POINT('Ctrl Pts',(86.3524082609104,-4.91827737396147,130.93907704791));
#49967=CARTESIAN_POINT('Ctrl Pts',(86.3446759578523,-4.91268341904247,131.075014422619));
#49968=CARTESIAN_POINT('Ctrl Pts',(86.3369436547941,-4.90143815997771,131.210669645788));
#49969=CARTESIAN_POINT('Ctrl Pts',(86.3292207938126,-4.89020663273363,131.34615921753));
#49970=CARTESIAN_POINT('Ctrl Pts',(86.3214979328312,-4.87333756169104,131.481366932733));
#49971=CARTESIAN_POINT('Ctrl Pts',(86.3137750718497,-4.85085304816715,131.615783914981));
#49972=CARTESIAN_POINT('Ctrl Pts',(86.3060597424904,-4.82839046237952,131.750069808774));
#49973=CARTESIAN_POINT('Ctrl Pts',(86.2983444131311,-4.80032339511772,131.883566116271));
#49974=CARTESIAN_POINT('Ctrl Pts',(86.2906290837717,-4.76672582936199,132.015768034661));
#49975=CARTESIAN_POINT('Ctrl Pts',(86.2829193826055,-4.73315277242225,132.147873514145));
#49976=CARTESIAN_POINT('Ctrl Pts',(86.2752096814392,-4.69405734287461,132.278686101701));
#49977=CARTESIAN_POINT('Ctrl Pts',(86.267499980273,-4.64956470873308,132.40771057369));
#49978=CARTESIAN_POINT('Ctrl Pts',(86.2597932472713,-4.60508920384931,132.536685372436));
#49979=CARTESIAN_POINT('Ctrl Pts',(86.2520865142695,-4.55522075419097,132.663873050959));
#49980=CARTESIAN_POINT('Ctrl Pts',(86.2443797812678,-4.50013447636924,132.788793220879));
#49981=CARTESIAN_POINT('Ctrl Pts',(86.236674393087,-4.44505781107418,132.913691592295));
#49982=CARTESIAN_POINT('Ctrl Pts',(86.2289690049061,-4.38476528788441,133.036322880162));
#49983=CARTESIAN_POINT('Ctrl Pts',(86.2212636167253,-4.31948011112654,133.15622681956));
#49984=CARTESIAN_POINT('Ctrl Pts',(86.2135578585224,-4.25419179929563,133.27613651689));
#49985=CARTESIAN_POINT('Ctrl Pts',(86.2058521003194,-4.18391054613569,133.393318257734));
#49986=CARTESIAN_POINT('Ctrl Pts',(86.1981463421165,-4.10890521767763,133.507336935376));
#49987=CARTESIAN_POINT('Ctrl Pts',(86.1904384991179,-4.03387959650045,133.621386460813));
#49988=CARTESIAN_POINT('Ctrl Pts',(86.1827306561194,-3.95412757487608,133.732270890298));
#49989=CARTESIAN_POINT('Ctrl Pts',(86.1750228131208,-3.86996071508352,133.839585012271));
#49990=CARTESIAN_POINT('Ctrl Pts',(86.1673066825565,-3.78570335806874,133.947014519681));
#49991=CARTESIAN_POINT('Ctrl Pts',(86.1595905519922,-3.69702192855418,134.05086574247));
#49992=CARTESIAN_POINT('Ctrl Pts',(86.1518744214279,-3.60426784015897,134.150767107952));
#49993=CARTESIAN_POINT('Ctrl Pts',(86.1441537660352,-3.5114593596916,134.250727056752));
#49994=CARTESIAN_POINT('Ctrl Pts',(86.1364331106425,-3.41457374424503,134.346732257083));
#49995=CARTESIAN_POINT('Ctrl Pts',(86.1287124552499,-3.31399763511203,134.43844960065));
#49996=CARTESIAN_POINT('Ctrl Pts',(86.1209801595676,-3.21326988923563,134.530305224763));
#49997=CARTESIAN_POINT('Ctrl Pts',(86.1132478638852,-3.1088408402803,134.61785982786));
#49998=CARTESIAN_POINT('Ctrl Pts',(86.1055155682029,-3.00112886320961,134.700821654059));
#49999=CARTESIAN_POINT('Ctrl Pts',(86.1006128465567,-2.9328332543458,134.75342423909));
#50000=CARTESIAN_POINT('Ctrl Pts',(86.0957101249105,-2.8632183992832,134.804181267004));
#50001=CARTESIAN_POINT('Ctrl Pts',(86.0908074032643,-2.79239623547075,134.853027846004));
#50002=CARTESIAN_POINT('Ctrl Pts',(86.0830330691453,-2.6800922532648,134.930484747114));
#50003=CARTESIAN_POINT('Ctrl Pts',(86.0752587350262,-2.5643851390634,135.003388076089));
#50004=CARTESIAN_POINT('Ctrl Pts',(86.0674844009071,-2.44568050828408,135.071424000491));
#50005=CARTESIAN_POINT('Ctrl Pts',(86.05971964796,-2.32712217035335,135.139376076697));
#50006=CARTESIAN_POINT('Ctrl Pts',(86.0519548950129,-2.20557400208879,135.202472491291));
#50007=CARTESIAN_POINT('Ctrl Pts',(86.0441901420659,-2.08147216534957,135.260441483908));
#50008=CARTESIAN_POINT('Ctrl Pts',(86.0364331011809,-1.95749358830405,135.318352900904));
#50009=CARTESIAN_POINT('Ctrl Pts',(86.0286760602958,-1.83096674214791,135.371146866091));
#50010=CARTESIAN_POINT('Ctrl Pts',(86.0209190194108,-1.70235375663139,135.418596713583));
#50011=CARTESIAN_POINT('Ctrl Pts',(86.0131678281707,-1.5738377591677,135.466010778775));
#50012=CARTESIAN_POINT('Ctrl Pts',(86.0054166369305,-1.44323911896507,135.508088613046));
#50013=CARTESIAN_POINT('Ctrl Pts',(85.9976654456904,-1.31104105636989,135.544651158346));
#50014=CARTESIAN_POINT('Ctrl Pts',(85.9899175489133,-1.17889918147782,135.58119816359));
#50015=CARTESIAN_POINT('Ctrl Pts',(85.9821696521363,-1.0451596122878,135.612234438188));
#50016=CARTESIAN_POINT('Ctrl Pts',(85.9744217553592,-0.910321676117569,
135.637630474349));
#50017=CARTESIAN_POINT('Ctrl Pts',(85.9666754792751,-0.775511945136911,
135.663021198207));
#50018=CARTESIAN_POINT('Ctrl Pts',(85.958929203191,-0.639604688137216,135.682773958028));
#50019=CARTESIAN_POINT('Ctrl Pts',(85.9511829271069,-0.503110008515032,
135.69681024754));
#50020=CARTESIAN_POINT('Ctrl Pts',(85.9434365938415,-0.366614321319944,
135.710846640664));
#50021=CARTESIAN_POINT('Ctrl Pts',(85.9356902605761,-0.229531591764014,
135.719166439283));
#50022=CARTESIAN_POINT('Ctrl Pts',(85.9279439273108,-0.0923772421223119,
135.721743001278));
#50023=CARTESIAN_POINT('Ctrl Pts',(85.9201958593078,0.0448078222849374,
135.724320140276));
#50024=CARTESIAN_POINT('Ctrl Pts',(85.9124477913048,0.182064147871934,135.721151476003));
#50025=CARTESIAN_POINT('Ctrl Pts',(85.9046997233018,0.318876512293178,135.712262494377));
#50026=CARTESIAN_POINT('Ctrl Pts',(85.89694342056,0.455834282523323,135.703364065436));
#50027=CARTESIAN_POINT('Ctrl Pts',(85.8891871178182,0.592346758257384,135.688733199831));
#50028=CARTESIAN_POINT('Ctrl Pts',(85.8814308150763,0.727903482690584,135.668447333732));
#50029=CARTESIAN_POINT('Ctrl Pts',(85.8736703725621,0.863532557829333,135.648150640456));
#50030=CARTESIAN_POINT('Ctrl Pts',(85.865909930048,0.998204481512188,135.622193006538));
#50031=CARTESIAN_POINT('Ctrl Pts',(85.8581494875338,1.13142016893736,135.590702797542));
#50032=CARTESIAN_POINT('Ctrl Pts',(85.8503765872684,1.26484970601023,135.559162037668));
#50033=CARTESIAN_POINT('Ctrl Pts',(85.8426036870029,1.39681795879816,135.522071060734));
#50034=CARTESIAN_POINT('Ctrl Pts',(85.8348307867375,1.52684129285869,135.479608068656));
#50035=CARTESIAN_POINT('Ctrl Pts',(85.8273404509754,1.65213795121718,135.438688713298));
#50036=CARTESIAN_POINT('Ctrl Pts',(85.8198501152134,1.77562835251854,135.392781241775));
#50037=CARTESIAN_POINT('Ctrl Pts',(85.8123597794514,1.89690003015802,135.342086186404));
#50038=CARTESIAN_POINT('Ctrl Pts',(85.8045854453323,2.02276976031493,135.2894690126));
#50039=CARTESIAN_POINT('Ctrl Pts',(85.7968111112132,2.14664791724025,135.2315273705));
#50040=CARTESIAN_POINT('Ctrl Pts',(85.7890367770941,2.26805121977541,135.168432881745));
#50041=CARTESIAN_POINT('Ctrl Pts',(85.781272024147,2.38930490359008,135.105416151308));
#50042=CARTESIAN_POINT('Ctrl Pts',(85.7735072712,2.50808945809706,135.037259388228));
#50043=CARTESIAN_POINT('Ctrl Pts',(85.7657425182529,2.62394048746622,134.964182654713));
#50044=CARTESIAN_POINT('Ctrl Pts',(85.7579854773679,2.73967645195987,134.891178502041));
#50045=CARTESIAN_POINT('Ctrl Pts',(85.7502284364829,2.85248436101213,134.813264310691));
#50046=CARTESIAN_POINT('Ctrl Pts',(85.7424713955979,2.96192372177463,134.730706365063));
#50047=CARTESIAN_POINT('Ctrl Pts',(85.7347202043578,3.07128055346372,134.648210677024));
#50048=CARTESIAN_POINT('Ctrl Pts',(85.7269690131177,3.17727358222047,134.561078439508));
#50049=CARTESIAN_POINT('Ctrl Pts',(85.7192178218775,3.27949096903656,134.469619414228));
#50050=CARTESIAN_POINT('Ctrl Pts',(85.7114699251005,3.38166491073673,134.378199261473));
#50051=CARTESIAN_POINT('Ctrl Pts',(85.7037220283234,3.48006611146722,134.282456238736));
#50052=CARTESIAN_POINT('Ctrl Pts',(85.6959741315463,3.57431571404229,134.182740442105));
#50053=CARTESIAN_POINT('Ctrl Pts',(85.6882278554622,3.66854560163235,134.083045503869));
#50054=CARTESIAN_POINT('Ctrl Pts',(85.6804815793781,3.75862535002504,133.979379728633));
#50055=CARTESIAN_POINT('Ctrl Pts',(85.672735303294,3.84421318632328,133.872129846272));
#50056=CARTESIAN_POINT('Ctrl Pts',(85.6649889700287,3.92980165441137,133.764879172218));
#50057=CARTESIAN_POINT('Ctrl Pts',(85.6572426367633,4.01089790037469,133.654044643834));
#50058=CARTESIAN_POINT('Ctrl Pts',(85.6494963034979,4.08720091111563,133.540045499762));
#50059=CARTESIAN_POINT('Ctrl Pts',(85.641748235495,4.16352100938694,133.426020826372));
#50060=CARTESIAN_POINT('Ctrl Pts',(85.634000167492,4.23504551904515,133.308830451916));
#50061=CARTESIAN_POINT('Ctrl Pts',(85.626252099489,4.3015173918517,133.188921623306));
#50062=CARTESIAN_POINT('Ctrl Pts',(85.6184957967472,4.3680599117556,133.068885354167));
#50063=CARTESIAN_POINT('Ctrl Pts',(85.6107394940053,4.42953887779171,132.94612520186));
#50064=CARTESIAN_POINT('Ctrl Pts',(85.6029831912635,4.48574352483045,132.821112484292));
#50065=CARTESIAN_POINT('Ctrl Pts',(85.5952227487493,4.54197816998169,132.696033043672));
#50066=CARTESIAN_POINT('Ctrl Pts',(85.5874623062351,4.59293274170323,132.568699004988));
#50067=CARTESIAN_POINT('Ctrl Pts',(85.579701863721,4.63844547005359,132.439599647139));
#50068=CARTESIAN_POINT('Ctrl Pts',(85.5719289634555,4.68403125947587,132.310293047541));
#50069=CARTESIAN_POINT('Ctrl Pts',(85.5641560631901,4.7241576342459,132.179215839905));
#50070=CARTESIAN_POINT('Ctrl Pts',(85.5563831629247,4.75871310445237,132.046871242073));
#50071=CARTESIAN_POINT('Ctrl Pts',(85.5488928271626,4.7920123962769,131.919337703728));
#50072=CARTESIAN_POINT('Ctrl Pts',(85.5414024914006,4.82013871864219,131.790627621974));
#50073=CARTESIAN_POINT('Ctrl Pts',(85.5339121556386,4.84303783678936,131.661196409259));
#50074=CARTESIAN_POINT('Ctrl Pts',(85.5261378215195,4.86680518196106,131.526857772775));
#50075=CARTESIAN_POINT('Ctrl Pts',(85.5183634874004,4.88501640718023,131.391316698084));
#50076=CARTESIAN_POINT('Ctrl Pts',(85.5105891532813,4.89755467732237,131.255072549001));
#50077=CARTESIAN_POINT('Ctrl Pts',(85.5028244003342,4.91007749516717,131.118996308654));
#50078=CARTESIAN_POINT('Ctrl Pts',(85.4950596473871,4.91694123327284,130.982219103527));
#50079=CARTESIAN_POINT('Ctrl Pts',(85.48729489444,4.91808001891918,130.845250591984));
#50080=CARTESIAN_POINT('Ctrl Pts',(85.479537853555,4.91921767350756,130.708418119497));
#50081=CARTESIAN_POINT('Ctrl Pts',(85.47178081267,4.91464168800971,130.571395107141));
#50082=CARTESIAN_POINT('Ctrl Pts',(85.464023771785,4.90433799788751,130.434696087246));
#50083=CARTESIAN_POINT('Ctrl Pts',(85.4562725805448,4.89404207785817,130.298100153145));
#50084=CARTESIAN_POINT('Ctrl Pts',(85.4485213893047,4.87802707978905,130.161828113472));
#50085=CARTESIAN_POINT('Ctrl Pts',(85.4407701980646,4.85633100593914,130.026393893821));
#50086=CARTESIAN_POINT('Ctrl Pts',(85.4330223012875,4.83464415349942,129.891017237327));
#50087=CARTESIAN_POINT('Ctrl Pts',(85.4252744045104,4.80728108946488,129.756478077843));
#50088=CARTESIAN_POINT('Ctrl Pts',(85.4175265077333,4.77433157802729,129.623284394136));
#50089=CARTESIAN_POINT('Ctrl Pts',(85.4097802316492,4.74138895891712,129.490118571676));
#50090=CARTESIAN_POINT('Ctrl Pts',(85.4020339555651,4.70286231056995,129.35829804447));
#50091=CARTESIAN_POINT('Ctrl Pts',(85.394287679481,4.65889226318408,129.228319392679));
#50092=CARTESIAN_POINT('Ctrl Pts',(85.3865413462156,4.61492189122137,129.098339781415));
#50093=CARTESIAN_POINT('Ctrl Pts',(85.3787950129502,4.56550816532366,128.970202443046));
#50094=CARTESIAN_POINT('Ctrl Pts',(85.3710486796848,4.51084109790222,128.844387237141));
#50095=CARTESIAN_POINT('Ctrl Pts',(85.3633006116819,4.45616178817026,128.718543855793));
#50096=CARTESIAN_POINT('Ctrl Pts',(85.3555525436789,4.39622695169032,128.595024000211));
#50097=CARTESIAN_POINT('Ctrl Pts',(85.347804475676,4.33127392910448,128.474285680239));
#50098=CARTESIAN_POINT('Ctrl Pts',(85.3400481729341,4.26625187367311,128.353419038143));
#50099=CARTESIAN_POINT('Ctrl Pts',(85.3322918701923,4.19620116363837,128.235340181936));
#50100=CARTESIAN_POINT('Ctrl Pts',(85.3245355674504,4.12140440840354,128.120481193134));
#50101=CARTESIAN_POINT('Ctrl Pts',(85.3167751249362,4.04656773188832,128.00556090063));
#50102=CARTESIAN_POINT('Ctrl Pts',(85.3090146824221,3.96698018950555,127.893864218116));
#50103=CARTESIAN_POINT('Ctrl Pts',(85.3012542399079,3.88296598484741,127.785791714424));
#50104=CARTESIAN_POINT('Ctrl Pts',(85.2934813396425,3.79881691312958,127.677545723154));
#50105=CARTESIAN_POINT('Ctrl Pts',(85.285708439377,3.71022723175037,127.572935835156));
#50106=CARTESIAN_POINT('Ctrl Pts',(85.2779355391116,3.61756004911154,127.472327851585));
#50107=CARTESIAN_POINT('Ctrl Pts',(85.2704452033496,3.52826155197713,127.375377221634));
#50108=CARTESIAN_POINT('Ctrl Pts',(85.2629548675877,3.43517707920089,127.282142806943));
#50109=CARTESIAN_POINT('Ctrl Pts',(85.2554645318257,3.3386604669637,127.192916398305));
#50110=CARTESIAN_POINT('Ctrl Pts',(85.2476901977066,3.23848439803689,127.100306943263));
#50111=CARTESIAN_POINT('Ctrl Pts',(85.2399158635876,3.1342934652414,127.011722062072));
#50112=CARTESIAN_POINT('Ctrl Pts',(85.2321415294685,3.02644464525853,126.927529969771));
#50113=CARTESIAN_POINT('Ctrl Pts',(85.2243767765214,2.91872873930756,126.843441636699));
#50114=CARTESIAN_POINT('Ctrl Pts',(85.2166120235743,2.8073642210049,126.763735559099));
#50115=CARTESIAN_POINT('Ctrl Pts',(85.2088472706272,2.69274427455205,126.688742640352));
#50116=CARTESIAN_POINT('Ctrl Pts',(85.2010902297421,2.57823817024588,126.613824205629));
#50117=CARTESIAN_POINT('Ctrl Pts',(85.1933331888572,2.46048339732106,126.543609826675));
#50118=CARTESIAN_POINT('Ctrl Pts',(85.1855761479721,2.33990524417316,126.478389453678));
#50119=CARTESIAN_POINT('Ctrl Pts',(85.177824956732,2.21941801994792,126.413218263871));
#50120=CARTESIAN_POINT('Ctrl Pts',(85.1700737654918,2.09611199590156,126.353033769242));
#50121=CARTESIAN_POINT('Ctrl Pts',(85.1623225742516,1.97044009334086,126.298081786751));
#50122=CARTESIAN_POINT('Ctrl Pts',(85.1545746774746,1.84482160469167,126.243153160318));
#50123=CARTESIAN_POINT('Ctrl Pts',(85.1468267806974,1.71683959497981,126.19345277905));
#50124=CARTESIAN_POINT('Ctrl Pts',(85.1390788839203,1.58696996086753,126.14917969672));
#50125=CARTESIAN_POINT('Ctrl Pts',(85.1313326078362,1.45712749268314,126.104915875366));
#50126=CARTESIAN_POINT('Ctrl Pts',(85.1235863317522,1.32539855529597,126.066077220901));
#50127=CARTESIAN_POINT('Ctrl Pts',(85.1158400556681,1.19227694971759,126.032813830865));
#50128=CARTESIAN_POINT('Ctrl Pts',(85.1080937224027,1.05915436146558,125.999550195287));
#50129=CARTESIAN_POINT('Ctrl Pts',(85.1003473891373,0.924639463812012,125.971862001037));
#50130=CARTESIAN_POINT('Ctrl Pts',(85.0926010558719,0.789238682553677,125.949848761111));
#50131=CARTESIAN_POINT('Ctrl Pts',(85.084852987869,0.653807579229459,125.927830591473));
#50132=CARTESIAN_POINT('Ctrl Pts',(85.077104919866,0.517490583356969,125.911489967764));
#50133=CARTESIAN_POINT('Ctrl Pts',(85.069356851863,0.380801320003617,125.900874774089));
#50134=CARTESIAN_POINT('Ctrl Pts',(85.0616005491212,0.243966781674364,125.890248298459));
#50135=CARTESIAN_POINT('Ctrl Pts',(85.0538442463793,0.106759575923239,125.885359438734));
#50136=CARTESIAN_POINT('Ctrl Pts',(85.0460879436374,-0.0303040175490168,
125.886203978232));
#50137=CARTESIAN_POINT('Ctrl Pts',(85.0383275011232,-0.1674407659882,125.887048968487));
#50138=CARTESIAN_POINT('Ctrl Pts',(85.0305670586091,-0.304433359093195,
125.893633436688));
#50139=CARTESIAN_POINT('Ctrl Pts',(85.0228066160949,-0.44076954700117,125.90590113841));
#50140=CARTESIAN_POINT('Ctrl Pts',(85.0150337158295,-0.577324593861055,
125.918188533335));
#50141=CARTESIAN_POINT('Ctrl Pts',(85.007260815564,-0.713220742048475,125.936177341568));
#50142=CARTESIAN_POINT('Ctrl Pts',(84.9994879152986,-0.847953963730991,
125.959759794186));
#50143=CARTESIAN_POINT('Ctrl Pts',(84.9919975795366,-0.977789293432203,
125.982484965251));
#50144=CARTESIAN_POINT('Ctrl Pts',(84.9845072437746,-1.10654447829828,126.01040408997));
#50145=CARTESIAN_POINT('Ctrl Pts',(84.9770169080126,-1.23378276937296,126.043377195992));
#50146=CARTESIAN_POINT('Ctrl Pts',(84.9692425738935,-1.36584533892763,126.077600487352));
#50147=CARTESIAN_POINT('Ctrl Pts',(84.9614682397744,-1.49669205250879,126.117376977864));
#50148=CARTESIAN_POINT('Ctrl Pts',(84.9536939056553,-1.62582016576019,126.162605362158));
#50149=CARTESIAN_POINT('Ctrl Pts',(84.9459291527082,-1.75478914015226,126.207778006511));
#50150=CARTESIAN_POINT('Ctrl Pts',(84.9381643997612,-1.88204336300204,126.258389047894));
#50151=CARTESIAN_POINT('Ctrl Pts',(84.9303996468141,-2.00709191025934,126.314286550663));
#50152=CARTESIAN_POINT('Ctrl Pts',(84.9226426059291,-2.13201625753672,126.370128535245));
#50153=CARTESIAN_POINT('Ctrl Pts',(84.9148855650441,-2.25473893421092,126.431246373789));
#50154=CARTESIAN_POINT('Ctrl Pts',(84.9071285241591,-2.37478611821173,126.497438984282));
#50155=CARTESIAN_POINT('Ctrl Pts',(84.899377332919,-2.49474277369709,126.563581678412));
#50156=CARTESIAN_POINT('Ctrl Pts',(84.8916261416789,-2.61202761145537,126.634791339215));
#50157=CARTESIAN_POINT('Ctrl Pts',(84.8838749504388,-2.72618900368645,126.710819781239));
#50158=CARTESIAN_POINT('Ctrl Pts',(84.8761270536617,-2.84030187428096,126.786815909147));
#50159=CARTESIAN_POINT('Ctrl Pts',(84.8683791568846,-2.9512936150138,126.867626528481));
#50160=CARTESIAN_POINT('Ctrl Pts',(84.8606312601075,-3.05873952253601,126.95295884733));
#50161=CARTESIAN_POINT('Ctrl Pts',(84.8528849840234,-3.16616295469033,127.038273316497));
#50162=CARTESIAN_POINT('Ctrl Pts',(84.8451387079393,-3.27004172297506,127.128107360853));
#50163=CARTESIAN_POINT('Ctrl Pts',(84.8373924318552,-3.36998263457143,127.222126663008));
#50164=CARTESIAN_POINT('Ctrl Pts',(84.8296460985898,-3.46992428390917,127.316146659192));
#50165=CARTESIAN_POINT('Ctrl Pts',(84.8218997653245,-3.5659277337931,127.414351706934));
#50166=CARTESIAN_POINT('Ctrl Pts',(84.8141534320591,-3.65763552560786,127.516369525073));
#50167=CARTESIAN_POINT('Ctrl Pts',(84.8064053640561,-3.74936385474624,127.618410189395));
#50168=CARTESIAN_POINT('Ctrl Pts',(84.7986572960532,-3.83679435025959,127.724265032463));
#50169=CARTESIAN_POINT('Ctrl Pts',(84.7909092280503,-3.91960909900015,127.833527809491));
#50170=CARTESIAN_POINT('Ctrl Pts',(84.7831529253084,-4.00251186424158,127.942906712299));
#50171=CARTESIAN_POINT('Ctrl Pts',(84.7753966225665,-4.08078884656849,128.055700472309));
#50172=CARTESIAN_POINT('Ctrl Pts',(84.7676403198246,-4.15416453180601,128.171472449568));
#50173=CARTESIAN_POINT('Ctrl Pts',(84.7598798773105,-4.22757937985613,128.287306217817));
#50174=CARTESIAN_POINT('Ctrl Pts',(84.7521194347963,-4.29608752308006,128.406121032125));
#50175=CARTESIAN_POINT('Ctrl Pts',(84.7443589922821,-4.35945939794346,128.527455520689));
#50176=CARTESIAN_POINT('Ctrl Pts',(84.7365860920167,-4.42293300296619,128.648984786146));
#50177=CARTESIAN_POINT('Ctrl Pts',(84.7288131917512,-4.48125369667361,128.773041454646));
#50178=CARTESIAN_POINT('Ctrl Pts',(84.7210402914858,-4.53423970875748,128.899143221564));
#50179=CARTESIAN_POINT('Ctrl Pts',(84.7135499557238,-4.58529954583825,129.020660871624));
#50180=CARTESIAN_POINT('Ctrl Pts',(84.7060596199618,-4.63140571794234,129.144077224061));
#50181=CARTESIAN_POINT('Ctrl Pts',(84.6985692841997,-4.67243991429253,129.268949171137));
#50182=CARTESIAN_POINT('Ctrl Pts',(84.6923665005971,-4.7064205325662,129.372356239974));
#50183=CARTESIAN_POINT('Ctrl Pts',(84.6861637169944,-4.73698299476726,129.476938621189));
#50184=CARTESIAN_POINT('Ctrl Pts',(84.6799609333917,-4.76405452823403,129.582490119308));
#50185=CARTESIAN_POINT('Origin',(213.235140564004,0.,130.804360617566));
#50186=CARTESIAN_POINT('',(82.5850015336781,-4.76405452823407,129.582490119308));
#50187=CARTESIAN_POINT('',(82.9299460717117,-4.76405452823408,129.582490119308));
#50188=CARTESIAN_POINT('',(213.235140564004,-4.76405452823405,129.582490119308));
#50189=CARTESIAN_POINT('',(84.2648594359911,-4.91520650470561,130.80752635475));
#50190=CARTESIAN_POINT('Ctrl Pts',(84.2648594359911,-4.91824897989084,130.807528314317));
#50191=CARTESIAN_POINT('Ctrl Pts',(84.2561178632596,-4.91814915973146,130.962511709407));
#50192=CARTESIAN_POINT('Ctrl Pts',(84.2473762905281,-4.9107195796762,131.117215891758));
#50193=CARTESIAN_POINT('Ctrl Pts',(84.2386347177967,-4.89606346316109,131.270992835913));
#50194=CARTESIAN_POINT('Ctrl Pts',(84.2298585400784,-4.8813493279422,131.425378531981));
#50195=CARTESIAN_POINT('Ctrl Pts',(84.22108236236,-4.85935143879908,131.578829450587));
#50196=CARTESIAN_POINT('Ctrl Pts',(84.2123061846417,-4.83022408257366,131.730707407178));
#50197=CARTESIAN_POINT('Ctrl Pts',(84.203481116158,-4.80093446223002,131.883431453011));
#50198=CARTESIAN_POINT('Ctrl Pts',(84.1946560476744,-4.76443581593382,132.034564780633));
#50199=CARTESIAN_POINT('Ctrl Pts',(84.1858309791907,-4.720933766625,132.183478971312));
#50200=CARTESIAN_POINT('Ctrl Pts',(84.1776416637049,-4.68056558061833,132.321665466981));
#50201=CARTESIAN_POINT('Ctrl Pts',(84.1694523482191,-4.63416726118915,132.45794114906));
#50202=CARTESIAN_POINT('Ctrl Pts',(84.1612630327332,-4.58193918638087,132.591821485615));
#50203=CARTESIAN_POINT('Ctrl Pts',(84.1534886986142,-4.53235769148566,132.718917635489));
#50204=CARTESIAN_POINT('Ctrl Pts',(84.1457143644951,-4.47740546934383,132.844150558214));
#50205=CARTESIAN_POINT('Ctrl Pts',(84.137940030376,-4.41724249475759,132.967032993357));
#50206=CARTESIAN_POINT('Ctrl Pts',(84.1301752774289,-4.35715366566061,133.08976398688));
#50207=CARTESIAN_POINT('Ctrl Pts',(84.1224105244818,-4.29186703182705,133.210149908756));
#50208=CARTESIAN_POINT('Ctrl Pts',(84.1146457715348,-4.22159144787465,133.327721216));
#50209=CARTESIAN_POINT('Ctrl Pts',(84.1068887306498,-4.151385662623,133.445175749765));
#50210=CARTESIAN_POINT('Ctrl Pts',(84.0991316897647,-4.0762009874072,133.559820898686));
#50211=CARTESIAN_POINT('Ctrl Pts',(84.0913746488797,-3.99629305932868,133.671209906674));
#50212=CARTESIAN_POINT('Ctrl Pts',(84.0836234576396,-3.9164453904402,133.782514915345));
#50213=CARTESIAN_POINT('Ctrl Pts',(84.0758722663995,-3.83188178529054,133.890568354179));
#50214=CARTESIAN_POINT('Ctrl Pts',(84.0681210751594,-3.74290203338909,133.99495106934));
#50215=CARTESIAN_POINT('Ctrl Pts',(84.0603731783823,-3.65396010025588,134.099289419062));
#50216=CARTESIAN_POINT('Ctrl Pts',(84.0526252816052,-3.56060600663916,134.199959851231));
#50217=CARTESIAN_POINT('Ctrl Pts',(84.0448773848282,-3.4631806562809,134.296575216422));
#50218=CARTESIAN_POINT('Ctrl Pts',(84.0371311087441,-3.36577568520561,134.393170371761));
#50219=CARTESIAN_POINT('Ctrl Pts',(84.0293848326599,-3.26430142873579,134.485711872179));
#50220=CARTESIAN_POINT('Ctrl Pts',(84.0216385565758,-3.15913630377159,134.573848762751));
#50221=CARTESIAN_POINT('Ctrl Pts',(84.0138922233105,-3.0539704025024,134.66198630393));
#50222=CARTESIAN_POINT('Ctrl Pts',(84.0061458900452,-2.94511387802007,134.745718919255));
#50223=CARTESIAN_POINT('Ctrl Pts',(83.9983995567798,-2.83297862475211,134.824735621741));
#50224=CARTESIAN_POINT('Ctrl Pts',(83.9906514887768,-2.72081825957183,134.90377001947));
#50225=CARTESIAN_POINT('Ctrl Pts',(83.9829034207739,-2.60537802406574,134.978086177694));
#50226=CARTESIAN_POINT('Ctrl Pts',(83.9751553527709,-2.48709886790086,135.047416389505));
#50227=CARTESIAN_POINT('Ctrl Pts',(83.9673990500291,-2.36869400324111,135.11682028629));
#50228=CARTESIAN_POINT('Ctrl Pts',(83.9596427472872,-2.24744452849331,135.181227453072));
#50229=CARTESIAN_POINT('Ctrl Pts',(83.9518864445454,-2.12381656805513,135.240415875084));
#50230=CARTESIAN_POINT('Ctrl Pts',(83.9441260020312,-2.00012262365202,135.29963588774));
#50231=CARTESIAN_POINT('Ctrl Pts',(83.9363655595171,-1.87404802324866,135.353631451633));
#50232=CARTESIAN_POINT('Ctrl Pts',(83.9286051170029,-1.74607802281383,135.402229102065));
#50233=CARTESIAN_POINT('Ctrl Pts',(83.9208322167375,-1.61790259357365,135.450904765759));
#50234=CARTESIAN_POINT('Ctrl Pts',(83.913059316472,-1.48782605528891,135.494165076688));
#50235=CARTESIAN_POINT('Ctrl Pts',(83.9052864162066,-1.35634880543654,135.531886501207));
#50236=CARTESIAN_POINT('Ctrl Pts',(83.8977960804446,-1.22965108478769,135.568236656929));
#50237=CARTESIAN_POINT('Ctrl Pts',(83.8903057446826,-1.10165302254058,135.599443566678));
#50238=CARTESIAN_POINT('Ctrl Pts',(83.8828154089205,-0.972808598513784,
135.625442082669));
#50239=CARTESIAN_POINT('Ctrl Pts',(83.8750410748015,-0.839078998988413,
135.652426340296));
#50240=CARTESIAN_POINT('Ctrl Pts',(83.8672667406823,-0.704013975969372,
135.673884933197));
#50241=CARTESIAN_POINT('Ctrl Pts',(83.8594924065632,-0.568109945745981,
135.689689076538));
#50242=CARTESIAN_POINT('Ctrl Pts',(83.8517276536162,-0.43237340509384,135.705473742686));
#50243=CARTESIAN_POINT('Ctrl Pts',(83.8439629006691,-0.295800299212012,
135.715617779991));
#50244=CARTESIAN_POINT('Ctrl Pts',(83.836198147722,-0.158898558931744,135.720043104309));
#50245=CARTESIAN_POINT('Ctrl Pts',(83.828441106837,-0.0221327913898985,
135.724464033332));
#50246=CARTESIAN_POINT('Ctrl Pts',(83.820684065952,0.114960572758557,135.723177540087));
#50247=CARTESIAN_POINT('Ctrl Pts',(83.812927025067,0.251867486865856,135.71615721673));
#50248=CARTESIAN_POINT('Ctrl Pts',(83.8051758338269,0.388671158404247,135.709142187453));
#50249=CARTESIAN_POINT('Ctrl Pts',(83.7974246425867,0.525288270891732,135.696401954517));
#50250=CARTESIAN_POINT('Ctrl Pts',(83.7896734513466,0.661204134782529,135.677962176439));
#50251=CARTESIAN_POINT('Ctrl Pts',(83.7819255545695,0.797062230805592,135.659530235758));
#50252=CARTESIAN_POINT('Ctrl Pts',(83.7741776577924,0.932219284424532,135.635403620472));
#50253=CARTESIAN_POINT('Ctrl Pts',(83.7664297610153,1.06616530906384,135.605659878834));
#50254=CARTESIAN_POINT('Ctrl Pts',(83.7586834849312,1.20008331508235,135.575922358944));
#50255=CARTESIAN_POINT('Ctrl Pts',(83.7509372088471,1.33279041456422,135.540570134504));
#50256=CARTESIAN_POINT('Ctrl Pts',(83.743190932763,1.46378679561312,135.499731878658));
#50257=CARTESIAN_POINT('Ctrl Pts',(83.7354445994976,1.59478414364745,135.458893321353));
#50258=CARTESIAN_POINT('Ctrl Pts',(83.7276982662323,1.72407037480231,135.412568768195));
#50259=CARTESIAN_POINT('Ctrl Pts',(83.719951932967,1.85116120792071,135.36093666157));
#50260=CARTESIAN_POINT('Ctrl Pts',(83.712203864964,1.97828050214999,135.309292992292));
#50261=CARTESIAN_POINT('Ctrl Pts',(83.704455796961,2.10320305788241,135.252339551516));
#50262=CARTESIAN_POINT('Ctrl Pts',(83.696707728958,2.22546530164882,135.190302620563));
#50263=CARTESIAN_POINT('Ctrl Pts',(83.6889514262161,2.34785748718283,135.128199756022));
#50264=CARTESIAN_POINT('Ctrl Pts',(83.6811951234743,2.46758336348586,135.061002785831));
#50265=CARTESIAN_POINT('Ctrl Pts',(83.6734388207324,2.58420419162596,134.988983869244));
#50266=CARTESIAN_POINT('Ctrl Pts',(83.6656783782182,2.70088726381351,134.916926513993));
#50267=CARTESIAN_POINT('Ctrl Pts',(83.6579179357041,2.81446166201237,134.840042303254));
#50268=CARTESIAN_POINT('Ctrl Pts',(83.6501574931899,2.92451915275325,134.758645734712));
#50269=CARTESIAN_POINT('Ctrl Pts',(83.6423845929245,3.03475331754872,134.677118501171));
#50270=CARTESIAN_POINT('Ctrl Pts',(83.634611692659,3.14145898856807,134.591064680302));
#50271=CARTESIAN_POINT('Ctrl Pts',(83.6268387923936,3.24426175639737,134.500838497721));
#50272=CARTESIAN_POINT('Ctrl Pts',(83.6193484566316,3.34332738467118,134.413892264144));
#50273=CARTESIAN_POINT('Ctrl Pts',(83.6118581208696,3.43876872083921,134.323071966272));
#50274=CARTESIAN_POINT('Ctrl Pts',(83.6043677851076,3.5302855670449,134.228724336217));
#50275=CARTESIAN_POINT('Ctrl Pts',(83.5965934509885,3.62527230229075,134.130799487092));
#50276=CARTESIAN_POINT('Ctrl Pts',(83.5888191168694,3.71633196832571,134.028764351604));
#50277=CARTESIAN_POINT('Ctrl Pts',(83.5810447827503,3.80308788969193,133.922966967489));
#50278=CARTESIAN_POINT('Ctrl Pts',(83.5732800298032,3.88973689213861,133.817299969194));
#50279=CARTESIAN_POINT('Ctrl Pts',(83.5655152768561,3.97209245773049,133.70788024721));
#50280=CARTESIAN_POINT('Ctrl Pts',(83.557750523909,4.04981434304294,133.595092931742));
#50281=CARTESIAN_POINT('Ctrl Pts',(83.5499934830241,4.1274590338832,133.482417638225));
#50282=CARTESIAN_POINT('Ctrl Pts',(83.5422364421391,4.20047898269506,133.366381727258));
#50283=CARTESIAN_POINT('Ctrl Pts',(83.5344794012541,4.26857411704109,133.247403406759));
#50284=CARTESIAN_POINT('Ctrl Pts',(83.5267282100139,4.33661790031661,133.128514808737));
#50285=CARTESIAN_POINT('Ctrl Pts',(83.5189770187738,4.39974406788301,133.006688555704));
#50286=CARTESIAN_POINT('Ctrl Pts',(83.5112258275337,4.45769600470672,132.882371539607));
#50287=CARTESIAN_POINT('Ctrl Pts',(83.5034779307566,4.51562331041136,132.758107361559));
#50288=CARTESIAN_POINT('Ctrl Pts',(83.4957300339795,4.56838059454582,132.631354879615));
#50289=CARTESIAN_POINT('Ctrl Pts',(83.4879821372024,4.6157574404497,132.502585076651));
#50290=CARTESIAN_POINT('Ctrl Pts',(83.4802358611183,4.66312437613874,132.373842209553));
#50291=CARTESIAN_POINT('Ctrl Pts',(83.4724895850343,4.70511297731109,132.243083227462));
#50292=CARTESIAN_POINT('Ctrl Pts',(83.4647433089502,4.74156133978977,132.110798187261));
#50293=CARTESIAN_POINT('Ctrl Pts',(83.4569969756849,4.77800997132198,131.978512170562));
#50294=CARTESIAN_POINT('Ctrl Pts',(83.4492506424195,4.80891817870165,131.844700450193));
#50295=CARTESIAN_POINT('Ctrl Pts',(83.4415043091542,4.83417432476711,131.709866918076));
#50296=CARTESIAN_POINT('Ctrl Pts',(83.4337562411512,4.85943612677136,131.575003190924));
#50297=CARTESIAN_POINT('Ctrl Pts',(83.4260081731482,4.87904327681805,131.439117580891));
#50298=CARTESIAN_POINT('Ctrl Pts',(83.4182601051453,4.89293557900721,131.302722416047));
#50299=CARTESIAN_POINT('Ctrl Pts',(83.4105038024034,4.90684264610045,131.166182288799));
#50300=CARTESIAN_POINT('Ctrl Pts',(83.4027474996616,4.9150226925705,131.029131914487));
#50301=CARTESIAN_POINT('Ctrl Pts',(83.3949911969197,4.91746754459602,130.892087525324));
#50302=CARTESIAN_POINT('Ctrl Pts',(83.3872307544056,4.91991370151268,130.754969991444));
#50303=CARTESIAN_POINT('Ctrl Pts',(83.3794703118914,4.91661857398014,130.61785883974));
#50304=CARTESIAN_POINT('Ctrl Pts',(83.3717098693772,4.90762609764359,130.481267522271));
#50305=CARTESIAN_POINT('Ctrl Pts',(83.3639369691118,4.89861918578571,130.344456936292));
#50306=CARTESIAN_POINT('Ctrl Pts',(83.3561640688464,4.88389669073476,130.208168241041));
#50307=CARTESIAN_POINT('Ctrl Pts',(83.3483911685809,4.86355425510033,130.072907905359));
#50308=CARTESIAN_POINT('Ctrl Pts',(83.3409008328188,4.84395131824052,129.942564623577));
#50309=CARTESIAN_POINT('Ctrl Pts',(83.3334104970567,4.81913000295944,129.81317653501));
#50310=CARTESIAN_POINT('Ctrl Pts',(83.3259201612946,4.78921976052727,129.68518362179));
#50311=CARTESIAN_POINT('Ctrl Pts',(83.3181458271755,4.75817546216255,129.552337818363));
#50312=CARTESIAN_POINT('Ctrl Pts',(83.3103714930564,4.72155038663917,129.420574259306));
#50313=CARTESIAN_POINT('Ctrl Pts',(83.3025971589373,4.67943374567492,129.290397975247));
#50314=CARTESIAN_POINT('Ctrl Pts',(83.2948324059902,4.63736900970662,129.160382121823));
#50315=CARTESIAN_POINT('Ctrl Pts',(83.2870676530432,4.58982629352253,129.031950019602));
#50316=CARTESIAN_POINT('Ctrl Pts',(83.2793029000961,4.53694570819007,128.905596097296));
#50317=CARTESIAN_POINT('Ctrl Pts',(83.2715458592111,4.4841176446004,128.779367671487));
#50318=CARTESIAN_POINT('Ctrl Pts',(83.263788818326,4.42596241234019,128.655213676307));
#50319=CARTESIAN_POINT('Ctrl Pts',(83.256031777441,4.36266966509301,128.53361262279));
#50320=CARTESIAN_POINT('Ctrl Pts',(83.2482805862009,4.29942464739888,128.412103269574));
#50321=CARTESIAN_POINT('Ctrl Pts',(83.2405293949608,4.2310500059352,128.293143371438));
#50322=CARTESIAN_POINT('Ctrl Pts',(83.2327782037206,4.15778301686013,128.177190381892));
#50323=CARTESIAN_POINT('Ctrl Pts',(83.2250303069435,4.08454716820992,128.06128667546));
#50324=CARTESIAN_POINT('Ctrl Pts',(83.2172824101664,4.00642331607687,127.948387665562));
#50325=CARTESIAN_POINT('Ctrl Pts',(83.2095345133893,3.92369397634716,127.838924959441));
#50326=CARTESIAN_POINT('Ctrl Pts',(83.2017882373052,3.84098194181183,127.729485150559));
#50327=CARTESIAN_POINT('Ctrl Pts',(83.1940419612211,3.75366657145433,127.623480527428));
#50328=CARTESIAN_POINT('Ctrl Pts',(83.186295685137,3.66207265084623,127.521312192333));
#50329=CARTESIAN_POINT('Ctrl Pts',(83.1785493518716,3.57047805411269,127.419143103055));
#50330=CARTESIAN_POINT('Ctrl Pts',(83.1708030186063,3.47460510508494,127.320810649428));
#50331=CARTESIAN_POINT('Ctrl Pts',(83.1630566853409,3.37481739969444,127.22668112085));
#50332=CARTESIAN_POINT('Ctrl Pts',(83.155308617338,3.27500734753928,127.132530512618));
#50333=CARTESIAN_POINT('Ctrl Pts',(83.147560549335,3.17128107886975,127.042584970567));
#50334=CARTESIAN_POINT('Ctrl Pts',(83.139812481332,3.06403709244642,126.95717206505));
#50335=CARTESIAN_POINT('Ctrl Pts',(83.1320561785901,2.95667912583795,126.87166838168));
#50336=CARTESIAN_POINT('Ctrl Pts',(83.1242998758483,2.84579627938628,126.790707201957));
#50337=CARTESIAN_POINT('Ctrl Pts',(83.1165435731064,2.73181845572317,126.714574438868));
#50338=CARTESIAN_POINT('Ctrl Pts',(83.1087831305922,2.61777979866376,126.638401041431));
#50339=CARTESIAN_POINT('Ctrl Pts',(83.101022688078,2.50064320662612,126.567061398925));
#50340=CARTESIAN_POINT('Ctrl Pts',(83.0932622455639,2.38086440965835,126.500796080427));
#50341=CARTESIAN_POINT('Ctrl Pts',(83.0854893452984,2.26089333313223,126.434424386956));
#50342=CARTESIAN_POINT('Ctrl Pts',(83.077716445033,2.13827192572876,126.373143470186));
#50343=CARTESIAN_POINT('Ctrl Pts',(83.0699435447675,2.01347799119524,126.317146622059));
#50344=CARTESIAN_POINT('Ctrl Pts',(83.0624532090056,1.89322063052057,126.26318540041));
#50345=CARTESIAN_POINT('Ctrl Pts',(83.0549628732436,1.77094623994652,126.214130853583));
#50346=CARTESIAN_POINT('Ctrl Pts',(83.0474725374817,1.64709496047675,126.170111891648));
#50347=CARTESIAN_POINT('Ctrl Pts',(83.0396982033626,1.51854782210056,126.124423937392));
#50348=CARTESIAN_POINT('Ctrl Pts',(83.0319238692435,1.38789466019064,126.084016228531));
#50349=CARTESIAN_POINT('Ctrl Pts',(83.0241495351245,1.25560859243,126.049086690113));
#50350=CARTESIAN_POINT('Ctrl Pts',(83.0163847821774,1.12348555542521,126.014200199229));
#50351=CARTESIAN_POINT('Ctrl Pts',(83.0086200292303,0.989733991047752,125.984778544455));
#50352=CARTESIAN_POINT('Ctrl Pts',(83.0008552762832,0.854845609630931,125.960971097179));
#50353=CARTESIAN_POINT('Ctrl Pts',(82.9930982353982,0.720091201256126,125.937187295795));
#50354=CARTESIAN_POINT('Ctrl Pts',(82.9853411945132,0.584202605330228,125.919006672712));
#50355=CARTESIAN_POINT('Ctrl Pts',(82.9775841536282,0.447684919187686,125.906528313819));
#50356=CARTESIAN_POINT('Ctrl Pts',(82.9698329623881,0.311270182094217,125.894059364952));
#50357=CARTESIAN_POINT('Ctrl Pts',(82.962081771148,0.174227686818944,125.887284156587));
#50358=CARTESIAN_POINT('Ctrl Pts',(82.9543305799078,0.0370705555139816,
125.886250326365));
#50359=CARTESIAN_POINT('Ctrl Pts',(82.9465826831307,-0.100028280351483,
125.88521693555));
#50360=CARTESIAN_POINT('Ctrl Pts',(82.9388347863537,-0.237241265203965,
125.88992007237));
#50361=CARTESIAN_POINT('Ctrl Pts',(82.9310868895766,-0.374052568908428,
125.900355342468));
#50362=CARTESIAN_POINT('Ctrl Pts',(82.9233406134925,-0.510835254637467,
125.910788429732));
#50363=CARTESIAN_POINT('Ctrl Pts',(82.9155943374084,-0.647216036759036,
125.926951235604));
#50364=CARTESIAN_POINT('Ctrl Pts',(82.9078480613243,-0.782681902026623,
125.948787314367));
#50365=CARTESIAN_POINT('Ctrl Pts',(82.9001017280589,-0.918148767272268,
125.970623554319));
#50366=CARTESIAN_POINT('Ctrl Pts',(82.8923553947936,-1.05270031620454,125.99813308851));
#50367=CARTESIAN_POINT('Ctrl Pts',(82.8846090615282,-1.1858318466972,126.031208001751));
#50368=CARTESIAN_POINT('Ctrl Pts',(82.8768609935253,-1.31899319107304,126.064290321891));
#50369=CARTESIAN_POINT('Ctrl Pts',(82.8691129255224,-1.45073350486117,126.102940406882));
#50370=CARTESIAN_POINT('Ctrl Pts',(82.8613648575194,-1.58056179553372,126.147000048209));
#50371=CARTESIAN_POINT('Ctrl Pts',(82.8536085547776,-1.71052806925866,126.191106516647));
#50372=CARTESIAN_POINT('Ctrl Pts',(82.8458522520357,-1.83857788967085,126.240633900505));
#50373=CARTESIAN_POINT('Ctrl Pts',(82.8380959492938,-1.96423833720213,126.295375053477));
#50374=CARTESIAN_POINT('Ctrl Pts',(82.8303355067796,-2.0899658534979,126.35014542345));
#50375=CARTESIAN_POINT('Ctrl Pts',(82.8225750642655,-2.21330110439849,126.41013493647));
#50376=CARTESIAN_POINT('Ctrl Pts',(82.8148146217513,-2.33379535910342,126.475090207401));
#50377=CARTESIAN_POINT('Ctrl Pts',(82.8070417214859,-2.45448304188299,126.5401497503));
#50378=CARTESIAN_POINT('Ctrl Pts',(82.7992688212205,-2.57232027862376,126.610190780783));
#50379=CARTESIAN_POINT('Ctrl Pts',(82.791495920955,-2.68688618274251,126.684915788043));
#50380=CARTESIAN_POINT('Ctrl Pts',(82.784005585193,-2.79728732767313,126.756924353067));
#50381=CARTESIAN_POINT('Ctrl Pts',(82.7765152494309,-2.90465060204122,126.833282080065));
#50382=CARTESIAN_POINT('Ctrl Pts',(82.7690249136688,-3.00862964318992,126.913688344987));
#50383=CARTESIAN_POINT('Ctrl Pts',(82.7613420431602,-3.11528140542439,126.996161406421));
#50384=CARTESIAN_POINT('Ctrl Pts',(82.7536591726516,-3.21872733800515,127.083168532652));
#50385=CARTESIAN_POINT('Ctrl Pts',(82.745976302143,-3.31855067135844,127.174428868328));
#50386=CARTESIAN_POINT('Ctrl Pts',(82.7383022090127,-3.41825996046872,127.26558494265));
#50387=CARTESIAN_POINT('Ctrl Pts',(82.7306281158823,-3.51435458540387,127.360984299332));
#50388=CARTESIAN_POINT('Ctrl Pts',(82.7229540227519,-3.6064479870395,127.460303802965));
#50389=CARTESIAN_POINT('Ctrl Pts',(82.7152869408815,-3.69845724964197,127.559532565602));
#50390=CARTESIAN_POINT('Ctrl Pts',(82.707619859011,-3.78647228722919,127.662674061862));
#50391=CARTESIAN_POINT('Ctrl Pts',(82.6999527771406,-3.87014120156489,127.769366360166));
#50392=CARTESIAN_POINT('Ctrl Pts',(82.6922909466049,-3.95375280941995,127.875985582822));
#50393=CARTESIAN_POINT('Ctrl Pts',(82.6846291160692,-4.03302396835301,127.986150456225));
#50394=CARTESIAN_POINT('Ctrl Pts',(82.6769672855335,-4.1076414774153,128.099464213724));
#50395=CARTESIAN_POINT('Ctrl Pts',(82.6693034728789,-4.18227829006,128.212807285542));
#50396=CARTESIAN_POINT('Ctrl Pts',(82.6616396602243,-4.25225879858586,128.329300553625));
#50397=CARTESIAN_POINT('Ctrl Pts',(82.6539758475697,-4.31731150377491,128.448515876953));
#50398=CARTESIAN_POINT('Ctrl Pts',(82.6463181977752,-4.38231189678708,128.567635333199));
#50399=CARTESIAN_POINT('Ctrl Pts',(82.6386605479807,-4.44239221228738,128.689472118773));
#50400=CARTESIAN_POINT('Ctrl Pts',(82.6310028981862,-4.49732678689444,128.813573126551));
#50401=CARTESIAN_POINT('Ctrl Pts',(82.6233360041015,-4.55232767834325,128.937823948666));
#50402=CARTESIAN_POINT('Ctrl Pts',(82.6156691100169,-4.60217022978223,129.064344097086));
#50403=CARTESIAN_POINT('Ctrl Pts',(82.6080022159322,-4.64667602726679,129.192658113962));
#50404=CARTESIAN_POINT('Ctrl Pts',(82.6003353218475,-4.69118182475133,129.320972130837));
#50405=CARTESIAN_POINT('Ctrl Pts',(82.5926684277628,-4.73035075754575,129.451079628921));
#50406=CARTESIAN_POINT('Ctrl Pts',(82.5850015336782,-4.76405452823407,129.582490119308));
#50407=CARTESIAN_POINT('Ctrl Pts',(84.3346156335084,-4.75804253168638,129.583987249709));
#50408=CARTESIAN_POINT('Ctrl Pts',(84.3113635676693,-4.85784354785265,129.98349577336));
#50409=CARTESIAN_POINT('Ctrl Pts',(84.2881115018302,-4.90980811696373,130.395781134632));
#50410=CARTESIAN_POINT('Ctrl Pts',(84.2648594359911,-4.91222318036076,130.80752443328));
#50411=CARTESIAN_POINT('',(84.6101405640561,-4.91824832607103,130.800302834979));
#50412=CARTESIAN_POINT('Ctrl Pts',(84.6799609333917,-4.76405452823403,129.582490119308));
#50413=CARTESIAN_POINT('Ctrl Pts',(84.6707042004072,-4.80445476993726,129.74001004855));
#50414=CARTESIAN_POINT('Ctrl Pts',(84.6614474674228,-4.83707811757595,129.89968928916));
#50415=CARTESIAN_POINT('Ctrl Pts',(84.6521907344383,-4.86172162268382,130.060824521584));
#50416=CARTESIAN_POINT('Ctrl Pts',(84.6430287442445,-4.88611290117459,130.220310532665));
#50417=CARTESIAN_POINT('Ctrl Pts',(84.6338667540507,-4.90268679106901,130.381222826308));
#50418=CARTESIAN_POINT('Ctrl Pts',(84.624704763857,-4.91129310170885,130.542858931898));
#50419=CARTESIAN_POINT('Ctrl Pts',(84.61985003059,-4.91585339283395,130.628506281694));
#50420=CARTESIAN_POINT('Ctrl Pts',(84.6149952973231,-4.91817741637721,130.71435651443));
#50421=CARTESIAN_POINT('Ctrl Pts',(84.6101405640561,-4.91824832607103,130.800302834979));
#50422=CARTESIAN_POINT('Ctrl Pts',(84.6101405640085,-4.91824832607172,130.800302835822));
#50423=CARTESIAN_POINT('Ctrl Pts',(84.6022231096909,-4.91836397076609,130.940470385572));
#50424=CARTESIAN_POINT('Ctrl Pts',(84.5943056553734,-4.91248282886161,131.080726137906));
#50425=CARTESIAN_POINT('Ctrl Pts',(84.5863882010559,-4.90061189985685,131.220516921713));
#50426=CARTESIAN_POINT('Ctrl Pts',(84.578667859878,-4.88903650979596,131.356827470689));
#50427=CARTESIAN_POINT('Ctrl Pts',(84.5709475187001,-4.87176610452158,131.492695517939));
#50428=CARTESIAN_POINT('Ctrl Pts',(84.5632271775222,-4.8488598733744,131.627610877742));
#50429=CARTESIAN_POINT('Ctrl Pts',(84.5555069731711,-4.82595404819188,131.762523846455));
#50430=CARTESIAN_POINT('Ctrl Pts',(84.54778676882,-4.79741266131601,131.896483773269));
#50431=CARTESIAN_POINT('Ctrl Pts',(84.5400665644689,-4.76334632654458,132.028989065665));
#50432=CARTESIAN_POINT('Ctrl Pts',(84.5323447993181,-4.72927310455587,132.161521146759));
#50433=CARTESIAN_POINT('Ctrl Pts',(84.5246230341673,-4.68967281016804,132.292597627195));
#50434=CARTESIAN_POINT('Ctrl Pts',(84.5169012690165,-4.64470626867822,132.421730933913));
#50435=CARTESIAN_POINT('Ctrl Pts',(84.5088363016307,-4.59774114043548,132.556603710638));
#50436=CARTESIAN_POINT('Ctrl Pts',(84.5007713342449,-4.54492193281031,132.68935615759));
#50437=CARTESIAN_POINT('Ctrl Pts',(84.4927063668591,-4.48648790788609,132.819455978806));
#50438=CARTESIAN_POINT('Ctrl Pts',(84.4849719812259,-4.43044908451035,132.944223028686));
#50439=CARTESIAN_POINT('Ctrl Pts',(84.4772375955927,-4.36924685834616,133.066550280504));
#50440=CARTESIAN_POINT('Ctrl Pts',(84.4695032099595,-4.30313890311398,133.185994225619));
#50441=CARTESIAN_POINT('Ctrl Pts',(84.4617632195596,-4.23698304237429,133.305524726472));
#50442=CARTESIAN_POINT('Ctrl Pts',(84.4540232291596,-4.16591457714448,133.422167425126));
#50443=CARTESIAN_POINT('Ctrl Pts',(84.4462832387597,-4.09023414508859,133.535508306881));
#50444=CARTESIAN_POINT('Ctrl Pts',(84.438532281005,-4.01444647593027,133.649009789566));
#50445=CARTESIAN_POINT('Ctrl Pts',(84.4307813232504,-3.93403403030331,133.759199803597));
#50446=CARTESIAN_POINT('Ctrl Pts',(84.4230303654957,-3.84933743120659,133.865697646253));
#50447=CARTESIAN_POINT('Ctrl Pts',(84.4220607971261,-3.83874272199816,133.879019476012));
#50448=CARTESIAN_POINT('Ctrl Pts',(84.4210912287565,-3.82808102276651,133.892283580521));
#50449=CARTESIAN_POINT('Ctrl Pts',(84.4201216603869,-3.81735303935774,133.905489256531));
#50450=CARTESIAN_POINT('Ctrl Pts',(84.4123473262678,-3.73133236246876,134.011376928601));
#50451=CARTESIAN_POINT('Ctrl Pts',(84.4045729921487,-3.6407663472809,134.113850479068));
#50452=CARTESIAN_POINT('Ctrl Pts',(84.3967986580296,-3.54595610683364,134.212494762653));
#50453=CARTESIAN_POINT('Ctrl Pts',(84.3890339050825,-3.45126271153431,134.311017475975));
#50454=CARTESIAN_POINT('Ctrl Pts',(84.3812691521355,-3.35233576668802,134.405720033102));
#50455=CARTESIAN_POINT('Ctrl Pts',(84.3735043991884,-3.24951752112357,134.496219084844));
#50456=CARTESIAN_POINT('Ctrl Pts',(84.3657473583034,-3.14680139608996,134.586628251652));
#50457=CARTESIAN_POINT('Ctrl Pts',(84.3579903174183,-3.04020195322999,134.672841964832));
#50458=CARTESIAN_POINT('Ctrl Pts',(84.3502332765333,-2.93009903210777,134.754512858245));
#50459=CARTESIAN_POINT('Ctrl Pts',(84.3424820852932,-2.82007914045499,134.836122163002));
#50460=CARTESIAN_POINT('Ctrl Pts',(84.3347308940531,-2.70656134201906,134.91319523481));
#50461=CARTESIAN_POINT('Ctrl Pts',(84.326979702813,-2.58995909232361,134.985424472925));
#50462=CARTESIAN_POINT('Ctrl Pts',(84.3192318060359,-2.47340640169484,135.057623011687));
#50463=CARTESIAN_POINT('Ctrl Pts',(84.3114839092588,-2.35377219890244,135.124981606019));
#50464=CARTESIAN_POINT('Ctrl Pts',(84.3037360124817,-2.23149931820796,135.187235684841));
#50465=CARTESIAN_POINT('Ctrl Pts',(84.2959897363977,-2.10925201436422,135.249476741451));
#50466=CARTESIAN_POINT('Ctrl Pts',(84.2882434603135,-1.98436747867226,135.3066152291));
#50467=CARTESIAN_POINT('Ctrl Pts',(84.2804971842294,-1.85731321564461,135.358432496829));
#50468=CARTESIAN_POINT('Ctrl Pts',(84.2727508509641,-1.73025801473109,135.410250147061));
#50469=CARTESIAN_POINT('Ctrl Pts',(84.2650045176987,-1.6010334165379,135.456746351351));
#50470=CARTESIAN_POINT('Ctrl Pts',(84.2572581844333,-1.47012660075453,135.497750739882));
#50471=CARTESIAN_POINT('Ctrl Pts',(84.2495101164304,-1.3391904692975,135.538764311062));
#50472=CARTESIAN_POINT('Ctrl Pts',(84.2417620484274,-1.20657174363826,135.574283502373));
#50473=CARTESIAN_POINT('Ctrl Pts',(84.2340139804244,-1.07277205622993,135.604188028825));
#50474=CARTESIAN_POINT('Ctrl Pts',(84.2262576776826,-0.938830164921678,
135.634124338163));
#50475=CARTESIAN_POINT('Ctrl Pts',(84.2185013749408,-0.803705186746459,
135.658433976839));
#50476=CARTESIAN_POINT('Ctrl Pts',(84.2107450721989,-0.667908775237267,
135.677047856704));
#50477=CARTESIAN_POINT('Ctrl Pts',(84.2029846296847,-0.532039885094409,
135.695671671358));
#50478=CARTESIAN_POINT('Ctrl Pts',(84.1952241871706,-0.395499236582211,
135.708593632932));
#50479=CARTESIAN_POINT('Ctrl Pts',(84.1874637446564,-0.258801877121319,
135.715796726374));
#50480=CARTESIAN_POINT('Ctrl Pts',(84.179690844391,-0.121885078923599,135.723011382861));
#50481=CARTESIAN_POINT('Ctrl Pts',(84.1719179441256,0.0151885417650007,
135.724488821566));
#50482=CARTESIAN_POINT('Ctrl Pts',(84.1641450438601,0.151904764818353,135.720264197268));
#50483=CARTESIAN_POINT('Ctrl Pts',(84.1566547080981,0.28365100879633,135.716193148704));
#50484=CARTESIAN_POINT('Ctrl Pts',(84.149164372336,0.415065081377441,135.706827430218));
#50485=CARTESIAN_POINT('Ctrl Pts',(84.141674036574,0.545694790682726,135.692243621272));
#50486=CARTESIAN_POINT('Ctrl Pts',(84.1338997024549,0.681277365120273,135.677106862778));
#50487=CARTESIAN_POINT('Ctrl Pts',(84.1261253683358,0.816444408737128,135.65630056632));
#50488=CARTESIAN_POINT('Ctrl Pts',(84.1183510342168,0.950683889099185,135.629853670665));
#50489=CARTESIAN_POINT('Ctrl Pts',(84.1105862812697,1.08475793129884,135.603439368445));
#50490=CARTESIAN_POINT('Ctrl Pts',(84.1028215283226,1.21790630483996,135.571398373355));
#50491=CARTESIAN_POINT('Ctrl Pts',(84.0950567753756,1.34962149333913,135.533811419426));
#50492=CARTESIAN_POINT('Ctrl Pts',(84.0872997344906,1.48120586045632,135.49626179739));
#50493=CARTESIAN_POINT('Ctrl Pts',(84.0795426936056,1.61135950175615,135.45317728492));
#50494=CARTESIAN_POINT('Ctrl Pts',(84.0717856527206,1.73958485570378,135.404689691916));
#50495=CARTESIAN_POINT('Ctrl Pts',(84.0640344614805,1.86771351391429,135.356238663782));
#50496=CARTESIAN_POINT('Ctrl Pts',(84.0562832702404,1.99391641493001,135.302392802894));
#50497=CARTESIAN_POINT('Ctrl Pts',(84.0485320790003,2.11771128272307,135.243333695377));
#50498=CARTESIAN_POINT('Ctrl Pts',(84.0407841822232,2.24145353439541,135.184299689555));
#50499=CARTESIAN_POINT('Ctrl Pts',(84.0330362854461,2.3627894363381,135.120057012091));
#50500=CARTESIAN_POINT('Ctrl Pts',(84.025288388669,2.48125703467484,135.050835224858));
#50501=CARTESIAN_POINT('Ctrl Pts',(84.0175421125849,2.59969985214396,134.981627917331));
#50502=CARTESIAN_POINT('Ctrl Pts',(84.0097958365008,2.71527522206464,134.907443768799));
#50503=CARTESIAN_POINT('Ctrl Pts',(84.0020495604167,2.82754648958596,134.828557917865));
#50504=CARTESIAN_POINT('Ctrl Pts',(83.9943032271513,2.93981858586836,134.749671484613));
#50505=CARTESIAN_POINT('Ctrl Pts',(83.986556893886,3.04878621118814,134.666083504474));
#50506=CARTESIAN_POINT('Ctrl Pts',(83.9788105606206,3.15404269607171,134.57811176647));
#50507=CARTESIAN_POINT('Ctrl Pts',(83.9710624926177,3.25932275241521,134.490120327806));
#50508=CARTESIAN_POINT('Ctrl Pts',(83.9633144246147,3.36088971463278,134.39774342846));
#50509=CARTESIAN_POINT('Ctrl Pts',(83.9555663566117,3.45837123896024,134.301338089045));
#50510=CARTESIAN_POINT('Ctrl Pts',(83.9478100538699,3.55595636781174,134.204830288888));
#50511=CARTESIAN_POINT('Ctrl Pts',(83.940053751128,3.64944710662891,134.104285771311));
#50512=CARTESIAN_POINT('Ctrl Pts',(83.9322974483862,3.73850876836502,134.000097661091));
#50513=CARTESIAN_POINT('Ctrl Pts',(83.924537005872,3.82761796499148,133.895853942539));
#50514=CARTESIAN_POINT('Ctrl Pts',(83.9167765633578,3.91229313294367,133.787963063781));
#50515=CARTESIAN_POINT('Ctrl Pts',(83.9090161208437,3.99224156126581,133.676849151747));
#50516=CARTESIAN_POINT('Ctrl Pts',(83.9012432205782,4.07231832990279,133.565556869797));
#50517=CARTESIAN_POINT('Ctrl Pts',(83.8934703203128,4.14765298112051,133.451031542294));
#50518=CARTESIAN_POINT('Ctrl Pts',(83.8856974200474,4.21799714309085,133.333724799209));
#50519=CARTESIAN_POINT('Ctrl Pts',(83.8782070842853,4.28578411758761,133.220682451712));
#50520=CARTESIAN_POINT('Ctrl Pts',(83.8707167485232,4.34893698957217,133.105057670997));
#50521=CARTESIAN_POINT('Ctrl Pts',(83.8632264127612,4.40727576675886,132.987272291968));
#50522=CARTESIAN_POINT('Ctrl Pts',(83.8554520786421,4.46782647641402,132.865021044493));
#50523=CARTESIAN_POINT('Ctrl Pts',(83.847677744523,4.52338263865331,132.740054871111));
#50524=CARTESIAN_POINT('Ctrl Pts',(83.8399034104039,4.57369183444076,132.61282020132));
#50525=CARTESIAN_POINT('Ctrl Pts',(83.8321386574568,4.62393902864056,132.485742336887));
#50526=CARTESIAN_POINT('Ctrl Pts',(83.8243739045097,4.66895198025211,132.356401898778));
#50527=CARTESIAN_POINT('Ctrl Pts',(83.8166091515626,4.70852428810017,132.225269513615));
#50528=CARTESIAN_POINT('Ctrl Pts',(83.8088521106776,4.74805729217426,132.094267370985));
#50529=CARTESIAN_POINT('Ctrl Pts',(83.8010950697926,4.78216029391859,131.961477195029));
#50530=CARTESIAN_POINT('Ctrl Pts',(83.7933380289076,4.81067524457085,131.827388844827));
#50531=CARTESIAN_POINT('Ctrl Pts',(83.7855868376674,4.83916869187696,131.693401611694));
#50532=CARTESIAN_POINT('Ctrl Pts',(83.7778356464273,4.86208239479386,131.558118533749));
#50533=CARTESIAN_POINT('Ctrl Pts',(83.7700844551872,4.8793084448986,131.422043515209));
#50534=CARTESIAN_POINT('Ctrl Pts',(83.7623365584102,4.89652717347253,131.286026332183));
#50535=CARTESIAN_POINT('Ctrl Pts',(83.7545886616331,4.90806300826837,131.149218265083));
#50536=CARTESIAN_POINT('Ctrl Pts',(83.746840764856,4.91385938883968,131.01213205259));
#50537=CARTESIAN_POINT('Ctrl Pts',(83.7390944887719,4.91965455693313,130.875074515578));
#50538=CARTESIAN_POINT('Ctrl Pts',(83.7313482126878,4.91971264229594,130.73773933927));
#50539=CARTESIAN_POINT('Ctrl Pts',(83.7236019366037,4.91402910421499,130.600642612893));
#50540=CARTESIAN_POINT('Ctrl Pts',(83.7158556033384,4.90834552417944,130.463544874499));
#50541=CARTESIAN_POINT('Ctrl Pts',(83.7081092700731,4.89692025232132,130.326685980179));
#50542=CARTESIAN_POINT('Ctrl Pts',(83.7003629368077,4.87980083876222,130.190579845209));
#50543=CARTESIAN_POINT('Ctrl Pts',(83.6926148688048,4.86267759142913,130.054443230213));
#50544=CARTESIAN_POINT('Ctrl Pts',(83.6848668008018,4.839857713749,129.919060097846));
#50545=CARTESIAN_POINT('Ctrl Pts',(83.6771187327988,4.81144031637585,129.784936689824));
#50546=CARTESIAN_POINT('Ctrl Pts',(83.669362430057,4.78299271665458,129.650670733848));
#50547=CARTESIAN_POINT('Ctrl Pts',(83.6616061273151,4.74893579441718,129.517667559799));
#50548=CARTESIAN_POINT('Ctrl Pts',(83.6538498245733,4.70941939014874,129.386421242913));
#50549=CARTESIAN_POINT('Ctrl Pts',(83.6460893820591,4.66988189478548,129.255104875916));
#50550=CARTESIAN_POINT('Ctrl Pts',(83.6383289395449,4.62487923944162,129.125547603642));
#50551=CARTESIAN_POINT('Ctrl Pts',(83.6305684970308,4.57461003669489,128.998224943075));
#50552=CARTESIAN_POINT('Ctrl Pts',(83.6227955967653,4.52426013736125,128.870697892869));
#50553=CARTESIAN_POINT('Ctrl Pts',(83.6150226964999,4.46862695494123,128.74541298026));
#50554=CARTESIAN_POINT('Ctrl Pts',(83.6072497962345,4.40795620748108,128.62282328453));
#50555=CARTESIAN_POINT('Ctrl Pts',(83.5997594604724,4.34949099451108,128.504690033024));
#50556=CARTESIAN_POINT('Ctrl Pts',(83.5922691247103,4.28634826173377,128.389059714973));
#50557=CARTESIAN_POINT('Ctrl Pts',(83.5847787889482,4.21878562057418,128.276311775052));
#50558=CARTESIAN_POINT('Ctrl Pts',(83.5770044548292,4.1486613213403,128.159288962721));
#50559=CARTESIAN_POINT('Ctrl Pts',(83.5692301207101,4.07355320317336,128.045000720816));
#50560=CARTESIAN_POINT('Ctrl Pts',(83.561455786591,3.99370042119825,127.933900722667));
#50561=CARTESIAN_POINT('Ctrl Pts',(83.5536910336439,3.91394605064022,127.822937645338));
#50562=CARTESIAN_POINT('Ctrl Pts',(83.5459262806968,3.82945887679586,127.7151553082));
#50563=CARTESIAN_POINT('Ctrl Pts',(83.5381615277497,3.74052328629487,127.610981747594));
#50564=CARTESIAN_POINT('Ctrl Pts',(83.5304044868647,3.65167602787645,127.506911653637));
#50565=CARTESIAN_POINT('Ctrl Pts',(83.5226474459798,3.55838939748659,127.406443498738));
#50566=CARTESIAN_POINT('Ctrl Pts',(83.5148904050948,3.46099009822698,127.309975034595));
#50567=CARTESIAN_POINT('Ctrl Pts',(83.5071392138547,3.36366424853672,127.213579318072));
#50568=CARTESIAN_POINT('Ctrl Pts',(83.4993880226145,3.26223217977089,127.121177562756));
#50569=CARTESIAN_POINT('Ctrl Pts',(83.4916368313744,3.15705951368052,127.033132927598));
#50570=CARTESIAN_POINT('Ctrl Pts',(83.4838889345974,3.05193154877831,126.945125713759));
#50571=CARTESIAN_POINT('Ctrl Pts',(83.4761410378203,2.94306644780682,126.861472187243));
#50572=CARTESIAN_POINT('Ctrl Pts',(83.4683931410432,2.83086502003662,126.782497081737));
#50573=CARTESIAN_POINT('Ctrl Pts',(83.4606468649591,2.71868706238611,126.70353849612));
#50574=CARTESIAN_POINT('Ctrl Pts',(83.452900588875,2.60317448558009,126.629256609866));
#50575=CARTESIAN_POINT('Ctrl Pts',(83.4451543127909,2.48475903573677,126.559934202039));
#50576=CARTESIAN_POINT('Ctrl Pts',(83.4374079795255,2.36634271177799,126.49061128249));
#50577=CARTESIAN_POINT('Ctrl Pts',(83.4296616462602,2.24502380942433,126.42624811194));
#50578=CARTESIAN_POINT('Ctrl Pts',(83.4219153129948,2.12126040215382,126.367082468886));
#50579=CARTESIAN_POINT('Ctrl Pts',(83.4141672449918,1.99746927892603,126.307903576096));
#50580=CARTESIAN_POINT('Ctrl Pts',(83.4064191769888,1.87123291412311,126.253924695519));
#50581=CARTESIAN_POINT('Ctrl Pts',(83.3986711089859,1.74303079496808,126.205336078569));
#50582=CARTESIAN_POINT('Ctrl Pts',(83.390914806244,1.61469242107529,126.156695821059));
#50583=CARTESIAN_POINT('Ctrl Pts',(83.3831585035021,1.48438448554622,126.113457409923));
#50584=CARTESIAN_POINT('Ctrl Pts',(83.3754022007603,1.35260366031213,126.075761839851));
#50585=CARTESIAN_POINT('Ctrl Pts',(83.3676417582461,1.22075249968341,126.038046150517));
#50586=CARTESIAN_POINT('Ctrl Pts',(83.3598813157319,1.08742726280206,126.005879288723));
#50587=CARTESIAN_POINT('Ctrl Pts',(83.3521208732177,0.953135370523119,125.979351184626));
#50588=CARTESIAN_POINT('Ctrl Pts',(83.3443479729523,0.818627900977277,125.952780495262));
#50589=CARTESIAN_POINT('Ctrl Pts',(83.3365750726869,0.683151061731547,125.931866711726));
#50590=CARTESIAN_POINT('Ctrl Pts',(83.3288021724214,0.547218857826103,125.916648004887));
#50591=CARTESIAN_POINT('Ctrl Pts',(83.3213118366594,0.416228131925276,125.901982536376));
#50592=CARTESIAN_POINT('Ctrl Pts',(83.3138215008974,0.284814881115421,125.892605294422));
#50593=CARTESIAN_POINT('Ctrl Pts',(83.3063311651354,0.153437588217663,125.888504642355));
#50594=CARTESIAN_POINT('Ctrl Pts',(83.2985568310163,0.0170790853282307,
125.884248512817));
#50595=CARTESIAN_POINT('Ctrl Pts',(83.2907824968972,-0.119672621885078,
125.885663513408));
#50596=CARTESIAN_POINT('Ctrl Pts',(83.2830081627781,-0.256306576012906,
125.892793657665));
#50597=CARTESIAN_POINT('Ctrl Pts',(83.275243409831,-0.392772141003785,125.899915014656));
#50598=CARTESIAN_POINT('Ctrl Pts',(83.2674786568839,-0.529119854969217,
125.912737480859));
#50599=CARTESIAN_POINT('Ctrl Pts',(83.2597139039368,-0.664835880894192,
125.931253157846));
#50600=CARTESIAN_POINT('Ctrl Pts',(83.2519568630518,-0.800417111748958,
125.949750444802));
#50601=CARTESIAN_POINT('Ctrl Pts',(83.2441998221668,-0.935367518250482,
125.97392963717));
#50602=CARTESIAN_POINT('Ctrl Pts',(83.2364427812818,-1.06917586962323,126.003730864886));
#50603=CARTESIAN_POINT('Ctrl Pts',(83.2286915900417,-1.2028833150766,126.033509619265));
#50604=CARTESIAN_POINT('Ctrl Pts',(83.2209403988015,-1.33545003956144,126.068901885636));
#50605=CARTESIAN_POINT('Ctrl Pts',(83.2131892075614,-1.46637287968032,126.109796352351));
#50606=CARTESIAN_POINT('Ctrl Pts',(83.2054413107844,-1.59724007410003,126.150673437826));
#50607=CARTESIAN_POINT('Ctrl Pts',(83.1976934140073,-1.72646440140175,126.19704795606));
#50608=CARTESIAN_POINT('Ctrl Pts',(83.1899455172302,-1.85355600673697,126.248758221352));
#50609=CARTESIAN_POINT('Ctrl Pts',(83.1821992411461,-1.98062102724805,126.300457669972));
#50610=CARTESIAN_POINT('Ctrl Pts',(83.174452965062,-2.10555385124076,126.357490498368));
#50611=CARTESIAN_POINT('Ctrl Pts',(83.1667066889779,-2.22788319935621,126.419646315297));
#50612=CARTESIAN_POINT('Ctrl Pts',(83.1589603557126,-2.35021345047912,126.481802591045));
#50613=CARTESIAN_POINT('Ctrl Pts',(83.1512140224473,-2.46993983882313,126.549081753685));
#50614=CARTESIAN_POINT('Ctrl Pts',(83.1434676891819,-2.58661471470199,126.621226938111));
#50615=CARTESIAN_POINT('Ctrl Pts',(83.135719621179,-2.70331571911033,126.693388278952));
#50616=CARTESIAN_POINT('Ctrl Pts',(83.127971553176,-2.81696351877103,126.770417604401));
#50617=CARTESIAN_POINT('Ctrl Pts',(83.120223485173,-2.92713887522575,126.852014343814));
#50618=CARTESIAN_POINT('Ctrl Pts',(83.1124671824312,-3.03743132736064,126.933697805213));
#50619=CARTESIAN_POINT('Ctrl Pts',(83.1047108796893,-3.14424364932664,127.01995814451));
#50620=CARTESIAN_POINT('Ctrl Pts',(83.0969545769474,-3.24718875498737,127.110453708617));
#50621=CARTESIAN_POINT('Ctrl Pts',(83.0891941344333,-3.35018880555083,127.200997572931));
#50622=CARTESIAN_POINT('Ctrl Pts',(83.0814336919191,-3.4493172445754,127.295780896167));
#50623=CARTESIAN_POINT('Ctrl Pts',(83.0736732494049,-3.54422413790561,127.394425380236));
#50624=CARTESIAN_POINT('Ctrl Pts',(83.0659003491395,-3.63928338420618,127.493228217187));
#50625=CARTESIAN_POINT('Ctrl Pts',(83.058127448874,-3.73010728342227,127.595904308099));
#50626=CARTESIAN_POINT('Ctrl Pts',(83.0503545486086,-3.81638588904121,127.702041838261));
#50627=CARTESIAN_POINT('Ctrl Pts',(83.0428642128466,-3.89952805002321,127.804321001857));
#50628=CARTESIAN_POINT('Ctrl Pts',(83.0353738770846,-3.97844946126611,127.909814063253));
#50629=CARTESIAN_POINT('Ctrl Pts',(83.0278835413225,-4.05291209186718,128.018128997959));
#50630=CARTESIAN_POINT('Ctrl Pts',(83.0197220855216,-4.13404643454255,128.13614874771));
#50631=CARTESIAN_POINT('Ctrl Pts',(83.0115606297207,-4.21014831198426,128.257899455109));
#50632=CARTESIAN_POINT('Ctrl Pts',(83.0033991739198,-4.28086393652291,128.382917448818));
#50633=CARTESIAN_POINT('Ctrl Pts',(82.9955264872026,-4.34907749689586,128.50351204891));
#50634=CARTESIAN_POINT('Ctrl Pts',(82.9876538004853,-4.41227920792827,128.627146321197));
#50635=CARTESIAN_POINT('Ctrl Pts',(82.9797811137681,-4.47019316825711,128.753371563239));
#50636=CARTESIAN_POINT('Ctrl Pts',(82.971916466424,-4.52804798842798,128.879467907505));
#50637=CARTESIAN_POINT('Ctrl Pts',(82.9640518190799,-4.58062564658625,129.008149616813));
#50638=CARTESIAN_POINT('Ctrl Pts',(82.9561871717358,-4.62769532321257,129.138942034141));
#50639=CARTESIAN_POINT('Ctrl Pts',(82.9483306012287,-4.67471666021335,129.269600130247));
#50640=CARTESIAN_POINT('Ctrl Pts',(82.9404740307217,-4.71624115631711,129.402364263728));
#50641=CARTESIAN_POINT('Ctrl Pts',(82.9326174602146,-4.7520856600064,129.536738851241));
#50642=CARTESIAN_POINT('Ctrl Pts',(82.9317269973803,-4.75614827209916,129.551968852161));
#50643=CARTESIAN_POINT('Ctrl Pts',(82.930836534546,-4.76013797056555,129.567219520401));
#50644=CARTESIAN_POINT('Ctrl Pts',(82.9299460717117,-4.76405452823408,129.582490119308));
#50645=CARTESIAN_POINT('Origin',(213.235140564004,0.,130.804360617566));
#50646=CARTESIAN_POINT('',(80.8348654436249,-4.76405452823406,129.582490119308));
#50647=CARTESIAN_POINT('',(81.1802785703833,-4.76405452823402,129.582490119308));
#50648=CARTESIAN_POINT('',(213.235140564004,-4.76405452823405,129.582490119308));
#50649=CARTESIAN_POINT('',(82.5148594360284,-4.91824936146013,130.806866809299));
#50650=CARTESIAN_POINT('Ctrl Pts',(82.5148594359911,-4.9182493614598,130.806866809955));
#50651=CARTESIAN_POINT('Ctrl Pts',(82.5067653872794,-4.91817690027791,130.949067449884));
#50652=CARTESIAN_POINT('Ctrl Pts',(82.4986713385677,-4.91193788385077,131.091106696134));
#50653=CARTESIAN_POINT('Ctrl Pts',(82.490577289856,-4.89957058449461,131.232602546918));
#50654=CARTESIAN_POINT('Ctrl Pts',(82.4828029557369,-4.88769179295649,131.368509317391));
#50655=CARTESIAN_POINT('Ctrl Pts',(82.4750286216178,-4.87013512454896,131.504136729985));
#50656=CARTESIAN_POINT('Ctrl Pts',(82.4672542874987,-4.84691722233577,131.638972205267));
#50657=CARTESIAN_POINT('Ctrl Pts',(82.4594895345516,-4.82372793411203,131.773641507876));
#50658=CARTESIAN_POINT('Ctrl Pts',(82.4517247816046,-4.79489135987155,131.907520433511));
#50659=CARTESIAN_POINT('Ctrl Pts',(82.4439600286575,-4.76047603140207,132.040099674546));
#50660=CARTESIAN_POINT('Ctrl Pts',(82.4362029877725,-4.726094884722,132.17254723601));
#50661=CARTESIAN_POINT('Ctrl Pts',(82.4284459468875,-4.68614610804533,132.303697305779));
#50662=CARTESIAN_POINT('Ctrl Pts',(82.4206889060025,-4.64074953320795,132.43304930253));
#50663=CARTESIAN_POINT('Ctrl Pts',(82.4129377147623,-4.59538719228079,132.562303753934));
#50664=CARTESIAN_POINT('Ctrl Pts',(82.4051865235222,-4.54458535931464,132.689762463825));
#50665=CARTESIAN_POINT('Ctrl Pts',(82.3974353322821,-4.48851399484798,132.814938937491));
#50666=CARTESIAN_POINT('Ctrl Pts',(82.389687435505,-4.43246646220698,132.940062207817));
#50667=CARTESIAN_POINT('Ctrl Pts',(82.3819395387279,-4.37115401213281,133.062904815141));
#50668=CARTESIAN_POINT('Ctrl Pts',(82.3741916419508,-4.30479505477375,133.182999429764));
#50669=CARTESIAN_POINT('Ctrl Pts',(82.3664453658667,-4.23844997827803,133.303068923183));
#50670=CARTESIAN_POINT('Ctrl Pts',(82.3586990897826,-4.16706068314926,133.420391225269));
#50671=CARTESIAN_POINT('Ctrl Pts',(82.3509528136985,-4.09089175024567,133.534523204349));
#50672=CARTESIAN_POINT('Ctrl Pts',(82.3432064804331,-4.01472225508037,133.648656025926));
#50673=CARTESIAN_POINT('Ctrl Pts',(82.3354601471678,-3.93377326876532,133.759598152307));
#50674=CARTESIAN_POINT('Ctrl Pts',(82.3277138139024,-3.84835272986233,133.866935405071));
#50675=CARTESIAN_POINT('Ctrl Pts',(82.3199657458995,-3.76291306162192,133.974296695268));
#50676=CARTESIAN_POINT('Ctrl Pts',(82.3122176778965,-3.67300009158274,134.078051199583));
#50677=CARTESIAN_POINT('Ctrl Pts',(82.3044696098935,-3.57896180232162,134.177818113967));
#50678=CARTESIAN_POINT('Ctrl Pts',(82.2967133071516,-3.48482356804753,134.277691061815));
#50679=CARTESIAN_POINT('Ctrl Pts',(82.2889570044098,-3.38655152475659,134.373567668799));
#50680=CARTESIAN_POINT('Ctrl Pts',(82.2812007016679,-3.28453065244961,134.465103910344));
#50681=CARTESIAN_POINT('Ctrl Pts',(82.2734402591538,-3.18245532853136,134.556689007537));
#50682=CARTESIAN_POINT('Ctrl Pts',(82.2656798166396,-3.07662749023608,134.643928874735));
#50683=CARTESIAN_POINT('Ctrl Pts',(82.2579193741255,-2.96746411810112,134.726520707399));
#50684=CARTESIAN_POINT('Ctrl Pts',(82.25014647386,-2.85812550723007,134.809245123806));
#50685=CARTESIAN_POINT('Ctrl Pts',(82.2423735735946,-2.74544098410032,134.887306372584));
#50686=CARTESIAN_POINT('Ctrl Pts',(82.2346006733291,-2.62985608838645,134.960445315557));
#50687=CARTESIAN_POINT('Ctrl Pts',(82.2271103375671,-2.51847299477234,135.030925473728));
#50688=CARTESIAN_POINT('Ctrl Pts',(82.2196200018051,-2.40439700593382,135.09683483517));
#50689=CARTESIAN_POINT('Ctrl Pts',(82.212129666043,-2.28804551597863,135.157983336556));
#50690=CARTESIAN_POINT('Ctrl Pts',(82.2043553319239,-2.16728252391777,135.221450301959));
#50691=CARTESIAN_POINT('Ctrl Pts',(82.1965809978048,-2.04368553241509,135.279989308987));
#50692=CARTESIAN_POINT('Ctrl Pts',(82.1888066636858,-1.91769478504621,135.33333729822));
#50693=CARTESIAN_POINT('Ctrl Pts',(82.1810419107387,-1.79185931001342,135.386619540823));
#50694=CARTESIAN_POINT('Ctrl Pts',(82.1732771577916,-1.66363630547921,135.434723343701));
#50695=CARTESIAN_POINT('Ctrl Pts',(82.1655124048445,-1.53349130947839,135.477431071374));
#50696=CARTESIAN_POINT('Ctrl Pts',(82.1577553639595,-1.40347557532224,135.52009638113));
#50697=CARTESIAN_POINT('Ctrl Pts',(82.1499983230745,-1.27154201766559,135.557376160133));
#50698=CARTESIAN_POINT('Ctrl Pts',(82.1422412821895,-1.13817656178746,135.589100649866));
#50699=CARTESIAN_POINT('Ctrl Pts',(82.1344900909494,-1.00491167783714,135.620801215915));
#50700=CARTESIAN_POINT('Ctrl Pts',(82.1267388997092,-0.870217423766029,
135.646954741106));
#50701=CARTESIAN_POINT('Ctrl Pts',(82.1189877084691,-0.734594969174971,
135.667441255779));
#50702=CARTESIAN_POINT('Ctrl Pts',(82.111239811692,-0.599030157744871,135.687919063137));
#50703=CARTESIAN_POINT('Ctrl Pts',(82.103491914915,-0.4625383162154,135.702734592286));
#50704=CARTESIAN_POINT('Ctrl Pts',(82.0957440181379,-0.325630678316247,
135.711818994755));
#50705=CARTESIAN_POINT('Ctrl Pts',(82.0879977420538,-0.188751678543555,
135.720901496962));
#50706=CARTESIAN_POINT('Ctrl Pts',(82.0802514659697,-0.0514574452606876,
135.724255231154));
#50707=CARTESIAN_POINT('Ctrl Pts',(82.0725051898856,0.0857361898891255,
135.721863273208));
#50708=CARTESIAN_POINT('Ctrl Pts',(82.0647588566203,0.222930837771094,135.719471297604));
#50709=CARTESIAN_POINT('Ctrl Pts',(82.0570125233549,0.360024495132422,135.711333552044));
#50710=CARTESIAN_POINT('Ctrl Pts',(82.0492661900896,0.496502253621075,135.697485240407));
#50711=CARTESIAN_POINT('Ctrl Pts',(82.0415181220866,0.633010575357471,135.683633827536));
#50712=CARTESIAN_POINT('Ctrl Pts',(82.0337700540836,0.768902334870384,135.664069343301));
#50713=CARTESIAN_POINT('Ctrl Pts',(82.0260219860807,0.903669057845986,135.63887872141));
#50714=CARTESIAN_POINT('Ctrl Pts',(82.0182656833388,1.0385790124986,135.613661326626));
#50715=CARTESIAN_POINT('Ctrl Pts',(82.0105093805969,1.172361157148,135.582805921387));
#50716=CARTESIAN_POINT('Ctrl Pts',(82.0027530778551,1.30451796308115,135.546450446586));
#50717=CARTESIAN_POINT('Ctrl Pts',(81.9949926353409,1.43674530508087,135.510075567774));
#50718=CARTESIAN_POINT('Ctrl Pts',(81.9872321928268,1.56734520770359,135.468194889389));
#50719=CARTESIAN_POINT('Ctrl Pts',(81.9794717503126,1.69583752474888,135.420995555717));
#50720=CARTESIAN_POINT('Ctrl Pts',(81.9716988500472,1.82453610906841,135.373720453484));
#50721=CARTESIAN_POINT('Ctrl Pts',(81.9639259497818,1.9511199856992,135.3211097845));
#50722=CARTESIAN_POINT('Ctrl Pts',(81.9561530495163,2.07513030927651,135.263398323397));
#50723=CARTESIAN_POINT('Ctrl Pts',(81.9486627137543,2.19463254522889,135.207784819271));
#50724=CARTESIAN_POINT('Ctrl Pts',(81.9411723779922,2.31174481608836,135.147435078846));
#50725=CARTESIAN_POINT('Ctrl Pts',(81.9336820422302,2.42608160448446,135.082597533736));
#50726=CARTESIAN_POINT('Ctrl Pts',(81.9259077081111,2.54475350696426,135.015301653397));
#50727=CARTESIAN_POINT('Ctrl Pts',(81.918133373992,2.66081122441982,134.94295776719));
#50728=CARTESIAN_POINT('Ctrl Pts',(81.910359039873,2.77379547510258,134.865794074463));
#50729=CARTESIAN_POINT('Ctrl Pts',(81.9025942869259,2.886640482794,134.78872547909));
#50730=CARTESIAN_POINT('Ctrl Pts',(81.8948295339788,2.99641924049701,134.706849114367));
#50731=CARTESIAN_POINT('Ctrl Pts',(81.8870647810317,3.10269701064094,134.620439013336));
#50732=CARTESIAN_POINT('Ctrl Pts',(81.8793077401467,3.2088692242053,134.534114736034));
#50733=CARTESIAN_POINT('Ctrl Pts',(81.8715506992617,3.31154706866801,134.443265928586));
#50734=CARTESIAN_POINT('Ctrl Pts',(81.8637936583767,3.41032506689953,134.348209655064));
#50735=CARTESIAN_POINT('Ctrl Pts',(81.8560424671366,3.50902857587426,134.253225064218));
#50736=CARTESIAN_POINT('Ctrl Pts',(81.8482912758964,3.60383781173919,134.154039592729));
#50737=CARTESIAN_POINT('Ctrl Pts',(81.8405400846563,3.6943809462108,134.051010042246));
#50738=CARTESIAN_POINT('Ctrl Pts',(81.8327921878792,3.78488559743488,133.94802428207));
#50739=CARTESIAN_POINT('Ctrl Pts',(81.8250442911022,3.87112749605116,133.841197985536));
#50740=CARTESIAN_POINT('Ctrl Pts',(81.8172963943251,3.95277238357095,133.730924053779));
#50741=CARTESIAN_POINT('Ctrl Pts',(81.809550118241,4.0344001927404,133.620673188951));
#50742=CARTESIAN_POINT('Ctrl Pts',(81.8018038421569,4.11143267098657,133.506976437366));
#50743=CARTESIAN_POINT('Ctrl Pts',(81.7940575660728,4.18357675996161,133.390258634892));
#50744=CARTESIAN_POINT('Ctrl Pts',(81.7863112328074,4.25572138148787,133.273539970833));
#50745=CARTESIAN_POINT('Ctrl Pts',(81.7785648995421,4.32297733617789,133.15380054395));
#50746=CARTESIAN_POINT('Ctrl Pts',(81.7708185662767,4.3850959215103,133.031492589779));
#50747=CARTESIAN_POINT('Ctrl Pts',(81.7630704982737,4.44722841786919,132.909157245589));
#50748=CARTESIAN_POINT('Ctrl Pts',(81.7553224302708,4.50422107854499,132.784252578039));
#50749=CARTESIAN_POINT('Ctrl Pts',(81.7475743622678,4.55587220054092,132.65725337076));
#50750=CARTESIAN_POINT('Ctrl Pts',(81.739818059526,4.60757821796396,132.530119187212));
#50751=CARTESIAN_POINT('Ctrl Pts',(81.7320617567842,4.6539312086601,132.400886379795));
#50752=CARTESIAN_POINT('Ctrl Pts',(81.7243054540423,4.69477829978572,132.270048093927));
#50753=CARTESIAN_POINT('Ctrl Pts',(81.7165450115281,4.7356471922338,132.139139975726));
#50754=CARTESIAN_POINT('Ctrl Pts',(81.7087845690139,4.77100422883346,132.006625049208));
#50755=CARTESIAN_POINT('Ctrl Pts',(81.7010241264998,4.80074732862297,131.873008431029));
#50756=CARTESIAN_POINT('Ctrl Pts',(81.6932512262343,4.83053817467672,131.739177319593));
#50757=CARTESIAN_POINT('Ctrl Pts',(81.6854783259689,4.85469700615102,131.604241367469));
#50758=CARTESIAN_POINT('Ctrl Pts',(81.6777054257035,4.87317332846537,131.468713515681));
#50759=CARTESIAN_POINT('Ctrl Pts',(81.6702150899414,4.89097798992463,131.338112442679));
#50760=CARTESIAN_POINT('Ctrl Pts',(81.6627247541794,4.90350608713774,131.206962063589));
#50761=CARTESIAN_POINT('Ctrl Pts',(81.6552344184173,4.91075825110139,131.075721008448));
#50762=CARTESIAN_POINT('Ctrl Pts',(81.6474600842982,4.91828538306595,130.939503908812));
#50763=CARTESIAN_POINT('Ctrl Pts',(81.6396857501791,4.92015245386743,130.802757626599));
#50764=CARTESIAN_POINT('Ctrl Pts',(81.63191141606,4.91630320107411,130.665991915872));
#50765=CARTESIAN_POINT('Ctrl Pts',(81.6241466631129,4.91245869214083,130.52939475666));
#50766=CARTESIAN_POINT('Ctrl Pts',(81.6163819101659,4.90291188767403,130.392778603635));
#50767=CARTESIAN_POINT('Ctrl Pts',(81.6086171572188,4.8876583531565,130.256657335378));
#50768=CARTESIAN_POINT('Ctrl Pts',(81.6008601163338,4.87241996866449,130.120671264684));
#50769=CARTESIAN_POINT('Ctrl Pts',(81.5931030754487,4.85148617696365,129.985179486618));
#50770=CARTESIAN_POINT('Ctrl Pts',(81.5853460345637,4.82490456274736,129.850694521451));
#50771=CARTESIAN_POINT('Ctrl Pts',(81.5775948433236,4.79834299393312,129.716310972442));
#50772=CARTESIAN_POINT('Ctrl Pts',(81.5698436520835,4.76614215552057,129.582933107092));
#50773=CARTESIAN_POINT('Ctrl Pts',(81.5620924608434,4.72840125257126,129.451066615073));
#50774=CARTESIAN_POINT('Ctrl Pts',(81.5543445640663,4.69067639051244,129.319256169831));
#50775=CARTESIAN_POINT('Ctrl Pts',(81.5465966672892,4.64741625453818,129.188956195374));
#50776=CARTESIAN_POINT('Ctrl Pts',(81.5388487705121,4.59877072862245,129.060660285495));
#50777=CARTESIAN_POINT('Ctrl Pts',(81.531102494428,4.55013537830209,128.932391212354));
#50778=CARTESIAN_POINT('Ctrl Pts',(81.5233562183439,4.49611701724912,128.806125735303));
#50779=CARTESIAN_POINT('Ctrl Pts',(81.5156099422598,4.43691466671601,128.682340046794));
#50780=CARTESIAN_POINT('Ctrl Pts',(81.5078636089945,4.37771187916459,128.558553444526));
#50781=CARTESIAN_POINT('Ctrl Pts',(81.5001172757291,4.31332519445919,128.43724702003));
#50782=CARTESIAN_POINT('Ctrl Pts',(81.4923709424638,4.24400066137644,128.318874458132));
#50783=CARTESIAN_POINT('Ctrl Pts',(81.4846228744608,4.1746606035452,128.20047538752));
#50784=CARTESIAN_POINT('Ctrl Pts',(81.4768748064578,4.1003806944691,128.085011824201));
#50785=CARTESIAN_POINT('Ctrl Pts',(81.4691267384549,4.0214513576687,127.972910098767));
#50786=CARTESIAN_POINT('Ctrl Pts',(81.461370435713,3.94243813382978,127.860689230286));
#50787=CARTESIAN_POINT('Ctrl Pts',(81.4536141329712,3.85876583659238,127.751837657333));
#50788=CARTESIAN_POINT('Ctrl Pts',(81.4458578302293,3.77076673165735,127.646750553304));
#50789=CARTESIAN_POINT('Ctrl Pts',(81.4380973877152,3.68272065895036,127.541607361124));
#50790=CARTESIAN_POINT('Ctrl Pts',(81.4303369452009,3.59034344017912,127.44023293023));
#50791=CARTESIAN_POINT('Ctrl Pts',(81.4225765026868,3.49400486703745,127.342986172115));
#50792=CARTESIAN_POINT('Ctrl Pts',(81.4148036024213,3.3975116426657,127.245583304872));
#50793=CARTESIAN_POINT('Ctrl Pts',(81.407030702156,3.2970446430831,127.152321617622));
#50794=CARTESIAN_POINT('Ctrl Pts',(81.3992578018905,3.19300812654605,127.063520850039));
#50795=CARTESIAN_POINT('Ctrl Pts',(81.3917674661285,3.09275359943771,126.977948214034));
#50796=CARTESIAN_POINT('Ctrl Pts',(81.3842771303665,2.98918481369777,126.896517987611));
#50797=CARTESIAN_POINT('Ctrl Pts',(81.3767867946045,2.88268796883494,126.819477540632));
#50798=CARTESIAN_POINT('Ctrl Pts',(81.3690124604854,2.77215326372966,126.73951608169));
#50799=CARTESIAN_POINT('Ctrl Pts',(81.3612381263663,2.65811394102197,126.664030556397));
#50800=CARTESIAN_POINT('Ctrl Pts',(81.3534637922472,2.54096846002318,126.593343834452));
#50801=CARTESIAN_POINT('Ctrl Pts',(81.3456990393001,2.42396735036012,126.522744227575));
#50802=CARTESIAN_POINT('Ctrl Pts',(81.337934286353,2.30386803064109,126.456931856807));
#50803=CARTESIAN_POINT('Ctrl Pts',(81.3301695334059,2.18110044450705,126.396188216959));
#50804=CARTESIAN_POINT('Ctrl Pts',(81.3224124925209,2.0584547928702,126.335504908551));
#50805=CARTESIAN_POINT('Ctrl Pts',(81.3146554516359,1.93314649690615,126.27988048477));
#50806=CARTESIAN_POINT('Ctrl Pts',(81.3068984107509,1.80563247512261,126.229551940989));
#50807=CARTESIAN_POINT('Ctrl Pts',(81.2991472195108,1.67821461265507,126.179261350355));
#50808=CARTESIAN_POINT('Ctrl Pts',(81.2913960282707,1.54859469736793,126.13425883353));
#50809=CARTESIAN_POINT('Ctrl Pts',(81.2836448370306,1.41725180306267,126.094734264105));
#50810=CARTESIAN_POINT('Ctrl Pts',(81.2758969402535,1.28596473299101,126.055226493676));
#50811=CARTESIAN_POINT('Ctrl Pts',(81.2681490434763,1.15295651401138,126.021192152314));
#50812=CARTESIAN_POINT('Ctrl Pts',(81.2604011466993,1.01872343651059,125.992771937888));
#50813=CARTESIAN_POINT('Ctrl Pts',(81.2526548706151,0.884518437675891,125.964357668359));
#50814=CARTESIAN_POINT('Ctrl Pts',(81.244908594531,0.749089472187793,125.94155527084));
#50815=CARTESIAN_POINT('Ctrl Pts',(81.2371623184469,0.61294475009084,125.924454696768));
#50816=CARTESIAN_POINT('Ctrl Pts',(81.2294159851816,0.476799023004475,125.907353996464));
#50817=CARTESIAN_POINT('Ctrl Pts',(81.2216696519163,0.339937916683439,125.895955252318));
#50818=CARTESIAN_POINT('Ctrl Pts',(81.2139233186509,0.202876124396793,125.890296684257));
#50819=CARTESIAN_POINT('Ctrl Pts',(81.2061752506479,0.0657836380721764,
125.884636848999));
#50820=CARTESIAN_POINT('Ctrl Pts',(81.1984271826449,-0.0715092330902062,
125.884719763892));
#50821=CARTESIAN_POINT('Ctrl Pts',(81.1906791146419,-0.208486824079857,
125.890531529504));
#50822=CARTESIAN_POINT('Ctrl Pts',(81.1829228119001,-0.345609996483358,
125.896349471929));
#50823=CARTESIAN_POINT('Ctrl Pts',(81.1751665091582,-0.482416828112082,
125.907908411289));
#50824=CARTESIAN_POINT('Ctrl Pts',(81.1674102064163,-0.618395250667723,
125.925142403912));
#50825=CARTESIAN_POINT('Ctrl Pts',(81.1596497639022,-0.754446249001807,
125.942385594836));
#50826=CARTESIAN_POINT('Ctrl Pts',(81.151889321388,-0.889667571971185,125.965309809141));
#50827=CARTESIAN_POINT('Ctrl Pts',(81.1441288788739,-1.02355737572774,125.99379793103));
#50828=CARTESIAN_POINT('Ctrl Pts',(81.1363559786084,-1.15766211128347,126.022331784581));
#50829=CARTESIAN_POINT('Ctrl Pts',(81.128583078343,-1.29043067739237,126.056447296702));
#50830=CARTESIAN_POINT('Ctrl Pts',(81.1208101780776,-1.42137555654968,126.095977180574));
#50831=CARTESIAN_POINT('Ctrl Pts',(81.1133198423155,-1.54756025951983,126.134070053597));
#50832=CARTESIAN_POINT('Ctrl Pts',(81.1058295065534,-1.67205127373518,126.177190379836));
#50833=CARTESIAN_POINT('Ctrl Pts',(81.0983391707913,-1.79443172965663,126.225146948157));
#50834=CARTESIAN_POINT('Ctrl Pts',(81.0905645511766,-1.92145694231566,126.274923632216));
#50835=CARTESIAN_POINT('Ctrl Pts',(81.082789931562,-2.04661061911688,126.330068596351));
#50836=CARTESIAN_POINT('Ctrl Pts',(81.0750153119473,-2.16940569024455,126.390421105788));
#50837=CARTESIAN_POINT('Ctrl Pts',(81.0672503393391,-2.29204839316452,126.450698727824));
#50838=CARTESIAN_POINT('Ctrl Pts',(81.059485366731,-2.41233796615942,126.516170867084));
#50839=CARTESIAN_POINT('Ctrl Pts',(81.0517203941228,-2.52980514577362,126.586627934368));
#50840=CARTESIAN_POINT('Ctrl Pts',(81.0439631991324,-2.64715466691435,126.657014429847));
#50841=CARTESIAN_POINT('Ctrl Pts',(81.0362060041421,-2.76168708758237,126.732375716743));
#50842=CARTESIAN_POINT('Ctrl Pts',(81.0284488091517,-2.87295601645599,126.812455459623));
#50843=CARTESIAN_POINT('Ctrl Pts',(81.0203828355881,-2.98865405419512,126.895722812044));
#50844=CARTESIAN_POINT('Ctrl Pts',(81.0123168620245,-3.1008230318001,126.984091844958));
#50845=CARTESIAN_POINT('Ctrl Pts',(81.0042508884609,-3.20899182468354,127.077223038724));
#50846=CARTESIAN_POINT('Ctrl Pts',(80.9965033315683,-3.31289048865175,127.166677735852));
#50847=CARTESIAN_POINT('Ctrl Pts',(80.9887557746757,-3.41309844799211,127.260525492969));
#50848=CARTESIAN_POINT('Ctrl Pts',(80.9810082177832,-3.50923050459839,127.3584232519));
#50849=CARTESIAN_POINT('Ctrl Pts',(80.9732623064951,-3.60534214246561,127.45630021705));
#50850=CARTESIAN_POINT('Ctrl Pts',(80.9655163952071,-3.69737932647029,127.558225193637));
#50851=CARTESIAN_POINT('Ctrl Pts',(80.957770483919,-3.78499327957319,127.66381784026));
#50852=CARTESIAN_POINT('Ctrl Pts',(80.950024540456,-3.8726075966066,127.769410925495));
#50853=CARTESIAN_POINT('Ctrl Pts',(80.942278596993,-3.9557983970433,127.878671409902));
#50854=CARTESIAN_POINT('Ctrl Pts',(80.93453265353,-4.03425707023025,127.991185728975));
#50855=CARTESIAN_POINT('Ctrl Pts',(80.9267850004671,-4.11273305995673,128.103724880978));
#50856=CARTESIAN_POINT('Ctrl Pts',(80.9190373474043,-4.18647462132941,128.219518975694));
#50857=CARTESIAN_POINT('Ctrl Pts',(80.9112896943415,-4.25521659140841,128.338125668762));
#50858=CARTESIAN_POINT('Ctrl Pts',(80.9035350182762,-4.32402087390902,128.456839875046));
#50859=CARTESIAN_POINT('Ctrl Pts',(80.8957803422108,-4.38781632098078,128.578371431358));
#50860=CARTESIAN_POINT('Ctrl Pts',(80.8880256661455,-4.4463836983863,128.702253325056));
#50861=CARTESIAN_POINT('Ctrl Pts',(80.880266827541,-4.50498251346924,128.826201715824));
#50862=CARTESIAN_POINT('Ctrl Pts',(80.8725079889365,-4.55834751555681,128.952502598175));
#50863=CARTESIAN_POINT('Ctrl Pts',(80.864749150332,-4.60630808629086,129.080670135875));
#50864=CARTESIAN_POINT('Ctrl Pts',(80.8569807784024,-4.65432758642592,129.208995153691));
#50865=CARTESIAN_POINT('Ctrl Pts',(80.8492124064728,-4.69692927701624,129.339191035204));
#50866=CARTESIAN_POINT('Ctrl Pts',(80.8414440345432,-4.7339926362512,129.470757684749));
#50867=CARTESIAN_POINT('Ctrl Pts',(80.8392511709038,-4.74445491760923,129.507896447486));
#50868=CARTESIAN_POINT('Ctrl Pts',(80.8370583072644,-4.75447620437195,129.545144379941));
#50869=CARTESIAN_POINT('Ctrl Pts',(80.834865443625,-4.76405452823406,129.582490119308));
#50870=CARTESIAN_POINT('Ctrl Pts',(82.5850015336782,-4.76405452823407,129.582490119308));
#50871=CARTESIAN_POINT('Ctrl Pts',(82.5773335909647,-4.79776290870888,129.713918583184));
#50872=CARTESIAN_POINT('Ctrl Pts',(82.5696656482512,-4.82600456944424,129.846649998683));
#50873=CARTESIAN_POINT('Ctrl Pts',(82.5619977055377,-4.8487025933768,129.9801845299));
#50874=CARTESIAN_POINT('Ctrl Pts',(82.5541413272862,-4.87195840895081,130.117000599878));
#50875=CARTESIAN_POINT('Ctrl Pts',(82.5462849490346,-4.88939453811731,130.254659320202));
#50876=CARTESIAN_POINT('Ctrl Pts',(82.5384285707831,-4.90098484835512,130.39261970547));
#50877=CARTESIAN_POINT('Ctrl Pts',(82.5305721925315,-4.91257515859294,130.530580090738));
#50878=CARTESIAN_POINT('Ctrl Pts',(82.52271581428,-4.91831969490199,130.668841692983));
#50879=CARTESIAN_POINT('Ctrl Pts',(82.5148594360285,-4.91824936146013,130.806866809299));
#50880=CARTESIAN_POINT('',(82.8601405639574,-4.91824929785569,130.806988666655));
#50881=CARTESIAN_POINT('Ctrl Pts',(82.9299460717117,-4.76405452823408,129.582490119308));
#50882=CARTESIAN_POINT('Ctrl Pts',(82.922096320366,-4.79858039797789,129.717105961436));
#50883=CARTESIAN_POINT('Ctrl Pts',(82.9142465690203,-4.82741833376636,129.853271812892));
#50884=CARTESIAN_POINT('Ctrl Pts',(82.9063968176746,-4.8504404544737,129.99047459354));
#50885=CARTESIAN_POINT('Ctrl Pts',(82.8985501336065,-4.87345357932459,130.127623762423));
#50886=CARTESIAN_POINT('Ctrl Pts',(82.8907034495385,-4.89065534906821,130.265808683398));
#50887=CARTESIAN_POINT('Ctrl Pts',(82.8828567654704,-4.90196890338083,130.404505727903));
#50888=CARTESIAN_POINT('Ctrl Pts',(82.8752846983164,-4.91288650784435,130.538348676841));
#50889=CARTESIAN_POINT('Ctrl Pts',(82.8677126311625,-4.91832107151274,130.672668169506));
#50890=CARTESIAN_POINT('Ctrl Pts',(82.8601405640085,-4.91824929785617,130.806988665748));
#50891=CARTESIAN_POINT('Ctrl Pts',(82.8601405639574,-4.91824929785569,130.806988666655));
#50892=CARTESIAN_POINT('Ctrl Pts',(82.851577185383,-4.9181681277878,130.958893983424));
#50893=CARTESIAN_POINT('Ctrl Pts',(82.8430138068086,-4.91104525378221,131.110552142097));
#50894=CARTESIAN_POINT('Ctrl Pts',(82.8344504282341,-4.89697364043576,131.261342266407));
#50895=CARTESIAN_POINT('Ctrl Pts',(82.8258400492867,-4.88282479459631,131.412960007063));
#50896=CARTESIAN_POINT('Ctrl Pts',(82.8172296703393,-4.86165081058521,131.563699927854));
#50897=CARTESIAN_POINT('Ctrl Pts',(82.8086192913919,-4.83359637437726,131.71294696575));
#50898=CARTESIAN_POINT('Ctrl Pts',(82.7999845646764,-4.80546260799013,131.862616032954));
#50899=CARTESIAN_POINT('Ctrl Pts',(82.791349837961,-4.7704095404838,132.010783547129));
#50900=CARTESIAN_POINT('Ctrl Pts',(82.7827151112456,-4.72863183602382,132.156848703222));
#50901=CARTESIAN_POINT('Ctrl Pts',(82.774048941806,-4.68670200111655,132.30344574487));
#50902=CARTESIAN_POINT('Ctrl Pts',(82.7653827723665,-4.63799858526797,132.447924879106));
#50903=CARTESIAN_POINT('Ctrl Pts',(82.7567166029269,-4.5827656387525,132.589701526964));
#50904=CARTESIAN_POINT('Ctrl Pts',(82.7542897077878,-4.56729807025514,132.629405003791));
#50905=CARTESIAN_POINT('Ctrl Pts',(82.7518628126487,-4.55131870898378,132.668896688921));
#50906=CARTESIAN_POINT('Ctrl Pts',(82.7494359175096,-4.53483355529004,132.708164097003));
#50907=CARTESIAN_POINT('Ctrl Pts',(82.7416615833905,-4.4820248901134,132.833953607023));
#50908=CARTESIAN_POINT('Ctrl Pts',(82.7338872492714,-4.42389479364209,132.957743443183));
#50909=CARTESIAN_POINT('Ctrl Pts',(82.7261129151523,-4.36061562278928,133.079050586064));
#50910=CARTESIAN_POINT('Ctrl Pts',(82.7183481622052,-4.29741443785907,133.200208228733));
#50911=CARTESIAN_POINT('Ctrl Pts',(82.7105834092581,-4.22907698383168,133.318888922698));
#50912=CARTESIAN_POINT('Ctrl Pts',(82.702818656311,-4.15582402939334,133.434628607566));
#50913=CARTESIAN_POINT('Ctrl Pts',(82.695061615426,-4.08264383082204,133.550253338146));
#50914=CARTESIAN_POINT('Ctrl Pts',(82.687304574541,-4.00455805526149,133.662942544433));
#50915=CARTESIAN_POINT('Ctrl Pts',(82.679547533656,-3.921833657157,133.772256139327));
#50916=CARTESIAN_POINT('Ctrl Pts',(82.6717963424159,-3.83917164216473,133.881487299989));
#50917=CARTESIAN_POINT('Ctrl Pts',(82.6640451511758,-3.75187820219944,133.987347605575));
#50918=CARTESIAN_POINT('Ctrl Pts',(82.6562939599357,-3.66026372536504,134.089425688958));
#50919=CARTESIAN_POINT('Ctrl Pts',(82.6485460631586,-3.56868818712707,134.191460386432));
#50920=CARTESIAN_POINT('Ctrl Pts',(82.6407981663814,-3.47279552538185,134.289715768633));
#50921=CARTESIAN_POINT('Ctrl Pts',(82.6330502696044,-3.37293641236893,134.383813511601));
#50922=CARTESIAN_POINT('Ctrl Pts',(82.6253039935202,-3.27309818772981,134.477891571349));
#50923=CARTESIAN_POINT('Ctrl Pts',(82.6175577174362,-3.1692954464943,134.567813453768));
#50924=CARTESIAN_POINT('Ctrl Pts',(82.6098114413521,-3.06191543821069,134.653237974893));
#50925=CARTESIAN_POINT('Ctrl Pts',(82.6020651080867,-2.95453463727226,134.738663126603));
#50926=CARTESIAN_POINT('Ctrl Pts',(82.5943187748213,-2.84357682255117,134.819590607373));
#50927=CARTESIAN_POINT('Ctrl Pts',(82.586572441556,-2.72946169029487,134.895720042465));
#50928=CARTESIAN_POINT('Ctrl Pts',(82.578824373553,-2.61532100274585,134.971866526217));
#50929=CARTESIAN_POINT('Ctrl Pts',(82.57107630555,-2.49802191586648,135.04321260925));
#50930=CARTESIAN_POINT('Ctrl Pts',(82.563328237547,-2.37801206723457,135.109501924258));
#50931=CARTESIAN_POINT('Ctrl Pts',(82.5555719348052,-2.25787467070748,135.175861692339));
#50932=CARTESIAN_POINT('Ctrl Pts',(82.5478156320633,-2.13502110003358,135.237153767129));
#50933=CARTESIAN_POINT('Ctrl Pts',(82.5400593293215,-2.00992299332331,135.293168101009));
#50934=CARTESIAN_POINT('Ctrl Pts',(82.5322988868073,-1.88475811798676,135.349212331425));
#50935=CARTESIAN_POINT('Ctrl Pts',(82.5245384442931,-1.75734668256869,135.399973063411));
#50936=CARTESIAN_POINT('Ctrl Pts',(82.516778001779,-1.62817821159039,135.445289271812));
#50937=CARTESIAN_POINT('Ctrl Pts',(82.5090051015135,-1.49880238791544,135.490678225814));
#50938=CARTESIAN_POINT('Ctrl Pts',(82.5012322012481,-1.36766426655302,135.530605076922));
#50939=CARTESIAN_POINT('Ctrl Pts',(82.4934593009826,-1.23526723443079,135.564959101165));
#50940=CARTESIAN_POINT('Ctrl Pts',(82.4859689652206,-1.10768316791465,135.598064270094));
#50941=CARTESIAN_POINT('Ctrl Pts',(82.4784786294586,-0.97893043172973,135.625994685055));
#50942=CARTESIAN_POINT('Ctrl Pts',(82.4709882936966,-0.849464520335529,
135.648696804413));
#50943=CARTESIAN_POINT('Ctrl Pts',(82.4632139595775,-0.715089869560122,
135.672259681526));
#50944=CARTESIAN_POINT('Ctrl Pts',(82.4554396254585,-0.579521237438656,
135.690264615214));
#50945=CARTESIAN_POINT('Ctrl Pts',(82.4476652913394,-0.443258165010642,
135.702595530435));
#50946=CARTESIAN_POINT('Ctrl Pts',(82.4399005383923,-0.307163024641307,
135.714911248905));
#50947=CARTESIAN_POINT('Ctrl Pts',(82.4321357854452,-0.170375532459404,
135.72156682744));
#50948=CARTESIAN_POINT('Ctrl Pts',(82.4243710324981,-0.0334054464857481,
135.72249716901));
#50949=CARTESIAN_POINT('Ctrl Pts',(82.4166139916131,0.103428598867672,135.72342658655));
#50950=CARTESIAN_POINT('Ctrl Pts',(82.4088569507281,0.240444488682426,135.718642080652));
#50951=CARTESIAN_POINT('Ctrl Pts',(82.4010999098431,0.377127669820007,135.708130369824));
#50952=CARTESIAN_POINT('Ctrl Pts',(82.393348718603,0.513707777107358,135.697626585958));
#50953=CARTESIAN_POINT('Ctrl Pts',(82.3855975273628,0.64995528687834,135.681404223587));
#50954=CARTESIAN_POINT('Ctrl Pts',(82.3778463361227,0.785356331966813,135.659502067034));
#50955=CARTESIAN_POINT('Ctrl Pts',(82.3700984393456,0.920699827999275,135.637609219481));
#50956=CARTESIAN_POINT('Ctrl Pts',(82.3623505425686,1.05519718976395,135.610041441435));
#50957=CARTESIAN_POINT('Ctrl Pts',(82.3546026457915,1.18834057568716,135.576889270039));
#50958=CARTESIAN_POINT('Ctrl Pts',(82.3468563697074,1.32145611088417,135.543744033363));
#50959=CARTESIAN_POINT('Ctrl Pts',(82.3391100936233,1.45321785444385,135.505016821227));
#50960=CARTESIAN_POINT('Ctrl Pts',(82.3313638175392,1.58312944079426,135.460849019376));
#50961=CARTESIAN_POINT('Ctrl Pts',(82.3236174842739,1.71304198612249,135.416680891488));
#50962=CARTESIAN_POINT('Ctrl Pts',(82.3158711510085,1.84110397683198,135.367072219595));
#50963=CARTESIAN_POINT('Ctrl Pts',(82.3081248177432,1.96683584307418,135.312213746152));
#50964=CARTESIAN_POINT('Ctrl Pts',(82.3003767497402,2.09259586609605,135.257342987533));
#50965=CARTESIAN_POINT('Ctrl Pts',(82.2926286817372,2.21602436802573,135.197220244264));
#50966=CARTESIAN_POINT('Ctrl Pts',(82.2848806137343,2.33666370074194,135.132083553723));
#50967=CARTESIAN_POINT('Ctrl Pts',(82.2771243109924,2.45743125037659,135.066877635132));
#50968=CARTESIAN_POINT('Ctrl Pts',(82.2693680082506,2.57540336459376,134.996647310296));
#50969=CARTESIAN_POINT('Ctrl Pts',(82.2616117055087,2.69014839246293,134.921675845846));
#50970=CARTESIAN_POINT('Ctrl Pts',(82.2538512629946,2.80495466320845,134.846664366869));
#50971=CARTESIAN_POINT('Ctrl Pts',(82.2460908204804,2.91653009768779,134.76690693331));
#50972=CARTESIAN_POINT('Ctrl Pts',(82.2383303779662,3.02447462091655,134.682728357986));
#50973=CARTESIAN_POINT('Ctrl Pts',(82.2305574777008,3.13259242627686,134.59841465174));
#50974=CARTESIAN_POINT('Ctrl Pts',(82.2227845774354,3.23706737472395,134.509665874504));
#50975=CARTESIAN_POINT('Ctrl Pts',(82.21501167717,3.33753421811541,134.416845690948));
#50976=CARTESIAN_POINT('Ctrl Pts',(82.2075213414079,3.4343488386893,134.327399754864));
#50977=CARTESIAN_POINT('Ctrl Pts',(82.2000310056458,3.52744148669571,134.234173502969));
#50978=CARTESIAN_POINT('Ctrl Pts',(82.1925406698838,3.6165209101586,134.13752121509));
#50979=CARTESIAN_POINT('Ctrl Pts',(82.1847663357647,3.70897780703686,134.03720432634));
#50980=CARTESIAN_POINT('Ctrl Pts',(82.1769920016456,3.79740402478476,133.932878703086));
#50981=CARTESIAN_POINT('Ctrl Pts',(82.1692176675265,3.88143189204782,133.824901881958));
#50982=CARTESIAN_POINT('Ctrl Pts',(82.1614529145794,3.96535620247422,133.717058132612));
#50983=CARTESIAN_POINT('Ctrl Pts',(82.1536881616323,4.04489270993608,133.605572444186));
#50984=CARTESIAN_POINT('Ctrl Pts',(82.1459234086852,4.11971110979609,133.490838504004));
#50985=CARTESIAN_POINT('Ctrl Pts',(82.1381663678002,4.1944551989666,133.37621851919));
#50986=CARTESIAN_POINT('Ctrl Pts',(82.1304093269152,4.26449029389417,133.258357028291));
#50987=CARTESIAN_POINT('Ctrl Pts',(82.1226522860302,4.32952709194406,133.137679760466));
#50988=CARTESIAN_POINT('Ctrl Pts',(82.1149010947901,4.39451484523863,133.017093496307));
#50989=CARTESIAN_POINT('Ctrl Pts',(82.10714990355,4.45451161939667,132.893696024492));
#50990=CARTESIAN_POINT('Ctrl Pts',(82.0993987123099,4.50927228701171,132.767940639895));
#50991=CARTESIAN_POINT('Ctrl Pts',(82.0916508155328,4.56400967988226,132.642238704691));
#50992=CARTESIAN_POINT('Ctrl Pts',(82.0839029187557,4.61351523676614,132.51418120766));
#50993=CARTESIAN_POINT('Ctrl Pts',(82.0761550219786,4.65759062835227,132.38424434784));
#50994=CARTESIAN_POINT('Ctrl Pts',(82.0684087458945,4.70165680031662,132.25433466801));
#50995=CARTESIAN_POINT('Ctrl Pts',(82.0606624698104,4.7402949407882,132.122546777342));
#50996=CARTESIAN_POINT('Ctrl Pts',(82.0529161937263,4.77335570388328,131.9893747047));
#50997=CARTESIAN_POINT('Ctrl Pts',(82.045169860461,4.80641671102539,131.856201649011));
#50998=CARTESIAN_POINT('Ctrl Pts',(82.0374235271956,4.83390016443737,131.721644770405));
#50999=CARTESIAN_POINT('Ctrl Pts',(82.0296771939302,4.85570732193208,131.586210645535));
#51000=CARTESIAN_POINT('Ctrl Pts',(82.0219291259273,4.87751936298852,131.450746191132));
#51001=CARTESIAN_POINT('Ctrl Pts',(82.0141810579243,4.8936525165128,131.314404485464));
#51002=CARTESIAN_POINT('Ctrl Pts',(82.0064329899213,4.9040596801063,131.177699225877));
#51003=CARTESIAN_POINT('Ctrl Pts',(81.9986766871794,4.9144779045571,131.040848674313));
#51004=CARTESIAN_POINT('Ctrl Pts',(81.9909203844376,4.9191579526102,130.903634187434));
#51005=CARTESIAN_POINT('Ctrl Pts',(81.9831640816957,4.91810482663278,130.766572037924));
#51006=CARTESIAN_POINT('Ctrl Pts',(81.9754036391816,4.91705113857032,130.629436734219));
#51007=CARTESIAN_POINT('Ctrl Pts',(81.9676431966674,4.91025819858745,130.492454320189));
#51008=CARTESIAN_POINT('Ctrl Pts',(81.9598827541533,4.8977830306026,130.35613695951));
#51009=CARTESIAN_POINT('Ctrl Pts',(81.9521098538878,4.88528783637061,130.219600770102));
#51010=CARTESIAN_POINT('Ctrl Pts',(81.9443369536223,4.86709223816449,130.083732155184));
#51011=CARTESIAN_POINT('Ctrl Pts',(81.9365640533569,4.84330477182661,129.949034977998));
#51012=CARTESIAN_POINT('Ctrl Pts',(81.9290737175949,4.82038203980718,129.819234382486));
#51013=CARTESIAN_POINT('Ctrl Pts',(81.9215833818329,4.79226700394512,129.690521834871));
#51014=CARTESIAN_POINT('Ctrl Pts',(81.9140930460709,4.75910030108536,129.56333387059));
#51015=CARTESIAN_POINT('Ctrl Pts',(81.9063187119518,4.7246760726058,129.431323535986));
#51016=CARTESIAN_POINT('Ctrl Pts',(81.8985443778327,4.68470050173065,129.30053750697));
#51017=CARTESIAN_POINT('Ctrl Pts',(81.8907700437136,4.63927565880348,129.171478373149));
#51018=CARTESIAN_POINT('Ctrl Pts',(81.8830052907665,4.59390679793552,129.042578293175));
#51019=CARTESIAN_POINT('Ctrl Pts',(81.8752405378195,4.54310215589425,128.915401239073));
#51020=CARTESIAN_POINT('Ctrl Pts',(81.8674757848724,4.48701441525125,128.790437903104));
#51021=CARTESIAN_POINT('Ctrl Pts',(81.8597187439874,4.43098238174296,128.665598682481));
#51022=CARTESIAN_POINT('Ctrl Pts',(81.8519617031024,4.36967785094957,128.542969158864));
#51023=CARTESIAN_POINT('Ctrl Pts',(81.8442046622174,4.30330262572821,128.423022847761));
#51024=CARTESIAN_POINT('Ctrl Pts',(81.8364534709772,4.23697745458051,128.303166989104));
#51025=CARTESIAN_POINT('Ctrl Pts',(81.8287022797371,4.16558938867971,128.185990656141));
#51026=CARTESIAN_POINT('Ctrl Pts',(81.820951088497,4.08938730049043,128.071945098453));
#51027=CARTESIAN_POINT('Ctrl Pts',(81.8132031917199,4.01321760022133,127.95794801317));
#51028=CARTESIAN_POINT('Ctrl Pts',(81.8054552949428,3.93223816392902,127.84707938097));
#51029=CARTESIAN_POINT('Ctrl Pts',(81.7977073981658,3.84674242951302,127.739763459132));
#51030=CARTESIAN_POINT('Ctrl Pts',(81.7899611220817,3.76126457896165,127.632469985471));
#51031=CARTESIAN_POINT('Ctrl Pts',(81.7822148459976,3.67127255282988,127.528728049599));
#51032=CARTESIAN_POINT('Ctrl Pts',(81.7744685699135,3.57710126649333,127.428930335105));
#51033=CARTESIAN_POINT('Ctrl Pts',(81.7667222366481,3.48292928500574,127.329131883928));
#51034=CARTESIAN_POINT('Ctrl Pts',(81.7589759033827,3.38457825007597,127.23327799658));
#51035=CARTESIAN_POINT('Ctrl Pts',(81.7512295701174,3.28242098642447,127.141725564714));
#51036=CARTESIAN_POINT('Ctrl Pts',(81.7434815021144,3.18024084536216,127.050152630316));
#51037=CARTESIAN_POINT('Ctrl Pts',(81.7357334341115,3.07425307054073,126.962883329097));
#51038=CARTESIAN_POINT('Ctrl Pts',(81.7279853661085,2.96486439008743,126.880234955601));
#51039=CARTESIAN_POINT('Ctrl Pts',(81.7202290633667,2.85535945004272,126.79749874243));
#51040=CARTESIAN_POINT('Ctrl Pts',(81.7124727606248,2.74244669640408,126.719393503649));
#51041=CARTESIAN_POINT('Ctrl Pts',(81.7047164578829,2.62656318790534,126.646194088621));
#51042=CARTESIAN_POINT('Ctrl Pts',(81.6969560153688,2.51061782888877,126.572955604861));
#51043=CARTESIAN_POINT('Ctrl Pts',(81.6891955728546,2.3916988944344,126.50462835689));
#51044=CARTESIAN_POINT('Ctrl Pts',(81.6814351303404,2.27026810516819,126.441441205847));
#51045=CARTESIAN_POINT('Ctrl Pts',(81.673662230075,2.14864238441902,126.37815262118));
#51046=CARTESIAN_POINT('Ctrl Pts',(81.6658893298096,2.02449710540683,126.320020788138));
#51047=CARTESIAN_POINT('Ctrl Pts',(81.6581164295442,1.8983148488219,126.267226742834));
#51048=CARTESIAN_POINT('Ctrl Pts',(81.6506260937821,1.77671963509715,126.216351894057));
#51049=CARTESIAN_POINT('Ctrl Pts',(81.6431357580201,1.65323325982777,126.170433594022));
#51050=CARTESIAN_POINT('Ctrl Pts',(81.635645422258,1.52829901028968,126.129589479034));
#51051=CARTESIAN_POINT('Ctrl Pts',(81.6278710881389,1.39862784070796,126.087196747014));
#51052=CARTESIAN_POINT('Ctrl Pts',(81.6200967540198,1.26698607792881,126.050136283649));
#51053=CARTESIAN_POINT('Ctrl Pts',(81.6123224199007,1.13385173633451,126.018593876227));
#51054=CARTESIAN_POINT('Ctrl Pts',(81.6045576669536,1.00088147091768,125.987090342003));
#51055=CARTESIAN_POINT('Ctrl Pts',(81.5967929140065,0.866422663464341,125.961091422));
#51056=CARTESIAN_POINT('Ctrl Pts',(81.5890281610594,0.730970675930676,125.940733891199));
#51057=CARTESIAN_POINT('Ctrl Pts',(81.5812711201744,0.59565322122066,125.920396579785));
#51058=CARTESIAN_POINT('Ctrl Pts',(81.5735140792894,0.459344933612567,125.905689564869));
#51059=CARTESIAN_POINT('Ctrl Pts',(81.5657570384044,0.322553274488322,125.896699010689));
#51060=CARTESIAN_POINT('Ctrl Pts',(81.5580058471643,0.185864771018213,125.887715236356));
#51061=CARTESIAN_POINT('Ctrl Pts',(81.5502546559242,0.0486940101203715,
125.884439367856));
#51062=CARTESIAN_POINT('Ctrl Pts',(81.542503464684,-0.0884448375064001,
125.886905933157));
#51063=CARTESIAN_POINT('Ctrl Pts',(81.534755567907,-0.225525397464632,125.889371450102));
#51064=CARTESIAN_POINT('Ctrl Pts',(81.5270076711299,-0.362573681045943,
125.89757453949));
#51065=CARTESIAN_POINT('Ctrl Pts',(81.5192597743528,-0.499074138234663,
125.911497645129));
#51066=CARTESIAN_POINT('Ctrl Pts',(81.5115134982687,-0.635546042470348,
125.925417838354));
#51067=CARTESIAN_POINT('Ctrl Pts',(81.5037672221846,-0.771469959545438,
125.945055628269));
#51068=CARTESIAN_POINT('Ctrl Pts',(81.4960209461005,-0.906334483693587,
125.970341496155));
#51069=CARTESIAN_POINT('Ctrl Pts',(81.4882746128351,-1.04120000338102,125.995627550695));
#51070=CARTESIAN_POINT('Ctrl Pts',(81.4805282795698,-1.17500573026741,126.026561694355));
#51071=CARTESIAN_POINT('Ctrl Pts',(81.4727819463044,-1.30724988042935,126.063023167793));
#51072=CARTESIAN_POINT('Ctrl Pts',(81.4650338783015,-1.43952364575162,126.099492806526));
#51073=CARTESIAN_POINT('Ctrl Pts',(81.4572858102985,-1.5702347616486,126.141492134233));
#51074=CARTESIAN_POINT('Ctrl Pts',(81.4495377422955,-1.69889643274634,126.188850464473));
#51075=CARTESIAN_POINT('Ctrl Pts',(81.4417814395537,-1.8276948469993,126.236259127711));
#51076=CARTESIAN_POINT('Ctrl Pts',(81.4340251368118,-1.95443909783057,126.289038035815));
#51077=CARTESIAN_POINT('Ctrl Pts',(81.4262688340699,-2.07866170576452,126.346968041688));
#51078=CARTESIAN_POINT('Ctrl Pts',(81.4185083915558,-2.20295061504476,126.404928966551));
#51079=CARTESIAN_POINT('Ctrl Pts',(81.4107479490416,-2.3247148527201,126.468046287552));
#51080=CARTESIAN_POINT('Ctrl Pts',(81.4029875065274,-2.44351230015598,126.53605525109));
#51081=CARTESIAN_POINT('Ctrl Pts',(81.395214606262,-2.56250045180074,126.604173388654));
#51082=CARTESIAN_POINT('Ctrl Pts',(81.3874417059966,-2.67851196504096,126.677198652156));
#51083=CARTESIAN_POINT('Ctrl Pts',(81.3796688057311,-2.79113368241745,126.754822887235));
#51084=CARTESIAN_POINT('Ctrl Pts',(81.3721784699691,-2.8996613166897,126.829625285845));
#51085=CARTESIAN_POINT('Ctrl Pts',(81.3646881342072,-3.00504108513744,126.908697907888));
#51086=CARTESIAN_POINT('Ctrl Pts',(81.3571977984452,-3.10693440940455,126.991731388522));
#51087=CARTESIAN_POINT('Ctrl Pts',(81.3495289385518,-3.21125625193625,127.076743883245));
#51088=CARTESIAN_POINT('Ctrl Pts',(81.3418600786585,-3.31227284385009,127.166193516741));
#51089=CARTESIAN_POINT('Ctrl Pts',(81.3341912187651,-3.40957549528741,127.259790403219));
#51090=CARTESIAN_POINT('Ctrl Pts',(81.326531144205,-3.50676667823614,127.353280066479));
#51091=CARTESIAN_POINT('Ctrl Pts',(81.318871069645,-3.60025209160735,127.450907262715));
#51092=CARTESIAN_POINT('Ctrl Pts',(81.3112109950849,-3.68965426932632,127.552340562993));
#51093=CARTESIAN_POINT('Ctrl Pts',(81.3035579300338,-3.77897463774127,127.653681044642));
#51094=CARTESIAN_POINT('Ctrl Pts',(81.2959048649828,-3.86421893559665,127.758820405727));
#51095=CARTESIAN_POINT('Ctrl Pts',(81.2882517999317,-3.94504530048864,127.867389279675));
#51096=CARTESIAN_POINT('Ctrl Pts',(81.2806039750461,-4.02581632238755,127.975883814929));
#51097=CARTESIAN_POINT('Ctrl Pts',(81.2729561501605,-4.10217518854663,128.08780287122));
#51098=CARTESIAN_POINT('Ctrl Pts',(81.2653083252748,-4.17381959123836,128.202743220197));
#51099=CARTESIAN_POINT('Ctrl Pts',(81.2576631539417,-4.24543913559636,128.31764368852));
#51100=CARTESIAN_POINT('Ctrl Pts',(81.2500179826086,-4.31234725350306,128.435563026244));
#51101=CARTESIAN_POINT('Ctrl Pts',(81.2423728112755,-4.37428458156263,128.556068496421));
#51102=CARTESIAN_POINT('Ctrl Pts',(81.2347293281183,-4.43620823287052,128.676547357065));
#51103=CARTESIAN_POINT('Ctrl Pts',(81.2270858449612,-4.49316309720848,128.799610854807));
#51104=CARTESIAN_POINT('Ctrl Pts',(81.2194423618041,-4.54493580077072,128.924801725333));
#51105=CARTESIAN_POINT('Ctrl Pts',(81.2117965489251,-4.59672428457306,129.050030753842));
#51106=CARTESIAN_POINT('Ctrl Pts',(81.204150736046,-4.64332729735608,129.177388078851));
#51107=CARTESIAN_POINT('Ctrl Pts',(81.196504923167,-4.68457970185101,129.306396639526));
#51108=CARTESIAN_POINT('Ctrl Pts',(81.1910961389058,-4.71376238781293,129.397659593981));
#51109=CARTESIAN_POINT('Ctrl Pts',(81.1856873546445,-4.74026842832691,129.489748476775));
#51110=CARTESIAN_POINT('Ctrl Pts',(81.1802785703833,-4.76405452823402,129.582490119308));
#51111=CARTESIAN_POINT('Origin',(213.235140564004,0.,130.804360617566));
#51112=CARTESIAN_POINT('',(79.0845758390371,-4.76405452823407,129.582490119308));
#51113=CARTESIAN_POINT('',(79.4301745447722,-4.76405452823408,129.582490119308));
#51114=CARTESIAN_POINT('',(213.235140564004,-4.76405452823405,129.582490119308));
#51115=CARTESIAN_POINT('',(80.7648594359615,-4.91824805085141,130.799981942384));
#51116=CARTESIAN_POINT('Ctrl Pts',(80.7648594359614,-4.91824805085141,130.799981942385));
#51117=CARTESIAN_POINT('Ctrl Pts',(80.7572118377638,-4.91836808905016,130.934812139328));
#51118=CARTESIAN_POINT('Ctrl Pts',(80.7495642395661,-4.91293955423797,131.069824535811));
#51119=CARTESIAN_POINT('Ctrl Pts',(80.7419166413684,-4.90194425981586,131.204517506996));
#51120=CARTESIAN_POINT('Ctrl Pts',(80.7342755102555,-4.89095826341109,131.339096576949));
#51121=CARTESIAN_POINT('Ctrl Pts',(80.7266343791426,-4.87441490385902,131.473356359034));
#51122=CARTESIAN_POINT('Ctrl Pts',(80.7189932480296,-4.85234805594347,131.606795291843));
#51123=CARTESIAN_POINT('Ctrl Pts',(80.7113561437386,-4.83029283710029,131.74016390328));
#51124=CARTESIAN_POINT('Ctrl Pts',(80.7037190394476,-4.80271998351891,131.872712128746));
#51125=CARTESIAN_POINT('Ctrl Pts',(80.6960819351566,-4.76971516029594,132.003944025313));
#51126=CARTESIAN_POINT('Ctrl Pts',(80.6884468335639,-4.73671899201585,132.13514150859));
#51127=CARTESIAN_POINT('Ctrl Pts',(80.6808117319711,-4.69829378405131,132.26502295834));
#51128=CARTESIAN_POINT('Ctrl Pts',(80.6731766303783,-4.65457610529979,132.393103624623));
#51129=CARTESIAN_POINT('Ctrl Pts',(80.6655417659445,-4.61085978449238,132.521180312506));
#51130=CARTESIAN_POINT('Ctrl Pts',(80.6579069015108,-4.56185145022658,132.64745594647));
#51131=CARTESIAN_POINT('Ctrl Pts',(80.650272037077,-4.50773705983245,132.771462460866));
#51132=CARTESIAN_POINT('Ctrl Pts',(80.6426356446608,-4.45361183940423,132.895493792963));
#51133=CARTESIAN_POINT('Ctrl Pts',(80.6349992522445,-4.39437869263396,133.017254733084));
#51134=CARTESIAN_POINT('Ctrl Pts',(80.6273628598282,-4.33027084295917,133.136299186465));
#51135=CARTESIAN_POINT('Ctrl Pts',(80.6197186820037,-4.26609763444075,133.25546500732));
#51136=CARTESIAN_POINT('Ctrl Pts',(80.6120745041792,-4.19703999081989,133.371908455793));
#51137=CARTESIAN_POINT('Ctrl Pts',(80.6044303263548,-4.12337620251523,133.485209691093));
#51138=CARTESIAN_POINT('Ctrl Pts',(80.5967820282655,-4.04967270891822,133.598571996544));
#51139=CARTESIAN_POINT('Ctrl Pts',(80.5891337301762,-3.97135836115872,133.708788388718));
#51140=CARTESIAN_POINT('Ctrl Pts',(80.5814854320869,-3.88875274177736,133.815470907114));
#51141=CARTESIAN_POINT('Ctrl Pts',(80.5738254851517,-3.80602130876754,133.922315909791));
#51142=CARTESIAN_POINT('Ctrl Pts',(80.5661655382165,-3.71898581138502,134.025615982294));
#51143=CARTESIAN_POINT('Ctrl Pts',(80.5585055912813,-3.62800415247761,134.125018524082));
#51144=CARTESIAN_POINT('Ctrl Pts',(80.5528183685761,-3.56045369022636,134.198821175378));
#51145=CARTESIAN_POINT('Ctrl Pts',(80.5471311458709,-3.49072869504952,134.270476063957));
#51146=CARTESIAN_POINT('Ctrl Pts',(80.5414439231657,-3.41898725962216,134.339853395248));
#51147=CARTESIAN_POINT('Ctrl Pts',(80.5336695890466,-3.32091797025072,134.43469099555));
#51148=CARTESIAN_POINT('Ctrl Pts',(80.5258952549275,-3.21874437560722,134.525595276033));
#51149=CARTESIAN_POINT('Ctrl Pts',(80.5181209208084,-3.11281508625975,134.612190091328));
#51150=CARTESIAN_POINT('Ctrl Pts',(80.5103561678613,-3.00701634529437,134.698678186253));
#51151=CARTESIAN_POINT('Ctrl Pts',(80.5025914149143,-2.89747141886499,134.780867138288));
#51152=CARTESIAN_POINT('Ctrl Pts',(80.4948266619672,-2.78456595452368,134.858417290506));
#51153=CARTESIAN_POINT('Ctrl Pts',(80.4870696210822,-2.67177262948109,134.935890418819));
#51154=CARTESIAN_POINT('Ctrl Pts',(80.4793125801972,-2.55562572894983,135.008733696171));
#51155=CARTESIAN_POINT('Ctrl Pts',(80.4715555393122,-2.43654391702278,135.076647686914));
#51156=CARTESIAN_POINT('Ctrl Pts',(80.4638043480721,-2.31755190561634,135.144510463188));
#51157=CARTESIAN_POINT('Ctrl Pts',(80.4560531568319,-2.19562972637481,135.207451158837));
#51158=CARTESIAN_POINT('Ctrl Pts',(80.4483019655918,-2.07122466125247,135.265213839218));
#51159=CARTESIAN_POINT('Ctrl Pts',(80.4405540688147,-1.9468724716016,135.322951968918));
#51160=CARTESIAN_POINT('Ctrl Pts',(80.4328061720376,-1.82003984882979,135.37551629626));
#51161=CARTESIAN_POINT('Ctrl Pts',(80.4250582752605,-1.69119809548402,135.422697121583));
#51162=CARTESIAN_POINT('Ctrl Pts',(80.4173119991764,-1.56238329305555,135.469868077694));
#51163=CARTESIAN_POINT('Ctrl Pts',(80.4095657230923,-1.43156056287851,135.511657637332));
#51164=CARTESIAN_POINT('Ctrl Pts',(80.4018194470082,-1.29922020765802,135.547904642292));
#51165=CARTESIAN_POINT('Ctrl Pts',(80.3940731137429,-1.16687887553118,135.584151914819));
#51166=CARTESIAN_POINT('Ctrl Pts',(80.3863267804775,-1.03302027308394,135.614856447748));
#51167=CARTESIAN_POINT('Ctrl Pts',(80.3785804472122,-0.898148461546721,
135.639907370884));
#51168=CARTESIAN_POINT('Ctrl Pts',(80.3708323792092,-0.763246446402719,
135.664963904));
#51169=CARTESIAN_POINT('Ctrl Pts',(80.3630843112063,-0.627331154979045,
135.684364236575));
#51170=CARTESIAN_POINT('Ctrl Pts',(80.3553362432033,-0.490915006359956,
135.698048952455));
#51171=CARTESIAN_POINT('Ctrl Pts',(80.3475799404615,-0.35435387303437,135.711748212614));
#51172=CARTESIAN_POINT('Ctrl Pts',(80.3398236377196,-0.217291208785866,
135.719719682272));
#51173=CARTESIAN_POINT('Ctrl Pts',(80.3320673349778,-0.0802432576695204,
135.721955973235));
#51174=CARTESIAN_POINT('Ctrl Pts',(80.3243068924636,0.0568778400650496,
135.724193457774));
#51175=CARTESIAN_POINT('Ctrl Pts',(80.3165464499494,0.193983818373639,135.720689674225));
#51176=CARTESIAN_POINT('Ctrl Pts',(80.3087860074352,0.330561292654718,135.711489339568));
#51177=CARTESIAN_POINT('Ctrl Pts',(80.3010131071698,0.467358013222105,135.702274235718));
#51178=CARTESIAN_POINT('Ctrl Pts',(80.2932402069044,0.60362414552211,135.687344349521));
#51179=CARTESIAN_POINT('Ctrl Pts',(80.2854673066389,0.738853366851134,135.666796094237));
#51180=CARTESIAN_POINT('Ctrl Pts',(80.2779769708769,0.869166665362811,135.646994819791));
#51181=CARTESIAN_POINT('Ctrl Pts',(80.2704866351149,0.998516830283219,135.621976626608));
#51182=CARTESIAN_POINT('Ctrl Pts',(80.2629962993529,1.12646407699086,135.591871635386));
#51183=CARTESIAN_POINT('Ctrl Pts',(80.2552219652338,1.25926248244623,135.560625204272));
#51184=CARTESIAN_POINT('Ctrl Pts',(80.2474476311147,1.39097015179278,135.523799649453));
#51185=CARTESIAN_POINT('Ctrl Pts',(80.2396732969956,1.52108219075252,135.481484951115));
#51186=CARTESIAN_POINT('Ctrl Pts',(80.2319085440485,1.65103387825269,135.439222401861));
#51187=CARTESIAN_POINT('Ctrl Pts',(80.2241437911015,1.77939347983067,135.391484288934));
#51188=CARTESIAN_POINT('Ctrl Pts',(80.2163790381544,1.90566678057145,135.338411475676));
#51189=CARTESIAN_POINT('Ctrl Pts',(80.2086219972694,2.03181466488979,135.285391375084));
#51190=CARTESIAN_POINT('Ctrl Pts',(80.2008649563843,2.15588001393795,135.227047268921));
#51191=CARTESIAN_POINT('Ctrl Pts',(80.1931079154993,2.2773846058556,135.163569538863));
#51192=CARTESIAN_POINT('Ctrl Pts',(80.1853567242592,2.39879757021539,135.100139677854));
#51193=CARTESIAN_POINT('Ctrl Pts',(80.1776055330191,2.5176532760326,135.031584078853));
#51194=CARTESIAN_POINT('Ctrl Pts',(80.1698543417789,2.63349463142193,134.958140713909));
#51195=CARTESIAN_POINT('Ctrl Pts',(80.1621064450019,2.74928675114489,134.884728564354));
#51196=CARTESIAN_POINT('Ctrl Pts',(80.1543585482248,2.86206673910389,134.806432989613));
#51197=CARTESIAN_POINT('Ctrl Pts',(80.1466106514477,2.97140341849634,134.723537162077));
#51198=CARTESIAN_POINT('Ctrl Pts',(80.1388643753636,3.0807172270124,134.640658674562));
#51199=CARTESIAN_POINT('Ctrl Pts',(80.1311180992795,3.18658884826157,134.553182084324));
#51200=CARTESIAN_POINT('Ctrl Pts',(80.1233718231954,3.28861767469218,134.461432786966));
#51201=CARTESIAN_POINT('Ctrl Pts',(80.1156254899301,3.39064725427655,134.369682812336));
#51202=CARTESIAN_POINT('Ctrl Pts',(80.1078791566648,3.48883369172806,134.273660329073));
#51203=CARTESIAN_POINT('Ctrl Pts',(80.1001328233994,3.58281125140452,134.173729490116));
#51204=CARTESIAN_POINT('Ctrl Pts',(80.0923847553964,3.67680985670381,134.073776272341));
#51205=CARTESIAN_POINT('Ctrl Pts',(80.0846366873934,3.76659744087556,133.969913241981));
#51206=CARTESIAN_POINT('Ctrl Pts',(80.0768886193904,3.85184704039493,133.862539395843));
#51207=CARTESIAN_POINT('Ctrl Pts',(80.0691323166486,3.93718724420322,133.755051431502));
#51208=CARTESIAN_POINT('Ctrl Pts',(80.0613760139068,4.01797958535831,133.644045504318));
#51209=CARTESIAN_POINT('Ctrl Pts',(80.0536197111649,4.09393880544138,133.529951951534));
#51210=CARTESIAN_POINT('Ctrl Pts',(80.0458592686507,4.1699385672473,133.415797503586));
#51211=CARTESIAN_POINT('Ctrl Pts',(80.0380988261366,4.24109986519031,133.298552480399));
#51212=CARTESIAN_POINT('Ctrl Pts',(80.0303383836224,4.3071828240157,133.178672977599));
#51213=CARTESIAN_POINT('Ctrl Pts',(80.022565483357,4.37337186507316,133.058601033578));
#51214=CARTESIAN_POINT('Ctrl Pts',(80.0147925830915,4.43446610197331,132.935886509045));
#51215=CARTESIAN_POINT('Ctrl Pts',(80.0070196828261,4.49027297013191,132.811007501351));
#51216=CARTESIAN_POINT('Ctrl Pts',(79.9995293470641,4.54405111806405,132.690668160137));
#51217=CARTESIAN_POINT('Ctrl Pts',(79.992039011302,4.59291952728006,132.568319258483));
#51218=CARTESIAN_POINT('Ctrl Pts',(79.98454867554,4.6367499576783,132.444401133063));
#51219=CARTESIAN_POINT('Ctrl Pts',(79.9767743414209,4.68224223216699,132.315784614253));
#51220=CARTESIAN_POINT('Ctrl Pts',(79.9690000073018,4.72245106236455,132.185070109983));
#51221=CARTESIAN_POINT('Ctrl Pts',(79.9612256731827,4.75717924345912,132.052731038596));
#51222=CARTESIAN_POINT('Ctrl Pts',(79.9534609202356,4.79186462517414,131.920555063287));
#51223=CARTESIAN_POINT('Ctrl Pts',(79.9456961672886,4.82108269876557,131.786758879042));
#51224=CARTESIAN_POINT('Ctrl Pts',(79.9379314143415,4.84468484131862,131.651834422942));
#51225=CARTESIAN_POINT('Ctrl Pts',(79.9301743734566,4.8682635418909,131.517043975714));
#51226=CARTESIAN_POINT('Ctrl Pts',(79.9224173325716,4.88623734460999,131.381127869331));
#51227=CARTESIAN_POINT('Ctrl Pts',(79.9146602916866,4.89850793237532,131.244591351336));
#51228=CARTESIAN_POINT('Ctrl Pts',(79.9069091004465,4.91076926679497,131.108157796592));
#51229=CARTESIAN_POINT('Ctrl Pts',(79.8991579092064,4.91733591196603,130.971105149296));
#51230=CARTESIAN_POINT('Ctrl Pts',(79.8914067179663,4.91816101118458,130.833946603504));
#51231=CARTESIAN_POINT('Ctrl Pts',(79.8836588211892,4.91898575971395,130.696846353751));
#51232=CARTESIAN_POINT('Ctrl Pts',(79.8759109244121,4.91407381353474,130.559640685163));
#51233=CARTESIAN_POINT('Ctrl Pts',(79.868163027635,4.90343035200612,130.422845420588));
#51234=CARTESIAN_POINT('Ctrl Pts',(79.8604167515509,4.89278911686022,130.286078770634));
#51235=CARTESIAN_POINT('Ctrl Pts',(79.8526704754668,4.87641878137003,130.149722743478));
#51236=CARTESIAN_POINT('Ctrl Pts',(79.8449241993827,4.85437657190657,130.014290265873));
#51237=CARTESIAN_POINT('Ctrl Pts',(79.8371778661174,4.83233419973252,129.878856788535));
#51238=CARTESIAN_POINT('Ctrl Pts',(79.829431532852,4.80461993284453,129.74434726024));
#51239=CARTESIAN_POINT('Ctrl Pts',(79.8216851995867,4.77134245437662,129.611266218299));
#51240=CARTESIAN_POINT('Ctrl Pts',(79.8139371315837,4.73805752364807,129.478155373781));
#51241=CARTESIAN_POINT('Ctrl Pts',(79.8061890635807,4.69920699708112,129.346474031395));
#51242=CARTESIAN_POINT('Ctrl Pts',(79.7984409955777,4.65494983021665,129.216712942335));
#51243=CARTESIAN_POINT('Ctrl Pts',(79.7906846928359,4.61064562630863,129.086813941646));
#51244=CARTESIAN_POINT('Ctrl Pts',(79.782928390094,4.56092342977415,128.95883964176));
#51245=CARTESIAN_POINT('Ctrl Pts',(79.7751720873522,4.50599110638188,128.833262646458));
#51246=CARTESIAN_POINT('Ctrl Pts',(79.767411644838,4.45102946395463,128.707618626932));
#51247=CARTESIAN_POINT('Ctrl Pts',(79.7596512023238,4.39085232514546,128.584374812678));
#51248=CARTESIAN_POINT('Ctrl Pts',(79.7518907598097,4.32571375768699,128.463979548369));
#51249=CARTESIAN_POINT('Ctrl Pts',(79.7441178595442,4.26047062401726,128.343391014893));
#51250=CARTESIAN_POINT('Ctrl Pts',(79.7363449592788,4.19025034642582,128.225660505131));
#51251=CARTESIAN_POINT('Ctrl Pts',(79.7285720590133,4.11535107589342,128.111208452418));
#51252=CARTESIAN_POINT('Ctrl Pts',(79.7210817232513,4.04317458250418,128.000917020107));
#51253=CARTESIAN_POINT('Ctrl Pts',(79.7135913874892,3.96665355529998,127.893670073526));
#51254=CARTESIAN_POINT('Ctrl Pts',(79.7061010517271,3.88608914508753,127.789813517431));
#51255=CARTESIAN_POINT('Ctrl Pts',(79.698326717608,3.80247011077556,127.682019208446));
#51256=CARTESIAN_POINT('Ctrl Pts',(79.6905523834889,3.71423015118311,127.57753599839));
#51257=CARTESIAN_POINT('Ctrl Pts',(79.6827780493698,3.62166097255255,127.476785695436));
#51258=CARTESIAN_POINT('Ctrl Pts',(79.6750132964227,3.52920587716163,127.376159558226));
#51259=CARTESIAN_POINT('Ctrl Pts',(79.6672485434757,3.43243244051844,127.279257459676));
#51260=CARTESIAN_POINT('Ctrl Pts',(79.6594837905286,3.33167420890646,127.186470344464));
#51261=CARTESIAN_POINT('Ctrl Pts',(79.6517267496436,3.23101605179008,127.093775386722));
#51262=CARTESIAN_POINT('Ctrl Pts',(79.6439697087586,3.12638126155002,127.005187542014));
#51263=CARTESIAN_POINT('Ctrl Pts',(79.6362126678735,3.01814177445785,126.921062625939));
#51264=CARTESIAN_POINT('Ctrl Pts',(79.6284614766334,2.90998391160531,126.837001149118));
#51265=CARTESIAN_POINT('Ctrl Pts',(79.6207102853933,2.79822707001655,126.757396140999));
#51266=CARTESIAN_POINT('Ctrl Pts',(79.6129590941532,2.68327768719087,126.682564417373));
#51267=CARTESIAN_POINT('Ctrl Pts',(79.6052111973761,2.56837716091925,126.607764499227));
#51268=CARTESIAN_POINT('Ctrl Pts',(79.597463300599,2.4502871191785,126.537734043354));
#51269=CARTESIAN_POINT('Ctrl Pts',(79.5897154038219,2.32944433791154,126.472747507064));
#51270=CARTESIAN_POINT('Ctrl Pts',(79.5819691277378,2.20862683434936,126.407774564557));
#51271=CARTESIAN_POINT('Ctrl Pts',(79.5742228516537,2.08505808069978,126.347843628078));
#51272=CARTESIAN_POINT('Ctrl Pts',(79.5664765755696,1.95920054901721,126.293183800899));
#51273=CARTESIAN_POINT('Ctrl Pts',(79.5587302423043,1.83334208828294,126.238523570234));
#51274=CARTESIAN_POINT('Ctrl Pts',(79.5509839090389,1.70519517440829,126.189134682254));
#51275=CARTESIAN_POINT('Ctrl Pts',(79.5432375757736,1.5752430348128,126.145198413503));
#51276=CARTESIAN_POINT('Ctrl Pts',(79.5354895077706,1.44526179333632,126.101252305528));
#51277=CARTESIAN_POINT('Ctrl Pts',(79.5277414397676,1.31347489199163,126.062761371778));
#51278=CARTESIAN_POINT('Ctrl Pts',(79.5199933717646,1.18038113300863,126.029857141461));
#51279=CARTESIAN_POINT('Ctrl Pts',(79.5122370690227,1.04714592039503,125.996917940137));
#51280=CARTESIAN_POINT('Ctrl Pts',(79.5044807662809,0.912601455721774,125.969577397253));
#51281=CARTESIAN_POINT('Ctrl Pts',(79.4967244635391,0.777257710458418,125.947916083338));
#51282=CARTESIAN_POINT('Ctrl Pts',(79.4889640210249,0.641841728163002,125.926243208127));
#51283=CARTESIAN_POINT('Ctrl Pts',(79.4812035785107,0.505626003350469,125.910255647311));
#51284=CARTESIAN_POINT('Ctrl Pts',(79.4734431359965,0.36912507090641,125.899981987757));
#51285=CARTESIAN_POINT('Ctrl Pts',(79.4656702357311,0.232405015047702,125.889691836012));
#51286=CARTESIAN_POINT('Ctrl Pts',(79.4578973354657,0.0953992276199499,
125.885133928038));
#51287=CARTESIAN_POINT('Ctrl Pts',(79.4501244352002,-0.041377411016928,
125.886284675456));
#51288=CARTESIAN_POINT('Ctrl Pts',(79.4426340994382,-0.173181874319512,
125.887393590308));
#51289=CARTESIAN_POINT('Ctrl Pts',(79.4351437636762,-0.304773252202186,
125.893803303403));
#51290=CARTESIAN_POINT('Ctrl Pts',(79.4276534279142,-0.435697745829174,
125.90544741801));
#51291=CARTESIAN_POINT('Ctrl Pts',(79.4198790937951,-0.571586281426142,
125.917533022762));
#51292=CARTESIAN_POINT('Ctrl Pts',(79.412104759676,-0.707186818704931,125.935296072674));
#51293=CARTESIAN_POINT('Ctrl Pts',(79.4043304255569,-0.841986804155042,
125.958719144641));
#51294=CARTESIAN_POINT('Ctrl Pts',(79.3965656726098,-0.976620660670781,
125.982113349766));
#51295=CARTESIAN_POINT('Ctrl Pts',(79.3888009196627,-1.11045554691931,126.011153631549));
#51296=CARTESIAN_POINT('Ctrl Pts',(79.3810361667156,-1.24298226015877,126.045770683202));
#51297=CARTESIAN_POINT('Ctrl Pts',(79.3732791258306,-1.37537734599815,126.080353352711));
#51298=CARTESIAN_POINT('Ctrl Pts',(79.3655220849456,-1.50646646866026,126.120501671209));
#51299=CARTESIAN_POINT('Ctrl Pts',(79.3577650440606,-1.63574922976492,126.166095045197));
#51300=CARTESIAN_POINT('Ctrl Pts',(79.3500138528205,-1.76493449773253,126.211654036867));
#51301=CARTESIAN_POINT('Ctrl Pts',(79.3422626615804,-1.89231574828529,126.262649781464));
#51302=CARTESIAN_POINT('Ctrl Pts',(79.3345114703403,-2.01740674592696,126.318911578285));
#51303=CARTESIAN_POINT('Ctrl Pts',(79.3267635735633,-2.14244457655867,126.375149462341));
#51304=CARTESIAN_POINT('Ctrl Pts',(79.3190156767862,-2.26519373452042,126.436648786953));
#51305=CARTESIAN_POINT('Ctrl Pts',(79.3112677800091,-2.38518722303943,126.50319043103));
#51306=CARTESIAN_POINT('Ctrl Pts',(79.303521503925,-2.5051556115074,126.569718156028));
#51307=CARTESIAN_POINT('Ctrl Pts',(79.2957752278409,-2.62236913538159,126.641285913061));
#51308=CARTESIAN_POINT('Ctrl Pts',(79.2880289517568,-2.73638506614919,126.717628447206));
#51309=CARTESIAN_POINT('Ctrl Pts',(79.2802826184915,-2.8504018385561,126.793971544894));
#51310=CARTESIAN_POINT('Ctrl Pts',(79.2725362852262,-2.961220645891,126.875089272501));
#51311=CARTESIAN_POINT('Ctrl Pts',(79.2647899519608,-3.06842777884041,126.960673061515));
#51312=CARTESIAN_POINT('Ctrl Pts',(79.2570418839579,-3.17565892008443,127.046276016425));
#51313=CARTESIAN_POINT('Ctrl Pts',(79.2492938159548,-3.27927647201899,127.13634677904));
#51314=CARTESIAN_POINT('Ctrl Pts',(79.2415457479518,-3.37890016060658,127.230536787667));
#51315=CARTESIAN_POINT('Ctrl Pts',(79.23378944521,-3.47862973043593,127.324826902556));
#51316=CARTESIAN_POINT('Ctrl Pts',(79.2260331424681,-3.57435667307585,127.423244739924));
#51317=CARTESIAN_POINT('Ctrl Pts',(79.2182768397263,-3.66573755022288,127.52540479667));
#51318=CARTESIAN_POINT('Ctrl Pts',(79.2105163972121,-3.75716720009572,127.627619379315));
#51319=CARTESIAN_POINT('Ctrl Pts',(79.2027559546979,-3.8442459143172,127.733579859291));
#51320=CARTESIAN_POINT('Ctrl Pts',(79.1949955121837,-3.9266715232722,127.842868795726));
#51321=CARTESIAN_POINT('Ctrl Pts',(79.1872226119182,-4.00922944913182,127.952333172465));
#51322=CARTESIAN_POINT('Ctrl Pts',(79.1794497116528,-4.08711912085463,128.06513636104));
#51323=CARTESIAN_POINT('Ctrl Pts',(79.1716768113874,-4.16008207859903,128.180832427929));
#51324=CARTESIAN_POINT('Ctrl Pts',(79.1641864756254,-4.23039264904657,128.292322651366));
#51325=CARTESIAN_POINT('Ctrl Pts',(79.1566961398633,-4.29612832993051,128.406498810934));
#51326=CARTESIAN_POINT('Ctrl Pts',(79.1492058041013,-4.35709969334681,128.522943223765));
#51327=CARTESIAN_POINT('Ctrl Pts',(79.1409632472063,-4.42419413983025,128.65108163149));
#51328=CARTESIAN_POINT('Ctrl Pts',(79.1327206903113,-4.48571150014336,128.782333424784));
#51329=CARTESIAN_POINT('Ctrl Pts',(79.1244781334162,-4.54136974383764,128.916201749182));
#51330=CARTESIAN_POINT('Ctrl Pts',(79.1162547834092,-4.59689829213924,129.049758132281));
#51331=CARTESIAN_POINT('Ctrl Pts',(79.1080314334022,-4.6465948238171,129.185918594868));
#51332=CARTESIAN_POINT('Ctrl Pts',(79.0998080833951,-4.69022365273293,129.324162945009));
#51333=CARTESIAN_POINT('Ctrl Pts',(79.0947306686091,-4.71716178145714,129.409520361011));
#51334=CARTESIAN_POINT('Ctrl Pts',(79.0896532538231,-4.74178760065504,129.495671706625));
#51335=CARTESIAN_POINT('Ctrl Pts',(79.0845758390371,-4.76405452823407,129.582490119308));
#51336=CARTESIAN_POINT('Ctrl Pts',(80.834865443625,-4.76405452823406,129.582490119308));
#51337=CARTESIAN_POINT('Ctrl Pts',(80.8298741447429,-4.78585628385885,129.667494833602));
#51338=CARTESIAN_POINT('Ctrl Pts',(80.8248828458608,-4.80536250632687,129.753006308476));
#51339=CARTESIAN_POINT('Ctrl Pts',(80.8198915469787,-4.82255633145487,129.838890010844));
#51340=CARTESIAN_POINT('Ctrl Pts',(80.8086626854037,-4.86123706103406,130.032101483092));
#51341=CARTESIAN_POINT('Ctrl Pts',(80.7974338238288,-4.88831646052915,130.22770670874));
#51342=CARTESIAN_POINT('Ctrl Pts',(80.7862049622537,-4.90356361051494,130.424562012864));
#51343=CARTESIAN_POINT('Ctrl Pts',(80.7790897868329,-4.91322497699388,130.549299504017));
#51344=CARTESIAN_POINT('Ctrl Pts',(80.771974611412,-4.91813636965101,130.674538570167));
#51345=CARTESIAN_POINT('Ctrl Pts',(80.7648594359911,-4.91824805085094,130.799981941862));
#51346=CARTESIAN_POINT('',(81.1101405640462,-4.91824902053953,130.807464560535));
#51347=CARTESIAN_POINT('Ctrl Pts',(81.1802785703833,-4.76405452823402,129.582490119308));
#51348=CARTESIAN_POINT('Ctrl Pts',(81.1726260494128,-4.7977078631708,129.713703961466));
#51349=CARTESIAN_POINT('Ctrl Pts',(81.1649735284423,-4.8259143747193,129.846224591726));
#51350=CARTESIAN_POINT('Ctrl Pts',(81.1573210074718,-4.84859535890923,129.979553908049));
#51351=CARTESIAN_POINT('Ctrl Pts',(81.1494576002342,-4.871901380013,130.116557480468));
#51352=CARTESIAN_POINT('Ctrl Pts',(81.1415941929966,-4.88937286395555,130.254414499012));
#51353=CARTESIAN_POINT('Ctrl Pts',(81.133730785759,-4.90098157502492,130.392580744617));
#51354=CARTESIAN_POINT('Ctrl Pts',(81.1258673785213,-4.9125902860943,130.530746990221));
#51355=CARTESIAN_POINT('Ctrl Pts',(81.1180039712838,-4.9183362664278,130.669222006222));
#51356=CARTESIAN_POINT('Ctrl Pts',(81.1101405640462,-4.91824902053953,130.807464560535));
#51357=CARTESIAN_POINT('Ctrl Pts',(81.1101405640085,-4.91824902053911,130.807464561198));
#51358=CARTESIAN_POINT('Ctrl Pts',(81.0996771008831,-4.91813292654806,130.991417372709));
#51359=CARTESIAN_POINT('Ctrl Pts',(81.0892136377577,-4.90769710711438,131.175044159719));
#51360=CARTESIAN_POINT('Ctrl Pts',(81.0787501746323,-4.88704688904051,131.357493302208));
#51361=CARTESIAN_POINT('Ctrl Pts',(81.0709758405132,-4.87170381447581,131.493052684074));
#51362=CARTESIAN_POINT('Ctrl Pts',(81.0632015063941,-4.85069184088119,131.628187907528));
#51363=CARTESIAN_POINT('Ctrl Pts',(81.055427172275,-4.82404068621336,131.76238698477));
#51364=CARTESIAN_POINT('Ctrl Pts',(81.0476624193279,-4.79742237671175,131.896420673643));
#51365=CARTESIAN_POINT('Ctrl Pts',(81.0398976663808,-4.76517878956605,132.029520132061));
#51366=CARTESIAN_POINT('Ctrl Pts',(81.0321329134337,-4.72739143106729,132.161177967091));
#51367=CARTESIAN_POINT('Ctrl Pts',(81.0243758725487,-4.68964160350576,132.292705037703));
#51368=CARTESIAN_POINT('Ctrl Pts',(81.0166188316638,-4.64635906924106,132.422792960993));
#51369=CARTESIAN_POINT('Ctrl Pts',(81.0088617907788,-4.59767639522331,132.550944376596));
#51370=CARTESIAN_POINT('Ctrl Pts',(81.0011105995387,-4.54903043318877,132.678999152219));
#51371=CARTESIAN_POINT('Ctrl Pts',(80.9933594082985,-4.49499257532123,132.80511996286));
#51372=CARTESIAN_POINT('Ctrl Pts',(80.9856082170584,-4.43574514147814,132.928824809393));
#51373=CARTESIAN_POINT('Ctrl Pts',(80.9778603202813,-4.37652288937483,133.052477078066));
#51374=CARTESIAN_POINT('Ctrl Pts',(80.9701124235042,-4.3120956337143,133.173715073085));
#51375=CARTESIAN_POINT('Ctrl Pts',(80.9623645267272,-4.24269363912157,133.292077190461));
#51376=CARTESIAN_POINT('Ctrl Pts',(80.9546182506431,-4.17330616192998,133.410414549034));
#51377=CARTESIAN_POINT('Ctrl Pts',(80.9468719745589,-4.09894621326297,133.525876889475));
#51378=CARTESIAN_POINT('Ctrl Pts',(80.9391256984748,-4.01988959592007,133.638027976152));
#51379=CARTESIAN_POINT('Ctrl Pts',(80.9313793652095,-3.94083239499918,133.750179890702));
#51380=CARTESIAN_POINT('Ctrl Pts',(80.9236330319441,-3.85707868147744,133.859020183162));
#51381=CARTESIAN_POINT('Ctrl Pts',(80.9158866986788,-3.76894686289186,133.964142668151));
#51382=CARTESIAN_POINT('Ctrl Pts',(80.9081386306758,-3.68079530779669,134.069288694591));
#51383=CARTESIAN_POINT('Ctrl Pts',(80.9003905626729,-3.58826394779479,134.17071495728));
#51384=CARTESIAN_POINT('Ctrl Pts',(80.8926424946699,-3.49171036973018,134.268049656209));
#51385=CARTESIAN_POINT('Ctrl Pts',(80.884886191928,-3.39505417337366,134.365487803616));
#51386=CARTESIAN_POINT('Ctrl Pts',(80.8771298891862,-3.29436749523585,134.458825422532));
#51387=CARTESIAN_POINT('Ctrl Pts',(80.8693735864444,-3.19004396897555,134.547728424569));
#51388=CARTESIAN_POINT('Ctrl Pts',(80.8616131439302,-3.0856647621081,134.636678876814));
#51389=CARTESIAN_POINT('Ctrl Pts',(80.853852701416,-2.97764514709398,134.721189755163));
#51390=CARTESIAN_POINT('Ctrl Pts',(80.8460922589018,-2.86640969582959,134.800968994447));
#51391=CARTESIAN_POINT('Ctrl Pts',(80.8383193586364,-2.75499567954388,134.880876302448));
#51392=CARTESIAN_POINT('Ctrl Pts',(80.8305464583709,-2.64035583814411,134.956036578377));
#51393=CARTESIAN_POINT('Ctrl Pts',(80.8227735581055,-2.52294217905883,135.026202137996));
#51394=CARTESIAN_POINT('Ctrl Pts',(80.8152832223434,-2.40979680222775,135.093817002787));
#51395=CARTESIAN_POINT('Ctrl Pts',(80.8077928865814,-2.29407604748352,135.156793840408));
#51396=CARTESIAN_POINT('Ctrl Pts',(80.8003025508193,-2.17620202315962,135.214953300743));
#51397=CARTESIAN_POINT('Ctrl Pts',(80.7925282167002,-2.05385876937729,135.275317894694));
#51398=CARTESIAN_POINT('Ctrl Pts',(80.7847538825811,-1.92880819368285,135.330683815357));
#51399=CARTESIAN_POINT('Ctrl Pts',(80.7769795484621,-1.80149710919527,135.380799323379));
#51400=CARTESIAN_POINT('Ctrl Pts',(80.769214795515,-1.67434292424121,135.430853068516));
#51401=CARTESIAN_POINT('Ctrl Pts',(80.7614500425679,-1.54493413385633,135.475669133874));
#51402=CARTESIAN_POINT('Ctrl Pts',(80.7536852896208,-1.41374167822589,135.515041834731));
#51403=CARTESIAN_POINT('Ctrl Pts',(80.7459282487358,-1.28267952479186,135.554375430065));
#51404=CARTESIAN_POINT('Ctrl Pts',(80.7381712078508,-1.14983760364137,135.588276308276));
#51405=CARTESIAN_POINT('Ctrl Pts',(80.7304141669658,-1.01570601381134,135.616587166265));
#51406=CARTESIAN_POINT('Ctrl Pts',(80.7226629757257,-0.881675573656675,
135.644876674816));
#51407=CARTESIAN_POINT('Ctrl Pts',(80.7149117844855,-0.746357781611912,
135.667584473384));
#51408=CARTESIAN_POINT('Ctrl Pts',(80.7071605932454,-0.610256705529213,
135.684603420527));
#51409=CARTESIAN_POINT('Ctrl Pts',(80.6994126964683,-0.474213476034372,
135.701615134164));
#51410=CARTESIAN_POINT('Ctrl Pts',(80.6916647996913,-0.337388011779061,
135.712942757012));
#51411=CARTESIAN_POINT('Ctrl Pts',(80.6839169029142,-0.200293136925427,
135.718530508992));
#51412=CARTESIAN_POINT('Ctrl Pts',(80.6761706268301,-0.0632269393641897,
135.724117092135));
#51413=CARTESIAN_POINT('Ctrl Pts',(80.668424350746,0.0741081663090297,135.723966176671));
#51414=CARTESIAN_POINT('Ctrl Pts',(80.6606780746619,0.211196084552891,135.718074007292));
#51415=CARTESIAN_POINT('Ctrl Pts',(80.6529317413966,0.34828501474853,135.712181794418));
#51416=CARTESIAN_POINT('Ctrl Pts',(80.6451854081312,0.485126363269211,135.70054825985));
#51417=CARTESIAN_POINT('Ctrl Pts',(80.6374390748658,0.621206287798106,135.683221735747));
#51418=CARTESIAN_POINT('Ctrl Pts',(80.6296910068629,0.757316686482588,135.665891331489));
#51419=CARTESIAN_POINT('Ctrl Pts',(80.6219429388599,0.892664934109089,135.642865450153));
#51420=CARTESIAN_POINT('Ctrl Pts',(80.614194870857,1.02674494037685,135.614243972691));
#51421=CARTESIAN_POINT('Ctrl Pts',(80.6064385681151,1.16096744847094,135.585592075983));
#51422=CARTESIAN_POINT('Ctrl Pts',(80.5986822653732,1.29391863966632,135.551332784993));
#51423=CARTESIAN_POINT('Ctrl Pts',(80.5909259626314,1.42510466733082,135.511616691932));
#51424=CARTESIAN_POINT('Ctrl Pts',(80.5831655201172,1.55636071292831,135.471879401196));
#51425=CARTESIAN_POINT('Ctrl Pts',(80.5754050776031,1.68584934879639,135.42667963385));
#51426=CARTESIAN_POINT('Ctrl Pts',(80.5676446350889,1.8130953607569,135.376216725899));
#51427=CARTESIAN_POINT('Ctrl Pts',(80.5598717348235,1.9405456393121,135.325672810408));
#51428=CARTESIAN_POINT('Ctrl Pts',(80.552098834558,2.06574574261073,135.269849030101));
#51429=CARTESIAN_POINT('Ctrl Pts',(80.5443259342926,2.18824296583373,135.208991792248));
#51430=CARTESIAN_POINT('Ctrl Pts',(80.5368355985305,2.30628710644093,135.150346868281));
#51431=CARTESIAN_POINT('Ctrl Pts',(80.5293452627685,2.42182119810366,135.087028238962));
#51432=CARTESIAN_POINT('Ctrl Pts',(80.5218549270065,2.53446618862478,135.019294092868));
#51433=CARTESIAN_POINT('Ctrl Pts',(80.5140805928874,2.65138214819897,134.948991786037));
#51434=CARTESIAN_POINT('Ctrl Pts',(80.5063062587683,2.76555595599027,134.873709827595));
#51435=CARTESIAN_POINT('Ctrl Pts',(80.4985319246492,2.87653430314573,134.793688062804));
#51436=CARTESIAN_POINT('Ctrl Pts',(80.4907671717021,2.98737587940666,134.713764917685));
#51437=CARTESIAN_POINT('Ctrl Pts',(80.483002418755,3.09502951663782,134.629113815307));
#51438=CARTESIAN_POINT('Ctrl Pts',(80.475237665808,3.1990676117833,134.540019793366));
#51439=CARTESIAN_POINT('Ctrl Pts',(80.467480624923,3.30300237482599,134.451014260864));
#51440=CARTESIAN_POINT('Ctrl Pts',(80.459723584038,3.40332844701351,134.357574843069));
#51441=CARTESIAN_POINT('Ctrl Pts',(80.451966543153,3.49964857429439,134.260028848016));
#51442=CARTESIAN_POINT('Ctrl Pts',(80.4442153519128,3.59589606581808,134.162556413156));
#51443=CARTESIAN_POINT('Ctrl Pts',(80.4364641606727,3.6881433517926,134.060983842104));
#51444=CARTESIAN_POINT('Ctrl Pts',(80.4287129694326,3.77602783010214,133.955677308855));
#51445=CARTESIAN_POINT('Ctrl Pts',(80.4209650726555,3.86387495516399,133.850415533691));
#51446=CARTESIAN_POINT('Ctrl Pts',(80.4132171758784,3.94736271065898,133.741423252356));
#51447=CARTESIAN_POINT('Ctrl Pts',(80.4054692791013,4.02616697324001,133.629101767847));
#51448=CARTESIAN_POINT('Ctrl Pts',(80.3977230030172,4.10495475166813,133.516803778571));
#51449=CARTESIAN_POINT('Ctrl Pts',(80.3899767269331,4.17906076142679,133.401178291141));
#51450=CARTESIAN_POINT('Ctrl Pts',(80.382230450849,4.24820288082263,133.282657481517));
#51451=CARTESIAN_POINT('Ctrl Pts',(80.3744841175837,4.3173455106099,133.164135797));
#51452=CARTESIAN_POINT('Ctrl Pts',(80.3667377843183,4.38152397991067,133.042719085342));
#51453=CARTESIAN_POINT('Ctrl Pts',(80.3589914510529,4.44050120761483,132.91886578135));
#51454=CARTESIAN_POINT('Ctrl Pts',(80.35124338305,4.49949164286018,132.79498474127));
#51455=CARTESIAN_POINT('Ctrl Pts',(80.343495315047,4.55327835067198,132.66866637598));
#51456=CARTESIAN_POINT('Ctrl Pts',(80.335747247044,4.60167180955522,132.540390461677));
#51457=CARTESIAN_POINT('Ctrl Pts',(80.3279909443021,4.6501167015825,132.411978214206));
#51458=CARTESIAN_POINT('Ctrl Pts',(80.3202346415603,4.69315675615369,132.281604628071));
#51459=CARTESIAN_POINT('Ctrl Pts',(80.3124783388184,4.73065173459248,132.149766589196));
#51460=CARTESIAN_POINT('Ctrl Pts',(80.3047178963043,4.76816672523025,132.01785818439));
#51461=CARTESIAN_POINT('Ctrl Pts',(80.2969574537901,4.8001306514611,131.88448414941));
#51462=CARTESIAN_POINT('Ctrl Pts',(80.289197011276,4.82645435543933,131.75015204138));
#51463=CARTESIAN_POINT('Ctrl Pts',(80.2814241110105,4.8528203165641,131.615604291526));
#51464=CARTESIAN_POINT('Ctrl Pts',(80.2736512107451,4.87352790319527,131.480095781941));
#51465=CARTESIAN_POINT('Ctrl Pts',(80.2658783104796,4.88853972673615,131.344140575162));
#51466=CARTESIAN_POINT('Ctrl Pts',(80.2583879747176,4.90300583267882,131.2131276826));
#51467=CARTESIAN_POINT('Ctrl Pts',(80.2508976389555,4.9121830751767,131.081700313398));
#51468=CARTESIAN_POINT('Ctrl Pts',(80.2434073031935,4.91608378862042,130.950316932138));
#51469=CARTESIAN_POINT('Ctrl Pts',(80.2356329690744,4.92013239879994,130.813952110045));
#51470=CARTESIAN_POINT('Ctrl Pts',(80.2278586349554,4.91850928702849,130.677202714578));
#51471=CARTESIAN_POINT('Ctrl Pts',(80.2200843008363,4.91117121740962,130.540579769536));
#51472=CARTESIAN_POINT('Ctrl Pts',(80.2123195478892,4.90384219130573,130.404125200064));
#51473=CARTESIAN_POINT('Ctrl Pts',(80.2045547949421,4.89081224194038,130.267797157598));
#51474=CARTESIAN_POINT('Ctrl Pts',(80.1967900419951,4.87209004970578,130.132109466538));
#51475=CARTESIAN_POINT('Ctrl Pts',(80.1890330011101,4.85338645261645,129.996556542407));
#51476=CARTESIAN_POINT('Ctrl Pts',(80.1812759602251,4.82900191670185,129.861643088791));
#51477=CARTESIAN_POINT('Ctrl Pts',(80.1735189193401,4.79899708996234,129.727880244762));
#51478=CARTESIAN_POINT('Ctrl Pts',(80.1657677280999,4.76901489009605,129.594218272334));
#51479=CARTESIAN_POINT('Ctrl Pts',(80.1580165368598,4.73342092072011,129.461705562363));
#51480=CARTESIAN_POINT('Ctrl Pts',(80.1502653456197,4.69232725908536,129.330845108267));
#51481=CARTESIAN_POINT('Ctrl Pts',(80.1425174488426,4.65125106335302,129.200040273355));
#51482=CARTESIAN_POINT('Ctrl Pts',(80.1347695520655,4.60467994139138,129.070886669815));
#51483=CARTESIAN_POINT('Ctrl Pts',(80.1270216552884,4.55277632419008,128.943873905871));
#51484=CARTESIAN_POINT('Ctrl Pts',(80.1192753792044,4.50088356410662,128.816887710259));
#51485=CARTESIAN_POINT('Ctrl Pts',(80.1115291031202,4.44366067526238,128.692041825192));
#51486=CARTESIAN_POINT('Ctrl Pts',(80.1037828270361,4.38131876586578,128.569807209305));
#51487=CARTESIAN_POINT('Ctrl Pts',(80.0960364937708,4.31897639627537,128.447571691109));
#51488=CARTESIAN_POINT('Ctrl Pts',(80.0882901605054,4.25151510836129,128.327947828839));
#51489=CARTESIAN_POINT('Ctrl Pts',(80.0805438272401,4.1791924481783,128.211382880757));
#51490=CARTESIAN_POINT('Ctrl Pts',(80.0727957592371,4.10685359183697,128.094791828763));
#51491=CARTESIAN_POINT('Ctrl Pts',(80.0650476912341,4.02965140298172,127.981261386225));
#51492=CARTESIAN_POINT('Ctrl Pts',(80.0572996232312,3.94788708991859,127.871210333698));
#51493=CARTESIAN_POINT('Ctrl Pts',(80.0495433204893,3.86603587677058,127.761042317603));
#51494=CARTESIAN_POINT('Ctrl Pts',(80.0417870177475,3.77961308719027,127.654361392877));
#51495=CARTESIAN_POINT('Ctrl Pts',(80.0340307150056,3.6889609629497,127.551554125268));
#51496=CARTESIAN_POINT('Ctrl Pts',(80.0262702724915,3.59826045494081,127.448691986326));
#51497=CARTESIAN_POINT('Ctrl Pts',(80.0185098299773,3.50332638485288,127.349707906173));
#51498=CARTESIAN_POINT('Ctrl Pts',(80.0107493874631,3.40453758287727,127.254951242856));
#51499=CARTESIAN_POINT('Ctrl Pts',(80.0029764871977,3.30559019634674,127.160042467731));
#51500=CARTESIAN_POINT('Ctrl Pts',(79.9952035869322,3.20277600581824,127.06937492922));
#51501=CARTESIAN_POINT('Ctrl Pts',(79.9874306866668,3.09650729721128,126.983257946763));
#51502=CARTESIAN_POINT('Ctrl Pts',(79.9799403509048,2.99410172383655,126.900271533534));
#51503=CARTESIAN_POINT('Ctrl Pts',(79.9724500151427,2.8884886796471,126.821510756162));
#51504=CARTESIAN_POINT('Ctrl Pts',(79.9649596793807,2.78006055091892,126.747213048679));
#51505=CARTESIAN_POINT('Ctrl Pts',(79.9571853452616,2.66752133673431,126.670098321035));
#51506=CARTESIAN_POINT('Ctrl Pts',(79.9494110111425,2.55159286582454,126.597547502398));
#51507=CARTESIAN_POINT('Ctrl Pts',(79.9416366770234,2.43268170692635,126.529873189197));
#51508=CARTESIAN_POINT('Ctrl Pts',(79.9338719240763,2.31391709540427,126.462282278539));
#51509=CARTESIAN_POINT('Ctrl Pts',(79.9261071711292,2.19217744636074,126.399556107017));
#51510=CARTESIAN_POINT('Ctrl Pts',(79.9183424181822,2.06789974677971,126.34196510621));
#51511=CARTESIAN_POINT('Ctrl Pts',(79.9105853772972,1.94374548156191,126.284431305597));
#51512=CARTESIAN_POINT('Ctrl Pts',(79.9028283364122,1.81705853479989,126.232022689145));
#51513=CARTESIAN_POINT('Ctrl Pts',(79.8950712955272,1.68830172399631,126.184964515125));
#51514=CARTESIAN_POINT('Ctrl Pts',(79.887320104287,1.55964200970525,126.13794182804));
#51515=CARTESIAN_POINT('Ctrl Pts',(79.8795689130469,1.42891590397324,126.096261686007));
#51516=CARTESIAN_POINT('Ctrl Pts',(79.8718177218068,1.29660716989956,126.06010167549));
#51517=CARTESIAN_POINT('Ctrl Pts',(79.8640698250297,1.16435467056731,126.023957033943));
#51518=CARTESIAN_POINT('Ctrl Pts',(79.8563219282526,1.030521257106,125.993327960346));
#51519=CARTESIAN_POINT('Ctrl Pts',(79.8485740314756,0.895606648697689,125.968342442113));
#51520=CARTESIAN_POINT('Ctrl Pts',(79.8408277553915,0.760720261517129,125.943362150312));
#51521=CARTESIAN_POINT('Ctrl Pts',(79.8330814793073,0.624753513424354,125.924023136925));
#51522=CARTESIAN_POINT('Ctrl Pts',(79.8253352032232,0.488216744399233,125.910402355281));
#51523=CARTESIAN_POINT('Ctrl Pts',(79.8175888699579,0.351678967490605,125.896781473092));
#51524=CARTESIAN_POINT('Ctrl Pts',(79.8098425366925,0.214571550287528,125.888878945684));
#51525=CARTESIAN_POINT('Ctrl Pts',(79.8020962034272,0.0774099937671157,
125.886719846285));
#51526=CARTESIAN_POINT('Ctrl Pts',(79.7943481354242,-0.0597822791327743,
125.88456026337));
#51527=CARTESIAN_POINT('Ctrl Pts',(79.7866000674212,-0.197028324633647,
125.888146674007));
#51528=CARTESIAN_POINT('Ctrl Pts',(79.7788519994183,-0.333813000346846,
125.897452024236));
#51529=CARTESIAN_POINT('Ctrl Pts',(79.7710956966764,-0.470743052441243,
125.906767264301));
#51530=CARTESIAN_POINT('Ctrl Pts',(79.7633393939345,-0.607210364536801,
125.921813559155));
#51531=CARTESIAN_POINT('Ctrl Pts',(79.7555830911927,-0.742704717882201,
125.94251191933));
#51532=CARTESIAN_POINT('Ctrl Pts',(79.7478226486785,-0.878271388643729,
125.963221326844));
#51533=CARTESIAN_POINT('Ctrl Pts',(79.7400622061644,-1.01286368242679,125.989588735539));
#51534=CARTESIAN_POINT('Ctrl Pts',(79.7323017636502,-1.14598290744194,126.021484261402));
#51535=CARTESIAN_POINT('Ctrl Pts',(79.7245288633847,-1.27931582725477,126.053430988795));
#51536=CARTESIAN_POINT('Ctrl Pts',(79.7167559631193,-1.41117057659969,126.090923459893));
#51537=CARTESIAN_POINT('Ctrl Pts',(79.7089830628539,-1.54106406565972,126.133782001588));
#51538=CARTESIAN_POINT('Ctrl Pts',(79.7014927270918,-1.66623559921065,126.175082527338));
#51539=CARTESIAN_POINT('Ctrl Pts',(79.6940023913298,-1.78958570196112,126.221365648523));
#51540=CARTESIAN_POINT('Ctrl Pts',(79.6865120555678,-1.91070251956831,126.272429578349));
#51541=CARTESIAN_POINT('Ctrl Pts',(79.6787372956776,-2.03641840273769,126.325432515208));
#51542=CARTESIAN_POINT('Ctrl Pts',(79.6709625357874,-2.16012629599077,126.383754417044));
#51543=CARTESIAN_POINT('Ctrl Pts',(79.6631877758972,-2.2813433638567,126.447222162262));
#51544=CARTESIAN_POINT('Ctrl Pts',(79.6554226943927,-2.40240953503272,126.510610899855));
#51545=CARTESIAN_POINT('Ctrl Pts',(79.6476576128882,-2.52099070744273,126.579132554978));
#51546=CARTESIAN_POINT('Ctrl Pts',(79.6398925313837,-2.63662309986672,126.652565621212));
#51547=CARTESIAN_POINT('Ctrl Pts',(79.6321352587413,-2.75213920794696,126.725924840354));
#51548=CARTESIAN_POINT('Ctrl Pts',(79.6243779860988,-2.86471210971172,126.804185432721));
#51549=CARTESIAN_POINT('Ctrl Pts',(79.6166207134564,-2.97390208826842,126.887079745342));
#51550=CARTESIAN_POINT('Ctrl Pts',(79.6088521230946,-3.08325137301405,126.970094999255));
#51551=CARTESIAN_POINT('Ctrl Pts',(79.6010835327327,-3.18920751056089,127.057757314326));
#51552=CARTESIAN_POINT('Ctrl Pts',(79.5933149423708,-3.29135687202745,127.149753524668));
#51553=CARTESIAN_POINT('Ctrl Pts',(79.5855673853042,-3.39322966624365,127.241500657204));
#51554=CARTESIAN_POINT('Ctrl Pts',(79.5778198282376,-3.49131597439789,127.337557991071));
#51555=CARTESIAN_POINT('Ctrl Pts',(79.570072271171,-3.58523813826385,127.437574233722));
#51556=CARTESIAN_POINT('Ctrl Pts',(79.5623264684862,-3.6791390340918,127.537567828372));
#51557=CARTESIAN_POINT('Ctrl Pts',(79.5545806658014,-3.76887739469223,127.64151826309));
#51558=CARTESIAN_POINT('Ctrl Pts',(79.5468348631166,-3.85411277790421,127.749037761026));
#51559=CARTESIAN_POINT('Ctrl Pts',(79.5390891370196,-3.93934731833801,127.856556195846));
#51560=CARTESIAN_POINT('Ctrl Pts',(79.5313434109227,-4.02007872793979,127.967643316808));
#51561=CARTESIAN_POINT('Ctrl Pts',(79.5235976848257,-4.09600743652683,128.081879002859));
#51562=CARTESIAN_POINT('Ctrl Pts',(79.5158124231546,-4.17232369885024,128.196697768325));
#51563=CARTESIAN_POINT('Ctrl Pts',(79.5080271614835,-4.2437878623242,128.314697006798));
#51564=CARTESIAN_POINT('Ctrl Pts',(79.5002418998124,-4.3101407549323,128.435422092578));
#51565=CARTESIAN_POINT('Ctrl Pts',(79.49248811021,-4.37622541470655,128.555659144897));
#51566=CARTESIAN_POINT('Ctrl Pts',(79.4847343206076,-4.43723991423492,128.678599676034));
#51567=CARTESIAN_POINT('Ctrl Pts',(79.4769805310053,-4.49297545682033,128.803772052441));
#51568=CARTESIAN_POINT('Ctrl Pts',(79.4691795332998,-4.54905033918414,128.929706527223));
#51569=CARTESIAN_POINT('Ctrl Pts',(79.4613785355943,-4.59978161849782,129.057899743097));
#51570=CARTESIAN_POINT('Ctrl Pts',(79.4535775378887,-4.64500696200414,129.187854080173));
#51571=CARTESIAN_POINT('Ctrl Pts',(79.4457765401832,-4.69023230551044,129.317808417249));
#51572=CARTESIAN_POINT('Ctrl Pts',(79.4379755424777,-4.72995164131195,129.449523480783));
#51573=CARTESIAN_POINT('Ctrl Pts',(79.4301745447722,-4.76405452823407,129.582490119308));
#51574=CARTESIAN_POINT('Origin',(213.235140564004,0.,130.804360617566));
#51575=CARTESIAN_POINT('',(77.3348925457121,-4.76405452823405,129.582490119308));
#51576=CARTESIAN_POINT('',(77.6798548998299,-4.76405452823404,129.582490119308));
#51577=CARTESIAN_POINT('',(213.235140564004,-4.76405452823405,129.582490119308));
#51578=CARTESIAN_POINT('',(79.0148594360372,-4.91824997683007,130.803883217332));
#51579=CARTESIAN_POINT('Ctrl Pts',(79.0148594359911,-4.91824997683015,130.803883218151));
#51580=CARTESIAN_POINT('Ctrl Pts',(79.006801254778,-4.91826386524818,130.946964062875));
#51581=CARTESIAN_POINT('Ctrl Pts',(78.9987430735649,-4.91202970327439,131.089943852501));
#51582=CARTESIAN_POINT('Ctrl Pts',(78.9906848923518,-4.89959985564133,131.23226751994));
#51583=CARTESIAN_POINT('Ctrl Pts',(78.982618049138,-4.88715664676137,131.374744175712));
#51584=CARTESIAN_POINT('Ctrl Pts',(78.9745512059242,-4.86850449730708,131.516562960778));
#51585=CARTESIAN_POINT('Ctrl Pts',(78.9664843627104,-4.84374728067055,131.657176742822));
#51586=CARTESIAN_POINT('Ctrl Pts',(78.958400333963,-4.81893732147206,131.798090087261));
#51587=CARTESIAN_POINT('Ctrl Pts',(78.9503163052157,-4.78799635360567,131.937792957518));
#51588=CARTESIAN_POINT('Ctrl Pts',(78.9422322764683,-4.7510791765238,132.075749512005));
#51589=CARTESIAN_POINT('Ctrl Pts',(78.9341394529842,-4.71412183668822,132.213856151508));
#51590=CARTESIAN_POINT('Ctrl Pts',(78.9260466295,-4.67117541861149,132.350212357506));
#51591=CARTESIAN_POINT('Ctrl Pts',(78.9179538060158,-4.62244372778178,132.484300213501));
#51592=CARTESIAN_POINT('Ctrl Pts',(78.9098426664952,-4.5736017452318,132.618691543069));
#51593=CARTESIAN_POINT('Ctrl Pts',(78.9017315269746,-4.51894843833848,132.750803938434));
#51594=CARTESIAN_POINT('Ctrl Pts',(78.893620387454,-4.45873540362251,132.88014038984));
#51595=CARTESIAN_POINT('Ctrl Pts',(78.8859996517321,-4.40216288093094,133.001657090777));
#51596=CARTESIAN_POINT('Ctrl Pts',(78.8783789160102,-4.34068314080648,133.120723396886));
#51597=CARTESIAN_POINT('Ctrl Pts',(78.8707581802883,-4.27453987883232,133.236950160989));
#51598=CARTESIAN_POINT('Ctrl Pts',(78.8629838461692,-4.20706347798609,133.355519513175));
#51599=CARTESIAN_POINT('Ctrl Pts',(78.8552095120502,-4.13454305546345,133.471467001158));
#51600=CARTESIAN_POINT('Ctrl Pts',(78.8474351779311,-4.05720750929386,133.584333691002));
#51601=CARTESIAN_POINT('Ctrl Pts',(78.839670424984,-3.97996727227313,133.697061282738));
#51602=CARTESIAN_POINT('Ctrl Pts',(78.8319056720369,-3.89792393777996,133.80671531143));
#51603=CARTESIAN_POINT('Ctrl Pts',(78.8241409190898,-3.81135220013507,133.912861457042));
#51604=CARTESIAN_POINT('Ctrl Pts',(78.8163838782047,-3.72486644676045,134.018902176806));
#51605=CARTESIAN_POINT('Ctrl Pts',(78.8086268373198,-3.63386148631231,134.12144164595));
#51606=CARTESIAN_POINT('Ctrl Pts',(78.8008697964347,-3.53865499956588,134.220074870332));
#51607=CARTESIAN_POINT('Ctrl Pts',(78.7931186051946,-3.44352030877209,134.318633714631));
#51608=CARTESIAN_POINT('Ctrl Pts',(78.7853674139545,-3.34419066862125,134.413291897305));
#51609=CARTESIAN_POINT('Ctrl Pts',(78.7776162227144,-3.24102344620704,134.503678133492));
#51610=CARTESIAN_POINT('Ctrl Pts',(78.7698683259373,-3.13790007261416,134.594025953117));
#51611=CARTESIAN_POINT('Ctrl Pts',(78.7621204291602,-3.03094265429462,134.680105180429));
#51612=CARTESIAN_POINT('Ctrl Pts',(78.7543725323831,-2.9205446006123,134.761582155253));
#51613=CARTESIAN_POINT('Ctrl Pts',(78.746626256299,-2.81016963982283,134.843042086851));
#51614=CARTESIAN_POINT('Ctrl Pts',(78.7388799802149,-2.69635578957786,134.919901448793));
#51615=CARTESIAN_POINT('Ctrl Pts',(78.7311337041308,-2.5795283312385,134.9918678296));
#51616=CARTESIAN_POINT('Ctrl Pts',(78.7233873708655,-2.46270001050554,135.063834741646));
#51617=CARTESIAN_POINT('Ctrl Pts',(78.7156410376001,-2.34285837016483,135.130908395431));
#51618=CARTESIAN_POINT('Ctrl Pts',(78.7078947043347,-2.22045602371151,135.192840776945));
#51619=CARTESIAN_POINT('Ctrl Pts',(78.7001466363318,-2.09802626610153,135.254787027787));
#51620=CARTESIAN_POINT('Ctrl Pts',(78.6923985683288,-1.97303501006068,135.311589538824));
#51621=CARTESIAN_POINT('Ctrl Pts',(78.6846505003258,-1.84595734562999,135.363047329835));
#51622=CARTESIAN_POINT('Ctrl Pts',(78.676894197584,-1.71874462154513,135.414559810798));
#51623=CARTESIAN_POINT('Ctrl Pts',(78.6691378948421,-1.58944142241624,135.460716077484));
#51624=CARTESIAN_POINT('Ctrl Pts',(78.6613815921003,-1.45854112573695,135.501364007711));
#51625=CARTESIAN_POINT('Ctrl Pts',(78.6536211495861,-1.32757096362773,135.542033632962));
#51626=CARTESIAN_POINT('Ctrl Pts',(78.6458607070719,-1.19500238316923,135.577188963459));
#51627=CARTESIAN_POINT('Ctrl Pts',(78.6381002645577,-1.06134065578097,135.606728687059));
#51628=CARTESIAN_POINT('Ctrl Pts',(78.6303273642923,-0.927464362722071,
135.636315830446));
#51629=CARTESIAN_POINT('Ctrl Pts',(78.6225544640269,-0.792491801222578,
135.660269284396));
#51630=CARTESIAN_POINT('Ctrl Pts',(78.6147815637614,-0.656935988556452,
135.678539334995));
#51631=CARTESIAN_POINT('Ctrl Pts',(78.6072912279995,-0.526307971126326,
135.696145223236));
#51632=CARTESIAN_POINT('Ctrl Pts',(78.5998008922375,-0.395138678276404,
135.70847371739));
#51633=CARTESIAN_POINT('Ctrl Pts',(78.5923105564755,-0.263886738552775,
135.715526146411));
#51634=CARTESIAN_POINT('Ctrl Pts',(78.5845362223564,-0.127658341640397,
135.722845970422));
#51635=CARTESIAN_POINT('Ctrl Pts',(78.5767618882373,0.00909062358639984,
135.724504934498));
#51636=CARTESIAN_POINT('Ctrl Pts',(78.5689875541183,0.145850318033386,135.720447552032));
#51637=CARTESIAN_POINT('Ctrl Pts',(78.5612228011712,0.282441468379067,135.716395169928));
#51638=CARTESIAN_POINT('Ctrl Pts',(78.5534580482241,0.419042934593818,135.706640469987));
#51639=CARTESIAN_POINT('Ctrl Pts',(78.545693295277,0.555140831940946,135.691179799735));
#51640=CARTESIAN_POINT('Ctrl Pts',(78.537936254392,0.691103554938062,135.675734485238));
#51641=CARTESIAN_POINT('Ctrl Pts',(78.5301792135071,0.826563318439076,135.654594522357));
#51642=CARTESIAN_POINT('Ctrl Pts',(78.5224221726221,0.961007675183125,135.627808275698));
#51643=CARTESIAN_POINT('Ctrl Pts',(78.514670981382,1.09535064639166,135.601042228756));
#51644=CARTESIAN_POINT('Ctrl Pts',(78.5069197901419,1.228679353097,135.568638449226));
#51645=CARTESIAN_POINT('Ctrl Pts',(78.4991685989018,1.36048825718647,135.530696911627));
#51646=CARTESIAN_POINT('Ctrl Pts',(78.4914207021247,1.49224113897594,135.492771500193));
#51647=CARTESIAN_POINT('Ctrl Pts',(78.4836728053476,1.62247512798519,135.449313119934));
#51648=CARTESIAN_POINT('Ctrl Pts',(78.4759249085705,1.75069685909023,135.400472405814));
#51649=CARTESIAN_POINT('Ctrl Pts',(78.4681786324864,1.87889176897335,135.351641908119));
#51650=CARTESIAN_POINT('Ctrl Pts',(78.4604323564024,2.00507489306106,135.297431455056));
#51651=CARTESIAN_POINT('Ctrl Pts',(78.4526860803182,2.12877034232941,135.238040792333));
#51652=CARTESIAN_POINT('Ctrl Pts',(78.4449397470529,2.25246670468938,135.178649691201));
#51653=CARTESIAN_POINT('Ctrl Pts',(78.4371934137875,2.37367500314165,135.114078473326));
#51654=CARTESIAN_POINT('Ctrl Pts',(78.4294470805222,2.49194192782743,135.044573877632));
#51655=CARTESIAN_POINT('Ctrl Pts',(78.4216990125192,2.61023533757091,134.975053716865));
#51656=CARTESIAN_POINT('Ctrl Pts',(78.4139509445162,2.72558572580896,134.900598177916));
#51657=CARTESIAN_POINT('Ctrl Pts',(78.4062028765132,2.83756720441572,134.821498332771));
#51658=CARTESIAN_POINT('Ctrl Pts',(78.3984465737714,2.94966769827062,134.74231441937));
#51659=CARTESIAN_POINT('Ctrl Pts',(78.3906902710296,3.05839181018284,134.65847656546));
#51660=CARTESIAN_POINT('Ctrl Pts',(78.3829339682877,3.16334487286462,134.570317637743));
#51661=CARTESIAN_POINT('Ctrl Pts',(78.3751735257736,3.26835395215603,134.482111656952));
#51662=CARTESIAN_POINT('Ctrl Pts',(78.3674130832594,3.36958768325885,134.389580270526));
#51663=CARTESIAN_POINT('Ctrl Pts',(78.3596526407453,3.46668771785457,134.293093815931));
#51664=CARTESIAN_POINT('Ctrl Pts',(78.3518797404799,3.56394362604601,134.196452472714));
#51665=CARTESIAN_POINT('Ctrl Pts',(78.3441068402144,3.65705231162963,134.095843661059));
#51666=CARTESIAN_POINT('Ctrl Pts',(78.336333939949,3.7456946505146,133.991672125343));
#51667=CARTESIAN_POINT('Ctrl Pts',(78.3288436041869,3.83111461710567,133.891287487341));
#51668=CARTESIAN_POINT('Ctrl Pts',(78.3213532684247,3.91238713517407,133.787594898587));
#51669=CARTESIAN_POINT('Ctrl Pts',(78.3138629326626,3.98926542287362,133.680980934599));
#51670=CARTESIAN_POINT('Ctrl Pts',(78.3060885985435,4.06905857421684,133.570324669762));
#51671=CARTESIAN_POINT('Ctrl Pts',(78.2983142644245,4.14437046366273,133.456170602991));
#51672=CARTESIAN_POINT('Ctrl Pts',(78.2905399303054,4.21487882827283,133.338917684487));
#51673=CARTESIAN_POINT('Ctrl Pts',(78.2827751773583,4.28530029762511,133.221809269725));
#51674=CARTESIAN_POINT('Ctrl Pts',(78.2750104244112,4.35092982146337,133.101609933854));
#51675=CARTESIAN_POINT('Ctrl Pts',(78.2672456714641,4.41148655960332,132.978750048404));
#51676=CARTESIAN_POINT('Ctrl Pts',(78.2594886305791,4.47198315193708,132.856012189124));
#51677=CARTESIAN_POINT('Ctrl Pts',(78.2517315896942,4.52741681341114,132.730619387361));
#51678=CARTESIAN_POINT('Ctrl Pts',(78.2439745488092,4.57755124427728,132.603028921761));
#51679=CARTESIAN_POINT('Ctrl Pts',(78.236223357569,4.62764786837942,132.475534673123));
#51680=CARTESIAN_POINT('Ctrl Pts',(78.2284721663289,4.67245307364692,132.345846421763));
#51681=CARTESIAN_POINT('Ctrl Pts',(78.2207209750887,4.71177771577674,132.214443529883));
#51682=CARTESIAN_POINT('Ctrl Pts',(78.2129730783116,4.75108564388447,132.083096487739));
#51683=CARTESIAN_POINT('Ctrl Pts',(78.2052251815346,4.7849175299681,131.950036628307));
#51684=CARTESIAN_POINT('Ctrl Pts',(78.1974772847575,4.81313343159022,131.815760455518));
#51685=CARTESIAN_POINT('Ctrl Pts',(78.1897310086734,4.84134343105397,131.681512370409));
#51686=CARTESIAN_POINT('Ctrl Pts',(78.1819847325893,4.86393970233621,131.546048860378));
#51687=CARTESIAN_POINT('Ctrl Pts',(78.1742384565052,4.88083306751467,131.409878271772));
#51688=CARTESIAN_POINT('Ctrl Pts',(78.1664921232399,4.89772655739614,131.273706677986));
#51689=CARTESIAN_POINT('Ctrl Pts',(78.1587457899745,4.90891700903694,131.136828383199));
#51690=CARTESIAN_POINT('Ctrl Pts',(78.1509994567091,4.91436698582944,130.999758138251));
#51691=CARTESIAN_POINT('Ctrl Pts',(78.1432513887062,4.91981818310644,130.862657197371));
#51692=CARTESIAN_POINT('Ctrl Pts',(78.1355033207032,4.9195263319306,130.725364611374));
#51693=CARTESIAN_POINT('Ctrl Pts',(78.1277552527003,4.91350611647311,130.58839602352));
#51694=CARTESIAN_POINT('Ctrl Pts',(78.1199989499584,4.90747950265899,130.451281863821));
#51695=CARTESIAN_POINT('Ctrl Pts',(78.1122426472166,4.89571237997539,130.314492781351));
#51696=CARTESIAN_POINT('Ctrl Pts',(78.1044863444747,4.87827147129727,130.178540743459));
#51697=CARTESIAN_POINT('Ctrl Pts',(78.0967259019605,4.86082125388104,130.042516143871));
#51698=CARTESIAN_POINT('Ctrl Pts',(78.0889654594464,4.83769128228768,129.907329864238));
#51699=CARTESIAN_POINT('Ctrl Pts',(78.0812050169322,4.80899943589805,129.773483569596));
#51700=CARTESIAN_POINT('Ctrl Pts',(78.0734321166668,4.78026153080945,129.639422412999));
#51701=CARTESIAN_POINT('Ctrl Pts',(78.0656592164013,4.7459440070381,129.506705918636));
#51702=CARTESIAN_POINT('Ctrl Pts',(78.0578863161359,4.70621489312572,129.375821348865));
#51703=CARTESIAN_POINT('Ctrl Pts',(78.0503959803739,4.6679300325755,129.249694762883));
#51704=CARTESIAN_POINT('Ctrl Pts',(78.0429056446118,4.62462030213842,129.125269514622));
#51705=CARTESIAN_POINT('Ctrl Pts',(78.0354153088498,4.57647754712891,129.002962182148));
#51706=CARTESIAN_POINT('Ctrl Pts',(78.0276409747307,4.52650944493073,128.87601752999));
#51707=CARTESIAN_POINT('Ctrl Pts',(78.0198666406116,4.47117631138528,128.750952442997));
#51708=CARTESIAN_POINT('Ctrl Pts',(78.0120923064925,4.41063960360692,128.628253692437));
#51709=CARTESIAN_POINT('Ctrl Pts',(78.0043275535454,4.35017750191063,128.505706157121));
#51710=CARTESIAN_POINT('Ctrl Pts',(77.9965628005983,4.28452475714507,128.385519502921));
#51711=CARTESIAN_POINT('Ctrl Pts',(77.9887980476512,4.21389165208789,128.268162634962));
#51712=CARTESIAN_POINT('Ctrl Pts',(77.9810410067662,4.1433287008267,128.1509223275));
#51713=CARTESIAN_POINT('Ctrl Pts',(77.9732839658813,4.06779543346437,128.036506545897));
#51714=CARTESIAN_POINT('Ctrl Pts',(77.9655269249963,3.98754884569005,127.925361266101));
#51715=CARTESIAN_POINT('Ctrl Pts',(77.9577757337562,3.90736277249174,127.814299801825));
#51716=CARTESIAN_POINT('Ctrl Pts',(77.9500245425161,3.82247068153627,127.706504246014));
#51717=CARTESIAN_POINT('Ctrl Pts',(77.942273351276,3.73317363670454,127.602392838104));
#51718=CARTESIAN_POINT('Ctrl Pts',(77.9345254544989,3.64391454549869,127.498325680319));
#51719=CARTESIAN_POINT('Ctrl Pts',(77.9267775577219,3.5502544781255,127.397939852198));
#51720=CARTESIAN_POINT('Ctrl Pts',(77.9190296609448,3.45253551509754,127.301621463776));
#51721=CARTESIAN_POINT('Ctrl Pts',(77.9112833848607,3.35483699277,127.205323223086));
#51722=CARTESIAN_POINT('Ctrl Pts',(77.9035371087766,3.25308154182775,127.113091004044));
#51723=CARTESIAN_POINT('Ctrl Pts',(77.8957908326925,3.14764864560424,127.025274608181));
#51724=CARTESIAN_POINT('Ctrl Pts',(77.8880444994271,3.04221497109896,126.937457564078));
#51725=CARTESIAN_POINT('Ctrl Pts',(77.8802981661618,2.93310409755433,126.854056658412));
#51726=CARTESIAN_POINT('Ctrl Pts',(77.8725518328964,2.82072886402738,126.775381623063));
#51727=CARTESIAN_POINT('Ctrl Pts',(77.8648037648934,2.70832846484634,126.696688968986));
#51728=CARTESIAN_POINT('Ctrl Pts',(77.8570556968905,2.59266257122968,126.622724515357));
#51729=CARTESIAN_POINT('Ctrl Pts',(77.8493076288875,2.47417294560971,126.553754625744));
#51730=CARTESIAN_POINT('Ctrl Pts',(77.8415513261456,2.35555738780526,126.484711434111));
#51731=CARTESIAN_POINT('Ctrl Pts',(77.8337950234038,2.23411244141613,126.420673607353));
#51732=CARTESIAN_POINT('Ctrl Pts',(77.8260387206619,2.11030490441751,126.361861740482));
#51733=CARTESIAN_POINT('Ctrl Pts',(77.8182782781477,1.98643128760853,126.303018483947));
#51734=CARTESIAN_POINT('Ctrl Pts',(77.8105178356336,1.86019292725123,126.249406897873));
#51735=CARTESIAN_POINT('Ctrl Pts',(77.8027573931194,1.73207560503359,126.201198969204));
#51736=CARTESIAN_POINT('Ctrl Pts',(77.794984492854,1.60375261751669,126.152913652889));
#51737=CARTESIAN_POINT('Ctrl Pts',(77.7872115925885,1.47354501223205,126.110049450576));
#51738=CARTESIAN_POINT('Ctrl Pts',(77.7794386923231,1.34195356033271,126.072728372303));
#51739=CARTESIAN_POINT('Ctrl Pts',(77.771948356561,1.21514578916798,126.036764009231));
#51740=CARTESIAN_POINT('Ctrl Pts',(77.7644580207989,1.08705333669959,126.005946826103));
#51741=CARTESIAN_POINT('Ctrl Pts',(77.7569676850368,0.958130378930791,125.980340588641));
#51742=CARTESIAN_POINT('Ctrl Pts',(77.7491933509177,0.824319268033662,125.953763482903));
#51743=CARTESIAN_POINT('Ctrl Pts',(77.7414190167986,0.689189558051129,125.932716080867));
#51744=CARTESIAN_POINT('Ctrl Pts',(77.7336446826795,0.553238054949885,125.917325655848));
#51745=CARTESIAN_POINT('Ctrl Pts',(77.7258799297324,0.417454099926246,125.901954198152));
#51746=CARTESIAN_POINT('Ctrl Pts',(77.7181151767854,0.280850751681747,125.892225889389));
#51747=CARTESIAN_POINT('Ctrl Pts',(77.7103504238383,0.143936176356196,125.888217267374));
#51748=CARTESIAN_POINT('Ctrl Pts',(77.7025933829533,0.00715758651664383,
125.88421262678));
#51749=CARTESIAN_POINT('Ctrl Pts',(77.6948363420683,-0.129931226982009,
125.885916379108));
#51750=CARTESIAN_POINT('Ctrl Pts',(77.6870793011833,-0.266816139496606,
125.8933533675));
#51751=CARTESIAN_POINT('Ctrl Pts',(77.6793281099431,-0.403597826033775,
125.900784747601));
#51752=CARTESIAN_POINT('Ctrl Pts',(77.671576918703,-0.540175528833602,125.913940737022));
#51753=CARTESIAN_POINT('Ctrl Pts',(77.6638257274629,-0.67603463883003,125.932794110825));
#51754=CARTESIAN_POINT('Ctrl Pts',(77.6560778306858,-0.811836005080364,
125.951639471441));
#51755=CARTESIAN_POINT('Ctrl Pts',(77.6483299339087,-0.946918999543146,
125.976177346553));
#51756=CARTESIAN_POINT('Ctrl Pts',(77.6405820371317,-1.08077387403529,126.006328636045));
#51757=CARTESIAN_POINT('Ctrl Pts',(77.6328357610475,-1.21460074897345,126.036473618536));
#51758=CARTESIAN_POINT('Ctrl Pts',(77.6250894849635,-1.34719963375454,126.072229593989));
#51759=CARTESIAN_POINT('Ctrl Pts',(77.6173432088794,-1.47807111043409,126.113466368598));
#51760=CARTESIAN_POINT('Ctrl Pts',(77.609596875614,-1.60894355317689,126.154703447608));
#51761=CARTESIAN_POINT('Ctrl Pts',(77.6018505423486,-1.73808818948174,126.201421289009));
#51762=CARTESIAN_POINT('Ctrl Pts',(77.5941042090833,-1.86502128355201,126.253439977256));
#51763=CARTESIAN_POINT('Ctrl Pts',(77.5863561410803,-1.99198280340921,126.305470314729));
#51764=CARTESIAN_POINT('Ctrl Pts',(77.5786080730773,-2.11673143382669,126.362803712988));
#51765=CARTESIAN_POINT('Ctrl Pts',(77.5708600050743,-2.23880429220509,126.425212480804));
#51766=CARTESIAN_POINT('Ctrl Pts',(77.5631037023325,-2.36100689106963,126.487687577401));
#51767=CARTESIAN_POINT('Ctrl Pts',(77.5553473995906,-2.48052768834805,126.555248640724));
#51768=CARTESIAN_POINT('Ctrl Pts',(77.5475910968488,-2.59692877549976,126.627622177409));
#51769=CARTESIAN_POINT('Ctrl Pts',(77.5398306543346,-2.71339198941677,126.700034342031));
#51770=CARTESIAN_POINT('Ctrl Pts',(77.5320702118204,-2.8267318524565,126.777263878047));
#51771=CARTESIAN_POINT('Ctrl Pts',(77.5243097693062,-2.93654109026335,126.85899504671));
#51772=CARTESIAN_POINT('Ctrl Pts',(77.5165368690408,-3.04652660360691,126.940857417501));
#51773=CARTESIAN_POINT('Ctrl Pts',(77.5087639687753,-3.15296986214332,127.027235615132));
#51774=CARTESIAN_POINT('Ctrl Pts',(77.5009910685099,-3.25549753633386,127.117774276054));
#51775=CARTESIAN_POINT('Ctrl Pts',(77.4935007327479,-3.35429807131511,127.205021628597));
#51776=CARTESIAN_POINT('Ctrl Pts',(77.486010396986,-3.44946253965899,127.296131996392));
#51777=CARTESIAN_POINT('Ctrl Pts',(77.478520061224,-3.54069180023272,127.390757735234));
#51778=CARTESIAN_POINT('Ctrl Pts',(77.470846416256,-3.63415369280847,127.487699227283));
#51779=CARTESIAN_POINT('Ctrl Pts',(77.4631727712879,-3.72379809036211,127.5886551613));
#51780=CARTESIAN_POINT('Ctrl Pts',(77.4554991263198,-3.80925352721912,127.693288354203));
#51781=CARTESIAN_POINT('Ctrl Pts',(77.447834521834,-3.89460828723173,127.797798276544));
#51782=CARTESIAN_POINT('Ctrl Pts',(77.4401699173482,-3.97578364684764,127.905976536633));
#51783=CARTESIAN_POINT('Ctrl Pts',(77.4325053128624,-4.05244416295984,128.017448460968));
#51784=CARTESIAN_POINT('Ctrl Pts',(77.4248479741973,-4.12903200714726,128.128814713183));
#51785=CARTESIAN_POINT('Ctrl Pts',(77.4171906355321,-4.20111329310754,128.243468091448));
#51786=CARTESIAN_POINT('Ctrl Pts',(77.409533296867,-4.26839250749628,128.361000540858));
#51787=CARTESIAN_POINT('Ctrl Pts',(77.4018819124277,-4.33561940662809,128.478441598888));
#51788=CARTESIAN_POINT('Ctrl Pts',(77.3942305279885,-4.39805146679596,128.598756925088));
#51789=CARTESIAN_POINT('Ctrl Pts',(77.3865791435492,-4.45543657273441,128.721509684628));
#51790=CARTESIAN_POINT('Ctrl Pts',(77.3789311472552,-4.51279626770592,128.844208087445));
#51791=CARTESIAN_POINT('Ctrl Pts',(77.3712831509613,-4.56511328486775,128.969341412917));
#51792=CARTESIAN_POINT('Ctrl Pts',(77.3636351546673,-4.61218172281993,129.09644878782));
#51793=CARTESIAN_POINT('Ctrl Pts',(77.355988294649,-4.65924316773515,129.223537278167));
#51794=CARTESIAN_POINT('Ctrl Pts',(77.3483414346307,-4.70105744378289,129.352598858408));
#51795=CARTESIAN_POINT('Ctrl Pts',(77.3406945746124,-4.73746718313463,129.483153687815));
#51796=CARTESIAN_POINT('Ctrl Pts',(77.3387605649789,-4.74667577156033,129.516173031331));
#51797=CARTESIAN_POINT('Ctrl Pts',(77.3368265553455,-4.75553889964443,129.54928781268));
#51798=CARTESIAN_POINT('Ctrl Pts',(77.3348925457121,-4.76405452823405,129.582490119308));
#51799=CARTESIAN_POINT('Ctrl Pts',(79.0845758390371,-4.76405452823407,129.582490119308));
#51800=CARTESIAN_POINT('Ctrl Pts',(79.0763773866997,-4.80000871991458,129.72267496699));
#51801=CARTESIAN_POINT('Ctrl Pts',(79.0681789343622,-4.82981020052689,129.86459984855));
#51802=CARTESIAN_POINT('Ctrl Pts',(79.0599804820248,-4.85330185278545,130.007715032472));
#51803=CARTESIAN_POINT('Ctrl Pts',(79.0518001104447,-4.87674169686777,130.150514592079));
#51804=CARTESIAN_POINT('Ctrl Pts',(79.0436197388646,-4.89389941114362,130.294498904072));
#51805=CARTESIAN_POINT('Ctrl Pts',(79.0354393672845,-4.90466844418986,130.439106575743));
#51806=CARTESIAN_POINT('Ctrl Pts',(79.028579390202,-4.91369924666305,130.560373110385));
#51807=CARTESIAN_POINT('Ctrl Pts',(79.0217194131196,-4.91823815351782,130.682077652307));
#51808=CARTESIAN_POINT('Ctrl Pts',(79.0148594360371,-4.91824997683007,130.803883217332));
#51809=CARTESIAN_POINT('',(79.3601405639593,-4.91824827266494,130.800238612192));
#51810=CARTESIAN_POINT('Ctrl Pts',(79.4301745447722,-4.76405452823407,129.582490119308));
#51811=CARTESIAN_POINT('Ctrl Pts',(79.4228045070997,-4.79627342777008,129.708111119609));
#51812=CARTESIAN_POINT('Ctrl Pts',(79.4154344694273,-4.82347969088767,129.834848857671));
#51813=CARTESIAN_POINT('Ctrl Pts',(79.4080644317549,-4.84562331757989,129.962269335919));
#51814=CARTESIAN_POINT('Ctrl Pts',(79.395942616872,-4.88204388359722,130.171843223904));
#51815=CARTESIAN_POINT('Ctrl Pts',(79.3838208019891,-4.90487565833682,130.383842954193));
#51816=CARTESIAN_POINT('Ctrl Pts',(79.3716989871062,-4.9138708413202,130.596860214378));
#51817=CARTESIAN_POINT('Ctrl Pts',(79.367846179407,-4.91672987774251,130.664565797086));
#51818=CARTESIAN_POINT('Ctrl Pts',(79.3639933717077,-4.91819139497684,130.73237394268));
#51819=CARTESIAN_POINT('Ctrl Pts',(79.3601405640085,-4.91824827266422,130.800238611325));
#51820=CARTESIAN_POINT('Ctrl Pts',(79.3601405639593,-4.91824827266494,130.800238612192));
#51821=CARTESIAN_POINT('Ctrl Pts',(79.3524935954593,-4.91836116223177,130.934934923014));
#51822=CARTESIAN_POINT('Ctrl Pts',(79.3448466269593,-4.91293649359095,131.069828220389));
#51823=CARTESIAN_POINT('Ctrl Pts',(79.3371996584593,-4.90195240701566,131.204417690811));
#51824=CARTESIAN_POINT('Ctrl Pts',(79.3295598048268,-4.89097854021836,131.338881936937));
#51825=CARTESIAN_POINT('Ctrl Pts',(79.3219199511942,-4.87445557616604,131.473042518561));
#51826=CARTESIAN_POINT('Ctrl Pts',(79.3142800975617,-4.8524137038026,131.606398216216));
#51827=CARTESIAN_POINT('Ctrl Pts',(79.3065857938276,-4.83021473651977,131.740704355024));
#51828=CARTESIAN_POINT('Ctrl Pts',(79.2988914900934,-4.80241787379798,131.874193677035));
#51829=CARTESIAN_POINT('Ctrl Pts',(79.2911971863593,-4.76910726066446,132.006358537189));
#51830=CARTESIAN_POINT('Ctrl Pts',(79.2835648230416,-4.73606480347094,132.137459448379));
#51831=CARTESIAN_POINT('Ctrl Pts',(79.275932459724,-4.69759715576904,132.267256748717));
#51832=CARTESIAN_POINT('Ctrl Pts',(79.2683000964063,-4.65383771736922,132.395265254209));
#51833=CARTESIAN_POINT('Ctrl Pts',(79.2606685338525,-4.61008287007373,132.523260329446));
#51834=CARTESIAN_POINT('Ctrl Pts',(79.2530369712986,-4.56103746654411,132.649466601059));
#51835=CARTESIAN_POINT('Ctrl Pts',(79.2454054087448,-4.50688442699455,132.773415168414));
#51836=CARTESIAN_POINT('Ctrl Pts',(79.237772879891,-4.45272453064732,132.897379429998));
#51837=CARTESIAN_POINT('Ctrl Pts',(79.2301403510372,-4.39345587438817,133.019085049171));
#51838=CARTESIAN_POINT('Ctrl Pts',(79.2225078221834,-4.32930882260372,133.138084718874));
#51839=CARTESIAN_POINT('Ctrl Pts',(79.2147669043299,-4.26425082309718,133.258774294427));
#51840=CARTESIAN_POINT('Ctrl Pts',(79.2070259864765,-4.1941750058629,133.376680096048));
#51841=CARTESIAN_POINT('Ctrl Pts',(79.199285068623,-4.11936840775755,133.491363963985));
#51842=CARTESIAN_POINT('Ctrl Pts',(79.1916413917208,-4.04550152570298,133.604607179972));
#51843=CARTESIAN_POINT('Ctrl Pts',(79.1839977148185,-3.96702232233983,133.714708651486));
#51844=CARTESIAN_POINT('Ctrl Pts',(79.1763540379162,-3.88424856211802,133.821278940985));
#51845=CARTESIAN_POINT('Ctrl Pts',(79.1685644995872,-3.79989526119619,133.929882871451));
#51846=CARTESIAN_POINT('Ctrl Pts',(79.1607749612582,-3.71108212784948,134.034819148194));
#51847=CARTESIAN_POINT('Ctrl Pts',(79.1529854229292,-3.61818496038963,134.13571479491));
#51848=CARTESIAN_POINT('Ctrl Pts',(79.1451958846001,-3.52528779292972,134.236610441627));
#51849=CARTESIAN_POINT('Ctrl Pts',(79.1374063462711,-3.42830694881053,134.333465199769));
#51850=CARTESIAN_POINT('Ctrl Pts',(79.1296168079421,-3.32765300859565,134.425949842876));
#51851=CARTESIAN_POINT('Ctrl Pts',(79.121842473823,-3.22719553235255,134.518253967463));
#51852=CARTESIAN_POINT('Ctrl Pts',(79.1140681397039,-3.12273546025575,134.606521316976));
#51853=CARTESIAN_POINT('Ctrl Pts',(79.1062938055848,-3.01463088805298,134.690384764596));
#51854=CARTESIAN_POINT('Ctrl Pts',(79.0985290526377,-2.90665954507379,134.774144858011));
#51855=CARTESIAN_POINT('Ctrl Pts',(79.0907642996906,-2.79505294472124,134.853511611131));
#51856=CARTESIAN_POINT('Ctrl Pts',(79.0829995467435,-2.6802052765317,134.928155318827));
#51857=CARTESIAN_POINT('Ctrl Pts',(79.0752425058584,-2.56547167666536,135.00272488934));
#51858=CARTESIAN_POINT('Ctrl Pts',(79.0674854649735,-2.44750374075563,135.072580538043));
#51859=CARTESIAN_POINT('Ctrl Pts',(79.0597284240885,-2.32672763773676,135.137433610523));
#51860=CARTESIAN_POINT('Ctrl Pts',(79.0519772328483,-2.20604261291718,135.202237776796));
#51861=CARTESIAN_POINT('Ctrl Pts',(79.0442260416083,-2.08255397911777,135.262046691532));
#51862=CARTESIAN_POINT('Ctrl Pts',(79.0364748503681,-1.9567154037297,135.316615917447));
#51863=CARTESIAN_POINT('Ctrl Pts',(79.028726953591,-1.83093031309267,135.371161949986));
#51864=CARTESIAN_POINT('Ctrl Pts',(79.020979056814,-1.70279762532049,135.420472567832));
#51865=CARTESIAN_POINT('Ctrl Pts',(79.0132311600369,-1.5727938407223,135.464350166598));
#51866=CARTESIAN_POINT('Ctrl Pts',(79.0054848839528,-1.4428172501133,135.508218587116));
#51867=CARTESIAN_POINT('Ctrl Pts',(78.9977386078687,-1.31097071138136,135.54665612411));
#51868=CARTESIAN_POINT('Ctrl Pts',(78.9899923317845,-1.17774848009606,135.579514183697));
#51869=CARTESIAN_POINT('Ctrl Pts',(78.9822459985192,-1.04452526539461,135.612372485834));
#51870=CARTESIAN_POINT('Ctrl Pts',(78.9744996652539,-0.909926717466218,
135.639651134757));
#51871=CARTESIAN_POINT('Ctrl Pts',(78.9667533319885,-0.774459562645285,
135.661252159316));
#51872=CARTESIAN_POINT('Ctrl Pts',(78.9590052639855,-0.638962070894385,
135.682858021275));
#51873=CARTESIAN_POINT('Ctrl Pts',(78.9512571959825,-0.502595971195422,
135.698783667251));
#51874=CARTESIAN_POINT('Ctrl Pts',(78.9435091279796,-0.365875031979472,
135.70898277666));
#51875=CARTESIAN_POINT('Ctrl Pts',(78.9357528252377,-0.229008784122138,
135.719192725803));
#51876=CARTESIAN_POINT('Ctrl Pts',(78.9279965224959,-0.0917873338982612,
135.723663951346));
#51877=CARTESIAN_POINT('Ctrl Pts',(78.920240219754,0.0452730542169191,135.722402241329));
#51878=CARTESIAN_POINT('Ctrl Pts',(78.9124797772398,0.182406595588418,135.721139857899));
#51879=CARTESIAN_POINT('Ctrl Pts',(78.9047193347257,0.319378513296868,135.714138461866));
#51880=CARTESIAN_POINT('Ctrl Pts',(78.8969588922115,0.455676731040842,135.70145585651));
#51881=CARTESIAN_POINT('Ctrl Pts',(78.8891859919461,0.592193746783647,135.68875289191));
#51882=CARTESIAN_POINT('Ctrl Pts',(78.8814130916806,0.728034513765061,135.670350545871));
#51883=CARTESIAN_POINT('Ctrl Pts',(78.8736401914151,0.862695334498785,135.646358120904));
#51884=CARTESIAN_POINT('Ctrl Pts',(78.8661498556531,0.992460895208244,135.623237881019));
#51885=CARTESIAN_POINT('Ctrl Pts',(78.8586595198912,1.12113050747743,135.594926999127));
#51886=CARTESIAN_POINT('Ctrl Pts',(78.8511691841292,1.24826785040078,135.561566776243));
#51887=CARTESIAN_POINT('Ctrl Pts',(78.8433948500101,1.3802256443241,135.526941690369));
#51888=CARTESIAN_POINT('Ctrl Pts',(78.835620515891,1.51095068587766,135.486767131713));
#51889=CARTESIAN_POINT('Ctrl Pts',(78.8278461817719,1.6399405413726,135.441145935355));
#51890=CARTESIAN_POINT('Ctrl Pts',(78.8200814288248,1.76877142839854,135.395580963044));
#51891=CARTESIAN_POINT('Ctrl Pts',(78.8123166758778,1.89587101921497,135.344582838007));
#51892=CARTESIAN_POINT('Ctrl Pts',(78.8045519229307,2.02074885448547,135.288304989388));
#51893=CARTESIAN_POINT('Ctrl Pts',(78.7967948820457,2.14550265932984,135.232083036722));
#51894=CARTESIAN_POINT('Ctrl Pts',(78.7890378411607,2.26803874588437,135.170591955658));
#51895=CARTESIAN_POINT('Ctrl Pts',(78.7812808002757,2.38788390629803,135.104034269431));
#51896=CARTESIAN_POINT('Ctrl Pts',(78.7735296090355,2.50763869054421,135.037526774873));
#51897=CARTESIAN_POINT('Ctrl Pts',(78.7657784177953,2.62470624733536,134.965960469206));
#51898=CARTESIAN_POINT('Ctrl Pts',(78.7580272265552,2.73863570635442,134.889584911333));
#51899=CARTESIAN_POINT('Ctrl Pts',(78.7502793297781,2.85251674231392,134.813241815109));
#51900=CARTESIAN_POINT('Ctrl Pts',(78.742531433001,2.96326200921285,134.732093749404));
#51901=CARTESIAN_POINT('Ctrl Pts',(78.7347835362239,3.07044769682727,134.646434797426));
#51902=CARTESIAN_POINT('Ctrl Pts',(78.7270372601399,3.17761096350643,134.560793763454));
#51903=CARTESIAN_POINT('Ctrl Pts',(78.7192909840557,3.28121582670241,134.470643963965));
#51904=CARTESIAN_POINT('Ctrl Pts',(78.7115447079716,3.38087011296483,134.376320911545));
#51905=CARTESIAN_POINT('Ctrl Pts',(78.7037983747063,3.48052513485256,134.281997162853));
#51906=CARTESIAN_POINT('Ctrl Pts',(78.696052041441,3.57622923767062,134.183500368513));
#51907=CARTESIAN_POINT('Ctrl Pts',(78.6883057081756,3.66762609755516,134.081203895941));
#51908=CARTESIAN_POINT('Ctrl Pts',(78.6805576401727,3.75904342513277,133.978884514784));
#51909=CARTESIAN_POINT('Ctrl Pts',(78.6728095721697,3.84615132994452,133.872764053674));
#51910=CARTESIAN_POINT('Ctrl Pts',(78.6650615041667,3.92863313678456,133.763249723136));
#51911=CARTESIAN_POINT('Ctrl Pts',(78.6573052014248,4.01120260627058,133.653618999463));
#51912=CARTESIAN_POINT('Ctrl Pts',(78.649548898683,4.08913592061772,133.540587513698));
#51913=CARTESIAN_POINT('Ctrl Pts',(78.6417925959411,4.16215889590909,133.424592742341));
#51914=CARTESIAN_POINT('Ctrl Pts',(78.634032153427,4.23522084576107,133.308536061083));
#51915=CARTESIAN_POINT('Ctrl Pts',(78.6262717109127,4.30336704023561,133.189513281894));
#51916=CARTESIAN_POINT('Ctrl Pts',(78.6185112683986,4.36636932111877,133.067986473155));
#51917=CARTESIAN_POINT('Ctrl Pts',(78.6107383681331,4.42947273885629,132.946264578794));
#51918=CARTESIAN_POINT('Ctrl Pts',(78.6029654678677,4.48741557660095,132.822030976786));
#51919=CARTESIAN_POINT('Ctrl Pts',(78.5951925676023,4.54001753285584,132.695768522768));
#51920=CARTESIAN_POINT('Ctrl Pts',(78.5877022318403,4.59070727550465,132.57409602699));
#51921=CARTESIAN_POINT('Ctrl Pts',(78.5802118960782,4.63643759712486,132.45053991488));
#51922=CARTESIAN_POINT('Ctrl Pts',(78.5727215603162,4.67709153615477,132.325543652223));
#51923=CARTESIAN_POINT('Ctrl Pts',(78.5649472261971,4.71928688163942,132.195808118277));
#51924=CARTESIAN_POINT('Ctrl Pts',(78.557172892078,4.75614696573537,132.06411010822));
#51925=CARTESIAN_POINT('Ctrl Pts',(78.5493985579589,4.78748672882742,131.930927918619));
#51926=CARTESIAN_POINT('Ctrl Pts',(78.5416338050118,4.81878786846238,131.797909864163));
#51927=CARTESIAN_POINT('Ctrl Pts',(78.5338690520647,4.84458213494296,131.66341164648));
#51928=CARTESIAN_POINT('Ctrl Pts',(78.5261042991176,4.86473350730262,131.527928835101));
#51929=CARTESIAN_POINT('Ctrl Pts',(78.5183472582326,4.88486486503517,131.39258058716));
#51930=CARTESIAN_POINT('Ctrl Pts',(78.5105902173476,4.89936442491144,131.256250075822));
#51931=CARTESIAN_POINT('Ctrl Pts',(78.5028331764626,4.90814679506125,131.119444893007));
#51932=CARTESIAN_POINT('Ctrl Pts',(78.4950819852225,4.91692254235735,130.982742876045));
#51933=CARTESIAN_POINT('Ctrl Pts',(78.4873307939824,4.91998965651643,130.845567288675));
#51934=CARTESIAN_POINT('Ctrl Pts',(78.4795796027423,4.91731439209068,130.708432353546));
#51935=CARTESIAN_POINT('Ctrl Pts',(78.4718317059652,4.91464026472366,130.571355704422));
#51936=CARTESIAN_POINT('Ctrl Pts',(78.4640838091881,4.90622862067617,130.434320063246));
#51937=CARTESIAN_POINT('Ctrl Pts',(78.456335912411,4.89209780070101,130.297840952719));
#51938=CARTESIAN_POINT('Ctrl Pts',(78.4485896363269,4.87796993658877,130.16139039068));
#51939=CARTESIAN_POINT('Ctrl Pts',(78.4408433602428,4.85812531635059,130.025496516376));
#51940=CARTESIAN_POINT('Ctrl Pts',(78.4330970841587,4.83263423689746,129.890670629186));
#51941=CARTESIAN_POINT('Ctrl Pts',(78.4253507508934,4.80714296927496,129.755843746741));
#51942=CARTESIAN_POINT('Ctrl Pts',(78.417604417628,4.77600523189807,129.6220852513));
#51943=CARTESIAN_POINT('Ctrl Pts',(78.4098580843626,4.73934254759697,129.48989674243));
#51944=CARTESIAN_POINT('Ctrl Pts',(78.4021100163596,4.70267165294192,129.35767863086));
#51945=CARTESIAN_POINT('Ctrl Pts',(78.3943619483567,4.66047345380189,129.227031582152));
#51946=CARTESIAN_POINT('Ctrl Pts',(78.3866138803537,4.61291937724,129.098442131359));
#51947=CARTESIAN_POINT('Ctrl Pts',(78.3788575776118,4.56531475963967,128.969716014167));
#51948=CARTESIAN_POINT('Ctrl Pts',(78.37110127487,4.51234302947892,128.843052230617));
#51949=CARTESIAN_POINT('Ctrl Pts',(78.3633449721281,4.45422404502419,128.718917926139));
#51950=CARTESIAN_POINT('Ctrl Pts',(78.3555845296139,4.39607404071757,128.594717367444));
#51951=CARTESIAN_POINT('Ctrl Pts',(78.3478240870998,4.332771488363,128.473049324588));
#51952=CARTESIAN_POINT('Ctrl Pts',(78.3400636445856,4.2645818140865,128.354355512783));
#51953=CARTESIAN_POINT('Ctrl Pts',(78.3322907443201,4.19628267569111,128.235471163134));
#51954=CARTESIAN_POINT('Ctrl Pts',(78.3245178440547,4.12308094697651,128.119570916253));
#51955=CARTESIAN_POINT('Ctrl Pts',(78.3167449437893,4.04528541070257,128.007067460162));
#51956=CARTESIAN_POINT('Ctrl Pts',(78.3092546080273,3.97031793812805,127.898653788081));
#51957=CARTESIAN_POINT('Ctrl Pts',(78.3017642722653,3.8910850375808,127.793394476732));
#51958=CARTESIAN_POINT('Ctrl Pts',(78.2942739365033,3.80789658880433,127.691627633278));
#51959=CARTESIAN_POINT('Ctrl Pts',(78.2864996023843,3.72155402470724,127.586002269023));
#51960=CARTESIAN_POINT('Ctrl Pts',(78.2787252682652,3.63067653477672,127.483804845003));
#51961=CARTESIAN_POINT('Ctrl Pts',(78.2709509341461,3.53556649421695,127.38544958809));
#51962=CARTESIAN_POINT('Ctrl Pts',(78.263186181199,3.440573668282,127.287215545241));
#51963=CARTESIAN_POINT('Ctrl Pts',(78.2554214282519,3.341358939651,127.192814526361));
#51964=CARTESIAN_POINT('Ctrl Pts',(78.2476566753049,3.23826572235054,127.102628837176));
#51965=CARTESIAN_POINT('Ctrl Pts',(78.2398996344199,3.13527489868692,127.012532721689));
#51966=CARTESIAN_POINT('Ctrl Pts',(78.2321425935349,3.02841354470191,126.92664385988));
#51967=CARTESIAN_POINT('Ctrl Pts',(78.2243855526499,2.91806255546323,126.84530846018));
#51968=CARTESIAN_POINT('Ctrl Pts',(78.2166343614098,2.80779478276455,126.764034396138));
#51969=CARTESIAN_POINT('Ctrl Pts',(78.2088831701697,2.69404292621752,126.687307190457));
#51970=CARTESIAN_POINT('Ctrl Pts',(78.2011319789296,2.57722137566154,126.615433184042));
#51971=CARTESIAN_POINT('Ctrl Pts',(78.1933840821525,2.46044947738031,126.543589725996));
#51972=CARTESIAN_POINT('Ctrl Pts',(78.1856361853755,2.34061081233478,126.476595569026));
#51973=CARTESIAN_POINT('Ctrl Pts',(78.1778882885984,2.2181490179987,126.414713935149));
#51974=CARTESIAN_POINT('Ctrl Pts',(78.1701420125143,2.09571284002993,126.352845245577));
#51975=CARTESIAN_POINT('Ctrl Pts',(78.1623957364302,1.97065497289314,126.296087128158));
#51976=CARTESIAN_POINT('Ctrl Pts',(78.1546494603461,1.8434435844337,126.244656809915));
#51977=CARTESIAN_POINT('Ctrl Pts',(78.1469031270808,1.71623125692876,126.193226112025));
#51978=CARTESIAN_POINT('Ctrl Pts',(78.1391567938154,1.58686573884364,126.147123438327));
#51979=CARTESIAN_POINT('Ctrl Pts',(78.1314104605501,1.45583472615832,126.106517675043));
#51980=CARTESIAN_POINT('Ctrl Pts',(78.1236623925471,1.32477436998648,126.06590281838));
#51981=CARTESIAN_POINT('Ctrl Pts',(78.1159143245442,1.19204815040842,126.030787437373));
#51982=CARTESIAN_POINT('Ctrl Pts',(78.1081662565412,1.05815806365989,126.00129028966));
#51983=CARTESIAN_POINT('Ctrl Pts',(78.1004099537994,0.924125676933488,125.971761792027));
#51984=CARTESIAN_POINT('Ctrl Pts',(78.0926536510576,0.788927334470095,125.947863539905));
#51985=CARTESIAN_POINT('Ctrl Pts',(78.0848973483157,0.653074897713318,125.929663063822));
#51986=CARTESIAN_POINT('Ctrl Pts',(78.0771369058016,0.517149952420606,125.911452873597));
#51987=CARTESIAN_POINT('Ctrl Pts',(78.0693764632874,0.38057060634952,125.898946554643));
#51988=CARTESIAN_POINT('Ctrl Pts',(78.0616160207733,0.243851956322985,125.892159554306));
#51989=CARTESIAN_POINT('Ctrl Pts',(78.0538431205078,0.106913833382116,125.885361658872));
#51990=CARTESIAN_POINT('Ctrl Pts',(78.0460702202424,-0.0301636492058501,
125.88430143196));
#51991=CARTESIAN_POINT('Ctrl Pts',(78.038297319977,-0.166866380695651,125.888942153845));
#51992=CARTESIAN_POINT('Ctrl Pts',(78.0308069842148,-0.298599623565729,
125.893414173799));
#51993=CARTESIAN_POINT('Ctrl Pts',(78.0233166484526,-0.429984581423569,
125.903179828136));
#51994=CARTESIAN_POINT('Ctrl Pts',(78.0158263126904,-0.560569297566246,
125.918161161432));
#51995=CARTESIAN_POINT('Ctrl Pts',(78.0080519785713,-0.696105172908503,
125.933710516532));
#51996=CARTESIAN_POINT('Ctrl Pts',(78.0002776444522,-0.831208263231464,
125.954928118601));
#51997=CARTESIAN_POINT('Ctrl Pts',(77.9925033103331,-0.965366626552349,
125.981783470559));
#51998=CARTESIAN_POINT('Ctrl Pts',(77.984738557386,-1.09935965168088,126.008605725694));
#51999=CARTESIAN_POINT('Ctrl Pts',(77.976973804439,-1.2324098867209,126.041051830221));
#52000=CARTESIAN_POINT('Ctrl Pts',(77.9692090514919,-1.36401006336641,126.079039505775));
#52001=CARTESIAN_POINT('Ctrl Pts',(77.9614520106069,-1.49547953286105,126.116989451435));
#52002=CARTESIAN_POINT('Ctrl Pts',(77.9536949697219,-1.62550143686279,126.160469907253));
#52003=CARTESIAN_POINT('Ctrl Pts',(77.9459379288369,-1.75357861732545,126.209347549537));
#52004=CARTESIAN_POINT('Ctrl Pts',(77.9381867375968,-1.88155921378855,126.258188332809));
#52005=CARTESIAN_POINT('Ctrl Pts',(77.9304355463568,-2.00759764196169,126.312418062506));
#52006=CARTESIAN_POINT('Ctrl Pts',(77.9226843551168,-2.13121218073661,126.371853685459));
#52007=CARTESIAN_POINT('Ctrl Pts',(77.9149364583397,-2.25477418003645,126.431264046687));
#52008=CARTESIAN_POINT('Ctrl Pts',(77.9071885615626,-2.3759139873479,126.495875731332));
#52009=CARTESIAN_POINT('Ctrl Pts',(77.8994406647855,-2.4941703496418,126.565457772552));
#52010=CARTESIAN_POINT('Ctrl Pts',(77.8916943887014,-2.61240197525402,126.635025258709));
#52011=CARTESIAN_POINT('Ctrl Pts',(77.8839481126173,-2.72775101880756,126.709560835295));
#52012=CARTESIAN_POINT('Ctrl Pts',(77.8762018365332,-2.83978166490133,126.788788035954));
#52013=CARTESIAN_POINT('Ctrl Pts',(77.8684555032679,-2.95181313797966,126.868015821451));
#52014=CARTESIAN_POINT('Ctrl Pts',(77.8607091700025,-3.06052584551001,126.951935074384));
#52015=CARTESIAN_POINT('Ctrl Pts',(77.8529628367372,-3.16551408714294,127.040226769441));
#52016=CARTESIAN_POINT('Ctrl Pts',(77.8452147687342,-3.27052584016485,127.128538236811));
#52017=CARTESIAN_POINT('Ctrl Pts',(77.8374667007312,-3.37181116842586,127.22122384317));
#52018=CARTESIAN_POINT('Ctrl Pts',(77.8297186327283,-3.46899881653439,127.317925436269));
#52019=CARTESIAN_POINT('Ctrl Pts',(77.8219623299864,-3.56628975683167,127.414729804973));
#52020=CARTESIAN_POINT('Ctrl Pts',(77.8142060272446,-3.65947403968033,127.515558410484));
#52021=CARTESIAN_POINT('Ctrl Pts',(77.8064497245028,-3.74821817612046,127.620017111174));
#52022=CARTESIAN_POINT('Ctrl Pts',(77.7986892819886,-3.83700967797842,127.724531564618));
#52023=CARTESIAN_POINT('Ctrl Pts',(77.7909288394744,-3.92135607099913,127.832679665718));
#52024=CARTESIAN_POINT('Ctrl Pts',(77.7831683969602,-4.00096593647908,127.944036398595));
#52025=CARTESIAN_POINT('Ctrl Pts',(77.7753954966948,-4.08070359878254,128.055571891185));
#52026=CARTESIAN_POINT('Ctrl Pts',(77.7676225964294,-4.15568932535336,128.170325980979));
#52027=CARTESIAN_POINT('Ctrl Pts',(77.7598496961639,-4.22567612012016,128.287846284138));
#52028=CARTESIAN_POINT('Ctrl Pts',(77.7523593604019,-4.2931187186116,128.401094428263));
#52029=CARTESIAN_POINT('Ctrl Pts',(77.7448690246398,-4.35591937601727,128.516910889031));
#52030=CARTESIAN_POINT('Ctrl Pts',(77.7373786888777,-4.41389938480556,128.634873285657));
#52031=CARTESIAN_POINT('Ctrl Pts',(77.7290264058955,-4.47855141858496,128.766410155188));
#52032=CARTESIAN_POINT('Ctrl Pts',(77.7206741229133,-4.53739134454764,128.900984554709));
#52033=CARTESIAN_POINT('Ctrl Pts',(77.7123218399311,-4.59014481042747,129.038078170785));
#52034=CARTESIAN_POINT('Ctrl Pts',(77.703990322518,-4.64276711986235,129.174830942691));
#52035=CARTESIAN_POINT('Ctrl Pts',(77.695658805105,-4.68933303616603,129.314090161865));
#52036=CARTESIAN_POINT('Ctrl Pts',(77.687327287692,-4.72961527939854,129.45531563263));
#52037=CARTESIAN_POINT('Ctrl Pts',(77.684836491738,-4.7416580854671,129.497536492739));
#52038=CARTESIAN_POINT('Ctrl Pts',(77.6823456957839,-4.75313958750526,129.539932931064));
#52039=CARTESIAN_POINT('Ctrl Pts',(77.6798548998299,-4.76405452823404,129.582490119308));
#52040=CARTESIAN_POINT('Origin',(213.235140564004,0.,130.804360617566));
#52041=CARTESIAN_POINT('',(75.5849534216701,-4.76405452823407,129.582490119308));
#52042=CARTESIAN_POINT('',(75.9301393004801,-4.76405452823408,129.582490119308));
#52043=CARTESIAN_POINT('',(213.235140564004,-4.76405452823405,129.582490119308));
#52044=CARTESIAN_POINT('',(77.2648594359911,-4.91824790196687,130.808903446917));
#52045=CARTESIAN_POINT('Ctrl Pts',(77.2648594359911,-4.91824790196687,130.808903446917));
#52046=CARTESIAN_POINT('Ctrl Pts',(77.2546216692904,-4.91808097156089,130.98962894981));
#52047=CARTESIAN_POINT('Ctrl Pts',(77.2443839025897,-4.90794932828341,131.169911861407));
#52048=CARTESIAN_POINT('Ctrl Pts',(77.2341461358891,-4.88801892813298,131.348836531371));
#52049=CARTESIAN_POINT('Ctrl Pts',(77.2236182800186,-4.86752379610282,131.532831067691));
#52050=CARTESIAN_POINT('Ctrl Pts',(77.2130904241482,-4.83666667707839,131.715389732876));
#52051=CARTESIAN_POINT('Ctrl Pts',(77.2025625682778,-4.79567552321711,131.895543158902));
#52052=CARTESIAN_POINT('Ctrl Pts',(77.2017325246556,-4.79244367370771,131.909746924999));
#52053=CARTESIAN_POINT('Ctrl Pts',(77.2009024810333,-4.78914885370999,131.923935750888));
#52054=CARTESIAN_POINT('Ctrl Pts',(77.2000724374111,-4.78579118739459,131.938109166917));
#52055=CARTESIAN_POINT('Ctrl Pts',(77.192298103292,-4.75434269589643,132.070859866845));
#52056=CARTESIAN_POINT('Ctrl Pts',(77.1845237691729,-4.71731674706899,132.202511341451));
#52057=CARTESIAN_POINT('Ctrl Pts',(77.1767494350539,-4.67480408935632,132.332558833976));
#52058=CARTESIAN_POINT('Ctrl Pts',(77.1689846821068,-4.6323438246948,132.462446054588));
#52059=CARTESIAN_POINT('Ctrl Pts',(77.1612199291597,-4.58441042558499,132.590732858247));
#52060=CARTESIAN_POINT('Ctrl Pts',(77.1534551762126,-4.53114550731624,132.716925244978));
#52061=CARTESIAN_POINT('Ctrl Pts',(77.1456981353276,-4.47793349251521,132.842992295652));
#52062=CARTESIAN_POINT('Ctrl Pts',(77.1379410944426,-4.41940064757198,132.966968711237));
#52063=CARTESIAN_POINT('Ctrl Pts',(77.1301840535576,-4.35573808171466,133.088376560155));
#52064=CARTESIAN_POINT('Ctrl Pts',(77.1224328623175,-4.29212352429368,133.209692854469));
#52065=CARTESIAN_POINT('Ctrl Pts',(77.1146816710773,-4.22338712652755,133.328444092702));
#52066=CARTESIAN_POINT('Ctrl Pts',(77.1069304798372,-4.14976755580649,133.444173545649));
#52067=CARTESIAN_POINT('Ctrl Pts',(77.0991825830602,-4.07617927536665,133.559853810492));
#52068=CARTESIAN_POINT('Ctrl Pts',(77.0914346862831,-3.99771215934754,133.672514515318));
#52069=CARTESIAN_POINT('Ctrl Pts',(77.083686789506,-3.91465003599075,133.781724914762));
#52070=CARTESIAN_POINT('Ctrl Pts',(77.0759405134219,-3.83160528743949,133.890912469745));
#52071=CARTESIAN_POINT('Ctrl Pts',(77.0681942373378,-3.74396767991217,133.996650843918));
#52072=CARTESIAN_POINT('Ctrl Pts',(77.0604479612537,-3.65206321829336,134.098539925389));
#52073=CARTESIAN_POINT('Ctrl Pts',(77.0527016279884,-3.56015807825664,134.200429758982));
#52074=CARTESIAN_POINT('Ctrl Pts',(77.044955294723,-3.46398628314191,134.298469952862));
#52075=CARTESIAN_POINT('Ctrl Pts',(77.0372089614576,-3.36391254205541,134.392295325988));
#52076=CARTESIAN_POINT('Ctrl Pts',(77.0294608934546,-3.26381639014854,134.486141710657));
#52077=CARTESIAN_POINT('Ctrl Pts',(77.0217128254516,-3.15981683864191,134.575771129004));
#52078=CARTESIAN_POINT('Ctrl Pts',(77.0139647574487,-3.05231338146174,134.660857225091));
#52079=CARTESIAN_POINT('Ctrl Pts',(77.0062084547068,-2.94469566832798,134.746033751692));
#52080=CARTESIAN_POINT('Ctrl Pts',(76.9984521519649,-2.83356691749657,134.826657067167));
#52081=CARTESIAN_POINT('Ctrl Pts',(76.990695849223,-2.71935789982876,134.902442568325));
#52082=CARTESIAN_POINT('Ctrl Pts',(76.9829354067089,-2.60508792536938,134.978268518488));
#52083=CARTESIAN_POINT('Ctrl Pts',(76.9751749641947,-2.48773474256846,135.04925130706));
#52084=CARTESIAN_POINT('Ctrl Pts',(76.9674145216806,-2.36775481157271,135.115151753167));
#52085=CARTESIAN_POINT('Ctrl Pts',(76.9596416214151,-2.24758227814048,135.18115798852));
#52086=CARTESIAN_POINT('Ctrl Pts',(76.9518687211497,-2.12477492068018,135.242065404057));
#52087=CARTESIAN_POINT('Ctrl Pts',(76.9440958208843,-1.99981112904014,135.297682163001));
#52088=CARTESIAN_POINT('Ctrl Pts',(76.9366054851223,-1.87939008599151,135.351277112666));
#52089=CARTESIAN_POINT('Ctrl Pts',(76.9291151493603,-1.75696695661656,135.399959271092));
#52090=CARTESIAN_POINT('Ctrl Pts',(76.9216248135983,-1.63298227223813,135.443601068443));
#52091=CARTESIAN_POINT('Ctrl Pts',(76.9138504794792,-1.50429667086663,135.488897557806));
#52092=CARTESIAN_POINT('Ctrl Pts',(76.9060761453601,-1.37352112696702,135.528907416218));
#52093=CARTESIAN_POINT('Ctrl Pts',(76.898301811241,-1.2411293584466,135.563434159559));
#52094=CARTESIAN_POINT('Ctrl Pts',(76.8905370582939,-1.1089007509487,135.597918351775));
#52095=CARTESIAN_POINT('Ctrl Pts',(76.8827723053468,-0.975060256702649,
135.626932776517));
#52096=CARTESIAN_POINT('Ctrl Pts',(76.8750075523997,-0.840100038399312,
135.650329559685));
#52097=CARTESIAN_POINT('Ctrl Pts',(76.8672505115147,-0.705273864487582,
135.673703104838));
#52098=CARTESIAN_POINT('Ctrl Pts',(76.8594934706297,-0.569330562425579,
135.691470045567));
#52099=CARTESIAN_POINT('Ctrl Pts',(76.8517364297447,-0.432775528791537,
135.703532833786));
#52100=CARTESIAN_POINT('Ctrl Pts',(76.8439852385046,-0.296323472370509,
135.715586525362));
#52101=CARTESIAN_POINT('Ctrl Pts',(76.8362340472645,-0.159260990462933,
135.72194459213));
#52102=CARTESIAN_POINT('Ctrl Pts',(76.8284828560244,-0.0221013478367807,
135.722560958435));
#52103=CARTESIAN_POINT('Ctrl Pts',(76.8207349592473,0.114999998282496,135.723177062768));
#52104=CARTESIAN_POINT('Ctrl Pts',(76.8129870624702,0.252198032843212,135.718056318605));
#52105=CARTESIAN_POINT('Ctrl Pts',(76.8052391656931,0.388976941474538,135.707204690296));
#52106=CARTESIAN_POINT('Ctrl Pts',(76.797492889609,0.525727238906792,135.696355331913));
#52107=CARTESIAN_POINT('Ctrl Pts',(76.7897466135248,0.66205819530066,135.679777504718));
#52108=CARTESIAN_POINT('Ctrl Pts',(76.7820003374407,0.797456971587216,135.657529215602));
#52109=CARTESIAN_POINT('Ctrl Pts',(76.7742540041754,0.932856747356688,135.635280762255));
#52110=CARTESIAN_POINT('Ctrl Pts',(76.7665076709101,1.06732394349632,135.607361826856));
#52111=CARTESIAN_POINT('Ctrl Pts',(76.7587613376447,1.20035418867435,135.573881860231));
#52112=CARTESIAN_POINT('Ctrl Pts',(76.7510132696417,1.33341422505343,135.540394396));
#52113=CARTESIAN_POINT('Ctrl Pts',(76.7432652016387,1.46503629106591,135.501343517834));
#52114=CARTESIAN_POINT('Ctrl Pts',(76.7355171336358,1.59472987799049,135.456888927931));
#52115=CARTESIAN_POINT('Ctrl Pts',(76.7277608308939,1.72456130480271,135.41238709116));
#52116=CARTESIAN_POINT('Ctrl Pts',(76.720004528152,1.85245978777724,135.362470197103));
#52117=CARTESIAN_POINT('Ctrl Pts',(76.7122482254102,1.97795304001854,135.307346830512));
#52118=CARTESIAN_POINT('Ctrl Pts',(76.704487782896,2.10351327178717,135.25219404292));
#52119=CARTESIAN_POINT('Ctrl Pts',(76.6967273403818,2.22666536396528,135.191829417689));
#52120=CARTESIAN_POINT('Ctrl Pts',(76.6889668978677,2.34696135904811,135.126507704563));
#52121=CARTESIAN_POINT('Ctrl Pts',(76.6811939976022,2.46745046394154,135.061081131223));
#52122=CARTESIAN_POINT('Ctrl Pts',(76.6734210973368,2.58507397406459,134.990681769151));
#52123=CARTESIAN_POINT('Ctrl Pts',(76.6656481970713,2.69941191030411,134.91560840881));
#52124=CARTESIAN_POINT('Ctrl Pts',(76.6581578613092,2.80959337456222,134.843264154215));
#52125=CARTESIAN_POINT('Ctrl Pts',(76.6506675255472,2.91672374497599,134.766580004025));
#52126=CARTESIAN_POINT('Ctrl Pts',(76.6431771897851,3.0204575754891,134.685857635106));
#52127=CARTESIAN_POINT('Ctrl Pts',(76.635402855666,3.12812450571457,134.602074653035));
#52128=CARTESIAN_POINT('Ctrl Pts',(76.6276285215469,3.23247330858299,134.513675789963));
#52129=CARTESIAN_POINT('Ctrl Pts',(76.6198541874278,3.33308262033824,134.420953393716));
#52130=CARTESIAN_POINT('Ctrl Pts',(76.6120894344808,3.43356794010847,134.328345269535));
#52131=CARTESIAN_POINT('Ctrl Pts',(76.6043246815337,3.53032265375021,134.231424476455));
#52132=CARTESIAN_POINT('Ctrl Pts',(76.5965599285866,3.62295632464049,134.130525155325));
#52133=CARTESIAN_POINT('Ctrl Pts',(76.5888028877016,3.71549799046288,134.029726048824));
#52134=CARTESIAN_POINT('Ctrl Pts',(76.5810458468166,3.80392649624825,133.92495656413));
#52135=CARTESIAN_POINT('Ctrl Pts',(76.5732888059316,3.88788659283367,133.816589178576));
#52136=CARTESIAN_POINT('Ctrl Pts',(76.5655376146915,3.97178337445719,133.70830351371));
#52137=CARTESIAN_POINT('Ctrl Pts',(76.5577864234513,4.05121821550742,133.596425656263));
#52138=CARTESIAN_POINT('Ctrl Pts',(76.5500352322112,4.12587491908604,133.481362525402));
#52139=CARTESIAN_POINT('Ctrl Pts',(76.5422873354341,4.20049989157411,133.366348299441));
#52140=CARTESIAN_POINT('Ctrl Pts',(76.534539438657,4.27035055341159,133.248151820014));
#52141=CARTESIAN_POINT('Ctrl Pts',(76.5267915418799,4.33515311230626,133.127210280235));
#52142=CARTESIAN_POINT('Ctrl Pts',(76.5190452657958,4.3999421159026,133.006294038819));
#52143=CARTESIAN_POINT('Ctrl Pts',(76.5112989897117,4.45968493237443,132.882634223577));
#52144=CARTESIAN_POINT('Ctrl Pts',(76.5035527136276,4.51415316251924,132.756693654683));
#52145=CARTESIAN_POINT('Ctrl Pts',(76.4958063803623,4.56862179473611,132.630752156124));
#52146=CARTESIAN_POINT('Ctrl Pts',(76.488060047097,4.61781560773609,132.502530229161));
#52147=CARTESIAN_POINT('Ctrl Pts',(76.4803137138316,4.66155406057587,132.372511376527));
#52148=CARTESIAN_POINT('Ctrl Pts',(76.4725656458286,4.70530230833894,132.242463407071));
#52149=CARTESIAN_POINT('Ctrl Pts',(76.4648175778257,4.74359264028721,132.110618081685));
#52150=CARTESIAN_POINT('Ctrl Pts',(76.4570695098227,4.77629428645647,131.977474402185));
#52151=CARTESIAN_POINT('Ctrl Pts',(76.4493132070808,4.80903068832443,131.844189215998));
#52152=CARTESIAN_POINT('Ctrl Pts',(76.441556904339,4.83616644577664,131.709603299473));
#52153=CARTESIAN_POINT('Ctrl Pts',(76.4338006015971,4.85762176446778,131.574226746103));
#52154=CARTESIAN_POINT('Ctrl Pts',(76.4260401590829,4.87908853450852,131.438777938191));
#52155=CARTESIAN_POINT('Ctrl Pts',(76.4182797165687,4.89486877966622,131.302538040768));
#52156=CARTESIAN_POINT('Ctrl Pts',(76.4105192740546,4.90493469614097,131.166021631628));
#52157=CARTESIAN_POINT('Ctrl Pts',(76.4027463737891,4.91501677131845,131.02928607423));
#52158=CARTESIAN_POINT('Ctrl Pts',(76.3949734735236,4.91936617452899,130.892273509092));
#52159=CARTESIAN_POINT('Ctrl Pts',(76.3872005732582,4.91800727768246,130.755498780082));
#52160=CARTESIAN_POINT('Ctrl Pts',(76.3797102374962,4.91669778015917,130.623696156987));
#52161=CARTESIAN_POINT('Ctrl Pts',(76.3722199017344,4.91008781480973,130.492114685978));
#52162=CARTESIAN_POINT('Ctrl Pts',(76.3647295659724,4.89824446889413,130.36120806432));
#52163=CARTESIAN_POINT('Ctrl Pts',(76.3569552318533,4.88595207891834,130.225338078313));
#52164=CARTESIAN_POINT('Ctrl Pts',(76.3491808977342,4.86798268864196,130.089764730396));
#52165=CARTESIAN_POINT('Ctrl Pts',(76.3414065636152,4.84435450116717,129.955000546971));
#52166=CARTESIAN_POINT('Ctrl Pts',(76.3336418106681,4.82075543332172,129.820402448357));
#52167=CARTESIAN_POINT('Ctrl Pts',(76.325877057721,4.79151151125301,129.686611911453));
#52168=CARTESIAN_POINT('Ctrl Pts',(76.3181123047739,4.75669281658857,129.554138032938));
#52169=CARTESIAN_POINT('Ctrl Pts',(76.3103552638889,4.72190870434256,129.421795729346));
#52170=CARTESIAN_POINT('Ctrl Pts',(76.3025982230039,4.68156093700724,129.29076785739));
#52171=CARTESIAN_POINT('Ctrl Pts',(76.2948411821189,4.63577086946081,129.161554631347));
#52172=CARTESIAN_POINT('Ctrl Pts',(76.2870899908788,4.59001533256052,129.032438846002));
#52173=CARTESIAN_POINT('Ctrl Pts',(76.2793387996387,4.53882579443605,128.905135349796));
#52174=CARTESIAN_POINT('Ctrl Pts',(76.2715876083986,4.48237369556122,128.780130117885));
#52175=CARTESIAN_POINT('Ctrl Pts',(76.2638397116215,4.42594559033429,128.655178016531));
#52176=CARTESIAN_POINT('Ctrl Pts',(76.2560918148444,4.3642595336146,128.532522592214));
#52177=CARTESIAN_POINT('Ctrl Pts',(76.2483439180673,4.29753535692961,128.4126305077));
#52178=CARTESIAN_POINT('Ctrl Pts',(76.2405976419832,4.23082513750398,128.292763502026));
#52179=CARTESIAN_POINT('Ctrl Pts',(76.2328513658992,4.1590790843152,128.175659027826));
#52180=CARTESIAN_POINT('Ctrl Pts',(76.2251050898151,4.08256312573636,128.061759409428));
#52181=CARTESIAN_POINT('Ctrl Pts',(76.2173587565497,4.00604660233411,127.947858950249));
#52182=CARTESIAN_POINT('Ctrl Pts',(76.2096124232844,3.92476032129899,127.837163718613));
#52183=CARTESIAN_POINT('Ctrl Pts',(76.2018660900191,3.83901348038315,127.730086953766));
#52184=CARTESIAN_POINT('Ctrl Pts',(76.1941180220161,3.75324743705686,127.622986209819));
#52185=CARTESIAN_POINT('Ctrl Pts',(76.1863699540131,3.66301909046738,127.51950585024));
#52186=CARTESIAN_POINT('Ctrl Pts',(76.1786218860101,3.56867758061624,127.420025618174));
#52187=CARTESIAN_POINT('Ctrl Pts',(76.1708655832682,3.47423580348568,127.320439657334));
#52188=CARTESIAN_POINT('Ctrl Pts',(76.1631092805264,3.37567239997271,127.224862600739));
#52189=CARTESIAN_POINT('Ctrl Pts',(76.1553529777846,3.2733733953874,127.133637299626));
#52190=CARTESIAN_POINT('Ctrl Pts',(76.1475925352704,3.1710197907431,127.042363308822));
#52191=CARTESIAN_POINT('Ctrl Pts',(76.1398320927562,3.06492691448858,126.955445949249));
#52192=CARTESIAN_POINT('Ctrl Pts',(76.1320716502421,2.95551266686261,126.873186754899));
#52193=CARTESIAN_POINT('Ctrl Pts',(76.1242987499766,2.84592277777308,126.790795510788));
#52194=CARTESIAN_POINT('Ctrl Pts',(76.1165258497112,2.73300118500108,126.71307759651));
#52195=CARTESIAN_POINT('Ctrl Pts',(76.1087529494458,2.61719421488499,126.640290792975));
#52196=CARTESIAN_POINT('Ctrl Pts',(76.1012626136837,2.50559711983159,126.570149973086));
#52197=CARTESIAN_POINT('Ctrl Pts',(76.0937722779216,2.39132105396002,126.504588125));
#52198=CARTESIAN_POINT('Ctrl Pts',(76.0862819421595,2.27478398793205,126.443794040761));
#52199=CARTESIAN_POINT('Ctrl Pts',(76.0785076080404,2.15382838362607,126.380694930341));
#52200=CARTESIAN_POINT('Ctrl Pts',(76.0707332739213,2.0300537920153,126.322532381187));
#52201=CARTESIAN_POINT('Ctrl Pts',(76.0629589398022,1.90390125529857,126.269568111555));
#52202=CARTESIAN_POINT('Ctrl Pts',(76.0551941868551,1.77790419030886,126.216669115652));
#52203=CARTESIAN_POINT('Ctrl Pts',(76.0474294339081,1.64953536826582,126.168955802307));
#52204=CARTESIAN_POINT('Ctrl Pts',(76.039664680961,1.51926098745546,126.126644389053));
#52205=CARTESIAN_POINT('Ctrl Pts',(76.0319076400759,1.38911599699667,126.084375000091));
#52206=CARTESIAN_POINT('Ctrl Pts',(76.0241505991909,1.25706958362367,126.047496954132));
#52207=CARTESIAN_POINT('Ctrl Pts',(76.0163935583059,1.12360818705126,126.016178529916));
#52208=CARTESIAN_POINT('Ctrl Pts',(76.0086423670658,0.990247434756191,125.984883723168));
#52209=CARTESIAN_POINT('Ctrl Pts',(76.0008911758257,0.855474202245346,125.959140282095));
#52210=CARTESIAN_POINT('Ctrl Pts',(75.9931399845856,0.719790021944568,125.939066650414));
#52211=CARTESIAN_POINT('Ctrl Pts',(75.9853920878085,0.58416351103982,125.919001550562));
#52212=CARTESIAN_POINT('Ctrl Pts',(75.9776441910314,0.44762720835677,125.904601524251));
#52213=CARTESIAN_POINT('Ctrl Pts',(75.9698962942543,0.310692554808173,125.895933863617));
#52214=CARTESIAN_POINT('Ctrl Pts',(75.9621500181702,0.173786545037129,125.88726801607));
#52215=CARTESIAN_POINT('Ctrl Pts',(75.954403742086,0.0364827400784687,125.884332173831));
#52216=CARTESIAN_POINT('Ctrl Pts',(75.9466574660019,-0.100702979302659,
125.887141690931));
#52217=CARTESIAN_POINT('Ctrl Pts',(75.9389111327366,-0.237889711357603,
125.88995122877));
#52218=CARTESIAN_POINT('Ctrl Pts',(75.9311647994712,-0.374957965212396,
125.898506202571));
#52219=CARTESIAN_POINT('Ctrl Pts',(75.9234184662059,-0.511392942048524,
125.912769841415));
#52220=CARTESIAN_POINT('Ctrl Pts',(75.9156703982029,-0.647858472551647,
125.927036674502));
#52221=CARTESIAN_POINT('Ctrl Pts',(75.9079223301999,-0.78369005506314,125.947014675887));
#52222=CARTESIAN_POINT('Ctrl Pts',(75.900174262197,-0.918379482220692,125.972615364644));
#52223=CARTESIAN_POINT('Ctrl Pts',(75.8924179594551,-1.05321205890425,125.998243262118));
#52224=CARTESIAN_POINT('Ctrl Pts',(75.8846616567132,-1.1868996706441,126.029505711265));
#52225=CARTESIAN_POINT('Ctrl Pts',(75.8769053539714,-1.31894521087635,126.066263257527));
#52226=CARTESIAN_POINT('Ctrl Pts',(75.8691449114572,-1.45106122778941,126.103040422399));
#52227=CARTESIAN_POINT('Ctrl Pts',(75.8613844689431,-1.58153305510366,126.145318407975));
#52228=CARTESIAN_POINT('Ctrl Pts',(75.8536240264289,-1.70988111844552,126.192908609436));
#52229=CARTESIAN_POINT('Ctrl Pts',(75.8458511261635,-1.83843521749277,126.240575206914));
#52230=CARTESIAN_POINT('Ctrl Pts',(75.838078225898,-1.96485837901661,126.293570909987));
#52231=CARTESIAN_POINT('Ctrl Pts',(75.8303053256325,-2.0886924743509,126.351659548542));
#52232=CARTESIAN_POINT('Ctrl Pts',(75.8228149898706,-2.20802488839984,126.407636518769));
#52233=CARTESIAN_POINT('Ctrl Pts',(75.8153246541086,-2.32495293295197,126.468342429125));
#52234=CARTESIAN_POINT('Ctrl Pts',(75.8078343183466,-2.43909184856289,126.533527675765));
#52235=CARTESIAN_POINT('Ctrl Pts',(75.8000588645336,-2.55757543792452,126.601194185071));
#52236=CARTESIAN_POINT('Ctrl Pts',(75.7922834107205,-2.67342873198506,126.673902173205));
#52237=CARTESIAN_POINT('Ctrl Pts',(75.7845079569074,-2.78619294902018,126.75142194133));
#52238=CARTESIAN_POINT('Ctrl Pts',(75.7767423286274,-2.89881467038056,126.828843750794));
#52239=CARTESIAN_POINT('Ctrl Pts',(75.7689767003473,-3.00835476318595,126.911065021064));
#52240=CARTESIAN_POINT('Ctrl Pts',(75.7612110720673,-3.11437918435546,126.997810294957));
#52241=CARTESIAN_POINT('Ctrl Pts',(75.7534548404659,-3.2202753123113,127.084450604071));
#52242=CARTESIAN_POINT('Ctrl Pts',(75.7456986088644,-3.32266394081346,127.175603767778));
#52243=CARTESIAN_POINT('Ctrl Pts',(75.737942377263,-3.42114069247982,127.270951580282));
#52244=CARTESIAN_POINT('Ctrl Pts',(75.7301914739738,-3.51954979339658,127.36623389153));
#52245=CARTESIAN_POINT('Ctrl Pts',(75.7224405706846,-3.61405208432284,127.465704847871));
#52246=CARTESIAN_POINT('Ctrl Pts',(75.7146896673954,-3.70427687070828,127.5690065523));
#52247=CARTESIAN_POINT('Ctrl Pts',(75.7069424101299,-3.79445921536855,127.672259663623));
#52248=CARTESIAN_POINT('Ctrl Pts',(75.6991951528643,-3.88036780317911,127.77933964323));
#52249=CARTESIAN_POINT('Ctrl Pts',(75.6914478955988,-3.96166965843234,127.889852669394));
#52250=CARTESIAN_POINT('Ctrl Pts',(75.6837026048881,-4.04295087611694,128.00033764306));
#52251=CARTESIAN_POINT('Ctrl Pts',(75.6759573141774,-4.11962745824334,128.114253613544));
#52252=CARTESIAN_POINT('Ctrl Pts',(75.6682120234667,-4.19140775088568,128.231175018291));
#52253=CARTESIAN_POINT('Ctrl Pts',(75.6604647800918,-4.26320614004766,128.348125900077));
#52254=CARTESIAN_POINT('Ctrl Pts',(75.6527175367169,-4.33010556436869,128.468083399465));
#52255=CARTESIAN_POINT('Ctrl Pts',(75.644970293342,-4.39185861014737,128.590594367264));
#52256=CARTESIAN_POINT('Ctrl Pts',(75.6372220623902,-4.45361952787191,128.713120952102));
#52257=CARTESIAN_POINT('Ctrl Pts',(75.6294738314384,-4.51023259159163,128.83820130099));
#52258=CARTESIAN_POINT('Ctrl Pts',(75.6217256004867,-4.56149753334166,128.965359987926));
#52259=CARTESIAN_POINT('Ctrl Pts',(75.613971480313,-4.61280144019459,129.092615324758));
#52260=CARTESIAN_POINT('Ctrl Pts',(75.6062173601394,-4.65874896788764,129.221951788917));
#52261=CARTESIAN_POINT('Ctrl Pts',(75.5984632399657,-4.69918886814165,129.352876189805));
#52262=CARTESIAN_POINT('Ctrl Pts',(75.5939599672005,-4.72267469211181,129.428911674891));
#52263=CARTESIAN_POINT('Ctrl Pts',(75.5894566944353,-4.74430383295107,129.505482458159));
#52264=CARTESIAN_POINT('Ctrl Pts',(75.5849534216701,-4.76405452823408,129.582490119308));
#52265=CARTESIAN_POINT('Ctrl Pts',(77.3348925457121,-4.76405452823405,129.582490119308));
#52266=CARTESIAN_POINT('Ctrl Pts',(77.3272431990384,-4.79773533007694,129.713811054516));
#52267=CARTESIAN_POINT('Ctrl Pts',(77.3195938523647,-4.82597605115416,129.846501919531));
#52268=CARTESIAN_POINT('Ctrl Pts',(77.311944505691,-4.84868252185261,129.980066456007));
#52269=CARTESIAN_POINT('Ctrl Pts',(77.3040969940744,-4.87197722925453,130.117091132267));
#52270=CARTESIAN_POINT('Ctrl Pts',(77.2962494824577,-4.88944694813033,130.255034923563));
#52271=CARTESIAN_POINT('Ctrl Pts',(77.2884019708411,-4.90104660224639,130.393355428902));
#52272=CARTESIAN_POINT('Ctrl Pts',(77.2805544592244,-4.91264625636247,130.53167593424));
#52273=CARTESIAN_POINT('Ctrl Pts',(77.2727069476077,-4.91837585841854,130.670372698479));
#52274=CARTESIAN_POINT('Ctrl Pts',(77.2648594359911,-4.91824790196687,130.808903446917));
#52275=CARTESIAN_POINT('',(77.610140564059,-4.91824986258823,130.803198012381));
#52276=CARTESIAN_POINT('Ctrl Pts',(77.6798548998299,-4.76405452823404,129.582490119308));
#52277=CARTESIAN_POINT('Ctrl Pts',(77.6715497968428,-4.8004483993194,129.724389270316));
#52278=CARTESIAN_POINT('Ctrl Pts',(77.6632446938558,-4.83053974511505,129.868076996986));
#52279=CARTESIAN_POINT('Ctrl Pts',(77.6549395908687,-4.85416491434517,130.012990889285));
#52280=CARTESIAN_POINT('Ctrl Pts',(77.6466578611242,-4.8777235947174,130.157496947078));
#52281=CARTESIAN_POINT('Ctrl Pts',(77.6383761313797,-4.89485234025123,130.30322199338));
#52282=CARTESIAN_POINT('Ctrl Pts',(77.6300944016353,-4.90543804606879,130.44959218791));
#52283=CARTESIAN_POINT('Ctrl Pts',(77.6234431224431,-4.91393971021512,130.567146015342));
#52284=CARTESIAN_POINT('Ctrl Pts',(77.6167918432511,-4.91822194956528,130.685115603136));
#52285=CARTESIAN_POINT('Ctrl Pts',(77.610140564059,-4.91824986258823,130.803198012381));
#52286=CARTESIAN_POINT('Ctrl Pts',(77.6101405640085,-4.91824986258845,130.803198013277));
#52287=CARTESIAN_POINT('Ctrl Pts',(77.6021562717305,-4.91828336976134,130.944945854718));
#52288=CARTESIAN_POINT('Ctrl Pts',(77.5941719794525,-4.9121846040386,131.086623373462));
#52289=CARTESIAN_POINT('Ctrl Pts',(77.5861876871745,-4.89999794552716,131.227684602629));
#52290=CARTESIAN_POINT('Ctrl Pts',(77.578197210792,-4.88780184803631,131.368855088492));
#52291=CARTESIAN_POINT('Ctrl Pts',(77.5702067344094,-4.86950848728427,131.509407978856));
#52292=CARTESIAN_POINT('Ctrl Pts',(77.5622162580269,-4.84521387953863,131.648804531646));
#52293=CARTESIAN_POINT('Ctrl Pts',(77.5542183824385,-4.82089677491125,131.788330166074));
#52294=CARTESIAN_POINT('Ctrl Pts',(77.5462205068502,-4.79056740431481,131.926696978207));
#52295=CARTESIAN_POINT('Ctrl Pts',(77.5382226312619,-4.75437242730818,132.063378443076));
#52296=CARTESIAN_POINT('Ctrl Pts',(77.5302103941641,-4.71811245622919,132.20030534214));
#52297=CARTESIAN_POINT('Ctrl Pts',(77.5221981570663,-4.67596592520096,132.335540503171));
#52298=CARTESIAN_POINT('Ctrl Pts',(77.5141859199685,-4.62812909180166,132.468573396065));
#52299=CARTESIAN_POINT('Ctrl Pts',(77.506165460645,-4.58024316783804,132.601742808442));
#52300=CARTESIAN_POINT('Ctrl Pts',(77.4981450013216,-4.5266554290561,132.732705116981));
#52301=CARTESIAN_POINT('Ctrl Pts',(77.4901245419981,-4.46760931258675,132.860971930524));
#52302=CARTESIAN_POINT('Ctrl Pts',(77.4820894853217,-4.40845573132449,132.989472191539));
#52303=CARTESIAN_POINT('Ctrl Pts',(77.4740544286453,-4.34382408587754,133.115266840236));
#52304=CARTESIAN_POINT('Ctrl Pts',(77.4660193719689,-4.27400307237721,133.237893193845));
#52305=CARTESIAN_POINT('Ctrl Pts',(77.4636566030008,-4.2534716771846,133.273952397239));
#52306=CARTESIAN_POINT('Ctrl Pts',(77.4612938340328,-4.23249183570568,133.309737841135));
#52307=CARTESIAN_POINT('Ctrl Pts',(77.4589310650647,-4.21107156838282,133.345238282559));
#52308=CARTESIAN_POINT('Ctrl Pts',(77.4511567309456,-4.14059141677328,133.462047118603));
#52309=CARTESIAN_POINT('Ctrl Pts',(77.4433823968265,-4.06513579240713,133.576106227857));
#52310=CARTESIAN_POINT('Ctrl Pts',(77.4356080627074,-3.98494523012703,133.686962666998));
#52311=CARTESIAN_POINT('Ctrl Pts',(77.4278433097603,-3.90485349554822,133.797682485484));
#52312=CARTESIAN_POINT('Ctrl Pts',(77.4200785568133,-3.82003866068413,133.905207173487));
#52313=CARTESIAN_POINT('Ctrl Pts',(77.4123138038662,-3.73078641364259,134.009109562223));
#52314=CARTESIAN_POINT('Ctrl Pts',(77.4045567629812,-3.64162281319116,134.112908753642));
#52315=CARTESIAN_POINT('Ctrl Pts',(77.3967997220962,-3.54803082439464,134.213092510766));
#52316=CARTESIAN_POINT('Ctrl Pts',(77.3890426812112,-3.45033835946079,134.30926407811));
#52317=CARTESIAN_POINT('Ctrl Pts',(77.3812914899711,-3.35271956517468,134.405363121727));
#52318=CARTESIAN_POINT('Ctrl Pts',(77.373540298731,-3.25100672707678,134.497455724719));
#52319=CARTESIAN_POINT('Ctrl Pts',(77.3657891074909,-3.14556657055547,134.585179842642));
#52320=CARTESIAN_POINT('Ctrl Pts',(77.3580412107138,-3.04017122891317,134.672866675475));
#52321=CARTESIAN_POINT('Ctrl Pts',(77.3502933139367,-2.93105201963838,134.756188466594));
#52322=CARTESIAN_POINT('Ctrl Pts',(77.3425454171597,-2.81861073852276,134.834821703743));
#52323=CARTESIAN_POINT('Ctrl Pts',(77.3347991410756,-2.7061929776992,134.913438492513));
#52324=CARTESIAN_POINT('Ctrl Pts',(77.3270528649915,-2.59045484743002,134.987368454149));
#52325=CARTESIAN_POINT('Ctrl Pts',(77.3193065889074,-2.47182895251582,135.056330124983));
#52326=CARTESIAN_POINT('Ctrl Pts',(77.311560255642,-2.35320218193213,135.125292304877));
#52327=CARTESIAN_POINT('Ctrl Pts',(77.3038139223767,-2.23168794216799,135.189285924294));
#52328=CARTESIAN_POINT('Ctrl Pts',(77.2960675891113,-2.10774502829557,135.248074600058));
#52329=CARTESIAN_POINT('Ctrl Pts',(77.2883195211084,-1.9837743582672,135.306876441139));
#52330=CARTESIAN_POINT('Ctrl Pts',(77.2805714531054,-1.85737428503835,135.360470851618));
#52331=CARTESIAN_POINT('Ctrl Pts',(77.2728233851024,-1.72902487267096,135.408669040357));
#52332=CARTESIAN_POINT('Ctrl Pts',(77.2650670823606,-1.60053904902064,135.456918454705));
#52333=CARTESIAN_POINT('Ctrl Pts',(77.2573107796187,-1.47010011421914,135.499760053032));
#52334=CARTESIAN_POINT('Ctrl Pts',(77.2495544768769,-1.33820516703648,135.537054353));
#52335=CARTESIAN_POINT('Ctrl Pts',(77.2417940343627,-1.20623982354905,135.574368558059));
#52336=CARTESIAN_POINT('Ctrl Pts',(77.2340335918486,-1.07281729935912,135.606129474699));
#52337=CARTESIAN_POINT('Ctrl Pts',(77.2262731493344,-0.938445286687876,
135.632248717594));
#52338=CARTESIAN_POINT('Ctrl Pts',(77.218500249069,-0.803857568132993,135.658409889416));
#52339=CARTESIAN_POINT('Ctrl Pts',(77.2107273488036,-0.668317702043727,
135.678911231185));
#52340=CARTESIAN_POINT('Ctrl Pts',(77.2029544485382,-0.532339807258399,
135.693716136661));
#52341=CARTESIAN_POINT('Ctrl Pts',(77.195464112776,-0.401305051454326,135.707982846533));
#52342=CARTESIAN_POINT('Ctrl Pts',(77.1879737770139,-0.26986386824087,135.716960068321));
#52343=CARTESIAN_POINT('Ctrl Pts',(77.1804834412518,-0.138474702897517,
135.720660834107));
#52344=CARTESIAN_POINT('Ctrl Pts',(77.1727091071327,-0.00210387741711957,
135.724501915552));
#52345=CARTESIAN_POINT('Ctrl Pts',(77.1649347730136,0.134642889596524,135.722670696359));
#52346=CARTESIAN_POINT('Ctrl Pts',(77.1571604388945,0.271254509138723,135.715124718373));
#52347=CARTESIAN_POINT('Ctrl Pts',(77.1493956859474,0.407697767069261,135.70758804013));
#52348=CARTESIAN_POINT('Ctrl Pts',(77.1416309330004,0.544005822304882,135.694350637779));
#52349=CARTESIAN_POINT('Ctrl Pts',(77.1338661800533,0.679664864250737,135.675421973657));
#52350=CARTESIAN_POINT('Ctrl Pts',(77.1261091391683,0.815189167723767,135.656512109751));
#52351=CARTESIAN_POINT('Ctrl Pts',(77.1183520982832,0.950065355999913,135.631922286763));
#52352=CARTESIAN_POINT('Ctrl Pts',(77.1105950573982,1.08378238289549,135.60171393049));
#52353=CARTESIAN_POINT('Ctrl Pts',(77.1028438661581,1.21739857274074,135.571528354574));
#52354=CARTESIAN_POINT('Ctrl Pts',(77.095092674918,1.34985696130164,135.535732764628));
#52355=CARTESIAN_POINT('Ctrl Pts',(77.0873414836778,1.48065472630576,135.494440003245));
#52356=CARTESIAN_POINT('Ctrl Pts',(77.0795935869007,1.61139689877062,135.453164792386));
#52357=CARTESIAN_POINT('Ctrl Pts',(77.0718456901237,1.74047947943285,135.406397174554));
#52358=CARTESIAN_POINT('Ctrl Pts',(77.0640977933466,1.86741310782857,135.354300325651));
#52359=CARTESIAN_POINT('Ctrl Pts',(77.0563515172625,1.9943201844455,135.302214374286));
#52360=CARTESIAN_POINT('Ctrl Pts',(77.0486052411784,2.11907884144682,135.24480155752));
#52361=CARTESIAN_POINT('Ctrl Pts',(77.0408589650943,2.24121844201513,135.182273700037));
#52362=CARTESIAN_POINT('Ctrl Pts',(77.0331126318289,2.36335894419048,135.119745380987));
#52363=CARTESIAN_POINT('Ctrl Pts',(77.0253662985636,2.48288000334231,135.052102124037));
#52364=CARTESIAN_POINT('Ctrl Pts',(77.0176199652982,2.5993347536669,134.979602155595));
#52365=CARTESIAN_POINT('Ctrl Pts',(77.0098718972953,2.71581558322506,134.907085951287));
#52366=CARTESIAN_POINT('Ctrl Pts',(77.0021238292923,2.82922840570717,134.829711077823));
#52367=CARTESIAN_POINT('Ctrl Pts',(76.9943757612893,2.93915489943044,134.747779380474));
#52368=CARTESIAN_POINT('Ctrl Pts',(76.9866194585474,3.04919822433953,134.665760605142));
#52369=CARTESIAN_POINT('Ctrl Pts',(76.9788631558056,3.15574750475749,134.57917556543));
#52370=CARTESIAN_POINT('Ctrl Pts',(76.9711068530638,3.25841669621541,134.488367091003));
#52371=CARTESIAN_POINT('Ctrl Pts',(76.9633464105496,3.36114068531206,134.397510149359));
#52372=CARTESIAN_POINT('Ctrl Pts',(76.9555859680354,3.45998017734825,134.302425552283));
#52373=CARTESIAN_POINT('Ctrl Pts',(76.9478255255212,3.55458639119861,134.203492661192));
#52374=CARTESIAN_POINT('Ctrl Pts',(76.9400526252558,3.64934447534232,134.104400954242));
#52375=CARTESIAN_POINT('Ctrl Pts',(76.9322797249904,3.73985544316665,134.001448902211));
#52376=CARTESIAN_POINT('Ctrl Pts',(76.924506824725,3.82581060301693,133.895049261274));
#52377=CARTESIAN_POINT('Ctrl Pts',(76.917016488963,3.90864107629849,133.792517515289));
#52378=CARTESIAN_POINT('Ctrl Pts',(76.9095261532009,3.98724103739184,133.686784732903));
#52379=CARTESIAN_POINT('Ctrl Pts',(76.9020358174389,4.06137364968444,133.57824366127));
#52380=CARTESIAN_POINT('Ctrl Pts',(76.8942614833198,4.13831702250445,133.465587221916));
#52381=CARTESIAN_POINT('Ctrl Pts',(76.8864871492007,4.21069133373102,133.349548475254));
#52382=CARTESIAN_POINT('Ctrl Pts',(76.8787128150816,4.27818460602471,133.230534465268));
#52383=CARTESIAN_POINT('Ctrl Pts',(76.8709480621345,4.34559469889244,133.111667129413));
#52384=CARTESIAN_POINT('Ctrl Pts',(76.8631833091874,4.40813553075663,132.989832162786));
#52385=CARTESIAN_POINT('Ctrl Pts',(76.8554185562403,4.46553733537104,132.865466963417));
#52386=CARTESIAN_POINT('Ctrl Pts',(76.8476615153553,4.5228821277038,132.741225285317));
#52387=CARTESIAN_POINT('Ctrl Pts',(76.8399044744703,4.57509788750142,132.614458728263));
#52388=CARTESIAN_POINT('Ctrl Pts',(76.8321474335853,4.62196006108111,132.485630452028));
#52389=CARTESIAN_POINT('Ctrl Pts',(76.8243962423451,4.66878689553123,132.356899326197));
#52390=CARTESIAN_POINT('Ctrl Pts',(76.816645051105,4.7102680464194,132.226109941763));
#52391=CARTESIAN_POINT('Ctrl Pts',(76.8088938598648,4.74622666369328,132.093746331519));
#52392=CARTESIAN_POINT('Ctrl Pts',(76.8011459630877,4.78216999759554,131.961438979342));
#52393=CARTESIAN_POINT('Ctrl Pts',(76.7933980663107,4.8125953640511,131.827559108621));
#52394=CARTESIAN_POINT('Ctrl Pts',(76.7856501695336,4.83737553628356,131.692606632736));
#52395=CARTESIAN_POINT('Ctrl Pts',(76.7779038934495,4.86215052503818,131.557682386));
#52396=CARTESIAN_POINT('Ctrl Pts',(76.7701576173653,4.88128259778654,131.421686364668));
#52397=CARTESIAN_POINT('Ctrl Pts',(76.7624113412812,4.89469557793779,131.285129025239));
#52398=CARTESIAN_POINT('Ctrl Pts',(76.7546650080159,4.90810865710057,131.148570677775));
#52399=CARTESIAN_POINT('Ctrl Pts',(76.7469186747505,4.91580252120763,131.011451393039));
#52400=CARTESIAN_POINT('Ctrl Pts',(76.7391723414852,4.91775288156668,130.874286709568));
#52401=CARTESIAN_POINT('Ctrl Pts',(76.7314242734822,4.91970367869542,130.737091309016));
#52402=CARTESIAN_POINT('Ctrl Pts',(76.7236762054792,4.91590840709392,130.599850880349));
#52403=CARTESIAN_POINT('Ctrl Pts',(76.7159281374762,4.90639490464888,130.463080524189));
#52404=CARTESIAN_POINT('Ctrl Pts',(76.7081718347343,4.89687129114028,130.326164806867));
#52405=CARTESIAN_POINT('Ctrl Pts',(76.7004155319925,4.88161733369204,130.189720550698));
#52406=CARTESIAN_POINT('Ctrl Pts',(76.6926592292506,4.86071279814397,130.054257853633));
#52407=CARTESIAN_POINT('Ctrl Pts',(76.6848987867364,4.83979710521585,129.918722856049));
#52408=CARTESIAN_POINT('Ctrl Pts',(76.6771383442223,4.81322490049464,129.784170844829));
#52409=CARTESIAN_POINT('Ctrl Pts',(76.6693779017082,4.78112682676611,129.651100313525));
#52410=CARTESIAN_POINT('Ctrl Pts',(76.6616050014428,4.7489772263601,129.51781616559));
#52411=CARTESIAN_POINT('Ctrl Pts',(76.6538321011773,4.71128413819533,129.38601862609));
#52412=CARTESIAN_POINT('Ctrl Pts',(76.6460592009119,4.66822797035095,129.256190510849));
#52413=CARTESIAN_POINT('Ctrl Pts',(76.6385688651499,4.62673700266022,129.131081974616));
#52414=CARTESIAN_POINT('Ctrl Pts',(76.631078529388,4.58026621721277,129.007802449736));
#52415=CARTESIAN_POINT('Ctrl Pts',(76.6235881936261,4.5290180273398,128.886763482991));
#52416=CARTESIAN_POINT('Ctrl Pts',(76.615813859507,4.47582674677051,128.76113528703));
#52417=CARTESIAN_POINT('Ctrl Pts',(76.6080395253879,4.41732014587441,128.637522952274));
#52418=CARTESIAN_POINT('Ctrl Pts',(76.6002651912688,4.3536720509113,128.516408971308));
#52419=CARTESIAN_POINT('Ctrl Pts',(76.5925004383217,4.29010239653689,128.3954442525));
#52420=CARTESIAN_POINT('Ctrl Pts',(76.5847356853746,4.22140403583596,128.276972103959));
#52421=CARTESIAN_POINT('Ctrl Pts',(76.5769709324275,4.14779914891238,128.161455911985));
#52422=CARTESIAN_POINT('Ctrl Pts',(76.5692138915425,4.0742673674002,128.046054452322));
#52423=CARTESIAN_POINT('Ctrl Pts',(76.5614568506576,3.99583896634726,127.933603434245));
#52424=CARTESIAN_POINT('Ctrl Pts',(76.5536998097726,3.91278223843609,127.824542130295));
#52425=CARTESIAN_POINT('Ctrl Pts',(76.5459486185324,3.82978814424896,127.715563070323));
#52426=CARTESIAN_POINT('Ctrl Pts',(76.5381974272922,3.74217290626452,127.609968946278));
#52427=CARTESIAN_POINT('Ctrl Pts',(76.530446236052,3.65024816320902,127.508170178667));
#52428=CARTESIAN_POINT('Ctrl Pts',(76.5226983392749,3.55836249062194,127.406414678248));
#52429=CARTESIAN_POINT('Ctrl Pts',(76.5149504424979,3.46217121745989,127.308451615436));
#52430=CARTESIAN_POINT('Ctrl Pts',(76.5072025457208,3.36202616582613,127.214658245112));
#52431=CARTESIAN_POINT('Ctrl Pts',(76.4994562696367,3.2619020623783,127.12088449434));
#52432=CARTESIAN_POINT('Ctrl Pts',(76.4917099935526,3.15782611067157,127.031278968271));
#52433=CARTESIAN_POINT('Ctrl Pts',(76.4839637174685,3.05018659690714,126.946181670634));
#52434=CARTESIAN_POINT('Ctrl Pts',(76.4762173842031,2.9425462885725,126.861083744829));
#52435=CARTESIAN_POINT('Ctrl Pts',(76.4684710509378,2.8313426723869,126.780494356329));
#52436=CARTESIAN_POINT('Ctrl Pts',(76.4607247176724,2.71699635689118,126.704712601072));
#52437=CARTESIAN_POINT('Ctrl Pts',(76.4529766496694,2.60262443433084,126.628913875017));
#52438=CARTESIAN_POINT('Ctrl Pts',(76.4452285816665,2.48510873783818,126.557925140525));
#52439=CARTESIAN_POINT('Ctrl Pts',(76.4374805136635,2.36489768321145,126.492001401262));
#52440=CARTESIAN_POINT('Ctrl Pts',(76.4297242109216,2.24455886684518,126.426007597465));
#52441=CARTESIAN_POINT('Ctrl Pts',(76.4219679081798,2.12151931322841,126.365089730585));
#52442=CARTESIAN_POINT('Ctrl Pts',(76.4142116054379,1.99625129759965,126.309456411765));
#52443=CARTESIAN_POINT('Ctrl Pts',(76.4064511629237,1.87091642265929,126.253793399767));
#52444=CARTESIAN_POINT('Ctrl Pts',(76.3986907204095,1.7433510791951,126.203420699483));
#52445=CARTESIAN_POINT('Ctrl Pts',(76.3909302778954,1.61404527956611,126.158497845377));
#52446=CARTESIAN_POINT('Ctrl Pts',(76.3831573776299,1.48453190678832,126.113502877118));
#52447=CARTESIAN_POINT('Ctrl Pts',(76.3753844773645,1.35327286924824,126.07397535028));
#52448=CARTESIAN_POINT('Ctrl Pts',(76.3676115770991,1.22077188854755,126.040024456186));
#52449=CARTESIAN_POINT('Ctrl Pts',(76.3601212413371,1.09308765224506,126.007307762609));
#52450=CARTESIAN_POINT('Ctrl Pts',(76.352630905575,0.964250501858037,125.97976935606));
#52451=CARTESIAN_POINT('Ctrl Pts',(76.345140569813,0.834716092698463,125.957461391557));
#52452=CARTESIAN_POINT('Ctrl Pts',(76.3373662356939,0.700270347044384,125.934307613799));
#52453=CARTESIAN_POINT('Ctrl Pts',(76.3295919015748,0.564647542042625,125.916715387791));
#52454=CARTESIAN_POINT('Ctrl Pts',(76.3218175674557,0.428347569711353,125.904799267606));
#52455=CARTESIAN_POINT('Ctrl Pts',(76.3140528145086,0.292215574914962,125.892897832974));
#52456=CARTESIAN_POINT('Ctrl Pts',(76.3062880615616,0.155408459031892,125.886658619341));
#52457=CARTESIAN_POINT('Ctrl Pts',(76.2985233086145,0.0184361758547634,
125.886145171907));
#52458=CARTESIAN_POINT('Ctrl Pts',(76.2907662677295,-0.118400064520302,
125.885632234436));
#52459=CARTESIAN_POINT('Ctrl Pts',(76.2830092268444,-0.255400757296971,
125.89083374741));
#52460=CARTESIAN_POINT('Ctrl Pts',(76.2752521859594,-0.392051311295803,
125.901761426136));
#52461=CARTESIAN_POINT('Ctrl Pts',(76.2675009947193,-0.528598816048227,
125.912680864214));
#52462=CARTESIAN_POINT('Ctrl Pts',(76.2597498034792,-0.664796319438987,
125.929317841996));
#52463=CARTESIAN_POINT('Ctrl Pts',(76.2519986122391,-0.800130074728278,
125.951632011306));
#52464=CARTESIAN_POINT('Ctrl Pts',(76.244250715462,-0.935406309561701,125.973936696498));
#52465=CARTESIAN_POINT('Ctrl Pts',(76.2365028186849,-1.06981914151023,126.001913710557));
#52466=CARTESIAN_POINT('Ctrl Pts',(76.2287549219078,-1.20286100691642,126.035470971061));
#52467=CARTESIAN_POINT('Ctrl Pts',(76.2210086458237,-1.33587504283241,126.06902121211));
#52468=CARTESIAN_POINT('Ctrl Pts',(76.2132623697396,-1.46751830376856,126.108149282288));
#52469=CARTESIAN_POINT('Ctrl Pts',(76.2055160936555,-1.59729485678162,126.152712285738));
#52470=CARTESIAN_POINT('Ctrl Pts',(76.1977697603901,-1.72707236777616,126.197275618142));
#52471=CARTESIAN_POINT('Ctrl Pts',(76.1900234271248,-1.85498277357909,126.2472738369));
#52472=CARTESIAN_POINT('Ctrl Pts',(76.1822770938594,-1.98054708711762,126.302514740794));
#52473=CARTESIAN_POINT('Ctrl Pts',(76.1745290258565,-2.10613951991306,126.357768015505));
#52474=CARTESIAN_POINT('Ctrl Pts',(76.1667809578535,-2.22938445718106,126.418266154193));
#52475=CARTESIAN_POINT('Ctrl Pts',(76.1590328898505,-2.34982497742408,126.483769727656));
#52476=CARTESIAN_POINT('Ctrl Pts',(76.1512765871086,-2.47039350328543,126.549342919096));
#52477=CARTESIAN_POINT('Ctrl Pts',(76.1435202843668,-2.58815131411329,126.619931985165));
#52478=CARTESIAN_POINT('Ctrl Pts',(76.1357639816249,-2.70266762314266,126.695252346747));
#52479=CARTESIAN_POINT('Ctrl Pts',(76.1280035391108,-2.81724505297434,126.770612909073));
#52480=CARTESIAN_POINT('Ctrl Pts',(76.1202430965966,-2.92857721645162,126.850709570443));
#52481=CARTESIAN_POINT('Ctrl Pts',(76.1124826540824,-3.03626502906172,126.935216301855));
#52482=CARTESIAN_POINT('Ctrl Pts',(76.1047097538169,-3.14412571170862,127.019858690975));
#52483=CARTESIAN_POINT('Ctrl Pts',(76.0969368535515,-3.24833005548526,127.108925042938));
#52484=CARTESIAN_POINT('Ctrl Pts',(76.089163953286,-3.34851392081119,127.20205058307));
#52485=CARTESIAN_POINT('Ctrl Pts',(76.0816736175241,-3.44505585028365,127.291790775248));
#52486=CARTESIAN_POINT('Ctrl Pts',(76.0741832817621,-3.5378643184477,127.385299937322));
#52487=CARTESIAN_POINT('Ctrl Pts',(76.0666929460002,-3.62664915298228,127.482222904636));
#52488=CARTESIAN_POINT('Ctrl Pts',(76.0590029828683,-3.71780022096293,127.581728997414));
#52489=CARTESIAN_POINT('Ctrl Pts',(76.0513130197365,-3.80501329057441,127.685164594423));
#52490=CARTESIAN_POINT('Ctrl Pts',(76.0436230566047,-3.88792480186614,127.792181373641));
#52491=CARTESIAN_POINT('Ctrl Pts',(76.035942259654,-3.9707374853851,127.899070592405));
#52492=CARTESIAN_POINT('Ctrl Pts',(76.0282614627032,-4.04925856324953,128.009532192583));
#52493=CARTESIAN_POINT('Ctrl Pts',(76.0205806657525,-4.12316150282434,128.123181346401));
#52494=CARTESIAN_POINT('Ctrl Pts',(76.0129084811636,-4.19698157614698,128.236703067135));
#52495=CARTESIAN_POINT('Ctrl Pts',(76.0052362965747,-4.26619360138958,128.353404894275));
#52496=CARTESIAN_POINT('Ctrl Pts',(75.9975641119859,-4.33051198459884,128.472869889781));
#52497=CARTESIAN_POINT('Ctrl Pts',(75.9898969959661,-4.39478787636778,128.592255961666));
#52498=CARTESIAN_POINT('Ctrl Pts',(75.9822298799464,-4.45417636577332,128.714401221262));
#52499=CARTESIAN_POINT('Ctrl Pts',(75.9745627639267,-4.50843587467326,128.83886092882));
#52500=CARTESIAN_POINT('Ctrl Pts',(75.9668982869073,-4.56267670759917,128.963277797689));
#52501=CARTESIAN_POINT('Ctrl Pts',(75.9592338098879,-4.61179190649494,129.09000716624));
#52502=CARTESIAN_POINT('Ctrl Pts',(75.9515693328685,-4.6555866404337,129.218581283637));
#52503=CARTESIAN_POINT('Ctrl Pts',(75.9444259887391,-4.69640362700555,129.338413225775));
#52504=CARTESIAN_POINT('Ctrl Pts',(75.9372826446096,-4.73259941719584,129.459847118768));
#52505=CARTESIAN_POINT('Ctrl Pts',(75.9301393004801,-4.76405452823408,129.582490119308));
#52506=CARTESIAN_POINT('Origin',(213.235140564004,0.,130.804360617566));
#52507=CARTESIAN_POINT('',(73.8346539883595,-4.76405452823405,129.582490119308));
#52508=CARTESIAN_POINT('',(74.1802344108983,-4.76405452823402,129.582490119308));
#52509=CARTESIAN_POINT('',(213.235140564004,-4.76405452823405,129.582490119308));
#52510=CARTESIAN_POINT('',(75.5148594359626,-4.91824975138238,130.802796799436));
#52511=CARTESIAN_POINT('Ctrl Pts',(75.5148594359626,-4.91824975138238,130.802796799436));
#52512=CARTESIAN_POINT('Ctrl Pts',(75.5071480679706,-4.91829279726256,130.93817724134));
#52513=CARTESIAN_POINT('Ctrl Pts',(75.4994366999785,-4.91274186277529,131.073785176132));
#52514=CARTESIAN_POINT('Ctrl Pts',(75.4917253319864,-4.9015667560916,131.209115355744));
#52515=CARTESIAN_POINT('Ctrl Pts',(75.484023229282,-4.89040507641316,131.344282934758));
#52516=CARTESIAN_POINT('Ctrl Pts',(75.4763211265776,-4.87363269840611,131.479173029789));
#52517=CARTESIAN_POINT('Ctrl Pts',(75.4686190238732,-4.85127141023658,131.61327888706));
#52518=CARTESIAN_POINT('Ctrl Pts',(75.4609242586911,-4.82893142487945,131.7472569864));
#52519=CARTESIAN_POINT('Ctrl Pts',(75.453229493509,-4.80101318715482,131.880451944431));
#52520=CARTESIAN_POINT('Ctrl Pts',(75.4455347283269,-4.76759037113984,132.012361079286));
#52521=CARTESIAN_POINT('Ctrl Pts',(75.4378453800766,-4.73419108399346,132.144177353242));
#52522=CARTESIAN_POINT('Ctrl Pts',(75.4301560318263,-4.69529502713937,132.274709221102));
#52523=CARTESIAN_POINT('Ctrl Pts',(75.4224666835761,-4.65102705737138,132.403463608026));
#52524=CARTESIAN_POINT('Ctrl Pts',(75.4147800166523,-4.60677452413606,132.532173097448));
#52525=CARTESIAN_POINT('Ctrl Pts',(75.4070933497284,-4.55715393016955,132.659105962261));
#52526=CARTESIAN_POINT('Ctrl Pts',(75.3994066828046,-4.50234006970444,132.783784008161));
#52527=CARTESIAN_POINT('Ctrl Pts',(75.3917211385253,-4.44753421485211,132.908443844722));
#52528=CARTESIAN_POINT('Ctrl Pts',(75.3840355942459,-4.38753676183005,133.030849153161));
#52529=CARTESIAN_POINT('Ctrl Pts',(75.3763500499666,-4.32257055738247,133.150541948783));
#52530=CARTESIAN_POINT('Ctrl Pts',(75.3686638977918,-4.25759921437067,133.270244211621));
#52531=CARTESIAN_POINT('Ctrl Pts',(75.3609777456169,-4.18765852810816,133.387233185288));
#52532=CARTESIAN_POINT('Ctrl Pts',(75.3532915934421,-4.11301694566277,133.501076150801));
#52533=CARTESIAN_POINT('Ctrl Pts',(75.3456031026954,-4.03835265293261,133.614953753926));
#52534=CARTESIAN_POINT('Ctrl Pts',(75.3379146119487,-3.95898483720637,133.725683112525));
#52535=CARTESIAN_POINT('Ctrl Pts',(75.330226121202,-3.87522454920135,133.832861526558));
#52536=CARTESIAN_POINT('Ctrl Pts',(75.3225292817413,-3.79137330827571,133.940156322591));
#52537=CARTESIAN_POINT('Ctrl Pts',(75.3148324422806,-3.70312031831821,134.043892162812));
#52538=CARTESIAN_POINT('Ctrl Pts',(75.3071356028199,-3.61081632476517,134.14370015276));
#52539=CARTESIAN_POINT('Ctrl Pts',(75.2994339805125,-3.51845497314282,134.243570163791));
#52540=CARTESIAN_POINT('Ctrl Pts',(75.2917323582051,-3.42203788672323,134.339507184623));
#52541=CARTESIAN_POINT('Ctrl Pts',(75.2840307358977,-3.32195086392682,134.431180921931));
#52542=CARTESIAN_POINT('Ctrl Pts',(75.2763179510522,-3.22171877751165,134.522987528853));
#52543=CARTESIAN_POINT('Ctrl Pts',(75.2686051662068,-3.11780643955999,134.610518261872));
#52544=CARTESIAN_POINT('Ctrl Pts',(75.2608923813613,-3.01063104336579,134.693484398474));
#52545=CARTESIAN_POINT('Ctrl Pts',(75.2575746111478,-2.96452793738835,134.72917352792));
#52546=CARTESIAN_POINT('Ctrl Pts',(75.2542568409344,-2.91782137235664,134.764018575186));
#52547=CARTESIAN_POINT('Ctrl Pts',(75.2509390707209,-2.87054600307479,134.79799914737));
#52548=CARTESIAN_POINT('Ctrl Pts',(75.2431647366018,-2.75976843478319,134.877623806316));
#52549=CARTESIAN_POINT('Ctrl Pts',(75.2353904024827,-2.64549988832472,134.952761885495));
#52550=CARTESIAN_POINT('Ctrl Pts',(75.2276160683636,-2.52813980386932,135.023091729475));
#52551=CARTESIAN_POINT('Ctrl Pts',(75.2198513154165,-2.41092435522924,135.093334898209));
#52552=CARTESIAN_POINT('Ctrl Pts',(75.2120865624694,-2.29062528158387,135.158781423122));
#52553=CARTESIAN_POINT('Ctrl Pts',(75.2043218095223,-2.16767338135606,135.219151119307));
#52554=CARTESIAN_POINT('Ctrl Pts',(75.1965647686373,-2.0448435986892,135.279460855458));
#52555=CARTESIAN_POINT('Ctrl Pts',(75.1888077277524,-1.91936658153298,135.334703626243));
#52556=CARTESIAN_POINT('Ctrl Pts',(75.1810506868674,-1.79169996761107,135.384643828085));
#52557=CARTESIAN_POINT('Ctrl Pts',(75.1732994956272,-1.66412962807539,135.434546369633));
#52558=CARTESIAN_POINT('Ctrl Pts',(75.1655483043871,-1.53437334099751,135.479154159575));
#52559=CARTESIAN_POINT('Ctrl Pts',(75.157797113147,-1.40291075586978,135.518278783335));
#52560=CARTESIAN_POINT('Ctrl Pts',(75.1500492163699,-1.27150404584779,135.557386778086));
#52561=CARTESIAN_POINT('Ctrl Pts',(75.1423013195928,-1.13839285412539,135.591016130537));
#52562=CARTESIAN_POINT('Ctrl Pts',(75.1345534228157,-1.00407389702651,135.619027654009));
#52563=CARTESIAN_POINT('Ctrl Pts',(75.1268071467316,-0.86978303655796,135.647033318074));
#52564=CARTESIAN_POINT('Ctrl Pts',(75.1190608706475,-0.734285295713348,
135.669423410787));
#52565=CARTESIAN_POINT('Ctrl Pts',(75.1113145945635,-0.59808915596445,135.686109527948));
#52566=CARTESIAN_POINT('Ctrl Pts',(75.1035682612981,-0.461892010846495,
135.702795768282));
#52567=CARTESIAN_POINT('Ctrl Pts',(75.0958219280327,-0.324996844600614,
135.713777901501));
#52568=CARTESIAN_POINT('Ctrl Pts',(75.0880755947673,-0.187918464440154,
135.719019274403));
#52569=CARTESIAN_POINT('Ctrl Pts',(75.0803275267644,-0.0508093865270786,
135.724261821074));
#52570=CARTESIAN_POINT('Ctrl Pts',(75.0725794587615,0.0864825963395565,
135.723761034292));
#52571=CARTESIAN_POINT('Ctrl Pts',(75.0648313907585,0.223441863842868,135.717532382931));
#52572=CARTESIAN_POINT('Ctrl Pts',(75.0570750880166,0.360546693285705,135.711297111686));
#52573=CARTESIAN_POINT('Ctrl Pts',(75.0493187852747,0.497317709799175,135.69932183293));
#52574=CARTESIAN_POINT('Ctrl Pts',(75.0415624825329,0.633243048166705,135.68167404859));
#52575=CARTESIAN_POINT('Ctrl Pts',(75.0338020400187,0.769240933980048,135.664016845096));
#52576=CARTESIAN_POINT('Ctrl Pts',(75.0260415975046,0.904391857190708,135.640681169782));
#52577=CARTESIAN_POINT('Ctrl Pts',(75.0182811549904,1.03819433273526,135.611785665341));
#52578=CARTESIAN_POINT('Ctrl Pts',(75.010508254725,1.17221159989199,135.582843775272));
#52579=CARTESIAN_POINT('Ctrl Pts',(75.0027353544596,1.30487571514227,135.548324319327));
#52580=CARTESIAN_POINT('Ctrl Pts',(74.9949624541941,1.435699672403,135.508396067386));
#52581=CARTESIAN_POINT('Ctrl Pts',(74.9874721184321,1.56176784929163,135.469919307976));
#52582=CARTESIAN_POINT('Ctrl Pts',(74.97998178267,1.68612704343233,135.426420273644));
#52583=CARTESIAN_POINT('Ctrl Pts',(74.972491446908,1.80836096919779,135.378091443444));
#52584=CARTESIAN_POINT('Ctrl Pts',(74.9647171127889,1.93522943141076,135.327930210957));
#52585=CARTESIAN_POINT('Ctrl Pts',(74.9569427786698,2.0602101659701,135.272406813714));
#52586=CARTESIAN_POINT('Ctrl Pts',(74.9491684445508,2.18281664788325,135.211683449425));
#52587=CARTESIAN_POINT('Ctrl Pts',(74.9414036916037,2.3052720282651,135.151034921255));
#52588=CARTESIAN_POINT('Ctrl Pts',(74.9336389386566,2.4253586309896,135.085199348886));
#52589=CARTESIAN_POINT('Ctrl Pts',(74.9258741857095,2.54260787148895,135.014387728446));
#52590=CARTESIAN_POINT('Ctrl Pts',(74.9181171448245,2.65974065839003,134.943646439105));
#52591=CARTESIAN_POINT('Ctrl Pts',(74.9103601039395,2.77404135872734,134.867939137866));
#52592=CARTESIAN_POINT('Ctrl Pts',(74.9026030630545,2.88506438817311,134.787523498819));
#52593=CARTESIAN_POINT('Ctrl Pts',(74.8948518718144,2.99600369428821,134.707168501833));
#52594=CARTESIAN_POINT('Ctrl Pts',(74.8871006805742,3.10366993396344,134.622112462695));
#52595=CARTESIAN_POINT('Ctrl Pts',(74.8793494893341,3.20764532641281,134.532657081427));
#52596=CARTESIAN_POINT('Ctrl Pts',(74.871601592557,3.31157652654705,134.443239721083));
#52597=CARTESIAN_POINT('Ctrl Pts',(74.8638536957799,3.41181970374504,134.349426992025));
#52598=CARTESIAN_POINT('Ctrl Pts',(74.8561057990028,3.50798926900413,134.251561561963));
#52599=CARTESIAN_POINT('Ctrl Pts',(74.8483595229187,3.60413871766346,134.153716603239));
#52600=CARTESIAN_POINT('Ctrl Pts',(74.8406132468346,3.69621597542709,134.051820908391));
#52601=CARTESIAN_POINT('Ctrl Pts',(74.8328669707504,3.78387181867998,133.946254492651));
#52602=CARTESIAN_POINT('Ctrl Pts',(74.8251206374851,3.87152830898816,133.840687297645));
#52603=CARTESIAN_POINT('Ctrl Pts',(74.8173743042198,3.95476306990133,133.731449628468));
#52604=CARTESIAN_POINT('Ctrl Pts',(74.8096279709545,4.03326699816961,133.618954795059));
#52605=CARTESIAN_POINT('Ctrl Pts',(74.8018799029515,4.11178850684843,133.506434769212));
#52606=CARTESIAN_POINT('Ctrl Pts',(74.7941318349485,4.18557685102805,133.390656448226));
#52607=CARTESIAN_POINT('Ctrl Pts',(74.7863837669455,4.25436633973549,133.272061999384));
#52608=CARTESIAN_POINT('Ctrl Pts',(74.7786274642037,4.32322893873014,133.15334150695));
#52609=CARTESIAN_POINT('Ctrl Pts',(74.7708711614618,4.38708187279911,133.031799246521));
#52610=CARTESIAN_POINT('Ctrl Pts',(74.7631148587199,4.44570525757098,132.907902351239));
#52611=CARTESIAN_POINT('Ctrl Pts',(74.7553544162057,4.50435993140837,132.783939328455));
#52612=CARTESIAN_POINT('Ctrl Pts',(74.7475939736916,4.55777934210613,132.657619526572));
#52613=CARTESIAN_POINT('Ctrl Pts',(74.7398335311775,4.60579224219589,132.529428988451));
#52614=CARTESIAN_POINT('Ctrl Pts',(74.732060630912,4.65388221685529,132.401032667498));
#52615=CARTESIAN_POINT('Ctrl Pts',(74.7242877306466,4.69654821572148,132.270759980973));
#52616=CARTESIAN_POINT('Ctrl Pts',(74.7165148303811,4.73366899098852,132.139111885126));
#52617=CARTESIAN_POINT('Ctrl Pts',(74.709024494619,4.76944033257327,132.012249529164));
#52618=CARTESIAN_POINT('Ctrl Pts',(74.701534158857,4.80006254510861,131.884110326518));
#52619=CARTESIAN_POINT('Ctrl Pts',(74.6940438230949,4.82547255412337,131.755148549705));
#52620=CARTESIAN_POINT('Ctrl Pts',(74.6862694889758,4.85184599135294,131.621297147929));
#52621=CARTESIAN_POINT('Ctrl Pts',(74.6784951548567,4.87268772460145,131.486135563861));
#52622=CARTESIAN_POINT('Ctrl Pts',(74.6707208207376,4.8878712367538,131.350160796583));
#52623=CARTESIAN_POINT('Ctrl Pts',(74.6629560677905,4.90303603658441,131.214353606053));
#52624=CARTESIAN_POINT('Ctrl Pts',(74.6551913148435,4.91255644704091,131.077735611162));
#52625=CARTESIAN_POINT('Ctrl Pts',(74.6474265618964,4.91635670373674,130.940815093941));
#52626=CARTESIAN_POINT('Ctrl Pts',(74.6396695210114,4.92015318596405,130.804030568107));
#52627=CARTESIAN_POINT('Ctrl Pts',(74.6319124801263,4.91824080977142,130.666944506176));
#52628=CARTESIAN_POINT('Ctrl Pts',(74.6241554392413,4.91059551445619,130.530071070002));
#52629=CARTESIAN_POINT('Ctrl Pts',(74.6164042480012,4.90295598451768,130.393300851152));
#52630=CARTESIAN_POINT('Ctrl Pts',(74.6086530567611,4.88959216231733,130.256743327684));
#52631=CARTESIAN_POINT('Ctrl Pts',(74.600901865521,4.87053205590813,130.120913066637));
#52632=CARTESIAN_POINT('Ctrl Pts',(74.5931539687439,4.85148005055249,129.985140537073));
#52633=CARTESIAN_POINT('Ctrl Pts',(74.5854060719669,4.82673663053243,129.850095041502));
#52634=CARTESIAN_POINT('Ctrl Pts',(74.5776581751898,4.79638167162292,129.716286207142));
#52635=CARTESIAN_POINT('Ctrl Pts',(74.5699118991057,4.76603306231643,129.582505362705));
#52636=CARTESIAN_POINT('Ctrl Pts',(74.5621656230216,4.73007533533806,129.449961045979));
#52637=CARTESIAN_POINT('Ctrl Pts',(74.5544193469375,4.68863944437119,129.319152476198));
#52638=CARTESIAN_POINT('Ctrl Pts',(74.5466730136721,4.64720324753399,129.188342940817));
#52639=CARTESIAN_POINT('Ctrl Pts',(74.5389266804068,4.60028892407935,129.059269550661));
#52640=CARTESIAN_POINT('Ctrl Pts',(74.5311803471414,4.54807712550698,128.932415767166));
#52641=CARTESIAN_POINT('Ctrl Pts',(74.5234322791384,4.49585363446423,128.805533575644));
#52642=CARTESIAN_POINT('Ctrl Pts',(74.5156842111354,4.43833045641633,128.680872341356));
#52643=CARTESIAN_POINT('Ctrl Pts',(74.5079361431324,4.37573598675864,128.558894599857));
#52644=CARTESIAN_POINT('Ctrl Pts',(74.5001798403906,4.31307499095384,128.436787218963));
#52645=CARTESIAN_POINT('Ctrl Pts',(74.4924235376487,4.24533211555801,128.317369376525));
#52646=CARTESIAN_POINT('Ctrl Pts',(74.4846672349069,4.17278152004028,128.201078564367));
#52647=CARTESIAN_POINT('Ctrl Pts',(74.4769067923927,4.10019220208532,128.0847256843));
#52648=CARTESIAN_POINT('Ctrl Pts',(74.4691463498785,4.02279027152226,127.971503482714));
#52649=CARTESIAN_POINT('Ctrl Pts',(74.4613859073644,3.94089208653534,127.86181875299));
#52650=CARTESIAN_POINT('Ctrl Pts',(74.4536130070989,3.8588624313112,127.751957947601));
#52651=CARTESIAN_POINT('Ctrl Pts',(74.4458401068335,3.77232234518507,127.645646265236));
#52652=CARTESIAN_POINT('Ctrl Pts',(74.4380672065681,3.68162775943859,127.543256494201));
#52653=CARTESIAN_POINT('Ctrl Pts',(74.4305768708061,3.59423015033061,127.444588849247));
#52654=CARTESIAN_POINT('Ctrl Pts',(74.4230865350441,3.50297506391935,127.349563145572));
#52655=CARTESIAN_POINT('Ctrl Pts',(74.4155961992822,3.40821059924742,127.258477994907));
#52656=CARTESIAN_POINT('Ctrl Pts',(74.4078218651631,3.30985311109372,127.163939323068));
#52657=CARTESIAN_POINT('Ctrl Pts',(74.400047531044,3.20740330835137,127.073346444924));
#52658=CARTESIAN_POINT('Ctrl Pts',(74.3922731969249,3.10121094483079,126.987074443049));
#52659=CARTESIAN_POINT('Ctrl Pts',(74.3845084439778,2.99514945390779,126.900908763705));
#52660=CARTESIAN_POINT('Ctrl Pts',(74.3767436910308,2.88535487998499,126.819053609438));
#52661=CARTESIAN_POINT('Ctrl Pts',(74.3689789380837,2.77221390262702,126.741847461823));
#52662=CARTESIAN_POINT('Ctrl Pts',(74.3612218971987,2.65918529848254,126.664717996443));
#52663=CARTESIAN_POINT('Ctrl Pts',(74.3534648563137,2.54281722605666,126.592228567708));
#52664=CARTESIAN_POINT('Ctrl Pts',(74.3457078154287,2.42352925888212,126.524677335611));
#52665=CARTESIAN_POINT('Ctrl Pts',(74.3379566241886,2.30433124769205,126.457177044424));
#52666=CARTESIAN_POINT('Ctrl Pts',(74.3302054329485,2.18221806335954,126.394607729487));
#52667=CARTESIAN_POINT('Ctrl Pts',(74.3224542417084,2.05763776474414,126.337223962885));
#52668=CARTESIAN_POINT('Ctrl Pts',(74.3147063449313,1.93311041607842,126.279864585913));
#52669=CARTESIAN_POINT('Ctrl Pts',(74.3069584481542,1.80611839305563,126.227686536921));
#52670=CARTESIAN_POINT('Ctrl Pts',(74.2992105513771,1.67713363429334,126.180898080114));
#52671=CARTESIAN_POINT('Ctrl Pts',(74.291464275293,1.54817585636173,126.134119410444));
#52672=CARTESIAN_POINT('Ctrl Pts',(74.2837179992089,1.41722653910186,126.092728223761));
#52673=CARTESIAN_POINT('Ctrl Pts',(74.2759717231248,1.28477647345796,126.056884185213));
#52674=CARTESIAN_POINT('Ctrl Pts',(74.2682253898594,1.15232543009793,126.021039882072));
#52675=CARTESIAN_POINT('Ctrl Pts',(74.260479056594,1.01837399363812,125.990742910905));
#52676=CARTESIAN_POINT('Ctrl Pts',(74.2527327233287,0.883426560424877,125.966102607204));
#52677=CARTESIAN_POINT('Ctrl Pts',(74.2449846553257,0.748448906669721,125.941456785477));
#52678=CARTESIAN_POINT('Ctrl Pts',(74.2372365873228,0.612475196857113,125.922470222157));
#52679=CARTESIAN_POINT('Ctrl Pts',(74.2294885193198,0.476018028540152,125.909200773495));
#52680=CARTESIAN_POINT('Ctrl Pts',(74.2217322165779,0.339415831920844,125.895917221905));
#52681=CARTESIAN_POINT('Ctrl Pts',(74.2139759138361,0.202329540125689,125.888362960773));
#52682=CARTESIAN_POINT('Ctrl Pts',(74.2062196110942,0.0652754173056658,
125.886543806989));
#52683=CARTESIAN_POINT('Ctrl Pts',(74.1984591685801,-0.0718518554262336,
125.884723682268));
#52684=CARTESIAN_POINT('Ctrl Pts',(74.1906987260658,-0.20894653435704,125.888644753023));
#52685=CARTESIAN_POINT('Ctrl Pts',(74.1829382835517,-0.34549537336629,125.898260739915));
#52686=CARTESIAN_POINT('Ctrl Pts',(74.1751653832863,-0.482263412694153,
125.907892163244));
#52687=CARTESIAN_POINT('Ctrl Pts',(74.1673924830209,-0.618483472380627,
125.923236727519));
#52688=CARTESIAN_POINT('Ctrl Pts',(74.1596195827555,-0.753649525516159,
125.944196478857));
#52689=CARTESIAN_POINT('Ctrl Pts',(74.1521292469934,-0.883901952158292,
125.96439429044));
#52690=CARTESIAN_POINT('Ctrl Pts',(74.1446389112313,-1.01317537116423,125.989806065149));
#52691=CARTESIAN_POINT('Ctrl Pts',(74.1371485754692,-1.14103039599215,126.020300344333));
#52692=CARTESIAN_POINT('Ctrl Pts',(74.1293742413502,-1.27373308294637,126.051950823382));
#52693=CARTESIAN_POINT('Ctrl Pts',(74.1215999072311,-1.40532805791054,126.089177080467));
#52694=CARTESIAN_POINT('Ctrl Pts',(74.113825573112,-1.53531070281407,126.131887599097));
#52695=CARTESIAN_POINT('Ctrl Pts',(74.1060608201649,-1.66513315572456,126.174545480829));
#52696=CARTESIAN_POINT('Ctrl Pts',(74.0982960672179,-1.79334686435497,126.222674055109));
#52697=CARTESIAN_POINT('Ctrl Pts',(74.0905313142708,-1.91945804481905,126.276130955029));
#52698=CARTESIAN_POINT('Ctrl Pts',(74.0827742733858,-2.04544396988066,126.329534760802));
#52699=CARTESIAN_POINT('Ctrl Pts',(74.0750172325008,-2.16933116487668,126.388256208965));
#52700=CARTESIAN_POINT('Ctrl Pts',(74.0672601916158,-2.2906419896182,126.452103463181));
#52701=CARTESIAN_POINT('Ctrl Pts',(74.0595090003757,-2.41186133292386,126.515902569686));
#52702=CARTESIAN_POINT('Ctrl Pts',(74.0517578091355,-2.53050782854871,126.584819607026));
#52703=CARTESIAN_POINT('Ctrl Pts',(74.0440066178953,-2.6461251110297,126.658615213024));
#52704=CARTESIAN_POINT('Ctrl Pts',(74.0362587211182,-2.76169325308097,126.732379453921));
#52705=CARTESIAN_POINT('Ctrl Pts',(74.0285108243412,-2.87423441385383,126.811017929491));
#52706=CARTESIAN_POINT('Ctrl Pts',(74.0207629275641,-2.9833182804222,126.8942461563));
#52707=CARTESIAN_POINT('Ctrl Pts',(74.01301665148,-3.09237932899719,126.977456973559));
#52708=CARTESIAN_POINT('Ctrl Pts',(74.0052703753959,-3.19798421120625,127.065255395409));
#52709=CARTESIAN_POINT('Ctrl Pts',(73.9975240993118,-3.29973331174558,127.157314808441));
#52710=CARTESIAN_POINT('Ctrl Pts',(73.9897777660465,-3.40148316337352,127.249374901035));
#52711=CARTESIAN_POINT('Ctrl Pts',(73.9820314327811,-3.49937688662317,127.345695785269));
#52712=CARTESIAN_POINT('Ctrl Pts',(73.9742850995158,-3.59304985590273,127.445912196718));
#52713=CARTESIAN_POINT('Ctrl Pts',(73.9665370315129,-3.68674380259395,127.546151050936));
#52714=CARTESIAN_POINT('Ctrl Pts',(73.95878896351,-3.77621484753823,127.65028688273));
#52715=CARTESIAN_POINT('Ctrl Pts',(73.951040895507,-3.86113724313427,127.757919701976));
#52716=CARTESIAN_POINT('Ctrl Pts',(73.9432845927652,-3.94614989526328,127.865666914664));
#52717=CARTESIAN_POINT('Ctrl Pts',(73.9355282900234,-4.02660399833575,127.976918231771));
#52718=CARTESIAN_POINT('Ctrl Pts',(73.9277719872815,-4.10221560505266,128.091242449818));
#52719=CARTESIAN_POINT('Ctrl Pts',(73.9200115447674,-4.17786756796064,128.205627686143));
#52720=CARTESIAN_POINT('Ctrl Pts',(73.9122511022532,-4.24867168276926,128.323088756771));
#52721=CARTESIAN_POINT('Ctrl Pts',(73.9044906597391,-4.31438946353308,128.443168838092));
#52722=CARTESIAN_POINT('Ctrl Pts',(73.8967177594737,-4.38021274031282,128.56344168262));
#52723=CARTESIAN_POINT('Ctrl Pts',(73.8889448592082,-4.44093319342798,128.68634158859));
#52724=CARTESIAN_POINT('Ctrl Pts',(73.8811719589428,-4.49635971435013,128.811389874763));
#52725=CARTESIAN_POINT('Ctrl Pts',(73.8736816231807,-4.54977134162642,128.931892340758));
#52726=CARTESIAN_POINT('Ctrl Pts',(73.8661912874185,-4.59826713651736,129.054389414328));
#52727=CARTESIAN_POINT('Ctrl Pts',(73.8587009516564,-4.64172019974865,129.178440370523));
#52728=CARTESIAN_POINT('Ctrl Pts',(73.8506852972241,-4.68822075058504,129.311191375075));
#52729=CARTESIAN_POINT('Ctrl Pts',(73.8426696427918,-4.72905423412978,129.446024503799));
#52730=CARTESIAN_POINT('Ctrl Pts',(73.8346539883595,-4.76405452823405,129.582490119308));
#52731=CARTESIAN_POINT('Ctrl Pts',(75.5849534216701,-4.76405452823408,129.582490119308));
#52732=CARTESIAN_POINT('Ctrl Pts',(75.5771898855308,-4.79810426152783,129.715249512644));
#52733=CARTESIAN_POINT('Ctrl Pts',(75.5694263493916,-4.82656819574603,129.849307539283));
#52734=CARTESIAN_POINT('Ctrl Pts',(75.5616628132524,-4.84937572042938,129.98415443336));
#52735=CARTESIAN_POINT('Ctrl Pts',(75.5538880904119,-4.87221610912731,130.119195632182));
#52736=CARTESIAN_POINT('Ctrl Pts',(75.5461133675714,-4.88938376665781,130.255027581356));
#52737=CARTESIAN_POINT('Ctrl Pts',(75.5383386447309,-4.90086001478842,130.391136492002));
#52738=CARTESIAN_POINT('Ctrl Pts',(75.5353546613319,-4.90526466491014,130.443375875729));
#52739=CARTESIAN_POINT('Ctrl Pts',(75.5323706779328,-4.90883147788219,130.495656069877));
#52740=CARTESIAN_POINT('Ctrl Pts',(75.5293866945337,-4.91156143249047,130.547948142495));
#52741=CARTESIAN_POINT('Ctrl Pts',(75.5245442750195,-4.91599161312486,130.632807915159));
#52742=CARTESIAN_POINT('Ctrl Pts',(75.5197018555053,-4.91822272034478,130.717783492037));
#52743=CARTESIAN_POINT('Ctrl Pts',(75.5148594359911,-4.91824975138222,130.802796798936));
#52744=CARTESIAN_POINT('',(75.8601405639734,-4.91824791822853,130.808885807146));
#52745=CARTESIAN_POINT('Ctrl Pts',(75.9301393004801,-4.76405452823408,129.582490119308));
#52746=CARTESIAN_POINT('Ctrl Pts',(75.9224754798333,-4.79780151354726,129.714069102862));
#52747=CARTESIAN_POINT('Ctrl Pts',(75.9148116591865,-4.82609118446505,129.847039594704));
#52748=CARTESIAN_POINT('Ctrl Pts',(75.9071478385396,-4.84882489549495,129.98090436777));
#52749=CARTESIAN_POINT('Ctrl Pts',(75.8993132927844,-4.87206503999421,130.117751214522));
#52750=CARTESIAN_POINT('Ctrl Pts',(75.8914787470293,-4.88949867655914,130.255532226787));
#52751=CARTESIAN_POINT('Ctrl Pts',(75.8836442012741,-4.90107623634819,130.393708954958));
#52752=CARTESIAN_POINT('Ctrl Pts',(75.8758096555189,-4.91265379613726,130.531885683128));
#52753=CARTESIAN_POINT('Ctrl Pts',(75.8679751097637,-4.91837528338702,130.670457681576));
#52754=CARTESIAN_POINT('Ctrl Pts',(75.8601405640085,-4.9182479182291,130.808885806526));
#52755=CARTESIAN_POINT('Ctrl Pts',(75.8601405639734,-4.91824791822853,130.808885807146));
#52756=CARTESIAN_POINT('Ctrl Pts',(75.8503022766471,-4.91808797849113,130.982717923244));
#52757=CARTESIAN_POINT('Ctrl Pts',(75.8404639893208,-4.90870856374795,131.15613754042));
#52758=CARTESIAN_POINT('Ctrl Pts',(75.8306257019945,-4.89026174281333,131.328310185059));
#52759=CARTESIAN_POINT('Ctrl Pts',(75.8205861445655,-4.87143753977756,131.504005110022));
#52760=CARTESIAN_POINT('Ctrl Pts',(75.8105465871366,-4.8431711433919,131.678401729631));
#52761=CARTESIAN_POINT('Ctrl Pts',(75.8005070297076,-4.8056723255412,131.850638096071));
#52762=CARTESIAN_POINT('Ctrl Pts',(75.7964197938675,-4.79040606371979,131.920757785596));
#52763=CARTESIAN_POINT('Ctrl Pts',(75.7923325580274,-4.77361015724972,131.990519695717));
#52764=CARTESIAN_POINT('Ctrl Pts',(75.7882453221872,-4.75530099873472,132.059866680448));
#52765=CARTESIAN_POINT('Ctrl Pts',(75.7804709880682,-4.72047513565686,132.19177162808));
#52766=CARTESIAN_POINT('Ctrl Pts',(75.7726966539491,-4.68010168226192,132.322435379416));
#52767=CARTESIAN_POINT('Ctrl Pts',(75.76492231983,-4.63428423813055,132.451355657848));
#52768=CARTESIAN_POINT('Ctrl Pts',(75.7571575668829,-4.58852325990428,132.580117053559));
#52769=CARTESIAN_POINT('Ctrl Pts',(75.7493928139358,-4.53733176998093,132.707138886732));
#52770=CARTESIAN_POINT('Ctrl Pts',(75.7416280609887,-4.4808639437233,132.83193093209));
#52771=CARTESIAN_POINT('Ctrl Pts',(75.7338710201037,-4.42445220210681,132.95659903223));
#52772=CARTESIAN_POINT('Ctrl Pts',(75.7261139792187,-4.36277471318464,133.079041397932));
#52773=CARTESIAN_POINT('Ctrl Pts',(75.7183569383337,-4.29603472009752,133.198785130099));
#52774=CARTESIAN_POINT('Ctrl Pts',(75.7106057470936,-4.22934505615845,133.318438562585));
#52775=CARTESIAN_POINT('Ctrl Pts',(75.7028545558535,-4.15760067647177,133.435397072079));
#52776=CARTESIAN_POINT('Ctrl Pts',(75.6951033646134,-4.08105182579783,133.549210168571));
#52777=CARTESIAN_POINT('Ctrl Pts',(75.6873554678363,-4.00453551042728,133.662974891462));
#52778=CARTESIAN_POINT('Ctrl Pts',(75.6796075710593,-3.92321900324693,133.773596536577));
#52779=CARTESIAN_POINT('Ctrl Pts',(75.6718596742822,-3.83739703209034,133.880651741729));
#52780=CARTESIAN_POINT('Ctrl Pts',(75.6641133981981,-3.75159301304001,133.98768455324));
#52781=CARTESIAN_POINT('Ctrl Pts',(75.656367122114,-3.66128564897798,134.091152103815));
#52782=CARTESIAN_POINT('Ctrl Pts',(75.6486208460299,-3.56681104892234,134.19066273105));
#52783=CARTESIAN_POINT('Ctrl Pts',(75.6408745127645,-3.47233575147679,134.29017409285));
#52784=CARTESIAN_POINT('Ctrl Pts',(75.6331281794992,-3.37369342584159,134.38572818949));
#52785=CARTESIAN_POINT('Ctrl Pts',(75.6253818462338,-3.2712579812657,134.476969265721));
#52786=CARTESIAN_POINT('Ctrl Pts',(75.6176337782309,-3.1687995969821,134.568230774759));
#52787=CARTESIAN_POINT('Ctrl Pts',(75.6098857102279,-3.06254669535508,134.655177081424));
#52788=CARTESIAN_POINT('Ctrl Pts',(75.6021376422249,-2.9529069683634,134.737492130583));
#52789=CARTESIAN_POINT('Ctrl Pts',(75.594381339483,-2.84315071496514,134.819894665156));
#52790=CARTESIAN_POINT('Ctrl Pts',(75.5866250367412,-2.73000075885075,134.897655874578));
#52791=CARTESIAN_POINT('Ctrl Pts',(75.5788687339993,-2.61389499327657,134.970502241014));
#52792=CARTESIAN_POINT('Ctrl Pts',(75.5711082914851,-2.49772725855935,135.043387487749));
#52793=CARTESIAN_POINT('Ctrl Pts',(75.563347848971,-2.37860091029006,135.111352470902));
#52794=CARTESIAN_POINT('Ctrl Pts',(75.5555874064568,-2.25697836353062,135.174169735715));
#52795=CARTESIAN_POINT('Ctrl Pts',(75.5478145061914,-2.13516057746198,135.237087840377));
#52796=CARTESIAN_POINT('Ctrl Pts',(75.540041605926,-2.01083894017883,135.294841548631));
#52797=CARTESIAN_POINT('Ctrl Pts',(75.5322687056605,-1.88449658114783,135.347251294012));
#52798=CARTESIAN_POINT('Ctrl Pts',(75.5247783698985,-1.76274708510464,135.397755813137));
#52799=CARTESIAN_POINT('Ctrl Pts',(75.5172880341364,-1.63912152230594,135.443298050433));
#52800=CARTESIAN_POINT('Ctrl Pts',(75.5097976983744,-1.51406353601884,135.483761719352));
#52801=CARTESIAN_POINT('Ctrl Pts',(75.5020233642553,-1.38426393817138,135.525759580578));
#52802=CARTESIAN_POINT('Ctrl Pts',(75.4942490301362,-1.25250998584571,135.562419200038));
#52803=CARTESIAN_POINT('Ctrl Pts',(75.4864746960171,-1.11928025668258,135.593556246218));
#52804=CARTESIAN_POINT('Ctrl Pts',(75.47870994307,-0.986214721253562,135.624654918772));
#52805=CARTESIAN_POINT('Ctrl Pts',(75.470945190123,-0.851677404835057,135.650244471991));
#52806=CARTESIAN_POINT('Ctrl Pts',(75.4631804371759,-0.716164083384742,
135.670189639241));
#52807=CARTESIAN_POINT('Ctrl Pts',(75.4554233962909,-0.580785355675603,
135.690114996668));
#52808=CARTESIAN_POINT('Ctrl Pts',(75.4476663554059,-0.444432936343657,
135.704407067924));
#52809=CARTESIAN_POINT('Ctrl Pts',(75.4399093145209,-0.307614546674604,
135.712981233704));
#52810=CARTESIAN_POINT('Ctrl Pts',(75.4321581232807,-0.170899332817772,
135.721548933639));
#52811=CARTESIAN_POINT('Ctrl Pts',(75.4244069320406,-0.033719236668912,
135.724407286354));
#52812=CARTESIAN_POINT('Ctrl Pts',(75.4166557408005,0.103411468363519,135.721523328999));
#52813=CARTESIAN_POINT('Ctrl Pts',(75.4089078440234,0.240483889188416,135.718640597404));
#52814=CARTESIAN_POINT('Ctrl Pts',(75.4011599472464,0.377506570589019,135.710020418178));
#52815=CARTESIAN_POINT('Ctrl Pts',(75.3934120504693,0.513964018372659,135.695681916593));
#52816=CARTESIAN_POINT('Ctrl Pts',(75.3856657743852,0.650392922199905,135.681346414314));
#52817=CARTESIAN_POINT('Ctrl Pts',(75.3779194983011,0.786256439007236,135.661295009712));
#52818=CARTESIAN_POINT('Ctrl Pts',(75.3701732222169,0.921043376988179,135.635598777728));
#52819=CARTESIAN_POINT('Ctrl Pts',(75.3624268889516,1.05583130993568,135.609902356061));
#52820=CARTESIAN_POINT('Ctrl Pts',(75.3546805556862,1.18954226415061,135.578561097081));
#52821=CARTESIAN_POINT('Ctrl Pts',(75.3469342224209,1.32167482558368,135.541697286826));
#52822=CARTESIAN_POINT('Ctrl Pts',(75.3391861544179,1.45383697718765,135.504825221177));
#52823=CARTESIAN_POINT('Ctrl Pts',(75.3314380864149,1.58441965613331,135.462428248334));
#52824=CARTESIAN_POINT('Ctrl Pts',(75.323690018412,1.71293658881232,135.414678535585));
#52825=CARTESIAN_POINT('Ctrl Pts',(75.3159337156701,1.84159011081684,135.366878073873));
#52826=CARTESIAN_POINT('Ctrl Pts',(75.3081774129282,1.96817313373631,135.313713644336));
#52827=CARTESIAN_POINT('Ctrl Pts',(75.3004211101864,2.09221884726884,135.255405815902));
#52828=CARTESIAN_POINT('Ctrl Pts',(75.2926606676722,2.21633076773362,135.197066866825));
#52829=CARTESIAN_POINT('Ctrl Pts',(75.2849002251581,2.33790233399149,135.133579229724));
#52830=CARTESIAN_POINT('Ctrl Pts',(75.2771397826439,2.45649223527464,135.065209002634));
#52831=CARTESIAN_POINT('Ctrl Pts',(75.2693668823785,2.57527250759533,134.996729021585));
#52832=CARTESIAN_POINT('Ctrl Pts',(75.261593982113,2.69106121969569,134.923350997191));
#52833=CARTESIAN_POINT('Ctrl Pts',(75.2538210818476,2.80344615394611,134.845384339895));
#52834=CARTESIAN_POINT('Ctrl Pts',(75.2463307460856,2.91174561275604,134.770251966977));
#52835=CARTESIAN_POINT('Ctrl Pts',(75.2388404103235,3.01688422323087,134.690858971426));
#52836=CARTESIAN_POINT('Ctrl Pts',(75.2313500745615,3.11852435018292,134.607515747168));
#52837=CARTESIAN_POINT('Ctrl Pts',(75.2235757404424,3.22401819344106,134.52101253923));
#52838=CARTESIAN_POINT('Ctrl Pts',(75.2158014063233,3.3260771990486,134.429979627452));
#52839=CARTESIAN_POINT('Ctrl Pts',(75.2080270722042,3.42428760077671,134.33472001707));
#52840=CARTESIAN_POINT('Ctrl Pts',(75.2002623192571,3.52237696696193,134.239577805644));
#52841=CARTESIAN_POINT('Ctrl Pts',(75.1924975663101,3.61662688860021,134.140219529622));
#52842=CARTESIAN_POINT('Ctrl Pts',(75.184732813363,3.70665558302411,134.036989184435));
#52843=CARTESIAN_POINT('Ctrl Pts',(75.176975772478,3.79659485967952,133.933861369082));
#52844=CARTESIAN_POINT('Ctrl Pts',(75.169218731593,3.882320997241,133.826869430614));
#52845=CARTESIAN_POINT('Ctrl Pts',(75.161461690708,3.96348836733584,133.716394790527));
#52846=CARTESIAN_POINT('Ctrl Pts',(75.1537104994679,4.04459452848551,133.606003460226));
#52847=CARTESIAN_POINT('Ctrl Pts',(75.1459593082277,4.121148534356,133.492134969655));
#52848=CARTESIAN_POINT('Ctrl Pts',(75.1382081169876,4.19284467502947,133.375204174373));
#52849=CARTESIAN_POINT('Ctrl Pts',(75.1304602202105,4.2645103429306,133.258323077798));
#52850=CARTESIAN_POINT('Ctrl Pts',(75.1227123234335,4.33132204827438,133.138382597821));
#52851=CARTESIAN_POINT('Ctrl Pts',(75.1149644266564,4.39301724448878,133.015826771981));
#52852=CARTESIAN_POINT('Ctrl Pts',(75.1072181505723,4.45469953539814,132.893296582178));
#52853=CARTESIAN_POINT('Ctrl Pts',(75.0994718744882,4.51126727030657,132.768152483663));
#52854=CARTESIAN_POINT('Ctrl Pts',(75.0917255984041,4.56250393491628,132.640862974323));
#52855=CARTESIAN_POINT('Ctrl Pts',(75.0839792651388,4.61374097774341,132.51357252536));
#52856=CARTESIAN_POINT('Ctrl Pts',(75.0762329318734,4.65964672575764,132.384136996657));
#52857=CARTESIAN_POINT('Ctrl Pts',(75.0684865986081,4.70005303512522,132.253044340644));
#52858=CARTESIAN_POINT('Ctrl Pts',(75.0607385306051,4.74046839320559,132.121922327339));
#52859=CARTESIAN_POINT('Ctrl Pts',(75.0529904626021,4.77538174683741,131.989142821823));
#52860=CARTESIAN_POINT('Ctrl Pts',(75.0452423945991,4.804675102473,131.855208000479));
#52861=CARTESIAN_POINT('Ctrl Pts',(75.0374860918573,4.83399959143558,131.721130831613));
#52862=CARTESIAN_POINT('Ctrl Pts',(75.0297297891155,4.8576920670216,131.585896276636));
#52863=CARTESIAN_POINT('Ctrl Pts',(75.0219734863736,4.8756857777461,131.450016299168));
#52864=CARTESIAN_POINT('Ctrl Pts',(75.0142130438595,4.89368909225581,131.314063798464));
#52865=CARTESIAN_POINT('Ctrl Pts',(75.0064526013453,4.90598754621258,131.177465578061));
#52866=CARTESIAN_POINT('Ctrl Pts',(74.9986921588311,4.9125664761791,131.040736757693));
#52867=CARTESIAN_POINT('Ctrl Pts',(74.9909192585657,4.91915596722805,130.903788448084));
#52868=CARTESIAN_POINT('Ctrl Pts',(74.9831463583002,4.9200075843185,130.766709510745));
#52869=CARTESIAN_POINT('Ctrl Pts',(74.9753734580348,4.91515882952152,130.630013999943));
#52870=CARTESIAN_POINT('Ctrl Pts',(74.9678831222728,4.91048633917467,130.498287715273));
#52871=CARTESIAN_POINT('Ctrl Pts',(74.9603927865107,4.900520750606,130.366917771223));
#52872=CARTESIAN_POINT('Ctrl Pts',(74.9529024507486,4.88534070695033,130.236356005336));
#52873=CARTESIAN_POINT('Ctrl Pts',(74.9451281166295,4.86958510732567,130.100843950414));
#52874=CARTESIAN_POINT('Ctrl Pts',(74.9373537825105,4.84816192592134,129.965773306116));
#52875=CARTESIAN_POINT('Ctrl Pts',(74.9295794483914,4.82110243887114,129.831655967423));
#52876=CARTESIAN_POINT('Ctrl Pts',(74.9218146954443,4.79407630022036,129.697703916362));
#52877=CARTESIAN_POINT('Ctrl Pts',(74.9140499424972,4.76142775345753,129.56470321284));
#52878=CARTESIAN_POINT('Ctrl Pts',(74.9062851895501,4.72323984882572,129.433160999361));
#52879=CARTESIAN_POINT('Ctrl Pts',(74.8985281486651,4.68508987295917,129.301749435463));
#52880=CARTESIAN_POINT('Ctrl Pts',(74.8907711077801,4.64141159628598,129.171793851877));
#52881=CARTESIAN_POINT('Ctrl Pts',(74.8830140668951,4.59233909893608,129.043791203177));
#52882=CARTESIAN_POINT('Ctrl Pts',(74.8752628756549,4.54330360753817,128.91588508227));
#52883=CARTESIAN_POINT('Ctrl Pts',(74.8675116844148,4.48888213160629,128.789929328463));
#52884=CARTESIAN_POINT('Ctrl Pts',(74.8597604931747,4.42925845719295,128.66640538373));
#52885=CARTESIAN_POINT('Ctrl Pts',(74.8520125963976,4.3696601244317,128.54293393997));
#52886=CARTESIAN_POINT('Ctrl Pts',(74.8442646996205,4.30486416044099,128.421892600921));
#52887=CARTESIAN_POINT('Ctrl Pts',(74.8365168028434,4.23510223374301,128.303742267588));
#52888=CARTESIAN_POINT('Ctrl Pts',(74.8287705267593,4.16535489973621,128.185616648758));
#52889=CARTESIAN_POINT('Ctrl Pts',(74.8210242506752,4.09064386785236,128.070381169236));
#52890=CARTESIAN_POINT('Ctrl Pts',(74.8132779745911,4.01124626736472,127.958471223185));
#52891=CARTESIAN_POINT('Ctrl Pts',(74.8055316413258,3.93184808078202,127.846560451039));
#52892=CARTESIAN_POINT('Ctrl Pts',(74.7977853080604,3.8477634827909,127.737975580214));
#52893=CARTESIAN_POINT('Ctrl Pts',(74.7900389747951,3.75931211574209,127.633121825085));
#52894=CARTESIAN_POINT('Ctrl Pts',(74.7822909067921,3.67084094062291,127.528244588685));
#52895=CARTESIAN_POINT('Ctrl Pts',(74.7745428387891,3.57800130256527,127.427100429426));
#52896=CARTESIAN_POINT('Ctrl Pts',(74.7667947707861,3.48115191838819,127.330060057223));
#52897=CARTESIAN_POINT('Ctrl Pts',(74.7590384680443,3.38419960153308,127.232916549357));
#52898=CARTESIAN_POINT('Ctrl Pts',(74.7512821653024,3.2832293021638,127.139885818387));
#52899=CARTESIAN_POINT('Ctrl Pts',(74.7435258625605,3.178635668966,127.051300753072));
#52900=CARTESIAN_POINT('Ctrl Pts',(74.7357654200464,3.07398621099685,126.96266840724));
#52901=CARTESIAN_POINT('Ctrl Pts',(74.7280049775322,2.96570987427895,126.878486694891));
#52902=CARTESIAN_POINT('Ctrl Pts',(74.720244535018,2.85423211768801,126.799046387589));
#52903=CARTESIAN_POINT('Ctrl Pts',(74.7124716347526,2.74257540710567,126.719478555653));
#52904=CARTESIAN_POINT('Ctrl Pts',(74.7046987344872,2.62770733468377,126.644667552105));
#52905=CARTESIAN_POINT('Ctrl Pts',(74.6969258342217,2.51008065962286,126.574859684278));
#52906=CARTESIAN_POINT('Ctrl Pts',(74.6894354984598,2.39673001048507,126.507589508282));
#52907=CARTESIAN_POINT('Ctrl Pts',(74.6819451626978,2.28081811192248,126.444965176537));
#52908=CARTESIAN_POINT('Ctrl Pts',(74.6744548269358,2.16276761619343,126.387164753577));
#52909=CARTESIAN_POINT('Ctrl Pts',(74.6666804928167,2.04024120003718,126.327172810011));
#52910=CARTESIAN_POINT('Ctrl Pts',(74.6589061586976,1.91502268875096,126.272187756736));
#52911=CARTESIAN_POINT('Ctrl Pts',(74.6511318245785,1.78755965959214,126.222459971993));
#52912=CARTESIAN_POINT('Ctrl Pts',(74.6433670716314,1.66025371722515,126.172793472301));
#52913=CARTESIAN_POINT('Ctrl Pts',(74.6356023186843,1.53070912156609,126.128371490371));
#52914=CARTESIAN_POINT('Ctrl Pts',(74.6278375657373,1.39939743665238,126.089398276593));
#52915=CARTESIAN_POINT('Ctrl Pts',(74.6200805248523,1.2682161723553,126.05046377156));
#52916=CARTESIAN_POINT('Ctrl Pts',(74.6123234839673,1.13527168390767,126.016967375489));
#52917=CARTESIAN_POINT('Ctrl Pts',(74.6045664430823,1.00105454685282,125.989064899053));
#52918=CARTESIAN_POINT('Ctrl Pts',(74.5968152518422,0.866938623984995,125.961183464093));
#52919=CARTESIAN_POINT('Ctrl Pts',(74.589064060602,0.731552343995152,125.938887631517));
#52920=CARTESIAN_POINT('Ctrl Pts',(74.5813128693619,0.595400098502344,125.922283008064));
#52921=CARTESIAN_POINT('Ctrl Pts',(74.5735649725848,0.459305721345851,125.905685442018));
#52922=CARTESIAN_POINT('Ctrl Pts',(74.5658170758077,0.322446413469263,125.894774321286));
#52923=CARTESIAN_POINT('Ctrl Pts',(74.5580691790306,0.185335166434737,125.889603864828));
#52924=CARTESIAN_POINT('Ctrl Pts',(74.5503229029465,0.048252600117314,125.884434489919));
#52925=CARTESIAN_POINT('Ctrl Pts',(74.5425766268624,-0.0890814100943838,
125.885003405504));
#52926=CARTESIAN_POINT('Ctrl Pts',(74.5348303507783,-0.226150759619665,
125.891312796058));
#52927=CARTESIAN_POINT('Ctrl Pts',(74.5270840175129,-0.363221120959654,
125.897622233186));
#52928=CARTESIAN_POINT('Ctrl Pts',(74.5193376842476,-0.500026427163158,
125.909672211862));
#52929=CARTESIAN_POINT('Ctrl Pts',(74.5115913509823,-0.636052985399898,
125.92741283619));
#52930=CARTESIAN_POINT('Ctrl Pts',(74.5038432829793,-0.772110005841306,
125.945157433409));
#52931=CARTESIAN_POINT('Ctrl Pts',(74.4960952149763,-0.907387543681894,
125.968595161599));
#52932=CARTESIAN_POINT('Ctrl Pts',(74.4883471469734,-1.04137981496835,125.997624599905));
#52933=CARTESIAN_POINT('Ctrl Pts',(74.4805908442315,-1.17551449483525,126.026684891044));
#52934=CARTESIAN_POINT('Ctrl Pts',(74.4728345414896,-1.30836079671276,126.06134868104));
#52935=CARTESIAN_POINT('Ctrl Pts',(74.4650782387478,-1.43942533460707,126.101463875281));
#52936=CARTESIAN_POINT('Ctrl Pts',(74.4573177962336,-1.57055982559161,126.14160048021));
#52937=CARTESIAN_POINT('Ctrl Pts',(74.4495573537194,-1.69991028913348,126.187194157058));
#52938=CARTESIAN_POINT('Ctrl Pts',(74.4417969112052,-1.8270021199659,126.238044124358));
#52939=CARTESIAN_POINT('Ctrl Pts',(74.4340240109398,-1.95429796988785,126.28897572054));
#52940=CARTESIAN_POINT('Ctrl Pts',(74.4262511106744,-2.07932758488358,126.345180308323));
#52941=CARTESIAN_POINT('Ctrl Pts',(74.4184782104089,-2.2016390122099,126.4064101037));
#52942=CARTESIAN_POINT('Ctrl Pts',(74.4109878746469,-2.31950411106951,126.465414041786));
#52943=CARTESIAN_POINT('Ctrl Pts',(74.4034975388848,-2.4348449474596,126.529084023851));
#52944=CARTESIAN_POINT('Ctrl Pts',(74.3960072031228,-2.54728325677598,126.597160708809));
#52945=CARTESIAN_POINT('Ctrl Pts',(74.3882315941812,-2.66400383527471,126.667830128322));
#52946=CARTESIAN_POINT('Ctrl Pts',(74.3804559852396,-2.77796621339256,126.743472462004));
#52947=CARTESIAN_POINT('Ctrl Pts',(74.372680376298,-2.8887175935236,126.823846363432));
#52948=CARTESIAN_POINT('Ctrl Pts',(74.3646617944063,-3.00292974306261,126.906731795992));
#52949=CARTESIAN_POINT('Ctrl Pts',(74.3566432125147,-3.11372655075258,126.994649195824));
#52950=CARTESIAN_POINT('Ctrl Pts',(74.348624630623,-3.22063854773003,127.087282409164));
#52951=CARTESIAN_POINT('Ctrl Pts',(74.3408685462443,-3.32405065735999,127.176883167583));
#52952=CARTESIAN_POINT('Ctrl Pts',(74.3331124618656,-3.42382796139808,127.270895573751));
#52953=CARTESIAN_POINT('Ctrl Pts',(74.3253563774869,-3.5195753913396,127.368989876703));
#52954=CARTESIAN_POINT('Ctrl Pts',(74.3176056108797,-3.61525717437204,127.467016923669));
#52955=CARTESIAN_POINT('Ctrl Pts',(74.3098548442726,-3.70691430864919,127.569120020638));
#52956=CARTESIAN_POINT('Ctrl Pts',(74.3021040776655,-3.79418655244898,127.674930722567));
#52957=CARTESIAN_POINT('Ctrl Pts',(74.2943569465692,-3.8814178610486,127.780691793799));
#52958=CARTESIAN_POINT('Ctrl Pts',(74.2866098154728,-3.96426812432516,127.890156708005));
#52959=CARTESIAN_POINT('Ctrl Pts',(74.2788626843765,-4.04241585072074,128.002922209829));
#52960=CARTESIAN_POINT('Ctrl Pts',(74.2711175093536,-4.12054384559356,128.115659239488));
#52961=CARTESIAN_POINT('Ctrl Pts',(74.2633723343307,-4.19397144569641,128.231694876198));
#52962=CARTESIAN_POINT('Ctrl Pts',(74.2556271593079,-4.26241938771938,128.350595342383));
#52963=CARTESIAN_POINT('Ctrl Pts',(74.2478803958074,-4.33088136790436,128.469520194166));
#52964=CARTESIAN_POINT('Ctrl Pts',(74.240133632307,-4.39436145126947,128.591310712345));
#52965=CARTESIAN_POINT('Ctrl Pts',(74.2323868688065,-4.45262543002663,128.715506902635));
#52966=CARTESIAN_POINT('Ctrl Pts',(74.2246390865264,-4.51089707110035,128.839719426011));
#52967=CARTESIAN_POINT('Ctrl Pts',(74.2168913042463,-4.56395108278894,128.966337894346));
#52968=CARTESIAN_POINT('Ctrl Pts',(74.2091435219662,-4.61160101714329,129.094881421675));
#52969=CARTESIAN_POINT('Ctrl Pts',(74.2013908164532,-4.65928123006226,129.223506630407));
#52970=CARTESIAN_POINT('Ctrl Pts',(74.1936381109402,-4.70155038350649,129.354058970607));
#52971=CARTESIAN_POINT('Ctrl Pts',(74.1858854054271,-4.73827157912007,129.486041420633));
#52972=CARTESIAN_POINT('Ctrl Pts',(74.1840017405842,-4.74719368057893,129.51810902601));
#52973=CARTESIAN_POINT('Ctrl Pts',(74.1821180757413,-4.7557885000028,129.550261000689));
#52974=CARTESIAN_POINT('Ctrl Pts',(74.1802344108984,-4.76405452823402,129.582490119308));
#52975=CARTESIAN_POINT('Origin',(213.235140564004,0.,130.804360617566));
#52976=CARTESIAN_POINT('',(72.0846889553802,-4.76405452823408,129.582490119308));
#52977=CARTESIAN_POINT('',(72.4299696197722,-4.76405452823407,129.582490119308));
#52978=CARTESIAN_POINT('',(213.235140564004,-4.76405452823405,129.582490119308));
#52979=CARTESIAN_POINT('',(73.764859436044,-4.91824854295789,130.800574829328));
#52980=CARTESIAN_POINT('Ctrl Pts',(73.7648594359911,-4.91824854295861,130.800574830266));
#52981=CARTESIAN_POINT('Ctrl Pts',(73.7571129956196,-4.91835416522511,130.937792406713));
#52982=CARTESIAN_POINT('Ctrl Pts',(73.7493665552481,-4.91271299733684,131.075074362928));
#52983=CARTESIAN_POINT('Ctrl Pts',(73.7416201148767,-4.90133565926305,131.211904256624));
#52984=CARTESIAN_POINT('Ctrl Pts',(73.7338747671406,-4.8899599259627,131.348714850464));
#52985=CARTESIAN_POINT('Ctrl Pts',(73.7261294194045,-4.87284966382949,131.485073119667));
#52986=CARTESIAN_POINT('Ctrl Pts',(73.7183840716684,-4.85006751003875,131.620466131925));
#52987=CARTESIAN_POINT('Ctrl Pts',(73.7106381452548,-4.82728365412693,131.755869259789));
#52988=CARTESIAN_POINT('Ctrl Pts',(73.7028922188412,-4.79882712764685,131.89030660211));
#52989=CARTESIAN_POINT('Ctrl Pts',(73.6951462924276,-4.76481192753374,132.023274214886));
#52990=CARTESIAN_POINT('Ctrl Pts',(73.6873981159975,-4.73078684677441,132.156280451747));
#52991=CARTESIAN_POINT('Ctrl Pts',(73.6796499395675,-4.69119997565195,132.287815731318));
#52992=CARTESIAN_POINT('Ctrl Pts',(73.6719017631375,-4.64621542224321,132.417390472407));
#52993=CARTESIAN_POINT('Ctrl Pts',(73.6641446191071,-4.60117880451946,132.547115180977));
#52994=CARTESIAN_POINT('Ctrl Pts',(73.6563874750767,-4.55073215402375,132.674874449209));
#52995=CARTESIAN_POINT('Ctrl Pts',(73.6486303310463,-4.49508829535229,132.800197354247));
#52996=CARTESIAN_POINT('Ctrl Pts',(73.6408686127013,-4.43941162402268,132.925594161019));
#52997=CARTESIAN_POINT('Ctrl Pts',(73.6331068943563,-4.3785318114894,133.048551392652));
#52998=CARTESIAN_POINT('Ctrl Pts',(73.6253451760113,-4.31270760178373,133.168622913509));
#52999=CARTESIAN_POINT('Ctrl Pts',(73.6175704459995,-4.24677304503256,133.28889572106));
#53000=CARTESIAN_POINT('Ctrl Pts',(73.6097957159876,-4.17587773049316,133.406272817251));
#53001=CARTESIAN_POINT('Ctrl Pts',(73.6020209859758,-4.10032417432361,133.520336451029));
#53002=CARTESIAN_POINT('Ctrl Pts',(73.5947650999316,-4.02981265907372,133.626788086933));
#53003=CARTESIAN_POINT('Ctrl Pts',(73.5875092138875,-3.95524446899847,133.730353859054));
#53004=CARTESIAN_POINT('Ctrl Pts',(73.5802533278434,-3.87689590057486,133.830721673125));
#53005=CARTESIAN_POINT('Ctrl Pts',(73.5724789937243,-3.79294916478359,133.938260975238));
#53006=CARTESIAN_POINT('Ctrl Pts',(73.5647046596052,-3.70439160296181,134.042475129251));
#53007=CARTESIAN_POINT('Ctrl Pts',(73.5569303254861,-3.61151620383971,134.142943216799));
#53008=CARTESIAN_POINT('Ctrl Pts',(73.5491655725391,-3.51875526534665,134.243287486409));
#53009=CARTESIAN_POINT('Ctrl Pts',(73.541400819592,-3.42168734029623,134.339894591062));
#53010=CARTESIAN_POINT('Ctrl Pts',(73.5336360666449,-3.3206471633281,134.432374603093));
#53011=CARTESIAN_POINT('Ctrl Pts',(73.5258790257599,-3.21970734088822,134.524762762673));
#53012=CARTESIAN_POINT('Ctrl Pts',(73.5181219848749,-3.11480340438348,134.613031724739));
#53013=CARTESIAN_POINT('Ctrl Pts',(73.5103649439899,-3.00630837134294,134.696826807386));
#53014=CARTESIAN_POINT('Ctrl Pts',(73.5026137527498,-2.89789515525086,134.78055869951));
#53015=CARTESIAN_POINT('Ctrl Pts',(73.4948625615097,-2.78589654105055,134.859823189522));
#53016=CARTESIAN_POINT('Ctrl Pts',(73.4871113702696,-2.67071992863701,134.934304700151));
#53017=CARTESIAN_POINT('Ctrl Pts',(73.4793634734925,-2.55559226935603,135.008754554152));
#53018=CARTESIAN_POINT('Ctrl Pts',(73.4716155767154,-2.43728962598206,135.078425260182));
#53019=CARTESIAN_POINT('Ctrl Pts',(73.4638676799383,-2.31624960778856,135.143043691601));
#53020=CARTESIAN_POINT('Ctrl Pts',(73.4561214038542,-2.19523490855745,135.207648606237));
#53021=CARTESIAN_POINT('Ctrl Pts',(73.4483751277702,-2.07148431811454,135.26720316434));
#53022=CARTESIAN_POINT('Ctrl Pts',(73.4406288516861,-1.94546100368361,135.321479671304));
#53023=CARTESIAN_POINT('Ctrl Pts',(73.4328825184207,-1.81943675897737,135.375756578926));
#53024=CARTESIAN_POINT('Ctrl Pts',(73.4251361851554,-1.69114011588459,135.424755203015));
#53025=CARTESIAN_POINT('Ctrl Pts',(73.41738985189,-1.56105485132995,135.468295738646));
#53026=CARTESIAN_POINT('Ctrl Pts',(73.4096417838871,-1.43094045508253,135.511846024877));
#53027=CARTESIAN_POINT('Ctrl Pts',(73.4018937158842,-1.29903701100444,135.549935666345));
#53028=CARTESIAN_POINT('Ctrl Pts',(73.3941456478812,-1.16584371934485,135.582434652631));
#53029=CARTESIAN_POINT('Ctrl Pts',(73.3863893451393,-1.0325088682695,135.614968179227));
#53030=CARTESIAN_POINT('Ctrl Pts',(73.3786330423975,-0.897881811589283,
135.641899088402));
#53031=CARTESIAN_POINT('Ctrl Pts',(73.3708767396557,-0.76247276364059,135.663148362179));
#53032=CARTESIAN_POINT('Ctrl Pts',(73.3631162971415,-0.626991443805735,
135.684408977334));
#53033=CARTESIAN_POINT('Ctrl Pts',(73.3553558546273,-0.490727689299462,
135.699981870287));
#53034=CARTESIAN_POINT('Ctrl Pts',(73.3475954121132,-0.35419611963266,135.70984002037));
#53035=CARTESIAN_POINT('Ctrl Pts',(73.3398225118477,-0.217445377369619,
135.719713995631));
#53036=CARTESIAN_POINT('Ctrl Pts',(73.3320496115823,-0.0804263518392551,
135.723854884005));
#53037=CARTESIAN_POINT('Ctrl Pts',(73.3242767113169,0.0563461507783298,
135.722287840878));
#53038=CARTESIAN_POINT('Ctrl Pts',(73.3167863755548,0.188146628417826,135.720777763716));
#53039=CARTESIAN_POINT('Ctrl Pts',(73.3092960397927,0.319717887817951,135.713967561421));
#53040=CARTESIAN_POINT('Ctrl Pts',(73.3018057040306,0.450606334333693,135.701925011625));
#53041=CARTESIAN_POINT('Ctrl Pts',(73.2940313699115,0.586457456080612,135.689425864894));
#53042=CARTESIAN_POINT('Ctrl Pts',(73.2862570357924,0.722003300653231,135.67125017587));
#53043=CARTESIAN_POINT('Ctrl Pts',(73.2784827016733,0.856731369945098,135.647416927609));
#53044=CARTESIAN_POINT('Ctrl Pts',(73.2707179487262,0.991293398932373,135.623613051698));
#53045=CARTESIAN_POINT('Ctrl Pts',(73.2629531957792,1.12503927663804,135.594165557071));
#53046=CARTESIAN_POINT('Ctrl Pts',(73.2551884428321,1.25746001362484,135.559145300034));
#53047=CARTESIAN_POINT('Ctrl Pts',(73.2474314019471,1.38974922846869,135.52415982561));
#53048=CARTESIAN_POINT('Ctrl Pts',(73.2396743610621,1.52071554626341,135.483612702881));
#53049=CARTESIAN_POINT('Ctrl Pts',(73.2319173201771,1.64985893799172,135.437626047825));
#53050=CARTESIAN_POINT('Ctrl Pts',(73.224166128937,1.77890494168338,135.391674071663));
#53051=CARTESIAN_POINT('Ctrl Pts',(73.2164149376969,1.90613038871053,135.340290858565));
#53052=CARTESIAN_POINT('Ctrl Pts',(73.2086637464568,2.03104956538335,135.283648588377));
#53053=CARTESIAN_POINT('Ctrl Pts',(73.2009158496797,2.15591564807444,135.227030392666));
#53054=CARTESIAN_POINT('Ctrl Pts',(73.1931679529027,2.27847705468136,135.165157746701));
#53055=CARTESIAN_POINT('Ctrl Pts',(73.1854200561256,2.39826745752363,135.098251191938));
#53056=CARTESIAN_POINT('Ctrl Pts',(73.1776737800415,2.51803280279601,135.031358632584));
#53057=CARTESIAN_POINT('Ctrl Pts',(73.1699275039574,2.63502795611112,134.959434449401));
#53058=CARTESIAN_POINT('Ctrl Pts',(73.1621812278732,2.7488109983516,134.882745243596));
#53059=CARTESIAN_POINT('Ctrl Pts',(73.1544348946079,2.8625948805128,134.806055471689));
#53060=CARTESIAN_POINT('Ctrl Pts',(73.1466885613425,2.97316628008363,134.724600825483));
#53061=CARTESIAN_POINT('Ctrl Pts',(73.1389422280772,3.0801124288433,134.638691131252));
#53062=CARTESIAN_POINT('Ctrl Pts',(73.1311941600742,3.18708252745132,134.552762198141));
#53063=CARTESIAN_POINT('Ctrl Pts',(73.1234460920712,3.29042545501798,134.462376476542));
#53064=CARTESIAN_POINT('Ctrl Pts',(73.1156980240682,3.38976200016907,134.367883683958));
#53065=CARTESIAN_POINT('Ctrl Pts',(73.1079417213264,3.4892041213824,134.27329046331));
#53066=CARTESIAN_POINT('Ctrl Pts',(73.1001854185845,3.58463107057883,134.174581721921));
#53067=CARTESIAN_POINT('Ctrl Pts',(73.0924291158427,3.67570058438456,134.072144006418));
#53068=CARTESIAN_POINT('Ctrl Pts',(73.0846686733285,3.76681870473185,133.969651616821));
#53069=CARTESIAN_POINT('Ctrl Pts',(73.0769082308143,3.85357450835811,133.863426589995));
#53070=CARTESIAN_POINT('Ctrl Pts',(73.0691477883001,3.93566709759427,133.753887284578));
#53071=CARTESIAN_POINT('Ctrl Pts',(73.0613748880347,4.0178914691425,133.644172136943));
#53072=CARTESIAN_POINT('Ctrl Pts',(73.0536019877693,4.09543744598224,133.531132401497));
#53073=CARTESIAN_POINT('Ctrl Pts',(73.0458290875039,4.16804792673728,133.415214796359));
#53074=CARTESIAN_POINT('Ctrl Pts',(73.0383387517418,4.23801883362236,133.303511088146));
#53075=CARTESIAN_POINT('Ctrl Pts',(73.0308484159798,4.3034066970687,133.189135380633));
#53076=CARTESIAN_POINT('Ctrl Pts',(73.0233580802177,4.36402336133263,133.072505931307));
#53077=CARTESIAN_POINT('Ctrl Pts',(73.0155837460986,4.42693832484599,132.95145444096));
#53078=CARTESIAN_POINT('Ctrl Pts',(73.0078094119796,4.48491244278982,132.82759147918));
#53079=CARTESIAN_POINT('Ctrl Pts',(73.0000350778605,4.53768466840429,132.701358485943));
#53080=CARTESIAN_POINT('Ctrl Pts',(72.9922703249134,4.59039185696704,132.57528106359));
#53081=CARTESIAN_POINT('Ctrl Pts',(72.9845055719663,4.63790975956583,132.446839778655));
#53082=CARTESIAN_POINT('Ctrl Pts',(72.9767408190192,4.68002286839308,132.316501157932));
#53083=CARTESIAN_POINT('Ctrl Pts',(72.9689837781342,4.72209414988702,132.186291991364));
#53084=CARTESIAN_POINT('Ctrl Pts',(72.9612267372492,4.75877120097884,132.05418960879));
#53085=CARTESIAN_POINT('Ctrl Pts',(72.9534696963642,4.78988648340216,131.920680705454));
#53086=CARTESIAN_POINT('Ctrl Pts',(72.9457185051241,4.82097830154879,131.78727248222));
#53087=CARTESIAN_POINT('Ctrl Pts',(72.9379673138839,4.84651661089373,131.65246022864));
#53088=CARTESIAN_POINT('Ctrl Pts',(72.9302161226439,4.86638373110485,131.51674565681));
#53089=CARTESIAN_POINT('Ctrl Pts',(72.9224682258668,4.88624240726,131.381088767292));
#53090=CARTESIAN_POINT('Ctrl Pts',(72.9147203290897,4.9004346318855,131.244530708327));
#53091=CARTESIAN_POINT('Ctrl Pts',(72.9069724323126,4.90889389125081,131.107583022643));
#53092=CARTESIAN_POINT('Ctrl Pts',(72.8992261562285,4.91735138112142,130.970663983462));
#53093=CARTESIAN_POINT('Ctrl Pts',(72.8914798801445,4.92007826694303,130.833355869647));
#53094=CARTESIAN_POINT('Ctrl Pts',(72.8837336040604,4.91705997978462,130.696174584731));
#53095=CARTESIAN_POINT('Ctrl Pts',(72.875987270795,4.9140416703459,130.558992287175));
#53096=CARTESIAN_POINT('Ctrl Pts',(72.8682409375297,4.90527811190195,130.421937211257));
#53097=CARTESIAN_POINT('Ctrl Pts',(72.8604946042643,4.89080685876596,130.285524099241));
#53098=CARTESIAN_POINT('Ctrl Pts',(72.8527465362614,4.8763323648932,130.149080438454));
#53099=CARTESIAN_POINT('Ctrl Pts',(72.8449984682585,4.85614767409693,130.013279416351));
#53100=CARTESIAN_POINT('Ctrl Pts',(72.8372504002555,4.8303420406053,129.878629105052));
#53101=CARTESIAN_POINT('Ctrl Pts',(72.8294940975137,4.80450898057928,129.7438356858));
#53102=CARTESIAN_POINT('Ctrl Pts',(72.8217377947718,4.77304311784609,129.610195804994));
#53103=CARTESIAN_POINT('Ctrl Pts',(72.81398149203,4.73608466331452,129.478206356397));
#53104=CARTESIAN_POINT('Ctrl Pts',(72.8062210495158,4.69910648294285,129.346146461056));
#53105=CARTESIAN_POINT('Ctrl Pts',(72.7984606070016,4.6566299904133,129.215739124723));
#53106=CARTESIAN_POINT('Ctrl Pts',(72.7907001644874,4.60884452015681,129.087463634191));
#53107=CARTESIAN_POINT('Ctrl Pts',(72.782927264222,4.56098234042133,128.958982224455));
#53108=CARTESIAN_POINT('Ctrl Pts',(72.7751543639566,4.50779430418635,128.832639859765));
#53109=CARTESIAN_POINT('Ctrl Pts',(72.7673814636911,4.44951727848421,128.708894308848));
#53110=CARTESIAN_POINT('Ctrl Pts',(72.7598911279291,4.39335876945708,128.589647220403));
#53111=CARTESIAN_POINT('Ctrl Pts',(72.752400792167,4.3324749848179,128.472811695312));
#53112=CARTESIAN_POINT('Ctrl Pts',(72.7449104564049,4.26711611366088,128.35877211272));
#53113=CARTESIAN_POINT('Ctrl Pts',(72.7371361222858,4.19927914103882,128.240408684693));
#53114=CARTESIAN_POINT('Ctrl Pts',(72.7293617881668,4.12640615015668,128.124682460991));
#53115=CARTESIAN_POINT('Ctrl Pts',(72.7215874540477,4.04872743482068,128.012051676738));
#53116=CARTESIAN_POINT('Ctrl Pts',(72.7138227011006,3.9711444515591,127.89955969986));
#53117=CARTESIAN_POINT('Ctrl Pts',(72.7060579481535,3.88876774794136,127.790155890767));
#53118=CARTESIAN_POINT('Ctrl Pts',(72.6982931952064,3.80187333893661,127.684273731407));
#53119=CARTESIAN_POINT('Ctrl Pts',(72.6905361543214,3.71506523468359,127.5784967357));
#53120=CARTESIAN_POINT('Ctrl Pts',(72.6827791134364,3.62374860089221,127.476234729307));
#53121=CARTESIAN_POINT('Ctrl Pts',(72.6750220725514,3.52824234952909,127.377891737583));
#53122=CARTESIAN_POINT('Ctrl Pts',(72.6672708813112,3.43280812017318,127.279622907075));
#53123=CARTESIAN_POINT('Ctrl Pts',(72.6595196900711,3.33319083316311,127.185267488108));
#53124=CARTESIAN_POINT('Ctrl Pts',(72.6517684988309,3.22974898400071,127.095195676121));
#53125=CARTESIAN_POINT('Ctrl Pts',(72.6440206020538,3.12635110038367,127.005162147056));
#53126=CARTESIAN_POINT('Ctrl Pts',(72.6362727052768,3.01913218192569,126.919408860048));
#53127=CARTESIAN_POINT('Ctrl Pts',(72.6285248084997,2.90848665171518,126.838268276319));
#53128=CARTESIAN_POINT('Ctrl Pts',(72.6207785324156,2.79786426616427,126.757144665452));
#53129=CARTESIAN_POINT('Ctrl Pts',(72.6130322563314,2.68381700963804,126.680632069727));
#53130=CARTESIAN_POINT('Ctrl Pts',(72.6052859802473,2.56677105152774,126.609021604859));
#53131=CARTESIAN_POINT('Ctrl Pts',(72.597539646982,2.44972422941076,126.53741061138));
#53132=CARTESIAN_POINT('Ctrl Pts',(72.5897933137166,2.32967899503847,126.470702025005));
#53133=CARTESIAN_POINT('Ctrl Pts',(72.5820469804513,2.20708871467882,126.409142480996));
#53134=CARTESIAN_POINT('Ctrl Pts',(72.5742989124483,2.08447098107628,126.347569151153));
#53135=CARTESIAN_POINT('Ctrl Pts',(72.5665508444453,1.95930741668214,126.291147333609));
#53136=CARTESIAN_POINT('Ctrl Pts',(72.5588027764423,1.83207372105153,126.240076561645));
#53137=CARTESIAN_POINT('Ctrl Pts',(72.5510464737005,1.70470479993467,126.188951511057));
#53138=CARTESIAN_POINT('Ctrl Pts',(72.5432901709586,1.57526171593054,126.143189012623));
#53139=CARTESIAN_POINT('Ctrl Pts',(72.5355338682168,1.44423830725503,126.10293968615));
#53140=CARTESIAN_POINT('Ctrl Pts',(72.5277734257026,1.31314496744117,126.062668877399));
#53141=CARTESIAN_POINT('Ctrl Pts',(72.5200129831884,1.18047000029822,126.027917202897));
#53142=CARTESIAN_POINT('Ctrl Pts',(72.5122525406742,1.04671898326458,125.998784436443));
#53143=CARTESIAN_POINT('Ctrl Pts',(72.5044796404088,0.912753257224633,125.969604903487));
#53144=CARTESIAN_POINT('Ctrl Pts',(72.4967067401434,0.777708414834669,125.946062370536));
#53145=CARTESIAN_POINT('Ctrl Pts',(72.4889338398779,0.642097622304449,125.928204989827));
#53146=CARTESIAN_POINT('Ctrl Pts',(72.4814435041159,0.511416623665579,125.910996769886));
#53147=CARTESIAN_POINT('Ctrl Pts',(72.4739531683538,0.380210414686311,125.899067567044));
#53148=CARTESIAN_POINT('Ctrl Pts',(72.4664628325918,0.248937617743522,125.892414656445));
#53149=CARTESIAN_POINT('Ctrl Pts',(72.4586884984727,0.112687572805058,125.885509498719));
#53150=CARTESIAN_POINT('Ctrl Pts',(72.4509141643536,-0.024065808326198,
125.884266759137));
#53151=CARTESIAN_POINT('Ctrl Pts',(72.4431398302345,-0.160812520035402,
125.888740372277));
#53152=CARTESIAN_POINT('Ctrl Pts',(72.4353750772874,-0.29739070364355,125.893208472087));
#53153=CARTESIAN_POINT('Ctrl Pts',(72.4276103243403,-0.433961847179008,
125.903378894719));
#53154=CARTESIAN_POINT('Ctrl Pts',(72.4198455713932,-0.570012057168461,
125.919253728543));
#53155=CARTESIAN_POINT('Ctrl Pts',(72.4120885305081,-0.705927140171936,
125.935112795258));
#53156=CARTESIAN_POINT('Ctrl Pts',(72.4043314896231,-0.841321933458148,
125.956664953144));
#53157=CARTESIAN_POINT('Ctrl Pts',(72.3965744487381,-0.975684139345104,
125.983860278106));
#53158=CARTESIAN_POINT('Ctrl Pts',(72.388823257498,-1.10994502164659,126.011035094862));
#53159=CARTESIAN_POINT('Ctrl Pts',(72.3810720662579,-1.24317448482418,126.043844531021));
#53160=CARTESIAN_POINT('Ctrl Pts',(72.3733208750178,-1.37486729739485,126.082187073841));
#53161=CARTESIAN_POINT('Ctrl Pts',(72.3655729782407,-1.50650413700743,126.120513320058));
#53162=CARTESIAN_POINT('Ctrl Pts',(72.3578250814636,-1.63660525042133,126.164367886486));
#53163=CARTESIAN_POINT('Ctrl Pts',(72.3500771846865,-1.76467773327882,126.213598637222));
#53164=CARTESIAN_POINT('Ctrl Pts',(72.3423309086024,-1.89272342613399,126.262819089947));
#53165=CARTESIAN_POINT('Ctrl Pts',(72.3345846325183,-2.01874096777867,126.317413349935));
#53166=CARTESIAN_POINT('Ctrl Pts',(72.3268383564342,-2.14225507935043,126.377180223964));
#53167=CARTESIAN_POINT('Ctrl Pts',(72.3190920231689,-2.26577010267488,126.436947539177));
#53168=CARTESIAN_POINT('Ctrl Pts',(72.3113456899035,-2.38678130712269,126.501887374329));
#53169=CARTESIAN_POINT('Ctrl Pts',(72.3035993566381,-2.50483613592317,126.57175161192));
#53170=CARTESIAN_POINT('Ctrl Pts',(72.2958512886351,-2.62291740228515,126.641631495123));
#53171=CARTESIAN_POINT('Ctrl Pts',(72.288103220632,-2.73804063918003,126.716437776103));
#53172=CARTESIAN_POINT('Ctrl Pts',(72.280355152629,-2.84978084637762,126.795878087965));
#53173=CARTESIAN_POINT('Ctrl Pts',(72.2725988498871,-2.96163981239646,126.875402829934));
#53174=CARTESIAN_POINT('Ctrl Pts',(72.2648425471453,-3.07010824711773,126.959571214311));
#53175=CARTESIAN_POINT('Ctrl Pts',(72.2570862444034,-3.1747924982135,127.048049174703));
#53176=CARTESIAN_POINT('Ctrl Pts',(72.2493258018892,-3.27953262244607,127.136574358446));
#53177=CARTESIAN_POINT('Ctrl Pts',(72.241565359375,-3.3804842509303,127.229413436928));
#53178=CARTESIAN_POINT('Ctrl Pts',(72.2338049168609,-3.47729016418737,127.326194983709));
#53179=CARTESIAN_POINT('Ctrl Pts',(72.2260320165954,-3.57425147889035,127.42313189282));
#53180=CARTESIAN_POINT('Ctrl Pts',(72.21825911633,-3.66705351458595,127.524023629274));
#53181=CARTESIAN_POINT('Ctrl Pts',(72.2104862160645,-3.7553783805642,127.628464479263));
#53182=CARTESIAN_POINT('Ctrl Pts',(72.2029958803027,-3.84049241518525,127.729108641281));
#53183=CARTESIAN_POINT('Ctrl Pts',(72.1955055445408,-3.92144895223041,127.833048115323));
#53184=CARTESIAN_POINT('Ctrl Pts',(72.188015208779,-3.99800238759951,127.939895576542));
#53185=CARTESIAN_POINT('Ctrl Pts',(72.1801680009989,-4.07820315999718,128.051833713311));
#53186=CARTESIAN_POINT('Ctrl Pts',(72.1723207932188,-4.1538238619774,128.167316490552));
#53187=CARTESIAN_POINT('Ctrl Pts',(72.1644735854388,-4.22453841970315,128.285936863915));
#53188=CARTESIAN_POINT('Ctrl Pts',(72.15663976097,-4.29513237466587,128.404354931767));
#53189=CARTESIAN_POINT('Ctrl Pts',(72.1488059365013,-4.36083665984594,128.525899611086));
#53190=CARTESIAN_POINT('Ctrl Pts',(72.1409721120325,-4.42136704575762,128.650133027642));
#53191=CARTESIAN_POINT('Ctrl Pts',(72.1331460284686,-4.48183761925449,128.774243684356));
#53192=CARTESIAN_POINT('Ctrl Pts',(72.1253199449047,-4.53714429870375,128.90103745197));
#53193=CARTESIAN_POINT('Ctrl Pts',(72.1174938613408,-4.58704729095068,129.030049423586));
#53194=CARTESIAN_POINT('Ctrl Pts',(72.1096754184713,-4.63690156233876,129.158935439348));
#53195=CARTESIAN_POINT('Ctrl Pts',(72.1018569756018,-4.68136251686823,129.290034991461));
#53196=CARTESIAN_POINT('Ctrl Pts',(72.0940385327322,-4.72023752319487,129.422861147018));
#53197=CARTESIAN_POINT('Ctrl Pts',(72.0909220069482,-4.73573357037371,129.475807257324));
#53198=CARTESIAN_POINT('Ctrl Pts',(72.0878054811642,-4.75034258938988,129.529027477863));
#53199=CARTESIAN_POINT('Ctrl Pts',(72.0846889553802,-4.76405452823408,129.582490119308));
#53200=CARTESIAN_POINT('Ctrl Pts',(73.8346539883595,-4.76405452823405,129.582490119308));
#53201=CARTESIAN_POINT('Ctrl Pts',(73.8255849805719,-4.80365428175128,129.736888957262));
#53202=CARTESIAN_POINT('Ctrl Pts',(73.8165159727843,-4.83578606109947,129.893377862653));
#53203=CARTESIAN_POINT('Ctrl Pts',(73.8074469649967,-4.86025312007588,130.051285142403));
#53204=CARTESIAN_POINT('Ctrl Pts',(73.7984546414948,-4.88451329435409,130.207857214682));
#53205=CARTESIAN_POINT('Ctrl Pts',(73.7894623179928,-4.9012377478513,130.365823666452));
#53206=CARTESIAN_POINT('Ctrl Pts',(73.7804699944909,-4.91028171654727,130.524509716832));
#53207=CARTESIAN_POINT('Ctrl Pts',(73.7752664750086,-4.91551512116138,130.616335367293));
#53208=CARTESIAN_POINT('Ctrl Pts',(73.7700629555264,-4.91817759325308,130.708401611938));
#53209=CARTESIAN_POINT('Ctrl Pts',(73.7648594360441,-4.91824854295789,130.800574829327));
#53210=CARTESIAN_POINT('',(74.1101405639752,-4.91824993278002,130.803547469765));
#53211=CARTESIAN_POINT('Ctrl Pts',(74.1802344108984,-4.76405452823402,129.582490119308));
#53212=CARTESIAN_POINT('Ctrl Pts',(74.1724725663659,-4.79811559078052,129.715293685228));
#53213=CARTESIAN_POINT('Ctrl Pts',(74.1647107218333,-4.82658990219488,129.849407549553));
#53214=CARTESIAN_POINT('Ctrl Pts',(74.1569488773009,-4.84940405230466,129.984321959946));
#53215=CARTESIAN_POINT('Ctrl Pts',(74.1491751916872,-4.87225300653901,130.119442189005));
#53216=CARTESIAN_POINT('Ctrl Pts',(74.1414015060735,-4.8894245022994,130.255365016246));
#53217=CARTESIAN_POINT('Ctrl Pts',(74.1336278204598,-4.90089705890828,130.391576072695));
#53218=CARTESIAN_POINT('Ctrl Pts',(74.1282717400766,-4.90880166663911,130.485425683252));
#53219=CARTESIAN_POINT('Ctrl Pts',(74.1229156596932,-4.91400195047625,130.579412074753));
#53220=CARTESIAN_POINT('Ctrl Pts',(74.1175595793099,-4.91650525847084,130.673367847046));
#53221=CARTESIAN_POINT('Ctrl Pts',(74.1150865742095,-4.91766108381245,130.716749030201));
#53222=CARTESIAN_POINT('Ctrl Pts',(74.112613569109,-4.91824275702076,130.760145578916));
#53223=CARTESIAN_POINT('Ctrl Pts',(74.1101405640085,-4.91824993277992,130.80354746918));
#53224=CARTESIAN_POINT('Ctrl Pts',(74.1101405639751,-4.91824993278002,130.803547469765));
#53225=CARTESIAN_POINT('Ctrl Pts',(74.1024010897476,-4.9182723898963,130.939377279035));
#53226=CARTESIAN_POINT('Ctrl Pts',(74.0946616155201,-4.91266366247495,131.075431159965));
#53227=CARTESIAN_POINT('Ctrl Pts',(74.0869221412926,-4.90139408870185,131.211200942188));
#53228=CARTESIAN_POINT('Ctrl Pts',(74.0791921512183,-4.89013832495776,131.346804348587));
#53229=CARTESIAN_POINT('Ctrl Pts',(74.071462161144,-4.87323554730515,131.482123959232));
#53230=CARTESIAN_POINT('Ctrl Pts',(74.0637321710696,-4.85070806910426,131.616650153893));
#53231=CARTESIAN_POINT('Ctrl Pts',(74.0560097611196,-4.82820268162847,131.751044430497));
#53232=CARTESIAN_POINT('Ctrl Pts',(74.0482873511696,-4.80008363301125,131.884646452297));
#53233=CARTESIAN_POINT('Ctrl Pts',(74.0405649412196,-4.76642511610775,132.016950686401));
#53234=CARTESIAN_POINT('Ctrl Pts',(74.0328482143336,-4.73279136912823,132.149157555377));
#53235=CARTESIAN_POINT('Ctrl Pts',(74.0251314874476,-4.69362636385047,132.280068156235));
#53236=CARTESIAN_POINT('Ctrl Pts',(74.0174147605616,-4.64905547675876,132.409186538506));
#53237=CARTESIAN_POINT('Ctrl Pts',(74.0097010786887,-4.60450217729633,132.538253970786));
#53238=CARTESIAN_POINT('Ctrl Pts',(74.0019873968157,-4.55454736596363,132.665530218108));
#53239=CARTESIAN_POINT('Ctrl Pts',(73.9942737149428,-4.49936636838801,132.790534161222));
#53240=CARTESIAN_POINT('Ctrl Pts',(73.986561439136,-4.44419542932082,132.915515318354));
#53241=CARTESIAN_POINT('Ctrl Pts',(73.9788491633293,-4.38380035794345,133.038224633974));
#53242=CARTESIAN_POINT('Ctrl Pts',(73.9711368875225,-4.31840457467215,133.158201094733));
#53243=CARTESIAN_POINT('Ctrl Pts',(73.9634243087146,-4.25300622212107,133.278182269147));
#53244=CARTESIAN_POINT('Ctrl Pts',(73.9557117299068,-4.18260695575512,133.395430028371));
#53245=CARTESIAN_POINT('Ctrl Pts',(73.9479991510989,-4.10747587241486,133.509508491533));
#53246=CARTESIAN_POINT('Ctrl Pts',(73.9402845603475,-4.03232518998874,133.623616713798));
#53247=CARTESIAN_POINT('Ctrl Pts',(73.9325699695962,-3.95244045207264,133.734553665618));
#53248=CARTESIAN_POINT('Ctrl Pts',(73.9248553788449,-3.86813347597635,133.841913328966));
#53249=CARTESIAN_POINT('Ctrl Pts',(73.9171325154805,-3.78373609469729,133.949388117661));
#53250=CARTESIAN_POINT('Ctrl Pts',(73.9094096521162,-3.69490724946674,134.05327764649));
#53251=CARTESIAN_POINT('Ctrl Pts',(73.9016867887518,-3.60199865307248,134.153209489307));
#53252=CARTESIAN_POINT('Ctrl Pts',(73.8939594770243,-3.50903654140076,134.253198892787));
#53253=CARTESIAN_POINT('Ctrl Pts',(73.8862321652968,-3.41199027813661,134.349225792332));
#53254=CARTESIAN_POINT('Ctrl Pts',(73.8785048535693,-3.31124685375613,134.44095618705));
#53255=CARTESIAN_POINT('Ctrl Pts',(73.8707657502589,-3.21034969875357,134.53282655885));
#53256=CARTESIAN_POINT('Ctrl Pts',(73.8630266469485,-3.10574441657411,134.620387077677));
#53257=CARTESIAN_POINT('Ctrl Pts',(73.8552875436381,-2.99784983306095,134.70334502904));
#53258=CARTESIAN_POINT('Ctrl Pts',(73.8498956809244,-2.9226792663274,134.761142149303));
#53259=CARTESIAN_POINT('Ctrl Pts',(73.8445038182107,-2.84591271882602,134.816706096356));
#53260=CARTESIAN_POINT('Ctrl Pts',(73.8391119554971,-2.76769911226722,134.86995094204));
#53261=CARTESIAN_POINT('Ctrl Pts',(73.831337621378,-2.65492570865199,134.946722781837));
#53262=CARTESIAN_POINT('Ctrl Pts',(73.8235632872589,-2.53877695497952,135.018920418037));
#53263=CARTESIAN_POINT('Ctrl Pts',(73.8157889531398,-2.41966036953933,135.086232493111));
#53264=CARTESIAN_POINT('Ctrl Pts',(73.8080242001927,-2.30069058464511,135.153461612068));
#53265=CARTESIAN_POINT('Ctrl Pts',(73.8002594472457,-2.17876058260213,135.215816959432));
#53266=CARTESIAN_POINT('Ctrl Pts',(73.7924946942986,-2.05430817147097,135.273029434913));
#53267=CARTESIAN_POINT('Ctrl Pts',(73.7847376534136,-1.92997936822893,135.330185086157));
#53268=CARTESIAN_POINT('Ctrl Pts',(73.7769806125286,-1.80313349447147,135.382207868369));
#53269=CARTESIAN_POINT('Ctrl Pts',(73.7692235716436,-1.67423405116622,135.428873932977));
#53270=CARTESIAN_POINT('Ctrl Pts',(73.7614723804034,-1.54543181193333,135.475504806343));
#53271=CARTESIAN_POINT('Ctrl Pts',(73.7537211891633,-1.41457945170024,135.516786870018));
#53272=CARTESIAN_POINT('Ctrl Pts',(73.7459699979231,-1.28216127183758,135.55254401077));
#53273=CARTESIAN_POINT('Ctrl Pts',(73.7382221011461,-1.14979937323427,135.588285953783));
#53274=CARTESIAN_POINT('Ctrl Pts',(73.730474204369,-1.01587335531616,135.618507542634));
#53275=CARTESIAN_POINT('Ctrl Pts',(73.7227263075919,-0.880883324500299,
135.643082311476));
#53276=CARTESIAN_POINT('Ctrl Pts',(73.7149800315078,-0.745921530688839,
135.667651939807));
#53277=CARTESIAN_POINT('Ctrl Pts',(73.7072337554237,-0.609896551080293,
135.686577027607));
#53278=CARTESIAN_POINT('Ctrl Pts',(73.6994874793396,-0.473318957510143,
135.699782175201));
#53279=CARTESIAN_POINT('Ctrl Pts',(73.6917411460742,-0.336740355755131,
135.712987420274));
#53280=CARTESIAN_POINT('Ctrl Pts',(73.6839948128089,-0.199609521049129,
135.720472603262));
#53281=CARTESIAN_POINT('Ctrl Pts',(73.6762484795435,-0.0624420282957672,
135.722214220064));
#53282=CARTESIAN_POINT('Ctrl Pts',(73.6685004115405,0.0747561821669182,
135.723956226889));
#53283=CARTESIAN_POINT('Ctrl Pts',(73.6607523435376,0.211990676153668,135.719952103112));
#53284=CARTESIAN_POINT('Ctrl Pts',(73.6530042755346,0.348746396004895,135.710230470484));
#53285=CARTESIAN_POINT('Ctrl Pts',(73.6452479727927,0.485647461462126,135.70049850559));
#53286=CARTESIAN_POINT('Ctrl Pts',(73.6374916700509,0.622068345704522,135.685036920874));
#53287=CARTESIAN_POINT('Ctrl Pts',(73.629735367309,0.757499072760819,135.663926258368));
#53288=CARTESIAN_POINT('Ctrl Pts',(73.6219749247949,0.893002083273795,135.642804328466));
#53289=CARTESIAN_POINT('Ctrl Pts',(73.6142144822807,1.02751350031223,135.616027389259));
#53290=CARTESIAN_POINT('Ctrl Pts',(73.6064540397665,1.16053502971884,135.583726842004));
#53291=CARTESIAN_POINT('Ctrl Pts',(73.5986811395011,1.29377009709373,135.551374443042));
#53292=CARTESIAN_POINT('Ctrl Pts',(73.5909082392357,1.42551012151131,135.513480825106));
#53293=CARTESIAN_POINT('Ctrl Pts',(73.5831353389702,1.55527256225537,135.47022713083));
#53294=CARTESIAN_POINT('Ctrl Pts',(73.5756450032082,1.68031781142644,135.428545817289));
#53295=CARTESIAN_POINT('Ctrl Pts',(73.5681546674462,1.80352647292725,135.381887475203));
#53296=CARTESIAN_POINT('Ctrl Pts',(73.5606643316842,1.92448730849223,135.330455143971));
#53297=CARTESIAN_POINT('Ctrl Pts',(73.5528899975651,2.05003441090299,135.277072740268));
#53298=CARTESIAN_POINT('Ctrl Pts',(73.545115663446,2.17355756543163,135.21837809019));
#53299=CARTESIAN_POINT('Ctrl Pts',(73.5373413293269,2.29457454458329,135.154545754069));
#53300=CARTESIAN_POINT('Ctrl Pts',(73.5295765763798,2.41544238112357,135.090792085597));
#53301=CARTESIAN_POINT('Ctrl Pts',(73.5218118234328,2.53380984526579,135.021913510005));
#53302=CARTESIAN_POINT('Ctrl Pts',(73.5140470704857,2.64921388936514,134.948132912335));
#53303=CARTESIAN_POINT('Ctrl Pts',(73.5062900296007,2.76450331254058,134.874425594595));
#53304=CARTESIAN_POINT('Ctrl Pts',(73.4985329887158,2.87683484572569,134.795826153054));
#53305=CARTESIAN_POINT('Ctrl Pts',(73.4907759478308,2.98576962518211,134.712603548582));
#53306=CARTESIAN_POINT('Ctrl Pts',(73.4830247565907,3.09462225607425,134.629443702924));
#53307=CARTESIAN_POINT('Ctrl Pts',(73.4752735653506,3.20008292236485,134.541667870116));
#53308=CARTESIAN_POINT('Ctrl Pts',(73.4675223741105,3.30174167828348,134.449588313113));
#53309=CARTESIAN_POINT('Ctrl Pts',(73.4597744773334,3.40335722651923,134.357547892379));
#53310=CARTESIAN_POINT('Ctrl Pts',(73.4520265805563,3.50117378914889,134.2612076475));
#53311=CARTESIAN_POINT('Ctrl Pts',(73.4442786837792,3.59481464714033,134.160919974289));
#53312=CARTESIAN_POINT('Ctrl Pts',(73.4365324076951,3.68843591748294,134.060653279098));
#53313=CARTESIAN_POINT('Ctrl Pts',(73.428786131611,3.77788295390878,133.956441083553));
#53314=CARTESIAN_POINT('Ctrl Pts',(73.4210398555269,3.86281634398755,133.848672190832));
#53315=CARTESIAN_POINT('Ctrl Pts',(73.4132935222616,3.94775036102526,133.740902502586));
#53316=CARTESIAN_POINT('Ctrl Pts',(73.4055471889962,4.02817042323014,133.629576371842));
#53317=CARTESIAN_POINT('Ctrl Pts',(73.3978008557308,4.10377807510627,133.515114861827));
#53318=CARTESIAN_POINT('Ctrl Pts',(73.3900527877279,4.17940265879176,133.400627718949));
#53319=CARTESIAN_POINT('Ctrl Pts',(73.3823047197249,4.25021247219443,133.283004125769));
#53320=CARTESIAN_POINT('Ctrl Pts',(73.3745566517219,4.3159531943571,133.162692885636));
#53321=CARTESIAN_POINT('Ctrl Pts',(73.3668003489801,4.38176378654169,133.042253777285));
#53322=CARTESIAN_POINT('Ctrl Pts',(73.3590440462383,4.44249433762443,132.919121659523));
#53323=CARTESIAN_POINT('Ctrl Pts',(73.3512877434964,4.49793695542664,132.793769124512));
#53324=CARTESIAN_POINT('Ctrl Pts',(73.3435273009823,4.55340916462324,132.668349685078));
#53325=CARTESIAN_POINT('Ctrl Pts',(73.3357668584681,4.60358767383935,132.540707830658));
#53326=CARTESIAN_POINT('Ctrl Pts',(73.328006415954,4.64831369451026,132.411333815827));
#53327=CARTESIAN_POINT('Ctrl Pts',(73.3202335156885,4.6931115133602,132.281752118341));
#53328=CARTESIAN_POINT('Ctrl Pts',(73.3124606154231,4.73243924051452,132.15043307863));
#53329=CARTESIAN_POINT('Ctrl Pts',(73.3046877151577,4.76618845135738,132.017880583882));
#53330=CARTESIAN_POINT('Ctrl Pts',(73.2971973793955,4.79871079337739,131.890146706196));
#53331=CARTESIAN_POINT('Ctrl Pts',(73.2897070436334,4.8260530998275,131.761267796232));
#53332=CARTESIAN_POINT('Ctrl Pts',(73.2822167078713,4.84816390917852,131.631699588145));
#53333=CARTESIAN_POINT('Ctrl Pts',(73.2744423737522,4.87111305658625,131.497218762069));
#53334=CARTESIAN_POINT('Ctrl Pts',(73.2666680396331,4.8884988674008,131.361569341743));
#53335=CARTESIAN_POINT('Ctrl Pts',(73.258893705514,4.90020754843163,131.225251392938));
#53336=CARTESIAN_POINT('Ctrl Pts',(73.2511289525669,4.91190179955954,131.089101443823));
#53337=CARTESIAN_POINT('Ctrl Pts',(73.2433641996198,4.91793280882639,130.952284991339));
#53338=CARTESIAN_POINT('Ctrl Pts',(73.2355994466727,4.91823780716757,130.815312085393));
#53339=CARTESIAN_POINT('Ctrl Pts',(73.2278424057877,4.91854250258009,130.678475222869));
#53340=CARTESIAN_POINT('Ctrl Pts',(73.2200853649027,4.91313250389666,130.541482604555));
#53341=CARTESIAN_POINT('Ctrl Pts',(73.2123283240177,4.90199687894406,130.404848838863));
#53342=CARTESIAN_POINT('Ctrl Pts',(73.2045771327776,4.89086965145283,130.268318109755));
#53343=CARTESIAN_POINT('Ctrl Pts',(73.1968259415375,4.87402542352043,130.132146082727));
#53344=CARTESIAN_POINT('Ctrl Pts',(73.1890747502973,4.85150532511271,129.996846442518));
#53345=CARTESIAN_POINT('Ctrl Pts',(73.1813268535202,4.8289947983476,129.861604308266));
#53346=CARTESIAN_POINT('Ctrl Pts',(73.1735789567432,4.80081326323675,129.727234208219));
#53347=CARTESIAN_POINT('Ctrl Pts',(73.1658310599661,4.76705357451973,129.594243565311));
#53348=CARTESIAN_POINT('Ctrl Pts',(73.158084783882,4.73330094760181,129.461280741179));
#53349=CARTESIAN_POINT('Ctrl Pts',(73.1503385077979,4.69397258410012,129.329697178945));
#53350=CARTESIAN_POINT('Ctrl Pts',(73.1425922317138,4.64921213443177,129.199988593517));
#53351=CARTESIAN_POINT('Ctrl Pts',(73.1348458984484,4.60445135435186,129.070279050608));
#53352=CARTESIAN_POINT('Ctrl Pts',(73.1270995651831,4.5542585356277,128.942444881702));
#53353=CARTESIAN_POINT('Ctrl Pts',(73.1193532319178,4.49882660819147,128.816964780817));
#53354=CARTESIAN_POINT('Ctrl Pts',(73.1116051639148,4.44338226715946,128.691456579533));
#53355=CARTESIAN_POINT('Ctrl Pts',(73.1038570959118,4.38269664071301,128.568303852849));
#53356=CARTESIAN_POINT('Ctrl Pts',(73.0961090279088,4.31700985313275,128.447963157362));
#53357=CARTESIAN_POINT('Ctrl Pts',(73.0883527251669,4.25125325285301,128.327494562352));
#53358=CARTESIAN_POINT('Ctrl Pts',(73.0805964224251,4.18048506118321,128.209844312428));
#53359=CARTESIAN_POINT('Ctrl Pts',(73.0728401196832,4.10499051249334,128.095442760775));
#53360=CARTESIAN_POINT('Ctrl Pts',(73.0650796771691,4.02945567008975,127.98098014957));
#53361=CARTESIAN_POINT('Ctrl Pts',(73.0573192346549,3.94918967287014,127.869770008497));
#53362=CARTESIAN_POINT('Ctrl Pts',(73.0495587921407,3.86451915679611,127.762210925448));
#53363=CARTESIAN_POINT('Ctrl Pts',(73.0417858918753,3.77971272009299,127.654479179009));
#53364=CARTESIAN_POINT('Ctrl Pts',(73.0340129916099,3.69048788999537,127.550410499726));
#53365=CARTESIAN_POINT('Ctrl Pts',(73.0262400913444,3.59720999491291,127.45036847163));
#53366=CARTESIAN_POINT('Ctrl Pts',(73.0187497555824,3.50732298626972,127.353963223247));
#53367=CARTESIAN_POINT('Ctrl Pts',(73.0112594198204,3.4136726937871,127.26129716758));
#53368=CARTESIAN_POINT('Ctrl Pts',(73.0037690840584,3.31661472330351,127.172659936113));
#53369=CARTESIAN_POINT('Ctrl Pts',(72.9959947499393,3.21587677036862,127.080661997074));
#53370=CARTESIAN_POINT('Ctrl Pts',(72.9882204158202,3.11114852667453,126.992712996937));
#53371=CARTESIAN_POINT('Ctrl Pts',(72.9804460817011,3.00278920371803,126.909178970899));
#53372=CARTESIAN_POINT('Ctrl Pts',(72.972681328754,2.89456342394287,126.825747893082));
#53373=CARTESIAN_POINT('Ctrl Pts',(72.9649165758069,2.78271577544925,126.746721199684));
#53374=CARTESIAN_POINT('Ctrl Pts',(72.9571518228599,2.66764144945669,126.672427394529));
#53375=CARTESIAN_POINT('Ctrl Pts',(72.9493947819749,2.55268141690743,126.598207379028));
#53376=CARTESIAN_POINT('Ctrl Pts',(72.9416377410899,2.43450141085251,126.528711107711));
#53377=CARTESIAN_POINT('Ctrl Pts',(72.933880700205,2.31352847681695,126.464225936539));
#53378=CARTESIAN_POINT('Ctrl Pts',(72.9261295089649,2.19264676941173,126.399789394136));
#53379=CARTESIAN_POINT('Ctrl Pts',(72.9183783177248,2.0689766698402,126.340356613353));
#53380=CARTESIAN_POINT('Ctrl Pts',(72.9106271264847,1.94297258737516,126.286170649536));
#53381=CARTESIAN_POINT('Ctrl Pts',(72.9028792297076,1.81702206000609,126.232007716199));
#53382=CARTESIAN_POINT('Ctrl Pts',(72.8951313329305,1.68873988117719,126.183087318582));
#53383=CARTESIAN_POINT('Ctrl Pts',(72.8873834361534,1.55860315043029,126.139605609855));
#53384=CARTESIAN_POINT('Ctrl Pts',(72.8796371600693,1.42849364148203,126.096132996564));
#53385=CARTESIAN_POINT('Ctrl Pts',(72.8718908839852,1.29653072281361,126.05809693312));
#53386=CARTESIAN_POINT('Ctrl Pts',(72.8641446079011,1.16320909997391,126.025644508375));
#53387=CARTESIAN_POINT('Ctrl Pts',(72.8563982746357,1.0298864929841,125.993191844074));
#53388=CARTESIAN_POINT('Ctrl Pts',(72.8486519413703,0.895205541682873,125.966322993184));
#53389=CARTESIAN_POINT('Ctrl Pts',(72.840905608105,0.75967326824796,125.945134384099));
#53390=CARTESIAN_POINT('Ctrl Pts',(72.833157540102,0.624110643300587,125.923941029973));
#53391=CARTESIAN_POINT('Ctrl Pts',(72.8254094720991,0.487696703052019,125.908430509263));
#53392=CARTESIAN_POINT('Ctrl Pts',(72.8176614040961,0.35094535453753,125.898647578605));
#53393=CARTESIAN_POINT('Ctrl Pts',(72.8099051013542,0.214048665062105,125.888854250532));
#53394=CARTESIAN_POINT('Ctrl Pts',(72.8021487986123,0.0768142415660106,
125.884800700592));
#53395=CARTESIAN_POINT('Ctrl Pts',(72.7943924958705,-0.0602416714836149,
125.88647956944));
#53396=CARTESIAN_POINT('Ctrl Pts',(72.7866320533563,-0.197370735400709,
125.888159334351));
#53397=CARTESIAN_POINT('Ctrl Pts',(72.7788716108422,-0.334320708823159,
125.895577593354));
#53398=CARTESIAN_POINT('Ctrl Pts',(72.771111168328,-0.47057969375474,125.908674984856));
#53399=CARTESIAN_POINT('Ctrl Pts',(72.7633382680626,-0.607057413705437,
125.921793401453));
#53400=CARTESIAN_POINT('Ctrl Pts',(72.7555653677971,-0.742841541070479,
125.940609114821));
#53401=CARTESIAN_POINT('Ctrl Pts',(72.7477924675317,-0.87742871337592,125.965011289873));
#53402=CARTESIAN_POINT('Ctrl Pts',(72.7403021317696,-1.00712330296425,125.988526384397));
#53403=CARTESIAN_POINT('Ctrl Pts',(72.7328117960075,-1.13570615065991,126.017228761194));
#53404=CARTESIAN_POINT('Ctrl Pts',(72.7253214602454,-1.26274136764996,126.050975791894));
#53405=CARTESIAN_POINT('Ctrl Pts',(72.7175471261263,-1.39459316350288,126.086002351521));
#53406=CARTESIAN_POINT('Ctrl Pts',(72.7097727920073,-1.52519532200987,126.12657460615));
#53407=CARTESIAN_POINT('Ctrl Pts',(72.7019984578882,-1.65404572480389,126.172588191943));
#53408=CARTESIAN_POINT('Ctrl Pts',(72.6942337049411,-1.78273733099207,126.218545070104));
#53409=CARTESIAN_POINT('Ctrl Pts',(72.686468951994,-1.90968111234199,126.269929806356));
#53410=CARTESIAN_POINT('Ctrl Pts',(72.6787041990469,-2.03438707877458,126.326587479474));
#53411=CARTESIAN_POINT('Ctrl Pts',(72.670947158162,-2.15896918548292,126.383188879393));
#53412=CARTESIAN_POINT('Ctrl Pts',(72.663190117277,-2.28131754675942,126.445052633331));
#53413=CARTESIAN_POINT('Ctrl Pts',(72.655433076392,-2.40095957335598,126.51197477871));
#53414=CARTESIAN_POINT('Ctrl Pts',(72.6476818851518,-2.52051137697057,126.57884645758));
#53415=CARTESIAN_POINT('Ctrl Pts',(72.6399306939117,-2.63736056829631,126.65076874513));
#53416=CARTESIAN_POINT('Ctrl Pts',(72.6321795026715,-2.751057038676,126.72749071132));
#53417=CARTESIAN_POINT('Ctrl Pts',(72.6244316058945,-2.86470518502214,126.804180068628));
#53418=CARTESIAN_POINT('Ctrl Pts',(72.6166837091173,-2.97520295215812,126.885664828958));
#53419=CARTESIAN_POINT('Ctrl Pts',(72.6089358123402,-3.08212742691119,126.971649620532));
#53420=CARTESIAN_POINT('Ctrl Pts',(72.6011895362561,-3.18902953536932,127.057616425942));
#53421=CARTESIAN_POINT('Ctrl Pts',(72.5934432601721,-3.29235953369525,127.148081145428));
#53422=CARTESIAN_POINT('Ctrl Pts',(72.5856969840879,-3.39172627144004,127.242707074319));
#53423=CARTESIAN_POINT('Ctrl Pts',(72.5779506508226,-3.49109374268744,127.337333701717));
#53424=CARTESIAN_POINT('Ctrl Pts',(72.5702043175573,-3.58649761185007,127.436121330195));
#53425=CARTESIAN_POINT('Ctrl Pts',(72.5624579842919,-3.67758269311653,127.538695509538));
#53426=CARTESIAN_POINT('Ctrl Pts',(72.554709916289,-3.76868817225541,127.641292659658));
#53427=CARTESIAN_POINT('Ctrl Pts',(72.546961848286,-3.85547267940951,127.747677755724));
#53428=CARTESIAN_POINT('Ctrl Pts',(72.539213780283,-3.93762078024857,127.857442625247));
#53429=CARTESIAN_POINT('Ctrl Pts',(72.5314574775412,-4.01985618906673,127.967324154179));
#53430=CARTESIAN_POINT('Ctrl Pts',(72.5237011747993,-4.0974451134704,128.080592318591));
#53431=CARTESIAN_POINT('Ctrl Pts',(72.5159448720574,-4.17011470234065,128.196808809486));
#53432=CARTESIAN_POINT('Ctrl Pts',(72.5081844295432,-4.24282307715867,128.313087328621));
#53433=CARTESIAN_POINT('Ctrl Pts',(72.5004239870291,-4.3106066915869,128.432316970079));
#53434=CARTESIAN_POINT('Ctrl Pts',(72.4926635445149,-4.3732387948454,128.554034973185));
#53435=CARTESIAN_POINT('Ctrl Pts',(72.4848906442495,-4.43597144071613,128.675948368835));
#53436=CARTESIAN_POINT('Ctrl Pts',(72.4771177439841,-4.49353588572341,128.800357753468));
#53437=CARTESIAN_POINT('Ctrl Pts',(72.4693448437187,-4.54575329885191,128.926779724907));
#53438=CARTESIAN_POINT('Ctrl Pts',(72.4618545079567,-4.59607247748532,129.048605939247));
#53439=CARTESIAN_POINT('Ctrl Pts',(72.4543641721947,-4.64142652498172,129.172300666421));
#53440=CARTESIAN_POINT('Ctrl Pts',(72.4468738364327,-4.68169983007849,129.297420086708));
#53441=CARTESIAN_POINT('Ctrl Pts',(72.4412390975458,-4.7119961432934,129.391543405794));
#53442=CARTESIAN_POINT('Ctrl Pts',(72.435604358659,-4.73946555878566,129.486618100619));
#53443=CARTESIAN_POINT('Ctrl Pts',(72.4299696197722,-4.76405452823407,129.582490119308));
#53444=CARTESIAN_POINT('Origin',(213.235140564004,0.,130.804360617566));
#53445=CARTESIAN_POINT('',(70.3350012833218,-4.76405452823407,129.582490119308));
#53446=CARTESIAN_POINT('',(70.6799389637606,-4.76405452823405,129.582490119308));
#53447=CARTESIAN_POINT('',(213.235140564004,-4.76405452823405,129.582490119308));
#53448=CARTESIAN_POINT('',(72.0148594359372,-4.91824905725685,130.807405825623));
#53449=CARTESIAN_POINT('Ctrl Pts',(72.0148594359372,-4.91824905725685,130.807405825623));
#53450=CARTESIAN_POINT('Ctrl Pts',(72.006085115023,-4.91815272426633,130.962991135701));
#53451=CARTESIAN_POINT('Ctrl Pts',(71.9973107941087,-4.91066945928422,131.118299997196));
#53452=CARTESIAN_POINT('Ctrl Pts',(71.9885364731944,-4.8959029357732,131.272674087357));
#53453=CARTESIAN_POINT('Ctrl Pts',(71.9798018354719,-4.88120319609536,131.426349997375));
#53454=CARTESIAN_POINT('Ctrl Pts',(71.9710671977494,-4.8592861090345,131.579099399438));
#53455=CARTESIAN_POINT('Ctrl Pts',(71.9623325600269,-4.83030408212401,131.730290170349));
#53456=CARTESIAN_POINT('Ctrl Pts',(71.9535383975168,-4.80112454856788,131.882511275752));
#53457=CARTESIAN_POINT('Ctrl Pts',(71.9447442350066,-4.76478354229904,132.033152235707));
#53458=CARTESIAN_POINT('Ctrl Pts',(71.9359500724964,-4.72148566284163,132.181588339506));
#53459=CARTESIAN_POINT('Ctrl Pts',(71.9271559099863,-4.67818778338425,132.330024443306));
#53460=CARTESIAN_POINT('Ctrl Pts',(71.9183617474761,-4.62793317195716,132.476255525112));
#53461=CARTESIAN_POINT('Ctrl Pts',(71.909567584966,-4.57097351201412,132.619679932443));
#53462=CARTESIAN_POINT('Ctrl Pts',(71.9017932508469,-4.52061926541078,132.746471910887));
#53463=CARTESIAN_POINT('Ctrl Pts',(71.8940189167278,-4.46490573306048,132.871368003562));
#53464=CARTESIAN_POINT('Ctrl Pts',(71.8862445826088,-4.40399585289402,132.993881932875));
#53465=CARTESIAN_POINT('Ctrl Pts',(71.8784798296617,-4.34316103871114,133.11624487472));
#53466=CARTESIAN_POINT('Ctrl Pts',(71.8707150767146,-4.27714279121172,133.236231147852));
#53467=CARTESIAN_POINT('Ctrl Pts',(71.8629503237675,-4.2061528193853,133.353372489346));
#53468=CARTESIAN_POINT('Ctrl Pts',(71.8551932828825,-4.13523335579972,133.470397484409));
#53469=CARTESIAN_POINT('Ctrl Pts',(71.8474362419976,-4.05935219602026,133.584582838763));
#53470=CARTESIAN_POINT('Ctrl Pts',(71.8396792011126,-3.97876769194306,133.695483360732));
#53471=CARTESIAN_POINT('Ctrl Pts',(71.8319280098725,-3.89824395726725,133.806300251754));
#53472=CARTESIAN_POINT('Ctrl Pts',(71.8241768186323,-3.81302416693415,133.913836925942));
#53473=CARTESIAN_POINT('Ctrl Pts',(71.8164256273922,-3.72341065640713,134.017676062127));
#53474=CARTESIAN_POINT('Ctrl Pts',(71.8086777306151,-3.6338352340126,134.121471063909));
#53475=CARTESIAN_POINT('Ctrl Pts',(71.800929833838,-3.53987006053692,134.221571358023));
#53476=CARTESIAN_POINT('Ctrl Pts',(71.793181937061,-3.44185839009431,134.317591877395));
#53477=CARTESIAN_POINT('Ctrl Pts',(71.7854356609769,-3.34386722158028,134.413592311343));
#53478=CARTESIAN_POINT('Ctrl Pts',(71.7776893848929,-3.24183151881422,134.505514394581));
#53479=CARTESIAN_POINT('Ctrl Pts',(71.7699431088088,-3.13613182804734,134.593009482215));
#53480=CARTESIAN_POINT('Ctrl Pts',(71.7621967755434,-3.03043135702936,134.680505215719));
#53481=CARTESIAN_POINT('Ctrl Pts',(71.7544504422781,-2.92106714521088,134.76357363911));
#53482=CARTESIAN_POINT('Ctrl Pts',(71.7467041090128,-2.80845297245401,134.841906278486));
#53483=CARTESIAN_POINT('Ctrl Pts',(71.7389560410098,-2.69581358053396,134.920256459913));
#53484=CARTESIAN_POINT('Ctrl Pts',(71.7312079730068,-2.57992310031957,134.993868523751));
#53485=CARTESIAN_POINT('Ctrl Pts',(71.7234599050039,-2.461224102916,135.062477452239));
#53486=CARTESIAN_POINT('Ctrl Pts',(71.715703602262,-2.34239895080545,135.131159299112));
#53487=CARTESIAN_POINT('Ctrl Pts',(71.7079472995202,-2.22075965782467,135.19482719261));
#53488=CARTESIAN_POINT('Ctrl Pts',(71.7001909967784,-2.096773691202,135.253261959514));
#53489=CARTESIAN_POINT('Ctrl Pts',(71.6924305542642,-1.97272154953571,135.311727914812));
#53490=CARTESIAN_POINT('Ctrl Pts',(71.6846701117501,-1.84632059867971,135.364955026416));
#53491=CARTESIAN_POINT('Ctrl Pts',(71.6769096692359,-1.71805714154095,135.41277278673));
#53492=CARTESIAN_POINT('Ctrl Pts',(71.6691367689705,-1.58958778451411,135.460667308359));
#53493=CARTESIAN_POINT('Ctrl Pts',(71.6613638687051,-1.45925031845517,135.503135004966));
#53494=CARTESIAN_POINT('Ctrl Pts',(71.6535909684396,-1.32754588355426,135.540055391256));
#53495=CARTESIAN_POINT('Ctrl Pts',(71.6461006326775,-1.20062923660357,135.575633628509));
#53496=CARTESIAN_POINT('Ctrl Pts',(71.6386102969154,-1.07244358054496,135.606060799531));
#53497=CARTESIAN_POINT('Ctrl Pts',(71.6311199611533,-0.943443283358898,
135.631274521251));
#53498=CARTESIAN_POINT('Ctrl Pts',(71.6233456270342,-0.809551900698114,
135.657444228892));
#53499=CARTESIAN_POINT('Ctrl Pts',(71.6155712929151,-0.674358755575522,
135.678080245084));
#53500=CARTESIAN_POINT('Ctrl Pts',(71.607796958796,-0.538361039032828,135.693056809206));
#53501=CARTESIAN_POINT('Ctrl Pts',(71.6000322058489,-0.402530927521401,
135.70801491605));
#53502=CARTESIAN_POINT('Ctrl Pts',(71.5922674529019,-0.265898602388661,
135.717327406151));
#53503=CARTESIAN_POINT('Ctrl Pts',(71.5845026999548,-0.128972460375438,
135.720919288727));
#53504=CARTESIAN_POINT('Ctrl Pts',(71.5767456590698,0.00781768466321653,
135.724507603794));
#53505=CARTESIAN_POINT('Ctrl Pts',(71.5689886181848,0.144900677539574,135.722386608166));
#53506=CARTESIAN_POINT('Ctrl Pts',(71.5612315772998,0.281762320377915,135.714533023634));
#53507=CARTESIAN_POINT('Ctrl Pts',(71.5534803860597,0.418520754786671,135.706685361552));
#53508=CARTESIAN_POINT('Ctrl Pts',(71.5457291948195,0.555057782661346,135.693113737522));
#53509=CARTESIAN_POINT('Ctrl Pts',(71.5379780035794,0.690858880182849,135.673846942649));
#53510=CARTESIAN_POINT('Ctrl Pts',(71.5302301068023,0.826602258615478,135.654588336678));
#53511=CARTESIAN_POINT('Ctrl Pts',(71.5224822100252,0.961609942532017,135.629639429055));
#53512=CARTESIAN_POINT('Ctrl Pts',(71.5147343132482,1.09537242686405,135.599080871029));
#53513=CARTESIAN_POINT('Ctrl Pts',(71.5069880371641,1.22910693096795,135.568528705194));
#53514=CARTESIAN_POINT('Ctrl Pts',(71.49924176108,1.36159637267027,135.532369309967));
#53515=CARTESIAN_POINT('Ctrl Pts',(71.4914954849959,1.49234173260498,135.490734398607));
#53516=CARTESIAN_POINT('Ctrl Pts',(71.4837491517305,1.62308805767215,135.449099179907));
#53517=CARTESIAN_POINT('Ctrl Pts',(71.4760028184652,1.75208990274901,135.401988483051));
#53518=CARTESIAN_POINT('Ctrl Pts',(71.4682564851998,1.87886408188063,135.349583695075));
#53519=CARTESIAN_POINT('Ctrl Pts',(71.4605084171968,2.00566665121076,135.29716717141));
#53520=CARTESIAN_POINT('Ctrl Pts',(71.4527603491939,2.1302402006583,135.239454346796));
#53521=CARTESIAN_POINT('Ctrl Pts',(71.4450122811909,2.25212254278166,135.176674320263));
#53522=CARTESIAN_POINT('Ctrl Pts',(71.4372559784491,2.37413442290857,135.113827570372));
#53523=CARTESIAN_POINT('Ctrl Pts',(71.4294996757072,2.49344903393805,135.045903039794));
#53524=CARTESIAN_POINT('Ctrl Pts',(71.4217433729654,2.60962930177763,134.973175553468));
#53525=CARTESIAN_POINT('Ctrl Pts',(71.4139829304512,2.72587157852443,134.900409250294));
#53526=CARTESIAN_POINT('Ctrl Pts',(71.406222487937,2.83897585643969,134.822835104444));
#53527=CARTESIAN_POINT('Ctrl Pts',(71.3984620454228,2.94853582405441,134.740770092807));
#53528=CARTESIAN_POINT('Ctrl Pts',(71.3906891451574,3.05827166705535,134.658573343128));
#53529=CARTESIAN_POINT('Ctrl Pts',(71.382916244892,3.16445152703313,134.571871568931));
#53530=CARTESIAN_POINT('Ctrl Pts',(71.3751433446266,3.26670315778261,134.481021268406));
#53531=CARTESIAN_POINT('Ctrl Pts',(71.3676530088645,3.36523768419839,134.393473605142));
#53532=CARTESIAN_POINT('Ctrl Pts',(71.3601626731024,3.46012440312911,134.302074011457));
#53533=CARTESIAN_POINT('Ctrl Pts',(71.3526723373404,3.55106523293699,134.207171040426));
#53534=CARTESIAN_POINT('Ctrl Pts',(71.3448980032213,3.64545411194756,134.108669794404));
#53535=CARTESIAN_POINT('Ctrl Pts',(71.3371236691022,3.735890974027,134.006082243358));
#53536=CARTESIAN_POINT('Ctrl Pts',(71.3293493349831,3.82200126930088,133.899758711505));
#53537=CARTESIAN_POINT('Ctrl Pts',(71.321584582036,3.90800544133174,133.793566213903));
#53538=CARTESIAN_POINT('Ctrl Pts',(71.313819829089,3.98969341216099,133.68364719751));
#53539=CARTESIAN_POINT('Ctrl Pts',(71.3060550761419,4.06672728906478,133.570388856553));
#53540=CARTESIAN_POINT('Ctrl Pts',(71.2982980352569,4.14368465483599,133.457243005378));
#53541=CARTESIAN_POINT('Ctrl Pts',(71.2905409943719,4.21599690723227,133.340764751133));
#53542=CARTESIAN_POINT('Ctrl Pts',(71.2827839534869,4.28336652512617,133.221374120617));
#53543=CARTESIAN_POINT('Ctrl Pts',(71.2750327622468,4.35068533906715,133.102073523503));
#53544=CARTESIAN_POINT('Ctrl Pts',(71.2672815710066,4.41306874607118,132.979865260729));
#53545=CARTESIAN_POINT('Ctrl Pts',(71.2595303797665,4.4702628562173,132.85519777805));
#53546=CARTESIAN_POINT('Ctrl Pts',(71.2517824829894,4.52743265734095,132.730583282378));
#53547=CARTESIAN_POINT('Ctrl Pts',(71.2440345862124,4.57941738567087,132.603512000301));
#53548=CARTESIAN_POINT('Ctrl Pts',(71.2362866894353,4.62600949545162,132.474456186835));
#53549=CARTESIAN_POINT('Ctrl Pts',(71.2285404133512,4.67259185916741,132.345427369062));
#53550=CARTESIAN_POINT('Ctrl Pts',(71.2207941372671,4.71378371535038,132.2144152131));
#53551=CARTESIAN_POINT('Ctrl Pts',(71.213047861183,4.74942614593861,132.081910752306));
#53552=CARTESIAN_POINT('Ctrl Pts',(71.2053015279176,4.78506883963114,131.949405313395));
#53553=CARTESIAN_POINT('Ctrl Pts',(71.1975551946522,4.81516192443107,131.815407925216));
#53554=CARTESIAN_POINT('Ctrl Pts',(71.1898088613869,4.83959683257826,131.680423149922));
#53555=CARTESIAN_POINT('Ctrl Pts',(71.1820607933839,4.86403721275371,131.545408145724));
#53556=CARTESIAN_POINT('Ctrl Pts',(71.174312725381,4.88281682524807,131.409405699049));
#53557=CARTESIAN_POINT('Ctrl Pts',(71.166564657378,4.89587859396303,131.272928494906));
#53558=CARTESIAN_POINT('Ctrl Pts',(71.1588083546361,4.90895424488122,131.136306241165));
#53559=CARTESIAN_POINT('Ctrl Pts',(71.1510520518943,4.91629987526594,130.999208611814));
#53560=CARTESIAN_POINT('Ctrl Pts',(71.1432957491525,4.9179104538993,130.862151879258));
#53561=CARTESIAN_POINT('Ctrl Pts',(71.1355353066383,4.91952189214697,130.725021995397));
#53562=CARTESIAN_POINT('Ctrl Pts',(71.1277748641241,4.91539219116826,130.587933442422));
#53563=CARTESIAN_POINT('Ctrl Pts',(71.1200144216099,4.90556841132274,130.451399395429));
#53564=CARTESIAN_POINT('Ctrl Pts',(71.1122415213445,4.8957288614737,130.314646171863));
#53565=CARTESIAN_POINT('Ctrl Pts',(71.104468621079,4.88017701122511,130.178449621732));
#53566=CARTESIAN_POINT('Ctrl Pts',(71.0966957208136,4.8590115844341,130.04331562229));
#53567=CARTESIAN_POINT('Ctrl Pts',(71.0892053850515,4.83861557421938,129.913094084109));
#53568=CARTESIAN_POINT('Ctrl Pts',(71.0817150492895,4.81300709680015,129.783859487195));
#53569=CARTESIAN_POINT('Ctrl Pts',(71.0742247135275,4.78231827934427,129.656051017524));
#53570=CARTESIAN_POINT('Ctrl Pts',(71.0664503794084,4.75046588604696,129.523396650878));
#53571=CARTESIAN_POINT('Ctrl Pts',(71.0586760452893,4.71303940691852,129.391858480325));
#53572=CARTESIAN_POINT('Ctrl Pts',(71.0509017111702,4.67013112628863,129.261940984078));
#53573=CARTESIAN_POINT('Ctrl Pts',(71.0431369582231,4.62727572627983,129.132183599534));
#53574=CARTESIAN_POINT('Ctrl Pts',(71.0353722052761,4.57895208829263,129.00404328287));
#53575=CARTESIAN_POINT('Ctrl Pts',(71.027607452329,4.52530333052641,128.878013600742));
#53576=CARTESIAN_POINT('Ctrl Pts',(71.019850411444,4.47170785746271,128.752109093071));
#53577=CARTESIAN_POINT('Ctrl Pts',(71.0120933705589,4.41279794207661,128.628311405582));
#53578=CARTESIAN_POINT('Ctrl Pts',(71.0043363296739,4.34876614737032,128.507097885969));
#53579=CARTESIAN_POINT('Ctrl Pts',(70.9965851384338,4.28478263953856,128.385975774413));
#53580=CARTESIAN_POINT('Ctrl Pts',(70.9888339471937,4.21568512223401,128.267434296179));
#53581=CARTESIAN_POINT('Ctrl Pts',(70.9810827559535,4.141713651868,128.151929451931));
#53582=CARTESIAN_POINT('Ctrl Pts',(70.9733348591764,4.06777362135009,128.036473700324));
#53583=CARTESIAN_POINT('Ctrl Pts',(70.9655869623994,3.98896396835337,127.924052344245));
#53584=CARTESIAN_POINT('Ctrl Pts',(70.9578390656223,3.90556983084545,127.815095263187));
#53585=CARTESIAN_POINT('Ctrl Pts',(70.9500927895382,3.82219313759333,127.706160973602));
#53586=CARTESIAN_POINT('Ctrl Pts',(70.9423465134541,3.73423410475888,127.600689827934));
#53587=CARTESIAN_POINT('Ctrl Pts',(70.9346002373699,3.64201995351961,127.499080943973));
#53588=CARTESIAN_POINT('Ctrl Pts',(70.9268539041046,3.54980512157643,127.397471309959));
#53589=CARTESIAN_POINT('Ctrl Pts',(70.9191075708392,3.45333537129719,127.299724284058));
#53590=CARTESIAN_POINT('Ctrl Pts',(70.9113612375739,3.35297652158428,127.206203935568));
#53591=CARTESIAN_POINT('Ctrl Pts',(70.9036131695709,3.25259519720282,127.112662643845));
#53592=CARTESIAN_POINT('Ctrl Pts',(70.895865101568,3.1483233262968,127.023350179515));
#53593=CARTESIAN_POINT('Ctrl Pts',(70.888117033565,3.04056139425724,126.938591681086));
#53594=CARTESIAN_POINT('Ctrl Pts',(70.8803607308231,2.93268493155391,126.853743100316));
#53595=CARTESIAN_POINT('Ctrl Pts',(70.8726044280813,2.82131130582427,126.773458395975));
#53596=CARTESIAN_POINT('Ctrl Pts',(70.8648481253394,2.70687215216847,126.698020858813));
#53597=CARTESIAN_POINT('Ctrl Pts',(70.8570876828253,2.5923719188905,126.622543058367));
#53598=CARTESIAN_POINT('Ctrl Pts',(70.849327240311,2.47480323247012,126.551917781302));
#53599=CARTESIAN_POINT('Ctrl Pts',(70.8415667977969,2.35462327892404,126.486382818081));
#53600=CARTESIAN_POINT('Ctrl Pts',(70.8337938975314,2.23425040184753,126.420742652318));
#53601=CARTESIAN_POINT('Ctrl Pts',(70.826020997266,2.11125823200087,126.360209302252));
#53602=CARTESIAN_POINT('Ctrl Pts',(70.8182480970006,1.98612574090169,126.304973147718));
#53603=CARTESIAN_POINT('Ctrl Pts',(70.8107577612386,1.86554213104403,126.251744966532));
#53604=CARTESIAN_POINT('Ctrl Pts',(70.8032674254765,1.74297139698017,126.203435647493));
#53605=CARTESIAN_POINT('Ctrl Pts',(70.7957770897145,1.61885445627116,126.160171419018));
#53606=CARTESIAN_POINT('Ctrl Pts',(70.7880027555954,1.49003158403027,126.115266814171));
#53607=CARTESIAN_POINT('Ctrl Pts',(70.7802284214764,1.35913486962784,126.075655176852));
#53608=CARTESIAN_POINT('Ctrl Pts',(70.7724540873573,1.22663862680702,126.041531548439));
#53609=CARTESIAN_POINT('Ctrl Pts',(70.7646893344102,1.09430567376403,126.007449974348));
#53610=CARTESIAN_POINT('Ctrl Pts',(70.7569245814631,0.960377489529723,125.978843048425));
#53611=CARTESIAN_POINT('Ctrl Pts',(70.749159828516,0.82534668459318,125.955857146109));
#53612=CARTESIAN_POINT('Ctrl Pts',(70.741402787631,0.690449994155701,125.932894073715));
#53613=CARTESIAN_POINT('Ctrl Pts',(70.733645746746,0.554453245317691,125.915540979931));
#53614=CARTESIAN_POINT('Ctrl Pts',(70.725888705861,0.417862129219237,125.903893874136));
#53615=CARTESIAN_POINT('Ctrl Pts',(70.7181375146209,0.281374017543864,125.892255551514));
#53616=CARTESIAN_POINT('Ctrl Pts',(70.7103863233807,0.144292818732098,125.886314685243));
#53617=CARTESIAN_POINT('Ctrl Pts',(70.7026351321406,0.00713193541294979,
125.886115788565));
#53618=CARTESIAN_POINT('Ctrl Pts',(70.6948872353635,-0.129970650871808,
125.885916976423));
#53619=CARTESIAN_POINT('Ctrl Pts',(70.6871393385865,-0.267152464156722,
125.891455280489));
#53620=CARTESIAN_POINT('Ctrl Pts',(70.6793914418094,-0.403897710613602,
125.902723166483));
#53621=CARTESIAN_POINT('Ctrl Pts',(70.6716451657253,-0.540614352912809,
125.913988695478));
#53622=CARTESIAN_POINT('Ctrl Pts',(70.6638988896412,-0.676894220627435,
125.930981390421));
#53623=CARTESIAN_POINT('Ctrl Pts',(70.6561526135571,-0.812224653617011,
125.953641683783));
#53624=CARTESIAN_POINT('Ctrl Pts',(70.6484062802917,-0.9475560855851,125.976302144419));
#53625=CARTESIAN_POINT('Ctrl Pts',(70.6406599470264,-1.08193768324619,126.004630222391));
#53626=CARTESIAN_POINT('Ctrl Pts',(70.6329136137611,-1.21486541073539,126.038514932244));
#53627=CARTESIAN_POINT('Ctrl Pts',(70.6251655457581,-1.34782290646742,126.072407230344));
#53628=CARTESIAN_POINT('Ctrl Pts',(70.6174174777551,-1.47932550537516,126.111858539921));
#53629=CARTESIAN_POINT('Ctrl Pts',(70.6096694097522,-1.60888318708784,126.15670766658));
#53630=CARTESIAN_POINT('Ctrl Pts',(70.6019131070103,-1.73857856424649,126.201604459425));
#53631=CARTESIAN_POINT('Ctrl Pts',(70.5941568042685,-1.86632452494904,126.251910401257));
#53632=CARTESIAN_POINT('Ctrl Pts',(70.5864005015266,-1.99164941934777,126.307415470812));
#53633=CARTESIAN_POINT('Ctrl Pts',(70.5786400590125,-2.1170412034161,126.362950165095));
#53634=CARTESIAN_POINT('Ctrl Pts',(70.5708796164983,-2.24000899600728,126.423689343327));
#53635=CARTESIAN_POINT('Ctrl Pts',(70.5631191739841,-2.36010561706203,126.489376893516));
#53636=CARTESIAN_POINT('Ctrl Pts',(70.5553462737187,-2.48039502787466,126.555169891193));
#53637=CARTESIAN_POINT('Ctrl Pts',(70.5475733734533,-2.59780372173181,126.625926932684));
#53638=CARTESIAN_POINT('Ctrl Pts',(70.5398004731878,-2.71191263088104,126.701347950638));
#53639=CARTESIAN_POINT('Ctrl Pts',(70.5323101374258,-2.82187339375954,126.774027224616));
#53640=CARTESIAN_POINT('Ctrl Pts',(70.5248198016638,-2.92876986777689,126.851037087606));
#53641=CARTESIAN_POINT('Ctrl Pts',(70.5173294659018,-3.03225752667745,126.932074812721));
#53642=CARTESIAN_POINT('Ctrl Pts',(70.5096504214894,-3.13835241401994,127.015154171244));
#53643=CARTESIAN_POINT('Ctrl Pts',(70.5019713770771,-3.24121802712842,127.102744192016));
#53644=CARTESIAN_POINT('Ctrl Pts',(70.4942923326647,-3.34043953367328,127.19456189958));
#53645=CARTESIAN_POINT('Ctrl Pts',(70.4866220665762,-3.43954761484029,127.286274645442));
#53646=CARTESIAN_POINT('Ctrl Pts',(70.4789518004876,-3.53501957954672,127.382205201285));
#53647=CARTESIAN_POINT('Ctrl Pts',(70.4712815343991,-3.62647104661938,127.482028483277));
#53648=CARTESIAN_POINT('Ctrl Pts',(70.463618277831,-3.71783894019916,127.58176054114));
#53649=CARTESIAN_POINT('Ctrl Pts',(70.4559550212629,-3.80519337265196,127.685377958043));
#53650=CARTESIAN_POINT('Ctrl Pts',(70.4482917646948,-3.88818484862489,127.792517054991));
#53651=CARTESIAN_POINT('Ctrl Pts',(70.4406337551094,-3.9711195008654,127.899582794485));
#53652=CARTESIAN_POINT('Ctrl Pts',(70.432975745524,-4.04969689349164,128.010165102239));
#53653=CARTESIAN_POINT('Ctrl Pts',(70.4253177359387,-4.12360643396907,128.123865693074));
#53654=CARTESIAN_POINT('Ctrl Pts',(70.4176622211966,-4.19749189603343,128.237529242279));
#53655=CARTESIAN_POINT('Ctrl Pts',(70.4100067064544,-4.26671230702162,128.354308721683));
#53656=CARTESIAN_POINT('Ctrl Pts',(70.4023511917123,-4.33099942319238,128.473775485285));
#53657=CARTESIAN_POINT('Ctrl Pts',(70.3946973965434,-4.39527209926215,128.593215414396));
#53658=CARTESIAN_POINT('Ctrl Pts',(70.3870436013745,-4.45461349788046,128.715341072046));
#53659=CARTESIAN_POINT('Ctrl Pts',(70.3793898062057,-4.50880088122335,128.839698388077));
#53660=CARTESIAN_POINT('Ctrl Pts',(70.3717331260633,-4.56300868961845,128.964102578575));
#53661=CARTESIAN_POINT('Ctrl Pts',(70.3640764459209,-4.61205843806267,129.090739741065));
#53662=CARTESIAN_POINT('Ctrl Pts',(70.3564197657785,-4.65577518997623,129.219134941865));
#53663=CARTESIAN_POINT('Ctrl Pts',(70.3492802716263,-4.69653900521189,129.338857428406));
#53664=CARTESIAN_POINT('Ctrl Pts',(70.342140777474,-4.7326663351914,129.460108031017));
#53665=CARTESIAN_POINT('Ctrl Pts',(70.3350012833217,-4.76405452823407,129.582490119308));
#53666=CARTESIAN_POINT('Ctrl Pts',(72.0846889553802,-4.76405452823408,129.582490119308));
#53667=CARTESIAN_POINT('Ctrl Pts',(72.0768771839665,-4.79842438085585,129.716497653045));
#53668=CARTESIAN_POINT('Ctrl Pts',(72.0690654125529,-4.8271544673346,129.852029213444));
#53669=CARTESIAN_POINT('Ctrl Pts',(72.0612536411393,-4.85012136542963,129.988575227219));
#53670=CARTESIAN_POINT('Ctrl Pts',(72.0534433806316,-4.873083821405,130.125094831084));
#53671=CARTESIAN_POINT('Ctrl Pts',(72.0456331201239,-4.89028523801872,130.262628122795));
#53672=CARTESIAN_POINT('Ctrl Pts',(72.0378228596163,-4.90165330297286,130.400655329075));
#53673=CARTESIAN_POINT('Ctrl Pts',(72.0301683850745,-4.91279461685024,130.535929400343));
#53674=CARTESIAN_POINT('Ctrl Pts',(72.0225139105328,-4.91833309546384,130.671677509427));
#53675=CARTESIAN_POINT('Ctrl Pts',(72.0148594359911,-4.91824905725744,130.807405824667));
#53676=CARTESIAN_POINT('',(72.3601405640541,-4.91824826462081,130.80022902533));
#53677=CARTESIAN_POINT('Ctrl Pts',(72.4299696197722,-4.76405452823407,129.582490119308));
#53678=CARTESIAN_POINT('Ctrl Pts',(72.420648395519,-4.804730645262,129.741085682254));
#53679=CARTESIAN_POINT('Ctrl Pts',(72.4113271712659,-4.83752185098372,129.901864273602));
#53680=CARTESIAN_POINT('Ctrl Pts',(72.4020059470127,-4.86222315289459,130.064111285276));
#53681=CARTESIAN_POINT('Ctrl Pts',(72.3927861825788,-4.88665558565701,130.224592267936));
#53682=CARTESIAN_POINT('Ctrl Pts',(72.3835664181449,-4.90317321832964,130.386509839184));
#53683=CARTESIAN_POINT('Ctrl Pts',(72.374346653711,-4.91162412170554,130.549151782334));
#53684=CARTESIAN_POINT('Ctrl Pts',(72.369611290492,-4.91596459019584,130.632686310898));
#53685=CARTESIAN_POINT('Ctrl Pts',(72.364875927273,-4.91817785348301,130.716411592138));
#53686=CARTESIAN_POINT('Ctrl Pts',(72.3601405640541,-4.91824826462081,130.800229025329));
#53687=CARTESIAN_POINT('Ctrl Pts',(72.3601405640086,-4.91824826462148,130.800229026135));
#53688=CARTESIAN_POINT('Ctrl Pts',(72.3521524660341,-4.91836704135129,130.941620897751));
#53689=CARTESIAN_POINT('Ctrl Pts',(72.3441643680595,-4.91238371391025,131.083109084369));
#53690=CARTESIAN_POINT('Ctrl Pts',(72.336176270085,-4.90030416846064,131.224124978925));
#53691=CARTESIAN_POINT('Ctrl Pts',(72.328463029565,-4.88864026051642,131.360288745984));
#53692=CARTESIAN_POINT('Ctrl Pts',(72.3207497890451,-4.87129276819467,131.496011763084));
#53693=CARTESIAN_POINT('Ctrl Pts',(72.3130365485251,-4.84831995643009,131.630784638624));
#53694=CARTESIAN_POINT('Ctrl Pts',(72.3053236522739,-4.82534817002179,131.765551498783));
#53695=CARTESIAN_POINT('Ctrl Pts',(72.2976107560226,-4.79675162952417,131.899367912903));
#53696=CARTESIAN_POINT('Ctrl Pts',(72.2898978597713,-4.76264004127198,132.031732973362));
#53697=CARTESIAN_POINT('Ctrl Pts',(72.2821836032061,-4.7285224368013,132.164121378883));
#53698=CARTESIAN_POINT('Ctrl Pts',(72.2744693466409,-4.68888794776022,132.295057539556));
#53699=CARTESIAN_POINT('Ctrl Pts',(72.2667550900757,-4.64389651894893,132.424054472526));
#53700=CARTESIAN_POINT('Ctrl Pts',(72.2590377680226,-4.59888721146346,132.55310266624));
#53701=CARTESIAN_POINT('Ctrl Pts',(72.2513204459696,-4.54851685859578,132.68020972698));
#53702=CARTESIAN_POINT('Ctrl Pts',(72.2436031239165,-4.49299385105062,132.804907871925));
#53703=CARTESIAN_POINT('Ctrl Pts',(72.2358767886456,-4.43740599705268,132.929751654375));
#53704=CARTESIAN_POINT('Ctrl Pts',(72.2281504533747,-4.37665363631315,133.052180544785));
#53705=CARTESIAN_POINT('Ctrl Pts',(72.2204241181038,-4.31099167701347,133.17175028199));
#53706=CARTESIAN_POINT('Ctrl Pts',(72.2126924048926,-4.24528401349726,133.291403246093));
#53707=CARTESIAN_POINT('Ctrl Pts',(72.2049606916814,-4.17466014955658,133.408192757649));
#53708=CARTESIAN_POINT('Ctrl Pts',(72.1972289784701,-4.09941814286994,133.521703796557));
#53709=CARTESIAN_POINT('Ctrl Pts',(72.1894861168925,-4.02406764464513,133.635378507166));
#53710=CARTESIAN_POINT('Ctrl Pts',(72.1817432553149,-3.9440859441397,133.745764992871));
#53711=CARTESIAN_POINT('Ctrl Pts',(72.1740003937372,-3.85981134077771,133.852481264145));
#53712=CARTESIAN_POINT('Ctrl Pts',(72.1721423333647,-3.83958790021258,133.878090048801));
#53713=CARTESIAN_POINT('Ctrl Pts',(72.1702842729921,-3.81911741400135,133.90348764891));
#53714=CARTESIAN_POINT('Ctrl Pts',(72.1684262126196,-3.7984048624164,133.928669111244));
#53715=CARTESIAN_POINT('Ctrl Pts',(72.1606518785005,-3.71174121097692,134.034031189185));
#53716=CARTESIAN_POINT('Ctrl Pts',(72.1528775443814,-3.6205530881804,134.135951540015));
#53717=CARTESIAN_POINT('Ctrl Pts',(72.1451032102623,-3.52514412859453,134.234016859106));
#53718=CARTESIAN_POINT('Ctrl Pts',(72.1373384573153,-3.42985275202453,134.331961321456));
#53719=CARTESIAN_POINT('Ctrl Pts',(72.1295737043682,-3.33035115872052,134.426059927572));
#53720=CARTESIAN_POINT('Ctrl Pts',(72.1218089514211,-3.22698392472551,134.515931418731));
#53721=CARTESIAN_POINT('Ctrl Pts',(72.1140519105361,-3.12371935652432,134.605713648259));
#53722=CARTESIAN_POINT('Ctrl Pts',(72.1062948696511,-3.01659708136271,134.691276863034));
#53723=CARTESIAN_POINT('Ctrl Pts',(72.0985378287661,-2.90599904628351,134.772276015543));
#53724=CARTESIAN_POINT('Ctrl Pts',(72.090786637526,-2.79548441404283,134.85321408596));
#53725=CARTESIAN_POINT('Ctrl Pts',(72.0830354462858,-2.68149955316458,134.929594714724));
#53726=CARTESIAN_POINT('Ctrl Pts',(72.0752842550457,-2.56445978396509,135.001112823609));
#53727=CARTESIAN_POINT('Ctrl Pts',(72.0675363582686,-2.44746975978988,135.07260053539));
#53728=CARTESIAN_POINT('Ctrl Pts',(72.0597884614916,-2.32742774265982,135.139229634374));
#53729=CARTESIAN_POINT('Ctrl Pts',(72.0520405647145,-2.20477816915101,135.200738250042));
#53730=CARTESIAN_POINT('Ctrl Pts',(72.0442942886304,-2.08215425128896,135.262233999434));
#53731=CARTESIAN_POINT('Ctrl Pts',(72.0365480125463,-1.95692421122605,135.318611220823));
#53732=CARTESIAN_POINT('Ctrl Pts',(72.0288017364622,-1.82955687580346,135.369654113137));
#53733=CARTESIAN_POINT('Ctrl Pts',(72.0210554031969,-1.70218860018439,135.420697382237));
#53734=CARTESIAN_POINT('Ctrl Pts',(72.0133090699315,-1.57268336063143,135.466406098253));
#53735=CARTESIAN_POINT('Ctrl Pts',(72.0055627366662,-1.4415293648972,135.506612860124));
#53736=CARTESIAN_POINT('Ctrl Pts',(71.9978146686632,-1.31034599813435,135.546828626021));
#53737=CARTESIAN_POINT('Ctrl Pts',(71.9900666006602,-1.1775135141936,135.581539871419));
#53738=CARTESIAN_POINT('Ctrl Pts',(71.9823185326572,-1.04353426844288,135.610629367135));
#53739=CARTESIAN_POINT('Ctrl Pts',(71.9745622299154,-0.909412627955762,
135.639749779513));
#53740=CARTESIAN_POINT('Ctrl Pts',(71.9668059271736,-0.774142173662908,
135.663236423692));
#53741=CARTESIAN_POINT('Ctrl Pts',(71.9590496244317,-0.638234970176708,
135.681023327385));
#53742=CARTESIAN_POINT('Ctrl Pts',(71.9512891819175,-0.50225522892355,135.698819724485));
#53743=CARTESIAN_POINT('Ctrl Pts',(71.9435287394034,-0.365638450545266,
135.710910284962));
#53744=CARTESIAN_POINT('Ctrl Pts',(71.9357682968892,-0.228899776495294,
135.717281129321));
#53745=CARTESIAN_POINT('Ctrl Pts',(71.9279953966238,-0.0919415973870206,
135.723662200725));
#53746=CARTESIAN_POINT('Ctrl Pts',(71.9202224963584,0.0451384772335222,
135.724305206021));
#53747=CARTESIAN_POINT('Ctrl Pts',(71.912449596093,0.181826450764625,135.719248429541));
#53748=CARTESIAN_POINT('Ctrl Pts',(71.9049592603309,0.313545472161917,135.714375479623));
#53749=CARTESIAN_POINT('Ctrl Pts',(71.8974689245689,0.44490009815809,135.704209979903));
#53750=CARTESIAN_POINT('Ctrl Pts',(71.8899785888068,0.575438611413163,135.688831261044));
#53751=CARTESIAN_POINT('Ctrl Pts',(71.8822042546877,0.710926532074436,135.672869453384));
#53752=CARTESIAN_POINT('Ctrl Pts',(71.8744299205686,0.845964417527061,135.65124074226));
#53753=CARTESIAN_POINT('Ctrl Pts',(71.8666555864496,0.980040420982166,135.623977182786));
#53754=CARTESIAN_POINT('Ctrl Pts',(71.8588908335025,1.11395118774573,135.596747223212));
#53755=CARTESIAN_POINT('Ctrl Pts',(71.8511260805554,1.24690205172469,135.563896309825));
#53756=CARTESIAN_POINT('Ctrl Pts',(71.8433613276083,1.37838599738973,135.525508264558));
#53757=CARTESIAN_POINT('Ctrl Pts',(71.8356042867233,1.50973935134625,135.487158346839));
#53758=CARTESIAN_POINT('Ctrl Pts',(71.8278472458383,1.63962831354438,135.443282350468));
#53759=CARTESIAN_POINT('Ctrl Pts',(71.8200902049533,1.76755613403222,135.394015111702));
#53760=CARTESIAN_POINT('Ctrl Pts',(71.8123390137131,1.89538748315593,135.344785025744));
#53761=CARTESIAN_POINT('Ctrl Pts',(71.804587822473,2.02126027088641,135.290171929615));
#53762=CARTESIAN_POINT('Ctrl Pts',(71.7968366312328,2.14469333549757,135.230360341829));
#53763=CARTESIAN_POINT('Ctrl Pts',(71.7890887344558,2.26807393776324,135.170574175562));
#53764=CARTESIAN_POINT('Ctrl Pts',(71.7813408376787,2.38901652822067,135.105594082291));
#53765=CARTESIAN_POINT('Ctrl Pts',(71.7735929409016,2.50706055896076,135.035652431682));
#53766=CARTESIAN_POINT('Ctrl Pts',(71.7658466648175,2.62507989743435,134.965725411358));
#53767=CARTESIAN_POINT('Ctrl Pts',(71.7581003887334,2.74020154604287,134.890839097205));
#53768=CARTESIAN_POINT('Ctrl Pts',(71.7503541126493,2.85199053287238,134.811271280771));
#53769=CARTESIAN_POINT('Ctrl Pts',(71.7426077793839,2.96378034490288,134.731702876986));
#53770=CARTESIAN_POINT('Ctrl Pts',(71.7348614461186,3.07223712754459,134.647453128674));
#53771=CARTESIAN_POINT('Ctrl Pts',(71.7271151128532,3.17695615333055,134.558842294484));
#53772=CARTESIAN_POINT('Ctrl Pts',(71.7193670448502,3.28169863021613,134.470211616513));
#53773=CARTESIAN_POINT('Ctrl Pts',(71.7116189768472,3.38270138622691,134.377218161769));
#53774=CARTESIAN_POINT('Ctrl Pts',(71.7038709088443,3.47959425778319,134.280221210815));
#53775=CARTESIAN_POINT('Ctrl Pts',(71.6961146061024,3.57659010823639,134.183121170347));
#53776=CARTESIAN_POINT('Ctrl Pts',(71.6883583033606,3.66946707187015,134.082009410964));
#53777=CARTESIAN_POINT('Ctrl Pts',(71.6806020006187,3.75789286090079,133.977281087494));
#53778=CARTESIAN_POINT('Ctrl Pts',(71.6728415581046,3.84636584543755,133.872496867365));
#53779=CARTESIAN_POINT('Ctrl Pts',(71.6650811155904,3.93038268215294,133.764092545794));
#53780=CARTESIAN_POINT('Ctrl Pts',(71.6573206730762,4.00965324729545,133.652494023668));
#53781=CARTESIAN_POINT('Ctrl Pts',(71.6495477728108,4.08905106458643,133.540716353687));
#53782=CARTESIAN_POINT('Ctrl Pts',(71.6417748725454,4.16368717185269,133.425734564668));
#53783=CARTESIAN_POINT('Ctrl Pts',(71.6340019722799,4.23331595106767,133.308001790126));
#53784=CARTESIAN_POINT('Ctrl Pts',(71.6265116365179,4.30041354877379,133.194548898489));
#53785=CARTESIAN_POINT('Ctrl Pts',(71.6190213007559,4.36286140982298,133.078541830577));
#53786=CARTESIAN_POINT('Ctrl Pts',(71.6115309649939,4.4204821130932,132.960403509144));
#53787=CARTESIAN_POINT('Ctrl Pts',(71.6037566308748,4.48028752284144,132.837785937345));
#53788=CARTESIAN_POINT('Ctrl Pts',(71.5959822967557,4.53508195118663,132.712483893169));
#53789=CARTESIAN_POINT('Ctrl Pts',(71.5882079626366,4.58461570131261,132.584945334387));
#53790=CARTESIAN_POINT('Ctrl Pts',(71.5804432096895,4.63408840551846,132.457563955481));
#53791=CARTESIAN_POINT('Ctrl Pts',(71.5726784567425,4.67831319118628,132.327951907138));
#53792=CARTESIAN_POINT('Ctrl Pts',(71.5649137037954,4.71708652580282,132.196581063684));
#53793=CARTESIAN_POINT('Ctrl Pts',(71.5571566629104,4.75582135019678,132.065340699604));
#53794=CARTESIAN_POINT('Ctrl Pts',(71.5493996220255,4.78911538860001,131.932345389292));
#53795=CARTESIAN_POINT('Ctrl Pts',(71.5416425811405,4.81681357708976,131.798085944839));
#53796=CARTESIAN_POINT('Ctrl Pts',(71.5338913899004,4.84449087816003,131.663927746478));
#53797=CARTESIAN_POINT('Ctrl Pts',(71.5261401986602,4.86658065004571,131.528507692802));
#53798=CARTESIAN_POINT('Ctrl Pts',(71.5183890074202,4.88297805373112,131.392330335562));
#53799=CARTESIAN_POINT('Ctrl Pts',(71.5106411106431,4.89936848808262,131.256210857331));
#53800=CARTESIAN_POINT('Ctrl Pts',(71.502893213866,4.91007131961105,131.119335103067));
#53801=CARTESIAN_POINT('Ctrl Pts',(71.4951453170889,4.91503311010378,130.98221614625));
#53802=CARTESIAN_POINT('Ctrl Pts',(71.4873990410048,4.91999386269691,130.845125871764));
#53803=CARTESIAN_POINT('Ctrl Pts',(71.4796527649208,4.91921594878504,130.707792886375));
#53804=CARTESIAN_POINT('Ctrl Pts',(71.4719064888367,4.91269796932078,130.570733297393));
#53805=CARTESIAN_POINT('Ctrl Pts',(71.4641601555713,4.9061799417423,130.433672696667));
#53806=CARTESIAN_POINT('Ctrl Pts',(71.456413822306,4.89392178263315,130.296885886899));
#53807=CARTESIAN_POINT('Ctrl Pts',(71.4486674890406,4.87597416958209,130.160886484389));
#53808=CARTESIAN_POINT('Ctrl Pts',(71.4409194210377,4.85802253728749,130.024856625755));
#53809=CARTESIAN_POINT('Ctrl Pts',(71.4331713530347,4.8343789668538,129.889614912796));
#53810=CARTESIAN_POINT('Ctrl Pts',(71.4254232850317,4.80514564873579,129.755666974534));
#53811=CARTESIAN_POINT('Ctrl Pts',(71.4176669822898,4.77588126109942,129.621576674809));
#53812=CARTESIAN_POINT('Ctrl Pts',(71.409910679548,4.74101534178669,129.488783279153));
#53813=CARTESIAN_POINT('Ctrl Pts',(71.4021543768062,4.70070073608266,129.357779941526));
#53814=CARTESIAN_POINT('Ctrl Pts',(71.394393934292,4.66036461325975,129.226706683474));
#53815=CARTESIAN_POINT('Ctrl Pts',(71.3866334917779,4.61457413982189,129.097425755532));
#53816=CARTESIAN_POINT('Ctrl Pts',(71.3788730492637,4.56353081927382,128.970411456864));
#53817=CARTESIAN_POINT('Ctrl Pts',(71.3711001489983,4.51240555945615,128.843193263568));
#53818=CARTESIAN_POINT('Ctrl Pts',(71.3633272487328,4.45601076296702,128.71824932717));
#53819=CARTESIAN_POINT('Ctrl Pts',(71.3555543484674,4.39459490132233,128.596031222804));
#53820=CARTESIAN_POINT('Ctrl Pts',(71.3480640127053,4.3354116609449,128.478256054378));
#53821=CARTESIAN_POINT('Ctrl Pts',(71.3405736769432,4.27156622349005,128.363012246424));
#53822=CARTESIAN_POINT('Ctrl Pts',(71.333083341181,4.20331850539734,128.250677668435));
#53823=CARTESIAN_POINT('Ctrl Pts',(71.3253090070619,4.13248315433055,128.134083890778));
#53824=CARTESIAN_POINT('Ctrl Pts',(71.3175346729429,4.05668072277566,128.020254970803));
#53825=CARTESIAN_POINT('Ctrl Pts',(71.3097603388238,3.97615312306491,127.909643117629));
#53826=CARTESIAN_POINT('Ctrl Pts',(71.3019955858767,3.8957247664239,127.799167583679));
#53827=CARTESIAN_POINT('Ctrl Pts',(71.2942308329296,3.81058305625279,127.691901540906));
#53828=CARTESIAN_POINT('Ctrl Pts',(71.2864660799825,3.72101497949097,127.588271286577));
#53829=CARTESIAN_POINT('Ctrl Pts',(71.2787090390975,3.63153586300561,127.484743959277));
#53830=CARTESIAN_POINT('Ctrl Pts',(71.2709519982125,3.53763938282546,127.384845528017));
#53831=CARTESIAN_POINT('Ctrl Pts',(71.2631949573274,3.43965465722664,127.288971748391));
#53832=CARTESIAN_POINT('Ctrl Pts',(71.2554437660873,3.34174382267147,127.193170267928));
#53833=CARTESIAN_POINT('Ctrl Pts',(71.2476925748472,3.23975115749493,127.101387670395));
#53834=CARTESIAN_POINT('Ctrl Pts',(71.2399413836071,3.13404448732548,127.01398488237));
#53835=CARTESIAN_POINT('Ctrl Pts',(71.23219348683,3.02838274531089,126.926619242861));
#53836=CARTESIAN_POINT('Ctrl Pts',(71.2244455900528,2.91901043859797,126.843629959021));
#53837=CARTESIAN_POINT('Ctrl Pts',(71.2166976932758,2.80633034577734,126.765339318678));
#53838=CARTESIAN_POINT('Ctrl Pts',(71.2089514171917,2.69367382320295,126.68706505505));
#53839=CARTESIAN_POINT('Ctrl Pts',(71.2012051411076,2.57771121165227,126.613487702908));
#53840=CARTESIAN_POINT('Ctrl Pts',(71.1934588650235,2.45887597060068,126.544887407919));
#53841=CARTESIAN_POINT('Ctrl Pts',(71.1857125317581,2.34003985233441,126.476286606537));
#53842=CARTESIAN_POINT('Ctrl Pts',(71.1779661984928,2.21833140085124,126.412663131081));
#53843=CARTESIAN_POINT('Ctrl Pts',(71.1702198652274,2.09421012856732,126.354251967218));
#53844=CARTESIAN_POINT('Ctrl Pts',(71.1624717972245,1.97006106018539,126.295827722579));
#53845=CARTESIAN_POINT('Ctrl Pts',(71.1547237292215,1.8434984494833,126.242618278689));
#53846=CARTESIAN_POINT('Ctrl Pts',(71.1469756612185,1.71500293291465,126.194810964661));
#53847=CARTESIAN_POINT('Ctrl Pts',(71.1392193584767,1.58637084978152,126.146952840451));
#53848=CARTESIAN_POINT('Ctrl Pts',(71.1314630557349,1.45580212407566,126.104508451812));
#53849=CARTESIAN_POINT('Ctrl Pts',(71.123706752993,1.32379427680081,126.067615767438));
#53850=CARTESIAN_POINT('Ctrl Pts',(71.1159463104788,1.19171597296336,126.030703392328));
#53851=CARTESIAN_POINT('Ctrl Pts',(71.1081858679647,1.05819739747268,125.999348715071));
#53852=CARTESIAN_POINT('Ctrl Pts',(71.1004254254505,0.923746509212891,125.973638575343));
#53853=CARTESIAN_POINT('Ctrl Pts',(71.0926525251851,0.789079788451096,125.947887163417));
#53854=CARTESIAN_POINT('Ctrl Pts',(71.0848796249197,0.653478151141005,125.927798453338));
#53855=CARTESIAN_POINT('Ctrl Pts',(71.0771067246542,0.517455825156352,125.913407486375));
#53856=CARTESIAN_POINT('Ctrl Pts',(71.0696163888922,0.386378253340808,125.899539667309));
#53857=CARTESIAN_POINT('Ctrl Pts',(71.0621260531302,0.254910355380659,125.890962548851));
#53858=CARTESIAN_POINT('Ctrl Pts',(71.0546357173681,0.123510534766719,125.88766170363));
#53859=CARTESIAN_POINT('Ctrl Pts',(71.0468613832491,-0.0128713499838206,
125.884235705859));
#53860=CARTESIAN_POINT('Ctrl Pts',(71.03908704913,-0.14961190999431,125.88648312669));
#53861=CARTESIAN_POINT('Ctrl Pts',(71.0313127150109,-0.286199929399382,
125.894444868501));
#53862=CARTESIAN_POINT('Ctrl Pts',(71.0235479620638,-0.422619616277758,
125.902396798178));
#53863=CARTESIAN_POINT('Ctrl Pts',(71.0157832091168,-0.558886750044252,
125.916049014046));
#53864=CARTESIAN_POINT('Ctrl Pts',(71.0080184561697,-0.694487551284044,
125.935390489951));
#53865=CARTESIAN_POINT('Ctrl Pts',(71.0002614152847,-0.82995367189604,125.954712755629));
#53866=CARTESIAN_POINT('Ctrl Pts',(70.9925043743997,-0.964754392471565,
125.97971298144));
#53867=CARTESIAN_POINT('Ctrl Pts',(70.9847473335147,-1.09837885615307,126.010328186422));
#53868=CARTESIAN_POINT('Ctrl Pts',(70.9769961422746,-1.23190255258751,126.040920304241));
#53869=CARTESIAN_POINT('Ctrl Pts',(70.9692449510345,-1.36425137814753,126.077118886155));
#53870=CARTESIAN_POINT('Ctrl Pts',(70.9614937597943,-1.49492285634377,126.118809559677));
#53871=CARTESIAN_POINT('Ctrl Pts',(70.9537458630172,-1.62553879567608,126.160482513552));
#53872=CARTESIAN_POINT('Ctrl Pts',(70.9459979662401,-1.75447843389537,126.207642797732));
#53873=CARTESIAN_POINT('Ctrl Pts',(70.9382500694631,-1.88125290945574,126.260125747628));
#53874=CARTESIAN_POINT('Ctrl Pts',(70.930503793379,-2.00800086652884,126.312597719221));
#53875=CARTESIAN_POINT('Ctrl Pts',(70.9227575172949,-2.13258420079174,126.370389992492));
#53876=CARTESIAN_POINT('Ctrl Pts',(70.9150112412108,-2.25453292232848,126.43328931128));
#53877=CARTESIAN_POINT('Ctrl Pts',(70.9072649079454,-2.37648254406289,126.496189094377));
#53878=CARTESIAN_POINT('Ctrl Pts',(70.89951857468,-2.49579716679538,126.564195818998));
#53879=CARTESIAN_POINT('Ctrl Pts',(70.8917722414147,-2.61203071274441,126.637049899827));
#53880=CARTESIAN_POINT('Ctrl Pts',(70.8840241734117,-2.72829028839078,126.709920295823));
#53881=CARTESIAN_POINT('Ctrl Pts',(70.8762761054087,-2.84146708305424,126.787640000511));
#53882=CARTESIAN_POINT('Ctrl Pts',(70.8685280374057,-2.95114369570283,126.869905896793));
#53883=CARTESIAN_POINT('Ctrl Pts',(70.8607717346638,-3.06093687395969,126.952259226248));
#53884=CARTESIAN_POINT('Ctrl Pts',(70.8530154319219,-3.16722212577158,127.039168164261));
#53885=CARTESIAN_POINT('Ctrl Pts',(70.8452591291801,-3.26961445191326,127.130288707772));
#53886=CARTESIAN_POINT('Ctrl Pts',(70.8374986866659,-3.37206142792266,127.22145788506));
#53887=CARTESIAN_POINT('Ctrl Pts',(70.8297382441518,-3.47061105733544,127.316842875125));
#53888=CARTESIAN_POINT('Ctrl Pts',(70.8219778016376,-3.5649157152874,127.416063256738));
#53889=CARTESIAN_POINT('Ctrl Pts',(70.8142049013722,-3.65937175944821,127.515442915715));
#53890=CARTESIAN_POINT('Ctrl Pts',(70.8064320011067,-3.74956895739949,127.61866997513));
#53891=CARTESIAN_POINT('Ctrl Pts',(70.7986591008413,-3.83519987520419,127.725330741171));
#53892=CARTESIAN_POINT('Ctrl Pts',(70.7911687650793,-3.91771789345501,127.828114119703));
#53893=CARTESIAN_POINT('Ctrl Pts',(70.7836784293173,-3.99599567625939,127.934085643587));
#53894=CARTESIAN_POINT('Ctrl Pts',(70.7761880935553,-4.06979758348905,128.042851846635));
#53895=CARTESIAN_POINT('Ctrl Pts',(70.7681673327391,-4.14882574250351,128.159320283734));
#53896=CARTESIAN_POINT('Ctrl Pts',(70.7601465719229,-4.22297037620041,128.279360341728));
#53897=CARTESIAN_POINT('Ctrl Pts',(70.7521258111067,-4.29189898167231,128.402530858066));
#53898=CARTESIAN_POINT('Ctrl Pts',(70.744239767767,-4.35966985560124,128.523632590465));
#53899=CARTESIAN_POINT('Ctrl Pts',(70.7363537244274,-4.42239831387511,128.647760124096));
#53900=CARTESIAN_POINT('Ctrl Pts',(70.7284676810877,-4.47980973293724,128.774462142474));
#53901=CARTESIAN_POINT('Ctrl Pts',(70.7203795615332,-4.53869229307202,128.9044108415));
#53902=CARTESIAN_POINT('Ctrl Pts',(70.7122914419787,-4.59198139575677,129.037067438954));
#53903=CARTESIAN_POINT('Ctrl Pts',(70.7042033224242,-4.63942941463817,129.171915283385));
#53904=CARTESIAN_POINT('Ctrl Pts',(70.6961152028696,-4.68687743351954,129.306763127815));
#53905=CARTESIAN_POINT('Ctrl Pts',(70.6880270833151,-4.72848417136962,129.443801837749));
#53906=CARTESIAN_POINT('Ctrl Pts',(70.6799389637605,-4.76405452823405,129.582490119308));
#53907=CARTESIAN_POINT('Origin',(213.235140564004,0.,130.804360617566));
#53908=CARTESIAN_POINT('',(68.5848726604778,-4.764054528234,129.582490119308));
#53909=CARTESIAN_POINT('',(68.9302764532207,-4.76405452823407,129.582490119308));
#53910=CARTESIAN_POINT('',(213.235140564004,-4.76405452823405,129.582490119308));
#53911=CARTESIAN_POINT('',(70.2648594360286,-4.9182492826405,130.80701698844));
#53912=CARTESIAN_POINT('Ctrl Pts',(70.2648594359911,-4.91824928264014,130.807016989099));
#53913=CARTESIAN_POINT('Ctrl Pts',(70.2562002380237,-4.91816710427662,130.959169529675));
#53914=CARTESIAN_POINT('Ctrl Pts',(70.2475410400562,-4.91102501605397,131.111127544565));
#53915=CARTESIAN_POINT('Ctrl Pts',(70.2388818420887,-4.89687297662618,131.262419689399));
#53916=CARTESIAN_POINT('Ctrl Pts',(70.2311075079696,-4.88416710208777,131.398251632258));
#53917=CARTESIAN_POINT('Ctrl Pts',(70.2233331738506,-4.86578515640856,131.533769659566));
#53918=CARTESIAN_POINT('Ctrl Pts',(70.2155588397315,-4.84174690256046,131.668461302698));
#53919=CARTESIAN_POINT('Ctrl Pts',(70.2077940867844,-4.8177382737119,131.802986950418));
#53920=CARTESIAN_POINT('Ctrl Pts',(70.2000293338373,-4.78808727472672,131.936687859174));
#53921=CARTESIAN_POINT('Ctrl Pts',(70.1922645808903,-4.75286553642302,132.06905514795));
#53922=CARTESIAN_POINT('Ctrl Pts',(70.1845075400053,-4.71767878084629,132.201290967668));
#53923=CARTESIAN_POINT('Ctrl Pts',(70.1767504991203,-4.67693239662847,132.332195427988));
#53924=CARTESIAN_POINT('Ctrl Pts',(70.1689934582353,-4.63074926056585,132.46126868631));
#53925=CARTESIAN_POINT('Ctrl Pts',(70.1612422669952,-4.58460095156539,132.590244609484));
#53926=CARTESIAN_POINT('Ctrl Pts',(70.153491075755,-4.5330241824954,132.717391712683));
#53927=CARTESIAN_POINT('Ctrl Pts',(70.1457398845149,-4.47619187217681,132.842224544809));
#53928=CARTESIAN_POINT('Ctrl Pts',(70.1379919877378,-4.41938371710624,132.967004319651));
#53929=CARTESIAN_POINT('Ctrl Pts',(70.1302440909608,-4.35732462519227,133.089471424699));
#53930=CARTESIAN_POINT('Ctrl Pts',(70.1224961941837,-4.29023584730505,133.209159868439));
#53931=CARTESIAN_POINT('Ctrl Pts',(70.1147499180996,-4.2231611029439,133.328823275936));
#53932=CARTESIAN_POINT('Ctrl Pts',(70.1070036420156,-4.15105895634079,133.44570883741));
#53933=CARTESIAN_POINT('Ctrl Pts',(70.0992573659315,-4.07419668092015,133.559375039975));
#53934=CARTESIAN_POINT('Ctrl Pts',(70.0915110326661,-3.99733383811966,133.673042081598));
#53935=CARTESIAN_POINT('Ctrl Pts',(70.0837646994008,-3.9157110153896,133.783489393023));
#53936=CARTESIAN_POINT('Ctrl Pts',(70.0760183661355,-3.82963866680803,133.89030467801));
#53937=CARTESIAN_POINT('Ctrl Pts',(70.0682702981325,-3.7435470429209,133.997143883539));
#53938=CARTESIAN_POINT('Ctrl Pts',(70.0605222301296,-3.65300415564433,134.100349139754));
#53939=CARTESIAN_POINT('Ctrl Pts',(70.0527741621266,-3.55836029917016,134.19954176793));
#53940=CARTESIAN_POINT('Ctrl Pts',(70.0450178593848,-3.46361585407893,134.298839819212));
#53941=CARTESIAN_POINT('Ctrl Pts',(70.0372615566429,-3.36476200342189,134.394116440004));
#53942=CARTESIAN_POINT('Ctrl Pts',(70.0295052539011,-3.26218581424232,134.485029955588));
#53943=CARTESIAN_POINT('Ctrl Pts',(70.021744811387,-3.15955487706193,134.575991994453));
#53944=CARTESIAN_POINT('Ctrl Pts',(70.0139843688728,-3.05319794567822,134.662586041209));
#53945=CARTESIAN_POINT('Ctrl Pts',(70.0062239263586,-2.94353383616001,134.744511835207));
#53946=CARTESIAN_POINT('Ctrl Pts',(69.9984510260932,-2.83369368407769,134.826569143763));
#53947=CARTESIAN_POINT('Ctrl Pts',(69.9906781258278,-2.72053606775357,134.903943003572));
#53948=CARTESIAN_POINT('Ctrl Pts',(69.9829052255624,-2.60450809605509,134.976376993383));
#53949=CARTESIAN_POINT('Ctrl Pts',(69.9754148898002,-2.49269803338263,135.046177825215));
#53950=CARTESIAN_POINT('Ctrl Pts',(69.9679245540381,-2.37822294911583,135.111391552588));
#53951=CARTESIAN_POINT('Ctrl Pts',(69.9604342182759,-2.2615013865985,135.171830656492));
#53952=CARTESIAN_POINT('Ctrl Pts',(69.9526598841568,-2.1403542905638,135.234561327389));
#53953=CARTESIAN_POINT('Ctrl Pts',(69.9448855500377,-2.01640324547606,135.292346879857));
#53954=CARTESIAN_POINT('Ctrl Pts',(69.9371112159187,-1.89009008807158,135.344926939235));
#53955=CARTESIAN_POINT('Ctrl Pts',(69.9293464629716,-1.76393260034467,135.397442198389));
#53956=CARTESIAN_POINT('Ctrl Pts',(69.9215817100245,-1.63541914998415,135.444764580192));
#53957=CARTESIAN_POINT('Ctrl Pts',(69.9138169570774,-1.50501659120844,135.48667928706));
#53958=CARTESIAN_POINT('Ctrl Pts',(69.9060599161924,-1.37474355009245,135.52855236365));
#53959=CARTESIAN_POINT('Ctrl Pts',(69.8983028753074,-1.24258550426309,135.565028334931));
#53960=CARTESIAN_POINT('Ctrl Pts',(69.8905458344224,-1.10902940336458,135.5959404035));
#53961=CARTESIAN_POINT('Ctrl Pts',(69.8827946431823,-0.975574018160483,
135.626829161038));
#53962=CARTESIAN_POINT('Ctrl Pts',(69.8750434519422,-0.840723055730653,
135.652162279509));
#53963=CARTESIAN_POINT('Ctrl Pts',(69.867292260702,-0.704978406679796,135.671822842239));
#53964=CARTESIAN_POINT('Ctrl Pts',(69.859544363925,-0.569291452726078,135.691475048705));
#53965=CARTESIAN_POINT('Ctrl Pts',(69.8517964671478,-0.432711953743312,
135.705459438777));
#53966=CARTESIAN_POINT('Ctrl Pts',(69.8440485703708,-0.295751553089399,
135.713710277281));
#53967=CARTESIAN_POINT('Ctrl Pts',(69.8363022942867,-0.158819801598778,
135.721959389888));
#53968=CARTESIAN_POINT('Ctrl Pts',(69.8285560182026,-0.0215076969282203,
135.724477312977));
#53969=CARTESIAN_POINT('Ctrl Pts',(69.8208097421185,0.115668835814261,135.72125026275));
#53970=CARTESIAN_POINT('Ctrl Pts',(69.8130634088532,0.252846381162745,135.718023188702));
#53971=CARTESIAN_POINT('Ctrl Pts',(69.8053170755878,0.389887961729139,135.709051065912));
#53972=CARTESIAN_POINT('Ctrl Pts',(69.7975707423224,0.526278892997474,135.694372231999));
#53973=CARTESIAN_POINT('Ctrl Pts',(69.7898226743195,0.662700368069012,135.679690110862));
#53974=CARTESIAN_POINT('Ctrl Pts',(69.7820746063165,0.798470515253588,135.659298777401));
#53975=CARTESIAN_POINT('Ctrl Pts',(69.7743265383136,0.933081398848373,135.63328825894));
#53976=CARTESIAN_POINT('Ctrl Pts',(69.7665702355717,1.06783534849232,135.60725009619));
#53977=CARTESIAN_POINT('Ctrl Pts',(69.7588139328299,1.20142718885886,135.575580892744));
#53978=CARTESIAN_POINT('Ctrl Pts',(69.751057630088,1.33336024013838,135.538421615538));
#53979=CARTESIAN_POINT('Ctrl Pts',(69.7432971875738,1.46536370805997,135.501242505306));
#53980=CARTESIAN_POINT('Ctrl Pts',(69.7355367450596,1.59570625139251,135.458567604197));
#53981=CARTESIAN_POINT('Ctrl Pts',(69.7277763025455,1.72390887203196,135.410586975815));
#53982=CARTESIAN_POINT('Ctrl Pts',(69.72000340228,1.85231729489918,135.362529324669));
#53983=CARTESIAN_POINT('Ctrl Pts',(69.7122305020147,1.97857857014905,135.309149078453));
#53984=CARTESIAN_POINT('Ctrl Pts',(69.7044576017493,2.10223529005804,135.250683800572));
#53985=CARTESIAN_POINT('Ctrl Pts',(69.6969672659872,2.22139677672685,135.194343882806));
#53986=CARTESIAN_POINT('Ctrl Pts',(69.6894769302251,2.33813951176859,135.133282364889));
#53987=CARTESIAN_POINT('Ctrl Pts',(69.681986594463,2.45207949722928,135.067750020584));
#53988=CARTESIAN_POINT('Ctrl Pts',(69.6742122603439,2.57033955186919,134.999732997528));
#53989=CARTESIAN_POINT('Ctrl Pts',(69.6664379262248,2.68595474127514,134.926683975419));
#53990=CARTESIAN_POINT('Ctrl Pts',(69.6586635921057,2.79846718132218,134.848833945153));
#53991=CARTESIAN_POINT('Ctrl Pts',(69.6508988391586,2.91084095984239,134.771079858092));
#53992=CARTESIAN_POINT('Ctrl Pts',(69.6431340862115,3.02011927892806,134.688536755891));
#53993=CARTESIAN_POINT('Ctrl Pts',(69.6353693332644,3.12586907718008,134.601481312886));
#53994=CARTESIAN_POINT('Ctrl Pts',(69.6276122923794,3.23151384324152,134.514512334575));
#53995=CARTESIAN_POINT('Ctrl Pts',(69.6198552514944,3.33363676284464,134.423040181161));
#53996=CARTESIAN_POINT('Ctrl Pts',(69.6120982106094,3.43183429643148,134.3273843791));
#53997=CARTESIAN_POINT('Ctrl Pts',(69.6043470193693,3.52995777849452,134.231800711824));
#53998=CARTESIAN_POINT('Ctrl Pts',(69.5965958281292,3.62416148764677,134.132039947284));
#53999=CARTESIAN_POINT('Ctrl Pts',(69.5888446368891,3.71407577444676,134.02846114394));
#54000=CARTESIAN_POINT('Ctrl Pts',(69.581096740112,3.80395184527631,133.924926364352));
#54001=CARTESIAN_POINT('Ctrl Pts',(69.5733488433349,3.8895418640421,133.817577068146));
#54002=CARTESIAN_POINT('Ctrl Pts',(69.5656009465578,3.9705139701492,133.706808183906));
#54003=CARTESIAN_POINT('Ctrl Pts',(69.5578546704737,4.05146913863726,133.596062470127));
#54004=CARTESIAN_POINT('Ctrl Pts',(69.5501083943896,4.12780808525213,133.48189890652));
#54005=CARTESIAN_POINT('Ctrl Pts',(69.5423621183054,4.19924034317215,133.36474410501));
#54006=CARTESIAN_POINT('Ctrl Pts',(69.5346157850401,4.27067312838887,133.24758843869));
#54007=CARTESIAN_POINT('Ctrl Pts',(69.5268694517747,4.3371989491043,133.127441824215));
#54008=CARTESIAN_POINT('Ctrl Pts',(69.5191231185094,4.39857186029102,133.004758002666));
#54009=CARTESIAN_POINT('Ctrl Pts',(69.5113750505064,4.45995851551567,132.882046706926));
#54010=CARTESIAN_POINT('Ctrl Pts',(69.5036269825035,4.5161897900859,132.756797423067));
#54011=CARTESIAN_POINT('Ctrl Pts',(69.4958789145005,4.56706687488476,132.62948615375));
#54012=CARTESIAN_POINT('Ctrl Pts',(69.4881226117586,4.61799803245479,132.5020395765));
#54013=CARTESIAN_POINT('Ctrl Pts',(69.4803663090167,4.66356348755793,132.372526999657));
#54014=CARTESIAN_POINT('Ctrl Pts',(69.4726100062749,4.70361337209909,132.241442490081));
#54015=CARTESIAN_POINT('Ctrl Pts',(69.4648495637607,4.74368463246956,132.110288016755));
#54016=CARTESIAN_POINT('Ctrl Pts',(69.4570891212465,4.77823435801524,131.977560317115));
#54017=CARTESIAN_POINT('Ctrl Pts',(69.4493286787323,4.80716354445415,131.843765119851));
#54018=CARTESIAN_POINT('Ctrl Pts',(69.4415557784669,4.83613917059129,131.70975514266));
#54019=CARTESIAN_POINT('Ctrl Pts',(69.4337828782014,4.8594761610183,131.574674628922));
#54020=CARTESIAN_POINT('Ctrl Pts',(69.426009977936,4.87712714450783,131.439036817533));
#54021=CARTESIAN_POINT('Ctrl Pts',(69.418519642174,4.89413647028723,131.308329782241));
#54022=CARTESIAN_POINT('Ctrl Pts',(69.4110293064121,4.90586598580105,131.177105570981));
#54023=CARTESIAN_POINT('Ctrl Pts',(69.4035389706501,4.91231911384552,131.045822801454));
#54024=CARTESIAN_POINT('Ctrl Pts',(69.395764636531,4.91901691420122,130.909562405817));
#54025=CARTESIAN_POINT('Ctrl Pts',(69.3879903024119,4.92005153697714,130.772807291806));
#54026=CARTESIAN_POINT('Ctrl Pts',(69.3802159682929,4.91536982380163,130.636067546525));
#54027=CARTESIAN_POINT('Ctrl Pts',(69.3724512153458,4.91069388041919,130.49949632076));
#54028=CARTESIAN_POINT('Ctrl Pts',(69.3646864623987,4.90031563153282,130.362940813024));
#54029=CARTESIAN_POINT('Ctrl Pts',(69.3569217094516,4.88423377083227,130.226914919373));
#54030=CARTESIAN_POINT('Ctrl Pts',(69.3491646685666,4.86816788286248,130.091024128558));
#54031=CARTESIAN_POINT('Ctrl Pts',(69.3414076276816,4.8464097021061,129.955662290772));
#54032=CARTESIAN_POINT('Ctrl Pts',(69.3336505867966,4.81900993223122,129.82134162713));
#54033=CARTESIAN_POINT('Ctrl Pts',(69.3258993955565,4.79163082473589,129.687122255746));
#54034=CARTESIAN_POINT('Ctrl Pts',(69.3181482043163,4.75861867400674,129.553942877222));
#54035=CARTESIAN_POINT('Ctrl Pts',(69.3103970130762,4.72007576154382,129.422308567972));
#54036=CARTESIAN_POINT('Ctrl Pts',(69.3026491162991,4.68154923084692,129.290730206815));
#54037=CARTESIAN_POINT('Ctrl Pts',(69.2949012195221,4.63749672345477,129.160695983241));
#54038=CARTESIAN_POINT('Ctrl Pts',(69.287153322745,4.58807112520987,129.032698569512));
#54039=CARTESIAN_POINT('Ctrl Pts',(69.2794070466609,4.53865586573464,128.904727930082));
#54040=CARTESIAN_POINT('Ctrl Pts',(69.2716607705768,4.48386989171959,128.778793617534));
#54041=CARTESIAN_POINT('Ctrl Pts',(69.2639144944927,4.42391511944843,128.655370603998));
#54042=CARTESIAN_POINT('Ctrl Pts',(69.2561681612274,4.36395990460476,128.531946679381));
#54043=CARTESIAN_POINT('Ctrl Pts',(69.248421827962,4.29883598619877,128.411034442437));
#54044=CARTESIAN_POINT('Ctrl Pts',(69.2406754946966,4.22879217015668,128.293086071818));
#54045=CARTESIAN_POINT('Ctrl Pts',(69.2329274266936,4.15873266828765,128.17511128748));
#54046=CARTESIAN_POINT('Ctrl Pts',(69.2251793586907,4.08375127596382,128.060102026322));
#54047=CARTESIAN_POINT('Ctrl Pts',(69.2174312906877,4.00414100652024,127.94848284315));
#54048=CARTESIAN_POINT('Ctrl Pts',(69.2096749879459,3.92444612633492,127.836745029782));
#54049=CARTESIAN_POINT('Ctrl Pts',(69.201918685204,3.84011276893118,127.728404810618));
#54050=CARTESIAN_POINT('Ctrl Pts',(69.1941623824622,3.75147559938637,127.62385532914));
#54051=CARTESIAN_POINT('Ctrl Pts',(69.186401939948,3.66279112151537,127.519250046454));
#54052=CARTESIAN_POINT('Ctrl Pts',(69.1786414974338,3.56979851934587,127.418439820144));
#54053=CARTESIAN_POINT('Ctrl Pts',(69.1708810549196,3.47286976251647,127.321781304026));
#54054=CARTESIAN_POINT('Ctrl Pts',(69.1631081546542,3.37578540704155,127.224967623076));
#54055=CARTESIAN_POINT('Ctrl Pts',(69.1553352543888,3.27475255851865,127.132319234892));
#54056=CARTESIAN_POINT('Ctrl Pts',(69.1475623541234,3.17017741406035,127.044153412387));
#54057=CARTESIAN_POINT('Ctrl Pts',(69.1400720183613,3.06940383951158,126.959192639606));
#54058=CARTESIAN_POINT('Ctrl Pts',(69.1325816825992,2.96534128375956,126.878394374491));
#54059=CARTESIAN_POINT('Ctrl Pts',(69.1250913468372,2.8583774449682,126.802003631414));
#54060=CARTESIAN_POINT('Ctrl Pts',(69.1173170127181,2.74735803971859,126.722716510096));
#54061=CARTESIAN_POINT('Ctrl Pts',(69.109542678599,2.63286132807756,126.647926573101));
#54062=CARTESIAN_POINT('Ctrl Pts',(69.1017683444799,2.51528772737339,126.57795425861));
#54063=CARTESIAN_POINT('Ctrl Pts',(69.0940035915328,2.39785902562423,126.508068178743));
#54064=CARTESIAN_POINT('Ctrl Pts',(69.0862388385857,2.27736131248673,126.442988105973));
#54065=CARTESIAN_POINT('Ctrl Pts',(69.0784740856386,2.1542262371748,126.382992912707));
#54066=CARTESIAN_POINT('Ctrl Pts',(69.0707170447536,2.03121346135574,126.323057307513));
#54067=CARTESIAN_POINT('Ctrl Pts',(69.0629600038686,1.90556888540873,126.268196701488));
#54068=CARTESIAN_POINT('Ctrl Pts',(69.0552029629836,1.77775086203394,126.218645304222));
#54069=CARTESIAN_POINT('Ctrl Pts',(69.0474517717435,1.65002922722469,126.169131274051));
#54070=CARTESIAN_POINT('Ctrl Pts',(69.0397005805034,1.52013777040098,126.124918624232));
#54071=CARTESIAN_POINT('Ctrl Pts',(69.0319493892632,1.3885567123026,126.086194308583));
#54072=CARTESIAN_POINT('Ctrl Pts',(69.0242014924861,1.25703157966414,126.047486451801));
#54073=CARTESIAN_POINT('Ctrl Pts',(69.0164535957091,1.1238186483229,126.014262399798));
#54074=CARTESIAN_POINT('Ctrl Pts',(69.008705698932,0.989415055938439,125.986659826776));
#54075=CARTESIAN_POINT('Ctrl Pts',(69.0009594228479,0.855039577887912,125.959063027617));
#54076=CARTESIAN_POINT('Ctrl Pts',(68.9932131467637,0.719474316919027,125.937085447126));
#54077=CARTESIAN_POINT('Ctrl Pts',(68.9854668706796,0.58322802122029,125.920813941454));
#54078=CARTESIAN_POINT('Ctrl Pts',(68.9777205374143,0.446980719782534,125.90454231567));
#54079=CARTESIAN_POINT('Ctrl Pts',(68.969974204149,0.310052761789971,125.893976895116));
#54080=CARTESIAN_POINT('Ctrl Pts',(68.9622278708836,0.172959063631132,125.889152765928));
#54081=CARTESIAN_POINT('Ctrl Pts',(68.9544798028806,0.0358346642889456,
125.884327556409));
#54082=CARTESIAN_POINT('Ctrl Pts',(68.9467317348777,-0.10145515842818,125.885246210441));
#54083=CARTESIAN_POINT('Ctrl Pts',(68.9389836668747,-0.238394833673622,
125.89189168985));
#54084=CARTESIAN_POINT('Ctrl Pts',(68.9312273641329,-0.37548005003533,125.898544232153));
#54085=CARTESIAN_POINT('Ctrl Pts',(68.923471061391,-0.512213984405493,125.910935739367));
#54086=CARTESIAN_POINT('Ctrl Pts',(68.9157147586492,-0.648084979391088,
125.928997151937));
#54087=CARTESIAN_POINT('Ctrl Pts',(68.907954316135,-0.784028492817888,125.947068204428));
#54088=CARTESIAN_POINT('Ctrl Pts',(68.9001938736208,-0.919107764250167,
125.970815124573));
#54089=CARTESIAN_POINT('Ctrl Pts',(68.8924334311066,-1.05282167205489,126.000117743881));
#54090=CARTESIAN_POINT('Ctrl Pts',(68.8846605308412,-1.18675022929499,126.029467402355));
#54091=CARTESIAN_POINT('Ctrl Pts',(68.8768876305758,-1.31930866470442,126.06439048234));
#54092=CARTESIAN_POINT('Ctrl Pts',(68.8691147303103,-1.45001048813332,126.104716732461));
#54093=CARTESIAN_POINT('Ctrl Pts',(68.8616243945483,-1.57596097106219,126.143577021814));
#54094=CARTESIAN_POINT('Ctrl Pts',(68.8541340587863,-1.70018719308175,126.187454361271));
#54095=CARTESIAN_POINT('Ctrl Pts',(68.8466437230243,-1.82227345633294,126.236155005639));
#54096=CARTESIAN_POINT('Ctrl Pts',(68.8388690701877,-1.94899385219394,126.286704221977));
#54097=CARTESIAN_POINT('Ctrl Pts',(68.8310944173512,-2.07381005234418,126.342610272175));
#54098=CARTESIAN_POINT('Ctrl Pts',(68.8233197645146,-2.19623596822923,126.403709457299));
#54099=CARTESIAN_POINT('Ctrl Pts',(68.8155547661712,-2.31850985672469,126.464732770011));
#54100=CARTESIAN_POINT('Ctrl Pts',(68.8077897678278,-2.43839902053174,126.530936213092));
#54101=CARTESIAN_POINT('Ctrl Pts',(68.8000247694845,-2.55543547617925,126.602107342288));
#54102=CARTESIAN_POINT('Ctrl Pts',(68.7922675562135,-2.67235459280879,126.673207116363));
#54103=CARTESIAN_POINT('Ctrl Pts',(68.7845103429426,-2.7864263612898,126.749264462785));
#54104=CARTESIAN_POINT('Ctrl Pts',(68.7767531296716,-2.89720595602794,126.830020331323));
#54105=CARTESIAN_POINT('Ctrl Pts',(68.7687581101219,-3.01138162642746,126.913251863726));
#54106=CARTESIAN_POINT('Ctrl Pts',(68.7607630905721,-3.12205965059716,127.001474441783));
#54107=CARTESIAN_POINT('Ctrl Pts',(68.7527680710223,-3.22878309858132,127.094354854118));
#54108=CARTESIAN_POINT('Ctrl Pts',(68.7450205156125,-3.33220321177032,127.184360405271));
#54109=CARTESIAN_POINT('Ctrl Pts',(68.7372729602028,-3.43190961048867,127.27873944472));
#54110=CARTESIAN_POINT('Ctrl Pts',(68.729525404793,-3.52751887892082,127.377146935673));
#54111=CARTESIAN_POINT('Ctrl Pts',(68.721779520941,-3.62310751937272,127.47553319492));
#54112=CARTESIAN_POINT('Ctrl Pts',(68.714033637089,-3.71460051624365,127.577945896049));
#54113=CARTESIAN_POINT('Ctrl Pts',(68.706287753237,-3.80165106594283,127.684002908053));
#54114=CARTESIAN_POINT('Ctrl Pts',(68.6985418631607,-3.88870168559236,127.79006000528));
#54115=CARTESIAN_POINT('Ctrl Pts',(68.6907959730844,-3.9713096035126,127.899761116662));
#54116=CARTESIAN_POINT('Ctrl Pts',(68.6830500830082,-4.04916835248726,128.012691096345));
#54117=CARTESIAN_POINT('Ctrl Pts',(68.6753025092992,-4.12704402469869,128.125645622284));
#54118=CARTESIAN_POINT('Ctrl Pts',(68.6675549355903,-4.2001682528382,128.24183009085));
#54119=CARTESIAN_POINT('Ctrl Pts',(68.6598073618814,-4.26827816424066,128.360800801403));
#54120=CARTESIAN_POINT('Ctrl Pts',(68.6520529055,-4.33644858209741,128.479877201359));
#54121=CARTESIAN_POINT('Ctrl Pts',(68.6442984491186,-4.39959559598578,128.601744445292));
#54122=CARTESIAN_POINT('Ctrl Pts',(68.6365439927371,-4.4575023965855,128.725934422837));
#54123=CARTESIAN_POINT('Ctrl Pts',(68.6287853919948,-4.51544014541292,128.850190773583));
#54124=CARTESIAN_POINT('Ctrl Pts',(68.6210267912524,-4.56813195087572,128.976771971067));
#54125=CARTESIAN_POINT('Ctrl Pts',(68.6132681905101,-4.61540971117823,129.105191332162));
#54126=CARTESIAN_POINT('Ctrl Pts',(68.6055003269813,-4.6627439151376,129.233764009706));
#54127=CARTESIAN_POINT('Ctrl Pts',(68.5977324634524,-4.70465105193333,129.364178860521));
#54128=CARTESIAN_POINT('Ctrl Pts',(68.5899645999236,-4.74101319515054,129.495935248694));
#54129=CARTESIAN_POINT('Ctrl Pts',(68.588267286775,-4.74895848713026,129.52472461262));
#54130=CARTESIAN_POINT('Ctrl Pts',(68.5865699736264,-4.75663923244104,129.553577993554));
#54131=CARTESIAN_POINT('Ctrl Pts',(68.5848726604777,-4.764054528234,129.582490119308));
#54132=CARTESIAN_POINT('Ctrl Pts',(70.3350012833217,-4.76405452823407,129.582490119308));
#54133=CARTESIAN_POINT('Ctrl Pts',(70.3273374882257,-4.79774776682839,129.713859545221));
#54134=CARTESIAN_POINT('Ctrl Pts',(70.3196736931296,-4.82597963576157,129.846532485872));
#54135=CARTESIAN_POINT('Ctrl Pts',(70.3120098980335,-4.84867284953609,129.980009563299));
#54136=CARTESIAN_POINT('Ctrl Pts',(70.3041514876994,-4.87194233722539,130.116876172006));
#54137=CARTESIAN_POINT('Ctrl Pts',(70.2962930773652,-4.88938805275968,130.254587853234));
#54138=CARTESIAN_POINT('Ctrl Pts',(70.2884346670311,-4.90098342265885,130.392602735646));
#54139=CARTESIAN_POINT('Ctrl Pts',(70.2805762566969,-4.91257879255801,130.530617618058));
#54140=CARTESIAN_POINT('Ctrl Pts',(70.2727178463627,-4.91832386127279,130.668935251341));
#54141=CARTESIAN_POINT('Ctrl Pts',(70.2648594360285,-4.9182492826405,130.807016988441));
#54142=CARTESIAN_POINT('',(70.610140563959,-4.91824936975562,130.806850476685));
#54143=CARTESIAN_POINT('Ctrl Pts',(70.6799389637605,-4.76405452823405,129.582490119308));
#54144=CARTESIAN_POINT('Ctrl Pts',(70.6720764007095,-4.79863292086401,129.717310747372));
#54145=CARTESIAN_POINT('Ctrl Pts',(70.6642138376585,-4.82750701748767,129.853689778277));
#54146=CARTESIAN_POINT('Ctrl Pts',(70.6563512746074,-4.85054752096174,129.991112925044));
#54147=CARTESIAN_POINT('Ctrl Pts',(70.6484922998902,-4.87357750916011,130.128473354334));
#54148=CARTESIAN_POINT('Ctrl Pts',(70.640633325173,-4.89077914228013,130.266876581894));
#54149=CARTESIAN_POINT('Ctrl Pts',(70.6327743504558,-4.9020741159162,130.405797668254));
#54150=CARTESIAN_POINT('Ctrl Pts',(70.6252297549734,-4.91291726150903,130.539161553275));
#54151=CARTESIAN_POINT('Ctrl Pts',(70.6176851594909,-4.91831713022705,130.673002336079));
#54152=CARTESIAN_POINT('Ctrl Pts',(70.6101405640085,-4.91824936975607,130.806850475807));
#54153=CARTESIAN_POINT('Ctrl Pts',(70.610140563959,-4.91824936975562,130.806850476685));
#54154=CARTESIAN_POINT('Ctrl Pts',(70.6016108271431,-4.91817276138222,130.958175939769));
#54155=CARTESIAN_POINT('Ctrl Pts',(70.5930810903272,-4.91110805520333,131.109261575527));
#54156=CARTESIAN_POINT('Ctrl Pts',(70.5845513535113,-4.89714603271158,131.259491144775));
#54157=CARTESIAN_POINT('Ctrl Pts',(70.5759770590162,-4.8831110753411,131.410505483953));
#54158=CARTESIAN_POINT('Ctrl Pts',(70.567402764521,-4.86210663986195,131.560654550213));
#54159=CARTESIAN_POINT('Ctrl Pts',(70.5588284700258,-4.83427521236157,131.709328149385));
#54160=CARTESIAN_POINT('Ctrl Pts',(70.5502311723227,-4.80636911841312,131.858400611662));
#54161=CARTESIAN_POINT('Ctrl Pts',(70.5416338746195,-4.77159947113251,132.005989455552));
#54162=CARTESIAN_POINT('Ctrl Pts',(70.5330365769164,-4.73015873715347,132.151498837583));
#54163=CARTESIAN_POINT('Ctrl Pts',(70.5244085520494,-4.68856989195753,132.297528277286));
#54164=CARTESIAN_POINT('Ctrl Pts',(70.5157805271824,-4.64026231123063,132.44146314563));
#54165=CARTESIAN_POINT('Ctrl Pts',(70.5071525023153,-4.58547784383415,132.58272391178));
#54166=CARTESIAN_POINT('Ctrl Pts',(70.5040151581244,-4.56555697744916,132.634089508301));
#54167=CARTESIAN_POINT('Ctrl Pts',(70.5008778139334,-4.54478017037869,132.685101764255));
#54168=CARTESIAN_POINT('Ctrl Pts',(70.4977404697424,-4.5231605431846,132.735733642923));
#54169=CARTESIAN_POINT('Ctrl Pts',(70.4899661356233,-4.46958713997907,132.861199361022));
#54170=CARTESIAN_POINT('Ctrl Pts',(70.4821918015042,-4.41070457665497,132.984633049248));
#54171=CARTESIAN_POINT('Ctrl Pts',(70.4744174673851,-4.3466881472084,133.105552746315));
#54172=CARTESIAN_POINT('Ctrl Pts',(70.4666527144379,-4.28275061228981,133.226323420663));
#54173=CARTESIAN_POINT('Ctrl Pts',(70.4588879614908,-4.21369198132697,133.344585926272));
#54174=CARTESIAN_POINT('Ctrl Pts',(70.4511232085436,-4.1397358437831,133.459877555226));
#54175=CARTESIAN_POINT('Ctrl Pts',(70.4433661676586,-4.06585316051765,133.575054674909));
#54176=CARTESIAN_POINT('Ctrl Pts',(70.4356091267735,-3.98708286052146,133.687266463047));
#54177=CARTESIAN_POINT('Ctrl Pts',(70.4278520858885,-3.9036945722289,133.796074465722));
#54178=CARTESIAN_POINT('Ctrl Pts',(70.4201008946483,-3.82036916769308,133.904800415437));
#54179=CARTESIAN_POINT('Ctrl Pts',(70.4123497034081,-3.73243294334538,134.010127379731));
#54180=CARTESIAN_POINT('Ctrl Pts',(70.404598512168,-3.64019878564739,134.11164588852));
#54181=CARTESIAN_POINT('Ctrl Pts',(70.3968506153908,-3.54800382992697,134.213121249235));
#54182=CARTESIAN_POINT('Ctrl Pts',(70.3891027186137,-3.45151483645035,134.310791085142));
#54183=CARTESIAN_POINT('Ctrl Pts',(70.3813548218366,-3.35108477392525,134.404279213933));
#54184=CARTESIAN_POINT('Ctrl Pts',(70.3736085457524,-3.25067571920421,134.497747787022));
#54185=CARTESIAN_POINT('Ctrl Pts',(70.3658622696683,-3.14632752117113,134.587036126648));
#54186=CARTESIAN_POINT('Ctrl Pts',(70.3581159935842,-3.03842949908311,134.671805412466));
#54187=CARTESIAN_POINT('Ctrl Pts',(70.3503696603188,-2.9305306805164,134.756575324032));
#54188=CARTESIAN_POINT('Ctrl Pts',(70.3426233270534,-2.81908229304039,134.836825873692));
#54189=CARTESIAN_POINT('Ctrl Pts',(70.334876993788,-2.70450585359283,134.912259247082));
#54190=CARTESIAN_POINT('Ctrl Pts',(70.3271289257849,-2.58990375554607,134.987709513254));
#54191=CARTESIAN_POINT('Ctrl Pts',(70.319380857782,-2.47217253808847,135.058340241574));
#54192=CARTESIAN_POINT('Ctrl Pts',(70.3116327897789,-2.35176139108469,135.123897794383));
#54193=CARTESIAN_POINT('Ctrl Pts',(70.303876487037,-2.23122226968098,135.189525022539));
#54194=CARTESIAN_POINT('Ctrl Pts',(70.2961201842951,-2.10799787294231,135.250068117174));
#54195=CARTESIAN_POINT('Ctrl Pts',(70.2883638815532,-1.98256110886023,135.305319905555));
#54196=CARTESIAN_POINT('Ctrl Pts',(70.280603439039,-1.85705739540033,135.360601183479));
#54197=CARTESIAN_POINT('Ctrl Pts',(70.2728429965248,-1.72933932563703,135.410585385415));
#54198=CARTESIAN_POINT('Ctrl Pts',(70.2650825540106,-1.59989739522771,135.455114469066));
#54199=CARTESIAN_POINT('Ctrl Pts',(70.2573096537452,-1.47024767314038,135.499715034756));
#54200=CARTESIAN_POINT('Ctrl Pts',(70.2495367534797,-1.33886893538751,135.538842871145));
#54201=CARTESIAN_POINT('Ctrl Pts',(70.2417638532142,-1.20626523357843,135.572390320573));
#54202=CARTESIAN_POINT('Ctrl Pts',(70.2342735174526,-1.07848201034693,135.604718235712));
#54203=CARTESIAN_POINT('Ctrl Pts',(70.226783181691,-0.949561639295706,135.631864378736));
#54204=CARTESIAN_POINT('Ctrl Pts',(70.2192928459294,-0.819959932368054,
135.653777981725));
#54205=CARTESIAN_POINT('Ctrl Pts',(70.2115185118103,-0.685444337322694,
135.676522445634));
#54206=CARTESIAN_POINT('Ctrl Pts',(70.2037441776912,-0.549768615832144,
135.69370180099));
#54207=CARTESIAN_POINT('Ctrl Pts',(70.1959698435722,-0.413433006262309,
135.70520301575));
#54208=CARTESIAN_POINT('Ctrl Pts',(70.1882050906251,-0.277265418146605,
135.71669005629));
#54209=CARTESIAN_POINT('Ctrl Pts',(70.180440337678,-0.140439945924335,135.722512847223));
#54210=CARTESIAN_POINT('Ctrl Pts',(70.1726755847309,-0.00346673443578061,
135.722609395765));
#54211=CARTESIAN_POINT('Ctrl Pts',(70.1649185438459,0.133370433327954,135.722705848413));
#54212=CARTESIAN_POINT('Ctrl Pts',(70.1571615029609,0.270354659910084,135.71708737655));
#54213=CARTESIAN_POINT('Ctrl Pts',(70.1494044620759,0.406971320857371,135.70574383116));
#54214=CARTESIAN_POINT('Ctrl Pts',(70.1416532708358,0.543484958117916,135.694408840026));
#54215=CARTESIAN_POINT('Ctrl Pts',(70.1339020795956,0.679631193413864,135.677357400954));
#54216=CARTESIAN_POINT('Ctrl Pts',(70.1261508883555,0.814896405191022,135.654631425604));
#54217=CARTESIAN_POINT('Ctrl Pts',(70.1184029915784,0.950104125644858,135.6319151094));
#54218=CARTESIAN_POINT('Ctrl Pts',(70.1106550948013,1.08443118259516,135.603529118504));
#54219=CARTESIAN_POINT('Ctrl Pts',(70.1029071980243,1.21737029500267,135.569567079761));
#54220=CARTESIAN_POINT('Ctrl Pts',(70.0951609219402,1.35028159941389,135.535612145144));
#54221=CARTESIAN_POINT('Ctrl Pts',(70.087414645856,1.48180515820139,135.496083579402));
#54222=CARTESIAN_POINT('Ctrl Pts',(70.0796683697719,1.61144547564495,135.451125787178));
#54223=CARTESIAN_POINT('Ctrl Pts',(70.0719220365066,1.7410867500637,135.406167663087));
#54224=CARTESIAN_POINT('Ctrl Pts',(70.0641757032412,1.86884438601461,135.355780360642));
#54225=CARTESIAN_POINT('Ctrl Pts',(70.0564293699759,1.99423998363794,135.300157538042));
#54226=CARTESIAN_POINT('Ctrl Pts',(70.0486813019729,2.11966366273593,135.244522259096));
#54227=CARTESIAN_POINT('Ctrl Pts',(70.04093323397,2.24272389361813,135.183649285437));
#54228=CARTESIAN_POINT('Ctrl Pts',(70.033185165967,2.36296448564355,135.117779435869));
#54229=CARTESIAN_POINT('Ctrl Pts',(70.0254288632251,2.48333287080122,135.05183957904));
#54230=CARTESIAN_POINT('Ctrl Pts',(70.0176725604833,2.60087528734744,134.980892425666));
#54231=CARTESIAN_POINT('Ctrl Pts',(70.0099162577414,2.71516181667355,134.90522386471));
#54232=CARTESIAN_POINT('Ctrl Pts',(70.0021558152273,2.82950934416146,134.829514917165));
#54233=CARTESIAN_POINT('Ctrl Pts',(69.9943953727131,2.9405972052705,134.749079769989));
#54234=CARTESIAN_POINT('Ctrl Pts',(69.9866349301989,3.04802730965653,134.664245665348));
#54235=CARTESIAN_POINT('Ctrl Pts',(69.9788620299335,3.15562987038333,134.57927537747));
#54236=CARTESIAN_POINT('Ctrl Pts',(69.971089129668,3.25956264415466,134.489892275879));
#54237=CARTESIAN_POINT('Ctrl Pts',(69.9633162294026,3.35946260332538,134.396462241874));
#54238=CARTESIAN_POINT('Ctrl Pts',(69.9558258936406,3.4557309473473,134.306428624942));
#54239=CARTESIAN_POINT('Ctrl Pts',(69.9483355578786,3.548254375906,134.212637418942));
#54240=CARTESIAN_POINT('Ctrl Pts',(69.9408452221165,3.63674379902352,134.115444670073));
#54241=CARTESIAN_POINT('Ctrl Pts',(69.9330708879975,3.72858832551419,134.014566828589));
#54242=CARTESIAN_POINT('Ctrl Pts',(69.9252965538784,3.81637784524895,133.909704862762));
#54243=CARTESIAN_POINT('Ctrl Pts',(69.9175222197593,3.89974687011235,133.801218540716));
#54244=CARTESIAN_POINT('Ctrl Pts',(69.9097574668123,3.9830131501034,133.692865918367));
#54245=CARTESIAN_POINT('Ctrl Pts',(69.9019927138652,4.0618695389089,133.580898134217));
#54246=CARTESIAN_POINT('Ctrl Pts',(69.8942279609181,4.13598813449779,133.465710878955));
#54247=CARTESIAN_POINT('Ctrl Pts',(69.8864709200331,4.21003311445275,133.350638029298));
#54248=CARTESIAN_POINT('Ctrl Pts',(69.8787138791482,4.27934945544398,133.232352398599));
#54249=CARTESIAN_POINT('Ctrl Pts',(69.8709568382632,4.34365045173104,133.111281469194));
#54250=CARTESIAN_POINT('Ctrl Pts',(69.8632056470231,4.40790295813652,132.99030184032));
#54251=CARTESIAN_POINT('Ctrl Pts',(69.855454455783,4.46714746525789,132.866541437381));
#54252=CARTESIAN_POINT('Ctrl Pts',(69.8477032645429,4.52114160956485,132.740455039014));
#54253=CARTESIAN_POINT('Ctrl Pts',(69.8399553677659,4.57511280492015,132.614422230729));
#54254=CARTESIAN_POINT('Ctrl Pts',(69.8322074709888,4.62383792224919,132.486065751932));
#54255=CARTESIAN_POINT('Ctrl Pts',(69.8244595742118,4.6671215346742,132.355863000123));
#54256=CARTESIAN_POINT('Ctrl Pts',(69.8167132981277,4.71039609310064,132.225687483923));
#54257=CARTESIAN_POINT('Ctrl Pts',(69.8089670220436,4.74823128740072,132.093666833652));
#54258=CARTESIAN_POINT('Ctrl Pts',(69.8012207459595,4.78048078175164,131.96029597813));
#54259=CARTESIAN_POINT('Ctrl Pts',(69.7934744126942,4.81273051416095,131.826924138096));
#54260=CARTESIAN_POINT('Ctrl Pts',(69.7857280794288,4.83939437245644,131.692202452937));
#54261=CARTESIAN_POINT('Ctrl Pts',(69.7779817461635,4.86037669995633,131.55663809099));
#54262=CARTESIAN_POINT('Ctrl Pts',(69.7702336781606,4.88136372630301,131.421043370345));
#54263=CARTESIAN_POINT('Ctrl Pts',(69.7624856101576,4.89666663025674,131.284605983689));
#54264=CARTESIAN_POINT('Ctrl Pts',(69.7547375421547,4.90624143731314,131.147839905575));
#54265=CARTESIAN_POINT('Ctrl Pts',(69.7469812394128,4.91582642058842,131.010928470846));
#54266=CARTESIAN_POINT('Ctrl Pts',(69.739224936671,4.91967111840357,130.873688037453));
#54267=CARTESIAN_POINT('Ctrl Pts',(69.7314686339292,4.91778367573147,130.736634838064));
#54268=CARTESIAN_POINT('Ctrl Pts',(69.723708191415,4.91589522567438,130.599508489257));
#54269=CARTESIAN_POINT('Ctrl Pts',(69.7159477489009,4.90826856071481,130.462569963748));
#54270=CARTESIAN_POINT('Ctrl Pts',(69.7081873063868,4.89496382140032,130.326331068603));
#54271=CARTESIAN_POINT('Ctrl Pts',(69.7004144061214,4.88163772413715,130.189873470688));
#54272=CARTESIAN_POINT('Ctrl Pts',(69.6926415058559,4.86261539223056,130.054118134872));
#54273=CARTESIAN_POINT('Ctrl Pts',(69.6848686055905,4.83800842667057,129.919568254373));
#54274=CARTESIAN_POINT('Ctrl Pts',(69.6773782698283,4.81429598628915,129.789909600937));
#54275=CARTESIAN_POINT('Ctrl Pts',(69.6698879340661,4.78539796152252,129.661370582267));
#54276=CARTESIAN_POINT('Ctrl Pts',(69.6623975983038,4.75145764392505,129.534386869614));
#54277=CARTESIAN_POINT('Ctrl Pts',(69.6546232641847,4.71623046887089,129.402588530905));
#54278=CARTESIAN_POINT('Ctrl Pts',(69.6468489300656,4.67545950697025,129.272048267698));
#54279=CARTESIAN_POINT('Ctrl Pts',(69.6390745959465,4.62924988608115,129.143268038955));
#54280=CARTESIAN_POINT('Ctrl Pts',(69.6313098429994,4.58309721441994,129.014646520334));
#54281=CARTESIAN_POINT('Ctrl Pts',(69.6235450900523,4.53151935084535,128.887781084804));
#54282=CARTESIAN_POINT('Ctrl Pts',(69.6157803371052,4.4746719620832,128.763161486113));
#54283=CARTESIAN_POINT('Ctrl Pts',(69.6080232962202,4.41788103494906,128.638665661363));
#54284=CARTESIAN_POINT('Ctrl Pts',(69.6002662553352,4.35583115926982,128.516411587866));
#54285=CARTESIAN_POINT('Ctrl Pts',(69.5925092144502,4.28872701658698,128.396871543926));
#54286=CARTESIAN_POINT('Ctrl Pts',(69.58475802321,4.22167347766014,128.277421646063));
#54287=CARTESIAN_POINT('Ctrl Pts',(69.5770068319699,4.14957344881735,128.160682043525));
#54288=CARTESIAN_POINT('Ctrl Pts',(69.5692556407298,4.07267854479646,128.047102462577));
#54289=CARTESIAN_POINT('Ctrl Pts',(69.5615077439527,3.99581632316091,127.93357115598));
#54290=CARTESIAN_POINT('Ctrl Pts',(69.5537598471755,3.9141634983973,127.823197522732));
#54291=CARTESIAN_POINT('Ctrl Pts',(69.5460119503984,3.82801608554287,127.716404026011));
#54292=CARTESIAN_POINT('Ctrl Pts',(69.5382656743143,3.7418866928701,127.609632868188));
#54293=CARTESIAN_POINT('Ctrl Pts',(69.5305193982302,3.65126482747268,127.50644066142));
#54294=CARTESIAN_POINT('Ctrl Pts',(69.522773122146,3.55648778889753,127.407218043295));
#54295=CARTESIAN_POINT('Ctrl Pts',(69.5150267888807,3.46171005069981,127.307994692732));
#54296=CARTESIAN_POINT('Ctrl Pts',(69.5072804556154,3.3627773481677,127.212741271999));
#54297=CARTESIAN_POINT('Ctrl Pts',(69.49953412235,3.26006467161488,127.121812396648));
#54298=CARTESIAN_POINT('Ctrl Pts',(69.491786054347,3.15732899327044,127.030863158405));
#54299=CARTESIAN_POINT('Ctrl Pts',(69.484037986344,3.05081194915019,126.944240651752));
#54300=CARTESIAN_POINT('Ctrl Pts',(69.476289918341,2.94092219130759,126.862259689485));
#54301=CARTESIAN_POINT('Ctrl Pts',(69.4685336155991,2.8309156413225,126.780191596876));
#54302=CARTESIAN_POINT('Ctrl Pts',(69.4607773128572,2.71752953093789,126.702775137184));
#54303=CARTESIAN_POINT('Ctrl Pts',(69.4530210101154,2.601202583876,126.630282494179));
#54304=CARTESIAN_POINT('Ctrl Pts',(69.4452605676012,2.48481354961978,126.557751159668));
#54305=CARTESIAN_POINT('Ctrl Pts',(69.4375001250869,2.36548089110542,126.49014907095));
#54306=CARTESIAN_POINT('Ctrl Pts',(69.4297396825727,2.24366771354702,126.427702274299));
#54307=CARTESIAN_POINT('Ctrl Pts',(69.4219667823073,2.12165899066209,126.365155232507));
#54308=CARTESIAN_POINT('Ctrl Pts',(69.4141938820418,1.99716214680654,126.307780184063));
#54309=CARTESIAN_POINT('Ctrl Pts',(69.4064209817764,1.87066085574772,126.255755224121));
#54310=CARTESIAN_POINT('Ctrl Pts',(69.3989306460145,1.74875820525897,126.205621502517));
#54311=CARTESIAN_POINT('Ctrl Pts',(69.3914403102526,1.62499460018356,126.160455749859));
#54312=CARTESIAN_POINT('Ctrl Pts',(69.3839499744907,1.49981403566988,126.120372901858));
#54313=CARTESIAN_POINT('Ctrl Pts',(69.3761756403717,1.36988721200246,126.07877030049));
#54314=CARTESIAN_POINT('Ctrl Pts',(69.3684013062526,1.23802229068093,126.042511864544));
#54315=CARTESIAN_POINT('Ctrl Pts',(69.3606269721335,1.10469840817102,126.011780468055));
#54316=CARTESIAN_POINT('Ctrl Pts',(69.3528622191864,0.971538835430809,125.981086945266));
#54317=CARTESIAN_POINT('Ctrl Pts',(69.3450974662393,0.836924256382496,125.955906995888));
#54318=CARTESIAN_POINT('Ctrl Pts',(69.3373327132923,0.701350856392471,125.936374376959));
#54319=CARTESIAN_POINT('Ctrl Pts',(69.3295756724073,0.565912109814567,125.916861158103));
#54320=CARTESIAN_POINT('Ctrl Pts',(69.3218186315223,0.42951682190927,125.902984162909));
#54321=CARTESIAN_POINT('Ctrl Pts',(69.3140615906373,0.292672969162603,125.894826464958));
#54322=CARTESIAN_POINT('Ctrl Pts',(69.3063103993971,0.155932311429783,125.886674918791));
#54323=CARTESIAN_POINT('Ctrl Pts',(69.298559208157,0.0187441508472424,125.884234108341));
#54324=CARTESIAN_POINT('Ctrl Pts',(69.2908080169169,-0.118377141231064,
125.887535431032));
#54325=CARTESIAN_POINT('Ctrl Pts',(69.2830601201398,-0.255440153102407,
125.890835350573));
#54326=CARTESIAN_POINT('Ctrl Pts',(69.2753122233627,-0.392435962962857,
125.899872539779));
#54327=CARTESIAN_POINT('Ctrl Pts',(69.2675643265857,-0.528849137218226,
125.914626304481));
#54328=CARTESIAN_POINT('Ctrl Pts',(69.2598180505016,-0.66523377677827,125.929376983013));
#54329=CARTESIAN_POINT('Ctrl Pts',(69.2520717744175,-0.801035634696752,
125.949841816548));
#54330=CARTESIAN_POINT('Ctrl Pts',(69.2443254983334,-0.935743737862675,
125.975948174583));
#54331=CARTESIAN_POINT('Ctrl Pts',(69.2365791650681,-1.07045283541321,126.002054725329));
#54332=CARTESIAN_POINT('Ctrl Pts',(69.2288328318027,-1.20406777827664,126.033802809289));
#54333=CARTESIAN_POINT('Ctrl Pts',(69.2210864985373,-1.33608752692281,126.071068614858));
#54334=CARTESIAN_POINT('Ctrl Pts',(69.2133384305344,-1.46813684047616,126.108342765845));
#54335=CARTESIAN_POINT('Ctrl Pts',(69.2055903625315,-1.5985898727702,126.151136991065));
#54336=CARTESIAN_POINT('Ctrl Pts',(69.1978422945285,-1.72696087646697,126.199277643976));
#54337=CARTESIAN_POINT('Ctrl Pts',(69.1900859917867,-1.85546831439429,126.247469461345));
#54338=CARTESIAN_POINT('Ctrl Pts',(69.1823296890448,-1.98188893675404,126.301018919807));
#54339=CARTESIAN_POINT('Ctrl Pts',(69.1745733863029,-2.1057566067425,126.359704030645));
#54340=CARTESIAN_POINT('Ctrl Pts',(69.1668129437887,-2.22969038863619,126.418420463494));
#54341=CARTESIAN_POINT('Ctrl Pts',(69.1590525012746,-2.35106815725444,126.482277828553));
#54342=CARTESIAN_POINT('Ctrl Pts',(69.1512920587604,-2.46944941378446,126.551008685823));
#54343=CARTESIAN_POINT('Ctrl Pts',(69.143519158495,-2.58802070641685,126.619849875967));
#54344=CARTESIAN_POINT('Ctrl Pts',(69.1357462582296,-2.70358554472652,126.693579981489));
#54345=CARTESIAN_POINT('Ctrl Pts',(69.1279733579642,-2.81573265473219,126.771888338731));
#54346=CARTESIAN_POINT('Ctrl Pts',(69.1204830222021,-2.92380293480823,126.84734998994));
#54347=CARTESIAN_POINT('Ctrl Pts',(69.11299268644,-3.02869941332029,126.927062623513));
#54348=CARTESIAN_POINT('Ctrl Pts',(69.1055023506779,-3.13008540137689,127.010714819315));
#54349=CARTESIAN_POINT('Ctrl Pts',(69.0978360489836,-3.23385318919103,127.096332205609));
#54350=CARTESIAN_POINT('Ctrl Pts',(69.0901697472893,-3.33429156583331,127.186364052398));
#54351=CARTESIAN_POINT('Ctrl Pts',(69.0825034455951,-3.43099375406175,127.280518265518));
#54352=CARTESIAN_POINT('Ctrl Pts',(69.0748459328249,-3.5275850794212,127.374564536859));
#54353=CARTESIAN_POINT('Ctrl Pts',(69.0671884200548,-3.62044844565388,127.472723502388));
#54354=CARTESIAN_POINT('Ctrl Pts',(69.0595309072847,-3.70920854237395,127.574661707191));
#54355=CARTESIAN_POINT('Ctrl Pts',(69.0518804058702,-3.79788736876317,127.676506575551));
#54356=CARTESIAN_POINT('Ctrl Pts',(69.0442299044556,-3.88247013323087,127.782123501593));
#54357=CARTESIAN_POINT('Ctrl Pts',(69.036579403041,-3.96261735362609,127.891141303604));
#54358=CARTESIAN_POINT('Ctrl Pts',(69.0289341419549,-4.04270967595161,128.000084432197));
#54359=CARTESIAN_POINT('Ctrl Pts',(69.0212888808688,-4.11837225937918,128.11242348059));
#54360=CARTESIAN_POINT('Ctrl Pts',(69.0136436197827,-4.18930537909567,128.227753642651));
#54361=CARTESIAN_POINT('Ctrl Pts',(69.006001064684,-4.26021339252376,128.343042984397));
#54362=CARTESIAN_POINT('Ctrl Pts',(68.9983585095853,-4.32639505752586,128.46132099407));
#54363=CARTESIAN_POINT('Ctrl Pts',(68.9907159544867,-4.38759377732882,128.582153627287));
#54364=CARTESIAN_POINT('Ctrl Pts',(68.9830750803242,-4.44877903682396,128.702959684058));
#54365=CARTESIAN_POINT('Ctrl Pts',(68.9754342061618,-4.50498335275461,128.826318885969));
#54366=CARTESIAN_POINT('Ctrl Pts',(68.9677933319993,-4.5559962659104,128.951772944199));
#54367=CARTESIAN_POINT('Ctrl Pts',(68.9601502965188,-4.60702360871435,129.077262488698));
#54368=CARTESIAN_POINT('Ctrl Pts',(68.9525072610383,-4.65285646314337,129.204847700251));
#54369=CARTESIAN_POINT('Ctrl Pts',(68.9448642255579,-4.69333273727326,129.334050827168));
#54370=CARTESIAN_POINT('Ctrl Pts',(68.9400016347788,-4.71908422800734,129.416251405091));
#54371=CARTESIAN_POINT('Ctrl Pts',(68.9351390439998,-4.74266854441486,129.499106492975));
#54372=CARTESIAN_POINT('Ctrl Pts',(68.9302764532207,-4.76405452823407,129.582490119308));
#54373=CARTESIAN_POINT('Origin',(213.235140564004,0.,130.804360617566));
#54374=CARTESIAN_POINT('',(66.8345747415593,-4.7640545282341,129.582490119308));
#54375=CARTESIAN_POINT('',(67.1801803489693,-4.76405452823408,129.582490119308));
#54376=CARTESIAN_POINT('',(213.235140564004,-4.76405452823405,129.582490119308));
#54377=CARTESIAN_POINT('',(68.5148594359566,-4.91824809583631,130.800032765609));
#54378=CARTESIAN_POINT('Ctrl Pts',(68.5148594359566,-4.9182480958363,130.800032765609));
#54379=CARTESIAN_POINT('Ctrl Pts',(68.5072124510153,-4.91836670518795,130.934822546704));
#54380=CARTESIAN_POINT('Ctrl Pts',(68.4995654660739,-4.91294006782637,131.069798280582));
#54381=CARTESIAN_POINT('Ctrl Pts',(68.4919184811327,-4.90194906913478,131.204458588204));
#54382=CARTESIAN_POINT('Ctrl Pts',(68.4842781235352,-4.89096759591342,131.339002190985));
#54383=CARTESIAN_POINT('Ctrl Pts',(68.4766377659378,-4.87443138624882,131.47323051136));
#54384=CARTESIAN_POINT('Ctrl Pts',(68.4689974083404,-4.85237338428922,131.606642115509));
#54385=CARTESIAN_POINT('Ctrl Pts',(68.4613612904117,-4.83032762241411,131.739979688958));
#54386=CARTESIAN_POINT('Ctrl Pts',(68.4537251724831,-4.80276622695132,131.872501050486));
#54387=CARTESIAN_POINT('Ctrl Pts',(68.4460890545544,-4.76977394128991,132.003710279463));
#54388=CARTESIAN_POINT('Ctrl Pts',(68.4384550823034,-4.7367909261517,132.134882639876));
#54389=CARTESIAN_POINT('Ctrl Pts',(68.4308211100523,-4.69838015266099,132.264743209749));
#54390=CARTESIAN_POINT('Ctrl Pts',(68.4231871378013,-4.65467729142473,132.392807146472));
#54391=CARTESIAN_POINT('Ctrl Pts',(68.4155535448375,-4.61097660152694,132.520864720451));
#54392=CARTESIAN_POINT('Ctrl Pts',(68.4079199518736,-4.56198447712011,132.647125456961));
#54393=CARTESIAN_POINT('Ctrl Pts',(68.4002863589098,-4.5078860138274,132.771121088198));
#54394=CARTESIAN_POINT('Ctrl Pts',(68.3926513793562,-4.45377772392009,132.89513924239));
#54395=CARTESIAN_POINT('Ctrl Pts',(68.3850163998027,-4.39456141258378,133.016891103625));
#54396=CARTESIAN_POINT('Ctrl Pts',(68.3773814202491,-4.33046949035708,133.135930272452));
#54397=CARTESIAN_POINT('Ctrl Pts',(68.3697387349083,-4.26631288181285,133.25508958443));
#54398=CARTESIAN_POINT('Ctrl Pts',(68.3620960495676,-4.19727102724456,133.371530380898));
#54399=CARTESIAN_POINT('Ctrl Pts',(68.3544533642268,-4.12362146972974,133.484832411278));
#54400=CARTESIAN_POINT('Ctrl Pts',(68.3468066842611,-4.04993341758311,133.598193661565));
#54401=CARTESIAN_POINT('Ctrl Pts',(68.3391600042954,-3.97163310107924,133.708412551059));
#54402=CARTESIAN_POINT('Ctrl Pts',(68.3315133243297,-3.88903942880687,133.815100623559));
#54403=CARTESIAN_POINT('Ctrl Pts',(68.3238548412143,-3.80631826780864,133.921953376064));
#54404=CARTESIAN_POINT('Ctrl Pts',(68.3161963580988,-3.71929077470398,134.025264118247));
#54405=CARTESIAN_POINT('Ctrl Pts',(68.3085378749833,-3.62831429920305,134.124679639693));
#54406=CARTESIAN_POINT('Ctrl Pts',(68.3022747417884,-3.55391343220651,134.205981986786));
#54407=CARTESIAN_POINT('Ctrl Pts',(68.2960116085934,-3.47687224182813,134.284679833575));
#54408=CARTESIAN_POINT('Ctrl Pts',(68.2897484753985,-3.39740236567618,134.36060023663));
#54409=CARTESIAN_POINT('Ctrl Pts',(68.2819741412794,-3.29875758991056,134.454839104211));
#54410=CARTESIAN_POINT('Ctrl Pts',(68.2741998071603,-3.1960325281503,134.545119740777));
#54411=CARTESIAN_POINT('Ctrl Pts',(68.2664254730413,-3.08957807420817,134.63106813002));
#54412=CARTESIAN_POINT('Ctrl Pts',(68.2586607200942,-2.98325481586642,134.716910595555));
#54413=CARTESIAN_POINT('Ctrl Pts',(68.2508959671471,-2.87321161157181,134.79843119376));
#54414=CARTESIAN_POINT('Ctrl Pts',(68.2431312142,-2.7598361693194,134.875292621545));
#54415=CARTESIAN_POINT('Ctrl Pts',(68.235374173315,-2.64657333315455,134.952077709476));
#54416=CARTESIAN_POINT('Ctrl Pts',(68.22761713243,-2.52998516685193,135.024212618061));
#54417=CARTESIAN_POINT('Ctrl Pts',(68.2198600915451,-2.41049214949732,135.091400465726));
#54418=CARTESIAN_POINT('Ctrl Pts',(68.2121089003049,-2.2910892427563,135.158537646513));
#54419=CARTESIAN_POINT('Ctrl Pts',(68.2043577090648,-2.16878618457121,135.220735001106));
#54420=CARTESIAN_POINT('Ctrl Pts',(68.1966065178246,-2.04403180655608,135.277739322336));
#54421=CARTESIAN_POINT('Ctrl Pts',(68.1888586210476,-1.91933045248004,135.334719415208));
#54422=CARTESIAN_POINT('Ctrl Pts',(68.1811107242705,-1.79218020564322,135.386510702481));
#54423=CARTESIAN_POINT('Ctrl Pts',(68.1733628274934,-1.66305363636179,135.43290635733));
#54424=CARTESIAN_POINT('Ctrl Pts',(68.1656165514094,-1.53395407757501,135.479292307208));
#54425=CARTESIAN_POINT('Ctrl Pts',(68.1578702753253,-1.40287938632966,135.520284737492));
#54426=CARTESIAN_POINT('Ctrl Pts',(68.1501239992412,-1.27032083726244,135.555725477574));
#54427=CARTESIAN_POINT('Ctrl Pts',(68.1423776659759,-1.1377613096783,135.591166479271));
#54428=CARTESIAN_POINT('Ctrl Pts',(68.1346313327106,-1.00371828011441,135.621055608009));
#54429=CARTESIAN_POINT('Ctrl Pts',(68.1268849994452,-0.868696475360461,
135.645285064012));
#54430=CARTESIAN_POINT('Ctrl Pts',(68.1191369314423,-0.733644433409144,
135.669519946033));
#54431=CARTESIAN_POINT('Ctrl Pts',(68.1113888634393,-0.597613564849928,
135.688092564209));
#54432=CARTESIAN_POINT('Ctrl Pts',(68.1036407954363,-0.461116640956121,
135.700946622726));
#54433=CARTESIAN_POINT('Ctrl Pts',(68.0958844926945,-0.324474646507265,
135.71381434269));
#54434=CARTESIAN_POINT('Ctrl Pts',(68.0881281899526,-0.187365997114212,
135.720951325315));
#54435=CARTESIAN_POINT('Ctrl Pts',(68.0803718872108,-0.0503069722412662,
135.722353325068));
#54436=CARTESIAN_POINT('Ctrl Pts',(68.0726114446966,0.0868252051600223,
135.72375607311));
#54437=CARTESIAN_POINT('Ctrl Pts',(68.0648510021825,0.22390731468705,135.719417751473));
#54438=CARTESIAN_POINT('Ctrl Pts',(68.0570905596683,0.36042625345506,135.709386201426));
#54439=CARTESIAN_POINT('Ctrl Pts',(68.0493176594029,0.497164344543161,135.699338547844));
#54440=CARTESIAN_POINT('Ctrl Pts',(68.0415447591375,0.63333706969227,135.68357944764));
#54441=CARTESIAN_POINT('Ctrl Pts',(68.033771858872,0.768438702474648,135.662208394415));
#54442=CARTESIAN_POINT('Ctrl Pts',(68.0262815231099,0.898629050606371,135.641614232805));
#54443=CARTESIAN_POINT('Ctrl Pts',(68.0187911873478,1.02782452612636,135.615809111983));
#54444=CARTESIAN_POINT('Ctrl Pts',(68.0113008515857,1.15558614464289,135.58492582733));
#54445=CARTESIAN_POINT('Ctrl Pts',(68.0035265174666,1.28819188375612,135.552871593553));
#54446=CARTESIAN_POINT('Ctrl Pts',(67.9957521833476,1.4196729452598,135.515244979061));
#54447=CARTESIAN_POINT('Ctrl Pts',(67.9879778492285,1.54952499196543,135.472139035805));
#54448=CARTESIAN_POINT('Ctrl Pts',(67.9802130962814,1.6792170076287,135.429086216771));
#54449=CARTESIAN_POINT('Ctrl Pts',(67.9724483433343,1.80728363555723,135.380567626994));
#54450=CARTESIAN_POINT('Ctrl Pts',(67.9646835903873,1.93323152746781,135.32672713563));
#54451=CARTESIAN_POINT('Ctrl Pts',(67.9569265495023,2.05905432615643,135.272940119401));
#54452=CARTESIAN_POINT('Ctrl Pts',(67.9491695086173,2.18276221942639,135.213841873226));
#54453=CARTESIAN_POINT('Ctrl Pts',(67.9414124677324,2.30387815318501,135.149625686325));
#54454=CARTESIAN_POINT('Ctrl Pts',(67.9336612764923,2.42490275247552,135.08545792535));
#54455=CARTESIAN_POINT('Ctrl Pts',(67.9259100852522,2.54333893878154,135.01618008811));
#54456=CARTESIAN_POINT('Ctrl Pts',(67.9181588940121,2.65873107729005,134.942032924691));
#54457=CARTESIAN_POINT('Ctrl Pts',(67.910410997235,2.77407417106214,134.867917275795));
#54458=CARTESIAN_POINT('Ctrl Pts',(67.902663100458,2.88637546208292,134.788936627892));
#54459=CARTESIAN_POINT('Ctrl Pts',(67.8949152036809,2.99520550528921,134.705376772824));
#54460=CARTESIAN_POINT('Ctrl Pts',(67.8871689275968,3.10401278359656,134.621834396676));
#54461=CARTESIAN_POINT('Ctrl Pts',(67.8794226515127,3.2093499484564,134.533714956568));
#54462=CARTESIAN_POINT('Ctrl Pts',(67.8716763754286,3.3108183805148,134.441346280687));
#54463=CARTESIAN_POINT('Ctrl Pts',(67.8639300421633,3.41228756158984,134.348976922961));
#54464=CARTESIAN_POINT('Ctrl Pts',(67.8561837088979,3.50988766376385,134.252358530059));
#54465=CARTESIAN_POINT('Ctrl Pts',(67.8484373756326,3.60325517487317,134.15185747451));
#54466=CARTESIAN_POINT('Ctrl Pts',(67.8406893076297,3.69664359498936,134.051333912446));
#54467=CARTESIAN_POINT('Ctrl Pts',(67.8329412396267,3.78579727185954,133.946926243919));
#54468=CARTESIAN_POINT('Ctrl Pts',(67.8251931716237,3.87039167682359,133.83903544866));
#54469=CARTESIAN_POINT('Ctrl Pts',(67.8174368688819,3.95507598972792,133.73102998578));
#54470=CARTESIAN_POINT('Ctrl Pts',(67.80968056614,4.0351911094021,133.619534309366));
#54471=CARTESIAN_POINT('Ctrl Pts',(67.8019242633982,4.11045440229741,133.50498048514));
#54472=CARTESIAN_POINT('Ctrl Pts',(67.794163820884,4.18575786547838,133.390365520088));
#54473=CARTESIAN_POINT('Ctrl Pts',(67.7864033783699,4.25620414123331,133.272689490161));
#54474=CARTESIAN_POINT('Ctrl Pts',(67.7786429358557,4.32155613513531,133.152409942724));
#54475=CARTESIAN_POINT('Ctrl Pts',(67.7708700355903,4.3870130378596,133.031937311879));
#54476=CARTESIAN_POINT('Ctrl Pts',(67.7630971353249,4.44735914468388,132.908853163001));
#54477=CARTESIAN_POINT('Ctrl Pts',(67.7553242350594,4.50240480490596,132.783636756779));
#54478=CARTESIAN_POINT('Ctrl Pts',(67.7478338992972,4.55544941672865,132.662972282322));
#54479=CARTESIAN_POINT('Ctrl Pts',(67.740343563535,4.60357214803633,132.54032817163));
#54480=CARTESIAN_POINT('Ctrl Pts',(67.7328532277728,4.64664744155759,132.416145533852));
#54481=CARTESIAN_POINT('Ctrl Pts',(67.7250788936537,4.6913559479241,132.287254473621));
#54482=CARTESIAN_POINT('Ctrl Pts',(67.7173045595346,4.73076833685649,132.156297628626));
#54483=CARTESIAN_POINT('Ctrl Pts',(67.7095302254155,4.76469028902847,132.02374960888));
#54484=CARTESIAN_POINT('Ctrl Pts',(67.7017654724684,4.79857043542609,131.891364942722));
#54485=CARTESIAN_POINT('Ctrl Pts',(67.6940007195214,4.82697351232497,131.757393378703));
#54486=CARTESIAN_POINT('Ctrl Pts',(67.6862359665743,4.84975389412462,131.622327749499));
#54487=CARTESIAN_POINT('Ctrl Pts',(67.6784789256893,4.87251165012791,131.487396269383));
#54488=CARTESIAN_POINT('Ctrl Pts',(67.6707218848042,4.88965775991696,131.351373269572));
#54489=CARTESIAN_POINT('Ctrl Pts',(67.6629648439192,4.90109698379797,131.214764586731));
#54490=CARTESIAN_POINT('Ctrl Pts',(67.6552136526791,4.91252758127122,131.078258921561));
#54491=CARTESIAN_POINT('Ctrl Pts',(67.647462461439,4.91825982641321,130.941168840501));
#54492=CARTESIAN_POINT('Ctrl Pts',(67.6397112701989,4.91824998734602,130.804007813325));
#54493=CARTESIAN_POINT('Ctrl Pts',(67.6319633734218,4.91824015246071,130.666905083245));
#54494=CARTESIAN_POINT('Ctrl Pts',(67.6242154766447,4.9124930874401,130.52973185717));
#54495=CARTESIAN_POINT('Ctrl Pts',(67.6164675798677,4.90101711150753,130.393003916867));
#54496=CARTESIAN_POINT('Ctrl Pts',(67.6087213037836,4.88954353610172,130.2563045771));
#54497=CARTESIAN_POINT('Ctrl Pts',(67.6009750276995,4.87234346607608,130.120050727184));
#54498=CARTESIAN_POINT('Ctrl Pts',(67.5932287516154,4.84947724907209,129.984754936014));
#54499=CARTESIAN_POINT('Ctrl Pts',(67.58548241835,4.82661086327484,129.849458146121));
#54500=CARTESIAN_POINT('Ctrl Pts',(67.5777360850846,4.79807831219077,129.715119814583));
#54501=CARTESIAN_POINT('Ctrl Pts',(67.5699897518192,4.76399134820206,129.582243807782));
#54502=CARTESIAN_POINT('Ctrl Pts',(67.5622416838162,4.72989675067411,129.449338044321));
#54503=CARTESIAN_POINT('Ctrl Pts',(67.5544936158133,4.69024536221057,129.317895635868));
#54504=CARTESIAN_POINT('Ctrl Pts',(67.5467455478103,4.64519912274906,129.188406356916));
#54505=CARTESIAN_POINT('Ctrl Pts',(67.5389892450684,4.60010500760831,129.058779455219));
#54506=CARTESIAN_POINT('Ctrl Pts',(67.5312329423266,4.54960471642406,128.931110199524));
#54507=CARTESIAN_POINT('Ctrl Pts',(67.5234766395847,4.49390898798704,128.805869919517));
#54508=CARTESIAN_POINT('Ctrl Pts',(67.5157161970706,4.43818353306278,128.680562795001));
#54509=CARTESIAN_POINT('Ctrl Pts',(67.5079557545564,4.37725728911844,128.557687579494));
#54510=CARTESIAN_POINT('Ctrl Pts',(67.5001953120422,4.3113870483806,128.437691062779));
#54511=CARTESIAN_POINT('Ctrl Pts',(67.4924224117768,4.24541106688456,128.317501917002));
#54512=CARTESIAN_POINT('Ctrl Pts',(67.4846495115113,4.17447543128331,128.200201039274));
#54513=CARTESIAN_POINT('Ctrl Pts',(67.4768766112459,4.0988808463306,128.086207040212));
#54514=CARTESIAN_POINT('Ctrl Pts',(67.4693862754839,4.0260343149524,127.976357010149));
#54515=CARTESIAN_POINT('Ctrl Pts',(67.4618959397219,3.94886186290223,127.869577855818));
#54516=CARTESIAN_POINT('Ctrl Pts',(67.4544056039599,3.86766674102762,127.766213642377));
#54517=CARTESIAN_POINT('Ctrl Pts',(67.4466312698408,3.78339308142829,127.658930343367));
#54518=CARTESIAN_POINT('Ctrl Pts',(67.4388569357217,3.69451873776251,127.554986210823));
#54519=CARTESIAN_POINT('Ctrl Pts',(67.4310826016027,3.60133797853409,127.454801269403));
#54520=CARTESIAN_POINT('Ctrl Pts',(67.4233178486556,3.50827205626348,127.354739796969));
#54521=CARTESIAN_POINT('Ctrl Pts',(67.4155530957085,3.41091054202979,127.258428581168));
#54522=CARTESIAN_POINT('Ctrl Pts',(67.4077883427614,3.30958935572785,127.16625652904));
#54523=CARTESIAN_POINT('Ctrl Pts',(67.4000313018764,3.20836880305625,127.074176023493));
#54524=CARTESIAN_POINT('Ctrl Pts',(67.3922742609913,3.10319669210154,126.98622676178));
#54525=CARTESIAN_POINT('Ctrl Pts',(67.3845172201063,2.99444711819473,126.902762288825));
#54526=CARTESIAN_POINT('Ctrl Pts',(67.3767660288661,2.88577955318754,126.819360757078));
#54527=CARTESIAN_POINT('Ctrl Pts',(67.369014837626,2.77354020391473,126.74043751947));
#54528=CARTESIAN_POINT('Ctrl Pts',(67.3612636463859,2.65813742889289,126.666306911822));
#54529=CARTESIAN_POINT('Ctrl Pts',(67.3535157496088,2.54278370312938,126.592207811661));
#54530=CARTESIAN_POINT('Ctrl Pts',(67.3457678528317,2.42426955406166,126.522897500893));
#54531=CARTESIAN_POINT('Ctrl Pts',(67.3380199560546,2.30303342023976,126.458647772962));
#54532=CARTESIAN_POINT('Ctrl Pts',(67.3302736799705,2.18182264640334,126.394411484689));
#54533=CARTESIAN_POINT('Ctrl Pts',(67.3225274038864,2.05789136557562,126.335233856668));
#54534=CARTESIAN_POINT('Ctrl Pts',(67.3147811278023,1.93170343585908,126.281341172727));
#54535=CARTESIAN_POINT('Ctrl Pts',(67.3070347945369,1.80551457465208,126.227448090963));
#54536=CARTESIAN_POINT('Ctrl Pts',(67.2992884612715,1.67706939086354,126.178840184682));
#54537=CARTESIAN_POINT('Ctrl Pts',(67.2915421280062,1.5468522064417,126.135695785526));
#54538=CARTESIAN_POINT('Ctrl Pts',(67.2837940600032,1.4166058607841,126.092541724481));
#54539=CARTESIAN_POINT('Ctrl Pts',(67.2760459920003,1.28458709590686,126.054853728153));
#54540=CARTESIAN_POINT('Ctrl Pts',(67.2682979239973,1.15129550545385,126.022760286963));
#54541=CARTESIAN_POINT('Ctrl Pts',(67.2605416212554,1.01786225111233,125.990632736482));
#54542=CARTESIAN_POINT('Ctrl Pts',(67.2527853185135,0.883153849591547,125.9641117105));
#54543=CARTESIAN_POINT('Ctrl Pts',(67.2450290157717,0.747680753368192,125.943274673711));
#54544=CARTESIAN_POINT('Ctrl Pts',(67.2372685732575,0.612135351074182,125.922426515568));
#54545=CARTESIAN_POINT('Ctrl Pts',(67.2295081307434,0.475824829202853,125.907268434744));
#54546=CARTESIAN_POINT('Ctrl Pts',(67.2217476882292,0.339263887122995,125.897825885457));
#54547=CARTESIAN_POINT('Ctrl Pts',(67.2139747879637,0.202483725295785,125.888368178151));
#54548=CARTESIAN_POINT('Ctrl Pts',(67.2062018876983,0.0654527309883036,
125.884644347739));
#54549=CARTESIAN_POINT('Ctrl Pts',(67.1984289874328,-0.0713143685682095,
125.886627672058));
#54550=CARTESIAN_POINT('Ctrl Pts',(67.1909386516709,-0.203109639559009,
125.888538897542));
#54551=CARTESIAN_POINT('Ctrl Pts',(67.1834483159089,-0.334659561614416,
125.895749525948));
#54552=CARTESIAN_POINT('Ctrl Pts',(67.175957980147,-0.465510748482276,125.90819039937));
#54553=CARTESIAN_POINT('Ctrl Pts',(67.1681836460279,-0.60132319787256,125.92110297229));
#54554=CARTESIAN_POINT('Ctrl Pts',(67.1604093119089,-0.736813094060469,
125.939691132051));
#54555=CARTESIAN_POINT('Ctrl Pts',(67.1526349777898,-0.871467999091324,
125.963934335816));
#54556=CARTESIAN_POINT('Ctrl Pts',(67.1448702248427,-1.00595695398618,125.988147661998));
#54557=CARTESIAN_POINT('Ctrl Pts',(67.1371054718956,-1.13961258414576,126.018002096671));
#54558=CARTESIAN_POINT('Ctrl Pts',(67.1293407189486,-1.27192611815261,126.053425234669));
#54559=CARTESIAN_POINT('Ctrl Pts',(67.1215836780636,-1.404108236492,126.088813189907));
#54560=CARTESIAN_POINT('Ctrl Pts',(67.1138266371786,-1.53495053616552,126.129758741246));
#54561=CARTESIAN_POINT('Ctrl Pts',(67.1060695962936,-1.66395336215103,126.176138251356));
#54562=CARTESIAN_POINT('Ctrl Pts',(67.0983184050535,-1.79285890610162,126.222482786317));
#54563=CARTESIAN_POINT('Ctrl Pts',(67.0905672138135,-1.91992737100342,126.274252991908));
#54564=CARTESIAN_POINT('Ctrl Pts',(67.0828160225734,-2.04467356947265,126.331275210736));
#54565=CARTESIAN_POINT('Ctrl Pts',(67.0750681257963,-2.16936674748033,126.388273193599));
#54566=CARTESIAN_POINT('Ctrl Pts',(67.0673202290192,-2.29173926733986,126.450518587736));
#54567=CARTESIAN_POINT('Ctrl Pts',(67.0595723322422,-2.41132547478305,126.517789433372));
#54568=CARTESIAN_POINT('Ctrl Pts',(67.0518260561581,-2.53088666736995,126.585046207398));
#54569=CARTESIAN_POINT('Ctrl Pts',(67.044079780074,-2.64766236629879,126.657326150435));
#54570=CARTESIAN_POINT('Ctrl Pts',(67.0363335039899,-2.76121146594152,126.734361317461));
#54571=CARTESIAN_POINT('Ctrl Pts',(67.0285871707245,-2.87476140377776,126.811397053144));
#54572=CARTESIAN_POINT('Ctrl Pts',(67.0208408374592,-2.98508437126533,126.893187863362));
#54573=CARTESIAN_POINT('Ctrl Pts',(67.0130945041938,-3.09176854509996,126.979422666954));
#54574=CARTESIAN_POINT('Ctrl Pts',(67.0053464361909,-3.19847661011503,127.065676782232));
#54575=CARTESIAN_POINT('Ctrl Pts',(66.9975983681879,-3.30154395595853,127.156376625492));
#54576=CARTESIAN_POINT('Ctrl Pts',(66.989850300185,-3.4005924374325,127.251171326665));
#54577=CARTESIAN_POINT('Ctrl Pts',(66.9820939974431,-3.49974618881181,127.346066776774));
#54578=CARTESIAN_POINT('Ctrl Pts',(66.9743376947013,-3.59487226054278,127.445065507758));
#54579=CARTESIAN_POINT('Ctrl Pts',(66.9665813919595,-3.68562956735191,127.54777993305));
#54580=CARTESIAN_POINT('Ctrl Pts',(66.9588209494453,-3.77643531406844,127.650549180124));
#54581=CARTESIAN_POINT('Ctrl Pts',(66.9510605069311,-3.86286740340615,127.757037769747));
#54582=CARTESIAN_POINT('Ctrl Pts',(66.943300064417,-3.94462621242947,127.866826429388));
#54583=CARTESIAN_POINT('Ctrl Pts',(66.9355271641516,-4.02651626795113,127.976791331532));
#54584=CARTESIAN_POINT('Ctrl Pts',(66.9277542638861,-4.10371783153262,128.090066566665));
#54585=CARTESIAN_POINT('Ctrl Pts',(66.9199813636206,-4.17597516264491,128.206204636207));
#54586=CARTESIAN_POINT('Ctrl Pts',(66.9124910278585,-4.2456057577677,128.318120794389));
#54587=CARTESIAN_POINT('Ctrl Pts',(66.9050006920963,-4.31064519803317,128.432694990288));
#54588=CARTESIAN_POINT('Ctrl Pts',(66.8975103563341,-4.37090660160109,128.549508395672));
#54589=CARTESIAN_POINT('Ctrl Pts',(66.8892429190004,-4.43741995873967,128.678440868048));
#54590=CARTESIAN_POINT('Ctrl Pts',(66.8809754816667,-4.498302134916,128.810468544938));
#54591=CARTESIAN_POINT('Ctrl Pts',(66.8727080443329,-4.55327294673881,128.945089648881));
#54592=CARTESIAN_POINT('Ctrl Pts',(66.8644601753659,-4.6081136470217,129.079392115376));
#54593=CARTESIAN_POINT('Ctrl Pts',(66.8562123063989,-4.65707076253721,129.216275477697));
#54594=CARTESIAN_POINT('Ctrl Pts',(66.8479644374318,-4.69991063187567,129.355214967577));
#54595=CARTESIAN_POINT('Ctrl Pts',(66.8435012054743,-4.72309289564009,129.430400348659));
#54596=CARTESIAN_POINT('Ctrl Pts',(66.8390379735168,-4.74448463186782,129.506187390391));
#54597=CARTESIAN_POINT('Ctrl Pts',(66.8345747415593,-4.76405452823409,129.582490119308));
#54598=CARTESIAN_POINT('Ctrl Pts',(68.5848726604777,-4.764054528234,129.582490119308));
#54599=CARTESIAN_POINT('Ctrl Pts',(68.5793138067223,-4.78834029123518,129.677179940662));
#54600=CARTESIAN_POINT('Ctrl Pts',(68.5737549529669,-4.80977775907463,129.772499935554));
#54601=CARTESIAN_POINT('Ctrl Pts',(68.5681960992114,-4.82834407427217,129.868264167973));
#54602=CARTESIAN_POINT('Ctrl Pts',(68.5567818981128,-4.86646697957742,130.064900426987));
#54603=CARTESIAN_POINT('Ctrl Pts',(68.5453676970142,-4.89258700281412,130.263933162505));
#54604=CARTESIAN_POINT('Ctrl Pts',(68.5339534959156,-4.90647035960978,130.464167036247));
#54605=CARTESIAN_POINT('Ctrl Pts',(68.5275888092741,-4.91421187518088,130.575819691599));
#54606=CARTESIAN_POINT('Ctrl Pts',(68.5212241226326,-4.91814937569076,130.687845448596));
#54607=CARTESIAN_POINT('Ctrl Pts',(68.5148594359911,-4.91824809583577,130.800032765));
#54608=CARTESIAN_POINT('',(68.8601405640458,-4.91824893709338,130.807594080086));
#54609=CARTESIAN_POINT('Ctrl Pts',(68.9302764532207,-4.76405452823407,129.582490119308));
#54610=CARTESIAN_POINT('Ctrl Pts',(68.9226268490548,-4.79769797436187,129.71366540515));
#54611=CARTESIAN_POINT('Ctrl Pts',(68.9149772448887,-4.82589836869319,129.846148951193));
#54612=CARTESIAN_POINT('Ctrl Pts',(68.9073276407228,-4.84857649036195,129.979442997673));
#54613=CARTESIAN_POINT('Ctrl Pts',(68.8994631279433,-4.87189173306073,130.116481818145));
#54614=CARTESIAN_POINT('Ctrl Pts',(68.8915986151638,-4.88936978039464,130.254376893832));
#54615=CARTESIAN_POINT('Ctrl Pts',(68.8837341023843,-4.90098179994194,130.392583421575));
#54616=CARTESIAN_POINT('Ctrl Pts',(68.8758695896048,-4.91259381948925,130.530789949319));
#54617=CARTESIAN_POINT('Ctrl Pts',(68.8680050768253,-4.9183398524931,130.669307470833));
#54618=CARTESIAN_POINT('Ctrl Pts',(68.8601405640458,-4.91824893709338,130.807594080086));
#54619=CARTESIAN_POINT('Ctrl Pts',(68.8601405640086,-4.91824893709295,130.80759408074));
#54620=CARTESIAN_POINT('Ctrl Pts',(68.8491119516274,-4.91812144401943,131.001517017064));
#54621=CARTESIAN_POINT('Ctrl Pts',(68.8380833392462,-4.9065250417326,131.195064423835));
#54622=CARTESIAN_POINT('Ctrl Pts',(68.827054726865,-4.88358926773127,131.387231895465));
#54623=CARTESIAN_POINT('Ctrl Pts',(68.8192803927459,-4.86742128900431,131.52269536808));
#54624=CARTESIAN_POINT('Ctrl Pts',(68.8115060586268,-4.84558709825159,131.657700181946));
#54625=CARTESIAN_POINT('Ctrl Pts',(68.8037317245076,-4.81811952949426,131.791734539647));
#54626=CARTESIAN_POINT('Ctrl Pts',(68.7959669715605,-4.79068581206062,131.925603711982));
#54627=CARTESIAN_POINT('Ctrl Pts',(68.7882022186133,-4.75763260813217,132.058504428508));
#54628=CARTESIAN_POINT('Ctrl Pts',(68.7804374656662,-4.71904451113463,132.189929801847));
#54629=CARTESIAN_POINT('Ctrl Pts',(68.7726804247812,-4.68049474037897,132.321224641653));
#54630=CARTESIAN_POINT('Ctrl Pts',(68.7649233838962,-4.63642112592656,132.451046681645));
#54631=CARTESIAN_POINT('Ctrl Pts',(68.7571663430111,-4.58695925984507,132.578899377645));
#54632=CARTESIAN_POINT('Ctrl Pts',(68.749415151771,-4.53753469334155,132.706655658932));
#54633=CARTESIAN_POINT('Ctrl Pts',(68.7416639605307,-4.48273010349809,132.832445189068));
#54634=CARTESIAN_POINT('Ctrl Pts',(68.7339127692906,-4.42273074085967,132.955787087691));
#54635=CARTESIAN_POINT('Ctrl Pts',(68.7261648725135,-4.36275687955099,133.079076562717));
#54636=CARTESIAN_POINT('Ctrl Pts',(68.7184169757364,-4.29759280749071,133.199920124484));
#54637=CARTESIAN_POINT('Ctrl Pts',(68.7106690789593,-4.22747159495209,133.317857579246));
#54638=CARTESIAN_POINT('Ctrl Pts',(68.7029228028752,-4.1573650502595,133.435770364034));
#54639=CARTESIAN_POINT('Ctrl Pts',(68.6951765267911,-4.08230362727125,133.550777915111));
#54640=CARTESIAN_POINT('Ctrl Pts',(68.6874302507069,-4.00256577916699,133.662445683819));
#54641=CARTESIAN_POINT('Ctrl Pts',(68.6796839174416,-3.92282734245606,133.774114276834));
#54642=CARTESIAN_POINT('Ctrl Pts',(68.6719375841762,-3.83841263894339,133.882442720109));
#54643=CARTESIAN_POINT('Ctrl Pts',(68.6641912509108,-3.74964254283232,133.987026774027));
#54644=CARTESIAN_POINT('Ctrl Pts',(68.6564431829078,-3.6608525672736,134.091634248819));
#54645=CARTESIAN_POINT('Ctrl Pts',(68.6486951149048,-3.56770551121351,134.192495367662));
#54646=CARTESIAN_POINT('Ctrl Pts',(68.6409470469018,-3.47056121812299,134.289240514171));
#54647=CARTESIAN_POINT('Ctrl Pts',(68.6331907441599,-3.37331367892187,134.386088482572));
#54648=CARTESIAN_POINT('Ctrl Pts',(68.625434441418,-3.27206069369573,134.478811463771));
#54649=CARTESIAN_POINT('Ctrl Pts',(68.6176781386761,-3.16719792250111,134.567077771725));
#54650=CARTESIAN_POINT('Ctrl Pts',(68.6099176961619,-3.06227918288801,134.655391190066));
#54651=CARTESIAN_POINT('Ctrl Pts',(68.6021572536477,-2.95374712752299,134.739242956568));
#54652=CARTESIAN_POINT('Ctrl Pts',(68.5943968111335,-2.84202809831967,134.818343595963));
#54653=CARTESIAN_POINT('Ctrl Pts',(68.5866239108681,-2.73012972781272,134.897571214727));
#54654=CARTESIAN_POINT('Ctrl Pts',(68.5788510106026,-2.61503448849036,134.972032252856));
#54655=CARTESIAN_POINT('Ctrl Pts',(68.5710781103372,-2.49719588713077,135.041481782201));
#54656=CARTESIAN_POINT('Ctrl Pts',(68.5635877745755,-2.38364101575402,135.108406646218));
#54657=CARTESIAN_POINT('Ctrl Pts',(68.5560974388139,-2.26753904716802,135.170677891941));
#54658=CARTESIAN_POINT('Ctrl Pts',(68.5486071030522,-2.14931317364053,135.22811874207));
#54659=CARTESIAN_POINT('Ctrl Pts',(68.5408327689331,-2.02660473017823,135.287737479494));
#54660=CARTESIAN_POINT('Ctrl Pts',(68.533058434814,-1.9012194433073,135.342341156007));
#54661=CARTESIAN_POINT('Ctrl Pts',(68.5252841006949,-1.77360565027721,135.391680756798));
#54662=CARTESIAN_POINT('Ctrl Pts',(68.5175193477478,-1.64614912984187,135.440959550941));
#54663=CARTESIAN_POINT('Ctrl Pts',(68.5097545948007,-1.51646992899177,135.484987037924));
#54664=CARTESIAN_POINT('Ctrl Pts',(68.5019898418536,-1.38504023124802,135.523560403581));
#54665=CARTESIAN_POINT('Ctrl Pts',(68.4942328009686,-1.25374107133307,135.562095457628));
#54666=CARTESIAN_POINT('Ctrl Pts',(68.4864757600836,-1.12069524716776,135.595187061255));
#54667=CARTESIAN_POINT('Ctrl Pts',(68.4787187191986,-0.986393806257207,
135.622680897651));
#54668=CARTESIAN_POINT('Ctrl Pts',(68.4709675279585,-0.852193643107774,
135.650154000731));
#54669=CARTESIAN_POINT('Ctrl Pts',(68.4632163367183,-0.716740129372833,
135.672037660768));
#54670=CARTESIAN_POINT('Ctrl Pts',(68.4554651454781,-0.580537975765703,
135.68822780671));
#54671=CARTESIAN_POINT('Ctrl Pts',(68.4477172487011,-0.444393711707353,
135.704411071407));
#54672=CARTESIAN_POINT('Ctrl Pts',(68.439969351924,-0.307501828055501,135.714905588944));
#54673=CARTESIAN_POINT('Ctrl Pts',(68.4322214551469,-0.170375479020028,
135.71965870198));
#54674=CARTESIAN_POINT('Ctrl Pts',(68.4244751790628,-0.0332778138606709,
135.724410820768));
#54675=CARTESIAN_POINT('Ctrl Pts',(68.4167289029787,0.104053828645908,135.723423910331));
#54676=CARTESIAN_POINT('Ctrl Pts',(68.4089826268946,0.24110333966079,135.716697357052));
#54677=CARTESIAN_POINT('Ctrl Pts',(68.4012362936293,0.378153862344217,135.709970754119));
#54678=CARTESIAN_POINT('Ctrl Pts',(68.3934899603639,0.514921858885063,135.697504442965));
#54679=CARTESIAN_POINT('Ctrl Pts',(68.3857436270985,0.650893790698375,135.679349882757));
#54680=CARTESIAN_POINT('Ctrl Pts',(68.3779955590955,0.78689617248287,135.661191256962));
#54681=CARTESIAN_POINT('Ctrl Pts',(68.3702474910926,0.922101747344729,135.637341899042));
#54682=CARTESIAN_POINT('Ctrl Pts',(68.3624994230896,1.05600504236359,135.607904768815));
#54683=CARTESIAN_POINT('Ctrl Pts',(68.3547431203477,1.19005065139804,135.578436352457));
#54684=CARTESIAN_POINT('Ctrl Pts',(68.3469868176058,1.32279083328778,135.543368384575));
#54685=CARTESIAN_POINT('Ctrl Pts',(68.339230514864,1.45373266724798,135.502854460775));
#54686=CARTESIAN_POINT('Ctrl Pts',(68.3314700723498,1.58474438880756,135.462318913475));
#54687=CARTESIAN_POINT('Ctrl Pts',(68.3237096298356,1.71395548173818,135.416331749496));
#54688=CARTESIAN_POINT('Ctrl Pts',(68.3159491873214,1.84089195408112,135.365095193914));
#54689=CARTESIAN_POINT('Ctrl Pts',(68.308176287056,1.96803219611835,135.313776388865));
#54690=CARTESIAN_POINT('Ctrl Pts',(68.3004033867905,2.09289016455381,135.257191514278));
#54691=CARTESIAN_POINT('Ctrl Pts',(68.2926304865251,2.21501466290698,135.195589728602));
#54692=CARTESIAN_POINT('Ctrl Pts',(68.2851401507631,2.33269962813115,135.136227323001));
#54693=CARTESIAN_POINT('Ctrl Pts',(68.2776498150011,2.44784614074524,135.072206578021));
#54694=CARTESIAN_POINT('Ctrl Pts',(68.2701594792391,2.56007672724223,135.003787984855));
#54695=CARTESIAN_POINT('Ctrl Pts',(68.2623851451201,2.6765625705385,134.932775279932));
#54696=CARTESIAN_POINT('Ctrl Pts',(68.254610811001,2.79027600030487,134.856799707916));
#54697=CARTESIAN_POINT('Ctrl Pts',(68.2468364768819,2.90076517609331,134.776103869044));
#54698=CARTESIAN_POINT('Ctrl Pts',(68.2390717239349,3.01111818384715,134.695507480582));
#54699=CARTESIAN_POINT('Ctrl Pts',(68.2313069709878,3.11825453121856,134.610202628347));
#54700=CARTESIAN_POINT('Ctrl Pts',(68.2235422180407,3.22174835817949,134.520476947697));
#54701=CARTESIAN_POINT('Ctrl Pts',(68.2157851771557,3.32513939361262,134.430840383859));
#54702=CARTESIAN_POINT('Ctrl Pts',(68.2080281362707,3.42489481473299,134.336791984003));
#54703=CARTESIAN_POINT('Ctrl Pts',(68.2002710953857,3.52061936726625,134.238661468297));
#54704=CARTESIAN_POINT('Ctrl Pts',(68.1925199041456,3.61627173316981,134.140604953576));
#54705=CARTESIAN_POINT('Ctrl Pts',(68.1847687129055,3.70789900894599,134.038472729016));
#54706=CARTESIAN_POINT('Ctrl Pts',(68.1770175216654,3.79514082820219,133.932633169089));
#54707=CARTESIAN_POINT('Ctrl Pts',(68.1692696248883,3.88234556735784,133.826838593798));
#54708=CARTESIAN_POINT('Ctrl Pts',(68.1615217281112,3.96516830906575,133.717340118174));
#54709=CARTESIAN_POINT('Ctrl Pts',(68.1537738313341,4.04328737882934,133.604541010808));
#54710=CARTESIAN_POINT('Ctrl Pts',(68.1460275552501,4.12139010776759,133.491765498584));
#54711=CARTESIAN_POINT('Ctrl Pts',(68.138281279166,4.19479089935299,133.375691049112));
#54712=CARTESIAN_POINT('Ctrl Pts',(68.1305350030819,4.26321026789703,133.256751547699));
#54713=CARTESIAN_POINT('Ctrl Pts',(68.1227886698166,4.3316301414973,133.137811168301));
#54714=CARTESIAN_POINT('Ctrl Pts',(68.1150423365513,4.39506832373357,133.016006033656));
#54715=CARTESIAN_POINT('Ctrl Pts',(68.1072960032859,4.45329052851111,132.891796013255));
#54716=CARTESIAN_POINT('Ctrl Pts',(68.099547935283,4.51152577174772,132.76755817688));
#54717=CARTESIAN_POINT('Ctrl Pts',(68.09179986728,4.56454254727345,132.64091473702));
#54718=CARTESIAN_POINT('Ctrl Pts',(68.084051799277,4.61215425763861,132.512346614653));
#54719=CARTESIAN_POINT('Ctrl Pts',(68.0762954965352,4.65981657029614,132.383641848556));
#54720=CARTESIAN_POINT('Ctrl Pts',(68.0685391937934,4.70206220641158,132.253008680913));
#54721=CARTESIAN_POINT('Ctrl Pts',(68.0607828910515,4.73875395459257,132.120944842116));
#54722=CARTESIAN_POINT('Ctrl Pts',(68.0530224485374,4.77546528626439,131.988810516871));
#54723=CARTESIAN_POINT('Ctrl Pts',(68.0452620060232,4.80661673467081,131.855244379512));
#54724=CARTESIAN_POINT('Ctrl Pts',(68.037501563509,4.8321222332623,131.720754520488));
#54725=CARTESIAN_POINT('Ctrl Pts',(68.0297286632436,4.8576686755444,131.586048766403));
#54726=CARTESIAN_POINT('Ctrl Pts',(68.0219557629782,4.87755099975233,131.45041671452));
#54727=CARTESIAN_POINT('Ctrl Pts',(68.0141828627128,4.89173494722666,131.314372645445));
#54728=CARTESIAN_POINT('Ctrl Pts',(68.0066925269506,4.90540327248334,131.183274120953));
#54729=CARTESIAN_POINT('Ctrl Pts',(67.9992021911885,4.91378030924849,131.051793322314));
#54730=CARTESIAN_POINT('Ctrl Pts',(67.9917118554263,4.91688118248826,130.920388630532));
#54731=CARTESIAN_POINT('Ctrl Pts',(67.9839375213072,4.92009962627935,130.784001689924));
#54732=CARTESIAN_POINT('Ctrl Pts',(67.9761631871881,4.91764411219603,130.647264708449));
#54733=CARTESIAN_POINT('Ctrl Pts',(67.968388853069,4.90947451588986,130.510688963626));
#54734=CARTESIAN_POINT('Ctrl Pts',(67.9606241001219,4.90131498788099,130.374281536202));
#54735=CARTESIAN_POINT('Ctrl Pts',(67.9528593471749,4.88745541244134,130.238035336579));
#54736=CARTESIAN_POINT('Ctrl Pts',(67.9450945942278,4.86790759759728,130.102464126796));
#54737=CARTESIAN_POINT('Ctrl Pts',(67.9373375533428,4.8483791979185,129.967027568251));
#54738=CARTESIAN_POINT('Ctrl Pts',(67.9295805124577,4.82317385730762,129.832265049859));
#54739=CARTESIAN_POINT('Ctrl Pts',(67.9218234715727,4.79235533408991,129.698687332043));
#54740=CARTESIAN_POINT('Ctrl Pts',(67.9140722803326,4.76156005136029,129.565210346222));
#54741=CARTESIAN_POINT('Ctrl Pts',(67.9063210890925,4.72516009898088,129.432916761999));
#54742=CARTESIAN_POINT('Ctrl Pts',(67.8985698978524,4.6832706139897,129.302308881226));
#54743=CARTESIAN_POINT('Ctrl Pts',(67.8908220010753,4.64139893314707,129.171756512287));
#54744=CARTESIAN_POINT('Ctrl Pts',(67.8830741042981,4.59404247939745,129.042888793302));
#54745=CARTESIAN_POINT('Ctrl Pts',(67.875326207521,4.5413666611052,128.91619433466));
#54746=CARTESIAN_POINT('Ctrl Pts',(67.8675799314369,4.48870186145858,128.789526377768));
#54747=CARTESIAN_POINT('Ctrl Pts',(67.8598336553529,4.43072006048388,128.665031137772));
#54748=CARTESIAN_POINT('Ctrl Pts',(67.8520873792688,4.36763522933708,128.543178279506));
#54749=CARTESIAN_POINT('Ctrl Pts',(67.8443410460034,4.30454993251239,128.42132452175));
#54750=CARTESIAN_POINT('Ctrl Pts',(67.836594712738,4.23636171009661,128.30211353184));
#54751=CARTESIAN_POINT('Ctrl Pts',(67.8288483794727,4.16333082596077,128.185990991997));
#54752=CARTESIAN_POINT('Ctrl Pts',(67.8211003114697,4.09028358706489,128.069842447316));
#54753=CARTESIAN_POINT('Ctrl Pts',(67.8133522434667,4.01239173655985,127.95678405987));
#54754=CARTESIAN_POINT('Ctrl Pts',(67.8056041754637,3.92995902640709,127.847232768916));
#54755=CARTESIAN_POINT('Ctrl Pts',(67.7978478727219,3.84743870578892,127.737565045546));
#54756=CARTESIAN_POINT('Ctrl Pts',(67.79009156998,3.76036812035407,127.63141217742));
#54757=CARTESIAN_POINT('Ctrl Pts',(67.7823352672382,3.66909185866908,127.529158639802));
#54758=CARTESIAN_POINT('Ctrl Pts',(67.774574824724,3.57776688009496,127.426850526393));
#54759=CARTESIAN_POINT('Ctrl Pts',(67.7668143822098,3.48223202472447,127.328446170816));
#54760=CARTESIAN_POINT('Ctrl Pts',(67.7590539396956,3.38286824237172,127.234292618598));
#54761=CARTESIAN_POINT('Ctrl Pts',(67.7512810394302,3.28334495245443,127.13998792274));
#54762=CARTESIAN_POINT('Ctrl Pts',(67.7435081391648,3.17998074779317,127.049947923247));
#54763=CARTESIAN_POINT('Ctrl Pts',(67.7357352388993,3.07318978958398,126.964479424131));
#54764=CARTESIAN_POINT('Ctrl Pts',(67.7282449031374,2.9702809516966,126.88211792024));
#54765=CARTESIAN_POINT('Ctrl Pts',(67.7207545673754,2.86419042506642,126.8040014987));
#54766=CARTESIAN_POINT('Ctrl Pts',(67.7132642316134,2.75531203402774,126.730365200578));
#54767=CARTESIAN_POINT('Ctrl Pts',(67.7054898974943,2.64230548569932,126.65393695983));
#54768=CARTESIAN_POINT('Ctrl Pts',(67.6977155633752,2.52593752525034,126.582093174899));
#54769=CARTESIAN_POINT('Ctrl Pts',(67.6899412292562,2.40661661674796,126.515143961521));
#54770=CARTESIAN_POINT('Ctrl Pts',(67.6821764763091,2.28744276060129,126.448277257066));
#54771=CARTESIAN_POINT('Ctrl Pts',(67.674411723362,2.16532353510161,126.386293311512));
#54772=CARTESIAN_POINT('Ctrl Pts',(67.6666469704149,2.04069756533032,126.329459891365));
#54773=CARTESIAN_POINT('Ctrl Pts',(67.6588899295299,1.91619537582912,126.272682918972));
#54774=CARTESIAN_POINT('Ctrl Pts',(67.6511328886449,1.78919175015911,126.221046452932));
#54775=CARTESIAN_POINT('Ctrl Pts',(67.6433758477599,1.66015086845906,126.174772930044));
#54776=CARTESIAN_POINT('Ctrl Pts',(67.6356246565198,1.53120729749151,126.128534302379));
#54777=CARTESIAN_POINT('Ctrl Pts',(67.6278734652796,1.40022989495658,126.087650699494));
#54778=CARTESIAN_POINT('Ctrl Pts',(67.6201222740395,1.26770349600975,126.052296759756));
#54779=CARTESIAN_POINT('Ctrl Pts',(67.6123743772624,1.13523342431791,126.016957846386));
#54780=CARTESIAN_POINT('Ctrl Pts',(67.6046264804854,1.00121604261531,125.987144022249));
#54781=CARTESIAN_POINT('Ctrl Pts',(67.5968785837083,0.866151839921082,125.962980230455));
#54782=CARTESIAN_POINT('Ctrl Pts',(67.5891323076242,0.731115889746415,125.938821493205));
#54783=CARTESIAN_POINT('Ctrl Pts',(67.5813860315401,0.595033938739008,125.920310506312));
#54784=CARTESIAN_POINT('Ctrl Pts',(67.573639755456,0.458416785860073,125.907521115097));
#54785=CARTESIAN_POINT('Ctrl Pts',(67.5658934221907,0.321798624504351,125.894731629473));
#54786=CARTESIAN_POINT('Ctrl Pts',(67.5581470889253,0.184645642656913,125.887663860246));
#54787=CARTESIAN_POINT('Ctrl Pts',(67.5504007556599,0.0474734843716824,
125.886339742175));
#54788=CARTESIAN_POINT('Ctrl Pts',(67.542652687657,-0.0897293926673115,
125.885015327577));
#54789=CARTESIAN_POINT('Ctrl Pts',(67.534904619654,-0.226951063817352,125.8894371274));
#54790=CARTESIAN_POINT('Ctrl Pts',(67.527156551651,-0.363676560919306,125.899574952367));
#54791=CARTESIAN_POINT('Ctrl Pts',(67.5194002489092,-0.50054737150682,125.909723551936));
#54792=CARTESIAN_POINT('Ctrl Pts',(67.5116439461673,-0.636920564111838,
125.925600283279));
#54793=CARTESIAN_POINT('Ctrl Pts',(67.5038876434254,-0.7722864102675,125.947123052549));
#54794=CARTESIAN_POINT('Ctrl Pts',(67.4961272009113,-0.907724505251042,
125.968657309168));
#54795=CARTESIAN_POINT('Ctrl Pts',(67.4883667583971,-1.04215379944995,125.99584353083));
#54796=CARTESIAN_POINT('Ctrl Pts',(67.4806063158829,-1.17507640095522,126.02854880025));
#54797=CARTESIAN_POINT('Ctrl Pts',(67.4728334156175,-1.30821238162074,126.061306571071));
#54798=CARTESIAN_POINT('Ctrl Pts',(67.4650605153521,-1.43983646068943,126.099600984804));
#54799=CARTESIAN_POINT('Ctrl Pts',(67.4572876150866,-1.56946665101604,126.143249430966));
#54800=CARTESIAN_POINT('Ctrl Pts',(67.4497972793246,-1.69438445740572,126.185311146166));
#54801=CARTESIAN_POINT('Ctrl Pts',(67.4423069435626,-1.8174505362692,126.232344276918));
#54802=CARTESIAN_POINT('Ctrl Pts',(67.4348166078005,-1.93825426922783,126.284144533094));
#54803=CARTESIAN_POINT('Ctrl Pts',(67.4270418140675,-2.06364572506759,126.337911990239));
#54804=CARTESIAN_POINT('Ctrl Pts',(67.4192670203345,-2.18699683237101,126.396986136842));
#54805=CARTESIAN_POINT('Ctrl Pts',(67.4114922266015,-2.30782581219541,126.461190912953));
#54806=CARTESIAN_POINT('Ctrl Pts',(67.4037271187352,-2.42850426283095,126.525315702518));
#54807=CARTESIAN_POINT('Ctrl Pts',(67.3959620108689,-2.54666649606018,126.594558221521));
#54808=CARTESIAN_POINT('Ctrl Pts',(67.3881969030026,-2.66185008304264,126.668694141905));
#54809=CARTESIAN_POINT('Ctrl Pts',(67.3804396114472,-2.7769177269199,126.742755437518));
#54810=CARTESIAN_POINT('Ctrl Pts',(67.3726823198917,-2.88901236495634,126.821700121321));
#54811=CARTESIAN_POINT('Ctrl Pts',(67.3649250283362,-2.99769591471208,126.905257866237));
#54812=CARTESIAN_POINT('Ctrl Pts',(67.3571740386271,-3.1062911724367,126.988747730752));
#54813=CARTESIAN_POINT('Ctrl Pts',(67.3494230489179,-3.21148055074902,127.076842957219));
#54814=CARTESIAN_POINT('Ctrl Pts',(67.3416720592087,-3.3128550918911,127.169230055587));
#54815=CARTESIAN_POINT('Ctrl Pts',(67.3339245176007,-3.41418453560908,127.26157605468));
#54816=CARTESIAN_POINT('Ctrl Pts',(67.3261769759928,-3.51170223007268,127.358209864512));
#54817=CARTESIAN_POINT('Ctrl Pts',(67.3184294343847,-3.60503258532045,127.458777989491));
#54818=CARTESIAN_POINT('Ctrl Pts',(67.3106836615481,-3.69834163315655,127.559323154668));
#54819=CARTESIAN_POINT('Ctrl Pts',(67.3029378887114,-3.78746497852078,127.663800561191));
#54820=CARTESIAN_POINT('Ctrl Pts',(67.2951921158747,-3.87206446114142,127.771820449445));
#54821=CARTESIAN_POINT('Ctrl Pts',(67.2874464340175,-3.95666295008322,127.879839068932));
#54822=CARTESIAN_POINT('Ctrl Pts',(67.2797007521603,-4.03673744186551,127.99139977903));
#54823=CARTESIAN_POINT('Ctrl Pts',(67.271955070303,-4.11199083712506,128.106080717722));
#54824=CARTESIAN_POINT('Ctrl Pts',(67.2642040531959,-4.1872960671584,128.220840649004));
#54825=CARTESIAN_POINT('Ctrl Pts',(67.2564530360887,-4.25777334983864,128.338724776482));
#54826=CARTESIAN_POINT('Ctrl Pts',(67.2487020189816,-4.32316944740157,128.459283008711));
#54827=CARTESIAN_POINT('Ctrl Pts',(67.2409484295368,-4.38858724803102,128.579881250718));
#54828=CARTESIAN_POINT('Ctrl Pts',(67.2331948400921,-4.44892032817435,128.703155016199));
#54829=CARTESIAN_POINT('Ctrl Pts',(67.2254412506474,-4.50396245748309,128.828631576406));
#54830=CARTESIAN_POINT('Ctrl Pts',(67.217677895398,-4.55907391348107,128.954266176911));
#54831=CARTESIAN_POINT('Ctrl Pts',(67.2099145401486,-4.60888095666048,129.082108752829));
#54832=CARTESIAN_POINT('Ctrl Pts',(67.2021511848992,-4.65322612099232,129.211668014012));
#54833=CARTESIAN_POINT('Ctrl Pts',(67.1948275729225,-4.69505942195193,129.333888590863));
#54834=CARTESIAN_POINT('Ctrl Pts',(67.1875039609459,-4.73203243839533,129.45763647703));
#54835=CARTESIAN_POINT('Ctrl Pts',(67.1801803489693,-4.76405452823408,129.582490119308));
#54836=CARTESIAN_POINT('Origin',(213.235140564004,0.,130.804360617566));
#54837=CARTESIAN_POINT('',(65.0848845757186,-4.764054528234,129.582490119308));
#54838=CARTESIAN_POINT('',(65.4298554009981,-4.76405452823407,129.582490119308));
#54839=CARTESIAN_POINT('',(213.235140564004,-4.76405452823405,129.582490119308));
#54840=CARTESIAN_POINT('',(66.7648594360216,-4.91824995804488,130.803718206823));
#54841=CARTESIAN_POINT('Ctrl Pts',(66.7648594359911,-4.91824995804495,130.803718207364));
#54842=CARTESIAN_POINT('Ctrl Pts',(66.7568197494795,-4.91826860358419,130.946467220818));
#54843=CARTESIAN_POINT('Ctrl Pts',(66.7487800629679,-4.9120681202326,131.089122546079));
#54844=CARTESIAN_POINT('Ctrl Pts',(66.7407403764563,-4.89969894598051,131.231131400607));
#54845=CARTESIAN_POINT('Ctrl Pts',(66.7326926649578,-4.88731742516968,131.373282004344));
#54846=CARTESIAN_POINT('Ctrl Pts',(66.7246449534593,-4.86875496264839,131.514784505445));
#54847=CARTESIAN_POINT('Ctrl Pts',(66.7165972419608,-4.84411353660799,131.6550938936));
#54848=CARTESIAN_POINT('Ctrl Pts',(66.7084693661741,-4.81922665415721,131.796800921595));
#54849=CARTESIAN_POINT('Ctrl Pts',(66.7003414903875,-4.78813913118351,131.937290584989));
#54850=CARTESIAN_POINT('Ctrl Pts',(66.6922136146009,-4.75100775206522,132.076016389509));
#54851=CARTESIAN_POINT('Ctrl Pts',(66.6841409245608,-4.71412848345291,132.213800288999));
#54852=CARTESIAN_POINT('Ctrl Pts',(66.6760682345207,-4.67128735843842,132.349843902826));
#54853=CARTESIAN_POINT('Ctrl Pts',(66.6679955444806,-4.62268674879548,132.483631377453));
#54854=CARTESIAN_POINT('Ctrl Pts',(66.6598400758208,-4.5735877809387,132.618790729663));
#54855=CARTESIAN_POINT('Ctrl Pts',(66.6516846071609,-4.51861071253405,132.751647085802));
#54856=CARTESIAN_POINT('Ctrl Pts',(66.643529138501,-4.45801197923393,132.881693584499));
#54857=CARTESIAN_POINT('Ctrl Pts',(66.6353736698411,-4.39741324593388,133.011740083196));
#54858=CARTESIAN_POINT('Ctrl Pts',(66.6272182011812,-4.33119306907287,133.138976436277));
#54859=CARTESIAN_POINT('Ctrl Pts',(66.6190627325213,-4.2596528185075,133.262925428239));
#54860=CARTESIAN_POINT('Ctrl Pts',(66.6112883984022,-4.19145590254206,133.381081835605));
#54861=CARTESIAN_POINT('Ctrl Pts',(66.6035140642831,-4.11823101838583,133.496585722954));
#54862=CARTESIAN_POINT('Ctrl Pts',(66.595739730164,-4.04020985348845,133.60897955822));
#54863=CARTESIAN_POINT('Ctrl Pts',(66.5879749772169,-3.96228484270385,133.721234878129));
#54864=CARTESIAN_POINT('Ctrl Pts',(66.5802102242698,-3.87957553308772,133.830387454122));
#54865=CARTESIAN_POINT('Ctrl Pts',(66.5724454713227,-3.79235925770069,133.936004646352));
#54866=CARTESIAN_POINT('Ctrl Pts',(66.5646884304377,-3.70522960674778,134.041516938099));
#54867=CARTESIAN_POINT('Ctrl Pts',(66.5569313895527,-3.61360214555809,134.143500534399));
#54868=CARTESIAN_POINT('Ctrl Pts',(66.5491743486677,-3.51779701433527,134.241552382428));
#54869=CARTESIAN_POINT('Ctrl Pts',(66.5414231574276,-3.42206413050729,134.339530288795));
#54870=CARTESIAN_POINT('Ctrl Pts',(66.5336719661875,-3.32216011947938,134.43358206996));
#54871=CARTESIAN_POINT('Ctrl Pts',(66.5259207749473,-3.2184446018404,134.523338623334));
#54872=CARTESIAN_POINT('Ctrl Pts',(66.5181728781703,-3.11477316606312,134.613057027778));
#54873=CARTESIAN_POINT('Ctrl Pts',(66.5104249813932,-3.00729374072816,134.698483580078));
#54874=CARTESIAN_POINT('Ctrl Pts',(66.5026770846161,-2.89640175899458,134.779287021035));
#54875=CARTESIAN_POINT('Ctrl Pts',(66.494930808532,-2.78553297347302,134.860073559654));
#54876=CARTESIAN_POINT('Ctrl Pts',(66.4871845324479,-2.67125336718392,134.93623868036));
#54877=CARTESIAN_POINT('Ctrl Pts',(66.4794382563638,-2.55398999360058,135.007492565898));
#54878=CARTESIAN_POINT('Ctrl Pts',(66.4716919230985,-2.43672575440566,135.078746977416));
#54879=CARTESIAN_POINT('Ctrl Pts',(66.4639455898331,-2.31647803808475,135.145089878401));
#54880=CARTESIAN_POINT('Ctrl Pts',(66.4561992565678,-2.19370095947873,135.206276014627));
#54881=CARTESIAN_POINT('Ctrl Pts',(66.4484511885648,-2.07089638579707,135.267475853064));
#54882=CARTESIAN_POINT('Ctrl Pts',(66.4407031205618,-1.94556167254729,135.323516454431));
#54883=CARTESIAN_POINT('Ctrl Pts',(66.4329550525588,-1.81817312439181,135.374199734235));
#54884=CARTESIAN_POINT('Ctrl Pts',(66.4251987498169,-1.69064918617141,135.424936880833));
#54885=CARTESIAN_POINT('Ctrl Pts',(66.4174424470751,-1.56106741643523,135.470305187077));
#54886=CARTESIAN_POINT('Ctrl Pts',(66.4096861443333,-1.42992210954663,135.510155536932));
#54887=CARTESIAN_POINT('Ctrl Pts',(66.4019257018191,-1.29870680645904,135.550027156119));
#54888=CARTESIAN_POINT('Ctrl Pts',(66.3941652593049,-1.16592668171449,135.584374852692));
#54889=CARTESIAN_POINT('Ctrl Pts',(66.3864048167908,-1.03208761408673,135.613100392117));
#54890=CARTESIAN_POINT('Ctrl Pts',(66.3786319165253,-0.898033696106121,
135.641872044328));
#54891=CARTESIAN_POINT('Ctrl Pts',(66.3708590162599,-0.762917823862867,
135.665003438184));
#54892=CARTESIAN_POINT('Ctrl Pts',(66.3630861159945,-0.627253307748616,
135.682447983575));
#54893=CARTESIAN_POINT('Ctrl Pts',(66.3555957802324,-0.496520538513051,
135.699258375801));
#54894=CARTESIAN_POINT('Ctrl Pts',(66.3481054444704,-0.365278628881969,
135.710788176821));
#54895=CARTESIAN_POINT('Ctrl Pts',(66.3406151087084,-0.233986190814424,
135.717041507366));
#54896=CARTESIAN_POINT('Ctrl Pts',(66.3328407745893,-0.0977157600522679,
135.72353193484));
#54897=CARTESIAN_POINT('Ctrl Pts',(66.3250664404702,0.0390407701182173,
135.724358438414));
#54898=CARTESIAN_POINT('Ctrl Pts',(66.3172921063511,0.175773232286202,135.719468636044));
#54899=CARTESIAN_POINT('Ctrl Pts',(66.309527353404,0.312337183914696,135.71458485992));
#54900=CARTESIAN_POINT('Ctrl Pts',(66.3017626004569,0.448876739593951,135.703998808814));
#54901=CARTESIAN_POINT('Ctrl Pts',(66.2939978475098,0.584878001874702,135.687709958482));
#54902=CARTESIAN_POINT('Ctrl Pts',(66.2862408066248,0.720744185784659,135.671437286465));
#54903=CARTESIAN_POINT('Ctrl Pts',(66.2784837657398,0.856072754576127,135.64947313323));
#54904=CARTESIAN_POINT('Ctrl Pts',(66.2707267248547,0.990351564891798,135.621868981899));
#54905=CARTESIAN_POINT('Ctrl Pts',(66.2629755336146,1.12452911451226,135.594285647073));
#54906=CARTESIAN_POINT('Ctrl Pts',(66.2552243423745,1.25765809994303,135.561070858228));
#54907=CARTESIAN_POINT('Ctrl Pts',(66.2474731511343,1.38923360101116,135.522327665387));
#54908=CARTESIAN_POINT('Ctrl Pts',(66.2397252543573,1.52075317898091,135.483600939436));
#54909=CARTESIAN_POINT('Ctrl Pts',(66.2319773575801,1.65072021156031,135.439350593103));
#54910=CARTESIAN_POINT('Ctrl Pts',(66.2242294608031,1.77864225972406,135.389730261818));
#54911=CARTESIAN_POINT('Ctrl Pts',(66.216483184719,1.9065375493532,135.340120310036));
#54912=CARTESIAN_POINT('Ctrl Pts',(66.2087369086349,2.03238834114532,135.285142748876));
#54913=CARTESIAN_POINT('Ctrl Pts',(66.2009906325508,2.15571997080239,135.225000217215));
#54914=CARTESIAN_POINT('Ctrl Pts',(66.1932442992854,2.27905251086554,135.164857241595));
#54915=CARTESIAN_POINT('Ctrl Pts',(66.1854979660201,2.39986550027812,135.09954939076));
#54916=CARTESIAN_POINT('Ctrl Pts',(66.1777516327547,2.51770713954999,135.029326158486));
#54917=CARTESIAN_POINT('Ctrl Pts',(66.1700035647517,2.63557516863977,134.959087200205));
#54918=CARTESIAN_POINT('Ctrl Pts',(66.1622554967488,2.75047018770366,134.883930870191));
#54919=CARTESIAN_POINT('Ctrl Pts',(66.1545074287458,2.86196808834432,134.804150827539));
#54920=CARTESIAN_POINT('Ctrl Pts',(66.146751126004,2.97358449028078,134.724285993708));
#54921=CARTESIAN_POINT('Ctrl Pts',(66.1389948232621,3.08179624297426,134.63978785859));
#54922=CARTESIAN_POINT('Ctrl Pts',(66.1312385205202,3.18621071270336,134.550991685173));
#54923=CARTESIAN_POINT('Ctrl Pts',(66.123478078006,3.29068091157882,134.462148118563));
#54924=CARTESIAN_POINT('Ctrl Pts',(66.1157176354919,3.39134950224234,134.369002208074));
#54925=CARTESIAN_POINT('Ctrl Pts',(66.1079571929778,3.48786039736403,134.271926465679));
#54926=CARTESIAN_POINT('Ctrl Pts',(66.1001842927123,3.58452622034241,134.174694888684));
#54927=CARTESIAN_POINT('Ctrl Pts',(66.0924113924469,3.67702074644487,134.073521162081));
#54928=CARTESIAN_POINT('Ctrl Pts',(66.0846384921815,3.76502732128719,133.968811965345));
#54929=CARTESIAN_POINT('Ctrl Pts',(66.0771481564195,3.84983463545808,133.867909211658));
#54930=CARTESIAN_POINT('Ctrl Pts',(66.0696578206575,3.93047444151396,133.763723815205));
#54931=CARTESIAN_POINT('Ctrl Pts',(66.0621674848956,4.00670231537586,133.656643846571));
#54932=CARTESIAN_POINT('Ctrl Pts',(66.0543931507765,4.08582039224497,133.545503908378));
#54933=CARTESIAN_POINT('Ctrl Pts',(66.0466188166573,4.16043599813095,133.43089351177));
#54934=CARTESIAN_POINT('Ctrl Pts',(66.0388444825382,4.23022930458927,133.313213561262));
#54935=CARTESIAN_POINT('Ctrl Pts',(66.0310797295911,4.2999365970349,133.195678640777));
#54936=CARTESIAN_POINT('Ctrl Pts',(66.0233149766441,4.36483321743604,133.075082026382));
#54937=CARTESIAN_POINT('Ctrl Pts',(66.015550223697,4.4246409506054,132.951855791187));
#54938=CARTESIAN_POINT('Ctrl Pts',(66.007793182812,4.48438928189103,132.828751946026));
#54939=CARTESIAN_POINT('Ctrl Pts',(66.0000361419269,4.53905861473284,132.70302402707));
#54940=CARTESIAN_POINT('Ctrl Pts',(65.9922791010419,4.58841543734564,132.575130742915));
#54941=CARTESIAN_POINT('Ctrl Pts',(65.9845279098018,4.63773503959436,132.447333904081));
#54942=CARTESIAN_POINT('Ctrl Pts',(65.9767767185618,4.68174996552895,132.317375313543));
#54943=CARTESIAN_POINT('Ctrl Pts',(65.9690255273217,4.72027399236456,132.185735475998));
#54944=CARTESIAN_POINT('Ctrl Pts',(65.9612776305446,4.75878164546126,132.054151588894));
#54945=CARTESIAN_POINT('Ctrl Pts',(65.9535297337675,4.79180293158724,131.92088825046));
#54946=CARTESIAN_POINT('Ctrl Pts',(65.9457818369904,4.81920093325826,131.786442807295));
#54947=CARTESIAN_POINT('Ctrl Pts',(65.9380355609063,4.84659320385795,131.652025487219));
#54948=CARTESIAN_POINT('Ctrl Pts',(65.9302892848222,4.86836445164901,131.516426937096));
#54949=CARTESIAN_POINT('Ctrl Pts',(65.9225430087381,4.88442859480994,131.380156036706));
#54950=CARTESIAN_POINT('Ctrl Pts',(65.9147966754727,4.90049285655268,131.243884130396));
#54951=CARTESIAN_POINT('Ctrl Pts',(65.9070503422074,4.9108498838293,131.106940252193));
#54952=CARTESIAN_POINT('Ctrl Pts',(65.899304008942,4.91546537416024,130.969839371283));
#54953=CARTESIAN_POINT('Ctrl Pts',(65.8915559409391,4.92008189809823,130.832707787581));
#54954=CARTESIAN_POINT('Ctrl Pts',(65.8838078729361,4.91895431339053,130.695419521879));
#54955=CARTESIAN_POINT('Ctrl Pts',(65.8760598049332,4.91210044280317,130.558490118496));
#54956=CARTESIAN_POINT('Ctrl Pts',(65.8683035021913,4.90523928784057,130.421415184914));
#54957=CARTESIAN_POINT('Ctrl Pts',(65.8605471994494,4.89263970920417,130.284700266643));
#54958=CARTESIAN_POINT('Ctrl Pts',(65.8527908967076,4.87437154502329,130.148856915389));
#54959=CARTESIAN_POINT('Ctrl Pts',(65.8450304541934,4.85609363057314,130.012941060449));
#54960=CARTESIAN_POINT('Ctrl Pts',(65.8372700116793,4.83214117027004,129.877898084206));
#54961=CARTESIAN_POINT('Ctrl Pts',(65.8295095691651,4.8026350950883,129.744228924838));
#54962=CARTESIAN_POINT('Ctrl Pts',(65.8217366688996,4.77308165413526,129.610345187869));
#54963=CARTESIAN_POINT('Ctrl Pts',(65.8139637686342,4.73795688321754,129.477840052943));
#54964=CARTESIAN_POINT('Ctrl Pts',(65.8061908683688,4.69743177386798,129.347199750553));
#54965=CARTESIAN_POINT('Ctrl Pts',(65.7987005326067,4.65837985431943,129.221308552216));
#54966=CARTESIAN_POINT('Ctrl Pts',(65.7912101968445,4.61431351450875,129.097149247888));
#54967=CARTESIAN_POINT('Ctrl Pts',(65.7837198610824,4.56542713202485,128.975137240099));
#54968=CARTESIAN_POINT('Ctrl Pts',(65.7759455269633,4.51468720749096,128.848499109952));
#54969=CARTESIAN_POINT('Ctrl Pts',(65.7681711928443,4.45859379245806,128.723773168615));
#54970=CARTESIAN_POINT('Ctrl Pts',(65.7603968587252,4.39731130416395,128.601445195501));
#54971=CARTESIAN_POINT('Ctrl Pts',(65.7526321057781,4.33610434105961,128.479267980681));
#54972=CARTESIAN_POINT('Ctrl Pts',(65.744867352831,4.26972120241002,128.359483200153));
#54973=CARTESIAN_POINT('Ctrl Pts',(65.7371025998839,4.19837502145539,128.242558470303));
#54974=CARTESIAN_POINT('Ctrl Pts',(65.7293455589989,4.12709970253359,128.125749871744));
#54975=CARTESIAN_POINT('Ctrl Pts',(65.7215885181139,4.05087135328964,128.011796002438));
#54976=CARTESIAN_POINT('Ctrl Pts',(65.7138314772289,3.96994967943336,127.901141265663));
#54977=CARTESIAN_POINT('Ctrl Pts',(65.7060802859888,3.88908902924115,127.790569974486));
#54978=CARTESIAN_POINT('Ctrl Pts',(65.6983290947487,3.80354232899519,127.683293178129));
#54979=CARTESIAN_POINT('Ctrl Pts',(65.6905779035086,3.71361318294052,127.57972727562));
#54980=CARTESIAN_POINT('Ctrl Pts',(65.6828300067315,3.62372225917162,127.476205391382));
#54981=CARTESIAN_POINT('Ctrl Pts',(65.6750821099545,3.52945285007382,127.376391558591));
#54982=CARTESIAN_POINT('Ctrl Pts',(65.6673342131774,3.43114938018312,127.280669797791));
#54983=CARTESIAN_POINT('Ctrl Pts',(65.6595879370933,3.33286647325929,127.184968059919));
#54984=CARTESIAN_POINT('Ctrl Pts',(65.6518416610092,3.23055146391411,127.093356964039));
#54985=CARTESIAN_POINT('Ctrl Pts',(65.6440953849251,3.12458595779127,127.006183995176));
#54986=CARTESIAN_POINT('Ctrl Pts',(65.6363490516597,3.01861966945485,126.919010382821));
#54987=CARTESIAN_POINT('Ctrl Pts',(65.6286027183944,2.90900313249718,126.836275211237));
#54988=CARTESIAN_POINT('Ctrl Pts',(65.620856385129,2.79615106375221,126.758285693497));
#54989=CARTESIAN_POINT('Ctrl Pts',(65.613108317126,2.6832737225689,126.680278710546));
#54990=CARTESIAN_POINT('Ctrl Pts',(65.6053602491231,2.56715972935017,126.60701971843));
#54991=CARTESIAN_POINT('Ctrl Pts',(65.5976121811201,2.44825245977412,126.538772386652));
#54992=CARTESIAN_POINT('Ctrl Pts',(65.5898558783782,2.32921881413694,126.470452520798));
#54993=CARTESIAN_POINT('Ctrl Pts',(65.5820995756364,2.20738630141379,126.407155150371));
#54994=CARTESIAN_POINT('Ctrl Pts',(65.5743432728945,2.08322305375562,126.349098024766));
#54995=CARTESIAN_POINT('Ctrl Pts',(65.5665828303803,1.9589935364337,126.291009912326));
#54996=CARTESIAN_POINT('Ctrl Pts',(65.5588223878662,1.8324311660397,126.238167768281));
#54997=CARTESIAN_POINT('Ctrl Pts',(65.551061945352,1.70402276219455,126.190740619298));
#54998=CARTESIAN_POINT('Ctrl Pts',(65.5432890450866,1.57540822577998,126.143237336045));
#54999=CARTESIAN_POINT('Ctrl Pts',(65.5355161448212,1.4449421063749,126.101166538557));
#55000=CARTESIAN_POINT('Ctrl Pts',(65.5277432445557,1.31312590856396,126.064647186275));
#55001=CARTESIAN_POINT('Ctrl Pts',(65.5202529087937,1.1861015615686,126.029455404435));
#55002=CARTESIAN_POINT('Ctrl Pts',(65.5127625730317,1.05782388941703,125.999418527393));
#55003=CARTESIAN_POINT('Ctrl Pts',(65.5052722372697,0.928747447857728,125.974597554993));
#55004=CARTESIAN_POINT('Ctrl Pts',(65.4974979031506,0.794777033784942,125.94883548788));
#55005=CARTESIAN_POINT('Ctrl Pts',(65.4897235690315,0.659521705933291,125.928611048702));
#55006=CARTESIAN_POINT('Ctrl Pts',(65.4819492349125,0.523479035813597,125.914048484219));
#55007=CARTESIAN_POINT('Ctrl Pts',(65.4741844819654,0.38760402612616,125.899503866795));
#55008=CARTESIAN_POINT('Ctrl Pts',(65.4664197290183,0.250943989848566,125.890607281628));
#55009=CARTESIAN_POINT('Ctrl Pts',(65.4586549760712,0.114007549612928,125.887432171765));
#55010=CARTESIAN_POINT('Ctrl Pts',(65.4508979351862,-0.0227928834199881,
125.884260215465));
#55011=CARTESIAN_POINT('Ctrl Pts',(65.4431408943012,-0.159868785756313,
125.886798434745));
#55012=CARTESIAN_POINT('Ctrl Pts',(65.4353838534162,-0.296705891051209,
125.895068542662));
#55013=CARTESIAN_POINT('Ctrl Pts',(65.427632662176,-0.433439806420751,125.903332414026));
#55014=CARTESIAN_POINT('Ctrl Pts',(65.4198814709359,-0.569934894510545,
125.917319546939));
#55015=CARTESIAN_POINT('Ctrl Pts',(65.4121302796958,-0.705676721514948,
125.936999584397));
#55016=CARTESIAN_POINT('Ctrl Pts',(65.4043823829187,-0.841360854621289,
125.956671257314));
#55017=CARTESIAN_POINT('Ctrl Pts',(65.3966344861416,-0.976291977298376,
125.982030966324));
#55018=CARTESIAN_POINT('Ctrl Pts',(65.3888865893645,-1.10996083231246,126.012996509795));
#55019=CARTESIAN_POINT('Ctrl Pts',(65.3811403132805,-1.24360172668364,126.043955575942));
#55020=CARTESIAN_POINT('Ctrl Pts',(65.3733940371964,-1.37598049794283,126.080518055968));
#55021=CARTESIAN_POINT('Ctrl Pts',(65.3656477611123,-1.50659852992527,126.122550718379));
#55022=CARTESIAN_POINT('Ctrl Pts',(65.357901427847,-1.63721752610017,126.164583691066));
#55023=CARTESIAN_POINT('Ctrl Pts',(65.3501550945816,-1.76607538489307,126.21208680695));
#55024=CARTESIAN_POINT('Ctrl Pts',(65.3424087613163,-1.89268947466686,126.264877209183));
#55025=CARTESIAN_POINT('Ctrl Pts',(65.3346606933133,-2.01933191878851,126.317679433461));
#55026=CARTESIAN_POINT('Ctrl Pts',(65.3269126253104,-2.14372923323401,126.375771149786));
#55027=CARTESIAN_POINT('Ctrl Pts',(65.3191645573074,-2.26541993000123,126.438921853449));
#55028=CARTESIAN_POINT('Ctrl Pts',(65.3114082545656,-2.38723996108896,126.502139674432));
#55029=CARTESIAN_POINT('Ctrl Pts',(65.3036519518237,-2.50634728055511,126.570427043021));
#55030=CARTESIAN_POINT('Ctrl Pts',(65.2958956490819,-2.62230565280428,126.643507805248));
#55031=CARTESIAN_POINT('Ctrl Pts',(65.2881352065677,-2.73832591552831,126.716627572879));
#55032=CARTESIAN_POINT('Ctrl Pts',(65.2803747640536,-2.85119356053653,126.794545609926));
#55033=CARTESIAN_POINT('Ctrl Pts',(65.2726143215394,-2.96050324301058,126.876943704298));
#55034=CARTESIAN_POINT('Ctrl Pts',(65.264841421274,-3.06998839909099,126.959474071406));
#55035=CARTESIAN_POINT('Ctrl Pts',(65.2570685210085,-3.17590387687434,127.046498618975));
#55036=CARTESIAN_POINT('Ctrl Pts',(65.2492956207431,-3.2778785169376,127.137659717479));
#55037=CARTESIAN_POINT('Ctrl Pts',(65.241805284981,-3.37614612197718,127.225506880432));
#55038=CARTESIAN_POINT('Ctrl Pts',(65.2343149492189,-3.47075421247686,127.317194853294));
#55039=CARTESIAN_POINT('Ctrl Pts',(65.2268246134568,-3.56140576905517,127.412374177345));
#55040=CARTESIAN_POINT('Ctrl Pts',(65.2191475807491,-3.65431681963504,127.5099258502));
#55041=CARTESIAN_POINT('Ctrl Pts',(65.2114705480414,-3.74338205395473,127.611471582107));
#55042=CARTESIAN_POINT('Ctrl Pts',(65.2037935153337,-3.82823189034494,127.716671569711));
#55043=CARTESIAN_POINT('Ctrl Pts',(65.1961255500607,-3.91298150958423,127.821747304358));
#55044=CARTESIAN_POINT('Ctrl Pts',(65.1884575847876,-3.99352538054134,127.930468404211));
#55045=CARTESIAN_POINT('Ctrl Pts',(65.1807896195146,-4.06953018480535,128.042457806557));
#55046=CARTESIAN_POINT('Ctrl Pts',(65.1727975325316,-4.14874768060431,128.159180954466));
#55047=CARTESIAN_POINT('Ctrl Pts',(65.1648054455486,-4.22303364486602,128.279454471617));
#55048=CARTESIAN_POINT('Ctrl Pts',(65.1568133585656,-4.29205620188384,128.402811820983));
#55049=CARTESIAN_POINT('Ctrl Pts',(65.1491588987257,-4.35816288864318,128.520957917075));
#55050=CARTESIAN_POINT('Ctrl Pts',(65.1415044388858,-4.41944155453826,128.641932227695));
#55051=CARTESIAN_POINT('Ctrl Pts',(65.1338499790459,-4.47564455395244,128.765294927311));
#55052=CARTESIAN_POINT('Ctrl Pts',(65.1261988623244,-4.53182300646449,128.888603747736));
#55053=CARTESIAN_POINT('Ctrl Pts',(65.1185477456028,-4.5829300369661,129.014298517022));
#55054=CARTESIAN_POINT('Ctrl Pts',(65.1108966288812,-4.62876447172692,129.141915873288));
#55055=CARTESIAN_POINT('Ctrl Pts',(65.1032467506769,-4.67459148708259,129.269512571616));
#55056=CARTESIAN_POINT('Ctrl Pts',(65.0955968724725,-4.71514746886405,129.399030860214));
#55057=CARTESIAN_POINT('Ctrl Pts',(65.0879469942681,-4.75027998543829,129.529988959672));
#55058=CARTESIAN_POINT('Ctrl Pts',(65.086926188085,-4.75496809800567,129.547464118634));
#55059=CARTESIAN_POINT('Ctrl Pts',(65.0859053819018,-4.75955971051597,129.564964893244));
#55060=CARTESIAN_POINT('Ctrl Pts',(65.0848845757186,-4.764054528234,129.582490119308));
#55061=CARTESIAN_POINT('Ctrl Pts',(66.8345747415593,-4.76405452823409,129.582490119308));
#55062=CARTESIAN_POINT('Ctrl Pts',(66.8263521180634,-4.80010819768355,129.723062829301));
#55063=CARTESIAN_POINT('Ctrl Pts',(66.8181294945675,-4.82997550392153,129.865386831657));
#55064=CARTESIAN_POINT('Ctrl Pts',(66.8099068710717,-4.85349778080253,130.008909579321));
#55065=CARTESIAN_POINT('Ctrl Pts',(66.8017034909999,-4.87696500844651,130.152096440379));
#55066=CARTESIAN_POINT('Ctrl Pts',(66.7935001109281,-4.89411676822097,130.296476141404));
#55067=CARTESIAN_POINT('Ctrl Pts',(66.7852967308564,-4.90484495065059,130.44148450568));
#55068=CARTESIAN_POINT('Ctrl Pts',(66.7784842992448,-4.91375408426128,130.561905546288));
#55069=CARTESIAN_POINT('Ctrl Pts',(66.7716718676332,-4.91823415872638,130.682759772639));
#55070=CARTESIAN_POINT('Ctrl Pts',(66.7648594360216,-4.91824995804488,130.803718206823));
#55071=CARTESIAN_POINT('',(67.1101405639552,-4.91824833737017,130.800316553325));
#55072=CARTESIAN_POINT('Ctrl Pts',(67.1801803489693,-4.76405452823408,129.582490119308));
#55073=CARTESIAN_POINT('Ctrl Pts',(67.1722432273088,-4.79875915536151,129.717802933762));
#55074=CARTESIAN_POINT('Ctrl Pts',(67.1643061056482,-4.82764789875426,129.854414213236));
#55075=CARTESIAN_POINT('Ctrl Pts',(67.1563689839877,-4.85065958804843,129.991781622407));
#55076=CARTESIAN_POINT('Ctrl Pts',(67.1439813375631,-4.88657445527619,130.206174064384));
#55077=CARTESIAN_POINT('Ctrl Pts',(67.1315936911385,-4.90828242222668,130.423009367747));
#55078=CARTESIAN_POINT('Ctrl Pts',(67.1192060447139,-4.91552932682745,130.64079259013));
#55079=CARTESIAN_POINT('Ctrl Pts',(67.1161842178121,-4.9172971276289,130.69391835572));
#55080=CARTESIAN_POINT('Ctrl Pts',(67.1131623909104,-4.91820457997885,130.747100369239));
#55081=CARTESIAN_POINT('Ctrl Pts',(67.1101405640086,-4.91824833736939,130.800316552386));
#55082=CARTESIAN_POINT('Ctrl Pts',(67.1101405639552,-4.91824833737017,130.800316553325));
#55083=CARTESIAN_POINT('Ctrl Pts',(67.1024929960437,-4.91835907751146,130.934994808511));
#55084=CARTESIAN_POINT('Ctrl Pts',(67.0948454281322,-4.91293374377952,131.069873198528));
#55085=CARTESIAN_POINT('Ctrl Pts',(67.0871978602207,-4.90194968703462,131.204451017702));
#55086=CARTESIAN_POINT('Ctrl Pts',(67.0795575524082,-4.89097605783222,131.338901077529));
#55087=CARTESIAN_POINT('Ctrl Pts',(67.0719172445957,-4.87445423398753,131.473050734335));
#55088=CARTESIAN_POINT('Ctrl Pts',(67.0642769367832,-4.85241361143598,131.606398775044));
#55089=CARTESIAN_POINT('Ctrl Pts',(67.0565121210911,-4.83001381079315,131.741919880267));
#55090=CARTESIAN_POINT('Ctrl Pts',(67.0487473053991,-4.80191375142125,131.87661259095));
#55091=CARTESIAN_POINT('Ctrl Pts',(67.0409824897071,-4.76819932657029,132.009955178185));
#55092=CARTESIAN_POINT('Ctrl Pts',(67.0333500180552,-4.73505953264051,132.14102506541));
#55093=CARTESIAN_POINT('Ctrl Pts',(67.0257175464032,-4.69649534909657,132.270790082721));
#55094=CARTESIAN_POINT('Ctrl Pts',(67.0180850747513,-4.65263987246651,132.398764982724));
#55095=CARTESIAN_POINT('Ctrl Pts',(67.0104535181768,-4.60878965378661,132.526724539474));
#55096=CARTESIAN_POINT('Ctrl Pts',(67.0028219616023,-4.55964953417331,132.652894023819));
#55097=CARTESIAN_POINT('Ctrl Pts',(66.9951904050278,-4.50540214616269,132.776804422558));
#55098=CARTESIAN_POINT('Ctrl Pts',(66.987557996453,-4.45114870187897,132.900728654871));
#55099=CARTESIAN_POINT('Ctrl Pts',(66.9799255878781,-4.39178701776272,133.022392930459));
#55100=CARTESIAN_POINT('Ctrl Pts',(66.9722931793033,-4.32754719246508,133.141349783028));
#55101=CARTESIAN_POINT('Ctrl Pts',(66.9644288610426,-4.2613554489021,133.263921123218));
#55102=CARTESIAN_POINT('Ctrl Pts',(66.9565645427819,-4.18998461287187,133.383617484527));
#55103=CARTESIAN_POINT('Ctrl Pts',(66.9487002245212,-4.11373581287558,133.499979419319));
#55104=CARTESIAN_POINT('Ctrl Pts',(66.9410567650359,-4.03962835762559,133.613073486056));
#55105=CARTESIAN_POINT('Ctrl Pts',(66.9334133055505,-3.96091354320488,133.723017613029));
#55106=CARTESIAN_POINT('Ctrl Pts',(66.9257698460652,-3.87790958048365,133.829422657937));
#55107=CARTESIAN_POINT('Ctrl Pts',(66.9177950984168,-3.79130800199817,133.940439584668));
#55108=CARTESIAN_POINT('Ctrl Pts',(66.9098203507684,-3.70003745642511,134.047603378814));
#55109=CARTESIAN_POINT('Ctrl Pts',(66.90184560312,-3.60450218679224,134.150514685733));
#55110=CARTESIAN_POINT('Ctrl Pts',(66.8938708554716,-3.50896691715949,134.253425992652));
#55111=CARTESIAN_POINT('Ctrl Pts',(66.8858961078232,-3.40916732640844,134.352084522751));
#55112=CARTESIAN_POINT('Ctrl Pts',(66.8779213601748,-3.30554571334739,134.446139111581));
#55113=CARTESIAN_POINT('Ctrl Pts',(66.8701470260557,-3.20452821694329,134.537830012815));
#55114=CARTESIAN_POINT('Ctrl Pts',(66.8623726919366,-3.09953277183999,134.62545984883));
#55115=CARTESIAN_POINT('Ctrl Pts',(66.8545983578175,-2.99091970195566,134.708663679439));
#55116=CARTESIAN_POINT('Ctrl Pts',(66.8468336048704,-2.88244048797293,134.791764968763));
#55117=CARTESIAN_POINT('Ctrl Pts',(66.8390688519233,-2.7703528274791,134.870450870348));
#55118=CARTESIAN_POINT('Ctrl Pts',(66.8313040989762,-2.65505290971584,134.944394084714));
#55119=CARTESIAN_POINT('Ctrl Pts',(66.8235470580912,-2.5398675094565,135.018263857638));
#55120=CARTESIAN_POINT('Ctrl Pts',(66.8157900172062,-2.42147652805856,135.087400107768));
#55121=CARTESIAN_POINT('Ctrl Pts',(66.8080329763212,-2.30030788368171,135.151516780251));
#55122=CARTESIAN_POINT('Ctrl Pts',(66.8002817850811,-2.17923061352214,135.215585101853));
#55123=CARTESIAN_POINT('Ctrl Pts',(66.792530593841,-2.05538019384104,135.274641198104));
#55124=CARTESIAN_POINT('Ctrl Pts',(66.7847794026009,-1.92921177158329,135.328443397852));
#55125=CARTESIAN_POINT('Ctrl Pts',(66.7770315058238,-1.80309697427066,135.38222273023));
#55126=CARTESIAN_POINT('Ctrl Pts',(66.7692836090467,-1.67466649277362,135.430752454426));
#55127=CARTESIAN_POINT('Ctrl Pts',(66.7615357122696,-1.5443980214469,135.473837870305));
#55128=CARTESIAN_POINT('Ctrl Pts',(66.7537894361856,-1.41415679947611,135.516914273645));
#55129=CARTESIAN_POINT('Ctrl Pts',(66.7460431601014,-1.28207872335766,135.554548511176));
#55130=CARTESIAN_POINT('Ctrl Pts',(66.7382968840173,-1.14865894403689,135.586595000444));
#55131=CARTESIAN_POINT('Ctrl Pts',(66.730550550752,-1.01523817984162,135.618641726272));
#55132=CARTESIAN_POINT('Ctrl Pts',(66.7228042174866,-0.880476072833954,
135.64510053022));
#55133=CARTESIAN_POINT('Ctrl Pts',(66.7150578842213,-0.744879936338025,
135.665876527541));
#55134=CARTESIAN_POINT('Ctrl Pts',(66.7073098162183,-0.60925343402767,135.686657177502));
#55135=CARTESIAN_POINT('Ctrl Pts',(66.6995617482154,-0.472792916949479,
135.701752429259));
#55136=CARTESIAN_POINT('Ctrl Pts',(66.6918136802124,-0.336012425982121,
135.711119090538));
#55137=CARTESIAN_POINT('Ctrl Pts',(66.6840573774706,-0.199086563081068,
135.720495706817));
#55138=CARTESIAN_POINT('Ctrl Pts',(66.6763010747287,-0.0618404376339475,
135.724131543603));
#55139=CARTESIAN_POINT('Ctrl Pts',(66.6685447719869,0.0752097306826276,
135.722035531477));
#55140=CARTESIAN_POINT('Ctrl Pts',(66.6607843294727,0.212333046800534,135.719938400647));
#55141=CARTESIAN_POINT('Ctrl Pts',(66.6530238869585,0.349259807251273,135.712103347394));
#55142=CARTESIAN_POINT('Ctrl Pts',(66.6452634444443,0.485478297085964,135.698591291079));
#55143=CARTESIAN_POINT('Ctrl Pts',(66.6374905441789,0.621915456933632,135.685057544012));
#55144=CARTESIAN_POINT('Ctrl Pts',(66.6297176439135,0.757641686796736,135.665828637622));
#55145=CARTESIAN_POINT('Ctrl Pts',(66.6219447436481,0.892153963876741,135.641016938542));
#55146=CARTESIAN_POINT('Ctrl Pts',(66.614454407886,1.02177638086946,135.617107207221));
#55147=CARTESIAN_POINT('Ctrl Pts',(66.6069640721239,1.15027127281611,135.588013601413));
#55148=CARTESIAN_POINT('Ctrl Pts',(66.5994737363619,1.2772031870345,135.553880075525));
#55149=CARTESIAN_POINT('Ctrl Pts',(66.5916994022428,1.40894776336004,135.518452366628));
#55150=CARTESIAN_POINT('Ctrl Pts',(66.5839250681237,1.53942582893993,135.477482791881));
#55151=CARTESIAN_POINT('Ctrl Pts',(66.5761507340046,1.66813558538054,135.431077242916));
#55152=CARTESIAN_POINT('Ctrl Pts',(66.5683859810575,1.79668671854929,135.384728884643));
#55153=CARTESIAN_POINT('Ctrl Pts',(66.5606212281104,1.92347351444267,135.332958013198));
#55154=CARTESIAN_POINT('Ctrl Pts',(66.5528564751634,2.04800645677809,135.275921040449));
#55155=CARTESIAN_POINT('Ctrl Pts',(66.5450994342784,2.17241571123975,135.218940717626));
#55156=CARTESIAN_POINT('Ctrl Pts',(66.5373423933933,2.29457521382065,135.156704863911));
#55157=CARTESIAN_POINT('Ctrl Pts',(66.5295853525083,2.41401299825359,135.089418879336));
#55158=CARTESIAN_POINT('Ctrl Pts',(66.5218341612682,2.5333607137242,135.022183635645));
#55159=CARTESIAN_POINT('Ctrl Pts',(66.5140829700281,2.64999045710881,134.949906032491));
#55160=CARTESIAN_POINT('Ctrl Pts',(66.5063317787879,2.76345288557983,134.872838368726));
#55161=CARTESIAN_POINT('Ctrl Pts',(66.4985838820109,2.87686708949188,134.795803460773));
#55162=CARTESIAN_POINT('Ctrl Pts',(66.4908359852338,2.98711633322886,134.713982760682));
#55163=CARTESIAN_POINT('Ctrl Pts',(66.4830880884567,3.09377860458702,134.627672926062));
#55164=CARTESIAN_POINT('Ctrl Pts',(66.4753418123726,3.20041856449737,134.5413811456));
#55165=CARTESIAN_POINT('Ctrl Pts',(66.4675955362885,3.30347274071809,134.450602344169));
#55166=CARTESIAN_POINT('Ctrl Pts',(66.4598492602044,3.40255100942519,134.35567441541));
#55167=CARTESIAN_POINT('Ctrl Pts',(66.452102926939,3.50163000950569,134.260745785915));
#55168=CARTESIAN_POINT('Ctrl Pts',(66.4443565936737,3.59673276120459,134.161668238454));
#55169=CARTESIAN_POINT('Ctrl Pts',(66.4366102604083,3.68750522005332,134.058817302572));
#55170=CARTESIAN_POINT('Ctrl Pts',(66.4288621924053,3.77829800676484,133.955943333935));
#55171=CARTESIAN_POINT('Ctrl Pts',(66.4211141244024,3.86475831230156,133.849294588451));
#55172=CARTESIAN_POINT('Ctrl Pts',(66.4133660563994,3.94657194613094,133.73928019679));
#55173=CARTESIAN_POINT('Ctrl Pts',(66.4056097536576,4.02847253246385,133.629148880525));
#55174=CARTESIAN_POINT('Ctrl Pts',(66.3978534509157,4.10571634815101,133.515645086767));
#55175=CARTESIAN_POINT('Ctrl Pts',(66.3900971481739,4.17803187739915,133.399207952948));
#55176=CARTESIAN_POINT('Ctrl Pts',(66.3823367056597,4.25038600362273,133.282708673124));
#55177=CARTESIAN_POINT('Ctrl Pts',(66.3745762631455,4.31780641006646,133.163273273924));
#55178=CARTESIAN_POINT('Ctrl Pts',(66.3668158206313,4.38006775548502,133.04136520403));
#55179=CARTESIAN_POINT('Ctrl Pts',(66.3590429203659,4.44242904834255,132.919261436479));
#55180=CARTESIAN_POINT('Ctrl Pts',(66.3512700201005,4.49961456734348,132.794677421732));
#55181=CARTESIAN_POINT('Ctrl Pts',(66.3434971198351,4.55144695361076,132.668097104027));
#55182=CARTESIAN_POINT('Ctrl Pts',(66.336006784073,4.60139510207919,132.546118299708));
#55183=CARTESIAN_POINT('Ctrl Pts',(66.3285164483111,4.64637245529841,132.42228610336));
#55184=CARTESIAN_POINT('Ctrl Pts',(66.321026112549,4.68626475337587,132.29704468453));
#55185=CARTESIAN_POINT('Ctrl Pts',(66.31325177843,4.72766958006006,132.167054699238));
#55186=CARTESIAN_POINT('Ctrl Pts',(66.3054774443109,4.7637272980565,132.035134751446));
#55187=CARTESIAN_POINT('Ctrl Pts',(66.2977031101918,4.79425576270565,131.901764255369));
#55188=CARTESIAN_POINT('Ctrl Pts',(66.2899383572447,4.82474660375058,131.768558126509));
#55189=CARTESIAN_POINT('Ctrl Pts',(66.2821736042976,4.84972166349704,131.633905383745));
#55190=CARTESIAN_POINT('Ctrl Pts',(66.2744088513505,4.86904794017105,131.498302415425));
#55191=CARTESIAN_POINT('Ctrl Pts',(66.2666518104655,4.8883550217146,131.362834129885));
#55192=CARTESIAN_POINT('Ctrl Pts',(66.2588947695804,4.90202443042993,131.226417881499));
#55193=CARTESIAN_POINT('Ctrl Pts',(66.2511377286954,4.90997386588508,131.089561772587));
#55194=CARTESIAN_POINT('Ctrl Pts',(66.2433865374554,4.91791730660904,130.952808867933));
#55195=CARTESIAN_POINT('Ctrl Pts',(66.2356353462153,4.92014933720628,130.815617151715));
#55196=CARTESIAN_POINT('Ctrl Pts',(66.2278841549752,4.91663934307343,130.678501042473));
#55197=CARTESIAN_POINT('Ctrl Pts',(66.2201362581981,4.91313084078168,130.541443211234));
#55198=CARTESIAN_POINT('Ctrl Pts',(66.212388361421,4.90388517773935,130.404461313076));
#55199=CARTESIAN_POINT('Ctrl Pts',(66.2046404646439,4.88892383249246,130.268070749503));
#55200=CARTESIAN_POINT('Ctrl Pts',(66.1968941885598,4.87396561683648,130.131708715896));
#55201=CARTESIAN_POINT('Ctrl Pts',(66.1891479124757,4.85329413968906,129.995938159226));
#55202=CARTESIAN_POINT('Ctrl Pts',(66.1814016363916,4.8269828090832,129.861269941483));
#55203=CARTESIAN_POINT('Ctrl Pts',(66.1736553031263,4.80067128425308,129.726600729649));
#55204=CARTESIAN_POINT('Ctrl Pts',(66.165908969861,4.76871989785951,129.593034256689));
#55205=CARTESIAN_POINT('Ctrl Pts',(66.1581626365956,4.73125322386009,129.461071373131));
#55206=CARTESIAN_POINT('Ctrl Pts',(66.1504145685926,4.69377815945876,129.329078937401));
#55207=CARTESIAN_POINT('Ctrl Pts',(66.1426665005896,4.65078545648614,129.198691181695));
#55208=CARTESIAN_POINT('Ctrl Pts',(66.1349184325866,4.60244950050618,129.070393588528));
#55209=CARTESIAN_POINT('Ctrl Pts',(66.1271621298448,4.55406217249707,128.941959639153));
#55210=CARTESIAN_POINT('Ctrl Pts',(66.1194058271029,4.50032038537794,128.815620656346));
#55211=CARTESIAN_POINT('Ctrl Pts',(66.111649524361,4.44144683698859,128.691842438543));
#55212=CARTESIAN_POINT('Ctrl Pts',(66.1038890818469,4.38254186601374,128.567998156578));
#55213=CARTESIAN_POINT('Ctrl Pts',(66.0961286393327,4.31849985859843,128.446717708552));
#55214=CARTESIAN_POINT('Ctrl Pts',(66.0883681968185,4.2495889247968,128.32844118577));
#55215=CARTESIAN_POINT('Ctrl Pts',(66.0805952965531,4.18056736904661,128.209974795014));
#55216=CARTESIAN_POINT('Ctrl Pts',(66.0728223962876,4.10666147889138,128.094522295196));
#55217=CARTESIAN_POINT('Ctrl Pts',(66.0650494960222,4.0281825435191,127.982494487044));
#55218=CARTESIAN_POINT('Ctrl Pts',(66.0575591602601,3.9525565151239,127.874539171899));
#55219=CARTESIAN_POINT('Ctrl Pts',(66.0500688244981,3.87268433927344,127.769764123914));
#55220=CARTESIAN_POINT('Ctrl Pts',(66.042578488736,3.78887794812418,127.668505557663));
#55221=CARTESIAN_POINT('Ctrl Pts',(66.0348041546169,3.70189401218245,127.563407742096));
#55222=CARTESIAN_POINT('Ctrl Pts',(66.0270298204978,3.61039610127415,127.461765408633));
#55223=CARTESIAN_POINT('Ctrl Pts',(66.0192554863787,3.51468910651767,127.363990935827));
#55224=CARTESIAN_POINT('Ctrl Pts',(66.0114907334316,3.41910006207865,127.266336961321));
#55225=CARTESIAN_POINT('Ctrl Pts',(66.0037259804846,3.31931252587049,127.172541639686));
#55226=CARTESIAN_POINT('Ctrl Pts',(65.9959612275375,3.21567223276058,127.082985179109));
#55227=CARTESIAN_POINT('Ctrl Pts',(65.9882041866524,3.11213487665057,126.99351766727));
#55228=CARTESIAN_POINT('Ctrl Pts',(65.9804471457674,3.0047526726784,126.908280892175));
#55229=CARTESIAN_POINT('Ctrl Pts',(65.9726901048824,2.89390861632368,126.827618737224));
#55230=CARTESIAN_POINT('Ctrl Pts',(65.9649389136423,2.78314814833485,126.747017410232));
#55231=CARTESIAN_POINT('Ctrl Pts',(65.9571877224022,2.66893133906706,126.670984065966));
#55232=CARTESIAN_POINT('Ctrl Pts',(65.9494365311621,2.55167443546606,126.599822517145));
#55233=CARTESIAN_POINT('Ctrl Pts',(65.941688634385,2.43446736917655,126.528691213881));
#55234=CARTESIAN_POINT('Ctrl Pts',(65.9339407376079,2.31422311201487,126.462427790126));
#55235=CARTESIAN_POINT('Ctrl Pts',(65.9261928408308,2.1913868955423,126.401292762474));
#55236=CARTESIAN_POINT('Ctrl Pts',(65.9184465647467,2.06857637375801,126.340170522951));
#55237=CARTESIAN_POINT('Ctrl Pts',(65.9107002886626,1.94317532088278,126.284174719862));
#55238=CARTESIAN_POINT('Ctrl Pts',(65.9029540125785,1.81565321841043,126.233519726332));
#55239=CARTESIAN_POINT('Ctrl Pts',(65.8952076793131,1.68813017459889,126.182864358878));
#55240=CARTESIAN_POINT('Ctrl Pts',(65.8874613460478,1.55848641329632,126.137550023984));
#55241=CARTESIAN_POINT('Ctrl Pts',(65.8797150127824,1.4272106495052,126.097742635996));
#55242=CARTESIAN_POINT('Ctrl Pts',(65.8719669447794,1.29590548741734,126.057926333419));
#55243=CARTESIAN_POINT('Ctrl Pts',(65.8642188767764,1.1629679696571,126.02361954519));
#55244=CARTESIAN_POINT('Ctrl Pts',(65.8564708087735,1.02890080607087,125.994937970952));
#55245=CARTESIAN_POINT('Ctrl Pts',(65.8487145060316,0.894691154307397,125.966225913595));
#55246=CARTESIAN_POINT('Ctrl Pts',(65.8409582032897,0.759349841311873,125.943151094937));
#55247=CARTESIAN_POINT('Ctrl Pts',(65.8332019005479,0.623389130121796,125.925777928409));
#55248=CARTESIAN_POINT('Ctrl Pts',(65.8254414580337,0.487355852606459,125.908395489299));
#55249=CARTESIAN_POINT('Ctrl Pts',(65.8176810155195,0.350702907520669,125.896720799304));
#55250=CARTESIAN_POINT('Ctrl Pts',(65.8099205730053,0.213945476176173,125.890766169942));
#55251=CARTESIAN_POINT('Ctrl Pts',(65.8021476727399,0.0769685096623139,
125.88480198168));
#55252=CARTESIAN_POINT('Ctrl Pts',(65.7943747724745,-0.060112887099783,
125.884576203956));
#55253=CARTESIAN_POINT('Ctrl Pts',(65.786601872209,-0.196784836413529,125.890048988186));
#55254=CARTESIAN_POINT('Ctrl Pts',(65.7791115364471,-0.328488416112371,
125.895322822925));
#55255=CARTESIAN_POINT('Ctrl Pts',(65.7716212006851,-0.459811493396904,
125.905888073856));
#55256=CARTESIAN_POINT('Ctrl Pts',(65.7641308649232,-0.590302594474758,
125.921664035814));
#55257=CARTESIAN_POINT('Ctrl Pts',(65.7563565308041,-0.72574130531305,125.938038148164));
#55258=CARTESIAN_POINT('Ctrl Pts',(65.748582196685,-0.860712734922414,125.960077767977));
#55259=CARTESIAN_POINT('Ctrl Pts',(65.740807862566,-0.994705136449562,125.987749282403));
#55260=CARTESIAN_POINT('Ctrl Pts',(65.7330431096189,-1.12853240431671,126.01538669416));
#55261=CARTESIAN_POINT('Ctrl Pts',(65.7252783566719,-1.26138266559559,126.04864211208));
#55262=CARTESIAN_POINT('Ctrl Pts',(65.7175136037248,-1.39274916223049,126.087430171438));
#55263=CARTESIAN_POINT('Ctrl Pts',(65.7097565628398,-1.52398518380933,126.126179705949));
#55264=CARTESIAN_POINT('Ctrl Pts',(65.7019995219549,-1.65374000093024,126.17045083641));
#55265=CARTESIAN_POINT('Ctrl Pts',(65.6942424810699,-1.78151727633739,126.220107215254));
#55266=CARTESIAN_POINT('Ctrl Pts',(65.6864912898298,-1.90919819390755,126.269726147836));
#55267=CARTESIAN_POINT('Ctrl Pts',(65.6787400985896,-2.03490417512514,126.324722104468));
#55268=CARTESIAN_POINT('Ctrl Pts',(65.6709889073494,-2.15815462210365,126.384909103001));
#55269=CARTESIAN_POINT('Ctrl Pts',(65.6632410105723,-2.28135268435421,126.445070520454));
#55270=CARTESIAN_POINT('Ctrl Pts',(65.6554931137953,-2.40209693756204,126.510418420384));
#55271=CARTESIAN_POINT('Ctrl Pts',(65.6477452170182,-2.51992754320466,126.580719032453));
#55272=CARTESIAN_POINT('Ctrl Pts',(65.6399989409341,-2.63773350122471,126.651004939149));
#55273=CARTESIAN_POINT('Ctrl Pts',(65.63225266485,-2.75262668841713,126.726241297131));
#55274=CARTESIAN_POINT('Ctrl Pts',(65.6245063887659,-2.86417298038462,126.806148992235));
#55275=CARTESIAN_POINT('Ctrl Pts',(65.6167600555006,-2.97572009576164,126.886057277199));
#55276=CARTESIAN_POINT('Ctrl Pts',(65.6090137222352,-3.08391994878583,126.97063674041));
#55277=CARTESIAN_POINT('Ctrl Pts',(65.6012673889699,-3.18836878862205,127.059565892853));
#55278=CARTESIAN_POINT('Ctrl Pts',(65.5935193209669,-3.29284101905133,127.148514960362));
#55279=CARTESIAN_POINT('Ctrl Pts',(65.5857712529639,-3.39356026713621,127.241815402012));
#55280=CARTESIAN_POINT('Ctrl Pts',(65.578023184961,-3.49015746453798,127.339106812254));
#55281=CARTESIAN_POINT('Ctrl Pts',(65.5702668822191,-3.58685732659107,127.436501624965));
#55282=CARTESIAN_POINT('Ctrl Pts',(65.5625105794773,-3.67942611061071,127.537895601534));
#55283=CARTESIAN_POINT('Ctrl Pts',(65.5547542767354,-3.76753273306773,127.642892577594));
#55284=CARTESIAN_POINT('Ctrl Pts',(65.5469938342212,-3.85568638068187,127.747945593701));
#55285=CARTESIAN_POINT('Ctrl Pts',(65.5392333917071,-3.9393728827717,127.856605131502));
#55286=CARTESIAN_POINT('Ctrl Pts',(65.5314729491929,-4.01830341322532,127.968444409043));
#55287=CARTESIAN_POINT('Ctrl Pts',(65.5237000489275,-4.09736064997366,128.080463220922));
#55288=CARTESIAN_POINT('Ctrl Pts',(65.5159271486621,-4.171646446517,128.19567164399));
#55289=CARTESIAN_POINT('Ctrl Pts',(65.5081542483966,-4.24091656514903,128.313615799255));
#55290=CARTESIAN_POINT('Ctrl Pts',(65.5006639126345,-4.30766854048874,128.427272387394));
#55291=CARTESIAN_POINT('Ctrl Pts',(65.4931735768724,-4.36976302667466,128.543468987778));
#55292=CARTESIAN_POINT('Ctrl Pts',(65.4856832411102,-4.42702389063793,128.661782139605));
#55293=CARTESIAN_POINT('Ctrl Pts',(65.477302578159,-4.49109097873786,128.79415840145));
#55294=CARTESIAN_POINT('Ctrl Pts',(65.4689219152079,-4.54928649637606,128.929554254977));
#55295=CARTESIAN_POINT('Ctrl Pts',(65.4605412522567,-4.60133789404382,129.067445925551));
#55296=CARTESIAN_POINT('Ctrl Pts',(65.4521817467578,-4.65325788504737,129.204989480892));
#55297=CARTESIAN_POINT('Ctrl Pts',(65.4438222412588,-4.69906458275434,129.345016013224));
#55298=CARTESIAN_POINT('Ctrl Pts',(65.4354627357599,-4.73853267723818,129.486980213413));
#55299=CARTESIAN_POINT('Ctrl Pts',(65.4335936241726,-4.74735739453008,129.518722154559));
#55300=CARTESIAN_POINT('Ctrl Pts',(65.4317245125853,-4.75586541040771,129.550560873191));
#55301=CARTESIAN_POINT('Ctrl Pts',(65.429855400998,-4.76405452823407,129.582490119308));
#55302=CARTESIAN_POINT('Origin',(213.235140564004,0.,130.804360617566));
#55303=CARTESIAN_POINT('',(63.3349537467758,-4.76405452823404,129.582490119308));
#55304=CARTESIAN_POINT('',(63.6801307828278,-4.76405452823405,129.582490119308));
#55305=CARTESIAN_POINT('',(213.235140564004,-4.76405452823405,129.582490119308));
#55306=CARTESIAN_POINT('',(65.0148594359565,-4.91824789621477,130.808909670108));
#55307=CARTESIAN_POINT('Ctrl Pts',(65.0148594359565,-4.91824789621477,130.808909670108));
#55308=CARTESIAN_POINT('Ctrl Pts',(65.0047250992943,-4.91808238954424,130.987848652825));
#55309=CARTESIAN_POINT('Ctrl Pts',(64.9945907626321,-4.90814809073405,131.166352314953));
#55310=CARTESIAN_POINT('Ctrl Pts',(64.9844564259699,-4.8886074676266,131.343526723665));
#55311=CARTESIAN_POINT('Ctrl Pts',(64.9740577776672,-4.86855720937276,131.525321983268));
#55312=CARTESIAN_POINT('Ctrl Pts',(64.9636591293646,-4.83839296868917,131.705718119363));
#55313=CARTESIAN_POINT('Ctrl Pts',(64.953260481062,-4.79833791901245,131.883775402284));
#55314=CARTESIAN_POINT('Ctrl Pts',(64.9516326505893,-4.79206760112586,131.911648935707));
#55315=CARTESIAN_POINT('Ctrl Pts',(64.9500048201166,-4.78555499743603,131.939465198035));
#55316=CARTESIAN_POINT('Ctrl Pts',(64.9483769896439,-4.77880106855221,131.96722063051));
#55317=CARTESIAN_POINT('Ctrl Pts',(64.9406026555249,-4.74654506853212,132.099777434981));
#55318=CARTESIAN_POINT('Ctrl Pts',(64.9328283214058,-4.70871840581664,132.23120108293));
#55319=CARTESIAN_POINT('Ctrl Pts',(64.9250539872867,-4.66541489976612,132.360987379362));
#55320=CARTESIAN_POINT('Ctrl Pts',(64.9172892343396,-4.62216476141667,132.490613725783));
#55321=CARTESIAN_POINT('Ctrl Pts',(64.9095244813925,-4.5734513322157,132.618606368379));
#55322=CARTESIAN_POINT('Ctrl Pts',(64.9017597284454,-4.51941923194677,132.744472178381));
#55323=CARTESIAN_POINT('Ctrl Pts',(64.8940026875604,-4.46544079712163,132.870212976687));
#55324=CARTESIAN_POINT('Ctrl Pts',(64.8862456466754,-4.40615435702613,132.993830789235));
#55325=CARTESIAN_POINT('Ctrl Pts',(64.8784886057904,-4.34175392665275,133.114848856639));
#55326=CARTESIAN_POINT('Ctrl Pts',(64.8707374145503,-4.27740206114478,133.235775663377));
#55327=CARTESIAN_POINT('Ctrl Pts',(64.8629862233101,-4.20794406441188,133.354106283462));
#55328=CARTESIAN_POINT('Ctrl Pts',(64.85523503207,-4.13362137966262,133.469385448988));
#55329=CARTESIAN_POINT('Ctrl Pts',(64.8474871352929,-4.05933028403699,133.584615617794));
#55330=CARTESIAN_POINT('Ctrl Pts',(64.8397392385158,-3.9801788241445,133.696796583671));
#55331=CARTESIAN_POINT('Ctrl Pts',(64.8319913417387,-3.89645344503732,133.805499336978));
#55332=CARTESIAN_POINT('Ctrl Pts',(64.8242450656546,-3.81274557947455,133.914179352014));
#55333=CARTESIAN_POINT('Ctrl Pts',(64.8164987895705,-3.72446593617333,134.019382292108));
#55334=CARTESIAN_POINT('Ctrl Pts',(64.8087525134864,-3.63194294957278,134.120710037267));
#55335=CARTESIAN_POINT('Ctrl Pts',(64.8010061802211,-3.53941927998857,134.222038530404));
#55336=CARTESIAN_POINT('Ctrl Pts',(64.7932598469556,-3.44265246822719,134.319491482812));
#55337=CARTESIAN_POINT('Ctrl Pts',(64.7855135136903,-3.34200943959831,134.412705940305));
#55338=CARTESIAN_POINT('Ctrl Pts',(64.7777654456873,-3.24134387266084,134.50594127253));
#55339=CARTESIAN_POINT('Ctrl Pts',(64.7700173776844,-3.13680064831548,134.594935955464));
#55340=CARTESIAN_POINT('Ctrl Pts',(64.7622693096814,-3.02878123970798,134.679366071045));
#55341=CARTESIAN_POINT('Ctrl Pts',(64.7545130069395,-2.92064702678771,134.763885919958));
#55342=CARTESIAN_POINT('Ctrl Pts',(64.7467567041976,-2.80902955790968,134.84383126942));
#55343=CARTESIAN_POINT('Ctrl Pts',(64.7390004014557,-2.69436132841434,134.918920143742));
#55344=CARTESIAN_POINT('Ctrl Pts',(64.7312399589416,-2.57963189703217,134.994049095257));
#55345=CARTESIAN_POINT('Ctrl Pts',(64.7234795164274,-2.46184879613242,135.06431620655));
#55346=CARTESIAN_POINT('Ctrl Pts',(64.7157190739132,-2.34146993336652,135.12948507978));
#55347=CARTESIAN_POINT('Ctrl Pts',(64.7079461736478,-2.22089782776354,135.19475856787));
#55348=CARTESIAN_POINT('Ctrl Pts',(64.7001732733823,-2.09772198491311,135.254917291692));
#55349=CARTESIAN_POINT('Ctrl Pts',(64.6924003731169,-1.97242195356502,135.309772330117));
#55350=CARTESIAN_POINT('Ctrl Pts',(64.6849100373549,-1.85167689396918,135.362633249724));
#55351=CARTESIAN_POINT('Ctrl Pts',(64.6774197015929,-1.72895969069575,135.410569281846));
#55352=CARTESIAN_POINT('Ctrl Pts',(64.6699293658309,-1.60471164345935,135.45345554065));
#55353=CARTESIAN_POINT('Ctrl Pts',(64.6621550317118,-1.47575269374651,135.497967844992));
#55354=CARTESIAN_POINT('Ctrl Pts',(64.6543806975928,-1.34473602145048,135.537180894261));
#55355=CARTESIAN_POINT('Ctrl Pts',(64.6466063634737,-1.21213653175627,135.570901091629));
#55356=CARTESIAN_POINT('Ctrl Pts',(64.6388416105266,-1.07970045908236,135.604579731868));
#55357=CARTESIAN_POINT('Ctrl Pts',(64.6310768575795,-0.945685825551951,
135.632778893962));
#55358=CARTESIAN_POINT('Ctrl Pts',(64.6233121046324,-0.810585684888883,
135.655353702487));
#55359=CARTESIAN_POINT('Ctrl Pts',(64.6155550637474,-0.675619727590283,
135.677906089394));
#55360=CARTESIAN_POINT('Ctrl Pts',(64.6077980228624,-0.539570791831687,
135.694845175478));
#55361=CARTESIAN_POINT('Ctrl Pts',(64.6000409819774,-0.402944858630383,
135.706076490952));
#55362=CARTESIAN_POINT('Ctrl Pts',(64.5922897907373,-0.266421956108101,
135.717299336804));
#55363=CARTESIAN_POINT('Ctrl Pts',(64.5845385994971,-0.12932331029386,135.722822947541));
#55364=CARTESIAN_POINT('Ctrl Pts',(64.576787408257,0.00783754307838197,
135.722604372751));
#55365=CARTESIAN_POINT('Ctrl Pts',(64.5690395114799,0.144940099429055,135.722385890861));
#55366=CARTESIAN_POINT('Ctrl Pts',(64.5612916147029,0.282104420604652,135.716430078196));
#55367=CARTESIAN_POINT('Ctrl Pts',(64.5535437179258,0.418814738097866,135.704746038903));
#55368=CARTESIAN_POINT('Ctrl Pts',(64.5457974418417,0.55549645873998,135.693064443659));
#55369=CARTESIAN_POINT('Ctrl Pts',(64.5380511657576,0.691723975297531,135.675657038385));
#55370=CARTESIAN_POINT('Ctrl Pts',(64.5303048896735,0.826984811307728,135.652584950697));
#55371=CARTESIAN_POINT('Ctrl Pts',(64.5225585564081,0.962246645782506,135.629512692696));
#55372=CARTESIAN_POINT('Ctrl Pts',(64.5148122231428,1.09654140007225,135.60077573458));
#55373=CARTESIAN_POINT('Ctrl Pts',(64.5070658898774,1.2293653784483,135.566486595401));
#55374=CARTESIAN_POINT('Ctrl Pts',(64.4993178218745,1.36221910183318,135.532189777407));
#55375=CARTESIAN_POINT('Ctrl Pts',(64.4915697538715,1.49360101541403,135.492338401889));
#55376=CARTESIAN_POINT('Ctrl Pts',(64.4838216858685,1.62302159171013,135.447095153951));
#55377=CARTESIAN_POINT('Ctrl Pts',(64.4760653831267,1.75257971773501,135.401803820951));
#55378=CARTESIAN_POINT('Ctrl Pts',(64.4683090803848,1.8801719727445,135.351109297371));
#55379=CARTESIAN_POINT('Ctrl Pts',(64.460552777643,2.00532734830802,135.295223039042));
#55380=CARTESIAN_POINT('Ctrl Pts',(64.4527923351288,2.13054952306384,135.239306952535));
#55381=CARTESIAN_POINT('Ctrl Pts',(64.4450318926147,2.25333187691139,135.178193783981));
#55382=CARTESIAN_POINT('Ctrl Pts',(64.4372714501005,2.37322801137952,135.112141005249));
#55383=CARTESIAN_POINT('Ctrl Pts',(64.4294985498351,2.49331661376673,135.045982192732));
#55384=CARTESIAN_POINT('Ctrl Pts',(64.4217256495697,2.61050940369994,134.974868127305));
#55385=CARTESIAN_POINT('Ctrl Pts',(64.4139527493043,2.72438822866959,134.899100150428));
#55386=CARTESIAN_POINT('Ctrl Pts',(64.4064624135422,2.83412727150845,134.826086530359));
#55387=CARTESIAN_POINT('Ctrl Pts',(64.3989720777802,2.9407888588564,134.748751667977));
#55388=CARTESIAN_POINT('Ctrl Pts',(64.3914817420181,3.04402938745015,134.667399337387));
#55389=CARTESIAN_POINT('Ctrl Pts',(64.383707407899,3.1511843120645,134.582962508457));
#55390=CARTESIAN_POINT('Ctrl Pts',(64.3759330737799,3.25499307262124,134.493930082431));
#55391=CARTESIAN_POINT('Ctrl Pts',(64.3681587396608,3.35503609277531,134.400596966678));
#55392=CARTESIAN_POINT('Ctrl Pts',(64.3603939867137,3.45495581884814,134.307378875649));
#55393=CARTESIAN_POINT('Ctrl Pts',(64.3526292337666,3.5511187554723,134.209870904883));
#55394=CARTESIAN_POINT('Ctrl Pts',(64.3448644808195,3.64313650726891,134.108409565736));
#55395=CARTESIAN_POINT('Ctrl Pts',(64.3371074399345,3.73506286573708,134.007048999422));
#55396=CARTESIAN_POINT('Ctrl Pts',(64.3293503990496,3.8228519715566,133.901743166451));
#55397=CARTESIAN_POINT('Ctrl Pts',(64.3215933581646,3.9061508495217,133.792866699755));
#55398=CARTESIAN_POINT('Ctrl Pts',(64.3138421669244,3.98938691115495,133.68407233765));
#55399=CARTESIAN_POINT('Ctrl Pts',(64.3060909756843,4.06813924818851,133.571713010616));
#55400=CARTESIAN_POINT('Ctrl Pts',(64.2983397844442,4.14209414661494,133.456197555064));
#55401=CARTESIAN_POINT('Ctrl Pts',(64.2905918876671,4.21601761223683,133.340731196661));
#55402=CARTESIAN_POINT('Ctrl Pts',(64.2828439908901,4.28514748438497,133.222111706337));
#55403=CARTESIAN_POINT('Ctrl Pts',(64.275096094113,4.34921263715847,133.100777935756));
#55404=CARTESIAN_POINT('Ctrl Pts',(64.2673498180289,4.41326438888309,132.979469545584));
#55405=CARTESIAN_POINT('Ctrl Pts',(64.2596035419447,4.47225334606476,132.85544834999));
#55406=CARTESIAN_POINT('Ctrl Pts',(64.2518572658606,4.52595393105044,132.729178550906));
#55407=CARTESIAN_POINT('Ctrl Pts',(64.2441109325953,4.57965491244157,132.602907819728));
#55408=CARTESIAN_POINT('Ctrl Pts',(64.2363645993299,4.62806729073105,132.474388811718));
#55409=CARTESIAN_POINT('Ctrl Pts',(64.2286182660646,4.67101347153892,132.344106119655));
#55410=CARTESIAN_POINT('Ctrl Pts',(64.2208701980616,4.71396926984627,132.213794251685));
#55411=CARTESIAN_POINT('Ctrl Pts',(64.2131221300586,4.75145631244567,132.081718284969));
#55412=CARTESIAN_POINT('Ctrl Pts',(64.2053740620557,4.78334686936146,131.948378008111));
#55413=CARTESIAN_POINT('Ctrl Pts',(64.1976177593138,4.8152713199406,131.814896015621));
#55414=CARTESIAN_POINT('Ctrl Pts',(64.189861456572,4.8415873119562,131.680147409603));
#55415=CARTESIAN_POINT('Ctrl Pts',(64.1821051538301,4.86221815762524,131.544642759833));
#55416=CARTESIAN_POINT('Ctrl Pts',(64.174344711316,4.88286001459783,131.409065787151));
#55417=CARTESIAN_POINT('Ctrl Pts',(64.1665842688018,4.89781063645912,131.272732355106));
#55418=CARTESIAN_POINT('Ctrl Pts',(64.1588238262876,4.90704535230545,131.136157201209));
#55419=CARTESIAN_POINT('Ctrl Pts',(64.1510509260222,4.91629489253747,130.999362804751));
#55420=CARTESIAN_POINT('Ctrl Pts',(64.1432780257567,4.91981018079097,130.862326302087));
#55421=CARTESIAN_POINT('Ctrl Pts',(64.1355051254913,4.91761872252499,130.725562379187));
#55422=CARTESIAN_POINT('Ctrl Pts',(64.1280147897293,4.91550692928694,130.593770169372));
#55423=CARTESIAN_POINT('Ctrl Pts',(64.1205244539673,4.90809611264359,130.462231372997));
#55424=CARTESIAN_POINT('Ctrl Pts',(64.1130341182053,4.89545612039598,130.331399270543));
#55425=CARTESIAN_POINT('Ctrl Pts',(64.1052597840862,4.88233687900042,130.195606629159));
#55426=CARTESIAN_POINT('Ctrl Pts',(64.0974854499671,4.86354254820619,130.060145177881));
#55427=CARTESIAN_POINT('Ctrl Pts',(64.089711115848,4.83909445067185,129.925527322807));
#55428=CARTESIAN_POINT('Ctrl Pts',(64.081946362901,4.81467648323273,129.791075372208));
#55429=CARTESIAN_POINT('Ctrl Pts',(64.0741816099539,4.78461868201375,129.657465330187));
#55430=CARTESIAN_POINT('Ctrl Pts',(64.0664168570068,4.74899422635998,129.525205857383));
#55431=CARTESIAN_POINT('Ctrl Pts',(64.0586598161218,4.71340515341778,129.393077746551));
#55432=CARTESIAN_POINT('Ctrl Pts',(64.0509027752368,4.67226052978635,129.26229791055));
#55433=CARTESIAN_POINT('Ctrl Pts',(64.0431457343518,4.62568475304174,129.133365815666));
#55434=CARTESIAN_POINT('Ctrl Pts',(64.0353945431116,4.57914409945268,129.004530949478));
#55435=CARTESIAN_POINT('Ctrl Pts',(64.0276433518715,4.52718057723726,128.877541417159));
#55436=CARTESIAN_POINT('Ctrl Pts',(64.0198921606314,4.46996858196161,128.752882141253));
#55437=CARTESIAN_POINT('Ctrl Pts',(64.0121442638543,4.41278090331013,128.628275848865));
#55438=CARTESIAN_POINT('Ctrl Pts',(64.0043963670772,4.35034935110855,128.505998197604));
#55439=CARTESIAN_POINT('Ctrl Pts',(63.9966484703001,4.28289659352007,128.386514503415));
#55440=CARTESIAN_POINT('Ctrl Pts',(63.988902194216,4.21545794559435,128.267055802639));
#55441=CARTESIAN_POINT('Ctrl Pts',(63.9811559181319,4.14300037352101,128.150390236704));
#55442=CARTESIAN_POINT('Ctrl Pts',(63.9734096420478,4.06579249329982,128.03695850296));
#55443=CARTESIAN_POINT('Ctrl Pts',(63.9656633087824,3.9885840431477,127.923525931889));
#55444=CARTESIAN_POINT('Ctrl Pts',(63.9579169755171,3.90662543486509,127.813327563843));
#55445=CARTESIAN_POINT('Ctrl Pts',(63.9501706422517,3.82022837597998,127.706774748239));
#55446=CARTESIAN_POINT('Ctrl Pts',(63.9424225742488,3.73381196907245,127.600198070869));
#55447=CARTESIAN_POINT('Ctrl Pts',(63.9346745062458,3.6429553798851,127.497268874097));
#55448=CARTESIAN_POINT('Ctrl Pts',(63.9269264382428,3.548010053555,127.398364768718));
#55449=CARTESIAN_POINT('Ctrl Pts',(63.9191701355009,3.45296381820221,127.299355546878));
#55450=CARTESIAN_POINT('Ctrl Pts',(63.911413832759,3.35382043616919,127.204380244517));
#55451=CARTESIAN_POINT('Ctrl Pts',(63.9036575300172,3.25096801264665,127.113779356674));
#55452=CARTESIAN_POINT('Ctrl Pts',(63.895897087503,3.14806069368886,127.023130112409));
#55453=CARTESIAN_POINT('Ctrl Pts',(63.8881366449889,3.04144069245173,126.936860180664));
#55454=CARTESIAN_POINT('Ctrl Pts',(63.8803762024747,2.93152773695433,126.855268545967));
#55455=CARTESIAN_POINT('Ctrl Pts',(63.8726033022093,2.82143833942314,126.773545933134));
#55456=CARTESIAN_POINT('Ctrl Pts',(63.8648304019438,2.70804574782339,126.696516844576));
#55457=CARTESIAN_POINT('Ctrl Pts',(63.8570575016784,2.59179784940959,126.624436339508));
#55458=CARTESIAN_POINT('Ctrl Pts',(63.8495671659163,2.47977585491329,126.554976142359));
#55459=CARTESIAN_POINT('Ctrl Pts',(63.8420768301543,2.36510281273498,126.490111139832));
#55460=CARTESIAN_POINT('Ctrl Pts',(63.8345864943922,2.24819783502318,126.430027576164));
#55461=CARTESIAN_POINT('Ctrl Pts',(63.8268121602731,2.12686036954963,126.367665925919));
#55462=CARTESIAN_POINT('Ctrl Pts',(63.8190378261541,2.00273401925019,126.310257905454));
#55463=CARTESIAN_POINT('Ctrl Pts',(63.811263492035,1.87626141130551,126.258062543424));
#55464=CARTESIAN_POINT('Ctrl Pts',(63.8034987390879,1.74994466954694,126.205931507514));
#55465=CARTESIAN_POINT('Ctrl Pts',(63.7957339861408,1.6212877813998,126.159000495641));
#55466=CARTESIAN_POINT('Ctrl Pts',(63.7879692331937,1.49075825269003,126.117482883452));
#55467=CARTESIAN_POINT('Ctrl Pts',(63.7802121923087,1.36035836774831,126.07600650714));
#55468=CARTESIAN_POINT('Ctrl Pts',(63.7724551514237,1.22808991375647,126.039932948444));
#55469=CARTESIAN_POINT('Ctrl Pts',(63.7646981105387,1.09444034577713,126.009427521887));
#55470=CARTESIAN_POINT('Ctrl Pts',(63.7569469192985,0.960891563976645,125.978945099711));
#55471=CARTESIAN_POINT('Ctrl Pts',(63.7491957280584,0.825964120868906,125.954022538523));
#55472=CARTESIAN_POINT('Ctrl Pts',(63.7414445368182,0.690160260588042,125.934775226878));
#55473=CARTESIAN_POINT('Ctrl Pts',(63.7336966400412,0.554414120570484,125.915536095853));
#55474=CARTESIAN_POINT('Ctrl Pts',(63.7259487432641,0.417792690541549,125.90196747157));
#55475=CARTESIAN_POINT('Ctrl Pts',(63.718200846487,0.280807811564492,125.89413353163));
#55476=CARTESIAN_POINT('Ctrl Pts',(63.7104545704029,0.143851586871065,125.886301230381));
#55477=CARTESIAN_POINT('Ctrl Pts',(63.7027082943188,0.00653245452892467,
125.884201249768));
#55478=CARTESIAN_POINT('Ctrl Pts',(63.6949620182347,-0.130633620790511,
125.887845803227));
#55479=CARTESIAN_POINT('Ctrl Pts',(63.6872156849694,-0.267800708638755,
125.891490383588));
#55480=CARTESIAN_POINT('Ctrl Pts',(63.679469351704,-0.404814346382526,125.900879572251));
#55481=CARTESIAN_POINT('Ctrl Pts',(63.6717230184386,-0.541159968576361,
125.915973465252));
#55482=CARTESIAN_POINT('Ctrl Pts',(63.6639749504356,-0.677536124426932,
125.931070738425));
#55483=CARTESIAN_POINT('Ctrl Pts',(63.6562268824327,-0.813243578529007,
125.95187521506));
#55484=CARTESIAN_POINT('Ctrl Pts',(63.6484788144297,-0.94777467154469,125.978295322268));
#55485=CARTESIAN_POINT('Ctrl Pts',(63.6407225116878,-1.08244874580697,126.004743509081));
#55486=CARTESIAN_POINT('Ctrl Pts',(63.632966208946,-1.21594357722377,126.036819173445));
#55487=CARTESIAN_POINT('Ctrl Pts',(63.6252099062041,-1.34776291734092,126.074379837358));
#55488=CARTESIAN_POINT('Ctrl Pts',(63.6174494636899,-1.47965261340907,126.111960548527));
#55489=CARTESIAN_POINT('Ctrl Pts',(63.6096890211758,-1.60986466528448,126.155031969836));
#55490=CARTESIAN_POINT('Ctrl Pts',(63.6019285786616,-1.73792065557005,126.203402580652));
#55491=CARTESIAN_POINT('Ctrl Pts',(63.5941556783962,-1.86618221269932,126.251850840267));
#55492=CARTESIAN_POINT('Ctrl Pts',(63.5863827781307,-1.99228043200819,126.305615135119));
#55493=CARTESIAN_POINT('Ctrl Pts',(63.5786098778653,-2.11575863095306,126.364456510713));
#55494=CARTESIAN_POINT('Ctrl Pts',(63.5711195421033,-2.23474808634247,126.421158854091));
#55495=CARTESIAN_POINT('Ctrl Pts',(63.5636292063413,-2.35130443038167,126.482575413903));
#55496=CARTESIAN_POINT('Ctrl Pts',(63.5561388705794,-2.46504443016443,126.548454248787));
#55497=CARTESIAN_POINT('Ctrl Pts',(63.5483633800025,-2.5831144773057,126.616841070971));
#55498=CARTESIAN_POINT('Ctrl Pts',(63.5405878894257,-2.69852356378702,126.690253314783));
#55499=CARTESIAN_POINT('Ctrl Pts',(63.5328123988489,-2.81081430818872,126.768458489493));
#55500=CARTESIAN_POINT('Ctrl Pts',(63.5250467412648,-2.92296304816458,126.84656476486));
#55501=CARTESIAN_POINT('Ctrl Pts',(63.5172810836807,-3.03200097539874,126.929451688261));
#55502=CARTESIAN_POINT('Ctrl Pts',(63.5095154260966,-3.1374957269162,127.016841162028));
#55503=CARTESIAN_POINT('Ctrl Pts',(63.5017591825011,-3.24286259146789,127.104124697114));
#55504=CARTESIAN_POINT('Ctrl Pts',(63.4940029389056,-3.34469453602573,127.195899663385));
#55505=CARTESIAN_POINT('Ctrl Pts',(63.4862466953101,-3.44258912612857,127.291845397505));
#55506=CARTESIAN_POINT('Ctrl Pts',(63.478495790603,-3.54041633202876,127.387725088886));
#55507=CARTESIAN_POINT('Ctrl Pts',(63.4707448858959,-3.63431129752257,127.487769563984));
#55508=CARTESIAN_POINT('Ctrl Pts',(63.4629939811888,-3.72390551370555,127.591618675316));
#55509=CARTESIAN_POINT('Ctrl Pts',(63.455246733062,-3.81345746276433,127.695418794609));
#55510=CARTESIAN_POINT('Ctrl Pts',(63.4474994849352,-3.89871244547512,127.803019682853));
#55511=CARTESIAN_POINT('Ctrl Pts',(63.4397522368085,-3.97933989115521,127.914025499771));
#55512=CARTESIAN_POINT('Ctrl Pts',(63.4320069657834,-4.05994676067018,128.025002987947));
#55513=CARTESIAN_POINT('Ctrl Pts',(63.4242616947583,-4.1359282151993,128.139383358595));
#55514=CARTESIAN_POINT('Ctrl Pts',(63.4165164237332,-4.2069951992801,128.256739284688));
#55515=CARTESIAN_POINT('Ctrl Pts',(63.4087693006532,-4.27807917695116,128.374123273018));
#55516=CARTESIAN_POINT('Ctrl Pts',(63.401022177573,-4.3442461294841,128.494483906459));
#55517=CARTESIAN_POINT('Ctrl Pts',(63.3932750544929,-4.40525141754686,128.617366559343));
#55518=CARTESIAN_POINT('Ctrl Pts',(63.3855269480811,-4.46626444892787,128.740264809555));
#55519=CARTESIAN_POINT('Ctrl Pts',(63.3777788416692,-4.52211434429908,128.865685363115));
#55520=CARTESIAN_POINT('Ctrl Pts',(63.3700307352573,-4.57260374214846,128.993151607046));
#55521=CARTESIAN_POINT('Ctrl Pts',(63.3622769768212,-4.62312997058361,129.120710833991));
#55522=CARTESIAN_POINT('Ctrl Pts',(63.3545232183852,-4.668287756345,129.250318364881));
#55523=CARTESIAN_POINT('Ctrl Pts',(63.3467694599491,-4.70792887445211,129.381480167352));
#55524=CARTESIAN_POINT('Ctrl Pts',(63.3428308888913,-4.72806483326005,129.448104641582));
#55525=CARTESIAN_POINT('Ctrl Pts',(63.3388923178335,-4.74677818570645,129.515129921998));
#55526=CARTESIAN_POINT('Ctrl Pts',(63.3349537467757,-4.76405452823404,129.582490119308));
#55527=CARTESIAN_POINT('Ctrl Pts',(65.0848845757186,-4.764054528234,129.582490119308));
#55528=CARTESIAN_POINT('Ctrl Pts',(65.0772322777973,-4.7977491559196,129.713864961267));
#55529=CARTESIAN_POINT('Ctrl Pts',(65.0695799798758,-4.82600021089149,129.846614648772));
#55530=CARTESIAN_POINT('Ctrl Pts',(65.0619276819544,-4.84871248717968,129.980242738153));
#55531=CARTESIAN_POINT('Ctrl Pts',(65.0540829742939,-4.87199584201207,130.117230778505));
#55532=CARTESIAN_POINT('Ctrl Pts',(65.0462382666333,-4.88945810571101,130.255141541152));
#55533=CARTESIAN_POINT('Ctrl Pts',(65.0383935589728,-4.9010531451034,130.393433456901));
#55534=CARTESIAN_POINT('Ctrl Pts',(65.0305488513122,-4.9126481844958,130.53172537265));
#55535=CARTESIAN_POINT('Ctrl Pts',(65.0227041436517,-4.91837601030066,130.67039798834));
#55536=CARTESIAN_POINT('Ctrl Pts',(65.0148594359911,-4.91824789621533,130.808909669497));
#55537=CARTESIAN_POINT('',(65.3601405640372,-4.91824982213702,130.80303791232));
#55538=CARTESIAN_POINT('Ctrl Pts',(65.429855400998,-4.76405452823407,129.582490119308));
#55539=CARTESIAN_POINT('Ctrl Pts',(65.4215226915695,-4.8005625354538,129.724834285372));
#55540=CARTESIAN_POINT('Ctrl Pts',(65.4131899821409,-4.83072868413131,129.868979158078));
#55541=CARTESIAN_POINT('Ctrl Pts',(65.4048572727123,-4.85438774821024,130.014358938754));
#55542=CARTESIAN_POINT('Ctrl Pts',(65.3965493778483,-4.8779763562897,130.159305782703));
#55543=CARTESIAN_POINT('Ctrl Pts',(65.3882414829842,-4.89509647502741,130.305479910784));
#55544=CARTESIAN_POINT('Ctrl Pts',(65.3799335881201,-4.90563342858695,130.452304191932));
#55545=CARTESIAN_POINT('Ctrl Pts',(65.3733359134258,-4.91400129950882,130.568903987679));
#55546=CARTESIAN_POINT('Ctrl Pts',(65.3667382387315,-4.91821832289317,130.685913442699));
#55547=CARTESIAN_POINT('Ctrl Pts',(65.3601405640372,-4.91824982213702,130.80303791232));
#55548=CARTESIAN_POINT('Ctrl Pts',(65.3601405640086,-4.91824982213716,130.803037912827));
#55549=CARTESIAN_POINT('Ctrl Pts',(65.3521725263887,-4.91828786388298,130.944489594425));
#55550=CARTESIAN_POINT('Ctrl Pts',(65.3442044887688,-4.91221920987186,131.085878215402));
#55551=CARTESIAN_POINT('Ctrl Pts',(65.3362364511489,-4.90008637273233,131.22665980329));
#55552=CARTESIAN_POINT('Ctrl Pts',(65.3282627522565,-4.88794491523975,131.367541416174));
#55553=CARTESIAN_POINT('Ctrl Pts',(65.3202890533641,-4.86973071607465,131.507814779279));
#55554=CARTESIAN_POINT('Ctrl Pts',(65.3123153544717,-4.84553795241052,131.646942966212));
#55555=CARTESIAN_POINT('Ctrl Pts',(65.3043347342982,-4.82132418909227,131.786191918338));
#55556=CARTESIAN_POINT('Ctrl Pts',(65.2963541141246,-4.79112157690867,131.924293360148));
#55557=CARTESIAN_POINT('Ctrl Pts',(65.2883734939511,-4.75507497764448,132.060722436263));
#55558=CARTESIAN_POINT('Ctrl Pts',(65.2803789381551,-4.71896543442539,132.197389742496));
#55559=CARTESIAN_POINT('Ctrl Pts',(65.2723843823592,-4.67699160683641,132.332378501668));
#55560=CARTESIAN_POINT('Ctrl Pts',(65.2643898265632,-4.62934800013868,132.465179739599));
#55561=CARTESIAN_POINT('Ctrl Pts',(65.2563873827478,-4.5816573847383,132.598112009044));
#55562=CARTESIAN_POINT('Ctrl Pts',(65.2483849389324,-4.52828596843571,132.728852121924));
#55563=CARTESIAN_POINT('Ctrl Pts',(65.240382495117,-4.46947549004429,132.856913151947));
#55564=CARTESIAN_POINT('Ctrl Pts',(65.2323654589606,-4.41055777159297,132.985207699412));
#55565=CARTESIAN_POINT('Ctrl Pts',(65.2243484228043,-4.3461813371905,133.110813084765));
#55566=CARTESIAN_POINT('Ctrl Pts',(65.2163313866479,-4.27663326362702,133.233267983222));
#55567=CARTESIAN_POINT('Ctrl Pts',(65.2132994635311,-4.25033122284085,133.279578593548));
#55568=CARTESIAN_POINT('Ctrl Pts',(65.2102675404142,-4.22328994696924,133.325438920385));
#55569=CARTESIAN_POINT('Ctrl Pts',(65.2072356172974,-4.19552650344427,133.370825193865));
#55570=CARTESIAN_POINT('Ctrl Pts',(65.1994612831783,-4.12433660912941,133.487202833024));
#55571=CARTESIAN_POINT('Ctrl Pts',(65.1916869490592,-4.04818807260937,133.600800509225));
#55572=CARTESIAN_POINT('Ctrl Pts',(65.1839126149401,-3.96732418146484,133.711166751739));
#55573=CARTESIAN_POINT('Ctrl Pts',(65.176147861993,-3.88655994783903,133.821396977723));
#55574=CARTESIAN_POINT('Ctrl Pts',(65.1683831090459,-3.80109215110217,133.928403381569));
#55575=CARTESIAN_POINT('Ctrl Pts',(65.1606183560988,-3.71120907436658,134.031760541474));
#55576=CARTESIAN_POINT('Ctrl Pts',(65.1528613152139,-3.62141527077019,134.13501504559));
#55577=CARTESIAN_POINT('Ctrl Pts',(65.1451042743289,-3.52721516905121,134.234627225541));
#55578=CARTESIAN_POINT('Ctrl Pts',(65.1373472334439,-3.42893909050521,134.330202329286));
#55579=CARTESIAN_POINT('Ctrl Pts',(65.1295960422037,-3.33073712271412,134.425705359103));
#55580=CARTESIAN_POINT('Ctrl Pts',(65.1218448509636,-3.2284655753056,134.517177100917));
#55581=CARTESIAN_POINT('Ctrl Pts',(65.1140936597235,-3.12249337074076,134.604257749355));
#55582=CARTESIAN_POINT('Ctrl Pts',(65.1063457629464,-3.01656620719005,134.691301386195));
#55583=CARTESIAN_POINT('Ctrl Pts',(65.0985978661693,-2.90694181624934,134.773957393956));
#55584=CARTESIAN_POINT('Ctrl Pts',(65.0908499693923,-2.79402395557692,134.851904712219));
#55585=CARTESIAN_POINT('Ctrl Pts',(65.0831036933082,-2.68112971488672,134.929835725584));
#55586=CARTESIAN_POINT('Ctrl Pts',(65.0753574172241,-2.5649436963167,135.00305978662));
#55587=CARTESIAN_POINT('Ctrl Pts',(65.06761114114,-2.44590021000154,135.071298070261));
#55588=CARTESIAN_POINT('Ctrl Pts',(65.0598648078746,-2.32685584493441,135.139536857622));
#55589=CARTESIAN_POINT('Ctrl Pts',(65.0521184746093,-2.20495430922282,135.202789599718));
#55590=CARTESIAN_POINT('Ctrl Pts',(65.0443721413439,-2.08065582837002,135.260822710569));
#55591=CARTESIAN_POINT('Ctrl Pts',(65.036624073341,-1.95632951173442,135.318868817532));
#55592=CARTESIAN_POINT('Ctrl Pts',(65.028876005338,-1.82960553601768,135.371692801908));
#55593=CARTESIAN_POINT('Ctrl Pts',(65.021127937335,-1.70096510561251,135.419108798343));
#55594=CARTESIAN_POINT('Ctrl Pts',(65.0133716345932,-1.57218795462689,135.466575189064));
#55595=CARTESIAN_POINT('Ctrl Pts',(65.0056153318514,-1.44149064758776,135.508621974816));
#55596=CARTESIAN_POINT('Ctrl Pts',(64.9978590291095,-1.30937112312363,135.545112701828));
#55597=CARTESIAN_POINT('Ctrl Pts',(64.9900985865954,-1.17718108249107,135.581622905038));
#55598=CARTESIAN_POINT('Ctrl Pts',(64.9823381440812,-1.043567692597,135.612571052448));
#55599=CARTESIAN_POINT('Ctrl Pts',(64.974577701567,-0.909039174282838,135.637871850833));
#55600=CARTESIAN_POINT('Ctrl Pts',(64.9668048013016,-0.774294698848376,
135.663213264306));
#55601=CARTESIAN_POINT('Ctrl Pts',(64.9590319010362,-0.63863254651262,135.682889156596));
#55602=CARTESIAN_POINT('Ctrl Pts',(64.9512590007707,-0.502567049421009,
135.696866051731));
#55603=CARTESIAN_POINT('Ctrl Pts',(64.9437686650087,-0.371447875876249,
135.710334851523));
#55604=CARTESIAN_POINT('Ctrl Pts',(64.9362783292466,-0.239954481067576,
135.718511787194));
#55605=CARTESIAN_POINT('Ctrl Pts',(64.9287879934845,-0.108545222450552,
135.721412681271));
#55606=CARTESIAN_POINT('Ctrl Pts',(64.9210136593655,0.0278464581471533,
135.724423563629));
#55607=CARTESIAN_POINT('Ctrl Pts',(64.9132393252464,0.1645795444088,135.72175996198));
#55608=CARTESIAN_POINT('Ctrl Pts',(64.9054649911273,0.301142698344161,135.713382530099));
#55609=CARTESIAN_POINT('Ctrl Pts',(64.8977002381802,0.437537550397666,135.705015422655));
#55610=CARTESIAN_POINT('Ctrl Pts',(64.8899354852331,0.573762500335554,135.690948519742));
#55611=CARTESIAN_POINT('Ctrl Pts',(64.882170732286,0.709303804682606,135.671194411231));
#55612=CARTESIAN_POINT('Ctrl Pts',(64.874413691401,0.8447104874952,135.651459922779));
#55613=CARTESIAN_POINT('Ctrl Pts',(64.866656650516,0.979434491595894,135.626049525744));
#55614=CARTESIAN_POINT('Ctrl Pts',(64.858899609631,1.11296515418576,135.595027755666));
#55615=CARTESIAN_POINT('Ctrl Pts',(64.8511484183908,1.24639512026371,135.564029379346));
#55616=CARTESIAN_POINT('Ctrl Pts',(64.8433972271507,1.378633156761,135.527428140803));
#55617=CARTESIAN_POINT('Ctrl Pts',(64.8356460359106,1.5091771376262,135.485339941358));
#55618=CARTESIAN_POINT('Ctrl Pts',(64.8278981391335,1.63966563381769,135.44326963052));
#55619=CARTESIAN_POINT('Ctrl Pts',(64.8201502423564,1.76846113511477,135.395717116878));
#55620=CARTESIAN_POINT('Ctrl Pts',(64.8124023455794,1.8950752834183,135.342848552184));
#55621=CARTESIAN_POINT('Ctrl Pts',(64.8046560694953,2.02166294677132,135.289991046455));
#55622=CARTESIAN_POINT('Ctrl Pts',(64.7969097934112,2.14606980417232,135.23181985206));
#55623=CARTESIAN_POINT('Ctrl Pts',(64.7891635173271,2.26782651696071,135.168549654658));
#55624=CARTESIAN_POINT('Ctrl Pts',(64.7814171840617,2.38958412852948,135.105278990209));
#55625=CARTESIAN_POINT('Ctrl Pts',(64.7736708507963,2.50869120952819,135.03690942792));
#55626=CARTESIAN_POINT('Ctrl Pts',(64.765924517531,2.6247024743299,134.963701909615));
#55627=CARTESIAN_POINT('Ctrl Pts',(64.758176449528,2.74073971905016,134.890477996994));
#55628=CARTESIAN_POINT('Ctrl Pts',(64.750428381525,2.85367943743922,134.812414181067));
#55629=CARTESIAN_POINT('Ctrl Pts',(64.742680313522,2.96310515298264,134.729814847954));
#55630=CARTESIAN_POINT('Ctrl Pts',(64.7349240107801,3.07264716747873,134.647127727286));
#55631=CARTESIAN_POINT('Ctrl Pts',(64.7271677080384,3.17866740607291,134.559895696083));
#55632=CARTESIAN_POINT('Ctrl Pts',(64.7194114052965,3.28078191835024,134.468463927617));
#55633=CARTESIAN_POINT('Ctrl Pts',(64.7116509627823,3.38295093221738,134.376983359263));
#55634=CARTESIAN_POINT('Ctrl Pts',(64.7038905202681,3.48120978605622,134.281298859843));
#55635=CARTESIAN_POINT('Ctrl Pts',(64.696130077754,3.57521201448411,134.181791906873));
#55636=CARTESIAN_POINT('Ctrl Pts',(64.6883571774885,3.66936514363409,134.082125216508));
#55637=CARTESIAN_POINT('Ctrl Pts',(64.6805842772231,3.75924773613774,133.97862410599));
#55638=CARTESIAN_POINT('Ctrl Pts',(64.6728113769577,3.84455361862368,133.871703202937));
#55639=CARTESIAN_POINT('Ctrl Pts',(64.6653210411956,3.92675841740883,133.768669144027));
#55640=CARTESIAN_POINT('Ctrl Pts',(64.6578307054336,4.00471329677018,133.662459860351));
#55641=CARTESIAN_POINT('Ctrl Pts',(64.6503403696716,4.07818381524667,133.55346953348));
#55642=CARTESIAN_POINT('Ctrl Pts',(64.6425660355525,4.15443999076197,133.44034680524));
#55643=CARTESIAN_POINT('Ctrl Pts',(64.6347917014334,4.2261066002734,133.323869645532));
#55644=CARTESIAN_POINT('Ctrl Pts',(64.6270173673144,4.29287415001397,133.204446989896));
#55645=CARTESIAN_POINT('Ctrl Pts',(64.6192526143673,4.35955941471667,133.085171512009));
#55646=CARTESIAN_POINT('Ctrl Pts',(64.6114878614202,4.42135744382118,132.962958098908));
#55647=CARTESIAN_POINT('Ctrl Pts',(64.6037231084731,4.47800113864534,132.83824578266));
#55648=CARTESIAN_POINT('Ctrl Pts',(64.5959660675881,4.53458857415319,132.713657332444));
#55649=CARTESIAN_POINT('Ctrl Pts',(64.5882090267031,4.58603170250018,132.586575271931));
#55650=CARTESIAN_POINT('Ctrl Pts',(64.5804519858181,4.63210879354899,132.457464119234));
#55651=CARTESIAN_POINT('Ctrl Pts',(64.5727007945779,4.67815113750526,132.32845033026));
#55652=CARTESIAN_POINT('Ctrl Pts',(64.5649496033378,4.71883536773837,132.197410861511));
#55653=CARTESIAN_POINT('Ctrl Pts',(64.5571984120977,4.75398758391762,132.064830813349));
#55654=CARTESIAN_POINT('Ctrl Pts',(64.5494505153206,4.78912485946715,131.932307115245));
#55655=CARTESIAN_POINT('Ctrl Pts',(64.5417026185435,4.81873469743844,131.798244517167));
#55656=CARTESIAN_POINT('Ctrl Pts',(64.5339547217665,4.84269291652695,131.663143697697));
#55657=CARTESIAN_POINT('Ctrl Pts',(64.5262084456824,4.86664612407251,131.528071138406));
#55658=CARTESIAN_POINT('Ctrl Pts',(64.5184621695982,4.88494999596582,131.391961174409));
#55659=CARTESIAN_POINT('Ctrl Pts',(64.5107158935141,4.897531464321,131.255324716454));
#55660=CARTESIAN_POINT('Ctrl Pts',(64.5029695602488,4.91011302554975,131.118687249879));
#55661=CARTESIAN_POINT('Ctrl Pts',(64.4952232269835,4.91697206310214,130.981523670911));
#55662=CARTESIAN_POINT('Ctrl Pts',(64.4874768937181,4.91808742696531,130.844349656386));
#55663=CARTESIAN_POINT('Ctrl Pts',(64.4797288257152,4.91920304060647,130.707144922693));
#55664=CARTESIAN_POINT('Ctrl Pts',(64.4719807577122,4.91457241787994,130.56993013967));
#55665=CARTESIAN_POINT('Ctrl Pts',(64.4642326897093,4.90422653172033,130.433220228939));
#55666=CARTESIAN_POINT('Ctrl Pts',(64.4564763869675,4.89386964982974,130.296365021286));
#55667=CARTESIAN_POINT('Ctrl Pts',(64.4487200842256,4.87778540008737,130.160016148282));
#55668=CARTESIAN_POINT('Ctrl Pts',(64.4409637814837,4.85605665196616,130.024683212869));
#55669=CARTESIAN_POINT('Ctrl Pts',(64.4332033389696,4.83431630655784,129.889278046193));
#55670=CARTESIAN_POINT('Ctrl Pts',(64.4254428964554,4.80692553787551,129.754890280463));
#55671=CARTESIAN_POINT('Ctrl Pts',(64.4176824539413,4.77401802075615,129.622017604733));
#55672=CARTESIAN_POINT('Ctrl Pts',(64.4099095536758,4.74105767756888,129.488931629987));
#55673=CARTESIAN_POINT('Ctrl Pts',(64.4021366534104,4.70256299873831,129.357365980916));
#55674=CARTESIAN_POINT('Ctrl Pts',(64.3943637531449,4.65871732803803,129.227802366204));
#55675=CARTESIAN_POINT('Ctrl Pts',(64.3868734173829,4.61646555790804,129.102948715237));
#55676=CARTESIAN_POINT('Ctrl Pts',(64.3793830816208,4.56924519599688,128.9799543553));
#55677=CARTESIAN_POINT('Ctrl Pts',(64.3718927458588,4.51726115708756,128.859229593401));
#55678=CARTESIAN_POINT('Ctrl Pts',(64.3641184117397,4.46330612754309,128.733927515463));
#55679=CARTESIAN_POINT('Ctrl Pts',(64.3563440776206,4.40404814727171,128.610673617242));
#55680=CARTESIAN_POINT('Ctrl Pts',(64.3485697435015,4.33966397638195,128.489949324258));
#55681=CARTESIAN_POINT('Ctrl Pts',(64.3408049905544,4.27535915322854,128.369373813175));
#55682=CARTESIAN_POINT('Ctrl Pts',(64.3330402376073,4.20594089175434,128.251322046068));
#55683=CARTESIAN_POINT('Ctrl Pts',(64.3252754846602,4.13163418871067,128.13625604818));
#55684=CARTESIAN_POINT('Ctrl Pts',(64.3175184437752,4.0574012881322,128.021304335464));
#55685=CARTESIAN_POINT('Ctrl Pts',(64.3097614028902,3.97828981891137,127.909332816781));
#55686=CARTESIAN_POINT('Ctrl Pts',(64.3020043620052,3.89457074273651,127.800779123363));
#55687=CARTESIAN_POINT('Ctrl Pts',(64.2942531707651,3.81091479976834,127.692307291129));
#55688=CARTESIAN_POINT('Ctrl Pts',(64.286501979525,3.72265840368777,127.587248462321));
#55689=CARTESIAN_POINT('Ctrl Pts',(64.2787507882849,3.63011568579323,127.486011152808));
#55690=CARTESIAN_POINT('Ctrl Pts',(64.2710028915078,3.53761230102221,127.384816871852));
#55691=CARTESIAN_POINT('Ctrl Pts',(64.2632549947307,3.44082648109317,127.287441167651));
#55692=CARTESIAN_POINT('Ctrl Pts',(64.2555070979536,3.34011233804845,127.194259146455));
#55693=CARTESIAN_POINT('Ctrl Pts',(64.2477608218695,3.23941926223132,127.10109661693));
#55694=CARTESIAN_POINT('Ctrl Pts',(64.2400145457854,3.13479978454073,127.012126290902));
#55695=CARTESIAN_POINT('Ctrl Pts',(64.2322682697013,3.02664425368308,126.927685802193));
#55696=CARTESIAN_POINT('Ctrl Pts',(64.2245219364359,2.91848792444557,126.843244690164));
#55697=CARTESIAN_POINT('Ctrl Pts',(64.2167756031705,2.80679579812318,126.763333722774));
#55698=CARTESIAN_POINT('Ctrl Pts',(64.2090292699052,2.69199029614568,126.688249430054));
#55699=CARTESIAN_POINT('Ctrl Pts',(64.2012812019022,2.57715908427265,126.613148322729));
#55700=CARTESIAN_POINT('Ctrl Pts',(64.1935331338993,2.45921343649804,126.542876254894));
#55701=CARTESIAN_POINT('Ctrl Pts',(64.1857850658963,2.3386033125917,126.477685495855));
#55702=CARTESIAN_POINT('Ctrl Pts',(64.1780287631545,2.21786500281007,126.412425451301));
#55703=CARTESIAN_POINT('Ctrl Pts',(64.1702724604125,2.09445690448507,126.352257689774));
#55704=CARTESIAN_POINT('Ctrl Pts',(64.1625161576707,1.96885255398031,126.297387943677));
#55705=CARTESIAN_POINT('Ctrl Pts',(64.1547557151565,1.84318116465148,126.242488911944));
#55706=CARTESIAN_POINT('Ctrl Pts',(64.1469952726423,1.71531155175319,126.192893671402));
#55707=CARTESIAN_POINT('Ctrl Pts',(64.1392348301281,1.58573468969725,126.148758770716));
#55708=CARTESIAN_POINT('Ctrl Pts',(64.1314619298627,1.45594981935939,126.10455302077));
#55709=CARTESIAN_POINT('Ctrl Pts',(64.1236890295973,1.32445259847015,126.065825237303));
#55710=CARTESIAN_POINT('Ctrl Pts',(64.1159161293318,1.19174740397696,126.032681543318));
#55711=CARTESIAN_POINT('Ctrl Pts',(64.1084257935699,1.0638663775689,126.000742706094));
#55712=CARTESIAN_POINT('Ctrl Pts',(64.1009354578079,0.934863980140043,125.97398907807));
#55713=CARTESIAN_POINT('Ctrl Pts',(64.0934451220459,0.805196176042556,125.952470039597));
#55714=CARTESIAN_POINT('Ctrl Pts',(64.0856707879269,0.670611977739899,125.930135100239));
#55715=CARTESIAN_POINT('Ctrl Pts',(64.0778964538078,0.534884596641799,125.913368774682));
#55716=CARTESIAN_POINT('Ctrl Pts',(64.0701221196887,0.398514612827742,125.902282571894));
#55717=CARTESIAN_POINT('Ctrl Pts',(64.0623573667416,0.262312692831556,125.891210031859));
#55718=CARTESIAN_POINT('Ctrl Pts',(64.0545926137946,0.125470131803469,125.885803717569));
#55719=CARTESIAN_POINT('Ctrl Pts',(64.0468278608475,-0.0115027390944946,
125.886124068813));
#55720=CARTESIAN_POINT('Ctrl Pts',(64.0390708199626,-0.148339566605917,
125.886444101879));
#55721=CARTESIAN_POINT('Ctrl Pts',(64.0313137790776,-0.285306057990205,
125.892479480584));
#55722=CARTESIAN_POINT('Ctrl Pts',(64.0235567381926,-0.421887560287729,
125.904238787553));
#55723=CARTESIAN_POINT('Ctrl Pts',(64.0158055469525,-0.558366065412477,
125.915989226737));
#55724=CARTESIAN_POINT('Ctrl Pts',(64.0080543557124,-0.694459771373267,
125.933454969135));
#55725=CARTESIAN_POINT('Ctrl Pts',(64.0003031644723,-0.829655186559642,
125.956592539995));
#55726=CARTESIAN_POINT('Ctrl Pts',(63.9925552676952,-0.964793140088108,
125.979720276771));
#55727=CARTESIAN_POINT('Ctrl Pts',(63.9848073709181,-1.09903317765276,126.008514981539));
#55728=CARTESIAN_POINT('Ctrl Pts',(63.977059474141,-1.23186830553191,126.042881483901));
#55729=CARTESIAN_POINT('Ctrl Pts',(63.9693131980569,-1.36467564716625,126.077240797532));
#55730=CARTESIAN_POINT('Ctrl Pts',(63.9615669219728,-1.49607828538895,126.117169492652));
#55731=CARTESIAN_POINT('Ctrl Pts',(63.9538206458887,-1.62558116629291,126.162521657165));
#55732=CARTESIAN_POINT('Ctrl Pts',(63.9460743126233,-1.75508500315789,126.207874156458));
#55733=CARTESIAN_POINT('Ctrl Pts',(63.938327979358,-1.88268868572854,126.25865007581));
#55734=CARTESIAN_POINT('Ctrl Pts',(63.9305816460926,-2.00791440579,126.314654301834));
#55735=CARTESIAN_POINT('Ctrl Pts',(63.9228335780896,-2.13316816928287,126.370671069616));
#55736=CARTESIAN_POINT('Ctrl Pts',(63.9150855100866,-2.25604255376626,126.431918314328));
#55737=CARTESIAN_POINT('Ctrl Pts',(63.9073374420836,-2.37608210368182,126.498153829793));
#55738=CARTESIAN_POINT('Ctrl Pts',(63.8995811393418,-2.49624923305936,126.564459741152));
#55739=CARTESIAN_POINT('Ctrl Pts',(63.8918248366,-2.61357516642692,126.635764324587));
#55740=CARTESIAN_POINT('Ctrl Pts',(63.8840685338581,-2.72763085731484,126.711780383933));
#55741=CARTESIAN_POINT('Ctrl Pts',(63.8763080913439,-2.84174742315945,126.787837015339));
#55742=CARTESIAN_POINT('Ctrl Pts',(63.8685476488297,-2.95258995279779,126.868609903182));
#55743=CARTESIAN_POINT('Ctrl Pts',(63.8607872063156,-3.05976135374225,126.953770595161));
#55744=CARTESIAN_POINT('Ctrl Pts',(63.8530143060501,-3.1671047957336,127.039067994643));
#55745=CARTESIAN_POINT('Ctrl Pts',(63.8452414057847,-3.27076503668067,127.12876701783));
#55746=CARTESIAN_POINT('Ctrl Pts',(63.8374685055193,-3.3703801642367,127.222500680184));
#55747=CARTESIAN_POINT('Ctrl Pts',(63.8299781697572,-3.46637403099191,127.312826887813));
#55748=CARTESIAN_POINT('Ctrl Pts',(63.822487833995,-3.55861156282144,127.406899268869));
#55749=CARTESIAN_POINT('Ctrl Pts',(63.8149974982329,-3.64680475476847,127.504360898915));
#55750=CARTESIAN_POINT('Ctrl Pts',(63.8073028132597,-3.73740400830844,127.604481449447));
#55751=CARTESIAN_POINT('Ctrl Pts',(63.7996081282865,-3.82403581350862,127.7085114365));
#55752=CARTESIAN_POINT('Ctrl Pts',(63.7919134433133,-3.9063384991868,127.816099820334));
#55753=CARTESIAN_POINT('Ctrl Pts',(63.7842279597593,-3.98854276608501,127.923559548374));
#55754=CARTESIAN_POINT('Ctrl Pts',(63.7765424762052,-4.06642796712949,128.034568897793));
#55755=CARTESIAN_POINT('Ctrl Pts',(63.7688569926512,-4.13966969626655,128.148740564111));
#55756=CARTESIAN_POINT('Ctrl Pts',(63.7611802099884,-4.21282850696225,128.262782974379));
#55757=CARTESIAN_POINT('Ctrl Pts',(63.7535034273255,-4.28135409549743,128.379980241164));
#55758=CARTESIAN_POINT('Ctrl Pts',(63.7458266446627,-4.3449632047769,128.499913219244));
#55759=CARTESIAN_POINT('Ctrl Pts',(63.7381549607444,-4.40853006633148,128.619766540564));
#55760=CARTESIAN_POINT('Ctrl Pts',(63.7304832768262,-4.46718675547075,128.742351608546));
#55761=CARTESIAN_POINT('Ctrl Pts',(63.7228115929079,-4.52069420216972,128.867221749811));
#55762=CARTESIAN_POINT('Ctrl Pts',(63.7151427412837,-4.57418189455909,128.992045790511));
#55763=CARTESIAN_POINT('Ctrl Pts',(63.7074738896594,-4.62252396468919,129.119152861596));
#55764=CARTESIAN_POINT('Ctrl Pts',(63.6998050380352,-4.66552823982081,129.248073592003));
#55765=CARTESIAN_POINT('Ctrl Pts',(63.693246952966,-4.70230371918418,129.358321274265));
#55766=CARTESIAN_POINT('Ctrl Pts',(63.6866888678969,-4.73517640793081,129.469894766533));
#55767=CARTESIAN_POINT('Ctrl Pts',(63.6801307828278,-4.76405452823405,129.582490119308));
#55768=CARTESIAN_POINT('Origin',(213.235140564004,0.,130.804360617566));
#55769=CARTESIAN_POINT('',(61.5846617476392,-4.76405452823404,129.582490119308));
#55770=CARTESIAN_POINT('',(61.9302338125864,-4.76405452823398,129.582490119308));
#55771=CARTESIAN_POINT('',(213.235140564004,-4.76405452823405,129.582490119308));
#55772=CARTESIAN_POINT('',(63.264859435939,-4.91824980396436,130.802971983528));
#55773=CARTESIAN_POINT('Ctrl Pts',(63.264859435939,-4.91824980396436,130.802971983528));
#55774=CARTESIAN_POINT('Ctrl Pts',(63.2571418302039,-4.91828805502452,130.93844919633));
#55775=CARTESIAN_POINT('Ctrl Pts',(63.2494242244688,-4.91272432380155,131.074153444162));
#55776=CARTESIAN_POINT('Ctrl Pts',(63.2417066187337,-4.90152846008028,131.209578852006));
#55777=CARTESIAN_POINT('Ctrl Pts',(63.2339983402522,-4.89034612732488,131.344840588997));
#55778=CARTESIAN_POINT('Ctrl Pts',(63.2262900617706,-4.87354523437112,131.479823764385));
#55779=CARTESIAN_POINT('Ctrl Pts',(63.2185817832891,-4.85114760933017,131.614021000066));
#55780=CARTESIAN_POINT('Ctrl Pts',(63.210880909227,-4.82877149900356,131.748089328545));
#55781=CARTESIAN_POINT('Ctrl Pts',(63.2031800351649,-4.80080941755057,131.881372830076));
#55782=CARTESIAN_POINT('Ctrl Pts',(63.1954791611028,-4.76733507809624,132.013368192254));
#55783=CARTESIAN_POINT('Ctrl Pts',(63.1877837757607,-4.73388459713836,132.145269476074));
#55784=CARTESIAN_POINT('Ctrl Pts',(63.1800883904185,-4.69492977372091,132.275884064037));
#55785=CARTESIAN_POINT('Ctrl Pts',(63.1723930050764,-4.65059550550699,132.404718235931));
#55786=CARTESIAN_POINT('Ctrl Pts',(63.1647003972949,-4.60627723923585,132.533505906616));
#55787=CARTESIAN_POINT('Ctrl Pts',(63.1570077895134,-4.55658351663959,132.660514063682));
#55788=CARTESIAN_POINT('Ctrl Pts',(63.1493151817319,-4.50168917783681,132.785263848077));
#55789=CARTESIAN_POINT('Ctrl Pts',(63.1416237703605,-4.44680337659991,132.90999423048));
#55790=CARTESIAN_POINT('Ctrl Pts',(63.1339323589891,-4.3867187275044,133.032466575268));
#55791=CARTESIAN_POINT('Ctrl Pts',(63.1262409476178,-4.32165813623516,133.152222201223));
#55792=CARTESIAN_POINT('Ctrl Pts',(63.1185490066165,-4.25659306489875,133.271986073541));
#55793=CARTESIAN_POINT('Ctrl Pts',(63.1108570656151,-4.1865515595093,133.389032505933));
#55794=CARTESIAN_POINT('Ctrl Pts',(63.1031651246138,-4.11180214760816,133.502928045188));
#55795=CARTESIAN_POINT('Ctrl Pts',(63.0954709278749,-4.03703081470508,133.616856985434));
#55796=CARTESIAN_POINT('Ctrl Pts',(63.0877767311361,-3.95754904691294,133.727632862686));
#55797=CARTESIAN_POINT('Ctrl Pts',(63.0800825343972,-3.87366800687072,133.834852200634));
#55798=CARTESIAN_POINT('Ctrl Pts',(63.0723800101768,-3.78969618180665,133.942187582803));
#55799=CARTESIAN_POINT('Ctrl Pts',(63.0646774859563,-3.70131582336188,134.045958427595));
#55800=CARTESIAN_POINT('Ctrl Pts',(63.0569749617358,-3.60887784046913,134.145795009421));
#55801=CARTESIAN_POINT('Ctrl Pts',(63.0492677377164,-3.51638345529507,134.245692507883));
#55802=CARTESIAN_POINT('Ctrl Pts',(63.0415605136969,-3.41982679653603,134.341650683781));
#55803=CARTESIAN_POINT('Ctrl Pts',(63.0338532896774,-3.31959388321576,134.433338367982));
#55804=CARTESIAN_POINT('Ctrl Pts',(63.0261347544936,-3.21921386751972,134.525160613534));
#55805=CARTESIAN_POINT('Ctrl Pts',(63.0184162193096,-3.11514712843326,134.612699599544));
#55806=CARTESIAN_POINT('Ctrl Pts',(63.0106976841257,-3.00781118819578,134.695665658123));
#55807=CARTESIAN_POINT('Ctrl Pts',(63.006879663735,-2.95471681229151,134.736705323791));
#55808=CARTESIAN_POINT('Ctrl Pts',(63.0030616433443,-2.90082294085479,134.77662674693));
#55809=CARTESIAN_POINT('Ctrl Pts',(62.9992436229536,-2.84618240724453,134.815398982777));
#55810=CARTESIAN_POINT('Ctrl Pts',(62.9914692888345,-2.7349221935055,134.894347831962));
#55811=CARTESIAN_POINT('Ctrl Pts',(62.9836949547154,-2.62019837736383,134.96878893393));
#55812=CARTESIAN_POINT('Ctrl Pts',(62.9759206205964,-2.50241234959665,135.038403070717));
#55813=CARTESIAN_POINT('Ctrl Pts',(62.9681558676493,-2.38477148258202,135.107931414302));
#55814=CARTESIAN_POINT('Ctrl Pts',(62.9603911147022,-2.26407624622692,135.172644432036));
#55815=CARTESIAN_POINT('Ctrl Pts',(62.9526263617551,-2.14075913653756,135.232264566595));
#55816=CARTESIAN_POINT('Ctrl Pts',(62.9448693208701,-2.01756450713984,135.291825485597));
#55817=CARTESIAN_POINT('Ctrl Pts',(62.937112279985,-1.89175353635624,135.346303418643));
#55818=CARTESIAN_POINT('Ctrl Pts',(62.9293552391,-1.76378528761729,135.395465552294));
#55819=CARTESIAN_POINT('Ctrl Pts',(62.9216040478599,-1.63591354073033,135.444590612398));
#55820=CARTESIAN_POINT('Ctrl Pts',(62.9138528566198,-1.50588811745759,135.488407712512));
#55821=CARTESIAN_POINT('Ctrl Pts',(62.9061016653797,-1.37418980533761,135.526731361314));
#55822=CARTESIAN_POINT('Ctrl Pts',(62.8983537686026,-1.24254746851345,135.565038721543));
#55823=CARTESIAN_POINT('Ctrl Pts',(62.8906058718255,-1.10923403161969,135.597857165315));
#55824=CARTESIAN_POINT('Ctrl Pts',(62.8828579750485,-0.974747049046067,
135.625050532182));
#55825=CARTESIAN_POINT('Ctrl Pts',(62.8751116989644,-0.84028819825018,135.652238210782));
#55826=CARTESIAN_POINT('Ctrl Pts',(62.8673654228803,-0.704656673015628,
135.673803075452));
#55827=CARTESIAN_POINT('Ctrl Pts',(62.8596191467962,-0.568361483534681,
135.689659818898));
#55828=CARTESIAN_POINT('Ctrl Pts',(62.8518728135309,-0.432065287953422,
135.705516679395));
#55829=CARTESIAN_POINT('Ctrl Pts',(62.8441264802655,-0.295105806695978,
135.715665289407));
#55830=CARTESIAN_POINT('Ctrl Pts',(62.8363801470002,-0.157998060555954,
135.720072130192));
#55831=CARTESIAN_POINT('Ctrl Pts',(62.8286320789972,-0.0208596100868197,
135.724479957857));
#55832=CARTESIAN_POINT('Ctrl Pts',(62.8208840109942,0.116426780646181,135.723143445086));
#55833=CARTESIAN_POINT('Ctrl Pts',(62.8131359429913,0.253345595042856,135.716081199192));
#55834=CARTESIAN_POINT('Ctrl Pts',(62.8053796402494,0.390409928384827,135.70901144746));
#55835=CARTESIAN_POINT('Ctrl Pts',(62.7976233375076,0.527105513927296,135.696203826581));
#55836=CARTESIAN_POINT('Ctrl Pts',(62.7898670347657,0.662920906840735,135.677728953099));
#55837=CARTESIAN_POINT('Ctrl Pts',(62.7821065922515,0.798808788518695,135.65924421902));
#55838=CARTESIAN_POINT('Ctrl Pts',(62.7743461497374,0.933815156816525,135.635086274032));
#55839=CARTESIAN_POINT('Ctrl Pts',(62.7665857072232,1.0674392581739,135.605376811312));
#55840=CARTESIAN_POINT('Ctrl Pts',(62.7588128069578,1.20127786480155,135.575619656325));
#55841=CARTESIAN_POINT('Ctrl Pts',(62.7510399066924,1.33372939236694,135.540293275822));
#55842=CARTESIAN_POINT('Ctrl Pts',(62.7432670064269,1.46430787116021,135.499569401098));
#55843=CARTESIAN_POINT('Ctrl Pts',(62.7357766706649,1.59013949334254,135.460325941798));
#55844=CARTESIAN_POINT('Ctrl Pts',(62.7282863349028,1.71423159242746,135.41607070369));
#55845=CARTESIAN_POINT('Ctrl Pts',(62.7207959991407,1.83616906217512,135.366998696311));
#55846=CARTESIAN_POINT('Ctrl Pts',(62.7130216650216,1.96272982814982,135.316066108856));
#55847=CARTESIAN_POINT('Ctrl Pts',(62.7052473309026,2.08737026042727,135.259782947128));
#55848=CARTESIAN_POINT('Ctrl Pts',(62.6974729967835,2.2096048303726,135.198314367447));
#55849=CARTESIAN_POINT('Ctrl Pts',(62.6897082438364,2.33168875713472,135.136921542297));
#55850=CARTESIAN_POINT('Ctrl Pts',(62.6819434908893,2.45137237511715,135.070356188473));
#55851=CARTESIAN_POINT('Ctrl Pts',(62.6741787379422,2.56818839282721,134.998832150602));
#55852=CARTESIAN_POINT('Ctrl Pts',(62.6664216970572,2.68488838722183,134.927379151413));
#55853=CARTESIAN_POINT('Ctrl Pts',(62.6586646561722,2.79872611800074,134.85097747205));
#55854=CARTESIAN_POINT('Ctrl Pts',(62.6509076152872,2.90925757762716,134.769887494227));
#55855=CARTESIAN_POINT('Ctrl Pts',(62.6431564240471,3.01970568461976,134.688858666987));
#55856=CARTESIAN_POINT('Ctrl Pts',(62.6354052328069,3.12685216923693,134.603148808781));
#55857=CARTESIAN_POINT('Ctrl Pts',(62.6276540415668,3.23028109496689,134.513062157189));
#55858=CARTESIAN_POINT('Ctrl Pts',(62.6199061447897,3.33366606064463,134.423013794827));
#55859=CARTESIAN_POINT('Ctrl Pts',(62.6121582480127,3.43333631585974,134.328592595229));
#55860=CARTESIAN_POINT('Ctrl Pts',(62.6044103512356,3.52890836466922,134.230143566947));
#55861=CARTESIAN_POINT('Ctrl Pts',(62.5966640751515,3.62446042186626,134.131715132079));
#55862=CARTESIAN_POINT('Ctrl Pts',(62.5889177990674,3.71591570563536,134.02926082472));
#55863=CARTESIAN_POINT('Ctrl Pts',(62.5811715229833,3.80292731209237,133.923162778884));
#55864=CARTESIAN_POINT('Ctrl Pts',(62.5734251897179,3.88993956084953,133.817063949856));
#55865=CARTESIAN_POINT('Ctrl Pts',(62.5656788564526,3.97250781891797,133.707321630985));
#55866=CARTESIAN_POINT('Ctrl Pts',(62.5579325231872,4.0503255047097,133.594351006151));
#55867=CARTESIAN_POINT('Ctrl Pts',(62.5501844551843,4.12816061723252,133.481355082329));
#55868=CARTESIAN_POINT('Ctrl Pts',(62.5424363871812,4.20124281878338,133.365129735853));
#55869=CARTESIAN_POINT('Ctrl Pts',(62.5346883191783,4.2693091149097,133.246118743149));
#55870=CARTESIAN_POINT('Ctrl Pts',(62.5269320164364,4.33744775270554,133.126981264145));
#55871=CARTESIAN_POINT('Ctrl Pts',(62.5191757136946,4.40055964149048,133.005052564679));
#55872=CARTESIAN_POINT('Ctrl Pts',(62.5114194109527,4.45842774453909,132.880801107738));
#55873=CARTESIAN_POINT('Ctrl Pts',(62.5036589684385,4.51632673353659,132.756483334053));
#55874=CARTESIAN_POINT('Ctrl Pts',(62.4958985259244,4.56897621000845,132.629840693468));
#55875=CARTESIAN_POINT('Ctrl Pts',(62.4881380834102,4.61620788833998,132.501360262271));
#55876=CARTESIAN_POINT('Ctrl Pts',(62.4803651831448,4.66351538715467,132.372673582879));
#55877=CARTESIAN_POINT('Ctrl Pts',(62.4725922828793,4.70538758870002,132.242143589959));
#55878=CARTESIAN_POINT('Ctrl Pts',(62.4648193826139,4.74170629687945,132.110271968552));
#55879=CARTESIAN_POINT('Ctrl Pts',(62.4573290468519,4.77670472853521,131.983194212747));
#55880=CARTESIAN_POINT('Ctrl Pts',(62.4498387110899,4.80654635401489,131.854870978125));
#55881=CARTESIAN_POINT('Ctrl Pts',(62.4423483753279,4.83117086530171,131.72575691274));
#55882=CARTESIAN_POINT('Ctrl Pts',(62.4345740412088,4.85672902241847,131.591747448321));
#55883=CARTESIAN_POINT('Ctrl Pts',(62.4267997070897,4.87674760259234,131.456461498939));
#55884=CARTESIAN_POINT('Ctrl Pts',(62.4190253729706,4.89110311642676,131.32039682461));
#55885=CARTESIAN_POINT('Ctrl Pts',(62.4112606200235,4.90544093837332,131.184499837832));
#55886=CARTESIAN_POINT('Ctrl Pts',(62.4034958670765,4.914129539927,131.047826420717));
#55887=CARTESIAN_POINT('Ctrl Pts',(62.3957311141294,4.91709625216194,130.910885307075));
#55888=CARTESIAN_POINT('Ctrl Pts',(62.3879740732444,4.92006001781648,130.774080205277));
#55889=CARTESIAN_POINT('Ctrl Pts',(62.3802170323594,4.91731319528724,130.637008324411));
#55890=CARTESIAN_POINT('Ctrl Pts',(62.3724599914744,4.9088348541665,130.500183963268));
#55891=CARTESIAN_POINT('Ctrl Pts',(62.3647088002344,4.90036290662878,130.36346278244));
#55892=CARTESIAN_POINT('Ctrl Pts',(62.3569576089942,4.88616806762424,130.226989138446));
#55893=CARTESIAN_POINT('Ctrl Pts',(62.3492064177541,4.86628147700257,130.091277418296));
#55894=CARTESIAN_POINT('Ctrl Pts',(62.3414585209771,4.84640333871233,129.955623379247));
#55895=CARTESIAN_POINT('Ctrl Pts',(62.3337106242,4.82083831686868,129.820731005977));
#55896=CARTESIAN_POINT('Ctrl Pts',(62.3259627274229,4.78966938801219,129.687109430035));
#55897=CARTESIAN_POINT('Ctrl Pts',(62.3182164513388,4.7585069790237,129.553515804846));
#55898=CARTESIAN_POINT('Ctrl Pts',(62.3104701752547,4.72174308338244,129.42119282875));
#55899=CARTESIAN_POINT('Ctrl Pts',(62.3027238991706,4.67951169123469,129.290638914578));
#55900=CARTESIAN_POINT('Ctrl Pts',(62.2949775659052,4.63727998734435,129.160084036686));
#55901=CARTESIAN_POINT('Ctrl Pts',(62.2872312326399,4.58958082674231,129.031298618764));
#55902=CARTESIAN_POINT('Ctrl Pts',(62.2794848993745,4.53659780054823,128.904765013612));
#55903=CARTESIAN_POINT('Ctrl Pts',(62.2717368313715,4.48360290917272,128.778203072137));
#55904=CARTESIAN_POINT('Ctrl Pts',(62.2639887633686,4.42532194858005,128.653894307444));
#55905=CARTESIAN_POINT('Ctrl Pts',(62.2562406953656,4.36198612551915,128.532299856213));
#55906=CARTESIAN_POINT('Ctrl Pts',(62.2484843926238,4.29858298839197,128.410576172953));
#55907=CARTESIAN_POINT('Ctrl Pts',(62.2407280898819,4.2301144378132,128.291572913161));
#55908=CARTESIAN_POINT('Ctrl Pts',(62.2329717871401,4.15685729130931,128.17572589167));
#55909=CARTESIAN_POINT('Ctrl Pts',(62.2252113446259,4.08356104526051,128.059817039134));
#55910=CARTESIAN_POINT('Ctrl Pts',(62.2174509021117,4.00547133309866,127.947068102813));
#55911=CARTESIAN_POINT('Ctrl Pts',(62.2096904595975,3.92290698341341,127.837883942791));
#55912=CARTESIAN_POINT('Ctrl Pts',(62.2019175593321,3.84021009410445,127.728524510662));
#55913=CARTESIAN_POINT('Ctrl Pts',(62.1941446590667,3.75302446198057,127.622741592074));
#55914=CARTESIAN_POINT('Ctrl Pts',(62.1863717588013,3.66170828099704,127.520905801769));
#55915=CARTESIAN_POINT('Ctrl Pts',(62.1788814230392,3.57371167320297,127.42277199895));
#55916=CARTESIAN_POINT('Ctrl Pts',(62.1713910872771,3.48187982910589,127.328303551492));
#55917=CARTESIAN_POINT('Ctrl Pts',(62.163900751515,3.38656265903332,127.237796946616));
#55918=CARTESIAN_POINT('Ctrl Pts',(62.1561264173959,3.28763150948712,127.143858756308));
#55919=CARTESIAN_POINT('Ctrl Pts',(62.1483520832768,3.18463214033952,127.053891197667));
#55920=CARTESIAN_POINT('Ctrl Pts',(62.1405777491577,3.07791658215494,126.96826721727));
#55921=CARTESIAN_POINT('Ctrl Pts',(62.1328129962106,2.97133254135852,126.882748760776));
#55922=CARTESIAN_POINT('Ctrl Pts',(62.1250482432635,2.86104172611729,126.80156347383));
#55923=CARTESIAN_POINT('Ctrl Pts',(62.1172834903164,2.74743286926502,126.725047477909));
#55924=CARTESIAN_POINT('Ctrl Pts',(62.1095264494314,2.63393685033129,126.648607478753));
#55925=CARTESIAN_POINT('Ctrl Pts',(62.1017694085464,2.51712967020883,126.576827758566));
#55926=CARTESIAN_POINT('Ctrl Pts',(62.0940123676614,2.39743270964121,126.510003917751));
#55927=CARTESIAN_POINT('Ctrl Pts',(62.0862611764213,2.27782601348201,126.443230469315));
#55928=CARTESIAN_POINT('Ctrl Pts',(62.0785099851811,2.15533421444377,126.381405651254));
#55929=CARTESIAN_POINT('Ctrl Pts',(62.070758793941,2.03040691273705,126.324781303478));
#55930=CARTESIAN_POINT('Ctrl Pts',(62.0630108971639,1.90553270846643,126.268181022559));
#55931=CARTESIAN_POINT('Ctrl Pts',(62.0552630003868,1.77822541571749,126.216776976794));
#55932=CARTESIAN_POINT('Ctrl Pts',(62.0475151036097,1.64895823212723,126.170774553706));
#55933=CARTESIAN_POINT('Ctrl Pts',(62.0397688275256,1.51971808844474,126.124781753333));
#55934=CARTESIAN_POINT('Ctrl Pts',(62.0320225514415,1.3885192374707,126.084188459195));
#55935=CARTESIAN_POINT('Ctrl Pts',(62.0242762753573,1.25585343298319,126.049151345897));
#55936=CARTESIAN_POINT('Ctrl Pts',(62.016529942092,1.12318664918702,126.014113973964));
#55937=CARTESIAN_POINT('Ctrl Pts',(62.0087836088266,0.989053268274115,125.984632964543));
#55938=CARTESIAN_POINT('Ctrl Pts',(62.0010372755612,0.853958342801723,125.960814580698));
#55939=CARTESIAN_POINT('Ctrl Pts',(61.9932892075583,0.718833163757822,125.936990862891));
#55940=CARTESIAN_POINT('Ctrl Pts',(61.9855411395553,0.582746396623301,125.918832361914));
#55941=CARTESIAN_POINT('Ctrl Pts',(61.9777930715523,0.446210981641435,125.906393812619));
#55942=CARTESIAN_POINT('Ctrl Pts',(61.9700367688105,0.309530455195548,125.893942043486));
#55943=CARTESIAN_POINT('Ctrl Pts',(61.9622804660686,0.172400718360169,125.887222405485));
#55944=CARTESIAN_POINT('Ctrl Pts',(61.9545241633268,0.0353380611301516,
125.886237572751));
#55945=CARTESIAN_POINT('Ctrl Pts',(61.9467637208126,-0.101797750566906,
125.885252214384));
#55946=CARTESIAN_POINT('Ctrl Pts',(61.9390032782984,-0.238866020780342,
125.890007746714));
#55947=CARTESIAN_POINT('Ctrl Pts',(61.9312428357842,-0.375353794614429,
125.900454766984));
#55948=CARTESIAN_POINT('Ctrl Pts',(61.9234699355188,-0.512060670739889,
125.91091855774));
#55949=CARTESIAN_POINT('Ctrl Pts',(61.9156970352534,-0.648184799866215,
125.927092047883));
#55950=CARTESIAN_POINT('Ctrl Pts',(61.907924134988,-0.783220760732462,125.948874205016));
#55951=CARTESIAN_POINT('Ctrl Pts',(61.900433799226,-0.913347824284512,125.969864525871));
#55952=CARTESIAN_POINT('Ctrl Pts',(61.8929434634641,-1.04246415946571,125.996062753751));
#55953=CARTESIAN_POINT('Ctrl Pts',(61.8854531277022,-1.17013118810115,126.027334757773));
#55954=CARTESIAN_POINT('Ctrl Pts',(61.8776787935831,-1.30263875093255,126.059792449332));
#55955=CARTESIAN_POINT('Ctrl Pts',(61.869904459464,-1.43400468095375,126.097819072665));
#55956=CARTESIAN_POINT('Ctrl Pts',(61.8621301253449,-1.5637249265304,126.14132004122));
#55957=CARTESIAN_POINT('Ctrl Pts',(61.8543653723978,-1.69328530349746,126.184767398719));
#55958=CARTESIAN_POINT('Ctrl Pts',(61.8466006194507,-1.82120366433245,126.233675554525));
#55959=CARTESIAN_POINT('Ctrl Pts',(61.8388358665037,-1.94698710092558,126.287899138562));
#55960=CARTESIAN_POINT('Ctrl Pts',(61.8310788256187,-2.07264560763589,126.342068866971));
#55961=CARTESIAN_POINT('Ctrl Pts',(61.8233217847338,-2.19617305316668,126.40154336368));
#55962=CARTESIAN_POINT('Ctrl Pts',(61.8155647438488,-2.31709297394084,126.466127888376));
#55963=CARTESIAN_POINT('Ctrl Pts',(61.8078135526088,-2.43792170806164,126.530663709379));
#55964=CARTESIAN_POINT('Ctrl Pts',(61.8000623613687,-2.55614648787296,126.600301704741));
#55965=CARTESIAN_POINT('Ctrl Pts',(61.7923111701286,-2.6713124134327,126.67479973869));
#55966=CARTESIAN_POINT('Ctrl Pts',(61.7845632733515,-2.78642939040287,126.749266108989));
#55967=CARTESIAN_POINT('Ctrl Pts',(61.7768153765745,-2.89848977132767,126.828588197559));
#55968=CARTESIAN_POINT('Ctrl Pts',(61.7690674797974,-3.00706498298513,126.912478906799));
#55969=CARTESIAN_POINT('Ctrl Pts',(61.7613212037133,-3.11561748304877,126.996352067911));
#55970=CARTESIAN_POINT('Ctrl Pts',(61.7535749276292,-3.22068595473,127.084791709951));
#55971=CARTESIAN_POINT('Ctrl Pts',(61.7458286515451,-3.32187277831748,127.17746879299));
#55972=CARTESIAN_POINT('Ctrl Pts',(61.7380823182798,-3.42306034884379,127.270146560151));
#55973=CARTESIAN_POINT('Ctrl Pts',(61.7303359850143,-3.52036592578884,127.367061566662));
#55974=CARTESIAN_POINT('Ctrl Pts',(61.722589651749,-3.6134271137847,127.467846335285));
#55975=CARTESIAN_POINT('Ctrl Pts',(61.714841583746,-3.70650914218761,127.568653673957));
#55976=CARTESIAN_POINT('Ctrl Pts',(61.7070935157431,-3.79534462507557,127.673332212));
#55977=CARTESIAN_POINT('Ctrl Pts',(61.6993454477401,-3.87961025573602,127.781479983785));
#55978=CARTESIAN_POINT('Ctrl Pts',(61.6915891449983,-3.96396544491174,127.889742696309));
#55979=CARTESIAN_POINT('Ctrl Pts',(61.6838328422565,-4.04374083901207,128.001481699149));
#55980=CARTESIAN_POINT('Ctrl Pts',(61.6760765395146,-4.11865512085688,128.116264068344));
#55981=CARTESIAN_POINT('Ctrl Pts',(61.6683160970005,-4.19360938670953,128.231107700346));
#55982=CARTESIAN_POINT('Ctrl Pts',(61.6605556544863,-4.26369717080579,128.348997599436));
#55983=CARTESIAN_POINT('Ctrl Pts',(61.6527952119721,-4.32868277243377,128.469475498736));
#55984=CARTESIAN_POINT('Ctrl Pts',(61.6450223117067,-4.39377269471863,128.590146799855));
#55985=CARTESIAN_POINT('Ctrl Pts',(61.6372494114413,-4.45374389621378,128.713414051406));
#55986=CARTESIAN_POINT('Ctrl Pts',(61.6294765111759,-4.50840818580015,128.838797417689));
#55987=CARTESIAN_POINT('Ctrl Pts',(61.6219861754136,-4.56108529077072,128.95962278279));
#55988=CARTESIAN_POINT('Ctrl Pts',(61.6144958396513,-4.60883451269228,129.082412794444));
#55989=CARTESIAN_POINT('Ctrl Pts',(61.607005503889,-4.65153163745955,129.206725963394));
#55990=CARTESIAN_POINT('Ctrl Pts',(61.5995575851391,-4.69398697273639,129.330335159466));
#55991=CARTESIAN_POINT('Ctrl Pts',(61.5921096663892,-4.73153827174323,129.455709728754));
#55992=CARTESIAN_POINT('Ctrl Pts',(61.5846617476392,-4.76405452823404,129.582490119308));
#55993=CARTESIAN_POINT('Ctrl Pts',(63.3349537467757,-4.76405452823404,129.582490119308));
#55994=CARTESIAN_POINT('Ctrl Pts',(63.3271906269684,-4.7981070602073,129.715260424653));
#55995=CARTESIAN_POINT('Ctrl Pts',(63.319427507161,-4.82657353511072,129.849332155469));
#55996=CARTESIAN_POINT('Ctrl Pts',(63.3116643873537,-4.8493826737915,129.984195545382));
#55997=CARTESIAN_POINT('Ctrl Pts',(63.3038899276852,-4.87222513058033,130.119255934973));
#55998=CARTESIAN_POINT('Ctrl Pts',(63.2961154680168,-4.88939370113894,130.255109905985));
#55999=CARTESIAN_POINT('Ctrl Pts',(63.2883410083483,-4.90086903852806,130.391243527993));
#56000=CARTESIAN_POINT('Ctrl Pts',(63.284791087821,-4.90610882849322,130.453403930109));
#56001=CARTESIAN_POINT('Ctrl Pts',(63.2812411672937,-4.91016232332491,130.515622647955));
#56002=CARTESIAN_POINT('Ctrl Pts',(63.2776912467664,-4.91303128814727,130.577850961732));
#56003=CARTESIAN_POINT('Ctrl Pts',(63.273413976508,-4.91648808043679,130.652829348912));
#56004=CARTESIAN_POINT('Ctrl Pts',(63.2691367062496,-4.91822860435436,130.727887471573));
#56005=CARTESIAN_POINT('Ctrl Pts',(63.2648594359911,-4.91824980396411,130.802971982613));
#56006=CARTESIAN_POINT('',(63.6101405639656,-4.91824793751526,130.808864796387));
#56007=CARTESIAN_POINT('Ctrl Pts',(63.6801307828278,-4.76405452823405,129.582490119308));
#56008=CARTESIAN_POINT('Ctrl Pts',(63.6724626857052,-4.79782051767604,129.714143199672));
#56009=CARTESIAN_POINT('Ctrl Pts',(63.6647945885826,-4.82612406158235,129.84719330369));
#56010=CARTESIAN_POINT('Ctrl Pts',(63.65712649146,-4.84886539797774,129.981142897401));
#56011=CARTESIAN_POINT('Ctrl Pts',(63.6492955035514,-4.87208982086775,130.117937936891));
#56012=CARTESIAN_POINT('Ctrl Pts',(63.6414645156428,-4.88951296919464,130.255670685851));
#56013=CARTESIAN_POINT('Ctrl Pts',(63.6336335277342,-4.90108418362794,130.393803815781));
#56014=CARTESIAN_POINT('Ctrl Pts',(63.6258025398256,-4.91265539806124,130.53193694571));
#56015=CARTESIAN_POINT('Ctrl Pts',(63.6179715519171,-4.91837468076857,130.670470013715));
#56016=CARTESIAN_POINT('Ctrl Pts',(63.6101405640085,-4.91824793751596,130.808864795629));
#56017=CARTESIAN_POINT('Ctrl Pts',(63.6101405639656,-4.91824793751526,130.808864796387));
#56018=CARTESIAN_POINT('Ctrl Pts',(63.6003856693909,-4.9180900561228,130.98126022376));
#56019=CARTESIAN_POINT('Ctrl Pts',(63.5906307748162,-4.90886436956287,131.153250222946));
#56020=CARTESIAN_POINT('Ctrl Pts',(63.5808758802415,-4.89071988369391,131.324016351433));
#56021=CARTESIAN_POINT('Ctrl Pts',(63.5709349483462,-4.8722293611244,131.498039190973));
#56022=CARTESIAN_POINT('Ctrl Pts',(63.5609940164509,-4.84447662962381,131.670791202816));
#56023=CARTESIAN_POINT('Ctrl Pts',(63.5510530845557,-4.80766771366139,131.841430633292));
#56024=CARTESIAN_POINT('Ctrl Pts',(63.5462186811771,-4.78976706314237,131.924414788893));
#56025=CARTESIAN_POINT('Ctrl Pts',(63.5413842777985,-4.76972534017766,132.006899665763));
#56026=CARTESIAN_POINT('Ctrl Pts',(63.53654987442,-4.74757027226103,132.088790285724));
#56027=CARTESIAN_POINT('Ctrl Pts',(63.5287755403009,-4.71194211157042,132.220480794549));
#56028=CARTESIAN_POINT('Ctrl Pts',(63.5210012061818,-4.67077401886086,132.350896360319));
#56029=CARTESIAN_POINT('Ctrl Pts',(63.5132268720627,-4.62417264929384,132.47953534637));
#56030=CARTESIAN_POINT('Ctrl Pts',(63.5054621191156,-4.57762871175,132.608015796367));
#56031=CARTESIAN_POINT('Ctrl Pts',(63.4976973661685,-4.52566495233479,132.73472365899));
#56032=CARTESIAN_POINT('Ctrl Pts',(63.4899326132214,-4.46843852769493,132.859169656555));
#56033=CARTESIAN_POINT('Ctrl Pts',(63.4821755723364,-4.41126894114677,132.983492052601));
#56034=CARTESIAN_POINT('Ctrl Pts',(63.4744185314515,-4.3488472535323,133.105556701348));
#56035=CARTESIAN_POINT('Ctrl Pts',(63.4666614905665,-4.28137958289765,133.22489194966));
#56036=CARTESIAN_POINT('Ctrl Pts',(63.4589102993263,-4.21396279015807,133.344137206332));
#56037=CARTESIAN_POINT('Ctrl Pts',(63.4511591080862,-4.14150778008419,133.460656820454));
#56038=CARTESIAN_POINT('Ctrl Pts',(63.443407916846,-4.06426753506044,133.574001833672));
#56039=CARTESIAN_POINT('Ctrl Pts',(63.4356600200689,-3.98706011920139,133.687298672236));
#56040=CARTESIAN_POINT('Ctrl Pts',(63.4279121232919,-3.9050717332755,133.797423271129));
#56041=CARTESIAN_POINT('Ctrl Pts',(63.4201642265148,-3.81859967678151,133.903954070099));
#56042=CARTESIAN_POINT('Ctrl Pts',(63.4124179504307,-3.73214570837762,134.010462585122));
#56043=CARTESIAN_POINT('Ctrl Pts',(63.4046716743466,-3.64121018115383,134.113378492125));
#56044=CARTESIAN_POINT('Ctrl Pts',(63.3969253982625,-3.54613158206114,134.212312181953));
#56045=CARTESIAN_POINT('Ctrl Pts',(63.3891790649971,-3.45105228111983,134.311246602087));
#56046=CARTESIAN_POINT('Ctrl Pts',(63.3814327317318,-3.35183011819047,134.406198464498));
#56047=CARTESIAN_POINT('Ctrl Pts',(63.3736863984664,-3.24884116117753,134.496814296617));
#56048=CARTESIAN_POINT('Ctrl Pts',(63.3659383304635,-3.14582914050188,134.587450421524));
#56049=CARTESIAN_POINT('Ctrl Pts',(63.3581902624605,-3.03904894064808,134.673748325705));
#56050=CARTESIAN_POINT('Ctrl Pts',(63.3504421944575,-2.92891016995861,134.755394441619));
#56051=CARTESIAN_POINT('Ctrl Pts',(63.3426858917156,-2.81865434247283,134.837127331997));
#56052=CARTESIAN_POINT('Ctrl Pts',(63.3349295889738,-2.70503312821193,134.914198324785));
#56053=CARTESIAN_POINT('Ctrl Pts',(63.3271732862319,-2.58848607729979,134.986336572796));
#56054=CARTESIAN_POINT('Ctrl Pts',(63.3194128437178,-2.47187682171742,135.058513323163));
#56055=CARTESIAN_POINT('Ctrl Pts',(63.3116524012036,-2.3523389584402,135.125751891189));
#56056=CARTESIAN_POINT('Ctrl Pts',(63.3038919586894,-2.23033627854425,135.18782764118));
#56057=CARTESIAN_POINT('Ctrl Pts',(63.296119058424,-2.10813774911563,135.250003040675));
#56058=CARTESIAN_POINT('Ctrl Pts',(63.2883461581586,-1.98346685200986,135.306998897794));
#56059=CARTESIAN_POINT('Ctrl Pts',(63.2805732578931,-1.85680780081433,135.358638590344));
#56060=CARTESIAN_POINT('Ctrl Pts',(63.2730829221311,-1.73475312516517,135.408401049998));
#56061=CARTESIAN_POINT('Ctrl Pts',(63.2655925863692,-1.61085262433766,135.453189899611));
#56062=CARTESIAN_POINT('Ctrl Pts',(63.2581022506072,-1.48555064124843,135.492891555374));
#56063=CARTESIAN_POINT('Ctrl Pts',(63.2503279164881,-1.3554977953851,135.534098511483));
#56064=CARTESIAN_POINT('Ctrl Pts',(63.242553582369,-1.22352312664602,135.569955428021));
#56065=CARTESIAN_POINT('Ctrl Pts',(63.2347792482499,-1.09010632588325,135.600280890128));
#56066=CARTESIAN_POINT('Ctrl Pts',(63.2270144953028,-0.95685394940363,135.630568978812));
#56067=CARTESIAN_POINT('Ctrl Pts',(63.2192497423557,-0.82216335477627,135.655339091086));
#56068=CARTESIAN_POINT('Ctrl Pts',(63.2114849894086,-0.686531132179684,
135.674458980746));
#56069=CARTESIAN_POINT('Ctrl Pts',(63.2037279485236,-0.551033621418844,
135.693559880262));
#56070=CARTESIAN_POINT('Ctrl Pts',(63.1959709076386,-0.4145967284873,135.707021670841));
#56071=CARTESIAN_POINT('Ctrl Pts',(63.1882138667536,-0.277728680365565,
135.71476282539));
#56072=CARTESIAN_POINT('Ctrl Pts',(63.1804626755135,-0.140963845503597,
135.722498142274));
#56073=CARTESIAN_POINT('Ctrl Pts',(63.1727114842734,-0.00376889137982753,
135.724521387849));
#56074=CARTESIAN_POINT('Ctrl Pts',(63.1649602930333,0.133341717471359,135.720802730403));
#56075=CARTESIAN_POINT('Ctrl Pts',(63.1572123962562,0.270394050656239,135.717085653487));
#56076=CARTESIAN_POINT('Ctrl Pts',(63.1494644994791,0.407361719866178,135.70763153802));
#56077=CARTESIAN_POINT('Ctrl Pts',(63.141716602702,0.543729356880365,135.692462646878));
#56078=CARTESIAN_POINT('Ctrl Pts',(63.1339703266179,0.680068468724636,135.677296928741));
#56079=CARTESIAN_POINT('Ctrl Pts',(63.1262240505339,0.815807409704502,135.656418855856));
#56080=CARTESIAN_POINT('Ctrl Pts',(63.1184777744498,0.950435430138027,135.629902613616));
#56081=CARTESIAN_POINT('Ctrl Pts',(63.1107314411844,1.08506444436502,135.603386175638));
#56082=CARTESIAN_POINT('Ctrl Pts',(63.1029851079191,1.21858213808644,135.571231560809));
#56083=CARTESIAN_POINT('Ctrl Pts',(63.0952387746537,1.35048785093288,135.533564105151));
#56084=CARTESIAN_POINT('Ctrl Pts',(63.0874907066508,1.48242310314914,135.495888214127));
#56085=CARTESIAN_POINT('Ctrl Pts',(63.0797426386477,1.61274528029281,135.452697132971));
#56086=CARTESIAN_POINT('Ctrl Pts',(63.0719945706448,1.74096916579623,135.404165985867));
#56087=CARTESIAN_POINT('Ctrl Pts',(63.0642382679029,1.86932932917104,135.355583259282));
#56088=CARTESIAN_POINT('Ctrl Pts',(63.0564819651611,1.99558637982774,135.30164926797));
#56089=CARTESIAN_POINT('Ctrl Pts',(63.0487256624192,2.11927485877901,135.242587418378));
#56090=CARTESIAN_POINT('Ctrl Pts',(63.0409652199051,2.24302935399585,135.183494045699));
#56091=CARTESIAN_POINT('Ctrl Pts',(63.0332047773909,2.36421220054728,135.119267544247));
#56092=CARTESIAN_POINT('Ctrl Pts',(63.0254443348767,2.48238371565623,135.05017669351));
#56093=CARTESIAN_POINT('Ctrl Pts',(63.0176714346113,2.60074493017201,134.980974932006));
#56094=CARTESIAN_POINT('Ctrl Pts',(63.0098985343458,2.71608482411405,134.906893428381));
#56095=CARTESIAN_POINT('Ctrl Pts',(63.0021256340804,2.8279930709594,134.828244096633));
#56096=CARTESIAN_POINT('Ctrl Pts',(62.9946352983183,2.9358331711522,134.752453866199));
#56097=CARTESIAN_POINT('Ctrl Pts',(62.9871449625563,3.04048654595383,134.672422333052));
#56098=CARTESIAN_POINT('Ctrl Pts',(62.9796546267943,3.14161745588812,134.588461940649));
#56099=CARTESIAN_POINT('Ctrl Pts',(62.9718802926752,3.24658277501035,134.501318164449));
#56100=CARTESIAN_POINT('Ctrl Pts',(62.9641059585561,3.3480857465286,134.409665677165));
#56101=CARTESIAN_POINT('Ctrl Pts',(62.956331624437,3.44571445635907,134.313809997132));
#56102=CARTESIAN_POINT('Ctrl Pts',(62.94856687149,3.54322284753,134.218072450658));
#56103=CARTESIAN_POINT('Ctrl Pts',(62.9408021185429,3.63686620090813,134.11814228949));
#56104=CARTESIAN_POINT('Ctrl Pts',(62.9330373655958,3.72626483489741,134.014365826706));
#56105=CARTESIAN_POINT('Ctrl Pts',(62.9252803247108,3.81557467690312,133.910692436168));
#56106=CARTESIAN_POINT('Ctrl Pts',(62.9175232838258,3.90064793586042,133.803180640681));
#56107=CARTESIAN_POINT('Ctrl Pts',(62.9097662429408,3.98114131162124,133.692213958614));
#56108=CARTESIAN_POINT('Ctrl Pts',(62.9020150517007,4.06157398670125,133.581330957385));
#56109=CARTESIAN_POINT('Ctrl Pts',(62.8942638604605,4.13743342438148,133.466998570571));
#56110=CARTESIAN_POINT('Ctrl Pts',(62.8865126692204,4.20841644575172,133.349633506988));
#56111=CARTESIAN_POINT('Ctrl Pts',(62.8787647724433,4.27936929744435,133.232318326688));
#56112=CARTESIAN_POINT('Ctrl Pts',(62.8710168756663,4.34544965317717,133.111973367116));
#56113=CARTESIAN_POINT('Ctrl Pts',(62.8632689788892,4.40639767422509,132.989044255781));
#56114=CARTESIAN_POINT('Ctrl Pts',(62.8555227028051,4.46733294626091,132.866140858566));
#56115=CARTESIAN_POINT('Ctrl Pts',(62.847776426721,4.52313784545243,132.740654734823));
#56116=CARTESIAN_POINT('Ctrl Pts',(62.8400301506369,4.57359871339299,132.613055691742));
#56117=CARTESIAN_POINT('Ctrl Pts',(62.8322838173716,4.6240599538242,132.485455706755));
#56118=CARTESIAN_POINT('Ctrl Pts',(62.8245374841063,4.66917694050983,132.355743134874));
#56119=CARTESIAN_POINT('Ctrl Pts',(62.8167911508409,4.70878450303639,132.22440694303));
#56120=CARTESIAN_POINT('Ctrl Pts',(62.8090430828379,4.74840093540196,132.093041339357));
#56121=CARTESIAN_POINT('Ctrl Pts',(62.8012950148349,4.78250537563281,131.960051766445));
#56122=CARTESIAN_POINT('Ctrl Pts',(62.793546946832,4.81098288925761,131.825941109632));
#56123=CARTESIAN_POINT('Ctrl Pts',(62.7857906440901,4.83949066912279,131.691687918418));
#56124=CARTESIAN_POINT('Ctrl Pts',(62.7780343413482,4.8623594946218,131.5563116462));
#56125=CARTESIAN_POINT('Ctrl Pts',(62.7702780386064,4.8795257319743,131.420324653449));
#56126=CARTESIAN_POINT('Ctrl Pts',(62.7625175960922,4.89670113146455,131.284265080345));
#56127=CARTESIAN_POINT('Ctrl Pts',(62.7547571535781,4.90816784542063,131.14759452661));
#56128=CARTESIAN_POINT('Ctrl Pts',(62.7469967110639,4.91391434635695,131.010828191697));
#56129=CARTESIAN_POINT('Ctrl Pts',(62.7392238107985,4.91967007208672,130.873842307321));
#56130=CARTESIAN_POINT('Ctrl Pts',(62.7314509105331,4.91968723499943,130.736760725701));
#56131=CARTESIAN_POINT('Ctrl Pts',(62.7236780102676,4.91400646566557,130.600097263298));
#56132=CARTESIAN_POINT('Ctrl Pts',(62.7161876745055,4.90853220660595,130.468401861986));
#56133=CARTESIAN_POINT('Ctrl Pts',(62.7086973387435,4.89776711653985,130.337095015282));
#56134=CARTESIAN_POINT('Ctrl Pts',(62.7012070029814,4.88179258760838,130.206628073637));
#56135=CARTESIAN_POINT('Ctrl Pts',(62.6934326688623,4.86521237955723,130.071214438246));
#56136=CARTESIAN_POINT('Ctrl Pts',(62.6856583347432,4.84296738172533,129.93627670548));
#56137=CARTESIAN_POINT('Ctrl Pts',(62.6778840006241,4.81509198571704,129.802326570448));
#56138=CARTESIAN_POINT('Ctrl Pts',(62.670119247677,4.78725094364304,129.668541516986));
#56139=CARTESIAN_POINT('Ctrl Pts',(62.6623544947299,4.75379338874968,129.53574201863));
#56140=CARTESIAN_POINT('Ctrl Pts',(62.6545897417828,4.71480545686168,129.404434702938));
#56141=CARTESIAN_POINT('Ctrl Pts',(62.6468327008978,4.6758562483373,129.273257803523));
#56142=CARTESIAN_POINT('Ctrl Pts',(62.6390756600128,4.63138770439831,129.14357050978));
#56143=CARTESIAN_POINT('Ctrl Pts',(62.6313186191278,4.581536927794,129.015868950893));
#56144=CARTESIAN_POINT('Ctrl Pts',(62.6235674278877,4.53172374404811,128.888263692744));
#56145=CARTESIAN_POINT('Ctrl Pts',(62.6158162366476,4.4765365479962,128.762641551576));
#56146=CARTESIAN_POINT('Ctrl Pts',(62.6080650454075,4.41616205295959,128.639482841686));
#56147=CARTESIAN_POINT('Ctrl Pts',(62.6003171486304,4.35581321869391,128.516376477533));
#56148=CARTESIAN_POINT('Ctrl Pts',(62.5925692518533,4.29028164223597,128.395731812524));
#56149=CARTESIAN_POINT('Ctrl Pts',(62.5848213550763,4.21980179345092,128.278008328892));
#56150=CARTESIAN_POINT('Ctrl Pts',(62.5770750789922,4.14933668753086,128.160309470475));
#56151=CARTESIAN_POINT('Ctrl Pts',(62.5693288029081,4.0739255687979,128.045530913256));
#56152=CARTESIAN_POINT('Ctrl Pts',(62.561582526824,3.99384821175853,127.934106356367));
#56153=CARTESIAN_POINT('Ctrl Pts',(62.5538361935586,3.91377026360631,127.822680976966));
#56154=CARTESIAN_POINT('Ctrl Pts',(62.5460898602933,3.82902623657936,127.714609964781));
#56155=CARTESIAN_POINT('Ctrl Pts',(62.5383435270279,3.73993823376111,127.610296580927));
#56156=CARTESIAN_POINT('Ctrl Pts',(62.530595459025,3.65083028030233,127.505959836813));
#56157=CARTESIAN_POINT('Ctrl Pts',(62.5228473910219,3.55737666914271,127.405382692749));
#56158=CARTESIAN_POINT('Ctrl Pts',(62.515099323019,3.45993836707158,127.30893366817));
#56159=CARTESIAN_POINT('Ctrl Pts',(62.5073430202771,3.36239650641335,127.212382136419));
#56160=CARTESIAN_POINT('Ctrl Pts',(62.4995867175353,3.26086177332516,127.119967763965));
#56161=CARTESIAN_POINT('Ctrl Pts',(62.4918304147934,3.15573083556911,127.032021031058));
#56162=CARTESIAN_POINT('Ctrl Pts',(62.4840699722792,3.05054378626614,126.944027358331));
#56163=CARTESIAN_POINT('Ctrl Pts',(62.4763095297651,2.94175701768135,126.860506314468));
#56164=CARTESIAN_POINT('Ctrl Pts',(62.4685490872509,2.82979775081672,126.781746075757));
#56165=CARTESIAN_POINT('Ctrl Pts',(62.4607761869855,2.71765875699764,126.702859404119));
#56166=CARTESIAN_POINT('Ctrl Pts',(62.45300328672,2.60233741700265,126.628749021205));
#56167=CARTESIAN_POINT('Ctrl Pts',(62.4452303864546,2.48428798098635,126.559658473713));
#56168=CARTESIAN_POINT('Ctrl Pts',(62.4377400506926,2.37052993931783,126.493079541652));
#56169=CARTESIAN_POINT('Ctrl Pts',(62.4302497149306,2.25423897625108,126.431161958817));
#56170=CARTESIAN_POINT('Ctrl Pts',(62.4227593791685,2.13583882014304,126.374081213638));
#56171=CARTESIAN_POINT('Ctrl Pts',(62.4149850450494,2.01294948612922,126.314836234656));
#56172=CARTESIAN_POINT('Ctrl Pts',(62.4072107109304,1.88739858522604,126.260614440746));
#56173=CARTESIAN_POINT('Ctrl Pts',(62.3994363768113,1.75963521052172,126.211663480981));
#56174=CARTESIAN_POINT('Ctrl Pts',(62.3916716238642,1.63202929275819,126.1627728489));
#56175=CARTESIAN_POINT('Ctrl Pts',(62.383906870917,1.50221668804784,126.119140264729));
#56176=CARTESIAN_POINT('Ctrl Pts',(62.3761421179699,1.3706701950212,126.080967104531));
#56177=CARTESIAN_POINT('Ctrl Pts',(62.368385077085,1.23925435582608,126.042831858454));
#56178=CARTESIAN_POINT('Ctrl Pts',(62.3606280362,1.10610842846165,126.010145353828));
#56179=CARTESIAN_POINT('Ctrl Pts',(62.352870995315,0.971723927845806,125.98306041217));
#56180=CARTESIAN_POINT('Ctrl Pts',(62.3451198040749,0.837440767627235,125.955995895477));
#56181=CARTESIAN_POINT('Ctrl Pts',(62.3373686128347,0.701921274970532,125.934524610705));
#56182=CARTESIAN_POINT('Ctrl Pts',(62.3296174215946,0.565670475007717,125.91874909226));
#56183=CARTESIAN_POINT('Ctrl Pts',(62.3218695248175,0.42947758526931,125.90298027883));
#56184=CARTESIAN_POINT('Ctrl Pts',(62.3141216280404,0.292554393989836,125.892902461708));
#56185=CARTESIAN_POINT('Ctrl Pts',(62.3063737312633,0.155414213273108,125.888566736125));
#56186=CARTESIAN_POINT('Ctrl Pts',(62.2986274551792,0.0183027193259736,
125.884231917482));
#56187=CARTESIAN_POINT('Ctrl Pts',(62.2908811790951,-0.119025283253796,
125.885636813627));
#56188=CARTESIAN_POINT('Ctrl Pts',(62.283134903011,-0.256053686150223,125.892780467318));
#56189=CARTESIAN_POINT('Ctrl Pts',(62.2753885697457,-0.393083100559192,
125.899924173742));
#56190=CARTESIAN_POINT('Ctrl Pts',(62.2676422364804,-0.529812520436778,
125.912806701888));
#56191=CARTESIAN_POINT('Ctrl Pts',(62.259895903215,-0.665728566200701,125.931375029793));
#56192=CARTESIAN_POINT('Ctrl Pts',(62.252147835212,-0.801675049420699,125.949947515946));
#56193=CARTESIAN_POINT('Ctrl Pts',(62.2443997672091,-0.936807408777758,
125.974208282659));
#56194=CARTESIAN_POINT('Ctrl Pts',(62.2366516992061,-1.0706204870671,126.004052832103));
#56195=CARTESIAN_POINT('Ctrl Pts',(62.2288953964643,-1.20457578348844,126.033929100691));
#56196=CARTESIAN_POINT('Ctrl Pts',(62.2211390937224,-1.33720861570305,126.069400921593));
#56197=CARTESIAN_POINT('Ctrl Pts',(62.2133827909805,-1.46802653270147,126.110313199635));
#56198=CARTESIAN_POINT('Ctrl Pts',(62.2056223484664,-1.59891427116123,126.151247313792));
#56199=CARTESIAN_POINT('Ctrl Pts',(62.1978619059522,-1.72798479648652,126.197627538881));
#56200=CARTESIAN_POINT('Ctrl Pts',(62.1901014634381,-1.85476473441771,126.249250208096));
#56201=CARTESIAN_POINT('Ctrl Pts',(62.1823285631726,-1.98174819076026,126.300955746603));
#56202=CARTESIAN_POINT('Ctrl Pts',(62.1745556629072,-2.10643335596814,126.357920383799));
#56203=CARTESIAN_POINT('Ctrl Pts',(62.1667827626418,-2.22836979400339,126.419893589104));
#56204=CARTESIAN_POINT('Ctrl Pts',(62.1592924268797,-2.34587353537686,126.479613912294));
#56205=CARTESIAN_POINT('Ctrl Pts',(62.1518020911177,-2.46082465751549,126.54398482711));
#56206=CARTESIAN_POINT('Ctrl Pts',(62.1443117553556,-2.57284648150626,126.612744694667));
#56207=CARTESIAN_POINT('Ctrl Pts',(62.136536109027,-2.68913527177037,126.684123659337));
#56208=CARTESIAN_POINT('Ctrl Pts',(62.1287604626984,-2.80263561438379,126.760458703787));
#56209=CARTESIAN_POINT('Ctrl Pts',(62.1209848163697,-2.91289618281779,126.841505726124));
#56210=CARTESIAN_POINT('Ctrl Pts',(62.1130368578788,-3.02560017989628,126.924348790498));
#56211=CARTESIAN_POINT('Ctrl Pts',(62.1050888993877,-3.13491874251687,127.012114984055));
#56212=CARTESIAN_POINT('Ctrl Pts',(62.0971409408968,-3.24039644520109,127.104493871259));
#56213=CARTESIAN_POINT('Ctrl Pts',(62.0893847860394,-3.34332871352529,127.194643430485));
#56214=CARTESIAN_POINT('Ctrl Pts',(62.081628631182,-3.44260304548939,127.289185343095));
#56215=CARTESIAN_POINT('Ctrl Pts',(62.0738724763246,-3.53782608525522,127.387787824109));
#56216=CARTESIAN_POINT('Ctrl Pts',(62.0661216651445,-3.63298352019386,127.486322371998));
#56217=CARTESIAN_POINT('Ctrl Pts',(62.0583708539645,-3.7240949459022,127.588911642184));
#56218=CARTESIAN_POINT('Ctrl Pts',(62.0506200427844,-3.8108020325401,127.695185336034));
#56219=CARTESIAN_POINT('Ctrl Pts',(62.0428728929696,-3.8974681600686,127.801408827807));
#56220=CARTESIAN_POINT('Ctrl Pts',(62.0351257431549,-3.97973384270997,127.911312977104));
#56221=CARTESIAN_POINT('Ctrl Pts',(62.0273785933402,-4.05727967981009,128.024492875694));
#56222=CARTESIAN_POINT('Ctrl Pts',(62.0192831949441,-4.13831134439668,128.142760418137));
#56223=CARTESIAN_POINT('Ctrl Pts',(62.0111877965479,-4.21418867069417,128.264604719481));
#56224=CARTESIAN_POINT('Ctrl Pts',(62.0030923981517,-4.28459647969843,128.389528103983));
#56225=CARTESIAN_POINT('Ctrl Pts',(61.995345734245,-4.35197125312783,128.509070024772));
#56226=CARTESIAN_POINT('Ctrl Pts',(61.9875990703384,-4.41433773627809,128.631430899895));
#56227=CARTESIAN_POINT('Ctrl Pts',(61.9798524064317,-4.47146622546811,128.75614850526));
#56228=CARTESIAN_POINT('Ctrl Pts',(61.9721046736809,-4.52860259694843,128.880883318507));
#56229=CARTESIAN_POINT('Ctrl Pts',(61.96435694093,-4.58049937994932,129.007975150914));
#56230=CARTESIAN_POINT('Ctrl Pts',(61.9566092081791,-4.62697483225407,129.136941364892));
#56231=CARTESIAN_POINT('Ctrl Pts',(61.9488567769419,-4.67347846884025,129.265985788331));
#56232=CARTESIAN_POINT('Ctrl Pts',(61.9411043457046,-4.71455408953464,129.396906491452));
#56233=CARTESIAN_POINT('Ctrl Pts',(61.9333519144674,-4.75006966796013,129.529205249768));
#56234=CARTESIAN_POINT('Ctrl Pts',(61.9323125471737,-4.75483123623481,129.546942524459));
#56235=CARTESIAN_POINT('Ctrl Pts',(61.93127317988,-4.75949293913251,129.564704552633));
#56236=CARTESIAN_POINT('Ctrl Pts',(61.9302338125864,-4.76405452823398,129.582490119308));
#56237=CARTESIAN_POINT('Origin',(213.235140564004,0.,130.804360617566));
#56238=CARTESIAN_POINT('',(59.8346812321181,-4.76405452823407,129.582490119308));
#56239=CARTESIAN_POINT('',(60.1799785705036,-4.76405452823408,129.582490119308));
#56240=CARTESIAN_POINT('',(213.235140564004,-4.76405452823405,129.582490119308));
#56241=CARTESIAN_POINT('',(61.5148594360427,-4.91824847206951,130.800483829468));
#56242=CARTESIAN_POINT('Ctrl Pts',(61.5148594359911,-4.91824847207023,130.800483830382));
#56243=CARTESIAN_POINT('Ctrl Pts',(61.5070968711613,-4.91835683968032,130.937963348214));
#56244=CARTESIAN_POINT('Ctrl Pts',(61.4993343063315,-4.91269642418725,131.075513890078));
#56245=CARTESIAN_POINT('Ctrl Pts',(61.4915717415017,-4.90127649067233,131.21261522499));
#56246=CARTESIAN_POINT('Ctrl Pts',(61.4838346137862,-4.88989397908694,131.349267293145));
#56247=CARTESIAN_POINT('Ctrl Pts',(61.4760974860707,-4.87278968287947,131.48547270254));
#56248=CARTESIAN_POINT('Ctrl Pts',(61.4683603583553,-4.85002488767876,131.620719393716));
#56249=CARTESIAN_POINT('Ctrl Pts',(61.4606228913126,-4.82725909408254,131.755972016405));
#56250=CARTESIAN_POINT('Ctrl Pts',(61.45288542427,-4.7988323720717,131.890265451109));
#56251=CARTESIAN_POINT('Ctrl Pts',(61.4451479572273,-4.76485739254276,132.023096475425));
#56252=CARTESIAN_POINT('Ctrl Pts',(61.4374084705606,-4.73087354490682,132.15596217113));
#56253=CARTESIAN_POINT('Ctrl Pts',(61.4296689838938,-4.69133865478323,132.287364317687));
#56254=CARTESIAN_POINT('Ctrl Pts',(61.4219294972271,-4.64641554361799,132.416813921859));
#56255=CARTESIAN_POINT('Ctrl Pts',(61.4141485291312,-4.60125165745883,132.546957338789));
#56256=CARTESIAN_POINT('Ctrl Pts',(61.4063675610354,-4.55064175497602,132.675126844799));
#56257=CARTESIAN_POINT('Ctrl Pts',(61.3985865929395,-4.49480021507383,132.800846051791));
#56258=CARTESIAN_POINT('Ctrl Pts',(61.3908339172754,-4.43916172098069,132.926108130306));
#56259=CARTESIAN_POINT('Ctrl Pts',(61.3830812416113,-4.37832979695381,133.04893737307));
#56260=CARTESIAN_POINT('Ctrl Pts',(61.3753285659473,-4.31256219993804,133.168888125159));
#56261=CARTESIAN_POINT('Ctrl Pts',(61.3675334516354,-4.24643458684454,133.28949549542));
#56262=CARTESIAN_POINT('Ctrl Pts',(61.3597383373236,-4.17531732287121,133.407192432046));
#56263=CARTESIAN_POINT('Ctrl Pts',(61.3519432230118,-4.09951552627355,133.521556877011));
#56264=CARTESIAN_POINT('Ctrl Pts',(61.3441481087,-4.0237137296759,133.635921321976));
#56265=CARTESIAN_POINT('Ctrl Pts',(61.3363529943881,-3.94322768337033,133.746952992341));
#56266=CARTESIAN_POINT('Ctrl Pts',(61.3285578800763,-3.85840175194456,133.854265367405));
#56267=CARTESIAN_POINT('Ctrl Pts',(61.3207835459572,-3.77380194923675,133.961291669456));
#56268=CARTESIAN_POINT('Ctrl Pts',(61.3130092118382,-3.68461164704665,134.064964817607));
#56269=CARTESIAN_POINT('Ctrl Pts',(61.3052348777191,-3.5911263909256,134.164865684799));
#56270=CARTESIAN_POINT('Ctrl Pts',(61.297470124772,-3.49775634702795,134.2646434331));
#56271=CARTESIAN_POINT('Ctrl Pts',(61.289705371825,-3.40010214555527,134.360657867836));
#56272=CARTESIAN_POINT('Ctrl Pts',(61.2819406188779,-3.29850088854574,134.452521106191));
#56273=CARTESIAN_POINT('Ctrl Pts',(61.2741835779929,-3.19700054333671,134.544293104683));
#56274=CARTESIAN_POINT('Ctrl Pts',(61.2664265371079,-3.0915612322331,134.631921851292));
#56275=CARTESIAN_POINT('Ctrl Pts',(61.2586694962229,-2.98255812490224,134.71505494135));
#56276=CARTESIAN_POINT('Ctrl Pts',(61.2509183049828,-2.87363721766269,134.798125340099));
#56277=CARTESIAN_POINT('Ctrl Pts',(61.2431671137427,-2.76115817308868,134.876706594169));
#56278=CARTESIAN_POINT('Ctrl Pts',(61.2354159225026,-2.64553030453546,134.950485612098));
#56279=CARTESIAN_POINT('Ctrl Pts',(61.2276680257255,-2.5299515809107,135.024233271976));
#56280=CARTESIAN_POINT('Ctrl Pts',(61.2199201289484,-2.41122702404822,135.093182545402));
#56281=CARTESIAN_POINT('Ctrl Pts',(61.2121722321714,-2.28979589771299,135.157062974645));
#56282=CARTESIAN_POINT('Ctrl Pts',(61.2044259560873,-2.1683901721518,135.220930041479));
#56283=CARTESIAN_POINT('Ctrl Pts',(61.1966796800032,-2.04427934902221,135.279730191205));
#56284=CARTESIAN_POINT('Ctrl Pts',(61.1889334039191,-1.91792797300829,135.333238552867));
#56285=CARTESIAN_POINT('Ctrl Pts',(61.1811870706538,-1.79157566429721,135.386747309515));
#56286=CARTESIAN_POINT('Ctrl Pts',(61.1734407373884,-1.66298312971189,135.434964047692));
#56287=CARTESIAN_POINT('Ctrl Pts',(61.1656944041231,-1.53263523173735,135.477711910689));
#56288=CARTESIAN_POINT('Ctrl Pts',(61.1579463361201,-1.40225814325484,135.520469346775));
#56289=CARTESIAN_POINT('Ctrl Pts',(61.1501982681172,-1.27012528058317,135.557755348827));
#56290=CARTESIAN_POINT('Ctrl Pts',(61.1424502001142,-1.13673662613277,135.589442947611));
#56291=CARTESIAN_POINT('Ctrl Pts',(61.1346938973724,-1.00320620463307,135.621164224352));
#56292=CARTESIAN_POINT('Ctrl Pts',(61.1269375946305,-0.868417706192536,
135.647275121455));
#56293=CARTESIAN_POINT('Ctrl Pts',(61.1191812918887,-0.732881816699323,
135.667699728224));
#56294=CARTESIAN_POINT('Ctrl Pts',(61.1114208493745,-0.59727358762098,135.68813523622));
#56295=CARTESIAN_POINT('Ctrl Pts',(61.1036604068604,-0.460917561147342,
135.702878364494));
#56296=CARTESIAN_POINT('Ctrl Pts',(61.0958999643462,-0.324328511737044,
135.711905225511));
#56297=CARTESIAN_POINT('Ctrl Pts',(61.0881270640808,-0.18752019745864,135.720946577248));
#56298=CARTESIAN_POINT('Ctrl Pts',(61.0803541638153,-0.0504785038106941,
135.724253315202));
#56299=CARTESIAN_POINT('Ctrl Pts',(61.0725812635499,0.0862819256928151,
135.721853728064));
#56300=CARTESIAN_POINT('Ctrl Pts',(61.0650909277877,0.218070769107917,135.719541371964));
#56301=CARTESIAN_POINT('Ctrl Pts',(61.0576005920255,0.349598135164484,135.711930384246));
#56302=CARTESIAN_POINT('Ctrl Pts',(61.0501102562634,0.480410850203245,135.699091302446));
#56303=CARTESIAN_POINT('Ctrl Pts',(61.0423359221443,0.616183369089502,135.685765422958));
#56304=CARTESIAN_POINT('Ctrl Pts',(61.0345615880252,0.7516160617334,135.666764964658));
#56305=CARTESIAN_POINT('Ctrl Pts',(61.0267872539061,0.886196555079165,135.642112029975));
#56306=CARTESIAN_POINT('Ctrl Pts',(61.0190225009591,1.02061118999468,135.617489477831));
#56307=CARTESIAN_POINT('Ctrl Pts',(61.011257748012,1.15417533444104,135.587228379679));
#56308=CARTESIAN_POINT('Ctrl Pts',(61.0034929950649,1.28638043973377,135.551402688874));
#56309=CARTESIAN_POINT('Ctrl Pts',(60.9957359541799,1.41845423705217,135.515612580651));
#56310=CARTESIAN_POINT('Ctrl Pts',(60.9879789132949,1.54917130649983,135.474268980017));
#56311=CARTESIAN_POINT('Ctrl Pts',(60.9802218724099,1.67803237167848,135.427497044506));
#56312=CARTESIAN_POINT('Ctrl Pts',(60.9724706811697,1.80679626172584,135.380760380075));
#56313=CARTESIAN_POINT('Ctrl Pts',(60.9647194899296,1.93370656735855,135.328603661582));
#56314=CARTESIAN_POINT('Ctrl Pts',(60.9569682986895,2.05827863199355,135.27120202236));
#56315=CARTESIAN_POINT('Ctrl Pts',(60.9492204019124,2.18279775017768,135.213824780365));
#56316=CARTESIAN_POINT('Ctrl Pts',(60.9414725051353,2.30498024964787,135.151207214689));
#56317=CARTESIAN_POINT('Ctrl Pts',(60.9337246083583,2.42436115386205,135.083572701367));
#56318=CARTESIAN_POINT('Ctrl Pts',(60.9259783322742,2.54371708616446,135.015952335727));
#56319=CARTESIAN_POINT('Ctrl Pts',(60.9182320561901,2.66027224891248,134.943317302427));
#56320=CARTESIAN_POINT('Ctrl Pts',(60.910485780106,2.77358635405368,134.865936887822));
#56321=CARTESIAN_POINT('Ctrl Pts',(60.9027394468406,2.88690129565401,134.788555902013));
#56322=CARTESIAN_POINT('Ctrl Pts',(60.8949931135753,2.99697480904156,134.70642968548));
#56323=CARTESIAN_POINT('Ctrl Pts',(60.88724678031,3.10339601964365,134.619870571394));
#56324=CARTESIAN_POINT('Ctrl Pts',(60.879498712307,3.20984106253783,134.533292072995));
#56325=CARTESIAN_POINT('Ctrl Pts',(60.871750644304,3.31263187185724,134.442278948302));
#56326=CARTESIAN_POINT('Ctrl Pts',(60.8640025763011,3.41139137208327,134.347183216706));
#56327=CARTESIAN_POINT('Ctrl Pts',(60.8562462735592,3.51025583508154,134.251986416234));
#56328=CARTESIAN_POINT('Ctrl Pts',(60.8484899708174,3.60508014811188,134.152698612765));
#56329=CARTESIAN_POINT('Ctrl Pts',(60.8407336680755,3.69552440716086,134.049708429216));
#56330=CARTESIAN_POINT('Ctrl Pts',(60.8329732255614,3.78601693903398,133.946663276704));
#56331=CARTESIAN_POINT('Ctrl Pts',(60.8252127830472,3.87212451338747,133.839912110781));
#56332=CARTESIAN_POINT('Ctrl Pts',(60.8174523405331,3.95354878479494,133.729875113983));
#56333=CARTESIAN_POINT('Ctrl Pts',(60.8096794402677,4.03510376567149,133.619661476029));
#56334=CARTESIAN_POINT('Ctrl Pts',(60.8019065400022,4.11196020080972,133.506151790576));
#56335=CARTESIAN_POINT('Ctrl Pts',(60.7941336397368,4.18386371289693,133.389794332517));
#56336=CARTESIAN_POINT('Ctrl Pts',(60.7866433039747,4.25315335120643,133.277666761144));
#56337=CARTESIAN_POINT('Ctrl Pts',(60.7791529682126,4.31784376577217,133.162895138263));
#56338=CARTESIAN_POINT('Ctrl Pts',(60.7716626324505,4.37774935038862,133.045898858969));
#56339=CARTESIAN_POINT('Ctrl Pts',(60.7638882983314,4.43992627345327,132.924466630186));
#56340=CARTESIAN_POINT('Ctrl Pts',(60.7561139642124,4.49714532826618,132.800253058388));
#56341=CARTESIAN_POINT('Ctrl Pts',(60.7483396300933,4.54914816007457,132.673701164441));
#56342=CARTESIAN_POINT('Ctrl Pts',(60.7405748771462,4.60108690304031,132.547305234393));
#56343=CARTESIAN_POINT('Ctrl Pts',(60.7328101241991,4.64782206668505,132.418577074217));
#56344=CARTESIAN_POINT('Ctrl Pts',(60.725045371252,4.68914098707509,132.28798451392));
#56345=CARTESIAN_POINT('Ctrl Pts',(60.717288330367,4.73041886893084,132.157521659995));
#56346=CARTESIAN_POINT('Ctrl Pts',(60.709531289482,4.76629109578391,132.025198461353));
#56347=CARTESIAN_POINT('Ctrl Pts',(60.701774248597,4.79659309512409,131.891502624071));
#56348=CARTESIAN_POINT('Ctrl Pts',(60.6940230573568,4.82687224349089,131.75790760786));
#56349=CARTESIAN_POINT('Ctrl Pts',(60.6862718661168,4.85158943921836,131.622942393101));
#56350=CARTESIAN_POINT('Ctrl Pts',(60.6785206748766,4.87063005821867,131.487109398947));
#56351=CARTESIAN_POINT('Ctrl Pts',(60.6707727780995,4.88966258444798,131.351334137439));
#56352=CARTESIAN_POINT('Ctrl Pts',(60.6630248813224,4.90302327845965,131.214692216479));
#56353=CARTESIAN_POINT('Ctrl Pts',(60.6552769845453,4.91064874166126,131.077695574205));
#56354=CARTESIAN_POINT('Ctrl Pts',(60.6475307084612,4.91827260978037,130.940727588675));
#56355=CARTESIAN_POINT('Ctrl Pts',(60.6397844323771,4.92016361161753,130.803405419533));
#56356=CARTESIAN_POINT('Ctrl Pts',(60.632038156293,4.91631031896289,130.666245049439));
#56357=CARTESIAN_POINT('Ctrl Pts',(60.6242918230277,4.91245699786414,130.529083666859));
#56358=CARTESIAN_POINT('Ctrl Pts',(60.6165454897623,4.90285930864056,130.392084476522));
#56359=CARTESIAN_POINT('Ctrl Pts',(60.608799156497,4.8875579382918,130.255761982551));
#56360=CARTESIAN_POINT('Ctrl Pts',(60.601051088494,4.87225314130715,130.119408960101));
#56361=CARTESIAN_POINT('Ctrl Pts',(60.593303020491,4.85124216511973,129.983733324017));
#56362=CARTESIAN_POINT('Ctrl Pts',(60.585554952488,4.8246173550832,129.849242593691));
#56363=CARTESIAN_POINT('Ctrl Pts',(60.5777986497461,4.79796424788179,129.714608925018));
#56364=CARTESIAN_POINT('Ctrl Pts',(60.5700423470042,4.76568546425192,129.581163061886));
#56365=CARTESIAN_POINT('Ctrl Pts',(60.5622860442624,4.72792423723797,129.44940103535));
#56366=CARTESIAN_POINT('Ctrl Pts',(60.5545256017482,4.69014285592013,129.317568683453));
#56367=CARTESIAN_POINT('Ctrl Pts',(60.546765159234,4.64687332391115,129.187422329733));
#56368=CARTESIAN_POINT('Ctrl Pts',(60.5390047167199,4.59830788968875,129.059440099569));
#56369=CARTESIAN_POINT('Ctrl Pts',(60.5312318164544,4.54966449391998,128.931252420968));
#56370=CARTESIAN_POINT('Ctrl Pts',(60.523458916189,4.49570836130183,128.805236167784));
#56371=CARTESIAN_POINT('Ctrl Pts',(60.5156860159235,4.4366791410462,128.681847658382));
#56372=CARTESIAN_POINT('Ctrl Pts',(60.5081956801616,4.37979578163313,128.562944632095));
#56373=CARTESIAN_POINT('Ctrl Pts',(60.5007053443996,4.31820191402721,128.446481888575));
#56374=CARTESIAN_POINT('Ctrl Pts',(60.4932150086377,4.25215006251213,128.332842276874));
#56375=CARTESIAN_POINT('Ctrl Pts',(60.4854406745186,4.18359383497015,128.214893984754));
#56376=CARTESIAN_POINT('Ctrl Pts',(60.4776663403995,4.11001773588511,128.09961350377));
#56377=CARTESIAN_POINT('Ctrl Pts',(60.4698920062804,4.03165484420368,127.987457658693));
#56378=CARTESIAN_POINT('Ctrl Pts',(60.4621272533334,3.95338852778296,127.875440035671));
#56379=CARTESIAN_POINT('Ctrl Pts',(60.4543625003863,3.87034737837648,127.766539703954));
#56380=CARTESIAN_POINT('Ctrl Pts',(60.4465977474393,3.78281004456712,127.661188457276));
#56381=CARTESIAN_POINT('Ctrl Pts',(60.4388407065543,3.69535965407188,127.555941846942));
#56382=CARTESIAN_POINT('Ctrl Pts',(60.4310836656693,3.60342221430857,127.454237605496));
#56383=CARTESIAN_POINT('Ctrl Pts',(60.4233266247843,3.50731909075212,127.356477809502));
#56384=CARTESIAN_POINT('Ctrl Pts',(60.4155754335442,3.41128843930847,127.258791734929));
#56385=CARTESIAN_POINT('Ctrl Pts',(60.4078242423041,3.31109862975987,127.16504446285));
#56386=CARTESIAN_POINT('Ctrl Pts',(60.400073051064,3.20711040445073,127.075603999581));
#56387=CARTESIAN_POINT('Ctrl Pts',(60.3923251542869,3.10316637691119,126.986201550895));
#56388=CARTESIAN_POINT('Ctrl Pts',(60.3845772575098,2.99542744037391,126.901102524685));
#56389=CARTESIAN_POINT('Ctrl Pts',(60.3768293607328,2.88429003440538,126.820636975051));
#56390=CARTESIAN_POINT('Ctrl Pts',(60.3690830846487,2.77317587598648,126.740188257076));
#56391=CARTESIAN_POINT('Ctrl Pts',(60.3613368085646,2.65866497860516,126.664371316973));
#56392=CARTESIAN_POINT('Ctrl Pts',(60.3535905324805,2.54118527586067,126.59347467085));
#56393=CARTESIAN_POINT('Ctrl Pts',(60.3458441992152,2.42370470590771,126.522577501385));
#56394=CARTESIAN_POINT('Ctrl Pts',(60.3380978659498,2.3032556215966,126.456600900381));
#56395=CARTESIAN_POINT('Ctrl Pts',(60.3303515326845,2.18029288213429,126.395788738758));
#56396=CARTESIAN_POINT('Ctrl Pts',(60.3226034646816,2.05730260601972,126.334962958674));
#56397=CARTESIAN_POINT('Ctrl Pts',(60.3148553966786,1.93179790499943,126.279304092638));
#56398=CARTESIAN_POINT('Ctrl Pts',(60.3071073286756,1.80425568443069,126.229008774516));
#56399=CARTESIAN_POINT('Ctrl Pts',(60.2993510259338,1.67657791047129,126.178660001931));
#56400=CARTESIAN_POINT('Ctrl Pts',(60.291594723192,1.54685865543108,126.133686308163));
#56401=CARTESIAN_POINT('Ctrl Pts',(60.2838384204501,1.41559266524179,126.094235304094));
#56402=CARTESIAN_POINT('Ctrl Pts',(60.2760779779359,1.28425661444102,126.054763243836));
#56403=CARTESIAN_POINT('Ctrl Pts',(60.2683175354218,1.15137256215172,126.020819843384));
#56404=CARTESIAN_POINT('Ctrl Pts',(60.2605570929076,1.01744668379657,125.992501797096));
#56405=CARTESIAN_POINT('Ctrl Pts',(60.2527841926422,0.883305815732105,125.964138292167));
#56406=CARTESIAN_POINT('Ctrl Pts',(60.2450112923767,0.748120165330152,125.941418251691));
#56407=CARTESIAN_POINT('Ctrl Pts',(60.2372383921113,0.612403182409007,125.924386703222));
#56408=CARTESIAN_POINT('Ctrl Pts',(60.2297480563491,0.481619853664547,125.90797429444));
#56409=CARTESIAN_POINT('Ctrl Pts',(60.2222577205869,0.350343459186021,125.896844002052));
#56410=CARTESIAN_POINT('Ctrl Pts',(60.2147673848247,0.219032596266184,125.890990309491));
#56411=CARTESIAN_POINT('Ctrl Pts',(60.2069930507056,0.0827430420705576,
125.884914672397));
#56412=CARTESIAN_POINT('Ctrl Pts',(60.1992187165865,-0.0540153702457747,
125.884504412487));
#56413=CARTESIAN_POINT('Ctrl Pts',(60.1914443824674,-0.190732316202125,
125.889810358788));
#56414=CARTESIAN_POINT('Ctrl Pts',(60.1836796295203,-0.327280770740772,
125.895109765984));
#56415=CARTESIAN_POINT('Ctrl Pts',(60.1759148765733,-0.463787473679632,
125.906111347496));
#56416=CARTESIAN_POINT('Ctrl Pts',(60.1681501236262,-0.599738528354169,
125.922814063439));
#56417=CARTESIAN_POINT('Ctrl Pts',(60.1603930827412,-0.735554554524998,
125.93950019001));
#56418=CARTESIAN_POINT('Ctrl Pts',(60.1526360418562,-0.870815645156497,
125.961876135121));
#56419=CARTESIAN_POINT('Ctrl Pts',(60.1448790009712,-1.00500981596048,125.9898888571));
#56420=CARTESIAN_POINT('Ctrl Pts',(60.1371278097311,-1.13910278989602,126.017880454468));
#56421=CARTESIAN_POINT('Ctrl Pts',(60.129376618491,-1.27213006428987,126.051500288301));
#56422=CARTESIAN_POINT('Ctrl Pts',(60.1216254272508,-1.40358703495665,126.090643772252));
#56423=CARTESIAN_POINT('Ctrl Pts',(60.1138775304738,-1.53498813290453,126.129770619177));
#56424=CARTESIAN_POINT('Ctrl Pts',(60.1061296336967,-1.66481988065294,126.174416335486));
#56425=CARTESIAN_POINT('Ctrl Pts',(60.0983817369196,-1.79259030907093,126.224425787645));
#56426=CARTESIAN_POINT('Ctrl Pts',(60.0906354608355,-1.92033401066954,126.274424778904));
#56427=CARTESIAN_POINT('Ctrl Pts',(60.0828891847514,-2.04601688674455,126.329785131931));
#56428=CARTESIAN_POINT('Ctrl Pts',(60.0751429086673,-2.16916489195958,126.390302764072));
#56429=CARTESIAN_POINT('Ctrl Pts',(60.067396575402,-2.2923138062252,126.450820842941));
#56430=CARTESIAN_POINT('Ctrl Pts',(60.0596502421367,-2.41292746140714,126.516496104456));
#56431=CARTESIAN_POINT('Ctrl Pts',(60.0519039088713,-2.53055481948119,126.587077680876));
#56432=CARTESIAN_POINT('Ctrl Pts',(60.0441558408683,-2.64820851938684,126.65767506355));
#56433=CARTESIAN_POINT('Ctrl Pts',(60.0364077728653,-2.76287425624932,126.733180746361));
#56434=CARTESIAN_POINT('Ctrl Pts',(60.0286597048623,-2.87412881743299,126.813299780733));
#56435=CARTESIAN_POINT('Ctrl Pts',(60.0209034021204,-2.98550162128808,126.893503966569));
#56436=CARTESIAN_POINT('Ctrl Pts',(60.0131470993786,-3.09345568949495,126.978331069649));
#56437=CARTESIAN_POINT('Ctrl Pts',(60.0053907966368,-3.19759941057609,127.067444633498));
#56438=CARTESIAN_POINT('Ctrl Pts',(59.9976303541226,-3.30179871629688,127.156605759939));
#56439=CARTESIAN_POINT('Ctrl Pts',(59.9898699116084,-3.40218333655968,127.250057639544));
#56440=CARTESIAN_POINT('Ctrl Pts',(59.9821094690942,-3.49839831948231,127.347426678257));
#56441=CARTESIAN_POINT('Ctrl Pts',(59.9743365688288,-3.59476775523709,127.444952022396));
#56442=CARTESIAN_POINT('Ctrl Pts',(59.9665636685634,-3.68695391488976,127.54640680189));
#56443=CARTESIAN_POINT('Ctrl Pts',(59.9587907682979,-3.77464138331522,127.651383375361));
#56444=CARTESIAN_POINT('Ctrl Pts',(59.9513004325359,-3.8591411913919,127.752543785965));
#56445=CARTESIAN_POINT('Ctrl Pts',(59.9438100967739,-3.93946351942171,127.85697413967));
#56446=CARTESIAN_POINT('Ctrl Pts',(59.9363197610119,-4.01536512561121,127.964285623745));
#56447=CARTESIAN_POINT('Ctrl Pts',(59.9284606122327,-4.0950040142499,128.076880966044));
#56448=CARTESIAN_POINT('Ctrl Pts',(59.9206014634536,-4.17002604765882,128.193001885756));
#56449=CARTESIAN_POINT('Ctrl Pts',(59.9127423146745,-4.24010706841768,128.312238006045));
#56450=CARTESIAN_POINT('Ctrl Pts',(59.904896692256,-4.31006747291255,128.431268909355));
#56451=CARTESIAN_POINT('Ctrl Pts',(59.8970510698376,-4.37510361483341,128.553404007396));
#56452=CARTESIAN_POINT('Ctrl Pts',(59.8892054474192,-4.43493339828359,128.678202388438));
#56453=CARTESIAN_POINT('Ctrl Pts',(59.8813676673364,-4.49470337701437,128.80287602338));
#56454=CARTESIAN_POINT('Ctrl Pts',(59.8735298872537,-4.54927718823693,128.930207304384));
#56455=CARTESIAN_POINT('Ctrl Pts',(59.865692107171,-4.59841734646034,129.059728573187));
#56456=CARTESIAN_POINT('Ctrl Pts',(59.857862136672,-4.64750854130667,129.189120786673));
#56457=CARTESIAN_POINT('Ctrl Pts',(59.850032166173,-4.69117673258091,129.320698287841));
#56458=CARTESIAN_POINT('Ctrl Pts',(59.842202195674,-4.72923173486454,129.453971688239));
#56459=CARTESIAN_POINT('Ctrl Pts',(59.8396952078221,-4.74141612667611,129.496642959584));
#56460=CARTESIAN_POINT('Ctrl Pts',(59.83718821997,-4.7530254545675,129.539487928472));
#56461=CARTESIAN_POINT('Ctrl Pts',(59.834681232118,-4.76405452823407,129.582490119308));
#56462=CARTESIAN_POINT('Ctrl Pts',(61.5846617476392,-4.76405452823404,129.582490119308));
#56463=CARTESIAN_POINT('Ctrl Pts',(61.5755367020045,-4.80389281518532,129.737818995501));
#56464=CARTESIAN_POINT('Ctrl Pts',(61.5664116563698,-4.83617178160265,129.89525866267));
#56465=CARTESIAN_POINT('Ctrl Pts',(61.557286610735,-4.86069278516076,130.054128179727));
#56466=CARTESIAN_POINT('Ctrl Pts',(61.5482434123213,-4.88499384724346,130.211572714486));
#56467=CARTESIAN_POINT('Ctrl Pts',(61.5392002139076,-4.90167542415839,130.370421469466));
#56468=CARTESIAN_POINT('Ctrl Pts',(61.530157015494,-4.91059106967392,130.529991506807));
#56469=CARTESIAN_POINT('Ctrl Pts',(61.5250578223435,-4.91561833950312,130.619968349535));
#56470=CARTESIAN_POINT('Ctrl Pts',(61.5199586291931,-4.91817728586783,130.710174166229));
#56471=CARTESIAN_POINT('Ctrl Pts',(61.5148594360427,-4.91824847206951,130.800483829468));
#56472=CARTESIAN_POINT('',(61.8601405639556,-4.91824995978084,130.803731637669));
#56473=CARTESIAN_POINT('Ctrl Pts',(61.9302338125864,-4.76405452823398,129.582490119308));
#56474=CARTESIAN_POINT('Ctrl Pts',(61.9224723506434,-4.79811813637933,129.715303610479));
#56475=CARTESIAN_POINT('Ctrl Pts',(61.9147108887005,-4.82659481655101,129.849430166516));
#56476=CARTESIAN_POINT('Ctrl Pts',(61.9069494267576,-4.84941049226405,129.984360044384));
#56477=CARTESIAN_POINT('Ctrl Pts',(61.8991759628984,-4.87226144893715,130.119498570713));
#56478=CARTESIAN_POINT('Ctrl Pts',(61.8914024990392,-4.88943386429407,130.255442512898));
#56479=CARTESIAN_POINT('Ctrl Pts',(61.88362903518,-4.9009055896504,130.391677368774));
#56480=CARTESIAN_POINT('Ctrl Pts',(61.8777074006343,-4.90964446930554,130.495457748216));
#56481=CARTESIAN_POINT('Ctrl Pts',(61.8717857660886,-4.91507630026852,130.599406853097));
#56482=CARTESIAN_POINT('Ctrl Pts',(61.8658641315429,-4.91721155718995,130.703298437016));
#56483=CARTESIAN_POINT('Ctrl Pts',(61.8639562756981,-4.91789950278441,130.736770642042));
#56484=CARTESIAN_POINT('Ctrl Pts',(61.8620484198533,-4.91824567789724,130.770249895539));
#56485=CARTESIAN_POINT('Ctrl Pts',(61.8601405640086,-4.91824995978073,130.803731636738));
#56486=CARTESIAN_POINT('Ctrl Pts',(61.8601405639556,-4.91824995978084,130.803731637669));
#56487=CARTESIAN_POINT('Ctrl Pts',(61.8523936239596,-4.91826734654802,130.939685850747));
#56488=CARTESIAN_POINT('Ctrl Pts',(61.8446466839636,-4.91264322818731,131.07586272131));
#56489=CARTESIAN_POINT('Ctrl Pts',(61.8368997439676,-4.90134821179031,131.211753265119));
#56490=CARTESIAN_POINT('Ctrl Pts',(61.8291623232629,-4.89006707449273,131.347476829235));
#56491=CARTESIAN_POINT('Ctrl Pts',(61.8214249025581,-4.87312893442009,131.482914377715));
#56492=CARTESIAN_POINT('Ctrl Pts',(61.8136874818533,-4.85055637356318,131.617555507728));
#56493=CARTESIAN_POINT('Ctrl Pts',(61.805957683371,-4.82800604919633,131.752064001211));
#56494=CARTESIAN_POINT('Ctrl Pts',(61.7982278848885,-4.79983241316138,131.885777251261));
#56495=CARTESIAN_POINT('Ctrl Pts',(61.7904980864062,-4.76610992436556,132.018188962664));
#56496=CARTESIAN_POINT('Ctrl Pts',(61.7827740199854,-4.73241244261029,132.150502483656));
#56497=CARTESIAN_POINT('Ctrl Pts',(61.7750499535647,-4.69317439419713,132.281516006551));
#56498=CARTESIAN_POINT('Ctrl Pts',(61.767325887144,-4.6485214192105,132.410732827747));
#56499=CARTESIAN_POINT('Ctrl Pts',(61.7596049357203,-4.60388645208125,132.539897537788));
#56500=CARTESIAN_POINT('Ctrl Pts',(61.7518839842966,-4.55384102912814,132.667266615246));
#56501=CARTESIAN_POINT('Ctrl Pts',(61.744163032873,-4.49856073868545,132.792358188706));
#56502=CARTESIAN_POINT('Ctrl Pts',(61.7364435444671,-4.44329092312385,132.917426058974));
#56503=CARTESIAN_POINT('Ctrl Pts',(61.7287240560611,-4.38278837203244,133.040216923306));
#56504=CARTESIAN_POINT('Ctrl Pts',(61.7210045676553,-4.31727677366038,133.16026900333));
#56505=CARTESIAN_POINT('Ctrl Pts',(61.7132848394377,-4.25176314012163,133.280324812861));
#56506=CARTESIAN_POINT('Ctrl Pts',(61.7055651112202,-4.18124033838913,133.397641322872));
#56507=CARTESIAN_POINT('Ctrl Pts',(61.6978453830026,-4.10597774563099,133.511781865707));
#56508=CARTESIAN_POINT('Ctrl Pts',(61.6901237123201,-4.03069621503663,133.625951128982));
#56509=CARTESIAN_POINT('Ctrl Pts',(61.6824020416376,-3.95067273752078,133.736942506331));
#56510=CARTESIAN_POINT('Ctrl Pts',(61.6746803709551,-3.86621943257266,133.844349163876));
#56511=CARTESIAN_POINT('Ctrl Pts',(61.6669504404176,-3.78167578810138,133.951870714098));
#56512=CARTESIAN_POINT('Ctrl Pts',(61.6592205098801,-3.6926930965086,134.055799576265));
#56513=CARTESIAN_POINT('Ctrl Pts',(61.6514905793427,-3.59962341446769,134.155762464035));
#56514=CARTESIAN_POINT('Ctrl Pts',(61.6437562747536,-3.50650106809962,134.255781916716));
#56515=CARTESIAN_POINT('Ctrl Pts',(61.6360219701646,-3.40928740441371,134.351830648011));
#56516=CARTESIAN_POINT('Ctrl Pts',(61.6282876655756,-3.30836980543768,134.443573759575));
#56517=CARTESIAN_POINT('Ctrl Pts',(61.6205414175746,-3.20729636821523,134.535458542024));
#56518=CARTESIAN_POINT('Ctrl Pts',(61.6127951695735,-3.10250787234992,134.623024170925));
#56519=CARTESIAN_POINT('Ctrl Pts',(61.6050489215724,-2.99442363468164,134.705976969613));
#56520=CARTESIAN_POINT('Ctrl Pts',(61.5991714502916,-2.912414641073,134.768917465695));
#56521=CARTESIAN_POINT('Ctrl Pts',(61.5932939790107,-2.82850893532166,134.829203201345));
#56522=CARTESIAN_POINT('Ctrl Pts',(61.5874165077298,-2.74289943095491,134.886723386131));
#56523=CARTESIAN_POINT('Ctrl Pts',(61.5796421736108,-2.62966078479028,134.962807319808));
#56524=CARTESIAN_POINT('Ctrl Pts',(61.5718678394917,-2.51307469558143,135.034296587921));
#56525=CARTESIAN_POINT('Ctrl Pts',(61.5640935053726,-2.39355056938918,135.100882319394));
#56526=CARTESIAN_POINT('Ctrl Pts',(61.5563287524255,-2.27417374600044,135.167385989903));
#56527=CARTESIAN_POINT('Ctrl Pts',(61.5485639994784,-2.15186642833995,135.228997959436));
#56528=CARTESIAN_POINT('Ctrl Pts',(61.5407992465313,-2.02706805444654,135.285451797752));
#56529=CARTESIAN_POINT('Ctrl Pts',(61.5330422056464,-1.90239363205743,135.34184956532));
#56530=CARTESIAN_POINT('Ctrl Pts',(61.5252851647613,-1.77523343101907,135.393099236834));
#56531=CARTESIAN_POINT('Ctrl Pts',(61.5175281238763,-1.64605230634128,135.438979789331));
#56532=CARTESIAN_POINT('Ctrl Pts',(61.5097769326362,-1.51696859815449,135.484825742946));
#56533=CARTESIAN_POINT('Ctrl Pts',(61.5020257413961,-1.38586736667427,135.525310506302));
#56534=CARTESIAN_POINT('Ctrl Pts',(61.494274550156,-1.2532339763495,135.560260917512));
#56535=CARTESIAN_POINT('Ctrl Pts',(61.4865266533789,-1.12065695875356,135.595196473864));
#56536=CARTESIAN_POINT('Ctrl Pts',(61.4787787566018,-0.986549454784961,
135.624602257095));
#56537=CARTESIAN_POINT('Ctrl Pts',(61.4710308598247,-0.851412331428461,
135.648354847991));
#56538=CARTESIAN_POINT('Ctrl Pts',(61.4632845837406,-0.716303475845133,
135.672102470357));
#56539=CARTESIAN_POINT('Ctrl Pts',(61.4555383076565,-0.580165814083412,
135.69019918486));
#56540=CARTESIAN_POINT('Ctrl Pts',(61.4477920315724,-0.443510367498282,
135.702572701217));
#56541=CARTESIAN_POINT('Ctrl Pts',(61.440045698307,-0.306853912153503,135.714946308912));
#56542=CARTESIAN_POINT('Ctrl Pts',(61.4322993650417,-0.169680053730782,
135.721596598904));
#56543=CARTESIAN_POINT('Ctrl Pts',(61.4245530317763,-0.0325045006574862,
135.722503205976));
#56544=CARTESIAN_POINT('Ctrl Pts',(61.4168049637733,0.104701771929812,135.723410016078));
#56545=CARTESIAN_POINT('Ctrl Pts',(61.4090568957703,0.241909349041014,135.718570581171));
#56546=CARTESIAN_POINT('Ctrl Pts',(61.4013088277674,0.378603356788063,135.70801665778));
#56547=CARTESIAN_POINT('Ctrl Pts',(61.3935525250255,0.515442644553225,135.697451517553));
#56548=CARTESIAN_POINT('Ctrl Pts',(61.3857962222837,0.651766882178081,135.681159786662));
#56549=CARTESIAN_POINT('Ctrl Pts',(61.3780399195418,0.787066593422253,135.659225110013));
#56550=CARTESIAN_POINT('Ctrl Pts',(61.3702794770276,0.922438518195928,135.637278726166));
#56551=CARTESIAN_POINT('Ctrl Pts',(61.3625190345135,1.05678444422027,135.609683473899));
#56552=CARTESIAN_POINT('Ctrl Pts',(61.3547585919993,1.18960688644697,135.576573785292));
#56553=CARTESIAN_POINT('Ctrl Pts',(61.3469856917339,1.32264254704954,135.543410946074));
#56554=CARTESIAN_POINT('Ctrl Pts',(61.3392127914685,1.45414946142179,135.504716091298));
#56555=CARTESIAN_POINT('Ctrl Pts',(61.331439891203,1.58364620045453,135.460673297604));
#56556=CARTESIAN_POINT('Ctrl Pts',(61.323949555441,1.70843540684064,135.418231570399));
#56557=CARTESIAN_POINT('Ctrl Pts',(61.316459219679,1.8313577629988,135.37082408669));
#56558=CARTESIAN_POINT('Ctrl Pts',(61.3089688839169,1.9520032742412,135.318656385441));
#56559=CARTESIAN_POINT('Ctrl Pts',(61.3011945497979,2.07722309671176,135.264510729943));
#56560=CARTESIAN_POINT('Ctrl Pts',(61.2934202156788,2.2003866716478,135.20506524684));
#56561=CARTESIAN_POINT('Ctrl Pts',(61.2856458815597,2.32101284308728,135.140497428683));
#56562=CARTESIAN_POINT('Ctrl Pts',(61.2778811286126,2.44149035355097,135.076009184592));
#56563=CARTESIAN_POINT('Ctrl Pts',(61.2701163756656,2.55943634117847,135.006411348809));
#56564=CARTESIAN_POINT('Ctrl Pts',(61.2623516227185,2.67438912366864,134.931929620951));
#56565=CARTESIAN_POINT('Ctrl Pts',(61.2545945818335,2.789227733435,134.857521869394));
#56566=CARTESIAN_POINT('Ctrl Pts',(61.2468375409485,2.90107872826772,134.778240090193));
#56567=CARTESIAN_POINT('Ctrl Pts',(61.2390805000635,3.00950488980073,134.694355910721));
#56568=CARTESIAN_POINT('Ctrl Pts',(61.2313293088233,3.11784928632189,134.610534988961));
#56569=CARTESIAN_POINT('Ctrl Pts',(61.2235781175832,3.22277368226279,134.522118813426));
#56570=CARTESIAN_POINT('Ctrl Pts',(61.2158269263431,3.32387004028159,134.429422136743));
#56571=CARTESIAN_POINT('Ctrl Pts',(61.208079029566,3.42492342965125,134.33676485862));
#56572=CARTESIAN_POINT('Ctrl Pts',(61.2003311327889,3.52215172955124,134.239830961522));
#56573=CARTESIAN_POINT('Ctrl Pts',(61.1925832360118,3.61518037306248,134.138975127929));
#56574=CARTESIAN_POINT('Ctrl Pts',(61.1848369599277,3.70818955698696,134.038140391202));
#56575=CARTESIAN_POINT('Ctrl Pts',(61.1770906838437,3.79700056695303,133.933385636968));
#56576=CARTESIAN_POINT('Ctrl Pts',(61.1693444077596,3.88127636357424,133.825101727304));
#56577=CARTESIAN_POINT('Ctrl Pts',(61.1615980744942,3.96555278230024,133.716817018312));
#56578=CARTESIAN_POINT('Ctrl Pts',(61.1538517412289,4.04529368075161,133.605003410438));
#56579=CARTESIAN_POINT('Ctrl Pts',(61.1461054079635,4.1202031720935,133.490083775892));
#56580=CARTESIAN_POINT('Ctrl Pts',(61.1383573399606,4.19512943889628,133.375138405891));
#56581=CARTESIAN_POINT('Ctrl Pts',(61.1306092719576,4.26522193215958,133.257085952571));
#56582=CARTESIAN_POINT('Ctrl Pts',(61.1228612039547,4.33022906763158,133.136376759092));
#56583=CARTESIAN_POINT('Ctrl Pts',(61.1151049012129,4.39530529346102,133.015539274445));
#56584=CARTESIAN_POINT('Ctrl Pts',(61.107348598471,4.45528517919736,132.892039753934));
#56585=CARTESIAN_POINT('Ctrl Pts',(61.0995922957292,4.50996371331631,132.766352046464));
#56586=CARTESIAN_POINT('Ctrl Pts',(61.091831853215,4.56467143101526,132.64059725568));
#56587=CARTESIAN_POINT('Ctrl Pts',(61.0840714107008,4.61407201834288,132.51265231534));
#56588=CARTESIAN_POINT('Ctrl Pts',(61.0763109681867,4.65800967399521,132.383008437527));
#56589=CARTESIAN_POINT('Ctrl Pts',(61.0685380679212,4.70201786227305,132.253156443851));
#56590=CARTESIAN_POINT('Ctrl Pts',(61.0607651676558,4.74054548450815,132.12160043814));
#56591=CARTESIAN_POINT('Ctrl Pts',(61.0529922673904,4.77348718539787,131.988844958257));
#56592=CARTESIAN_POINT('Ctrl Pts',(61.0455019316283,4.80523137248538,131.860915474458));
#56593=CARTESIAN_POINT('Ctrl Pts',(61.0380115958661,4.83178864984061,131.731872511942));
#56594=CARTESIAN_POINT('Ctrl Pts',(61.0305212601041,4.853110331071,131.602172109682));
#56595=CARTESIAN_POINT('Ctrl Pts',(61.022746925985,4.87524043032563,131.46755407725));
#56596=CARTESIAN_POINT('Ctrl Pts',(61.0149725918659,4.89180018249795,131.331801337828));
#56597=CARTESIAN_POINT('Ctrl Pts',(61.0071982577468,4.90267884054802,131.195414640615));
#56598=CARTESIAN_POINT('Ctrl Pts',(60.9994335047997,4.91354409162429,131.059196027817));
#56599=CARTESIAN_POINT('Ctrl Pts',(60.9916687518526,4.9187421485711,130.922345397759));
#56600=CARTESIAN_POINT('Ctrl Pts',(60.9839039989055,4.91821334830532,130.785373172993));
#56601=CARTESIAN_POINT('Ctrl Pts',(60.9761469580205,4.91768507325141,130.648536990971));
#56602=CARTESIAN_POINT('Ctrl Pts',(60.9683899171354,4.91144126185184,130.51157984301));
#56603=CARTESIAN_POINT('Ctrl Pts',(60.9606328762504,4.89947411470341,130.375016394534));
#56604=CARTESIAN_POINT('Ctrl Pts',(60.9528816850103,4.88751599207375,130.238555929617));
#56605=CARTESIAN_POINT('Ctrl Pts',(60.9451304937702,4.86984315844706,130.102488961136));
#56606=CARTESIAN_POINT('Ctrl Pts',(60.93737930253,4.84649986997196,129.967328913948));
#56607=CARTESIAN_POINT('Ctrl Pts',(60.9296314057529,4.82316650301722,129.832226313385));
#56608=CARTESIAN_POINT('Ctrl Pts',(60.9218835089758,4.7941675411071,129.698030251907));
#56609=CARTESIAN_POINT('Ctrl Pts',(60.9141356121987,4.75959892608824,129.565247577816));
#56610=CARTESIAN_POINT('Ctrl Pts',(60.9063893361146,4.72503754207842,129.432492678997));
#56611=CARTESIAN_POINT('Ctrl Pts',(60.8986430600305,4.68490892074898,129.301150957613));
#56612=CARTESIAN_POINT('Ctrl Pts',(60.8908967839464,4.63935972741285,129.171717244946));
#56613=CARTESIAN_POINT('Ctrl Pts',(60.8831504506811,4.59381019784285,129.042282576828));
#56614=CARTESIAN_POINT('Ctrl Pts',(60.8754041174157,4.54284014620555,128.914756314327));
#56615=CARTESIAN_POINT('Ctrl Pts',(60.8676577841503,4.48664541280495,128.789615968173));
#56616=CARTESIAN_POINT('Ctrl Pts',(60.8599097161474,4.43043809498344,128.664447597707));
#56617=CARTESIAN_POINT('Ctrl Pts',(60.8521616481444,4.36900392729882,128.541666563391));
#56618=CARTESIAN_POINT('Ctrl Pts',(60.8444135801414,4.30258580877236,128.421727951658));
#56619=CARTESIAN_POINT('Ctrl Pts',(60.8366572773996,4.23609710027915,128.301661867742));
#56620=CARTESIAN_POINT('Ctrl Pts',(60.8289009746577,4.16461404931552,128.184444583674));
#56621=CARTESIAN_POINT('Ctrl Pts',(60.8211446719158,4.08842450464875,128.070504708362));
#56622=CARTESIAN_POINT('Ctrl Pts',(60.8133842294016,4.01219429532796,127.956504019909));
#56623=CARTESIAN_POINT('Ctrl Pts',(60.8056237868875,3.93125281755737,127.84578454121));
#56624=CARTESIAN_POINT('Ctrl Pts',(60.7978633443734,3.84592912756436,127.738742864445));
#56625=CARTESIAN_POINT('Ctrl Pts',(60.7900904441079,3.76046846840949,127.631529354877));
#56626=CARTESIAN_POINT('Ctrl Pts',(60.7823175438425,3.6706117958522,127.528005740611));
#56627=CARTESIAN_POINT('Ctrl Pts',(60.7745446435771,3.57672664477264,127.428533375086));
#56628=CARTESIAN_POINT('Ctrl Pts',(60.7670543078151,3.48625445541802,127.332677080604));
#56629=CARTESIAN_POINT('Ctrl Pts',(60.7595639720531,3.3920418134763,127.240582817736));
#56630=CARTESIAN_POINT('Ctrl Pts',(60.7520736362911,3.29444608126646,127.152538047927));
#56631=CARTESIAN_POINT('Ctrl Pts',(60.7442993021721,3.19314997720558,127.061155033909));
#56632=CARTESIAN_POINT('Ctrl Pts',(60.736524968053,3.08788830335667,126.973845173808));
#56633=CARTESIAN_POINT('Ctrl Pts',(60.7287506339339,2.97902249272132,126.890972309417));
#56634=CARTESIAN_POINT('Ctrl Pts',(60.7209858809868,2.87029084946766,126.808201578424));
#56635=CARTESIAN_POINT('Ctrl Pts',(60.7132211280397,2.75796421533843,126.72985719759));
#56636=CARTESIAN_POINT('Ctrl Pts',(60.7054563750926,2.64243977392719,126.656265259011));
#56637=CARTESIAN_POINT('Ctrl Pts',(60.6976993342075,2.52703007301992,126.582746412983));
#56638=CARTESIAN_POINT('Ctrl Pts',(60.6899422933226,2.40842921303719,126.51397082451));
#56639=CARTESIAN_POINT('Ctrl Pts',(60.6821852524376,2.2870659808092,126.450223244684));
#56640=CARTESIAN_POINT('Ctrl Pts',(60.6744340611974,2.16579426953886,126.386523737405));
#56641=CARTESIAN_POINT('Ctrl Pts',(60.6666828699573,2.04176467708187,126.327844872771));
#56642=CARTESIAN_POINT('Ctrl Pts',(60.6589316787172,1.91543308383876,126.274426935509));
#56643=CARTESIAN_POINT('Ctrl Pts',(60.6511837819401,1.78915518489278,126.221031702295));
#56644=CARTESIAN_POINT('Ctrl Pts',(60.6434358851631,1.66057759049002,126.172893101093));
#56645=CARTESIAN_POINT('Ctrl Pts',(60.635687988386,1.53017858537276,126.130204377198));
#56646=CARTESIAN_POINT('Ctrl Pts',(60.6279417123019,1.3998068569163,126.087524582865));
#56647=CARTESIAN_POINT('Ctrl Pts',(60.6201954362177,1.26761484690105,126.050292519883));
